#129762=CARTESIAN_POINT('Ctrl Pts',(-218.454065709672,-2.10503019557442,
135.251474072395));
#129763=CARTESIAN_POINT('Ctrl Pts',(-218.461822012414,-1.97955658261512,
135.306642127948));
#129764=CARTESIAN_POINT('Ctrl Pts',(-218.469582454928,-1.85401600061064,
135.361839628353));
#129765=CARTESIAN_POINT('Ctrl Pts',(-218.477342897442,-1.72626459823451,
135.411738576017));
#129766=CARTESIAN_POINT('Ctrl Pts',(-218.485103339957,-1.59679297651733,
135.456181256052));
#129767=CARTESIAN_POINT('Ctrl Pts',(-218.492876240222,-1.46711351545902,
135.500695279422));
#129768=CARTESIAN_POINT('Ctrl Pts',(-218.500649140487,-1.33570869179546,
135.539735420711));
#129769=CARTESIAN_POINT('Ctrl Pts',(-218.508422040753,-1.20308262887788,
135.573194358701));
#129770=CARTESIAN_POINT('Ctrl Pts',(-218.515912376515,-1.07527785741188,
135.605436980018));
#129771=CARTESIAN_POINT('Ctrl Pts',(-218.523402712277,-0.946339396860306,
135.632497071405));
#129772=CARTESIAN_POINT('Ctrl Pts',(-218.530893048039,-0.816723092949144,
135.654324169176));
#129773=CARTESIAN_POINT('Ctrl Pts',(-218.538667382158,-0.682192347479364,
135.676978847993));
#129774=CARTESIAN_POINT('Ctrl Pts',(-218.546441716277,-0.546505190154853,
135.694067645192));
#129775=CARTESIAN_POINT('Ctrl Pts',(-218.554216050396,-0.410161934671308,
135.705477862628));
#129776=CARTESIAN_POINT('Ctrl Pts',(-218.561980803344,-0.27398671006517,
135.716874017992));
#129777=CARTESIAN_POINT('Ctrl Pts',(-218.569745556291,-0.137157382000985,
135.722605485916));
#129778=CARTESIAN_POINT('Ctrl Pts',(-218.577510309238,-0.000184136581379461,
135.722610614119));
#129779=CARTESIAN_POINT('Ctrl Pts',(-218.585267350123,0.136653065079891,
135.722615737229));
#129780=CARTESIAN_POINT('Ctrl Pts',(-218.593024391008,0.273633511202761,
135.716905838947));
#129781=CARTESIAN_POINT('Ctrl Pts',(-218.600781431893,0.410242570674838,
135.70547111374));
#129782=CARTESIAN_POINT('Ctrl Pts',(-218.608532623133,0.54674861219269,
135.694045011548));
#129783=CARTESIAN_POINT('Ctrl Pts',(-218.616283814373,0.682883436486953,
135.676902707907));
#129784=CARTESIAN_POINT('Ctrl Pts',(-218.624035005613,0.818133450091018,
135.654086457275));
#129785=CARTESIAN_POINT('Ctrl Pts',(-218.63178290239,0.953325978831206,
135.631279904158));
#129786=CARTESIAN_POINT('Ctrl Pts',(-218.639530799167,1.08763406014116,
135.602804265396));
#129787=CARTESIAN_POINT('Ctrl Pts',(-218.647278695945,1.22055047558416,
135.568753506387));
#129788=CARTESIAN_POINT('Ctrl Pts',(-218.655024972029,1.35343908777875,
135.534709870063));
#129789=CARTESIAN_POINT('Ctrl Pts',(-218.662771248113,1.48493623463844,
135.49509353008));
#129790=CARTESIAN_POINT('Ctrl Pts',(-218.670517524197,1.61454651693362,
135.450049221762));
#129791=CARTESIAN_POINT('Ctrl Pts',(-218.678263857462,1.74415775598228,
135.405004580937));
#129792=CARTESIAN_POINT('Ctrl Pts',(-218.686010190728,1.87188173337477,
135.354532020168));
#129793=CARTESIAN_POINT('Ctrl Pts',(-218.693756523993,1.99724017861159,
135.29882551691));
#129794=CARTESIAN_POINT('Ctrl Pts',(-218.701504591996,2.12262669700287,
135.243106538568));
#129795=CARTESIAN_POINT('Ctrl Pts',(-218.709252659999,2.24564627189922,
135.18215144412));
#129796=CARTESIAN_POINT('Ctrl Pts',(-218.717000728002,2.36584287349146,
135.116201356792));
#129797=CARTESIAN_POINT('Ctrl Pts',(-218.724757030744,2.4861672214624,135.050181176927));
#129798=CARTESIAN_POINT('Ctrl Pts',(-218.732513333486,2.60366225942089,
134.979155587774));
#129799=CARTESIAN_POINT('Ctrl Pts',(-218.740269636228,2.71789825966552,
134.903410765174));
#129800=CARTESIAN_POINT('Ctrl Pts',(-218.748030078742,2.83219523110306,
134.827625515283));
#129801=CARTESIAN_POINT('Ctrl Pts',(-218.755790521256,2.94322938247043,
134.747116242418));
#129802=CARTESIAN_POINT('Ctrl Pts',(-218.76355096377,3.05060284192411,134.662210454372));
#129803=CARTESIAN_POINT('Ctrl Pts',(-218.771323864036,3.15814866678707,
134.577168368018));
#129804=CARTESIAN_POINT('Ctrl Pts',(-218.779096764301,3.26202176025846,
134.487715918266));
#129805=CARTESIAN_POINT('Ctrl Pts',(-218.786869664567,3.36185933897489,
134.394219228632));
#129806=CARTESIAN_POINT('Ctrl Pts',(-218.794360000329,3.45806757022903,
134.304121379171));
#129807=CARTESIAN_POINT('Ctrl Pts',(-218.801850336091,3.55052837891852,
134.210268440956));
#129808=CARTESIAN_POINT('Ctrl Pts',(-218.809340671853,3.63895291276647,
134.113016653054));
#129809=CARTESIAN_POINT('Ctrl Pts',(-218.817115005972,3.73073008969169,
134.012077534053));
#129810=CARTESIAN_POINT('Ctrl Pts',(-218.824889340091,3.81844960163169,
133.907156998039));
#129811=CARTESIAN_POINT('Ctrl Pts',(-218.83266367421,3.90174620067321,133.798615056994));
#129812=CARTESIAN_POINT('Ctrl Pts',(-218.840428427157,3.98494014410062,
133.69020688419));
#129813=CARTESIAN_POINT('Ctrl Pts',(-218.848193180104,4.06372178444967,
133.578186493694));
#129814=CARTESIAN_POINT('Ctrl Pts',(-218.855957933051,4.13776348385898,
133.462949794957));
#129815=CARTESIAN_POINT('Ctrl Pts',(-218.863714973936,4.21173164400863,
133.347827550935));
#129816=CARTESIAN_POINT('Ctrl Pts',(-218.871472014821,4.28096902193457,
133.229495682631));
#129817=CARTESIAN_POINT('Ctrl Pts',(-218.879229055706,4.34518919727565,
133.108381863644));
#129818=CARTESIAN_POINT('Ctrl Pts',(-218.886980246946,4.40936094368304,
132.98735937753));
#129819=CARTESIAN_POINT('Ctrl Pts',(-218.894731438186,4.46852283594386,
132.863559460471));
#129820=CARTESIAN_POINT('Ctrl Pts',(-218.902482629427,4.52243281411565,
132.737437052762));
#129821=CARTESIAN_POINT('Ctrl Pts',(-218.910230526204,4.57631987910856,
132.611368250441));
#129822=CARTESIAN_POINT('Ctrl Pts',(-218.917978422981,4.62495931635136,
132.482979279525));
#129823=CARTESIAN_POINT('Ctrl Pts',(-218.925726319758,4.66815601764025,
132.352747667844));
#129824=CARTESIAN_POINT('Ctrl Pts',(-218.933472595842,4.71134368311044,
132.222543297809));
#129825=CARTESIAN_POINT('Ctrl Pts',(-218.941218871926,4.74909075416409,
132.09049742452));
#129826=CARTESIAN_POINT('Ctrl Pts',(-218.94896514801,4.78125122534236,131.957105074357));
#129827=CARTESIAN_POINT('Ctrl Pts',(-218.956711481275,4.81341193392196,
131.823711739522));
#129828=CARTESIAN_POINT('Ctrl Pts',(-218.964457814541,4.83998586870189,
131.688972288054));
#129829=CARTESIAN_POINT('Ctrl Pts',(-218.972204147806,4.8608777115221,131.553393952023));
#129830=CARTESIAN_POINT('Ctrl Pts',(-218.979952215809,4.88177423292563,
131.417785254164));
#129831=CARTESIAN_POINT('Ctrl Pts',(-218.987700283812,4.89698607077991,
131.281337684248));
#129832=CARTESIAN_POINT('Ctrl Pts',(-218.995448351815,4.90646959363344,
131.144565246063));
#129833=CARTESIAN_POINT('Ctrl Pts',(-219.003204654557,4.91596319568793,
131.007647444502));
#129834=CARTESIAN_POINT('Ctrl Pts',(-219.010960957299,4.91971629397654,
130.870404475602));
#129835=CARTESIAN_POINT('Ctrl Pts',(-219.01871726004,4.91773737802059,130.733352566479));
#129836=CARTESIAN_POINT('Ctrl Pts',(-219.026477702555,4.91575740585761,
130.596227508626));
#129837=CARTESIAN_POINT('Ctrl Pts',(-219.034238145069,4.90803934542951,
130.459294103899));
#129838=CARTESIAN_POINT('Ctrl Pts',(-219.041998587583,4.89464367886692,
130.323064119108));
#129839=CARTESIAN_POINT('Ctrl Pts',(-219.049771487848,4.88122650839115,
130.186615445852));
#129840=CARTESIAN_POINT('Ctrl Pts',(-219.057544388114,4.86211357325294,
130.050872836387));
#129841=CARTESIAN_POINT('Ctrl Pts',(-219.065317288379,4.83741681026475,
129.916339409335));
#129842=CARTESIAN_POINT('Ctrl Pts',(-219.072807624141,4.81361783681864,
129.786696611226));
#129843=CARTESIAN_POINT('Ctrl Pts',(-219.080297959903,4.78463402742281,
129.658176908659));
#129844=CARTESIAN_POINT('Ctrl Pts',(-219.087788295665,4.7506089643807,129.531215877151));
#129845=CARTESIAN_POINT('Ctrl Pts',(-219.095562629784,4.7152938307316,129.399441079545));
#129846=CARTESIAN_POINT('Ctrl Pts',(-219.103336963903,4.67443575115081,
129.268928057262));
#129847=CARTESIAN_POINT('Ctrl Pts',(-219.111111298022,4.62814018849646,
129.140178698987));
#129848=CARTESIAN_POINT('Ctrl Pts',(-219.118876050969,4.58190168098552,
129.01158801279));
#129849=CARTESIAN_POINT('Ctrl Pts',(-219.126640803917,4.53023915483583,
128.884757030239));
#129850=CARTESIAN_POINT('Ctrl Pts',(-219.134405556864,4.47330860361587,
128.760175401076));
#129851=CARTESIAN_POINT('Ctrl Pts',(-219.142162597749,4.41643459662197,
128.635717508144));
#129852=CARTESIAN_POINT('Ctrl Pts',(-219.149919638634,4.35430313847106,
128.513504875955));
#129853=CARTESIAN_POINT('Ctrl Pts',(-219.157676679519,4.28711922587275,
128.394009646099));
#129854=CARTESIAN_POINT('Ctrl Pts',(-219.165427870759,4.21998597718546,
128.274604528525));
#129855=CARTESIAN_POINT('Ctrl Pts',(-219.173179061999,4.14780804864432,
128.157913073863));
#129856=CARTESIAN_POINT('Ctrl Pts',(-219.180930253239,4.07083735509288,
128.044384840339));
#129857=CARTESIAN_POINT('Ctrl Pts',(-219.188678150016,3.99389937613956,
127.930904859343));
#129858=CARTESIAN_POINT('Ctrl Pts',(-219.196426046793,3.91217290265776,
127.820585748395));
#129859=CARTESIAN_POINT('Ctrl Pts',(-219.20417394357,3.82595423158429,127.713849773009));
#129860=CARTESIAN_POINT('Ctrl Pts',(-219.211920219654,3.73975359559815,
127.607136124488));
#129861=CARTESIAN_POINT('Ctrl Pts',(-219.219666495738,3.64906287659481,
127.504004424646));
#129862=CARTESIAN_POINT('Ctrl Pts',(-219.227412771822,3.55421963477011,
127.404845085859));
#129863=CARTESIAN_POINT('Ctrl Pts',(-219.235159105088,3.45937569283428,
127.305685015101));
#129864=CARTESIAN_POINT('Ctrl Pts',(-219.242905438353,3.36037943714812,
127.210497646446));
#129865=CARTESIAN_POINT('Ctrl Pts',(-219.250651771618,3.25760609462358,
127.119637345084));
#129866=CARTESIAN_POINT('Ctrl Pts',(-219.258399839621,3.15480973672142,
127.028756696187));
#129867=CARTESIAN_POINT('Ctrl Pts',(-219.266147907624,3.04823490168521,
126.942205301722));
#129868=CARTESIAN_POINT('Ctrl Pts',(-219.273895975627,2.93829045159357,
126.860297701666));
#129869=CARTESIAN_POINT('Ctrl Pts',(-219.281652278369,2.82822915123217,
126.778303049239));
#129870=CARTESIAN_POINT('Ctrl Pts',(-219.289408581111,2.71479139587311,
126.700962284319));
#129871=CARTESIAN_POINT('Ctrl Pts',(-219.297164883853,2.59841609080511,
126.628547297799));
#129872=CARTESIAN_POINT('Ctrl Pts',(-219.304925326367,2.4819786727328,126.55609366122));
#129873=CARTESIAN_POINT('Ctrl Pts',(-219.312685768881,2.36260092099488,
126.488571234006));
#129874=CARTESIAN_POINT('Ctrl Pts',(-219.320446211395,2.24074609157281,
126.426205753288));
#129875=CARTESIAN_POINT('Ctrl Pts',(-219.328219111661,2.11869564996046,
126.363740157964));
#129876=CARTESIAN_POINT('Ctrl Pts',(-219.335992011926,1.99416053988601,
126.306448215489));
#129877=CARTESIAN_POINT('Ctrl Pts',(-219.343764912191,1.86762455387554,
126.254507698156));
#129878=CARTESIAN_POINT('Ctrl Pts',(-219.351255247953,1.74568846968043,
126.204455349458));
#129879=CARTESIAN_POINT('Ctrl Pts',(-219.358745583716,1.62189474709496,
126.159372210661));
#129880=CARTESIAN_POINT('Ctrl Pts',(-219.366235919478,1.49668745788046,
126.119372921112));
#129881=CARTESIAN_POINT('Ctrl Pts',(-219.374010253597,1.36673289624037,
126.077857046343));
#129882=CARTESIAN_POINT('Ctrl Pts',(-219.381784587716,1.23484380424537,
126.041686629354));
#129883=CARTESIAN_POINT('Ctrl Pts',(-219.389558921835,1.10149944031048,
126.011044224348));
#129884=CARTESIAN_POINT('Ctrl Pts',(-219.397323674782,0.968319411387163,
125.980439583367));
#129885=CARTESIAN_POINT('Ctrl Pts',(-219.405088427729,0.833688056415686,
125.955349485688));
#129886=CARTESIAN_POINT('Ctrl Pts',(-219.412853180676,0.698101649925656,
125.935907357148));
#129887=CARTESIAN_POINT('Ctrl Pts',(-219.420610221561,0.562649909765617,
125.916484538805));
#129888=CARTESIAN_POINT('Ctrl Pts',(-219.428367262446,0.426245390287803,
125.902698581294));
#129889=CARTESIAN_POINT('Ctrl Pts',(-219.436124303331,0.289396123311074,
125.89463221914));
#129890=CARTESIAN_POINT('Ctrl Pts',(-219.443875494571,0.152650055431291,
125.886571939892));
#129891=CARTESIAN_POINT('Ctrl Pts',(-219.451626685811,0.0154602963297696,
125.884222693766));
#129892=CARTESIAN_POINT('Ctrl Pts',(-219.459377877051,-0.121658761798457,
125.887615534874));
#129893=CARTESIAN_POINT('Ctrl Pts',(-219.467125773828,-0.258719540669395,
125.891006933933));
#129894=CARTESIAN_POINT('Ctrl Pts',(-219.474873670606,-0.395709288306496,
125.900135556526));
#129895=CARTESIAN_POINT('Ctrl Pts',(-219.482621567383,-0.53211258504232,
125.914980364473));
#129896=CARTESIAN_POINT('Ctrl Pts',(-219.490367843467,-0.668487349148981,
125.929822067205));
#129897=CARTESIAN_POINT('Ctrl Pts',(-219.498114119551,-0.804275517933435,
125.950377534701));
#129898=CARTESIAN_POINT('Ctrl Pts',(-219.505860395635,-0.938966166874421,
125.976573795433));
#129899=CARTESIAN_POINT('Ctrl Pts',(-219.5136067289,-1.073657810071,126.002770249539));
#129900=CARTESIAN_POINT('Ctrl Pts',(-219.521353062166,-1.20725153348383,
126.034607505329));
#129901=CARTESIAN_POINT('Ctrl Pts',(-219.529099395431,-1.33924638033021,
126.071961416815));
#129902=CARTESIAN_POINT('Ctrl Pts',(-219.536847463434,-1.47127078650754,
126.10932369345));
#129903=CARTESIAN_POINT('Ctrl Pts',(-219.544595531437,-1.60169522750637,
126.152204977679));
#129904=CARTESIAN_POINT('Ctrl Pts',(-219.55234359944,-1.73003407199424,
126.200431298795));
#129905=CARTESIAN_POINT('Ctrl Pts',(-219.560099902182,-1.8585093165331,
126.248708875419));
#129906=CARTESIAN_POINT('Ctrl Pts',(-219.567856204924,-1.98489417010757,
126.302342699135));
#129907=CARTESIAN_POINT('Ctrl Pts',(-219.575612507665,-2.10872264418015,
126.36111047016));
#129908=CARTESIAN_POINT('Ctrl Pts',(-219.58337295018,-2.23261720923775,
126.419909607314));
#129909=CARTESIAN_POINT('Ctrl Pts',(-219.591133392694,-2.35395233036607,
126.483847969569));
#129910=CARTESIAN_POINT('Ctrl Pts',(-219.598893835208,-2.47228768734846,
126.552657822981));
#129911=CARTESIAN_POINT('Ctrl Pts',(-219.606666735473,-2.59081300675119,
126.621578136078));
#129912=CARTESIAN_POINT('Ctrl Pts',(-219.614439635739,-2.70632860948182,
126.69538535686));
#129913=CARTESIAN_POINT('Ctrl Pts',(-219.622212536004,-2.81842342899755,
126.77376854724));
#129914=CARTESIAN_POINT('Ctrl Pts',(-219.629702871766,-2.92644331947255,
126.849302311213));
#129915=CARTESIAN_POINT('Ctrl Pts',(-219.637193207528,-3.03128657184853,
126.929084938306));
#129916=CARTESIAN_POINT('Ctrl Pts',(-219.64468354329,-3.13261670516085,
127.012804783736));
#129917=CARTESIAN_POINT('Ctrl Pts',(-219.652349582752,-3.23632377855823,
127.098488477926));
#129918=CARTESIAN_POINT('Ctrl Pts',(-219.660015622214,-3.33669878099961,
127.188584155804));
#129919=CARTESIAN_POINT('Ctrl Pts',(-219.667681661675,-3.43333514465959,
127.282799479811));
#129920=CARTESIAN_POINT('Ctrl Pts',(-219.675338911775,-3.52986071160705,
127.376906782906));
#129921=CARTESIAN_POINT('Ctrl Pts',(-219.682996161875,-3.62265587551738,
127.475124065198));
#129922=CARTESIAN_POINT('Ctrl Pts',(-219.690653411975,-3.71134556209773,
127.577117648529));
#129923=CARTESIAN_POINT('Ctrl Pts',(-219.69830365046,-3.79995403703036,
127.67901783806));
#129924=CARTESIAN_POINT('Ctrl Pts',(-219.705953888946,-3.88446424695242,
127.784687151707));
#129925=CARTESIAN_POINT('Ctrl Pts',(-219.713604127431,-3.96453697041456,
127.893754207775));
#129926=CARTESIAN_POINT('Ctrl Pts',(-219.721249125501,-4.04455484404159,
128.002746552883));
#129927=CARTESIAN_POINT('Ctrl Pts',(-219.728894123571,-4.12014103953239,
128.115131688097));
#129928=CARTESIAN_POINT('Ctrl Pts',(-219.736539121641,-4.19099611494774,
128.230504633445));
#129929=CARTESIAN_POINT('Ctrl Pts',(-219.744181407903,-4.26182605688949,
128.345836654091));
#129930=CARTESIAN_POINT('Ctrl Pts',(-219.751823694165,-4.32792800274121,
128.464154036666));
#129931=CARTESIAN_POINT('Ctrl Pts',(-219.759465980427,-4.3890456586599,
128.585022592681));
#129932=CARTESIAN_POINT('Ctrl Pts',(-219.767106586471,-4.45014987736727,
128.705864574766));
#129933=CARTESIAN_POINT('Ctrl Pts',(-219.774747192515,-4.50627180773774,
128.829256253692));
#129934=CARTESIAN_POINT('Ctrl Pts',(-219.782387798558,-4.55720130961135,
128.954739227612));
#129935=CARTESIAN_POINT('Ctrl Pts',(-219.790030547643,-4.60814509621734,
129.080257397059));
#129936=CARTESIAN_POINT('Ctrl Pts',(-219.797673296727,-4.6538933931612,
129.207867660123));
#129937=CARTESIAN_POINT('Ctrl Pts',(-219.805316045812,-4.69428444174175,
129.337092188641));
#129938=CARTESIAN_POINT('Ctrl Pts',(-219.810118632032,-4.71966555672841,
129.418294898961));
#129939=CARTESIAN_POINT('Ctrl Pts',(-219.814921218252,-4.74293224799498,
129.500134669231));
#129940=CARTESIAN_POINT('Ctrl Pts',(-219.819723804473,-4.76405452823394,
129.582490119308));
#129941=CARTESIAN_POINT('Origin',(213.235140564004,0.,130.804360617566));
#129942=CARTESIAN_POINT('',(-221.915425355964,-4.76405452823393,129.582490119308));
#129943=CARTESIAN_POINT('',(-221.569819034442,-4.76405452823418,129.582490119309));
#129944=CARTESIAN_POINT('',(213.235140564004,-4.76405452823405,129.582490119308));
#129945=CARTESIAN_POINT('',(-220.235140564048,-4.91824810108724,130.800038736987));
#129946=CARTESIAN_POINT('Ctrl Pts',(-220.235140564048,-4.91824810108724,
130.800038736987));
#129947=CARTESIAN_POINT('Ctrl Pts',(-220.242787499465,-4.91836654317577,
130.934824408715));
#129948=CARTESIAN_POINT('Ctrl Pts',(-220.250434434882,-4.91294007670036,
131.069796436303));
#129949=CARTESIAN_POINT('Ctrl Pts',(-220.258081370299,-4.90194948723364,
131.204453465677));
#129950=CARTESIAN_POINT('Ctrl Pts',(-220.265721661022,-4.89096844788083,
131.338993486772));
#129951=CARTESIAN_POINT('Ctrl Pts',(-220.273361951745,-4.87443293515955,
131.473218654188));
#129952=CARTESIAN_POINT('Ctrl Pts',(-220.281002242468,-4.85237579310271,
131.606627546344));
#129953=CARTESIAN_POINT('Ctrl Pts',(-220.288638270407,-4.83033095749057,
131.739962005051));
#129954=CARTESIAN_POINT('Ctrl Pts',(-220.296274298347,-4.80277068438332,
131.872480697236));
#129955=CARTESIAN_POINT('Ctrl Pts',(-220.303910326287,-4.76977961799604,
132.003687703164));
#129956=CARTESIAN_POINT('Ctrl Pts',(-220.311544193053,-4.73679788884799,
132.134857574458));
#129957=CARTESIAN_POINT('Ctrl Pts',(-220.319178059819,-4.6983885201489,
132.264716106547));
#129958=CARTESIAN_POINT('Ctrl Pts',(-220.326811926585,-4.65468708584121,
132.392778445281));
#129959=CARTESIAN_POINT('Ctrl Pts',(-220.33444539865,-4.6109879110682,132.520834162693));
#129960=CARTESIAN_POINT('Ctrl Pts',(-220.342078870716,-4.56199734517058,
132.647093489588));
#129961=CARTESIAN_POINT('Ctrl Pts',(-220.349712342781,-4.50790039104962,
132.771088134757));
#129962=CARTESIAN_POINT('Ctrl Pts',(-220.357347186093,-4.45379371916913,
132.895105053825));
#129963=CARTESIAN_POINT('Ctrl Pts',(-220.364982029405,-4.39457899688891,
133.01685611266));
#129964=CARTESIAN_POINT('Ctrl Pts',(-220.372616872716,-4.33048854730502,
133.135894877267));
#129965=CARTESIAN_POINT('Ctrl Pts',(-220.380259413188,-4.26633348415524,
133.255053652252));
#129966=CARTESIAN_POINT('Ctrl Pts',(-220.38790195366,-4.19729306907339,
133.371494316662));
#129967=CARTESIAN_POINT('Ctrl Pts',(-220.395544494132,-4.12364476480766,
133.484796573931));
#129968=CARTESIAN_POINT('Ctrl Pts',(-220.403191015574,-4.04995809742099,
133.598157849914));
#129969=CARTESIAN_POINT('Ctrl Pts',(-220.410837537016,-3.97165899553329,
133.708377135488));
#129970=CARTESIAN_POINT('Ctrl Pts',(-220.418484058458,-3.88906629538656,
133.815065919084));
#129971=CARTESIAN_POINT('Ctrl Pts',(-220.426142400143,-3.80634592074331,
133.92191962569));
#129972=CARTESIAN_POINT('Ctrl Pts',(-220.433800741827,-3.71931895115071,
134.025231621794));
#129973=CARTESIAN_POINT('Ctrl Pts',(-220.441459083512,-3.62834267717324,
134.124648629095));
#129974=CARTESIAN_POINT('Ctrl Pts',(-220.447785195198,-3.55319245619403,
134.206771250094));
#129975=CARTESIAN_POINT('Ctrl Pts',(-220.454111306884,-3.47534820372095,
134.286236755806));
#129976=CARTESIAN_POINT('Ctrl Pts',(-220.46043741857,-3.39502806051355,
134.362866979908));
#129977=CARTESIAN_POINT('Ctrl Pts',(-220.468211752689,-3.29632040867479,
134.45703998781));
#129978=CARTESIAN_POINT('Ctrl Pts',(-220.475986086808,-3.19353511360062,
134.547252042264));
#129979=CARTESIAN_POINT('Ctrl Pts',(-220.483760420927,-3.08702331865612,
134.633129361245));
#129980=CARTESIAN_POINT('Ctrl Pts',(-220.491525173874,-2.98064278997966,
134.718900844105));
#129981=CARTESIAN_POINT('Ctrl Pts',(-220.499289926821,-2.87054520073186,
134.800347977787));
#129982=CARTESIAN_POINT('Ctrl Pts',(-220.507054679768,-2.75711848394831,
134.877133718043));
#129983=CARTESIAN_POINT('Ctrl Pts',(-220.514811720653,-2.6438044241789,
134.95384319362));
#129984=CARTESIAN_POINT('Ctrl Pts',(-220.522568761538,-2.52716813869132,
135.025900271455));
#129985=CARTESIAN_POINT('Ctrl Pts',(-220.530325802423,-2.40763030462598,
135.09300835068));
#129986=CARTESIAN_POINT('Ctrl Pts',(-220.538076993663,-2.28818261497133,
135.160065823181));
#129987=CARTESIAN_POINT('Ctrl Pts',(-220.545828184903,-2.16583807151714,
135.222181534935));
#129988=CARTESIAN_POINT('Ctrl Pts',(-220.553579376144,-2.04104567477602,
135.279102578392));
#129989=CARTESIAN_POINT('Ctrl Pts',(-220.561327272921,-1.91630631813264,
135.335999428888));
#129990=CARTESIAN_POINT('Ctrl Pts',(-220.569075169698,-1.7891215324493,
135.387705840469));
#129991=CARTESIAN_POINT('Ctrl Pts',(-220.576823066475,-1.65996402597979,
135.434015301768));
#129992=CARTESIAN_POINT('Ctrl Pts',(-220.584569342559,-1.53083353647596,
135.480315076126));
#129993=CARTESIAN_POINT('Ctrl Pts',(-220.592315618643,-1.39973151476155,
135.521220013824));
#129994=CARTESIAN_POINT('Ctrl Pts',(-220.600061894727,-1.26714934093197,
135.556572272183));
#129995=CARTESIAN_POINT('Ctrl Pts',(-220.607808227992,-1.13456618841109,
135.591924791503));
#129996=CARTESIAN_POINT('Ctrl Pts',(-220.615554561258,-1.00050323973906,
135.621724448965));
#129997=CARTESIAN_POINT('Ctrl Pts',(-220.623300894523,-0.865465293542188,
135.645863781685));
#129998=CARTESIAN_POINT('Ctrl Pts',(-220.631048962526,-0.730397106533365,
135.670008520241));
#129999=CARTESIAN_POINT('Ctrl Pts',(-220.638797030529,-0.594353872311261,
135.688490342913));
#130000=CARTESIAN_POINT('Ctrl Pts',(-220.646545098532,-0.457848399608611,
135.70125329614));
#130001=CARTESIAN_POINT('Ctrl Pts',(-220.654301401274,-0.321197847265323,
135.714029813986));
#130002=CARTESIAN_POINT('Ctrl Pts',(-220.662057704015,-0.18408446495979,
135.721075284309));
#130003=CARTESIAN_POINT('Ctrl Pts',(-220.669814006757,-0.0470245348749268,
135.722385806157));
#130004=CARTESIAN_POINT('Ctrl Pts',(-220.677574449271,0.0901085482214175,
135.723697027471));
#130005=CARTESIAN_POINT('Ctrl Pts',(-220.685334891786,0.227187731680498,
135.719267213801));
#130006=CARTESIAN_POINT('Ctrl Pts',(-220.6930953343,0.363699944662658,135.709144548867));
#130007=CARTESIAN_POINT('Ctrl Pts',(-220.700868234565,0.500431299168082,
135.699005634134));
#130008=CARTESIAN_POINT('Ctrl Pts',(-220.70864113483,0.636593475857676,
135.683155651393));
#130009=CARTESIAN_POINT('Ctrl Pts',(-220.716414035096,0.77168081482156,
135.661694431762));
#130010=CARTESIAN_POINT('Ctrl Pts',(-220.723904370858,0.90185738875219,
135.641013381523));
#130011=CARTESIAN_POINT('Ctrl Pts',(-220.73139470662,1.03103561233125,135.615122037242));
#130012=CARTESIAN_POINT('Ctrl Pts',(-220.738885042382,1.1587765898967,135.584153487263));
#130013=CARTESIAN_POINT('Ctrl Pts',(-220.746659376501,1.29136090545014,
135.5520107553));
#130014=CARTESIAN_POINT('Ctrl Pts',(-220.75443371062,1.42281682445883,135.514296394508));
#130015=CARTESIAN_POINT('Ctrl Pts',(-220.762208044739,1.55264007195242,
135.471103793429));
#130016=CARTESIAN_POINT('Ctrl Pts',(-220.769972797687,1.68230332389576,
135.427964423372));
#130017=CARTESIAN_POINT('Ctrl Pts',(-220.777737550634,1.81033754043559,
135.379360368624));
#130018=CARTESIAN_POINT('Ctrl Pts',(-220.785502303581,1.93624946942148,
135.325435827587));
#130019=CARTESIAN_POINT('Ctrl Pts',(-220.793259344466,2.06203634090445,
135.271564845165));
#130020=CARTESIAN_POINT('Ctrl Pts',(-220.801016385351,2.1857047625545,135.212384045534));
#130021=CARTESIAN_POINT('Ctrl Pts',(-220.808773426236,2.30677780939265,
135.148087036275));
#130022=CARTESIAN_POINT('Ctrl Pts',(-220.816524617476,2.42775955410453,
135.083838513891));
#130023=CARTESIAN_POINT('Ctrl Pts',(-220.824275808716,2.54614947577954,
135.014481643969));
#130024=CARTESIAN_POINT('Ctrl Pts',(-220.832026999956,2.66149210039046,
134.940257480649));
#130025=CARTESIAN_POINT('Ctrl Pts',(-220.839774896733,2.77678570130921,
134.866064864578));
#130026=CARTESIAN_POINT('Ctrl Pts',(-220.84752279351,2.8890342530977,134.787009280781));
#130027=CARTESIAN_POINT('Ctrl Pts',(-220.855270690287,2.99780850153503,
134.703376807661));
#130028=CARTESIAN_POINT('Ctrl Pts',(-220.863016966371,3.10655999674449,
134.619761828651));
#130029=CARTESIAN_POINT('Ctrl Pts',(-220.870763242455,3.21183832439996,
134.531572102766));
#130030=CARTESIAN_POINT('Ctrl Pts',(-220.87850951854,3.31324508403936,134.43913572417));
#130031=CARTESIAN_POINT('Ctrl Pts',(-220.886255851805,3.41465259224029,
134.34669866323));
#130032=CARTESIAN_POINT('Ctrl Pts',(-220.89400218507,3.5121881864595,134.250015150408));
#130033=CARTESIAN_POINT('Ctrl Pts',(-220.901748518335,3.60548859914309,
134.14945180077));
#130034=CARTESIAN_POINT('Ctrl Pts',(-220.909496586338,3.69880990580707,
134.048865930668));
#130035=CARTESIAN_POINT('Ctrl Pts',(-220.917244654342,3.78789387779097,
133.94439878137));
#130036=CARTESIAN_POINT('Ctrl Pts',(-220.924992722345,3.87241625413368,
133.836451549122));
#130037=CARTESIAN_POINT('Ctrl Pts',(-220.932749025086,3.95702846186391,
133.72838958927));
#130038=CARTESIAN_POINT('Ctrl Pts',(-220.940505327828,4.03706914790117,
133.616840466288));
#130039=CARTESIAN_POINT('Ctrl Pts',(-220.94826163057,4.11225596713424,133.502236434439));
#130040=CARTESIAN_POINT('Ctrl Pts',(-220.956022073084,4.18748291583656,
133.387571234968));
#130041=CARTESIAN_POINT('Ctrl Pts',(-220.963782515598,4.25785063514177,
133.269848213147));
#130042=CARTESIAN_POINT('Ctrl Pts',(-220.971542958113,4.3231223360576,133.149525074482));
#130043=CARTESIAN_POINT('Ctrl Pts',(-220.979315858378,4.38849881690228,
133.029008782433));
#130044=CARTESIAN_POINT('Ctrl Pts',(-220.987088758643,4.44876275997436,
132.905884384042));
#130045=CARTESIAN_POINT('Ctrl Pts',(-220.994861658909,4.50372483448786,
132.780631266469));
#130046=CARTESIAN_POINT('Ctrl Pts',(-221.002351994671,4.55668889915317,
132.659931415211));
#130047=CARTESIAN_POINT('Ctrl Pts',(-221.009842330433,4.60472976312694,
132.537255213181));
#130048=CARTESIAN_POINT('Ctrl Pts',(-221.017332666195,4.64772216357618,
132.413043853229));
#130049=CARTESIAN_POINT('Ctrl Pts',(-221.025107000315,4.69234463395464,
132.284122981814));
#130050=CARTESIAN_POINT('Ctrl Pts',(-221.032881334434,4.73166960930753,
132.153139860894));
#130051=CARTESIAN_POINT('Ctrl Pts',(-221.040655668553,4.76550308712181,
132.020569230071));
#130052=CARTESIAN_POINT('Ctrl Pts',(-221.0484204215,4.79929486819829,131.888161980704));
#130053=CARTESIAN_POINT('Ctrl Pts',(-221.056185174447,4.82760852184945,
131.7541714894));
#130054=CARTESIAN_POINT('Ctrl Pts',(-221.063949927394,4.85029875143955,
131.619090685922));
#130055=CARTESIAN_POINT('Ctrl Pts',(-221.071706968279,4.87296644477388,
131.484144046603));
#130056=CARTESIAN_POINT('Ctrl Pts',(-221.079464009164,4.89002176462856,
131.348109633224));
#130057=CARTESIAN_POINT('Ctrl Pts',(-221.087221050049,4.90136980894267,
131.211493345906));
#130058=CARTESIAN_POINT('Ctrl Pts',(-221.094972241289,4.9127092956083,131.074980081992));
#130059=CARTESIAN_POINT('Ctrl Pts',(-221.102723432529,4.91835004115387,
130.93788620558));
#130060=CARTESIAN_POINT('Ctrl Pts',(-221.11047462377,4.91824865641744,130.800725215521));
#130061=CARTESIAN_POINT('Ctrl Pts',(-221.118222520547,4.91814731477223,
130.663622522542));
#130062=CARTESIAN_POINT('Ctrl Pts',(-221.125970417324,4.91230869721828,
130.526453162796));
#130063=CARTESIAN_POINT('Ctrl Pts',(-221.133718314101,4.90074146722637,
130.38973291238));
#130064=CARTESIAN_POINT('Ctrl Pts',(-221.141464590185,4.88917665684962,
130.253041260893));
#130065=CARTESIAN_POINT('Ctrl Pts',(-221.149210866269,4.87188565046273,
130.116798921204));
#130066=CARTESIAN_POINT('Ctrl Pts',(-221.156957142353,4.84892913779867,
129.981518421816));
#130067=CARTESIAN_POINT('Ctrl Pts',(-221.164703475618,4.82597245567487,
129.846236923818));
#130068=CARTESIAN_POINT('Ctrl Pts',(-221.172449808884,4.79735024923217,
129.711917665742));
#130069=CARTESIAN_POINT('Ctrl Pts',(-221.180196142149,4.76317460712446,
129.579064439271));
#130070=CARTESIAN_POINT('Ctrl Pts',(-221.187944210152,4.72899131161871,
129.446181461241));
#130071=CARTESIAN_POINT('Ctrl Pts',(-221.195692278155,4.68925220310519,
129.314765546674));
#130072=CARTESIAN_POINT('Ctrl Pts',(-221.203440346158,4.64411954837663,
129.18530636187));
#130073=CARTESIAN_POINT('Ctrl Pts',(-221.2111966489,4.59893892612549,129.055709586305));
#130074=CARTESIAN_POINT('Ctrl Pts',(-221.218952951642,4.54835343563073,
128.928074064561));
#130075=CARTESIAN_POINT('Ctrl Pts',(-221.226709254384,4.49257413021671,
128.802870985565));
#130076=CARTESIAN_POINT('Ctrl Pts',(-221.234469696898,4.43676505370791,
128.677601081916));
#130077=CARTESIAN_POINT('Ctrl Pts',(-221.242230139412,4.37575681247151,
128.554766557908));
#130078=CARTESIAN_POINT('Ctrl Pts',(-221.249990581926,4.30980649687876,
128.434814031832));
#130079=CARTESIAN_POINT('Ctrl Pts',(-221.257763482192,4.24375031198462,
128.314668947313));
#130080=CARTESIAN_POINT('Ctrl Pts',(-221.265536382457,4.17273640181274,
128.197415440432));
#130081=CARTESIAN_POINT('Ctrl Pts',(-221.273309282723,4.09706575044405,
128.083471921011));
#130082=CARTESIAN_POINT('Ctrl Pts',(-221.280799618485,4.02414591785631,
127.97367053553));
#130083=CARTESIAN_POINT('Ctrl Pts',(-221.288289954246,3.9469022151612,127.866942912354));
#130084=CARTESIAN_POINT('Ctrl Pts',(-221.295780290008,3.86563812277885,
127.763632914167));
#130085=CARTESIAN_POINT('Ctrl Pts',(-221.303554624127,3.7812928776333,127.656405885997));
#130086=CARTESIAN_POINT('Ctrl Pts',(-221.311328958247,3.69234917811289,
127.552521094194));
#130087=CARTESIAN_POINT('Ctrl Pts',(-221.319103292366,3.5991015729938,127.452398366917));
#130088=CARTESIAN_POINT('Ctrl Pts',(-221.326868045313,3.50596888721424,
127.352399031954));
#130089=CARTESIAN_POINT('Ctrl Pts',(-221.33463279826,3.40854311347,127.256152819803));
#130090=CARTESIAN_POINT('Ctrl Pts',(-221.342397551207,3.30716043115016,
127.164048413217));
#130091=CARTESIAN_POINT('Ctrl Pts',(-221.350154592092,3.20587844353936,
127.072035486025));
#130092=CARTESIAN_POINT('Ctrl Pts',(-221.357911632977,3.10064765585033,
126.984156439143));
#130093=CARTESIAN_POINT('Ctrl Pts',(-221.365668673862,2.99184239929796,
126.900764567734));
#130094=CARTESIAN_POINT('Ctrl Pts',(-221.373419865102,2.88311919363638,
126.817435582784));
#130095=CARTESIAN_POINT('Ctrl Pts',(-221.381171056342,2.77082719346199,
126.738587274899));
#130096=CARTESIAN_POINT('Ctrl Pts',(-221.388922247582,2.65537496699824,
126.664533707279));
#130097=CARTESIAN_POINT('Ctrl Pts',(-221.396670144359,2.53997181081038,
126.5905116144));
#130098=CARTESIAN_POINT('Ctrl Pts',(-221.404418041136,2.42141142821396,
126.521280419216));
#130099=CARTESIAN_POINT('Ctrl Pts',(-221.412165937914,2.30013243906503,
126.457111622482));
#130100=CARTESIAN_POINT('Ctrl Pts',(-221.419912213998,2.17887881886615,
126.392956248477));
#130101=CARTESIAN_POINT('Ctrl Pts',(-221.427658490082,2.0549080685941,126.333861349351));
#130102=CARTESIAN_POINT('Ctrl Pts',(-221.435404766166,1.92868419727716,
126.280052899288));
#130103=CARTESIAN_POINT('Ctrl Pts',(-221.443151099431,1.80245939420445,
126.226244052023));
#130104=CARTESIAN_POINT('Ctrl Pts',(-221.450897432696,1.67398179654851,
126.177721885006));
#130105=CARTESIAN_POINT('Ctrl Pts',(-221.458643765962,1.54373584517392,
126.134664406588));
#130106=CARTESIAN_POINT('Ctrl Pts',(-221.466391833965,1.41346072612213,
126.091597285746));
#130107=CARTESIAN_POINT('Ctrl Pts',(-221.474139901968,1.28141683647249,
126.053997411372));
#130108=CARTESIAN_POINT('Ctrl Pts',(-221.481887969971,1.14810385551625,
126.021992940416));
#130109=CARTESIAN_POINT('Ctrl Pts',(-221.489644272712,1.0146491879365,125.989954454727));
#130110=CARTESIAN_POINT('Ctrl Pts',(-221.497400575454,0.8799231154359,125.963523343362));
#130111=CARTESIAN_POINT('Ctrl Pts',(-221.505156878196,0.744436142079828,
125.942776730306));
#130112=CARTESIAN_POINT('Ctrl Pts',(-221.51291732071,0.608876855246642,
125.922019044158));
#130113=CARTESIAN_POINT('Ctrl Pts',(-221.520677763225,0.472556246746744,
125.906951944727));
#130114=CARTESIAN_POINT('Ctrl Pts',(-221.528438205739,0.335989032823276,
125.897600542698));
#130115=CARTESIAN_POINT('Ctrl Pts',(-221.536211106004,0.199202589084151,
125.888234128968));
#130116=CARTESIAN_POINT('Ctrl Pts',(-221.54398400627,0.062169139894083,
125.884601758268));
#130117=CARTESIAN_POINT('Ctrl Pts',(-221.551756906535,-0.07459660546559,
125.886676364897));
#130118=CARTESIAN_POINT('Ctrl Pts',(-221.559247242297,-0.20639057149043,
125.888675554349));
#130119=CARTESIAN_POINT('Ctrl Pts',(-221.566737578059,-0.337935651642949,
125.895973981788));
#130120=CARTESIAN_POINT('Ctrl Pts',(-221.574227913821,-0.46877850593014,
125.908502186721));
#130121=CARTESIAN_POINT('Ctrl Pts',(-221.58200224794,-0.604582306805123,
125.921505402352));
#130122=CARTESIAN_POINT('Ctrl Pts',(-221.58977658206,-0.740059766480778,
125.940183988278));
#130123=CARTESIAN_POINT('Ctrl Pts',(-221.597550916179,-0.874698460827502,
125.964517059647));
#130124=CARTESIAN_POINT('Ctrl Pts',(-221.605315669126,-1.00917122501645,
125.988820142681));
#130125=CARTESIAN_POINT('Ctrl Pts',(-221.613080422073,-1.14280689959888,
126.018763776762));
#130126=CARTESIAN_POINT('Ctrl Pts',(-221.62084517502,-1.27509676159619,
126.054275217169));
#130127=CARTESIAN_POINT('Ctrl Pts',(-221.628602215905,-1.40725523143761,
126.089751387113));
#130128=CARTESIAN_POINT('Ctrl Pts',(-221.63635925679,-1.53807017359358,
126.130784257681));
#130129=CARTESIAN_POINT('Ctrl Pts',(-221.644116297675,-1.66704201567277,
126.177249858088));
#130130=CARTESIAN_POINT('Ctrl Pts',(-221.651867488915,-1.79591659908276,
126.223680418423));
#130131=CARTESIAN_POINT('Ctrl Pts',(-221.659618680155,-1.92295048258643,
126.275535422055));
#130132=CARTESIAN_POINT('Ctrl Pts',(-221.667369871395,-2.04765859481255,
126.332640887799));
#130133=CARTESIAN_POINT('Ctrl Pts',(-221.675117768172,-2.17231370276445,
126.389722082196));
#130134=CARTESIAN_POINT('Ctrl Pts',(-221.682865664949,-2.29464465079435,
126.452049137816));
#130135=CARTESIAN_POINT('Ctrl Pts',(-221.690613561726,-2.41418593288091,
126.519399784142));
#130136=CARTESIAN_POINT('Ctrl Pts',(-221.698359837811,-2.53370220950794,
126.586736342164));
#130137=CARTESIAN_POINT('Ctrl Pts',(-221.706106113895,-2.65042964047315,
126.659094208951));
#130138=CARTESIAN_POINT('Ctrl Pts',(-221.713852389979,-2.76392729908182,
126.736205145133));
#130139=CARTESIAN_POINT('Ctrl Pts',(-221.721598723244,-2.87742579550457,
126.813316650529));
#130140=CARTESIAN_POINT('Ctrl Pts',(-221.72934505651,-2.98769414860806,
126.89518107562));
#130141=CARTESIAN_POINT('Ctrl Pts',(-221.737091389775,-3.09432074280527,
126.981487064446));
#130142=CARTESIAN_POINT('Ctrl Pts',(-221.744839457778,-3.20097121528938,
127.0678123809));
#130143=CARTESIAN_POINT('Ctrl Pts',(-221.752587525781,-3.3039780021912,
127.158580994414));
#130144=CARTESIAN_POINT('Ctrl Pts',(-221.760335593784,-3.40296319257896,
127.253441782609));
#130145=CARTESIAN_POINT('Ctrl Pts',(-221.768091896526,-3.50205358560459,
127.348403389978));
#130146=CARTESIAN_POINT('Ctrl Pts',(-221.775848199268,-3.59711356121764,
127.447465589105));
#130147=CARTESIAN_POINT('Ctrl Pts',(-221.78360450201,-3.68780229290825,
127.550240565859));
#130148=CARTESIAN_POINT('Ctrl Pts',(-221.791364944524,-3.77853942790554,
127.653070396713));
#130149=CARTESIAN_POINT('Ctrl Pts',(-221.799125387038,-3.86490042408959,
127.759616650167));
#130150=CARTESIAN_POINT('Ctrl Pts',(-221.806885829552,-3.94658593842749,
127.869459853808));
#130151=CARTESIAN_POINT('Ctrl Pts',(-221.814658729818,-4.02840258160471,
127.979479387511));
#130152=CARTESIAN_POINT('Ctrl Pts',(-221.822431630083,-4.10552852446355,
128.092806124215));
#130153=CARTESIAN_POINT('Ctrl Pts',(-221.830204530348,-4.17770832520685,
128.208992394751));
#130154=CARTESIAN_POINT('Ctrl Pts',(-221.83769486611,-4.2472642083826,128.320955001697));
#130155=CARTESIAN_POINT('Ctrl Pts',(-221.845185201872,-4.31222716366422,
128.435572581482));
#130156=CARTESIAN_POINT('Ctrl Pts',(-221.852675537634,-4.37241058879256,
128.552426181239));
#130157=CARTESIAN_POINT('Ctrl Pts',(-221.860945750391,-4.43886017744144,
128.681446316258));
#130158=CARTESIAN_POINT('Ctrl Pts',(-221.869215963147,-4.49967258269311,
128.813559665546));
#130159=CARTESIAN_POINT('Ctrl Pts',(-221.877486175903,-4.55456782312679,
128.948263904828));
#130160=CARTESIAN_POINT('Ctrl Pts',(-221.885736780321,-4.60933290917299,
129.082648765824));
#130161=CARTESIAN_POINT('Ctrl Pts',(-221.893987384739,-4.65820868546935,
129.219611977023));
#130162=CARTESIAN_POINT('Ctrl Pts',(-221.902237989156,-4.70096171190115,
129.358628261374));
#130163=CARTESIAN_POINT('Ctrl Pts',(-221.906633778092,-4.72373983469675,
129.432693895081));
#130164=CARTESIAN_POINT('Ctrl Pts',(-221.911029567028,-4.74478073337568,
129.507341885676));
#130165=CARTESIAN_POINT('Ctrl Pts',(-221.915425355964,-4.76405452823393,
129.582490119308));
#130166=CARTESIAN_POINT('Ctrl Pts',(-220.165126569317,-4.76405452823397,
129.582490119308));
#130167=CARTESIAN_POINT('Ctrl Pts',(-220.170747644464,-4.7886126718321,
129.678241948475));
#130168=CARTESIAN_POINT('Ctrl Pts',(-220.17636871961,-4.81025828360901,
129.774638318243));
#130169=CARTESIAN_POINT('Ctrl Pts',(-220.181989794757,-4.82896777965386,
129.871486968262));
#130170=CARTESIAN_POINT('Ctrl Pts',(-220.19342524438,-4.86703015987755,
130.068514730655));
#130171=CARTESIAN_POINT('Ctrl Pts',(-220.204860694004,-4.89304326287675,
130.267939432194));
#130172=CARTESIAN_POINT('Ctrl Pts',(-220.216296143627,-4.90677295268619,
130.468559704394));
#130173=CARTESIAN_POINT('Ctrl Pts',(-220.222577617089,-4.91431464846764,
130.578760086305));
#130174=CARTESIAN_POINT('Ctrl Pts',(-220.228859090551,-4.91815080839338,
130.689320837773));
#130175=CARTESIAN_POINT('Ctrl Pts',(-220.235140564013,-4.9182481010867,
130.800038736369));
#130176=CARTESIAN_POINT('',(-219.889859435959,-4.9182489279511,130.807607956143));
#130177=CARTESIAN_POINT('Ctrl Pts',(-219.819723804473,-4.76405452823394,
129.582490119308));
#130178=CARTESIAN_POINT('Ctrl Pts',(-219.827373106639,-4.79769696515867,
129.713661470282));
#130179=CARTESIAN_POINT('Ctrl Pts',(-219.835022408805,-4.82589674123163,
129.84614125547));
#130180=CARTESIAN_POINT('Ctrl Pts',(-219.842671710971,-4.84857457688245,
129.979431750991));
#130181=CARTESIAN_POINT('Ctrl Pts',(-219.850536331803,-4.87189076635859,
130.116474213807));
#130182=CARTESIAN_POINT('Ctrl Pts',(-219.858400952634,-4.88936948971227,
130.254373244885));
#130183=CARTESIAN_POINT('Ctrl Pts',(-219.866265573465,-4.90098184698049,
130.39258398143));
#130184=CARTESIAN_POINT('Ctrl Pts',(-219.874130194296,-4.91259420424872,
130.530794717974));
#130185=CARTESIAN_POINT('Ctrl Pts',(-219.881994815128,-4.91834023657183,
130.669316701531));
#130186=CARTESIAN_POINT('Ctrl Pts',(-219.889859435959,-4.9182489279511,
130.807607956143));
#130187=CARTESIAN_POINT('Ctrl Pts',(-219.889859435996,-4.91824892795067,
130.807607956796));
#130188=CARTESIAN_POINT('Ctrl Pts',(-219.900950013032,-4.91812016579959,
131.00262432765));
#130189=CARTESIAN_POINT('Ctrl Pts',(-219.912040590068,-4.90639276669605,
131.197259495506));
#130190=CARTESIAN_POINT('Ctrl Pts',(-219.923131167104,-4.88319915299843,
131.390491229849));
#130191=CARTESIAN_POINT('Ctrl Pts',(-219.930905501223,-4.86694076520351,
131.525943881264));
#130192=CARTESIAN_POINT('Ctrl Pts',(-219.938679835342,-4.84501647276845,
131.66093409222));
#130193=CARTESIAN_POINT('Ctrl Pts',(-219.946454169461,-4.81745945129712,
131.79495008733));
#130194=CARTESIAN_POINT('Ctrl Pts',(-219.954218922408,-4.78993639139199,
131.928800919704));
#130195=CARTESIAN_POINT('Ctrl Pts',(-219.961983675355,-4.75679449262221,
132.06167954586));
#130196=CARTESIAN_POINT('Ctrl Pts',(-219.969748428302,-4.71811868670756,
132.193079134992));
#130197=CARTESIAN_POINT('Ctrl Pts',(-219.977505469187,-4.67948129414857,
132.324348216199));
#130198=CARTESIAN_POINT('Ctrl Pts',(-219.985262510072,-4.63532104211707,
132.45414081113));
#130199=CARTESIAN_POINT('Ctrl Pts',(-219.993019550957,-4.58577385406006,
132.581960466216));
#130200=CARTESIAN_POINT('Ctrl Pts',(-220.000770742197,-4.53626402992305,
132.709683731505));
#130201=CARTESIAN_POINT('Ctrl Pts',(-220.008521933437,-4.4813754963173,
132.835436655281));
#130202=CARTESIAN_POINT('Ctrl Pts',(-220.016273124677,-4.42129382470151,
132.958738480931));
#130203=CARTESIAN_POINT('Ctrl Pts',(-220.024021021455,-4.36123768939881,
133.081987900016));
#130204=CARTESIAN_POINT('Ctrl Pts',(-220.031768918232,-4.29599297698157,
133.202787942275));
#130205=CARTESIAN_POINT('Ctrl Pts',(-220.039516815009,-4.22579306481921,
133.320678569619));
#130206=CARTESIAN_POINT('Ctrl Pts',(-220.047263091093,-4.15560783696496,
133.438544536787));
#130207=CARTESIAN_POINT('Ctrl Pts',(-220.055009367177,-4.08046967096488,
133.553501963846));
#130208=CARTESIAN_POINT('Ctrl Pts',(-220.062755643261,-4.00065730996832,
133.665116488083));
#130209=CARTESIAN_POINT('Ctrl Pts',(-220.070501976526,-3.92084435981515,
133.776731836233));
#130210=CARTESIAN_POINT('Ctrl Pts',(-220.078248309792,-3.83635737322495,
133.885003914298));
#130211=CARTESIAN_POINT('Ctrl Pts',(-220.085994643057,-3.74751749413209,
133.98952869691));
#130212=CARTESIAN_POINT('Ctrl Pts',(-220.09374271106,-3.65865771996439,
134.094076887123));
#130213=CARTESIAN_POINT('Ctrl Pts',(-220.101490779063,-3.56544336670402,
134.194875814167));
#130214=CARTESIAN_POINT('Ctrl Pts',(-220.109238847066,-3.4682345244356,
134.291556101908));
#130215=CARTESIAN_POINT('Ctrl Pts',(-220.116995149808,-3.37092236745269,
134.388339142609));
#130216=CARTESIAN_POINT('Ctrl Pts',(-220.12475145255,-3.26960751848575,
134.480994523663));
#130217=CARTESIAN_POINT('Ctrl Pts',(-220.132507755291,-3.16468585888112,
134.569190823179));
#130218=CARTESIAN_POINT('Ctrl Pts',(-220.140268197806,-3.05970819942764,
134.657434195716));
#130219=CARTESIAN_POINT('Ctrl Pts',(-220.14802864032,-2.95112020287667,
134.741213505764));
#130220=CARTESIAN_POINT('Ctrl Pts',(-220.155789082834,-2.839348404252,134.820239562675));
#130221=CARTESIAN_POINT('Ctrl Pts',(-220.163561983099,-2.72739717961353,
134.899392479229));
#130222=CARTESIAN_POINT('Ctrl Pts',(-220.171334883365,-2.61225226824061,
134.973776682517));
#130223=CARTESIAN_POINT('Ctrl Pts',(-220.17910778363,-2.49436734028331,
135.043147547128));
#130224=CARTESIAN_POINT('Ctrl Pts',(-220.186598119392,-2.38076782639178,
135.109996606076));
#130225=CARTESIAN_POINT('Ctrl Pts',(-220.194088455154,-2.2646243218323,
135.172190347753));
#130226=CARTESIAN_POINT('Ctrl Pts',(-220.201578790916,-2.14636013676526,
135.229552277348));
#130227=CARTESIAN_POINT('Ctrl Pts',(-220.209353125035,-2.02361192917527,
135.289089101939));
#130228=CARTESIAN_POINT('Ctrl Pts',(-220.217127459154,-1.89819022598548,
135.343609080126));
#130229=CARTESIAN_POINT('Ctrl Pts',(-220.224901793273,-1.77054353054598,
135.392863496386));
#130230=CARTESIAN_POINT('Ctrl Pts',(-220.23266654622,-1.64305414825084,
135.442057210981));
#130231=CARTESIAN_POINT('Ctrl Pts',(-220.240431299168,-1.51334559092697,
135.485998136096));
#130232=CARTESIAN_POINT('Ctrl Pts',(-220.248196052115,-1.38189017735495,
135.524483772763));
#130233=CARTESIAN_POINT('Ctrl Pts',(-220.255953093,-1.2505653271529,135.562931184954));
#130234=CARTESIAN_POINT('Ctrl Pts',(-220.263710133885,-1.11749744622303,
135.595933982157));
#130235=CARTESIAN_POINT('Ctrl Pts',(-220.27146717477,-0.983177684957099,
135.623338175337));
#130236=CARTESIAN_POINT('Ctrl Pts',(-220.27921836601,-0.848959215267808,
135.650721702802));
#130237=CARTESIAN_POINT('Ctrl Pts',(-220.28696955725,-0.71349112584585,
135.672514951943));
#130238=CARTESIAN_POINT('Ctrl Pts',(-220.29472074849,-0.57727819675249,
135.688614188589));
#130239=CARTESIAN_POINT('Ctrl Pts',(-220.302468645267,-0.441123161787408,
135.704706582631));
#130240=CARTESIAN_POINT('Ctrl Pts',(-220.310216542045,-0.304224304247776,
135.715109731794));
#130241=CARTESIAN_POINT('Ctrl Pts',(-220.317964438822,-0.167094813374376,
135.719771321245));
#130242=CARTESIAN_POINT('Ctrl Pts',(-220.325710714906,-0.0299940070346701,
135.724431935593));
#130243=CARTESIAN_POINT('Ctrl Pts',(-220.33345699099,0.107336946187845,
135.72335336583));
#130244=CARTESIAN_POINT('Ctrl Pts',(-220.341203267074,0.244381937159659,
135.716535342806));
#130245=CARTESIAN_POINT('Ctrl Pts',(-220.348949600339,0.381427939766652,
135.709717269454));
#130246=CARTESIAN_POINT('Ctrl Pts',(-220.356695933605,0.518187585428513,
135.697159677726));
#130247=CARTESIAN_POINT('Ctrl Pts',(-220.36444226687,0.654147370020168,
135.678914369531));
#130248=CARTESIAN_POINT('Ctrl Pts',(-220.372190334873,0.790137601862718,
135.660664975425));
#130249=CARTESIAN_POINT('Ctrl Pts',(-220.379938402876,0.925327228782847,
135.636725382278));
#130250=CARTESIAN_POINT('Ctrl Pts',(-220.387686470879,1.05921084669146,
135.607198887251));
#130251=CARTESIAN_POINT('Ctrl Pts',(-220.395442773621,1.1932367577026,135.577641011114));
#130252=CARTESIAN_POINT('Ctrl Pts',(-220.403199076363,1.32595350453939,
135.542484455986));
#130253=CARTESIAN_POINT('Ctrl Pts',(-220.410955379105,1.45686826904143,
135.501883146427));
#130254=CARTESIAN_POINT('Ctrl Pts',(-220.418715821619,1.58785290669506,
135.461260166728));
#130255=CARTESIAN_POINT('Ctrl Pts',(-220.426476264133,1.71703327753685,
135.415186773362));
#130256=CARTESIAN_POINT('Ctrl Pts',(-220.434236706647,1.84393552468517,
135.363865507716));
#130257=CARTESIAN_POINT('Ctrl Pts',(-220.442009606913,1.97104148658646,
135.312461856619));
#130258=CARTESIAN_POINT('Ctrl Pts',(-220.449782507178,2.09586166065049,
135.25579366042));
#130259=CARTESIAN_POINT('Ctrl Pts',(-220.457555407443,2.2179450167936,135.194110378655));
#130260=CARTESIAN_POINT('Ctrl Pts',(-220.465045743205,2.33559033543083,
135.134669439553));
#130261=CARTESIAN_POINT('Ctrl Pts',(-220.472536078967,2.45069409289816,
135.070571856355));
#130262=CARTESIAN_POINT('Ctrl Pts',(-220.480026414729,2.56287898963283,
135.002078372132));
#130263=CARTESIAN_POINT('Ctrl Pts',(-220.487800748849,2.67931741082588,
134.930987936636));
#130264=CARTESIAN_POINT('Ctrl Pts',(-220.495575082967,2.79298010672972,
134.854936485549));
#130265=CARTESIAN_POINT('Ctrl Pts',(-220.503349417087,2.90341539891617,
134.774166920629));
#130266=CARTESIAN_POINT('Ctrl Pts',(-220.511114170034,3.01371458947458,
134.693496896978));
#130267=CARTESIAN_POINT('Ctrl Pts',(-220.518878922981,3.12079397778714,
134.608120557506));
#130268=CARTESIAN_POINT('Ctrl Pts',(-220.526643675928,3.22422789589776,
134.51832582174));
#130269=CARTESIAN_POINT('Ctrl Pts',(-220.534400716813,3.32755908198275,
134.428620271371));
#130270=CARTESIAN_POINT('Ctrl Pts',(-220.542157757698,3.4272517099638,134.334505312493));
#130271=CARTESIAN_POINT('Ctrl Pts',(-220.549914798583,3.52291074572038,
134.236310929005));
#130272=CARTESIAN_POINT('Ctrl Pts',(-220.557665989823,3.61849764425412,
134.138190594666));
#130273=CARTESIAN_POINT('Ctrl Pts',(-220.565417181063,3.71005673329742,
134.03599723787));
#130274=CARTESIAN_POINT('Ctrl Pts',(-220.573168372303,3.7972278924029,133.930099473526));
#130275=CARTESIAN_POINT('Ctrl Pts',(-220.58091626908,3.8843620014405,133.824246718557));
#130276=CARTESIAN_POINT('Ctrl Pts',(-220.588664165858,3.9671116419044,133.714692988765));
#130277=CARTESIAN_POINT('Ctrl Pts',(-220.596412062635,4.04515540852403,
133.601841767349));
#130278=CARTESIAN_POINT('Ctrl Pts',(-220.604158338719,4.12318285006989,
133.489014151975));
#130279=CARTESIAN_POINT('Ctrl Pts',(-220.611904614803,4.19650615349358,
133.372890738312));
#130280=CARTESIAN_POINT('Ctrl Pts',(-220.619650890887,4.26484612275778,
133.253905598108));
#130281=CARTESIAN_POINT('Ctrl Pts',(-220.627397224152,4.33318659649221,
133.134919579582));
#130282=CARTESIAN_POINT('Ctrl Pts',(-220.635143557418,4.3965434679426,133.013072131388));
#130283=CARTESIAN_POINT('Ctrl Pts',(-220.642889890683,4.45468275799805,
132.888823279284));
#130284=CARTESIAN_POINT('Ctrl Pts',(-220.650637958686,4.51283506794448,
132.76454660251));
#130285=CARTESIAN_POINT('Ctrl Pts',(-220.658386026689,4.56576730576534,
132.637867805759));
#130286=CARTESIAN_POINT('Ctrl Pts',(-220.666134094692,4.61329319503459,
132.509267934445));
#130287=CARTESIAN_POINT('Ctrl Pts',(-220.673890397434,4.66086959538445,
132.380531385657));
#130288=CARTESIAN_POINT('Ctrl Pts',(-220.681646700176,4.70302803332159,
132.249870051016));
#130289=CARTESIAN_POINT('Ctrl Pts',(-220.689403002918,4.73963162968545,
132.117781752383));
#130290=CARTESIAN_POINT('Ctrl Pts',(-220.697163445432,4.7762547624908,131.985622954249));
#130291=CARTESIAN_POINT('Ctrl Pts',(-220.704923887946,4.80731705763174,
131.852036055162));
#130292=CARTESIAN_POINT('Ctrl Pts',(-220.71268433046,4.83273278769379,131.717529202905));
#130293=CARTESIAN_POINT('Ctrl Pts',(-220.720457230726,4.85818931734204,
131.582806428307));
#130294=CARTESIAN_POINT('Ctrl Pts',(-220.728230130991,4.87798111193681,
131.447161136533));
#130295=CARTESIAN_POINT('Ctrl Pts',(-220.736003031256,4.89207425607369,
131.311107630938));
#130296=CARTESIAN_POINT('Ctrl Pts',(-220.743493367018,4.9056550789226,131.18000001297));
#130297=CARTESIAN_POINT('Ctrl Pts',(-220.75098370278,4.91394435931675,131.048513652516));
#130298=CARTESIAN_POINT('Ctrl Pts',(-220.758474038542,4.91695752815712,
130.917106920383));
#130299=CARTESIAN_POINT('Ctrl Pts',(-220.766248372661,4.92008494220994,
130.78071786206));
#130300=CARTESIAN_POINT('Ctrl Pts',(-220.774022706781,4.91753816602361,
130.643982549929));
#130301=CARTESIAN_POINT('Ctrl Pts',(-220.7817970409,4.90927741650165,130.507412288177));
#130302=CARTESIAN_POINT('Ctrl Pts',(-220.789561793847,4.90102684761518,
130.371010337067));
#130303=CARTESIAN_POINT('Ctrl Pts',(-220.797326546794,4.88707634017612,
130.234773418115));
#130304=CARTESIAN_POINT('Ctrl Pts',(-220.805091299741,4.86743804510946,
130.099215285368));
#130305=CARTESIAN_POINT('Ctrl Pts',(-220.812848340626,4.84781925507433,
129.963791790869));
#130306=CARTESIAN_POINT('Ctrl Pts',(-220.820605381511,4.82252397524754,
129.829046125347));
#130307=CARTESIAN_POINT('Ctrl Pts',(-220.828362422396,4.7916163048381,129.695489006553));
#130308=CARTESIAN_POINT('Ctrl Pts',(-220.836113613636,4.76073194214338,
129.562032604223));
#130309=CARTESIAN_POINT('Ctrl Pts',(-220.843864804876,4.72424370088741,
129.429763343962));
#130310=CARTESIAN_POINT('Ctrl Pts',(-220.851615996116,4.68226705333496,
129.299183450667));
#130311=CARTESIAN_POINT('Ctrl Pts',(-220.859363892894,4.64030824697743,
129.168659057309));
#130312=CARTESIAN_POINT('Ctrl Pts',(-220.867111789671,4.59286579332397,
129.039822974245));
#130313=CARTESIAN_POINT('Ctrl Pts',(-220.874859686448,4.54010542681638,
128.913163701353));
#130314=CARTESIAN_POINT('Ctrl Pts',(-220.882605962532,4.48735609664008,
128.786530922851));
#130315=CARTESIAN_POINT('Ctrl Pts',(-220.890352238616,4.42929121646095,
128.6620744095));
#130316=CARTESIAN_POINT('Ctrl Pts',(-220.8980985147,4.36612507085669,128.540263683215));
#130317=CARTESIAN_POINT('Ctrl Pts',(-220.905844847965,4.30295845897437,
128.418452057752));
#130318=CARTESIAN_POINT('Ctrl Pts',(-220.913591181231,4.23469068650564,
128.299286605402));
#130319=CARTESIAN_POINT('Ctrl Pts',(-220.921337514496,4.16158231472618,
128.183212834579));
#130320=CARTESIAN_POINT('Ctrl Pts',(-220.929085582499,4.08845757083364,
128.067113069839));
#130321=CARTESIAN_POINT('Ctrl Pts',(-220.936833650502,4.0104902788811,127.954106695096));
#130322=CARTESIAN_POINT('Ctrl Pts',(-220.944581718505,3.92798446904098,
127.844610446779));
#130323=CARTESIAN_POINT('Ctrl Pts',(-220.952338021247,3.84539097104444,
127.734997824546));
#130324=CARTESIAN_POINT('Ctrl Pts',(-220.960094323989,3.75824955517193,
127.628903093767));
#130325=CARTESIAN_POINT('Ctrl Pts',(-220.967850626731,3.66690506652434,
127.526710499631));
#130326=CARTESIAN_POINT('Ctrl Pts',(-220.975611069245,3.57551182457258,
127.424463362231));
#130327=CARTESIAN_POINT('Ctrl Pts',(-220.983371511759,3.47991131225539,
127.326122791601));
#130328=CARTESIAN_POINT('Ctrl Pts',(-220.991131954273,3.38048471093133,
127.232035578931));
#130329=CARTESIAN_POINT('Ctrl Pts',(-220.998904854539,3.28089850120042,
127.137797329115));
#130330=CARTESIAN_POINT('Ctrl Pts',(-221.006677754804,3.17747422397626,
127.047826338265));
#130331=CARTESIAN_POINT('Ctrl Pts',(-221.01445065507,3.07062624513349,126.962429133898));
#130332=CARTESIAN_POINT('Ctrl Pts',(-221.021940990832,2.96766245945721,
126.880136333014));
#130333=CARTESIAN_POINT('Ctrl Pts',(-221.029431326594,2.86151981905106,
126.802090737096));
#130334=CARTESIAN_POINT('Ctrl Pts',(-221.036921662355,2.75259230503557,
126.728527124309));
#130335=CARTESIAN_POINT('Ctrl Pts',(-221.044695996474,2.63953477121693,
126.652174324782));
#130336=CARTESIAN_POINT('Ctrl Pts',(-221.052470330594,2.52311888583939,
126.580408223564));
#130337=CARTESIAN_POINT('Ctrl Pts',(-221.060244664713,2.40375331986032,
126.513538663702));
#130338=CARTESIAN_POINT('Ctrl Pts',(-221.06800941766,2.28453486127299,126.446751514597));
#130339=CARTESIAN_POINT('Ctrl Pts',(-221.075774170607,2.16237429289868,
126.384849089139));
#130340=CARTESIAN_POINT('Ctrl Pts',(-221.083538923554,2.03771041843704,
126.328098861023));
#130341=CARTESIAN_POINT('Ctrl Pts',(-221.091295964439,1.91317036189297,
126.271404998033));
#130342=CARTESIAN_POINT('Ctrl Pts',(-221.099053005324,1.78613230067616,
126.21985330979));
#130343=CARTESIAN_POINT('Ctrl Pts',(-221.106810046209,1.65706056328343,
126.173665923234));
#130344=CARTESIAN_POINT('Ctrl Pts',(-221.114561237449,1.52808615989209,
126.127513366946));
#130345=CARTESIAN_POINT('Ctrl Pts',(-221.122312428689,1.39708149950177,
126.086717191689));
#130346=CARTESIAN_POINT('Ctrl Pts',(-221.130063619929,1.26453153371922,
126.051451712198));
#130347=CARTESIAN_POINT('Ctrl Pts',(-221.137811516706,1.13203790520784,
126.016201221476));
#130348=CARTESIAN_POINT('Ctrl Pts',(-221.145559413483,0.998000654652205,
125.986476851482));
#130349=CARTESIAN_POINT('Ctrl Pts',(-221.15330731026,0.862920354351025,
125.962403211253));
#130350=CARTESIAN_POINT('Ctrl Pts',(-221.161053586345,0.727868309937043,
125.938334606711));
#130351=CARTESIAN_POINT('Ctrl Pts',(-221.168799862429,0.59177403441315,
125.919914449403));
#130352=CARTESIAN_POINT('Ctrl Pts',(-221.176546138513,0.455148375913521,
125.907216243709));
#130353=CARTESIAN_POINT('Ctrl Pts',(-221.184292471778,0.318521708874132,
125.894517944279));
#130354=CARTESIAN_POINT('Ctrl Pts',(-221.192038805043,0.181364040319306,
125.887541716927));
#130355=CARTESIAN_POINT('Ctrl Pts',(-221.199785138309,0.0441910288280734,
125.886309152253));
#130356=CARTESIAN_POINT('Ctrl Pts',(-221.207533206312,-0.0930127016078046,
125.885076311553));
#130357=CARTESIAN_POINT('Ctrl Pts',(-221.215281274314,-0.23023139094262,
125.889589696539));
#130358=CARTESIAN_POINT('Ctrl Pts',(-221.223029342317,-0.366950091281238,
125.899818774233));
#130359=CARTESIAN_POINT('Ctrl Pts',(-221.230785645059,-0.503814097881735,
125.910058723512));
#130360=CARTESIAN_POINT('Ctrl Pts',(-221.238541947801,-0.64017666347159,
125.926026471164));
#130361=CARTESIAN_POINT('Ctrl Pts',(-221.246298250543,-0.775528114489551,
125.94763958315));
#130362=CARTESIAN_POINT('Ctrl Pts',(-221.254058693057,-0.910951806652642,
125.969264230705));
#130363=CARTESIAN_POINT('Ctrl Pts',(-221.261819135571,-1.04536292595293,
125.996540168737));
#130364=CARTESIAN_POINT('Ctrl Pts',(-221.269579578086,-1.17826366930557,
126.029334147682));
#130365=CARTESIAN_POINT('Ctrl Pts',(-221.277352478351,-1.31137775672946,
126.062180770433));
#130366=CARTESIAN_POINT('Ctrl Pts',(-221.285125378616,-1.44297624756009,
126.100563025771));
#130367=CARTESIAN_POINT('Ctrl Pts',(-221.292898278882,-1.57257727663969,
126.14429798156));
#130368=CARTESIAN_POINT('Ctrl Pts',(-221.300388614644,-1.69746698186977,
126.186443061546));
#130369=CARTESIAN_POINT('Ctrl Pts',(-221.307878950406,-1.82050164190373,
126.233558320073));
#130370=CARTESIAN_POINT('Ctrl Pts',(-221.315369286168,-1.94127077480415,
126.285439193001));
#130371=CARTESIAN_POINT('Ctrl Pts',(-221.323144083621,-2.06662637656044,
126.339290354215));
#130372=CARTESIAN_POINT('Ctrl Pts',(-221.330918881074,-2.1899380864231,
126.398446846992));
#130373=CARTESIAN_POINT('Ctrl Pts',(-221.338693678526,-2.3107242423772,
126.462732289601));
#130374=CARTESIAN_POINT('Ctrl Pts',(-221.346458789292,-2.4313599098228,
126.526937638425));
#130375=CARTESIAN_POINT('Ctrl Pts',(-221.354223900058,-2.54947594257647,
126.59625903987));
#130376=CARTESIAN_POINT('Ctrl Pts',(-221.361989010823,-2.66461006112031,
126.670471857007));
#130377=CARTESIAN_POINT('Ctrl Pts',(-221.369746304462,-2.77962827428892,
126.744609964192));
#130378=CARTESIAN_POINT('Ctrl Pts',(-221.3775035981,-2.89167022096498,126.823629476611));
#130379=CARTESIAN_POINT('Ctrl Pts',(-221.385260891738,-3.0002979989038,
126.907259774596));
#130380=CARTESIAN_POINT('Ctrl Pts',(-221.393011880304,-3.10883748497579,
126.990822098484));
#130381=CARTESIAN_POINT('Ctrl Pts',(-221.400762868871,-3.21396801915762,
127.078987508418));
#130382=CARTESIAN_POINT('Ctrl Pts',(-221.408513857437,-3.31528085322855,
127.171442241561));
#130383=CARTESIAN_POINT('Ctrl Pts',(-221.416261396742,-3.41654860215193,
127.263855831492));
#130384=CARTESIAN_POINT('Ctrl Pts',(-221.424008936047,-3.5140017427338,
127.360554684248));
#130385=CARTESIAN_POINT('Ctrl Pts',(-221.431756475352,-3.6072649213944,
127.461185053917));
#130386=CARTESIAN_POINT('Ctrl Pts',(-221.439502244726,-3.70050679401147,
127.561792434503));
#130387=CARTESIAN_POINT('Ctrl Pts',(-221.4472480141,-3.78956034409026,127.666329258117));
#130388=CARTESIAN_POINT('Ctrl Pts',(-221.454993783473,-3.87408767204341,
127.774405540041));
#130389=CARTESIAN_POINT('Ctrl Pts',(-221.462739460707,-3.95861399450273,
127.882480536344));
#130390=CARTESIAN_POINT('Ctrl Pts',(-221.470485137941,-4.03861396203924,
127.994094598687));
#130391=CARTESIAN_POINT('Ctrl Pts',(-221.478230815175,-4.11379075744866,
128.108825667611));
#130392=CARTESIAN_POINT('Ctrl Pts',(-221.485981813398,-4.18901919648106,
128.223635552452));
#130393=CARTESIAN_POINT('Ctrl Pts',(-221.49373281162,-4.25941762770265,
128.341566395407));
#130394=CARTESIAN_POINT('Ctrl Pts',(-221.501483809842,-4.32473311558681,
128.462167939444));
#130395=CARTESIAN_POINT('Ctrl Pts',(-221.50923737993,-4.39007027586261,
128.58280950039));
#130396=CARTESIAN_POINT('Ctrl Pts',(-221.516990950017,-4.45032095711604,
128.706123178454));
#130397=CARTESIAN_POINT('Ctrl Pts',(-221.524744520105,-4.5052792459048,
128.831636110971));
#130398=CARTESIAN_POINT('Ctrl Pts',(-221.532507821331,-4.56030651023185,
128.957306568809));
#130399=CARTESIAN_POINT('Ctrl Pts',(-221.540271122556,-4.61002796411655,
129.085181433099));
#130400=CARTESIAN_POINT('Ctrl Pts',(-221.548034423782,-4.65428647230588,
129.214769319084));
#130401=CARTESIAN_POINT('Ctrl Pts',(-221.555295960669,-4.69568442666006,
129.335981569752));
#130402=CARTESIAN_POINT('Ctrl Pts',(-221.562557497555,-4.73230319573831,
129.458692155801));
#130403=CARTESIAN_POINT('Ctrl Pts',(-221.569819034442,-4.76405452823418,
129.582490119309));
#130404=CARTESIAN_POINT('Origin',(213.235140564004,0.,130.804360617566));
#130405=CARTESIAN_POINT('',(-223.665116307759,-4.76405452823394,129.582490119308));
#130406=CARTESIAN_POINT('',(-223.320144520485,-4.76405452823402,129.582490119308));
#130407=CARTESIAN_POINT('',(213.235140564004,-4.76405452823405,129.582490119308));
#130408=CARTESIAN_POINT('',(-221.985140563982,-4.91824995565472,130.803700161376));
#130409=CARTESIAN_POINT('Ctrl Pts',(-221.985140564013,-4.91824995565479,
130.803700161931));
#130410=CARTESIAN_POINT('Ctrl Pts',(-221.993178256749,-4.91826912013828,
130.946413336073));
#130411=CARTESIAN_POINT('Ctrl Pts',(-222.001215949486,-4.91207227540122,
131.089033628501));
#130412=CARTESIAN_POINT('Ctrl Pts',(-222.009253642222,-4.89970964901554,
131.231008502647));
#130413=CARTESIAN_POINT('Ctrl Pts',(-222.017299291977,-4.88733478408705,
131.373123926667));
#130414=CARTESIAN_POINT('Ctrl Pts',(-222.025344941732,-4.86878199361895,
131.514592312837));
#130415=CARTESIAN_POINT('Ctrl Pts',(-222.033390591486,-4.84415304880318,
131.654868878708));
#130416=CARTESIAN_POINT('Ctrl Pts',(-222.041534972316,-4.81922187330652,
131.796866829005));
#130417=CARTESIAN_POINT('Ctrl Pts',(-222.049679353146,-4.78806451638956,
131.937643156266));
#130418=CARTESIAN_POINT('Ctrl Pts',(-222.057823733976,-4.75083869372908,
132.076647836973));
#130419=CARTESIAN_POINT('Ctrl Pts',(-222.06589426754,-4.71395040750041,
132.214392125281));
#130420=CARTESIAN_POINT('Ctrl Pts',(-222.073964801103,-4.6711034313127,
132.350396457847));
#130421=CARTESIAN_POINT('Ctrl Pts',(-222.082035334667,-4.62250005030999,
132.484145230957));
#130422=CARTESIAN_POINT('Ctrl Pts',(-222.09021663913,-4.57322957088086,
132.61972975282));
#130423=CARTESIAN_POINT('Ctrl Pts',(-222.098397943593,-4.51804366592107,
132.752996004699));
#130424=CARTESIAN_POINT('Ctrl Pts',(-222.106579248056,-4.45720141736564,
132.883432186208));
#130425=CARTESIAN_POINT('Ctrl Pts',(-222.11476055252,-4.39635916881021,
133.013868367716));
#130426=CARTESIAN_POINT('Ctrl Pts',(-222.122941856983,-4.32986080206274,
133.141474185439));
#130427=CARTESIAN_POINT('Ctrl Pts',(-222.131123161446,-4.25801094468777,
133.265767909629));
#130428=CARTESIAN_POINT('Ctrl Pts',(-222.138897495565,-4.18973518253385,
133.383878773867));
#130429=CARTESIAN_POINT('Ctrl Pts',(-222.146671829684,-4.11643322368602,
133.499333762852));
#130430=CARTESIAN_POINT('Ctrl Pts',(-222.154446163803,-4.03833706091389,
133.611675499254));
#130431=CARTESIAN_POINT('Ctrl Pts',(-222.16221091675,-3.96033714468272,
133.723878784507));
#130432=CARTESIAN_POINT('Ctrl Pts',(-222.169975669698,-3.87755500155651,
133.832976133341));
#130433=CARTESIAN_POINT('Ctrl Pts',(-222.177740422645,-3.79026825329181,
133.938535091106));
#130434=CARTESIAN_POINT('Ctrl Pts',(-222.18549746353,-3.70306819945601,
134.043989206226));
#130435=CARTESIAN_POINT('Ctrl Pts',(-222.193254504415,-3.61137269154984,
134.145911624703));
#130436=CARTESIAN_POINT('Ctrl Pts',(-222.2010115453,-3.51550213871602,134.243899507473));
#130437=CARTESIAN_POINT('Ctrl Pts',(-222.20876273654,-3.41970388261198,
134.341813496818));
#130438=CARTESIAN_POINT('Ctrl Pts',(-222.21651392778,-3.31973712065904,
134.435798577891));
#130439=CARTESIAN_POINT('Ctrl Pts',(-222.22426511902,-3.21596171971684,
134.525485888209));
#130440=CARTESIAN_POINT('Ctrl Pts',(-222.232013015797,-3.1122304260882,
134.615135079027));
#130441=CARTESIAN_POINT('Ctrl Pts',(-222.239760912574,-3.0046940082699,
134.700489877081));
#130442=CARTESIAN_POINT('Ctrl Pts',(-222.247508809351,-2.89374812042594,
134.781219287173));
#130443=CARTESIAN_POINT('Ctrl Pts',(-222.255255085435,-2.78282544007,134.861931810413));
#130444=CARTESIAN_POINT('Ctrl Pts',(-222.26300136152,-2.66849502418884,
134.938020640278));
#130445=CARTESIAN_POINT('Ctrl Pts',(-222.270747637604,-2.55118411959399,
135.009196244607));
#130446=CARTESIAN_POINT('Ctrl Pts',(-222.278493970869,-2.43387234903685,
135.080372374338));
#130447=CARTESIAN_POINT('Ctrl Pts',(-222.286240304134,-2.31358038011799,
135.146635003361));
#130448=CARTESIAN_POINT('Ctrl Pts',(-222.2939866374,-2.19076249126769,135.207739180596));
#130449=CARTESIAN_POINT('Ctrl Pts',(-222.301734705403,-2.06791709820258,
135.268857041689));
#130450=CARTESIAN_POINT('Ctrl Pts',(-222.309482773406,-1.9425450095733,
135.324813978163));
#130451=CARTESIAN_POINT('Ctrl Pts',(-222.317230841409,-1.8151226621441,
135.375412223474));
#130452=CARTESIAN_POINT('Ctrl Pts',(-222.32498714415,-1.68756488872789,
135.426064245201));
#130453=CARTESIAN_POINT('Ctrl Pts',(-222.332743446892,-1.5579528675906,
135.471346054309));
#130454=CARTESIAN_POINT('Ctrl Pts',(-222.340499749634,-1.42678099251033,
135.511108864701));
#130455=CARTESIAN_POINT('Ctrl Pts',(-222.348260192148,-1.29553910705082,
135.550892897703));
#130456=CARTESIAN_POINT('Ctrl Pts',(-222.356020634663,-1.16273608712611,
135.585151964909));
#130457=CARTESIAN_POINT('Ctrl Pts',(-222.363781077177,-1.02887787696217,
135.613788169448));
#130458=CARTESIAN_POINT('Ctrl Pts',(-222.371553977442,-0.894804785715897,
135.642470343364));
#130459=CARTESIAN_POINT('Ctrl Pts',(-222.379326877708,-0.759673504932953,
135.665511551398));
#130460=CARTESIAN_POINT('Ctrl Pts',(-222.387099777973,-0.623997375986374,
135.682865546052));
#130461=CARTESIAN_POINT('Ctrl Pts',(-222.394590113735,-0.49325341607235,
135.699588679288));
#130462=CARTESIAN_POINT('Ctrl Pts',(-222.402080449497,-0.362003840312219,
135.711030882678));
#130463=CARTESIAN_POINT('Ctrl Pts',(-222.409570785259,-0.23070725781262,
135.717196583044));
#130464=CARTESIAN_POINT('Ctrl Pts',(-222.417345119379,-0.0944325254829208,
135.723596057813));
#130465=CARTESIAN_POINT('Ctrl Pts',(-222.425119453498,0.0423245258622504,
135.724331285506));
#130466=CARTESIAN_POINT('Ctrl Pts',(-222.432893787617,0.179053693964256,
135.719350224592));
#130467=CARTESIAN_POINT('Ctrl Pts',(-222.440658540564,0.315614355586413,
135.714375302391));
#130468=CARTESIAN_POINT('Ctrl Pts',(-222.448423293511,0.452146815383447,
135.703698122763));
#130469=CARTESIAN_POINT('Ctrl Pts',(-222.456188046458,0.588137175670653,
135.687318504451));
#130470=CARTESIAN_POINT('Ctrl Pts',(-222.463945087343,0.723992468414893,
135.670955154608));
#130471=CARTESIAN_POINT('Ctrl Pts',(-222.471702128228,0.859306347483183,
135.648900683635));
#130472=CARTESIAN_POINT('Ctrl Pts',(-222.479459169113,0.993566703993762,
135.621206916465));
#130473=CARTESIAN_POINT('Ctrl Pts',(-222.487210360353,1.12772581372565,
135.59353403338));
#130474=CARTESIAN_POINT('Ctrl Pts',(-222.494961551593,1.26083260088827,
135.560230397376));
#130475=CARTESIAN_POINT('Ctrl Pts',(-222.502712742833,1.39238221420001,
135.521399395452));
#130476=CARTESIAN_POINT('Ctrl Pts',(-222.510460639611,1.52387591541635,
135.48258489774));
#130477=CARTESIAN_POINT('Ctrl Pts',(-222.518208536388,1.65381338494664,
135.438247817095));
#130478=CARTESIAN_POINT('Ctrl Pts',(-222.525956433165,1.78170228641648,
135.388542117581));
#130479=CARTESIAN_POINT('Ctrl Pts',(-222.533702709249,1.90956443628511,
135.338846815428));
#130480=CARTESIAN_POINT('Ctrl Pts',(-222.541448985333,2.03537850625734,
135.283785269656));
#130481=CARTESIAN_POINT('Ctrl Pts',(-222.549195261417,2.15866996738857,
135.223560435904));
#130482=CARTESIAN_POINT('Ctrl Pts',(-222.556941594682,2.28196233862919,
135.163335157585));
#130483=CARTESIAN_POINT('Ctrl Pts',(-222.564687927948,2.40273171257697,
135.09794668683));
#130484=CARTESIAN_POINT('Ctrl Pts',(-222.572434261213,2.52052645636256,
135.027644818905));
#130485=CARTESIAN_POINT('Ctrl Pts',(-222.580182329216,2.63834757946446,
134.957327207364));
#130486=CARTESIAN_POINT('Ctrl Pts',(-222.587930397219,2.75319241119095,
134.882094209466));
#130487=CARTESIAN_POINT('Ctrl Pts',(-222.595678465222,2.86463703923666,
134.802239767307));
#130488=CARTESIAN_POINT('Ctrl Pts',(-222.603434767964,2.97620011195942,
134.722300454896));
#130489=CARTESIAN_POINT('Ctrl Pts',(-222.611191070706,3.08435544378355,
134.637730114602));
#130490=CARTESIAN_POINT('Ctrl Pts',(-222.618947373447,3.1887106248404,134.548864271394));
#130491=CARTESIAN_POINT('Ctrl Pts',(-222.626707815962,3.29312150339945,
134.45995099781));
#130492=CARTESIAN_POINT('Ctrl Pts',(-222.634468258476,3.39372790307092,
134.366737918619));
#130493=CARTESIAN_POINT('Ctrl Pts',(-222.64222870099,3.4901739852307,134.269597783377));
#130494=CARTESIAN_POINT('Ctrl Pts',(-222.650001601255,3.58677489120363,
134.172301710167));
#130495=CARTESIAN_POINT('Ctrl Pts',(-222.657774501521,3.67920187011259,
134.071066272282));
#130496=CARTESIAN_POINT('Ctrl Pts',(-222.665547401786,3.76713853907477,
133.966298360457));
#130497=CARTESIAN_POINT('Ctrl Pts',(-222.673037737548,3.85187848862107,
133.865339026121));
#130498=CARTESIAN_POINT('Ctrl Pts',(-222.68052807331,3.93244874003939,133.761099831278));
#130499=CARTESIAN_POINT('Ctrl Pts',(-222.688018409072,4.00860512831597,
133.653969009563));
#130500=CARTESIAN_POINT('Ctrl Pts',(-222.695792743191,4.08764900920118,
133.542776290181));
#130501=CARTESIAN_POINT('Ctrl Pts',(-222.70356707731,4.16218810381081,133.428116118251));
#130502=CARTESIAN_POINT('Ctrl Pts',(-222.711341411429,4.23190285134811,
133.310389611662));
#130503=CARTESIAN_POINT('Ctrl Pts',(-222.719106164377,4.30153168168965,
133.192808192472));
#130504=CARTESIAN_POINT('Ctrl Pts',(-222.726870917324,4.36634779758546,
133.07216829085));
#130505=CARTESIAN_POINT('Ctrl Pts',(-222.734635670271,4.42607327228962,
132.948902165502));
#130506=CARTESIAN_POINT('Ctrl Pts',(-222.742392711156,4.48573942681049,
132.825758469807));
#130507=CARTESIAN_POINT('Ctrl Pts',(-222.750149752041,4.54032483262773,
132.699994090787));
#130508=CARTESIAN_POINT('Ctrl Pts',(-222.757906792926,4.58959628416496,
132.57206789279));
#130509=CARTESIAN_POINT('Ctrl Pts',(-222.765657984166,4.63883057971725,
132.444238164934));
#130510=CARTESIAN_POINT('Ctrl Pts',(-222.773409175406,4.68275875731443,
132.314250226368));
#130511=CARTESIAN_POINT('Ctrl Pts',(-222.781160366646,4.72119491491737,
132.18258470597));
#130512=CARTESIAN_POINT('Ctrl Pts',(-222.788908263423,4.75961473612796,
132.050975146932));
#130513=CARTESIAN_POINT('Ctrl Pts',(-222.7966561602,4.79254707067012,131.917689798713));
#130514=CARTESIAN_POINT('Ctrl Pts',(-222.804404056977,4.81985533303518,
131.783226099189));
#130515=CARTESIAN_POINT('Ctrl Pts',(-222.812150333062,4.84715788310045,
131.648790526571));
#130516=CARTESIAN_POINT('Ctrl Pts',(-222.819896609146,4.86883862321824,
131.513177475821));
#130517=CARTESIAN_POINT('Ctrl Pts',(-222.82764288523,4.88481181122892,131.376895884059));
#130518=CARTESIAN_POINT('Ctrl Pts',(-222.835389218495,4.90078511715007,
131.240613286297));
#130519=CARTESIAN_POINT('Ctrl Pts',(-222.843135551761,4.91105074138065,
131.103662525983));
#130520=CARTESIAN_POINT('Ctrl Pts',(-222.850881885026,4.91557472515568,
130.966558595083));
#130521=CARTESIAN_POINT('Ctrl Pts',(-222.858629953029,4.92009972204552,
130.829423960709));
#130522=CARTESIAN_POINT('Ctrl Pts',(-222.866378021032,4.91888050699444,
130.69213647817));
#130523=CARTESIAN_POINT('Ctrl Pts',(-222.874126089035,4.91193524685531,
130.555211679779));
#130524=CARTESIAN_POINT('Ctrl Pts',(-222.881882391777,4.90498260521107,
130.418141356082));
#130525=CARTESIAN_POINT('Ctrl Pts',(-222.889638694519,4.89229178145694,
130.281434877626));
#130526=CARTESIAN_POINT('Ctrl Pts',(-222.89739499726,4.87393295513269,130.145603749388));
#130527=CARTESIAN_POINT('Ctrl Pts',(-222.905155439775,4.85556433015007,
130.009700123987));
#130528=CARTESIAN_POINT('Ctrl Pts',(-222.912915882289,4.83152174316566,
129.874673164464));
#130529=CARTESIAN_POINT('Ctrl Pts',(-222.920676324803,4.80192645946905,
129.74102372817));
#130530=CARTESIAN_POINT('Ctrl Pts',(-222.928449225068,4.77228366679571,
129.607159745936));
#130531=CARTESIAN_POINT('Ctrl Pts',(-222.936222125334,4.73707046552185,
129.474678083922));
#130532=CARTESIAN_POINT('Ctrl Pts',(-222.943995025599,4.69645817166808,
129.344064858388));
#130533=CARTESIAN_POINT('Ctrl Pts',(-222.951485361361,4.6573222369923,129.218199752598));
#130534=CARTESIAN_POINT('Ctrl Pts',(-222.958975697123,4.61317303909308,
129.094069887216));
#130535=CARTESIAN_POINT('Ctrl Pts',(-222.966466032885,4.56420523276902,
128.972090534946));
#130536=CARTESIAN_POINT('Ctrl Pts',(-222.974240367004,4.51338079718451,
128.845486298459));
#130537=CARTESIAN_POINT('Ctrl Pts',(-222.982014701123,4.4572041485496,128.720797823449));
#130538=CARTESIAN_POINT('Ctrl Pts',(-222.989789035243,4.3958400282902,128.598510779481));
#130539=CARTESIAN_POINT('Ctrl Pts',(-222.99755378819,4.33455153382442,128.476374443364));
#130540=CARTESIAN_POINT('Ctrl Pts',(-223.005318541137,4.26808846175371,
128.356633995753));
#130541=CARTESIAN_POINT('Ctrl Pts',(-223.013083294084,4.19666425737296,
128.239756910677));
#130542=CARTESIAN_POINT('Ctrl Pts',(-223.020840334969,4.12531099251929,
128.12299590957));
#130543=CARTESIAN_POINT('Ctrl Pts',(-223.028597375854,4.04900660378461,
128.009092942892));
#130544=CARTESIAN_POINT('Ctrl Pts',(-223.036354416739,3.9680110934299,127.898492240485));
#130545=CARTESIAN_POINT('Ctrl Pts',(-223.044105607979,3.88707666241971,
127.787974942929));
#130546=CARTESIAN_POINT('Ctrl Pts',(-223.051856799219,3.80145838125106,
127.680755267079));
#130547=CARTESIAN_POINT('Ctrl Pts',(-223.059607990459,3.71146013201945,
127.577249409236));
#130548=CARTESIAN_POINT('Ctrl Pts',(-223.067355887236,3.62150013444443,
127.473787544143));
#130549=CARTESIAN_POINT('Ctrl Pts',(-223.075103784013,3.52716412738826,
127.374036652013));
#130550=CARTESIAN_POINT('Ctrl Pts',(-223.08285168079,3.42879679161789,127.278380523423));
#130551=CARTESIAN_POINT('Ctrl Pts',(-223.090597956875,3.33045003217361,
127.182744404034));
#130552=CARTESIAN_POINT('Ctrl Pts',(-223.098344232959,3.2280739014318,127.091201616879));
#130553=CARTESIAN_POINT('Ctrl Pts',(-223.106090509043,3.1220502368738,127.004099392211));
#130554=CARTESIAN_POINT('Ctrl Pts',(-223.113836842308,3.01602578967334,
126.916996524574));
#130555=CARTESIAN_POINT('Ctrl Pts',(-223.121583175573,2.90635405702249,
126.834334533014));
#130556=CARTESIAN_POINT('Ctrl Pts',(-223.129329508839,2.79344996070668,
126.756420353737));
#130557=CARTESIAN_POINT('Ctrl Pts',(-223.137077576842,2.68052058030087,
126.67848872612));
#130558=CARTESIAN_POINT('Ctrl Pts',(-223.144825644845,2.56435771754198,
126.605307248527));
#130559=CARTESIAN_POINT('Ctrl Pts',(-223.152573712848,2.44540492399086,
126.537139294477));
#130560=CARTESIAN_POINT('Ctrl Pts',(-223.16033001559,2.32632570599536,126.468898890715));
#130561=CARTESIAN_POINT('Ctrl Pts',(-223.168086318332,2.2044509737119,126.405682849315));
#130562=CARTESIAN_POINT('Ctrl Pts',(-223.175842621073,2.08024900452012,
126.347708607178));
#130563=CARTESIAN_POINT('Ctrl Pts',(-223.183603063588,1.95598074499774,
126.289703422443));
#130564=CARTESIAN_POINT('Ctrl Pts',(-223.191363506102,1.82938313425054,
126.236945761955));
#130565=CARTESIAN_POINT('Ctrl Pts',(-223.199123948616,1.70094310460485,
126.189604327425));
#130566=CARTESIAN_POINT('Ctrl Pts',(-223.206896848881,1.57229689162119,
126.142186896221));
#130567=CARTESIAN_POINT('Ctrl Pts',(-223.214669749147,1.44180272187478,
126.10020318538));
#130568=CARTESIAN_POINT('Ctrl Pts',(-223.222442649412,1.30996217923589,
126.063771819593));
#130569=CARTESIAN_POINT('Ctrl Pts',(-223.229932985174,1.18291437240822,
126.028664825717));
#130570=CARTESIAN_POINT('Ctrl Pts',(-223.237423320936,1.05461668125239,
125.998713572));
#130571=CARTESIAN_POINT('Ctrl Pts',(-223.244913656698,0.925523702128874,
125.973978754887));
#130572=CARTESIAN_POINT('Ctrl Pts',(-223.252687990817,0.791536123465112,
125.948306109666));
#130573=CARTESIAN_POINT('Ctrl Pts',(-223.260462324936,0.656267327299282,
125.928171948739));
#130574=CARTESIAN_POINT('Ctrl Pts',(-223.268236659056,0.520214967957649,
125.913700186744));
#130575=CARTESIAN_POINT('Ctrl Pts',(-223.276001412003,0.384330280989925,
125.899246259901));
#130576=CARTESIAN_POINT('Ctrl Pts',(-223.28376616495,0.247664337284899,
125.89044088801));
#130577=CARTESIAN_POINT('Ctrl Pts',(-223.291530917897,0.110725808379627,
125.887357174629));
#130578=CARTESIAN_POINT('Ctrl Pts',(-223.299287958782,-0.0260767112482416,
125.884276524035));
#130579=CARTESIAN_POINT('Ctrl Pts',(-223.307044999667,-0.163150888963735,
125.886906231606));
#130580=CARTESIAN_POINT('Ctrl Pts',(-223.314802040552,-0.299982444044545,
125.895267667156));
#130581=CARTESIAN_POINT('Ctrl Pts',(-223.322553231792,-0.436710813385089,
125.903622797283));
#130582=CARTESIAN_POINT('Ctrl Pts',(-223.330304423032,-0.573196535610651,
125.917701028282));
#130583=CARTESIAN_POINT('Ctrl Pts',(-223.338055614272,-0.708925197291414,
125.937471659808));
#130584=CARTESIAN_POINT('Ctrl Pts',(-223.345803511049,-0.844596170670836,
125.957233888288));
#130585=CARTESIAN_POINT('Ctrl Pts',(-223.353551407826,-0.979510337410891,
125.982683649012));
#130586=CARTESIAN_POINT('Ctrl Pts',(-223.361299304603,-1.11315849525526,
126.013738400469));
#130587=CARTESIAN_POINT('Ctrl Pts',(-223.369045580687,-1.24677869678613,
126.044786655942));
#130588=CARTESIAN_POINT('Ctrl Pts',(-223.376791856771,-1.37913303558788,
126.081437481664));
#130589=CARTESIAN_POINT('Ctrl Pts',(-223.384538132856,-1.50972298452976,
126.12355731338));
#130590=CARTESIAN_POINT('Ctrl Pts',(-223.392284466121,-1.64031389745681,
126.165677456014));
#130591=CARTESIAN_POINT('Ctrl Pts',(-223.400030799386,-1.76914002244498,
126.213266565188));
#130592=CARTESIAN_POINT('Ctrl Pts',(-223.407777132651,-1.89571885000921,
126.26614146197));
#130593=CARTESIAN_POINT('Ctrl Pts',(-223.415525200654,-2.02232602402372,
126.319028199718));
#130594=CARTESIAN_POINT('Ctrl Pts',(-223.423273268657,-2.14668453848543,
126.377202929864));
#130595=CARTESIAN_POINT('Ctrl Pts',(-223.43102133666,-2.26833305934123,
126.440434839737));
#130596=CARTESIAN_POINT('Ctrl Pts',(-223.438777639402,-2.39011086969346,
126.503733953237));
#130597=CARTESIAN_POINT('Ctrl Pts',(-223.446533942144,-2.50917258544954,
126.572100802664));
#130598=CARTESIAN_POINT('Ctrl Pts',(-223.454290244886,-2.62508215542526,
126.645258942953));
#130599=CARTESIAN_POINT('Ctrl Pts',(-223.4620506874,-2.74105358982813,126.718456129944));
#130600=CARTESIAN_POINT('Ctrl Pts',(-223.469811129914,-2.85386920469839,
126.796449481124));
#130601=CARTESIAN_POINT('Ctrl Pts',(-223.477571572429,-2.96312386769293,
126.878920513933));
#130602=CARTESIAN_POINT('Ctrl Pts',(-223.485344472694,-3.07255391597198,
126.961523936566));
#130603=CARTESIAN_POINT('Ctrl Pts',(-223.493117372959,-3.17841128718878,
127.048619156141));
#130604=CARTESIAN_POINT('Ctrl Pts',(-223.500890273225,-3.28032506069638,
127.139848295487));
#130605=CARTESIAN_POINT('Ctrl Pts',(-223.508380608987,-3.3785340118339,
127.227761025828));
#130606=CARTESIAN_POINT('Ctrl Pts',(-223.515870944749,-3.47308088576673,
127.319512122745));
#130607=CARTESIAN_POINT('Ctrl Pts',(-223.523361280511,-3.56366889641953,
127.414751929356));
#130608=CARTESIAN_POINT('Ctrl Pts',(-223.531038703737,-3.65651954011178,
127.51237055775));
#130609=CARTESIAN_POINT('Ctrl Pts',(-223.538716126964,-3.74552124665173,
127.61398101524));
#130610=CARTESIAN_POINT('Ctrl Pts',(-223.54639355019,-3.83030464099324,
127.719243209802));
#130611=CARTESIAN_POINT('Ctrl Pts',(-223.554061902916,-3.91498786790322,
127.824381042234));
#130612=CARTESIAN_POINT('Ctrl Pts',(-223.561730255642,-3.99546244221144,
127.933161724535));
#130613=CARTESIAN_POINT('Ctrl Pts',(-223.569398608368,-4.07139527848321,
128.045207930808));
#130614=CARTESIAN_POINT('Ctrl Pts',(-223.577375083318,-4.15037917345655,
128.161756267772));
#130615=CARTESIAN_POINT('Ctrl Pts',(-223.585351558267,-4.22444840748029,
128.281837740302));
#130616=CARTESIAN_POINT('Ctrl Pts',(-223.593328033216,-4.29327333591575,
128.404988381831));
#130617=CARTESIAN_POINT('Ctrl Pts',(-223.600982877338,-4.35932307621505,
128.523173290637));
#130618=CARTESIAN_POINT('Ctrl Pts',(-223.608637721461,-4.42054296849811,
128.644184290527));
#130619=CARTESIAN_POINT('Ctrl Pts',(-223.616292565583,-4.47668554955064,
128.767581406914));
#130620=CARTESIAN_POINT('Ctrl Pts',(-223.623944060619,-4.53280356755143,
128.890924535585));
#130621=CARTESIAN_POINT('Ctrl Pts',(-223.631595555656,-4.5838485280795,
129.016651338951));
#130622=CARTESIAN_POINT('Ctrl Pts',(-223.639247050692,-4.6296194500434,
129.144298326482));
#130623=CARTESIAN_POINT('Ctrl Pts',(-223.646897290597,-4.67538286386451,
129.271924375133));
#130624=CARTESIAN_POINT('Ctrl Pts',(-223.654547530502,-4.71587382474148,
129.401469603691));
#130625=CARTESIAN_POINT('Ctrl Pts',(-223.662197770407,-4.75094010211205,
129.532452126894));
#130626=CARTESIAN_POINT('Ctrl Pts',(-223.663170616191,-4.75539931914727,
129.549108571278));
#130627=CARTESIAN_POINT('Ctrl Pts',(-223.664143461975,-4.7597708795161,
129.56578823797));
#130628=CARTESIAN_POINT('Ctrl Pts',(-223.665116307759,-4.76405452823394,
129.582490119308));
#130629=CARTESIAN_POINT('Ctrl Pts',(-221.915425355964,-4.76405452823393,
129.582490119308));
#130630=CARTESIAN_POINT('Ctrl Pts',(-221.923650676202,-4.80011930232353,
129.723106126124));
#130631=CARTESIAN_POINT('Ctrl Pts',(-221.93187599644,-4.82999394762387,
129.865474671377));
#130632=CARTESIAN_POINT('Ctrl Pts',(-221.940101316678,-4.85351962780969,
130.00904289177));
#130633=CARTESIAN_POINT('Ctrl Pts',(-221.948307262482,-4.87698989413297,
130.152272942572));
#130634=CARTESIAN_POINT('Ctrl Pts',(-221.956513208285,-4.89414096725091,
130.296696723046));
#130635=CARTESIAN_POINT('Ctrl Pts',(-221.964719154088,-4.90486456665709,
130.441749744519));
#130636=CARTESIAN_POINT('Ctrl Pts',(-221.971526290719,-4.91376019040219,
130.562076609897));
#130637=CARTESIAN_POINT('Ctrl Pts',(-221.97833342735,-4.91823372520509,
130.682836114026));
#130638=CARTESIAN_POINT('Ctrl Pts',(-221.985140563982,-4.91824995565472,
130.803700161377));
#130639=CARTESIAN_POINT('',(-221.63985943605,-4.91824834470546,130.800325484114));
#130640=CARTESIAN_POINT('Ctrl Pts',(-221.569819034442,-4.76405452823418,
129.582490119309));
#130641=CARTESIAN_POINT('Ctrl Pts',(-221.577818326288,-4.79903172095484,
129.718865662874));
#130642=CARTESIAN_POINT('Ctrl Pts',(-221.585817618134,-4.82810131954953,
129.856560455278));
#130643=CARTESIAN_POINT('Ctrl Pts',(-221.59381690998,-4.85120084894627,
129.995019289273));
#130644=CARTESIAN_POINT('Ctrl Pts',(-221.60623517544,-4.88706103426808,
130.209965635635));
#130645=CARTESIAN_POINT('Ctrl Pts',(-221.6186534409,-4.90864232357969,130.427356960295));
#130646=CARTESIAN_POINT('Ctrl Pts',(-221.631071706359,-4.91568978847973,
130.64568810597));
#130647=CARTESIAN_POINT('Ctrl Pts',(-221.634000949572,-4.9173521574143,
130.697188456688));
#130648=CARTESIAN_POINT('Ctrl Pts',(-221.636930192784,-4.91820602261817,
130.748740948094));
#130649=CARTESIAN_POINT('Ctrl Pts',(-221.639859435996,-4.91824834470469,
130.800325483166));
#130650=CARTESIAN_POINT('Ctrl Pts',(-221.63985943605,-4.91824834470546,
130.800325484114));
#130651=CARTESIAN_POINT('Ctrl Pts',(-221.647507087154,-4.9183588389363,
130.935002087601));
#130652=CARTESIAN_POINT('Ctrl Pts',(-221.655154738257,-4.9129333950563,
131.069879161911));
#130653=CARTESIAN_POINT('Ctrl Pts',(-221.662802389361,-4.90194927947247,
131.204456011165));
#130654=CARTESIAN_POINT('Ctrl Pts',(-221.670442764659,-4.89097561393384,
131.338904826975));
#130655=CARTESIAN_POINT('Ctrl Pts',(-221.678083139956,-4.87445382754039,
131.473053586129));
#130656=CARTESIAN_POINT('Ctrl Pts',(-221.685723515254,-4.85241323137012,
131.606401074478));
#130657=CARTESIAN_POINT('Ctrl Pts',(-221.693496057693,-4.8299913656306,
131.742055276269));
#130658=CARTESIAN_POINT('Ctrl Pts',(-221.701268600132,-4.80185797109265,
131.876879804697));
#130659=CARTESIAN_POINT('Ctrl Pts',(-221.709041142571,-4.76809913468922,
132.010351373864));
#130660=CARTESIAN_POINT('Ctrl Pts',(-221.716673644061,-4.7349485444982,
132.141418133355));
#130661=CARTESIAN_POINT('Ctrl Pts',(-221.724306145551,-4.69637363020573,
132.271179871615));
#130662=CARTESIAN_POINT('Ctrl Pts',(-221.73193864704,-4.65250745695608,
132.399151332822));
#130663=CARTESIAN_POINT('Ctrl Pts',(-221.73957022108,-4.60864661403101,
132.527107243792));
#130664=CARTESIAN_POINT('Ctrl Pts',(-221.747201795119,-4.55949592136922,
132.653272928435));
#130665=CARTESIAN_POINT('Ctrl Pts',(-221.754833369158,-4.50523798177773,
132.777179359886));
#130666=CARTESIAN_POINT('Ctrl Pts',(-221.762465782816,-4.45097407278124,
132.9010994234));
#130667=CARTESIAN_POINT('Ctrl Pts',(-221.770098196473,-4.39160196193224,
133.022759369872));
#130668=CARTESIAN_POINT('Ctrl Pts',(-221.77773061013,-4.32735172049636,
133.141711714346));
#130669=CARTESIAN_POINT('Ctrl Pts',(-221.785608437102,-4.26103557102442,
133.264488863191));
#130670=CARTESIAN_POINT('Ctrl Pts',(-221.793486264074,-4.1895225256721,
133.384380951238));
#130671=CARTESIAN_POINT('Ctrl Pts',(-221.801364091046,-4.11311528286112,
133.500926161437));
#130672=CARTESIAN_POINT('Ctrl Pts',(-221.809007544998,-4.03898122989655,
133.614004038191));
#130673=CARTESIAN_POINT('Ctrl Pts',(-221.816650998949,-3.96024034488612,
133.723931060195));
#130674=CARTESIAN_POINT('Ctrl Pts',(-221.824294452901,-3.87721088908293,
133.830318116289));
#130675=CARTESIAN_POINT('Ctrl Pts',(-221.832289466383,-3.79036250577627,
133.941598429247));
#130676=CARTESIAN_POINT('Ctrl Pts',(-221.840284479865,-3.6988220030243,
134.049005008741));
#130677=CARTESIAN_POINT('Ctrl Pts',(-221.848279493347,-3.60299682209848,
134.152135544655));
#130678=CARTESIAN_POINT('Ctrl Pts',(-221.856274506829,-3.50717164117241,
134.25526608057));
#130679=CARTESIAN_POINT('Ctrl Pts',(-221.864269520312,-3.40706219025543,
134.354120279752));
#130680=CARTESIAN_POINT('Ctrl Pts',(-221.872264533794,-3.30311433724849,
134.448344527734));
#130681=CARTESIAN_POINT('Ctrl Pts',(-221.880038867913,-3.20203566589346,
134.539967986227));
#130682=CARTESIAN_POINT('Ctrl Pts',(-221.887813202032,-3.09698175721047,
134.627527725395));
#130683=CARTESIAN_POINT('Ctrl Pts',(-221.895587536151,-2.98831317861025,
134.710659045623));
#130684=CARTESIAN_POINT('Ctrl Pts',(-221.903352289099,-2.87977852432117,
134.79368791393));
#130685=CARTESIAN_POINT('Ctrl Pts',(-221.911117042046,-2.76763837129617,
134.872298987086));
#130686=CARTESIAN_POINT('Ctrl Pts',(-221.918881794993,-2.65228912713886,
134.946165230118));
#130687=CARTESIAN_POINT('Ctrl Pts',(-221.926638835878,-2.53705444947731,
135.019958108156));
#130688=CARTESIAN_POINT('Ctrl Pts',(-221.934395876763,-2.41861735069616,
135.089015324947));
#130689=CARTESIAN_POINT('Ctrl Pts',(-221.942152917648,-2.297405939782,135.153051111307));
#130690=CARTESIAN_POINT('Ctrl Pts',(-221.949904108888,-2.17628593533553,
135.217038607783));
#130691=CARTESIAN_POINT('Ctrl Pts',(-221.957655300128,-2.05239612730527,
135.276012029136));
#130692=CARTESIAN_POINT('Ctrl Pts',(-221.965406491369,-1.92619182383379,
135.329730008046));
#130693=CARTESIAN_POINT('Ctrl Pts',(-221.973154388146,-1.80004116055772,
135.383425155383));
#130694=CARTESIAN_POINT('Ctrl Pts',(-221.980902284923,-1.67157831737001,
135.431869150144));
#130695=CARTESIAN_POINT('Ctrl Pts',(-221.9886501817,-1.54128111846809,135.474867611068));
#130696=CARTESIAN_POINT('Ctrl Pts',(-221.996396457784,-1.4110111749313,
135.517857077642));
#130697=CARTESIAN_POINT('Ctrl Pts',(-222.004142733868,-1.2789080099321,
135.555403153644));
#130698=CARTESIAN_POINT('Ctrl Pts',(-222.011889009952,-1.14546687147195,
135.587360587131));
#130699=CARTESIAN_POINT('Ctrl Pts',(-222.019635343218,-1.01202474797981,
135.619318256521));
#130700=CARTESIAN_POINT('Ctrl Pts',(-222.027381676483,-0.877245011532458,
135.64568711002));
#130701=CARTESIAN_POINT('Ctrl Pts',(-222.035128009748,-0.741635038670149,
135.6663726015));
#130702=CARTESIAN_POINT('Ctrl Pts',(-222.042876077751,-0.605994696894486,
135.687062725352));
#130703=CARTESIAN_POINT('Ctrl Pts',(-222.050624145754,-0.469524135153988,
135.702066895617));
#130704=CARTESIAN_POINT('Ctrl Pts',(-222.058372213758,-0.332737423040753,
135.71134226312));
#130705=CARTESIAN_POINT('Ctrl Pts',(-222.066128516499,-0.195805332382288,
135.720627488595));
#130706=CARTESIAN_POINT('Ctrl Pts',(-222.073884819241,-0.0585568108295851,
135.724171722101));
#130707=CARTESIAN_POINT('Ctrl Pts',(-222.081641121983,0.0784919280162668,
135.721984238761));
#130708=CARTESIAN_POINT('Ctrl Pts',(-222.089401564497,0.215613813900871,
135.719795587895));
#130709=CARTESIAN_POINT('Ctrl Pts',(-222.097162007012,0.352535314488479,
135.711869147072));
#130710=CARTESIAN_POINT('Ctrl Pts',(-222.104922449526,0.48874475560372,
135.698266177175));
#130711=CARTESIAN_POINT('Ctrl Pts',(-222.112695349791,0.625172852205945,
135.684641370582));
#130712=CARTESIAN_POINT('Ctrl Pts',(-222.120468250057,0.760886217849805,
135.665321880432));
#130713=CARTESIAN_POINT('Ctrl Pts',(-222.128241150322,0.895381904845901,
135.640420409067));
#130714=CARTESIAN_POINT('Ctrl Pts',(-222.135731486084,1.02498833483822,
135.616424168911));
#130715=CARTESIAN_POINT('Ctrl Pts',(-222.143221821846,1.15346378015151,
135.58724480797));
#130716=CARTESIAN_POINT('Ctrl Pts',(-222.150712157607,1.28037288428042,
135.553026571252));
#130717=CARTESIAN_POINT('Ctrl Pts',(-222.158486491726,1.41209378567244,
135.517510939688));
#130718=CARTESIAN_POINT('Ctrl Pts',(-222.166260825845,1.54254447778172,
135.476454288817));
#130719=CARTESIAN_POINT('Ctrl Pts',(-222.174035159964,1.67122323300192,
135.429962845166));
#130720=CARTESIAN_POINT('Ctrl Pts',(-222.181799912911,1.79974340315665,
135.383528698064));
#130721=CARTESIAN_POINT('Ctrl Pts',(-222.189564665859,1.92649561726965,
135.331673216573));
#130722=CARTESIAN_POINT('Ctrl Pts',(-222.197329418806,2.05099046356164,
135.274553139245));
#130723=CARTESIAN_POINT('Ctrl Pts',(-222.205086459691,2.17536165981756,
135.217489794384));
#130724=CARTESIAN_POINT('Ctrl Pts',(-222.212843500576,2.29747959698378,
135.155172421358));
#130725=CARTESIAN_POINT('Ctrl Pts',(-222.220600541461,2.41687244598882,
135.087806735159));
#130726=CARTESIAN_POINT('Ctrl Pts',(-222.228351732701,2.53617525991816,
135.020491849947));
#130727=CARTESIAN_POINT('Ctrl Pts',(-222.236102923941,2.65275673693429,
134.948136420457));
#130728=CARTESIAN_POINT('Ctrl Pts',(-222.243854115181,2.76616770270203,
134.87099304539));
#130729=CARTESIAN_POINT('Ctrl Pts',(-222.251602011958,2.87953046578353,
134.793882458315));
#130730=CARTESIAN_POINT('Ctrl Pts',(-222.259349908735,2.98972507520356,
134.711988192564));
#130731=CARTESIAN_POINT('Ctrl Pts',(-222.267097805512,3.0963297168512,134.625607187345));
#130732=CARTESIAN_POINT('Ctrl Pts',(-222.274844081597,3.20291205910594,
134.539244251169));
#130733=CARTESIAN_POINT('Ctrl Pts',(-222.282590357681,3.30590562368785,
134.448396688293));
#130734=CARTESIAN_POINT('Ctrl Pts',(-222.290336633765,3.40492051238091,
134.353402652661));
#130735=CARTESIAN_POINT('Ctrl Pts',(-222.29808296703,3.50393613197952,134.258407915804));
#130736=CARTESIAN_POINT('Ctrl Pts',(-222.305829300296,3.59897273496108,
134.159266915781));
#130737=CARTESIAN_POINT('Ctrl Pts',(-222.313575633561,3.6896765275764,134.056355418354));
#130738=CARTESIAN_POINT('Ctrl Pts',(-222.321323701564,3.78040063267682,
133.953420874611));
#130739=CARTESIAN_POINT('Ctrl Pts',(-222.329071769567,3.86678973816017,
133.846714446497));
#130740=CARTESIAN_POINT('Ctrl Pts',(-222.33681983757,3.94852992663087,133.736645474295));
#130741=CARTESIAN_POINT('Ctrl Pts',(-222.344576140312,4.03035698954692,
133.626459519478));
#130742=CARTESIAN_POINT('Ctrl Pts',(-222.352332443053,4.10752503195465,
133.512904195999));
#130743=CARTESIAN_POINT('Ctrl Pts',(-222.360088745795,4.17976283121569,
133.396418822408));
#130744=CARTESIAN_POINT('Ctrl Pts',(-222.36784918831,4.25203918596504,133.279871277066));
#130745=CARTESIAN_POINT('Ctrl Pts',(-222.375609630824,4.31937986237311,
133.160390905925));
#130746=CARTESIAN_POINT('Ctrl Pts',(-222.383370073338,4.38155982856529,
133.038441307963));
#130747=CARTESIAN_POINT('Ctrl Pts',(-222.391142973604,4.44383961155944,
132.916295945679));
#130748=CARTESIAN_POINT('Ctrl Pts',(-222.398915873869,4.50094196645316,
132.79167379123));
#130749=CARTESIAN_POINT('Ctrl Pts',(-222.406688774134,4.55268985740884,
132.665058907119));
#130750=CARTESIAN_POINT('Ctrl Pts',(-222.414179109896,4.60255658218026,
132.543046792977));
#130751=CARTESIAN_POINT('Ctrl Pts',(-222.421669445658,4.64745127579681,
132.419184604888));
#130752=CARTESIAN_POINT('Ctrl Pts',(-222.429159781419,4.68725997484442,
132.293916588559));
#130753=CARTESIAN_POINT('Ctrl Pts',(-222.436934115538,4.72857803281806,
132.163898997311));
#130754=CARTESIAN_POINT('Ctrl Pts',(-222.444708449657,4.76454769517606,
132.031955012825));
#130755=CARTESIAN_POINT('Ctrl Pts',(-222.452482783776,4.79498713727588,
131.898564170777));
#130756=CARTESIAN_POINT('Ctrl Pts',(-222.460247536723,4.82538906548385,
131.76533772102));
#130757=CARTESIAN_POINT('Ctrl Pts',(-222.46801228967,4.85027424810539,131.630668339092));
#130758=CARTESIAN_POINT('Ctrl Pts',(-222.475777042618,4.86951001470163,
131.495052501998));
#130759=CARTESIAN_POINT('Ctrl Pts',(-222.483534083502,4.88872667606326,
131.359571360467));
#130760=CARTESIAN_POINT('Ctrl Pts',(-222.491291124388,4.90230503315158,
131.223146019063));
#130761=CARTESIAN_POINT('Ctrl Pts',(-222.499048165273,4.91016312467678,
131.086284634926));
#130762=CARTESIAN_POINT('Ctrl Pts',(-222.506799356513,4.91801529035404,
130.949526459023));
#130763=CARTESIAN_POINT('Ctrl Pts',(-222.514550547753,4.9201557542997,130.812333283633));
#130764=CARTESIAN_POINT('Ctrl Pts',(-222.522301738993,4.91655424525667,
130.675219547613));
#130765=CARTESIAN_POINT('Ctrl Pts',(-222.53004963577,4.91295426695105,130.538164088589));
#130766=CARTESIAN_POINT('Ctrl Pts',(-222.537797532547,4.90361717985295,
130.401188391794));
#130767=CARTESIAN_POINT('Ctrl Pts',(-222.545545429324,4.88856480649907,
130.264807844282));
#130768=CARTESIAN_POINT('Ctrl Pts',(-222.553291705408,4.87351558177722,
130.12845582464));
#130769=CARTESIAN_POINT('Ctrl Pts',(-222.561037981492,4.85275349160718,
129.992699095019));
#130770=CARTESIAN_POINT('Ctrl Pts',(-222.568784257576,4.82635228497129,
129.858048468298));
#130771=CARTESIAN_POINT('Ctrl Pts',(-222.576530590842,4.79995088344766,
129.723396847616));
#130772=CARTESIAN_POINT('Ctrl Pts',(-222.584276924107,4.76791035762011,
129.589851729786));
#130773=CARTESIAN_POINT('Ctrl Pts',(-222.592023257372,4.7303556157022,129.457913882082));
#130774=CARTESIAN_POINT('Ctrl Pts',(-222.599771325375,4.69279246366037,
129.325946487813));
#130775=CARTESIAN_POINT('Ctrl Pts',(-222.607519393378,4.64971274529124,
129.195587455859));
#130776=CARTESIAN_POINT('Ctrl Pts',(-222.615267461381,4.60129117014654,
129.067322152237));
#130777=CARTESIAN_POINT('Ctrl Pts',(-222.623023764123,4.55281813197549,
128.938920526724));
#130778=CARTESIAN_POINT('Ctrl Pts',(-222.630780066865,4.498992034135,128.812617441051));
#130779=CARTESIAN_POINT('Ctrl Pts',(-222.638536369607,4.4400358853041,128.688878544914));
#130780=CARTESIAN_POINT('Ctrl Pts',(-222.646296812121,4.38104826980127,
128.565073605602));
#130781=CARTESIAN_POINT('Ctrl Pts',(-222.654057254635,4.31692533018726,
128.443835928281));
#130782=CARTESIAN_POINT('Ctrl Pts',(-222.661817697149,4.24793547018755,
128.325605425212));
#130783=CARTESIAN_POINT('Ctrl Pts',(-222.669590597415,4.17883486153994,
128.207185128044));
#130784=CARTESIAN_POINT('Ctrl Pts',(-222.67736349768,4.10485193114276,128.091781981104));
#130785=CARTESIAN_POINT('Ctrl Pts',(-222.685136397945,4.02629824229625,
127.979806577265));
#130786=CARTESIAN_POINT('Ctrl Pts',(-222.692626733708,3.95060017790136,
127.8719017614));
#130787=CARTESIAN_POINT('Ctrl Pts',(-222.70011706947,3.87065808960908,127.767180046003));
#130788=CARTESIAN_POINT('Ctrl Pts',(-222.707607405232,3.78678413390681,
127.665977437377));
#130789=CARTESIAN_POINT('Ctrl Pts',(-222.715381739351,3.69973007168445,
127.56093770109));
#130790=CARTESIAN_POINT('Ctrl Pts',(-222.723156073471,3.60816434180061,
127.459356458908));
#130791=CARTESIAN_POINT('Ctrl Pts',(-222.73093040759,3.51239211054046,127.361645885801));
#130792=CARTESIAN_POINT('Ctrl Pts',(-222.738695160537,3.41673790999567,
127.264055732242));
#130793=CARTESIAN_POINT('Ctrl Pts',(-222.746459913484,3.31688779400566,
127.170327032902));
#130794=CARTESIAN_POINT('Ctrl Pts',(-222.754224666431,3.21318775112395,
127.08083976513));
#130795=CARTESIAN_POINT('Ctrl Pts',(-222.761981707316,3.10959070458702,
126.991441377373));
#130796=CARTESIAN_POINT('Ctrl Pts',(-222.769738748201,3.00215163477383,
126.906276291593));
#130797=CARTESIAN_POINT('Ctrl Pts',(-222.777495789086,2.8912537665975,126.825688135489));
#130798=CARTESIAN_POINT('Ctrl Pts',(-222.785246980326,2.78043952736638,
126.745160751541));
#130799=CARTESIAN_POINT('Ctrl Pts',(-222.792998171566,2.66617199644442,
126.669203656174));
#130800=CARTESIAN_POINT('Ctrl Pts',(-222.800749362806,2.54886762345901,
126.598120384224));
#130801=CARTESIAN_POINT('Ctrl Pts',(-222.808497259583,2.43161310796084,
126.527067324561));
#130802=CARTESIAN_POINT('Ctrl Pts',(-222.81624515636,2.31132465124602,126.460884170441));
#130803=CARTESIAN_POINT('Ctrl Pts',(-222.823993053137,2.18844765865376,
126.399831141239));
#130804=CARTESIAN_POINT('Ctrl Pts',(-222.831739329221,2.06559636927942,
126.338790883014));
#130805=CARTESIAN_POINT('Ctrl Pts',(-222.839485605305,1.94015797093936,
126.282878789084));
#130806=CARTESIAN_POINT('Ctrl Pts',(-222.84723188139,1.81260208810232,126.232308919181));
#130807=CARTESIAN_POINT('Ctrl Pts',(-222.854978214655,1.68504526367691,
126.181738675982));
#130808=CARTESIAN_POINT('Ctrl Pts',(-222.86272454792,1.55537128700937,126.136510879588));
#130809=CARTESIAN_POINT('Ctrl Pts',(-222.870470881186,1.42406898372989,
126.096791118124));
#130810=CARTESIAN_POINT('Ctrl Pts',(-222.878218949189,1.29273727621052,
126.057062461695));
#130811=CARTESIAN_POINT('Ctrl Pts',(-222.885967017192,1.15977689060906,
126.022844407872));
#130812=CARTESIAN_POINT('Ctrl Pts',(-222.893715085194,1.02569061388157,
125.99425232075));
#130813=CARTESIAN_POINT('Ctrl Pts',(-222.901471387936,0.891461828662974,
125.965629845618));
#130814=CARTESIAN_POINT('Ctrl Pts',(-222.909227690678,0.756105144938412,
125.942645363234));
#130815=CARTESIAN_POINT('Ctrl Pts',(-222.91698399342,0.620132868622877,
125.925362945118));
#130816=CARTESIAN_POINT('Ctrl Pts',(-222.924744435934,0.484088019809057,
125.908071302854));
#130817=CARTESIAN_POINT('Ctrl Pts',(-222.932504878448,0.347427313097739,
125.896487822021));
#130818=CARTESIAN_POINT('Ctrl Pts',(-222.940265320962,0.210665937903024,
125.890624470284));
#130819=CARTESIAN_POINT('Ctrl Pts',(-222.948038221228,0.0736850212077413,
125.884751706174));
#130820=CARTESIAN_POINT('Ctrl Pts',(-222.955811121493,-0.0633964957131659,
125.884617421023));
#130821=CARTESIAN_POINT('Ctrl Pts',(-222.963584021759,-0.200064761873793,
125.89018142328));
#130822=CARTESIAN_POINT('Ctrl Pts',(-222.971074357521,-0.331764792315863,
125.895543160039));
#130823=CARTESIAN_POINT('Ctrl Pts',(-222.978564693283,-0.463080788767365,
125.906196057855));
#130824=CARTESIAN_POINT('Ctrl Pts',(-222.986055029045,-0.593561331401663,
125.922059110247));
#130825=CARTESIAN_POINT('Ctrl Pts',(-222.993829363164,-0.728989083464304,
125.938523615093));
#130826=CARTESIAN_POINT('Ctrl Pts',(-223.001603697283,-0.86394577306058,
125.960653314261));
#130827=CARTESIAN_POINT('Ctrl Pts',(-223.009378031402,-0.997919675885488,
125.988414253353));
#130828=CARTESIAN_POINT('Ctrl Pts',(-223.017142784349,-1.13172846784912,
126.016140979568));
#130829=CARTESIAN_POINT('Ctrl Pts',(-223.024907537296,-1.26455650380447,
126.049485058608));
#130830=CARTESIAN_POINT('Ctrl Pts',(-223.032672290243,-1.39589708278385,
126.088360787543));
#130831=CARTESIAN_POINT('Ctrl Pts',(-223.040429331128,-1.52710721244824,
126.127197904556));
#130832=CARTESIAN_POINT('Ctrl Pts',(-223.048186372013,-1.65683245269427,
126.171555627685));
#130833=CARTESIAN_POINT('Ctrl Pts',(-223.055943412898,-1.78457655737942,
126.221297278122));
#130834=CARTESIAN_POINT('Ctrl Pts',(-223.063694604138,-1.91222432924239,
126.271001417995));
#130835=CARTESIAN_POINT('Ctrl Pts',(-223.071445795379,-2.03789357639425,
126.326081262583));
#130836=CARTESIAN_POINT('Ctrl Pts',(-223.079196986619,-2.16110382518599,
126.386350509014));
#130837=CARTESIAN_POINT('Ctrl Pts',(-223.086944883396,-2.28426170633475,
126.446594139407));
#130838=CARTESIAN_POINT('Ctrl Pts',(-223.094692780173,-2.40496231736249,
126.512022613372));
#130839=CARTESIAN_POINT('Ctrl Pts',(-223.10244067695,-2.52274597587496,
126.582401853709));
#130840=CARTESIAN_POINT('Ctrl Pts',(-223.110186953034,-2.64050499658552,
126.652766372227));
#130841=CARTESIAN_POINT('Ctrl Pts',(-223.117933229118,-2.75534794302714,
126.728079396852));
#130842=CARTESIAN_POINT('Ctrl Pts',(-223.125679505202,-2.866840877189,126.808061523732));
#130843=CARTESIAN_POINT('Ctrl Pts',(-223.133425838467,-2.97833463436652,
126.888044241022));
#130844=CARTESIAN_POINT('Ctrl Pts',(-223.141172171733,-3.08647801224248,
126.972695901448));
#130845=CARTESIAN_POINT('Ctrl Pts',(-223.148918504998,-3.19086747464377,
127.061694746591));
#130846=CARTESIAN_POINT('Ctrl Pts',(-223.156666573001,-3.29528031434096,
127.150713522408));
#130847=CARTESIAN_POINT('Ctrl Pts',(-223.164414641004,-3.39593726828292,
127.244081166534));
#130848=CARTESIAN_POINT('Ctrl Pts',(-223.172162709007,-3.4924695087594,
127.341437027175));
#130849=CARTESIAN_POINT('Ctrl Pts',(-223.179919011748,-3.58910434484994,
127.438896358783));
#130850=CARTESIAN_POINT('Ctrl Pts',(-223.18767531449,-3.68160543465689,
127.540352096145));
#130851=CARTESIAN_POINT('Ctrl Pts',(-223.195431617232,-3.76964195913766,
127.645407854005));
#130852=CARTESIAN_POINT('Ctrl Pts',(-223.203192059746,-3.85772547136227,
127.750519683286));
#130853=CARTESIAN_POINT('Ctrl Pts',(-223.21095250226,-3.94133943194928,
127.859235051941));
#130854=CARTESIAN_POINT('Ctrl Pts',(-223.218712944774,-4.0201952996991,
127.97112698534));
#130855=CARTESIAN_POINT('Ctrl Pts',(-223.22648584504,-4.09917775388832,
128.083198537604));
#130856=CARTESIAN_POINT('Ctrl Pts',(-223.234258745305,-4.17338664008651,
128.198456515734));
#130857=CARTESIAN_POINT('Ctrl Pts',(-223.242031645571,-4.24257802357517,
128.316446877828));
#130858=CARTESIAN_POINT('Ctrl Pts',(-223.249521981333,-4.30925412599592,
128.430147993068));
#130859=CARTESIAN_POINT('Ctrl Pts',(-223.257012317096,-4.37127104501416,
128.546386011429));
#130860=CARTESIAN_POINT('Ctrl Pts',(-223.264502652858,-4.42845293023154,
128.664737354647));
#130861=CARTESIAN_POINT('Ctrl Pts',(-223.27288648263,-4.4924558276875,128.797206384917));
#130862=CARTESIAN_POINT('Ctrl Pts',(-223.281270312402,-4.5505805484293,
128.932693044058));
#130863=CARTESIAN_POINT('Ctrl Pts',(-223.289654142175,-4.60255473983701,
129.070672949817));
#130864=CARTESIAN_POINT('Ctrl Pts',(-223.298016770948,-4.65439749909419,
129.208303932482));
#130865=CARTESIAN_POINT('Ctrl Pts',(-223.306379399721,-4.70012064041638,
129.348415314029));
#130866=CARTESIAN_POINT('Ctrl Pts',(-223.314742028494,-4.73949906895975,
129.49046121585));
#130867=CARTESIAN_POINT('Ctrl Pts',(-223.316542859158,-4.7479789242218,
129.521049757155));
#130868=CARTESIAN_POINT('Ctrl Pts',(-223.318343689822,-4.75616473135832,
129.551727921034));
#130869=CARTESIAN_POINT('Ctrl Pts',(-223.320144520485,-4.76405452823402,
129.582490119308));
#130870=CARTESIAN_POINT('Origin',(213.235140564004,0.,130.804360617566));
#130871=CARTESIAN_POINT('',(-225.41504623153,-4.76405452823393,129.582490119308));
#130872=CARTESIAN_POINT('',(-225.069870156977,-4.76405452823402,129.582490119308));
#130873=CARTESIAN_POINT('',(213.235140564004,-4.76405452823405,129.582490119308));
#130874=CARTESIAN_POINT('',(-223.735140564051,-4.91824789595331,130.808909952771));
#130875=CARTESIAN_POINT('Ctrl Pts',(-223.735140564051,-4.91824789595331,
130.808909952771));
#130876=CARTESIAN_POINT('Ctrl Pts',(-223.745263896723,-4.91808255474622,
130.987658936367));
#130877=CARTESIAN_POINT('Ctrl Pts',(-223.755387229394,-4.90816914338085,
131.165973392137));
#130878=CARTESIAN_POINT('Ctrl Pts',(-223.765510562065,-4.88866975464819,
131.342961668891));
#130879=CARTESIAN_POINT('Ctrl Pts',(-223.775895587255,-4.86866629829984,
131.524525168995));
#130880=CARTESIAN_POINT('Ctrl Pts',(-223.786280612445,-4.83857481507823,
131.704693402866));
#130881=CARTESIAN_POINT('Ctrl Pts',(-223.796665637636,-4.79861797404513,
131.882529714541));
#130882=CARTESIAN_POINT('Ctrl Pts',(-223.798380059865,-4.7920216591378,
131.911887999216));
#130883=CARTESIAN_POINT('Ctrl Pts',(-223.800094482094,-4.78515658405584,
131.941182779772));
#130884=CARTESIAN_POINT('Ctrl Pts',(-223.801808904323,-4.7780238740645,
131.9704098967));
#130885=CARTESIAN_POINT('Ctrl Pts',(-223.809583238442,-4.7456794085625,
132.102945142961));
#130886=CARTESIAN_POINT('Ctrl Pts',(-223.817357572562,-4.70776503791059,
132.234343514913));
#130887=CARTESIAN_POINT('Ctrl Pts',(-223.825131906681,-4.6643749179642,
132.364100880291));
#130888=CARTESIAN_POINT('Ctrl Pts',(-223.832896659628,-4.62103827246275,
132.493698331313));
#130889=CARTESIAN_POINT('Ctrl Pts',(-223.840661412576,-4.57223942771272,
132.621658432498));
#130890=CARTESIAN_POINT('Ctrl Pts',(-223.848426165523,-4.51812333259547,
132.747488151712));
#130891=CARTESIAN_POINT('Ctrl Pts',(-223.856183206408,-4.46406098634694,
132.873192895074));
#130892=CARTESIAN_POINT('Ctrl Pts',(-223.863940247293,-4.40469205295891,
132.996771110419));
#130893=CARTESIAN_POINT('Ctrl Pts',(-223.871697288178,-4.34021086558519,
133.117746167957));
#130894=CARTESIAN_POINT('Ctrl Pts',(-223.879448479419,-4.27577830397654,
133.238629997262));
#130895=CARTESIAN_POINT('Ctrl Pts',(-223.887199670659,-4.20624134505839,
133.356914232497));
#130896=CARTESIAN_POINT('Ctrl Pts',(-223.894950861899,-4.13184173584594,
133.472143767003));
#130897=CARTESIAN_POINT('Ctrl Pts',(-223.902698758677,-4.05747374845178,
133.587324325885));
#130898=CARTESIAN_POINT('Ctrl Pts',(-223.910446655454,-3.97824743300902,
133.699452438552));
#130899=CARTESIAN_POINT('Ctrl Pts',(-223.918194552231,-3.89444952084087,
133.808099286645));
#130900=CARTESIAN_POINT('Ctrl Pts',(-223.925940828316,-3.81066913738947,
133.91672340816));
#130901=CARTESIAN_POINT('Ctrl Pts',(-223.9336871044,-3.72231929792916,134.021867404156));
#130902=CARTESIAN_POINT('Ctrl Pts',(-223.941433380485,-3.62972870254399,
134.123133373937));
#130903=CARTESIAN_POINT('Ctrl Pts',(-223.94917971375,-3.53713742367594,
134.22440009124));
#130904=CARTESIAN_POINT('Ctrl Pts',(-223.956926047016,-3.44030559023594,
134.321788436668));
#130905=CARTESIAN_POINT('Ctrl Pts',(-223.964672380282,-3.3396003696992,
134.414935701013));
#130906=CARTESIAN_POINT('Ctrl Pts',(-223.972420448285,-3.2388725969267,
134.508103825041));
#130907=CARTESIAN_POINT('Ctrl Pts',(-223.980168516288,-3.13426999795533,
134.59702871265));
#130908=CARTESIAN_POINT('Ctrl Pts',(-223.987916584291,-3.02619426203474,
134.681386713806));
#130909=CARTESIAN_POINT('Ctrl Pts',(-223.995672887034,-2.91800366193575,
134.76583437165));
#130910=CARTESIAN_POINT('Ctrl Pts',(-224.003429189776,-2.80633285982248,
134.845705206225));
#130911=CARTESIAN_POINT('Ctrl Pts',(-224.011185492518,-2.6916145391387,
134.920717530565));
#130912=CARTESIAN_POINT('Ctrl Pts',(-224.018945935032,-2.57683498983308,
134.995769891242));
#130913=CARTESIAN_POINT('Ctrl Pts',(-224.026706377547,-2.45900501663815,
135.065958374662));
#130914=CARTESIAN_POINT('Ctrl Pts',(-224.034466820061,-2.3385826848829,
135.131046888659));
#130915=CARTESIAN_POINT('Ctrl Pts',(-224.042239720327,-2.21796704051013,
135.196239888517));
#130916=CARTESIAN_POINT('Ctrl Pts',(-224.050012620593,-2.09475107322762,
135.256316387428));
#130917=CARTESIAN_POINT('Ctrl Pts',(-224.057785520858,-1.96941445777039,
135.311087784372));
#130918=CARTESIAN_POINT('Ctrl Pts',(-224.065275856618,-1.84863414402862,
135.363868103058));
#130919=CARTESIAN_POINT('Ctrl Pts',(-224.072766192378,-1.72588497407771,
135.411722219088));
#130920=CARTESIAN_POINT('Ctrl Pts',(-224.080256528138,-1.60160833088641,
135.454525541193));
#130921=CARTESIAN_POINT('Ctrl Pts',(-224.088030862257,-1.47261970095671,
135.49895176428));
#130922=CARTESIAN_POINT('Ctrl Pts',(-224.095805196376,-1.34157688579506,
135.538077360082));
#130923=CARTESIAN_POINT('Ctrl Pts',(-224.103579530495,-1.2089549196934,
135.571709048785));
#130924=CARTESIAN_POINT('Ctrl Pts',(-224.111344283442,-1.07649639831256,
135.605299289438));
#130925=CARTESIAN_POINT('Ctrl Pts',(-224.119109036389,-0.94246297360639,
135.633408999584));
#130926=CARTESIAN_POINT('Ctrl Pts',(-224.126873789336,-0.807347795883414,
135.655893632911));
#130927=CARTESIAN_POINT('Ctrl Pts',(-224.134630830222,-0.672366816459376,
135.678355934183));
#130928=CARTESIAN_POINT('Ctrl Pts',(-224.142387871107,-0.536306605313661,
135.695204213068));
#130929=CARTESIAN_POINT('Ctrl Pts',(-224.150144911992,-0.399673206403032,
135.706344337509));
#130930=CARTESIAN_POINT('Ctrl Pts',(-224.157896103232,-0.26314284380156,
135.717476061094));
#130931=CARTESIAN_POINT('Ctrl Pts',(-224.165647294472,-0.126040541888781,
135.722908166566));
#130932=CARTESIAN_POINT('Ctrl Pts',(-224.173398485712,0.0111201350492467,
135.722598046269));
#130933=CARTESIAN_POINT('Ctrl Pts',(-224.181146382489,0.148222515040508,
135.722288057782));
#130934=CARTESIAN_POINT('Ctrl Pts',(-224.188894279266,0.285382830564257,
135.716240698574));
#130935=CARTESIAN_POINT('Ctrl Pts',(-224.196642176043,0.422085319304466,
135.70446541703));
#130936=CARTESIAN_POINT('Ctrl Pts',(-224.204388452127,0.558759212830996,
135.692692598621));
#130937=CARTESIAN_POINT('Ctrl Pts',(-224.212134728211,0.69497508078477,
135.675194274608));
#130938=CARTESIAN_POINT('Ctrl Pts',(-224.219881004295,0.830220487615677,
135.652031914637));
#130939=CARTESIAN_POINT('Ctrl Pts',(-224.22762733756,0.965466892797638,
135.628869383686));
#130940=CARTESIAN_POINT('Ctrl Pts',(-224.235373670826,1.09974243720733,
135.600042799342));
#130941=CARTESIAN_POINT('Ctrl Pts',(-224.243120004091,1.23254350032708,
135.565665016814));
#130942=CARTESIAN_POINT('Ctrl Pts',(-224.250868072094,1.36537430332433,
135.531279535621));
#130943=CARTESIAN_POINT('Ctrl Pts',(-224.258616140097,1.49672958955542,
135.491340480474));
#130944=CARTESIAN_POINT('Ctrl Pts',(-224.2663642081,1.62611994022991,135.446010863167));
#130945=CARTESIAN_POINT('Ctrl Pts',(-224.274120510841,1.75564780850868,
135.400633069003));
#130946=CARTESIAN_POINT('Ctrl Pts',(-224.281876813583,1.88320619994714,
135.34985339755));
#130947=CARTESIAN_POINT('Ctrl Pts',(-224.289633116325,2.00832424735202,
135.293883618955));
#130948=CARTESIAN_POINT('Ctrl Pts',(-224.297393558839,2.13350907402604,
135.237883967604));
#130949=CARTESIAN_POINT('Ctrl Pts',(-224.305154001353,2.25625061163589,
135.176688863779));
#130950=CARTESIAN_POINT('Ctrl Pts',(-224.312914443867,2.37610263365482,
135.110556077231));
#130951=CARTESIAN_POINT('Ctrl Pts',(-224.320687344133,2.49614705277945,
135.044317128463));
#130952=CARTESIAN_POINT('Ctrl Pts',(-224.328460244398,2.61329235280028,
134.973124860647));
#130953=CARTESIAN_POINT('Ctrl Pts',(-224.336233144664,2.72712058242583,
134.897280894264));
#130954=CARTESIAN_POINT('Ctrl Pts',(-224.343723480426,2.83681086919125,
134.824194047097));
#130955=CARTESIAN_POINT('Ctrl Pts',(-224.351213816188,2.94342081701531,
134.746788012573));
#130956=CARTESIAN_POINT('Ctrl Pts',(-224.35870415195,3.04660702545978,134.665366794059));
#130957=CARTESIAN_POINT('Ctrl Pts',(-224.366478486069,3.15370557035735,
134.580858465301));
#130958=CARTESIAN_POINT('Ctrl Pts',(-224.374252820188,3.25745488469366,
134.491756773807));
#130959=CARTESIAN_POINT('Ctrl Pts',(-224.382027154307,3.35743558904776,
134.398356906921));
#130960=CARTESIAN_POINT('Ctrl Pts',(-224.389791907254,3.45729307611901,
134.305072147023));
#130961=CARTESIAN_POINT('Ctrl Pts',(-224.397556660201,3.55339091137502,
134.207500015746));
#130962=CARTESIAN_POINT('Ctrl Pts',(-224.405321413148,3.64534092412187,
134.105977283598));
#130963=CARTESIAN_POINT('Ctrl Pts',(-224.413078454033,3.73719961082005,
134.004555385259));
#130964=CARTESIAN_POINT('Ctrl Pts',(-224.420835494918,3.82491841259353,
133.899190982477));
#130965=CARTESIAN_POINT('Ctrl Pts',(-224.428592535803,3.90814460435721,
133.790258943687));
#130966=CARTESIAN_POINT('Ctrl Pts',(-224.436343727043,3.99130803460216,
133.681409051396));
#130967=CARTESIAN_POINT('Ctrl Pts',(-224.444094918283,4.06998536187414,
133.568997187552));
#130968=CARTESIAN_POINT('Ctrl Pts',(-224.451846109524,4.14386314510612,
133.453432397856));
#130969=CARTESIAN_POINT('Ctrl Pts',(-224.459594006301,4.21770952830937,
133.33791672628));
#130970=CARTESIAN_POINT('Ctrl Pts',(-224.467341903078,4.2867602146052,133.219251122881));
#130971=CARTESIAN_POINT('Ctrl Pts',(-224.475089799855,4.35074437105678,
133.097874620187));
#130972=CARTESIAN_POINT('Ctrl Pts',(-224.482836075939,4.41471514340217,
132.97652350684));
#130973=CARTESIAN_POINT('Ctrl Pts',(-224.490582352023,4.47362131171893,
132.852462967748));
#130974=CARTESIAN_POINT('Ctrl Pts',(-224.498328628107,4.52723760822754,
132.726157355296));
#130975=CARTESIAN_POINT('Ctrl Pts',(-224.506074961372,4.58085430051955,
132.599850810484));
#130976=CARTESIAN_POINT('Ctrl Pts',(-224.513821294638,4.62918089031577,
132.471299519126));
#130977=CARTESIAN_POINT('Ctrl Pts',(-224.521567627903,4.6720401067086,132.340988192421));
#130978=CARTESIAN_POINT('Ctrl Pts',(-224.529315695906,4.71490892112572,
132.2106476834));
#130979=CARTESIAN_POINT('Ctrl Pts',(-224.537063763909,4.75230780363691,
132.078546726046));
#130980=CARTESIAN_POINT('Ctrl Pts',(-224.544811831912,4.78410935786991,
131.945185194108));
#130981=CARTESIAN_POINT('Ctrl Pts',(-224.552568134654,4.81594471117315,
131.811681923946));
#130982=CARTESIAN_POINT('Ctrl Pts',(-224.560324437395,4.8421707617836,131.676915783805));
#130983=CARTESIAN_POINT('Ctrl Pts',(-224.568080740137,4.86271116270596,
131.541397394528));
#130984=CARTESIAN_POINT('Ctrl Pts',(-224.575841182651,4.88326252665881,
131.405806675006));
#130985=CARTESIAN_POINT('Ctrl Pts',(-224.583601625165,4.89812215188278,
131.269463294804));
#130986=CARTESIAN_POINT('Ctrl Pts',(-224.59136206768,4.90726571103205,131.132882007782));
#130987=CARTESIAN_POINT('Ctrl Pts',(-224.599134967945,4.91642394823418,
130.996081468352));
#130988=CARTESIAN_POINT('Ctrl Pts',(-224.60690786821,4.91984777314559,130.859042649995));
#130989=CARTESIAN_POINT('Ctrl Pts',(-224.614680768476,4.91756503473715,
130.722280220207));
#130990=CARTESIAN_POINT('Ctrl Pts',(-224.622171104238,4.91536527961958,
130.590489449217));
#130991=CARTESIAN_POINT('Ctrl Pts',(-224.629661440001,4.90786667141257,
130.458955628349));
#130992=CARTESIAN_POINT('Ctrl Pts',(-224.637151775763,4.89513936043556,
130.328131991364));
#130993=CARTESIAN_POINT('Ctrl Pts',(-224.644926109882,4.88192948959521,
130.192348136427));
#130994=CARTESIAN_POINT('Ctrl Pts',(-224.652700444001,4.86304475166706,
130.05689925926));
#130995=CARTESIAN_POINT('Ctrl Pts',(-224.660474778121,4.83850681130121,
129.922297751614));
#130996=CARTESIAN_POINT('Ctrl Pts',(-224.668239531068,4.81399911175392,
129.787862128297));
#130997=CARTESIAN_POINT('Ctrl Pts',(-224.676004284015,4.78385214159972,
129.654272177576));
#130998=CARTESIAN_POINT('Ctrl Pts',(-224.683769036962,4.74813941966383,
129.522036511135));
#130999=CARTESIAN_POINT('Ctrl Pts',(-224.691526077847,4.71246216810684,
129.389932183022));
#131000=CARTESIAN_POINT('Ctrl Pts',(-224.699283118732,4.67123026697988,
129.259179837391));
#131001=CARTESIAN_POINT('Ctrl Pts',(-224.707040159617,4.62456844719116,
129.130278857393));
#131002=CARTESIAN_POINT('Ctrl Pts',(-224.714791350857,4.57794181544364,
129.001475082626));
#131003=CARTESIAN_POINT('Ctrl Pts',(-224.722542542097,4.52589354791264,
128.874520260714));
#131004=CARTESIAN_POINT('Ctrl Pts',(-224.730293733337,4.46859836377831,
128.749899197695));
#131005=CARTESIAN_POINT('Ctrl Pts',(-224.738041630114,4.41132753162555,
128.625331101952));
#131006=CARTESIAN_POINT('Ctrl Pts',(-224.745789526891,4.34881438130046,
128.503095146748));
#131007=CARTESIAN_POINT('Ctrl Pts',(-224.753537423668,4.28128189148343,
128.383656499307));
#131008=CARTESIAN_POINT('Ctrl Pts',(-224.761283699753,4.21376352800743,
128.264242835856));
#131009=CARTESIAN_POINT('Ctrl Pts',(-224.769029975837,4.14122810572948,
128.147625656414));
#131010=CARTESIAN_POINT('Ctrl Pts',(-224.776776251921,4.06394453472509,
128.034245478952));
#131011=CARTESIAN_POINT('Ctrl Pts',(-224.784522585186,3.98666039323103,
127.920864464543));
#131012=CARTESIAN_POINT('Ctrl Pts',(-224.792268918451,3.90462825327537,
127.810720822848));
#131013=CARTESIAN_POINT('Ctrl Pts',(-224.800015251717,3.81816009686446,
127.704225695145));
#131014=CARTESIAN_POINT('Ctrl Pts',(-224.80776331972,3.73167257650934,127.597706718597));
#131015=CARTESIAN_POINT('Ctrl Pts',(-224.815511387723,3.64074730930894,
127.494838185354));
#131016=CARTESIAN_POINT('Ctrl Pts',(-224.823259455726,3.54573599235164,
127.395997471561));
#131017=CARTESIAN_POINT('Ctrl Pts',(-224.831015758468,3.45062369623616,
127.297051708682));
#131018=CARTESIAN_POINT('Ctrl Pts',(-224.838772061209,3.35141694672032,
127.20214259895));
#131019=CARTESIAN_POINT('Ctrl Pts',(-224.846528363951,3.24850407616572,
127.111610378295));
#131020=CARTESIAN_POINT('Ctrl Pts',(-224.854288806465,3.14553627791346,
127.021029837868));
#131021=CARTESIAN_POINT('Ctrl Pts',(-224.86204924898,3.03885872110251,126.934831086949));
#131022=CARTESIAN_POINT('Ctrl Pts',(-224.869809691494,2.92889133321031,
126.853312829859));
#131023=CARTESIAN_POINT('Ctrl Pts',(-224.877582591759,2.81874741590463,
126.771663712426));
#131024=CARTESIAN_POINT('Ctrl Pts',(-224.885355492025,2.70530343787483,
126.694710322879));
#131025=CARTESIAN_POINT('Ctrl Pts',(-224.89312839229,2.58900745651038,126.622707421444));
#131026=CARTESIAN_POINT('Ctrl Pts',(-224.900618728052,2.47693912700546,
126.553322006844));
#131027=CARTESIAN_POINT('Ctrl Pts',(-224.908109063813,2.36222281738965,
126.488533555236));
#131028=CARTESIAN_POINT('Ctrl Pts',(-224.915599399575,2.24527776402342,
126.428528031088));
#131029=CARTESIAN_POINT('Ctrl Pts',(-224.923373733694,2.12389870340883,
126.366247379251));
#131030=CARTESIAN_POINT('Ctrl Pts',(-224.931148067813,1.99973406480101,
126.308922217482));
#131031=CARTESIAN_POINT('Ctrl Pts',(-224.938922401932,1.87322664816605,
126.256811278955));
#131032=CARTESIAN_POINT('Ctrl Pts',(-224.946687154879,1.74687514061615,
126.204764562503));
#131033=CARTESIAN_POINT('Ctrl Pts',(-224.954451907826,1.61818695786183,
126.15791943082));
#131034=CARTESIAN_POINT('Ctrl Pts',(-224.962216660774,1.48762974803866,
126.116488947474));
#131035=CARTESIAN_POINT('Ctrl Pts',(-224.969973701659,1.35720220947681,
126.075099613469));
#131036=CARTESIAN_POINT('Ctrl Pts',(-224.977730742544,1.22490970829489,
126.039114343018));
#131037=CARTESIAN_POINT('Ctrl Pts',(-224.985487783429,1.09123980978319,
126.008698125267));
#131038=CARTESIAN_POINT('Ctrl Pts',(-224.993238974669,0.957670712781931,
125.978304844622));
#131039=CARTESIAN_POINT('Ctrl Pts',(-225.000990165909,0.822726665610151,
125.953472343892));
#131040=CARTESIAN_POINT('Ctrl Pts',(-225.008741357149,0.686909989304128,
125.934315676388));
#131041=CARTESIAN_POINT('Ctrl Pts',(-225.016489253926,0.551151038708379,
125.915167150978));
#131042=CARTESIAN_POINT('Ctrl Pts',(-225.024237150703,0.414520582974383,
125.901689715244));
#131043=CARTESIAN_POINT('Ctrl Pts',(-225.03198504748,0.277530505885588,
125.893947205153));
#131044=CARTESIAN_POINT('Ctrl Pts',(-225.039731323564,0.140569084167755,
125.886206314629));
#131045=CARTESIAN_POINT('Ctrl Pts',(-225.047477599648,0.00324858081679325,
125.88419798568));
#131046=CARTESIAN_POINT('Ctrl Pts',(-225.055223875733,-0.133915031459165,
125.887934087367));
#131047=CARTESIAN_POINT('Ctrl Pts',(-225.062970208998,-0.271079656245937,
125.891670216632));
#131048=CARTESIAN_POINT('Ctrl Pts',(-225.070716542263,-0.408086996826478,
125.901150850503));
#131049=CARTESIAN_POINT('Ctrl Pts',(-225.078462875529,-0.544422514503125,
125.916335741586));
#131050=CARTESIAN_POINT('Ctrl Pts',(-225.086210943532,-0.680788563573486,
125.931524033219));
#131051=CARTESIAN_POINT('Ctrl Pts',(-225.093959011535,-0.816482101873551,
125.95241908073));
#131052=CARTESIAN_POINT('Ctrl Pts',(-225.101707079538,-0.950995531297179,
125.978928972422));
#131053=CARTESIAN_POINT('Ctrl Pts',(-225.10946338228,-1.08565192319451,
126.005467039143));
#131054=CARTESIAN_POINT('Ctrl Pts',(-225.117219685022,-1.21912531654991,
126.037631795098));
#131055=CARTESIAN_POINT('Ctrl Pts',(-225.124975987764,-1.35091955811411,
126.075280431102));
#131056=CARTESIAN_POINT('Ctrl Pts',(-225.132736430278,-1.48278414223329,
126.112949161317));
#131057=CARTESIAN_POINT('Ctrl Pts',(-225.140496872792,-1.61296741785725,
126.156107480734));
#131058=CARTESIAN_POINT('Ctrl Pts',(-225.148257315306,-1.74099109552245,
126.204563549454));
#131059=CARTESIAN_POINT('Ctrl Pts',(-225.156030215571,-1.86922028816044,
126.253097404157));
#131060=CARTESIAN_POINT('Ctrl Pts',(-225.163803115837,-1.99528259536736,
126.306945849033));
#131061=CARTESIAN_POINT('Ctrl Pts',(-225.171576016102,-2.11872149418723,
126.365869624833));
#131062=CARTESIAN_POINT('Ctrl Pts',(-225.179066351864,-2.23767307811118,
126.422651372963));
#131063=CARTESIAN_POINT('Ctrl Pts',(-225.186556687627,-2.35418840480747,
126.48414571254));
#131064=CARTESIAN_POINT('Ctrl Pts',(-225.194047023389,-2.46788440960898,
126.550100446478));
#131065=CARTESIAN_POINT('Ctrl Pts',(-225.201822518005,-2.58590884821408,
126.618566092741));
#131066=CARTESIAN_POINT('Ctrl Pts',(-225.209598012622,-2.70126896985381,
126.692055388726));
#131067=CARTESIAN_POINT('Ctrl Pts',(-225.217373507239,-2.813507547675,126.770335538111));
#131068=CARTESIAN_POINT('Ctrl Pts',(-225.225139168045,-2.92560417530918,
126.848516685155));
#131069=CARTESIAN_POINT('Ctrl Pts',(-225.232904828851,-3.03458679731917,
126.931476406748));
#131070=CARTESIAN_POINT('Ctrl Pts',(-225.240670489657,-3.14002323591865,
127.01893631633));
#131071=CARTESIAN_POINT('Ctrl Pts',(-225.248426734605,-3.24533183291024,
127.106290180832));
#131072=CARTESIAN_POINT('Ctrl Pts',(-225.256182979553,-3.34710251134443,
127.198133117486));
#131073=CARTESIAN_POINT('Ctrl Pts',(-225.263939224501,-3.44493305069194,
127.294144194217));
#131074=CARTESIAN_POINT('Ctrl Pts',(-225.271690129401,-3.54269623531167,
127.39008916889));
#131075=CARTESIAN_POINT('Ctrl Pts',(-225.279441034301,-3.63652440006573,
127.490196301678));
#131076=CARTESIAN_POINT('Ctrl Pts',(-225.2871919392,-3.72604927651803,127.594105199152));
#131077=CARTESIAN_POINT('Ctrl Pts',(-225.294939186363,-3.81553190519101,
127.697965060867));
#131078=CARTESIAN_POINT('Ctrl Pts',(-225.302686433525,-3.90071503239147,
127.805622821377));
#131079=CARTESIAN_POINT('Ctrl Pts',(-225.310433680687,-3.98126835187258,
127.916682419969));
#131080=CARTESIAN_POINT('Ctrl Pts',(-225.318178949591,-4.06180110207999,
128.027713659515));
#131081=CARTESIAN_POINT('Ctrl Pts',(-225.325924218495,-4.13770616936105,
128.142144691342));
#131082=CARTESIAN_POINT('Ctrl Pts',(-225.3336694874,-4.20869478380431,128.259547995922));
#131083=CARTESIAN_POINT('Ctrl Pts',(-225.341416597441,-4.27970027303588,
128.376979208581));
#131084=CARTESIAN_POINT('Ctrl Pts',(-225.349163707482,-4.34578676788941,
128.497383773566));
#131085=CARTESIAN_POINT('Ctrl Pts',(-225.356910817524,-4.40670993374779,
128.620306904328));
#131086=CARTESIAN_POINT('Ctrl Pts',(-225.364658910431,-4.46764082885362,
128.743245630197));
#131087=CARTESIAN_POINT('Ctrl Pts',(-225.372407003339,-4.52340692386009,
128.868703204464));
#131088=CARTESIAN_POINT('Ctrl Pts',(-225.380155096247,-4.57381117634789,
128.996202885062));
#131089=CARTESIAN_POINT('Ctrl Pts',(-225.387908815622,-4.62425203111784,
129.123795152674));
#131090=CARTESIAN_POINT('Ctrl Pts',(-225.395662534997,-4.66932313191583,
129.253432121399));
#131091=CARTESIAN_POINT('Ctrl Pts',(-225.403416254372,-4.70887658549987,
129.384619667593));
#131092=CARTESIAN_POINT('Ctrl Pts',(-225.407292913424,-4.72865228880864,
129.450210046087));
#131093=CARTESIAN_POINT('Ctrl Pts',(-225.411169572477,-4.74704950926761,
129.516187808445));
#131094=CARTESIAN_POINT('Ctrl Pts',(-225.41504623153,-4.76405452823393,
129.582490119308));
#131095=CARTESIAN_POINT('Ctrl Pts',(-223.665116307759,-4.76405452823394,
129.582490119308));
#131096=CARTESIAN_POINT('Ctrl Pts',(-223.672768948211,-4.79775074606203,
129.713871161208));
#131097=CARTESIAN_POINT('Ctrl Pts',(-223.680421588662,-4.82600298496374,
129.846627596572));
#131098=CARTESIAN_POINT('Ctrl Pts',(-223.688074229114,-4.84871592411686,
129.980262959691));
#131099=CARTESIAN_POINT('Ctrl Pts',(-223.695918618263,-4.87199797095897,
130.117246762752));
#131100=CARTESIAN_POINT('Ctrl Pts',(-223.703763007413,-4.88945937353219,
130.255153683256));
#131101=CARTESIAN_POINT('Ctrl Pts',(-223.711607396563,-4.90105388213603,
130.393442247449));
#131102=CARTESIAN_POINT('Ctrl Pts',(-223.719451785713,-4.91264839073989,
130.531730811643));
#131103=CARTESIAN_POINT('Ctrl Pts',(-223.727296174863,-4.91837601587455,
130.670400566594));
#131104=CARTESIAN_POINT('Ctrl Pts',(-223.735140564013,-4.91824789595394,
130.808909952094));
#131105=CARTESIAN_POINT('',(-223.389859435967,-4.91824981741226,130.803020459256));
#131106=CARTESIAN_POINT('Ctrl Pts',(-223.320144520485,-4.76405452823402,
129.582490119308));
#131107=CARTESIAN_POINT('Ctrl Pts',(-223.328480310977,-4.80057528230012,
129.724883985132));
#131108=CARTESIAN_POINT('Ctrl Pts',(-223.33681610147,-4.83074977404695,
129.869079901701));
#131109=CARTESIAN_POINT('Ctrl Pts',(-223.345151891962,-4.85441260434725,
130.014511689445));
#131110=CARTESIAN_POINT('Ctrl Pts',(-223.353462705121,-4.87800453142564,
130.159507705889));
#131111=CARTESIAN_POINT('Ctrl Pts',(-223.361773518279,-4.89512365879074,
130.305731919146));
#131112=CARTESIAN_POINT('Ctrl Pts',(-223.370084331438,-4.90565513818706,
130.45260682913));
#131113=CARTESIAN_POINT('Ctrl Pts',(-223.376676032948,-4.91400815579326,
130.569100311465));
#131114=CARTESIAN_POINT('Ctrl Pts',(-223.383267734457,-4.91821793163162,
130.68600276536));
#131115=CARTESIAN_POINT('Ctrl Pts',(-223.389859435967,-4.91824981741226,
130.803020459257));
#131116=CARTESIAN_POINT('Ctrl Pts',(-223.389859435996,-4.9182498174124,
130.803020459769));
#131117=CARTESIAN_POINT('Ctrl Pts',(-223.397825722162,-4.91828835240305,
130.94444015766));
#131118=CARTESIAN_POINT('Ctrl Pts',(-223.405792008328,-4.91222295066778,
131.085797589312));
#131119=CARTESIAN_POINT('Ctrl Pts',(-223.413758294494,-4.90009592097111,
131.226548997063));
#131120=CARTESIAN_POINT('Ctrl Pts',(-223.421730186026,-4.88796035826073,
131.36739944256));
#131121=CARTESIAN_POINT('Ctrl Pts',(-223.429702077557,-4.86975469569824,
131.50764265691));
#131122=CARTESIAN_POINT('Ctrl Pts',(-223.437673969088,-4.84557290965292,
131.646741908751));
#131123=CARTESIAN_POINT('Ctrl Pts',(-223.445652730692,-4.82137028405894,
131.785961034517));
#131124=CARTESIAN_POINT('Ctrl Pts',(-223.453631492296,-4.79118132918627,
131.924033879671));
#131125=CARTESIAN_POINT('Ctrl Pts',(-223.461610253899,-4.75515071053607,
132.060435767622));
#131126=CARTESIAN_POINT('Ctrl Pts',(-223.469602905369,-4.71905736780639,
132.197075111469));
#131127=CARTESIAN_POINT('Ctrl Pts',(-223.477595556839,-4.67710213439243,
132.33203733918));
#131128=CARTESIAN_POINT('Ctrl Pts',(-223.485588208309,-4.62947932429489,
132.464813642625));
#131129=CARTESIAN_POINT('Ctrl Pts',(-223.493588711762,-4.58180972953302,
132.597720385554));
#131130=CARTESIAN_POINT('Ctrl Pts',(-223.501589215216,-4.52846158909981,
132.728436590422));
#131131=CARTESIAN_POINT('Ctrl Pts',(-223.509589718669,-4.46967645655695,
132.856475486719));
#131132=CARTESIAN_POINT('Ctrl Pts',(-223.517604814205,-4.41078410607477,
132.984747912585));
#131133=CARTESIAN_POINT('Ctrl Pts',(-223.525619909741,-4.34643511271477,
133.110332954569));
#131134=CARTESIAN_POINT('Ctrl Pts',(-223.533635005277,-4.27691637680558,
133.232769431648));
#131135=CARTESIAN_POINT('Ctrl Pts',(-223.536740095741,-4.2499844502882,
133.280201971389));
#131136=CARTESIAN_POINT('Ctrl Pts',(-223.539845186206,-4.22227708499426,
133.327162289319));
#131137=CARTESIAN_POINT('Ctrl Pts',(-223.542950276671,-4.19381262813753,
133.373624851267));
#131138=CARTESIAN_POINT('Ctrl Pts',(-223.55072461079,-4.12254507550592,
133.489954950088));
#131139=CARTESIAN_POINT('Ctrl Pts',(-223.558498944909,-4.04632073720989,
133.603501777012));
#131140=CARTESIAN_POINT('Ctrl Pts',(-223.566273279029,-3.96538320210203,
133.71381402379));
#131141=CARTESIAN_POINT('Ctrl Pts',(-223.574038031976,-3.88454541527281,
133.823990320582));
#131142=CARTESIAN_POINT('Ctrl Pts',(-223.581802784923,-3.79900621806242,
133.930939656645));
#131143=CARTESIAN_POINT('Ctrl Pts',(-223.589567537871,-3.70905417745916,
134.034236802681));
#131144=CARTESIAN_POINT('Ctrl Pts',(-223.597324578756,-3.61919147849049,
134.137431352535));
#131145=CARTESIAN_POINT('Ctrl Pts',(-223.605081619641,-3.52492491338456,
134.236980638129));
#131146=CARTESIAN_POINT('Ctrl Pts',(-223.612838660526,-3.42658506683357,
134.33249012798));
#131147=CARTESIAN_POINT('Ctrl Pts',(-223.620589851766,-3.32831937912596,
134.427927593381));
#131148=CARTESIAN_POINT('Ctrl Pts',(-223.628341043007,-3.22598680331828,
134.519331055509));
#131149=CARTESIAN_POINT('Ctrl Pts',(-223.636092234247,-3.11995650193513,
134.606340955302));
#131150=CARTESIAN_POINT('Ctrl Pts',(-223.643840131024,-3.01397126625837,
134.693313873567));
#131151=CARTESIAN_POINT('Ctrl Pts',(-223.651588027801,-2.90429173245949,
134.775896696082));
#131152=CARTESIAN_POINT('Ctrl Pts',(-223.659335924579,-2.79132187239289,
134.85376863198));
#131153=CARTESIAN_POINT('Ctrl Pts',(-223.667082200663,-2.67837564318566,
134.931624278748));
#131154=CARTESIAN_POINT('Ctrl Pts',(-223.674828476747,-2.5621407784028,
135.004770777197));
#131155=CARTESIAN_POINT('Ctrl Pts',(-223.682574752831,-2.44305177417905,
135.072929592197));
#131156=CARTESIAN_POINT('Ctrl Pts',(-223.690321086097,-2.32396189086749,
135.141088910329));
#131157=CARTESIAN_POINT('Ctrl Pts',(-223.698067419362,-2.20201816539445,
135.204260277339));
#131158=CARTESIAN_POINT('Ctrl Pts',(-223.705813752628,-2.07768097906349,
135.262210414468));
#131159=CARTESIAN_POINT('Ctrl Pts',(-223.713561820631,-1.95331594828191,
135.320173529128));
#131160=CARTESIAN_POINT('Ctrl Pts',(-223.721309888634,-1.82655674436542,
135.372912922089));
#131161=CARTESIAN_POINT('Ctrl Pts',(-223.729057956637,-1.69788469565208,
135.420243049211));
#131162=CARTESIAN_POINT('Ctrl Pts',(-223.736814259379,-1.56907589275363,
135.467623479355));
#131163=CARTESIAN_POINT('Ctrl Pts',(-223.744570562121,-1.43835055144765,
135.509583024164));
#131164=CARTESIAN_POINT('Ctrl Pts',(-223.752326864863,-1.30620670132538,
135.545985562236));
#131165=CARTESIAN_POINT('Ctrl Pts',(-223.760087307378,-1.17399232205152,
135.582407529438));
#131166=CARTESIAN_POINT('Ctrl Pts',(-223.767847749892,-1.04035830612776,
135.613266492088));
#131167=CARTESIAN_POINT('Ctrl Pts',(-223.775608192406,-0.905812931209745,
135.638477496185));
#131168=CARTESIAN_POINT('Ctrl Pts',(-223.783381092672,-0.771051572111542,
135.663728971225));
#131169=CARTESIAN_POINT('Ctrl Pts',(-223.791153992937,-0.635376317667153,
135.683314313856));
#131170=CARTESIAN_POINT('Ctrl Pts',(-223.798926893203,-0.499301522250402,
135.697200391397));
#131171=CARTESIAN_POINT('Ctrl Pts',(-223.806417228963,-0.368173388428244,
135.710581675038));
#131172=CARTESIAN_POINT('Ctrl Pts',(-223.813907564724,-0.236674565385695,
135.718670845973));
#131173=CARTESIAN_POINT('Ctrl Pts',(-223.821397900484,-0.105263399915473,
135.721484032647));
#131174=CARTESIAN_POINT('Ctrl Pts',(-223.829172234604,0.0311302598637276,
135.724403882149));
#131175=CARTESIAN_POINT('Ctrl Pts',(-223.836946568723,0.167861537898053,
135.721649021043));
#131176=CARTESIAN_POINT('Ctrl Pts',(-223.844720902842,0.304419070050243,
135.713180444397));
#131177=CARTESIAN_POINT('Ctrl Pts',(-223.852485655789,0.440808307248184,
135.704722304515));
#131178=CARTESIAN_POINT('Ctrl Pts',(-223.860250408736,0.577023838141903,
135.690564483831));
#131179=CARTESIAN_POINT('Ctrl Pts',(-223.868015161683,0.712551927773481,
135.670719915103));
#131180=CARTESIAN_POINT('Ctrl Pts',(-223.875772202568,0.847945408995826,
135.650895056281));
#131181=CARTESIAN_POINT('Ctrl Pts',(-223.883529243453,0.982652423374748,
135.62539474578));
#131182=CARTESIAN_POINT('Ctrl Pts',(-223.891286284338,1.11616235129815,
135.594283859962));
#131183=CARTESIAN_POINT('Ctrl Pts',(-223.899037475578,1.24957159834654,
135.563196435105));
#131184=CARTESIAN_POINT('Ctrl Pts',(-223.906788666818,1.38178517654963,
135.526506944803));
#131185=CARTESIAN_POINT('Ctrl Pts',(-223.914539858059,1.51230103732411,
135.48433162549));
#131186=CARTESIAN_POINT('Ctrl Pts',(-223.922287754836,1.64276142537632,
135.442174231812));
#131187=CARTESIAN_POINT('Ctrl Pts',(-223.930035651613,1.77152515991307,
135.39453576651));
#131188=CARTESIAN_POINT('Ctrl Pts',(-223.93778354839,1.898103993839,135.341582707245));
#131189=CARTESIAN_POINT('Ctrl Pts',(-223.945529824474,2.0246563502016,135.288640724619));
#131190=CARTESIAN_POINT('Ctrl Pts',(-223.953276100558,2.14902435457151,
135.230386510051));
#131191=CARTESIAN_POINT('Ctrl Pts',(-223.961022376642,2.27073881168078,
135.167035062402));
#131192=CARTESIAN_POINT('Ctrl Pts',(-223.968768709908,2.39245416725835,
135.103683147107));
#131193=CARTESIAN_POINT('Ctrl Pts',(-223.976515043173,2.51151558968812,
135.035234104158));
#131194=CARTESIAN_POINT('Ctrl Pts',(-223.984261376438,2.62747796760326,
134.961949172517));
#131195=CARTESIAN_POINT('Ctrl Pts',(-223.992009444441,2.74346631448908,
134.888647829223));
#131196=CARTESIAN_POINT('Ctrl Pts',(-223.999757512445,2.85635390542677,
134.81050865109));
#131197=CARTESIAN_POINT('Ctrl Pts',(-224.007505580448,2.96572446715174,
134.727836302139));
#131198=CARTESIAN_POINT('Ctrl Pts',(-224.015261883189,3.07521126921138,
134.645076088032));
#131199=CARTESIAN_POINT('Ctrl Pts',(-224.023018185931,3.18117326273432,
134.557773314948));
#131200=CARTESIAN_POINT('Ctrl Pts',(-224.030774488673,3.28322672777085,
134.466273412343));
#131201=CARTESIAN_POINT('Ctrl Pts',(-224.038534931187,3.38533466181416,
134.374724673485));
#131202=CARTESIAN_POINT('Ctrl Pts',(-224.046295373702,3.48352963086155,
134.278974614264));
#131203=CARTESIAN_POINT('Ctrl Pts',(-224.054055816216,3.57746542421788,
134.179404943353));
#131204=CARTESIAN_POINT('Ctrl Pts',(-224.061828716481,3.67155201164893,
134.079675434367));
#131205=CARTESIAN_POINT('Ctrl Pts',(-224.069601616747,3.76136550416974,
133.976114356373));
#131206=CARTESIAN_POINT('Ctrl Pts',(-224.077374517012,3.84660000521288,
133.869136541251));
#131207=CARTESIAN_POINT('Ctrl Pts',(-224.084864852774,3.92873601744643,
133.766047639173));
#131208=CARTESIAN_POINT('Ctrl Pts',(-224.092355188536,4.00661999195626,
133.65978634957));
#131209=CARTESIAN_POINT('Ctrl Pts',(-224.099845524297,4.08001775042296,
133.550747010398));
#131210=CARTESIAN_POINT('Ctrl Pts',(-224.107619858416,4.15619840721381,
133.437573411535));
#131211=CARTESIAN_POINT('Ctrl Pts',(-224.115394192535,4.22778726016786,
133.321048445176));
#131212=CARTESIAN_POINT('Ctrl Pts',(-224.123168526655,4.29447508852375,
133.201581253333));
#131213=CARTESIAN_POINT('Ctrl Pts',(-224.130933279602,4.36108073009126,
133.082261294128));
#131214=CARTESIAN_POINT('Ctrl Pts',(-224.138698032549,4.42279717627691,
132.96000666226));
#131215=CARTESIAN_POINT('Ctrl Pts',(-224.146462785496,4.47935762148213,
132.835256567971));
#131216=CARTESIAN_POINT('Ctrl Pts',(-224.154219826381,4.53586189005581,
132.710630377234));
#131217=CARTESIAN_POINT('Ctrl Pts',(-224.161976867266,4.58722018829892,
132.583514010232));
#131218=CARTESIAN_POINT('Ctrl Pts',(-224.169733908151,4.6332110961578,132.454372132962));
#131219=CARTESIAN_POINT('Ctrl Pts',(-224.177485099391,4.67916732191513,
132.325327642588));
#131220=CARTESIAN_POINT('Ctrl Pts',(-224.185236290631,4.71976408313914,
132.194261049065));
#131221=CARTESIAN_POINT('Ctrl Pts',(-224.192987481871,4.75482780330945,
132.061657568718));
#131222=CARTESIAN_POINT('Ctrl Pts',(-224.200735378648,4.78987662046337,
131.929110448386));
#131223=CARTESIAN_POINT('Ctrl Pts',(-224.208483275425,4.81939697415904,
131.795028117613));
#131224=CARTESIAN_POINT('Ctrl Pts',(-224.216231172202,4.8432650172885,131.659911337751));
#131225=CARTESIAN_POINT('Ctrl Pts',(-224.223977448286,4.86712806773788,
131.524822821407));
#131226=CARTESIAN_POINT('Ctrl Pts',(-224.23172372437,4.88534109139618,131.388700671134));
#131227=CARTESIAN_POINT('Ctrl Pts',(-224.239470000454,4.89783136139199,
131.252055846338));
#131228=CARTESIAN_POINT('Ctrl Pts',(-224.247216333719,4.91032172358816,
131.11541001286));
#131229=CARTESIAN_POINT('Ctrl Pts',(-224.254962666985,4.91708921223833,
130.978241886502));
#131230=CARTESIAN_POINT('Ctrl Pts',(-224.26270900025,4.91811302151363,130.841067158101));
#131231=CARTESIAN_POINT('Ctrl Pts',(-224.270457068253,4.91913706006392,
130.703861710372));
#131232=CARTESIAN_POINT('Ctrl Pts',(-224.278205136256,4.91441485681918,
130.566650048538));
#131233=CARTESIAN_POINT('Ctrl Pts',(-224.285953204259,4.90397772838234,
130.429947073433));
#131234=CARTESIAN_POINT('Ctrl Pts',(-224.293709507001,4.89352950724115,
130.293098808779));
#131235=CARTESIAN_POINT('Ctrl Pts',(-224.301465809742,4.87735425746788,
130.156760701289));
#131236=CARTESIAN_POINT('Ctrl Pts',(-224.309222112484,4.85553518864238,
130.021442298483));
#131237=CARTESIAN_POINT('Ctrl Pts',(-224.316982554998,4.83370447432288,
129.886051672171));
#131238=CARTESIAN_POINT('Ctrl Pts',(-224.324742997512,4.80622401703399,
129.751682217852));
#131239=CARTESIAN_POINT('Ctrl Pts',(-224.332503440026,4.77322782375656,
129.61883153525));
#131240=CARTESIAN_POINT('Ctrl Pts',(-224.340276340292,4.74017866206041,
129.485767588939));
#131241=CARTESIAN_POINT('Ctrl Pts',(-224.348049240557,4.70159618066785,
129.354227661756));
#131242=CARTESIAN_POINT('Ctrl Pts',(-224.355822140823,4.65766404481944,
129.22469333991));
#131243=CARTESIAN_POINT('Ctrl Pts',(-224.363312476585,4.61532895276476,
129.099867916933));
#131244=CARTESIAN_POINT('Ctrl Pts',(-224.370802812348,4.56802651098553,
128.976905100769));
#131245=CARTESIAN_POINT('Ctrl Pts',(-224.37829314811,4.51596190807124,128.856215061569));
#131246=CARTESIAN_POINT('Ctrl Pts',(-224.386067482229,4.46192325991574,
128.730949022857));
#131247=CARTESIAN_POINT('Ctrl Pts',(-224.393841816348,4.40258302923531,
128.607734702767));
#131248=CARTESIAN_POINT('Ctrl Pts',(-224.401616150467,4.33811829741793,
128.487053408733));
#131249=CARTESIAN_POINT('Ctrl Pts',(-224.409380903414,4.2737330126215,128.36652084361));
#131250=CARTESIAN_POINT('Ctrl Pts',(-224.417145656361,4.20423597507095,
128.248515434773));
#131251=CARTESIAN_POINT('Ctrl Pts',(-224.424910409309,4.12985248983799,
128.133499057193));
#131252=CARTESIAN_POINT('Ctrl Pts',(-224.432667450194,4.05554288333078,
128.0185969155));
#131253=CARTESIAN_POINT('Ctrl Pts',(-224.440424491079,3.97635669834492,
127.90667822329));
#131254=CARTESIAN_POINT('Ctrl Pts',(-224.448181531964,3.89256518859751,
127.798180430848));
#131255=CARTESIAN_POINT('Ctrl Pts',(-224.455932723204,3.8088368666793,127.689764457434));
#131256=CARTESIAN_POINT('Ctrl Pts',(-224.463683914444,3.72051037062131,
127.584764557177));
#131257=CARTESIAN_POINT('Ctrl Pts',(-224.471435105684,3.62790010430862,
127.483589036193));
#131258=CARTESIAN_POINT('Ctrl Pts',(-224.479183002461,3.53532919982994,
127.382456517504));
#131259=CARTESIAN_POINT('Ctrl Pts',(-224.486930899238,3.43847840978776,
127.285145432954));
#131260=CARTESIAN_POINT('Ctrl Pts',(-224.494678796015,3.33770209650352,
127.192030652364));
#131261=CARTESIAN_POINT('Ctrl Pts',(-224.502425072099,3.23694686345152,
127.098935349379));
#131262=CARTESIAN_POINT('Ctrl Pts',(-224.510171348183,3.13226802741177,
127.010034869565));
#131263=CARTESIAN_POINT('Ctrl Pts',(-224.517917624268,3.02405616235136,
126.925666586137));
#131264=CARTESIAN_POINT('Ctrl Pts',(-224.525663957533,2.91584349849538,
126.841297679921));
#131265=CARTESIAN_POINT('Ctrl Pts',(-224.533410290798,2.804098061906,126.76146127724));
#131266=CARTESIAN_POINT('Ctrl Pts',(-224.541156624064,2.68924247183255,
126.686453626121));
#131267=CARTESIAN_POINT('Ctrl Pts',(-224.548904692067,2.57436116064653,
126.611429177559));
#131268=CARTESIAN_POINT('Ctrl Pts',(-224.55665276007,2.45636863730857,126.541235846087));
#131269=CARTESIAN_POINT('Ctrl Pts',(-224.564400828072,2.33571502986092,
126.476125600636));
#131270=CARTESIAN_POINT('Ctrl Pts',(-224.572157130814,2.21493319032331,
126.410946155241));
#131271=CARTESIAN_POINT('Ctrl Pts',(-224.579913433556,2.09148496159011,
126.35086077364));
#131272=CARTESIAN_POINT('Ctrl Pts',(-224.587669736298,1.96584401723188,
126.29607487214));
#131273=CARTESIAN_POINT('Ctrl Pts',(-224.595430178812,1.84013601451799,
126.241259729754));
#131274=CARTESIAN_POINT('Ctrl Pts',(-224.603190621326,1.71223332864473,
126.191749844542));
#131275=CARTESIAN_POINT('Ctrl Pts',(-224.610951063841,1.58262703840013,
126.147701437443));
#131276=CARTESIAN_POINT('Ctrl Pts',(-224.618723964106,1.45281269263288,
126.10358231993));
#131277=CARTESIAN_POINT('Ctrl Pts',(-224.626496864372,1.32128965286626,
126.064942310556));
#131278=CARTESIAN_POINT('Ctrl Pts',(-224.634269764637,1.18856236676532,
126.031887195659));
#131279=CARTESIAN_POINT('Ctrl Pts',(-224.641760100399,1.06066005183867,
126.000033717451));
#131280=CARTESIAN_POINT('Ctrl Pts',(-224.649250436161,0.93163982691611,
125.973366195727));
#131281=CARTESIAN_POINT('Ctrl Pts',(-224.656740771922,0.801957689206216,
125.951933706501));
#131282=CARTESIAN_POINT('Ctrl Pts',(-224.664515106041,0.66735861382538,
125.929688597932));
#131283=CARTESIAN_POINT('Ctrl Pts',(-224.67228944016,0.531620072575311,
125.91301286492));
#131284=CARTESIAN_POINT('Ctrl Pts',(-224.680063774279,0.395242719848658,
125.902017682305));
#131285=CARTESIAN_POINT('Ctrl Pts',(-224.687828527226,0.259033440021218,
125.891036050269));
#131286=CARTESIAN_POINT('Ctrl Pts',(-224.695593280173,0.122187301125484,
125.8857210703));
#131287=CARTESIAN_POINT('Ctrl Pts',(-224.70335803312,-0.0147853254507163,
125.886132841563));
#131288=CARTESIAN_POINT('Ctrl Pts',(-224.711115074005,-0.151621908883225,
125.886544203848));
#131289=CARTESIAN_POINT('Ctrl Pts',(-224.71887211489,-0.288584341554595,
125.89267099704));
#131290=CARTESIAN_POINT('Ctrl Pts',(-224.726629155775,-0.425157964891527,
125.904521460268));
#131291=CARTESIAN_POINT('Ctrl Pts',(-224.734380347015,-0.561628596996526,
125.916362986969));
#131292=CARTESIAN_POINT('Ctrl Pts',(-224.742131538255,-0.697710615446485,
125.933919558784));
#131293=CARTESIAN_POINT('Ctrl Pts',(-224.749882729495,-0.832890557761763,
125.95714735825));
#131294=CARTESIAN_POINT('Ctrl Pts',(-224.757630626272,-0.968013044996067,
125.980365285281));
#131295=CARTESIAN_POINT('Ctrl Pts',(-224.765378523049,-1.10223383415023,
126.009249579745));
#131296=CARTESIAN_POINT('Ctrl Pts',(-224.773126419827,-1.23504599513528,
126.043704732879));
#131297=CARTESIAN_POINT('Ctrl Pts',(-224.780872695911,-1.36783037467863,
126.078152678739));
#131298=CARTESIAN_POINT('Ctrl Pts',(-224.788618971995,-1.49920633393927,
126.118169067302));
#131299=CARTESIAN_POINT('Ctrl Pts',(-224.796365248079,-1.62867891650682,
126.163607656092));
#131300=CARTESIAN_POINT('Ctrl Pts',(-224.804111581344,-1.7581524548121,
126.2090465803));
#131301=CARTESIAN_POINT('Ctrl Pts',(-224.811857914609,-1.88572221948171,
126.259907655135));
#131302=CARTESIAN_POINT('Ctrl Pts',(-224.819604247875,-2.01091053263215,
126.315995448348));
#131303=CARTESIAN_POINT('Ctrl Pts',(-224.827352315878,-2.13612688083783,
126.372095802034));
#131304=CARTESIAN_POINT('Ctrl Pts',(-224.83510038388,-2.25896035957585,
126.433425043411));
#131305=CARTESIAN_POINT('Ctrl Pts',(-224.842848451883,-2.37895567504547,
126.49974066237));
#131306=CARTESIAN_POINT('Ctrl Pts',(-224.850604754625,-2.49907852296384,
126.566126762359));
#131307=CARTESIAN_POINT('Ctrl Pts',(-224.858361057367,-2.61635683923091,
126.637509637004));
#131308=CARTESIAN_POINT('Ctrl Pts',(-224.866117360109,-2.73036176915656,
126.713601803846));
#131309=CARTESIAN_POINT('Ctrl Pts',(-224.873877802623,-2.84442754694593,
126.789734583369));
#131310=CARTESIAN_POINT('Ctrl Pts',(-224.881638245137,-2.95521614147743,
126.870581433081));
#131311=CARTESIAN_POINT('Ctrl Pts',(-224.889398687651,-3.06233067957151,
126.955813635723));
#131312=CARTESIAN_POINT('Ctrl Pts',(-224.897171587916,-3.16961716743133,
127.041182660663));
#131313=CARTESIAN_POINT('Ctrl Pts',(-224.904944488182,-3.27321751728239,
127.130950850041));
#131314=CARTESIAN_POINT('Ctrl Pts',(-224.912717388447,-3.37277006179579,
127.224750977849));
#131315=CARTESIAN_POINT('Ctrl Pts',(-224.92020772421,-3.46870362056756,
127.315141234752));
#131316=CARTESIAN_POINT('Ctrl Pts',(-224.927698059972,-3.56087834493337,
127.409275157151));
#131317=CARTESIAN_POINT('Ctrl Pts',(-224.935188395735,-3.64900646822336,
127.506795628462));
#131318=CARTESIAN_POINT('Ctrl Pts',(-224.942883618158,-3.73954520131624,
127.606983622868));
#131319=CARTESIAN_POINT('Ctrl Pts',(-224.95057884058,-3.82611323979784,
127.711078857721));
#131320=CARTESIAN_POINT('Ctrl Pts',(-224.958274063002,-3.90834911965968,
127.818729993836));
#131321=CARTESIAN_POINT('Ctrl Pts',(-224.965960080009,-3.99048662478202,
127.926252352189));
#131322=CARTESIAN_POINT('Ctrl Pts',(-224.973646097015,-4.06830203621734,
128.037321839102));
#131323=CARTESIAN_POINT('Ctrl Pts',(-224.981332114021,-4.14147118111289,
128.151550877213));
#131324=CARTESIAN_POINT('Ctrl Pts',(-224.989009420355,-4.21455740237118,
128.265650457923));
#131325=CARTESIAN_POINT('Ctrl Pts',(-224.996686726688,-4.28300762449184,
128.382902128035));
#131326=CARTESIAN_POINT('Ctrl Pts',(-225.004364033021,-4.34653884654452,
128.502886499098));
#131327=CARTESIAN_POINT('Ctrl Pts',(-225.012036237156,-4.41002784689328,
128.622791130712));
#131328=CARTESIAN_POINT('Ctrl Pts',(-225.01970844129,-4.46860416159031,
128.745424500333));
#131329=CARTESIAN_POINT('Ctrl Pts',(-225.027380645424,-4.52202899545416,
128.870339721409));
#131330=CARTESIAN_POINT('Ctrl Pts',(-225.035049996425,-4.57543396173566,
128.995208489118));
#131331=CARTESIAN_POINT('Ctrl Pts',(-225.042719347426,-4.62369109700592,
129.122357055415));
#131332=CARTESIAN_POINT('Ctrl Pts',(-225.050388698427,-4.66660851965282,
129.251315870367));
#131333=CARTESIAN_POINT('Ctrl Pts',(-225.056882517944,-4.70294770881461,
129.360508326054));
#131334=CARTESIAN_POINT('Ctrl Pts',(-225.063376337461,-4.73545938964632,
129.470998107947));
#131335=CARTESIAN_POINT('Ctrl Pts',(-225.069870156977,-4.76405452823403,
129.582490119308));
#131336=CARTESIAN_POINT('Origin',(213.235140564004,0.,130.804360617566));
#131337=CARTESIAN_POINT('',(-227.165337382971,-4.76405452823413,129.582490119309));
#131338=CARTESIAN_POINT('',(-226.819766265743,-4.76405452823404,129.582490119308));
#131339=CARTESIAN_POINT('',(213.235140564004,-4.76405452823405,129.582490119308));
#131340=CARTESIAN_POINT('',(-225.485140564065,-4.91824980939642,130.802991357867));
#131341=CARTESIAN_POINT('Ctrl Pts',(-225.485140564065,-4.91824980939641,
130.802991357866));
#131342=CARTESIAN_POINT('Ctrl Pts',(-225.492858871425,-4.91828752983759,
130.938479572856));
#131343=CARTESIAN_POINT('Ctrl Pts',(-225.500577178786,-4.9127223578869,
131.074194759287));
#131344=CARTESIAN_POINT('Ctrl Pts',(-225.508295486146,-4.90152415104786,
131.20963097078));
#131345=CARTESIAN_POINT('Ctrl Pts',(-225.516004459813,-4.89033948612087,
131.344903400225));
#131346=CARTESIAN_POINT('Ctrl Pts',(-225.523713433479,-4.87353536893283,
131.479897133919));
#131347=CARTESIAN_POINT('Ctrl Pts',(-225.531422407145,-4.85113363514974,
131.614104723083));
#131348=CARTESIAN_POINT('Ctrl Pts',(-225.539123969384,-4.82875343845062,
131.748183284728));
#131349=CARTESIAN_POINT('Ctrl Pts',(-225.546825531624,-4.8007863969902,
131.88147681636));
#131350=CARTESIAN_POINT('Ctrl Pts',(-225.554527093863,-4.76730623132601,
132.013481934581));
#131351=CARTESIAN_POINT('Ctrl Pts',(-225.562223159812,-4.73384995908458,
132.145392846157));
#131352=CARTESIAN_POINT('Ctrl Pts',(-225.569919225762,-4.69488848950265,
132.276016790645));
#131353=CARTESIAN_POINT('Ctrl Pts',(-225.577615291712,-4.65054672781533,
132.40485997555));
#131354=CARTESIAN_POINT('Ctrl Pts',(-225.58530856989,-4.60622102819074,
132.533656489162));
#131355=CARTESIAN_POINT('Ctrl Pts',(-225.593001848068,-4.55651903941725,
132.660673150561));
#131356=CARTESIAN_POINT('Ctrl Pts',(-225.600695126247,-4.50161560965181,
132.785431026572));
#131357=CARTESIAN_POINT('Ctrl Pts',(-225.608387200152,-4.4467207742352,
132.910169373517));
#131358=CARTESIAN_POINT('Ctrl Pts',(-225.616079274058,-4.38662627684785,
133.032649274864));
#131359=CARTESIAN_POINT('Ctrl Pts',(-225.623771347963,-4.32155503253321,
133.152411972048));
#131360=CARTESIAN_POINT('Ctrl Pts',(-225.63146394312,-4.2564793786793,133.272182784927));
#131361=CARTESIAN_POINT('Ctrl Pts',(-225.639156538277,-4.1864264967233,
133.389235678472));
#131362=CARTESIAN_POINT('Ctrl Pts',(-225.646849133434,-4.11166492579988,
133.503137118213));
#131363=CARTESIAN_POINT('Ctrl Pts',(-225.654543975428,-4.036881518678,133.617071826042));
#131364=CARTESIAN_POINT('Ctrl Pts',(-225.662238817422,-3.95738690479067,
133.727852917352));
#131365=CARTESIAN_POINT('Ctrl Pts',(-225.669933659416,-3.87349226168471,
133.835076830142));
#131366=CARTESIAN_POINT('Ctrl Pts',(-225.677636826674,-3.78950685061555,
133.942416751485));
#131367=CARTESIAN_POINT('Ctrl Pts',(-225.685339993933,-3.70111215078513,
134.046191497544));
#131368=CARTESIAN_POINT('Ctrl Pts',(-225.693043161192,-3.60865909155127,
134.146031251166));
#131369=CARTESIAN_POINT('Ctrl Pts',(-225.700751019266,-3.51614973336657,
134.24593180184));
#131370=CARTESIAN_POINT('Ctrl Pts',(-225.70845887734,-3.41957737552138,
134.341892309152));
#131371=CARTESIAN_POINT('Ctrl Pts',(-225.716166735414,-3.31932806359591,
134.433581507609));
#131372=CARTESIAN_POINT('Ctrl Pts',(-225.723885921011,-3.21893142457809,
134.525405453155));
#131373=CARTESIAN_POINT('Ctrl Pts',(-225.731605106607,-3.11484734573308,
134.61294530241));
#131374=CARTESIAN_POINT('Ctrl Pts',(-225.739324292203,-3.00749338761577,
134.695911283553));
#131375=CARTESIAN_POINT('Ctrl Pts',(-225.743196951807,-2.95363468300403,
134.737534716444));
#131376=CARTESIAN_POINT('Ctrl Pts',(-225.747069611411,-2.89895340086588,
134.7780076219));
#131377=CARTESIAN_POINT('Ctrl Pts',(-225.750942271014,-2.84350467758067,
134.817297722864));
#131378=CARTESIAN_POINT('Ctrl Pts',(-225.758716605133,-2.73219179562714,
134.896172295827));
#131379=CARTESIAN_POINT('Ctrl Pts',(-225.766490939252,-2.61741832065757,
134.970536810859));
#131380=CARTESIAN_POINT('Ctrl Pts',(-225.774265273371,-2.49958585641601,
135.040072317966));
#131381=CARTESIAN_POINT('Ctrl Pts',(-225.782030026319,-2.38189861015628,
135.109522128774));
#131382=CARTESIAN_POINT('Ctrl Pts',(-225.789794779266,-2.2611602091394,
135.17415457622));
#131383=CARTESIAN_POINT('Ctrl Pts',(-225.797559532213,-2.13780333452593,
135.233692391704));
#131384=CARTESIAN_POINT('Ctrl Pts',(-225.805316573098,-2.01456897969869,
135.293171073391));
#131385=CARTESIAN_POINT('Ctrl Pts',(-225.813073613983,-1.88872167661626,
135.347565024023));
#131386=CARTESIAN_POINT('Ctrl Pts',(-225.820830654868,-1.76072064399407,
135.396641736608));
#131387=CARTESIAN_POINT('Ctrl Pts',(-225.828581846108,-1.63281613794611,
135.445681440063));
#131388=CARTESIAN_POINT('Ctrl Pts',(-225.836333037348,-1.50276149869489,
135.489411747278));
#131389=CARTESIAN_POINT('Ctrl Pts',(-225.844084228588,-1.37103763747473,
135.527647487864));
#131390=CARTESIAN_POINT('Ctrl Pts',(-225.851832125365,-1.23936976240962,
135.56586697724));
#131391=CARTESIAN_POINT('Ctrl Pts',(-225.859580022142,-1.10603445112609,
135.598596436037));
#131392=CARTESIAN_POINT('Ctrl Pts',(-225.86732791892,-0.971529348780938,
135.625700035918));
#131393=CARTESIAN_POINT('Ctrl Pts',(-225.875074195004,-0.837052382003607,
135.652797966311));
#131394=CARTESIAN_POINT('Ctrl Pts',(-225.882820471088,-0.701406493895269,
135.674272301345));
#131395=CARTESIAN_POINT('Ctrl Pts',(-225.890566747172,-0.565100751471642,
135.690038073476));
#131396=CARTESIAN_POINT('Ctrl Pts',(-225.898313080437,-0.428794002870174,
135.705803961986));
#131397=CARTESIAN_POINT('Ctrl Pts',(-225.906059413703,-0.291827778609822,
135.715861158585));
#131398=CARTESIAN_POINT('Ctrl Pts',(-225.913805746968,-0.15471712174097,
135.720176488278));
#131399=CARTESIAN_POINT('Ctrl Pts',(-225.921553814971,-0.0175757598913571,
135.724492784358));
#131400=CARTESIAN_POINT('Ctrl Pts',(-225.929301882974,0.11970970823201,
135.723064642541));
#131401=CARTESIAN_POINT('Ctrl Pts',(-225.937049950977,0.256623778562881,
135.71591101421));
#131402=CARTESIAN_POINT('Ctrl Pts',(-225.944806253719,0.393683362797184,
135.708749782918));
#131403=CARTESIAN_POINT('Ctrl Pts',(-225.952562556461,0.530370369676102,
135.695850929871));
#131404=CARTESIAN_POINT('Ctrl Pts',(-225.960318859203,0.666173401615767,
135.677285412951));
#131405=CARTESIAN_POINT('Ctrl Pts',(-225.968079301717,0.802048915722529,
135.658709987056));
#131406=CARTESIAN_POINT('Ctrl Pts',(-225.975839744231,0.937039130162459,
135.634461939866));
#131407=CARTESIAN_POINT('Ctrl Pts',(-225.983600186745,1.07064337270872,
135.604663298749));
#131408=CARTESIAN_POINT('Ctrl Pts',(-225.991373087011,1.20446208864594,
135.574816822208));
#131409=CARTESIAN_POINT('Ctrl Pts',(-225.999145987276,1.33689000875,135.539402047174));
#131410=CARTESIAN_POINT('Ctrl Pts',(-226.006918887542,1.46744127803828,
135.498591029253));
#131411=CARTESIAN_POINT('Ctrl Pts',(-226.014409223304,1.5932466798477,135.459263594631));
#131412=CARTESIAN_POINT('Ctrl Pts',(-226.021899559065,1.71730921392521,
135.414925543332));
#131413=CARTESIAN_POINT('Ctrl Pts',(-226.029389894827,1.83921390427903,
135.365772161903));
#131414=CARTESIAN_POINT('Ctrl Pts',(-226.037164228946,1.96574064801962,
135.314755115076));
#131415=CARTESIAN_POINT('Ctrl Pts',(-226.044938563065,2.09034348734575,
135.258388776861));
#131416=CARTESIAN_POINT('Ctrl Pts',(-226.052712897184,2.21253700396133,
135.196838627597));
#131417=CARTESIAN_POINT('Ctrl Pts',(-226.060477650131,2.33457992798875,
135.13536433339));
#131418=CARTESIAN_POINT('Ctrl Pts',(-226.068242403078,2.45421909145953,
135.068719113706));
#131419=CARTESIAN_POINT('Ctrl Pts',(-226.076007156025,2.57098734571181,
134.997117125007));
#131420=CARTESIAN_POINT('Ctrl Pts',(-226.08376419691,2.68763962408718,134.925586252413));
#131421=CARTESIAN_POINT('Ctrl Pts',(-226.091521237795,2.8014263365765,134.849108611113));
#131422=CARTESIAN_POINT('Ctrl Pts',(-226.09927827868,2.91190364952899,134.76794487911));
#131423=CARTESIAN_POINT('Ctrl Pts',(-226.10702946992,3.02229765068023,134.686842353309));
#131424=CARTESIAN_POINT('Ctrl Pts',(-226.11478066116,3.12938690592123,134.601061001191));
#131425=CARTESIAN_POINT('Ctrl Pts',(-226.1225318524,3.23275568189076,134.510905337882));
#131426=CARTESIAN_POINT('Ctrl Pts',(-226.130279749177,3.33608052337347,
134.420787993134));
#131427=CARTESIAN_POINT('Ctrl Pts',(-226.138027645954,3.43568773664912,
134.326300291442));
#131428=CARTESIAN_POINT('Ctrl Pts',(-226.145775542731,3.53119405612993,
134.227787497237));
#131429=CARTESIAN_POINT('Ctrl Pts',(-226.153521818815,3.62668039774784,
134.129295309784));
#131430=CARTESIAN_POINT('Ctrl Pts',(-226.161268094899,3.71806727985388,
134.026779985055));
#131431=CARTESIAN_POINT('Ctrl Pts',(-226.169014370983,3.80500805368966,
133.920623888514));
#131432=CARTESIAN_POINT('Ctrl Pts',(-226.176760704248,3.89194946930259,
133.814467008352));
#131433=CARTESIAN_POINT('Ctrl Pts',(-226.184507037514,3.97444446343468,
133.704669605221));
#131434=CARTESIAN_POINT('Ctrl Pts',(-226.192253370779,4.05218673167326,
133.59164706753));
#131435=CARTESIAN_POINT('Ctrl Pts',(-226.200001438782,4.12994640975347,
133.478599219226));
#131436=CARTESIAN_POINT('Ctrl Pts',(-226.207749506785,4.20295102250017,
133.362325121232));
#131437=CARTESIAN_POINT('Ctrl Pts',(-226.215497574788,4.27093787170999,
133.243268725407));
#131438=CARTESIAN_POINT('Ctrl Pts',(-226.223253877529,4.33899697815228,
133.124085795028));
#131439=CARTESIAN_POINT('Ctrl Pts',(-226.231010180271,4.40202747375333,
133.002114999821));
#131440=CARTESIAN_POINT('Ctrl Pts',(-226.238766483013,4.45981263450326,
132.877824947528));
#131441=CARTESIAN_POINT('Ctrl Pts',(-226.246526925527,4.51762863693335,
132.753468557892));
#131442=CARTESIAN_POINT('Ctrl Pts',(-226.254287368041,4.57019357631639,
132.626790805566));
#131443=CARTESIAN_POINT('Ctrl Pts',(-226.262047810555,4.61733949216553,
132.49827887905));
#131444=CARTESIAN_POINT('Ctrl Pts',(-226.26982071082,4.66456109082433,132.36956065378));
#131445=CARTESIAN_POINT('Ctrl Pts',(-226.277593611086,4.70634616313795,
132.239002743085));
#131446=CARTESIAN_POINT('Ctrl Pts',(-226.285366511351,4.74257684787682,
132.10710691078));
#131447=CARTESIAN_POINT('Ctrl Pts',(-226.292856847114,4.77749045597035,
131.980005824189));
#131448=CARTESIAN_POINT('Ctrl Pts',(-226.300347182877,4.80724642776265,
131.851662700875));
#131449=CARTESIAN_POINT('Ctrl Pts',(-226.30783751864,4.83178475869705,131.722532229043));
#131450=CARTESIAN_POINT('Ctrl Pts',(-226.315611852759,4.85725346790459,
131.588505736137));
#131451=CARTESIAN_POINT('Ctrl Pts',(-226.323386186878,4.87718174943586,
131.453206455842));
#131452=CARTESIAN_POINT('Ctrl Pts',(-226.331160520997,4.89144644614283,
131.317132230486));
#131453=CARTESIAN_POINT('Ctrl Pts',(-226.338925273945,4.90569356288602,
131.181225704451));
#131454=CARTESIAN_POINT('Ctrl Pts',(-226.346690026892,4.9142909422798,131.044546518723));
#131455=CARTESIAN_POINT('Ctrl Pts',(-226.354454779839,4.91716625495979,
130.9076034555));
#131456=CARTESIAN_POINT('Ctrl Pts',(-226.362211820724,4.92003871183869,
130.770796406058));
#131457=CARTESIAN_POINT('Ctrl Pts',(-226.36996886161,4.91720040374859,130.633726389037));
#131458=CARTESIAN_POINT('Ctrl Pts',(-226.377725902495,4.90863074354596,
130.496907717083));
#131459=CARTESIAN_POINT('Ctrl Pts',(-226.385477093735,4.90006754579078,
130.360192221155));
#131460=CARTESIAN_POINT('Ctrl Pts',(-226.393228284975,4.88578162305726,
130.223728081646));
#131461=CARTESIAN_POINT('Ctrl Pts',(-226.400979476215,4.86580445850655,
130.088029664669));
#131462=CARTESIAN_POINT('Ctrl Pts',(-226.408727372993,4.84583578478367,
129.95238892314));
#131463=CARTESIAN_POINT('Ctrl Pts',(-226.41647526977,4.82018073713402,129.81751364283));
#131464=CARTESIAN_POINT('Ctrl Pts',(-226.424223166547,4.78892263189044,
129.683912899791));
#131465=CARTESIAN_POINT('Ctrl Pts',(-226.431969442631,4.75767106516864,
129.550340103147));
#131466=CARTESIAN_POINT('Ctrl Pts',(-226.439715718716,4.72081886111349,
129.418041693925));
#131467=CARTESIAN_POINT('Ctrl Pts',(-226.4474619948,4.67850034249818,129.287515995416));
#131468=CARTESIAN_POINT('Ctrl Pts',(-226.455208328065,4.63618151149724,
129.156989333396));
#131469=CARTESIAN_POINT('Ctrl Pts',(-226.462954661331,4.5883964059966,129.028235780108));
#131470=CARTESIAN_POINT('Ctrl Pts',(-226.470700994596,4.53532893901277,
128.90173756571));
#131471=CARTESIAN_POINT('Ctrl Pts',(-226.478449062599,4.48224958793759,
128.775211022914));
#131472=CARTESIAN_POINT('Ctrl Pts',(-226.486197130603,4.42388567266496,
128.650941184491));
#131473=CARTESIAN_POINT('Ctrl Pts',(-226.493945198606,4.36046870766976,
128.529389032703));
#131474=CARTESIAN_POINT('Ctrl Pts',(-226.501701501348,4.29698434236941,
128.407707693842));
#131475=CARTESIAN_POINT('Ctrl Pts',(-226.50945780409,4.22843638044344,128.288750158662));
#131476=CARTESIAN_POINT('Ctrl Pts',(-226.517214106832,4.15510193023349,
128.172952057143));
#131477=CARTESIAN_POINT('Ctrl Pts',(-226.524974549346,4.08172833921941,
128.057092150689));
#131478=CARTESIAN_POINT('Ctrl Pts',(-226.53273499186,4.00356339218927,127.94439535906));
#131479=CARTESIAN_POINT('Ctrl Pts',(-226.540495434375,3.92092618787832,
127.835266329452));
#131480=CARTESIAN_POINT('Ctrl Pts',(-226.54826833464,3.83815632699083,127.725962116238));
#131481=CARTESIAN_POINT('Ctrl Pts',(-226.556041234906,3.75090011136795,
127.6202374117));
#131482=CARTESIAN_POINT('Ctrl Pts',(-226.563814135171,3.65951598224535,
127.518462591426));
#131483=CARTESIAN_POINT('Ctrl Pts',(-226.571304470932,3.57145389641489,
127.420387542242));
#131484=CARTESIAN_POINT('Ctrl Pts',(-226.578794806693,3.47955902151275,
127.325980407362));
#131485=CARTESIAN_POINT('Ctrl Pts',(-226.586285142454,3.3841814656734,127.235537440398));
#131486=CARTESIAN_POINT('Ctrl Pts',(-226.594059476573,3.28518764079927,
127.141665300837));
#131487=CARTESIAN_POINT('Ctrl Pts',(-226.601833810692,3.18212824735688,
127.05176650732));
#131488=CARTESIAN_POINT('Ctrl Pts',(-226.609608144811,3.07535556474875,
126.966213771382));
#131489=CARTESIAN_POINT('Ctrl Pts',(-226.617372897758,2.96871446992938,
126.880766471546));
#131490=CARTESIAN_POINT('Ctrl Pts',(-226.625137650705,2.85836949358723,
126.799654814312));
#131491=CARTESIAN_POINT('Ctrl Pts',(-226.632902403652,2.74470959280777,
126.72321466163));
#131492=CARTESIAN_POINT('Ctrl Pts',(-226.640659444537,2.6311625806444,126.646850430386));
#131493=CARTESIAN_POINT('Ctrl Pts',(-226.648416485422,2.51430751844954,
126.575148687048));
#131494=CARTESIAN_POINT('Ctrl Pts',(-226.656173526307,2.39456598416612,
126.50840475071));
#131495=CARTESIAN_POINT('Ctrl Pts',(-226.663924717547,2.27491474790499,
126.441711146494));
#131496=CARTESIAN_POINT('Ctrl Pts',(-226.671675908788,2.15238171228218,
126.379968097162));
#131497=CARTESIAN_POINT('Ctrl Pts',(-226.679427100028,2.02741664549414,
126.323427142488));
#131498=CARTESIAN_POINT('Ctrl Pts',(-226.687174996805,1.90250469219253,
126.266910219228));
#131499=CARTESIAN_POINT('Ctrl Pts',(-226.694922893582,1.77516311908862,
126.215591153885));
#131500=CARTESIAN_POINT('Ctrl Pts',(-226.702670790359,1.64586526079623,
126.16967501811));
#131501=CARTESIAN_POINT('Ctrl Pts',(-226.710417066443,1.51659444882881,
126.123768487001));
#131502=CARTESIAN_POINT('Ctrl Pts',(-226.718163342527,1.38536853380987,
126.083262768229));
#131503=CARTESIAN_POINT('Ctrl Pts',(-226.725909618612,1.25267937397761,
126.048314208151));
#131504=CARTESIAN_POINT('Ctrl Pts',(-226.733655951877,1.11998923466429,
126.013365390091));
#131505=CARTESIAN_POINT('Ctrl Pts',(-226.741402285142,0.98583620705556,
125.98397391216));
#131506=CARTESIAN_POINT('Ctrl Pts',(-226.749148618408,0.850725414519564,
125.960245700309));
#131507=CARTESIAN_POINT('Ctrl Pts',(-226.756896686411,0.71558436485782,
125.93651217469));
#131508=CARTESIAN_POINT('Ctrl Pts',(-226.764644754414,0.579485508467145,
125.918444506433));
#131509=CARTESIAN_POINT('Ctrl Pts',(-226.772392822417,0.442941822008387,
125.906097088027));
#131510=CARTESIAN_POINT('Ctrl Pts',(-226.780149125159,0.306253015294957,
125.893736546637));
#131511=CARTESIAN_POINT('Ctrl Pts',(-226.787905427901,0.169118824100376,
125.88710843492));
#131512=CARTESIAN_POINT('Ctrl Pts',(-226.795661730643,0.0320555400893031,
125.886215082423));
#131513=CARTESIAN_POINT('Ctrl Pts',(-226.803422173157,-0.105080898722969,
125.885321253116));
#131514=CARTESIAN_POINT('Ctrl Pts',(-226.811182615671,-0.242145964411954,
125.89016826815));
#131515=CARTESIAN_POINT('Ctrl Pts',(-226.818943058185,-0.378626735169176,
125.900706382415));
#131516=CARTESIAN_POINT('Ctrl Pts',(-226.82671595845,-0.515326596976182,
125.911261413396));
#131517=CARTESIAN_POINT('Ctrl Pts',(-226.834488858716,-0.65143990107724,
125.92752575355));
#131518=CARTESIAN_POINT('Ctrl Pts',(-226.842261758982,-0.786461293756218,
125.949398033166));
#131519=CARTESIAN_POINT('Ctrl Pts',(-226.849752094743,-0.916574318704911,
125.970475200324));
#131520=CARTESIAN_POINT('Ctrl Pts',(-226.857242430505,-1.04567313958366,
125.996759598753));
#131521=CARTESIAN_POINT('Ctrl Pts',(-226.864732766266,-1.1733192678386,
126.02811680488));
#131522=CARTESIAN_POINT('Ctrl Pts',(-226.872507100385,-1.30580513785045,
126.06066292901));
#131523=CARTESIAN_POINT('Ctrl Pts',(-226.880281434504,-1.43714565842267,
126.09877722171));
#131524=CARTESIAN_POINT('Ctrl Pts',(-226.888055768624,-1.56683684116329,
126.142364760031));
#131525=CARTESIAN_POINT('Ctrl Pts',(-226.895820521571,-1.69636819111237,
126.185898580607));
#131526=CARTESIAN_POINT('Ctrl Pts',(-226.903585274518,-1.82425388058314,
126.234892102338));
#131527=CARTESIAN_POINT('Ctrl Pts',(-226.911350027465,-1.95000109860021,
126.289199626199));
#131528=CARTESIAN_POINT('Ctrl Pts',(-226.91910706835,-2.07562342270729,
126.343453211063));
#131529=CARTESIAN_POINT('Ctrl Pts',(-226.926864109235,-2.19911114553693,
126.403010140707));
#131530=CARTESIAN_POINT('Ctrl Pts',(-226.93462115012,-2.31998793359411,
126.467675356854));
#131531=CARTESIAN_POINT('Ctrl Pts',(-226.94237234136,-2.44077356752529,
126.532291808458));
#131532=CARTESIAN_POINT('Ctrl Pts',(-226.9501235326,-2.55895184237208,126.602008695321));
#131533=CARTESIAN_POINT('Ctrl Pts',(-226.95787472384,-2.67406801990288,
126.676583578113));
#131534=CARTESIAN_POINT('Ctrl Pts',(-226.965622620617,-2.78913526998725,
126.751126764591));
#131535=CARTESIAN_POINT('Ctrl Pts',(-226.973370517394,-2.90114268384491,
126.830523628187));
#131536=CARTESIAN_POINT('Ctrl Pts',(-226.981118414171,-3.00966187996747,
126.914486785323));
#131537=CARTESIAN_POINT('Ctrl Pts',(-226.988864690255,-3.1181583762136,
126.998432379176));
#131538=CARTESIAN_POINT('Ctrl Pts',(-226.996610966339,-3.22316779703744,
127.086942127588));
#131539=CARTESIAN_POINT('Ctrl Pts',(-227.004357242424,-3.32429274242802,
127.179686725319));
#131540=CARTESIAN_POINT('Ctrl Pts',(-227.012103575689,-3.42541843429956,
127.272432007668));
#131541=CARTESIAN_POINT('Ctrl Pts',(-227.019849908954,-3.52265930538509,
127.369411937457));
#131542=CARTESIAN_POINT('Ctrl Pts',(-227.027596242219,-3.61565320566346,
127.470258795654));
#131543=CARTESIAN_POINT('Ctrl Pts',(-227.035344310222,-3.7086679312814,
127.571128237806));
#131544=CARTESIAN_POINT('Ctrl Pts',(-227.043092378225,-3.79743352856755,
127.675866044187));
#131545=CARTESIAN_POINT('Ctrl Pts',(-227.050840446228,-3.88162695916609,
127.784070033471));
#131546=CARTESIAN_POINT('Ctrl Pts',(-227.05859674897,-3.96590987154448,
127.892389023242));
#131547=CARTESIAN_POINT('Ctrl Pts',(-227.066353051712,-4.04561066967987,
128.004181245852));
#131548=CARTESIAN_POINT('Ctrl Pts',(-227.074109354454,-4.1204483254021,
128.119013589677));
#131549=CARTESIAN_POINT('Ctrl Pts',(-227.081869796968,-4.1953259242345,
128.233907222982));
#131550=CARTESIAN_POINT('Ctrl Pts',(-227.089630239482,-4.26533500921803,
128.351843874651));
#131551=CARTESIAN_POINT('Ctrl Pts',(-227.097390681996,-4.3302401855553,
128.472365120593));
#131552=CARTESIAN_POINT('Ctrl Pts',(-227.105163582262,-4.39524955344365,
128.593079837938));
#131553=CARTESIAN_POINT('Ctrl Pts',(-227.112936482527,-4.45513846906175,
128.716387088739));
#131554=CARTESIAN_POINT('Ctrl Pts',(-227.120709382793,-4.5097190615902,
128.841806911796));
#131555=CARTESIAN_POINT('Ctrl Pts',(-227.128199718555,-4.56231551210254,
128.962667408378));
#131556=CARTESIAN_POINT('Ctrl Pts',(-227.135690054317,-4.60998276939513,
129.085489262049));
#131557=CARTESIAN_POINT('Ctrl Pts',(-227.14318039008,-4.65259691405446,
129.209830900743));
#131558=CARTESIAN_POINT('Ctrl Pts',(-227.150566054377,-4.69461556004669,
129.332434964257));
#131559=CARTESIAN_POINT('Ctrl Pts',(-227.157951718674,-4.73181060005727,
129.456771532717));
#131560=CARTESIAN_POINT('Ctrl Pts',(-227.165337382971,-4.76405452823413,
129.582490119309));
#131561=CARTESIAN_POINT('Ctrl Pts',(-225.41504623153,-4.76405452823393,
129.582490119308));
#131562=CARTESIAN_POINT('Ctrl Pts',(-225.422809306179,-4.79810736338305,
129.71526160673));
#131563=CARTESIAN_POINT('Ctrl Pts',(-225.430572380828,-4.82657411435382,
129.84933482539));
#131564=CARTESIAN_POINT('Ctrl Pts',(-225.438335455478,-4.84938342871073,
129.984200008999));
#131565=CARTESIAN_POINT('Ctrl Pts',(-225.446109886893,-4.87222611129406,
130.119262489725));
#131566=CARTESIAN_POINT('Ctrl Pts',(-225.453884318307,-4.88939478205187,
130.25511886208));
#131567=CARTESIAN_POINT('Ctrl Pts',(-225.461658749722,-4.90087002073647,
130.391255180242));
#131568=CARTESIAN_POINT('Ctrl Pts',(-225.465270715548,-4.90620136495505,
130.454503500623));
#131569=CARTESIAN_POINT('Ctrl Pts',(-225.468882681374,-4.91030452498705,
130.517812256196));
#131570=CARTESIAN_POINT('Ctrl Pts',(-225.472494647201,-4.9131813736671,
130.581130126928));
#131571=CARTESIAN_POINT('Ctrl Pts',(-225.476709952805,-4.91653876876631,
130.655024562308));
#131572=CARTESIAN_POINT('Ctrl Pts',(-225.480925258409,-4.91822920859789,
130.728995310251));
#131573=CARTESIAN_POINT('Ctrl Pts',(-225.485140564013,-4.91824980939616,
130.802991356954));
#131574=CARTESIAN_POINT('',(-225.13985943604,-4.91824793997955,130.80886210475));
#131575=CARTESIAN_POINT('Ctrl Pts',(-225.069870156977,-4.76405452823403,
129.582490119308));
#131576=CARTESIAN_POINT('Ctrl Pts',(-225.077538742587,-4.79782267774008,
129.714151621729));
#131577=CARTESIAN_POINT('Ctrl Pts',(-225.085207328198,-4.82612779473598,
129.847210760949));
#131578=CARTESIAN_POINT('Ctrl Pts',(-225.092875913808,-4.84886999374076,
129.981169967534));
#131579=CARTESIAN_POINT('Ctrl Pts',(-225.100706500839,-4.87209262926181,
130.117959106902));
#131580=CARTESIAN_POINT('Ctrl Pts',(-225.108537087871,-4.88951458321308,
130.255686342715));
#131581=CARTESIAN_POINT('Ctrl Pts',(-225.116367674902,-4.90108507640122,
130.393814473537));
#131582=CARTESIAN_POINT('Ctrl Pts',(-225.124198261933,-4.91265556958939,
130.531942604359));
#131583=CARTESIAN_POINT('Ctrl Pts',(-225.132028848965,-4.9183746039543,
130.670471187608));
#131584=CARTESIAN_POINT('Ctrl Pts',(-225.139859435996,-4.91824793998026,
130.808862103977));
#131585=CARTESIAN_POINT('Ctrl Pts',(-225.13985943604,-4.91824793997955,
130.80886210475));
#131586=CARTESIAN_POINT('Ctrl Pts',(-225.149605429622,-4.91809029324308,
130.981104233894));
#131587=CARTESIAN_POINT('Ctrl Pts',(-225.159351423203,-4.90888095054794,
131.15294170875));
#131588=CARTESIAN_POINT('Ctrl Pts',(-225.169097416785,-4.89076858680166,
131.323557779398));
#131589=CARTESIAN_POINT('Ctrl Pts',(-225.179027880941,-4.8723133951939,
131.497403243152));
#131590=CARTESIAN_POINT('Ctrl Pts',(-225.188958345097,-4.84461498244356,
131.669980793286));
#131591=CARTESIAN_POINT('Ctrl Pts',(-225.198888809253,-4.80787897277174,
131.840450790128));
#131592=CARTESIAN_POINT('Ctrl Pts',(-225.203804546018,-4.7896940671611,
131.92483613382));
#131593=CARTESIAN_POINT('Ctrl Pts',(-225.208720282783,-4.76929531813874,
132.008705397411));
#131594=CARTESIAN_POINT('Ctrl Pts',(-225.213636019548,-4.74671194523966,
132.091958680402));
#131595=CARTESIAN_POINT('Ctrl Pts',(-225.221410353667,-4.71099589801225,
132.223625380519));
#131596=CARTESIAN_POINT('Ctrl Pts',(-225.229184687787,-4.66974077093761,
132.354013440337));
#131597=CARTESIAN_POINT('Ctrl Pts',(-225.236959021906,-4.62305355396191,
132.482621294487));
#131598=CARTESIAN_POINT('Ctrl Pts',(-225.244723774853,-4.57642387480845,
132.611070650952));
#131599=CARTESIAN_POINT('Ctrl Pts',(-225.2524885278,-4.52437555807236,132.737743803074));
#131600=CARTESIAN_POINT('Ctrl Pts',(-225.260253280747,-4.46706608692499,
132.86215157817));
#131601=CARTESIAN_POINT('Ctrl Pts',(-225.268010321632,-4.40981353635229,
132.98643578971));
#131602=CARTESIAN_POINT('Ctrl Pts',(-225.275767362517,-4.34731039277597,
133.108458749034));
#131603=CARTESIAN_POINT('Ctrl Pts',(-225.283524403403,-4.27976308899272,
133.227748940678));
#131604=CARTESIAN_POINT('Ctrl Pts',(-225.291275594643,-4.21226672315697,
133.34694917466));
#131605=CARTESIAN_POINT('Ctrl Pts',(-225.299026785883,-4.13973396029038,
133.46342040403));
#131606=CARTESIAN_POINT('Ctrl Pts',(-225.306777977123,-4.06241808237026,
133.576713839385));
#131607=CARTESIAN_POINT('Ctrl Pts',(-225.3145258739,-3.98513506576062,133.689959122008));
#131608=CARTESIAN_POINT('Ctrl Pts',(-225.322273770677,-3.90307319740353,
133.800028974693));
#131609=CARTESIAN_POINT('Ctrl Pts',(-225.330021667455,-3.81653005809438,
133.90650203571));
#131610=CARTESIAN_POINT('Ctrl Pts',(-225.337767943539,-3.73000502174408,
134.012952824857));
#131611=CARTESIAN_POINT('Ctrl Pts',(-225.345514219623,-3.63900082539391,
134.115808015649));
#131612=CARTESIAN_POINT('Ctrl Pts',(-225.353260495707,-3.54385621595714,
134.214678224934));
#131613=CARTESIAN_POINT('Ctrl Pts',(-225.361006828973,-3.44871090418461,
134.313549164056));
#131614=CARTESIAN_POINT('Ctrl Pts',(-225.368753162238,-3.34942538943357,
134.408434781261));
#131615=CARTESIAN_POINT('Ctrl Pts',(-225.376499495504,-3.2463759754437,
134.498981855063));
#131616=CARTESIAN_POINT('Ctrl Pts',(-225.384247563507,-3.14330348425193,
134.589549206254));
#131617=CARTESIAN_POINT('Ctrl Pts',(-225.39199563151,-3.036465710189,134.675775822682));
#131618=CARTESIAN_POINT('Ctrl Pts',(-225.399743699513,-2.92627247079122,
134.75734841026));
#131619=CARTESIAN_POINT('Ctrl Pts',(-225.407500002255,-2.81596211670714,
134.839007694156));
#131620=CARTESIAN_POINT('Ctrl Pts',(-225.415256304996,-2.70228948809756,
134.916002835333));
#131621=CARTESIAN_POINT('Ctrl Pts',(-225.423012607738,-2.58569431576058,
134.988063280034));
#131622=CARTESIAN_POINT('Ctrl Pts',(-225.430773050253,-2.46903691306952,
135.060162185565));
#131623=CARTESIAN_POINT('Ctrl Pts',(-225.438533492767,-2.34945419923728,
135.127320955208));
#131624=CARTESIAN_POINT('Ctrl Pts',(-225.446293935281,-2.22741011516574,
135.189315262868));
#131625=CARTESIAN_POINT('Ctrl Pts',(-225.454066835547,-2.10517011509589,
135.251409089295));
#131626=CARTESIAN_POINT('Ctrl Pts',(-225.461839735812,-1.98046120489236,
135.30832172436));
#131627=CARTESIAN_POINT('Ctrl Pts',(-225.469612636078,-1.85376771591805,
135.359876869092));
#131628=CARTESIAN_POINT('Ctrl Pts',(-225.477102971839,-1.731679854404,135.409557854448));
#131629=CARTESIAN_POINT('Ctrl Pts',(-225.4845933076,-1.60774948767011,135.454263998909));
#131630=CARTESIAN_POINT('Ctrl Pts',(-225.492083643361,-1.48242103434339,
135.493882015261));
#131631=CARTESIAN_POINT('Ctrl Pts',(-225.49985797748,-1.35234071460227,
135.535002160748));
#131632=CARTESIAN_POINT('Ctrl Pts',(-225.507632311599,-1.22034214320157,
135.57077098517));
#131633=CARTESIAN_POINT('Ctrl Pts',(-225.515406645719,-1.08690513196861,
135.601007393867));
#131634=CARTESIAN_POINT('Ctrl Pts',(-225.523171398666,-0.953632569926398,
135.631206538893));
#131635=CARTESIAN_POINT('Ctrl Pts',(-225.530936151613,-0.818925472931342,
135.655886748823));
#131636=CARTESIAN_POINT('Ctrl Pts',(-225.53870090456,-0.683280519316704,
135.674916108927));
#131637=CARTESIAN_POINT('Ctrl Pts',(-225.546457945445,-0.547770290182254,
135.693926568801));
#131638=CARTESIAN_POINT('Ctrl Pts',(-225.55421498633,-0.411324442808616,
135.70729729402));
#131639=CARTESIAN_POINT('Ctrl Pts',(-225.561972027215,-0.274451258476907,
135.714947096717));
#131640=CARTESIAN_POINT('Ctrl Pts',(-225.569723218455,-0.137681291278408,
135.722591130638));
#131641=CARTESIAN_POINT('Ctrl Pts',(-225.577474409695,-0.000485017333626381,
135.724522807447));
#131642=CARTESIAN_POINT('Ctrl Pts',(-225.585225600935,0.136623079027003,
135.720712638809));
#131643=CARTESIAN_POINT('Ctrl Pts',(-225.592973497712,0.273672900789388,
135.716904089594));
#131644=CARTESIAN_POINT('Ctrl Pts',(-225.600721394489,0.410634229512033,
135.707358559615));
#131645=CARTESIAN_POINT('Ctrl Pts',(-225.608469291266,0.546991711947881,
135.692098655714));
#131646=CARTESIAN_POINT('Ctrl Pts',(-225.616215567351,0.683320671337931,
135.676841943856));
#131647=CARTESIAN_POINT('Ctrl Pts',(-225.623961843435,0.819045647388365,
135.655873279096));
#131648=CARTESIAN_POINT('Ctrl Pts',(-225.631708119519,0.953655940044716,
135.629267187699));
#131649=CARTESIAN_POINT('Ctrl Pts',(-225.639454452784,1.08826722636385,
135.602660899903));
#131650=CARTESIAN_POINT('Ctrl Pts',(-225.647200786049,1.22176342932477,
135.570417178242));
#131651=CARTESIAN_POINT('Ctrl Pts',(-225.654947119315,1.35364397232283,
135.532661692867));
#131652=CARTESIAN_POINT('Ctrl Pts',(-225.662695187318,1.48555404905392,
135.494897752413));
#131653=CARTESIAN_POINT('Ctrl Pts',(-225.670443255321,1.61584737005681,
135.451619699674));
#131654=CARTESIAN_POINT('Ctrl Pts',(-225.678191323324,1.7440388357554,135.403002982643));
#131655=CARTESIAN_POINT('Ctrl Pts',(-225.685947626066,1.87236654486941,
135.354334595186));
#131656=CARTESIAN_POINT('Ctrl Pts',(-225.693703928808,1.99858757012791,
135.300316347879));
#131657=CARTESIAN_POINT('Ctrl Pts',(-225.701460231549,2.12223660175588,
135.241171957782));
#131658=CARTESIAN_POINT('Ctrl Pts',(-225.709220674064,2.24595162859504,
135.181996000543));
#131659=CARTESIAN_POINT('Ctrl Pts',(-225.716981116578,2.36709158132668,
135.117688632075));
#131660=CARTESIAN_POINT('Ctrl Pts',(-225.724741559092,2.48521695666374,
135.048518925265));
#131661=CARTESIAN_POINT('Ctrl Pts',(-225.732514459357,2.60353195733997,
134.979238181101));
#131662=CARTESIAN_POINT('Ctrl Pts',(-225.740287359623,2.71882238121892,
134.90507971243));
#131663=CARTESIAN_POINT('Ctrl Pts',(-225.748060259888,2.83067811005041,
134.826355707044));
#131664=CARTESIAN_POINT('Ctrl Pts',(-225.75555059565,2.9384676013916,134.750493517547));
#131665=CARTESIAN_POINT('Ctrl Pts',(-225.763040931412,3.04306753726984,
134.670392153204));
#131666=CARTESIAN_POINT('Ctrl Pts',(-225.770531267175,3.14414238681853,
134.586364281487));
#131667=CARTESIAN_POINT('Ctrl Pts',(-225.778305601294,3.24904952000846,
134.499150467474));
#131668=CARTESIAN_POINT('Ctrl Pts',(-225.786079935412,3.35049129710711,
134.407430254263));
#131669=CARTESIAN_POINT('Ctrl Pts',(-225.793854269532,3.44805600803517,
134.311509435046));
#131670=CARTESIAN_POINT('Ctrl Pts',(-225.801619022479,3.54550047917662,
134.215706829666));
#131671=CARTESIAN_POINT('Ctrl Pts',(-225.809383775426,3.63907711510054,
134.115714190176));
#131672=CARTESIAN_POINT('Ctrl Pts',(-225.817148528373,3.7284064654359,134.011878082989));
#131673=CARTESIAN_POINT('Ctrl Pts',(-225.824905569258,3.81764709260095,
133.908145107288));
#131674=CARTESIAN_POINT('Ctrl Pts',(-225.832662610143,3.90264857578659,
133.800576555125));
#131675=CARTESIAN_POINT('Ctrl Pts',(-225.840419651028,3.98306787089368,
133.689556173911));
#131676=CARTESIAN_POINT('Ctrl Pts',(-225.848170842268,4.06342652118486,
133.578619514031));
#131677=CARTESIAN_POINT('Ctrl Pts',(-225.855922033508,4.13920963286425,
133.464236521659));
#131678=CARTESIAN_POINT('Ctrl Pts',(-225.863673224748,4.21011430521399,
133.346824107871));
#131679=CARTESIAN_POINT('Ctrl Pts',(-225.871421121525,4.28098884118663,
133.22946159749));
#131680=CARTESIAN_POINT('Ctrl Pts',(-225.879169018302,4.34698886011281,
133.109072560573));
#131681=CARTESIAN_POINT('Ctrl Pts',(-225.88691691508,4.40785482075141,132.986102797953));
#131682=CARTESIAN_POINT('Ctrl Pts',(-225.894663191164,4.46870804954317,
132.863158757956));
#131683=CARTESIAN_POINT('Ctrl Pts',(-225.902409467248,4.52442918283877,
132.737635416182));
#131684=CARTESIAN_POINT('Ctrl Pts',(-225.910155743332,4.5748048758435,132.610002722319));
#131685=CARTESIAN_POINT('Ctrl Pts',(-225.917902076597,4.62518094071009,
132.482369086301));
#131686=CARTESIAN_POINT('Ctrl Pts',(-225.925648409863,4.67021134301315,
132.352626430787));
#131687=CARTESIAN_POINT('Ctrl Pts',(-225.933394743128,4.70973123872821,
132.221263832838));
#131688=CARTESIAN_POINT('Ctrl Pts',(-225.941142811131,4.74925998464985,
132.089871817146));
#131689=CARTESIAN_POINT('Ctrl Pts',(-225.948890879134,4.78327565577531,
131.956859511457));
#131690=CARTESIAN_POINT('Ctrl Pts',(-225.956638947137,4.81166365330068,
131.822729877709));
#131691=CARTESIAN_POINT('Ctrl Pts',(-225.964395249878,4.84008182192769,
131.688457689391));
#131692=CARTESIAN_POINT('Ctrl Pts',(-225.97215155262,4.86286028786421,131.553066183937));
#131693=CARTESIAN_POINT('Ctrl Pts',(-225.979907855362,4.87993575930992,
131.417067764177));
#131694=CARTESIAN_POINT('Ctrl Pts',(-225.987668297876,4.89702034444886,
131.280996757965));
#131695=CARTESIAN_POINT('Ctrl Pts',(-225.99542874039,4.90839583753709,131.144318581419));
#131696=CARTESIAN_POINT('Ctrl Pts',(-226.003189182905,4.91405105495221,
131.007548441569));
#131697=CARTESIAN_POINT('Ctrl Pts',(-226.01096208317,4.91971535062437,130.870558746149));
#131698=CARTESIAN_POINT('Ctrl Pts',(-226.018734983435,4.91964102088623,
130.733477183607));
#131699=CARTESIAN_POINT('Ctrl Pts',(-226.026507883701,4.91386903923685,
130.596817543171));
#131700=CARTESIAN_POINT('Ctrl Pts',(-226.033998219463,4.90830688365904,
130.465125824886));
#131701=CARTESIAN_POINT('Ctrl Pts',(-226.041488555225,4.89745415758686,
130.333826192394));
#131702=CARTESIAN_POINT('Ctrl Pts',(-226.048978890987,4.88139255438909,
130.203369941719));
#131703=CARTESIAN_POINT('Ctrl Pts',(-226.056753225106,4.8647219706246,130.067967402652));
#131704=CARTESIAN_POINT('Ctrl Pts',(-226.064527559225,4.8423869159738,129.933044546967));
#131705=CARTESIAN_POINT('Ctrl Pts',(-226.072301893345,4.81442212355511,
129.799113046704));
#131706=CARTESIAN_POINT('Ctrl Pts',(-226.080066646292,4.7864917952438,129.665346605046));
#131707=CARTESIAN_POINT('Ctrl Pts',(-226.087831399239,4.75294561315524,
129.532569466915));
#131708=CARTESIAN_POINT('Ctrl Pts',(-226.095596152186,4.71387005123443,
129.401288202266));
#131709=CARTESIAN_POINT('Ctrl Pts',(-226.103353193071,4.67483329971259,
129.270137328021));
#131710=CARTESIAN_POINT('Ctrl Pts',(-226.111110233956,4.63027820821611,
129.140479742897));
#131711=CARTESIAN_POINT('Ctrl Pts',(-226.118867274841,4.58034221059627,
129.012811484461));
#131712=CARTESIAN_POINT('Ctrl Pts',(-226.126618466081,4.53044387010061,
128.885239501651));
#131713=CARTESIAN_POINT('Ctrl Pts',(-226.134369657321,4.47517284209181,
128.759654222169));
#131714=CARTESIAN_POINT('Ctrl Pts',(-226.142120848561,4.41471616042677,
128.636535835586));
#131715=CARTESIAN_POINT('Ctrl Pts',(-226.149868745338,4.35428517446425,
128.513469777602));
#131716=CARTESIAN_POINT('Ctrl Pts',(-226.157616642115,4.28867309048085,
128.392868877342));
#131717=CARTESIAN_POINT('Ctrl Pts',(-226.165364538892,4.21811468496269,
128.275192460444));
#131718=CARTESIAN_POINT('Ctrl Pts',(-226.173110814977,4.1475710387419,128.157540658915));
#131719=CARTESIAN_POINT('Ctrl Pts',(-226.180857091061,4.07208332991259,
128.042812459062));
#131720=CARTESIAN_POINT('Ctrl Pts',(-226.188603367145,3.99193162238366,
127.931441373189));
#131721=CARTESIAN_POINT('Ctrl Pts',(-226.19634970041,3.91177932319293,127.820069465199));
#131722=CARTESIAN_POINT('Ctrl Pts',(-226.204096033676,3.82696318497908,
127.712055037968));
#131723=CARTESIAN_POINT('Ctrl Pts',(-226.211842366941,3.73780557990322,
127.60780113754));
#131724=CARTESIAN_POINT('Ctrl Pts',(-226.219590434944,3.6486280086,127.503523890174));
#131725=CARTESIAN_POINT('Ctrl Pts',(-226.227338502947,3.55510728984161,
127.403009142451));
#131726=CARTESIAN_POINT('Ctrl Pts',(-226.23508657095,3.45760463629866,127.306625172804));
#131727=CARTESIAN_POINT('Ctrl Pts',(-226.242842873692,3.35999835577536,
127.210138765127));
#131728=CARTESIAN_POINT('Ctrl Pts',(-226.250599176433,3.25840196498437,
127.117792180796));
#131729=CARTESIAN_POINT('Ctrl Pts',(-226.258355479175,3.15321235217255,
127.02991563524));
#131730=CARTESIAN_POINT('Ctrl Pts',(-226.266115921689,3.04796659649689,
126.941992187325));
#131731=CARTESIAN_POINT('Ctrl Pts',(-226.273876364204,2.93912410751723,
126.858543769846));
#131732=CARTESIAN_POINT('Ctrl Pts',(-226.281636806718,2.8271122984785,126.779858273885));
#131733=CARTESIAN_POINT('Ctrl Pts',(-226.289409706983,2.71492067813996,
126.701046464981));
#131734=CARTESIAN_POINT('Ctrl Pts',(-226.297182607249,2.59954990018272,
126.627013067738));
#131735=CARTESIAN_POINT('Ctrl Pts',(-226.304955507514,2.48145437721108,
126.558001325617));
#131736=CARTESIAN_POINT('Ctrl Pts',(-226.312445843276,2.3676519239638,126.491498334153));
#131737=CARTESIAN_POINT('Ctrl Pts',(-226.319936179038,2.25131966101654,
126.42965838143));
#131738=CARTESIAN_POINT('Ctrl Pts',(-226.3274265148,2.13288143375845,126.372656673029));
#131739=CARTESIAN_POINT('Ctrl Pts',(-226.335200848919,2.00995258511587,
126.313493727529));
#131740=CARTESIAN_POINT('Ctrl Pts',(-226.342975183039,1.88436552281168,
126.259355742396));
#131741=CARTESIAN_POINT('Ctrl Pts',(-226.350749517158,1.75656950512303,
126.210490066911));
#131742=CARTESIAN_POINT('Ctrl Pts',(-226.358514270105,1.62893098460473,
126.161684614004));
#131743=CARTESIAN_POINT('Ctrl Pts',(-226.366279023052,1.49908928702106,
126.118138680651));
#131744=CARTESIAN_POINT('Ctrl Pts',(-226.374043775999,1.36751734530206,
126.080053327307));
#131745=CARTESIAN_POINT('Ctrl Pts',(-226.381800816884,1.23607608269007,
126.042005800872));
#131746=CARTESIAN_POINT('Ctrl Pts',(-226.389557857769,1.102908368959,126.009408169392));
#131747=CARTESIAN_POINT('Ctrl Pts',(-226.397314898654,0.968505820915303,
125.982412926295));
#131748=CARTESIAN_POINT('Ctrl Pts',(-226.405066089894,0.834204626878764,
125.955438040521));
#131749=CARTESIAN_POINT('Ctrl Pts',(-226.412817281134,0.69867083378196,
125.934057210591));
#131750=CARTESIAN_POINT('Ctrl Pts',(-226.420568472374,0.562409535079179,
125.918372633816));
#131751=CARTESIAN_POINT('Ctrl Pts',(-226.428316369152,0.42620615106305,
125.902694723404));
#131752=CARTESIAN_POINT('Ctrl Pts',(-226.436064265929,0.2892762640221,125.892708295459));
#131753=CARTESIAN_POINT('Ctrl Pts',(-226.443812162706,0.152133220048413,
125.8884641026));
#131754=CARTESIAN_POINT('Ctrl Pts',(-226.45155843879,0.0150188634430627,
125.884220797534));
#131755=CARTESIAN_POINT('Ctrl Pts',(-226.459304714874,-0.122308170876832,
125.885717350483));
#131756=CARTESIAN_POINT('Ctrl Pts',(-226.467050990958,-0.259331775349145,
125.892952459736));
#131757=CARTESIAN_POINT('Ctrl Pts',(-226.474797324223,-0.396356391298392,
125.900187622398));
#131758=CARTESIAN_POINT('Ctrl Pts',(-226.482543657489,-0.533077182509269,
125.913161405278));
#131759=CARTESIAN_POINT('Ctrl Pts',(-226.490289990754,-0.668980804902403,
125.931820443779));
#131760=CARTESIAN_POINT('Ctrl Pts',(-226.498038058757,-0.804914861969297,
125.950483660841));
#131761=CARTESIAN_POINT('Ctrl Pts',(-226.50578612676,-0.940030998813575,
125.974834613824));
#131762=CARTESIAN_POINT('Ctrl Pts',(-226.513534194763,-1.07382412808817,
126.004768467765));
#131763=CARTESIAN_POINT('Ctrl Pts',(-226.521290497505,-1.20775945429291,
126.034734135762));
#131764=CARTESIAN_POINT('Ctrl Pts',(-226.529046800247,-1.34036858193426,
126.070294472172));
#131765=CARTESIAN_POINT('Ctrl Pts',(-226.536803102989,-1.47115916362795,
126.111294053178));
#131766=CARTESIAN_POINT('Ctrl Pts',(-226.544563545503,-1.60201955219313,
126.152315516896));
#131767=CARTESIAN_POINT('Ctrl Pts',(-226.552323988017,-1.73105909311937,
126.198781877465));
#131768=CARTESIAN_POINT('Ctrl Pts',(-226.560084430531,-1.85780454818622,
126.250489152182));
#131769=CARTESIAN_POINT('Ctrl Pts',(-226.567857330797,-1.98475346630948,
126.302279432006));
#131770=CARTESIAN_POINT('Ctrl Pts',(-226.575630231062,-2.10940058371873,
126.359327275396));
#131771=CARTESIAN_POINT('Ctrl Pts',(-226.583403131327,-2.23129563168847,
126.421381851189));
#131772=CARTESIAN_POINT('Ctrl Pts',(-226.590893467089,-2.34875948762841,
126.481180586846));
#131773=CARTESIAN_POINT('Ctrl Pts',(-226.598383802851,-2.463667620948,126.545628209392));
#131774=CARTESIAN_POINT('Ctrl Pts',(-226.605874138613,-2.57564352744432,
126.614462828594));
#131775=CARTESIAN_POINT('Ctrl Pts',(-226.61364978905,-2.69188471260912,
126.685919429989));
#131776=CARTESIAN_POINT('Ctrl Pts',(-226.621425439487,-2.80533413994567,
126.7623302542));
#131777=CARTESIAN_POINT('Ctrl Pts',(-226.629201089924,-2.91554064523804,
126.843450897759));
#131778=CARTESIAN_POINT('Ctrl Pts',(-226.637141305583,-3.0280795802354,
126.92628839277));
#131779=CARTESIAN_POINT('Ctrl Pts',(-226.645081521242,-3.13723639965859,
127.014037165253));
#131780=CARTESIAN_POINT('Ctrl Pts',(-226.653021736901,-3.24255719969909,
127.106387406579));
#131781=CARTESIAN_POINT('Ctrl Pts',(-226.660777899543,-3.34543667926793,
127.196596983053));
#131782=CARTESIAN_POINT('Ctrl Pts',(-226.668534062185,-3.4446556925028,
127.291196790052));
#131783=CARTESIAN_POINT('Ctrl Pts',(-226.676290224826,-3.53982107198123,
127.38985482011));
#131784=CARTESIAN_POINT('Ctrl Pts',(-226.684041040951,-3.63492085157508,
127.488444842713));
#131785=CARTESIAN_POINT('Ctrl Pts',(-226.691791857075,-3.72597228670709,
127.59108724237));
#131786=CARTESIAN_POINT('Ctrl Pts',(-226.699542673199,-3.8126172577398,
127.697411517808));
#131787=CARTESIAN_POINT('Ctrl Pts',(-226.707289825123,-3.89922126734433,
127.803685528423));
#131788=CARTESIAN_POINT('Ctrl Pts',(-226.715036977048,-3.9814227124175,
127.913637648249));
#131789=CARTESIAN_POINT('Ctrl Pts',(-226.722784128972,-4.05890242207442,
128.02686278848));
#131790=CARTESIAN_POINT('Ctrl Pts',(-226.730865973703,-4.13972941364076,
128.144979486323));
#131791=CARTESIAN_POINT('Ctrl Pts',(-226.738947818434,-4.21541727253825,
128.266657995164));
#131792=CARTESIAN_POINT('Ctrl Pts',(-226.747029663165,-4.28565263699557,
128.391402984802));
#131793=CARTESIAN_POINT('Ctrl Pts',(-226.754776314275,-4.35297499744343,
128.510974189727));
#131794=CARTESIAN_POINT('Ctrl Pts',(-226.762522965385,-4.41528789834733,
128.633362234604));
#131795=CARTESIAN_POINT('Ctrl Pts',(-226.770269616496,-4.47236181691145,
128.758104807279));
#131796=CARTESIAN_POINT('Ctrl Pts',(-226.778017331852,-4.52944357637199,
128.882864517268));
#131797=CARTESIAN_POINT('Ctrl Pts',(-226.785765047208,-4.5812847650445,
129.009979040522));
#131798=CARTESIAN_POINT('Ctrl Pts',(-226.793512762565,-4.62770382906203,
129.138965669518));
#131799=CARTESIAN_POINT('Ctrl Pts',(-226.801265156259,-4.67415092251131,
129.268030185089));
#131800=CARTESIAN_POINT('Ctrl Pts',(-226.809017549953,-4.71516923349835,
129.398968691975));
#131801=CARTESIAN_POINT('Ctrl Pts',(-226.816769943647,-4.7506269304247,
129.531282917493));
#131802=CARTESIAN_POINT('Ctrl Pts',(-226.817768717679,-4.75519509715136,
129.548329524996));
#131803=CARTESIAN_POINT('Ctrl Pts',(-226.818767491711,-4.7596710365228,
129.565398951655));
#131804=CARTESIAN_POINT('Ctrl Pts',(-226.819766265743,-4.76405452823404,
129.582490119308));
#131805=CARTESIAN_POINT('Origin',(213.235140564004,0.,130.804360617566));
#131806=CARTESIAN_POINT('',(-228.915319603984,-4.76405452823406,129.582490119308));
#131807=CARTESIAN_POINT('',(-228.570020432611,-4.76405452823418,129.582490119309));
#131808=CARTESIAN_POINT('',(213.235140564004,-4.76405452823405,129.582490119308));
#131809=CARTESIAN_POINT('',(-227.235140563962,-4.91824846444471,130.800474168388));
#131810=CARTESIAN_POINT('Ctrl Pts',(-227.235140564014,-4.91824846444543,
130.800474169299));
#131811=CARTESIAN_POINT('Ctrl Pts',(-227.242910874425,-4.91835720842715,
130.938088228303));
#131812=CARTESIAN_POINT('Ctrl Pts',(-227.250681184837,-4.9126858626062,
131.075774149936));
#131813=CARTESIAN_POINT('Ctrl Pts',(-227.258451495249,-4.9012435845361,
131.213010085379));
#131814=CARTESIAN_POINT('Ctrl Pts',(-227.266187743251,-4.88985146553826,
131.349644424954));
#131815=CARTESIAN_POINT('Ctrl Pts',(-227.273923991253,-4.87273895711793,
131.485832323658));
#131816=CARTESIAN_POINT('Ctrl Pts',(-227.281660239255,-4.84996723784876,
131.621061820145));
#131817=CARTESIAN_POINT('Ctrl Pts',(-227.289396802041,-4.82719459200822,
131.756296819061));
#131818=CARTESIAN_POINT('Ctrl Pts',(-227.297133364828,-4.79876234172717,
131.890572951961));
#131819=CARTESIAN_POINT('Ctrl Pts',(-227.304869927615,-4.76478305287311,
132.023387082231));
#131820=CARTESIAN_POINT('Ctrl Pts',(-227.312608486423,-4.73079499741358,
132.156235478347));
#131821=CARTESIAN_POINT('Ctrl Pts',(-227.320347045231,-4.69125715245796,
132.287620741974));
#131822=CARTESIAN_POINT('Ctrl Pts',(-227.328085604039,-4.64633223752828,
132.417053955124));
#131823=CARTESIAN_POINT('Ctrl Pts',(-227.33588080486,-4.60107849682236,
132.547434548517));
#131824=CARTESIAN_POINT('Ctrl Pts',(-227.343676005681,-4.55035863971752,
132.675834019239));
#131825=CARTESIAN_POINT('Ctrl Pts',(-227.351471206502,-4.4943882496115,
132.801773275044));
#131826=CARTESIAN_POINT('Ctrl Pts',(-227.359222925504,-4.43873006370029,
132.927010038623));
#131827=CARTESIAN_POINT('Ctrl Pts',(-227.366974644506,-4.37788000325017,
133.049813640815));
#131828=CARTESIAN_POINT('Ctrl Pts',(-227.374726363507,-4.31209581913861,
133.169738538548));
#131829=CARTESIAN_POINT('Ctrl Pts',(-227.382543305238,-4.24575812889225,
133.290672480741));
#131830=CARTESIAN_POINT('Ctrl Pts',(-227.390360246969,-4.17440312209688,
133.408678710674));
#131831=CARTESIAN_POINT('Ctrl Pts',(-227.3981771887,-4.0983386554529,133.523331622877));
#131832=CARTESIAN_POINT('Ctrl Pts',(-227.405994130431,-4.02227418880913,
133.637984535079));
#131833=CARTESIAN_POINT('Ctrl Pts',(-227.413811072162,-3.94150054956011,
133.749283842464));
#131834=CARTESIAN_POINT('Ctrl Pts',(-227.421628013892,-3.85636528823487,
133.856839909256));
#131835=CARTESIAN_POINT('Ctrl Pts',(-227.429402348011,-3.77169407158126,
133.963809722845));
#131836=CARTESIAN_POINT('Ctrl Pts',(-227.43717668213,-3.68243459447034,
134.067423319435));
#131837=CARTESIAN_POINT('Ctrl Pts',(-227.44495101625,-3.58888268212647,
134.167261769315));
#131838=CARTESIAN_POINT('Ctrl Pts',(-227.452715769197,-3.4954460641536,
134.266977177228));
#131839=CARTESIAN_POINT('Ctrl Pts',(-227.460480522144,-3.39772780131615,
134.362926413031));
#131840=CARTESIAN_POINT('Ctrl Pts',(-227.468245275091,-3.29606525446265,
134.454721818985));
#131841=CARTESIAN_POINT('Ctrl Pts',(-227.476002315976,-3.19450368028387,
134.546426052448));
#131842=CARTESIAN_POINT('Ctrl Pts',(-227.483759356861,-3.08900590642713,
134.633984405959));
#131843=CARTESIAN_POINT('Ctrl Pts',(-227.491516397746,-2.97994733768238,
134.717044725329));
#131844=CARTESIAN_POINT('Ctrl Pts',(-227.499267588986,-2.87097101085252,
134.800042408265));
#131845=CARTESIAN_POINT('Ctrl Pts',(-227.507018780226,-2.75843954367994,
134.878548572709));
#131846=CARTESIAN_POINT('Ctrl Pts',(-227.514769971466,-2.64276245839599,
134.952250400455));
#131847=CARTESIAN_POINT('Ctrl Pts',(-227.522517868243,-2.52713453895924,
135.025920902957));
#131848=CARTESIAN_POINT('Ctrl Pts',(-227.53026576502,-2.40836398958257,
135.094790920445));
#131849=CARTESIAN_POINT('Ctrl Pts',(-227.538013661797,-2.28689025444527,
135.158590288429));
#131850=CARTESIAN_POINT('Ctrl Pts',(-227.545759937882,-2.1654419289947,
135.22237631096));
#131851=CARTESIAN_POINT('Ctrl Pts',(-227.553506213966,-2.04129188840132,
135.281093612043));
#131852=CARTESIAN_POINT('Ctrl Pts',(-227.56125249005,-1.91490482733184,
135.334517630823));
#131853=CARTESIAN_POINT('Ctrl Pts',(-227.568998823315,-1.78851683330196,
135.387942043967));
#131854=CARTESIAN_POINT('Ctrl Pts',(-227.576745156581,-1.65989214595977,
135.436072944619));
#131855=CARTESIAN_POINT('Ctrl Pts',(-227.584491489846,-1.52951574572216,
135.478733799725));
#131856=CARTESIAN_POINT('Ctrl Pts',(-227.592239557849,-1.39911014859386,
135.521404208433));
#131857=CARTESIAN_POINT('Ctrl Pts',(-227.599987625852,-1.26695242947814,
135.558602012467));
#131858=CARTESIAN_POINT('Ctrl Pts',(-227.607735693855,-1.13354265541742,
135.590200576324));
#131859=CARTESIAN_POINT('Ctrl Pts',(-227.615491996597,-0.999991091861054,
135.621832723511));
#131860=CARTESIAN_POINT('Ctrl Pts',(-227.623248299339,-0.865185196191498,
135.647853652628));
#131861=CARTESIAN_POINT('Ctrl Pts',(-227.63100460208,-0.729635704848385,
135.668187793845));
#131862=CARTESIAN_POINT('Ctrl Pts',(-227.638765044595,-0.594013866660427,
135.688532788006));
#131863=CARTESIAN_POINT('Ctrl Pts',(-227.646525487109,-0.457648030520637,
135.703184904607));
#131864=CARTESIAN_POINT('Ctrl Pts',(-227.654285929623,-0.321052986716322,
135.712120599698));
#131865=CARTESIAN_POINT('Ctrl Pts',(-227.662058829889,-0.184238668420982,
135.721070639161));
#131866=CARTESIAN_POINT('Ctrl Pts',(-227.669831730154,-0.0471947982733746,
135.724285910354));
#131867=CARTESIAN_POINT('Ctrl Pts',(-227.677604630419,0.0895639992079477,
135.721795045451));
#131868=CARTESIAN_POINT('Ctrl Pts',(-227.685094966181,0.221351269923615,
135.719394729761));
#131869=CARTESIAN_POINT('Ctrl Pts',(-227.692585301943,0.352873526862216,
135.711695958153));
#131870=CARTESIAN_POINT('Ctrl Pts',(-227.700075637705,0.483677643544477,
135.69876957061));
#131871=CARTESIAN_POINT('Ctrl Pts',(-227.707849971824,0.619441238069909,
135.685353075154));
#131872=CARTESIAN_POINT('Ctrl Pts',(-227.715624305943,0.75486121903268,
135.66626222896));
#131873=CARTESIAN_POINT('Ctrl Pts',(-227.723398640062,0.889425228243008,
135.641519476428));
#131874=CARTESIAN_POINT('Ctrl Pts',(-227.731163393009,1.02382339933795,
135.616807217127));
#131875=CARTESIAN_POINT('Ctrl Pts',(-227.738928145956,1.15736731680661,
135.586456980718));
#131876=CARTESIAN_POINT('Ctrl Pts',(-227.746692898903,1.28954848143668,
135.550543059964));
#131877=CARTESIAN_POINT('Ctrl Pts',(-227.754449939788,1.4215983618706,135.514664809422));
#131878=CARTESIAN_POINT('Ctrl Pts',(-227.762206980673,1.55228780815694,
135.473233973229));
#131879=CARTESIAN_POINT('Ctrl Pts',(-227.769964021558,1.68111762754279,
135.426376042125));
#131880=CARTESIAN_POINT('Ctrl Pts',(-227.777715212799,1.80985029535952,
135.379553446952));
#131881=CARTESIAN_POINT('Ctrl Pts',(-227.785466404039,1.93672576165647,
135.327312036066));
#131882=CARTESIAN_POINT('Ctrl Pts',(-227.793217595279,2.06125948684816,
135.269827266235));
#131883=CARTESIAN_POINT('Ctrl Pts',(-227.800965492056,2.18574028188509,
135.212366928965));
#131884=CARTESIAN_POINT('Ctrl Pts',(-227.808713388833,2.30788096116836,
135.149667828715));
#131885=CARTESIAN_POINT('Ctrl Pts',(-227.81646128561,2.42721669734777,135.08195365181));
#131886=CARTESIAN_POINT('Ctrl Pts',(-227.824207561694,2.54652747106343,
135.014253639252));
#131887=CARTESIAN_POINT('Ctrl Pts',(-227.831953837778,2.6630341288984,134.941540829475));
#131888=CARTESIAN_POINT('Ctrl Pts',(-227.839700113862,2.7762965626287,134.864084802635));
#131889=CARTESIAN_POINT('Ctrl Pts',(-227.847446447127,2.88955983243672,
134.786628204033));
#131890=CARTESIAN_POINT('Ctrl Pts',(-227.855192780393,2.99957850763467,
134.704428539197));
#131891=CARTESIAN_POINT('Ctrl Pts',(-227.862939113658,3.10594192220258,
134.61779841546));
#131892=CARTESIAN_POINT('Ctrl Pts',(-227.870687181661,3.21232915611956,
134.531148891507));
#131893=CARTESIAN_POINT('Ctrl Pts',(-227.878435249664,3.31505919746381,
134.440067181202));
#131894=CARTESIAN_POINT('Ctrl Pts',(-227.886183317667,3.41375520574974,
134.344905555526));
#131895=CARTESIAN_POINT('Ctrl Pts',(-227.893939620409,3.51255610932791,
134.249642790943));
#131896=CARTESIAN_POINT('Ctrl Pts',(-227.901695923151,3.60731413337136,
134.150291720799));
#131897=CARTESIAN_POINT('Ctrl Pts',(-227.909452225892,3.69768963332176,
134.047241194788));
#131898=CARTESIAN_POINT('Ctrl Pts',(-227.917212668407,3.78811336939789,
133.944135667609));
#131899=CARTESIAN_POINT('Ctrl Pts',(-227.924973110921,3.87414967541873,
133.837327054504));
#131900=CARTESIAN_POINT('Ctrl Pts',(-227.932733553435,3.95550048646769,
133.727235737042));
#131901=CARTESIAN_POINT('Ctrl Pts',(-227.9405064537,4.03698188906032,133.616967691225));
#131902=CARTESIAN_POINT('Ctrl Pts',(-227.948279353966,4.11376254707328,
133.503406734603));
#131903=CARTESIAN_POINT('Ctrl Pts',(-227.956052254231,4.18558838244359,
133.38700131175));
#131904=CARTESIAN_POINT('Ctrl Pts',(-227.963542589993,4.25480316778177,
133.274827519221));
#131905=CARTESIAN_POINT('Ctrl Pts',(-227.971032925756,4.31941696567561,
133.160012745443));
#131906=CARTESIAN_POINT('Ctrl Pts',(-227.978523261518,4.37924444987864,
133.042976509296));
#131907=CARTESIAN_POINT('Ctrl Pts',(-227.986297595637,4.44134031132791,
132.921502808687));
#131908=CARTESIAN_POINT('Ctrl Pts',(-227.994071929756,4.49847644927214,
132.797251074722));
#131909=CARTESIAN_POINT('Ctrl Pts',(-228.001846263875,4.55039480470242,
132.670664500603));
#131910=CARTESIAN_POINT('Ctrl Pts',(-228.009611016822,4.60224917539944,
132.544233933123));
#131911=CARTESIAN_POINT('Ctrl Pts',(-228.017375769769,4.64889841132926,
132.415474609072));
#131912=CARTESIAN_POINT('Ctrl Pts',(-228.025140522716,4.69013016085034,
132.28485450029));
#131913=CARTESIAN_POINT('Ctrl Pts',(-228.032897563601,4.73132095841674,
132.15436412524));
#131914=CARTESIAN_POINT('Ctrl Pts',(-228.040654604486,4.76710486053068,
132.022017013794));
#131915=CARTESIAN_POINT('Ctrl Pts',(-228.048411645371,4.7973176202293,131.888300981764));
#131916=CARTESIAN_POINT('Ctrl Pts',(-228.056162836611,4.82750759625084,
131.754685786033));
#131917=CARTESIAN_POINT('Ctrl Pts',(-228.063914027851,4.85213470635737,
131.619704104285));
#131918=CARTESIAN_POINT('Ctrl Pts',(-228.071665219092,4.87108466181725,
131.483858432065));
#131919=CARTESIAN_POINT('Ctrl Pts',(-228.079413115869,4.89002656304048,
131.34807049788));
#131920=CARTESIAN_POINT('Ctrl Pts',(-228.087161012646,4.90329605487305,
131.211419689999));
#131921=CARTESIAN_POINT('Ctrl Pts',(-228.094908909423,4.91083008042062,
131.07441798876));
#131922=CARTESIAN_POINT('Ctrl Pts',(-228.102655185507,4.91836253001247,
130.937444945323));
#131923=CARTESIAN_POINT('Ctrl Pts',(-228.110401461591,4.92016187820577,
130.800121544652));
#131924=CARTESIAN_POINT('Ctrl Pts',(-228.118147737675,4.91621704117659,
130.662963776919));
#131925=CARTESIAN_POINT('Ctrl Pts',(-228.125894070941,4.91227217502753,
130.52580499672));
#131926=CARTESIAN_POINT('Ctrl Pts',(-228.133640404206,4.90258305028537,
130.388812242702));
#131927=CARTESIAN_POINT('Ctrl Pts',(-228.141386737471,4.88719069733727,
130.252499991719));
#131928=CARTESIAN_POINT('Ctrl Pts',(-228.149134805474,4.87179489737851,
130.116157214553));
#131929=CARTESIAN_POINT('Ctrl Pts',(-228.156882873477,4.8506933715974,129.98049563209));
#131930=CARTESIAN_POINT('Ctrl Pts',(-228.16463094148,4.82397880406177,129.846022701973));
#131931=CARTESIAN_POINT('Ctrl Pts',(-228.172387244222,4.79723584396575,
129.711406852426));
#131932=CARTESIAN_POINT('Ctrl Pts',(-228.180143546964,4.76486800147383,
129.577982562913));
#131933=CARTESIAN_POINT('Ctrl Pts',(-228.187899849706,4.72701884066552,
129.44624576878));
#131934=CARTESIAN_POINT('Ctrl Pts',(-228.19566029222,4.68914947862057,129.314438662753));
#131935=CARTESIAN_POINT('Ctrl Pts',(-228.203420734734,4.64579309239619,
129.184321217495));
#131936=CARTESIAN_POINT('Ctrl Pts',(-228.211181177248,4.59714224954354,
129.056371429967));
#131937=CARTESIAN_POINT('Ctrl Pts',(-228.218954077513,4.54841330803879,
128.928216246082));
#131938=CARTESIAN_POINT('Ctrl Pts',(-228.226726977779,4.49437308014699,
128.802236033019));
#131939=CARTESIAN_POINT('Ctrl Pts',(-228.234499878044,4.43526151958818,
128.678886949096));
#131940=CARTESIAN_POINT('Ctrl Pts',(-228.241990213806,4.37829881314889,
128.560021915071));
#131941=CARTESIAN_POINT('Ctrl Pts',(-228.249480549568,4.31662722828887,
128.443600307214));
#131942=CARTESIAN_POINT('Ctrl Pts',(-228.25697088533,4.25049954476134,128.330004805949));
#131943=CARTESIAN_POINT('Ctrl Pts',(-228.264745219449,4.18186461001331,
128.212102296725));
#131944=CARTESIAN_POINT('Ctrl Pts',(-228.272519553568,4.10821158542302,
128.096870948468));
#131945=CARTESIAN_POINT('Ctrl Pts',(-228.280293887688,4.02977385478476,
127.984767430279));
#131946=CARTESIAN_POINT('Ctrl Pts',(-228.288058640635,3.95143279163954,
127.872802069659));
#131947=CARTESIAN_POINT('Ctrl Pts',(-228.295823393582,3.86831897715227,
127.763957186524));
#131948=CARTESIAN_POINT('Ctrl Pts',(-228.303588146529,3.78071134803678,
127.658664388537));
#131949=CARTESIAN_POINT('Ctrl Pts',(-228.311345187414,3.69319073205381,
127.553476168842));
#131950=CARTESIAN_POINT('Ctrl Pts',(-228.319102228299,3.60118543209285,
127.451833312047));
#131951=CARTESIAN_POINT('Ctrl Pts',(-228.326859269184,3.50501708191603,
127.354137680135));
#131952=CARTESIAN_POINT('Ctrl Pts',(-228.334610460424,3.40892125304029,
127.256515721259));
#131953=CARTESIAN_POINT('Ctrl Pts',(-228.342361651664,3.30866889586918,
127.162835339955));
#131954=CARTESIAN_POINT('Ctrl Pts',(-228.350112842904,3.20462099828599,
127.073464301686));
#131955=CARTESIAN_POINT('Ctrl Pts',(-228.357860739681,3.10061732383441,
126.984131248493));
#131956=CARTESIAN_POINT('Ctrl Pts',(-228.365608636458,2.99282161347258,
126.899104149661));
#131957=CARTESIAN_POINT('Ctrl Pts',(-228.373356533235,2.88163052696741,
126.818712794621));
#131958=CARTESIAN_POINT('Ctrl Pts',(-228.38110280932,2.77046269924055,126.738338255719));
#131959=CARTESIAN_POINT('Ctrl Pts',(-228.388849085404,2.65590122470499,
126.66259776075));
#131960=CARTESIAN_POINT('Ctrl Pts',(-228.396595361488,2.5383742294296,126.591779540142));
#131961=CARTESIAN_POINT('Ctrl Pts',(-228.404341694753,2.42084636659648,
126.52096079677));
#131962=CARTESIAN_POINT('Ctrl Pts',(-228.412088028019,2.30035327421165,
126.455064602046));
#131963=CARTESIAN_POINT('Ctrl Pts',(-228.419834361284,2.17734997414808,
126.394334523247));
#131964=CARTESIAN_POINT('Ctrl Pts',(-228.427582429287,2.0543191283488,126.333590844368));
#131965=CARTESIAN_POINT('Ctrl Pts',(-228.43533049729,1.92877730676809,126.278015756594));
#131966=CARTESIAN_POINT('Ctrl Pts',(-228.443078565293,1.80120154589672,
126.227805575445));
#131967=CARTESIAN_POINT('Ctrl Pts',(-228.450834868035,1.67349019598835,
126.177542030319));
#131968=CARTESIAN_POINT('Ctrl Pts',(-228.458591170777,1.54374095295396,
126.132654925362));
#131969=CARTESIAN_POINT('Ctrl Pts',(-228.466347473518,1.41244866113536,
126.093291541214));
#131970=CARTESIAN_POINT('Ctrl Pts',(-228.474107916033,1.28108629466748,
126.053907147644));
#131971=CARTESIAN_POINT('Ctrl Pts',(-228.481868358547,1.14817961706084,
126.020052445834));
#131972=CARTESIAN_POINT('Ctrl Pts',(-228.489628801061,1.01423486816231,
125.991823792283));
#131973=CARTESIAN_POINT('Ctrl Pts',(-228.497401701326,0.880075099261423,
125.963549823592));
#131974=CARTESIAN_POINT('Ctrl Pts',(-228.505174601592,0.744874314885049,
125.940920015418));
#131975=CARTESIAN_POINT('Ctrl Pts',(-228.512947501857,0.609145994789944,
125.923979052613));
#131976=CARTESIAN_POINT('Ctrl Pts',(-228.520437837619,0.47835174101187,
125.907653936478));
#131977=CARTESIAN_POINT('Ctrl Pts',(-228.527928173381,0.347067947063592,
125.896611264649));
#131978=CARTESIAN_POINT('Ctrl Pts',(-228.535418509143,0.215753206453727,
125.890845214476));
#131979=CARTESIAN_POINT('Ctrl Pts',(-228.543192843262,0.0794596275388981,
125.884860542758));
#131980=CARTESIAN_POINT('Ctrl Pts',(-228.550967177381,-0.0572990281376561,
125.884541559892));
#131981=CARTESIAN_POINT('Ctrl Pts',(-228.5587415115,-0.194012402284007,
125.889938754288));
#131982=CARTESIAN_POINT('Ctrl Pts',(-228.566506264448,-0.330557289414035,
125.895329297125));
#131983=CARTESIAN_POINT('Ctrl Pts',(-228.574271017395,-0.467056619139458,
125.906421985141));
#131984=CARTESIAN_POINT('Ctrl Pts',(-228.582035770342,-0.602996495604233,
125.923215435461));
#131985=CARTESIAN_POINT('Ctrl Pts',(-228.589792811227,-0.738801354667286,
125.939992206289));
#131986=CARTESIAN_POINT('Ctrl Pts',(-228.597549852112,-0.874047480747141,
125.962458424009));
#131987=CARTESIAN_POINT('Ctrl Pts',(-228.605306892997,-1.00822292507135,
125.990560705245));
#131988=CARTESIAN_POINT('Ctrl Pts',(-228.613058084237,-1.14229718664944,
126.018641794332));
#131989=CARTESIAN_POINT('Ctrl Pts',(-228.620809275477,-1.27530199245758,
126.052350407349));
#131990=CARTESIAN_POINT('Ctrl Pts',(-228.628560466717,-1.40673280822708,
126.091581621182));
#131991=CARTESIAN_POINT('Ctrl Pts',(-228.636308363494,-1.53810776239401,
126.130796160703));
#131992=CARTESIAN_POINT('Ctrl Pts',(-228.644056260271,-1.6679096832405,
126.175528520942));
#131993=CARTESIAN_POINT('Ctrl Pts',(-228.651804157048,-1.79564670528629,
126.225623240046));
#131994=CARTESIAN_POINT('Ctrl Pts',(-228.659550433132,-1.92335700750075,
126.275707480416));
#131995=CARTESIAN_POINT('Ctrl Pts',(-228.667296709216,-2.04900290630574,
126.331151705897));
#131996=CARTESIAN_POINT('Ctrl Pts',(-228.675042985301,-2.17211049268177,
126.391751517489));
#131997=CARTESIAN_POINT('Ctrl Pts',(-228.682789318566,-2.29521898781021,
126.452351776416));
#131998=CARTESIAN_POINT('Ctrl Pts',(-228.690535651831,-2.41578878235045,
126.518107524728));
#131999=CARTESIAN_POINT('Ctrl Pts',(-228.698281985097,-2.53336900581594,
126.5887675937));
#132000=CARTESIAN_POINT('Ctrl Pts',(-228.7060300531,-2.65097556055739,126.659443486504));
#132001=CARTESIAN_POINT('Ctrl Pts',(-228.713778121103,-2.76559087696416,
126.73502568409));
#132002=CARTESIAN_POINT('Ctrl Pts',(-228.721526189106,-2.87679193935304,
126.815218955482));
#132003=CARTESIAN_POINT('Ctrl Pts',(-228.729282491847,-2.98811118755449,
126.895497457237));
#132004=CARTESIAN_POINT('Ctrl Pts',(-228.737038794589,-3.09600861538586,
126.980396593434));
#132005=CARTESIAN_POINT('Ctrl Pts',(-228.744795097331,-3.2000928360187,
127.069579646296));
#132006=CARTESIAN_POINT('Ctrl Pts',(-228.752555539845,-3.30423260953428,
127.158810298839));
#132007=CARTESIAN_POINT('Ctrl Pts',(-228.76031598236,-3.40455483465514,
127.252329157547));
#132008=CARTESIAN_POINT('Ctrl Pts',(-228.768076424874,-3.5007048089268,
127.349762391541));
#132009=CARTESIAN_POINT('Ctrl Pts',(-228.775849325139,-3.59700913167244,
127.447352034011));
#132010=CARTESIAN_POINT('Ctrl Pts',(-228.783622225405,-3.68912755661647,
127.54886831891));
#132011=CARTESIAN_POINT('Ctrl Pts',(-228.79139512567,-3.77674494077698,
127.653903394429));
#132012=CARTESIAN_POINT('Ctrl Pts',(-228.798885461432,-3.86117721233052,
127.755120180388));
#132013=CARTESIAN_POINT('Ctrl Pts',(-228.806375797194,-3.94142982230247,
127.859604120536));
#132014=CARTESIAN_POINT('Ctrl Pts',(-228.813866132957,-4.01725978845964,
127.96696623988));
#132015=CARTESIAN_POINT('Ctrl Pts',(-228.821726616999,-4.09683702743094,
128.07963384954));
#132016=CARTESIAN_POINT('Ctrl Pts',(-228.829587101042,-4.17179334796039,
128.195824948763));
#132017=CARTESIAN_POINT('Ctrl Pts',(-228.837447585084,-4.24180480278559,
128.315128792772));
#132018=CARTESIAN_POINT('Ctrl Pts',(-228.845294526829,-4.31169563959784,
128.434227096236));
#132019=CARTESIAN_POINT('Ctrl Pts',(-228.853141468574,-4.37665839146968,
128.556427136261));
#132020=CARTESIAN_POINT('Ctrl Pts',(-228.860988410319,-4.43641119637584,
128.681287665647));
#132021=CARTESIAN_POINT('Ctrl Pts',(-228.868827498221,-4.49610419592812,
128.806023224696));
#132022=CARTESIAN_POINT('Ctrl Pts',(-228.876666586123,-4.55059746044838,
128.933413634851));
#132023=CARTESIAN_POINT('Ctrl Pts',(-228.884505674025,-4.59965375729813,
129.062990933819));
#132024=CARTESIAN_POINT('Ctrl Pts',(-228.892336934124,-4.64866106846908,
129.192438842018));
#132025=CARTESIAN_POINT('Ctrl Pts',(-228.900168194223,-4.69224209171157,
129.324068935704));
#132026=CARTESIAN_POINT('Ctrl Pts',(-228.907999454322,-4.73020690944459,
129.457391554691));
#132027=CARTESIAN_POINT('Ctrl Pts',(-228.910439504209,-4.74203591883365,
129.49893197569));
#132028=CARTESIAN_POINT('Ctrl Pts',(-228.912879554097,-4.75332005219438,
129.540636560148));
#132029=CARTESIAN_POINT('Ctrl Pts',(-228.915319603984,-4.76405452823406,
129.582490119308));
#132030=CARTESIAN_POINT('Ctrl Pts',(-227.165337382971,-4.76405452823413,
129.582490119309));
#132031=CARTESIAN_POINT('Ctrl Pts',(-227.174468718987,-4.80391961427429,
129.737923484742));
#132032=CARTESIAN_POINT('Ctrl Pts',(-227.183600055004,-4.83621507933807,
129.895469963794));
#132033=CARTESIAN_POINT('Ctrl Pts',(-227.19273139102,-4.86074207082464,
130.054447566996));
#132034=CARTESIAN_POINT('Ctrl Pts',(-227.20178028834,-4.88504762996015,
130.211989903077));
#132035=CARTESIAN_POINT('Ctrl Pts',(-227.21082918566,-4.90172428360133,
130.370937546404));
#132036=CARTESIAN_POINT('Ctrl Pts',(-227.219878082981,-4.91062540018657,
130.530606637609));
#132037=CARTESIAN_POINT('Ctrl Pts',(-227.224965576641,-4.91562980819314,
130.620376193009));
#132038=CARTESIAN_POINT('Ctrl Pts',(-227.230053070302,-4.91817726594451,
130.710373436795));
#132039=CARTESIAN_POINT('Ctrl Pts',(-227.235140563963,-4.91824846444471,
130.800474168387));
#132040=CARTESIAN_POINT('',(-226.889859436047,-4.91824996233216,130.803751914262));
#132041=CARTESIAN_POINT('Ctrl Pts',(-226.819766265743,-4.76405452823404,
129.582490119308));
#132042=CARTESIAN_POINT('Ctrl Pts',(-226.827527686226,-4.79811841182178,
129.715304684425));
#132043=CARTESIAN_POINT('Ctrl Pts',(-226.83528910671,-4.82659534922294,
129.849432617361));
#132044=CARTESIAN_POINT('Ctrl Pts',(-226.843050527193,-4.84941119093025,
129.984364176244));
#132045=CARTESIAN_POINT('Ctrl Pts',(-226.850823967339,-4.87226236620946,
130.119504695813));
#132046=CARTESIAN_POINT('Ctrl Pts',(-226.858597407484,-4.88943488249307,
130.255450939986));
#132047=CARTESIAN_POINT('Ctrl Pts',(-226.86637084763,-4.90090651786403,
130.391688392116));
#132048=CARTESIAN_POINT('Ctrl Pts',(-226.872354485895,-4.90973685746664,
130.496557744218));
#132049=CARTESIAN_POINT('Ctrl Pts',(-226.87833812416,-4.91519036663282,
130.601599545051));
#132050=CARTESIAN_POINT('Ctrl Pts',(-226.884321762425,-4.91727791410797,
130.706580364314));
#132051=CARTESIAN_POINT('Ctrl Pts',(-226.886167653615,-4.91792190114796,
130.738965873079));
#132052=CARTESIAN_POINT('Ctrl Pts',(-226.888013544806,-4.91824595309002,
130.771357764929));
#132053=CARTESIAN_POINT('Ctrl Pts',(-226.889859435996,-4.91824996233205,
130.803751913359));
#132054=CARTESIAN_POINT('Ctrl Pts',(-226.889859436047,-4.91824996233216,
130.803751914262));
#132055=CARTESIAN_POINT('Ctrl Pts',(-226.897607212581,-4.91826679033664,
130.939720179568));
#132056=CARTESIAN_POINT('Ctrl Pts',(-226.905354989115,-4.91264094686343,
131.075910932816));
#132057=CARTESIAN_POINT('Ctrl Pts',(-226.913102765649,-4.90134307196643,
131.211815097707));
#132058=CARTESIAN_POINT('Ctrl Pts',(-226.920841019478,-4.89005908316085,
131.347552224311));
#132059=CARTESIAN_POINT('Ctrl Pts',(-226.928579273306,-4.87311696449167,
131.483003074584));
#132060=CARTESIAN_POINT('Ctrl Pts',(-226.936317527135,-4.85053933090291,
131.617657157497));
#132061=CARTESIAN_POINT('Ctrl Pts',(-226.94404815453,-4.82798394869374,
131.752178532122));
#132062=CARTESIAN_POINT('Ctrl Pts',(-226.951778781925,-4.7998041677737,
131.885904315899));
#132063=CARTESIAN_POINT('Ctrl Pts',(-226.95950940932,-4.76607447969522,
132.018328128045));
#132064=CARTESIAN_POINT('Ctrl Pts',(-226.967234299652,-4.73236982313674,
132.150653665659));
#132065=CARTESIAN_POINT('Ctrl Pts',(-226.974959189984,-4.69312355336305,
132.281678774401));
#132066=CARTESIAN_POINT('Ctrl Pts',(-226.982684080315,-4.64846134277032,
132.410906666477));
#132067=CARTESIAN_POINT('Ctrl Pts',(-226.990405848413,-4.60381718368202,
132.540082327419));
#132068=CARTESIAN_POINT('Ctrl Pts',(-226.99812761651,-4.55376156498401,
132.667461844523));
#132069=CARTESIAN_POINT('Ctrl Pts',(-227.005849384607,-4.49847010713594,
132.792563262596));
#132070=CARTESIAN_POINT('Ctrl Pts',(-227.013569683712,-4.44318916795728,
132.917640881324));
#132071=CARTESIAN_POINT('Ctrl Pts',(-227.021289982817,-4.38267452978856,
133.040440902818));
#132072=CARTESIAN_POINT('Ctrl Pts',(-227.029010281922,-4.31714991344633,
133.160501463808));
#132073=CARTESIAN_POINT('Ctrl Pts',(-227.036730814151,-4.25162331850994,
133.28056565017));
#132074=CARTESIAN_POINT('Ctrl Pts',(-227.04445134638,-4.1810866330653,133.397889865601));
#132075=CARTESIAN_POINT('Ctrl Pts',(-227.052171878608,-4.10580926808051,
133.512037355407));
#132076=CARTESIAN_POINT('Ctrl Pts',(-227.059894345895,-4.03051303573446,
133.626213454901));
#132077=CARTESIAN_POINT('Ctrl Pts',(-227.067616813182,-3.95047397675962,
133.737210915949));
#132078=CARTESIAN_POINT('Ctrl Pts',(-227.075339280468,-3.86600424669483,
133.844622814653));
#132079=CARTESIAN_POINT('Ctrl Pts',(-227.08307000635,-3.78144418264038,
133.952149582262));
#132080=CARTESIAN_POINT('Ctrl Pts',(-227.090800732232,-3.69244422831664,
134.056082819457));
#132081=CARTESIAN_POINT('Ctrl Pts',(-227.098531458113,-3.59935648086937,
134.156049145178));
#132082=CARTESIAN_POINT('Ctrl Pts',(-227.106266550032,-3.50621616079846,
134.256071928296));
#132083=CARTESIAN_POINT('Ctrl Pts',(-227.11400164195,-3.4089837286687,134.352123060586));
#132084=CARTESIAN_POINT('Ctrl Pts',(-227.121736733869,-3.30804661206096,
134.443867545013));
#132085=CARTESIAN_POINT('Ctrl Pts',(-227.129483785872,-3.2069534253635,
134.535753885779));
#132086=CARTESIAN_POINT('Ctrl Pts',(-227.137230837876,-3.10214441355839,
134.623320024407));
#132087=CARTESIAN_POINT('Ctrl Pts',(-227.144977889879,-2.99403894980162,
134.706272178528));
#132088=CARTESIAN_POINT('Ctrl Pts',(-227.150908388666,-2.91128239655924,
134.769773449607));
#132089=CARTESIAN_POINT('Ctrl Pts',(-227.156838887452,-2.82659472533501,
134.830571701648));
#132090=CARTESIAN_POINT('Ctrl Pts',(-227.162769386238,-2.74017412009895,
134.88855317596));
#132091=CARTESIAN_POINT('Ctrl Pts',(-227.170543720357,-2.62688471829739,
134.964561513583));
#132092=CARTESIAN_POINT('Ctrl Pts',(-227.178318054476,-2.51025094082447,
135.035972952477));
#132093=CARTESIAN_POINT('Ctrl Pts',(-227.186092388595,-2.39068239980026,
135.102478894881));
#132094=CARTESIAN_POINT('Ctrl Pts',(-227.193857141543,-2.2712612163164,
135.168902874654));
#132095=CARTESIAN_POINT('Ctrl Pts',(-227.20162189449,-2.1489128040917,135.230433198636));
#132096=CARTESIAN_POINT('Ctrl Pts',(-227.209386647437,-2.02407677889124,
135.286803729938));
#132097=CARTESIAN_POINT('Ctrl Pts',(-227.217143688322,-1.89936474259122,
135.343118273234));
#132098=CARTESIAN_POINT('Ctrl Pts',(-227.224900729207,-1.77217036420014,
135.394283062534));
#132099=CARTESIAN_POINT('Ctrl Pts',(-227.232657770092,-1.6429586461421,
135.440077385183));
#132100=CARTESIAN_POINT('Ctrl Pts',(-227.240408961332,-1.51384436764594,
135.485837173977));
#132101=CARTESIAN_POINT('Ctrl Pts',(-227.248160152572,-1.38271614453616,
135.526234427148));
#132102=CARTESIAN_POINT('Ctrl Pts',(-227.255911343812,-1.25005945672734,
135.561096306791));
#132103=CARTESIAN_POINT('Ctrl Pts',(-227.263659240589,-1.1174591515494,
135.595943369206));
#132104=CARTESIAN_POINT('Ctrl Pts',(-227.271407137366,-0.983332051087742,
135.625259638235));
#132105=CARTESIAN_POINT('Ctrl Pts',(-227.279155034143,-0.848179104589514,
135.648922028988));
#132106=CARTESIAN_POINT('Ctrl Pts',(-227.286901310227,-0.713054429174133,
135.672579470079));
#132107=CARTESIAN_POINT('Ctrl Pts',(-227.294647586311,-0.576904719406775,
135.690585317906));
#132108=CARTESIAN_POINT('Ctrl Pts',(-227.302393862396,-0.440241044777452,
135.702867623276));
#132109=CARTESIAN_POINT('Ctrl Pts',(-227.310140195661,-0.303576361327743,
135.715150019312));
#132110=CARTESIAN_POINT('Ctrl Pts',(-227.317886528926,-0.166398094841255,
135.721708753587));
#132111=CARTESIAN_POINT('Ctrl Pts',(-227.325632862192,-0.0292219672228785,
135.722523805092));
#132112=CARTESIAN_POINT('Ctrl Pts',(-227.333380930195,0.107984880038353,
135.723339039121));
#132113=CARTESIAN_POINT('Ctrl Pts',(-227.341128998198,0.245189196594871,
135.718408028553));
#132114=CARTESIAN_POINT('Ctrl Pts',(-227.348877066201,0.381876129868607,
135.707762873545));
#132115=CARTESIAN_POINT('Ctrl Pts',(-227.356633368943,0.518708335641436,
135.697106404739));
#132116=CARTESIAN_POINT('Ctrl Pts',(-227.364389671685,0.655021669278292,
135.680723690306));
#132117=CARTESIAN_POINT('Ctrl Pts',(-227.372145974426,0.790306710479554,
135.658698715172));
#132118=CARTESIAN_POINT('Ctrl Pts',(-227.379906416941,0.92566395738066,
135.636661984646));
#132119=CARTESIAN_POINT('Ctrl Pts',(-227.387666859455,1.05999143552488,
135.608977071743));
#132120=CARTESIAN_POINT('Ctrl Pts',(-227.395427301969,1.192791749699,135.575778740551));
#132121=CARTESIAN_POINT('Ctrl Pts',(-227.403200202234,1.32580524672689,
135.54252711645));
#132122=CARTESIAN_POINT('Ctrl Pts',(-227.4109731025,1.45728630562025,135.503744498358));
#132123=CARTESIAN_POINT('Ctrl Pts',(-227.418746002765,1.58675362023576,
135.459615284195));
#132124=CARTESIAN_POINT('Ctrl Pts',(-227.426236338527,1.71151447186036,
135.41709027812));
#132125=CARTESIAN_POINT('Ctrl Pts',(-227.43372667429,1.83440515936743,135.369600762643));
#132126=CARTESIAN_POINT('Ctrl Pts',(-227.441217010052,1.95501582534376,
135.317352550326));
#132127=CARTESIAN_POINT('Ctrl Pts',(-227.448991344171,2.0801994813757,135.26312333116));
#132128=CARTESIAN_POINT('Ctrl Pts',(-227.45676567829,2.20332335305605,135.203595657974));
#132129=CARTESIAN_POINT('Ctrl Pts',(-227.464540012409,2.32390640299417,
135.13894734442));
#132130=CARTESIAN_POINT('Ctrl Pts',(-227.472304765356,2.44434084510039,
135.074378704135));
#132131=CARTESIAN_POINT('Ctrl Pts',(-227.480069518303,2.56224035462873,
135.004702162917));
#132132=CARTESIAN_POINT('Ctrl Pts',(-227.48783427125,2.67714340002008,134.930143728471));
#132133=CARTESIAN_POINT('Ctrl Pts',(-227.495591312135,2.7919323220872,134.855659346513));
#132134=CARTESIAN_POINT('Ctrl Pts',(-227.50334835302,2.9037303768036,134.776302932026));
#132135=CARTESIAN_POINT('Ctrl Pts',(-227.511105393906,3.01210052719341,
134.692346404137));
#132136=CARTESIAN_POINT('Ctrl Pts',(-227.518856585146,3.12038895480938,
134.60845318852));
#132137=CARTESIAN_POINT('Ctrl Pts',(-227.526607776386,3.22525431558695,
134.519967002769));
#132138=CARTESIAN_POINT('Ctrl Pts',(-227.534358967626,3.32628878235119,
134.427202871778));
#132139=CARTESIAN_POINT('Ctrl Pts',(-227.542106864403,3.427280306772,134.334478168017));
#132140=CARTESIAN_POINT('Ctrl Pts',(-227.54985476118,3.52444388822232,134.237479399222));
#132141=CARTESIAN_POINT('Ctrl Pts',(-227.557602657957,3.61740519659297,
134.13656149779));
#132142=CARTESIAN_POINT('Ctrl Pts',(-227.565348934041,3.71034705946217,
134.035664706207));
#132143=CARTESIAN_POINT('Ctrl Pts',(-227.573095210126,3.79908813296247,
133.930850699986));
#132144=CARTESIAN_POINT('Ctrl Pts',(-227.58084148621,3.8832916386564,133.822510566068));
#132145=CARTESIAN_POINT('Ctrl Pts',(-227.588587819475,3.96749576592113,
133.714169632407));
#132146=CARTESIAN_POINT('Ctrl Pts',(-227.59633415274,4.04716201862105,133.602302827803));
#132147=CARTESIAN_POINT('Ctrl Pts',(-227.604080486006,4.12199479222569,
133.487333221855));
#132148=CARTESIAN_POINT('Ctrl Pts',(-227.611828554009,4.19684432411102,
133.37233786926));
#132149=CARTESIAN_POINT('Ctrl Pts',(-227.619576622012,4.26685800976634,
133.254238660254));
#132150=CARTESIAN_POINT('Ctrl Pts',(-227.627324690015,4.33178456556933,
133.133486105812));
#132151=CARTESIAN_POINT('Ctrl Pts',(-227.635080992757,4.39678012608874,
133.012605214117));
#132152=CARTESIAN_POINT('Ctrl Pts',(-227.642837295498,4.45667757092194,
132.889065688612));
#132153=CARTESIAN_POINT('Ctrl Pts',(-227.65059359824,4.51127220485229,132.763341514927));
#132154=CARTESIAN_POINT('Ctrl Pts',(-227.658354040754,4.56589597758258,
132.637550238466));
#132155=CARTESIAN_POINT('Ctrl Pts',(-227.666114483269,4.61521115934745,
132.509572355085));
#132156=CARTESIAN_POINT('Ctrl Pts',(-227.673874925783,4.65906227672837,
132.379899180746));
#132157=CARTESIAN_POINT('Ctrl Pts',(-227.681647826048,4.70298378781583,
132.250017843515));
#132158=CARTESIAN_POINT('Ctrl Pts',(-227.689420726314,4.74142359676889,
132.118436152533));
#132159=CARTESIAN_POINT('Ctrl Pts',(-227.697193626579,4.77427668505314,
131.985658715871));
#132160=CARTESIAN_POINT('Ctrl Pts',(-227.704683962341,4.80593548082553,
131.85770807348));
#132161=CARTESIAN_POINT('Ctrl Pts',(-227.712174298103,4.83240662484983,
131.728647414531));
#132162=CARTESIAN_POINT('Ctrl Pts',(-227.719664633865,4.85364173511936,
131.598932810389));
#132163=CARTESIAN_POINT('Ctrl Pts',(-227.727438967984,4.87568198104955,
131.464300037602));
#132164=CARTESIAN_POINT('Ctrl Pts',(-227.735213302103,4.89215112379825,
131.328536275907));
#132165=CARTESIAN_POINT('Ctrl Pts',(-227.742987636222,4.90293875056628,
131.192142348306));
#132166=CARTESIAN_POINT('Ctrl Pts',(-227.750752389169,4.91371308254838,
131.055916514031));
#132167=CARTESIAN_POINT('Ctrl Pts',(-227.758517142116,4.91881979983472,
130.919062445106));
#132168=CARTESIAN_POINT('Ctrl Pts',(-227.766281895063,4.91819958002786,
130.782090603786));
#132169=CARTESIAN_POINT('Ctrl Pts',(-227.774038935948,4.91757997623206,
130.64525480483));
#132170=CARTESIAN_POINT('Ctrl Pts',(-227.781795976833,4.9112447566271,130.508301854694));
#132171=CARTESIAN_POINT('Ctrl Pts',(-227.789553017718,4.89918646531574,
130.371746423893));
#132172=CARTESIAN_POINT('Ctrl Pts',(-227.797304208959,4.8871372672556,130.235293970605));
#132173=CARTESIAN_POINT('Ctrl Pts',(-227.805055400199,4.86937362210339,
130.099238827847));
#132174=CARTESIAN_POINT('Ctrl Pts',(-227.812806591439,4.8459401286741,129.964094390822));
#132175=CARTESIAN_POINT('Ctrl Pts',(-227.820554488216,4.82251659510478,
129.829007393789));
#132176=CARTESIAN_POINT('Ctrl Pts',(-227.828302384993,4.79342807289527,
129.694830717039));
#132177=CARTESIAN_POINT('Ctrl Pts',(-227.83605028177,4.75877084215767,129.562071144726));
#132178=CARTESIAN_POINT('Ctrl Pts',(-227.843796557854,4.72412086096552,
129.429339342852));
#132179=CARTESIAN_POINT('Ctrl Pts',(-227.851542833938,4.68390458689369,
129.298024433852));
#132180=CARTESIAN_POINT('Ctrl Pts',(-227.859289110022,4.63826901548873,
129.168621151007));
#132181=CARTESIAN_POINT('Ctrl Pts',(-227.867035443288,4.59263310721242,
129.039216912937));
#132182=CARTESIAN_POINT('Ctrl Pts',(-227.874781776553,4.54157795180728,
128.911724697888));
#132183=CARTESIAN_POINT('Ctrl Pts',(-227.882528109818,4.48529970823971,
128.786621885776));
#132184=CARTESIAN_POINT('Ctrl Pts',(-227.890276177821,4.42900886154946,
128.661491057756));
#132185=CARTESIAN_POINT('Ctrl Pts',(-227.898024245824,4.36749275954502,
128.538751053922));
#132186=CARTESIAN_POINT('Ctrl Pts',(-227.905772313827,4.30099460493286,
128.418856798487));
#132187=CARTESIAN_POINT('Ctrl Pts',(-227.913528616569,4.23442577529109,
128.298835118012));
#132188=CARTESIAN_POINT('Ctrl Pts',(-227.921284919311,4.16286450567179,
128.181665570135));
#132189=CARTESIAN_POINT('Ctrl Pts',(-227.929041222053,4.08659893084545,
128.067776571549));
#132190=CARTESIAN_POINT('Ctrl Pts',(-227.936801664567,4.01029265078531,
127.953826786976));
#132191=CARTESIAN_POINT('Ctrl Pts',(-227.944562107081,3.92927729330941,
127.843161355878));
#132192=CARTESIAN_POINT('Ctrl Pts',(-227.952322549595,3.84388217927022,
127.736176650724));
#132193=CARTESIAN_POINT('Ctrl Pts',(-227.960095449861,3.75834998141294,
127.629020204223));
#132194=CARTESIAN_POINT('Ctrl Pts',(-227.967868350126,3.66842423388693,
127.525556586242));
#132195=CARTESIAN_POINT('Ctrl Pts',(-227.975641250391,3.57447271266937,
127.426146904835));
#132196=CARTESIAN_POINT('Ctrl Pts',(-227.983131586153,3.48393656589894,
127.330351015747));
#132197=CARTESIAN_POINT('Ctrl Pts',(-227.990621921915,3.38966247827523,
127.238319653933));
#132198=CARTESIAN_POINT('Ctrl Pts',(-227.998112257677,3.29200800389859,
127.150340042259));
#132199=CARTESIAN_POINT('Ctrl Pts',(-228.005886591796,3.19065093044351,
127.059024656867));
#132200=CARTESIAN_POINT('Ctrl Pts',(-228.013660925915,3.08533100663732,
126.971785071232));
#132201=CARTESIAN_POINT('Ctrl Pts',(-228.021435260034,2.97640990824081,
126.888984885835));
#132202=CARTESIAN_POINT('Ctrl Pts',(-228.029200012981,2.86762304536323,
126.806286744267));
#132203=CARTESIAN_POINT('Ctrl Pts',(-228.036964765929,2.75524414669896,
126.728017351283));
#132204=CARTESIAN_POINT('Ctrl Pts',(-228.044729518876,2.63967061339744,
126.654502533816));
#132205=CARTESIAN_POINT('Ctrl Pts',(-228.052486559761,2.52421186935945,
126.581060732302));
#132206=CARTESIAN_POINT('Ctrl Pts',(-228.060243600645,2.40556513275915,
126.512364317169));
#132207=CARTESIAN_POINT('Ctrl Pts',(-228.06800064153,2.28415938038325,126.448697753259));
#132208=CARTESIAN_POINT('Ctrl Pts',(-228.07575183277,2.16284518102912,126.385079200799));
#132209=CARTESIAN_POINT('Ctrl Pts',(-228.08350302401,2.03877645204067,126.326483130566));
#132210=CARTESIAN_POINT('Ctrl Pts',(-228.091254215251,1.91240923409061,
126.273149522962));
#132211=CARTESIAN_POINT('Ctrl Pts',(-228.099002112028,1.78609572557931,
126.219838583563));
#132212=CARTESIAN_POINT('Ctrl Pts',(-228.106750008805,1.65748603056837,
126.171785809897));
#132213=CARTESIAN_POINT('Ctrl Pts',(-228.114497905582,1.52705856267167,
126.129184127991));
#132214=CARTESIAN_POINT('Ctrl Pts',(-228.122244181666,1.39665837738921,
126.08659135744));
#132215=CARTESIAN_POINT('Ctrl Pts',(-228.12999045775,1.26444154694417,126.049447531941));
#132216=CARTESIAN_POINT('Ctrl Pts',(-228.137736733834,1.13090375914098,
126.017896395402));
#132217=CARTESIAN_POINT('Ctrl Pts',(-228.145483067099,0.997364985591997,
125.986345025959));
#132218=CARTESIAN_POINT('Ctrl Pts',(-228.153229400365,0.862505615716626,
125.960386517753));
#132219=CARTESIAN_POINT('Ctrl Pts',(-228.16097573363,0.726833311470884,
125.940113872197));
#132220=CARTESIAN_POINT('Ctrl Pts',(-228.168723801633,0.591130624353477,
125.919836686721));
#132221=CARTESIAN_POINT('Ctrl Pts',(-228.176471869636,0.454615027203587,
125.9052479554));
#132222=CARTESIAN_POINT('Ctrl Pts',(-228.184219937639,0.317800717650317,
125.896388962558));
#132223=CARTESIAN_POINT('Ctrl Pts',(-228.191976240381,0.180841000220929,
125.887520554273));
#132224=CARTESIAN_POINT('Ctrl Pts',(-228.199732543123,0.0435823269677124,
125.884394074471));
#132225=CARTESIAN_POINT('Ctrl Pts',(-228.207488845864,-0.0934591191296018,
125.886998676896));
#132226=CARTESIAN_POINT('Ctrl Pts',(-228.215249288379,-0.23057370837331,
125.889604669476));
#132227=CARTESIAN_POINT('Ctrl Pts',(-228.223009730893,-0.367470449389297,
125.897947815532));
#132228=CARTESIAN_POINT('Ctrl Pts',(-228.230770173407,-0.503637856829301,
125.911965297105));
#132229=CARTESIAN_POINT('Ctrl Pts',(-228.238543073672,-0.640023852280102,
125.926005280784));
#132230=CARTESIAN_POINT('Ctrl Pts',(-228.246315973938,-0.775677787425283,
125.945737746248));
#132231=CARTESIAN_POINT('Ctrl Pts',(-228.254088874203,-0.910097059932253,
125.971048460876));
#132232=CARTESIAN_POINT('Ctrl Pts',(-228.261579209965,-1.03962985330771,
125.995439067275));
#132233=CARTESIAN_POINT('Ctrl Pts',(-228.269069545728,-1.16801589160583,
126.025009328124));
#132234=CARTESIAN_POINT('Ctrl Pts',(-228.27655988149,-1.29482025936989,
126.059613674006));
#132235=CARTESIAN_POINT('Ctrl Pts',(-228.284334215609,-1.42643245327404,
126.095530054178));
#132236=CARTESIAN_POINT('Ctrl Pts',(-228.292108549728,-1.55675757882226,
126.136983561911));
#132237=CARTESIAN_POINT('Ctrl Pts',(-228.299882883847,-1.68529423404915,
126.183866444084));
#132238=CARTESIAN_POINT('Ctrl Pts',(-228.307647636794,-1.81367247933542,
126.230691547295));
#132239=CARTESIAN_POINT('Ctrl Pts',(-228.315412389742,-1.94026627609201,
126.282932578733));
#132240=CARTESIAN_POINT('Ctrl Pts',(-228.323177142689,-2.06458669186481,
126.340431310971));
#132241=CARTESIAN_POINT('Ctrl Pts',(-228.330934183574,-2.18878363084839,
126.397872934659));
#132242=CARTESIAN_POINT('Ctrl Pts',(-228.338691224459,-2.31071132972482,
126.460561704028));
#132243=CARTESIAN_POINT('Ctrl Pts',(-228.346448265344,-2.42989858773376,
126.528290468956));
#132244=CARTESIAN_POINT('Ctrl Pts',(-228.354199456584,-2.54899596570382,
126.595968159096));
#132245=CARTESIAN_POINT('Ctrl Pts',(-228.361950647824,-2.66535667768285,
126.668678087354));
#132246=CARTESIAN_POINT('Ctrl Pts',(-228.369701839064,-2.77853232023985,
126.746166289064));
#132247=CARTESIAN_POINT('Ctrl Pts',(-228.377449735841,-2.89165986013017,
126.823621556223));
#132248=CARTESIAN_POINT('Ctrl Pts',(-228.385197632618,-3.00160470116137,
126.905850837131));
#132249=CARTESIAN_POINT('Ctrl Pts',(-228.392945529395,-3.10794593495714,
126.992555910097));
#132250=CARTESIAN_POINT('Ctrl Pts',(-228.400691805479,-3.21426492445924,
127.079242846231));
#132251=CARTESIAN_POINT('Ctrl Pts',(-228.408438081563,-3.31698150325051,
127.170403465289));
#132252=CARTESIAN_POINT('Ctrl Pts',(-228.416184357647,-3.4157068041452,
127.265698428176));
#132253=CARTESIAN_POINT('Ctrl Pts',(-228.423930690913,-3.51443283380775,
127.360994094509));
#132254=CARTESIAN_POINT('Ctrl Pts',(-228.431677024178,-3.60916724548504,
127.460423894045));
#132255=CARTESIAN_POINT('Ctrl Pts',(-228.439423357444,-3.69955739076832,
127.563610985936));
#132256=CARTESIAN_POINT('Ctrl Pts',(-228.447171425446,-3.78996777829778,
127.666821185861));
#132257=CARTESIAN_POINT('Ctrl Pts',(-228.454919493449,-3.8760317059711,
127.773790058437));
#132258=CARTESIAN_POINT('Ctrl Pts',(-228.462667561452,-3.95743650373772,
127.884107309823));
#132259=CARTESIAN_POINT('Ctrl Pts',(-228.470423864194,-4.03892781949202,
127.994541807696));
#132260=CARTESIAN_POINT('Ctrl Pts',(-228.478180166936,-4.11574988111916,
128.10833147817));
#132261=CARTESIAN_POINT('Ctrl Pts',(-228.485936469678,-4.18763280437161,
128.22503617922));
#132262=CARTESIAN_POINT('Ctrl Pts',(-228.493696912192,-4.25955409370456,
128.341803169082));
#132263=CARTESIAN_POINT('Ctrl Pts',(-228.501457354706,-4.32653080104514,
128.461487948652));
#132264=CARTESIAN_POINT('Ctrl Pts',(-228.50921779722,-4.3883393065969,128.583626236178));
#132265=CARTESIAN_POINT('Ctrl Pts',(-228.516990697486,-4.45024703264903,
128.705960590928));
#132266=CARTESIAN_POINT('Ctrl Pts',(-228.524763597751,-4.50696981607893,
128.83075596806));
#132267=CARTESIAN_POINT('Ctrl Pts',(-228.532536498017,-4.55833209518877,
128.957527768478));
#132268=CARTESIAN_POINT('Ctrl Pts',(-228.540026833778,-4.60782722607807,
129.079691094628));
#132269=CARTESIAN_POINT('Ctrl Pts',(-228.54751716954,-4.65234471785363,
129.203689353004));
#132270=CARTESIAN_POINT('Ctrl Pts',(-228.555007505302,-4.69177195976037,
129.329077953089));
#132271=CARTESIAN_POINT('Ctrl Pts',(-228.560011814405,-4.71811338314223,
129.41285034097));
#132272=CARTESIAN_POINT('Ctrl Pts',(-228.565016123508,-4.74221981315879,
129.497356896618));
#132273=CARTESIAN_POINT('Ctrl Pts',(-228.570020432611,-4.76405452823418,
129.582490119309));
#132274=CARTESIAN_POINT('Origin',(213.235140564004,0.,130.804360617566));
#132275=CARTESIAN_POINT('',(-230.664999534934,-4.76405452823393,129.582490119308));
#132276=CARTESIAN_POINT('',(-230.320068668528,-4.76405452823411,129.582490119308));
#132277=CARTESIAN_POINT('',(213.235140564004,-4.76405452823405,129.582490119308));
#132278=CARTESIAN_POINT('',(-228.985140564067,-4.91824914231909,130.807265196277));
#132279=CARTESIAN_POINT('Ctrl Pts',(-228.985140564067,-4.91824914231909,
130.807265196277));
#132280=CARTESIAN_POINT('Ctrl Pts',(-228.994071663459,-4.9181556026837,
130.965653478122));
#132281=CARTESIAN_POINT('Ctrl Pts',(-229.003002762851,-4.91040629817827,
131.123761141962));
#132282=CARTESIAN_POINT('Ctrl Pts',(-229.011933862243,-4.89511003228873,
131.280890610626));
#132283=CARTESIAN_POINT('Ctrl Pts',(-229.020624482857,-4.8802256336469,
131.433789211296));
#132284=CARTESIAN_POINT('Ctrl Pts',(-229.029315103471,-4.85819560038952,
131.585761459511));
#132285=CARTESIAN_POINT('Ctrl Pts',(-229.038005724085,-4.82917098077785,
131.736181791887));
#132286=CARTESIAN_POINT('Ctrl Pts',(-229.047057062866,-4.79894164771243,
131.892845561751));
#132287=CARTESIAN_POINT('Ctrl Pts',(-229.056108401646,-4.7611248288635,
132.047825549675));
#132288=CARTESIAN_POINT('Ctrl Pts',(-229.065159740427,-4.71594648954949,
132.200437897019));
#132289=CARTESIAN_POINT('Ctrl Pts',(-229.074211079208,-4.67076815023558,
132.353050244363));
#132290=CARTESIAN_POINT('Ctrl Pts',(-229.083262417989,-4.61822846161815,
132.503294741504));
#132291=CARTESIAN_POINT('Ctrl Pts',(-229.09231375677,-4.55860729181921,
132.650514083958));
#132292=CARTESIAN_POINT('Ctrl Pts',(-229.100088090889,-4.50739775190382,
132.776963041924));
#132293=CARTESIAN_POINT('Ctrl Pts',(-229.107862425008,-4.45084185464803,
132.901479956991));
#132294=CARTESIAN_POINT('Ctrl Pts',(-229.115636759127,-4.38910581892583,
133.02357966326));
#132295=CARTESIAN_POINT('Ctrl Pts',(-229.123401512074,-4.32744586735014,
133.145528892553));
#132296=CARTESIAN_POINT('Ctrl Pts',(-229.131166265021,-4.26061865439832,
133.265066494805));
#132297=CARTESIAN_POINT('Ctrl Pts',(-229.138931017968,-4.18883904720675,
133.381725647804));
#132298=CARTESIAN_POINT('Ctrl Pts',(-229.146688058853,-4.11713073253315,
133.498268933288));
#132299=CARTESIAN_POINT('Ctrl Pts',(-229.154445099738,-4.04048001578551,
133.611939128064));
#132300=CARTESIAN_POINT('Ctrl Pts',(-229.162202140623,-3.95914825010333,
133.722292795702));
#132301=CARTESIAN_POINT('Ctrl Pts',(-229.169953331863,-3.87787781733799,
133.832563244782));
#132302=CARTESIAN_POINT('Ctrl Pts',(-229.177704523104,-3.79193359293558,
133.939521831402));
#132303=CARTESIAN_POINT('Ctrl Pts',(-229.185455714344,-3.70162072434241,
134.042753286101));
#132304=CARTESIAN_POINT('Ctrl Pts',(-229.193203611121,-3.61134624112769,
134.145940864677));
#132305=CARTESIAN_POINT('Ctrl Pts',(-229.200951507898,-3.51670706362638,
134.245404168413));
#132306=CARTESIAN_POINT('Ctrl Pts',(-229.208699404675,-3.41804903913538,
134.340760457596));
#132307=CARTESIAN_POINT('Ctrl Pts',(-229.216445680759,-3.31941165177628,
134.4360968003));
#132308=CARTESIAN_POINT('Ctrl Pts',(-229.224191956843,-3.21675737047872,
134.527327565708));
#132309=CARTESIAN_POINT('Ctrl Pts',(-229.231938232927,-3.1104690878048,
134.61410668736));
#132310=CARTESIAN_POINT('Ctrl Pts',(-229.239684566193,-3.00418002053507,
134.700886449595));
#132311=CARTESIAN_POINT('Ctrl Pts',(-229.247430899458,-2.8942572012081,
134.783214255243));
#132312=CARTESIAN_POINT('Ctrl Pts',(-229.255177232723,-2.78111648389569,
134.860784432394));
#132313=CARTESIAN_POINT('Ctrl Pts',(-229.262925300726,-2.66795042950424,
134.938371980849));
#132314=CARTESIAN_POINT('Ctrl Pts',(-229.270673368729,-2.55156536555972,
135.011199559673));
#132315=CARTESIAN_POINT('Ctrl Pts',(-229.278421436732,-2.43240564318684,
135.079005146587));
#132316=CARTESIAN_POINT('Ctrl Pts',(-229.286177739474,-2.31311927644285,
135.146882798086));
#132317=CARTESIAN_POINT('Ctrl Pts',(-229.293934042216,-2.19105270079028,
135.209727601912));
#132318=CARTESIAN_POINT('Ctrl Pts',(-229.301690344958,-2.06667485324285,
135.267323547445));
#132319=CARTESIAN_POINT('Ctrl Pts',(-229.309450787472,-1.94223062149324,
135.324950233669));
#132320=CARTESIAN_POINT('Ctrl Pts',(-229.317211229986,-1.81547302096695,
135.377322330207));
#132321=CARTESIAN_POINT('Ctrl Pts',(-229.3249716725,-1.68688949520486,135.424272618185));
#132322=CARTESIAN_POINT('Ctrl Pts',(-229.332744572765,-1.55809955575209,
135.471298274934));
#132323=CARTESIAN_POINT('Ctrl Pts',(-229.340517473031,-1.42747820647184,
135.512884611945));
#132324=CARTESIAN_POINT('Ctrl Pts',(-229.348290373296,-1.29552738996386,
135.548914531724));
#132325=CARTESIAN_POINT('Ctrl Pts',(-229.355780709058,-1.16837331800179,
135.583634673165));
#132326=CARTESIAN_POINT('Ctrl Pts',(-229.36327104482,-1.03998505980053,
135.61319529411));
#132327=CARTESIAN_POINT('Ctrl Pts',(-229.370761380582,-0.910817394353961,
135.637537082029));
#132328=CARTESIAN_POINT('Ctrl Pts',(-229.378535714701,-0.776752297610621,
135.662801796237));
#132329=CARTESIAN_POINT('Ctrl Pts',(-229.38631004882,-0.641422846540744,
135.682524152218));
#132330=CARTESIAN_POINT('Ctrl Pts',(-229.394084382939,-0.505327070319028,
135.6965817506));
#132331=CARTESIAN_POINT('Ctrl Pts',(-229.401849135886,-0.369399019978647,
135.710622024247));
#132332=CARTESIAN_POINT('Ctrl Pts',(-229.409613888834,-0.232706908777922,
135.719011391232));
#132333=CARTESIAN_POINT('Ctrl Pts',(-229.417378641781,-0.0957596283998767,
135.721678296552));
#132334=CARTESIAN_POINT('Ctrl Pts',(-229.425135682666,0.0410516340090508,
135.724342553064));
#132335=CARTESIAN_POINT('Ctrl Pts',(-229.43289272355,0.17811717288134,135.721295651029));
#132336=CARTESIAN_POINT('Ctrl Pts',(-229.440649764435,0.314922644834436,
135.712517786022));
#132337=CARTESIAN_POINT('Ctrl Pts',(-229.448400955676,0.451624950716754,
135.703746540472));
#132338=CARTESIAN_POINT('Ctrl Pts',(-229.456152146916,0.588067191457631,
135.689252959092));
#132339=CARTESIAN_POINT('Ctrl Pts',(-229.463903338156,0.723735049451271,
135.669069307785));
#132340=CARTESIAN_POINT('Ctrl Pts',(-229.471651234933,0.85934524498602,
135.648894235069));
#132341=CARTESIAN_POINT('Ctrl Pts',(-229.47939913171,0.994181326495175,
135.623033959912));
#132342=CARTESIAN_POINT('Ctrl Pts',(-229.487147028487,1.12773434530897,
135.591572573278));
#132343=CARTESIAN_POINT('Ctrl Pts',(-229.494893304571,1.26125942771029,
135.560117767688));
#132344=CARTESIAN_POINT('Ctrl Pts',(-229.502639580655,1.39350160094927,
135.523064270651));
#132345=CARTESIAN_POINT('Ctrl Pts',(-229.510385856739,1.52396274672794,
135.480547163148));
#132346=CARTESIAN_POINT('Ctrl Pts',(-229.518132190005,1.65442485554134,
135.438029741794));
#132347=CARTESIAN_POINT('Ctrl Pts',(-229.52587852327,1.78310553893736,135.390048750639));
#132348=CARTESIAN_POINT('Ctrl Pts',(-229.533624856535,1.90952284719952,
135.33678883636));
#132349=CARTESIAN_POINT('Ctrl Pts',(-229.541372924538,2.03596846574152,
135.283516994893));
#132350=CARTESIAN_POINT('Ctrl Pts',(-229.549120992541,2.16014934031646,
135.224964029667));
#132351=CARTESIAN_POINT('Ctrl Pts',(-229.556869060544,2.28160484152249,
135.161362156427));
#132352=CARTESIAN_POINT('Ctrl Pts',(-229.564625363286,2.40318942708037,
135.09769268636));
#132353=CARTESIAN_POINT('Ctrl Pts',(-229.572381666028,2.52204250617795,
135.028963770696));
#132354=CARTESIAN_POINT('Ctrl Pts',(-229.58013796877,2.63772887105447,134.955453180411));
#132355=CARTESIAN_POINT('Ctrl Pts',(-229.587898411284,2.75347698122716,
134.88190335531));
#132356=CARTESIAN_POINT('Ctrl Pts',(-229.595658853798,2.86605468861081,
134.803566993465));
#132357=CARTESIAN_POINT('Ctrl Pts',(-229.603419296312,2.9750578320902,134.720763809044));
#132358=CARTESIAN_POINT('Ctrl Pts',(-229.611192196578,3.08423595709235,
134.6378277016));
#132359=CARTESIAN_POINT('Ctrl Pts',(-229.618965096843,3.18982775009587,
134.55041069202));
#132360=CARTESIAN_POINT('Ctrl Pts',(-229.626737997109,3.29146338142692,
134.458871784771));
#132361=CARTESIAN_POINT('Ctrl Pts',(-229.634228332871,3.38940430155686,
134.370660547371));
#132362=CARTESIAN_POINT('Ctrl Pts',(-229.641718668633,3.48367147877708,
134.278622107277));
#132363=CARTESIAN_POINT('Ctrl Pts',(-229.649209004395,3.57396919262221,
134.183107023067));
#132364=CARTESIAN_POINT('Ctrl Pts',(-229.656983338514,3.66769057173093,
134.08397045541));
#132365=CARTESIAN_POINT('Ctrl Pts',(-229.664757672633,3.75743242229338,
133.980774370649));
#132366=CARTESIAN_POINT('Ctrl Pts',(-229.672532006752,3.84282256931558,
133.873871614982));
#132367=CARTESIAN_POINT('Ctrl Pts',(-229.680296759699,3.92810748061311,
133.767100607407));
#132368=CARTESIAN_POINT('Ctrl Pts',(-229.688061512647,4.00905111765098,
133.656632320709));
#132369=CARTESIAN_POINT('Ctrl Pts',(-229.695826265594,4.08531821079547,
133.542856222646));
#132370=CARTESIAN_POINT('Ctrl Pts',(-229.703583306479,4.16150955438787,
133.429193128608));
#132371=CARTESIAN_POINT('Ctrl Pts',(-229.711340347364,4.23303338118517,
133.312229083882));
#132372=CARTESIAN_POINT('Ctrl Pts',(-229.719097388249,4.29959501400327,
133.192386115348));
#132373=CARTESIAN_POINT('Ctrl Pts',(-229.726848579489,4.36610645217638,
133.072633521329));
#132374=CARTESIAN_POINT('Ctrl Pts',(-229.734599770729,4.42766295558962,
132.950006665187));
#132375=CARTESIAN_POINT('Ctrl Pts',(-229.742350961969,4.48401366923161,
132.824955697399));
#132376=CARTESIAN_POINT('Ctrl Pts',(-229.750098858746,4.54034043231702,
132.699957879608));
#132377=CARTESIAN_POINT('Ctrl Pts',(-229.757846755523,4.59146564603659,
132.572538355083));
#132378=CARTESIAN_POINT('Ctrl Pts',(-229.7655946523,4.63718495931166,132.443170769973));
#132379=CARTESIAN_POINT('Ctrl Pts',(-229.773340928384,4.68289470909199,
132.313830245774));
#132380=CARTESIAN_POINT('Ctrl Pts',(-229.781087204469,4.72320067745572,
132.182542839905));
#132381=CARTESIAN_POINT('Ctrl Pts',(-229.788833480553,4.75794726675048,
132.049800647966));
#132382=CARTESIAN_POINT('Ctrl Pts',(-229.796579813818,4.79269411253672,
131.917057476154));
#132383=CARTESIAN_POINT('Ctrl Pts',(-229.804326147083,4.82188139836201,
131.782859875066));
#132384=CARTESIAN_POINT('Ctrl Pts',(-229.812072480349,4.84540396711009,
131.647713128687));
#132385=CARTESIAN_POINT('Ctrl Pts',(-229.819820548351,4.86893180357431,
131.512536117131));
#132386=CARTESIAN_POINT('Ctrl Pts',(-229.827568616355,4.88679233161814,
131.376409922426));
#132387=CARTESIAN_POINT('Ctrl Pts',(-229.835316684358,4.89893193947992,
131.239847603415));
#132388=CARTESIAN_POINT('Ctrl Pts',(-229.843072987099,4.91108444946142,
131.103140144345));
#132389=CARTESIAN_POINT('Ctrl Pts',(-229.850829289841,4.91750385860919,
130.965996025092));
#132390=CARTESIAN_POINT('Ctrl Pts',(-229.858585592583,4.91818862308651,
130.828931540268));
#132391=CARTESIAN_POINT('Ctrl Pts',(-229.866346035097,4.91887375304324,
130.691793900002));
#132392=CARTESIAN_POINT('Ctrl Pts',(-229.874106477611,4.91381815392553,
130.554736369364));
#132393=CARTESIAN_POINT('Ctrl Pts',(-229.881866920126,4.9030723513643,130.418271793865));
#132394=CARTESIAN_POINT('Ctrl Pts',(-229.889639820391,4.89230929868683,
130.281588153315));
#132395=CARTESIAN_POINT('Ctrl Pts',(-229.897412720656,4.87583783608927,
130.145499758388));
#132396=CARTESIAN_POINT('Ctrl Pts',(-229.905185620922,4.85376010222676,
130.010511807948));
#132397=CARTESIAN_POINT('Ctrl Pts',(-229.912675956684,4.83248494960055,
129.880431009521));
#132398=CARTESIAN_POINT('Ctrl Pts',(-229.920166292446,4.80600411517754,
129.751372338508));
#132399=CARTESIAN_POINT('Ctrl Pts',(-229.927656628208,4.77445268968183,
129.623774078387));
#132400=CARTESIAN_POINT('Ctrl Pts',(-229.935430962327,4.74170498229866,
129.491337891452));
#132401=CARTESIAN_POINT('Ctrl Pts',(-229.943205296446,4.70339085581963,
129.360055526434));
#132402=CARTESIAN_POINT('Ctrl Pts',(-229.950979630565,4.6596060000692,129.230430826686));
#132403=CARTESIAN_POINT('Ctrl Pts',(-229.958744383512,4.61587510524033,
129.100965877796));
#132404=CARTESIAN_POINT('Ctrl Pts',(-229.96650913646,4.56668701999335,128.973154896214));
#132405=CARTESIAN_POINT('Ctrl Pts',(-229.974273889407,4.51218819315842,
128.847490470617));
#132406=CARTESIAN_POINT('Ctrl Pts',(-229.982030930292,4.45774349532661,
128.721950856698));
#132407=CARTESIAN_POINT('Ctrl Pts',(-229.989787971177,4.39799870735506,
128.598553912373));
#132408=CARTESIAN_POINT('Ctrl Pts',(-229.997545012062,4.33314961219451,
128.47777567374));
#132409=CARTESIAN_POINT('Ctrl Pts',(-230.005296203302,4.26834942024117,
128.357088514916));
#132410=CARTESIAN_POINT('Ctrl Pts',(-230.013047394542,4.19845276689184,
128.239016474151));
#132411=CARTESIAN_POINT('Ctrl Pts',(-230.020798585782,4.12370278323008,
128.1240139202));
#132412=CARTESIAN_POINT('Ctrl Pts',(-230.028546482559,4.0489845703053,128.009060245402));
#132413=CARTESIAN_POINT('Ctrl Pts',(-230.036294379336,3.96941734243181,
127.897173789757));
#132414=CARTESIAN_POINT('Ctrl Pts',(-230.044042276113,3.88528913478027,
127.78878249693));
#132415=CARTESIAN_POINT('Ctrl Pts',(-230.051788552198,3.80117852493617,
127.680413877225));
#132416=CARTESIAN_POINT('Ctrl Pts',(-230.059534828282,3.71250907255368,
127.57553927477));
#132417=CARTESIAN_POINT('Ctrl Pts',(-230.067281104366,3.61961068726716,
127.47455558797));
#132418=CARTESIAN_POINT('Ctrl Pts',(-230.075027437631,3.52671161622599,
127.373571155732));
#132419=CARTESIAN_POINT('Ctrl Pts',(-230.082773770897,3.42958381468484,
127.276477984194));
#132420=CARTESIAN_POINT('Ctrl Pts',(-230.090520104162,3.32859555238029,
127.183637663352));
#132421=CARTESIAN_POINT('Ctrl Pts',(-230.098268172165,3.22758467445474,
127.090776551564));
#132422=CARTESIAN_POINT('Ctrl Pts',(-230.106016240168,3.12271190323041,
127.002170450179));
#132423=CARTESIAN_POINT('Ctrl Pts',(-230.113764308171,3.01437991117571,
126.918141785127));
#132424=CARTESIAN_POINT('Ctrl Pts',(-230.121520610913,2.90593278259053,
126.834023813411));
#132425=CARTESIAN_POINT('Ctrl Pts',(-230.129276913654,2.79401939838689,
126.7544932363));
#132426=CARTESIAN_POINT('Ctrl Pts',(-230.137033216396,2.67907329736261,
126.679830422518));
#132427=CARTESIAN_POINT('Ctrl Pts',(-230.14479365891,2.56406584614293,126.605127758945));
#132428=CARTESIAN_POINT('Ctrl Pts',(-230.152554101425,2.44602278913262,
126.535298234538));
#132429=CARTESIAN_POINT('Ctrl Pts',(-230.160314543939,2.32540290812225,
126.47057654618));
#132430=CARTESIAN_POINT('Ctrl Pts',(-230.168087444205,2.20458939737075,
126.405750960822));
#132431=CARTESIAN_POINT('Ctrl Pts',(-230.17586034447,2.08119114862293,126.3460497672));
#132432=CARTESIAN_POINT('Ctrl Pts',(-230.183633244735,1.95568840842861,
126.291660105496));
#132433=CARTESIAN_POINT('Ctrl Pts',(-230.191123580497,1.8347480089654,126.239247644995));
#132434=CARTESIAN_POINT('Ctrl Pts',(-230.198613916259,1.71185375607781,
126.191767356857));
#132435=CARTESIAN_POINT('Ctrl Pts',(-230.206104252021,1.58744740990348,
126.149342488354));
#132436=CARTESIAN_POINT('Ctrl Pts',(-230.21387858614,1.45832415929943,126.105309068067));
#132437=CARTESIAN_POINT('Ctrl Pts',(-230.221652920259,1.32716286626439,
126.066582502744));
#132438=CARTESIAN_POINT('Ctrl Pts',(-230.229427254378,1.19443915116726,
126.033354625466));
#132439=CARTESIAN_POINT('Ctrl Pts',(-230.237192007325,1.06187900618678,
126.000167698576));
#132440=CARTESIAN_POINT('Ctrl Pts',(-230.244956760272,0.927760646025438,
125.972466070272));
#132441=CARTESIAN_POINT('Ctrl Pts',(-230.252721513219,0.792577658656779,
125.950392785215));
#132442=CARTESIAN_POINT('Ctrl Pts',(-230.260478554104,0.657528936937288,
125.928341423656));
#132443=CARTESIAN_POINT('Ctrl Pts',(-230.26823559499,0.521418075648059,
125.911907343292));
#132444=CARTESIAN_POINT('Ctrl Pts',(-230.275992635875,0.38475140290749,
125.901183135518));
#132445=CARTESIAN_POINT('Ctrl Pts',(-230.283743827115,0.248187791567389,
125.890467014953));
#132446=CARTESIAN_POINT('Ctrl Pts',(-230.291495018355,0.111069591242116,
125.885452226889));
#132447=CARTESIAN_POINT('Ctrl Pts',(-230.299246209595,-0.0260895064780241,
125.886179815669));
#132448=CARTESIAN_POINT('Ctrl Pts',(-230.306994106372,-0.163190307922608,
125.886907095204));
#132449=CARTESIAN_POINT('Ctrl Pts',(-230.314742003149,-0.300331582048426,
125.89337189522));
#132450=CARTESIAN_POINT('Ctrl Pts',(-230.322489899926,-0.436997597686054,
125.905563197574));
#132451=CARTESIAN_POINT('Ctrl Pts',(-230.33023617601,-0.573635025739016,
125.917751949771));
#132452=CARTESIAN_POINT('Ctrl Pts',(-230.337982452094,-0.709797003871202,
125.935664786978));
#132453=CARTESIAN_POINT('Ctrl Pts',(-230.345728728178,-0.844971285998511,
125.959238680159));
#132454=CARTESIAN_POINT('Ctrl Pts',(-230.353475061444,-0.980146565951848,
125.982812747358));
#132455=CARTESIAN_POINT('Ctrl Pts',(-230.361221394709,-1.11433375019969,
126.012047886748));
#132456=CARTESIAN_POINT('Ctrl Pts',(-230.368967727974,-1.24702956404957,
126.046829710794));
#132457=CARTESIAN_POINT('Ctrl Pts',(-230.376715795977,-1.37975509420672,
126.08161932399));
#132458=CARTESIAN_POINT('Ctrl Pts',(-230.38446386398,-1.51098821126345,
126.121957994449));
#132459=CARTESIAN_POINT('Ctrl Pts',(-230.392211931983,-1.64023999484809,
126.167681221511));
#132460=CARTESIAN_POINT('Ctrl Pts',(-230.399968234725,-1.76962914876662,
126.213453043763));
#132461=CARTESIAN_POINT('Ctrl Pts',(-230.407724537467,-1.89703239351101,
126.264620723875));
#132462=CARTESIAN_POINT('Ctrl Pts',(-230.415480840209,-2.02197950862451,
126.320971059519));
#132463=CARTESIAN_POINT('Ctrl Pts',(-230.423241282723,-2.14699331177578,
126.377351471035));
#132464=CARTESIAN_POINT('Ctrl Pts',(-230.431001725237,-2.26954802400983,
126.438919874428));
#132465=CARTESIAN_POINT('Ctrl Pts',(-230.438762167751,-2.38919820542926,
126.505417142981));
#132466=CARTESIAN_POINT('Ctrl Pts',(-230.446535068017,-2.50904045994162,
126.572021158854));
#132467=CARTESIAN_POINT('Ctrl Pts',(-230.454307968282,-2.62596853257937,
126.643569646909));
#132468=CARTESIAN_POINT('Ctrl Pts',(-230.462080868548,-2.73956539201596,
126.719759715964));
#132469=CARTESIAN_POINT('Ctrl Pts',(-230.46957120431,-2.84903271948127,
126.793180084099));
#132470=CARTESIAN_POINT('Ctrl Pts',(-230.477061540072,-2.95540657615255,
126.870910244093));
#132471=CARTESIAN_POINT('Ctrl Pts',(-230.484551875834,-3.0583444884639,
126.952645148793));
#132472=CARTESIAN_POINT('Ctrl Pts',(-230.492227030782,-3.16382232711922,
127.036396809351));
#132473=CARTESIAN_POINT('Ctrl Pts',(-230.49990218573,-3.2660446810198,127.12463337676));
#132474=CARTESIAN_POINT('Ctrl Pts',(-230.507577340678,-3.36459885966315,
127.217069498065));
#132475=CARTESIAN_POINT('Ctrl Pts',(-230.515243715587,-3.46304029667819,
127.309399876529));
#132476=CARTESIAN_POINT('Ctrl Pts',(-230.522910090497,-3.55782161046869,
127.405919987239));
#132477=CARTESIAN_POINT('Ctrl Pts',(-230.530576465406,-3.64856082956961,
127.506302562372));
#132478=CARTESIAN_POINT('Ctrl Pts',(-230.538235831781,-3.73921709565125,
127.606593368612));
#132479=CARTESIAN_POINT('Ctrl Pts',(-230.545895198156,-3.82583834707426,
127.710739322577));
#132480=CARTESIAN_POINT('Ctrl Pts',(-230.553554564531,-3.90807774779082,
127.818374787104));
#132481=CARTESIAN_POINT('Ctrl Pts',(-230.561208687532,-3.99026084986255,
127.925936567596));
#132482=CARTESIAN_POINT('Ctrl Pts',(-230.568862810533,-4.06806782454047,
128.036982789623));
#132483=CARTESIAN_POINT('Ctrl Pts',(-230.576516933534,-4.14119096594603,
128.151113466231));
#132484=CARTESIAN_POINT('Ctrl Pts',(-230.58416850814,-4.21428976142867,
128.265206143697));
#132485=CARTESIAN_POINT('Ctrl Pts',(-230.591820082745,-4.28270760419785,
128.38238089874));
#132486=CARTESIAN_POINT('Ctrl Pts',(-230.59947165735,-4.34617934566822,
128.502207677862));
#132487=CARTESIAN_POINT('Ctrl Pts',(-230.607121524719,-4.40963692518023,
128.622007720963));
#132488=CARTESIAN_POINT('Ctrl Pts',(-230.614771392088,-4.46815041392961,
128.744458254543));
#132489=CARTESIAN_POINT('Ctrl Pts',(-230.622421259457,-4.52150033928332,
128.869104111477));
#132490=CARTESIAN_POINT('Ctrl Pts',(-230.630073816153,-4.57486901992336,
128.993793787942));
#132491=CARTESIAN_POINT('Ctrl Pts',(-230.63772637285,-4.62307035019042,
129.12067996096));
#132492=CARTESIAN_POINT('Ctrl Pts',(-230.645378929547,-4.6659328130657,
129.249286970932));
#132493=CARTESIAN_POINT('Ctrl Pts',(-230.651919131343,-4.70256490450463,
129.359200014488));
#132494=CARTESIAN_POINT('Ctrl Pts',(-230.658459333138,-4.73529817055404,
129.470369517153));
#132495=CARTESIAN_POINT('Ctrl Pts',(-230.664999534934,-4.76405452823392,
129.582490119308));
#132496=CARTESIAN_POINT('Ctrl Pts',(-228.915319603984,-4.76405452823406,
129.582490119308));
#132497=CARTESIAN_POINT('Ctrl Pts',(-228.923144081678,-4.79847663933562,
129.716701408065));
#132498=CARTESIAN_POINT('Ctrl Pts',(-228.930968559371,-4.82724292611982,
129.852445614384));
#132499=CARTESIAN_POINT('Ctrl Pts',(-228.938793037064,-4.85022842761036,
129.989212003815));
#132500=CARTESIAN_POINT('Ctrl Pts',(-228.946615480386,-4.87320795285048,
130.125942833865));
#132501=CARTESIAN_POINT('Ctrl Pts',(-228.954437923709,-4.89040961687128,
130.263694944493));
#132502=CARTESIAN_POINT('Ctrl Pts',(-228.962260367031,-4.90175953779381,
130.401947277644));
#132503=CARTESIAN_POINT('Ctrl Pts',(-228.969887099359,-4.91282549318019,
130.536740652959));
#132504=CARTESIAN_POINT('Ctrl Pts',(-228.977513831686,-4.91832902067497,
130.672009167332));
#132505=CARTESIAN_POINT('Ctrl Pts',(-228.985140564014,-4.91824914231965,
130.807265195338));
#132506=CARTESIAN_POINT('',(-228.639859435953,-4.91824820079851,130.800153737225));
#132507=CARTESIAN_POINT('Ctrl Pts',(-228.570020432611,-4.76405452823418,
129.582490119309));
#132508=CARTESIAN_POINT('Ctrl Pts',(-228.579416817742,-4.80505267360792,
129.742341265887));
#132509=CARTESIAN_POINT('Ctrl Pts',(-228.588813202874,-4.83803882552062,
129.904403081114));
#132510=CARTESIAN_POINT('Ctrl Pts',(-228.598209588006,-4.86280565366006,
130.06794752885));
#132511=CARTESIAN_POINT('Ctrl Pts',(-228.607496341774,-4.88728351736155,
130.229583838445));
#132512=CARTESIAN_POINT('Ctrl Pts',(-228.616783095542,-4.90373268959774,
130.392668369278));
#132513=CARTESIAN_POINT('Ctrl Pts',(-228.62606984931,-4.91199928481153,
130.556477402098));
#132514=CARTESIAN_POINT('Ctrl Pts',(-228.630666378191,-4.91609088071229,
130.637555566669));
#132515=CARTESIAN_POINT('Ctrl Pts',(-228.635262907072,-4.91817862326256,
130.718810898069));
#132516=CARTESIAN_POINT('Ctrl Pts',(-228.639859435953,-4.91824820079851,
130.800153737224));
#132517=CARTESIAN_POINT('Ctrl Pts',(-228.639859435996,-4.91824820079916,
130.800153737983));
#132518=CARTESIAN_POINT('Ctrl Pts',(-228.647925923209,-4.91837030298047,
130.942902970921));
#132519=CARTESIAN_POINT('Ctrl Pts',(-228.655992410423,-4.91227246476482,
131.085757714811));
#132520=CARTESIAN_POINT('Ctrl Pts',(-228.664058897636,-4.89995927907239,
131.228131930815));
#132521=CARTESIAN_POINT('Ctrl Pts',(-228.671764659131,-4.88819672745851,
131.36413930584));
#132522=CARTESIAN_POINT('Ctrl Pts',(-228.679470420626,-4.87076271627191,
131.499707764516));
#132523=CARTESIAN_POINT('Ctrl Pts',(-228.687176182121,-4.84771450852914,
131.634328753277));
#132524=CARTESIAN_POINT('Ctrl Pts',(-228.69488137582,-4.82466799908442,
131.768939822545));
#132525=CARTESIAN_POINT('Ctrl Pts',(-228.702586569519,-4.79600818229881,
131.902603171099));
#132526=CARTESIAN_POINT('Ctrl Pts',(-228.710291763218,-4.76184378070591,
132.0348186098));
#132527=CARTESIAN_POINT('Ctrl Pts',(-228.717998100802,-4.7276743071932,
132.167053676713));
#132528=CARTESIAN_POINT('Ctrl Pts',(-228.725704438385,-4.68799872201766,
132.297840023391));
#132529=CARTESIAN_POINT('Ctrl Pts',(-228.733410775968,-4.64297601545842,
132.426691281265));
#132530=CARTESIAN_POINT('Ctrl Pts',(-228.741119969578,-4.59793662314605,
132.555590292383));
#132531=CARTESIAN_POINT('Ctrl Pts',(-228.748829163188,-4.54754629724368,
132.682552415039));
#132532=CARTESIAN_POINT('Ctrl Pts',(-228.756538356798,-4.49201251122566,
132.807110392623));
#132533=CARTESIAN_POINT('Ctrl Pts',(-228.76425641601,-4.43641486114215,
132.931811612356));
#132534=CARTESIAN_POINT('Ctrl Pts',(-228.771974475222,-4.37566210427146,
133.054102806771));
#132535=CARTESIAN_POINT('Ctrl Pts',(-228.779692534434,-4.31000827834484,
133.173540159749));
#132536=CARTESIAN_POINT('Ctrl Pts',(-228.787415798043,-4.24431018110684,
133.293058051038));
#132537=CARTESIAN_POINT('Ctrl Pts',(-228.795139061652,-4.17370463775003,
133.40971793172));
#132538=CARTESIAN_POINT('Ctrl Pts',(-228.802862325262,-4.09848888371967,
133.52310516837));
#132539=CARTESIAN_POINT('Ctrl Pts',(-228.810596840686,-4.02316354988221,
133.636657595833));
#132540=CARTESIAN_POINT('Ctrl Pts',(-228.81833135611,-3.94321483021496,
133.746927544111));
#132541=CARTESIAN_POINT('Ctrl Pts',(-228.826065871534,-3.85898028499445,
133.853533328733));
#132542=CARTESIAN_POINT('Ctrl Pts',(-228.828528957395,-3.83215547362489,
133.887482346394));
#132543=CARTESIAN_POINT('Ctrl Pts',(-228.830992043255,-3.80489630373702,
133.921060052229));
#132544=CARTESIAN_POINT('Ctrl Pts',(-228.833455129115,-3.7772144349493,
133.954254929271));
#132545=CARTESIAN_POINT('Ctrl Pts',(-228.841229463234,-3.68984107112999,
134.059029216402));
#132546=CARTESIAN_POINT('Ctrl Pts',(-228.849003797354,-3.59796658701326,
134.160331293483));
#132547=CARTESIAN_POINT('Ctrl Pts',(-228.856778131473,-3.5018974019896,
134.257749916275));
#132548=CARTESIAN_POINT('Ctrl Pts',(-228.86454288442,-3.40594661365079,
134.355048479321));
#132549=CARTESIAN_POINT('Ctrl Pts',(-228.872307637367,-3.30581168224031,
134.44847283511));
#132550=CARTESIAN_POINT('Ctrl Pts',(-228.880072390314,-3.20183975122941,
134.537644061124));
#132551=CARTESIAN_POINT('Ctrl Pts',(-228.887829431199,-3.09797108660615,
134.62672672102));
#132552=CARTESIAN_POINT('Ctrl Pts',(-228.895586472084,-2.99027330121759,
134.711564404751));
#132553=CARTESIAN_POINT('Ctrl Pts',(-228.903343512969,-2.87913066408634,
134.791814652614));
#132554=CARTESIAN_POINT('Ctrl Pts',(-228.911094704209,-2.76807184048247,
134.87200438314));
#132555=CARTESIAN_POINT('Ctrl Pts',(-228.918845895449,-2.65357365156948,
134.947613335621));
#132556=CARTESIAN_POINT('Ctrl Pts',(-228.926597086689,-2.53605346890143,
135.018339244158));
#132557=CARTESIAN_POINT('Ctrl Pts',(-228.934344983466,-2.41858323544549,
135.089035092297));
#132558=CARTESIAN_POINT('Ctrl Pts',(-228.942092880244,-2.29809389714317,
135.154851823177));
#132559=CARTESIAN_POINT('Ctrl Pts',(-228.949840777021,-2.1750316492889,
135.215530574289));
#132560=CARTESIAN_POINT('Ctrl Pts',(-228.957587053105,-2.0519951434043,
135.276196632713));
#132561=CARTESIAN_POINT('Ctrl Pts',(-228.965333329189,-1.92638714890538,
135.331726676327));
#132562=CARTESIAN_POINT('Ctrl Pts',(-228.973079605273,-1.79867793960982,
135.381908075765));
#132563=CARTESIAN_POINT('Ctrl Pts',(-228.980825938538,-1.67096778759372,
135.43208984563));
#132564=CARTESIAN_POINT('Ctrl Pts',(-228.988572271804,-1.54115675371234,
135.476922749554));
#132565=CARTESIAN_POINT('Ctrl Pts',(-228.996318605069,-1.40973416532496,
135.516242687993));
#132566=CARTESIAN_POINT('Ctrl Pts',(-229.004066673072,-1.27828214576031,
135.555571431861));
#132567=CARTESIAN_POINT('Ctrl Pts',(-229.011814741075,-1.14521822803625,
135.589384641511));
#132568=CARTESIAN_POINT('Ctrl Pts',(-229.019562809078,-1.0110455479086,
135.617568483694));
#132569=CARTESIAN_POINT('Ctrl Pts',(-229.02731911182,-0.876730267459646,
135.64578228));
#132570=CARTESIAN_POINT('Ctrl Pts',(-229.035075414562,-0.741304253839631,
135.668354676736));
#132571=CARTESIAN_POINT('Ctrl Pts',(-229.042831717303,-0.605280005602222,
135.685223161965));
#132572=CARTESIAN_POINT('Ctrl Pts',(-229.050592159818,-0.469183157127547,
135.702100650413));
#132573=CARTESIAN_POINT('Ctrl Pts',(-229.058352602332,-0.332487827287851,
135.713268129411));
#132574=CARTESIAN_POINT('Ctrl Pts',(-229.066113044846,-0.195709239536393,
135.718715199407));
#132575=CARTESIAN_POINT('Ctrl Pts',(-229.073885945111,-0.0587110826536159,
135.724171013523));
#132576=CARTESIAN_POINT('Ctrl Pts',(-229.081658845377,0.0783702080327963,
135.723888069069));
#132577=CARTESIAN_POINT('Ctrl Pts',(-229.089431745642,0.215020906246339,
135.717908121394));
#132578=CARTESIAN_POINT('Ctrl Pts',(-229.096922081404,0.346704007381179,
135.71214555988));
#132579=CARTESIAN_POINT('Ctrl Pts',(-229.104412417167,0.477986971830102,
135.701093030686));
#132580=CARTESIAN_POINT('Ctrl Pts',(-229.111902752929,0.608418628413239,
135.684832913881));
#132581=CARTESIAN_POINT('Ctrl Pts',(-229.119677087048,0.743795640896688,
135.667956289806));
#132582=CARTESIAN_POINT('Ctrl Pts',(-229.127451421167,0.878684350192887,
135.6454159314));
#132583=CARTESIAN_POINT('Ctrl Pts',(-229.135225755286,1.01257313771261,
135.61724735042));
#132584=CARTESIAN_POINT('Ctrl Pts',(-229.142990508233,1.14629691926734,
135.589113484698));
#132585=CARTESIAN_POINT('Ctrl Pts',(-229.15075526118,1.27902285206684,135.555365277254));
#132586=CARTESIAN_POINT('Ctrl Pts',(-229.158520014128,1.41024449834063,
135.516089972845));
#132587=CARTESIAN_POINT('Ctrl Pts',(-229.166277055013,1.54133581342509,
135.476853677222));
#132588=CARTESIAN_POINT('Ctrl Pts',(-229.174034095898,1.67092544314303,
135.432101320547));
#132589=CARTESIAN_POINT('Ctrl Pts',(-229.181791136783,1.79851755965378,
135.381971091396));
#132590=CARTESIAN_POINT('Ctrl Pts',(-229.189542328023,1.92601345795746,
135.33187866584));
#132591=CARTESIAN_POINT('Ctrl Pts',(-229.197293519263,2.0515144789184,135.276416582417));
#132592=CARTESIAN_POINT('Ctrl Pts',(-229.205044710503,2.17454071815496,
135.215772605534));
#132593=CARTESIAN_POINT('Ctrl Pts',(-229.21279260728,2.29751466795817,135.155154403958));
#132594=CARTESIAN_POINT('Ctrl Pts',(-229.220540504057,2.41801557814188,
135.089358861912));
#132595=CARTESIAN_POINT('Ctrl Pts',(-229.228288400835,2.53558448089151,
135.018621454624));
#132596=CARTESIAN_POINT('Ctrl Pts',(-229.236034676919,2.65312879076117,
134.947898844077));
#132597=CARTESIAN_POINT('Ctrl Pts',(-229.243780953003,2.76774197831851,
134.872236625871));
#132598=CARTESIAN_POINT('Ctrl Pts',(-229.251527229087,2.87899095797187,
134.791915523322));
#132599=CARTESIAN_POINT('Ctrl Pts',(-229.259273562352,2.99024075883978,
134.71159382786));
#132600=CARTESIAN_POINT('Ctrl Pts',(-229.267019895618,3.09812598526795,
134.626613408291));
#132601=CARTESIAN_POINT('Ctrl Pts',(-229.274766228883,3.20224408227435,
134.537297249768));
#132602=CARTESIAN_POINT('Ctrl Pts',(-229.282514296886,3.30638549580652,
134.447961089512));
#132603=CARTESIAN_POINT('Ctrl Pts',(-229.290262364889,3.40675780452122,
134.354287512713));
#132604=CARTESIAN_POINT('Ctrl Pts',(-229.298010432892,3.50299328011654,
134.256638292082));
#132605=CARTESIAN_POINT('Ctrl Pts',(-229.305766735634,3.59933103592067,
134.158885288696));
#132606=CARTESIAN_POINT('Ctrl Pts',(-229.313523038376,3.69152290090394,
134.05714847977));
#132607=CARTESIAN_POINT('Ctrl Pts',(-229.321279341118,3.77923926401644,
133.951825255623));
#132608=CARTESIAN_POINT('Ctrl Pts',(-229.329039783632,3.86700244399303,
133.846445817299));
#132609=CARTESIAN_POINT('Ctrl Pts',(-229.336800226146,3.95028512510027,
133.73747646007));
#132610=CARTESIAN_POINT('Ctrl Pts',(-229.34456066866,4.02880006703898,133.625345034809));
#132611=CARTESIAN_POINT('Ctrl Pts',(-229.352333568926,4.10744104813272,
133.513033606229));
#132612=CARTESIAN_POINT('Ctrl Pts',(-229.360106469191,4.18129878496189,
133.397550295641));
#132613=CARTESIAN_POINT('Ctrl Pts',(-229.367879369457,4.25013072588525,
133.279349885298));
#132614=CARTESIAN_POINT('Ctrl Pts',(-229.375369705218,4.31646045237624,
133.165446357604));
#132615=CARTESIAN_POINT('Ctrl Pts',(-229.38286004098,4.37812329558615,133.049020119491));
#132616=CARTESIAN_POINT('Ctrl Pts',(-229.390350376742,4.43494469515777,
132.93049528249));
#132617=CARTESIAN_POINT('Ctrl Pts',(-229.398124710861,4.49392049536689,
132.807476540265));
#132618=CARTESIAN_POINT('Ctrl Pts',(-229.40589904498,4.54786729567827,132.681807234591));
#132619=CARTESIAN_POINT('Ctrl Pts',(-229.413673379099,4.59653843079351,
132.553936999648));
#132620=CARTESIAN_POINT('Ctrl Pts',(-229.421438132046,4.64514958308432,
132.426224353342));
#132621=CARTESIAN_POINT('Ctrl Pts',(-229.429202884993,4.6884978690515,132.296316536615));
#132622=CARTESIAN_POINT('Ctrl Pts',(-229.436967637941,4.72638294819557,
132.16468678783));
#132623=CARTESIAN_POINT('Ctrl Pts',(-229.444724678826,4.76423039934506,
132.033187775567));
#132624=CARTESIAN_POINT('Ctrl Pts',(-229.45248171971,4.79662533448668,131.899970607996));
#132625=CARTESIAN_POINT('Ctrl Pts',(-229.460238760595,4.82341600852472,
131.765527133424));
#132626=CARTESIAN_POINT('Ctrl Pts',(-229.467989951836,4.85018647950719,
131.631185043722));
#132627=CARTESIAN_POINT('Ctrl Pts',(-229.475741143076,4.87136102531784,
131.495618869587));
#132628=CARTESIAN_POINT('Ctrl Pts',(-229.483492334316,4.88683821742956,
131.359333859416));
#132629=CARTESIAN_POINT('Ctrl Pts',(-229.491240231093,4.9023088313217,131.223106774011));
#132630=CARTESIAN_POINT('Ctrl Pts',(-229.49898812787,4.91208686372415,131.08616184789));
#132631=CARTESIAN_POINT('Ctrl Pts',(-229.506736024647,4.91612234330196,
130.949012503787));
#132632=CARTESIAN_POINT('Ctrl Pts',(-229.514482300731,4.92015697874445,
130.81189184837));
#132633=CARTESIAN_POINT('Ctrl Pts',(-229.522228576816,4.91845143915975,
130.674567250572));
#132634=CARTESIAN_POINT('Ctrl Pts',(-229.5299748529,4.9110078116836,130.537554815375));
#132635=CARTESIAN_POINT('Ctrl Pts',(-229.537721186165,4.90356412926028,
130.400541368784));
#132636=CARTESIAN_POINT('Ctrl Pts',(-229.54546751943,4.89038229563376,130.263840479783));
#132637=CARTESIAN_POINT('Ctrl Pts',(-229.553213852696,4.87151645656185,
130.127965410644));
#132638=CARTESIAN_POINT('Ctrl Pts',(-229.560961920699,4.85264639261607,
129.992059913225));
#132639=CARTESIAN_POINT('Ctrl Pts',(-229.568709988702,4.82808984407219,
129.856980990848));
#132640=CARTESIAN_POINT('Ctrl Pts',(-229.576458056705,4.79795241442714,
129.723233570733));
#132641=CARTESIAN_POINT('Ctrl Pts',(-229.584214359446,4.76778295436327,
129.589344002269));
#132642=CARTESIAN_POINT('Ctrl Pts',(-229.591970662188,4.732020850613,129.456789144966));
#132643=CARTESIAN_POINT('Ctrl Pts',(-229.59972696493,4.69082227608267,129.326061109108));
#132644=CARTESIAN_POINT('Ctrl Pts',(-229.607487407444,4.64960171263276,
129.195263299762));
#132645=CARTESIAN_POINT('Ctrl Pts',(-229.615247849959,4.6029390296556,129.066294622153));
#132646=CARTESIAN_POINT('Ctrl Pts',(-229.623008292473,4.55103892980856,
128.939628003525));
#132647=CARTESIAN_POINT('Ctrl Pts',(-229.630781192738,4.49905551531364,
128.812758048396));
#132648=CARTESIAN_POINT('Ctrl Pts',(-229.638554093004,4.44181804629066,
128.688197892433));
#132649=CARTESIAN_POINT('Ctrl Pts',(-229.646326993269,4.37957803884262,
128.566397422116));
#132650=CARTESIAN_POINT('Ctrl Pts',(-229.653817329031,4.3196006124386,128.449024705693));
#132651=CARTESIAN_POINT('Ctrl Pts',(-229.661307664793,4.2549781939034,128.334214783745));
#132652=CARTESIAN_POINT('Ctrl Pts',(-229.668798000555,4.1859732461429,128.222343761487));
#132653=CARTESIAN_POINT('Ctrl Pts',(-229.676572334674,4.11435195481475,
128.106231115418));
#132654=CARTESIAN_POINT('Ctrl Pts',(-229.684346668793,4.03778237210415,
127.992916815104));
#132655=CARTESIAN_POINT('Ctrl Pts',(-229.692121002912,3.95650945936246,
127.882851425303));
#132656=CARTESIAN_POINT('Ctrl Pts',(-229.699885755859,3.87533670822194,
127.772921681259));
#132657=CARTESIAN_POINT('Ctrl Pts',(-229.707650508806,3.78947239023545,
127.666233192472));
#132658=CARTESIAN_POINT('Ctrl Pts',(-229.715415261753,3.69920636530636,
127.563210307973));
#132659=CARTESIAN_POINT('Ctrl Pts',(-229.723172302638,3.60902999386576,
127.460289747255));
#132660=CARTESIAN_POINT('Ctrl Pts',(-229.730929343523,3.51446087161696,
127.361027837766));
#132661=CARTESIAN_POINT('Ctrl Pts',(-229.738686384408,3.415830782539,127.265818102976));
#132662=CARTESIAN_POINT('Ctrl Pts',(-229.746437575648,3.31727507117885,
127.170680166588));
#132663=CARTESIAN_POINT('Ctrl Pts',(-229.754188766888,3.21466476867465,
127.079588592997));
#132664=CARTESIAN_POINT('Ctrl Pts',(-229.761939958128,3.10837013021514,
126.992901815993));
#132665=CARTESIAN_POINT('Ctrl Pts',(-229.769687854906,3.00212066981205,
126.906251883182));
#132666=CARTESIAN_POINT('Ctrl Pts',(-229.777435751683,2.89219029034001,
126.824003269959));
#132667=CARTESIAN_POINT('Ctrl Pts',(-229.78518364846,2.77898393815928,126.746475536153));
#132668=CARTESIAN_POINT('Ctrl Pts',(-229.792929924544,2.66580126630697,
126.668964019478));
#132669=CARTESIAN_POINT('Ctrl Pts',(-229.800676200628,2.54934430713946,
126.596171638784));
#132670=CARTESIAN_POINT('Ctrl Pts',(-229.808422476712,2.43004840254403,
126.528375605456));
#132671=CARTESIAN_POINT('Ctrl Pts',(-229.816168809977,2.31075161733382,
126.460579071673));
#132672=CARTESIAN_POINT('Ctrl Pts',(-229.823915143242,2.18861618478844,
126.397779152022));
#132673=CARTESIAN_POINT('Ctrl Pts',(-229.831661476508,2.06410319409927,
126.340207722939));
#132674=CARTESIAN_POINT('Ctrl Pts',(-229.839409544511,1.93956231958897,
126.282623401133));
#132675=CARTESIAN_POINT('Ctrl Pts',(-229.847157612514,1.81264318224541,
126.23027006387));
#132676=CARTESIAN_POINT('Ctrl Pts',(-229.854905680517,1.68382767290969,
126.183331789432));
#132677=CARTESIAN_POINT('Ctrl Pts',(-229.862661983258,1.55487525691755,
126.136343628438));
#132678=CARTESIAN_POINT('Ctrl Pts',(-229.870418286,1.42402281070542,126.094782160953));
#132679=CARTESIAN_POINT('Ctrl Pts',(-229.878174588742,1.29176877586443,
126.058781991919));
#132680=CARTESIAN_POINT('Ctrl Pts',(-229.885935031256,1.15944415306258,
126.02276260851));
#132681=CARTESIAN_POINT('Ctrl Pts',(-229.89369547377,1.02571683205874,125.992310524771));
#132682=CARTESIAN_POINT('Ctrl Pts',(-229.901455916284,0.891095346725003,
125.967509147286));
#132683=CARTESIAN_POINT('Ctrl Pts',(-229.90922881655,0.756257755031871,
125.942667956429));
#132684=CARTESIAN_POINT('Ctrl Pts',(-229.917001716815,0.620523517983609,
125.923495653318));
#132685=CARTESIAN_POINT('Ctrl Pts',(-229.924774617081,0.484407088416055,
125.910023804964));
#132686=CARTESIAN_POINT('Ctrl Pts',(-229.932264952843,0.353238833912496,
125.89704169223));
#132687=CARTESIAN_POINT('Ctrl Pts',(-229.939755288605,0.221715999275977,
125.889352795944));
#132688=CARTESIAN_POINT('Ctrl Pts',(-229.947245624368,0.0902968800871135,
125.886939592685));
#132689=CARTESIAN_POINT('Ctrl Pts',(-229.955019958487,-0.0461050349422831,
125.88443489209));
#132690=CARTESIAN_POINT('Ctrl Pts',(-229.962794292606,-0.182827294795918,
125.887605903412));
#132691=CARTESIAN_POINT('Ctrl Pts',(-229.970568626725,-0.319358418987533,
125.896490074986));
#132692=CARTESIAN_POINT('Ctrl Pts',(-229.978333379672,-0.45572128077146,
125.905363297613));
#132693=CARTESIAN_POINT('Ctrl Pts',(-229.986098132619,-0.591893089188019,
125.919935645938));
#132694=CARTESIAN_POINT('Ctrl Pts',(-229.993862885566,-0.727360151021741,
125.940192623633));
#132695=CARTESIAN_POINT('Ctrl Pts',(-230.001619926451,-0.862692665059899,
125.960429481811));
#132696=CARTESIAN_POINT('Ctrl Pts',(-230.009376967337,-0.997321441311664,
125.98633967601));
#132697=CARTESIAN_POINT('Ctrl Pts',(-230.017134008222,-1.13073605999144,
126.01785677602));
#132698=CARTESIAN_POINT('Ctrl Pts',(-230.024885199462,-1.26405006966928,
126.049350108739));
#132699=CARTESIAN_POINT('Ctrl Pts',(-230.032636390702,-1.3961513652799,
126.08644184175));
#132700=CARTESIAN_POINT('Ctrl Pts',(-230.040387581942,-1.52653825434919,
126.129014211094));
#132701=CARTESIAN_POINT('Ctrl Pts',(-230.048135478719,-1.65686972551225,
126.171568486046));
#132702=CARTESIAN_POINT('Ctrl Pts',(-230.055883375496,-1.78548786852207,
126.219598643205));
#132703=CARTESIAN_POINT('Ctrl Pts',(-230.063631272273,-1.91190494524551,
126.272936719623));
#132704=CARTESIAN_POINT('Ctrl Pts',(-230.071377548357,-2.03829557824208,
126.326263638866));
#132705=CARTESIAN_POINT('Ctrl Pts',(-230.079123824441,-2.16248570075706,
126.384896117029));
#132706=CARTESIAN_POINT('Ctrl Pts',(-230.086870100526,-2.28400677407834,
126.448617728177));
#132707=CARTESIAN_POINT('Ctrl Pts',(-230.094616433791,-2.40552874444075,
126.512339809704));
#132708=CARTESIAN_POINT('Ctrl Pts',(-230.102362767056,-2.52438128004492,
126.581150917615));
#132709=CARTESIAN_POINT('Ctrl Pts',(-230.110109100322,-2.64012006670736,
126.654788459395));
#132710=CARTESIAN_POINT('Ctrl Pts',(-230.117857168324,-2.75588477226749,
126.72844249179));
#132711=CARTESIAN_POINT('Ctrl Pts',(-230.125605236327,-2.86853401153698,
126.806924898982));
#132712=CARTESIAN_POINT('Ctrl Pts',(-230.13335330433,-2.97765244047183,
126.889929751367));
#132713=CARTESIAN_POINT('Ctrl Pts',(-230.141109607072,-3.08688684177222,
126.973022822297));
#132714=CARTESIAN_POINT('Ctrl Pts',(-230.148865909814,-3.19258262487569,
127.060647702859));
#132715=CARTESIAN_POINT('Ctrl Pts',(-230.156622212556,-3.29435712297832,
127.152457797284));
#132716=CARTESIAN_POINT('Ctrl Pts',(-230.16438265507,-3.39618594119524,
127.244316893521));
#132717=CARTESIAN_POINT('Ctrl Pts',(-230.172143097584,-3.49408902516683,
127.340365380943));
#132718=CARTESIAN_POINT('Ctrl Pts',(-230.179903540098,-3.5877213275915,
127.440220498896));
#132719=CARTESIAN_POINT('Ctrl Pts',(-230.187676440364,-3.68150393690005,
127.540235913149));
#132720=CARTESIAN_POINT('Ctrl Pts',(-230.195449340629,-3.77100180911301,
127.64406987283));
#132721=CARTESIAN_POINT('Ctrl Pts',(-230.203222240895,-3.85591031168543,
127.75130661694));
#132722=CARTESIAN_POINT('Ctrl Pts',(-230.210712576656,-3.9377321763145,
127.854645035284));
#132723=CARTESIAN_POINT('Ctrl Pts',(-230.218202912418,-4.01529236725859,
127.96114288472));
#132724=CARTESIAN_POINT('Ctrl Pts',(-230.22569324818,-4.08835790751209,
128.070405116358));
#132725=CARTESIAN_POINT('Ctrl Pts',(-230.233604311068,-4.16552749006171,
128.185804534124));
#132726=CARTESIAN_POINT('Ctrl Pts',(-230.241515373956,-4.23792147660652,
128.304644037511));
#132727=CARTESIAN_POINT('Ctrl Pts',(-230.249426436844,-4.30522448242884,
128.426499137497));
#132728=CARTESIAN_POINT('Ctrl Pts',(-230.257327785396,-4.37244484398277,
128.548204606342));
#132729=CARTESIAN_POINT('Ctrl Pts',(-230.265229133948,-4.43458648535344,
128.672917980837));
#132730=CARTESIAN_POINT('Ctrl Pts',(-230.2731304825,-4.49137645005342,128.800184815296));
#132731=CARTESIAN_POINT('Ctrl Pts',(-230.281020837594,-4.54808740063468,
128.927274578386));
#132732=CARTESIAN_POINT('Ctrl Pts',(-230.288911192688,-4.59946135799188,
129.056910385611));
#132733=CARTESIAN_POINT('Ctrl Pts',(-230.296801547782,-4.64527092374599,
129.188612769819));
#132734=CARTESIAN_POINT('Ctrl Pts',(-230.304557254697,-4.69029875350489,
129.318067665043));
#132735=CARTESIAN_POINT('Ctrl Pts',(-230.312312961613,-4.72995044961027,
129.449518834356));
#132736=CARTESIAN_POINT('Ctrl Pts',(-230.320068668528,-4.76405452823411,
129.582490119308));
#132737=CARTESIAN_POINT('Origin',(213.235140564004,0.,130.804360617566));
#132738=CARTESIAN_POINT('',(-232.415119734886,-4.76405452823408,129.582490119308));
#132739=CARTESIAN_POINT('',(-232.069726383436,-4.76405452823406,129.582490119308));
#132740=CARTESIAN_POINT('',(213.235140564004,-4.76405452823405,129.582490119308));
#132741=CARTESIAN_POINT('',(-230.735140563976,-4.91824919291643,130.807178218822));
#132742=CARTESIAN_POINT('Ctrl Pts',(-230.735140564014,-4.91824919291605,
130.807178219487));
#132743=CARTESIAN_POINT('Ctrl Pts',(-230.744426875891,-4.91815569747121,
130.970378667585));
#132744=CARTESIAN_POINT('Ctrl Pts',(-230.753713187769,-4.90993976197208,
131.133343395079));
#132745=CARTESIAN_POINT('Ctrl Pts',(-230.762999499647,-4.89366721036058,
131.29548615828));
#132746=CARTESIAN_POINT('Ctrl Pts',(-230.770773833766,-4.8800441213604,
131.431229177971));
#132747=CARTESIAN_POINT('Ctrl Pts',(-230.778548167885,-4.86074721111518,
131.566619949102));
#132748=CARTESIAN_POINT('Ctrl Pts',(-230.786322502004,-4.83579970371893,
131.701146148232));
#132749=CARTESIAN_POINT('Ctrl Pts',(-230.794087254951,-4.81088294189593,
131.835506555845));
#132750=CARTESIAN_POINT('Ctrl Pts',(-230.801852007898,-4.78032950952325,
131.969004130779));
#132751=CARTESIAN_POINT('Ctrl Pts',(-230.809616760845,-4.74421447312459,
132.101130487472));
#132752=CARTESIAN_POINT('Ctrl Pts',(-230.81737380173,-4.70813530668931,
132.233125614404));
#132753=CARTESIAN_POINT('Ctrl Pts',(-230.825130842615,-4.66650563138251,
132.363751858674));
#132754=CARTESIAN_POINT('Ctrl Pts',(-230.8328878835,-4.61945169748514,132.492510219083));
#132755=CARTESIAN_POINT('Ctrl Pts',(-230.84063907474,-4.57243324732528,
132.62117148181));
#132756=CARTESIAN_POINT('Ctrl Pts',(-230.848390265981,-4.51999881407111,
132.747967298654));
#132757=CARTESIAN_POINT('Ctrl Pts',(-230.856141457221,-4.46232459167631,
132.872413397604));
#132758=CARTESIAN_POINT('Ctrl Pts',(-230.863889353998,-4.40467488236445,
132.996806603642));
#132759=CARTESIAN_POINT('Ctrl Pts',(-230.871637250775,-4.34178997739594,
133.118851724131));
#132760=CARTESIAN_POINT('Ctrl Pts',(-230.879385147552,-4.27389427022736,
133.238084272671));
#132761=CARTESIAN_POINT('Ctrl Pts',(-230.887131423636,-4.20601276537707,
133.357291880332));
#132762=CARTESIAN_POINT('Ctrl Pts',(-230.89487769972,-4.1331227364989,133.473687746736));
#132763=CARTESIAN_POINT('Ctrl Pts',(-230.902623975804,-4.05549443320797,
133.586832174423));
#132764=CARTESIAN_POINT('Ctrl Pts',(-230.91037030907,-3.97786555688265,
133.699977437316));
#132765=CARTESIAN_POINT('Ctrl Pts',(-230.918116642335,-3.89549855753708,
133.809870891217));
#132766=CARTESIAN_POINT('Ctrl Pts',(-230.9258629756,-3.80870666710518,133.916102346317));
#132767=CARTESIAN_POINT('Ctrl Pts',(-230.933611043603,-3.72189534023132,
134.022357591214));
#132768=CARTESIAN_POINT('Ctrl Pts',(-230.941359111606,-3.63065739776129,
134.12494890274));
#132769=CARTESIAN_POINT('Ctrl Pts',(-230.949107179609,-3.53534568375761,
134.223499976942));
#132770=CARTESIAN_POINT('Ctrl Pts',(-230.956863482351,-3.43993267133019,
134.322155792399));
#132771=CARTESIAN_POINT('Ctrl Pts',(-230.964619785093,-3.34043751065132,
134.416762511298));
#132772=CARTESIAN_POINT('Ctrl Pts',(-230.972376087835,-3.23724956784499,
134.506981081236));
#132773=CARTESIAN_POINT('Ctrl Pts',(-230.980136530349,-3.13400655052636,
134.597247803542));
#132774=CARTESIAN_POINT('Ctrl Pts',(-230.987896972863,-3.02706712849241,
134.683121465406));
#132775=CARTESIAN_POINT('Ctrl Pts',(-230.995657415377,-2.9168521364287,
134.764304642008));
#132776=CARTESIAN_POINT('Ctrl Pts',(-231.003430315642,-2.8064602174753,
134.845618141051));
#132777=CARTESIAN_POINT('Ctrl Pts',(-231.011203215908,-2.69278254526388,
134.922225889709));
#132778=CARTESIAN_POINT('Ctrl Pts',(-231.018976116173,-2.57626795051102,
134.993874492668));
#132779=CARTESIAN_POINT('Ctrl Pts',(-231.026466451935,-2.46398895476093,
135.062918488437));
#132780=CARTESIAN_POINT('Ctrl Pts',(-231.033956787697,-2.34907598273907,
135.127357482966));
#132781=CARTESIAN_POINT('Ctrl Pts',(-231.041447123459,-2.23194883487598,
135.187006788659));
#132782=CARTESIAN_POINT('Ctrl Pts',(-231.049221457578,-2.1103807756011,
135.248917715908));
#132783=CARTESIAN_POINT('Ctrl Pts',(-231.056995791697,-1.98604223404277,
135.305864697701));
#132784=CARTESIAN_POINT('Ctrl Pts',(-231.064770125816,-1.85937679561084,
135.357590349794));
#132785=CARTESIAN_POINT('Ctrl Pts',(-231.072534878763,-1.73286746101136,
135.409252254643));
#132786=CARTESIAN_POINT('Ctrl Pts',(-231.08029963171,-1.60403729386557,
135.455705486781));
#132787=CARTESIAN_POINT('Ctrl Pts',(-231.088064384657,-1.4733545886351,
135.496738406987));
#132788=CARTESIAN_POINT('Ctrl Pts',(-231.095821425542,-1.34280167930977,
135.537730572717));
#132789=CARTESIAN_POINT('Ctrl Pts',(-231.103578466427,-1.21040026411328,
135.57331302362));
#132790=CARTESIAN_POINT('Ctrl Pts',(-231.111335507312,-1.07663840824776,
135.603322255294));
#132791=CARTESIAN_POINT('Ctrl Pts',(-231.119086698553,-0.942977423238074,
135.633308856774));
#132792=CARTESIAN_POINT('Ctrl Pts',(-231.126837889793,-0.807958419527763,
135.657730519221));
#132793=CARTESIAN_POINT('Ctrl Pts',(-231.134589081033,-0.672084066009092,
135.676473718749));
#132794=CARTESIAN_POINT('Ctrl Pts',(-231.14233697781,-0.536267462715418,
135.695208951917));
#132795=CARTESIAN_POINT('Ctrl Pts',(-231.150084874587,-0.399596619166442,
135.708270469117));
#132796=CARTESIAN_POINT('Ctrl Pts',(-231.157832771364,-0.262583611069324,
135.715595992673));
#132797=CARTESIAN_POINT('Ctrl Pts',(-231.165579047448,-0.125599263139469,
135.722919983887));
#132798=CARTESIAN_POINT('Ctrl Pts',(-231.173325323532,0.0117267168147697,
135.724510347158));
#132799=CARTESIAN_POINT('Ctrl Pts',(-231.181071599616,0.148878322349868,
135.720356783923));
#132800=CARTESIAN_POINT('Ctrl Pts',(-231.188817932882,0.286030940306776,
135.716203190027));
#132801=CARTESIAN_POINT('Ctrl Pts',(-231.196564266147,0.423008790490003,
135.706305596854));
#132802=CARTESIAN_POINT('Ctrl Pts',(-231.204310599412,0.559297459084418,
135.690705817689));
#132803=CARTESIAN_POINT('Ctrl Pts',(-231.212058667415,0.69561664858102,
135.675102545061));
#132804=CARTESIAN_POINT('Ctrl Pts',(-231.219806735418,0.831245961020516,
135.653794589881));
#132805=CARTESIAN_POINT('Ctrl Pts',(-231.227554803421,0.965678080395513,
135.626875408372));
#132806=CARTESIAN_POINT('Ctrl Pts',(-231.235311106163,1.10025307582693,
135.599927616837));
#132807=CARTESIAN_POINT('Ctrl Pts',(-231.243067408905,1.23362795248946,
135.567356762771));
#132808=CARTESIAN_POINT('Ctrl Pts',(-231.250823711647,1.36530699409404,
135.529307164817));
#132809=CARTESIAN_POINT('Ctrl Pts',(-231.258584154161,1.49705631676791,
135.491237258647));
#132810=CARTESIAN_POINT('Ctrl Pts',(-231.266344596675,1.6271076303131,135.447682906027));
#132811=CARTESIAN_POINT('Ctrl Pts',(-231.274105039189,1.75498323137612,
135.398837401715));
#132812=CARTESIAN_POINT('Ctrl Pts',(-231.281877939454,1.88306410970624,
135.349913486265));
#132813=CARTESIAN_POINT('Ctrl Pts',(-231.28965083972,2.00896193685782,135.295681600512));
#132814=CARTESIAN_POINT('Ctrl Pts',(-231.297423739985,2.13222092021232,
135.236382392096));
#132815=CARTESIAN_POINT('Ctrl Pts',(-231.304914075748,2.25099912905492,
135.17923885927));
#132816=CARTESIAN_POINT('Ctrl Pts',(-231.31240441151,2.36732674844701,135.117390171954));
#132817=CARTESIAN_POINT('Ctrl Pts',(-231.319894747272,2.48082148309694,
135.051089691984));
#132818=CARTESIAN_POINT('Ctrl Pts',(-231.327669081391,2.59861940510362,
134.982275409166));
#132819=CARTESIAN_POINT('Ctrl Pts',(-231.33544341551,2.71373853255926,134.908447107369));
#132820=CARTESIAN_POINT('Ctrl Pts',(-231.343217749629,2.82572255205946,
134.829838865089));
#132821=CARTESIAN_POINT('Ctrl Pts',(-231.350982502576,2.93756856126392,
134.751327500443));
#132822=CARTESIAN_POINT('Ctrl Pts',(-231.358747255523,3.04628683328025,
134.668048138817));
#132823=CARTESIAN_POINT('Ctrl Pts',(-231.36651200847,3.15144618544165,134.580280373435));
#132824=CARTESIAN_POINT('Ctrl Pts',(-231.374269049355,3.25650109185199,
134.492599780236));
#132825=CARTESIAN_POINT('Ctrl Pts',(-231.382026090241,3.35800381454203,
134.40043990369));
#132826=CARTESIAN_POINT('Ctrl Pts',(-231.389783131126,3.45555298146591,
134.304122988754));
#132827=CARTESIAN_POINT('Ctrl Pts',(-231.397534322366,3.55302858580432,
134.207878707152));
#132828=CARTESIAN_POINT('Ctrl Pts',(-231.405285513606,3.64655629160666,
134.107483900478));
#132829=CARTESIAN_POINT('Ctrl Pts',(-231.413036704846,3.73576888319733,
134.003300115874));
#132830=CARTESIAN_POINT('Ctrl Pts',(-231.420784601623,3.82494355705663,
133.899160612157));
#132831=CARTESIAN_POINT('Ctrl Pts',(-231.4285324984,3.9098065107072,133.791235629851));
#132832=CARTESIAN_POINT('Ctrl Pts',(-231.436280395177,3.99002855874991,
133.679922330147));
#132833=CARTESIAN_POINT('Ctrl Pts',(-231.444026671261,4.07023382606955,
133.568632314785));
#132834=CARTESIAN_POINT('Ctrl Pts',(-231.451772947345,4.14579989026932,
133.45395570877));
#132835=CARTESIAN_POINT('Ctrl Pts',(-231.45951922343,4.21643917279056,133.336321076313));
#132836=CARTESIAN_POINT('Ctrl Pts',(-231.467265556695,4.28707897675503,
133.218685575503));
#132837=CARTESIAN_POINT('Ctrl Pts',(-231.47501188996,4.352791725198,133.098092339857));
#132838=CARTESIAN_POINT('Ctrl Pts',(-231.482758223226,4.41333454358869,
132.974996761388));
#132839=CARTESIAN_POINT('Ctrl Pts',(-231.490506291229,4.47389092012371,
132.851873616518));
#132840=CARTESIAN_POINT('Ctrl Pts',(-231.498254359232,4.52927489026144,
132.726247364489));
#132841=CARTESIAN_POINT('Ctrl Pts',(-231.506002427235,4.57929086467661,
132.59859534));
#132842=CARTESIAN_POINT('Ctrl Pts',(-231.513758729976,4.62935999666452,
132.470807645421));
#132843=CARTESIAN_POINT('Ctrl Pts',(-231.521515032718,4.67404959338273,
132.340990242102));
#132844=CARTESIAN_POINT('Ctrl Pts',(-231.52927133546,4.71321312742965,132.209638197948));
#132845=CARTESIAN_POINT('Ctrl Pts',(-231.537031777974,4.75239756423399,
132.078216047253));
#132846=CARTESIAN_POINT('Ctrl Pts',(-231.544792220488,4.78604996550251,
131.945258002457));
#132847=CARTESIAN_POINT('Ctrl Pts',(-231.552552663003,4.81407474525854,
131.81127044946));
#132848=CARTESIAN_POINT('Ctrl Pts',(-231.560325563268,4.84214451287896,
131.677067807747));
#132849=CARTESIAN_POINT('Ctrl Pts',(-231.568098463533,4.86456854226935,
131.541832741215));
#132850=CARTESIAN_POINT('Ctrl Pts',(-231.575871363799,4.88130293005894,
131.40607879703));
#132851=CARTESIAN_POINT('Ctrl Pts',(-231.583361699561,4.89742898070105,
131.27525985066));
#132852=CARTESIAN_POINT('Ctrl Pts',(-231.590852035323,4.90827184815751,
131.143959403667));
#132853=CARTESIAN_POINT('Ctrl Pts',(-231.598342371085,4.91383805297244,
131.012636040168));
#132854=CARTESIAN_POINT('Ctrl Pts',(-231.606116705204,4.91961530213471,
130.876333511428));
#132855=CARTESIAN_POINT('Ctrl Pts',(-231.613891039323,4.91972616123747,
130.739574528679));
#132856=CARTESIAN_POINT('Ctrl Pts',(-231.621665373442,4.91412091860825,
130.602869526456));
#132857=CARTESIAN_POINT('Ctrl Pts',(-231.629430126389,4.90852258393961,
130.46633300093));
#132858=CARTESIAN_POINT('Ctrl Pts',(-231.637194879336,4.89722218002583,
130.329850710451));
#132859=CARTESIAN_POINT('Ctrl Pts',(-231.644959632284,4.88022187180129,
130.193936548175));
#132860=CARTESIAN_POINT('Ctrl Pts',(-231.652716673169,4.86323844852254,
130.05815737776));
#132861=CARTESIAN_POINT('Ctrl Pts',(-231.660473714054,4.84056643523716,
129.922945598052));
#132862=CARTESIAN_POINT('Ctrl Pts',(-231.668230754939,4.81225999435761,
129.788813075988));
#132863=CARTESIAN_POINT('Ctrl Pts',(-231.675981946179,4.78397489958527,
129.654781704302));
#132864=CARTESIAN_POINT('Ctrl Pts',(-231.683733137419,4.75006391492926,
129.521828351282));
#132865=CARTESIAN_POINT('Ctrl Pts',(-231.691484328659,4.71063273119703,
129.390457390936));
#132866=CARTESIAN_POINT('Ctrl Pts',(-231.699232225436,4.67121830676979,
129.259142266752));
#132867=CARTESIAN_POINT('Ctrl Pts',(-231.706980122213,4.6262884619024,129.129408571252));
#132868=CARTESIAN_POINT('Ctrl Pts',(-231.71472801899,4.57599940680393,129.001747932758));
#132869=CARTESIAN_POINT('Ctrl Pts',(-231.722474295074,4.52572087109168,
128.874113998118));
#132870=CARTESIAN_POINT('Ctrl Pts',(-231.730220571158,4.47008549814481,
128.748552621482));
#132871=CARTESIAN_POINT('Ctrl Pts',(-231.737966847243,4.40929840793594,
128.62553740026));
#132872=CARTESIAN_POINT('Ctrl Pts',(-231.745713180508,4.3485108690105,128.502521270967));
#132873=CARTESIAN_POINT('Ctrl Pts',(-231.753459513773,4.28257171013996,
128.3820516851));
#132874=CARTESIAN_POINT('Ctrl Pts',(-231.761205847039,4.21173278590663,
128.264579130387));
#132875=CARTESIAN_POINT('Ctrl Pts',(-231.768953915042,4.14087799778748,
128.14708026851));
#132876=CARTESIAN_POINT('Ctrl Pts',(-231.776701983045,4.06512146272388,
128.032580108064));
#132877=CARTESIAN_POINT('Ctrl Pts',(-231.784450051048,3.98475905510755,
127.921501214952));
#132878=CARTESIAN_POINT('Ctrl Pts',(-231.792206353789,3.9043112373682,127.810304265871));
#132879=CARTESIAN_POINT('Ctrl Pts',(-231.799962656531,3.81924799796628,
127.702536165017));
#132880=CARTESIAN_POINT('Ctrl Pts',(-231.807718959273,3.7299066499115,127.598587786337));
#132881=CARTESIAN_POINT('Ctrl Pts',(-231.815479401787,3.64051761768901,
127.494583927278));
#132882=CARTESIAN_POINT('Ctrl Pts',(-231.823239844301,3.54684619392603,
127.394404138112));
#132883=CARTESIAN_POINT('Ctrl Pts',(-231.831000286816,3.44926674886565,
127.298402551977));
#132884=CARTESIAN_POINT('Ctrl Pts',(-231.838773187081,3.35153066061737,
127.202246855573));
#132885=CARTESIAN_POINT('Ctrl Pts',(-231.846546087346,3.24987430471133,
127.110283027805));
#132886=CARTESIAN_POINT('Ctrl Pts',(-231.854318987612,3.1447060120775,127.022825590609));
#132887=CARTESIAN_POINT('Ctrl Pts',(-231.861809323374,3.04336085178356,
126.938547451546));
#132888=CARTESIAN_POINT('Ctrl Pts',(-231.869299659136,2.93875490181847,
126.858453941278));
#132889=CARTESIAN_POINT('Ctrl Pts',(-231.876789994898,2.83127750650062,
126.782787449801));
#132890=CARTESIAN_POINT('Ctrl Pts',(-231.884564329017,2.7197250730724,126.704252040302));
#132891=CARTESIAN_POINT('Ctrl Pts',(-231.892338663136,2.60472578972233,
126.6302372007));
#132892=CARTESIAN_POINT('Ctrl Pts',(-231.900112997255,2.48668222910833,
126.561060657165));
#132893=CARTESIAN_POINT('Ctrl Pts',(-231.907877750202,2.36878414663293,
126.491969367538));
#132894=CARTESIAN_POINT('Ctrl Pts',(-231.91564250315,2.24784958593007,126.427704705626));
#132895=CARTESIAN_POINT('Ctrl Pts',(-231.923407256097,2.1243120700664,126.36854262181));
#132896=CARTESIAN_POINT('Ctrl Pts',(-231.931164296982,2.00089725340506,
126.30943929861));
#132897=CARTESIAN_POINT('Ctrl Pts',(-231.938921337867,1.87488497676378,
126.255428635828));
#132898=CARTESIAN_POINT('Ctrl Pts',(-231.946678378752,1.74673516440225,
126.206741741676));
#132899=CARTESIAN_POINT('Ctrl Pts',(-231.954429569992,1.61868199081126,
126.158091562689));
#132900=CARTESIAN_POINT('Ctrl Pts',(-231.962180761232,1.48849485395208,
126.114757299616));
#132901=CARTESIAN_POINT('Ctrl Pts',(-231.969931952472,1.35665522642646,
126.076922658258));
#132902=CARTESIAN_POINT('Ctrl Pts',(-231.977679849249,1.2248716342593,126.039104097631));
#132903=CARTESIAN_POINT('Ctrl Pts',(-231.985427746026,1.09143732336178,
126.006780617258));
#132904=CARTESIAN_POINT('Ctrl Pts',(-231.993175642803,0.956850350000342,
125.980086530182));
#132905=CARTESIAN_POINT('Ctrl Pts',(-232.000921918888,0.822291529332377,
125.953398026934));
#132906=CARTESIAN_POINT('Ctrl Pts',(-232.008668194972,0.686580909037609,
125.932336650791));
#132907=CARTESIAN_POINT('Ctrl Pts',(-232.016414471056,0.550227812385761,
125.916985819479));
#132908=CARTESIAN_POINT('Ctrl Pts',(-232.024160804321,0.413873709206515,
125.901634874851));
#132909=CARTESIAN_POINT('Ctrl Pts',(-232.031907137587,0.276877508717496,
125.891994602908));
#132910=CARTESIAN_POINT('Ctrl Pts',(-232.039653470852,0.139754352556722,
125.888096610879));
#132911=CARTESIAN_POINT('Ctrl Pts',(-232.047401538855,0.00260048861568343,
125.884197745922));
#132912=CARTESIAN_POINT('Ctrl Pts',(-232.055149606858,-0.134679996838661,
125.886043730865));
#132913=CARTESIAN_POINT('Ctrl Pts',(-232.062897674861,-0.271571659809338,
125.893614045395));
#132914=CARTESIAN_POINT('Ctrl Pts',(-232.070653977603,-0.408608812868637,
125.901192405745));
#132915=CARTESIAN_POINT('Ctrl Pts',(-232.078410280345,-0.545255926951344,
125.914507227276));
#132916=CARTESIAN_POINT('Ctrl Pts',(-232.086166583086,-0.681001822813728,
125.933485995917));
#132917=CARTESIAN_POINT('Ctrl Pts',(-232.093927025601,-0.816820170347593,
125.952474894098));
#132918=CARTESIAN_POINT('Ctrl Pts',(-232.101687468115,-0.951735956807356,
125.977133692751));
#132919=CARTESIAN_POINT('Ctrl Pts',(-232.109447910629,-1.08524888369458,
126.007338841199));
#132920=CARTESIAN_POINT('Ctrl Pts',(-232.117220810894,-1.21897613738514,
126.037592477633));
#132921=CARTESIAN_POINT('Ctrl Pts',(-232.12499371116,-1.3512956536994,126.073410153665));
#132922=CARTESIAN_POINT('Ctrl Pts',(-232.132766611425,-1.48172210358327,
126.114618335707));
#132923=CARTESIAN_POINT('Ctrl Pts',(-232.140256947187,-1.60740722348663,
126.154328496535));
#132924=CARTESIAN_POINT('Ctrl Pts',(-232.147747282949,-1.73133423313736,
126.199043946141));
#132925=CARTESIAN_POINT('Ctrl Pts',(-232.155237618711,-1.85308875285092,
126.248568135839));
#132926=CARTESIAN_POINT('Ctrl Pts',(-232.163012308585,-1.97946541494861,
126.299972402407));
#132927=CARTESIAN_POINT('Ctrl Pts',(-232.17078699846,-2.10390172246025,
126.356720569307));
#132928=CARTESIAN_POINT('Ctrl Pts',(-232.178561688334,-2.22591269676149,
126.418645655454));
#132929=CARTESIAN_POINT('Ctrl Pts',(-232.186326715409,-2.34777202931791,
126.480493777801));
#132930=CARTESIAN_POINT('Ctrl Pts',(-232.194091742484,-2.46721168116132,
126.547505841568));
#132931=CARTESIAN_POINT('Ctrl Pts',(-232.20185676956,-2.58376510944525,
126.619466243545));
#132932=CARTESIAN_POINT('Ctrl Pts',(-232.209614003292,-2.70020155928215,
126.691354422712));
#132933=CARTESIAN_POINT('Ctrl Pts',(-232.217371237025,-2.81375721993365,
126.768180852184));
#132934=CARTESIAN_POINT('Ctrl Pts',(-232.225128470757,-2.92398902249743,
126.849683480452));
#132935=CARTESIAN_POINT('Ctrl Pts',(-232.233044773429,-3.03648122567941,
126.932857392206));
#132936=CARTESIAN_POINT('Ctrl Pts',(-232.240961076101,-3.14551139310726,
127.020901197916));
#132937=CARTESIAN_POINT('Ctrl Pts',(-232.248877378773,-3.25063799032476,
127.113488672028));
#132938=CARTESIAN_POINT('Ctrl Pts',(-232.256624933656,-3.35352365744953,
127.204102506144));
#132939=CARTESIAN_POINT('Ctrl Pts',(-232.264372488539,-3.45267019726962,
127.299067970012));
#132940=CARTESIAN_POINT('Ctrl Pts',(-232.272120043421,-3.54769618352665,
127.398037841919));
#132941=CARTESIAN_POINT('Ctrl Pts',(-232.279865897953,-3.64270131449172,
127.496985992972));
#132942=CARTESIAN_POINT('Ctrl Pts',(-232.287611752485,-3.73358742085743,
127.599936521495));
#132943=CARTESIAN_POINT('Ctrl Pts',(-232.295357607017,-3.82000989958489,
127.706505322435));
#132944=CARTESIAN_POINT('Ctrl Pts',(-232.303103438983,-3.9064321265463,
127.813073812918));
#132945=CARTESIAN_POINT('Ctrl Pts',(-232.31084927095,-3.98839050616377,
127.923260250786));
#132946=CARTESIAN_POINT('Ctrl Pts',(-232.318595102916,-4.06558095916253,
128.036647748247));
#132947=CARTESIAN_POINT('Ctrl Pts',(-232.326638822247,-4.1457399842507,
128.154395875127));
#132948=CARTESIAN_POINT('Ctrl Pts',(-232.334682541578,-4.22075675822784,
128.275595825386));
#132949=CARTESIAN_POINT('Ctrl Pts',(-232.342726260909,-4.29034091977056,
128.399748828806));
#132950=CARTESIAN_POINT('Ctrl Pts',(-232.350480606593,-4.35742178380676,
128.519435414913));
#132951=CARTESIAN_POINT('Ctrl Pts',(-232.358234952278,-4.41945400593222,
128.64186588242));
#132952=CARTESIAN_POINT('Ctrl Pts',(-232.365989297962,-4.47622530264491,
128.766570122333));
#132953=CARTESIAN_POINT('Ctrl Pts',(-232.373747825468,-4.53302721540442,
128.891341613675));
#132954=CARTESIAN_POINT('Ctrl Pts',(-232.381506352974,-4.58456240334656,
129.018388959012));
#132955=CARTESIAN_POINT('Ctrl Pts',(-232.389264880479,-4.63066746230612,
129.147223955718));
#132956=CARTESIAN_POINT('Ctrl Pts',(-232.397032317361,-4.67682546524075,
129.276206897944));
#132957=CARTESIAN_POINT('Ctrl Pts',(-232.404799754242,-4.71754077822091,
129.406981216686));
#132958=CARTESIAN_POINT('Ctrl Pts',(-232.412567191124,-4.75270031384212,
129.539045325117));
#132959=CARTESIAN_POINT('Ctrl Pts',(-232.413418039044,-4.75655170243177,
129.553511676601));
#132960=CARTESIAN_POINT('Ctrl Pts',(-232.414268886965,-4.76033647757936,
129.567993496235));
#132961=CARTESIAN_POINT('Ctrl Pts',(-232.415119734886,-4.76405452823408,
129.582490119308));
#132962=CARTESIAN_POINT('Ctrl Pts',(-230.664999534934,-4.76405452823392,
129.582490119308));
#132963=CARTESIAN_POINT('Ctrl Pts',(-230.672659072166,-4.7977324481482,
129.71379981792));
#132964=CARTESIAN_POINT('Ctrl Pts',(-230.680318609397,-4.82595448970105,
129.846413917723));
#132965=CARTESIAN_POINT('Ctrl Pts',(-230.687978146629,-4.84864291544807,
129.979833516146));
#132966=CARTESIAN_POINT('Ctrl Pts',(-230.69583854952,-4.8719263282634,130.116751944177));
#132967=CARTESIAN_POINT('Ctrl Pts',(-230.703698952411,-4.88938183373582,
130.254518247733));
#132968=CARTESIAN_POINT('Ctrl Pts',(-230.711559355303,-4.90098232377429,
130.392589656288));
#132969=CARTESIAN_POINT('Ctrl Pts',(-230.719419758194,-4.91258281381275,
130.530661064843));
#132970=CARTESIAN_POINT('Ctrl Pts',(-230.727280161085,-4.91832833215937,
130.669037125676));
#132971=CARTESIAN_POINT('Ctrl Pts',(-230.735140563976,-4.91824919291643,
130.807178218823));
#132972=CARTESIAN_POINT('',(-230.389859436043,-4.91824944680572,130.806693318839));
#132973=CARTESIAN_POINT('Ctrl Pts',(-230.320068668528,-4.76405452823411,
129.582490119308));
#132974=CARTESIAN_POINT('Ctrl Pts',(-230.327945977475,-4.79869332603803,
129.717546266229));
#132975=CARTESIAN_POINT('Ctrl Pts',(-230.335823286422,-4.82760892536237,
129.854170273547));
#132976=CARTESIAN_POINT('Ctrl Pts',(-230.343700595369,-4.85067044761666,
129.991846450847));
#132977=CARTESIAN_POINT('Ctrl Pts',(-230.351573717171,-4.87371971163376,
130.129449447062));
#132978=CARTESIAN_POINT('Ctrl Pts',(-230.359446838974,-4.89092103358712,
130.268103132679));
#132979=CARTESIAN_POINT('Ctrl Pts',(-230.367319960776,-4.90219449651391,
130.407281052682));
#132980=CARTESIAN_POINT('Ctrl Pts',(-230.374833119183,-4.91295253060557,
130.540095682749));
#132981=CARTESIAN_POINT('Ctrl Pts',(-230.382346277589,-4.91831267314133,
130.673387350445));
#132982=CARTESIAN_POINT('Ctrl Pts',(-230.389859435996,-4.91824944680612,
130.806693317998));
#132983=CARTESIAN_POINT('Ctrl Pts',(-230.389859436043,-4.91824944680572,
130.806693318839));
#132984=CARTESIAN_POINT('Ctrl Pts',(-230.398353064532,-4.91817796938352,
130.957395766794));
#132985=CARTESIAN_POINT('Ctrl Pts',(-230.406846693021,-4.91117576199927,
131.107866546464));
#132986=CARTESIAN_POINT('Ctrl Pts',(-230.41534032151,-4.89733120001217,
131.257494350461));
#132987=CARTESIAN_POINT('Ctrl Pts',(-230.423875977821,-4.88341813293515,
131.407862536579));
#132988=CARTESIAN_POINT('Ctrl Pts',(-230.432411634131,-4.86259491593276,
131.557379136073));
#132989=CARTESIAN_POINT('Ctrl Pts',(-230.440947290442,-4.83500161639621,
131.705439100244));
#132990=CARTESIAN_POINT('Ctrl Pts',(-230.449504551637,-4.80733847453758,
131.853873823936));
#132991=CARTESIAN_POINT('Ctrl Pts',(-230.458061812833,-4.77287105429389,
132.000844296161));
#132992=CARTESIAN_POINT('Ctrl Pts',(-230.466619074028,-4.73178941265174,
132.145759893254));
#132993=CARTESIAN_POINT('Ctrl Pts',(-230.475206302526,-4.69056390418703,
132.291182980936));
#132994=CARTESIAN_POINT('Ctrl Pts',(-230.483793531024,-4.64267789167879,
132.434536548416));
#132995=CARTESIAN_POINT('Ctrl Pts',(-230.492380759522,-4.58837081720295,
132.575246358189));
#132996=CARTESIAN_POINT('Ctrl Pts',(-230.496300797012,-4.56357984209304,
132.639479856779));
#132997=CARTESIAN_POINT('Ctrl Pts',(-230.500220834503,-4.53745142796362,
132.703162757044));
#132998=CARTESIAN_POINT('Ctrl Pts',(-230.504140871994,-4.51001150550466,
132.76624218451));
#132999=CARTESIAN_POINT('Ctrl Pts',(-230.511915206113,-4.4555918409206,
132.891343167941));
#133000=CARTESIAN_POINT('Ctrl Pts',(-230.519689540232,-4.39587686309395,
133.014376306061));
#133001=CARTESIAN_POINT('Ctrl Pts',(-230.527463874351,-4.33104511752674,
133.134860832637));
#133002=CARTESIAN_POINT('Ctrl Pts',(-230.535228627298,-4.26629327129177,
133.255196872803));
#133003=CARTESIAN_POINT('Ctrl Pts',(-230.542993380245,-4.19643738777442,
133.37299020997));
#133004=CARTESIAN_POINT('Ctrl Pts',(-230.550758133192,-4.12170417679129,
133.48777965706));
#133005=CARTESIAN_POINT('Ctrl Pts',(-230.558515174077,-4.04704519188666,
133.602455093654));
#133006=CARTESIAN_POINT('Ctrl Pts',(-230.566272214962,-3.96751873168534,
133.714132251955));
#133007=CARTESIAN_POINT('Ctrl Pts',(-230.574029255847,-3.88339738009621,
133.82237450931));
#133008=CARTESIAN_POINT('Ctrl Pts',(-230.581780447088,-3.79933946507302,
133.930535140337));
#133009=CARTESIAN_POINT('Ctrl Pts',(-230.589531638328,-3.71069379456016,
134.03526571877));
#133010=CARTESIAN_POINT('Ctrl Pts',(-230.597282829568,-3.61777601372976,
134.136158897321));
#133011=CARTESIAN_POINT('Ctrl Pts',(-230.605030726345,-3.52489772543451,
134.237009193581));
#133012=CARTESIAN_POINT('Ctrl Pts',(-230.612778623122,-3.42775120253087,
134.334025046904));
#133013=CARTESIAN_POINT('Ctrl Pts',(-230.620526519899,-3.32669194667371,
134.42683266776));
#133014=CARTESIAN_POINT('Ctrl Pts',(-230.628272795983,-3.22565383023456,
134.519620875262));
#133015=CARTESIAN_POINT('Ctrl Pts',(-230.636019072067,-3.12070489658031,
134.608202336927));
#133016=CARTESIAN_POINT('Ctrl Pts',(-230.643765348152,-3.01223674471693,
134.692240869873));
#133017=CARTESIAN_POINT('Ctrl Pts',(-230.651511681417,-2.90376779216615,
134.776280023172));
#133018=CARTESIAN_POINT('Ctrl Pts',(-230.659258014682,-2.79177987862718,
134.855775941387));
#133019=CARTESIAN_POINT('Ctrl Pts',(-230.667004347948,-2.67669652306891,
134.930433664167));
#133020=CARTESIAN_POINT('Ctrl Pts',(-230.674752415951,-2.56158739539156,
135.005108106027));
#133021=CARTESIAN_POINT('Ctrl Pts',(-230.682500483953,-2.44338177423179,
135.074941983716));
#133022=CARTESIAN_POINT('Ctrl Pts',(-230.690248551956,-2.32253055245363,
135.139684699503));
#133023=CARTESIAN_POINT('Ctrl Pts',(-230.698004854698,-2.20155088855865,
135.204496224618));
#133024=CARTESIAN_POINT('Ctrl Pts',(-230.70576115744,-2.07792035239654,
135.264205593964));
#133025=CARTESIAN_POINT('Ctrl Pts',(-230.713517460182,-1.95211324056038,
135.318608833884));
#133026=CARTESIAN_POINT('Ctrl Pts',(-230.721277902696,-1.82623898168032,
135.373041110451));
#133027=CARTESIAN_POINT('Ctrl Pts',(-230.72903834521,-1.69818619718442,
135.422161474557));
#133028=CARTESIAN_POINT('Ctrl Pts',(-230.736798787724,-1.56844643906889,
135.465815200663));
#133029=CARTESIAN_POINT('Ctrl Pts',(-230.74457168799,-1.43849841117587,
135.509539003604));
#133030=CARTESIAN_POINT('Ctrl Pts',(-230.752344588255,-1.3068583737185,
135.54777852311));
#133031=CARTESIAN_POINT('Ctrl Pts',(-230.760117488521,-1.17403109400243,
135.580429508696));
#133032=CARTESIAN_POINT('Ctrl Pts',(-230.767607824283,-1.04603242047541,
135.611893548712));
#133033=CARTESIAN_POINT('Ctrl Pts',(-230.775098160045,-0.916931626398108,
135.638168253731));
#133034=CARTESIAN_POINT('Ctrl Pts',(-230.782588495807,-0.787184856237522,
135.659205935865));
#133035=CARTESIAN_POINT('Ctrl Pts',(-230.790362829926,-0.652518697851182,
135.681041268111));
#133036=CARTESIAN_POINT('Ctrl Pts',(-230.798137164045,-0.516730030136942,
135.697303782455));
#133037=CARTESIAN_POINT('Ctrl Pts',(-230.805911498164,-0.380319843546427,
135.707883828392));
#133038=CARTESIAN_POINT('Ctrl Pts',(-230.813676251111,-0.244077770319558,
135.718450835367));
#133039=CARTESIAN_POINT('Ctrl Pts',(-230.821441004058,-0.107216088313928,
135.723349278144));
#133040=CARTESIAN_POINT('Ctrl Pts',(-230.829205757005,0.0297546505254653,
135.722520611229));
#133041=CARTESIAN_POINT('Ctrl Pts',(-230.83696279789,0.166589348096094,
135.721692767359));
#133042=CARTESIAN_POINT('Ctrl Pts',(-230.844719838775,0.303532498517019,
135.715149136013));
#133043=CARTESIAN_POINT('Ctrl Pts',(-230.85247687966,0.440069420521692,
135.702883044546));
#133044=CARTESIAN_POINT('Ctrl Pts',(-230.8602280709,0.576503378971193,135.690626203033));
#133045=CARTESIAN_POINT('Ctrl Pts',(-230.86797926214,0.712531330934243,
135.672655525684));
#133046=CARTESIAN_POINT('Ctrl Pts',(-230.87573045338,0.847639949674806,
135.649016392563));
#133047=CARTESIAN_POINT('Ctrl Pts',(-230.883478350158,0.982691143648449,
135.625387306705));
#133048=CARTESIAN_POINT('Ctrl Pts',(-230.891226246935,1.11682339724522,
135.596094624118));
#133049=CARTESIAN_POINT('Ctrl Pts',(-230.898974143712,1.24953007342004,
135.561235396044));
#133050=CARTESIAN_POINT('Ctrl Pts',(-230.906720419796,1.38220899021903,
135.526383459769));
#133051=CARTESIAN_POINT('Ctrl Pts',(-230.91446669588,1.51346254483487,135.485967393329));
#133052=CARTESIAN_POINT('Ctrl Pts',(-230.922212971964,1.64279622826155,
135.440134945001));
#133053=CARTESIAN_POINT('Ctrl Pts',(-230.929959305229,1.77213086640027,
135.394302158349));
#133054=CARTESIAN_POINT('Ctrl Pts',(-230.937705638495,1.89954523656009,
135.343053040617));
#133055=CARTESIAN_POINT('Ctrl Pts',(-230.94545197176,2.02456225789857,135.286584477035));
#133056=CARTESIAN_POINT('Ctrl Pts',(-230.953200039763,2.14960727593201,
135.23010326771));
#133057=CARTESIAN_POINT('Ctrl Pts',(-230.960948107766,2.27225352059958,
135.168400447549));
#133058=CARTESIAN_POINT('Ctrl Pts',(-230.968696175769,2.39204643832679,
135.101719911294));
#133059=CARTESIAN_POINT('Ctrl Pts',(-230.976452478511,2.51196667339268,
135.034968506171));
#133060=CARTESIAN_POINT('Ctrl Pts',(-230.984208781252,2.62902718151966,
134.963229007313));
#133061=CARTESIAN_POINT('Ctrl Pts',(-230.991965083994,2.74279998500172,
134.886790201132));
#133062=CARTESIAN_POINT('Ctrl Pts',(-230.999725526508,2.85663351245464,
134.810310597259));
#133063=CARTESIAN_POINT('Ctrl Pts',(-231.007485969023,2.96717552382122,
134.72912691965));
#133064=CARTESIAN_POINT('Ctrl Pts',(-231.015246411537,3.07403014826247,
134.643569091988));
#133065=CARTESIAN_POINT('Ctrl Pts',(-231.023019311802,3.18105630523297,
134.557873919305));
#133066=CARTESIAN_POINT('Ctrl Pts',(-231.030792212067,3.2843829517253,134.467790821898));
#133067=CARTESIAN_POINT('Ctrl Pts',(-231.038565112333,3.38364953979536,
134.373688124862));
#133068=CARTESIAN_POINT('Ctrl Pts',(-231.046055448095,3.4793075373519,134.283006297894));
#133069=CARTESIAN_POINT('Ctrl Pts',(-231.053545783857,3.57119532348375,
134.18859226337));
#133070=CARTESIAN_POINT('Ctrl Pts',(-231.061036119619,3.65902621979407,
134.090804012082));
#133071=CARTESIAN_POINT('Ctrl Pts',(-231.068810453738,3.75018725123324,
133.989308089525));
#133072=CARTESIAN_POINT('Ctrl Pts',(-231.076584787857,3.83726645685091,
133.883855523879));
#133073=CARTESIAN_POINT('Ctrl Pts',(-231.084359121976,3.91990078699615,
133.774808543823));
#133074=CARTESIAN_POINT('Ctrl Pts',(-231.092123874923,4.00243327771474,
133.665895954425));
#133075=CARTESIAN_POINT('Ctrl Pts',(-231.09988862787,4.08053155851035,133.553398073202));
#133076=CARTESIAN_POINT('Ctrl Pts',(-231.107653380818,4.1538704076052,133.437712796695));
#133077=CARTESIAN_POINT('Ctrl Pts',(-231.115410421703,4.22713641552123,
133.322142420435));
#133078=CARTESIAN_POINT('Ctrl Pts',(-231.123167462588,4.29565219096999,
133.203391276975));
#133079=CARTESIAN_POINT('Ctrl Pts',(-231.130924503473,4.35913392226761,
133.081888775512));
#133080=CARTESIAN_POINT('Ctrl Pts',(-231.138675694713,4.42256778149777,
132.96047790003));
#133081=CARTESIAN_POINT('Ctrl Pts',(-231.146426885953,4.48097497239187,
132.836320141467));
#133082=CARTESIAN_POINT('Ctrl Pts',(-231.154178077193,4.534116208843,132.709871905175));
#133083=CARTESIAN_POINT('Ctrl Pts',(-231.16192597397,4.58723485885113,132.583477412758));
#133084=CARTESIAN_POINT('Ctrl Pts',(-231.169673870747,4.63509185481077,
132.454794738532));
#133085=CARTESIAN_POINT('Ctrl Pts',(-231.177421767524,4.67749499898044,
132.32430258916));
#133086=CARTESIAN_POINT('Ctrl Pts',(-231.185168043608,4.71988927332645,
132.193837735932));
#133087=CARTESIAN_POINT('Ctrl Pts',(-231.192914319692,4.75683184430455,
132.061564532012));
#133088=CARTESIAN_POINT('Ctrl Pts',(-231.200660595776,4.78817972252712,
131.927978883384));
#133089=CARTESIAN_POINT('Ctrl Pts',(-231.208406929042,4.81952783215265,
131.794392248657));
#133090=CARTESIAN_POINT('Ctrl Pts',(-231.216153262307,4.84528107729446,
131.659493530516));
#133091=CARTESIAN_POINT('Ctrl Pts',(-231.223899595572,4.86534722922412,
131.52379053186));
#133092=CARTESIAN_POINT('Ctrl Pts',(-231.231647663575,4.88541787482935,
131.388057143459));
#133093=CARTESIAN_POINT('Ctrl Pts',(-231.239395731579,4.89979883575703,
131.251519502826));
#133094=CARTESIAN_POINT('Ctrl Pts',(-231.247143799581,4.90844961025101,
131.114691869822));
#133095=CARTESIAN_POINT('Ctrl Pts',(-231.254900102323,4.91710957889109,
130.977718814781));
#133096=CARTESIAN_POINT('Ctrl Pts',(-231.262656405065,4.92002717073763,
130.8404555425));
#133097=CARTESIAN_POINT('Ctrl Pts',(-231.270412707807,4.91721401757565,
130.703418218855));
#133098=CARTESIAN_POINT('Ctrl Pts',(-231.278173150321,4.91439936294913,
130.566307754264));
#133099=CARTESIAN_POINT('Ctrl Pts',(-231.285933592835,4.90584789301795,
130.42942386862));
#133100=CARTESIAN_POINT('Ctrl Pts',(-231.29369403535,4.89162320406197,130.29327795108));
#133101=CARTESIAN_POINT('Ctrl Pts',(-231.301466935615,4.87737568037248,
130.156913480027));
#133102=CARTESIAN_POINT('Ctrl Pts',(-231.30923983588,4.85743679556057,130.021289731419));
#133103=CARTESIAN_POINT('Ctrl Pts',(-231.317012736146,4.83192154699064,
129.886909133166));
#133104=CARTESIAN_POINT('Ctrl Pts',(-231.324503071908,4.80733384197518,
129.757413608143));
#133105=CARTESIAN_POINT('Ctrl Pts',(-231.33199340767,4.77756823367429,129.629072719422));
#133106=CARTESIAN_POINT('Ctrl Pts',(-231.339483743432,4.74277095320295,
129.502321160424));
#133107=CARTESIAN_POINT('Ctrl Pts',(-231.347258077551,4.70665432326629,
129.370763777542));
#133108=CARTESIAN_POINT('Ctrl Pts',(-231.35503241167,4.66500253088041,129.24050188809));
#133109=CARTESIAN_POINT('Ctrl Pts',(-231.362806745789,4.61792409208834,
129.112036729473));
#133110=CARTESIAN_POINT('Ctrl Pts',(-231.370571498736,4.57090367326456,
128.983729892682));
#133111=CARTESIAN_POINT('Ctrl Pts',(-231.378336251684,4.51847004811209,
128.857215744476));
#133112=CARTESIAN_POINT('Ctrl Pts',(-231.386101004631,4.46078218794617,
128.732982975946));
#133113=CARTESIAN_POINT('Ctrl Pts',(-231.393858045516,4.40315162417623,
128.608873597154));
#133114=CARTESIAN_POINT('Ctrl Pts',(-231.401615086401,4.34027737419711,
128.487041441103));
#133115=CARTESIAN_POINT('Ctrl Pts',(-231.409372127286,4.27236730498015,
128.367957392762));
#133116=CARTESIAN_POINT('Ctrl Pts',(-231.417123318526,4.20450844727456,
128.248963146627));
#133117=CARTESIAN_POINT('Ctrl Pts',(-231.424874509766,4.13162152201772,
128.132713221525));
#133118=CARTESIAN_POINT('Ctrl Pts',(-231.432625701006,4.05396117597433,
128.019655633875));
#133119=CARTESIAN_POINT('Ctrl Pts',(-231.440373597783,3.97633383764977,
127.906646098716));
#133120=CARTESIAN_POINT('Ctrl Pts',(-231.44812149456,3.89393733462957,127.796826523967));
#133121=CARTESIAN_POINT('Ctrl Pts',(-231.455869391337,3.80707052881091,
127.690617363674));
#133122=CARTESIAN_POINT('Ctrl Pts',(-231.463615667421,3.72022189365538,
127.584430420047));
#133123=CARTESIAN_POINT('Ctrl Pts',(-231.471361943505,3.62890506301179,
127.481852691144));
#133124=CARTESIAN_POINT('Ctrl Pts',(-231.47910821959,3.5334599673727,127.383272527283));
#133125=CARTESIAN_POINT('Ctrl Pts',(-231.486854552855,3.43801416717946,
127.284691635726));
#133126=CARTESIAN_POINT('Ctrl Pts',(-231.49460088612,3.33844031313392,127.190108648978));
#133127=CARTESIAN_POINT('Ctrl Pts',(-231.502347219386,3.23511578231743,
127.099875641554));
#133128=CARTESIAN_POINT('Ctrl Pts',(-231.510095287389,3.1317681126888,127.009622427073));
#133129=CARTESIAN_POINT('Ctrl Pts',(-231.517843355392,3.02466838933307,
126.923721387475));
#133130=CARTESIAN_POINT('Ctrl Pts',(-231.525591423395,2.9142273814477,126.842484568051));
#133131=CARTESIAN_POINT('Ctrl Pts',(-231.533347726136,2.80366899554474,
126.761161409169));
#133132=CARTESIAN_POINT('Ctrl Pts',(-231.541104028878,2.68976254673618,
126.684512605008));
#133133=CARTESIAN_POINT('Ctrl Pts',(-231.54886033162,2.57294858725588,126.612807369683));
#133134=CARTESIAN_POINT('Ctrl Pts',(-231.556620774134,2.4560722806482,126.541063863115));
#133135=CARTESIAN_POINT('Ctrl Pts',(-231.564381216648,2.33628571252351,
126.474269373193));
#133136=CARTESIAN_POINT('Ctrl Pts',(-231.572141659163,2.2140535044062,126.412646812896));
#133137=CARTESIAN_POINT('Ctrl Pts',(-231.579914559428,2.09162507829717,
126.350925330595));
#133138=CARTESIAN_POINT('Ctrl Pts',(-231.587687459693,1.96674352325454,
126.29439253017));
#133139=CARTESIAN_POINT('Ctrl Pts',(-231.595460359959,1.83989370499123,
126.243223235637));
#133140=CARTESIAN_POINT('Ctrl Pts',(-231.602950695721,1.7176551971372,126.193914073847));
#133141=CARTESIAN_POINT('Ctrl Pts',(-231.610441031483,1.59358933430168,
126.149585337863));
#133142=CARTESIAN_POINT('Ctrl Pts',(-231.617931367245,1.4681408778606,126.110348961716));
#133143=CARTESIAN_POINT('Ctrl Pts',(-231.625705701364,1.3379360050645,126.069624926442));
#133144=CARTESIAN_POINT('Ctrl Pts',(-231.633480035483,1.20582917707458,
126.034258025945));
#133145=CARTESIAN_POINT('Ctrl Pts',(-231.641254369602,1.07230075468556,
126.004427893662));
#133146=CARTESIAN_POINT('Ctrl Pts',(-231.649019122549,0.938936894143365,
125.974634524352));
#133147=CARTESIAN_POINT('Ctrl Pts',(-231.656783875496,0.804155303032998,
125.950364430805));
#133148=CARTESIAN_POINT('Ctrl Pts',(-231.664548628443,0.668453058890205,
125.931748015423));
#133149=CARTESIAN_POINT('Ctrl Pts',(-231.672305669328,0.532885596129361,
125.913150090128));
#133150=CARTESIAN_POINT('Ctrl Pts',(-231.680062710214,0.396399684875361,
125.900194721065));
#133151=CARTESIAN_POINT('Ctrl Pts',(-231.687819751098,0.259503851162931,
125.892961548692));
#133152=CARTESIAN_POINT('Ctrl Pts',(-231.695570942339,0.122711251663413,
125.885733830911));
#133153=CARTESIAN_POINT('Ctrl Pts',(-231.703322133579,-0.0144902661576784,
125.884219741315));
#133154=CARTESIAN_POINT('Ctrl Pts',(-231.711073324819,-0.151586130600617,
125.888447202186));
#133155=CARTESIAN_POINT('Ctrl Pts',(-231.718821221596,-0.288623725644202,
125.892672866274));
#133156=CARTESIAN_POINT('Ctrl Pts',(-231.726569118373,-0.425555366661926,
125.902635215211));
#133157=CARTESIAN_POINT('Ctrl Pts',(-231.73431701515,-0.561865771601263,
125.918310073701));
#133158=CARTESIAN_POINT('Ctrl Pts',(-231.742063291234,-0.698147663342027,
125.933981653348));
#133159=CARTESIAN_POINT('Ctrl Pts',(-231.749809567318,-0.833808189320973,
125.955363321123));
#133160=CARTESIAN_POINT('Ctrl Pts',(-231.757555843402,-0.968336878681481,
125.982378996709));
#133161=CARTESIAN_POINT('Ctrl Pts',(-231.765302176668,-1.1028665611024,
126.009394871718));
#133162=CARTESIAN_POINT('Ctrl Pts',(-231.773048509933,-1.23626400692059,
126.04204476055));
#133163=CARTESIAN_POINT('Ctrl Pts',(-231.780794843198,-1.36802902434677,
126.080201470052));
#133164=CARTESIAN_POINT('Ctrl Pts',(-231.788542911201,-1.49982354963519,
126.118366724484));
#133165=CARTESIAN_POINT('Ctrl Pts',(-231.796290979204,-1.62998454362307,
126.162041144813));
#133166=CARTESIAN_POINT('Ctrl Pts',(-231.804039047207,-1.75802744298462,
126.211047807381));
#133167=CARTESIAN_POINT('Ctrl Pts',(-231.811795349949,-1.88620642786315,
126.260106554812));
#133168=CARTESIAN_POINT('Ctrl Pts',(-231.819551652691,-2.01226245551108,
126.314508725294));
#133169=CARTESIAN_POINT('Ctrl Pts',(-231.827307955433,-2.13573089922645,
126.374029186557));
#133170=CARTESIAN_POINT('Ctrl Pts',(-231.835068397947,-2.25926524176812,
126.433581415682));
#133171=CARTESIAN_POINT('Ctrl Pts',(-231.842828840461,-2.38020890387919,
126.498257194629));
#133172=CARTESIAN_POINT('Ctrl Pts',(-231.850589282975,-2.49812320327363,
126.567786114059));
#133173=CARTESIAN_POINT('Ctrl Pts',(-231.858362183241,-2.61622678916907,
126.637426647483));
#133174=CARTESIAN_POINT('Ctrl Pts',(-231.866135083506,-2.73129096616132,
126.711935677049));
#133175=CARTESIAN_POINT('Ctrl Pts',(-231.873907983772,-2.84290656809211,
126.790999768153));
#133176=CARTESIAN_POINT('Ctrl Pts',(-231.881398319534,-2.95046466174907,
126.867189680394));
#133177=CARTESIAN_POINT('Ctrl Pts',(-231.888888655296,-3.05482031212694,
126.947609039936));
#133178=CARTESIAN_POINT('Ctrl Pts',(-231.896378991058,-3.15563894156551,
127.031944159515));
#133179=CARTESIAN_POINT('Ctrl Pts',(-231.904042805045,-3.25879255804118,
127.118232503533));
#133180=CARTESIAN_POINT('Ctrl Pts',(-231.911706619032,-3.35858974585892,
127.208910327928));
#133181=CARTESIAN_POINT('Ctrl Pts',(-231.919370433019,-3.45462584472503,
127.303683063798));
#133182=CARTESIAN_POINT('Ctrl Pts',(-231.927025453236,-3.55055174788039,
127.398347053591));
#133183=CARTESIAN_POINT('Ctrl Pts',(-231.934680473452,-3.64272485724723,
127.497096335079));
#133184=CARTESIAN_POINT('Ctrl Pts',(-231.942335493669,-3.73077224957203,
127.599595183978));
#133185=CARTESIAN_POINT('Ctrl Pts',(-231.949983499379,-3.81873896164382,
127.702000110355));
#133186=CARTESIAN_POINT('Ctrl Pts',(-231.95763150509,-3.9025872127649,127.808147469355));
#133187=CARTESIAN_POINT('Ctrl Pts',(-231.9652795108,-3.98198015682655,127.917664046546));
#133188=CARTESIAN_POINT('Ctrl Pts',(-231.972922274665,-4.06131868597262,
128.027105562465));
#133189=CARTESIAN_POINT('Ctrl Pts',(-231.980565038529,-4.13620774589511,
128.139911378913));
#133190=CARTESIAN_POINT('Ctrl Pts',(-231.988207802394,-4.20635047176246,
128.255674922702));
#133191=CARTESIAN_POINT('Ctrl Pts',(-231.995847800743,-4.27646781665669,
128.371396577737));
#133192=CARTESIAN_POINT('Ctrl Pts',(-232.003487799092,-4.34184203188347,
128.49007348944));
#133193=CARTESIAN_POINT('Ctrl Pts',(-232.011127797441,-4.40221958282907,
128.611270148147));
#133194=CARTESIAN_POINT('Ctrl Pts',(-232.018766121419,-4.46258390151233,
128.732440245558));
#133195=CARTESIAN_POINT('Ctrl Pts',(-232.026404445396,-4.51795355806227,
128.856128629348));
#133196=CARTESIAN_POINT('Ctrl Pts',(-232.034042769374,-4.56812131761873,
128.981875860423));
#133197=CARTESIAN_POINT('Ctrl Pts',(-232.04168307152,-4.61830206959523,
129.10765565745));
#133198=CARTESIAN_POINT('Ctrl Pts',(-232.049323373667,-4.66327808431924,
129.235494992454));
#133199=CARTESIAN_POINT('Ctrl Pts',(-232.056963675813,-4.70289063616154,
129.364915333158));
#133200=CARTESIAN_POINT('Ctrl Pts',(-232.061217911688,-4.72494750457854,
129.436978537689));
#133201=CARTESIAN_POINT('Ctrl Pts',(-232.065472147562,-4.74534234988716,
129.509531619931));
#133202=CARTESIAN_POINT('Ctrl Pts',(-232.069726383436,-4.76405452823406,
129.582490119308));
#133203=CARTESIAN_POINT('Origin',(213.235140564004,0.,130.804360617566));
#133204=CARTESIAN_POINT('',(-234.165426035895,-4.76405452823417,129.582490119309));
#133205=CARTESIAN_POINT('',(-233.819813589496,-4.76405452823394,129.582490119308));
#133206=CARTESIAN_POINT('',(213.235140564004,-4.76405452823405,129.582490119308));
#133207=CARTESIAN_POINT('',(-232.485140564054,-4.91824815178585,130.800096821715));
#133208=CARTESIAN_POINT('Ctrl Pts',(-232.485140564054,-4.91824815178585,
130.800096821715));
#133209=CARTESIAN_POINT('Ctrl Pts',(-232.492787208904,-4.91836497210817,
130.934847957654));
#133210=CARTESIAN_POINT('Ctrl Pts',(-232.500433853755,-4.91293972528396,
131.069789047598));
#133211=CARTESIAN_POINT('Ctrl Pts',(-232.508080498605,-4.90195230449137,
131.204418947053));
#133212=CARTESIAN_POINT('Ctrl Pts',(-232.515720342521,-4.89097465592257,
131.338929106531));
#133213=CARTESIAN_POINT('Ctrl Pts',(-232.523360186437,-4.87444470582854,
131.473128226128));
#133214=CARTESIAN_POINT('Ctrl Pts',(-232.531000030354,-4.85239440291908,
131.606514979905));
#133215=CARTESIAN_POINT('Ctrl Pts',(-232.538635402698,-4.83035700596813,
131.739823662922));
#133216=CARTESIAN_POINT('Ctrl Pts',(-232.546270775043,-4.80280574736142,
131.872320528752));
#133217=CARTESIAN_POINT('Ctrl Pts',(-232.553906147388,-4.76982438423958,
132.003509651679));
#133218=CARTESIAN_POINT('Ctrl Pts',(-232.561539218865,-4.73685295982771,
132.134659241654));
#133219=CARTESIAN_POINT('Ctrl Pts',(-232.569172290342,-4.69845478193037,
132.26450148112));
#133220=CARTESIAN_POINT('Ctrl Pts',(-232.576805361819,-4.65476455977488,
132.39255139816));
#133221=CARTESIAN_POINT('Ctrl Pts',(-232.584437899556,-4.61107739264138,
132.520592361358));
#133222=CARTESIAN_POINT('Ctrl Pts',(-232.592070437294,-4.56209904742062,
132.646840869405));
#133223=CARTESIAN_POINT('Ctrl Pts',(-232.599702975031,-4.5080136976276,
132.770828406395));
#133224=CARTESIAN_POINT('Ctrl Pts',(-232.607336745517,-4.45391961238895,
132.894835968889));
#133225=CARTESIAN_POINT('Ctrl Pts',(-232.614970516002,-4.39471704425763,
133.016581464515));
#133226=CARTESIAN_POINT('Ctrl Pts',(-232.622604286488,-4.33063753442429,
133.135618134001));
#133227=CARTESIAN_POINT('Ctrl Pts',(-232.63024567639,-4.26649406557284,
133.254773616327));
#133228=CARTESIAN_POINT('Ctrl Pts',(-232.637887066292,-4.19746412495438,
133.371214516855));
#133229=CARTESIAN_POINT('Ctrl Pts',(-232.645528456194,-4.12382445759133,
133.48452011011));
#133230=CARTESIAN_POINT('Ctrl Pts',(-232.653173703627,-4.05014761540808,
133.597882902361));
#133231=CARTESIAN_POINT('Ctrl Pts',(-232.66081895106,-3.97185664666404,
133.708106907284));
#133232=CARTESIAN_POINT('Ctrl Pts',(-232.668464198493,-3.88926974207377,
133.81480309931));
#133233=CARTESIAN_POINT('Ctrl Pts',(-232.676121423645,-3.80655344955241,
133.921666451004));
#133234=CARTESIAN_POINT('Ctrl Pts',(-232.683778648797,-3.71952803684931,
134.024990640997));
#133235=CARTESIAN_POINT('Ctrl Pts',(-232.691435873949,-3.62855026895896,
134.124421762807));
#133236=CARTESIAN_POINT('Ctrl Pts',(-232.698334871412,-3.5465812296047,
134.214007094758));
#133237=CARTESIAN_POINT('Ctrl Pts',(-232.705233868875,-3.46140445807237,
134.300432531783));
#133238=CARTESIAN_POINT('Ctrl Pts',(-232.712132866337,-3.37330352024979,
134.38346754846));
#133239=CARTESIAN_POINT('Ctrl Pts',(-232.719907200456,-3.27402443940633,
134.477037950061));
#133240=CARTESIAN_POINT('Ctrl Pts',(-232.727681534575,-3.17069190232462,
134.566622649829));
#133241=CARTESIAN_POINT('Ctrl Pts',(-232.735455868695,-3.06365932118117,
134.651850010175));
#133242=CARTESIAN_POINT('Ctrl Pts',(-232.743220621642,-2.9567586481285,
134.736972335416));
#133243=CARTESIAN_POINT('Ctrl Pts',(-232.750985374589,-2.84616730691387,
134.817747764795));
#133244=CARTESIAN_POINT('Ctrl Pts',(-232.758750127536,-2.73227527506937,
134.89384162177));
#133245=CARTESIAN_POINT('Ctrl Pts',(-232.766507168421,-2.6184963623965,
134.969859901253));
#133246=CARTESIAN_POINT('Ctrl Pts',(-232.774264209306,-2.50142360602416,
135.041205645862));
#133247=CARTESIAN_POINT('Ctrl Pts',(-232.782021250191,-2.38147948079228,
135.107584821005));
#133248=CARTESIAN_POINT('Ctrl Pts',(-232.789772441431,-2.26162580635811,
135.173913939096));
#133249=CARTESIAN_POINT('Ctrl Pts',(-232.797523632671,-2.1389054136967,
135.235283754028));
#133250=CARTESIAN_POINT('Ctrl Pts',(-232.805274823911,-2.01376883452175,
135.291444096131));
#133251=CARTESIAN_POINT('Ctrl Pts',(-232.813022720688,-1.88868544173091,
135.34758056859));
#133252=CARTESIAN_POINT('Ctrl Pts',(-232.820770617465,-1.76118826088311,
135.398511812282));
#133253=CARTESIAN_POINT('Ctrl Pts',(-232.828518514242,-1.6317512485673,
135.444034197173));
#133254=CARTESIAN_POINT('Ctrl Pts',(-232.836264790326,-1.50234131168448,
135.489547059761));
#133255=CARTESIAN_POINT('Ctrl Pts',(-232.84401106641,-1.37099271902099,
135.529653184369));
#133256=CARTESIAN_POINT('Ctrl Pts',(-232.851757342494,-1.23819780240132,
135.564197722408));
#133257=CARTESIAN_POINT('Ctrl Pts',(-232.85950367576,-1.10540190551956,
135.598742515447));
#133258=CARTESIAN_POINT('Ctrl Pts',(-232.867250009025,-0.971160041750084,
135.627725541569));
#133259=CARTESIAN_POINT('Ctrl Pts',(-232.87499634229,-0.8359776545235,135.651042412737));
#133260=CARTESIAN_POINT('Ctrl Pts',(-232.882744410293,-0.700764994138032,
135.674364505556));
#133261=CARTESIAN_POINT('Ctrl Pts',(-232.890492478296,-0.564611776380961,
135.692017852022));
#133262=CARTESIAN_POINT('Ctrl Pts',(-232.898240546299,-0.42803114108908,
135.703949621223));
#133263=CARTESIAN_POINT('Ctrl Pts',(-232.905996849041,-0.291305346272868,
135.715894071651));
#133264=CARTESIAN_POINT('Ctrl Pts',(-232.913753151783,-0.154151616582536,
135.722104763362));
#133265=CARTESIAN_POINT('Ctrl Pts',(-232.921509454525,-0.0170862483816585,
135.722580938232));
#133266=CARTESIAN_POINT('Ctrl Pts',(-232.929269897039,0.120052275732813,
135.723057367252));
#133267=CARTESIAN_POINT('Ctrl Pts',(-232.937030339553,0.25710195389921,
135.717793195758));
#133268=CARTESIAN_POINT('Ctrl Pts',(-232.944790782067,0.393550018091851,
135.706839729787));
#133269=CARTESIAN_POINT('Ctrl Pts',(-232.952563682333,0.530217120830424,
135.695868680339));
#133270=CARTESIAN_POINT('Ctrl Pts',(-232.960336582598,0.666280291406744,
135.679190133444));
#133271=CARTESIAN_POINT('Ctrl Pts',(-232.968109482864,0.801234486979995,
135.656906996466));
#133272=CARTESIAN_POINT('Ctrl Pts',(-232.975599818625,0.931282757613221,
135.635433907645));
#133273=CARTESIAN_POINT('Ctrl Pts',(-232.983090154387,1.06030097985337,
135.608756698559));
#133274=CARTESIAN_POINT('Ctrl Pts',(-232.990580490149,1.18785107631667,
135.577011126769));
#133275=CARTESIAN_POINT('Ctrl Pts',(-232.998354824268,1.32023727345744,
135.544061911975));
#133276=CARTESIAN_POINT('Ctrl Pts',(-233.006129158388,1.45146117887392,
135.505548040452));
#133277=CARTESIAN_POINT('Ctrl Pts',(-233.013903492507,1.58101909542139,
135.461565968677));
#133278=CARTESIAN_POINT('Ctrl Pts',(-233.021668245454,1.71041734341494,
135.417638100874));
#133279=CARTESIAN_POINT('Ctrl Pts',(-233.029432998401,1.83815332110045,
135.36825556603));
#133280=CARTESIAN_POINT('Ctrl Pts',(-233.037197751348,1.96373466324294,
135.31356556244));
#133281=CARTESIAN_POINT('Ctrl Pts',(-233.044954792233,2.08919127622636,
135.258929877733));
#133282=CARTESIAN_POINT('Ctrl Pts',(-233.052711833118,2.21249715626237,
135.198997369802));
#133283=CARTESIAN_POINT('Ctrl Pts',(-233.060468874003,2.33317656575259,
135.133964545817));
#133284=CARTESIAN_POINT('Ctrl Pts',(-233.068220065243,2.45376496996152,
135.06898076359));
#133285=CARTESIAN_POINT('Ctrl Pts',(-233.075971256483,2.57173050319267,
134.998904505633));
#133286=CARTESIAN_POINT('Ctrl Pts',(-233.083722447723,2.68661916722265,
134.92397959422));
#133287=CARTESIAN_POINT('Ctrl Pts',(-233.0914703445,2.80145900050519,134.849086527894));
#133288=CARTESIAN_POINT('Ctrl Pts',(-233.099218241277,2.91322423881038,
134.76934912002));
#133289=CARTESIAN_POINT('Ctrl Pts',(-233.106966138054,3.02148737731084,
134.685056056692));
#133290=CARTESIAN_POINT('Ctrl Pts',(-233.114712414138,3.12972786949719,
134.600780625655));
#133291=CARTESIAN_POINT('Ctrl Pts',(-233.122458690222,3.23446741069658,
134.511951674658));
#133292=CARTESIAN_POINT('Ctrl Pts',(-233.130204966307,3.3353096050307,134.418899716966));
#133293=CARTESIAN_POINT('Ctrl Pts',(-233.137951299572,3.43615254375856,
134.325847072385));
#133294=CARTESIAN_POINT('Ctrl Pts',(-233.145697632837,3.53309779088441,
134.228571624038));
#133295=CARTESIAN_POINT('Ctrl Pts',(-233.153443966103,3.62578431727483,
134.127442191513));
#133296=CARTESIAN_POINT('Ctrl Pts',(-233.161192034106,3.71849160016981,
134.026290111752));
#133297=CARTESIAN_POINT('Ctrl Pts',(-233.168940102108,3.80693800044464,
133.921282618567));
#133298=CARTESIAN_POINT('Ctrl Pts',(-233.176688170111,3.89080170534141,
133.812822874636));
#133299=CARTESIAN_POINT('Ctrl Pts',(-233.184444472853,3.97475454158207,
133.704247858397));
#133300=CARTESIAN_POINT('Ctrl Pts',(-233.192200775595,4.05411471347774,
133.592213571788));
#133301=CARTESIAN_POINT('Ctrl Pts',(-233.199957078337,4.12860251240276,
133.477153979777));
#133302=CARTESIAN_POINT('Ctrl Pts',(-233.207717520851,4.20313006770885,
133.362032976998));
#133303=CARTESIAN_POINT('Ctrl Pts',(-233.215477963365,4.27277986981554,
133.243883788031));
#133304=CARTESIAN_POINT('Ctrl Pts',(-233.223238405879,4.33731792030103,
133.123165551306));
#133305=CARTESIAN_POINT('Ctrl Pts',(-233.231011306145,4.40195957299458,
133.002253526949));
#133306=CARTESIAN_POINT('Ctrl Pts',(-233.23878420641,4.46147290635544,132.878764566042));
#133307=CARTESIAN_POINT('Ctrl Pts',(-233.246557106676,4.5156715112712,132.753179199372));
#133308=CARTESIAN_POINT('Ctrl Pts',(-233.254047442438,4.56789986038125,
132.632159177109));
#133309=CARTESIAN_POINT('Ctrl Pts',(-233.2615377782,4.61519306940726,132.509192809611));
#133310=CARTESIAN_POINT('Ctrl Pts',(-233.269028113962,4.65742856350315,
132.384722044065));
#133311=CARTESIAN_POINT('Ctrl Pts',(-233.276802448081,4.70126542919421,
132.255531931613));
#133312=CARTESIAN_POINT('Ctrl Pts',(-233.2845767822,4.73979234451194,132.12431185522));
#133313=CARTESIAN_POINT('Ctrl Pts',(-233.292351116319,4.77281820041242,
131.991537726641));
#133314=CARTESIAN_POINT('Ctrl Pts',(-233.300115869266,4.80580335489693,
131.85892723031));
#133315=CARTESIAN_POINT('Ctrl Pts',(-233.307880622214,4.83330084581008,
131.724766868294));
#133316=CARTESIAN_POINT('Ctrl Pts',(-233.315645375161,4.85516837981154,
131.589550445683));
#133317=CARTESIAN_POINT('Ctrl Pts',(-233.323402416046,4.87701419467007,
131.454468321929));
#133318=CARTESIAN_POINT('Ctrl Pts',(-233.331159456931,4.8932411184438,131.31833260838));
#133319=CARTESIAN_POINT('Ctrl Pts',(-233.338916497816,4.90375733038771,
131.181649773478));
#133320=CARTESIAN_POINT('Ctrl Pts',(-233.346667689056,4.9142656119744,131.045070012165));
#133321=CARTESIAN_POINT('Ctrl Pts',(-233.354418880296,4.91907172367244,
130.907944338966));
#133322=CARTESIAN_POINT('Ctrl Pts',(-233.362170071536,4.91813540293703,
130.77078650734));
#133323=CARTESIAN_POINT('Ctrl Pts',(-233.369917968313,4.9171994801629,130.633686971452));
#133324=CARTESIAN_POINT('Ctrl Pts',(-233.37766586509,4.91052598195897,130.496555694459));
#133325=CARTESIAN_POINT('Ctrl Pts',(-233.385413761867,4.898126711311,130.359908390165));
#133326=CARTESIAN_POINT('Ctrl Pts',(-233.393160037952,4.88573003432314,
130.223289669542));
#133327=CARTESIAN_POINT('Ctrl Pts',(-233.400906314035,4.86761000250677,
130.087155109372));
#133328=CARTESIAN_POINT('Ctrl Pts',(-233.40865259012,4.84383042437688,129.952016859226));
#133329=CARTESIAN_POINT('Ctrl Pts',(-233.416398923385,4.82005067071157,
129.816877611521));
#133330=CARTESIAN_POINT('Ctrl Pts',(-233.42414525665,4.79061135512395,129.682735073565));
#133331=CARTESIAN_POINT('Ctrl Pts',(-233.431891589916,4.75562763091414,
129.550092345391));
#133332=CARTESIAN_POINT('Ctrl Pts',(-233.439639657919,4.72063607234171,
129.417419912796));
#133333=CARTESIAN_POINT('Ctrl Pts',(-233.447387725922,4.68009773412952,
129.286248336294));
#133334=CARTESIAN_POINT('Ctrl Pts',(-233.455135793925,4.63417786080164,
129.157066285348));
#133335=CARTESIAN_POINT('Ctrl Pts',(-233.462892096666,4.58820918328613,
129.027746938182));
#133336=CARTESIAN_POINT('Ctrl Pts',(-233.470648399408,4.53684767637541,
128.900421709468));
#133337=CARTESIAN_POINT('Ctrl Pts',(-233.47840470215,4.48030725774423,128.77556049466));
#133338=CARTESIAN_POINT('Ctrl Pts',(-233.486165144664,4.42373666178922,
128.650632637662));
#133339=CARTESIAN_POINT('Ctrl Pts',(-233.493925587178,4.36198182228225,
128.528171763974));
#133340=CARTESIAN_POINT('Ctrl Pts',(-233.501686029693,4.29530254352355,
128.408622918631));
#133341=CARTESIAN_POINT('Ctrl Pts',(-233.509458929958,4.22851622526691,
128.288882162868));
#133342=CARTESIAN_POINT('Ctrl Pts',(-233.517231830224,4.1567898754415,128.17206311025));
#133343=CARTESIAN_POINT('Ctrl Pts',(-233.525004730489,4.08042701953107,
128.058582330672));
#133344=CARTESIAN_POINT('Ctrl Pts',(-233.532495066251,4.00684014577942,
127.949226863272));
#133345=CARTESIAN_POINT('Ctrl Pts',(-233.539985402013,3.9289481928952,127.842971421854));
#133346=CARTESIAN_POINT('Ctrl Pts',(-233.547475737775,3.8470567288655,127.740158015356));
#133347=CARTESIAN_POINT('Ctrl Pts',(-233.555250071894,3.76206032508663,
127.633446407301));
#133348=CARTESIAN_POINT('Ctrl Pts',(-233.563024406013,3.67248589727299,
127.530104965787));
#133349=CARTESIAN_POINT('Ctrl Pts',(-233.570798740132,3.57863054435664,
127.430551718192));
#133350=CARTESIAN_POINT('Ctrl Pts',(-233.578563493079,3.48489085977491,
127.331121161077));
#133351=CARTESIAN_POINT('Ctrl Pts',(-233.586328246026,3.3868810130933,127.235469790483));
#133352=CARTESIAN_POINT('Ctrl Pts',(-233.594092998974,3.28493954349448,
127.143984235541));
#133353=CARTESIAN_POINT('Ctrl Pts',(-233.601850039859,3.18309932360012,
127.052589545341));
#133354=CARTESIAN_POINT('Ctrl Pts',(-233.609607080744,3.07733554089243,
126.965352696328));
#133355=CARTESIAN_POINT('Ctrl Pts',(-233.617364121629,2.96802467025874,
126.882624698456));
#133356=CARTESIAN_POINT('Ctrl Pts',(-233.625115312869,2.85879623180336,
126.799959086412));
#133357=CARTESIAN_POINT('Ctrl Pts',(-233.632866504109,2.74602634010971,
126.72179579268));
#133358=CARTESIAN_POINT('Ctrl Pts',(-233.640617695349,2.6301254676233,126.648446387573));
#133359=CARTESIAN_POINT('Ctrl Pts',(-233.648365592126,2.51427385609897,
126.575128157919));
#133360=CARTESIAN_POINT('Ctrl Pts',(-233.656113488903,2.39529424021625,
126.506619956129));
#133361=CARTESIAN_POINT('Ctrl Pts',(-233.66386138568,2.27362688440672,126.443190607924));
#133362=CARTESIAN_POINT('Ctrl Pts',(-233.671607661765,2.15198497878518,
126.379774527771));
#133363=CARTESIAN_POINT('Ctrl Pts',(-233.679353937848,2.02765679797953,
126.32143536868));
#133364=CARTESIAN_POINT('Ctrl Pts',(-233.687100213933,1.90110771798999,
126.268396276095));
#133365=CARTESIAN_POINT('Ctrl Pts',(-233.694846547198,1.77455770384406,
126.215356791987));
#133366=CARTESIAN_POINT('Ctrl Pts',(-233.702592880463,1.64578711837715,
126.167617603576));
#133367=CARTESIAN_POINT('Ctrl Pts',(-233.710339213729,1.51528147706566,
126.125353766987));
#133368=CARTESIAN_POINT('Ctrl Pts',(-233.718087281732,1.38474660992119,
126.083080465705));
#133369=CARTESIAN_POINT('Ctrl Pts',(-233.725835349735,1.25247628563114,
126.046285076606));
#133370=CARTESIAN_POINT('Ctrl Pts',(-233.733583417738,1.11897095435657,
126.015092712572));
#133371=CARTESIAN_POINT('Ctrl Pts',(-233.741339720479,0.985323732026644,
125.983867196922));
#133372=CARTESIAN_POINT('Ctrl Pts',(-233.749096023221,0.850439262011116,
125.958256691108));
#133373=CARTESIAN_POINT('Ctrl Pts',(-233.756852325963,0.714828508392514,
125.938335210102));
#133374=CARTESIAN_POINT('Ctrl Pts',(-233.764612768478,0.579145375231176,
125.918403096401));
#133375=CARTESIAN_POINT('Ctrl Pts',(-233.772373210992,0.442735574725181,
125.904166098365));
#133376=CARTESIAN_POINT('Ctrl Pts',(-233.780133653506,0.306113966437026,
125.895646192989));
#133377=CARTESIAN_POINT('Ctrl Pts',(-233.787906553771,0.169273041014923,
125.887112610705));
#133378=CARTESIAN_POINT('Ctrl Pts',(-233.795679454037,0.0322200194657413,
125.884314468805));
#133379=CARTESIAN_POINT('Ctrl Pts',(-233.803452354302,-0.104530563222136,
125.887221568906));
#133380=CARTESIAN_POINT('Ctrl Pts',(-233.810942690064,-0.236309917774265,
125.890022988597));
#133381=CARTESIAN_POINT('Ctrl Pts',(-233.818433025826,-0.367808133099621,
125.898122033053));
#133382=CARTESIAN_POINT('Ctrl Pts',(-233.825923361588,-0.49857230043032,
125.911446483459));
#133383=CARTESIAN_POINT('Ctrl Pts',(-233.833697695707,-0.634294430911234,
125.925276134452));
#133384=CARTESIAN_POINT('Ctrl Pts',(-233.841472029826,-0.769655678649314,
125.944779064057));
#133385=CARTESIAN_POINT('Ctrl Pts',(-233.849246363946,-0.904143756141013,
125.969931268539));
#133386=CARTESIAN_POINT('Ctrl Pts',(-233.857011116893,-1.03846608909711,
125.995052475177));
#133387=CARTESIAN_POINT('Ctrl Pts',(-233.86477586984,-1.17191701232081,
126.025809032753));
#133388=CARTESIAN_POINT('Ctrl Pts',(-233.872540622787,-1.30398825507674,
126.062125101154));
#133389=CARTESIAN_POINT('Ctrl Pts',(-233.880297663672,-1.43592832281212,
126.098405099923));
#133390=CARTESIAN_POINT('Ctrl Pts',(-233.888054704557,-1.56649106254064,
126.140233517931));
#133391=CARTESIAN_POINT('Ctrl Pts',(-233.895811745442,-1.69517766577222,
126.187483345646));
#133392=CARTESIAN_POINT('Ctrl Pts',(-233.903562936682,-1.82376722543543,
126.2346975419));
#133393=CARTESIAN_POINT('Ctrl Pts',(-233.911314127922,-1.95048309917022,
126.287324876084));
#133394=CARTESIAN_POINT('Ctrl Pts',(-233.919065319162,-2.0748412836655,
126.345188417471));
#133395=CARTESIAN_POINT('Ctrl Pts',(-233.926813215939,-2.19914661261483,
126.40302736531));
#133396=CARTESIAN_POINT('Ctrl Pts',(-233.934561112717,-2.32109589165727,
126.466097929356));
#133397=CARTESIAN_POINT('Ctrl Pts',(-233.942309009494,-2.44022497641992,
126.534175009544));
#133398=CARTESIAN_POINT('Ctrl Pts',(-233.950055285578,-2.55932914194616,
126.602237849475));
#133399=CARTESIAN_POINT('Ctrl Pts',(-233.957801561662,-2.67561394734977,
126.675304928642));
#133400=CARTESIAN_POINT('Ctrl Pts',(-233.965547837746,-2.78864010695454,
126.753105328599));
#133401=CARTESIAN_POINT('Ctrl Pts',(-233.973294171011,-2.90166710089289,
126.830906302861));
#133402=CARTESIAN_POINT('Ctrl Pts',(-233.981040504277,-3.01143507898782,
126.913440445956));
#133403=CARTESIAN_POINT('Ctrl Pts',(-233.988786837542,-3.11753432859071,
127.000393902076));
#133404=CARTESIAN_POINT('Ctrl Pts',(-233.996534905545,-3.22365733838504,
127.087366830819));
#133405=CARTESIAN_POINT('Ctrl Pts',(-234.004282973548,-3.32610968249579,
127.178760794149));
#133406=CARTESIAN_POINT('Ctrl Pts',(-234.012031041551,-3.42451559437457,
127.274222375742));
#133407=CARTESIAN_POINT('Ctrl Pts',(-234.019787344293,-3.52302609322741,
127.369785415041));
#133408=CARTESIAN_POINT('Ctrl Pts',(-234.027543647035,-3.61748128787602,
127.469424435827));
#133409=CARTESIAN_POINT('Ctrl Pts',(-234.035299949777,-3.70754271885999,
127.57274955645));
#133410=CARTESIAN_POINT('Ctrl Pts',(-234.043060392291,-3.79765221834138,
127.6761298248));
#133411=CARTESIAN_POINT('Ctrl Pts',(-234.050820834805,-3.88336303717,127.783199808095));
#133412=CARTESIAN_POINT('Ctrl Pts',(-234.058581277319,-3.96437839130675,
127.893538219507));
#133413=CARTESIAN_POINT('Ctrl Pts',(-234.066354177585,-4.04552379848216,
128.004053755933));
#133414=CARTESIAN_POINT('Ctrl Pts',(-234.07412707785,-4.12195846036362,
128.11784788046));
#133415=CARTESIAN_POINT('Ctrl Pts',(-234.081899978116,-4.19342966497602,
128.234471377268));
#133416=CARTESIAN_POINT('Ctrl Pts',(-234.089390313878,-4.26230271127547,
128.34685531621));
#133417=CARTESIAN_POINT('Ctrl Pts',(-234.09688064964,-4.32656675320381,
128.461866220346));
#133418=CARTESIAN_POINT('Ctrl Pts',(-234.104370985402,-4.38603774224419,
128.579084008668));
#133419=CARTESIAN_POINT('Ctrl Pts',(-234.112666954865,-4.45190521797911,
128.7089093227));
#133420=CARTESIAN_POINT('Ctrl Pts',(-234.120962924329,-4.51208009368256,
128.841809729011));
#133421=CARTESIAN_POINT('Ctrl Pts',(-234.129258893793,-4.56628422471798,
128.977277849438));
#133422=CARTESIAN_POINT('Ctrl Pts',(-234.137534886936,-4.62035783465243,
129.112419768744));
#133423=CARTESIAN_POINT('Ctrl Pts',(-234.14581088008,-4.66848925287003,
129.250116785686));
#133424=CARTESIAN_POINT('Ctrl Pts',(-234.154086873223,-4.71044705088237,
129.389838916307));
#133425=CARTESIAN_POINT('Ctrl Pts',(-234.157866594114,-4.72960955656794,
129.453651276565));
#133426=CARTESIAN_POINT('Ctrl Pts',(-234.161646315004,-4.7474849804627,
129.517885704026));
#133427=CARTESIAN_POINT('Ctrl Pts',(-234.165426035895,-4.76405452823417,
129.582490119309));
#133428=CARTESIAN_POINT('Ctrl Pts',(-232.415119734886,-4.76405452823408,
129.582490119308));
#133429=CARTESIAN_POINT('Ctrl Pts',(-232.421308237432,-4.79109715874973,
129.68792892526));
#133430=CARTESIAN_POINT('Ctrl Pts',(-232.427496739978,-4.81460826343985,
129.794150964176));
#133431=CARTESIAN_POINT('Ctrl Pts',(-232.433685242524,-4.8345569767513,
129.900899549758));
#133432=CARTESIAN_POINT('Ctrl Pts',(-232.445323692852,-4.87207366309676,
130.101657019204));
#133433=CARTESIAN_POINT('Ctrl Pts',(-232.45696214318,-4.89709405481899,
130.304817288689));
#133434=CARTESIAN_POINT('Ctrl Pts',(-232.468600593508,-4.90938042835421,
130.509120254146));
#133435=CARTESIAN_POINT('Ctrl Pts',(-232.47411391701,-4.91520068363373,
130.605901896826));
#133436=CARTESIAN_POINT('Ctrl Pts',(-232.479627240512,-4.91816392290484,
130.702939620798));
#133437=CARTESIAN_POINT('Ctrl Pts',(-232.485140564014,-4.91824815178524,
130.800096821013));
#133438=CARTESIAN_POINT('',(-232.13985943596,-4.91824884483728,130.807731486412));
#133439=CARTESIAN_POINT('Ctrl Pts',(-232.069726383436,-4.76405452823406,
129.582490119308));
#133440=CARTESIAN_POINT('Ctrl Pts',(-232.077373093558,-4.79768844224308,
129.713628239564));
#133441=CARTESIAN_POINT('Ctrl Pts',(-232.085019803679,-4.82588305575135,
129.846076494561));
#133442=CARTESIAN_POINT('Ctrl Pts',(-232.092666513801,-4.84855853558596,
129.979337472741));
#133443=CARTESIAN_POINT('Ctrl Pts',(-232.100532000827,-4.8718827743262,
130.116411126419));
#133444=CARTESIAN_POINT('Ctrl Pts',(-232.108397487854,-4.88936726615883,
130.254344247945));
#133445=CARTESIAN_POINT('Ctrl Pts',(-232.11626297488,-4.90098247622702,
130.392591470815));
#133446=CARTESIAN_POINT('Ctrl Pts',(-232.124128461907,-4.91259768629521,
130.530838693686));
#133447=CARTESIAN_POINT('Ctrl Pts',(-232.131993948933,-4.91834365475898,
130.669399558018));
#133448=CARTESIAN_POINT('Ctrl Pts',(-232.139859435959,-4.91824884483728,
130.807731486412));
#133449=CARTESIAN_POINT('Ctrl Pts',(-232.139859435996,-4.91824884483684,
130.807731487053));
#133450=CARTESIAN_POINT('Ctrl Pts',(-232.151515162288,-4.91810834766186,
131.012723128297));
#133451=CARTESIAN_POINT('Ctrl Pts',(-232.16317088858,-4.90515198395722,
131.217279571715));
#133452=CARTESIAN_POINT('Ctrl Pts',(-232.174826614871,-4.87954073522697,
131.420205789473));
#133453=CARTESIAN_POINT('Ctrl Pts',(-232.18260094899,-4.86245810992703,
131.555556961842));
#133454=CARTESIAN_POINT('Ctrl Pts',(-232.190375283109,-4.83971249996939,
131.69041121235));
#133455=CARTESIAN_POINT('Ctrl Pts',(-232.198149617228,-4.81134019566529,
131.824256977044));
#133456=CARTESIAN_POINT('Ctrl Pts',(-232.205914370175,-4.78300285769054,
131.957937788794));
#133457=CARTESIAN_POINT('Ctrl Pts',(-232.213679123123,-4.74905270305039,
132.090612208872));
#133458=CARTESIAN_POINT('Ctrl Pts',(-232.22144387607,-4.709577747114,132.221773932866));
#133459=CARTESIAN_POINT('Ctrl Pts',(-232.229200916955,-4.67014199826045,
132.352805385186));
#133460=CARTESIAN_POINT('Ctrl Pts',(-232.23695795784,-4.62519248005125,
132.482326759372));
#133461=CARTESIAN_POINT('Ctrl Pts',(-232.244714998725,-4.57486813546882,
132.609842438458));
#133462=CARTESIAN_POINT('Ctrl Pts',(-232.252466189965,-4.52458174086604,
132.737261956979));
#133463=CARTESIAN_POINT('Ctrl Pts',(-232.260217381205,-4.46892873047756,
132.862678428762));
#133464=CARTESIAN_POINT('Ctrl Pts',(-232.267968572445,-4.40809759882585,
132.985612235726));
#133465=CARTESIAN_POINT('Ctrl Pts',(-232.275716469222,-4.34729232202789,
133.108493792543));
#133466=CARTESIAN_POINT('Ctrl Pts',(-232.283464365999,-4.28131347429969,
133.228894433573));
#133467=CARTESIAN_POINT('Ctrl Pts',(-232.291212262776,-4.21039722906912,
133.346355549887));
#133468=CARTESIAN_POINT('Ctrl Pts',(-232.298958538861,-4.13949581798827,
133.463792095868));
#133469=CARTESIAN_POINT('Ctrl Pts',(-232.306704814945,-4.06365926563728,
133.578290005688));
#133470=CARTESIAN_POINT('Ctrl Pts',(-232.314451091029,-3.98316895409016,
133.689416621472));
#133471=CARTESIAN_POINT('Ctrl Pts',(-232.322197424294,-3.90267804838196,
133.800544057566));
#133472=CARTESIAN_POINT('Ctrl Pts',(-232.329943757559,-3.81753354426975,
133.908299833332));
#133473=CARTESIAN_POINT('Ctrl Pts',(-232.337690090825,-3.72805903915496,
134.012281885782));
#133474=CARTESIAN_POINT('Ctrl Pts',(-232.345438158828,-3.63856449684499,
134.116287224292));
#133475=CARTESIAN_POINT('Ctrl Pts',(-232.353186226831,-3.54473827895168,
134.21651686154));
#133476=CARTESIAN_POINT('Ctrl Pts',(-232.360934294834,-3.44694271738539,
134.312603620205));
#133477=CARTESIAN_POINT('Ctrl Pts',(-232.368690597575,-3.34904321753236,
134.408792501021));
#133478=CARTESIAN_POINT('Ctrl Pts',(-232.376446900317,-3.24716622609176,
134.500829433143));
#133479=CARTESIAN_POINT('Ctrl Pts',(-232.384203203059,-3.14170963453427,
134.588385410663));
#133480=CARTESIAN_POINT('Ctrl Pts',(-232.391963645573,-3.03619675761863,
134.675988119445));
#133481=CARTESIAN_POINT('Ctrl Pts',(-232.399724088088,-2.92710078451211,
134.759104871301));
#133482=CARTESIAN_POINT('Ctrl Pts',(-232.407484530602,-2.81485000272133,
134.837449077379));
#133483=CARTESIAN_POINT('Ctrl Pts',(-232.415257430867,-2.70241902601045,
134.915919048533));
#133484=CARTESIAN_POINT('Ctrl Pts',(-232.423030331133,-2.58682345024791,
134.989600953896));
#133485=CARTESIAN_POINT('Ctrl Pts',(-232.430803231398,-2.46851842628261,
135.05825293421));
#133486=CARTESIAN_POINT('Ctrl Pts',(-232.43829356716,-2.35451408793114,
135.124409242116));
#133487=CARTESIAN_POINT('Ctrl Pts',(-232.445783902922,-2.23799414428353,
135.185894833008));
#133488=CARTESIAN_POINT('Ctrl Pts',(-232.453274238684,-2.11938297203123,
135.242535792158));
#133489=CARTESIAN_POINT('Ctrl Pts',(-232.461048572803,-1.99627462113138,
135.30132431049));
#133490=CARTESIAN_POINT('Ctrl Pts',(-232.468822906922,-1.87052336313341,
135.355079801041));
#133491=CARTESIAN_POINT('Ctrl Pts',(-232.476597241041,-1.74257920707969,
135.403556283066));
#133492=CARTESIAN_POINT('Ctrl Pts',(-232.484361993988,-1.61479273076394,
135.451973022159));
#133493=CARTESIAN_POINT('Ctrl Pts',(-232.492126746935,-1.48481909575611,
135.495123560347));
#133494=CARTESIAN_POINT('Ctrl Pts',(-232.499891499883,-1.35313184475452,
135.53280827755));
#133495=CARTESIAN_POINT('Ctrl Pts',(-232.507648540768,-1.22157538738709,
135.570455565762));
#133496=CARTESIAN_POINT('Ctrl Pts',(-232.515405581653,-1.08830907450297,
135.602647729539));
#133497=CARTESIAN_POINT('Ctrl Pts',(-232.523162622538,-0.953824984768978,
135.629233772472));
#133498=CARTESIAN_POINT('Ctrl Pts',(-232.530913813778,-0.819442310533371,
135.655799766663));
#133499=CARTESIAN_POINT('Ctrl Pts',(-232.538665005018,-0.683844069328535,
135.676767979314));
#133500=CARTESIAN_POINT('Ctrl Pts',(-232.546416196258,-0.547535663322658,
135.692037750918));
#133501=CARTESIAN_POINT('Ctrl Pts',(-232.554164093035,-0.411285192025293,
135.707301032461));
#133502=CARTESIAN_POINT('Ctrl Pts',(-232.561911989812,-0.274325543983062,
135.716870646676));
#133503=CARTESIAN_POINT('Ctrl Pts',(-232.569659886589,-0.137170217383779,
135.720697403626));
#133504=CARTESIAN_POINT('Ctrl Pts',(-232.577406162673,-4.35807220934559E-5,
135.724523360101));
#133505=CARTESIAN_POINT('Ctrl Pts',(-232.585152438757,0.13727826251566,
135.72260883783));
#133506=CARTESIAN_POINT('Ctrl Pts',(-232.592898714841,0.274279211119887,
135.714956709371));
#133507=CARTESIAN_POINT('Ctrl Pts',(-232.600645048107,0.411281171034182,
135.707304524425));
#133508=CARTESIAN_POINT('Ctrl Pts',(-232.608391381372,0.547961841231461,
135.693914670581));
#133509=CARTESIAN_POINT('Ctrl Pts',(-232.616137714638,0.683808042433603,
135.67484207463));
#133510=CARTESIAN_POINT('Ctrl Pts',(-232.623885782641,0.819684665450428,
135.655765207504));
#133511=CARTESIAN_POINT('Ctrl Pts',(-232.631633850644,0.954726060521546,
135.631003120271));
#133512=CARTESIAN_POINT('Ctrl Pts',(-232.639381918647,1.08842746172099,
135.600662184719));
#133513=CARTESIAN_POINT('Ctrl Pts',(-232.647138221388,1.22227096236087,
135.57028900246));
#133514=CARTESIAN_POINT('Ctrl Pts',(-232.65489452413,1.35477124233406,135.534325214193));
#133515=CARTESIAN_POINT('Ctrl Pts',(-232.662650826872,1.48543642959345,
135.492927741554));
#133516=CARTESIAN_POINT('Ctrl Pts',(-232.670411269386,1.61617135679754,
135.451508173836));
#133517=CARTESIAN_POINT('Ctrl Pts',(-232.6781717119,1.74506887240367,135.404649276521));
#133518=CARTESIAN_POINT('Ctrl Pts',(-232.685932154415,1.87165636123661,
135.352556471742));
#133519=CARTESIAN_POINT('Ctrl Pts',(-232.69370505468,1.99844705954452,135.300380042968));
#133520=CARTESIAN_POINT('Ctrl Pts',(-232.701477954945,2.12291996558523,
135.242953080872));
#133521=CARTESIAN_POINT('Ctrl Pts',(-232.709250855211,2.24462557616264,
135.180527785915));
#133522=CARTESIAN_POINT('Ctrl Pts',(-232.716741190973,2.36190688123762,
135.12037180767));
#133523=CARTESIAN_POINT('Ctrl Pts',(-232.724231526735,2.47661832591759,
135.055574742809));
#133524=CARTESIAN_POINT('Ctrl Pts',(-232.731721862497,2.58838420484736,
134.986399626303));
#133525=CARTESIAN_POINT('Ctrl Pts',(-232.739496196616,2.70438772104741,
134.914601714229));
#133526=CARTESIAN_POINT('Ctrl Pts',(-232.747270530735,2.81758536427601,
134.837859775108));
#133527=CARTESIAN_POINT('Ctrl Pts',(-232.755044864854,2.92752694308547,
134.756419455692));
#133528=CARTESIAN_POINT('Ctrl Pts',(-232.762809617801,3.03733302872451,
134.675079504191));
#133529=CARTESIAN_POINT('Ctrl Pts',(-232.770574370748,3.14389072309296,
134.589052923915));
#133530=CARTESIAN_POINT('Ctrl Pts',(-232.778339123695,3.24677611876926,
134.498630220219));
#133531=CARTESIAN_POINT('Ctrl Pts',(-232.78609616458,3.34955932722015,134.408297325628));
#133532=CARTESIAN_POINT('Ctrl Pts',(-232.793853205465,3.44867720366,134.31357725316));
#133533=CARTESIAN_POINT('Ctrl Pts',(-232.80161024635,3.54373672999305,134.214802385284));
#133534=CARTESIAN_POINT('Ctrl Pts',(-232.809361437591,3.63872457119796,
134.116102004305));
#133535=CARTESIAN_POINT('Ctrl Pts',(-232.817112628831,3.72965988389467,
134.013353194753));
#133536=CARTESIAN_POINT('Ctrl Pts',(-232.824863820071,3.81618479817155,
133.906926756862));
#133537=CARTESIAN_POINT('Ctrl Pts',(-232.832611716848,3.90267293705162,
133.800545553046));
#133538=CARTESIAN_POINT('Ctrl Pts',(-232.840359613625,3.98475415970784,
133.690490132483));
#133539=CARTESIAN_POINT('Ctrl Pts',(-232.848107510402,4.0621095229413,133.577165927379));
#133540=CARTESIAN_POINT('Ctrl Pts',(-232.855853786486,4.13944870510036,
133.463865427257));
#133541=CARTESIAN_POINT('Ctrl Pts',(-232.86360006257,4.21206377383438,133.347297825332));
#133542=CARTESIAN_POINT('Ctrl Pts',(-232.871346338654,4.27967818059685,
133.227898884857));
#133543=CARTESIAN_POINT('Ctrl Pts',(-232.87909267192,4.3472930864736,133.108499063006));
#133544=CARTESIAN_POINT('Ctrl Pts',(-232.886839005185,4.40990706406635,
132.986268201103));
#133545=CARTESIAN_POINT('Ctrl Pts',(-232.89458533845,4.46728893890667,132.861667740682));
#133546=CARTESIAN_POINT('Ctrl Pts',(-232.902333406453,4.52468366401992,
132.737039376851));
#133547=CARTESIAN_POINT('Ctrl Pts',(-232.910081474456,4.57684379133737,
132.61004071361));
#133548=CARTESIAN_POINT('Ctrl Pts',(-232.917829542459,4.62358597614422,
132.481153921376));
#133549=CARTESIAN_POINT('Ctrl Pts',(-232.925585845201,4.67037783910138,
132.352130146726));
#133550=CARTESIAN_POINT('Ctrl Pts',(-232.933342147943,4.7117401233103,132.221214602559));
#133551=CARTESIAN_POINT('Ctrl Pts',(-232.941098450685,4.74753898252945,
132.088905934736));
#133552=CARTESIAN_POINT('Ctrl Pts',(-232.948858893199,4.78335694867765,
131.956526649793));
#133553=CARTESIAN_POINT('Ctrl Pts',(-232.956619335713,4.81360548693504,
131.822753140755));
#133554=CARTESIAN_POINT('Ctrl Pts',(-232.964379778227,4.83820196471525,
131.688094067836));
#133555=CARTESIAN_POINT('Ctrl Pts',(-232.972152678493,4.86283792694517,
131.553218828218));
#133556=CARTESIAN_POINT('Ctrl Pts',(-232.979925578758,4.88180364345212,
131.417455571365));
#133557=CARTESIAN_POINT('Ctrl Pts',(-232.987698479024,4.89506833017058,
131.281318797558));
#133558=CARTESIAN_POINT('Ctrl Pts',(-232.995188814786,4.90785081211506,
131.150130938386));
#133559=CARTESIAN_POINT('Ctrl Pts',(-233.002679150547,4.91533954413174,
131.018596554867));
#133560=CARTESIAN_POINT('Ctrl Pts',(-233.010169486309,4.9175527470689,130.887173915382));
#133561=CARTESIAN_POINT('Ctrl Pts',(-233.017943820429,4.91984986426811,
130.750768346575));
#133562=CARTESIAN_POINT('Ctrl Pts',(-233.025718154548,4.91647078861257,
130.614051070782));
#133563=CARTESIAN_POINT('Ctrl Pts',(-233.033492488667,4.90737885019658,
130.477533624887));
#133564=CARTESIAN_POINT('Ctrl Pts',(-233.041257241614,4.89829811678214,
130.341184424544));
#133565=CARTESIAN_POINT('Ctrl Pts',(-233.049021994561,4.88351855501939,
130.205034950446));
#133566=CARTESIAN_POINT('Ctrl Pts',(-233.056786747508,4.86305544297488,
130.069598873153));
#133567=CARTESIAN_POINT('Ctrl Pts',(-233.064543788393,4.84261265518175,
129.934297312882));
#133568=CARTESIAN_POINT('Ctrl Pts',(-233.072300829278,4.81649760890657,
129.799708123433));
#133569=CARTESIAN_POINT('Ctrl Pts',(-233.080057870163,4.78477751105465,
129.666341622907));
#133570=CARTESIAN_POINT('Ctrl Pts',(-233.087809061403,4.75308133357522,
129.533075695095));
#133571=CARTESIAN_POINT('Ctrl Pts',(-233.095560252643,4.71578860783217,
129.401030999759));
#133572=CARTESIAN_POINT('Ctrl Pts',(-233.103311443884,4.6730178611363,129.270709049575));
#133573=CARTESIAN_POINT('Ctrl Pts',(-233.111059340661,4.63026529314866,
129.140442489696));
#133574=CARTESIAN_POINT('Ctrl Pts',(-233.118807237438,4.58203945668833,
129.011897589346));
#133575=CARTESIAN_POINT('Ctrl Pts',(-233.126555134215,4.52850905676385,
128.885561830484));
#133576=CARTESIAN_POINT('Ctrl Pts',(-233.134301410299,4.47498985424519,
128.759252498339));
#133577=CARTESIAN_POINT('Ctrl Pts',(-233.142047686383,4.41616844775224,
128.635151748285));
#133578=CARTESIAN_POINT('Ctrl Pts',(-233.149793962467,4.35226197600564,
128.513727789129));
#133579=CARTESIAN_POINT('Ctrl Pts',(-233.157540295733,4.2883550325159,128.392302933647));
#133580=CARTESIAN_POINT('Ctrl Pts',(-233.165286628998,4.21936313095926,
128.273555254465));
#133581=CARTESIAN_POINT('Ctrl Pts',(-233.173032962263,4.14554953971994,
128.15792866563));
#133582=CARTESIAN_POINT('Ctrl Pts',(-233.180781030266,4.07171941843855,
128.042276183022));
#133583=CARTESIAN_POINT('Ctrl Pts',(-233.188529098269,3.99306566916125,
127.929746511061));
#133584=CARTESIAN_POINT('Ctrl Pts',(-233.196277166272,3.90989485322046,
127.820754527738));
#133585=CARTESIAN_POINT('Ctrl Pts',(-233.204033469014,3.82663564234684,
127.711646706438));
#133586=CARTESIAN_POINT('Ctrl Pts',(-233.211789771756,3.73885001226341,
127.60608439588));
#133587=CARTESIAN_POINT('Ctrl Pts',(-233.219546074498,3.64688514069141,
127.504449734966));
#133588=CARTESIAN_POINT('Ctrl Pts',(-233.227306517012,3.55487118469845,
127.402760828572));
#133589=CARTESIAN_POINT('Ctrl Pts',(-233.235066959526,3.4586738166718,127.305004027419));
#133590=CARTESIAN_POINT('Ctrl Pts',(-233.24282740204,3.35867632192402,127.21152379591));
#133591=CARTESIAN_POINT('Ctrl Pts',(-233.250600302306,3.25851830232031,
127.117893501635));
#133592=CARTESIAN_POINT('Ctrl Pts',(-233.258373202571,3.15454826235037,
127.02855375067));
#133593=CARTESIAN_POINT('Ctrl Pts',(-233.266146102837,3.0471824261316,126.94380854249));
#133594=CARTESIAN_POINT('Ctrl Pts',(-233.273636438599,2.94371960849848,
126.862144036088));
#133595=CARTESIAN_POINT('Ctrl Pts',(-233.281126774361,2.83710384897438,
126.784746006553));
#133596=CARTESIAN_POINT('Ctrl Pts',(-233.288617110123,2.7277305505416,126.711846829423));
#133597=CARTESIAN_POINT('Ctrl Pts',(-233.296391444242,2.61421033025465,
126.636183657834));
#133598=CARTESIAN_POINT('Ctrl Pts',(-233.304165778361,2.49735974116572,
126.565127542813));
#133599=CARTESIAN_POINT('Ctrl Pts',(-233.31194011248,2.37758933276305,126.498985833969));
#133600=CARTESIAN_POINT('Ctrl Pts',(-233.319704865427,2.25796653068454,
126.432925638871));
#133601=CARTESIAN_POINT('Ctrl Pts',(-233.327469618374,2.13543140802883,
126.371767986375));
#133602=CARTESIAN_POINT('Ctrl Pts',(-233.335234371321,2.01042438855384,
126.315777674096));
#133603=CARTESIAN_POINT('Ctrl Pts',(-233.342991412206,1.88554152781289,
126.259842972185));
#133604=CARTESIAN_POINT('Ctrl Pts',(-233.350748453091,1.75819201055864,
126.209065555812));
#133605=CARTESIAN_POINT('Ctrl Pts',(-233.358505493976,1.62884150883475,
126.163664721302));
#133606=CARTESIAN_POINT('Ctrl Pts',(-233.366256685216,1.49958855133058,
126.118298123915));
#133607=CARTESIAN_POINT('Ctrl Pts',(-233.374007876456,1.36833798025505,
126.078300167068));
#133608=CARTESIAN_POINT('Ctrl Pts',(-233.381759067696,1.23557579933317,
126.043842210228));
#133609=CARTESIAN_POINT('Ctrl Pts',(-233.389506964473,1.10287004587954,
126.009398898939));
#133610=CARTESIAN_POINT('Ctrl Pts',(-233.397254861251,0.968654338046777,
125.980491002458));
#133611=CARTESIAN_POINT('Ctrl Pts',(-233.405002758028,0.833429997389721,
125.957240080386));
#133612=CARTESIAN_POINT('Ctrl Pts',(-233.412749034112,0.698233942749631,
125.933994021906));
#133613=CARTESIAN_POINT('Ctrl Pts',(-233.420495310196,0.562030060011294,
125.916402650364));
#133614=CARTESIAN_POINT('Ctrl Pts',(-233.42824158628,0.425329635286075,
125.9045363591));
#133615=CARTESIAN_POINT('Ctrl Pts',(-233.435987919545,0.288628201469933,
125.892669980243));
#133616=CARTESIAN_POINT('Ctrl Pts',(-233.443734252811,0.151430607853447,
125.886528799803));
#133617=CARTESIAN_POINT('Ctrl Pts',(-233.451480586076,0.0142526348897896,
125.88613126902));
#133618=CARTESIAN_POINT('Ctrl Pts',(-233.459228654079,-0.122956058129974,
125.885733649213));
#133619=CARTESIAN_POINT('Ctrl Pts',(-233.466976722082,-0.260144730864806,
125.891082239685));
#133620=CARTESIAN_POINT('Ctrl Pts',(-233.474724790085,-0.396798630823245,
125.902143373392));
#133621=CARTESIAN_POINT('Ctrl Pts',(-233.482481092827,-0.533597768172948,
125.913216263004));
#133622=CARTESIAN_POINT('Ctrl Pts',(-233.490237395568,-0.669860607068107,
125.930013792452));
#133623=CARTESIAN_POINT('Ctrl Pts',(-233.49799369831,-0.805077985189934,
125.952450426697));
#133624=CARTESIAN_POINT('Ctrl Pts',(-233.505754140824,-0.940367532897782,
125.974899036049));
#133625=CARTESIAN_POINT('Ctrl Pts',(-233.513514583338,-1.07461012549429,
126.002992667354));
#133626=CARTESIAN_POINT('Ctrl Pts',(-233.521275025852,-1.20730878024569,
126.036595043249));
#133627=CARTESIAN_POINT('Ctrl Pts',(-233.529047926118,-1.34022045465813,
126.070251360661));
#133628=CARTESIAN_POINT('Ctrl Pts',(-233.536820826383,-1.47158286359105,
126.109433982231));
#133629=CARTESIAN_POINT('Ctrl Pts',(-233.544593726649,-1.60091526437436,
126.153957045961));
#133630=CARTESIAN_POINT('Ctrl Pts',(-233.552084062411,-1.72554610662334,
126.19686158418));
#133631=CARTESIAN_POINT('Ctrl Pts',(-233.559574398173,-1.8482916831584,
126.244724916668));
#133632=CARTESIAN_POINT('Ctrl Pts',(-233.567064733935,-1.96874276488739,
126.297339984353));
#133633=CARTESIAN_POINT('Ctrl Pts',(-233.574839565395,-2.093768783658,126.351953461839));
#133634=CARTESIAN_POINT('Ctrl Pts',(-233.582614396855,-2.21671863517069,
126.411859777179));
#133635=CARTESIAN_POINT('Ctrl Pts',(-233.590389228315,-2.33711173374839,
126.476879617437));
#133636=CARTESIAN_POINT('Ctrl Pts',(-233.598154365608,-2.45735471836534,
126.541818386721));
#133637=CARTESIAN_POINT('Ctrl Pts',(-233.605919502901,-2.57504695260555,
126.611857810093));
#133638=CARTESIAN_POINT('Ctrl Pts',(-233.613684640195,-2.68972752834779,
126.686770438135));
#133639=CARTESIAN_POINT('Ctrl Pts',(-233.621441952913,-2.80429254570409,
126.761607580138));
#133640=CARTESIAN_POINT('Ctrl Pts',(-233.629199265632,-2.91585161890929,
126.841307941542));
#133641=CARTESIAN_POINT('Ctrl Pts',(-233.636956578351,-3.02396849818628,
126.925598239632));
#133642=CARTESIAN_POINT('Ctrl Pts',(-233.644707556841,-3.13199709470004,
127.009819710537));
#133643=CARTESIAN_POINT('Ctrl Pts',(-233.652458535331,-3.2365887867988,
127.098623415991));
#133644=CARTESIAN_POINT('Ctrl Pts',(-233.660209513821,-3.3373367456812,
127.191693111633));
#133645=CARTESIAN_POINT('Ctrl Pts',(-233.667957032468,-3.43803973317778,
127.284721263274));
#133646=CARTESIAN_POINT('Ctrl Pts',(-233.675704551114,-3.534902114388,127.382011351971));
#133647=CARTESIAN_POINT('Ctrl Pts',(-233.68345206976,-3.62755069929318,
127.483207356038));
#133648=CARTESIAN_POINT('Ctrl Pts',(-233.691197807897,-3.72017799201285,
127.584380103581));
#133649=CARTESIAN_POINT('Ctrl Pts',(-233.698943546035,-3.80859315191726,
127.689456691966));
#133650=CARTESIAN_POINT('Ctrl Pts',(-233.706689284172,-3.89246066385488,
127.798045091404));
#133651=CARTESIAN_POINT('Ctrl Pts',(-233.714434919588,-3.97632706357252,
127.906632050783));
#133652=CARTESIAN_POINT('Ctrl Pts',(-233.722180555005,-4.05564569735638,
128.018730418551));
#133653=CARTESIAN_POINT('Ctrl Pts',(-233.729926190421,-4.13012232744392,
128.133916343134));
#133654=CARTESIAN_POINT('Ctrl Pts',(-233.737677017795,-4.20464887977663,
128.249179477708));
#133655=CARTESIAN_POINT('Ctrl Pts',(-233.745427845169,-4.27432673041007,
128.367533975942));
#133656=CARTESIAN_POINT('Ctrl Pts',(-233.753178672543,-4.33890570523499,
128.48852807967));
#133657=CARTESIAN_POINT('Ctrl Pts',(-233.76093206748,-4.40350607269246,
128.609562264281));
#133658=CARTESIAN_POINT('Ctrl Pts',(-233.768685462417,-4.46300402586445,
128.733237445952));
#133659=CARTESIAN_POINT('Ctrl Pts',(-233.776438857354,-4.51719654556064,
128.859079550143));
#133660=CARTESIAN_POINT('Ctrl Pts',(-233.784201671387,-4.57145490022168,
128.985074531715));
#133661=CARTESIAN_POINT('Ctrl Pts',(-233.791964485419,-4.62039480057076,
129.113241331318));
#133662=CARTESIAN_POINT('Ctrl Pts',(-233.799727299451,-4.66386213048879,
129.243087710515));
#133663=CARTESIAN_POINT('Ctrl Pts',(-233.806422729466,-4.70135271885186,
129.355080261289));
#133664=CARTESIAN_POINT('Ctrl Pts',(-233.813118159481,-4.73477299282818,
129.46832185717));
#133665=CARTESIAN_POINT('Ctrl Pts',(-233.819813589496,-4.76405452823394,
129.582490119308));
#133666=CARTESIAN_POINT('Origin',(213.235140564004,0.,130.804360617566));
#133667=CARTESIAN_POINT('',(-235.915124447633,-4.76405452823405,129.582490119308));
#133668=CARTESIAN_POINT('',(-235.570143588767,-4.76405452823401,129.582490119308));
#133669=CARTESIAN_POINT('',(213.235140564004,-4.76405452823405,129.582490119308));
#133670=CARTESIAN_POINT('',(-234.235140563976,-4.91824993088488,130.803536086871));
#133671=CARTESIAN_POINT('Ctrl Pts',(-234.235140564014,-4.91824993088499,
130.803536087554));
#133672=CARTESIAN_POINT('Ctrl Pts',(-234.243160377497,-4.91827380234173,
130.945927254282));
#133673=CARTESIAN_POINT('Ctrl Pts',(-234.25118019098,-4.91210965921112,
131.088232882481));
#133674=CARTESIAN_POINT('Ctrl Pts',(-234.259200004463,-4.89980581763934,
131.229902638908));
#133675=CARTESIAN_POINT('Ctrl Pts',(-234.267227171366,-4.88749069459418,
131.371702293267));
#133676=CARTESIAN_POINT('Ctrl Pts',(-234.275254338268,-4.86902467683493,
131.512864564863));
#133677=CARTESIAN_POINT('Ctrl Pts',(-234.283281505171,-4.84450765492664,
131.652846706938));
#133678=CARTESIAN_POINT('Ctrl Pts',(-234.291576263841,-4.81917333928226,
131.79749526112));
#133679=CARTESIAN_POINT('Ctrl Pts',(-234.299871022512,-4.78737768946012,
131.94088323545));
#133680=CARTESIAN_POINT('Ctrl Pts',(-234.308165781182,-4.74928705413213,
132.082427728462));
#133681=CARTESIAN_POINT('Ctrl Pts',(-234.31621698266,-4.71231486583196,
132.219816081358));
#133682=CARTESIAN_POINT('Ctrl Pts',(-234.324268184138,-4.66941234589774,
132.355467387));
#133683=CARTESIAN_POINT('Ctrl Pts',(-234.332319385617,-4.6207809978444,
132.488868270401));
#133684=CARTESIAN_POINT('Ctrl Pts',(-234.340735922883,-4.56994292674358,
132.628322426347));
#133685=CARTESIAN_POINT('Ctrl Pts',(-234.349152460149,-4.51284414580398,
132.765316738622));
#133686=CARTESIAN_POINT('Ctrl Pts',(-234.357568997416,-4.44976871876674,
132.899292934369));
#133687=CARTESIAN_POINT('Ctrl Pts',(-234.365985534682,-4.38669329172966,
133.033269130116));
#133688=CARTESIAN_POINT('Ctrl Pts',(-234.374402071948,-4.31764148397627,
133.164226864535));
#133689=CARTESIAN_POINT('Ctrl Pts',(-234.382818609214,-4.24294876878563,
133.291642026647));
#133690=CARTESIAN_POINT('Ctrl Pts',(-234.390592943333,-4.17395529726889,
133.409335088621));
#133691=CARTESIAN_POINT('Ctrl Pts',(-234.398367277452,-4.09995188924855,
133.524341728663));
#133692=CARTESIAN_POINT('Ctrl Pts',(-234.406141611571,-4.02117331738154,
133.636205990124));
#133693=CARTESIAN_POINT('Ctrl Pts',(-234.413906364519,-3.94249183306371,
133.74793238888));
#133694=CARTESIAN_POINT('Ctrl Pts',(-234.421671117466,-3.859047117171,133.856523797991));
#133695=CARTESIAN_POINT('Ctrl Pts',(-234.429435870413,-3.77111941879046,
133.961549460781));
#133696=CARTESIAN_POINT('Ctrl Pts',(-234.437192911298,-3.68327905143929,
134.066470810603));
#133697=CARTESIAN_POINT('Ctrl Pts',(-234.444949952183,-3.59096481174796,
134.167833164111));
#133698=CARTESIAN_POINT('Ctrl Pts',(-234.452706993068,-3.49449955511849,
134.265235640126));
#133699=CARTESIAN_POINT('Ctrl Pts',(-234.460458184308,-3.39810704368956,
134.362564664176));
#133700=CARTESIAN_POINT('Ctrl Pts',(-234.468209375548,-3.29757002002429,
134.455939477869));
#133701=CARTESIAN_POINT('Ctrl Pts',(-234.475960566788,-3.19325058968546,
134.544993416168));
#133702=CARTESIAN_POINT('Ctrl Pts',(-234.483708463565,-3.0889754978872,
134.634009504167));
#133703=CARTESIAN_POINT('Ctrl Pts',(-234.491456360342,-2.98092149358705,
134.718708116097));
#133704=CARTESIAN_POINT('Ctrl Pts',(-234.499204257119,-2.86948623848019,
134.79876067135));
#133705=CARTESIAN_POINT('Ctrl Pts',(-234.506950533203,-2.75807429322643,
134.878796481335));
#133706=CARTESIAN_POINT('Ctrl Pts',(-234.514696809287,-2.64328282131883,
134.954187939758));
#133707=CARTESIAN_POINT('Ctrl Pts',(-234.522443085372,-2.52554082411746,
135.024648120594));
#133708=CARTESIAN_POINT('Ctrl Pts',(-234.530189418637,-2.40779795777158,
135.095108821552));
#133709=CARTESIAN_POINT('Ctrl Pts',(-234.537935751902,-2.28710485815356,
135.160637971524));
#133710=CARTESIAN_POINT('Ctrl Pts',(-234.545682085168,-2.16391728636374,
135.220993389291));
#133711=CARTESIAN_POINT('Ctrl Pts',(-234.553430153171,-2.0407021275715,
135.281362323235));
#133712=CARTESIAN_POINT('Ctrl Pts',(-234.561178221174,-1.9149917360419,
135.336555047469));
#133713=CARTESIAN_POINT('Ctrl Pts',(-234.568926289177,-1.78726374357305,
135.386376699315));
#133714=CARTESIAN_POINT('Ctrl Pts',(-234.576682591918,-1.65940000027365,
135.436251302206));
#133715=CARTESIAN_POINT('Ctrl Pts',(-234.58443889466,-1.52951473732209,
135.480743287185));
#133716=CARTESIAN_POINT('Ctrl Pts',(-234.592195197402,-1.39810324503968,
135.51970688043));
#133717=CARTESIAN_POINT('Ctrl Pts',(-234.599955639917,-1.26662161448711,
135.558691269718));
#133718=CARTESIAN_POINT('Ctrl Pts',(-234.607716082431,-1.13361251042853,
135.592141292507));
#133719=CARTESIAN_POINT('Ctrl Pts',(-234.615476524945,-0.999582463641959,
135.619962133564));
#133720=CARTESIAN_POINT('Ctrl Pts',(-234.62324942521,-0.86533725992566,
135.647827635104));
#133721=CARTESIAN_POINT('Ctrl Pts',(-234.631022325476,-0.730068224438899,
135.670045833778));
#133722=CARTESIAN_POINT('Ctrl Pts',(-234.638795225741,-0.594288970565359,
135.686573607795));
#133723=CARTESIAN_POINT('Ctrl Pts',(-234.646285561503,-0.463445634578529,
135.702500555596));
#133724=CARTESIAN_POINT('Ctrl Pts',(-234.653775897265,-0.332128838632401,
135.713143593568));
#133725=CARTESIAN_POINT('Ctrl Pts',(-234.661266233027,-0.200797156389273,
135.718509940133));
#133726=CARTESIAN_POINT('Ctrl Pts',(-234.669040567146,-0.0644859934955289,
135.724079753359));
#133727=CARTESIAN_POINT('Ctrl Pts',(-234.676814901265,0.0722729995977941,
135.723982488443));
#133728=CARTESIAN_POINT('Ctrl Pts',(-234.684589235384,0.208969313293336,
135.718169210562));
#133729=CARTESIAN_POINT('Ctrl Pts',(-234.692353988331,0.345497160998777,
135.712363097027));
#133730=CARTESIAN_POINT('Ctrl Pts',(-234.700118741278,0.48196209614215,
135.700855003386));
#133731=CARTESIAN_POINT('Ctrl Pts',(-234.707883494225,0.61785022945676,
135.68364787663));
#133732=CARTESIAN_POINT('Ctrl Pts',(-234.71564053511,0.753603396761675,
135.666457840234));
#133733=CARTESIAN_POINT('Ctrl Pts',(-234.723397575995,0.888780516952143,
135.643580083891));
#133734=CARTESIAN_POINT('Ctrl Pts',(-234.73115461688,1.02286980610768,135.615069548925));
#133735=CARTESIAN_POINT('Ctrl Pts',(-234.738905808121,1.15685797748738,
135.586580513975));
#133736=CARTESIAN_POINT('Ctrl Pts',(-234.746656999361,1.28975956980372,
135.552467236216));
#133737=CARTESIAN_POINT('Ctrl Pts',(-234.754408190601,1.42107037047482,
135.512836173907));
#133738=CARTESIAN_POINT('Ctrl Pts',(-234.762156087378,1.55232536055298,
135.473221955856));
#133739=CARTESIAN_POINT('Ctrl Pts',(-234.769903984155,1.68199053024865,
135.428094730416));
#133740=CARTESIAN_POINT('Ctrl Pts',(-234.777651880932,1.80957448953227,
135.377611455792));
#133741=CARTESIAN_POINT('Ctrl Pts',(-234.785398157016,1.93713176100199,
135.32713874118));
#133742=CARTESIAN_POINT('Ctrl Pts',(-234.7931444331,2.0626083246735,135.271312349617));
#133743=CARTESIAN_POINT('Ctrl Pts',(-234.800890709184,2.18553089584264,
135.210338121573));
#133744=CARTESIAN_POINT('Ctrl Pts',(-234.80863704245,2.30845437439844,135.149363443431));
#133745=CARTESIAN_POINT('Ctrl Pts',(-234.816383375715,2.42882347258885,
135.083241026715));
#133746=CARTESIAN_POINT('Ctrl Pts',(-234.824129708981,2.54618808648691,
135.012223411281));
#133747=CARTESIAN_POINT('Ctrl Pts',(-234.831877776983,2.66357898337634,
134.941189891945));
#133748=CARTESIAN_POINT('Ctrl Pts',(-234.839625844986,2.77796372268226,
134.865259194853));
#133749=CARTESIAN_POINT('Ctrl Pts',(-234.847373912989,2.88892018926236,
134.784727837129));
#133750=CARTESIAN_POINT('Ctrl Pts',(-234.855130215731,2.99999458169539,
134.70411088972));
#133751=CARTESIAN_POINT('Ctrl Pts',(-234.862886518473,3.10763310598619,
134.618883744115));
#133752=CARTESIAN_POINT('Ctrl Pts',(-234.870642821215,3.21144540197229,
134.529384307779));
#133753=CARTESIAN_POINT('Ctrl Pts',(-234.878403263729,3.31531310570647,
134.439837102899));
#133754=CARTESIAN_POINT('Ctrl Pts',(-234.886163706243,3.41535022690414,
134.346013331021));
#133755=CARTESIAN_POINT('Ctrl Pts',(-234.893924148757,3.51120320256636,
134.248287900885));
#133756=CARTESIAN_POINT('Ctrl Pts',(-234.901697049023,3.60721004993455,
134.150405593212));
#133757=CARTESIAN_POINT('Ctrl Pts',(-234.909469949288,3.69901906754108,
134.048609401732));
#133758=CARTESIAN_POINT('Ctrl Pts',(-234.917242849554,3.7863163552244,133.94330813555));
#133759=CARTESIAN_POINT('Ctrl Pts',(-234.924733185316,3.87044016661349,
133.84183483563));
#133760=CARTESIAN_POINT('Ctrl Pts',(-234.932223521078,3.95037439168747,
133.737107118107));
#133761=CARTESIAN_POINT('Ctrl Pts',(-234.93971385684,4.0258772332447,133.629514695726));
#133762=CARTESIAN_POINT('Ctrl Pts',(-234.947488190959,4.10424278798674,
133.517842873949));
#133763=CARTESIAN_POINT('Ctrl Pts',(-234.955262525078,4.17808253254862,
133.402731085781));
#133764=CARTESIAN_POINT('Ctrl Pts',(-234.963036859197,4.24707935377274,
133.284582386936));
#133765=CARTESIAN_POINT('Ctrl Pts',(-234.970801612144,4.31599114258113,
133.166579295804));
#133766=CARTESIAN_POINT('Ctrl Pts',(-234.978566365092,4.38007168826157,
133.045547075266));
#133767=CARTESIAN_POINT('Ctrl Pts',(-234.986331118039,4.43904570049892,
132.921919667836));
#133768=CARTESIAN_POINT('Ctrl Pts',(-234.994088158924,4.49796113891594,
132.798415048891));
#133769=CARTESIAN_POINT('Ctrl Pts',(-235.001845199809,4.55177996992062,
132.672320723136));
#133770=CARTESIAN_POINT('Ctrl Pts',(-235.009602240694,4.60027178549489,
132.544096966005));
#133771=CARTESIAN_POINT('Ctrl Pts',(-235.017353431934,4.64872703301389,
132.415969903407));
#133772=CARTESIAN_POINT('Ctrl Pts',(-235.025104623174,4.69186312324668,
132.28571696993));
#133773=CARTESIAN_POINT('Ctrl Pts',(-235.032855814414,4.7294970833229,132.153819917189));
#133774=CARTESIAN_POINT('Ctrl Pts',(-235.040603711191,4.76711504796221,
132.021978924214));
#133775=CARTESIAN_POINT('Ctrl Pts',(-235.048351607968,4.79923542659909,
131.888495576997));
#133776=CARTESIAN_POINT('Ctrl Pts',(-235.056099504745,4.82572466430102,
131.753868135628));
#133777=CARTESIAN_POINT('Ctrl Pts',(-235.063845780829,4.85220836102539,
131.619268855419));
#133778=CARTESIAN_POINT('Ctrl Pts',(-235.071592056914,4.87306318431779,
131.483526340446));
#133779=CARTESIAN_POINT('Ctrl Pts',(-235.079338332998,4.88820649165192,
131.347150040337));
#133780=CARTESIAN_POINT('Ctrl Pts',(-235.087084666263,4.90334991077052,
131.210772733529));
#133781=CARTESIAN_POINT('Ctrl Pts',(-235.094830999528,4.91278168665356,
131.073762020827));
#133782=CARTESIAN_POINT('Ctrl Pts',(-235.102577332794,4.91647099606753,
130.936633091372));
#133783=CARTESIAN_POINT('Ctrl Pts',(-235.110325400797,4.92016113167677,
130.799473452844));
#133784=CARTESIAN_POINT('Ctrl Pts',(-235.1180734688,4.91810623134189,130.662195935634));
#133785=CARTESIAN_POINT('Ctrl Pts',(-235.125821536802,4.9103275997707,130.525315951912));
#133786=CARTESIAN_POINT('Ctrl Pts',(-235.133577839544,4.90254070097732,
130.388290490514));
#133787=CARTESIAN_POINT('Ctrl Pts',(-235.141334142286,4.88901794121855,
130.251663797559));
#133788=CARTESIAN_POINT('Ctrl Pts',(-235.149090445028,4.86983261240989,
130.115946941344));
#133789=CARTESIAN_POINT('Ctrl Pts',(-235.156850887542,4.85063704381353,
129.980157648956));
#133790=CARTESIAN_POINT('Ctrl Pts',(-235.164611330056,4.82577295485478,
129.845279545221));
#133791=CARTESIAN_POINT('Ctrl Pts',(-235.172371772571,4.79536465743734,
129.711812740033));
#133792=CARTESIAN_POINT('Ctrl Pts',(-235.180144672836,4.76490754592135,
129.578131682082));
#133793=CARTESIAN_POINT('Ctrl Pts',(-235.187917573101,4.72888854358715,
129.445866827397));
#133794=CARTESIAN_POINT('Ctrl Pts',(-235.195690473367,4.68748192240888,
129.315503240384));
#133795=CARTESIAN_POINT('Ctrl Pts',(-235.203180809129,4.64758053620742,
129.189878698124));
#133796=CARTESIAN_POINT('Ctrl Pts',(-235.210671144891,4.60267654256751,
129.066019881279));
#133797=CARTESIAN_POINT('Ctrl Pts',(-235.218161480653,4.55296712056405,
128.944340869939));
#133798=CARTESIAN_POINT('Ctrl Pts',(-235.225935814772,4.50137295071654,
128.818048361901));
#133799=CARTESIAN_POINT('Ctrl Pts',(-235.233710148891,4.4444383287666,128.693704160284));
#133800=CARTESIAN_POINT('Ctrl Pts',(-235.24148448301,4.38233094949637,128.571792922828));
#133801=CARTESIAN_POINT('Ctrl Pts',(-235.249249235957,4.32030011202039,
128.450031930078));
#133802=CARTESIAN_POINT('Ctrl Pts',(-235.257013988904,4.25310937726583,
128.330698280564));
#133803=CARTESIAN_POINT('Ctrl Pts',(-235.264778741851,4.18097503222005,
128.214258140355));
#133804=CARTESIAN_POINT('Ctrl Pts',(-235.272535782736,4.1089123320225,128.097933650135));
#133805=CARTESIAN_POINT('Ctrl Pts',(-235.280292823621,4.03191599734352,
127.984497280286));
#133806=CARTESIAN_POINT('Ctrl Pts',(-235.288049864506,3.95024872978003,
127.874391669715));
#133807=CARTESIAN_POINT('Ctrl Pts',(-235.295801055747,3.86864304813795,
127.764369090641));
#133808=CARTESIAN_POINT('Ctrl Pts',(-235.303552246987,3.78237367667754,
127.657672584101));
#133809=CARTESIAN_POINT('Ctrl Pts',(-235.311303438227,3.69174702536906,
127.554716488868));
#133810=CARTESIAN_POINT('Ctrl Pts',(-235.319051335004,3.60115889280556,
127.451804152723));
#133811=CARTESIAN_POINT('Ctrl Pts',(-235.326799231781,3.50621742158396,
127.352629358797));
#133812=CARTESIAN_POINT('Ctrl Pts',(-235.334547128558,3.40726962232724,
127.257573792387));
#133813=CARTESIAN_POINT('Ctrl Pts',(-235.342293404642,3.3083425208168,127.162538109552));
#133814=CARTESIAN_POINT('Ctrl Pts',(-235.350039680726,3.20541103993886,
127.071620211038));
#133815=CARTESIAN_POINT('Ctrl Pts',(-235.35778595681,3.09885912378931,126.985164996312));
#133816=CARTESIAN_POINT('Ctrl Pts',(-235.365532290076,2.99230642109786,
126.898709143393));
#133817=CARTESIAN_POINT('Ctrl Pts',(-235.373278623341,2.88213353340489,
126.816716286332));
#133818=CARTESIAN_POINT('Ctrl Pts',(-235.381024956606,2.76875724321614,
126.739490829905));
#133819=CARTESIAN_POINT('Ctrl Pts',(-235.388773024609,2.65535556319314,
126.662248079372));
#133820=CARTESIAN_POINT('Ctrl Pts',(-235.396521092612,2.53874937623747,
126.58977507398));
#133821=CARTESIAN_POINT('Ctrl Pts',(-235.404269160615,2.41938382892133,
126.522332482342));
#133822=CARTESIAN_POINT('Ctrl Pts',(-235.412025463357,2.2998914184812,126.454818211915));
#133823=CARTESIAN_POINT('Ctrl Pts',(-235.419781766099,2.17763413026731,
126.392345227849));
#133824=CARTESIAN_POINT('Ctrl Pts',(-235.427538068841,2.05308155658333,
126.33512811248));
#133825=CARTESIAN_POINT('Ctrl Pts',(-235.435298511355,1.92846250544056,
126.277880458613));
#133826=CARTESIAN_POINT('Ctrl Pts',(-235.443058953869,1.80154608939999,
126.225894411192));
#133827=CARTESIAN_POINT('Ctrl Pts',(-235.450819396383,1.67282025870139,
126.179335704706));
#133828=CARTESIAN_POINT('Ctrl Pts',(-235.458592296649,1.54388778587162,
126.13270225805));
#133829=CARTESIAN_POINT('Ctrl Pts',(-235.466365196914,1.41314046711555,
126.09151368012));
#133830=CARTESIAN_POINT('Ctrl Pts',(-235.47413809718,1.28108059911248,126.055885540125));
#133831=CARTESIAN_POINT('Ctrl Pts',(-235.481628432942,1.15382143995185,
126.021552572762));
#133832=CARTESIAN_POINT('Ctrl Pts',(-235.489118768703,1.0253438040743,125.992382858434));
#133833=CARTESIAN_POINT('Ctrl Pts',(-235.496609104465,0.896102648894132,
125.968434325205));
#133834=CARTESIAN_POINT('Ctrl Pts',(-235.504383438584,0.761961276031598,
125.94357777606));
#133835=CARTESIAN_POINT('Ctrl Pts',(-235.512157772703,0.626572423730888,
125.924267407729));
#133836=CARTESIAN_POINT('Ctrl Pts',(-235.519932106822,0.490434491401467,
125.910624103189));
#133837=CARTESIAN_POINT('Ctrl Pts',(-235.52769685977,0.354464336906645,
125.896997612803));
#133838=CARTESIAN_POINT('Ctrl Pts',(-235.535461612717,0.217747324506621,
125.889024328444));
#133839=CARTESIAN_POINT('Ctrl Pts',(-235.543226365664,0.0807925613160798,
125.886774255891));
#133840=CARTESIAN_POINT('Ctrl Pts',(-235.550983406549,-0.0560261764729365,
125.884526418141));
#133841=CARTESIAN_POINT('Ctrl Pts',(-235.558740447434,-0.193081806745442,
125.887990486415));
#133842=CARTESIAN_POINT('Ctrl Pts',(-235.566497488319,-0.329859928223438,
125.897184699561));
#133843=CARTESIAN_POINT('Ctrl Pts',(-235.574248679559,-0.466534904256606,
125.906371979279));
#133844=CARTESIAN_POINT('Ctrl Pts',(-235.581999870799,-0.60293239953105,
125.921280776772));
#133845=CARTESIAN_POINT('Ctrl Pts',(-235.589751062039,-0.738538197029567,
125.941877260882));
#133846=CARTESIAN_POINT('Ctrl Pts',(-235.597498958816,-0.87408635844619,
125.962464990937));
#133847=CARTESIAN_POINT('Ctrl Pts',(-235.605246855593,-1.00884310562224,
125.988735540962));
#133848=CARTESIAN_POINT('Ctrl Pts',(-235.61299475237,-1.14229974818933,
126.020603271317));
#133849=CARTESIAN_POINT('Ctrl Pts',(-235.620741028455,-1.27572847450378,
126.052464335631));
#133850=CARTESIAN_POINT('Ctrl Pts',(-235.628487304539,-1.40785725710731,
126.089920160725));
#133851=CARTESIAN_POINT('Ctrl Pts',(-235.636233580623,-1.53818839114926,
126.132834150143));
#133852=CARTESIAN_POINT('Ctrl Pts',(-235.643979913888,-1.66852048726621,
126.175748456342));
#133853=CARTESIAN_POINT('Ctrl Pts',(-235.651726247154,-1.79705453699011,
126.224120884989));
#133854=CARTESIAN_POINT('Ctrl Pts',(-235.659472580419,-1.92330915483781,
126.277765323372));
#133855=CARTESIAN_POINT('Ctrl Pts',(-235.667220648422,-2.04959204653161,
126.331421775056));
#133856=CARTESIAN_POINT('Ctrl Pts',(-235.674968716425,-2.17359413082439,
126.390352432934));
#133857=CARTESIAN_POINT('Ctrl Pts',(-235.682716784428,-2.29485548723273,
126.454323680341));
#133858=CARTESIAN_POINT('Ctrl Pts',(-235.69047308717,-2.41624572165387,
126.518362917152));
#133859=CARTESIAN_POINT('Ctrl Pts',(-235.698229389912,-2.53488906305481,
126.587453262358));
#133860=CARTESIAN_POINT('Ctrl Pts',(-235.705985692653,-2.65035115112993,
126.661315621648));
#133861=CARTESIAN_POINT('Ctrl Pts',(-235.713746135168,-2.76587486479795,
126.735217403502));
#133862=CARTESIAN_POINT('Ctrl Pts',(-235.721506577682,-2.87821362179063,
126.813896050316));
#133863=CARTESIAN_POINT('Ctrl Pts',(-235.729267020196,-2.98696423596475,
126.897030619272));
#133864=CARTESIAN_POINT('Ctrl Pts',(-235.737039920461,-3.09588942627917,
126.980298643219));
#133865=CARTESIAN_POINT('Ctrl Pts',(-235.744812820727,-3.20121466288184,
127.068036632986));
#133866=CARTESIAN_POINT('Ctrl Pts',(-235.752585720993,-3.30257121049804,
127.159884460134));
#133867=CARTESIAN_POINT('Ctrl Pts',(-235.760076056755,-3.40024319230638,
127.248393387414));
#133868=CARTESIAN_POINT('Ctrl Pts',(-235.767566392516,-3.49422979953322,
127.340718318051));
#133869=CARTESIAN_POINT('Ctrl Pts',(-235.775056728278,-3.58423638006266,
127.436507795019));
#133870=CARTESIAN_POINT('Ctrl Pts',(-235.782737888104,-3.67653597147935,
127.534737608153));
#133871=CARTESIAN_POINT('Ctrl Pts',(-235.79041904793,-3.76495801641091,
127.636938955501));
#133872=CARTESIAN_POINT('Ctrl Pts',(-235.798100207756,-3.84913502487534,
127.742769099617));
#133873=CARTESIAN_POINT('Ctrl Pts',(-235.805772268089,-3.9332123129778,
127.848473871966));
#133874=CARTESIAN_POINT('Ctrl Pts',(-235.813444328422,-4.01305431640041,
127.957798583208));
#133875=CARTESIAN_POINT('Ctrl Pts',(-235.821116388756,-4.08833007477147,
128.070363495728));
#133876=CARTESIAN_POINT('Ctrl Pts',(-235.828950393662,-4.16519478057272,
128.185304468381));
#133877=CARTESIAN_POINT('Ctrl Pts',(-235.836784398569,-4.23729799436331,
128.303623684976));
#133878=CARTESIAN_POINT('Ctrl Pts',(-235.844618403475,-4.30432994138626,
128.424880250304));
#133879=CARTESIAN_POINT('Ctrl Pts',(-235.852276925475,-4.36986036255376,
128.543420650041));
#133880=CARTESIAN_POINT('Ctrl Pts',(-235.859935447474,-4.43054409252308,
128.664767828783));
#133881=CARTESIAN_POINT('Ctrl Pts',(-235.867593969474,-4.48613532636867,
128.788480438585));
#133882=CARTESIAN_POINT('Ctrl Pts',(-235.875515715834,-4.54363723788437,
128.916445066282));
#133883=CARTESIAN_POINT('Ctrl Pts',(-235.883437462194,-4.59569007538285,
129.046940270349));
#133884=CARTESIAN_POINT('Ctrl Pts',(-235.891359208554,-4.64207398189659,
129.179450709571));
#133885=CARTESIAN_POINT('Ctrl Pts',(-235.899280954914,-4.68845788841033,
129.311961148794));
#133886=CARTESIAN_POINT('Ctrl Pts',(-235.907202701273,-4.72917269435152,
129.446486378406));
#133887=CARTESIAN_POINT('Ctrl Pts',(-235.915124447633,-4.76405452823405,
129.582490119308));
#133888=CARTESIAN_POINT('Ctrl Pts',(-234.165426035895,-4.76405452823417,
129.582490119309));
#133889=CARTESIAN_POINT('Ctrl Pts',(-234.173676386822,-4.80022243263185,
129.723508229631));
#133890=CARTESIAN_POINT('Ctrl Pts',(-234.181926737749,-4.83016515151601,
129.866290352672));
#133891=CARTESIAN_POINT('Ctrl Pts',(-234.190177088676,-4.8537222931255,
130.010280669628));
#133892=CARTESIAN_POINT('Ctrl Pts',(-234.198406836468,-4.87722060681593,
130.1539114077));
#133893=CARTESIAN_POINT('Ctrl Pts',(-234.20663658426,-4.89436509346828,
130.298744017136));
#133894=CARTESIAN_POINT('Ctrl Pts',(-234.214866332052,-4.90504591090372,
130.4442111008));
#133895=CARTESIAN_POINT('Ctrl Pts',(-234.22162440936,-4.91381674954474,
130.563665283601));
#133896=CARTESIAN_POINT('Ctrl Pts',(-234.228382486668,-4.91822981504504,
130.683546948129));
#133897=CARTESIAN_POINT('Ctrl Pts',(-234.235140563976,-4.91824993088488,
130.803536086871));
#133898=CARTESIAN_POINT('',(-233.889859436025,-4.91824841365468,130.800410417158));
#133899=CARTESIAN_POINT('Ctrl Pts',(-233.819813589496,-4.76405452823394,
129.582490119308));
#133900=CARTESIAN_POINT('Ctrl Pts',(-233.827589425366,-4.79806106893753,
129.71508110539));
#133901=CARTESIAN_POINT('Ctrl Pts',(-233.835365261237,-4.82648427381513,
129.848921751465));
#133902=CARTESIAN_POINT('Ctrl Pts',(-233.843141097107,-4.84926531900179,
129.983501964431));
#133903=CARTESIAN_POINT('Ctrl Pts',(-233.84393151732,-4.85158103128089,
129.997182155535));
#133904=CARTESIAN_POINT('Ctrl Pts',(-233.844721937534,-4.85383848810793,
130.010869986596));
#133905=CARTESIAN_POINT('Ctrl Pts',(-233.845512357748,-4.85603765781549,
130.024564921003));
#133906=CARTESIAN_POINT('Ctrl Pts',(-233.858223934682,-4.89140481372163,
130.244807532866));
#133907=CARTESIAN_POINT('Ctrl Pts',(-233.870935511616,-4.91179492626046,
130.467516694233));
#133908=CARTESIAN_POINT('Ctrl Pts',(-233.88364708855,-4.91694540615843,
130.691086898824));
#133909=CARTESIAN_POINT('Ctrl Pts',(-233.885717871032,-4.91778444631852,
130.727507656495));
#133910=CARTESIAN_POINT('Ctrl Pts',(-233.887788653514,-4.91821913060618,
130.763951181314));
#133911=CARTESIAN_POINT('Ctrl Pts',(-233.889859435996,-4.91824841365427,
130.800410416651));
#133912=CARTESIAN_POINT('Ctrl Pts',(-233.889859436025,-4.91824841365468,
130.800410417158));
#133913=CARTESIAN_POINT('Ctrl Pts',(-233.897508004962,-4.91835657247153,
130.935074959338));
#133914=CARTESIAN_POINT('Ctrl Pts',(-233.9051565739,-4.91292978437815,131.069942951738));
#133915=CARTESIAN_POINT('Ctrl Pts',(-233.912805142837,-4.90194456494051,
131.204513769185));
#133916=CARTESIAN_POINT('Ctrl Pts',(-233.920446294681,-4.89096999826641,
131.338954088455));
#133917=CARTESIAN_POINT('Ctrl Pts',(-233.928087446525,-4.87444775344177,
131.473097406374));
#133918=CARTESIAN_POINT('Ctrl Pts',(-233.935728598369,-4.85240638693835,
131.606442482777));
#133919=CARTESIAN_POINT('Ctrl Pts',(-233.943571572669,-4.82978285130596,
131.743309545304));
#133920=CARTESIAN_POINT('Ctrl Pts',(-233.951414546968,-4.80134457381579,
131.879335180831));
#133921=CARTESIAN_POINT('Ctrl Pts',(-233.959257521268,-4.76717942709186,
132.013981786533));
#133922=CARTESIAN_POINT('Ctrl Pts',(-233.966890458481,-4.73392923273431,
132.145022517759));
#133923=CARTESIAN_POINT('Ctrl Pts',(-233.974523395693,-4.69525510859911,
132.274756725189));
#133924=CARTESIAN_POINT('Ctrl Pts',(-233.982156332906,-4.6512898508898,
132.402699062799));
#133925=CARTESIAN_POINT('Ctrl Pts',(-233.989788231278,-4.60733057684236,
132.530623987485));
#133926=CARTESIAN_POINT('Ctrl Pts',(-233.997420129649,-4.55808173209536,
132.656757145564));
#133927=CARTESIAN_POINT('Ctrl Pts',(-234.005052028021,-4.5037256650884,
132.780629373612));
#133928=CARTESIAN_POINT('Ctrl Pts',(-234.012684654446,-4.44936441272463,
132.904513418587));
#133929=CARTESIAN_POINT('Ctrl Pts',(-234.020317280871,-4.38989513193338,
133.026135735191));
#133930=CARTESIAN_POINT('Ctrl Pts',(-234.027949907296,-4.32554766040755,
133.145048657447));
#133931=CARTESIAN_POINT('Ctrl Pts',(-234.035950746818,-4.25809593872375,
133.269698175857));
#133932=CARTESIAN_POINT('Ctrl Pts',(-234.04395158634,-4.18528385613835,
133.391369933456));
#133933=CARTESIAN_POINT('Ctrl Pts',(-234.051952425862,-4.10742865771344,
133.509580180613));
#133934=CARTESIAN_POINT('Ctrl Pts',(-234.059595996102,-4.033050003314,133.622511870438));
#133935=CARTESIAN_POINT('Ctrl Pts',(-234.067239566342,-3.9540691714229,
133.732284209412));
#133936=CARTESIAN_POINT('Ctrl Pts',(-234.074883136582,-3.87080489606674,
133.838508359369));
#133937=CARTESIAN_POINT('Ctrl Pts',(-234.082531777,-3.7874853893612,133.944802970554));
#133938=CARTESIAN_POINT('Ctrl Pts',(-234.090180417419,-3.6998770452929,
134.047544402806));
#133939=CARTESIAN_POINT('Ctrl Pts',(-234.097829057837,-3.60833627717124,
134.146379823578));
#133940=CARTESIAN_POINT('Ctrl Pts',(-234.105488112923,-3.51667086380252,
134.245349822261));
#133941=CARTESIAN_POINT('Ctrl Pts',(-234.113147168008,-3.42106263007849,
134.34040291786));
#133942=CARTESIAN_POINT('Ctrl Pts',(-234.120806223094,-3.32190199557209,
134.431225681821));
#133943=CARTESIAN_POINT('Ctrl Pts',(-234.121857475916,-3.30829158335825,
134.44369166958));
#133944=CARTESIAN_POINT('Ctrl Pts',(-234.122908728739,-3.29461429213465,
134.45607802709));
#133945=CARTESIAN_POINT('Ctrl Pts',(-234.123959981561,-3.28087117384239,
134.468384007659));
#133946=CARTESIAN_POINT('Ctrl Pts',(-234.13173431568,-3.17923663724405,
134.559390474019));
#133947=CARTESIAN_POINT('Ctrl Pts',(-234.139508649799,-3.07365167398268,
134.646309097947));
#133948=CARTESIAN_POINT('Ctrl Pts',(-234.147282983918,-2.9644790648186,
134.728777381463));
#133949=CARTESIAN_POINT('Ctrl Pts',(-234.155047736865,-2.85544100113827,
134.811144030189));
#133950=CARTESIAN_POINT('Ctrl Pts',(-234.162812489812,-2.74282439789659,
134.889071017924));
#133951=CARTESIAN_POINT('Ctrl Pts',(-234.170577242759,-2.62702764610736,
134.962233728796));
#133952=CARTESIAN_POINT('Ctrl Pts',(-234.178334283644,-2.51134590528445,
135.035323773432));
#133953=CARTESIAN_POINT('Ctrl Pts',(-234.186091324529,-2.39249062998956,
135.103658750515));
#133954=CARTESIAN_POINT('Ctrl Pts',(-234.193848365414,-2.27089166083551,
135.166955502179));
#133955=CARTESIAN_POINT('Ctrl Pts',(-234.201599556655,-2.14938439040983,
135.230204521269));
#133956=CARTESIAN_POINT('Ctrl Pts',(-234.209350747895,-2.02513788981683,
135.288422697556));
#133957=CARTESIAN_POINT('Ctrl Pts',(-234.217101939135,-1.89860892803468,
135.34137143978));
#133958=CARTESIAN_POINT('Ctrl Pts',(-234.224849835912,-1.77213374443672,
135.394297677376));
#133959=CARTESIAN_POINT('Ctrl Pts',(-234.232597732689,-1.64337838902263,
135.441958784794));
#133960=CARTESIAN_POINT('Ctrl Pts',(-234.240345629466,-1.51282186039079,
135.484163293024));
#133961=CARTESIAN_POINT('Ctrl Pts',(-234.24809190555,-1.38229264136992,
135.526358972981));
#133962=CARTESIAN_POINT('Ctrl Pts',(-234.255838181634,-1.24996337031541,
135.563100203881));
#133963=CARTESIAN_POINT('Ctrl Pts',(-234.263584457719,-1.11633017024271,
135.594244751186));
#133964=CARTESIAN_POINT('Ctrl Pts',(-234.271330790984,-0.982695983720628,
135.625389528393));
#133965=CARTESIAN_POINT('Ctrl Pts',(-234.279077124249,-0.847758229734812,
135.650937450828));
#133966=CARTESIAN_POINT('Ctrl Pts',(-234.286823457515,-0.712024850954133,
135.670797062658));
#133967=CARTESIAN_POINT('Ctrl Pts',(-234.294571525518,-0.576261075624201,
135.690661121911));
#133968=CARTESIAN_POINT('Ctrl Pts',(-234.30231959352,-0.439701707724825,
135.70483427914));
#133969=CARTESIAN_POINT('Ctrl Pts',(-234.310067661523,-0.302861068158666,
135.713276815251));
#133970=CARTESIAN_POINT('Ctrl Pts',(-234.317823964265,-0.165874992732165,
135.72172832419));
#133971=CARTESIAN_POINT('Ctrl Pts',(-234.325580267007,-0.0286074393217352,
135.724437021324));
#133972=CARTESIAN_POINT('Ctrl Pts',(-234.333336569749,0.108425444496076,
135.721415323941));
#133973=CARTESIAN_POINT('Ctrl Pts',(-234.341097012263,0.24553146688996,
135.718392013787));
#133974=CARTESIAN_POINT('Ctrl Pts',(-234.348857454777,0.382402180143489,
135.709632239786));
#133975=CARTESIAN_POINT('Ctrl Pts',(-234.356617897292,0.518526292473832,
135.695200376392));
#133976=CARTESIAN_POINT('Ctrl Pts',(-234.364390797557,0.654868923313818,
135.680745345689));
#133977=CARTESIAN_POINT('Ctrl Pts',(-234.372163697823,0.790462171282616,
135.660600087708));
#133978=CARTESIAN_POINT('Ctrl Pts',(-234.379936598088,0.924803784060439,
135.63488036429));
#133979=CARTESIAN_POINT('Ctrl Pts',(-234.38742693385,1.05426174082805,135.610095617601));
#133980=CARTESIAN_POINT('Ctrl Pts',(-234.394917269612,1.18255718274369,
135.580134730783));
#133981=CARTESIAN_POINT('Ctrl Pts',(-234.402407605374,1.3092556394284,135.545144596311));
#133982=CARTESIAN_POINT('Ctrl Pts',(-234.410181939493,1.44075790660692,
135.508827800255));
#133983=CARTESIAN_POINT('Ctrl Pts',(-234.417956273612,1.57095625827954,
135.46697781968));
#133984=CARTESIAN_POINT('Ctrl Pts',(-234.425730607731,1.69934962276673,
135.419703933301));
#133985=CARTESIAN_POINT('Ctrl Pts',(-234.433495360678,1.82758475390704,
135.372488307763));
#133986=CARTESIAN_POINT('Ctrl Pts',(-234.441260113626,1.95401896056059,
135.31986221033));
#133987=CARTESIAN_POINT('Ctrl Pts',(-234.449024866573,2.07816379412782,
135.26198535584));
#133988=CARTESIAN_POINT('Ctrl Pts',(-234.456781907458,2.20218532529621,
135.204165985458));
#133989=CARTESIAN_POINT('Ctrl Pts',(-234.464538948342,2.32392165636191,
135.141106400485));
#133990=CARTESIAN_POINT('Ctrl Pts',(-234.472295989227,2.44290221924087,
135.073015184257));
#133991=CARTESIAN_POINT('Ctrl Pts',(-234.480047180468,2.56179305795231,
135.004975316144));
#133992=CARTESIAN_POINT('Ctrl Pts',(-234.487798371708,2.67793192694694,
134.931911562692));
#133993=CARTESIAN_POINT('Ctrl Pts',(-234.495549562948,2.79087119785176,
134.854079252175));
#133994=CARTESIAN_POINT('Ctrl Pts',(-234.503297459725,2.90376246655354,
134.776280022467));
#133995=CARTESIAN_POINT('Ctrl Pts',(-234.511045356502,3.01345652068257,
134.693716488162));
#133996=CARTESIAN_POINT('Ctrl Pts',(-234.518793253279,3.11953336149638,
134.606688150671));
#133997=CARTESIAN_POINT('Ctrl Pts',(-234.526539529364,3.22558801332185,
134.519678017633));
#133998=CARTESIAN_POINT('Ctrl Pts',(-234.534285805448,3.32802665477062,
134.428205186891));
#133999=CARTESIAN_POINT('Ctrl Pts',(-234.542032081532,3.42646145328966,
134.332610179547));
#134000=CARTESIAN_POINT('Ctrl Pts',(-234.549778414797,3.52489697843161,
134.237014466543));
#134001=CARTESIAN_POINT('Ctrl Pts',(-234.557524748062,3.61932832119783,
134.137296788598));
#134002=CARTESIAN_POINT('Ctrl Pts',(-234.565271081328,3.70940398178691,
134.033835058153));
#134003=CARTESIAN_POINT('Ctrl Pts',(-234.573019149331,3.79949981419577,
133.93035015817));
#134004=CARTESIAN_POINT('Ctrl Pts',(-234.580767217334,3.88523776677434,
133.823119832075));
#134005=CARTESIAN_POINT('Ctrl Pts',(-234.588515285337,3.96630641971367,
133.712555323468));
#134006=CARTESIAN_POINT('Ctrl Pts',(-234.596271588078,4.04746123338219,
133.601873305586));
#134007=CARTESIAN_POINT('Ctrl Pts',(-234.60402789082,4.12393660255991,133.487850342247));
#134008=CARTESIAN_POINT('Ctrl Pts',(-234.611784193562,4.19546398389031,
133.370927394874));
#134009=CARTESIAN_POINT('Ctrl Pts',(-234.619544636077,4.26702954153776,
133.253942042203));
#134010=CARTESIAN_POINT('Ctrl Pts',(-234.62730507859,4.33364165934758,133.134053962946));
#134011=CARTESIAN_POINT('Ctrl Pts',(-234.635065521105,4.39507813167303,
133.011728117324));
#134012=CARTESIAN_POINT('Ctrl Pts',(-234.64283842137,4.45661322727793,132.889205903396));
#134013=CARTESIAN_POINT('Ctrl Pts',(-234.650611321635,4.5129559137713,132.764238459666));
#134014=CARTESIAN_POINT('Ctrl Pts',(-234.658384221901,4.56393210522144,
132.637310917337));
#134015=CARTESIAN_POINT('Ctrl Pts',(-234.665874557663,4.61305518371081,
132.514997510883));
#134016=CARTESIAN_POINT('Ctrl Pts',(-234.673364893425,4.65719506123983,
132.390864330924));
#134017=CARTESIAN_POINT('Ctrl Pts',(-234.680855229187,4.6962404807556,132.265356308666));
#134018=CARTESIAN_POINT('Ctrl Pts',(-234.688629563306,4.73676631922008,
132.135089611596));
#134019=CARTESIAN_POINT('Ctrl Pts',(-234.696403897425,4.77193213465986,
132.002929114181));
#134020=CARTESIAN_POINT('Ctrl Pts',(-234.704178231544,4.80155902487095,
131.869355450032));
#134021=CARTESIAN_POINT('Ctrl Pts',(-234.711942984491,4.8311494025877,131.735946403487));
#134022=CARTESIAN_POINT('Ctrl Pts',(-234.719707737438,4.85521435339285,
131.601128033501));
#134023=CARTESIAN_POINT('Ctrl Pts',(-234.727472490386,4.87362423150206,
131.465397615484));
#134024=CARTESIAN_POINT('Ctrl Pts',(-234.735229531271,4.8920158246608,131.329802006831));
#134025=CARTESIAN_POINT('Ctrl Pts',(-234.742986572156,4.90476347039832,
131.193296537759));
#134026=CARTESIAN_POINT('Ctrl Pts',(-234.75074361304,4.91178830224006,131.056389854913));
#134027=CARTESIAN_POINT('Ctrl Pts',(-234.758494804281,4.9188078366015,130.919586414461));
#134028=CARTESIAN_POINT('Ctrl Pts',(-234.766245995521,4.92011312709053,
130.78238275133));
#134029=CARTESIAN_POINT('Ctrl Pts',(-234.773997186761,4.91567703454626,
130.645293479117));
#134030=CARTESIAN_POINT('Ctrl Pts',(-234.781745083538,4.91124282745968,
130.508262473502));
#134031=CARTESIAN_POINT('Ctrl Pts',(-234.789492980315,4.90107210341125,
130.371346152049));
#134032=CARTESIAN_POINT('Ctrl Pts',(-234.797240877092,4.88518982184064,
130.235059759421));
#134033=CARTESIAN_POINT('Ctrl Pts',(-234.804987153176,4.86931086250096,
130.098801874969));
#134034=CARTESIAN_POINT('Ctrl Pts',(-234.812733429261,4.84772276725855,
129.963174045341));
#134035=CARTESIAN_POINT('Ctrl Pts',(-234.820479705345,4.82050239319234,
129.828686625022));
#134036=CARTESIAN_POINT('Ctrl Pts',(-234.82822603861,4.79328181819148,129.694198211947));
#134037=CARTESIAN_POINT('Ctrl Pts',(-234.835972371875,4.7604289589635,129.560850608174));
#134038=CARTESIAN_POINT('Ctrl Pts',(-234.843718705141,4.72207176972025,
129.429143811346));
#134039=CARTESIAN_POINT('Ctrl Pts',(-234.851466773144,4.68370599065036,
129.297407519693));
#134040=CARTESIAN_POINT('Ctrl Pts',(-234.859214841147,4.63983353802021,
129.167313141463));
#134041=CARTESIAN_POINT('Ctrl Pts',(-234.86696290915,4.59063207270527,129.039344970171));
#134042=CARTESIAN_POINT('Ctrl Pts',(-234.874719211891,4.54137831548755,
128.911240792784));
#134043=CARTESIAN_POINT('Ctrl Pts',(-234.882475514633,4.48678437218778,
128.785267701949));
#134044=CARTESIAN_POINT('Ctrl Pts',(-234.890231817375,4.42707608189503,
128.661889981218));
#134045=CARTESIAN_POINT('Ctrl Pts',(-234.897992259889,4.3673359234898,128.538446410082));
#134046=CARTESIAN_POINT('Ctrl Pts',(-234.905752702404,4.30247616377143,
128.417601313548));
#134047=CARTESIAN_POINT('Ctrl Pts',(-234.913513144918,4.23276787936328,
128.299792961876));
#134048=CARTESIAN_POINT('Ctrl Pts',(-234.921286045183,4.16294769302879,
128.181795493779));
#134049=CARTESIAN_POINT('Ctrl Pts',(-234.929058945449,4.08826364165262,
128.066844840089));
#134050=CARTESIAN_POINT('Ctrl Pts',(-234.936831845714,4.00902978215786,
127.955349689494));
#134051=CARTESIAN_POINT('Ctrl Pts',(-234.944322181476,3.93267627303442,
127.847907668465));
#134052=CARTESIAN_POINT('Ctrl Pts',(-234.951812517238,3.85209819508192,
127.743674523504));
#134053=CARTESIAN_POINT('Ctrl Pts',(-234.959302853,3.76760974436991,127.642984354508));
#134054=CARTESIAN_POINT('Ctrl Pts',(-234.967077187119,3.67991788836859,
127.538476487148));
#134055=CARTESIAN_POINT('Ctrl Pts',(-234.974851521238,3.58773550113176,
127.437454513619));
#134056=CARTESIAN_POINT('Ctrl Pts',(-234.982625855357,3.49137025231658,
127.340328743616));
#134057=CARTESIAN_POINT('Ctrl Pts',(-234.990390608304,3.39512376505842,
127.243322672445));
#134058=CARTESIAN_POINT('Ctrl Pts',(-234.998155361251,3.29470494586347,
127.150203525679));
#134059=CARTESIAN_POINT('Ctrl Pts',(-235.005920114198,3.19046208990488,
127.061349167493));
#134060=CARTESIAN_POINT('Ctrl Pts',(-235.013677155083,3.08632276941954,
126.972583060707));
#134061=CARTESIAN_POINT('Ctrl Pts',(-235.021434195969,2.97836726615232,
126.888073564951));
#134062=CARTESIAN_POINT('Ctrl Pts',(-235.029191236854,2.86698088967546,
126.808161968758));
#134063=CARTESIAN_POINT('Ctrl Pts',(-235.036942428094,2.75567851053171,
126.728310634522));
#134064=CARTESIAN_POINT('Ctrl Pts',(-235.044693619334,2.64095072432235,
126.653050525357));
#134065=CARTESIAN_POINT('Ctrl Pts',(-235.052444810574,2.52321582066163,
126.582682635429));
#134066=CARTESIAN_POINT('Ctrl Pts',(-235.060192707351,2.40553095747613,
126.512344653731));
#134067=CARTESIAN_POINT('Ctrl Pts',(-235.067940604128,2.28484185378314,
126.44689495581));
#134068=CARTESIAN_POINT('Ctrl Pts',(-235.075688500905,2.16159549069878,
126.386591044909));
#134069=CARTESIAN_POINT('Ctrl Pts',(-235.083434776989,2.03837490809635,
126.326299748287));
#134070=CARTESIAN_POINT('Ctrl Pts',(-235.091181053074,1.91259848105292,
126.271152269413));
#134071=CARTESIAN_POINT('Ctrl Pts',(-235.098927329158,1.78473712837853,
126.221359805316));
#134072=CARTESIAN_POINT('Ctrl Pts',(-235.106673662423,1.6568748318612,126.171566973662));
#134073=CARTESIAN_POINT('Ctrl Pts',(-235.114419995688,1.52692794331774,
126.127129377536));
#134074=CARTESIAN_POINT('Ctrl Pts',(-235.122166328954,1.39538628730345,
126.088209626376));
#134075=CARTESIAN_POINT('Ctrl Pts',(-235.129914396957,1.26381517344716,
126.049281159407));
#134076=CARTESIAN_POINT('Ctrl Pts',(-235.13766246496,1.13064895628658,126.015873107172));
#134077=CARTESIAN_POINT('Ctrl Pts',(-235.145410532963,0.996391115716242,
125.98809777102));
#134078=CARTESIAN_POINT('Ctrl Pts',(-235.153166835705,0.861990584315074,
125.96029291491));
#134079=CARTESIAN_POINT('Ctrl Pts',(-235.160923138446,0.726496495367408,
125.938132812929));
#134080=CARTESIAN_POINT('Ctrl Pts',(-235.168679441188,0.590421535317904,
125.921678416856));
#134081=CARTESIAN_POINT('Ctrl Pts',(-235.176439883703,0.454273947965083,
125.905215238576));
#134082=CARTESIAN_POINT('Ctrl Pts',(-235.184200326217,0.317545261323974,
125.894463864868));
#134083=CARTESIAN_POINT('Ctrl Pts',(-235.191960768731,0.180750728114019,
125.889433127075));
#134084=CARTESIAN_POINT('Ctrl Pts',(-235.199733668996,0.0437366001753084,
125.884394313494));
#134085=CARTESIAN_POINT('Ctrl Pts',(-235.207506569262,-0.0933431943749275,
125.885094484934));
#134086=CARTESIAN_POINT('Ctrl Pts',(-235.215279469527,-0.229975058728639,
125.89149032263));
#134087=CARTESIAN_POINT('Ctrl Pts',(-235.222769805289,-0.361640010653015,
125.897653655516));
#134088=CARTESIAN_POINT('Ctrl Pts',(-235.230260141051,-0.492888726902967,
125.9091057137));
#134089=CARTESIAN_POINT('Ctrl Pts',(-235.237750476813,-0.623270289125128,
125.925762744284));
#134090=CARTESIAN_POINT('Ctrl Pts',(-235.245524810932,-0.758595307911966,
125.943051331246));
#134091=CARTESIAN_POINT('Ctrl Pts',(-235.253299145051,-0.893414787314326,
125.966002140077));
#134092=CARTESIAN_POINT('Ctrl Pts',(-235.26107347917,-1.02721721919833,
125.994578101996));
#134093=CARTESIAN_POINT('Ctrl Pts',(-235.268838232117,-1.16085475154366,
126.023118846596));
#134094=CARTESIAN_POINT('Ctrl Pts',(-235.276602985064,-1.29347735163081,
126.057270869804));
#134095=CARTESIAN_POINT('Ctrl Pts',(-235.284367738011,-1.42457884957813,
126.096945385845));
#134096=CARTESIAN_POINT('Ctrl Pts',(-235.292124778896,-1.55555013566913,
126.136580496598));
#134097=CARTESIAN_POINT('Ctrl Pts',(-235.299881819781,-1.68500295435694,
126.181727072239));
#134098=CARTESIAN_POINT('Ctrl Pts',(-235.307638860666,-1.81244190069604,
126.232245415704));
#134099=CARTESIAN_POINT('Ctrl Pts',(-235.315390051906,-1.9397847443342,
126.282725662892));
#134100=CARTESIAN_POINT('Ctrl Pts',(-235.323141243146,-2.06511637647834,
126.338569471355));
#134101=CARTESIAN_POINT('Ctrl Pts',(-235.330892434386,-2.18795746645997,
126.399587616893));
#134102=CARTESIAN_POINT('Ctrl Pts',(-235.338640331164,-2.31074634570197,
126.46057982809));
#134103=CARTESIAN_POINT('Ctrl Pts',(-235.346388227941,-2.43104643873598,
126.526741828696));
#134104=CARTESIAN_POINT('Ctrl Pts',(-235.354136124718,-2.54839949657897,
126.597836747631));
#134105=CARTESIAN_POINT('Ctrl Pts',(-235.361882400802,-2.66572800669178,
126.668916795041));
#134106=CARTESIAN_POINT('Ctrl Pts',(-235.369628676886,-2.78011037360252,
126.744927505902));
#134107=CARTESIAN_POINT('Ctrl Pts',(-235.37737495297,-2.89111436815078,
126.825586840035));
#134108=CARTESIAN_POINT('Ctrl Pts',(-235.385121286235,-3.00211918210516,
126.906246769576));
#134109=CARTESIAN_POINT('Ctrl Pts',(-235.392867619501,-3.1097452576507,
126.99155516104));
#134110=CARTESIAN_POINT('Ctrl Pts',(-235.400613952766,-3.21359102472567,
127.081187805528));
#134111=CARTESIAN_POINT('Ctrl Pts',(-235.408362020769,-3.31746004734059,
127.170840522625));
#134112=CARTESIAN_POINT('Ctrl Pts',(-235.416110088772,-3.41754678099235,
127.264819164315));
#134113=CARTESIAN_POINT('Ctrl Pts',(-235.423858156775,-3.51348460019401,
127.362760840326));
#134114=CARTESIAN_POINT('Ctrl Pts',(-235.431614459517,-3.60952438325146,
127.460806609915));
#134115=CARTESIAN_POINT('Ctrl Pts',(-235.439370762259,-3.70140616935787,
127.562823547927));
#134116=CARTESIAN_POINT('Ctrl Pts',(-235.447127065001,-3.78880155850952,
127.668413262661));
#134117=CARTESIAN_POINT('Ctrl Pts',(-235.454887507515,-3.87624359321179,
127.774059333805));
#134118=CARTESIAN_POINT('Ctrl Pts',(-235.462647950029,-3.95919422331985,
127.883281670127));
#134119=CARTESIAN_POINT('Ctrl Pts',(-235.470408392543,-4.03736751209587,
127.995651548479));
#134120=CARTESIAN_POINT('Ctrl Pts',(-235.478181292809,-4.11566629157493,
128.108201812935));
#134121=CARTESIAN_POINT('Ctrl Pts',(-235.485954193074,-4.18917219482737,
128.223909386157));
#134122=CARTESIAN_POINT('Ctrl Pts',(-235.49372709334,-4.25764405553614,
128.342318749754));
#134123=CARTESIAN_POINT('Ctrl Pts',(-235.501217429102,-4.32362679163999,
128.456423634733));
#134124=CARTESIAN_POINT('Ctrl Pts',(-235.508707764864,-4.38493498781607,
128.57303701406));
#134125=CARTESIAN_POINT('Ctrl Pts',(-235.516198100627,-4.4413953753653,
128.691734246864));
#134126=CARTESIAN_POINT('Ctrl Pts',(-235.524611330118,-4.50481231856901,
128.825056315627));
#134127=CARTESIAN_POINT('Ctrl Pts',(-235.533024559609,-4.56229001563584,
128.961378149476));
#134128=CARTESIAN_POINT('Ctrl Pts',(-235.5414377891,-4.61355790223604,129.100169740576));
#134129=CARTESIAN_POINT('Ctrl Pts',(-235.549829414691,-4.66469414065789,
129.238604935863));
#134130=CARTESIAN_POINT('Ctrl Pts',(-235.558221040281,-4.70965226663767,
129.379496971179));
#134131=CARTESIAN_POINT('Ctrl Pts',(-235.566612665872,-4.74820913826364,
129.522294690318));
#134132=CARTESIAN_POINT('Ctrl Pts',(-235.56778964017,-4.75361696377262,
129.542322901001));
#134133=CARTESIAN_POINT('Ctrl Pts',(-235.568966614468,-4.75889894093515,
129.562388562677));
#134134=CARTESIAN_POINT('Ctrl Pts',(-235.570143588767,-4.76405452823401,
129.582490119308));
#134135=CARTESIAN_POINT('Origin',(213.235140564004,0.,130.804360617566));
#134136=CARTESIAN_POINT('',(-237.665046159034,-4.76405452823396,129.582490119308));
#134137=CARTESIAN_POINT('',(-237.319878776621,-4.76405452823405,129.582490119308));
#134138=CARTESIAN_POINT('',(213.235140564004,-4.76405452823405,129.582490119308));
#134139=CARTESIAN_POINT('',(-235.98514056405,-4.91824789693063,130.808908896076));
#134140=CARTESIAN_POINT('Ctrl Pts',(-235.98514056405,-4.91824789693063,
130.808908896075));
#134141=CARTESIAN_POINT('Ctrl Pts',(-235.995166432559,-4.91808414983754,
130.985975624643));
#134142=CARTESIAN_POINT('Ctrl Pts',(-236.005192301068,-4.90835484506816,
131.162615021248));
#134143=CARTESIAN_POINT('Ctrl Pts',(-236.015218169578,-4.8892187176409,
131.33795540162));
#134144=CARTESIAN_POINT('Ctrl Pts',(-236.025483509521,-4.86962551700637,
131.517483849318));
#134145=CARTESIAN_POINT('Ctrl Pts',(-236.035748849464,-4.84017073368366,
131.695650792814));
#134146=CARTESIAN_POINT('Ctrl Pts',(-236.046014189407,-4.8010725964576,
131.871546161904));
#134147=CARTESIAN_POINT('Ctrl Pts',(-236.048510910302,-4.7915632049812,
131.914327175073));
#134148=CARTESIAN_POINT('Ctrl Pts',(-236.051007631197,-4.7814835776014,
131.956973916247));
#134149=CARTESIAN_POINT('Ctrl Pts',(-236.053504352091,-4.77083727542129,
131.999473479998));
#134150=CARTESIAN_POINT('Ctrl Pts',(-236.061278686211,-4.73768662952635,
132.131809380741));
#134151=CARTESIAN_POINT('Ctrl Pts',(-236.06905302033,-4.69897310215588,
132.262974522646));
#134152=CARTESIAN_POINT('Ctrl Pts',(-236.076827354449,-4.65479391621698,
132.392465355941));
#134153=CARTESIAN_POINT('Ctrl Pts',(-236.084592107396,-4.61066917717633,
132.521796603357));
#134154=CARTESIAN_POINT('Ctrl Pts',(-236.092356860343,-4.56109230710251,
132.649457281315));
#134155=CARTESIAN_POINT('Ctrl Pts',(-236.10012161329,-4.5062112534178,132.774955249161));
#134156=CARTESIAN_POINT('Ctrl Pts',(-236.107878654175,-4.4513847083693,
132.900328570656));
#134157=CARTESIAN_POINT('Ctrl Pts',(-236.11563569506,-4.39126461927995,
133.023543100831));
#134158=CARTESIAN_POINT('Ctrl Pts',(-236.123392735945,-4.32604821708376,
133.144123401689));
#134159=CARTESIAN_POINT('Ctrl Pts',(-236.131143927185,-4.26088099508388,
133.264612772004));
#134160=CARTESIAN_POINT('Ctrl Pts',(-236.138895118425,-4.19062529481431,
133.382471524497));
#134161=CARTESIAN_POINT('Ctrl Pts',(-236.146646309665,-4.11552562917464,
133.497246032526));
#134162=CARTESIAN_POINT('Ctrl Pts',(-236.154394206442,-4.04045788289612,
133.611971758329));
#134163=CARTESIAN_POINT('Ctrl Pts',(-236.162142103219,-3.96055047968925,
133.723615520451));
#134164=CARTESIAN_POINT('Ctrl Pts',(-236.169889999996,-3.87609275590384,
133.831750253891));
#134165=CARTESIAN_POINT('Ctrl Pts',(-236.17763627608,-3.79165269885331,
133.939862367877));
#134166=CARTESIAN_POINT('Ctrl Pts',(-236.185382552165,-3.70266445496727,
134.044466605248));
#134167=CARTESIAN_POINT('Ctrl Pts',(-236.193128828249,-3.60945914037416,
134.145167073569));
#134168=CARTESIAN_POINT('Ctrl Pts',(-236.200875161514,-3.51625313776097,
134.245868285237));
#134169=CARTESIAN_POINT('Ctrl Pts',(-236.208621494779,-3.41883026789406,
134.342665383429));
#134170=CARTESIAN_POINT('Ctrl Pts',(-236.216367828044,-3.31755989935976,
134.435197900709));
#134171=CARTESIAN_POINT('Ctrl Pts',(-236.224115896047,-3.21626685202845,
134.527751140004));
#134172=CARTESIAN_POINT('Ctrl Pts',(-236.231863964051,-3.1111248800744,
134.616037634331));
#134173=CARTESIAN_POINT('Ctrl Pts',(-236.239612032054,-3.00253763545448,
134.699736184848));
#134174=CARTESIAN_POINT('Ctrl Pts',(-236.247368334795,-2.89383498301892,
134.783523691181));
#134175=CARTESIAN_POINT('Ctrl Pts',(-236.255124637537,-2.78168005347156,
134.862713274066));
#134176=CARTESIAN_POINT('Ctrl Pts',(-236.262880940279,-2.66650723694804,
134.937025885623));
#134177=CARTESIAN_POINT('Ctrl Pts',(-236.270641382793,-2.55127294922425,
135.011378160058));
#134178=CARTESIAN_POINT('Ctrl Pts',(-236.278401825307,-2.43301790192989,
135.080848078559));
#134179=CARTESIAN_POINT('Ctrl Pts',(-236.286162267822,-2.31220158906708,
135.145202341704));
#134180=CARTESIAN_POINT('Ctrl Pts',(-236.293935168087,-2.19119133113328,
135.209659912025));
#134181=CARTESIAN_POINT('Ctrl Pts',(-236.301708068352,-2.06761194406125,
135.268985247294));
#134182=CARTESIAN_POINT('Ctrl Pts',(-236.309480968618,-1.94194424176665,
135.322992669899));
#134183=CARTESIAN_POINT('Ctrl Pts',(-236.31697130438,-1.82084487698727,
135.375036786656));
#134184=CARTESIAN_POINT('Ctrl Pts',(-236.324461640142,-1.69780667966961,
135.422142807038));
#134185=CARTESIAN_POINT('Ctrl Pts',(-236.331951975904,-1.57327178302742,
135.464188828909));
#134186=CARTESIAN_POINT('Ctrl Pts',(-236.339726310023,-1.44401510792876,
135.507829038479));
#134187=CARTESIAN_POINT('Ctrl Pts',(-236.347500644142,-1.31273655208019,
135.546156214564));
#134188=CARTESIAN_POINT('Ctrl Pts',(-236.355274978261,-1.17991231752151,
135.5789799726));
#134189=CARTESIAN_POINT('Ctrl Pts',(-236.363039731208,-1.04725177696108,
135.611763278287));
#134190=CARTESIAN_POINT('Ctrl Pts',(-236.370804484156,-0.913049723799389,
135.639056568126));
#134191=CARTESIAN_POINT('Ctrl Pts',(-236.378569237103,-0.777800179102438,
135.660718300428));
#134192=CARTESIAN_POINT('Ctrl Pts',(-236.386326277988,-0.642684966159964,
135.682358517992));
#134193=CARTESIAN_POINT('Ctrl Pts',(-236.394083318873,-0.506524715639203,
135.698378247593));
#134194=CARTESIAN_POINT('Ctrl Pts',(-236.401840359758,-0.369826035129639,
135.708686439352));
#134195=CARTESIAN_POINT('Ctrl Pts',(-236.409591550998,-0.233230440158594,
135.718986857624));
#134196=CARTESIAN_POINT('Ctrl Pts',(-236.417342742238,-0.0960976116661581,
135.723584281825));
#134197=CARTESIAN_POINT('Ctrl Pts',(-236.425093933478,0.0410586362118856,
135.722439231303));
#134198=CARTESIAN_POINT('Ctrl Pts',(-236.432841830255,0.178156589026005,
135.721294667457));
#134199=CARTESIAN_POINT('Ctrl Pts',(-236.440589727032,0.315277551295167,
135.714412486521));
#134200=CARTESIAN_POINT('Ctrl Pts',(-236.448337623809,0.451905827774221,
135.701805276296));
#134201=CARTESIAN_POINT('Ctrl Pts',(-236.456083899893,0.5885055245632,135.689200703227));
#134202=CARTESIAN_POINT('Ctrl Pts',(-236.463830175977,0.72461235148788,
135.670873518767));
#134203=CARTESIAN_POINT('Ctrl Pts',(-236.471576452061,0.859714256675553,
135.646888310762));
#134204=CARTESIAN_POINT('Ctrl Pts',(-236.479322785327,0.994817159154617,
135.622902925703));
#134205=CARTESIAN_POINT('Ctrl Pts',(-236.487069118592,1.12891474014856,
135.593259502098));
#134206=CARTESIAN_POINT('Ctrl Pts',(-236.494815451857,1.26150407545233,
135.558073958746));
#134207=CARTESIAN_POINT('Ctrl Pts',(-236.50256351986,1.39412310321826,135.522880535836));
#134208=CARTESIAN_POINT('Ctrl Pts',(-236.510311587863,1.525232835375,135.482142623757));
#134209=CARTESIAN_POINT('Ctrl Pts',(-236.518059655866,1.65434485449897,
135.436026210513));
#134210=CARTESIAN_POINT('Ctrl Pts',(-236.525815958608,1.78359409541349,
135.389860784197));
#134211=CARTESIAN_POINT('Ctrl Pts',(-236.53357226135,1.91084101321725,135.338305569438));
#134212=CARTESIAN_POINT('Ctrl Pts',(-236.541328564092,2.03561603854606,
135.281575198766));
#134213=CARTESIAN_POINT('Ctrl Pts',(-236.549089006606,2.16045766006314,
135.224814549387));
#134214=CARTESIAN_POINT('Ctrl Pts',(-236.55684944912,2.28282441159067,135.162873416788));
#134215=CARTESIAN_POINT('Ctrl Pts',(-236.564609891634,2.40227164398708,
135.096012282251));
#134216=CARTESIAN_POINT('Ctrl Pts',(-236.5723827919,2.52191062368496,135.029043816285));
#134217=CARTESIAN_POINT('Ctrl Pts',(-236.580155692165,2.63862038573402,
134.957139770806));
#134218=CARTESIAN_POINT('Ctrl Pts',(-236.587928592431,2.75198482263593,
134.880604304894));
#134219=CARTESIAN_POINT('Ctrl Pts',(-236.595418928193,2.8612281767099,134.806851095948));
#134220=CARTESIAN_POINT('Ctrl Pts',(-236.602909263955,2.96736495679474,
134.728797530567));
#134221=CARTESIAN_POINT('Ctrl Pts',(-236.610399599717,3.07005361936947,
134.646749696862));
#134222=CARTESIAN_POINT('Ctrl Pts',(-236.618173933836,3.17663575379591,
134.561590994606));
#134223=CARTESIAN_POINT('Ctrl Pts',(-236.625948267955,3.27984075861181,
134.471859402436));
#134224=CARTESIAN_POINT('Ctrl Pts',(-236.633722602074,3.37925105905551,
134.377852655107));
#134225=CARTESIAN_POINT('Ctrl Pts',(-236.641487355021,3.47853884518846,
134.283961762693));
#134226=CARTESIAN_POINT('Ctrl Pts',(-236.649252107968,3.57404095071726,
134.185806464402));
#134227=CARTESIAN_POINT('Ctrl Pts',(-236.657016860916,3.66537126215758,
134.083725887409));
#134228=CARTESIAN_POINT('Ctrl Pts',(-236.664773901801,3.75661086304505,
133.981746698283));
#134229=CARTESIAN_POINT('Ctrl Pts',(-236.672530942686,3.8436866565667,133.875850278415));
#134230=CARTESIAN_POINT('Ctrl Pts',(-236.680287983571,3.92624820610317,
133.766413636432));
#134231=CARTESIAN_POINT('Ctrl Pts',(-236.688039174811,4.00874749533279,
133.657059521472));
#134232=CARTESIAN_POINT('Ctrl Pts',(-236.695790366051,4.08673908197466,
133.544170809137));
#134233=CARTESIAN_POINT('Ctrl Pts',(-236.703541557291,4.15991202074636,
133.428158445553));
#134234=CARTESIAN_POINT('Ctrl Pts',(-236.711289454068,4.23305385906723,
133.312195390319));
#134235=CARTESIAN_POINT('Ctrl Pts',(-236.719037350845,4.30138091480472,
133.193111654392));
#134236=CARTESIAN_POINT('Ctrl Pts',(-236.726785247622,4.36462503255551,
133.071347910801));
#134237=CARTESIAN_POINT('Ctrl Pts',(-236.734531523706,4.42785592100025,
132.949609637561));
#134238=CARTESIAN_POINT('Ctrl Pts',(-236.74227779979,4.48600580620815,132.825192818456));
#134239=CARTESIAN_POINT('Ctrl Pts',(-236.750024075874,4.53885225121814,
132.698563168539));
#134240=CARTESIAN_POINT('Ctrl Pts',(-236.75777040914,4.59169908632851,132.57193258387));
#134241=CARTESIAN_POINT('Ctrl Pts',(-236.765516742405,4.63924225254704,
132.4430894966));
#134242=CARTESIAN_POINT('Ctrl Pts',(-236.77326307567,4.68130743282521,132.312519688047));
#134243=CARTESIAN_POINT('Ctrl Pts',(-236.781011143673,4.72338203330879,
132.181920639292));
#134244=CARTESIAN_POINT('Ctrl Pts',(-236.788759211676,4.75997608688292,
132.04959447185));
#134245=CARTESIAN_POINT('Ctrl Pts',(-236.796507279679,4.79096524240906,
131.916041825704));
#134246=CARTESIAN_POINT('Ctrl Pts',(-236.804263582421,4.82198733357852,
131.782347238217));
#134247=CARTESIAN_POINT('Ctrl Pts',(-236.812019885163,4.8473925385345,131.647423949566));
#134248=CARTESIAN_POINT('Ctrl Pts',(-236.819776187905,4.86710761999026,
131.51178303588));
#134249=CARTESIAN_POINT('Ctrl Pts',(-236.827536630419,4.88683322397865,
131.376069726554));
#134250=CARTESIAN_POINT('Ctrl Pts',(-236.835297072933,4.90086261303366,
131.239638417721));
#134251=CARTESIAN_POINT('Ctrl Pts',(-236.843057515447,4.90917459371302,
131.103004001793));
#134252=CARTESIAN_POINT('Ctrl Pts',(-236.850830415713,4.91749991752167,
130.966150248171));
#134253=CARTESIAN_POINT('Ctrl Pts',(-236.858603315978,4.92008948481346,
130.829093127031));
#134254=CARTESIAN_POINT('Ctrl Pts',(-236.866376216244,4.91697427697041,
130.69234712681));
#134255=CARTESIAN_POINT('Ctrl Pts',(-236.873866552006,4.91397231477915,
130.560572188138));
#134256=CARTESIAN_POINT('Ctrl Pts',(-236.881356887768,4.90567316180276,
130.429086450449));
#134257=CARTESIAN_POINT('Ctrl Pts',(-236.88884722353,4.8921497260235,130.298342712084));
#134258=CARTESIAN_POINT('Ctrl Pts',(-236.896621557649,4.87811354506645,
130.162641785142));
#134259=CARTESIAN_POINT('Ctrl Pts',(-236.904395891768,4.85840464126854,
130.027310374288));
#134260=CARTESIAN_POINT('Ctrl Pts',(-236.912170225887,4.83304779795251,
129.892860729905));
#134261=CARTESIAN_POINT('Ctrl Pts',(-236.919934978834,4.80772220467972,
129.758576782692));
#134262=CARTESIAN_POINT('Ctrl Pts',(-236.927699731781,4.77676259313181,
129.625172820248));
#134263=CARTESIAN_POINT('Ctrl Pts',(-236.935464484729,4.74024557683553,
129.493156997303));
#134264=CARTESIAN_POINT('Ctrl Pts',(-236.943221525614,4.70376482975463,
129.361272294334));
#134265=CARTESIAN_POINT('Ctrl Pts',(-236.950978566499,4.66173776591971,
129.230773361527));
#134266=CARTESIAN_POINT('Ctrl Pts',(-236.958735607384,4.61429215381493,
129.102158813507));
#134267=CARTESIAN_POINT('Ctrl Pts',(-236.966486798624,4.56688232081526,
128.973641254718));
#134268=CARTESIAN_POINT('Ctrl Pts',(-236.974237989864,4.51406220758329,
128.847005617562));
#134269=CARTESIAN_POINT('Ctrl Pts',(-236.981989181104,4.45600948121401,
128.722735635531));
#134270=CARTESIAN_POINT('Ctrl Pts',(-236.989737077881,4.39798142880212,
128.598518471558));
#134271=CARTESIAN_POINT('Ctrl Pts',(-236.997484974658,4.33472535174735,
128.476665316393));
#134272=CARTESIAN_POINT('Ctrl Pts',(-237.005232871435,4.26646705620375,
128.357639971307));
#134273=CARTESIAN_POINT('Ctrl Pts',(-237.012979147519,4.1982230388241,128.238639523758));
#134274=CARTESIAN_POINT('Ctrl Pts',(-237.020725423603,4.12497907858892,
128.122466048667));
#134275=CARTESIAN_POINT('Ctrl Pts',(-237.028471699688,4.04700676214935,
128.009558418909));
#134276=CARTESIAN_POINT('Ctrl Pts',(-237.036218032953,3.96903387013575,
127.896649955693));
#134277=CARTESIAN_POINT('Ctrl Pts',(-237.043964366218,3.88633277443656,
127.787007707624));
#134278=CARTESIAN_POINT('Ctrl Pts',(-237.051710699484,3.79921795401148,
127.68104090924));
#134279=CARTESIAN_POINT('Ctrl Pts',(-237.059458767487,3.71208362482651,
127.575050380327));
#134280=CARTESIAN_POINT('Ctrl Pts',(-237.06720683549,3.62053385230199,127.472737240909));
#134281=CARTESIAN_POINT('Ctrl Pts',(-237.074954903493,3.52492262420586,
127.37447671926));
#134282=CARTESIAN_POINT('Ctrl Pts',(-237.082711206234,3.42920977935859,
127.276111765158));
#134283=CARTESIAN_POINT('Ctrl Pts',(-237.090467508976,3.32942712922516,
127.181808313515));
#134284=CARTESIAN_POINT('Ctrl Pts',(-237.098223811718,3.22596507008493,
127.091904230066));
#134285=CARTESIAN_POINT('Ctrl Pts',(-237.105984254232,3.12244779012856,
127.0019521621));
#134286=CARTESIAN_POINT('Ctrl Pts',(-237.113744696746,3.01524749354317,
126.916404384811));
#134287=CARTESIAN_POINT('Ctrl Pts',(-237.121505139261,2.90478591832392,
126.835557040768));
#134288=CARTESIAN_POINT('Ctrl Pts',(-237.129278039526,2.79414702037781,
126.754579913391));
#134289=CARTESIAN_POINT('Ctrl Pts',(-237.137050939792,2.68023670707852,
126.678318515306));
#134290=CARTESIAN_POINT('Ctrl Pts',(-237.144823840057,2.56350457831185,
126.607024874565));
#134291=CARTESIAN_POINT('Ctrl Pts',(-237.152314175819,2.45101595645665,
126.538322937243));
#134292=CARTESIAN_POINT('Ctrl Pts',(-237.159804511581,2.33590738656979,
126.474233996749));
#134293=CARTESIAN_POINT('Ctrl Pts',(-237.167294847343,2.2185992292628,126.414941462095));
#134294=CARTESIAN_POINT('Ctrl Pts',(-237.175069181462,2.09684329751596,
126.353400832968));
#134295=CARTESIAN_POINT('Ctrl Pts',(-237.182843515581,1.97233200486079,
126.296832558698));
#134296=CARTESIAN_POINT('Ctrl Pts',(-237.1906178497,1.84550971804157,126.245492672219));
#134297=CARTESIAN_POINT('Ctrl Pts',(-237.198382602647,1.71884372835678,
126.194216057561));
#134298=CARTESIAN_POINT('Ctrl Pts',(-237.206147355594,1.58987277028362,
126.148155155304));
#134299=CARTESIAN_POINT('Ctrl Pts',(-237.213912108542,1.45906578027165,
126.107520178362));
#134300=CARTESIAN_POINT('Ctrl Pts',(-237.221669149427,1.32838870960621,
126.066925560652));
#134301=CARTESIAN_POINT('Ctrl Pts',(-237.229426190312,1.19587960694285,
126.031746258929));
#134302=CARTESIAN_POINT('Ctrl Pts',(-237.237183231197,1.06202703287415,
126.002144291332));
#134303=CARTESIAN_POINT('Ctrl Pts',(-237.244934422437,0.928275398072595,
125.97256464681));
#134304=CARTESIAN_POINT('Ctrl Pts',(-237.252685613677,0.793182688620832,
125.948554048885));
#134305=CARTESIAN_POINT('Ctrl Pts',(-237.260436804917,0.657251916610459,
125.930224490968));
#134306=CARTESIAN_POINT('Ctrl Pts',(-237.268184701694,0.521378918804447,
125.911902723601));
#134307=CARTESIAN_POINT('Ctrl Pts',(-237.275932598471,0.384668953539662,
125.899257245937));
#134308=CARTESIAN_POINT('Ctrl Pts',(-237.283680495248,0.247634283703189,
125.892348776779));
#134309=CARTESIAN_POINT('Ctrl Pts',(-237.291426771332,0.11062827856552,
125.885441752723));
#134310=CARTESIAN_POINT('Ctrl Pts',(-237.299173047416,-0.0267019058229216,
125.884269369864));
#134311=CARTESIAN_POINT('Ctrl Pts',(-237.306919323501,-0.16384023406344,
125.888840356169));
#134312=CARTESIAN_POINT('Ctrl Pts',(-237.314665656766,-0.30097957462813,
125.893411376216));
#134313=CARTESIAN_POINT('Ctrl Pts',(-237.322411990031,-0.437926665470685,
125.903725837003));
#134314=CARTESIAN_POINT('Ctrl Pts',(-237.330158323297,-0.574167222423959,
125.919740359737));
#134315=CARTESIAN_POINT('Ctrl Pts',(-237.3379063913,-0.710438289505151,
125.935758468813));
#134316=CARTESIAN_POINT('Ctrl Pts',(-237.345654459303,-0.846002119633315,
125.957479134269));
#134317=CARTESIAN_POINT('Ctrl Pts',(-237.353402527306,-0.980351683599512,
125.984807356219));
#134318=CARTESIAN_POINT('Ctrl Pts',(-237.361158830047,-1.11484403588126,
126.012164622928));
#134319=CARTESIAN_POINT('Ctrl Pts',(-237.368915132789,-1.24811916028487,
126.045141273374));
#134320=CARTESIAN_POINT('Ctrl Pts',(-237.376671435531,-1.37968178207371,
126.083591480792));
#134321=CARTESIAN_POINT('Ctrl Pts',(-237.384431878045,-1.51131462279508,
126.122062210244));
#134322=CARTESIAN_POINT('Ctrl Pts',(-237.39219232056,-1.64123276948438,
126.166012192587));
#134323=CARTESIAN_POINT('Ctrl Pts',(-237.399952763074,-1.76895910932358,
126.215246679991));
#134324=CARTESIAN_POINT('Ctrl Pts',(-237.407725663339,-1.89689048682249,
126.264560202966));
#134325=CARTESIAN_POINT('Ctrl Pts',(-237.415498563605,-2.02262266761886,
126.3191750272));
#134326=CARTESIAN_POINT('Ctrl Pts',(-237.42327146387,-2.14570059365397,
126.378849118892));
#134327=CARTESIAN_POINT('Ctrl Pts',(-237.430761799632,-2.26430432706278,
126.436353907042));
#134328=CARTESIAN_POINT('Ctrl Pts',(-237.438252135394,-2.38044316150043,
126.498556369135));
#134329=CARTESIAN_POINT('Ctrl Pts',(-237.445742471156,-2.49373557459233,
126.565201980936));
#134330=CARTESIAN_POINT('Ctrl Pts',(-237.453518002701,-2.61134161520883,
126.634385135522));
#134331=CARTESIAN_POINT('Ctrl Pts',(-237.461293534247,-2.72625278222702,
126.708575675901));
#134332=CARTESIAN_POINT('Ctrl Pts',(-237.469069065792,-2.83801326791923,
126.787538023324));
#134333=CARTESIAN_POINT('Ctrl Pts',(-237.477234778011,-2.9553819594637,
126.870462747039));
#134334=CARTESIAN_POINT('Ctrl Pts',(-237.485400490229,-3.06927518001104,
126.958650444667));
#134335=CARTESIAN_POINT('Ctrl Pts',(-237.493566202448,-3.17919324362247,
127.051773059333));
#134336=CARTESIAN_POINT('Ctrl Pts',(-237.501322143038,-3.28359540088084,
127.140222596572));
#134337=CARTESIAN_POINT('Ctrl Pts',(-237.509078083628,-3.38441125422789,
127.233123579161));
#134338=CARTESIAN_POINT('Ctrl Pts',(-237.516834024218,-3.48124220144521,
127.33015052067));
#134339=CARTESIAN_POINT('Ctrl Pts',(-237.524584701003,-3.5780074313946,
127.427111611892));
#134340=CARTESIAN_POINT('Ctrl Pts',(-237.532335377788,-3.67079286097035,
127.528192815284));
#134341=CARTESIAN_POINT('Ctrl Pts',(-237.540086054573,-3.75923429687218,
127.63302957781));
#134342=CARTESIAN_POINT('Ctrl Pts',(-237.54783314971,-3.84763486328633,
127.737817894438));
#134343=CARTESIAN_POINT('Ctrl Pts',(-237.555580244846,-3.93169517954091,
127.846358018197));
#134344=CARTESIAN_POINT('Ctrl Pts',(-237.563327339982,-4.01108942636183,
127.958250170618));
#134345=CARTESIAN_POINT('Ctrl Pts',(-237.571072532842,-4.09046417817019,
128.070114848266));
#134346=CARTESIAN_POINT('Ctrl Pts',(-237.578817725703,-4.16517491616811,
128.185329597026));
#134347=CARTESIAN_POINT('Ctrl Pts',(-237.586562918564,-4.23493771934843,
128.303463663323));
#134348=CARTESIAN_POINT('Ctrl Pts',(-237.594309924731,-4.30471685541391,
128.421625387199));
#134349=CARTESIAN_POINT('Ctrl Pts',(-237.602056930898,-4.36954553988217,
128.542707459543));
#134350=CARTESIAN_POINT('Ctrl Pts',(-237.609803937065,-4.42918460838025,
128.666252395939));
#134351=CARTESIAN_POINT('Ctrl Pts',(-237.617551999384,-4.48883180748766,
128.789814175248));
#134352=CARTESIAN_POINT('Ctrl Pts',(-237.625300061702,-4.54328781899816,
128.915839131811));
#134353=CARTESIAN_POINT('Ctrl Pts',(-237.633048124021,-4.59236101766155,
129.043848377915));
#134354=CARTESIAN_POINT('Ctrl Pts',(-237.640801543919,-4.6414681491421,
129.171946139021));
#134355=CARTESIAN_POINT('Ctrl Pts',(-237.648554963818,-4.68518490462915,
129.302030561176));
#134356=CARTESIAN_POINT('Ctrl Pts',(-237.656308383716,-4.72336901801277,
129.433606014372));
#134357=CARTESIAN_POINT('Ctrl Pts',(-237.659220975489,-4.73771297667216,
129.483032665772));
#134358=CARTESIAN_POINT('Ctrl Pts',(-237.662133567262,-4.75127670841368,
129.532669593759));
#134359=CARTESIAN_POINT('Ctrl Pts',(-237.665046159034,-4.76405452823396,
129.582490119308));
#134360=CARTESIAN_POINT('Ctrl Pts',(-235.915124447633,-4.76405452823405,
129.582490119308));
#134361=CARTESIAN_POINT('Ctrl Pts',(-235.92278038583,-4.79776592875833,
129.713930358311));
#134362=CARTESIAN_POINT('Ctrl Pts',(-235.930436324027,-4.82602943120796,
129.846751068765));
#134363=CARTESIAN_POINT('Ctrl Pts',(-235.938092262223,-4.84874865630454,
129.980455568131));
#134364=CARTESIAN_POINT('Ctrl Pts',(-235.945933645855,-4.87201819626461,
130.117398715514));
#134365=CARTESIAN_POINT('Ctrl Pts',(-235.953775029487,-4.8894713453082,
130.255268579083));
#134366=CARTESIAN_POINT('Ctrl Pts',(-235.961616413119,-4.90106078561815,
130.393524594102));
#134367=CARTESIAN_POINT('Ctrl Pts',(-235.969457796751,-4.91265022592809,
130.53178060912));
#134368=CARTESIAN_POINT('Ctrl Pts',(-235.977299180382,-4.9183759659952,
130.670422324837));
#134369=CARTESIAN_POINT('Ctrl Pts',(-235.985140564014,-4.91824789693122,
130.808908895438));
#134370=CARTESIAN_POINT('',(-235.639859435964,-4.9182497717662,130.802862277926));
#134371=CARTESIAN_POINT('Ctrl Pts',(-235.570143588767,-4.76405452823401,
129.582490119308));
#134372=CARTESIAN_POINT('Ctrl Pts',(-235.578507988208,-4.80069372382362,
129.725345786835));
#134373=CARTESIAN_POINT('Ctrl Pts',(-235.586872387649,-4.83094563354471,
129.870015896342));
#134374=CARTESIAN_POINT('Ctrl Pts',(-235.59523678709,-4.85464327593405,
130.015930705698));
#134375=CARTESIAN_POINT('Ctrl Pts',(-235.60357467919,-4.87826581890725,
130.161383101249));
#134376=CARTESIAN_POINT('Ctrl Pts',(-235.611912571289,-4.89537546784984,
130.308072046637));
#134377=CARTESIAN_POINT('Ctrl Pts',(-235.620250463388,-4.9058558003801,
130.455416598593));
#134378=CARTESIAN_POINT('Ctrl Pts',(-235.62678678758,-4.91407164801207,
130.570924420962));
#134379=CARTESIAN_POINT('Ctrl Pts',(-235.633323111772,-4.91821442410782,
130.686834771104));
#134380=CARTESIAN_POINT('Ctrl Pts',(-235.639859435964,-4.9182497717662,
130.802862277926));
#134381=CARTESIAN_POINT('Ctrl Pts',(-235.639859435996,-4.91824977176638,
130.802862278495));
#134382=CARTESIAN_POINT('Ctrl Pts',(-235.647810024064,-4.91829276757809,
130.943994646501));
#134383=CARTESIAN_POINT('Ctrl Pts',(-235.655760612132,-4.91225658512499,
131.085071975645));
#134384=CARTESIAN_POINT('Ctrl Pts',(-235.6637112002,-4.90018168205869,131.225552432914));
#134385=CARTESIAN_POINT('Ctrl Pts',(-235.671666896077,-4.88809902154042,
131.366123141045));
#134386=CARTESIAN_POINT('Ctrl Pts',(-235.679622591955,-4.86996993824622,
131.506095853258));
#134387=CARTESIAN_POINT('Ctrl Pts',(-235.687578287832,-4.84588658484825,
131.644935581081));
#134388=CARTESIAN_POINT('Ctrl Pts',(-235.695540397151,-4.82178381678535,
131.783887233799));
#134389=CARTESIAN_POINT('Ctrl Pts',(-235.70350250647,-4.79171727221365,
131.921703726235));
#134390=CARTESIAN_POINT('Ctrl Pts',(-235.711464615788,-4.75582983404403,
132.057861974612));
#134391=CARTESIAN_POINT('Ctrl Pts',(-235.719440205943,-4.71988163400236,
132.194250755747));
#134392=CARTESIAN_POINT('Ctrl Pts',(-235.727415796098,-4.67809294156459,
132.328975333825));
#134393=CARTESIAN_POINT('Ctrl Pts',(-235.735391386252,-4.63065633426484,
132.461528375046));
#134394=CARTESIAN_POINT('Ctrl Pts',(-235.743374505099,-4.58317494838628,
132.594206541928));
#134395=CARTESIAN_POINT('Ctrl Pts',(-235.751357623945,-4.53003515153502,
132.724708750582));
#134396=CARTESIAN_POINT('Ctrl Pts',(-235.759340742791,-4.47147681634625,
132.852549608694));
#134397=CARTESIAN_POINT('Ctrl Pts',(-235.767338454143,-4.41281144118253,
132.980624149717));
#134398=CARTESIAN_POINT('Ctrl Pts',(-235.775336165496,-4.3487079005738,
133.10602729868));
#134399=CARTESIAN_POINT('Ctrl Pts',(-235.783333876848,-4.27945149522177,
133.228299140414));
#134400=CARTESIAN_POINT('Ctrl Pts',(-235.787104492712,-4.24679974158869,
133.285945650253));
#134401=CARTESIAN_POINT('Ctrl Pts',(-235.790875108575,-4.21300324443521,
133.342896578187));
#134402=CARTESIAN_POINT('Ctrl Pts',(-235.794645724439,-4.17809508585806,
133.399106176581));
#134403=CARTESIAN_POINT('Ctrl Pts',(-235.802420058558,-4.10612071932053,
133.51500029425));
#134404=CARTESIAN_POINT('Ctrl Pts',(-235.810194392677,-4.02920660152256,
133.62808101823));
#134405=CARTESIAN_POINT('Ctrl Pts',(-235.817968726796,-3.94759906404498,
133.737898531426));
#134406=CARTESIAN_POINT('Ctrl Pts',(-235.825733479744,-3.8660921005641,
133.847580704351));
#134407=CARTESIAN_POINT('Ctrl Pts',(-235.833498232691,-3.77990345723433,
133.954007357516));
#134408=CARTESIAN_POINT('Ctrl Pts',(-235.841262985638,-3.68932428418892,
134.056755026089));
#134409=CARTESIAN_POINT('Ctrl Pts',(-235.849020026523,-3.59883507565487,
134.15940064423));
#134410=CARTESIAN_POINT('Ctrl Pts',(-235.856777067408,-3.50396427233535,
134.258374258067));
#134411=CARTESIAN_POINT('Ctrl Pts',(-235.864534108293,-3.40504485442267,
134.353283355788));
#134412=CARTESIAN_POINT('Ctrl Pts',(-235.872285299533,-3.30620003241265,
134.44812088182));
#134413=CARTESIAN_POINT('Ctrl Pts',(-235.880036490773,-3.2033129537756,
134.538899723017));
#134414=CARTESIAN_POINT('Ctrl Pts',(-235.887787682013,-3.09675496293443,
134.625262574178));
#134415=CARTESIAN_POINT('Ctrl Pts',(-235.89553557879,-2.99024226208174,
134.711588718823));
#134416=CARTESIAN_POINT('Ctrl Pts',(-235.903283475567,-2.8800620553127,
134.793502360815));
#134417=CARTESIAN_POINT('Ctrl Pts',(-235.911031372344,-2.76662025974206,
134.870685174323));
#134418=CARTESIAN_POINT('Ctrl Pts',(-235.918777648428,-2.65320219374954,
134.94785184285));
#134419=CARTESIAN_POINT('Ctrl Pts',(-235.926523924512,-2.53652421903467,
135.02028943145));
#134420=CARTESIAN_POINT('Ctrl Pts',(-235.934270200596,-2.41702251920439,
135.087722055054));
#134421=CARTESIAN_POINT('Ctrl Pts',(-235.942016533862,-2.29751993723986,
135.15515517643));
#134422=CARTESIAN_POINT('Ctrl Pts',(-235.949762867127,-2.17519392906321,
135.217583066952));
#134423=CARTESIAN_POINT('Ctrl Pts',(-235.957509200392,-2.05050628748219,
135.274775254655));
#134424=CARTESIAN_POINT('Ctrl Pts',(-235.965257268395,-1.92579072296819,
135.331980250151));
#134425=CARTESIAN_POINT('Ctrl Pts',(-235.973005336398,-1.79871282795443,
135.383947046721));
#134426=CARTESIAN_POINT('Ctrl Pts',(-235.980753404401,-1.66975505132088,
135.430493033644));
#134427=CARTESIAN_POINT('Ctrl Pts',(-235.988509707143,-1.54066021682789,
135.477088490195));
#134428=CARTESIAN_POINT('Ctrl Pts',(-235.996266009885,-1.40968187790405,
135.518251495335));
#134429=CARTESIAN_POINT('Ctrl Pts',(-236.004022312627,-1.27731888352287,
135.55384896183));
#134430=CARTESIAN_POINT('Ctrl Pts',(-236.011782755141,-1.14488524302586,
135.589465427764));
#134431=CARTESIAN_POINT('Ctrl Pts',(-236.019543197655,-1.01106585576917,
135.619510350486));
#134432=CARTESIAN_POINT('Ctrl Pts',(-236.027303640169,-0.876369507130365,
135.643901871597));
#134433=CARTESIAN_POINT('Ctrl Pts',(-236.035076540435,-0.741456931954944,
135.668332548144));
#134434=CARTESIAN_POINT('Ctrl Pts',(-236.0428494407,-0.605664969721866,
135.687091634123));
#134435=CARTESIAN_POINT('Ctrl Pts',(-236.050622340966,-0.469508166963199,
135.700149128486));
#134436=CARTESIAN_POINT('Ctrl Pts',(-236.058112676728,-0.338301006946043,
135.712731950038));
#134437=CARTESIAN_POINT('Ctrl Pts',(-236.065603012489,-0.206755379168454,
135.720020500442));
#134438=CARTESIAN_POINT('Ctrl Pts',(-236.073093348251,-0.0753295237528726,
135.722033697931));
#134439=CARTESIAN_POINT('Ctrl Pts',(-236.08086768237,0.0610793829189508,
135.724123226415));
#134440=CARTESIAN_POINT('Ctrl Pts',(-236.088642016489,0.197791358016512,
135.720536094252));
#134441=CARTESIAN_POINT('Ctrl Pts',(-236.096416350609,0.334294809442846,
135.711236410051));
#134442=CARTESIAN_POINT('Ctrl Pts',(-236.104181103556,0.47063003256496,
135.70194818688));
#134443=CARTESIAN_POINT('Ctrl Pts',(-236.111945856503,0.606756857026472,
135.686961445909));
#134444=CARTESIAN_POINT('Ctrl Pts',(-236.11971060945,0.742161636113154,
135.666292246907));
#134445=CARTESIAN_POINT('Ctrl Pts',(-236.127467650335,0.877431929264741,
135.645643576844));
#134446=CARTESIAN_POINT('Ctrl Pts',(-236.13522469122,1.01198122020633,135.619323738974));
#134447=CARTESIAN_POINT('Ctrl Pts',(-236.142981732105,1.14529929370727,
135.587400716743));
#134448=CARTESIAN_POINT('Ctrl Pts',(-236.150732923345,1.27851683101101,
135.555501767911));
#134449=CARTESIAN_POINT('Ctrl Pts',(-236.158484114585,1.41050462026009,
135.518008135805));
#134450=CARTESIAN_POINT('Ctrl Pts',(-236.166235305825,1.54076132973715,
135.475039110814));
#134451=CARTESIAN_POINT('Ctrl Pts',(-236.173983202602,1.6709626766385,135.432088348804));
#134452=CARTESIAN_POINT('Ctrl Pts',(-236.181731099379,1.79943403662083,
135.383666944733));
#134453=CARTESIAN_POINT('Ctrl Pts',(-236.189478996156,1.92568818503164,
135.329944345278));
#134454=CARTESIAN_POINT('Ctrl Pts',(-236.19722527224,2.05191592379634,135.276232983432));
#134455=CARTESIAN_POINT('Ctrl Pts',(-236.204971548324,2.17592701397578,
135.217222784838));
#134456=CARTESIAN_POINT('Ctrl Pts',(-236.212717824408,2.29725357775422,
135.153131600498));
#134457=CARTESIAN_POINT('Ctrl Pts',(-236.220464157673,2.41858103713762,
135.089039943053));
#134458=CARTESIAN_POINT('Ctrl Pts',(-236.228210490939,2.53722358488175,
135.019867407635));
#134459=CARTESIAN_POINT('Ctrl Pts',(-236.235956824204,2.6527377081024,134.945877937886));
#134460=CARTESIAN_POINT('Ctrl Pts',(-236.243704892207,2.76827769991019,
134.871871898709));
#134461=CARTESIAN_POINT('Ctrl Pts',(-236.25145296021,2.88068754394595,134.793046989507));
#134462=CARTESIAN_POINT('Ctrl Pts',(-236.259201028213,2.98955282923405,
134.709710402632));
#134463=CARTESIAN_POINT('Ctrl Pts',(-236.266957330955,3.09853381784301,
134.626285244642));
#134464=CARTESIAN_POINT('Ctrl Pts',(-236.274713633697,3.20396241137607,
134.538339068346));
#134465=CARTESIAN_POINT('Ctrl Pts',(-236.282469936439,3.3054569997201,134.446219632616));
#134466=CARTESIAN_POINT('Ctrl Pts',(-236.290230378953,3.40700575878188,
134.354051029969));
#134467=CARTESIAN_POINT('Ctrl Pts',(-236.297990821467,3.50461605071644,
134.257705004128));
#134468=CARTESIAN_POINT('Ctrl Pts',(-236.305751263981,3.59794399481218,
134.157565364177));
#134469=CARTESIAN_POINT('Ctrl Pts',(-236.313524164246,3.69142175720905,
134.057264971186));
#134470=CARTESIAN_POINT('Ctrl Pts',(-236.321297064512,3.78060318001821,
133.95315909172));
#134471=CARTESIAN_POINT('Ctrl Pts',(-236.329069964777,3.86518489753918,
133.845664412049));
#134472=CARTESIAN_POINT('Ctrl Pts',(-236.336560300539,3.94669185658299,
133.742077434742));
#134473=CARTESIAN_POINT('Ctrl Pts',(-236.344050636302,4.0239275454595,133.635344012048));
#134474=CARTESIAN_POINT('Ctrl Pts',(-236.351540972064,4.09666019063509,
133.525859900124));
#134475=CARTESIAN_POINT('Ctrl Pts',(-236.359315306183,4.17215051615626,
133.412224664825));
#134476=CARTESIAN_POINT('Ctrl Pts',(-236.367089640302,4.24302872219089,
133.295266075736));
#134477=CARTESIAN_POINT('Ctrl Pts',(-236.374863974421,4.30898808427034,
133.175395149604));
#134478=CARTESIAN_POINT('Ctrl Pts',(-236.382628727368,4.37486615733117,
133.055671953675));
#134479=CARTESIAN_POINT('Ctrl Pts',(-236.390393480315,4.43583726141008,
132.933043901376));
#134480=CARTESIAN_POINT('Ctrl Pts',(-236.398158233263,4.49163726944919,
132.807951818933));
#134481=CARTESIAN_POINT('Ctrl Pts',(-236.405915274148,4.54738185613368,
132.682983979709));
#134482=CARTESIAN_POINT('Ctrl Pts',(-236.413672315033,4.59796540942072,
132.55555733534));
#134483=CARTESIAN_POINT('Ctrl Pts',(-236.421429355918,4.64316934191289,
132.42613789106));
#134484=CARTESIAN_POINT('Ctrl Pts',(-236.429180547158,4.68833918576774,
132.29681604299));
#134485=CARTESIAN_POINT('Ctrl Pts',(-236.436931738398,4.72813735527188,
132.165504753819));
#134486=CARTESIAN_POINT('Ctrl Pts',(-236.444682929638,4.76239323077036,
132.032690287489));
#134487=CARTESIAN_POINT('Ctrl Pts',(-236.452430826415,4.796634546608,131.89993227085));
#134488=CARTESIAN_POINT('Ctrl Pts',(-236.460178723192,4.82533815615523,
131.765672725539));
#134489=CARTESIAN_POINT('Ctrl Pts',(-236.467926619969,4.84838326287521,
131.630413157524));
#134490=CARTESIAN_POINT('Ctrl Pts',(-236.475672896053,4.87142354905567,
131.495181882895));
#134491=CARTESIAN_POINT('Ctrl Pts',(-236.483419172137,4.88880762110378,
131.358951386806));
#134492=CARTESIAN_POINT('Ctrl Pts',(-236.491165448221,4.90046586385056,
131.222233061902));
#134493=CARTESIAN_POINT('Ctrl Pts',(-236.498911781487,4.91212419265584,
131.085513727775));
#134494=CARTESIAN_POINT('Ctrl Pts',(-236.506658114752,4.91805657460166,
130.948306947199));
#134495=CARTESIAN_POINT('Ctrl Pts',(-236.514404448018,4.91824534340113,
130.81112852811));
#134496=CARTESIAN_POINT('Ctrl Pts',(-236.522152516021,4.91843415447406,
130.673919388866));
#134497=CARTESIAN_POINT('Ctrl Pts',(-236.529900584023,4.91287679238941,
130.536739014637));
#134498=CARTESIAN_POINT('Ctrl Pts',(-236.537648652026,4.9016077075174,130.400102106084));
#134499=CARTESIAN_POINT('Ctrl Pts',(-236.545404954768,4.89032664572788,
130.263319978198));
#134500=CARTESIAN_POINT('Ctrl Pts',(-236.55316125751,4.87332176688625,130.127082860073));
#134501=CARTESIAN_POINT('Ctrl Pts',(-236.560917560252,4.85067938079108,
129.991899783268));
#134502=CARTESIAN_POINT('Ctrl Pts',(-236.568678002766,4.8280249097727,129.856644555185));
#134503=CARTESIAN_POINT('Ctrl Pts',(-236.57643844528,4.79972701662529,129.722444871763));
#134504=CARTESIAN_POINT('Ctrl Pts',(-236.584198887795,4.76592273487762,
129.58979750777));
#134505=CARTESIAN_POINT('Ctrl Pts',(-236.59197178806,4.73206418749589,129.456937206453));
#134506=CARTESIAN_POINT('Ctrl Pts',(-236.599744688325,4.6926817000743,129.325634578915));
#134507=CARTESIAN_POINT('Ctrl Pts',(-236.607517588591,4.64796186600247,
129.19637008442));
#134508=CARTESIAN_POINT('Ctrl Pts',(-236.615007924353,4.60486771054161,
129.071804679898));
#134509=CARTESIAN_POINT('Ctrl Pts',(-236.622498260115,4.55681763560663,
128.949132085347));
#134510=CARTESIAN_POINT('Ctrl Pts',(-236.629988595877,4.50401932280744,
128.828761214277));
#134511=CARTESIAN_POINT('Ctrl Pts',(-236.637762929996,4.44921914593055,
128.703826445044));
#134512=CARTESIAN_POINT('Ctrl Pts',(-236.645537264115,4.38912997414836,
128.580975628656));
#134513=CARTESIAN_POINT('Ctrl Pts',(-236.653311598234,4.32393181542294,
128.460688985687));
#134514=CARTESIAN_POINT('Ctrl Pts',(-236.661076351181,4.2588140076014,128.340550585256));
#134515=CARTESIAN_POINT('Ctrl Pts',(-236.668841104129,4.18859992525228,
128.222970410979));
#134516=CARTESIAN_POINT('Ctrl Pts',(-236.676605857076,4.11351768083691,
128.108408957773));
#134517=CARTESIAN_POINT('Ctrl Pts',(-236.684362897961,4.03851000916537,
127.993961288617));
#134518=CARTESIAN_POINT('Ctrl Pts',(-236.692119938846,3.95864401047074,
127.882526698786));
#134519=CARTESIAN_POINT('Ctrl Pts',(-236.699876979731,3.87419359632847,
127.77454097926));
#134520=CARTESIAN_POINT('Ctrl Pts',(-236.707628170971,3.78980686690009,
127.666636692604));
#134521=CARTESIAN_POINT('Ctrl Pts',(-236.715379362211,3.70084284313236,
127.562176406203));
#134522=CARTESIAN_POINT('Ctrl Pts',(-236.723130553451,3.60761840856041,
127.461566504744));
#134523=CARTESIAN_POINT('Ctrl Pts',(-236.730878450228,3.51443359685987,
127.360999365177));
#134524=CARTESIAN_POINT('Ctrl Pts',(-236.738626347005,3.41699224104641,
127.264279641824));
#134525=CARTESIAN_POINT('Ctrl Pts',(-236.746374243783,3.31565097881498,
127.171780040458));
#134526=CARTESIAN_POINT('Ctrl Pts',(-236.754120519867,3.21433091499121,
127.079299788015));
#134527=CARTESIAN_POINT('Ctrl Pts',(-236.761866795951,3.10911285595423,
126.991038165107));
#134528=CARTESIAN_POINT('Ctrl Pts',(-236.769613072035,3.0003894221212,126.907330161164));
#134529=CARTESIAN_POINT('Ctrl Pts',(-236.7773594053,2.89166518571693,126.823621539308));
#134530=CARTESIAN_POINT('Ctrl Pts',(-236.785105738566,2.77943583266885,
126.744466842001));
#134531=CARTESIAN_POINT('Ctrl Pts',(-236.792852071831,2.66412577774201,
126.670159739177));
#134532=CARTESIAN_POINT('Ctrl Pts',(-236.800600139834,2.54878989992771,
126.595835995793));
#134533=CARTESIAN_POINT('Ctrl Pts',(-236.808348207837,2.43037227598597,
126.52636221882));
#134534=CARTESIAN_POINT('Ctrl Pts',(-236.81609627584,2.30932455942561,126.461987632465));
#134535=CARTESIAN_POINT('Ctrl Pts',(-236.823852578582,2.18814819191144,
126.397544628034));
#134536=CARTESIAN_POINT('Ctrl Pts',(-236.831608881324,2.06433649361586,
126.338211824083));
#134537=CARTESIAN_POINT('Ctrl Pts',(-236.839365184066,1.93836437976073,
126.284191749728));
#134538=CARTESIAN_POINT('Ctrl Pts',(-236.84712562658,1.81232503079513,126.230142843232));
#134539=CARTESIAN_POINT('Ctrl Pts',(-236.854886069094,1.68412333393879,
126.181412455276));
#134540=CARTESIAN_POINT('Ctrl Pts',(-236.862646511608,1.55425130984237,
126.138153814567));
#134541=CARTESIAN_POINT('Ctrl Pts',(-236.870419411874,1.42417080364338,
126.094825731248));
#134542=CARTESIAN_POINT('Ctrl Pts',(-236.878192312139,1.29241498798955,
126.056987055857));
#134543=CARTESIAN_POINT('Ctrl Pts',(-236.885965212404,1.15948894515113,
126.024740502058));
#134544=CARTESIAN_POINT('Ctrl Pts',(-236.893455548166,1.03139509879362,
125.993666191714));
#134545=CARTESIAN_POINT('Ctrl Pts',(-236.900945883928,0.902214931541491,
125.967784546807));
#134546=CARTESIAN_POINT('Ctrl Pts',(-236.90843621969,0.772404730894424,
125.947141866656));
#134547=CARTESIAN_POINT('Ctrl Pts',(-236.916210553809,0.637672737032011,
125.925716513012));
#134548=CARTESIAN_POINT('Ctrl Pts',(-236.923984887928,0.501835200781801,
125.909867367991));
#134549=CARTESIAN_POINT('Ctrl Pts',(-236.931759222047,0.365393444013297,
125.899702556745));
#134550=CARTESIAN_POINT('Ctrl Pts',(-236.939523974995,0.229119839515861,
125.889550272721));
#134551=CARTESIAN_POINT('Ctrl Pts',(-236.947288727942,0.0922438822691649,
125.885068412515));
#134552=CARTESIAN_POINT('Ctrl Pts',(-236.955053480889,-0.0447236999542945,
125.886313967405));
#134553=CARTESIAN_POINT('Ctrl Pts',(-236.962810521774,-0.181555244044185,
125.887558285191));
#134554=CARTESIAN_POINT('Ctrl Pts',(-236.970567562659,-0.318477843591094,
125.894518694071));
#134555=CARTESIAN_POINT('Ctrl Pts',(-236.978324603544,-0.454976799403212,
125.907200300147));
#134556=CARTESIAN_POINT('Ctrl Pts',(-236.986075794784,-0.591372820290759,
125.919872342925));
#134557=CARTESIAN_POINT('Ctrl Pts',(-236.993826986024,-0.727345445621648,
125.938256959329));
#134558=CARTESIAN_POINT('Ctrl Pts',(-237.001578177264,-0.862381489158824,
125.962307207115));
#134559=CARTESIAN_POINT('Ctrl Pts',(-237.009326074041,-0.997360138775109,
125.986347232905));
#134560=CARTESIAN_POINT('Ctrl Pts',(-237.017073970818,-1.13140261423075,
126.01604803225));
#134561=CARTESIAN_POINT('Ctrl Pts',(-237.024821867595,-1.26400257621797,
126.051311012332));
#134562=CARTESIAN_POINT('Ctrl Pts',(-237.032568143679,-1.39657480115202,
126.086566616159));
#134563=CARTESIAN_POINT('Ctrl Pts',(-237.040314419764,-1.52770473520686,
126.127381986065));
#134564=CARTESIAN_POINT('Ctrl Pts',(-237.048060695848,-1.65689832136193,
126.173607869344));
#134565=CARTESIAN_POINT('Ctrl Pts',(-237.055807029113,-1.78609286119453,
126.219834093851));
#134566=CARTESIAN_POINT('Ctrl Pts',(-237.063553362379,-1.91335065649412,
126.271470779715));
#134567=CARTESIAN_POINT('Ctrl Pts',(-237.071299695644,-2.03819522787897,
126.328319590548));
#134568=CARTESIAN_POINT('Ctrl Pts',(-237.079047763647,-2.16306775734049,
126.385181132277));
#134569=CARTESIAN_POINT('Ctrl Pts',(-237.08679583165,-2.28552563175982,
126.447256959616));
#134570=CARTESIAN_POINT('Ctrl Pts',(-237.094543899653,-2.40511504199968,
126.514301795446));
#134571=CARTESIAN_POINT('Ctrl Pts',(-237.102300202395,-2.52483155328705,
126.581417887326));
#134572=CARTESIAN_POINT('Ctrl Pts',(-237.110056505137,-2.64167316884011,
126.653513345811));
#134573=CARTESIAN_POINT('Ctrl Pts',(-237.117812807878,-2.75521279190169,
126.73029808321));
#134574=CARTESIAN_POINT('Ctrl Pts',(-237.125573250393,-2.86881301447933,
126.807123802936));
#134575=CARTESIAN_POINT('Ctrl Pts',(-237.133333692907,-2.97910741863439,
126.888643556366));
#134576=CARTESIAN_POINT('Ctrl Pts',(-237.141094135421,-3.08570113953568,
126.97452621645));
#134577=CARTESIAN_POINT('Ctrl Pts',(-237.148867035686,-3.19246597414043,
127.060546743005));
#134578=CARTESIAN_POINT('Ctrl Pts',(-237.156639935952,-3.29551796006939,
127.150943913923));
#134579=CARTESIAN_POINT('Ctrl Pts',(-237.164412836217,-3.39449767210342,
127.24534830843));
#134580=CARTESIAN_POINT('Ctrl Pts',(-237.171903171979,-3.48987922229177,
127.336320865407));
#134581=CARTESIAN_POINT('Ctrl Pts',(-237.179393507741,-3.58147921896272,
127.431014137426));
#134582=CARTESIAN_POINT('Ctrl Pts',(-237.186883843504,-3.6690120746481,
127.529069262803));
#134583=CARTESIAN_POINT('Ctrl Pts',(-237.194584148885,-3.75899865749865,
127.629873076349));
#134584=CARTESIAN_POINT('Ctrl Pts',(-237.202284454265,-3.8449847776776,
127.734564138519));
#134585=CARTESIAN_POINT('Ctrl Pts',(-237.209984759646,-3.92661086149957,
127.842788365391));
#134586=CARTESIAN_POINT('Ctrl Pts',(-237.217675821897,-4.00813896472519,
127.950882684349));
#134587=CARTESIAN_POINT('Ctrl Pts',(-237.225366884148,-4.08531720106446,
128.06250141918));
#134588=CARTESIAN_POINT('Ctrl Pts',(-237.233057946399,-4.15782352492297,
128.177254491408));
#134589=CARTESIAN_POINT('Ctrl Pts',(-237.240740208052,-4.23024688248011,
128.291876255944));
#134590=CARTESIAN_POINT('Ctrl Pts',(-237.248422469705,-4.2980087575144,
128.409624883436));
#134591=CARTESIAN_POINT('Ctrl Pts',(-237.256104731358,-4.36082848494722,
128.530078755665));
#134592=CARTESIAN_POINT('Ctrl Pts',(-237.263781857921,-4.42360622149408,
128.650452112345));
#134593=CARTESIAN_POINT('Ctrl Pts',(-237.271458984483,-4.48144819595658,
128.77352676561));
#134594=CARTESIAN_POINT('Ctrl Pts',(-237.279136111046,-4.53411811845468,
128.898853873836));
#134595=CARTESIAN_POINT('Ctrl Pts',(-237.286810197679,-4.58676718512242,
129.024131355998));
#134596=CARTESIAN_POINT('Ctrl Pts',(-237.294484284313,-4.63424811655263,
129.151659153016));
#134597=CARTESIAN_POINT('Ctrl Pts',(-237.302158370946,-4.67637168339331,
129.280966072067));
#134598=CARTESIAN_POINT('Ctrl Pts',(-237.308065172838,-4.70879450791701,
129.380494575005));
#134599=CARTESIAN_POINT('Ctrl Pts',(-237.313971974729,-4.73804429293833,
129.481076606651));
#134600=CARTESIAN_POINT('Ctrl Pts',(-237.319878776621,-4.76405452823405,
129.582490119308));
#134601=CARTESIAN_POINT('Origin',(213.235140564004,0.,130.804360617566));
#134602=CARTESIAN_POINT('',(-239.415329287988,-4.76405452823416,129.582490119309));
#134603=CARTESIAN_POINT('',(-239.069767094363,-4.76405452823403,129.582490119308));
#134604=CARTESIAN_POINT('',(213.235140564004,-4.76405452823405,129.582490119308));
#134605=CARTESIAN_POINT('',(-237.73514056406,-4.91824985575658,130.803169462491));
#134606=CARTESIAN_POINT('Ctrl Pts',(-237.735140564061,-4.91824985575658,
130.803169462492));
#134607=CARTESIAN_POINT('Ctrl Pts',(-237.742865432421,-4.91828269493721,
130.938761627506));
#134608=CARTESIAN_POINT('Ctrl Pts',(-237.750590300782,-4.91270403941569,
131.074580060301));
#134609=CARTESIAN_POINT('Ctrl Pts',(-237.758315169143,-4.90148384634299,
131.210118139417));
#134610=CARTESIAN_POINT('Ctrl Pts',(-237.766030648401,-4.89027729072596,
131.345491480321));
#134611=CARTESIAN_POINT('Ctrl Pts',(-237.773746127658,-4.87344286997585,
131.480584754197));
#134612=CARTESIAN_POINT('Ctrl Pts',(-237.781461606916,-4.85100251809047,
131.614889847131));
#134613=CARTESIAN_POINT('Ctrl Pts',(-237.78916961392,-4.82858389913852,
131.749064868859));
#134614=CARTESIAN_POINT('Ctrl Pts',(-237.796877620924,-4.80057021590841,
131.882452839898));
#134615=CARTESIAN_POINT('Ctrl Pts',(-237.804585627929,-4.76703528595467,
132.014549712279));
#134616=CARTESIAN_POINT('Ctrl Pts',(-237.812288072446,-4.73352455649721,
132.146551256897));
#134617=CARTESIAN_POINT('Ctrl Pts',(-237.819990516964,-4.6945006066077,
132.277263174278));
#134618=CARTESIAN_POINT('Ctrl Pts',(-237.827692961482,-4.65008843923634,
132.406190998655));
#134619=CARTESIAN_POINT('Ctrl Pts',(-237.835392528332,-4.60569286444811,
132.535070655024));
#134620=CARTESIAN_POINT('Ctrl Pts',(-237.843092095182,-4.55591320289364,
132.662167169325));
#134621=CARTESIAN_POINT('Ctrl Pts',(-237.850791662032,-4.50092440392816,
132.787000920955));
#134622=CARTESIAN_POINT('Ctrl Pts',(-237.858489955009,-4.44594470272169,
132.911814019155));
#134623=CARTESIAN_POINT('Ctrl Pts',(-237.866188247985,-4.38575773771776,
133.034364736533));
#134624=CARTESIAN_POINT('Ctrl Pts',(-237.873886540961,-4.32058653617298,
133.154193600129));
#134625=CARTESIAN_POINT('Ctrl Pts',(-237.881585280676,-4.2554115526847,
133.274029417502));
#134626=CARTESIAN_POINT('Ctrl Pts',(-237.889284020391,-4.18525194673164,
133.391142718648));
#134627=CARTESIAN_POINT('Ctrl Pts',(-237.896982760106,-4.1103763888758,
133.505099221036));
#134628=CARTESIAN_POINT('Ctrl Pts',(-237.904683667168,-4.03547975206986,
133.619087804432));
#134629=CARTESIAN_POINT('Ctrl Pts',(-237.912384574231,-3.955864740056,133.729917490131));
#134630=CARTESIAN_POINT('Ctrl Pts',(-237.920085481293,-3.87184269080206,
133.837183929298));
#134631=CARTESIAN_POINT('Ctrl Pts',(-237.927794694456,-3.78773001643866,
133.944566064676));
#134632=CARTESIAN_POINT('Ctrl Pts',(-237.935503907619,-3.69920105859463,
134.048376967458));
#134633=CARTESIAN_POINT('Ctrl Pts',(-237.943213120781,-3.606606956095,134.148245981442));
#134634=CARTESIAN_POINT('Ctrl Pts',(-237.950926943952,-3.51395748353554,
134.248174715789));
#134635=CARTESIAN_POINT('Ctrl Pts',(-237.958640767123,-3.41723830596076,
134.344156588317));
#134636=CARTESIAN_POINT('Ctrl Pts',(-237.966354590294,-3.3168357331299,
134.435859451647));
#134637=CARTESIAN_POINT('Ctrl Pts',(-237.974079890696,-3.21628377348235,
134.527698757684));
#134638=CARTESIAN_POINT('Ctrl Pts',(-237.981805191097,-3.11203777795702,
134.615246087266));
#134639=CARTESIAN_POINT('Ctrl Pts',(-237.989530491499,-3.00451567741233,
134.698210718261));
#134640=CARTESIAN_POINT('Ctrl Pts',(-237.99389956726,-2.94370610641383,
134.745131710255));
#134641=CARTESIAN_POINT('Ctrl Pts',(-237.998268643021,-2.88184918344584,
134.790587717055));
#134642=CARTESIAN_POINT('Ctrl Pts',(-238.002637718782,-2.81902410685448,
134.834532592491));
#134643=CARTESIAN_POINT('Ctrl Pts',(-238.010412052901,-2.70723315535801,
134.912728110985));
#134644=CARTESIAN_POINT('Ctrl Pts',(-238.01818638702,-2.592009128965,134.986392589495));
#134645=CARTESIAN_POINT('Ctrl Pts',(-238.025960721139,-2.47375556551788,
135.055209528615));
#134646=CARTESIAN_POINT('Ctrl Pts',(-238.033725474086,-2.35564773901972,
135.123941657008));
#134647=CARTESIAN_POINT('Ctrl Pts',(-238.041490227033,-2.23451813895336,
135.187837938047));
#134648=CARTESIAN_POINT('Ctrl Pts',(-238.04925497998,-2.11080112627545,
135.246623742125));
#134649=CARTESIAN_POINT('Ctrl Pts',(-238.057012020865,-1.9872069910783,
135.305351159313));
#134650=CARTESIAN_POINT('Ctrl Pts',(-238.06476906175,-1.86103090823899,
135.358978033897));
#134651=CARTESIAN_POINT('Ctrl Pts',(-238.072526102635,-1.73273350330077,
135.407274658588));
#134652=CARTESIAN_POINT('Ctrl Pts',(-238.080277293875,-1.60453284843345,
135.455534862419));
#134653=CARTESIAN_POINT('Ctrl Pts',(-238.088028485115,-1.47421442000175,
135.498472679909));
#134654=CARTESIAN_POINT('Ctrl Pts',(-238.095779676355,-1.34226024751455,
135.535905871544));
#134655=CARTESIAN_POINT('Ctrl Pts',(-238.103527573132,-1.21036215907084,
135.573323153074));
#134656=CARTESIAN_POINT('Ctrl Pts',(-238.11127546991,-1.07683008467684,
135.605240355585));
#134657=CARTESIAN_POINT('Ctrl Pts',(-238.119023366687,-0.94216248709477,
135.631524682564));
#134658=CARTESIAN_POINT('Ctrl Pts',(-238.126769642771,-0.807523059071014,
135.657803511429));
#134659=CARTESIAN_POINT('Ctrl Pts',(-238.134515918855,-0.671748963794779,
135.678451733572));
#134660=CARTESIAN_POINT('Ctrl Pts',(-238.142262194939,-0.535349776071497,
135.693387481857));
#134661=CARTESIAN_POINT('Ctrl Pts',(-238.150008528204,-0.398949581480582,
135.708323340394));
#134662=CARTESIAN_POINT('Ctrl Pts',(-238.157754861469,-0.26192467387732,
135.717546598374));
#134663=CARTESIAN_POINT('Ctrl Pts',(-238.165501194735,-0.124790288715148,
135.721027216629));
#134664=CARTESIAN_POINT('Ctrl Pts',(-238.173249262738,0.0123748067419455,
135.724508614344));
#134665=CARTESIAN_POINT('Ctrl Pts',(-238.180997330741,0.149649037778895,
135.722244803376));
#134666=CARTESIAN_POINT('Ctrl Pts',(-238.188745398744,0.286517025242996,
135.714257872779));
#134667=CARTESIAN_POINT('Ctrl Pts',(-238.196501701486,0.423530477633109,
135.706262453576));
#134668=CARTESIAN_POINT('Ctrl Pts',(-238.204258004227,0.560136433038687,
135.692531786908));
#134669=CARTESIAN_POINT('Ctrl Pts',(-238.212014306969,0.695823935291642,
135.673139942363));
#134670=CARTESIAN_POINT('Ctrl Pts',(-238.219774749484,0.83158385805002,
135.653737747808));
#134671=CARTESIAN_POINT('Ctrl Pts',(-238.227535191998,0.966423966688222,
135.628668426128));
#134672=CARTESIAN_POINT('Ctrl Pts',(-238.235295634512,1.09984434107092,
135.598057050165));
#134673=CARTESIAN_POINT('Ctrl Pts',(-238.243068534777,1.23347889368309,
135.567396534104));
#134674=CARTESIAN_POINT('Ctrl Pts',(-238.250841435043,1.36568878041693,
135.531176288886));
#134675=CARTESIAN_POINT('Ctrl Pts',(-238.258614335308,1.49598920264289,
135.489571324469));
#134676=CARTESIAN_POINT('Ctrl Pts',(-238.26610467107,1.62155287631434,135.449478805304));
#134677=CARTESIAN_POINT('Ctrl Pts',(-238.273595006832,1.74534321349922,
135.404386371627));
#134678=CARTESIAN_POINT('Ctrl Pts',(-238.281085342594,1.86694643465895,
135.354491832445));
#134679=CARTESIAN_POINT('Ctrl Pts',(-238.288859676713,1.99316027890892,
135.302705526644));
#134680=CARTESIAN_POINT('Ctrl Pts',(-238.296634010832,2.11741769173488,
135.245581739916));
#134681=CARTESIAN_POINT('Ctrl Pts',(-238.304408344952,2.2392342711602,135.183288904414));
#134682=CARTESIAN_POINT('Ctrl Pts',(-238.312173097899,2.36090072253878,
135.121072839265));
#134683=CARTESIAN_POINT('Ctrl Pts',(-238.319937850846,2.48013198100569,
135.053700576816));
#134684=CARTESIAN_POINT('Ctrl Pts',(-238.327702603793,2.59646221018546,
134.981389113229));
#134685=CARTESIAN_POINT('Ctrl Pts',(-238.335459644678,2.71267689854133,
134.909149470407));
#134686=CARTESIAN_POINT('Ctrl Pts',(-238.343216685563,2.8259959617182,134.831980594044));
#134687=CARTESIAN_POINT('Ctrl Pts',(-238.350973726448,2.93597716110945,
134.750145859054));
#134688=CARTESIAN_POINT('Ctrl Pts',(-238.358724917688,3.04587542282287,
134.668372836274));
#134689=CARTESIAN_POINT('Ctrl Pts',(-238.366476108928,3.15244051851142,
134.581941190793));
#134690=CARTESIAN_POINT('Ctrl Pts',(-238.374227300168,3.25525857618644,
134.491157962778));
#134691=CARTESIAN_POINT('Ctrl Pts',(-238.381975196946,3.35803293344406,
134.400413320058));
#134692=CARTESIAN_POINT('Ctrl Pts',(-238.389723093723,3.45706312777038,
134.305321031623));
#134693=CARTESIAN_POINT('Ctrl Pts',(-238.3974709905,3.55196800240126,134.206228688555));
#134694=CARTESIAN_POINT('Ctrl Pts',(-238.405217266584,3.64685302497828,
134.10715707347));
#134695=CARTESIAN_POINT('Ctrl Pts',(-238.412963542668,3.73761417401833,
134.004087350221));
#134696=CARTESIAN_POINT('Ctrl Pts',(-238.420709818752,3.82390713475273,
133.897403987337));
#134697=CARTESIAN_POINT('Ctrl Pts',(-238.428456152017,3.91020073248229,
133.790719836942));
#134698=CARTESIAN_POINT('Ctrl Pts',(-238.436202485283,3.99202583021619,
133.680422297656));
#134699=CARTESIAN_POINT('Ctrl Pts',(-238.443948818548,4.06907865780404,
133.566928614757));
#134700=CARTESIAN_POINT('Ctrl Pts',(-238.451696886551,4.14614874083827,
133.453409515734));
#134701=CARTESIAN_POINT('Ctrl Pts',(-238.459444954554,4.21844420754164,
133.33669317223));
#134702=CARTESIAN_POINT('Ctrl Pts',(-238.467193022557,4.28570506703893,
133.217225126994));
#134703=CARTESIAN_POINT('Ctrl Pts',(-238.474949325299,4.35303741217801,
133.097630109698));
#134704=CARTESIAN_POINT('Ctrl Pts',(-238.482705628041,4.41532426911977,
132.975277889809));
#134705=CARTESIAN_POINT('Ctrl Pts',(-238.490461930783,4.47235177041802,
132.850638385646));
#134706=CARTESIAN_POINT('Ctrl Pts',(-238.498222373297,4.52940970901094,
132.725932357626));
#134707=CARTESIAN_POINT('Ctrl Pts',(-238.505982815811,4.58120255105312,
132.598936974638));
#134708=CARTESIAN_POINT('Ctrl Pts',(-238.513743258325,4.6275653048243,132.470140438577));
#134709=CARTESIAN_POINT('Ctrl Pts',(-238.521516158591,4.67400248420373,
132.341137146881));
#134710=CARTESIAN_POINT('Ctrl Pts',(-238.529289058856,4.71499203927674,
132.210327297524));
#134711=CARTESIAN_POINT('Ctrl Pts',(-238.537061959122,4.75041916537622,
132.078213362481));
#134712=CARTESIAN_POINT('Ctrl Pts',(-238.544552294884,4.78455842620654,
131.95090210175));
#134713=CARTESIAN_POINT('Ctrl Pts',(-238.552042630646,4.81353258566578,
131.822380223306));
#134714=CARTESIAN_POINT('Ctrl Pts',(-238.559532966408,4.83728440812522,
131.693102772192));
#134715=CARTESIAN_POINT('Ctrl Pts',(-238.567307300527,4.86193678815231,
131.558923727226));
#134716=CARTESIAN_POINT('Ctrl Pts',(-238.575081634646,4.88104109533654,
131.42350564461));
#134717=CARTESIAN_POINT('Ctrl Pts',(-238.582855968765,4.89447720531924,
131.287347107139));
#134718=CARTESIAN_POINT('Ctrl Pts',(-238.590620721712,4.90789675649721,
131.151356372897));
#134719=CARTESIAN_POINT('Ctrl Pts',(-238.598385474659,4.9156619716037,131.014627384832));
#134720=CARTESIAN_POINT('Ctrl Pts',(-238.606150227606,4.91770361971606,
130.877669356005));
#134721=CARTESIAN_POINT('Ctrl Pts',(-238.613907268491,4.91974324003474,
130.740847355824));
#134722=CARTESIAN_POINT('Ctrl Pts',(-238.621664309376,4.9160706004336,130.603797155981));
#134723=CARTESIAN_POINT('Ctrl Pts',(-238.629421350261,4.90666824491761,
130.467033184918));
#134724=CARTESIAN_POINT('Ctrl Pts',(-238.637172541501,4.89727297979103,
130.330372348628));
#134725=CARTESIAN_POINT('Ctrl Pts',(-238.644923732741,4.88215662579298,
130.193997699952));
#134726=CARTESIAN_POINT('Ctrl Pts',(-238.652674923982,4.86135379659384,
130.058423403826));
#134727=CARTESIAN_POINT('Ctrl Pts',(-238.660422820759,4.84055980915201,
129.922906730392));
#134728=CARTESIAN_POINT('Ctrl Pts',(-238.668170717536,4.81408421271863,
129.788190118567));
#134729=CARTESIAN_POINT('Ctrl Pts',(-238.675918614313,4.78201342097328,
129.654782127801));
#134730=CARTESIAN_POINT('Ctrl Pts',(-238.683664890397,4.74994933774629,
129.521402043111));
#134731=CARTESIAN_POINT('Ctrl Pts',(-238.691411166481,4.71229247851094,
129.3893304149));
#134732=CARTESIAN_POINT('Ctrl Pts',(-238.699157442565,4.66918019698701,
129.259064739566));
#134733=CARTESIAN_POINT('Ctrl Pts',(-238.70690377583,4.62606759721795,129.12879810264));
#134734=CARTESIAN_POINT('Ctrl Pts',(-238.714650109096,4.57749961764288,
129.000337816358));
#134735=CARTESIAN_POINT('Ctrl Pts',(-238.722396442361,4.52366310334266,
128.874164982415));
#134736=CARTESIAN_POINT('Ctrl Pts',(-238.730144510364,4.46981453272827,
128.74796389294));
#134737=CARTESIAN_POINT('Ctrl Pts',(-238.737892578367,4.41069523302737,
128.624051634669));
#134738=CARTESIAN_POINT('Ctrl Pts',(-238.74564064637,4.34653952055527,128.502887772027));
#134739=CARTESIAN_POINT('Ctrl Pts',(-238.753396949112,4.28231562262857,
128.381595134991));
#134740=CARTESIAN_POINT('Ctrl Pts',(-238.761153251854,4.21304480245928,
128.263057074722));
#134741=CARTESIAN_POINT('Ctrl Pts',(-238.768909554596,4.13900681505815,
128.147707526287));
#134742=CARTESIAN_POINT('Ctrl Pts',(-238.77666999711,4.06492931135391,128.032296412325));
#134743=CARTESIAN_POINT('Ctrl Pts',(-238.784430439624,3.98607979518424,
127.920077520926));
#134744=CARTESIAN_POINT('Ctrl Pts',(-238.792190882138,3.90277982257457,
127.811453549345));
#134745=CARTESIAN_POINT('Ctrl Pts',(-238.799963782403,3.81934612945383,
127.702655204922));
#134746=CARTESIAN_POINT('Ctrl Pts',(-238.807736682669,3.73144795420495,
127.597463612569));
#134747=CARTESIAN_POINT('Ctrl Pts',(-238.815509582934,3.63944598600381,
127.49624695908));
#134748=CARTESIAN_POINT('Ctrl Pts',(-238.822999918696,3.55078852108624,
127.398709785895));
#134749=CARTESIAN_POINT('Ctrl Pts',(-238.830490254458,3.45832066574396,
127.304863790331));
#134750=CARTESIAN_POINT('Ctrl Pts',(-238.83798059022,3.36239432500475,127.215003089306));
#134751=CARTESIAN_POINT('Ctrl Pts',(-238.845754924339,3.26283090789981,
127.121735292488));
#134752=CARTESIAN_POINT('Ctrl Pts',(-238.853529258458,3.15922618443732,
127.032465516368));
#134753=CARTESIAN_POINT('Ctrl Pts',(-238.861303592577,3.05193469629379,
126.947564321149));
#134754=CARTESIAN_POINT('Ctrl Pts',(-238.869068345525,2.94477543532019,
126.862767759065));
#134755=CARTESIAN_POINT('Ctrl Pts',(-238.876833098471,2.83393875373527,
126.782329305833));
#134756=CARTESIAN_POINT('Ctrl Pts',(-238.884597851419,2.71981564590503,
126.706582449486));
#134757=CARTESIAN_POINT('Ctrl Pts',(-238.892354892304,2.60580588675465,
126.630910825986));
#134758=CARTESIAN_POINT('Ctrl Pts',(-238.900111933189,2.48851652075054,
126.559921741045));
#134759=CARTESIAN_POINT('Ctrl Pts',(-238.907868974074,2.36837091571589,
126.493907942024));
#134760=CARTESIAN_POINT('Ctrl Pts',(-238.915620165314,2.2483159134161,126.427943924521));
#134761=CARTESIAN_POINT('Ctrl Pts',(-238.923371356554,2.12540930058039,
126.366947912511));
#134762=CARTESIAN_POINT('Ctrl Pts',(-238.931122547794,2.00010236826604,
126.311168703241));
#134763=CARTESIAN_POINT('Ctrl Pts',(-238.938870444571,1.87484869474111,
126.255413201622));
#134764=CARTESIAN_POINT('Ctrl Pts',(-238.946618341348,1.74719708726558,
126.204870251402));
#134765=CARTESIAN_POINT('Ctrl Pts',(-238.954366238125,1.61762212001283,
126.159742039109));
#134766=CARTESIAN_POINT('Ctrl Pts',(-238.962112514209,1.48807425704957,
126.114623266665));
#134767=CARTESIAN_POINT('Ctrl Pts',(-238.969858790294,1.35660420353594,
126.074917107761));
#134768=CARTESIAN_POINT('Ctrl Pts',(-238.977605066378,1.22370476032179,
126.040776911776));
#134769=CARTESIAN_POINT('Ctrl Pts',(-238.985351399643,1.09080433607469,
126.006636463776));
#134770=CARTESIAN_POINT('Ctrl Pts',(-238.993097732908,0.956474879742828,
125.978062157958));
#134771=CARTESIAN_POINT('Ctrl Pts',(-239.000844066174,0.821222150136914,
125.955156843479));
#134772=CARTESIAN_POINT('Ctrl Pts',(-239.008592134177,0.685939131619796,
125.932246399513));
#134773=CARTESIAN_POINT('Ctrl Pts',(-239.01634020218,0.549732813801621,
125.915007538376));
#134774=CARTESIAN_POINT('Ctrl Pts',(-239.024088270183,0.413116494941459,
125.903491528914));
#134775=CARTESIAN_POINT('Ctrl Pts',(-239.031844572924,0.276354978631671,
125.891963280099));
#134776=CARTESIAN_POINT('Ctrl Pts',(-239.039600875666,0.139182981019117,
125.88617006593));
#134777=CARTESIAN_POINT('Ctrl Pts',(-239.047357178408,0.00211679838342098,
125.886111073098));
#134778=CARTESIAN_POINT('Ctrl Pts',(-239.055117620922,-0.135022540601304,
125.886052048778));
#134779=CARTESIAN_POINT('Ctrl Pts',(-239.062878063437,-0.27205556163619,
125.891733327966));
#134780=CARTESIAN_POINT('Ctrl Pts',(-239.070638505951,-0.408469655228604,
125.903102044173));
#134781=CARTESIAN_POINT('Ctrl Pts',(-239.078411406216,-0.545102732833955,
125.914489010453));
#134782=CARTESIAN_POINT('Ctrl Pts',(-239.086184306482,-0.681114509415501,
125.931581609581));
#134783=CARTESIAN_POINT('Ctrl Pts',(-239.093957206747,-0.816000257686342,
125.954275397495));
#134784=CARTESIAN_POINT('Ctrl Pts',(-239.101447542509,-0.945982569249743,
125.976144209055));
#134785=CARTESIAN_POINT('Ctrl Pts',(-239.108937878271,-1.07491899763921,
126.003213981662));
#134786=CARTESIAN_POINT('Ctrl Pts',(-239.116428214033,-1.20237188069945,
126.035347625027));
#134787=CARTESIAN_POINT('Ctrl Pts',(-239.124202548152,-1.33465717856032,
126.068699625248));
#134788=CARTESIAN_POINT('Ctrl Pts',(-239.131976882271,-1.46576325317964,
126.107612718806));
#134789=CARTESIAN_POINT('Ctrl Pts',(-239.13975121639,-1.5951867033261,126.151988916591));
#134790=CARTESIAN_POINT('Ctrl Pts',(-239.147515969337,-1.72445065063717,
126.196310424679));
#134791=CARTESIAN_POINT('Ctrl Pts',(-239.155280722284,-1.85203573320956,
126.246081515163));
#134792=CARTESIAN_POINT('Ctrl Pts',(-239.163045475232,-1.97745003610985,
126.30115349184));
#134793=CARTESIAN_POINT('Ctrl Pts',(-239.170802516117,-2.10273977575715,
126.356170770254));
#134794=CARTESIAN_POINT('Ctrl Pts',(-239.178559557002,-2.22586267071119,
126.416478301265));
#134795=CARTESIAN_POINT('Ctrl Pts',(-239.186316597887,-2.3463435836774,
126.481878130634));
#134796=CARTESIAN_POINT('Ctrl Pts',(-239.194067789127,-2.46673364104879,
126.547228641482));
#134797=CARTESIAN_POINT('Ctrl Pts',(-239.201818980367,-2.58448533984699,
126.617663621354));
#134798=CARTESIAN_POINT('Ctrl Pts',(-239.209570171607,-2.69914542606264,
126.692937867293));
#134799=CARTESIAN_POINT('Ctrl Pts',(-239.217318068384,-2.81375677868376,
126.768180119669));
#134800=CARTESIAN_POINT('Ctrl Pts',(-239.225065965161,-2.9252788060595,
126.848257333146));
#134801=CARTESIAN_POINT('Ctrl Pts',(-239.232813861938,-3.03328488400385,
126.932879521787));
#134802=CARTESIAN_POINT('Ctrl Pts',(-239.240560138022,-3.14126836940444,
127.017484009291));
#134803=CARTESIAN_POINT('Ctrl Pts',(-239.248306414107,-3.24573706068587,
127.106631339972));
#134804=CARTESIAN_POINT('Ctrl Pts',(-239.256052690191,-3.34629556977457,
127.199989795605));
#134805=CARTESIAN_POINT('Ctrl Pts',(-239.263799023456,-3.44685482116347,
127.293348940388));
#134806=CARTESIAN_POINT('Ctrl Pts',(-239.271545356721,-3.54350354624211,
127.390919006147));
#134807=CARTESIAN_POINT('Ctrl Pts',(-239.279291689987,-3.63588184010929,
127.492330076151));
#134808=CARTESIAN_POINT('Ctrl Pts',(-239.28703975799,-3.72828082145476,
127.593763856462));
#134809=CARTESIAN_POINT('Ctrl Pts',(-239.294787825993,-3.81640720536389,
127.699040063678));
#134810=CARTESIAN_POINT('Ctrl Pts',(-239.302535893995,-3.89994040765793,
127.807754557501));
#134811=CARTESIAN_POINT('Ctrl Pts',(-239.310292196737,-3.98356239003378,
127.916584594383));
#134812=CARTESIAN_POINT('Ctrl Pts',(-239.318048499479,-4.06258120050844,
128.028859907122));
#134813=CARTESIAN_POINT('Ctrl Pts',(-239.325804802221,-4.13671845259193,
128.144145681422));
#134814=CARTESIAN_POINT('Ctrl Pts',(-239.333565244735,-4.2108952739593,
128.259492987211));
#134815=CARTESIAN_POINT('Ctrl Pts',(-239.34132568725,-4.28018514796353,
128.377853618958));
#134816=CARTESIAN_POINT('Ctrl Pts',(-239.349086129764,-4.34435547472612,
128.498767728152));
#134817=CARTESIAN_POINT('Ctrl Pts',(-239.356859030029,-4.40862881339384,
128.619875939407));
#134818=CARTESIAN_POINT('Ctrl Pts',(-239.364631930295,-4.46776601317441,
128.743545466438));
#134819=CARTESIAN_POINT('Ctrl Pts',(-239.37240483056,-4.52158212838933,
128.869295213315));
#134820=CARTESIAN_POINT('Ctrl Pts',(-239.379895166322,-4.57344189226171,
128.990473640149));
#134821=CARTESIAN_POINT('Ctrl Pts',(-239.387385502084,-4.62036061490404,
129.113583382334));
#134822=CARTESIAN_POINT('Ctrl Pts',(-239.394875837846,-4.66221706717321,
129.238182121653));
#134823=CARTESIAN_POINT('Ctrl Pts',(-239.40169365456,-4.70031544205587,
129.351593775608));
#134824=CARTESIAN_POINT('Ctrl Pts',(-239.408511471274,-4.73429411224294,
129.466454709036));
#134825=CARTESIAN_POINT('Ctrl Pts',(-239.415329287988,-4.76405452823416,
129.582490119309));
#134826=CARTESIAN_POINT('Ctrl Pts',(-237.665046159034,-4.76405452823396,
129.582490119308));
#134827=CARTESIAN_POINT('Ctrl Pts',(-237.672808826289,-4.7981100949745,
129.715272257164));
#134828=CARTESIAN_POINT('Ctrl Pts',(-237.680571493544,-4.82657934103726,
129.849358911575));
#134829=CARTESIAN_POINT('Ctrl Pts',(-237.688334160799,-4.84939024592774,
129.984240318341));
#134830=CARTESIAN_POINT('Ctrl Pts',(-237.696108340009,-4.87223497915706,
130.119321752855));
#134831=CARTESIAN_POINT('Ctrl Pts',(-237.70388251922,-4.88940456463171,
130.25519990647));
#134832=CARTESIAN_POINT('Ctrl Pts',(-237.711656698431,-4.90087891358886,
130.391360694031));
#134833=CARTESIAN_POINT('Ctrl Pts',(-237.715834497277,-4.90704516220861,
130.464532712025));
#134834=CARTESIAN_POINT('Ctrl Pts',(-237.720012296123,-4.91156756503128,
130.537786353004));
#134835=CARTESIAN_POINT('Ctrl Pts',(-237.724190094969,-4.91444921115301,
130.611042192429));
#134836=CARTESIAN_POINT('Ctrl Pts',(-237.727840251317,-4.91696691467898,
130.675046055994));
#134837=CARTESIAN_POINT('Ctrl Pts',(-237.731490407665,-4.91823433856953,
130.739099424647));
#134838=CARTESIAN_POINT('Ctrl Pts',(-237.735140564014,-4.91824985575638,
130.803169461676));
#134839=CARTESIAN_POINT('',(-237.389859436047,-4.91824796558502,130.80883404118));
#134840=CARTESIAN_POINT('Ctrl Pts',(-237.319878776621,-4.76405452823405,
129.582490119308));
#134841=CARTESIAN_POINT('Ctrl Pts',(-237.327551997428,-4.79784307952382,
129.714231167974));
#134842=CARTESIAN_POINT('Ctrl Pts',(-237.335225218235,-4.82616302052628,
129.847375521758));
#134843=CARTESIAN_POINT('Ctrl Pts',(-237.342898439042,-4.84891332956483,
129.981425270854));
#134844=CARTESIAN_POINT('Ctrl Pts',(-237.350725271868,-4.87211908240996,
130.118158593517));
#134845=CARTESIAN_POINT('Ctrl Pts',(-237.358552104693,-4.88952973660893,
130.255833525603));
#134846=CARTESIAN_POINT('Ctrl Pts',(-237.366378937519,-4.90109341756267,
130.393914062185));
#134847=CARTESIAN_POINT('Ctrl Pts',(-237.374205770345,-4.91265709851642,
130.531994598767));
#134848=CARTESIAN_POINT('Ctrl Pts',(-237.38203260317,-4.91837380608168,
130.670480300192));
#134849=CARTESIAN_POINT('Ctrl Pts',(-237.389859435996,-4.91824796558584,
130.808834040274));
#134850=CARTESIAN_POINT('Ctrl Pts',(-237.389859436047,-4.91824796558502,
130.80883404118));
#134851=CARTESIAN_POINT('Ctrl Pts',(-237.399526347849,-4.91809254010862,
130.979714579011));
#134852=CARTESIAN_POINT('Ctrl Pts',(-237.40919325965,-4.9090278711784,131.150197511862));
#134853=CARTESIAN_POINT('Ctrl Pts',(-237.418860171452,-4.89119965687045,
131.319480971591));
#134854=CARTESIAN_POINT('Ctrl Pts',(-237.428698113485,-4.87305601984195,
131.491759450814));
#134855=CARTESIAN_POINT('Ctrl Pts',(-237.438536055518,-4.84583602828776,
131.662795767414));
#134856=CARTESIAN_POINT('Ctrl Pts',(-237.448373997551,-4.80974174435836,
131.831768722983));
#134857=CARTESIAN_POINT('Ctrl Pts',(-237.454026487473,-4.78900340543954,
131.928853857781));
#134858=CARTESIAN_POINT('Ctrl Pts',(-237.459678977395,-4.76533637393173,
132.025258266715));
#134859=CARTESIAN_POINT('Ctrl Pts',(-237.465331467317,-4.73878602478449,
132.120829407096));
#134860=CARTESIAN_POINT('Ctrl Pts',(-237.473105801436,-4.70226914671795,
132.252276254015));
#134861=CARTESIAN_POINT('Ctrl Pts',(-237.480880135554,-4.66022107487715,
132.382410766373));
#134862=CARTESIAN_POINT('Ctrl Pts',(-237.488654469673,-4.61275185039667,
132.510732039374));
#134863=CARTESIAN_POINT('Ctrl Pts',(-237.49641922262,-4.56534112749304,
132.638895167874));
#134864=CARTESIAN_POINT('Ctrl Pts',(-237.504183975567,-4.5125226796618,
132.765249140156));
#134865=CARTESIAN_POINT('Ctrl Pts',(-237.511948728514,-4.45445696488943,
132.889305751244));
#134866=CARTESIAN_POINT('Ctrl Pts',(-237.519705769399,-4.39644892180355,
133.013239147557));
#134867=CARTESIAN_POINT('Ctrl Pts',(-237.527462810284,-4.33320414787966,
133.1348793717));
#134868=CARTESIAN_POINT('Ctrl Pts',(-237.535219851169,-4.26493194233811,
133.25375617356));
#134869=CARTESIAN_POINT('Ctrl Pts',(-237.542971042409,-4.19671122139775,
133.3725433295));
#134870=CARTESIAN_POINT('Ctrl Pts',(-237.550722233649,-4.1234708089651,
133.488570873411));
#134871=CARTESIAN_POINT('Ctrl Pts',(-237.558473424889,-4.04546671423317,
133.601391566006));
#134872=CARTESIAN_POINT('Ctrl Pts',(-237.566221321666,-3.96749577332244,
133.714164306797));
#134873=CARTESIAN_POINT('Ctrl Pts',(-237.573969218443,-3.88476539894875,
133.823732586256));
#134874=CARTESIAN_POINT('Ctrl Pts',(-237.58171711522,-3.79757573134244,
133.929676861919));
#134875=CARTESIAN_POINT('Ctrl Pts',(-237.589463391304,-3.710404301935,134.035598976324));
#134876=CARTESIAN_POINT('Ctrl Pts',(-237.597209667388,-3.618775682944,134.137898293073));
#134877=CARTESIAN_POINT('Ctrl Pts',(-237.604955943472,-3.52303098529225,
134.236187498277));
#134878=CARTESIAN_POINT('Ctrl Pts',(-237.612702276738,-3.42728558087503,
134.33447742903));
#134879=CARTESIAN_POINT('Ctrl Pts',(-237.620448610003,-3.32742430997343,
134.428756909115));
#134880=CARTESIAN_POINT('Ctrl Pts',(-237.628194943268,-3.22382561951452,
134.518675014256));
#134881=CARTESIAN_POINT('Ctrl Pts',(-237.635943011271,-3.12020372884704,
134.608613255934));
#134882=CARTESIAN_POINT('Ctrl Pts',(-237.643691079274,-3.01284304835499,
134.694187922927));
#134883=CARTESIAN_POINT('Ctrl Pts',(-237.651439147277,-2.9021552950917,
134.775088221629));
#134884=CARTESIAN_POINT('Ctrl Pts',(-237.659195450019,-2.79134990156718,
134.856074502132));
#134885=CARTESIAN_POINT('Ctrl Pts',(-237.66695175276,-2.67721068777296,
134.932376259212));
#134886=CARTESIAN_POINT('Ctrl Pts',(-237.674708055502,-2.56017902329741,
135.003725620893));
#134887=CARTESIAN_POINT('Ctrl Pts',(-237.682468498016,-2.44308489549878,
135.075113063876));
#134888=CARTESIAN_POINT('Ctrl Pts',(-237.69022894053,-2.32309558276755,
135.141542655303));
#134889=CARTESIAN_POINT('Ctrl Pts',(-237.697989383044,-2.20067638294647,
135.202792897372));
#134890=CARTESIAN_POINT('Ctrl Pts',(-237.70576228331,-2.07806066495797,
135.264141463768));
#134891=CARTESIAN_POINT('Ctrl Pts',(-237.713535183575,-1.9530076219614,
135.320293905842));
#134892=CARTESIAN_POINT('Ctrl Pts',(-237.721308083841,-1.82600264952798,
135.37107687615));
#134893=CARTESIAN_POINT('Ctrl Pts',(-237.728798419603,-1.7036146277391,
135.420013757577));
#134894=CARTESIAN_POINT('Ctrl Pts',(-237.736288755366,-1.57941441813558,
135.463964674428));
#134895=CARTESIAN_POINT('Ctrl Pts',(-237.743779091128,-1.45384712072204,
135.502819046888));
#134896=CARTESIAN_POINT('Ctrl Pts',(-237.751553425247,-1.32351890107106,
135.543146594687));
#134897=CARTESIAN_POINT('Ctrl Pts',(-237.759327759367,-1.19130504031147,
135.578111243626));
#134898=CARTESIAN_POINT('Ctrl Pts',(-237.767102093486,-1.0576864437554,
135.607534823151));
#134899=CARTESIAN_POINT('Ctrl Pts',(-237.774866846433,-0.924232520177739,
135.636922140744));
#134900=CARTESIAN_POINT('Ctrl Pts',(-237.78263159938,-0.789377683550235,
135.660781893073));
#134901=CARTESIAN_POINT('Ctrl Pts',(-237.790396352327,-0.653619406006261,
135.678985191273));
#134902=CARTESIAN_POINT('Ctrl Pts',(-237.798153393212,-0.517995965497401,
135.697170409701));
#134903=CARTESIAN_POINT('Ctrl Pts',(-237.805910434097,-0.381471254749789,
135.709710302591));
#134904=CARTESIAN_POINT('Ctrl Pts',(-237.813667474982,-0.244554039840854,
135.716526777632));
#134905=CARTESIAN_POINT('Ctrl Pts',(-237.821418666222,-0.107740075268928,
135.723338112317));
#134906=CARTESIAN_POINT('Ctrl Pts',(-237.829169857462,0.0294654154116941,
135.724434600675));
#134907=CARTESIAN_POINT('Ctrl Pts',(-237.836921048702,0.16654777789893,
135.719789886732));
#134908=CARTESIAN_POINT('Ctrl Pts',(-237.844668945479,0.303571876725503,
135.715147146917));
#134909=CARTESIAN_POINT('Ctrl Pts',(-237.852416842256,0.440472561521645,
135.704768071312));
#134910=CARTESIAN_POINT('Ctrl Pts',(-237.860164739033,0.576734626202866,
135.688678403443));
#134911=CARTESIAN_POINT('Ctrl Pts',(-237.867911015118,0.712968187797626,
135.672592101186));
#134912=CARTESIAN_POINT('Ctrl Pts',(-237.875657291202,0.848563006964617,
135.650797628474));
#134913=CARTESIAN_POINT('Ctrl Pts',(-237.883403567286,0.983008846773999,
135.623372618969));
#134914=CARTESIAN_POINT('Ctrl Pts',(-237.891149900551,1.11745567903185,
135.595947407018));
#134915=CARTESIAN_POINT('Ctrl Pts',(-237.898896233816,1.25075313193135,
135.56289165348));
#134916=CARTESIAN_POINT('Ctrl Pts',(-237.906642567082,1.38240140313231,
135.52433407333));
#134917=CARTESIAN_POINT('Ctrl Pts',(-237.914390635085,1.51407915605063,
135.485767858477));
#134918=CARTESIAN_POINT('Ctrl Pts',(-237.922138703088,1.64410661722893,
135.441697475153));
#134919=CARTESIAN_POINT('Ctrl Pts',(-237.929886771091,1.77199976408061,
135.392301321041));
#134920=CARTESIAN_POINT('Ctrl Pts',(-237.937643073832,1.90002883729089,
135.342852668107));
#134921=CARTESIAN_POINT('Ctrl Pts',(-237.945399376574,2.02591869956226,
135.288067078427));
#134922=CARTESIAN_POINT('Ctrl Pts',(-237.953155679316,2.14920541157007,
135.228171097387));
#134923=CARTESIAN_POINT('Ctrl Pts',(-237.96091612183,2.2725579254085,135.168243148059));
#134924=CARTESIAN_POINT('Ctrl Pts',(-237.968676564344,2.39330417649297,
135.103199557782));
#134925=CARTESIAN_POINT('Ctrl Pts',(-237.976437006859,2.5110063076024,135.033312069839));
#134926=CARTESIAN_POINT('Ctrl Pts',(-237.984209907124,2.6288973846218,134.963312392296));
#134927=CARTESIAN_POINT('Ctrl Pts',(-237.99198280739,2.74373424878877,134.888453492076));
#134928=CARTESIAN_POINT('Ctrl Pts',(-237.999755707655,2.85510868982739,
134.809050047693));
#134929=CARTESIAN_POINT('Ctrl Pts',(-238.007246043417,2.96243438940019,
134.732533118518));
#134930=CARTESIAN_POINT('Ctrl Pts',(-238.014736379179,3.06654478754454,
134.651796508769));
#134931=CARTESIAN_POINT('Ctrl Pts',(-238.022226714941,3.16710626290611,
134.567154922595));
#134932=CARTESIAN_POINT('Ctrl Pts',(-238.030001049061,3.27148055716997,
134.479304124956));
#134933=CARTESIAN_POINT('Ctrl Pts',(-238.03777538318,3.37236212781656,134.386968106218));
#134934=CARTESIAN_POINT('Ctrl Pts',(-238.045549717299,3.46934113384456,
134.290455160104));
#134935=CARTESIAN_POINT('Ctrl Pts',(-238.053314470246,3.56620062191489,
134.194061157571));
#134936=CARTESIAN_POINT('Ctrl Pts',(-238.061079223193,3.65916684050278,
134.093500743169));
#134937=CARTESIAN_POINT('Ctrl Pts',(-238.06884397614,3.74786245591568,133.989122786714));
#134938=CARTESIAN_POINT('Ctrl Pts',(-238.076601017025,3.83646997759296,
133.884848499917));
#134939=CARTESIAN_POINT('Ctrl Pts',(-238.08435805791,3.92081508558972,133.776764512595));
#134940=CARTESIAN_POINT('Ctrl Pts',(-238.092115098795,4.00055707814202,
133.665256653256));
#134941=CARTESIAN_POINT('Ctrl Pts',(-238.099866290035,4.08023893663733,
133.553832882862));
#134942=CARTESIAN_POINT('Ctrl Pts',(-238.107617481275,4.15532436249089,
133.438990696431));
#134943=CARTESIAN_POINT('Ctrl Pts',(-238.115368672515,4.22551299845294,
133.321148841157));
#134944=CARTESIAN_POINT('Ctrl Pts',(-238.123116569293,4.29567180237245,
133.203357071814));
#134945=CARTESIAN_POINT('Ctrl Pts',(-238.13086446607,4.36093775623293,133.082568504578));
#134946=CARTESIAN_POINT('Ctrl Pts',(-238.138612362847,4.42105403731816,
132.959230511925));
#134947=CARTESIAN_POINT('Ctrl Pts',(-238.146358638931,4.48115774337334,
132.83591831892));
#134948=CARTESIAN_POINT('Ctrl Pts',(-238.154104915015,4.53611374807617,
132.710058112449));
#134949=CARTESIAN_POINT('Ctrl Pts',(-238.161851191099,4.58571157130187,
132.582121132182));
#134950=CARTESIAN_POINT('Ctrl Pts',(-238.169597524365,4.63530976064736,
132.454183207514));
#134951=CARTESIAN_POINT('Ctrl Pts',(-238.17734385763,4.67954954827176,132.32416884299));
#134952=CARTESIAN_POINT('Ctrl Pts',(-238.185090190895,4.71826907035566,
132.192568110063));
#134953=CARTESIAN_POINT('Ctrl Pts',(-238.192838258898,4.75699726340812,
132.060937906064));
#134954=CARTESIAN_POINT('Ctrl Pts',(-238.200586326901,4.79020262064375,
131.92772100174));
#134955=CARTESIAN_POINT('Ctrl Pts',(-238.208334394904,4.81777360705397,
131.793421047304));
#134956=CARTESIAN_POINT('Ctrl Pts',(-238.216090697646,4.8453738962366,131.65897835728));
#134957=CARTESIAN_POINT('Ctrl Pts',(-238.223847000388,4.86732777361825,
131.523450701329));
#134958=CARTESIAN_POINT('Ctrl Pts',(-238.23160330313,4.88357506771269,131.387350858063));
#134959=CARTESIAN_POINT('Ctrl Pts',(-238.239363745644,4.89983103347718,
131.251178374213));
#134960=CARTESIAN_POINT('Ctrl Pts',(-238.247124188158,4.91037431694902,
131.114433484141));
#134961=CARTESIAN_POINT('Ctrl Pts',(-238.254884630672,4.91519687092446,
130.977631453411));
#134962=CARTESIAN_POINT('Ctrl Pts',(-238.262657530938,4.92002716649167,
130.840609815916));
#134963=CARTESIAN_POINT('Ctrl Pts',(-238.270430431203,4.91911838375073,
130.703531245644));
#134964=CARTESIAN_POINT('Ctrl Pts',(-238.278203331469,4.91251462302238,
130.566909272884));
#134965=CARTESIAN_POINT('Ctrl Pts',(-238.285693667231,4.90615092563052,
130.435253852967));
#134966=CARTESIAN_POINT('Ctrl Pts',(-238.293184002992,4.89449914250425,
130.304022716782));
#134967=CARTESIAN_POINT('Ctrl Pts',(-238.300674338754,4.87764371266572,
130.173666654702));
#134968=CARTESIAN_POINT('Ctrl Pts',(-238.308448672873,4.86014920408149,
130.038368102906));
#134969=CARTESIAN_POINT('Ctrl Pts',(-238.316223006992,4.8369932495294,129.903583706847));
#134970=CARTESIAN_POINT('Ctrl Pts',(-238.323997341111,4.8082136961773,129.769824917654));
#134971=CARTESIAN_POINT('Ctrl Pts',(-238.331762094059,4.77946961105252,
129.636230974213));
#134972=CARTESIAN_POINT('Ctrl Pts',(-238.339526847006,4.74511579837063,
129.503660501267));
#134973=CARTESIAN_POINT('Ctrl Pts',(-238.347291599953,4.70524181410956,
129.372619532993));
#134974=CARTESIAN_POINT('Ctrl Pts',(-238.355048640838,4.66540743325179,
129.241708716456));
#134975=CARTESIAN_POINT('Ctrl Pts',(-238.362805681723,4.62006390473615,
129.112324753075));
#134976=CARTESIAN_POINT('Ctrl Pts',(-238.370562722608,4.56935167938908,
128.984962834627));
#134977=CARTESIAN_POINT('Ctrl Pts',(-238.378313913848,4.51867769652569,
128.857696960792));
#134978=CARTESIAN_POINT('Ctrl Pts',(-238.386065105088,4.46264321931968,
128.73245045855));
#134979=CARTESIAN_POINT('Ctrl Pts',(-238.393816296328,4.40143820121287,
128.609702370047));
#134980=CARTESIAN_POINT('Ctrl Pts',(-238.401564193105,4.34025919687138,
128.487006452755));
#134981=CARTESIAN_POINT('Ctrl Pts',(-238.409312089882,4.27391419661751,
128.366807186329));
#134982=CARTESIAN_POINT('Ctrl Pts',(-238.417059986659,4.20264076863304,
128.249562458743));
#134983=CARTESIAN_POINT('Ctrl Pts',(-238.424806262743,4.13138224951323,
128.132342256227));
#134984=CARTESIAN_POINT('Ctrl Pts',(-238.432552538828,4.05519755618014,
128.018075697132));
#134985=CARTESIAN_POINT('Ctrl Pts',(-238.440298814912,3.97436938626618,
127.9071945809));
#134986=CARTESIAN_POINT('Ctrl Pts',(-238.448045148177,3.89354061969715,
127.796312646169));
#134987=CARTESIAN_POINT('Ctrl Pts',(-238.455791481442,3.80806853845349,
127.688816520103));
#134988=CARTESIAN_POINT('Ctrl Pts',(-238.463537814708,3.71827796217919,
127.585107278906));
#134989=CARTESIAN_POINT('Ctrl Pts',(-238.471285882711,3.62846727792776,
127.481374812744));
#134990=CARTESIAN_POINT('Ctrl Pts',(-238.479033950713,3.53433643009288,
127.381431214486));
#134991=CARTESIAN_POINT('Ctrl Pts',(-238.486782018716,3.43624886646806,
127.285642556937));
#134992=CARTESIAN_POINT('Ctrl Pts',(-238.494538321458,3.3380570542135,127.189752094063));
#134993=CARTESIAN_POINT('Ctrl Pts',(-238.5022946242,3.23590040589847,127.098025666768));
#134994=CARTESIAN_POINT('Ctrl Pts',(-238.510050926942,3.13017781253146,
127.01079106839));
#134995=CARTESIAN_POINT('Ctrl Pts',(-238.517811369456,3.02439879183313,
126.92350991028));
#134996=CARTESIAN_POINT('Ctrl Pts',(-238.52557181197,2.91505034525037,126.840725594031));
#134997=CARTESIAN_POINT('Ctrl Pts',(-238.533332254485,2.80256163058388,
126.762723403604));
#134998=CARTESIAN_POINT('Ctrl Pts',(-238.54110515475,2.68989233904632,126.684595997137));
#134999=CARTESIAN_POINT('Ctrl Pts',(-238.548878055015,2.57407303634056,
126.611266266233));
#135000=CARTESIAN_POINT('Ctrl Pts',(-238.556650955281,2.45555960734366,
126.542974683708));
#135001=CARTESIAN_POINT('Ctrl Pts',(-238.564141291043,2.34135444000556,
126.477165672223));
#135002=CARTESIAN_POINT('Ctrl Pts',(-238.571631626805,2.22464789507923,
126.416035012753));
#135003=CARTESIAN_POINT('Ctrl Pts',(-238.579121962567,2.10586487662709,
126.359755327567));
#135004=CARTESIAN_POINT('Ctrl Pts',(-238.586896296686,1.98257816392963,
126.301341781012));
#135005=CARTESIAN_POINT('Ctrl Pts',(-238.594670630806,1.85666387518112,
126.247969283026));
#135006=CARTESIAN_POINT('Ctrl Pts',(-238.602444964925,1.72857276602027,
126.199882443541));
#135007=CARTESIAN_POINT('Ctrl Pts',(-238.610209717872,1.60063951770362,
126.151854866788));
#135008=CARTESIAN_POINT('Ctrl Pts',(-238.617974470819,1.47053514932972,
126.109100123507));
#135009=CARTESIAN_POINT('Ctrl Pts',(-238.625739223766,1.33873380897834,
126.07181639155));
#135010=CARTESIAN_POINT('Ctrl Pts',(-238.633496264651,1.2070633755759,126.034569690321));
#135011=CARTESIAN_POINT('Ctrl Pts',(-238.641253305536,1.07369969809899,
126.00278329247));
#135012=CARTESIAN_POINT('Ctrl Pts',(-238.649010346421,0.939135312516304,
125.976606695991));
#135013=CARTESIAN_POINT('Ctrl Pts',(-238.656761537661,0.804672402983724,
125.950449839486));
#135014=CARTESIAN_POINT('Ctrl Pts',(-238.664512728901,0.669010969833791,
125.929894438361));
#135015=CARTESIAN_POINT('Ctrl Pts',(-238.672263920141,0.53265671926662,
125.915039613386));
#135016=CARTESIAN_POINT('Ctrl Pts',(-238.680011816918,0.396360422893123,
125.900191102107));
#135017=CARTESIAN_POINT('Ctrl Pts',(-238.687759713696,0.259372282624431,
125.891038390275));
#135018=CARTESIAN_POINT('Ctrl Pts',(-238.695507610473,0.122205943987116,
125.887629104685));
#135019=CARTESIAN_POINT('Ctrl Pts',(-238.703253886557,-0.0149317024091209,
125.884220532244));
#135020=CARTESIAN_POINT('Ctrl Pts',(-238.711000162641,-0.152247082434574,
125.886553006101));
#135021=CARTESIAN_POINT('Ctrl Pts',(-238.718746438725,-0.289224106013271,
125.894622082878));
#135022=CARTESIAN_POINT('Ctrl Pts',(-238.72649277199,-0.426202140725053,
125.902691219219));
#135023=CARTESIAN_POINT('Ctrl Pts',(-238.734239105256,-0.562841423717549,
125.916497019986));
#135024=CARTESIAN_POINT('Ctrl Pts',(-238.741985438521,-0.698628945267916,
125.935982996702));
#135025=CARTESIAN_POINT('Ctrl Pts',(-238.749733506524,-0.834446875492065,
125.955473337166));
#135026=CARTESIAN_POINT('Ctrl Pts',(-238.757481574527,-0.969412277784851,
125.980646329257));
#135027=CARTESIAN_POINT('Ctrl Pts',(-238.76522964253,-1.10302071231747,
126.011394065346));
#135028=CARTESIAN_POINT('Ctrl Pts',(-238.772985945272,-1.23677114748446,
126.042174480495));
#135029=CARTESIAN_POINT('Ctrl Pts',(-238.780742248014,-1.36916135232485,
126.078541387453));
#135030=CARTESIAN_POINT('Ctrl Pts',(-238.788498550756,-1.49969993468534,
126.120336368226));
#135031=CARTESIAN_POINT('Ctrl Pts',(-238.79625899327,-1.63030818941768,
126.162153656238));
#135032=CARTESIAN_POINT('Ctrl Pts',(-238.804019435784,-1.75906248561458,
126.209404656206));
#135033=CARTESIAN_POINT('Ctrl Pts',(-238.811779878298,-1.88549083552424,
126.261882508466));
#135034=CARTESIAN_POINT('Ctrl Pts',(-238.819552778564,-2.01212213944494,
126.314444602833));
#135035=CARTESIAN_POINT('Ctrl Pts',(-238.827325678829,-2.13641968101698,
126.372250151641));
#135036=CARTESIAN_POINT('Ctrl Pts',(-238.835098579094,-2.25793472673775,
126.435045587462));
#135037=CARTESIAN_POINT('Ctrl Pts',(-238.842588914856,-2.37503239446765,
126.495558251018));
#135038=CARTESIAN_POINT('Ctrl Pts',(-238.850079250618,-2.48954608783481,
126.560704157921));
#135039=CARTESIAN_POINT('Ctrl Pts',(-238.85756958638,-2.60110090381225,
126.630219130902));
#135040=CARTESIAN_POINT('Ctrl Pts',(-238.86534527437,-2.71690551795641,
126.702382349969));
#135041=CARTESIAN_POINT('Ctrl Pts',(-238.873120962359,-2.829888240962,126.779482753564));
#135042=CARTESIAN_POINT('Ctrl Pts',(-238.880896650348,-2.93959939826533,
126.86127319269));
#135043=CARTESIAN_POINT('Ctrl Pts',(-238.888766252182,-3.05063563402061,
126.944051487118));
#135044=CARTESIAN_POINT('Ctrl Pts',(-238.896635854016,-3.15832037898057,
127.031633709791));
#135045=CARTESIAN_POINT('Ctrl Pts',(-238.90450545585,-3.26221344406456,
127.123715768105));
#135046=CARTESIAN_POINT('Ctrl Pts',(-238.912261690011,-3.3646098495665,
127.214471313482));
#135047=CARTESIAN_POINT('Ctrl Pts',(-238.920017924172,-3.4633227704474,
127.309597660825));
#135048=CARTESIAN_POINT('Ctrl Pts',(-238.927774158334,-3.55796076349559,
127.408760778373));
#135049=CARTESIAN_POINT('Ctrl Pts',(-238.935525020074,-3.65253320474194,
127.507855209754));
#135050=CARTESIAN_POINT('Ctrl Pts',(-238.943275881815,-3.74303606522609,
127.610980566509));
#135051=CARTESIAN_POINT('Ctrl Pts',(-238.951026743555,-3.82911314771992,
127.717764504619));
#135052=CARTESIAN_POINT('Ctrl Pts',(-238.958773915244,-3.91514925040071,
127.824497604739));
#135053=CARTESIAN_POINT('Ctrl Pts',(-238.966521086933,-3.99676352385031,
127.934885515953));
#135054=CARTESIAN_POINT('Ctrl Pts',(-238.974268258622,-4.0736388974835,
128.048521508436));
#135055=CARTESIAN_POINT('Ctrl Pts',(-238.982226494934,-4.15260867051577,
128.165253409832));
#135056=CARTESIAN_POINT('Ctrl Pts',(-238.990184731246,-4.22657735310258,
128.285412585883));
#135057=CARTESIAN_POINT('Ctrl Pts',(-238.998142967557,-4.29524780853793,
128.408524787266));
#135058=CARTESIAN_POINT('Ctrl Pts',(-239.005889503974,-4.36209153658539,
128.528362036872));
#135059=CARTESIAN_POINT('Ctrl Pts',(-239.01363604039,-4.42391518069558,
128.650996819491));
#135060=CARTESIAN_POINT('Ctrl Pts',(-239.021382576807,-4.48049086939839,
128.775966022883));
#135061=CARTESIAN_POINT('Ctrl Pts',(-239.029446663066,-4.53938573664773,
128.906058025523));
#135062=CARTESIAN_POINT('Ctrl Pts',(-239.037510749325,-4.5925930445791,
129.038679492564));
#135063=CARTESIAN_POINT('Ctrl Pts',(-239.045574835585,-4.63991114167916,
129.173285003187));
#135064=CARTESIAN_POINT('Ctrl Pts',(-239.053638921844,-4.68722923877922,
129.30789051381));
#135065=CARTESIAN_POINT('Ctrl Pts',(-239.061703008104,-4.72865800359389,
129.444479606954));
#135066=CARTESIAN_POINT('Ctrl Pts',(-239.069767094363,-4.76405452823403,
129.582490119308));
#135067=CARTESIAN_POINT('Origin',(213.235140564004,0.,130.804360617566));
#135068=CARTESIAN_POINT('',(-241.165327127303,-4.76405452823409,129.582490119308));
#135069=CARTESIAN_POINT('',(-240.820011204651,-4.76405452823406,129.582490119308));
#135070=CARTESIAN_POINT('',(213.235140564004,-4.76405452823405,129.582490119308));
#135071=CARTESIAN_POINT('',(-239.485140563964,-4.91824839639984,130.800388991906));
#135072=CARTESIAN_POINT('Ctrl Pts',(-239.485140564014,-4.91824839640055,
130.800388992789));
#135073=CARTESIAN_POINT('Ctrl Pts',(-239.492981518083,-4.91836051407927,
130.939229549107));
#135074=CARTESIAN_POINT('Ctrl Pts',(-239.500822472151,-4.91258895669507,
131.078149716857));
#135075=CARTESIAN_POINT('Ctrl Pts',(-239.50866342622,-4.90094187300933,
131.216612749014));
#135076=CARTESIAN_POINT('Ctrl Pts',(-239.516391847359,-4.88946194760979,
131.353088567567));
#135077=CARTESIAN_POINT('Ctrl Pts',(-239.524120268498,-4.8722740815105,
131.489119884404));
#135078=CARTESIAN_POINT('Ctrl Pts',(-239.531848689638,-4.84943848763251,
131.624195611433));
#135079=CARTESIAN_POINT('Ctrl Pts',(-239.539577205338,-4.82660261435007,
131.759272991178));
#135080=CARTESIAN_POINT('Ctrl Pts',(-239.547305721038,-4.79811894081519,
131.893394370734));
#135081=CARTESIAN_POINT('Ctrl Pts',(-239.555034236738,-4.76409908540016,
132.026057374945));
#135082=CARTESIAN_POINT('Ctrl Pts',(-239.562764536443,-4.73007137704356,
132.158751002296));
#135083=CARTESIAN_POINT('Ctrl Pts',(-239.570494836148,-4.690505041369,132.289985204269));
#135084=CARTESIAN_POINT('Ctrl Pts',(-239.578225135853,-4.64556187844975,
132.419271728431));
#135085=CARTESIAN_POINT('Ctrl Pts',(-239.586149996337,-4.59948755928598,
132.551812212698));
#135086=CARTESIAN_POINT('Ctrl Pts',(-239.594074856821,-4.54776231027495,
132.682305263779));
#135087=CARTESIAN_POINT('Ctrl Pts',(-239.601999717305,-4.49061289323881,
132.81024668252));
#135088=CARTESIAN_POINT('Ctrl Pts',(-239.609742916342,-4.4347735113534,
132.935255302215));
#135089=CARTESIAN_POINT('Ctrl Pts',(-239.617486115378,-4.37375617727099,
133.057827681082));
#135090=CARTESIAN_POINT('Ctrl Pts',(-239.625229314415,-4.30781859575813,
133.177519273986));
#135091=CARTESIAN_POINT('Ctrl Pts',(-239.633245005623,-4.23956059414176,
133.301422953109));
#135092=CARTESIAN_POINT('Ctrl Pts',(-239.64126069683,-4.16602995590322,
133.422238978381));
#135093=CARTESIAN_POINT('Ctrl Pts',(-239.649276388037,-4.08756026267536,
133.539508540713));
#135094=CARTESIAN_POINT('Ctrl Pts',(-239.657292079245,-4.00909056944729,
133.656778103046));
#135095=CARTESIAN_POINT('Ctrl Pts',(-239.665307770452,-3.92568215040277,
133.77050087529));
#135096=CARTESIAN_POINT('Ctrl Pts',(-239.67332346166,-3.83771253088084,
133.880258143951));
#135097=CARTESIAN_POINT('Ctrl Pts',(-239.681097795779,-3.752391727372,133.986710557909));
#135098=CARTESIAN_POINT('Ctrl Pts',(-239.688872129898,-3.66250317866118,
134.089778887007));
#135099=CARTESIAN_POINT('Ctrl Pts',(-239.696646464017,-3.56834525463581,
134.189046010068));
#135100=CARTESIAN_POINT('Ctrl Pts',(-239.704411216964,-3.47430337183668,
134.288190795272));
#135101=CARTESIAN_POINT('Ctrl Pts',(-239.712175969911,-3.37600284926054,
134.383543414556));
#135102=CARTESIAN_POINT('Ctrl Pts',(-239.719940722858,-3.27378340128807,
134.474718270977));
#135103=CARTESIAN_POINT('Ctrl Pts',(-239.727697763743,-3.17166547911209,
134.565802571245));
#135104=CARTESIAN_POINT('Ctrl Pts',(-239.735454804628,-3.06563666733478,
134.65271710761));
#135105=CARTESIAN_POINT('Ctrl Pts',(-239.743211845513,-2.95607450745325,
134.735112017602));
#135106=CARTESIAN_POINT('Ctrl Pts',(-239.750963036753,-2.84659496924861,
134.817444792952));
#135107=CARTESIAN_POINT('Ctrl Pts',(-239.758714227994,-2.73358769771764,
134.895264491878));
#135108=CARTESIAN_POINT('Ctrl Pts',(-239.766465419234,-2.61746411171743,
134.968260794848));
#135109=CARTESIAN_POINT('Ctrl Pts',(-239.774213316011,-2.50138988133944,
135.041226072442));
#135110=CARTESIAN_POINT('Ctrl Pts',(-239.781961212788,-2.38220230116201,
135.109371823884));
#135111=CARTESIAN_POINT('Ctrl Pts',(-239.789709109565,-2.26034245179049,
135.172430564709));
#135112=CARTESIAN_POINT('Ctrl Pts',(-239.797455385649,-2.13850809287213,
135.235476115005));
#135113=CARTESIAN_POINT('Ctrl Pts',(-239.805201661733,-2.01400292361361,
135.293436591657));
#135114=CARTESIAN_POINT('Ctrl Pts',(-239.812947937817,-1.88729299703757,
135.346090266701));
#135115=CARTESIAN_POINT('Ctrl Pts',(-239.820694271083,-1.76058213511816,
135.398744330422));
#135116=CARTESIAN_POINT('Ctrl Pts',(-239.828440604348,-1.6316668444402,
135.446091364341));
#135117=CARTESIAN_POINT('Ctrl Pts',(-239.836186937613,-1.50103317104183,
135.487957790886));
#135118=CARTESIAN_POINT('Ctrl Pts',(-239.843935005616,-1.37037024313823,
135.529833593128));
#135119=CARTESIAN_POINT('Ctrl Pts',(-239.851683073619,-1.23798853900794,
135.566226226425));
#135120=CARTESIAN_POINT('Ctrl Pts',(-239.859431141622,-1.10438888729454,
135.597012101674));
#135121=CARTESIAN_POINT('Ctrl Pts',(-239.867187444364,-0.970647244280896,
135.627830696517));
#135122=CARTESIAN_POINT('Ctrl Pts',(-239.874943747106,-0.835685449470971,
135.653030541777));
#135123=CARTESIAN_POINT('Ctrl Pts',(-239.882700049847,-0.700014689856641,
135.672539178022));
#135124=CARTESIAN_POINT('Ctrl Pts',(-239.890460492361,-0.564271518672938,
135.692058226614));
#135125=CARTESIAN_POINT('Ctrl Pts',(-239.898220934876,-0.4278190174835,
135.705879974196));
#135126=CARTESIAN_POINT('Ctrl Pts',(-239.90598137739,-0.291172110356458,
135.713984010928));
#135127=CARTESIAN_POINT('Ctrl Pts',(-239.913754277655,-0.154305845483154,
135.72210105698));
#135128=CARTESIAN_POINT('Ctrl Pts',(-239.921527177921,-0.0172449421728213,
135.724482043666));
#135129=CARTESIAN_POINT('Ctrl Pts',(-239.929300078186,0.119496158882949,
135.721158735296));
#135130=CARTESIAN_POINT('Ctrl Pts',(-239.936790413948,0.251266376484923,
135.717956237556));
#135131=CARTESIAN_POINT('Ctrl Pts',(-239.94428074971,0.382739332014857,
135.70945699528));
#135132=CARTESIAN_POINT('Ctrl Pts',(-239.951771085472,0.513462338611925,
135.695734605448));
#135133=CARTESIAN_POINT('Ctrl Pts',(-239.959545419591,0.649141747736717,
135.681491927034));
#135134=CARTESIAN_POINT('Ctrl Pts',(-239.96731975371,0.784443008281681,
135.661577094689));
#135135=CARTESIAN_POINT('Ctrl Pts',(-239.975094087829,0.918853908175262,
135.636015671265));
#135136=CARTESIAN_POINT('Ctrl Pts',(-239.982858840776,1.05309915864737,
135.61048575001));
#135137=CARTESIAN_POINT('Ctrl Pts',(-239.990623593723,1.18645585135361,
135.579323156191));
#135138=CARTESIAN_POINT('Ctrl Pts',(-239.99838834667,1.3184159487441,135.542605276572));
#135139=CARTESIAN_POINT('Ctrl Pts',(-240.006145387555,1.45024498150556,
135.505923865668));
#135140=CARTESIAN_POINT('Ctrl Pts',(-240.01390242844,1.58067980516023,135.463698253339));
#135141=CARTESIAN_POINT('Ctrl Pts',(-240.021659469325,1.70922200010184,
135.416056966727));
#135142=CARTESIAN_POINT('Ctrl Pts',(-240.029410660565,1.83766726037521,
135.36845160678));
#135143=CARTESIAN_POINT('Ctrl Pts',(-240.037161851805,1.96422236766908,
135.31543883683));
#135144=CARTESIAN_POINT('Ctrl Pts',(-240.044913043046,2.08840385943053,
135.257197059927));
#135145=CARTESIAN_POINT('Ctrl Pts',(-240.052660939823,2.21253257074448,
135.198980037332));
#135146=CARTESIAN_POINT('Ctrl Pts',(-240.0604088366,2.33428931982447,135.135538593768));
#135147=CARTESIAN_POINT('Ctrl Pts',(-240.068156733377,2.45321064957463,
135.067099240953));
#135148=CARTESIAN_POINT('Ctrl Pts',(-240.075903009461,2.57210710354691,
134.998674204175));
#135149=CARTESIAN_POINT('Ctrl Pts',(-240.083649285545,2.68816897927273,
134.925253532501));
#135150=CARTESIAN_POINT('Ctrl Pts',(-240.091395561629,2.80095781769323,
134.84710948016));
#135151=CARTESIAN_POINT('Ctrl Pts',(-240.099141894895,2.91374748869485,
134.768964850977));
#135152=CARTESIAN_POINT('Ctrl Pts',(-240.10688822816,3.02326375281079,134.686096994207));
#135153=CARTESIAN_POINT('Ctrl Pts',(-240.114634561425,3.12909785455932,
134.598821011231));
#135154=CARTESIAN_POINT('Ctrl Pts',(-240.122382629428,3.23495565712099,
134.511525483404));
#135155=CARTESIAN_POINT('Ctrl Pts',(-240.130130697431,3.33712935489285,
134.419820113711));
#135156=CARTESIAN_POINT('Ctrl Pts',(-240.137878765434,3.43524425874479,
134.324059460544));
#135157=CARTESIAN_POINT('Ctrl Pts',(-240.145635068176,3.53346344028425,
134.228197031815));
#135158=CARTESIAN_POINT('Ctrl Pts',(-240.153391370918,3.62761493051781,
134.128270983428));
#135159=CARTESIAN_POINT('Ctrl Pts',(-240.16114767366,3.71736145821841,134.024672225385));
#135160=CARTESIAN_POINT('Ctrl Pts',(-240.168908116174,3.80715588634307,
133.921018173565));
#135161=CARTESIAN_POINT('Ctrl Pts',(-240.176668558688,3.89254042396627,
133.813687811961));
#135162=CARTESIAN_POINT('Ctrl Pts',(-240.184429001202,3.97321957067578,
133.70310332876));
#135163=CARTESIAN_POINT('Ctrl Pts',(-240.192201901467,4.05402823071395,
133.592341325529));
#135164=CARTESIAN_POINT('Ctrl Pts',(-240.199974801733,4.13011618838364,
133.47831508727));
#135165=CARTESIAN_POINT('Ctrl Pts',(-240.207747701998,4.20123210013872,
133.361474596892));
#135166=CARTESIAN_POINT('Ctrl Pts',(-240.21523803776,4.26976276937055,133.248881552644));
#135167=CARTESIAN_POINT('Ctrl Pts',(-240.222728373522,4.33367646000155,
133.133675583595));
#135168=CARTESIAN_POINT('Ctrl Pts',(-240.230218709284,4.39279040294944,
133.016277328985));
#135169=CARTESIAN_POINT('Ctrl Pts',(-240.237993043403,4.45414566901211,
132.894427883869));
#135170=CARTESIAN_POINT('Ctrl Pts',(-240.245767377522,4.51052439278442,
132.769830648112));
#135171=CARTESIAN_POINT('Ctrl Pts',(-240.253541711642,4.56167121788152,
132.642930377584));
#135172=CARTESIAN_POINT('Ctrl Pts',(-240.261306464589,4.61275500908781,
132.516186500297));
#135173=CARTESIAN_POINT('Ctrl Pts',(-240.269071217536,4.65861958616375,
132.387145594718));
#135174=CARTESIAN_POINT('Ctrl Pts',(-240.276835970483,4.69905545007956,
132.256276916661));
#135175=CARTESIAN_POINT('Ctrl Pts',(-240.284593011368,4.73945115252529,
132.12553821922));
#135176=CARTESIAN_POINT('Ctrl Pts',(-240.292350052253,4.77442875721439,
131.992975733091));
#135177=CARTESIAN_POINT('Ctrl Pts',(-240.300107093138,4.80382698970042,
131.859078264866));
#135178=CARTESIAN_POINT('Ctrl Pts',(-240.307858284378,4.83320305275076,
131.725281769763));
#135179=CARTESIAN_POINT('Ctrl Pts',(-240.315609475618,4.85700803476486,
131.590152676703));
#135180=CARTESIAN_POINT('Ctrl Pts',(-240.323360666858,4.8751307079616,131.454194167631));
#135181=CARTESIAN_POINT('Ctrl Pts',(-240.331108563635,4.89324567853873,
131.318293444552));
#135182=CARTESIAN_POINT('Ctrl Pts',(-240.338856460412,4.90568309226471,
131.181564393331));
#135183=CARTESIAN_POINT('Ctrl Pts',(-240.346604357189,4.91238300998312,
131.044519368665));
#135184=CARTESIAN_POINT('Ctrl Pts',(-240.354350633274,4.91908152622316,
130.907503010863));
#135185=CARTESIAN_POINT('Ctrl Pts',(-240.362096909358,4.92004491456186,
130.770171201334));
#135186=CARTESIAN_POINT('Ctrl Pts',(-240.369843185442,4.91526523235931,
130.633039988161));
#135187=CARTESIAN_POINT('Ctrl Pts',(-240.377589518707,4.91048551487422,
130.495907762716));
#135188=CARTESIAN_POINT('Ctrl Pts',(-240.385335851972,4.89996265587237,
130.35897652731));
#135189=CARTESIAN_POINT('Ctrl Pts',(-240.393082185238,4.88374081674733,
130.222760499498));
#135190=CARTESIAN_POINT('Ctrl Pts',(-240.400830253241,4.86751534485396,
130.086513967053));
#135191=CARTESIAN_POINT('Ctrl Pts',(-240.408578321244,4.84558839947765,
129.950983349061));
#135192=CARTESIAN_POINT('Ctrl Pts',(-240.416326389247,4.81805575200773,
129.816675529572));
#135193=CARTESIAN_POINT('Ctrl Pts',(-240.424082691988,4.79049384251232,
129.682224966134));
#135194=CARTESIAN_POINT('Ctrl Pts',(-240.43183899473,4.75731440820122,129.549000180909));
#135195=CARTESIAN_POINT('Ctrl Pts',(-240.439595297472,4.71866402939323,
129.417496226138));
#135196=CARTESIAN_POINT('Ctrl Pts',(-240.447355739986,4.67999302171433,
129.285922083747));
#135197=CARTESIAN_POINT('Ctrl Pts',(-240.455116182501,4.63584537696253,
129.156070971893));
#135198=CARTESIAN_POINT('Ctrl Pts',(-240.462876625015,4.58641656882432,
129.028419706467));
#135199=CARTESIAN_POINT('Ctrl Pts',(-240.47064952528,4.53690841317508,128.900563523898));
#135200=CARTESIAN_POINT('Ctrl Pts',(-240.478422425545,4.48210230920935,
128.774914603163));
#135201=CARTESIAN_POINT('Ctrl Pts',(-240.486195325811,4.42224098296653,
128.651927633459));
#135202=CARTESIAN_POINT('Ctrl Pts',(-240.493685661573,4.36455576671341,
128.533411549888));
#135203=CARTESIAN_POINT('Ctrl Pts',(-240.501175997335,4.30217663311262,
128.417367511494));
#135204=CARTESIAN_POINT('Ctrl Pts',(-240.508666333097,4.23535868671833,
128.304176652867));
#135205=CARTESIAN_POINT('Ctrl Pts',(-240.516440667216,4.16600731757869,
128.186694128433));
#135206=CARTESIAN_POINT('Ctrl Pts',(-240.524215001336,4.09165421168538,
128.071913262012));
#135207=CARTESIAN_POINT('Ctrl Pts',(-240.531989335455,4.0125355283831,127.960289293572));
#135208=CARTESIAN_POINT('Ctrl Pts',(-240.539754088402,3.93351435178673,
127.848802891697));
#135209=CARTESIAN_POINT('Ctrl Pts',(-240.547518841349,3.8497395075085,127.740465962586));
#135210=CARTESIAN_POINT('Ctrl Pts',(-240.555283594296,3.76149255441252,
127.635708407935));
#135211=CARTESIAN_POINT('Ctrl Pts',(-240.563040635181,3.67333324943442,
127.531054899964));
#135212=CARTESIAN_POINT('Ctrl Pts',(-240.570797676066,3.58071092519937,
127.429973988751));
#135213=CARTESIAN_POINT('Ctrl Pts',(-240.578554716951,3.48394965575835,
127.332865570955));
#135214=CARTESIAN_POINT('Ctrl Pts',(-240.586305908191,3.38726135474396,
127.235830383374));
#135215=CARTESIAN_POINT('Ctrl Pts',(-240.594057099431,3.28644059594651,
127.142762002304));
#135216=CARTESIAN_POINT('Ctrl Pts',(-240.601808290671,3.18185059925376,
127.054025988959));
#135217=CARTESIAN_POINT('Ctrl Pts',(-240.609556187448,3.07730505609921,
126.965327690786));
#135218=CARTESIAN_POINT('Ctrl Pts',(-240.617304084225,2.96899375885845,
126.880958350395));
#135219=CARTESIAN_POINT('Ctrl Pts',(-240.625051981003,2.85731536747108,
126.801245336524));
#135220=CARTESIAN_POINT('Ctrl Pts',(-240.632798257087,2.74566033679537,
126.721548996897));
#135221=CARTESIAN_POINT('Ctrl Pts',(-240.640544533171,2.63063993092811,
126.646507273436));
#135222=CARTESIAN_POINT('Ctrl Pts',(-240.648290809255,2.5126840225464,126.576405785104));
#135223=CARTESIAN_POINT('Ctrl Pts',(-240.65603714252,2.39472724344113,126.506303779299));
#135224=CARTESIAN_POINT('Ctrl Pts',(-240.663783475786,2.27383525467382,
126.441142281131));
#135225=CARTESIAN_POINT('Ctrl Pts',(-240.671529809051,2.15046455235006,
126.38116208352));
#135226=CARTESIAN_POINT('Ctrl Pts',(-240.679277877054,2.02706622201242,
126.321168453759));
#135227=CARTESIAN_POINT('Ctrl Pts',(-240.687025945057,1.90118842509697,
126.266358604363));
#135228=CARTESIAN_POINT('Ctrl Pts',(-240.69477401306,1.77330938428439,126.21692594336));
#135229=CARTESIAN_POINT('Ctrl Pts',(-240.702530315802,1.64529443210598,
126.167440744736));
#135230=CARTESIAN_POINT('Ctrl Pts',(-240.710286618544,1.51527435247633,
126.123344291902));
#135231=CARTESIAN_POINT('Ctrl Pts',(-240.718042921286,1.38374487710798,
126.084780850513));
#135232=CARTESIAN_POINT('Ctrl Pts',(-240.7258033638,1.25214520049835,126.046196826654));
#135233=CARTESIAN_POINT('Ctrl Pts',(-240.733563806314,1.11903490216574,
126.013151792763));
#135234=CARTESIAN_POINT('Ctrl Pts',(-240.741324248828,0.984920799126915,
125.985739021928));
#135235=CARTESIAN_POINT('Ctrl Pts',(-240.749097149094,0.850591404223804,
125.95828224568));
#135236=CARTESIAN_POINT('Ctrl Pts',(-240.756870049359,0.71525537073989,
125.936475862334));
#135237=CARTESIAN_POINT('Ctrl Pts',(-240.764642949624,0.579426440927723,
125.920361430214));
#135238=CARTESIAN_POINT('Ctrl Pts',(-240.772133285386,0.448535234847394,
125.904832798292));
#135239=CARTESIAN_POINT('Ctrl Pts',(-240.779623621148,0.31718665340473,
125.894589492774));
#135240=CARTESIAN_POINT('Ctrl Pts',(-240.78711395691,0.18583924616756,125.88962289953));
#135241=CARTESIAN_POINT('Ctrl Pts',(-240.794888291029,0.0495117620622287,
125.884467996394));
#135242=CARTESIAN_POINT('Ctrl Pts',(-240.802662625149,-0.087246301531893,
125.884981508192));
#135243=CARTESIAN_POINT('Ctrl Pts',(-240.810436959268,-0.223924288441308,
125.891210815703));
#135244=CARTESIAN_POINT('Ctrl Pts',(-240.818201712215,-0.360433831946748,
125.897432446149));
#135245=CARTESIAN_POINT('Ctrl Pts',(-240.825966465162,-0.496863108315479,
125.909355838806));
#135246=CARTESIAN_POINT('Ctrl Pts',(-240.833731218109,-0.632698239630725,
125.926976482595));
#135247=CARTESIAN_POINT('Ctrl Pts',(-240.841488258994,-0.768398457578609,
125.944579625312));
#135248=CARTESIAN_POINT('Ctrl Pts',(-240.849245299879,-0.903505319617219,
125.967868708342));
#135249=CARTESIAN_POINT('Ctrl Pts',(-240.857002340764,-1.03750721141912,
125.99678723292));
#135250=CARTESIAN_POINT('Ctrl Pts',(-240.864753532004,-1.17140805135184,
126.025683949815));
#135251=CARTESIAN_POINT('Ctrl Pts',(-240.872504723244,-1.30420519899371,
126.060201576293));
#135252=CARTESIAN_POINT('Ctrl Pts',(-240.880255914484,-1.43539476812064,
126.100232119943));
#135253=CARTESIAN_POINT('Ctrl Pts',(-240.888003811261,-1.56652857818128,
126.140245649543));
#135254=CARTESIAN_POINT('Ctrl Pts',(-240.895751708038,-1.69605579552528,
126.18576732213));
#135255=CARTESIAN_POINT('Ctrl Pts',(-240.903499604815,-1.82348551012593,
126.236638684604));
#135256=CARTESIAN_POINT('Ctrl Pts',(-240.911245880899,-1.9508885691777,
126.287499405886));
#135257=CARTESIAN_POINT('Ctrl Pts',(-240.918992156983,-2.07619463531786,
126.343707446363));
#135258=CARTESIAN_POINT('Ctrl Pts',(-240.926738433067,-2.19893105254213,
126.405055526001));
#135259=CARTESIAN_POINT('Ctrl Pts',(-240.934484766333,-2.32166837577857,
126.466404058498));
#135260=CARTESIAN_POINT('Ctrl Pts',(-240.942231099598,-2.44183566253587,
126.532892531069));
#135261=CARTESIAN_POINT('Ctrl Pts',(-240.949977432863,-2.55898357961639,
126.604267035066));
#135262=CARTESIAN_POINT('Ctrl Pts',(-240.957725500866,-2.67615773116052,
126.675657522889));
#135263=CARTESIAN_POINT('Ctrl Pts',(-240.965473568869,-2.79031083372095,
126.751936016075));
#135264=CARTESIAN_POINT('Ctrl Pts',(-240.973221636872,-2.90102167660669,
126.8328047141));
#135265=CARTESIAN_POINT('Ctrl Pts',(-240.980977939614,-3.01185018429387,
126.913759360339));
#135266=CARTESIAN_POINT('Ctrl Pts',(-240.988734242356,-3.11922880789606,
126.999313725819));
#135267=CARTESIAN_POINT('Ctrl Pts',(-240.996490545098,-3.22276821753299,
127.089128716519));
#135268=CARTESIAN_POINT('Ctrl Pts',(-241.004250987612,-3.32636288927064,
127.178991644184));
#135269=CARTESIAN_POINT('Ctrl Pts',(-241.012011430126,-3.42611397981587,
127.273119460062));
#135270=CARTESIAN_POINT('Ctrl Pts',(-241.01977187264,-3.52166906890069,
127.371136181027));
#135271=CARTESIAN_POINT('Ctrl Pts',(-241.027544772906,-3.61737755149723,
127.469310247134));
#135272=CARTESIAN_POINT('Ctrl Pts',(-241.035317673171,-3.7088763112602,
127.571385402169));
#135273=CARTESIAN_POINT('Ctrl Pts',(-241.043090573436,-3.79585269375627,
127.676951883517));
#135274=CARTESIAN_POINT('Ctrl Pts',(-241.050580909199,-3.87966726567068,
127.778680757365));
#135275=CARTESIAN_POINT('Ctrl Pts',(-241.058071244961,-3.95928236534808,
127.883651282082));
#135276=CARTESIAN_POINT('Ctrl Pts',(-241.065561580723,-4.03445738285836,
127.991473010782));
#135277=CARTESIAN_POINT('Ctrl Pts',(-241.07343448358,-4.11347194628202,
128.104801708306));
#135278=CARTESIAN_POINT('Ctrl Pts',(-241.081307386438,-4.18782825269689,
128.221634873634));
#135279=CARTESIAN_POINT('Ctrl Pts',(-241.089180289295,-4.25720427185024,
128.341558382258));
#135280=CARTESIAN_POINT('Ctrl Pts',(-241.09703950209,-4.32645965418085,
128.461273357857));
#135281=CARTESIAN_POINT('Ctrl Pts',(-241.104898714886,-4.39075181436689,
128.584067646285));
#135282=CARTESIAN_POINT('Ctrl Pts',(-241.112757927681,-4.44980102277204,
128.709496917886));
#135283=CARTESIAN_POINT('Ctrl Pts',(-241.120609178014,-4.50879040621353,
128.834799112397));
#135284=CARTESIAN_POINT('Ctrl Pts',(-241.128460428347,-4.56254724686084,
128.96273063843));
#135285=CARTESIAN_POINT('Ctrl Pts',(-241.136311678679,-4.61083661661783,
129.092820738581));
#135286=CARTESIAN_POINT('Ctrl Pts',(-241.144154937712,-4.65907683562503,
129.2227784281));
#135287=CARTESIAN_POINT('Ctrl Pts',(-241.151998196745,-4.70186053741541,
129.354889962274));
#135288=CARTESIAN_POINT('Ctrl Pts',(-241.159841455778,-4.73900024403813,
129.48866317913));
#135289=CARTESIAN_POINT('Ctrl Pts',(-241.161670012953,-4.74765889941888,
129.51985072177));
#135290=CARTESIAN_POINT('Ctrl Pts',(-241.163498570128,-4.7560109927566,
129.551128496559));
#135291=CARTESIAN_POINT('Ctrl Pts',(-241.165327127303,-4.76405452823409,
129.582490119308));
#135292=CARTESIAN_POINT('Ctrl Pts',(-239.415329287988,-4.76405452823416,
129.582490119309));
#135293=CARTESIAN_POINT('Ctrl Pts',(-239.424519392981,-4.80417020735727,
129.738900543369));
#135294=CARTESIAN_POINT('Ctrl Pts',(-239.433709497975,-4.83661958135147,
129.89744575293));
#135295=CARTESIAN_POINT('Ctrl Pts',(-239.442899602968,-4.86120185625379,
130.057433863958));
#135296=CARTESIAN_POINT('Ctrl Pts',(-239.452001625382,-4.88554852229458,
130.215888568626));
#135297=CARTESIAN_POINT('Ctrl Pts',(-239.461103647797,-4.90217810768683,
130.375758571777));
#135298=CARTESIAN_POINT('Ctrl Pts',(-239.470205670211,-4.91094228169329,
130.536351348366));
#135299=CARTESIAN_POINT('Ctrl Pts',(-239.475183968129,-4.91573579540056,
130.624186628143));
#135300=CARTESIAN_POINT('Ctrl Pts',(-239.480162266046,-4.9181772117805,
130.71223777378));
#135301=CARTESIAN_POINT('Ctrl Pts',(-239.485140563964,-4.91824839639984,
130.800388991905));
#135302=CARTESIAN_POINT('',(-239.139859436032,-4.9182499817972,130.803937472346));
#135303=CARTESIAN_POINT('Ctrl Pts',(-239.069767094363,-4.76405452823403,
129.582490119308));
#135304=CARTESIAN_POINT('Ctrl Pts',(-239.077528141177,-4.79812089061503,
129.715314349202));
#135305=CARTESIAN_POINT('Ctrl Pts',(-239.085289187991,-4.82660015141963,
129.849454706652));
#135306=CARTESIAN_POINT('Ctrl Pts',(-239.093050234805,-4.84941749545066,
129.984401461683));
#135307=CARTESIAN_POINT('Ctrl Pts',(-239.100823464149,-4.87227065590867,
130.119560042883));
#135308=CARTESIAN_POINT('Ctrl Pts',(-239.108596693492,-4.88944409361158,
130.255527162905));
#135309=CARTESIAN_POINT('Ctrl Pts',(-239.116369922836,-4.90091491880955,
130.391788174121));
#135310=CARTESIAN_POINT('Ctrl Pts',(-239.122919018622,-4.91057931048617,
130.506590706626));
#135311=CARTESIAN_POINT('Ctrl Pts',(-239.129468114408,-4.91619668330171,
130.621601691157));
#135312=CARTESIAN_POINT('Ctrl Pts',(-239.136017210194,-4.9177820244927,
130.736515042349));
#135313=CARTESIAN_POINT('Ctrl Pts',(-239.137297952128,-4.91809205400046,
130.758987510679));
#135314=CARTESIAN_POINT('Ctrl Pts',(-239.138578694062,-4.91824804811001,
130.781462108982));
#135315=CARTESIAN_POINT('Ctrl Pts',(-239.139859435996,-4.91824998179714,
130.803937471706));
#135316=CARTESIAN_POINT('Ctrl Pts',(-239.139859436033,-4.9182499817972,
130.803937472346));
#135317=CARTESIAN_POINT('Ctrl Pts',(-239.147615006544,-4.91826169127885,
130.940037693392));
#135318=CARTESIAN_POINT('Ctrl Pts',(-239.155370577054,-4.91261977115477,
131.076358722153));
#135319=CARTESIAN_POINT('Ctrl Pts',(-239.163126147566,-4.90129519437534,
131.212390616577));
#135320=CARTESIAN_POINT('Ctrl Pts',(-239.170872168394,-4.88998456191076,
131.348255010564));
#135321=CARTESIAN_POINT('Ctrl Pts',(-239.178618189222,-4.87300522619465,
131.48383059062));
#135322=CARTESIAN_POINT('Ctrl Pts',(-239.18636421005,-4.8503801351783,131.618606039271));
#135323=CARTESIAN_POINT('Ctrl Pts',(-239.194102569871,-4.82777742093952,
131.753248191652));
#135324=CARTESIAN_POINT('Ctrl Pts',(-239.201840929692,-4.79954012706133,
131.887091402182));
#135325=CARTESIAN_POINT('Ctrl Pts',(-239.209579289513,-4.76574307505788,
132.019628491344));
#135326=CARTESIAN_POINT('Ctrl Pts',(-239.217311870164,-4.73197126340409,
132.152066599019));
#135327=CARTESIAN_POINT('Ctrl Pts',(-239.225044450815,-4.69264805427752,
132.283200147361));
#135328=CARTESIAN_POINT('Ctrl Pts',(-239.232777031466,-4.64789944639699,
132.412531565781));
#135329=CARTESIAN_POINT('Ctrl Pts',(-239.240506428028,-4.60316926490614,
132.541809728665));
#135330=CARTESIAN_POINT('Ctrl Pts',(-239.24823582459,-4.55301825560546,
132.669286866611));
#135331=CARTESIAN_POINT('Ctrl Pts',(-239.255965221152,-4.49762236276382,
132.794480248258));
#135332=CARTESIAN_POINT('Ctrl Pts',(-239.263693096776,-4.44223737034809,
132.919648995206));
#135333=CARTESIAN_POINT('Ctrl Pts',(-239.271420972401,-4.38160970598779,
133.042534520364));
#135334=CARTESIAN_POINT('Ctrl Pts',(-239.279148848025,-4.31596341722965,
133.162674176793));
#135335=CARTESIAN_POINT('Ctrl Pts',(-239.286876898036,-4.25031564710143,
133.282816544286));
#135336=CARTESIAN_POINT('Ctrl Pts',(-239.294604948047,-4.17964921561703,
133.400212574749));
#135337=CARTESIAN_POINT('Ctrl Pts',(-239.302332998058,-4.10423387044656,
133.514424712598));
#135338=CARTESIAN_POINT('Ctrl Pts',(-239.310062917552,-4.02880028164126,
133.628664479366));
#135339=CARTESIAN_POINT('Ctrl Pts',(-239.317792837046,-3.94861571002192,
133.739718493164));
#135340=CARTESIAN_POINT('Ctrl Pts',(-239.32552275654,-3.86399266699195,
133.847179003854));
#135341=CARTESIAN_POINT('Ctrl Pts',(-239.333260924453,-3.77927932466312,
133.954754183178));
#135342=CARTESIAN_POINT('Ctrl Pts',(-239.340999092366,-3.69011829490393,
134.058727891459));
#135343=CARTESIAN_POINT('Ctrl Pts',(-239.34873726028,-3.59686206967548,
134.158725880061));
#135344=CARTESIAN_POINT('Ctrl Pts',(-239.356479722365,-3.50355409339292,
134.25877936095));
#135345=CARTESIAN_POINT('Ctrl Pts',(-239.364222184451,-3.40614667385498,
134.354852451133));
#135346=CARTESIAN_POINT('Ctrl Pts',(-239.371964646537,-3.30502767844634,
134.446609250925));
#135347=CARTESIAN_POINT('Ctrl Pts',(-239.379719220947,-3.20375049227857,
134.538509595238));
#135348=CARTESIAN_POINT('Ctrl Pts',(-239.387473795356,-3.09875043182109,
134.626079907394));
#135349=CARTESIAN_POINT('Ctrl Pts',(-239.395228369765,-2.99044740688375,
134.709025439182));
#135350=CARTESIAN_POINT('Ctrl Pts',(-239.401640524512,-2.90089307174618,
134.777611999494));
#135351=CARTESIAN_POINT('Ctrl Pts',(-239.408052679259,-2.80908100330681,
134.843037134247));
#135352=CARTESIAN_POINT('Ctrl Pts',(-239.414464834006,-2.71526171166901,
134.905157722964));
#135353=CARTESIAN_POINT('Ctrl Pts',(-239.422239168125,-2.60151172453313,
134.980475027585));
#135354=CARTESIAN_POINT('Ctrl Pts',(-239.430013502245,-2.48444540631676,
135.05117516048));
#135355=CARTESIAN_POINT('Ctrl Pts',(-239.437787836364,-2.36447424007298,
135.116952023036));
#135356=CARTESIAN_POINT('Ctrl Pts',(-239.445552589311,-2.24465092756914,
135.182647821487));
#135357=CARTESIAN_POINT('Ctrl Pts',(-239.453317342258,-2.12193022963106,
135.243432235941));
#135358=CARTESIAN_POINT('Ctrl Pts',(-239.461082095205,-1.99675337392947,
135.29904181051));
#135359=CARTESIAN_POINT('Ctrl Pts',(-239.46883913609,-1.871700845646,135.354596152864));
#135360=CARTESIAN_POINT('Ctrl Pts',(-239.476596176975,-1.74419736927777,
135.404985725915));
#135361=CARTESIAN_POINT('Ctrl Pts',(-239.48435321786,-1.61470928217404,
135.449992651699));
#135362=CARTESIAN_POINT('Ctrl Pts',(-239.4921044091,-1.4853188430439,135.494965637409));
#135363=CARTESIAN_POINT('Ctrl Pts',(-239.49985560034,-1.35394713989028,
135.534563927399));
#135364=CARTESIAN_POINT('Ctrl Pts',(-239.50760679158,-1.2210806957463,135.568617642221));
#135365=CARTESIAN_POINT('Ctrl Pts',(-239.515354688357,-1.08827072338559,
135.602656883306));
#135366=CARTESIAN_POINT('Ctrl Pts',(-239.523102585134,-0.95396765153832,
135.631156139442));
#135367=CARTESIAN_POINT('Ctrl Pts',(-239.530850481911,-0.81867316942286,
135.653995377439));
#135368=CARTESIAN_POINT('Ctrl Pts',(-239.538596757995,-0.683406987996448,
135.67682983796));
#135369=CARTESIAN_POINT('Ctrl Pts',(-239.546343034079,-0.54715019406188,
135.694006570253));
#135370=CARTESIAN_POINT('Ctrl Pts',(-239.554089310164,-0.410414285615395,
135.705456737483));
#135371=CARTESIAN_POINT('Ctrl Pts',(-239.561835643429,-0.273677367815681,
135.716906989235));
#135372=CARTESIAN_POINT('Ctrl Pts',(-239.569581976694,-0.136461718048383,
135.722630558948));
#135373=CARTESIAN_POINT('Ctrl Pts',(-239.57732830996,0.000716829463151165,
135.722610565327));
#135374=CARTESIAN_POINT('Ctrl Pts',(-239.585076377963,0.137926097159832,
135.722590567229));
#135375=CARTESIAN_POINT('Ctrl Pts',(-239.592824445965,0.275097855176846,
135.716824446403));
#135376=CARTESIAN_POINT('Ctrl Pts',(-239.600572513968,0.411717455877931,
135.705347436465));
#135377=CARTESIAN_POINT('Ctrl Pts',(-239.60832881671,0.54848225751625,135.693858228625));
#135378=CARTESIAN_POINT('Ctrl Pts',(-239.616085119452,0.68469333934966,
135.676646039773));
#135379=CARTESIAN_POINT('Ctrl Pts',(-239.623841422194,0.819841801757023,
135.653797954267));
#135380=CARTESIAN_POINT('Ctrl Pts',(-239.631601864708,0.955062396968015,
135.63093767405));
#135381=CARTESIAN_POINT('Ctrl Pts',(-239.639362307222,1.08921886041209,
135.602435584598));
#135382=CARTESIAN_POINT('Ctrl Pts',(-239.647122749736,1.22181462643886,
135.568429475288));
#135383=CARTESIAN_POINT('Ctrl Pts',(-239.654895650002,1.35462324696057,
135.534368776353));
#135384=CARTESIAN_POINT('Ctrl Pts',(-239.662668550267,1.48586578900997,
135.494786514289));
#135385=CARTESIAN_POINT('Ctrl Pts',(-239.670441450533,1.61506207784371,
135.449870013446));
#135386=CARTESIAN_POINT('Ctrl Pts',(-239.677931786295,1.73956175615639,
135.406586340546));
#135387=CARTESIAN_POINT('Ctrl Pts',(-239.685422122057,1.86216108462354,
135.358349634445));
#135388=CARTESIAN_POINT('Ctrl Pts',(-239.692912457819,1.98245146626512,
135.305368198809));
#135389=CARTESIAN_POINT('Ctrl Pts',(-239.700686791938,2.10730269428409,
135.250377955939));
#135390=CARTESIAN_POINT('Ctrl Pts',(-239.708461126058,2.23006192292105,
135.19010189571));
#135391=CARTESIAN_POINT('Ctrl Pts',(-239.716235460177,2.35024920610005,
135.124720756689));
#135392=CARTESIAN_POINT('Ctrl Pts',(-239.724000213124,2.47028836919398,
135.059420194079));
#135393=CARTESIAN_POINT('Ctrl Pts',(-239.731764966071,2.58776155343375,
134.989027256028));
#135394=CARTESIAN_POINT('Ctrl Pts',(-239.739529719018,2.70220861158442,
134.913770755527));
#135395=CARTESIAN_POINT('Ctrl Pts',(-239.747286759903,2.8165419993032,134.838589000844));
#135396=CARTESIAN_POINT('Ctrl Pts',(-239.755043800788,2.92785491764034,
134.758553510157));
#135397=CARTESIAN_POINT('Ctrl Pts',(-239.762800841673,3.03571199296619,
134.673938857925));
#135398=CARTESIAN_POINT('Ctrl Pts',(-239.770552032913,3.14348773243238,
134.589388014261));
#135399=CARTESIAN_POINT('Ctrl Pts',(-239.778303224153,3.24781250976893,
134.500265122739));
#135400=CARTESIAN_POINT('Ctrl Pts',(-239.786054415393,3.34828042300292,
134.406887684978));
#135401=CARTESIAN_POINT('Ctrl Pts',(-239.79380231217,3.44870563469413,134.313549935118));
#135402=CARTESIAN_POINT('Ctrl Pts',(-239.801550208947,3.54527695689084,
134.215961501187));
#135403=CARTESIAN_POINT('Ctrl Pts',(-239.809298105724,3.63762222699359,
134.114479587661));
#135404=CARTESIAN_POINT('Ctrl Pts',(-239.817044381808,3.72994818045657,
134.013018901964));
#135405=CARTESIAN_POINT('Ctrl Pts',(-239.824790657892,3.81804957718431,
133.907666645603));
#135406=CARTESIAN_POINT('Ctrl Pts',(-239.832536933976,3.90159202563624,
133.798815948338));
#135407=CARTESIAN_POINT('Ctrl Pts',(-239.840283267242,3.98513509077967,
133.689964447563));
#135408=CARTESIAN_POINT('Ctrl Pts',(-239.848029600507,4.06411890245744,
133.5776147645));
#135409=CARTESIAN_POINT('Ctrl Pts',(-239.855775933772,4.13825043696067,
133.462191760339));
#135410=CARTESIAN_POINT('Ctrl Pts',(-239.863524001775,4.21239857270696,
133.346742907997));
#135411=CARTESIAN_POINT('Ctrl Pts',(-239.871272069778,4.28169205776535,
133.22821969392));
#135412=CARTESIAN_POINT('Ctrl Pts',(-239.879020137781,4.3458823555574,133.107074150369));
#135413=CARTESIAN_POINT('Ctrl Pts',(-239.886776440523,4.41014087556173,
132.985799851894));
#135414=CARTESIAN_POINT('Ctrl Pts',(-239.894532743265,4.46928519047763,
132.861898002543));
#135415=CARTESIAN_POINT('Ctrl Pts',(-239.902289046006,4.52311349416601,
132.735843825206));
#135416=CARTESIAN_POINT('Ctrl Pts',(-239.910049488521,4.57697052764095,
132.609722368957));
#135417=CARTESIAN_POINT('Ctrl Pts',(-239.917809931035,4.62550575800948,
132.481446661202));
#135418=CARTESIAN_POINT('Ctrl Pts',(-239.925570373549,4.66856670551333,
132.351508955209));
#135419=CARTESIAN_POINT('Ctrl Pts',(-239.933343273814,4.71169677827276,
132.221362661676));
#135420=CARTESIAN_POINT('Ctrl Pts',(-239.94111617408,4.74933489992523,132.089549414572));
#135421=CARTESIAN_POINT('Ctrl Pts',(-239.948889074345,4.78137912557462,
131.956574451895));
#135422=CARTESIAN_POINT('Ctrl Pts',(-239.956379410107,4.81225846290869,
131.828433464049));
#135423=CARTESIAN_POINT('Ctrl Pts',(-239.96386974587,4.83794348762328,131.699214058919));
#135424=CARTESIAN_POINT('Ctrl Pts',(-239.971360081632,4.85838859484396,
131.569372593936));
#135425=CARTESIAN_POINT('Ctrl Pts',(-239.979134415751,4.87960888451809,
131.434608150351));
#135426=CARTESIAN_POINT('Ctrl Pts',(-239.98690874987,4.89525128957989,131.298746651697));
#135427=CARTESIAN_POINT('Ctrl Pts',(-239.994683083989,4.90520844792763,
131.162289583814));
#135428=CARTESIAN_POINT('Ctrl Pts',(-240.002447836936,4.91515333496764,
131.026000687071));
#135429=CARTESIAN_POINT('Ctrl Pts',(-240.010212589883,4.91942688807697,
130.889118067696));
#135430=CARTESIAN_POINT('Ctrl Pts',(-240.01797734283,4.91797289328593,130.752152539601));
#135431=CARTESIAN_POINT('Ctrl Pts',(-240.025734383715,4.91652034262302,
130.6153230476));
#135432=CARTESIAN_POINT('Ctrl Pts',(-240.033491424601,4.90935156891561,
130.478411199165));
#135433=CARTESIAN_POINT('Ctrl Pts',(-240.041248465485,4.89646224935012,
130.341931700662));
#135434=CARTESIAN_POINT('Ctrl Pts',(-240.048999656726,4.88358264972073,
130.20555512241));
#135435=CARTESIAN_POINT('Ctrl Pts',(-240.056750847966,4.86499112741673,
130.069610632789));
#135436=CARTESIAN_POINT('Ctrl Pts',(-240.064502039206,4.84073540560912,
129.934611346004));
#135437=CARTESIAN_POINT('Ctrl Pts',(-240.072249935983,4.81648999313036,
129.799669437517));
#135438=CARTESIAN_POINT('Ctrl Pts',(-240.07999783276,4.78658523834844,129.665672316841));
#135439=CARTESIAN_POINT('Ctrl Pts',(-240.087745729537,4.75112050453059,
129.533126172655));
#135440=CARTESIAN_POINT('Ctrl Pts',(-240.095492005621,4.71566318917052,
129.400607754264));
#135441=CARTESIAN_POINT('Ctrl Pts',(-240.103238281705,4.67464830909037,
129.269540086101));
#135442=CARTESIAN_POINT('Ctrl Pts',(-240.110984557789,4.62822586869511,
129.140416997475));
#135443=CARTESIAN_POINT('Ctrl Pts',(-240.118730891055,4.58180308562001,
129.011292955692));
#135444=CARTESIAN_POINT('Ctrl Pts',(-240.12647722432,4.52997279484901,128.884113890001));
#135445=CARTESIAN_POINT('Ctrl Pts',(-240.134223557585,4.47293405766117,
128.759355977397));
#135446=CARTESIAN_POINT('Ctrl Pts',(-240.141971625588,4.41588254704354,
128.634570126123));
#135447=CARTESIAN_POINT('Ctrl Pts',(-240.149719693591,4.35362043154904,
128.51220686235));
#135448=CARTESIAN_POINT('Ctrl Pts',(-240.157467761594,4.28639367863097,
128.39271962142));
#135449=CARTESIAN_POINT('Ctrl Pts',(-240.165224064336,4.21909547631998,
128.273105388029));
#135450=CARTESIAN_POINT('Ctrl Pts',(-240.172980367078,4.14682228827045,
128.156373624791));
#135451=CARTESIAN_POINT('Ctrl Pts',(-240.18073666982,4.0698648518084,128.042950986505));
#135452=CARTESIAN_POINT('Ctrl Pts',(-240.188497112334,3.99286634084558,
127.929467811143));
#135453=CARTESIAN_POINT('Ctrl Pts',(-240.196257554848,3.91117883250713,
127.819297593895));
#135454=CARTESIAN_POINT('Ctrl Pts',(-240.204017997362,3.82513405437569,
127.712834695217));
#135455=CARTESIAN_POINT('Ctrl Pts',(-240.211790897628,3.73895114952747,
127.606200892842));
#135456=CARTESIAN_POINT('Ctrl Pts',(-240.219563797893,3.64839725570815,
127.503286595352));
#135457=CARTESIAN_POINT('Ctrl Pts',(-240.227336698158,3.55384234024813,
127.404450665353));
#135458=CARTESIAN_POINT('Ctrl Pts',(-240.23482703392,3.46272473413556,127.309207670363));
#135459=CARTESIAN_POINT('Ctrl Pts',(-240.242317369682,3.36789217217108,
127.217751886806));
#135460=CARTESIAN_POINT('Ctrl Pts',(-240.249807705444,3.26970395023753,
127.130368355693));
#135461=CARTESIAN_POINT('Ctrl Pts',(-240.257582039563,3.16779289202469,
127.039671651438));
#135462=CARTESIAN_POINT('Ctrl Pts',(-240.265356373682,3.06194386743316,
126.95307479442));
#135463=CARTESIAN_POINT('Ctrl Pts',(-240.273130707801,2.952520758862,126.87093917676));
#135464=CARTESIAN_POINT('Ctrl Pts',(-240.280895460749,2.84323250449244,
126.788904783909));
#135465=CARTESIAN_POINT('Ctrl Pts',(-240.288660213696,2.73037923993795,
126.711320923329));
#135466=CARTESIAN_POINT('Ctrl Pts',(-240.296424966643,2.61436034238606,
126.638510996821));
#135467=CARTESIAN_POINT('Ctrl Pts',(-240.304182007528,2.4984566764388,126.565773386159));
#135468=CARTESIAN_POINT('Ctrl Pts',(-240.311939048413,2.37939396350909,
126.497800480172));
#135469=CARTESIAN_POINT('Ctrl Pts',(-240.319696089298,2.25760290405394,
126.434874127129));
#135470=CARTESIAN_POINT('Ctrl Pts',(-240.327447280538,2.13590368818494,
126.371995227339));
#135471=CARTESIAN_POINT('Ctrl Pts',(-240.335198471778,2.01148056699154,
126.314155484325));
#135472=CARTESIAN_POINT('Ctrl Pts',(-240.342949663018,1.88479103352591,
126.261592097991));
#135473=CARTESIAN_POINT('Ctrl Pts',(-240.350697559795,1.75815534649068,
126.209051052499));
#135474=CARTESIAN_POINT('Ctrl Pts',(-240.358445456572,1.62925552344608,
126.161782052856));
#135475=CARTESIAN_POINT('Ctrl Pts',(-240.366193353349,1.49857114353756,
126.119975109278));
#135476=CARTESIAN_POINT('Ctrl Pts',(-240.373939629434,1.36791409998444,
126.078176910812));
#135477=CARTESIAN_POINT('Ctrl Pts',(-240.381685905518,1.23547361420208,
126.041838614877));
#135478=CARTESIAN_POINT('Ctrl Pts',(-240.389432181602,1.10174623982095,
126.011100945324));
#135479=CARTESIAN_POINT('Ctrl Pts',(-240.397178514867,0.968017878294181,
125.980363048873));
#135480=CARTESIAN_POINT('Ctrl Pts',(-240.404924848133,0.833002990242403,
125.955225948881));
#135481=CARTESIAN_POINT('Ctrl Pts',(-240.412671181398,0.697209794341811,
125.935779554754));
#135482=CARTESIAN_POINT('Ctrl Pts',(-240.420419249401,0.561386188497077,
125.916328805742));
#135483=CARTESIAN_POINT('Ctrl Pts',(-240.428167317404,0.424784314916213,
125.902571353904));
#135484=CARTESIAN_POINT('Ctrl Pts',(-240.435915385407,0.287918613010828,
125.894545352734));
#135485=CARTESIAN_POINT('Ctrl Pts',(-240.443671688149,0.150907448608548,
125.886510821434));
#135486=CARTESIAN_POINT('Ctrl Pts',(-240.451427990891,0.0136322866698129,
125.884219932061));
#135487=CARTESIAN_POINT('Ctrl Pts',(-240.459184293633,-0.123390765413529,
125.887658696409));
#135488=CARTESIAN_POINT('Ctrl Pts',(-240.466944736147,-0.260486950825825,
125.891099296129));
#135489=CARTESIAN_POINT('Ctrl Pts',(-240.474705178661,-0.397330368365009,
125.900275616925));
#135490=CARTESIAN_POINT('Ctrl Pts',(-240.482465621175,-0.533409924550205,
125.915121728445));
#135491=CARTESIAN_POINT('Ctrl Pts',(-240.490238521441,-0.669707927719194,
125.929991672262));
#135492=CARTESIAN_POINT('Ctrl Pts',(-240.498011421706,-0.805239232393605,
125.950549536136));
#135493=CARTESIAN_POINT('Ctrl Pts',(-240.505784321971,-0.93950194091927,
125.976678030081));
#135494=CARTESIAN_POINT('Ctrl Pts',(-240.513274657733,-1.06888386180158,
126.001856687456));
#135495=CARTESIAN_POINT('Ctrl Pts',(-240.520764993495,-1.19708751882659,
126.032207922691));
#135496=CARTESIAN_POINT('Ctrl Pts',(-240.528255329257,-1.32367889071797,
126.067583521611));
#135497=CARTESIAN_POINT('Ctrl Pts',(-240.536029663376,-1.45507001295323,
126.104300397116));
#135498=CARTESIAN_POINT('Ctrl Pts',(-240.543803997496,-1.58514038461186,
126.146546462842));
#135499=CARTESIAN_POINT('Ctrl Pts',(-240.551578331615,-1.71338926894211,
126.194210915488));
#135500=CARTESIAN_POINT('Ctrl Pts',(-240.559343084562,-1.84148009798436,
126.241816625955));
#135501=CARTESIAN_POINT('Ctrl Pts',(-240.567107837509,-1.96775354326625,
126.294827301861));
#135502=CARTESIAN_POINT('Ctrl Pts',(-240.574872590456,-2.09172164456772,
126.35308174244));
#135503=CARTESIAN_POINT('Ctrl Pts',(-240.582629631341,-2.21556661900333,
126.411278323886));
#135504=CARTESIAN_POINT('Ctrl Pts',(-240.590386672226,-2.33711045451045,
126.474708140289));
#135505=CARTESIAN_POINT('Ctrl Pts',(-240.598143713111,-2.45588322004057,
126.54316117703));
#135506=CARTESIAN_POINT('Ctrl Pts',(-240.605894904352,-2.57456641810446,
126.611562592804));
#135507=CARTESIAN_POINT('Ctrl Pts',(-240.613646095592,-2.69048236821961,
126.684979494597));
#135508=CARTESIAN_POINT('Ctrl Pts',(-240.621397286832,-2.80318422121785,
126.763155192892));
#135509=CARTESIAN_POINT('Ctrl Pts',(-240.629145183609,-2.91583817292199,
126.841297664429));
#135510=CARTESIAN_POINT('Ctrl Pts',(-240.636893080386,-3.02528042395828,
126.924194687274));
#135511=CARTESIAN_POINT('Ctrl Pts',(-240.644640977164,-3.13109188910893,
127.011545483071));
#135512=CARTESIAN_POINT('Ctrl Pts',(-240.652387253248,-3.23688122078211,
127.098878006964));
#135513=CARTESIAN_POINT('Ctrl Pts',(-240.660133529332,-3.33904097591098,
127.190662201998));
#135514=CARTESIAN_POINT('Ctrl Pts',(-240.667879805416,-3.43718436016796,
127.28655636822));
#135515=CARTESIAN_POINT('Ctrl Pts',(-240.675626138681,-3.53532846889725,
127.382451242311));
#135516=CARTESIAN_POINT('Ctrl Pts',(-240.683372471947,-3.62945586795442,
127.482455874897));
#135517=CARTESIAN_POINT('Ctrl Pts',(-240.691118805212,-3.71921620940167,
127.586191285442));
#135518=CARTESIAN_POINT('Ctrl Pts',(-240.698866873215,-3.80899665205466,
127.689949926813));
#135519=CARTESIAN_POINT('Ctrl Pts',(-240.706614941218,-3.89440783527399,
127.797440713061));
#135520=CARTESIAN_POINT('Ctrl Pts',(-240.714363009221,-3.97513959237725,
127.908251454635));
#135521=CARTESIAN_POINT('Ctrl Pts',(-240.722119311963,-4.05595715215256,
128.019179967183));
#135522=CARTESIAN_POINT('Ctrl Pts',(-240.729875614705,-4.13208512042318,
128.133435167094));
#135523=CARTESIAN_POINT('Ctrl Pts',(-240.737631917447,-4.20325629721131,
128.250575277634));
#135524=CARTESIAN_POINT('Ctrl Pts',(-240.745392359961,-4.2744654601996,
128.367777909378));
#135525=CARTESIAN_POINT('Ctrl Pts',(-240.753152802475,-4.34071237139295,
128.487868177696));
#135526=CARTESIAN_POINT('Ctrl Pts',(-240.76091324499,-4.40177624135282,
128.610380448202));
#135527=CARTESIAN_POINT('Ctrl Pts',(-240.768686145255,-4.46293813645775,
128.733089386281));
#135528=CARTESIAN_POINT('Ctrl Pts',(-240.776459045521,-4.51890020406355,
128.858227738929));
#135529=CARTESIAN_POINT('Ctrl Pts',(-240.784231945786,-4.56948983561737,
128.985309847332));
#135530=CARTESIAN_POINT('Ctrl Pts',(-240.791722281548,-4.61824040663265,
129.107772200984));
#135531=CARTESIAN_POINT('Ctrl Pts',(-240.799212617309,-4.6620022610055,
129.232039152562));
#135532=CARTESIAN_POINT('Ctrl Pts',(-240.806702953071,-4.70066549641594,
129.357665434293));
#135533=CARTESIAN_POINT('Ctrl Pts',(-240.811139036931,-4.72356344919756,
129.432066467644));
#135534=CARTESIAN_POINT('Ctrl Pts',(-240.815575120791,-4.74470148622331,
129.507032902232));
#135535=CARTESIAN_POINT('Ctrl Pts',(-240.820011204651,-4.76405452823406,
129.582490119308));
#135536=CARTESIAN_POINT('Origin',(213.235140564004,0.,130.804360617566));
#135537=CARTESIAN_POINT('',(-242.915000748075,-4.76405452823401,129.582490119308));
#135538=CARTESIAN_POINT('',(-242.570075304501,-4.76405452823394,129.582490119308));
#135539=CARTESIAN_POINT('',(213.235140564004,-4.76405452823405,129.582490119308));
#135540=CARTESIAN_POINT('',(-241.235140564066,-4.91824921781847,130.807134410642));
#135541=CARTESIAN_POINT('Ctrl Pts',(-241.235140564066,-4.91824921781847,
130.807134410642));
#135542=CARTESIAN_POINT('Ctrl Pts',(-241.243741602721,-4.91816318054272,
130.959688243065));
#135543=CARTESIAN_POINT('Ctrl Pts',(-241.252342641376,-4.91097524265387,
131.111987004567));
#135544=CARTESIAN_POINT('Ctrl Pts',(-241.260943680032,-4.89678074903758,
131.26340457881));
#135545=CARTESIAN_POINT('Ctrl Pts',(-241.269594554463,-4.88250401028414,
131.415699490386));
#135546=CARTESIAN_POINT('Ctrl Pts',(-241.278245428894,-4.8611393738467,
131.567102752248));
#135547=CARTESIAN_POINT('Ctrl Pts',(-241.286896303325,-4.83283393080042,
131.716993763909));
#135548=CARTESIAN_POINT('Ctrl Pts',(-241.295573079827,-4.80444373683379,
131.867333572685));
#135549=CARTESIAN_POINT('Ctrl Pts',(-241.304249856328,-4.76907122737263,
132.016151856431));
#135550=CARTESIAN_POINT('Ctrl Pts',(-241.312926632829,-4.7269134761016,
132.162842141897));
#135551=CARTESIAN_POINT('Ctrl Pts',(-241.321635659586,-4.68459903089536,
132.310077652794));
#135552=CARTESIAN_POINT('Ctrl Pts',(-241.330344686343,-4.63544892768495,
132.455169116496));
#135553=CARTESIAN_POINT('Ctrl Pts',(-241.3390537131,-4.57970963792587,132.597526168983));
#135554=CARTESIAN_POINT('Ctrl Pts',(-241.340705543579,-4.56913763484539,
132.624526857437));
#135555=CARTESIAN_POINT('Ctrl Pts',(-241.342357374058,-4.55832872367434,
132.651429248468));
#135556=CARTESIAN_POINT('Ctrl Pts',(-241.344009204537,-4.54728477123908,
132.67822941547));
#135557=CARTESIAN_POINT('Ctrl Pts',(-241.351783538656,-4.49530644941974,
132.804364303626));
#135558=CARTESIAN_POINT('Ctrl Pts',(-241.359557872775,-4.43799363020899,
132.928534639887));
#135559=CARTESIAN_POINT('Ctrl Pts',(-241.367332206894,-4.37551548274368,
133.050256279161));
#135560=CARTESIAN_POINT('Ctrl Pts',(-241.375096959842,-4.31311433401129,
133.171827907393));
#135561=CARTESIAN_POINT('Ctrl Pts',(-241.382861712789,-4.24556069989832,
133.290956498679));
#135562=CARTESIAN_POINT('Ctrl Pts',(-241.390626465736,-4.17307228523948,
133.407176547413));
#135563=CARTESIAN_POINT('Ctrl Pts',(-241.398383506621,-4.10065586709599,
133.523281164757));
#135564=CARTESIAN_POINT('Ctrl Pts',(-241.406140547506,-4.0233146277682,
133.63648265882));
#135565=CARTESIAN_POINT('Ctrl Pts',(-241.413897588391,-3.94131261487676,
133.74633919232));
#135566=CARTESIAN_POINT('Ctrl Pts',(-241.421648779632,-3.85937244034102,
133.856112882154));
#135567=CARTESIAN_POINT('Ctrl Pts',(-241.429399970872,-3.77277872100946,
133.962546320192));
#135568=CARTESIAN_POINT('Ctrl Pts',(-241.437151162112,-3.6818391265378,
134.065226102187));
#135569=CARTESIAN_POINT('Ctrl Pts',(-241.444899058889,-3.5909381838198,
134.167862242536));
#135570=CARTESIAN_POINT('Ctrl Pts',(-241.452646955666,-3.49569529840085,
134.266747607913));
#135571=CARTESIAN_POINT('Ctrl Pts',(-241.460394852444,-3.39645864101536,
134.361501570968));
#135572=CARTESIAN_POINT('Ctrl Pts',(-241.468141128528,-3.29724274179929,
134.456235713538));
#135573=CARTESIAN_POINT('Ctrl Pts',(-241.475887404612,-3.19403501488272,
134.546839902905));
#135574=CARTESIAN_POINT('Ctrl Pts',(-241.483633680696,-3.08722045233845,
134.632970409796));
#135575=CARTESIAN_POINT('Ctrl Pts',(-241.491380013962,-2.9804051013135,
134.719101552484));
#135576=CARTESIAN_POINT('Ctrl Pts',(-241.499126347227,-2.86998316587963,
134.800758701387));
#135577=CARTESIAN_POINT('Ctrl Pts',(-241.506872680492,-2.7563723531155,
134.877638721683));
#135578=CARTESIAN_POINT('Ctrl Pts',(-241.514620748495,-2.64273609799741,
134.954535958727));
#135579=CARTESIAN_POINT('Ctrl Pts',(-241.522368816498,-2.52590986825316,
135.026653719308));
#135580=CARTESIAN_POINT('Ctrl Pts',(-241.530116884501,-2.40633960177869,
135.09373269089));
#135581=CARTESIAN_POINT('Ctrl Pts',(-241.537873187243,-2.28664225460227,
135.160882954802));
#135582=CARTESIAN_POINT('Ctrl Pts',(-241.545629489985,-2.16419538640035,
135.222983540365));
#135583=CARTESIAN_POINT('Ctrl Pts',(-241.553385792727,-2.03946924041631,
135.279821295518));
#135584=CARTESIAN_POINT('Ctrl Pts',(-241.561146235242,-1.91467652433272,
135.336689386692));
#135585=CARTESIAN_POINT('Ctrl Pts',(-241.568906677756,-1.78760246851266,
135.388288903404));
#135586=CARTESIAN_POINT('Ctrl Pts',(-241.57666712027,-1.65873552537455,
135.434455597084));
#135587=CARTESIAN_POINT('Ctrl Pts',(-241.584440020535,-1.52966171357904,
135.48069640164));
#135588=CARTESIAN_POINT('Ctrl Pts',(-241.592212920801,-1.39878963657093,
135.521486838924));
#135589=CARTESIAN_POINT('Ctrl Pts',(-241.599985821066,-1.26662194045584,
135.556712869078));
#135590=CARTESIAN_POINT('Ctrl Pts',(-241.607476156827,-1.13925887302456,
135.590658344303));
#135591=CARTESIAN_POINT('Ctrl Pts',(-241.614966492588,-1.01069304968676,
135.619436881785));
#135592=CARTESIAN_POINT('Ctrl Pts',(-241.622456828349,-0.881379602062333,
135.642991938463));
#135593=CARTESIAN_POINT('Ctrl Pts',(-241.630231162468,-0.747163195748146,
135.667440092278));
#135594=CARTESIAN_POINT('Ctrl Pts',(-241.638005496587,-0.611716196440621,
135.686338294071));
#135595=CARTESIAN_POINT('Ctrl Pts',(-241.645779830706,-0.475537369166859,
135.699567178379));
#135596=CARTESIAN_POINT('Ctrl Pts',(-241.653544583653,-0.339526370127431,
135.71277975927));
#135597=CARTESIAN_POINT('Ctrl Pts',(-241.6613093366,-0.202785723056727,
135.72033688714));
#135598=CARTESIAN_POINT('Ctrl Pts',(-241.669074089547,-0.0658247457847857,
135.722170106082));
#135599=CARTESIAN_POINT('Ctrl Pts',(-241.676831130432,0.0710001999140895,
135.724001504246));
#135600=CARTESIAN_POINT('Ctrl Pts',(-241.684588171317,0.20804465192206,
135.720120301824));
#135601=CARTESIAN_POINT('Ctrl Pts',(-241.692345212202,0.344794155831017,
135.710509825713));
#135602=CARTESIAN_POINT('Ctrl Pts',(-241.700096403443,0.481440535875133,
135.700906596937));
#135603=CARTESIAN_POINT('Ctrl Pts',(-241.707847594683,0.617792022113812,
135.685582721444));
#135604=CARTESIAN_POINT('Ctrl Pts',(-241.715598785923,0.753334502882079,
135.664573595334));
#135605=CARTESIAN_POINT('Ctrl Pts',(-241.7233466827,0.888819374480489,135.643573398664));
#135606=CARTESIAN_POINT('Ctrl Pts',(-241.731094579477,1.02349553895492,
135.616892817139));
#135607=CARTESIAN_POINT('Ctrl Pts',(-241.738842476254,1.15685456895081,
135.584619038279));
#135608=CARTESIAN_POINT('Ctrl Pts',(-241.746588752338,1.2901857031125,135.552352010398));
#135609=CARTESIAN_POINT('Ctrl Pts',(-241.754335028422,1.42219987105723,
135.514494204234));
#135610=CARTESIAN_POINT('Ctrl Pts',(-241.762081304506,1.55239978599228,
135.47118373045));
#135611=CARTESIAN_POINT('Ctrl Pts',(-241.769827637772,1.68260066203335,
135.427872936959));
#135612=CARTESIAN_POINT('Ctrl Pts',(-241.777573971037,1.8109868873626,135.379109518937));
#135613=CARTESIAN_POINT('Ctrl Pts',(-241.785320304303,1.93707764518968,
135.325081053404));
#135614=CARTESIAN_POINT('Ctrl Pts',(-241.793068372306,2.06319664016754,
135.271040488571));
#135615=CARTESIAN_POINT('Ctrl Pts',(-241.800816440309,2.18701878543954,
135.211732683966));
#135616=CARTESIAN_POINT('Ctrl Pts',(-241.808564508312,2.30808487370135,
135.147392655013));
#135617=CARTESIAN_POINT('Ctrl Pts',(-241.816320811053,2.42927963244263,
135.082984244711));
#135618=CARTESIAN_POINT('Ctrl Pts',(-241.824077113795,2.5477121370507,135.013533110008));
#135619=CARTESIAN_POINT('Ctrl Pts',(-241.831833416537,2.66294887869895,
134.939319665965));
#135620=CARTESIAN_POINT('Ctrl Pts',(-241.839593859051,2.77824712566594,
134.865066611973));
#135621=CARTESIAN_POINT('Ctrl Pts',(-241.847354301566,2.89034589157634,
134.78604640906));
#135622=CARTESIAN_POINT('Ctrl Pts',(-241.85511474408,2.998842968994,134.702581225717));
#135623=CARTESIAN_POINT('Ctrl Pts',(-241.862887644345,3.10751421555226,
134.618982056652));
#135624=CARTESIAN_POINT('Ctrl Pts',(-241.87066054461,3.21257192003518,134.530923899492));
#135625=CARTESIAN_POINT('Ctrl Pts',(-241.878433444876,3.31364844498309,
134.438768003311));
#135626=CARTESIAN_POINT('Ctrl Pts',(-241.885923780638,3.41105058365493,
134.349962206082));
#135627=CARTESIAN_POINT('Ctrl Pts',(-241.8934141164,3.50475575021393,134.257351640184));
#135628=CARTESIAN_POINT('Ctrl Pts',(-241.900904452163,3.5944703636233,134.161288657833));
#135629=CARTESIAN_POINT('Ctrl Pts',(-241.908678786282,3.68758653386628,
134.061583418312));
#135630=CARTESIAN_POINT('Ctrl Pts',(-241.916453120401,3.7766985378616,133.957842961419));
#135631=CARTESIAN_POINT('Ctrl Pts',(-241.92422745452,3.86143635538579,133.850422392351));
#135632=CARTESIAN_POINT('Ctrl Pts',(-241.931992207467,3.94606974112289,
133.743134209534));
#135633=CARTESIAN_POINT('Ctrl Pts',(-241.939756960414,4.02633942664666,
133.632175242664));
#135634=CARTESIAN_POINT('Ctrl Pts',(-241.947521713361,4.10191251933598,
133.517936993166));
#135635=CARTESIAN_POINT('Ctrl Pts',(-241.955278754246,4.17741055176445,
133.403812206708));
#135636=CARTESIAN_POINT('Ctrl Pts',(-241.963035795131,4.24822106005234,
133.28641494322));
#135637=CARTESIAN_POINT('Ctrl Pts',(-241.970792836016,4.31405194147264,
133.166169015548));
#135638=CARTESIAN_POINT('Ctrl Pts',(-241.978544027256,4.37983317931309,
133.046013766265));
#135639=CARTESIAN_POINT('Ctrl Pts',(-241.986295218496,4.4406420777478,132.923014470207));
#135640=CARTESIAN_POINT('Ctrl Pts',(-241.994046409736,4.49623052660688,
132.797622796535));
#135641=CARTESIAN_POINT('Ctrl Pts',(-242.001794306513,4.55179534889241,
132.67228441767));
#135642=CARTESIAN_POINT('Ctrl Pts',(-242.00954220329,4.6021439765685,132.544556040246));
#135643=CARTESIAN_POINT('Ctrl Pts',(-242.017290100067,4.64707494556122,
132.414912545582));
#135644=CARTESIAN_POINT('Ctrl Pts',(-242.025036376152,4.69199651596382,
132.285296169543));
#135645=CARTESIAN_POINT('Ctrl Pts',(-242.032782652236,4.73150255384806,
132.153765842255));
#135646=CARTESIAN_POINT('Ctrl Pts',(-242.04052892832,4.76544045997002,132.02081459737));
#135647=CARTESIAN_POINT('Ctrl Pts',(-242.048275261585,4.79937861661385,
131.887862371069));
#135648=CARTESIAN_POINT('Ctrl Pts',(-242.056021594851,4.82774846277871,
131.753489585059));
#135649=CARTESIAN_POINT('Ctrl Pts',(-242.063767928116,4.85044791910369,
131.618202154084));
#135650=CARTESIAN_POINT('Ctrl Pts',(-242.071515996119,4.8731524588145,131.482884426428));
#135651=CARTESIAN_POINT('Ctrl Pts',(-242.079264064122,4.8901840171598,131.346652031722));
#135652=CARTESIAN_POINT('Ctrl Pts',(-242.087012132125,4.90149210650604,
131.210018345656));
#135653=CARTESIAN_POINT('Ctrl Pts',(-242.094768434866,4.91281221422421,
131.073239443682));
#135654=CARTESIAN_POINT('Ctrl Pts',(-242.102524737608,4.9183966692553,130.936058788627));
#135655=CARTESIAN_POINT('Ctrl Pts',(-242.11028104035,4.91824707062302,130.798992674935));
#135656=CARTESIAN_POINT('Ctrl Pts',(-242.118041482864,4.91809739214544,
130.661853404931));
#135657=CARTESIAN_POINT('Ctrl Pts',(-242.125801925378,4.9122075786059,130.524829188518));
#135658=CARTESIAN_POINT('Ctrl Pts',(-242.133562367893,4.90063127653539,
130.388432554143));
#135659=CARTESIAN_POINT('Ctrl Pts',(-242.141335268158,4.8890363911571,130.251816963781));
#135660=CARTESIAN_POINT('Ctrl Pts',(-242.149108168423,4.87173682505142,
130.115831356725));
#135661=CARTESIAN_POINT('Ctrl Pts',(-242.156881068689,4.84883779026997,
129.980980300732));
#135662=CARTESIAN_POINT('Ctrl Pts',(-242.164371404451,4.82677119308153,
129.851031420291));
#135663=CARTESIAN_POINT('Ctrl Pts',(-242.171861740213,4.79950523252502,
129.72213633679));
#135664=CARTESIAN_POINT('Ctrl Pts',(-242.179352075975,4.76717766477755,
129.594732503249));
#135665=CARTESIAN_POINT('Ctrl Pts',(-242.187126410094,4.73362438747381,
129.462498114639));
#135666=CARTESIAN_POINT('Ctrl Pts',(-242.194900744213,4.69451181784857,
129.331451410942));
#135667=CARTESIAN_POINT('Ctrl Pts',(-242.202675078333,4.64993871099088,
129.202095643684));
#135668=CARTESIAN_POINT('Ctrl Pts',(-242.21043983128,4.6054205365039,129.072899295849));
#135669=CARTESIAN_POINT('Ctrl Pts',(-242.218204584227,4.55545534087641,
128.945390104145));
#135670=CARTESIAN_POINT('Ctrl Pts',(-242.225969337174,4.50019256875227,
128.820059756646));
#135671=CARTESIAN_POINT('Ctrl Pts',(-242.233726378059,4.44498468439248,
128.694853889015));
#135672=CARTESIAN_POINT('Ctrl Pts',(-242.241483418944,4.38448985112935,
128.571822914432));
#135673=CARTESIAN_POINT('Ctrl Pts',(-242.249240459829,4.31890674605306,
128.451441668389));
#135674=CARTESIAN_POINT('Ctrl Pts',(-242.256991651069,4.25337309770639,
128.331151202779));
#135675=CARTESIAN_POINT('Ctrl Pts',(-242.264742842309,4.18275900135524,
128.213506830384));
#135676=CARTESIAN_POINT('Ctrl Pts',(-242.272494033549,4.10731034945009,
128.098961431531));
#135677=CARTESIAN_POINT('Ctrl Pts',(-242.280241930326,4.03189376523455,
127.984464717527));
#135678=CARTESIAN_POINT('Ctrl Pts',(-242.287989827104,3.95164692694489,
127.87306468318));
#135679=CARTESIAN_POINT('Ctrl Pts',(-242.295737723881,3.86686046942969,
127.76518751087));
#135680=CARTESIAN_POINT('Ctrl Pts',(-242.303483999965,3.78209174741384,
127.65733290414));
#135681=CARTESIAN_POINT('Ctrl Pts',(-242.311230276049,3.69278553639915,
127.553000000893));
#135682=CARTESIAN_POINT('Ctrl Pts',(-242.318976552133,3.59927415594075,
127.452583683927));
#135683=CARTESIAN_POINT('Ctrl Pts',(-242.326722885398,3.50576208520245,
127.352166625709));
#135684=CARTESIAN_POINT('Ctrl Pts',(-242.334469218664,3.40804504952111,
127.255666497579));
#135685=CARTESIAN_POINT('Ctrl Pts',(-242.342215551929,3.30649351291106,
127.163442641069));
#135686=CARTESIAN_POINT('Ctrl Pts',(-242.349963619932,3.20491923453835,
127.071198131666));
#135687=CARTESIAN_POINT('Ctrl Pts',(-242.357711687935,3.09950903587483,
126.983232062272));
#135688=CARTESIAN_POINT('Ctrl Pts',(-242.365459755938,2.99066754462646,
126.899864401661));
#135689=CARTESIAN_POINT('Ctrl Pts',(-242.37321605868,2.88171037534611,126.816408136908));
#135690=CARTESIAN_POINT('Ctrl Pts',(-242.380972361422,2.76931493944201,
126.737560281849));
#135691=CARTESIAN_POINT('Ctrl Pts',(-242.388728664163,2.65391647436352,
126.663598560939));
#135692=CARTESIAN_POINT('Ctrl Pts',(-242.396489106678,2.53845641764963,
126.589597364431));
#135693=CARTESIAN_POINT('Ctrl Pts',(-242.404249549192,2.41999047556914,
126.520487695397));
#135694=CARTESIAN_POINT('Ctrl Pts',(-242.412009991706,2.298978850079,126.456501453634));
#135695=CARTESIAN_POINT('Ctrl Pts',(-242.419782891971,2.17777296598471,
126.392412495475));
#135696=CARTESIAN_POINT('Ctrl Pts',(-242.427555792237,2.05401358541031,
126.333463568142));
#135697=CARTESIAN_POINT('Ctrl Pts',(-242.435328692502,1.92818208518315,
126.279838884954));
#135698=CARTESIAN_POINT('Ctrl Pts',(-242.442819028264,1.80692487694069,
126.228163594072));
#135699=CARTESIAN_POINT('Ctrl Pts',(-242.450309364026,1.68374387500729,
126.181432277832));
#135700=CARTESIAN_POINT('Ctrl Pts',(-242.457799699788,1.55908158157693,
126.139765492104));
#135701=CARTESIAN_POINT('Ctrl Pts',(-242.465574033907,1.42969267939995,
126.096518897529));
#135702=CARTESIAN_POINT('Ctrl Pts',(-242.473348368026,1.29829807688462,
126.058591465739));
#135703=CARTESIAN_POINT('Ctrl Pts',(-242.481122702145,1.1653745533301,126.026172131021));
#135704=CARTESIAN_POINT('Ctrl Pts',(-242.488887455092,1.03261484613901,
125.993792750236));
#135705=CARTESIAN_POINT('Ctrl Pts',(-242.496652208039,0.8983303432066,125.966908051704));
#135706=CARTESIAN_POINT('Ctrl Pts',(-242.504416960986,0.763015494114828,
125.945658072828));
#135707=CARTESIAN_POINT('Ctrl Pts',(-242.512174001871,0.627835041638779,
125.924429199731));
#135708=CARTESIAN_POINT('Ctrl Pts',(-242.519931042756,0.491626663256989,
125.908823969297));
#135709=CARTESIAN_POINT('Ctrl Pts',(-242.527688083641,0.354897241336885,
125.898931889046));
#135710=CARTESIAN_POINT('Ctrl Pts',(-242.535439274881,0.218270928137265,
125.889047268489));
#135711=CARTESIAN_POINT('Ctrl Pts',(-242.543190466121,0.0811247418568937,
125.884867250741));
#135712=CARTESIAN_POINT('Ctrl Pts',(-242.550941657362,-0.0560273855828691,
125.886429752399));
#135713=CARTESIAN_POINT('Ctrl Pts',(-242.558689554139,-0.19312121970963,
125.887991589951));
#135714=CARTESIAN_POINT('Ctrl Pts',(-242.566437450916,-0.330220599852082,
125.895291088051));
#135715=CARTESIAN_POINT('Ctrl Pts',(-242.574185347693,-0.466809871466674,
125.908314089356));
#135716=CARTESIAN_POINT('Ctrl Pts',(-242.581931623777,-0.603370571550168,
125.921334366529));
#135717=CARTESIAN_POINT('Ctrl Pts',(-242.589677899861,-0.739420986391715,
125.940075728461));
#135718=CARTESIAN_POINT('Ctrl Pts',(-242.597424175945,-0.87444926307359,
125.964472029095));
#135719=CARTESIAN_POINT('Ctrl Pts',(-242.60517050921,-1.00947853650371,
125.988868509817));
#135720=CARTESIAN_POINT('Ctrl Pts',(-242.612916842475,-1.14348527198223,
126.018919943024));
#135721=CARTESIAN_POINT('Ctrl Pts',(-242.620663175741,-1.27596690045057,
126.054508879727));
#135722=CARTESIAN_POINT('Ctrl Pts',(-242.628411243744,-1.40847819726086,
126.090105786325));
#135723=CARTESIAN_POINT('Ctrl Pts',(-242.636159311747,-1.53946332993511,
126.131242562633));
#135724=CARTESIAN_POINT('Ctrl Pts',(-242.64390737975,-1.66843438852243,
126.177751734843));
#135725=CARTESIAN_POINT('Ctrl Pts',(-242.651663682491,-1.79754251908576,
126.224310337553));
#135726=CARTESIAN_POINT('Ctrl Pts',(-242.659419985233,-1.92463193115093,
126.276252609358));
#135727=CARTESIAN_POINT('Ctrl Pts',(-242.667176287975,-2.04923371079638,
126.333362489515));
#135728=CARTESIAN_POINT('Ctrl Pts',(-242.674936730489,-2.17390199416364,
126.390502850935));
#135729=CARTESIAN_POINT('Ctrl Pts',(-242.682697173003,-2.29607965139587,
126.452816138926));
#135730=CARTESIAN_POINT('Ctrl Pts',(-242.690457615517,-2.4153228282265,
126.520040520054));
#135731=CARTESIAN_POINT('Ctrl Pts',(-242.698230515783,-2.53475742479017,
126.587372815726));
#135732=CARTESIAN_POINT('Ctrl Pts',(-242.706003416048,-2.65124779506669,
126.659631752519));
#135733=CARTESIAN_POINT('Ctrl Pts',(-242.713776316314,-2.76437875924074,
126.736511906274));
#135734=CARTESIAN_POINT('Ctrl Pts',(-242.721266652076,-2.87339712791043,
126.810597272793));
#135735=CARTESIAN_POINT('Ctrl Pts',(-242.728756987838,-2.9792958481746,
126.888973520485));
#135736=CARTESIAN_POINT('Ctrl Pts',(-242.7362473236,-3.0817343097212,126.971333523116));
#135737=CARTESIAN_POINT('Ctrl Pts',(-242.743919292931,-3.18665680721284,
127.055690678026));
#135738=CARTESIAN_POINT('Ctrl Pts',(-242.751591262261,-3.28830002056774,
127.14450971462));
#135739=CARTESIAN_POINT('Ctrl Pts',(-242.759263231591,-3.3862531830133,
127.237503115081));
#135740=CARTESIAN_POINT('Ctrl Pts',(-242.766926418694,-3.48409421689378,
127.330390064497));
#135741=CARTESIAN_POINT('Ctrl Pts',(-242.774589605797,-3.57825330852022,
127.427441605249));
#135742=CARTESIAN_POINT('Ctrl Pts',(-242.7822527929,-3.66835065220018,127.528328481734));
#135743=CARTESIAN_POINT('Ctrl Pts',(-242.789908971473,-3.75836559544404,
127.629123089988));
#135744=CARTESIAN_POINT('Ctrl Pts',(-242.797565150046,-3.84432591104526,
127.733745761908));
#135745=CARTESIAN_POINT('Ctrl Pts',(-242.805221328619,-3.92588715360147,
127.841829078546));
#135746=CARTESIAN_POINT('Ctrl Pts',(-242.812872265948,-4.00739256119842,
127.949838403821));
#135747=CARTESIAN_POINT('Ctrl Pts',(-242.820523203276,-4.08450464423534,
128.061303342346));
#135748=CARTESIAN_POINT('Ctrl Pts',(-242.828174140605,-4.15691829166909,
128.175822358593));
#135749=CARTESIAN_POINT('Ctrl Pts',(-242.83582247977,-4.22930734832785,
128.290302485604));
#135750=CARTESIAN_POINT('Ctrl Pts',(-242.843470818935,-4.29700092391433,
128.407834291233));
#135751=CARTESIAN_POINT('Ctrl Pts',(-242.8511191581,-4.35973665121918,128.527986440389));
#135752=CARTESIAN_POINT('Ctrl Pts',(-242.858765799848,-4.42245845540937,
128.648111923845));
#135753=CARTESIAN_POINT('Ctrl Pts',(-242.866412441596,-4.48022441733024,
128.770856236093));
#135754=CARTESIAN_POINT('Ctrl Pts',(-242.874059083344,-4.53281799721013,
128.895763209345));
#135755=CARTESIAN_POINT('Ctrl Pts',(-242.881708240402,-4.58542887738673,
129.020711269887));
#135756=CARTESIAN_POINT('Ctrl Pts',(-242.88935739746,-4.63286381874236,
129.147823042512));
#135757=CARTESIAN_POINT('Ctrl Pts',(-242.897006554518,-4.6749543734349,
129.276622201213));
#135758=CARTESIAN_POINT('Ctrl Pts',(-242.903004619037,-4.70795956090417,
129.377619691263));
#135759=CARTESIAN_POINT('Ctrl Pts',(-242.909002683556,-4.73767949876136,
129.479654279691));
#135760=CARTESIAN_POINT('Ctrl Pts',(-242.915000748075,-4.76405452823401,
129.582490119308));
#135761=CARTESIAN_POINT('Ctrl Pts',(-241.165327127303,-4.76405452823409,
129.582490119308));
#135762=CARTESIAN_POINT('Ctrl Pts',(-241.173163504015,-4.79852551714263,
129.716891981893));
#135763=CARTESIAN_POINT('Ctrl Pts',(-241.180999880728,-4.82732559214713,
129.852834902042));
#135764=CARTESIAN_POINT('Ctrl Pts',(-241.18883625744,-4.85032839536548,
129.989807046822));
#135765=CARTESIAN_POINT('Ctrl Pts',(-241.196670112391,-4.87332379623385,
130.126735113681));
#135766=CARTESIAN_POINT('Ctrl Pts',(-241.204503967341,-4.89052557304048,
130.264691373754));
#135767=CARTESIAN_POINT('Ctrl Pts',(-241.212337822291,-4.90185841905944,
130.403153561302));
#135768=CARTESIAN_POINT('Ctrl Pts',(-241.219938736198,-4.91285428092652,
130.537498551567));
#135769=CARTESIAN_POINT('Ctrl Pts',(-241.227539650106,-4.91832525069541,
130.672319465504));
#135770=CARTESIAN_POINT('Ctrl Pts',(-241.235140564014,-4.91824921781899,
130.807134409724));
#135771=CARTESIAN_POINT('',(-240.889859435956,-4.91824814758057,130.800091973715));
#135772=CARTESIAN_POINT('Ctrl Pts',(-240.820011204651,-4.76405452823406,
129.582490119308));
#135773=CARTESIAN_POINT('Ctrl Pts',(-240.829478829728,-4.80535837902586,
129.743533206672));
#135774=CARTESIAN_POINT('Ctrl Pts',(-240.838946454805,-4.83852861212123,
129.906813185049));
#135775=CARTESIAN_POINT('Ctrl Pts',(-240.848414079882,-4.86335571906152,
130.071589021247));
#135776=CARTESIAN_POINT('Ctrl Pts',(-240.857763979629,-4.8878741129549,
130.234315949751));
#135777=CARTESIAN_POINT('Ctrl Pts',(-240.867113879375,-4.90425553807115,
130.398501772666));
#135778=CARTESIAN_POINT('Ctrl Pts',(-240.876463779121,-4.91234431771532,
130.563411729397));
#135779=CARTESIAN_POINT('Ctrl Pts',(-240.880928998066,-4.91620726524315,
130.642167553846));
#135780=CARTESIAN_POINT('Ctrl Pts',(-240.885394217011,-4.91817957867735,
130.721088221468));
#135781=CARTESIAN_POINT('Ctrl Pts',(-240.889859435956,-4.91824814758057,
130.800091973715));
#135782=CARTESIAN_POINT('Ctrl Pts',(-240.889859435996,-4.91824814758118,
130.800091974427));
#135783=CARTESIAN_POINT('Ctrl Pts',(-240.897561156383,-4.91836641690644,
130.936359605821));
#135784=CARTESIAN_POINT('Ctrl Pts',(-240.90526287677,-4.91281717295408,
131.072729329552));
#135785=CARTESIAN_POINT('Ctrl Pts',(-240.912964597156,-4.90160180444283,
131.208690697059));
#135786=CARTESIAN_POINT('Ctrl Pts',(-240.920664069363,-4.89038970976659,
131.344612376607));
#135787=CARTESIAN_POINT('Ctrl Pts',(-240.928363541571,-4.87351480886842,
131.480125542569));
#135788=CARTESIAN_POINT('Ctrl Pts',(-240.936063013778,-4.85103055027703,
131.614722057159));
#135789=CARTESIAN_POINT('Ctrl Pts',(-240.943761625337,-4.82854880497805,
131.749303526538));
#135790=CARTESIAN_POINT('Ctrl Pts',(-240.951460236897,-4.80045901402057,
131.882968157685));
#135791=CARTESIAN_POINT('Ctrl Pts',(-240.959158848456,-4.76686614985544,
132.015215758308));
#135792=CARTESIAN_POINT('Ctrl Pts',(-240.966858316943,-4.73326954648901,
132.147478079332));
#135793=CARTESIAN_POINT('Ctrl Pts',(-240.97455778543,-4.69416874887371,
132.27832267213));
#135794=CARTESIAN_POINT('Ctrl Pts',(-240.982257253918,-4.6497191058681,
132.40726276649));
#135795=CARTESIAN_POINT('Ctrl Pts',(-240.989959297187,-4.60525459843776,
132.536245979764));
#135796=CARTESIAN_POINT('Ctrl Pts',(-240.997661340457,-4.55543781628651,
132.663323053388));
#135797=CARTESIAN_POINT('Ctrl Pts',(-241.005363383727,-4.50047274065077,
132.78802595556));
#135798=CARTESIAN_POINT('Ctrl Pts',(-241.013074120844,-4.44544562200206,
132.912869618819));
#135799=CARTESIAN_POINT('Ctrl Pts',(-241.020784857961,-4.38525876797335,
133.03533339777));
#135800=CARTESIAN_POINT('Ctrl Pts',(-241.028495595079,-4.32016291498794,
133.15497233592));
#135801=CARTESIAN_POINT('Ctrl Pts',(-241.036211295946,-4.25502515685459,
133.274688291071));
#135802=CARTESIAN_POINT('Ctrl Pts',(-241.043926996814,-4.1849723098661,
133.391575445388));
#135803=CARTESIAN_POINT('Ctrl Pts',(-241.051642697681,-4.1102985330867,
133.505217709566));
#135804=CARTESIAN_POINT('Ctrl Pts',(-241.05936986681,-4.03551376465894,
133.61902888635));
#135805=CARTESIAN_POINT('Ctrl Pts',(-241.067097035939,-3.95609458477475,
133.72958522377));
#135806=CARTESIAN_POINT('Ctrl Pts',(-241.074824205067,-3.87237578563073,
133.83650323251));
#135807=CARTESIAN_POINT('Ctrl Pts',(-241.078266329006,-3.83508263495013,
133.884130640586));
#135808=CARTESIAN_POINT('Ctrl Pts',(-241.081708452945,-3.79693679776537,
133.931036570226));
#135809=CARTESIAN_POINT('Ctrl Pts',(-241.085150576883,-3.75797015117827,
133.977189545408));
#135810=CARTESIAN_POINT('Ctrl Pts',(-241.092924911002,-3.6699606153614,
134.081430024848));
#135811=CARTESIAN_POINT('Ctrl Pts',(-241.100699245122,-3.57747117897063,
134.182170958972));
#135812=CARTESIAN_POINT('Ctrl Pts',(-241.108473579241,-3.48081075907961,
134.279002976425));
#135813=CARTESIAN_POINT('Ctrl Pts',(-241.116238332188,-3.38426946451757,
134.37571565707));
#135814=CARTESIAN_POINT('Ctrl Pts',(-241.124003085134,-3.28356768780561,
134.468528732171));
#135815=CARTESIAN_POINT('Ctrl Pts',(-241.131767838081,-3.17905487259213,
134.557065399393));
#135816=CARTESIAN_POINT('Ctrl Pts',(-241.139524878966,-3.07464586097981,
134.64551413075));
#135817=CARTESIAN_POINT('Ctrl Pts',(-241.147281919851,-2.96643363992176,
134.729694655646));
#135818=CARTESIAN_POINT('Ctrl Pts',(-241.155038960736,-2.85480455597037,
134.809266859878));
#135819=CARTESIAN_POINT('Ctrl Pts',(-241.162790151976,-2.74325965237968,
134.888779058092));
#135820=CARTESIAN_POINT('Ctrl Pts',(-241.170541343216,-2.62830333169952,
134.963689626739));
#135821=CARTESIAN_POINT('Ctrl Pts',(-241.178292534457,-2.51035479772931,
135.03369884618));
#135822=CARTESIAN_POINT('Ctrl Pts',(-241.186040431234,-2.39245639503258,
135.103678309835));
#135823=CARTESIAN_POINT('Ctrl Pts',(-241.193788328011,-2.27156864399816,
135.168760368481));
#135824=CARTESIAN_POINT('Ctrl Pts',(-241.201536224788,-2.14813930742305,
135.228688880523));
#135825=CARTESIAN_POINT('Ctrl Pts',(-241.209282500872,-2.02473578960399,
135.288604856813));
#135826=CARTESIAN_POINT('Ctrl Pts',(-241.217028776956,-1.89879209519428,
135.343369260069));
#135827=CARTESIAN_POINT('Ctrl Pts',(-241.22477505304,-1.7707797836338,135.392772327556));
#135828=CARTESIAN_POINT('Ctrl Pts',(-241.232521386305,-1.64276652711604,
135.442175759725));
#135829=CARTESIAN_POINT('Ctrl Pts',(-241.24026771957,-1.51268498772267,
135.48621763639));
#135830=CARTESIAN_POINT('Ctrl Pts',(-241.248014052836,-1.38102548266735,
135.524736839725));
#135831=CARTESIAN_POINT('Ctrl Pts',(-241.255762120838,-1.24933649337855,
135.563264669168));
#135832=CARTESIAN_POINT('Ctrl Pts',(-241.263510188841,-1.11606921041738,
135.596267254502));
#135833=CARTESIAN_POINT('Ctrl Pts',(-241.271258256844,-0.98172745315296,
135.623633827317));
#135834=CARTESIAN_POINT('Ctrl Pts',(-241.279014559586,-0.847242915870052,
135.651029485652));
#135835=CARTESIAN_POINT('Ctrl Pts',(-241.286770862328,-0.711682006795786,
135.67277708759));
#135836=CARTESIAN_POINT('Ctrl Pts',(-241.29452716507,-0.575557595516321,
135.688817242078));
#135837=CARTESIAN_POINT('Ctrl Pts',(-241.302287607584,-0.43936053053993,
135.70486595768));
#135838=CARTESIAN_POINT('Ctrl Pts',(-241.310048050098,-0.302599753735192,
135.715201126499));
#135839=CARTESIAN_POINT('Ctrl Pts',(-241.317808492612,-0.165790542314485,
135.719815485488));
#135840=CARTESIAN_POINT('Ctrl Pts',(-241.325581392878,-0.0287617126022537,
135.724437251856));
#135841=CARTESIAN_POINT('Ctrl Pts',(-241.333354293143,0.108315315921087,
135.723319859919));
#135842=CARTESIAN_POINT('Ctrl Pts',(-241.341127193408,0.244927080673861,
135.716508191454));
#135843=CARTESIAN_POINT('Ctrl Pts',(-241.348617529171,0.376572663686177,
135.709944144294));
#135844=CARTESIAN_POINT('Ctrl Pts',(-241.356107864934,0.507785915891403,
135.69809266321));
#135845=CARTESIAN_POINT('Ctrl Pts',(-241.363598200696,0.638116175939619,
135.681038873152));
#135846=CARTESIAN_POINT('Ctrl Pts',(-241.371372534816,0.773387947398587,
135.663338483462));
#135847=CARTESIAN_POINT('Ctrl Pts',(-241.379146868935,0.908136947959049,
135.639977436818));
#135848=CARTESIAN_POINT('Ctrl Pts',(-241.386921203054,1.04185178468103,
135.610994358684));
#135849=CARTESIAN_POINT('Ctrl Pts',(-241.394685956001,1.17540182981682,
135.582046999605));
#135850=CARTESIAN_POINT('Ctrl Pts',(-241.402450708948,1.30791986859366,
135.547491477012));
#135851=CARTESIAN_POINT('Ctrl Pts',(-241.410215461895,1.43890000370779,
135.507418116877));
#135852=CARTESIAN_POINT('Ctrl Pts',(-241.41797250278,1.56975004750523,135.46738455817));
#135853=CARTESIAN_POINT('Ctrl Pts',(-241.425729543665,1.69906485592968,
135.421844181794));
#135854=CARTESIAN_POINT('Ctrl Pts',(-241.43348658455,1.8263494515201,135.370938192012));
#135855=CARTESIAN_POINT('Ctrl Pts',(-241.44123777579,1.95353806080668,135.320070590833));
#135856=CARTESIAN_POINT('Ctrl Pts',(-241.44898896703,2.07869914307951,135.263845574658));
#135857=CARTESIAN_POINT('Ctrl Pts',(-241.45674015827,2.20135394582371,135.202453825731));
#135858=CARTESIAN_POINT('Ctrl Pts',(-241.464488055047,2.32395661700498,
135.141088169934));
#135859=CARTESIAN_POINT('Ctrl Pts',(-241.472235951824,2.44405477844558,
135.074560323685));
#135860=CARTESIAN_POINT('Ctrl Pts',(-241.479983848601,2.56119090423909,
135.003108551718));
#135861=CARTESIAN_POINT('Ctrl Pts',(-241.487730124685,2.67830252768056,
134.93167172592));
#135862=CARTESIAN_POINT('Ctrl Pts',(-241.495476400769,2.79245301432282,
134.855313226557));
#135863=CARTESIAN_POINT('Ctrl Pts',(-241.503222676854,2.90321099544081,
134.774316408057));
#135864=CARTESIAN_POINT('Ctrl Pts',(-241.510969010119,3.01396979414861,
134.693318991657));
#135865=CARTESIAN_POINT('Ctrl Pts',(-241.518715343384,3.12133572177857,
134.607683418584));
#135866=CARTESIAN_POINT('Ctrl Pts',(-241.52646167665,3.2249081969094,134.517735118476));
#135867=CARTESIAN_POINT('Ctrl Pts',(-241.534209744653,3.32850386637805,
134.427766675069));
#135868=CARTESIAN_POINT('Ctrl Pts',(-241.541957812655,3.42830409777646,
134.333483839093));
#135869=CARTESIAN_POINT('Ctrl Pts',(-241.549705880658,3.52394337182907,
134.235250615022));
#135870=CARTESIAN_POINT('Ctrl Pts',(-241.5574621834,3.6196842924404,134.136912987511));
#135871=CARTESIAN_POINT('Ctrl Pts',(-241.565218486142,3.71125514848963,
134.034616865484));
#135872=CARTESIAN_POINT('Ctrl Pts',(-241.572974788884,3.79832875406143,
133.928761638333));
#135873=CARTESIAN_POINT('Ctrl Pts',(-241.580735231398,3.8854488334385,133.82284991306));
#135874=CARTESIAN_POINT('Ctrl Pts',(-241.588495673912,3.96806664410421,
133.713375609464));
#135875=CARTESIAN_POINT('Ctrl Pts',(-241.596256116426,4.04589755553098,
133.600768319002));
#135876=CARTESIAN_POINT('Ctrl Pts',(-241.604029016692,4.12385340804606,
133.48798026132));
#135877=CARTESIAN_POINT('Ctrl Pts',(-241.611801916957,4.19700679677301,
133.372049497364));
#135878=CARTESIAN_POINT('Ctrl Pts',(-241.619574817223,4.26511794295314,
133.25343227744));
#135879=CARTESIAN_POINT('Ctrl Pts',(-241.627065152985,4.33075307741003,
133.139127092236));
#135880=CARTESIAN_POINT('Ctrl Pts',(-241.634555488747,4.39170605859743,
133.022327651996));
#135881=CARTESIAN_POINT('Ctrl Pts',(-241.642045824509,4.44780491107956,
132.903459122991));
#135882=CARTESIAN_POINT('Ctrl Pts',(-241.649820158629,4.50603076860302,
132.780083657582));
#135883=CARTESIAN_POINT('Ctrl Pts',(-241.657594492748,4.55921158467241,
132.654088290784));
#135884=CARTESIAN_POINT('Ctrl Pts',(-241.665368826867,4.6071034356103,132.525924149965));
#135885=CARTESIAN_POINT('Ctrl Pts',(-241.673133579814,4.65493626412201,
132.397917959997));
#135886=CARTESIAN_POINT('Ctrl Pts',(-241.680898332761,4.69749296119333,
132.26774867684));
#135887=CARTESIAN_POINT('Ctrl Pts',(-241.688663085708,4.73457607077286,
132.135890749619));
#135888=CARTESIAN_POINT('Ctrl Pts',(-241.696420126593,4.77162234888519,
132.00416378555));
#135889=CARTESIAN_POINT('Ctrl Pts',(-241.704177167478,4.80320575311308,
131.870751889019));
#135890=CARTESIAN_POINT('Ctrl Pts',(-241.711934208363,4.82917753519255,
131.736147822936));
#135891=CARTESIAN_POINT('Ctrl Pts',(-241.719685399603,4.85512973174916,
131.601645262826));
#135892=CARTESIAN_POINT('Ctrl Pts',(-241.727436590843,4.87547865546412,
131.465952704948));
#135893=CARTESIAN_POINT('Ctrl Pts',(-241.735187782084,4.89012595527993,
131.329576005762));
#135894=CARTESIAN_POINT('Ctrl Pts',(-241.742935678861,4.90476702960261,
131.19325727031));
#135895=CARTESIAN_POINT('Ctrl Pts',(-241.750683575638,4.9137112582057,131.056255359802));
#135896=CARTESIAN_POINT('Ctrl Pts',(-241.758431472415,4.91691179603002,
130.919083991648));
#135897=CARTESIAN_POINT('Ctrl Pts',(-241.766177748499,4.92011166437083,
130.781941316788));
#135898=CARTESIAN_POINT('Ctrl Pts',(-241.773924024583,4.91757022258139,
130.644629645399));
#135899=CARTESIAN_POINT('Ctrl Pts',(-241.781670300667,4.90929269943627,
130.507665060198));
#135900=CARTESIAN_POINT('Ctrl Pts',(-241.789416633933,4.90101511518837,
130.370699463956));
#135901=CARTESIAN_POINT('Ctrl Pts',(-241.797162967198,4.88700138867867,
130.234081349268));
#135902=CARTESIAN_POINT('Ctrl Pts',(-241.804909300463,4.8673087890349,130.098323639297));
#135903=CARTESIAN_POINT('Ctrl Pts',(-241.812657368466,4.84761177937007,
129.962535527328));
#135904=CARTESIAN_POINT('Ctrl Pts',(-241.820405436469,4.82223342206145,
129.827608590332));
#135905=CARTESIAN_POINT('Ctrl Pts',(-241.828153504472,4.7912823922847,129.694047103336));
#135906=CARTESIAN_POINT('Ctrl Pts',(-241.835909807214,4.76029846738506,
129.560343665601));
#135907=CARTESIAN_POINT('Ctrl Pts',(-241.843666109956,4.7237301271834,129.428008958308));
#135908=CARTESIAN_POINT('Ctrl Pts',(-241.851422412698,4.68173653730752,
129.297534131955));
#135909=CARTESIAN_POINT('Ctrl Pts',(-241.859182855212,4.63972053418833,
129.166989667258));
#135910=CARTESIAN_POINT('Ctrl Pts',(-241.866943297726,4.59227364681575,
129.038307428135));
#135911=CARTESIAN_POINT('Ctrl Pts',(-241.874703740241,4.53960345289688,
128.911959086985));
#135912=CARTESIAN_POINT('Ctrl Pts',(-241.882476640506,4.4868487081069,128.785407920261));
#135913=CARTESIAN_POINT('Ctrl Pts',(-241.890249540772,4.42885406653741,
128.661198492828));
#135914=CARTESIAN_POINT('Ctrl Pts',(-241.898022441037,4.36587377821813,
128.539779151783));
#135915=CARTESIAN_POINT('Ctrl Pts',(-241.905512776799,4.30518298201941,
128.422773709627));
#135916=CARTESIAN_POINT('Ctrl Pts',(-241.913003112561,4.23986288020815,
128.308359289848));
#135917=CARTESIAN_POINT('Ctrl Pts',(-241.920493448322,4.17017822028657,
128.196910393008));
#135918=CARTESIAN_POINT('Ctrl Pts',(-241.928267782441,4.09785144530113,
128.081235877365));
#135919=CARTESIAN_POINT('Ctrl Pts',(-241.936042116561,4.02059350493841,
127.968389777285));
#135920=CARTESIAN_POINT('Ctrl Pts',(-241.94381645068,3.93865209872679,127.858821158028));
#135921=CARTESIAN_POINT('Ctrl Pts',(-241.951581203627,3.85681167797545,
127.749387572303));
#135922=CARTESIAN_POINT('Ctrl Pts',(-241.959345956574,3.77029950774274,
127.643223740681));
#135923=CARTESIAN_POINT('Ctrl Pts',(-241.967110709521,3.6794080256946,127.540752239872));
#135924=CARTESIAN_POINT('Ctrl Pts',(-241.974867750406,3.58860681834752,
127.438382515202));
#135925=CARTESIAN_POINT('Ctrl Pts',(-241.982624791291,3.49343521282821,
127.339698113895));
#135926=CARTESIAN_POINT('Ctrl Pts',(-241.990381832176,3.39422738245755,
127.245090532468));
#135927=CARTESIAN_POINT('Ctrl Pts',(-241.998133023416,3.2950943654831,127.150554295353));
#135928=CARTESIAN_POINT('Ctrl Pts',(-242.005884214656,3.19193146384553,
127.060089027512));
#135929=CARTESIAN_POINT('Ctrl Pts',(-242.013635405896,3.08511110776185,
126.974050902247));
#135930=CARTESIAN_POINT('Ctrl Pts',(-242.021383302673,2.97833615317946,
126.888049345481));
#135931=CARTESIAN_POINT('Ctrl Pts',(-242.02913119945,2.8679071398086,126.806471433557));
#135932=CARTESIAN_POINT('Ctrl Pts',(-242.036879096228,2.75423095175817,
126.729634255357));
#135933=CARTESIAN_POINT('Ctrl Pts',(-242.044625372312,2.64057854231601,
126.65281314984));
#135934=CARTESIAN_POINT('Ctrl Pts',(-242.052371648396,2.52368063294376,
126.580731024385));
#135935=CARTESIAN_POINT('Ctrl Pts',(-242.06011792448,2.40397424492724,126.513662435192));
#135936=CARTESIAN_POINT('Ctrl Pts',(-242.067864257745,2.28426697326519,
126.446593350914));
#135937=CARTESIAN_POINT('Ctrl Pts',(-242.07561059101,2.16175152266993,126.384538067844));
#135938=CARTESIAN_POINT('Ctrl Pts',(-242.083356924276,2.0368903852876,126.327725651342));
#135939=CARTESIAN_POINT('Ctrl Pts',(-242.091104992279,1.91200128611978,
126.270900512093));
#135940=CARTESIAN_POINT('Ctrl Pts',(-242.098853060282,1.78476581067006,
126.219320737629));
#135941=CARTESIAN_POINT('Ctrl Pts',(-242.106601128285,1.65566696138794,
126.173167469416));
#135942=CARTESIAN_POINT('Ctrl Pts',(-242.114357431026,1.52643090431199,
126.126965148961));
#135943=CARTESIAN_POINT('Ctrl Pts',(-242.122113733768,1.39532788604286,
126.086200987495));
#135944=CARTESIAN_POINT('Ctrl Pts',(-242.12987003651,1.2628571583152,126.051006553309));
#135945=CARTESIAN_POINT('Ctrl Pts',(-242.137630479024,1.13031572697117,
126.015793334793));
#135946=CARTESIAN_POINT('Ctrl Pts',(-242.145390921539,0.996405513147183,
125.98615585142));
#135947=CARTESIAN_POINT('Ctrl Pts',(-242.153151364053,0.861635549012902,
125.96217441264));
#135948=CARTESIAN_POINT('Ctrl Pts',(-242.160924264318,0.726649240168245,
125.938154476725));
#135949=CARTESIAN_POINT('Ctrl Pts',(-242.168697164583,0.590800810709943,
125.919808781659));
#135950=CARTESIAN_POINT('Ctrl Pts',(-242.176470064849,0.454604896099585,
125.907165762249));
#135951=CARTESIAN_POINT('Ctrl Pts',(-242.183960400611,0.323360046039914,
125.89498234844));
#135952=CARTESIAN_POINT('Ctrl Pts',(-242.191450736373,0.191792843727768,
125.888094211437));
#135953=CARTESIAN_POINT('Ctrl Pts',(-242.198941072135,0.0603614695825091,
125.886481038368));
#135954=CARTESIAN_POINT('Ctrl Pts',(-242.206715406254,-0.076053165060172,
125.884806701352));
#135955=CARTESIAN_POINT('Ctrl Pts',(-242.214489740374,-0.212753588922461,
125.888809921125));
#135956=CARTESIAN_POINT('Ctrl Pts',(-242.222264074493,-0.349228103035995,
125.898525031802));
#135957=CARTESIAN_POINT('Ctrl Pts',(-242.23002882744,-0.485534424507592,
125.908228169473));
#135958=CARTESIAN_POINT('Ctrl Pts',(-242.237793580387,-0.621615003955867,
125.923629164255));
#135959=CARTESIAN_POINT('Ctrl Pts',(-242.245558333334,-0.75695624592618,
125.94471039309));
#135960=CARTESIAN_POINT('Ctrl Pts',(-242.253315374219,-0.892163065066992,
125.965770683751));
#135961=CARTESIAN_POINT('Ctrl Pts',(-242.261072415104,-1.02663162425341,
125.992499921468));
#135962=CARTESIAN_POINT('Ctrl Pts',(-242.268829455989,-1.15985191753626,
126.024828570191));
#135963=CARTESIAN_POINT('Ctrl Pts',(-242.276580647229,-1.29297174835875,
126.057132839628));
#135964=CARTESIAN_POINT('Ctrl Pts',(-242.284331838469,-1.42484480853124,
126.095028023496));
#135965=CARTESIAN_POINT('Ctrl Pts',(-242.29208302971,-1.55497013173743,
126.138393306075));
#135966=CARTESIAN_POINT('Ctrl Pts',(-242.299830926487,-1.68504014821093,
126.181740157252));
#135967=CARTESIAN_POINT('Ctrl Pts',(-242.307578823264,-1.81336353502592,
126.230552359667));
#135968=CARTESIAN_POINT('Ctrl Pts',(-242.315326720041,-1.93945358552411,
126.284658984483));
#135969=CARTESIAN_POINT('Ctrl Pts',(-242.323072996125,-2.06551726070193,
126.338754291358));
#135970=CARTESIAN_POINT('Ctrl Pts',(-242.330819272209,-2.18934816972546,
126.398141663723));
#135971=CARTESIAN_POINT('Ctrl Pts',(-242.338565548293,-2.31047910000963,
126.462601827523));
#135972=CARTESIAN_POINT('Ctrl Pts',(-242.346311881559,-2.43161092445432,
126.527062467153));
#135973=CARTESIAN_POINT('Ctrl Pts',(-242.354058214824,-2.55004238525122,
126.596595789273));
#135974=CARTESIAN_POINT('Ctrl Pts',(-242.361804548089,-2.66533077492409,
126.670936501565));
#135975=CARTESIAN_POINT('Ctrl Pts',(-242.369552616092,-2.78064498263262,
126.745293861943));
#135976=CARTESIAN_POINT('Ctrl Pts',(-242.377300684096,-2.89281439008498,
126.824460542932));
#135977=CARTESIAN_POINT('Ctrl Pts',(-242.385048752099,-3.00142552321289,
126.908128092279));
#135978=CARTESIAN_POINT('Ctrl Pts',(-242.39280505484,-3.11015208954572,
126.991884564493));
#135979=CARTESIAN_POINT('Ctrl Pts',(-242.400561357582,-3.21531251683247,
127.080151221801));
#135980=CARTESIAN_POINT('Ctrl Pts',(-242.408317660324,-3.31652625518601,
127.172579145456));
#135981=CARTESIAN_POINT('Ctrl Pts',(-242.416078102838,-3.41779401435919,
127.265056400677));
#135982=CARTESIAN_POINT('Ctrl Pts',(-242.423838545352,-3.51511061000858,
127.361699072403));
#135983=CARTESIAN_POINT('Ctrl Pts',(-242.431598987867,-3.60813333119822,
127.462122306674));
#135984=CARTESIAN_POINT('Ctrl Pts',(-242.439371888132,-3.70130538071808,
127.562706749235));
#135985=CARTESIAN_POINT('Ctrl Pts',(-242.447144788398,-3.79016952795871,
127.667083584065));
#135986=CARTESIAN_POINT('Ctrl Pts',(-242.454917688663,-3.87442367687448,
127.774835203483));
#135987=CARTESIAN_POINT('Ctrl Pts',(-242.462408024425,-3.95561497525035,
127.878669780121));
#135988=CARTESIAN_POINT('Ctrl Pts',(-242.469898360187,-4.03252544654635,
127.985637787295));
#135989=CARTESIAN_POINT('Ctrl Pts',(-242.477388695948,-4.10492452284809,
128.09534276524));
#135990=CARTESIAN_POINT('Ctrl Pts',(-242.485314034205,-4.18152818754758,
128.211418878026));
#135991=CARTESIAN_POINT('Ctrl Pts',(-242.493239372462,-4.25331672785682,
128.330916190021));
#135992=CARTESIAN_POINT('Ctrl Pts',(-242.501164710719,-4.31997667751242,
128.453406647738));
#135993=CARTESIAN_POINT('Ctrl Pts',(-242.509080214655,-4.38655391078081,
128.575745110619));
#135994=CARTESIAN_POINT('Ctrl Pts',(-242.516995718591,-4.44801504155588,
128.701069006151));
#135995=CARTESIAN_POINT('Ctrl Pts',(-242.524911222527,-4.50408923847976,
128.828920617386));
#135996=CARTESIAN_POINT('Ctrl Pts',(-242.532815485652,-4.56008380441048,
128.956590666489));
#135997=CARTESIAN_POINT('Ctrl Pts',(-242.540719748777,-4.61070653017702,
129.086780942342));
#135998=CARTESIAN_POINT('Ctrl Pts',(-242.548624011902,-4.65573231343456,
129.219009019926));
#135999=CARTESIAN_POINT('Ctrl Pts',(-242.555774442768,-4.69646397245246,
129.338626460846));
#136000=CARTESIAN_POINT('Ctrl Pts',(-242.562924873635,-4.73261581172073,
129.459911040772));
#136001=CARTESIAN_POINT('Ctrl Pts',(-242.570075304501,-4.76405452823394,
129.582490119308));
#136002=CARTESIAN_POINT('Origin',(213.235140564004,0.,130.804360617566));
#136003=CARTESIAN_POINT('',(-244.66511323982,-4.76405452823407,129.582490119308));
#136004=CARTESIAN_POINT('',(-244.319729366371,-4.76405452823391,129.582490119308));
#136005=CARTESIAN_POINT('',(213.235140564004,-4.76405452823405,129.582490119308));
#136006=CARTESIAN_POINT('',(-242.985140563976,-4.9182491105998,130.807318418142));
#136007=CARTESIAN_POINT('Ctrl Pts',(-242.985140564014,-4.9182491105994,
130.807318418808));
#136008=CARTESIAN_POINT('Ctrl Pts',(-242.994992025147,-4.91814497261588,
130.98047966355));
#136009=CARTESIAN_POINT('Ctrl Pts',(-243.00484348628,-4.9088965499763,131.15336397321));
#136010=CARTESIAN_POINT('Ctrl Pts',(-243.014694947413,-4.89058692147893,
131.325266200142));
#136011=CARTESIAN_POINT('Ctrl Pts',(-243.022469281532,-4.87613777859409,
131.460923777221));
#136012=CARTESIAN_POINT('Ctrl Pts',(-243.030243615651,-4.85601706382389,
131.596194574106));
#136013=CARTESIAN_POINT('Ctrl Pts',(-243.03801794977,-4.83025111949025,
131.730566418219));
#136014=CARTESIAN_POINT('Ctrl Pts',(-243.045782702718,-4.80451692938022,
131.864772661044));
#136015=CARTESIAN_POINT('Ctrl Pts',(-243.053547455665,-4.77315142546234,
131.998081775163));
#136016=CARTESIAN_POINT('Ctrl Pts',(-243.061312208612,-4.7362327675567,
132.129985841384));
#136017=CARTESIAN_POINT('Ctrl Pts',(-243.069069249497,-4.69935077778265,
132.261758898627));
#136018=CARTESIAN_POINT('Ctrl Pts',(-243.076826290382,-4.6569267147524,
132.392129311046));
#136019=CARTESIAN_POINT('Ctrl Pts',(-243.084583331267,-4.60908986396974,
132.52059885521));
#136020=CARTESIAN_POINT('Ctrl Pts',(-243.092334522507,-4.5612890873283,
132.648971519491));
#136021=CARTESIAN_POINT('Ctrl Pts',(-243.100085713747,-4.5080837834367,
132.775445803825));
#136022=CARTESIAN_POINT('Ctrl Pts',(-243.107836904987,-4.44965309088534,
132.899538517715));
#136023=CARTESIAN_POINT('Ctrl Pts',(-243.115584801765,-4.39124723293692,
133.023578488893));
#136024=CARTESIAN_POINT('Ctrl Pts',(-243.123332698542,-4.32762056979108,
133.145238549903));
#136025=CARTESIAN_POINT('Ctrl Pts',(-243.131080595319,-4.25900031820745,
133.264055588901));
#136026=CARTESIAN_POINT('Ctrl Pts',(-243.138826871403,-4.19039442050118,
133.382847773935));
#136027=CARTESIAN_POINT('Ctrl Pts',(-243.146573147487,-4.11679720743047,
133.498797781499));
#136028=CARTESIAN_POINT('Ctrl Pts',(-243.154319423571,-4.03848160016657,
133.611467567366));
#136029=CARTESIAN_POINT('Ctrl Pts',(-243.162065756837,-3.96016541479474,
133.724138184936));
#136030=CARTESIAN_POINT('Ctrl Pts',(-243.169812090102,-3.87713098887342,
133.833528211463));
#136031=CARTESIAN_POINT('Ctrl Pts',(-243.177558423367,-3.78969404547483,
133.939229371468));
#136032=CARTESIAN_POINT('Ctrl Pts',(-243.18530649137,-3.7022375211789,134.044954202516));
#136033=CARTESIAN_POINT('Ctrl Pts',(-243.193054559373,-3.61037676670409,
134.146988222011));
#136034=CARTESIAN_POINT('Ctrl Pts',(-243.200802627376,-3.51446691024449,
134.244957280835));
#136035=CARTESIAN_POINT('Ctrl Pts',(-243.208558930118,-3.41845511964823,
134.34303046234));
#136036=CARTESIAN_POINT('Ctrl Pts',(-243.21631523286,-3.31838590443326,
134.437029773113));
#136037=CARTESIAN_POINT('Ctrl Pts',(-243.224071535602,-3.21465068741773,
134.526618537214));
#136038=CARTESIAN_POINT('Ctrl Pts',(-243.231831978116,-3.11086010379319,
134.616255117537));
#136039=CARTESIAN_POINT('Ctrl Pts',(-243.23959242063,-3.00339992574493,
134.701476217747));
#136040=CARTESIAN_POINT('Ctrl Pts',(-243.247352863144,-2.89269279067072,
134.781986980273));
#136041=CARTESIAN_POINT('Ctrl Pts',(-243.25512576341,-2.78180793867518,
134.862626985822));
#136042=CARTESIAN_POINT('Ctrl Pts',(-243.262898663675,-2.66766603953724,
134.93854132686));
#136043=CARTESIAN_POINT('Ctrl Pts',(-243.270671563941,-2.5507174581469,
135.009479344927));
#136044=CARTESIAN_POINT('Ctrl Pts',(-243.278161899702,-2.43802025226833,
135.077838587354));
#136045=CARTESIAN_POINT('Ctrl Pts',(-243.285652235464,-2.32271715086915,
135.141576880101));
#136046=CARTESIAN_POINT('Ctrl Pts',(-243.293142571226,-2.20522907084774,
135.200512094436));
#136047=CARTESIAN_POINT('Ctrl Pts',(-243.300916905345,-2.08328639456036,
135.261681855337));
#136048=CARTESIAN_POINT('Ctrl Pts',(-243.308691239464,-1.95860350426506,
135.317870898042));
#136049=CARTESIAN_POINT('Ctrl Pts',(-243.316465573584,-1.83162554392404,
135.368824543302));
#136050=CARTESIAN_POINT('Ctrl Pts',(-243.324230326531,-1.7048040725708,
135.419715392748));
#136051=CARTESIAN_POINT('Ctrl Pts',(-243.331995079478,-1.57569351834008,
135.465383538422));
#136052=CARTESIAN_POINT('Ctrl Pts',(-243.339759832425,-1.44476345532513,
135.505620195664));
#136053=CARTESIAN_POINT('Ctrl Pts',(-243.34751687331,-1.31396343389456,
135.54581688929));
#136054=CARTESIAN_POINT('Ctrl Pts',(-243.355273914195,-1.18134787131098,
135.580592715938));
#136055=CARTESIAN_POINT('Ctrl Pts',(-243.36303095508,-1.0474058190315,135.609787145228));
#136056=CARTESIAN_POINT('Ctrl Pts',(-243.37078214632,-0.913564773495737,
135.638959558772));
#136057=CARTESIAN_POINT('Ctrl Pts',(-243.37853333756,-0.778399609783712,
135.662558869744));
#136058=CARTESIAN_POINT('Ctrl Pts',(-243.3862845288,-0.64241367852652,135.680474616248));
#136059=CARTESIAN_POINT('Ctrl Pts',(-243.394032425577,-0.50648554491747,
135.698382748082));
#136060=CARTESIAN_POINT('Ctrl Pts',(-243.401780322354,-0.369737724399718,
135.710612069065));
#136061=CARTESIAN_POINT('Ctrl Pts',(-243.409528219131,-0.232682662294731,
135.717103419827));
#136062=CARTESIAN_POINT('Ctrl Pts',(-243.417274495216,-0.0956562691541705,
135.723593412738));
#136063=CARTESIAN_POINT('Ctrl Pts',(-243.4250207713,0.0416768474604148,
135.724347804325));
#136064=CARTESIAN_POINT('Ctrl Pts',(-243.432767047384,0.178800627975639,
135.719359437295));
#136065=CARTESIAN_POINT('Ctrl Pts',(-243.440513380649,0.315925420707648,
135.714371033441));
#136066=CARTESIAN_POINT('Ctrl Pts',(-243.448259713914,0.452840483550059,
135.703639800594));
#136067=CARTESIAN_POINT('Ctrl Pts',(-243.45600604718,0.589031666747969,
135.687210682648));
#136068=CARTESIAN_POINT('Ctrl Pts',(-243.463754115183,0.725253349016888,
135.670777885514));
#136069=CARTESIAN_POINT('Ctrl Pts',(-243.471502183186,0.860750440988623,
135.648644710999));
#136070=CARTESIAN_POINT('Ctrl Pts',(-243.479250251189,0.995016204949736,
135.620907701773));
#136071=CARTESIAN_POINT('Ctrl Pts',(-243.487006553931,1.12942466816275,
135.593141213324));
#136072=CARTESIAN_POINT('Ctrl Pts',(-243.494762856672,1.26259880566465,
135.55975907199));
#136073=CARTESIAN_POINT('Ctrl Pts',(-243.502519159414,1.39404378885936,
135.520908611305));
#136074=CARTESIAN_POINT('Ctrl Pts',(-243.510279601928,1.52555892819933,
135.482037414959));
#136075=CARTESIAN_POINT('Ctrl Pts',(-243.518040044443,1.65534270448857,
135.437692210042));
#136076=CARTESIAN_POINT('Ctrl Pts',(-243.525800486957,1.78291859986438,
135.388069195645));
#136077=CARTESIAN_POINT('Ctrl Pts',(-243.533573387222,1.9106992913931,135.338366521981));
#136078=CARTESIAN_POINT('Ctrl Pts',(-243.541346287488,2.03626466106833,
135.283369265211));
#136079=CARTESIAN_POINT('Ctrl Pts',(-243.549119187753,2.1591603896068,135.223320843055));
#136080=CARTESIAN_POINT('Ctrl Pts',(-243.556609523515,2.27758854885757,
135.165455332297));
#136081=CARTESIAN_POINT('Ctrl Pts',(-243.564099859277,2.39353752245083,
135.102899671658));
#136082=CARTESIAN_POINT('Ctrl Pts',(-243.571590195039,2.5066265644634,135.03590954542));
#136083=CARTESIAN_POINT('Ctrl Pts',(-243.579364529158,2.62400341187606,
134.966379468185));
#136084=CARTESIAN_POINT('Ctrl Pts',(-243.587138863278,2.73867099261287,
134.891851771452));
#136085=CARTESIAN_POINT('Ctrl Pts',(-243.594913197397,2.85017442662608,
134.81256330709));
#136086=CARTESIAN_POINT('Ctrl Pts',(-243.602677950344,2.96154044262223,
134.733372558674));
#136087=CARTESIAN_POINT('Ctrl Pts',(-243.610442703291,3.06974975522903,
134.649432941042));
#136088=CARTESIAN_POINT('Ctrl Pts',(-243.618207456238,3.17437289173182,
134.561026666969));
#136089=CARTESIAN_POINT('Ctrl Pts',(-243.625964497123,3.27889211506078,
134.472708199254));
#136090=CARTESIAN_POINT('Ctrl Pts',(-243.633721538008,3.37983195381406,
134.379932154334));
#136091=CARTESIAN_POINT('Ctrl Pts',(-243.641478578893,3.47679300497879,
134.28302321446));
#136092=CARTESIAN_POINT('Ctrl Pts',(-243.649229770133,3.57368093706045,
134.186187354372));
#136093=CARTESIAN_POINT('Ctrl Pts',(-243.656980961373,3.6665957783273,134.085225078089));
#136094=CARTESIAN_POINT('Ctrl Pts',(-243.664732152613,3.75517252074743,
133.980500161403));
#136095=CARTESIAN_POINT('Ctrl Pts',(-243.67248004939,3.84371161568929,133.875819755599));
#136096=CARTESIAN_POINT('Ctrl Pts',(-243.680227946168,3.92791602702597,
133.767380188007));
#136097=CARTESIAN_POINT('Ctrl Pts',(-243.687975842945,4.00745899309027,
133.655580616303));
#136098=CARTESIAN_POINT('Ctrl Pts',(-243.695722119029,4.08698532048081,
133.54380443066));
#136099=CARTESIAN_POINT('Ctrl Pts',(-243.703468395113,4.16185191556661,
133.428669957256));
#136100=CARTESIAN_POINT('Ctrl Pts',(-243.711214671197,4.23177381390916,
133.310607502933));
#136101=CARTESIAN_POINT('Ctrl Pts',(-243.718961004462,4.30169622839919,
133.192544177101));
#136102=CARTESIAN_POINT('Ctrl Pts',(-243.726707337728,4.36667367408318,
133.071553163616));
#136103=CARTESIAN_POINT('Ctrl Pts',(-243.734453670993,4.42646605303072,
132.948091324503));
#136104=CARTESIAN_POINT('Ctrl Pts',(-243.742201738996,4.48627182206704,
132.824601836968));
#136105=CARTESIAN_POINT('Ctrl Pts',(-243.749949806999,4.54089004341501,
132.698640774556));
#136106=CARTESIAN_POINT('Ctrl Pts',(-243.757697875002,4.59012803704497,
132.570686653731));
#136107=CARTESIAN_POINT('Ctrl Pts',(-243.765454177744,4.63941836140043,
132.442596541743));
#136108=CARTESIAN_POINT('Ctrl Pts',(-243.773210480486,4.6833168947433,132.31250950538));
#136109=CARTESIAN_POINT('Ctrl Pts',(-243.780966783228,4.72168012600565,
132.180921495327));
#136110=CARTESIAN_POINT('Ctrl Pts',(-243.788727225742,4.76006383287962,
132.049263252792));
#136111=CARTESIAN_POINT('Ctrl Pts',(-243.796487668256,4.79290625729025,
131.916102819682));
#136112=CARTESIAN_POINT('Ctrl Pts',(-243.80424811077,4.82011489754655,131.781947154375));
#136113=CARTESIAN_POINT('Ctrl Pts',(-243.812021011035,4.84736721552766,
131.647576130483));
#136114=CARTESIAN_POINT('Ctrl Pts',(-243.819793911301,4.86896761521828,
131.512207068113));
#136115=CARTESIAN_POINT('Ctrl Pts',(-243.827566811566,4.88487532016844,
131.376353772166));
#136116=CARTESIAN_POINT('Ctrl Pts',(-243.835057147328,4.9002047399744,131.245439085722));
#136117=CARTESIAN_POINT('Ctrl Pts',(-243.84254748309,4.91024814344905,131.114075067812));
#136118=CARTESIAN_POINT('Ctrl Pts',(-243.850037818852,4.91501484254739,
130.982720254365));
#136119=CARTESIAN_POINT('Ctrl Pts',(-243.857812152971,4.91996227249089,
130.846385083239));
#136120=CARTESIAN_POINT('Ctrl Pts',(-243.86558648709,4.91924063879485,130.709627959486));
#136121=CARTESIAN_POINT('Ctrl Pts',(-243.87336082121,4.91280333786775,130.572959610793));
#136122=CARTESIAN_POINT('Ctrl Pts',(-243.881125574157,4.90637397033873,
130.436459693626));
#136123=CARTESIAN_POINT('Ctrl Pts',(-243.888890327104,4.89424296935481,
130.300048720613));
#136124=CARTESIAN_POINT('Ctrl Pts',(-243.896655080051,4.87641562802379,
130.164240562213));
#136125=CARTESIAN_POINT('Ctrl Pts',(-243.904412120936,4.8586059930595,130.02856729039));
#136126=CARTESIAN_POINT('Ctrl Pts',(-243.912169161821,4.83511132735324,
129.893496026822));
#136127=CARTESIAN_POINT('Ctrl Pts',(-243.919926202706,4.80598890819332,
129.759538299264));
#136128=CARTESIAN_POINT('Ctrl Pts',(-243.927677393946,4.77688845047619,
129.625681590269));
#136129=CARTESIAN_POINT('Ctrl Pts',(-243.935428585186,4.74216876931568,
129.492937126355));
#136130=CARTESIAN_POINT('Ctrl Pts',(-243.943179776426,4.7019386238288,129.361808628816));
#136131=CARTESIAN_POINT('Ctrl Pts',(-243.950927673203,4.66172557722698,
129.230735864386));
#136132=CARTESIAN_POINT('Ctrl Pts',(-243.95867556998,4.61600683897823,129.101278073269));
#136133=CARTESIAN_POINT('Ctrl Pts',(-243.966423466757,4.56494160907855,
128.973925923783));
#136134=CARTESIAN_POINT('Ctrl Pts',(-243.974169742842,4.51388706092413,
128.846600413622));
#136135=CARTESIAN_POINT('Ctrl Pts',(-243.981916018926,4.45748839103371,
128.721380031654));
#136136=CARTESIAN_POINT('Ctrl Pts',(-243.98966229501,4.39595359850137,128.59873711789));
#136137=CARTESIAN_POINT('Ctrl Pts',(-243.997408628275,4.33441835173309,
128.476093298804));
#136138=CARTESIAN_POINT('Ctrl Pts',(-244.005154961541,4.26774708199992,
128.356027335335));
#136139=CARTESIAN_POINT('Ctrl Pts',(-244.012901294806,4.19619438146456,
128.238988173755));
#136140=CARTESIAN_POINT('Ctrl Pts',(-244.020649362809,4.12462565719812,
128.121922802066));
#136141=CARTESIAN_POINT('Ctrl Pts',(-244.028397430812,4.048173530752,128.007885914574));
#136142=CARTESIAN_POINT('Ctrl Pts',(-244.036145498815,3.96713644331463,
127.897298268282));
#136143=CARTESIAN_POINT('Ctrl Pts',(-244.043901801557,3.88601322869649,
127.786593088123));
#136144=CARTESIAN_POINT('Ctrl Pts',(-244.051658104299,3.80029555030125,
127.679344788044));
#136145=CARTESIAN_POINT('Ctrl Pts',(-244.05941440704,3.71032309424963,127.575942181431));
#136146=CARTESIAN_POINT('Ctrl Pts',(-244.067174849555,3.62030261718895,
127.472484385733));
#136147=CARTESIAN_POINT('Ctrl Pts',(-244.074935292069,3.52602310612943,
127.37287665721));
#136148=CARTESIAN_POINT('Ctrl Pts',(-244.082695734583,3.42786108008685,
127.27747084354));
#136149=CARTESIAN_POINT('Ctrl Pts',(-244.090468634848,3.32954147564566,
127.181911875989));
#136150=CARTESIAN_POINT('Ctrl Pts',(-244.098241535114,3.22732719327437,
127.09056856319));
#136151=CARTESIAN_POINT('Ctrl Pts',(-244.106014435379,3.12162847092181,
127.003752935625));
#136152=CARTESIAN_POINT('Ctrl Pts',(-244.113504771141,3.01977216336549,
126.920093274797));
#136153=CARTESIAN_POINT('Ctrl Pts',(-244.120995106903,2.91468059957612,
126.840638014584));
#136154=CARTESIAN_POINT('Ctrl Pts',(-244.128485442665,2.80674459215513,
126.765627170443));
#136155=CARTESIAN_POINT('Ctrl Pts',(-244.136259776785,2.6947161582068,126.687772267348));
#136156=CARTESIAN_POINT('Ctrl Pts',(-244.144034110904,2.57926845619083,
126.614458832348));
#136157=CARTESIAN_POINT('Ctrl Pts',(-244.151808445023,2.46080598539578,
126.546002135153));
#136158=CARTESIAN_POINT('Ctrl Pts',(-244.15957319797,2.34248950900869,126.477629804719));
#136159=CARTESIAN_POINT('Ctrl Pts',(-244.167337950917,2.22116599170592,
126.414102496478));
#136160=CARTESIAN_POINT('Ctrl Pts',(-244.175102703864,2.09727062831025,
126.355693516723));
#136161=CARTESIAN_POINT('Ctrl Pts',(-244.182859744749,1.97349831953612,
126.297342549589));
#136162=CARTESIAN_POINT('Ctrl Pts',(-244.190616785634,1.84715959937641,
126.244099959994));
#136163=CARTESIAN_POINT('Ctrl Pts',(-244.198373826519,1.71871579039075,
126.196194052178));
#136164=CARTESIAN_POINT('Ctrl Pts',(-244.206125017759,1.59036884188042,
126.14832427058));
#136165=CARTESIAN_POINT('Ctrl Pts',(-244.213876208999,1.4599203291283,126.105783296443));
#136166=CARTESIAN_POINT('Ctrl Pts',(-244.221627400239,1.32785283408493,
126.068751901307));
#136167=CARTESIAN_POINT('Ctrl Pts',(-244.229375297016,1.19584147125015,
126.031736245501));
#136168=CARTESIAN_POINT('Ctrl Pts',(-244.237123193793,1.06221287038219,
126.00022561653));
#136169=CARTESIAN_POINT('Ctrl Pts',(-244.244871090571,0.927465896121306,
125.974351293141));
#136170=CARTESIAN_POINT('Ctrl Pts',(-244.252617366655,0.792747108022631,
125.948482382103));
#136171=CARTESIAN_POINT('Ctrl Pts',(-244.260363642739,0.656910795557193,
125.928247505243));
#136172=CARTESIAN_POINT('Ctrl Pts',(-244.268109918823,0.520466780345514,
125.913726978347));
#136173=CARTESIAN_POINT('Ctrl Pts',(-244.275856252088,0.384021757934924,
125.899206344265));
#136174=CARTESIAN_POINT('Ctrl Pts',(-244.283602585354,0.246969412596659,
125.89040018569));
#136175=CARTESIAN_POINT('Ctrl Pts',(-244.291348918619,0.109825068826519,
125.887336973454));
#136176=CARTESIAN_POINT('Ctrl Pts',(-244.299096986622,-0.0273499874683305,
125.884273075232));
#136177=CARTESIAN_POINT('Ctrl Pts',(-244.306845054625,-0.16461669239856,
125.886954691253));
#136178=CARTESIAN_POINT('Ctrl Pts',(-244.314593122628,-0.301459736430147,
125.895358163929));
#136179=CARTESIAN_POINT('Ctrl Pts',(-244.32234942537,-0.438448218877197,
125.903770567916));
#136180=CARTESIAN_POINT('Ctrl Pts',(-244.330105728112,-0.575011750106765,
125.917916952523));
#136181=CARTESIAN_POINT('Ctrl Pts',(-244.337862030853,-0.710639601759831,
125.937721693328));
#136182=CARTESIAN_POINT('Ctrl Pts',(-244.345622473368,-0.846339842081371,
125.957537004519));
#136183=CARTESIAN_POINT('Ctrl Pts',(-244.353382915882,-0.981103023757691,
125.983016616988));
#136184=CARTESIAN_POINT('Ctrl Pts',(-244.361143358396,-1.11442960964777,
126.014033936885));
#136185=CARTESIAN_POINT('Ctrl Pts',(-244.368916258661,-1.2479702232097,
126.045101048539));
#136186=CARTESIAN_POINT('Ctrl Pts',(-244.376689158927,-1.38006925558917,
126.081723527404));
#136187=CARTESIAN_POINT('Ctrl Pts',(-244.384462059192,-1.51024244307228,
126.123724888774));
#136188=CARTESIAN_POINT('Ctrl Pts',(-244.391952394954,-1.63568350730427,
126.164199394864));
#136189=CARTESIAN_POINT('Ctrl Pts',(-244.399442730716,-1.75933602524378,
126.209668394879));
#136190=CARTESIAN_POINT('Ctrl Pts',(-244.406933066479,-1.88078682133141,
126.25993282133));
#136191=CARTESIAN_POINT('Ctrl Pts',(-244.414707789887,-2.00684877333719,
126.312105651141));
#136192=CARTESIAN_POINT('Ctrl Pts',(-244.422482513296,-2.13093785983965,
126.36961051682));
#136193=CARTESIAN_POINT('Ctrl Pts',(-244.430257236704,-2.25257012143072,
126.432277485861));
#136194=CARTESIAN_POINT('Ctrl Pts',(-244.43802228983,-2.37405109553231,
126.494866509066));
#136195=CARTESIAN_POINT('Ctrl Pts',(-244.445787342956,-2.49308098086626,
126.562604682468));
#136196=CARTESIAN_POINT('Ctrl Pts',(-244.453552396082,-2.60919455110486,
126.635273564387));
#136197=CARTESIAN_POINT('Ctrl Pts',(-244.461309648413,-2.72519147332305,
126.707869442942));
#136198=CARTESIAN_POINT('Ctrl Pts',(-244.469066900744,-2.83827758174439,
126.785385965881));
#136199=CARTESIAN_POINT('Ctrl Pts',(-244.476824153076,-2.94801140790485,
126.867558387156));
#136200=CARTESIAN_POINT('Ctrl Pts',(-244.48466953169,-3.05899186544952,
126.950664328412));
#136201=CARTESIAN_POINT('Ctrl Pts',(-244.492514910304,-3.16654303521455,
127.038532436224));
#136202=CARTESIAN_POINT('Ctrl Pts',(-244.500360288919,-3.27023694056918,
127.130842764739));
#136203=CARTESIAN_POINT('Ctrl Pts',(-244.508107844333,-3.37263789753697,
127.222002085489));
#136204=CARTESIAN_POINT('Ctrl Pts',(-244.515855399748,-3.47127693412199,
127.317493210834));
#136205=CARTESIAN_POINT('Ctrl Pts',(-244.523602955162,-3.56577442766546,
127.416966959677));
#136206=CARTESIAN_POINT('Ctrl Pts',(-244.531348784283,-3.66025086547981,
127.516418543992));
#136207=CARTESIAN_POINT('Ctrl Pts',(-244.539094613404,-3.75058732754578,
127.619850702729));
#136208=CARTESIAN_POINT('Ctrl Pts',(-244.546840442525,-3.83644120355387,
127.726877562507));
#136209=CARTESIAN_POINT('Ctrl Pts',(-244.554586223141,-3.9222945419454,
127.833903752083));
#136210=CARTESIAN_POINT('Ctrl Pts',(-244.562332003758,-4.0036651062496,
127.944524292504));
#136211=CARTESIAN_POINT('Ctrl Pts',(-244.570077784374,-4.0802509776755,
128.058320737725));
#136212=CARTESIAN_POINT('Ctrl Pts',(-244.577997405661,-4.15855568673843,
128.174671147657));
#136213=CARTESIAN_POINT('Ctrl Pts',(-244.585917026949,-4.23185812882442,
128.294341367758));
#136214=CARTESIAN_POINT('Ctrl Pts',(-244.593836648236,-4.29988323917117,
128.416854137576));
#136215=CARTESIAN_POINT('Ctrl Pts',(-244.601590724945,-4.36648641433009,
128.536806011609));
#136216=CARTESIAN_POINT('Ctrl Pts',(-244.609344801654,-4.42803057786307,
128.659482391777));
#136217=CARTESIAN_POINT('Ctrl Pts',(-244.617098878363,-4.48430511884091,
128.784412434162));
#136218=CARTESIAN_POINT('Ctrl Pts',(-244.625101271939,-4.54238179800055,
128.913343241289));
#136219=CARTESIAN_POINT('Ctrl Pts',(-244.633103665515,-4.59484552599068,
129.044674046821));
#136220=CARTESIAN_POINT('Ctrl Pts',(-244.641106059091,-4.64151974732242,
129.177868226647));
#136221=CARTESIAN_POINT('Ctrl Pts',(-244.649108452668,-4.68819396865428,
129.311062406474));
#136222=CARTESIAN_POINT('Ctrl Pts',(-244.657110846244,-4.729078601635,129.446119512332));
#136223=CARTESIAN_POINT('Ctrl Pts',(-244.66511323982,-4.76405452823407,
129.582490119308));
#136224=CARTESIAN_POINT('Ctrl Pts',(-242.915000748075,-4.76405452823401,
129.582490119308));
#136225=CARTESIAN_POINT('Ctrl Pts',(-242.922656758014,-4.79771996933577,
129.713751163219));
#136226=CARTESIAN_POINT('Ctrl Pts',(-242.930312767954,-4.82593408241573,
129.846317638161));
#136227=CARTESIAN_POINT('Ctrl Pts',(-242.937968777893,-4.84861868490206,
129.979691040754));
#136228=CARTESIAN_POINT('Ctrl Pts',(-242.94583074224,-4.8719135261307,130.116652322726));
#136229=CARTESIAN_POINT('Ctrl Pts',(-242.953692706587,-4.88937709266357,
130.254464105846));
#136230=CARTESIAN_POINT('Ctrl Pts',(-242.961554670935,-4.90098175486698,
130.392582885093));
#136231=CARTESIAN_POINT('Ctrl Pts',(-242.969416635282,-4.91258641707036,
130.530701664339));
#136232=CARTESIAN_POINT('Ctrl Pts',(-242.977278599629,-4.91833221796005,
130.669126985006));
#136233=CARTESIAN_POINT('Ctrl Pts',(-242.985140563976,-4.9182491105998,
130.807318418143));
#136234=CARTESIAN_POINT('',(-242.639859436042,-4.91824951337863,130.806548459172));
#136235=CARTESIAN_POINT('Ctrl Pts',(-242.570075304501,-4.76405452823394,
129.582490119308));
#136236=CARTESIAN_POINT('Ctrl Pts',(-242.577966389988,-4.79874972412332,
129.717766161507));
#136237=CARTESIAN_POINT('Ctrl Pts',(-242.585857475476,-4.82770399415613,
129.854618717759));
#136238=CARTESIAN_POINT('Ctrl Pts',(-242.593748560963,-4.85078502570779,
129.99253077279));
#136239=CARTESIAN_POINT('Ctrl Pts',(-242.601634899969,-4.8738521740395,
130.130359873843));
#136240=CARTESIAN_POINT('Ctrl Pts',(-242.609521238975,-4.89105305932652,
130.269246839461));
#136241=CARTESIAN_POINT('Ctrl Pts',(-242.617407577981,-4.90230630263031,
130.408663792091));
#136242=CARTESIAN_POINT('Ctrl Pts',(-242.624891530653,-4.91298536933349,
130.540967244216));
#136243=CARTESIAN_POINT('Ctrl Pts',(-242.632375483325,-4.91830858868205,
130.673747625574));
#136244=CARTESIAN_POINT('Ctrl Pts',(-242.639859435997,-4.91824951337898,
130.806548458368));
#136245=CARTESIAN_POINT('Ctrl Pts',(-242.639859436043,-4.91824951337863,
130.806548459173));
#136246=CARTESIAN_POINT('Ctrl Pts',(-242.648321581103,-4.91818271659492,
130.956707066607));
#136247=CARTESIAN_POINT('Ctrl Pts',(-242.656783726164,-4.91123507379679,
131.106641378728));
#136248=CARTESIAN_POINT('Ctrl Pts',(-242.665245871225,-4.89749280632251,
131.255744350679));
#136249=CARTESIAN_POINT('Ctrl Pts',(-242.673747913812,-4.88368574647396,
131.405550316921));
#136250=CARTESIAN_POINT('Ctrl Pts',(-242.682249956398,-4.86301992565743,
131.55451682982));
#136251=CARTESIAN_POINT('Ctrl Pts',(-242.690751998985,-4.83563325073444,
131.702043260203));
#136252=CARTESIAN_POINT('Ctrl Pts',(-242.699274464072,-4.80818079110469,
131.849924059379));
#136253=CARTESIAN_POINT('Ctrl Pts',(-242.707796929159,-4.77397527050883,
131.996357608693));
#136254=CARTESIAN_POINT('Ctrl Pts',(-242.716319394246,-4.73320459872661,
132.140757747574));
#136255=CARTESIAN_POINT('Ctrl Pts',(-242.724871172668,-4.6922936947056,
132.285654556092));
#136256=CARTESIAN_POINT('Ctrl Pts',(-242.73342295109,-4.64477252547405,
132.428503706896));
#136257=CARTESIAN_POINT('Ctrl Pts',(-242.741974729512,-4.5908783944708,
132.568735472771));
#136258=CARTESIAN_POINT('Ctrl Pts',(-242.746595259595,-4.56175936901203,
132.644502764769));
#136259=CARTESIAN_POINT('Ctrl Pts',(-242.751215789678,-4.53078072435257,
132.719506386205));
#136260=CARTESIAN_POINT('Ctrl Pts',(-242.755836319761,-4.49798541549023,
132.793659555518));
#136261=CARTESIAN_POINT('Ctrl Pts',(-242.76361065388,-4.44280523398341,
132.918426953171));
#136262=CARTESIAN_POINT('Ctrl Pts',(-242.771384987999,-4.38234242490538,
133.04109430975));
#136263=CARTESIAN_POINT('Ctrl Pts',(-242.779159322118,-4.31677845701063,
133.161181954789));
#136264=CARTESIAN_POINT('Ctrl Pts',(-242.786924075065,-4.2512952908467,
133.281121602538));
#136265=CARTESIAN_POINT('Ctrl Pts',(-242.794688828012,-4.18072366012136,
133.398487524675));
#136266=CARTESIAN_POINT('Ctrl Pts',(-242.802453580959,-4.10529307782744,
133.512819922714));
#136267=CARTESIAN_POINT('Ctrl Pts',(-242.810210621844,-4.02993741425145,
133.627038764203));
#136268=CARTESIAN_POINT('Ctrl Pts',(-242.817967662728,-3.94973261693294,
133.738229753248));
#136269=CARTESIAN_POINT('Ctrl Pts',(-242.825724703613,-3.86495392257645,
133.845957934579));
#136270=CARTESIAN_POINT('Ctrl Pts',(-242.833475894853,-3.78023916049298,
133.953604877251));
#136271=CARTESIAN_POINT('Ctrl Pts',(-242.841227086093,-3.69095760762414,
134.05779390391));
#136272=CARTESIAN_POINT('Ctrl Pts',(-242.848978277333,-3.59742738293242,
134.158119596239));
#136273=CARTESIAN_POINT('Ctrl Pts',(-242.85672617411,-3.50393691108082,
134.258402647472));
#136274=CARTESIAN_POINT('Ctrl Pts',(-242.864474070887,-3.40620162504394,
134.354825344856));
#136275=CARTESIAN_POINT('Ctrl Pts',(-242.872221967664,-3.30457929525294,
134.447016069827));
#136276=CARTESIAN_POINT('Ctrl Pts',(-242.879968243748,-3.20297822266261,
134.539187510485));
#136277=CARTESIAN_POINT('Ctrl Pts',(-242.887714519832,-3.09749201297154,
134.627128476993));
#136278=CARTESIAN_POINT('Ctrl Pts',(-242.895460795916,-2.98851430437089,
134.710505176472));
#136279=CARTESIAN_POINT('Ctrl Pts',(-242.903207129181,-2.8795357913217,
134.793882491419));
#136280=CARTESIAN_POINT('Ctrl Pts',(-242.910953462446,-2.76706603844406,
134.872695234542));
#136281=CARTESIAN_POINT('Ctrl Pts',(-242.918699795712,-2.65153035236737,
134.946651029038));
#136282=CARTESIAN_POINT('Ctrl Pts',(-242.926447863714,-2.53596879287502,
135.020623385422));
#136283=CARTESIAN_POINT('Ctrl Pts',(-242.934195931717,-2.41734026315914,
135.089736418084));
#136284=CARTESIAN_POINT('Ctrl Pts',(-242.94194399972,-2.29609717318926,
135.15374227865));
#136285=CARTESIAN_POINT('Ctrl Pts',(-242.949700302462,-2.17472522462039,
135.217816165406));
#136286=CARTESIAN_POINT('Ctrl Pts',(-242.957456605203,-2.05073351116927,
135.276771854312));
#136287=CARTESIAN_POINT('Ctrl Pts',(-242.965212907945,-1.92459756228686,
135.330408262669));
#136288=CARTESIAN_POINT('Ctrl Pts',(-242.972973350459,-1.798394290851,135.384073298392));
#136289=CARTESIAN_POINT('Ctrl Pts',(-242.980733792973,-1.6700448692812,
135.432413258767));
#136290=CARTESIAN_POINT('Ctrl Pts',(-242.988494235487,-1.54004178232462,
135.475276413338));
#136291=CARTESIAN_POINT('Ctrl Pts',(-242.996267135752,-1.40983000287137,
135.518208375651));
#136292=CARTESIAN_POINT('Ctrl Pts',(-243.004040036018,-1.27795962959266,
135.555645856396));
#136293=CARTESIAN_POINT('Ctrl Pts',(-243.011812936283,-1.14493605504428,
135.587487679683));
#136294=CARTESIAN_POINT('Ctrl Pts',(-243.019303272046,-1.01674822247133,
135.618171972495));
#136295=CARTESIAN_POINT('Ctrl Pts',(-243.02679360781,-0.887489878722426,
135.643660317534));
#136296=CARTESIAN_POINT('Ctrl Pts',(-243.034283943573,-0.757617450103246,
135.663907804475));
#136297=CARTESIAN_POINT('Ctrl Pts',(-243.042058277692,-0.622820868903974,
135.684922981035));
#136298=CARTESIAN_POINT('Ctrl Pts',(-243.049832611811,-0.486935722498623,
135.70035860991));
#136299=CARTESIAN_POINT('Ctrl Pts',(-243.05760694593,-0.350463659530369,
135.710108092299));
#136300=CARTESIAN_POINT('Ctrl Pts',(-243.065371698877,-0.214159786182866,
135.719845559323));
#136301=CARTESIAN_POINT('Ctrl Pts',(-243.073136451825,-0.0772708216957249,
135.723910795438));
#136302=CARTESIAN_POINT('Ctrl Pts',(-243.080901204772,0.0596923350623777,
135.722248364113));
#136303=CARTESIAN_POINT('Ctrl Pts',(-243.088658245657,0.196519458082346,
135.720587583938));
#136304=CARTESIAN_POINT('Ctrl Pts',(-243.096415286542,0.333420238322542,
135.713210462005));
#136305=CARTESIAN_POINT('Ctrl Pts',(-243.104172327427,0.469879963433971,
135.700113458801));
#136306=CARTESIAN_POINT('Ctrl Pts',(-243.111923518667,0.606236783205005,
135.68702633215));
#136307=CARTESIAN_POINT('Ctrl Pts',(-243.119674709907,0.742152822271439,
135.668227947003));
#136308=CARTESIAN_POINT('Ctrl Pts',(-243.127425901147,0.877115039649322,
135.64376680735));
#136309=CARTESIAN_POINT('Ctrl Pts',(-243.135173797924,1.01201989448477,
135.619316064334));
#136310=CARTESIAN_POINT('Ctrl Pts',(-243.142921694701,1.14597135004838,
135.589207423374));
#136311=CARTESIAN_POINT('Ctrl Pts',(-243.150669591478,1.27846336946034,
135.553541017956));
#136312=CARTESIAN_POINT('Ctrl Pts',(-243.158415867562,1.41092767439804,
135.517882073181));
#136313=CARTESIAN_POINT('Ctrl Pts',(-243.166162143647,1.54193277312165,
135.476667777916));
#136314=CARTESIAN_POINT('Ctrl Pts',(-243.173908419731,1.67098506517296,
135.430048887918));
#136315=CARTESIAN_POINT('Ctrl Pts',(-243.181654752996,1.80003830985915,
135.383429653789));
#136316=CARTESIAN_POINT('Ctrl Pts',(-243.189401086261,1.92713835139993,
135.331405878148));
#136317=CARTESIAN_POINT('Ctrl Pts',(-243.197147419527,2.05180931628837,
135.274177346705));
#136318=CARTESIAN_POINT('Ctrl Pts',(-243.20489548753,2.17650820037481,135.216935999329));
#136319=CARTESIAN_POINT('Ctrl Pts',(-243.212643555533,2.29877657011188,
135.154487739876));
#136320=CARTESIAN_POINT('Ctrl Pts',(-243.220391623536,2.41816136500342,
135.087079225565));
#136321=CARTESIAN_POINT('Ctrl Pts',(-243.228147926278,2.53767304347551,
135.019599068684));
#136322=CARTESIAN_POINT('Ctrl Pts',(-243.235904229019,2.65429468405046,
134.947148318453));
#136323=CARTESIAN_POINT('Ctrl Pts',(-243.243660531761,2.76760007487659,
134.87001836116));
#136324=CARTESIAN_POINT('Ctrl Pts',(-243.251420974275,2.88096594020166,
134.792847237285));
#136325=CARTESIAN_POINT('Ctrl Pts',(-243.25918141679,2.99101171539257,134.710992163223));
#136326=CARTESIAN_POINT('Ctrl Pts',(-243.266941859304,3.09734354528397,
134.624785466321));
#136327=CARTESIAN_POINT('Ctrl Pts',(-243.274714759569,3.20384606846841,
134.538440382777));
#136328=CARTESIAN_POINT('Ctrl Pts',(-243.282487659835,3.3066224391748,134.447729975776));
#136329=CARTESIAN_POINT('Ctrl Pts',(-243.2902605601,3.40531435823856,134.353024758348));
#136330=CARTESIAN_POINT('Ctrl Pts',(-243.297750895862,3.50041857745495,
134.261762314122));
#136331=CARTESIAN_POINT('Ctrl Pts',(-243.305241231624,3.5917299360932,134.166790681836));
#136332=CARTESIAN_POINT('Ctrl Pts',(-243.312731567386,3.67896394025951,
134.068469590742));
#136333=CARTESIAN_POINT('Ctrl Pts',(-243.320505901506,3.76950544820759,
133.966420625596));
#136334=CARTESIAN_POINT('Ctrl Pts',(-243.328280235625,3.85594112075141,
133.860439937901));
#136335=CARTESIAN_POINT('Ctrl Pts',(-243.336054569744,3.9379101199553,133.750891959611));
#136336=CARTESIAN_POINT('Ctrl Pts',(-243.343819322691,4.01977809969345,
133.641478989414));
#136337=CARTESIAN_POINT('Ctrl Pts',(-243.351584075638,4.09719012697526,
133.528507786113));
#136338=CARTESIAN_POINT('Ctrl Pts',(-243.359348828585,4.16982340815775,
133.412378218596));
#136339=CARTESIAN_POINT('Ctrl Pts',(-243.36710586947,4.24238454894141,133.296363992601));
#136340=CARTESIAN_POINT('Ctrl Pts',(-243.374862910355,4.31017618303581,
133.177197974352));
#136341=CARTESIAN_POINT('Ctrl Pts',(-243.38261995124,4.37291711795113,133.055311292732));
#136342=CARTESIAN_POINT('Ctrl Pts',(-243.39037114248,4.4356107394393,132.933516526806));
#136343=CARTESIAN_POINT('Ctrl Pts',(-243.39812233372,4.49326106466692,132.809005527449));
#136344=CARTESIAN_POINT('Ctrl Pts',(-243.405873524961,4.54563159022945,
132.682236148161));
#136345=CARTESIAN_POINT('Ctrl Pts',(-243.413621421738,4.59797985692164,
132.555520649241));
#136346=CARTESIAN_POINT('Ctrl Pts',(-243.421369318515,4.64505263823946,
132.426549040089));
#136347=CARTESIAN_POINT('Ctrl Pts',(-243.429117215292,4.6866606540257,132.29580118846));
#136348=CARTESIAN_POINT('Ctrl Pts',(-243.436863491376,4.72825996631201,
132.165080686462));
#136349=CARTESIAN_POINT('Ctrl Pts',(-243.44460976746,4.76439666829387,132.032585053343));
#136350=CARTESIAN_POINT('Ctrl Pts',(-243.452356043544,4.79493079195341,
131.898811056315));
#136351=CARTESIAN_POINT('Ctrl Pts',(-243.46010237681,4.82546514100888,131.765036071798));
#136352=CARTESIAN_POINT('Ctrl Pts',(-243.467848710075,4.85039674221636,
131.629983085704));
#136353=CARTESIAN_POINT('Ctrl Pts',(-243.47559504334,4.86963645969658,131.494160452949));
#136354=CARTESIAN_POINT('Ctrl Pts',(-243.483343111343,4.88888048577816,
131.358307403656));
#136355=CARTESIAN_POINT('Ctrl Pts',(-243.491091179346,4.90243003688723,
131.221684751758));
#136356=CARTESIAN_POINT('Ctrl Pts',(-243.498839247349,4.91024774246378,
131.084806994133));
#136357=CARTESIAN_POINT('Ctrl Pts',(-243.506595550091,4.91807375679086,
130.947783761198));
#136358=CARTESIAN_POINT('Ctrl Pts',(-243.514351852833,4.92015573408261,
130.810505271877));
#136359=CARTESIAN_POINT('Ctrl Pts',(-243.522108155575,4.91650844795673,
130.673487611678));
#136360=CARTESIAN_POINT('Ctrl Pts',(-243.529868598089,4.91285921516442,
130.536396821028));
#136361=CARTESIAN_POINT('Ctrl Pts',(-243.537629040603,4.90347465260768,
130.399567526749));
#136362=CARTESIAN_POINT('Ctrl Pts',(-243.545389483117,4.88842146835904,
130.263510721397));
#136363=CARTESIAN_POINT('Ctrl Pts',(-243.553162383383,4.87334411940269,
130.127235505581));
#136364=CARTESIAN_POINT('Ctrl Pts',(-243.560935283648,4.85258002375941,
129.991735643419));
#136365=CARTESIAN_POINT('Ctrl Pts',(-243.568708183914,4.82624723508423,
129.857512853487));
#136366=CARTESIAN_POINT('Ctrl Pts',(-243.576198519676,4.8008717096064,129.728169400059));
#136367=CARTESIAN_POINT('Ctrl Pts',(-243.583688855438,4.77032540537688,
129.600012080907));
#136368=CARTESIAN_POINT('Ctrl Pts',(-243.591179191199,4.73475719690355,
129.473474691248));
#136369=CARTESIAN_POINT('Ctrl Pts',(-243.598953525318,4.69784040899436,
129.342139597997));
#136370=CARTESIAN_POINT('Ctrl Pts',(-243.606727859438,4.6553964472259,129.21213366828));
#136371=CARTESIAN_POINT('Ctrl Pts',(-243.614502193557,4.607536876805,129.083957469643));
#136372=CARTESIAN_POINT('Ctrl Pts',(-243.622266946504,4.55973628902731,
128.955939236717));
#136373=CARTESIAN_POINT('Ctrl Pts',(-243.630031699451,4.50653350781934,
128.829746610883));
#136374=CARTESIAN_POINT('Ctrl Pts',(-243.637796452398,4.44809047635236,
128.705867306477));
#136375=CARTESIAN_POINT('Ctrl Pts',(-243.645553493283,4.38970549132814,
128.582111040743));
#136376=CARTESIAN_POINT('Ctrl Pts',(-243.653310534168,4.32609077934927,
128.460663875366));
#136377=CARTESIAN_POINT('Ctrl Pts',(-243.661067575053,4.25745706994627,
128.341995421243));
#136378=CARTESIAN_POINT('Ctrl Pts',(-243.668818766293,4.18887511775732,
128.223416455924));
#136379=CARTESIAN_POINT('Ctrl Pts',(-243.676569957533,4.11528189663663,
128.107612368065));
#136380=CARTESIAN_POINT('Ctrl Pts',(-243.684321148773,4.03693477583397,
127.995029615679));
#136381=CARTESIAN_POINT('Ctrl Pts',(-243.69206904555,3.95862095464774,127.882494713967));
#136382=CARTESIAN_POINT('Ctrl Pts',(-243.699816942327,3.87555747532189,
127.773178744821));
#136383=CARTESIAN_POINT('Ctrl Pts',(-243.707564839105,3.78804575363947,
127.66750033524));
#136384=CARTESIAN_POINT('Ctrl Pts',(-243.715311115189,3.70055233752269,
127.561844031305));
#136385=CARTESIAN_POINT('Ctrl Pts',(-243.723057391273,3.60861277901759,
127.459824074396));
#136386=CARTESIAN_POINT('Ctrl Pts',(-243.730803667357,3.51256936631723,
127.361826738385));
#136387=CARTESIAN_POINT('Ctrl Pts',(-243.738550000622,3.41652524464635,
127.26382867898));
#136388=CARTESIAN_POINT('Ctrl Pts',(-243.746296333887,3.31637748198778,
127.169853578948));
#136389=CARTESIAN_POINT('Ctrl Pts',(-243.754042667153,3.21250559160844,
127.080251209079));
#136390=CARTESIAN_POINT('Ctrl Pts',(-243.761790735156,3.1086104398393,126.990628773379));
#136391=CARTESIAN_POINT('Ctrl Pts',(-243.769538803159,3.00098979678373,
126.905381271743));
#136392=CARTESIAN_POINT('Ctrl Pts',(-243.777286871162,2.89005632353684,
126.824818243211));
#136393=CARTESIAN_POINT('Ctrl Pts',(-243.785043173904,2.77900494887462,
126.744169591334));
#136394=CARTESIAN_POINT('Ctrl Pts',(-243.792799476646,2.66463402746259,
126.668215588183));
#136395=CARTESIAN_POINT('Ctrl Pts',(-243.800555779387,2.54738574215493,
126.597222761117));
#136396=CARTESIAN_POINT('Ctrl Pts',(-243.808316221902,2.4300748779068,126.526192043042));
#136397=CARTESIAN_POINT('Ctrl Pts',(-243.816076664416,2.30988393213108,
126.460127965506));
#136398=CARTESIAN_POINT('Ctrl Pts',(-243.82383710693,2.1872788746784,126.399250609077));
#136399=CARTESIAN_POINT('Ctrl Pts',(-243.831610007195,2.06447700070312,
126.338275526912));
#136400=CARTESIAN_POINT('Ctrl Pts',(-243.839382907461,1.93925362822435,
126.282503963379));
#136401=CARTESIAN_POINT('Ctrl Pts',(-243.847155807726,1.81209467817496,
126.232107787742));
#136402=CARTESIAN_POINT('Ctrl Pts',(-243.854646143488,1.68955827625325,
126.18354364003));
#136403=CARTESIAN_POINT('Ctrl Pts',(-243.86213647925,1.56522487047215,126.139970949475));
#136404=CARTESIAN_POINT('Ctrl Pts',(-243.869626815012,1.43953989534146,
126.101498940648));
#136405=CARTESIAN_POINT('Ctrl Pts',(-243.877401149132,1.30908953617813,
126.061568253914));
#136406=CARTESIAN_POINT('Ctrl Pts',(-243.88517548325,1.17676986745971,126.027006180441));
#136407=CARTESIAN_POINT('Ctrl Pts',(-243.89294981737,1.04306233456069,125.997989426249));
#136408=CARTESIAN_POINT('Ctrl Pts',(-243.900714570317,0.909519584246181,
125.969008432613));
#136409=CARTESIAN_POINT('Ctrl Pts',(-243.908479323264,0.77459275137802,
125.945559242535));
#136410=CARTESIAN_POINT('Ctrl Pts',(-243.916244076211,0.638779698078696,
125.92776923015));
#136411=CARTESIAN_POINT('Ctrl Pts',(-243.924001117096,0.503101536218538,
125.909996887055));
#136412=CARTESIAN_POINT('Ctrl Pts',(-243.931758157981,0.366539290723279,
125.897872586507));
#136413=CARTESIAN_POINT('Ctrl Pts',(-243.939515198866,0.229601962999908,
125.891472871944));
#136414=CARTESIAN_POINT('Ctrl Pts',(-243.947266390106,0.0927679007807761,
125.885077983455));
#136415=CARTESIAN_POINT('Ctrl Pts',(-243.955017581346,-0.0444402917071382,
125.884399106492));
#136416=CARTESIAN_POINT('Ctrl Pts',(-243.962768772587,-0.181507882327065,
125.889461030478));
#136417=CARTESIAN_POINT('Ctrl Pts',(-243.970516669364,-0.318517215564767,
125.894520803012));
#136418=CARTESIAN_POINT('Ctrl Pts',(-243.978264566141,-0.455385675910752,
125.905316509134));
#136419=CARTESIAN_POINT('Ctrl Pts',(-243.986012462918,-0.591598138021364,
125.92182083733));
#136420=CARTESIAN_POINT('Ctrl Pts',(-243.993758739002,-0.727782107421303,
125.938321713175));
#136421=CARTESIAN_POINT('Ctrl Pts',(-244.001505015086,-0.863309963644738,
125.960528788925));
#136422=CARTESIAN_POINT('Ctrl Pts',(-244.00925129117,-0.997671708415375,
125.988362878288));
#136423=CARTESIAN_POINT('Ctrl Pts',(-244.016997624436,-1.13203444501371,
126.016197173117));
#136424=CARTESIAN_POINT('Ctrl Pts',(-244.024743957701,-1.26523067014577,
126.049658485138));
#136425=CARTESIAN_POINT('Ctrl Pts',(-244.032490290966,-1.39676097555051,
126.088616578745));
#136426=CARTESIAN_POINT('Ctrl Pts',(-244.040238358969,-1.52832073625535,
126.127583396747));
#136427=CARTESIAN_POINT('Ctrl Pts',(-244.047986426972,-1.65821346006871,
126.172049334804));
#136428=CARTESIAN_POINT('Ctrl Pts',(-244.055734494975,-1.78595566962713,
126.221834522864));
#136429=CARTESIAN_POINT('Ctrl Pts',(-244.063490797717,-1.9138336451262,
126.271672623214));
#136430=CARTESIAN_POINT('Ctrl Pts',(-244.071247100459,-2.03955617579538,
126.326841124568));
#136431=CARTESIAN_POINT('Ctrl Pts',(-244.079003403201,-2.16266001398518,
126.387112070517));
#136432=CARTESIAN_POINT('Ctrl Pts',(-244.086763845715,-2.28582955640001,
126.447415184884));
#136433=CARTESIAN_POINT('Ctrl Pts',(-244.094524288229,-2.40637727788154,
126.512825983937));
#136434=CARTESIAN_POINT('Ctrl Pts',(-244.102284730743,-2.52386615032989,
126.583071392967));
#136435=CARTESIAN_POINT('Ctrl Pts',(-244.110057631009,-2.64154362634616,
126.653429566162));
#136436=CARTESIAN_POINT('Ctrl Pts',(-244.117830531274,-2.75615211385458,
126.728637643554));
#136437=CARTESIAN_POINT('Ctrl Pts',(-244.12560343154,-2.86728436224317,
126.808379705633));
#136438=CARTESIAN_POINT('Ctrl Pts',(-244.133093767302,-2.97437667347519,
126.885222942895));
#136439=CARTESIAN_POINT('Ctrl Pts',(-244.140584103063,-3.07824085491587,
126.966276054915));
#136440=CARTESIAN_POINT('Ctrl Pts',(-244.148074438825,-3.17854424460739,
127.051223323571));
#136441=CARTESIAN_POINT('Ctrl Pts',(-244.1557363265,-3.28114489291352,127.138116148059));
#136442=CARTESIAN_POINT('Ctrl Pts',(-244.163398214174,-3.38036457420796,
127.229376101691));
#136443=CARTESIAN_POINT('Ctrl Pts',(-244.171060101849,-3.47580053161289,
127.324706363629));
#136444=CARTESIAN_POINT('Ctrl Pts',(-244.178713190564,-3.57112688977339,
127.419927147705));
#136445=CARTESIAN_POINT('Ctrl Pts',(-244.18636627928,-3.6626778796112,127.519208666794));
#136446=CARTESIAN_POINT('Ctrl Pts',(-244.194019367995,-3.75008272512324,
127.622213132418));
#136447=CARTESIAN_POINT('Ctrl Pts',(-244.201665438334,-3.83740741475088,
127.7251231363));
#136448=CARTESIAN_POINT('Ctrl Pts',(-244.209311508673,-3.9205932611194,
127.831748993263));
#136449=CARTESIAN_POINT('Ctrl Pts',(-244.216957579012,-3.99930578937825,
127.941715640356));
#136450=CARTESIAN_POINT('Ctrl Pts',(-244.224598404901,-4.077964328606,128.051606861175));
#136451=CARTESIAN_POINT('Ctrl Pts',(-244.23223923079,-4.15215541853202,
128.164833988209));
#136452=CARTESIAN_POINT('Ctrl Pts',(-244.239880056679,-4.22158476649726,
128.280988841196));
#136453=CARTESIAN_POINT('Ctrl Pts',(-244.247518062277,-4.29098848752677,
128.397100820486));
#136454=CARTESIAN_POINT('Ctrl Pts',(-244.255156067875,-4.35563375322521,
128.516138032661));
#136455=CARTESIAN_POINT('Ctrl Pts',(-244.262794073473,-4.41526978179896,
128.637663634499));
#136456=CARTESIAN_POINT('Ctrl Pts',(-244.270430409274,-4.47489277292685,
128.759162668782));
#136457=CARTESIAN_POINT('Ctrl Pts',(-244.278066745075,-4.52950853128234,
128.883148647215));
#136458=CARTESIAN_POINT('Ctrl Pts',(-244.285703080875,-4.57891271916398,
129.009161081921));
#136459=CARTESIAN_POINT('Ctrl Pts',(-244.293341233457,-4.62832866092438,
129.135203496574));
#136460=CARTESIAN_POINT('Ctrl Pts',(-244.300979386038,-4.67253040905139,
129.263272954891));
#136461=CARTESIAN_POINT('Ctrl Pts',(-244.308617538619,-4.71136226016039,
129.39289020837));
#136462=CARTESIAN_POINT('Ctrl Pts',(-244.312321481203,-4.7301928537381,
129.455745049208));
#136463=CARTESIAN_POINT('Ctrl Pts',(-244.316025423787,-4.74776144086651,
129.518963618944));
#136464=CARTESIAN_POINT('Ctrl Pts',(-244.319729366371,-4.76405452823392,
129.582490119308));
#136465=CARTESIAN_POINT('Origin',(213.235140564004,0.,130.804360617566));
#136466=CARTESIAN_POINT('',(-246.415426335729,-4.76405452823406,129.582490119308));
#136467=CARTESIAN_POINT('',(-246.069808463078,-4.7640545282341,129.582490119308));
#136468=CARTESIAN_POINT('',(213.235140564004,-4.76405452823405,129.582490119308));
#136469=CARTESIAN_POINT('',(-244.735140564058,-4.91824820735174,130.800161405576));
#136470=CARTESIAN_POINT('Ctrl Pts',(-244.735140564058,-4.91824820735175,
130.800161405576));
#136471=CARTESIAN_POINT('Ctrl Pts',(-244.742787207999,-4.91836323324733,
130.934883326289));
#136472=CARTESIAN_POINT('Ctrl Pts',(-244.750433851939,-4.91293859501576,
131.069798656309));
#136473=CARTESIAN_POINT('Ctrl Pts',(-244.75808049588,-4.90195332618797,
131.204406427911));
#136474=CARTESIAN_POINT('Ctrl Pts',(-244.765720186235,-4.89097804697146,
131.338891792012));
#136475=CARTESIAN_POINT('Ctrl Pts',(-244.773359876591,-4.87445222745457,
131.473069754113));
#136476=CARTESIAN_POINT('Ctrl Pts',(-244.780999566946,-4.85240695352329,
131.606439055064));
#136477=CARTESIAN_POINT('Ctrl Pts',(-244.788634580594,-4.83037517481314,
131.739726712746));
#136478=CARTESIAN_POINT('Ctrl Pts',(-244.796269594241,-4.80283072701636,
131.87220629686));
#136479=CARTESIAN_POINT('Ctrl Pts',(-244.803904607888,-4.7698565121021,
132.003381850263));
#136480=CARTESIAN_POINT('Ctrl Pts',(-244.811537183907,-4.73689282485557,
132.134515523285));
#136481=CARTESIAN_POINT('Ctrl Pts',(-244.819169759926,-4.69850291474428,
132.264345602206));
#136482=CARTESIAN_POINT('Ctrl Pts',(-244.826802335945,-4.65482065723309,
132.392386974871));
#136483=CARTESIAN_POINT('Ctrl Pts',(-244.834434241945,-4.61114223432908,
132.520417107541));
#136484=CARTESIAN_POINT('Ctrl Pts',(-244.842066147945,-4.56217251812639,
132.646658464179));
#136485=CARTESIAN_POINT('Ctrl Pts',(-244.849698053946,-4.50809488256194,
132.770642284144));
#136486=CARTESIAN_POINT('Ctrl Pts',(-244.857331056784,-4.45400947509808,
132.894643922746));
#136487=CARTESIAN_POINT('Ctrl Pts',(-244.864964059622,-4.39481485040865,
133.016387009761));
#136488=CARTESIAN_POINT('Ctrl Pts',(-244.87259706246,-4.33074179636042,
133.135424442466));
#136489=CARTESIAN_POINT('Ctrl Pts',(-244.880237608667,-4.26660542166536,
133.254579514752));
#136490=CARTESIAN_POINT('Ctrl Pts',(-244.887878154874,-4.19758117985893,
133.371023236098));
#136491=CARTESIAN_POINT('Ctrl Pts',(-244.895518701081,-4.12394512553602,
133.484334435361));
#136492=CARTESIAN_POINT('Ctrl Pts',(-244.903162983355,-4.05027306471865,
133.597701041437));
#136493=CARTESIAN_POINT('Ctrl Pts',(-244.91080726563,-3.97198493477172,
133.707931746652));
#136494=CARTESIAN_POINT('Ctrl Pts',(-244.918451547904,-3.88939830704602,
133.814636995517));
#136495=CARTESIAN_POINT('Ctrl Pts',(-244.92610796819,-3.8066805437355,133.921511676838));
#136496=CARTESIAN_POINT('Ctrl Pts',(-244.933764388476,-3.71965090705499,
134.024849409731));
#136497=CARTESIAN_POINT('Ctrl Pts',(-244.941420808762,-3.62866566174346,
134.124295643705));
#136498=CARTESIAN_POINT('Ctrl Pts',(-244.948889977209,-3.5399056279364,
134.221309737136));
#136499=CARTESIAN_POINT('Ctrl Pts',(-244.956359145657,-3.44738152776796,
134.314620289459));
#136500=CARTESIAN_POINT('Ctrl Pts',(-244.963828314104,-3.35145398099632,
134.403935491876));
#136501=CARTESIAN_POINT('Ctrl Pts',(-244.971602648223,-3.25160714997087,
134.496899819891));
#136502=CARTESIAN_POINT('Ctrl Pts',(-244.979376982342,-3.14773119990663,
134.585853845381));
#136503=CARTESIAN_POINT('Ctrl Pts',(-244.987151316461,-3.04018179869569,
134.670428088961));
#136504=CARTESIAN_POINT('Ctrl Pts',(-244.994916069408,-2.93276494250978,
134.754898102344));
#136505=CARTESIAN_POINT('Ctrl Pts',(-245.002680822355,-2.82168394733032,
134.834998834259));
#136506=CARTESIAN_POINT('Ctrl Pts',(-245.010445575302,-2.70733082073511,
134.910397988268));
#136507=CARTESIAN_POINT('Ctrl Pts',(-245.018202616187,-2.59309127127702,
134.985722254774));
#136508=CARTESIAN_POINT('Ctrl Pts',(-245.025959657072,-2.47558638219273,
135.056354022414));
#136509=CARTESIAN_POINT('Ctrl Pts',(-245.033716697957,-2.35524041036667,
135.122001833771));
#136510=CARTESIAN_POINT('Ctrl Pts',(-245.041467889198,-2.23498519237462,
135.187600139603));
#136511=CARTESIAN_POINT('Ctrl Pts',(-245.049219080438,-2.11189349795492,
135.248221783632));
#136512=CARTESIAN_POINT('Ctrl Pts',(-245.056970271678,-1.98641737332774,
135.303619343339));
#136513=CARTESIAN_POINT('Ctrl Pts',(-245.064718168455,-1.8609945794009,
135.358993357605));
#136514=CARTESIAN_POINT('Ctrl Pts',(-245.072466065232,-1.73318972784394,
135.409147546131));
#136515=CARTESIAN_POINT('Ctrl Pts',(-245.080213962009,-1.6034780060183,
135.453881167764));
#136516=CARTESIAN_POINT('Ctrl Pts',(-245.087960238093,-1.47379341708825,
135.498605432089));
#136517=CARTESIAN_POINT('Ctrl Pts',(-245.095706514178,-1.34220312064503,
135.537911257458));
#136518=CARTESIAN_POINT('Ctrl Pts',(-245.103452790262,-1.20920038199867,
135.571646795118));
#136519=CARTESIAN_POINT('Ctrl Pts',(-245.111199123527,-1.07619666155649,
135.605382581805));
#136520=CARTESIAN_POINT('Ctrl Pts',(-245.118945456792,-0.941780857070866,
135.633547902612));
#136521=CARTESIAN_POINT('Ctrl Pts',(-245.126691790058,-0.806459038047317,
135.656041448211));
#136522=CARTESIAN_POINT('Ctrl Pts',(-245.134439858061,-0.671106914640469,
135.678540031084));
#136523=CARTESIAN_POINT('Ctrl Pts',(-245.142187926064,-0.534848758556416,
135.695364247193));
#136524=CARTESIAN_POINT('Ctrl Pts',(-245.149935994067,-0.39819802172141,
135.706464390233));
#136525=CARTESIAN_POINT('Ctrl Pts',(-245.157692296809,-0.261402050856946,
135.717576330637));
#136526=CARTESIAN_POINT('Ctrl Pts',(-245.16544859955,-0.124213056063751,
135.722952013597));
#136527=CARTESIAN_POINT('Ctrl Pts',(-245.173204902292,0.0128526712454422,
135.722593823845));
#136528=CARTESIAN_POINT('Ctrl Pts',(-245.180965344807,0.149991554660269,
135.722235442916));
#136529=CARTESIAN_POINT('Ctrl Pts',(-245.188725787321,0.2870066491084,135.716137108664));
#136530=CARTESIAN_POINT('Ctrl Pts',(-245.196486229835,0.423385508378977,
135.70435324754));
#136531=CARTESIAN_POINT('Ctrl Pts',(-245.2042591301,0.559983295101601,135.692550469915));
#136532=CARTESIAN_POINT('Ctrl Pts',(-245.212032030366,0.695942417694476,
135.675043976896));
#136533=CARTESIAN_POINT('Ctrl Pts',(-245.219804930631,0.830758469100371,
135.651939748278));
#136534=CARTESIAN_POINT('Ctrl Pts',(-245.227295266393,0.96067361744886,
135.629675416569));
#136535=CARTESIAN_POINT('Ctrl Pts',(-245.234785602155,1.08952705753159,
135.602213331212));
#136536=CARTESIAN_POINT('Ctrl Pts',(-245.242275937916,1.21688154647621,
135.569691913955));
#136537=CARTESIAN_POINT('Ctrl Pts',(-245.250050272035,1.34906471958535,
135.535937437276));
#136538=CARTESIAN_POINT('Ctrl Pts',(-245.257824606155,1.48005174885979,
135.496625482168));
#136539=CARTESIAN_POINT('Ctrl Pts',(-245.265598940274,1.60933953364511,
135.451855569467));
#136540=CARTESIAN_POINT('Ctrl Pts',(-245.273363693221,1.7384679827901,135.407140831683));
#136541=CARTESIAN_POINT('Ctrl Pts',(-245.281128446168,1.86590098831853,
135.35698164663));
#136542=CARTESIAN_POINT('Ctrl Pts',(-245.288893199115,1.9911470901556,135.301528207046));
#136543=CARTESIAN_POINT('Ctrl Pts',(-245.29665024,2.11626879579832,135.246129844599));
#136544=CARTESIAN_POINT('Ctrl Pts',(-245.304407280885,2.23920756507533,
135.185447849188));
#136545=CARTESIAN_POINT('Ctrl Pts',(-245.31216432177,2.35948886539747,135.119681620292));
#136546=CARTESIAN_POINT('Ctrl Pts',(-245.31991551301,2.47967946065555,135.05396498622));
#136547=CARTESIAN_POINT('Ctrl Pts',(-245.32766670425,2.59721623418635,134.983171936931));
#136548=CARTESIAN_POINT('Ctrl Pts',(-245.33541789549,2.71164668039344,134.907549053796));
#136549=CARTESIAN_POINT('Ctrl Pts',(-245.343165792268,2.82602849060851,
134.831958312404));
#136550=CARTESIAN_POINT('Ctrl Pts',(-245.350913689045,2.9373062739293,134.75154203515));
#136551=CARTESIAN_POINT('Ctrl Pts',(-245.358661585822,3.04505429076332,
134.666591505124));
#136552=CARTESIAN_POINT('Ctrl Pts',(-245.366407861906,3.15277976903499,
134.581658744917));
#136553=CARTESIAN_POINT('Ctrl Pts',(-245.37415413799,3.25697664261577,134.492193860399));
#136554=CARTESIAN_POINT('Ctrl Pts',(-245.381900414074,3.35725053489967,
134.398529771684));
#136555=CARTESIAN_POINT('Ctrl Pts',(-245.389646747339,3.45752516738281,
134.304864991563));
#136556=CARTESIAN_POINT('Ctrl Pts',(-245.397393080605,3.55387647507396,
134.207001212268));
#136557=CARTESIAN_POINT('Ctrl Pts',(-245.40513941387,3.64594568063828,134.105309444242));
#136558=CARTESIAN_POINT('Ctrl Pts',(-245.412887481873,3.73803550446295,
134.00359490305));
#136559=CARTESIAN_POINT('Ctrl Pts',(-245.420635549876,3.82584105561582,
133.898050957066));
#136560=CARTESIAN_POINT('Ctrl Pts',(-245.428383617879,3.90904298146711,
133.789082720466));
#136561=CARTESIAN_POINT('Ctrl Pts',(-245.436139920621,3.99233333531543,
133.679998671128));
#136562=CARTESIAN_POINT('Ctrl Pts',(-245.443896223363,4.07101005234948,
133.567483372362));
#136563=CARTESIAN_POINT('Ctrl Pts',(-245.451652526105,4.14479607079393,
133.451972483764));
#136564=CARTESIAN_POINT('Ctrl Pts',(-245.459412968619,4.21862147105788,
133.336399943527));
#136565=CARTESIAN_POINT('Ctrl Pts',(-245.467173411133,4.28755077506701,
133.217828965476));
#136566=CARTESIAN_POINT('Ctrl Pts',(-245.474933853648,4.35135278364091,
133.096720103947));
#136567=CARTESIAN_POINT('Ctrl Pts',(-245.482706753913,4.41525721286305,
132.975416827722));
#136568=CARTESIAN_POINT('Ctrl Pts',(-245.490479654179,4.47401773122411,
132.851567880226));
#136569=CARTESIAN_POINT('Ctrl Pts',(-245.498252554444,4.52745085819272,
132.72565491807));
#136570=CARTESIAN_POINT('Ctrl Pts',(-245.505742890206,4.57894155640422,
132.604319209249));
#136571=CARTESIAN_POINT('Ctrl Pts',(-245.513233225968,4.62548535801299,
132.481067232852));
#136572=CARTESIAN_POINT('Ctrl Pts',(-245.520723561729,4.66696238070201,
132.356341674027));
#136573=CARTESIAN_POINT('Ctrl Pts',(-245.528497895849,4.71001201731434,
132.226887107725));
#136574=CARTESIAN_POINT('Ctrl Pts',(-245.536272229967,4.74773944496779,
132.095434938267));
#136575=CARTESIAN_POINT('Ctrl Pts',(-245.544046564087,4.77995645516916,
131.962462231928));
#136576=CARTESIAN_POINT('Ctrl Pts',(-245.551811317034,4.81213376078468,
131.829653402564));
#136577=CARTESIAN_POINT('Ctrl Pts',(-245.559576069981,4.83881407003022,
131.695328141197));
#136578=CARTESIAN_POINT('Ctrl Pts',(-245.567340822928,4.85985809813354,
131.559981109947));
#136579=CARTESIAN_POINT('Ctrl Pts',(-245.575097863813,4.88088122501143,
131.424768507277));
#136580=CARTESIAN_POINT('Ctrl Pts',(-245.582854904698,4.89627915140953,
131.288536538118));
#136581=CARTESIAN_POINT('Ctrl Pts',(-245.590611945583,4.90596314130119,
131.151792220467));
#136582=CARTESIAN_POINT('Ctrl Pts',(-245.598363136823,4.91563982842079,
131.015151022768));
#136583=CARTESIAN_POINT('Ctrl Pts',(-245.606114328063,4.9196111281792,130.877998634025));
#136584=CARTESIAN_POINT('Ctrl Pts',(-245.613865519303,4.91783990614071,
130.740849043267));
#136585=CARTESIAN_POINT('Ctrl Pts',(-245.62161341608,4.91606943691884,130.603757744744));
#136586=CARTESIAN_POINT('Ctrl Pts',(-245.629361312857,4.90856130535406,
130.466669631953));
#136587=CARTESIAN_POINT('Ctrl Pts',(-245.637109209634,4.89533045350976,
130.330100337298));
#136588=CARTESIAN_POINT('Ctrl Pts',(-245.644855485718,4.88210236927443,
130.193559609995));
#136589=CARTESIAN_POINT('Ctrl Pts',(-245.652601761802,4.86315398347323,
130.05753787386));
#136590=CARTESIAN_POINT('Ctrl Pts',(-245.660348037887,4.83855222103871,
129.922546880555));
#136591=CARTESIAN_POINT('Ctrl Pts',(-245.668094371152,4.81395027699961,
129.787554890777));
#136592=CARTESIAN_POINT('Ctrl Pts',(-245.675840704417,4.78369494315194,
129.653594043642));
#136593=CARTESIAN_POINT('Ctrl Pts',(-245.683587037682,4.74790443317498,
129.521166728889));
#136594=CARTESIAN_POINT('Ctrl Pts',(-245.691335105685,4.71210590816133,
129.388709757957));
#136595=CARTESIAN_POINT('Ctrl Pts',(-245.699083173688,4.67076984241394,
129.257787380131));
#136596=CARTESIAN_POINT('Ctrl Pts',(-245.706831241691,4.62406445206503,
129.128887249933));
#136597=CARTESIAN_POINT('Ctrl Pts',(-245.714587544433,4.57730942267152,
128.999850123142));
#136598=CARTESIAN_POINT('Ctrl Pts',(-245.722343847175,4.52517380256445,
128.87283990554));
#136599=CARTESIAN_POINT('Ctrl Pts',(-245.730100149917,4.46787436584216,
128.748325181697));
#136600=CARTESIAN_POINT('Ctrl Pts',(-245.737860592431,4.41054434668524,
128.623744000596));
#136601=CARTESIAN_POINT('Ctrl Pts',(-245.745621034945,4.34804519725599,
128.501661315061));
#136602=CARTESIAN_POINT('Ctrl Pts',(-245.753381477459,4.28063942615653,
128.382520580376));
#136603=CARTESIAN_POINT('Ctrl Pts',(-245.761154377725,4.2131254493293,128.263188590408));
#136604=CARTESIAN_POINT('Ctrl Pts',(-245.76892727799,4.140689317697,128.146808320826));
#136605=CARTESIAN_POINT('Ctrl Pts',(-245.776700178256,4.06363708689892,
128.033794486163));
#136606=CARTESIAN_POINT('Ctrl Pts',(-245.784190514018,3.9893858987707,127.92488898905));
#136607=CARTESIAN_POINT('Ctrl Pts',(-245.79168084978,3.91084858201084,127.819109666721));
#136608=CARTESIAN_POINT('Ctrl Pts',(-245.799171185542,3.82833278085045,
127.7167966617));
#136609=CARTESIAN_POINT('Ctrl Pts',(-245.806945519661,3.74268836801147,
127.610604427999));
#136610=CARTESIAN_POINT('Ctrl Pts',(-245.81471985378,3.65248653111821,127.507810166128));
#136611=CARTESIAN_POINT('Ctrl Pts',(-245.8224941879,3.55802690824946,127.408830087196));
#136612=CARTESIAN_POINT('Ctrl Pts',(-245.830258940847,3.46368369842405,
127.309971992366));
#136613=CARTESIAN_POINT('Ctrl Pts',(-245.838023693794,3.36509341059598,
127.214919007726));
#136614=CARTESIAN_POINT('Ctrl Pts',(-245.845788446741,3.26259693119686,
127.124055694459));
#136615=CARTESIAN_POINT('Ctrl Pts',(-245.853545487626,3.16020225274574,
127.033282627916));
#136616=CARTESIAN_POINT('Ctrl Pts',(-245.861302528511,3.05390939413526,
126.946691209363));
#136617=CARTESIAN_POINT('Ctrl Pts',(-245.869059569396,2.94409695997478,
126.864630150546));
#136618=CARTESIAN_POINT('Ctrl Pts',(-245.876810760636,2.83436733622586,
126.782630974612));
#136619=CARTESIAN_POINT('Ctrl Pts',(-245.884561951876,2.7211237317431,126.705155591403));
#136620=CARTESIAN_POINT('Ctrl Pts',(-245.892313143116,2.60477850798382,
126.632513066798));
#136621=CARTESIAN_POINT('Ctrl Pts',(-245.900061039893,2.48848273404778,
126.559901417204));
#136622=CARTESIAN_POINT('Ctrl Pts',(-245.90780893667,2.36908829371289,126.492118747404));
#136623=CARTESIAN_POINT('Ctrl Pts',(-245.915556833448,2.24703707967212,
126.429431198126));
#136624=CARTESIAN_POINT('Ctrl Pts',(-245.923303109532,2.12501139611388,
126.366756761732));
#136625=CARTESIAN_POINT('Ctrl Pts',(-245.931049385616,2.00033039180147,
126.309175504456));
#136626=CARTESIAN_POINT('Ctrl Pts',(-245.9387956617,1.87346079246246,126.256907734731));
#136627=CARTESIAN_POINT('Ctrl Pts',(-245.946541994965,1.74659025660072,
126.204639579177));
#136628=CARTESIAN_POINT('Ctrl Pts',(-245.954288328231,1.61753145496436,
126.157685138366));
#136629=CARTESIAN_POINT('Ctrl Pts',(-245.962034661496,1.4867709596506,126.116216509708));
#136630=CARTESIAN_POINT('Ctrl Pts',(-245.969782729499,1.35598118143071,
126.074738594439));
#136631=CARTESIAN_POINT('Ctrl Pts',(-245.977530797502,1.2234893238255,126.038749054079));
#136632=CARTESIAN_POINT('Ctrl Pts',(-245.985278865505,1.08979658932149,
126.008369952812));
#136633=CARTESIAN_POINT('Ctrl Pts',(-245.993035168247,0.955961764588458,
125.977958564275));
#136634=CARTESIAN_POINT('Ctrl Pts',(-246.000791470989,0.820923895251775,
125.953169613018));
#136635=CARTESIAN_POINT('Ctrl Pts',(-246.008547773731,0.685194386477115,
125.934074002259));
#136636=CARTESIAN_POINT('Ctrl Pts',(-246.016308216245,0.549392434776516,
125.914968199597));
#136637=CARTESIAN_POINT('Ctrl Pts',(-246.024068658759,0.412898496980256,
125.901561830513));
#136638=CARTESIAN_POINT('Ctrl Pts',(-246.031829101273,0.27622755689187,
125.893873737499));
#136639=CARTESIAN_POINT('Ctrl Pts',(-246.039602001539,0.13933722047775,
125.886173302875));
#136640=CARTESIAN_POINT('Ctrl Pts',(-246.047374901804,0.00226970511973851,
125.884209493461));
#136641=CARTESIAN_POINT('Ctrl Pts',(-246.05514780207,-0.134460647553049,
125.887948979312));
#136642=CARTESIAN_POINT('Ctrl Pts',(-246.062638137831,-0.266220507501721,
125.891552525433));
#136643=CARTESIAN_POINT('Ctrl Pts',(-246.070128473593,-0.397666985286885,
125.900451886793));
#136644=CARTESIAN_POINT('Ctrl Pts',(-246.077618809355,-0.528347620148437,
125.91457208893));
#136645=CARTESIAN_POINT('Ctrl Pts',(-246.085393143474,-0.663983051000893,
125.929227662822));
#136646=CARTESIAN_POINT('Ctrl Pts',(-246.093167477593,-0.799223070939665,
125.949554213418));
#136647=CARTESIAN_POINT('Ctrl Pts',(-246.100941811712,-0.933555548070249,
125.975524618988));
#136648=CARTESIAN_POINT('Ctrl Pts',(-246.10870656466,-1.06772247242841,
126.001463018353));
#136649=CARTESIAN_POINT('Ctrl Pts',(-246.116471317607,-1.20098369921872,
126.033031359728));
#136650=CARTESIAN_POINT('Ctrl Pts',(-246.124236070554,-1.33283142878319,
126.070150710417));
#136651=CARTESIAN_POINT('Ctrl Pts',(-246.131993111439,-1.46454820532394,
126.107233193643));
#136652=CARTESIAN_POINT('Ctrl Pts',(-246.139750152324,-1.59485390457379,
126.149855609121));
#136653=CARTESIAN_POINT('Ctrl Pts',(-246.147507193208,-1.72325050042752,
126.197887913286));
#136654=CARTESIAN_POINT('Ctrl Pts',(-246.155258384449,-1.85155027140936,
126.245883995916));
#136655=CARTESIAN_POINT('Ctrl Pts',(-246.163009575689,-1.97794343987086,
126.299281710527));
#136656=CARTESIAN_POINT('Ctrl Pts',(-246.170760766929,-2.10194708849594,
126.357901183402));
#136657=CARTESIAN_POINT('Ctrl Pts',(-246.178508663706,-2.22589803226261,
126.416495741438));
#136658=CARTESIAN_POINT('Ctrl Pts',(-246.186256560483,-2.3474611234418,
126.480307476806));
#136659=CARTESIAN_POINT('Ctrl Pts',(-246.19400445726,-2.46617359650813,
126.549108468235));
#136660=CARTESIAN_POINT('Ctrl Pts',(-246.201750733344,-2.58486123748424,
126.617895067979));
#136661=CARTESIAN_POINT('Ctrl Pts',(-246.209497009428,-2.70069910834935,
126.691668651998));
#136662=CARTESIAN_POINT('Ctrl Pts',(-246.217243285512,-2.8132495807237,
126.770155632807));
#136663=CARTESIAN_POINT('Ctrl Pts',(-246.224989618777,-2.92580088392023,
126.848643192988));
#136664=CARTESIAN_POINT('Ctrl Pts',(-246.232735952043,-3.03506441951327,
126.931843995755));
#136665=CARTESIAN_POINT('Ctrl Pts',(-246.240482285308,-3.14063239297462,
127.019441697074));
#136666=CARTESIAN_POINT('Ctrl Pts',(-246.248230353311,-3.24622400765125,
127.10705901529));
#136667=CARTESIAN_POINT('Ctrl Pts',(-246.255978421314,-3.34811811256095,
127.199074941799));
#136668=CARTESIAN_POINT('Ctrl Pts',(-246.263726489317,-3.44594109946291,
127.295133779425));
#136669=CARTESIAN_POINT('Ctrl Pts',(-246.271482792058,-3.54386805379986,
127.391294709527));
#136670=CARTESIAN_POINT('Ctrl Pts',(-246.2792390948,-3.63771496741181,127.491506859811));
#136671=CARTESIAN_POINT('Ctrl Pts',(-246.286995397542,-3.72714576042953,
127.59537829555));
#136672=CARTESIAN_POINT('Ctrl Pts',(-246.294755840056,-3.81662428535419,
127.699305170601));
#136673=CARTESIAN_POINT('Ctrl Pts',(-246.30251628257,-3.90168175078138,
127.806894916218));
#136674=CARTESIAN_POINT('Ctrl Pts',(-246.310276725084,-3.98202394266324,
127.917724446768));
#136675=CARTESIAN_POINT('Ctrl Pts',(-246.31804962535,-4.06249510696395,
128.02873189072));
#136676=CARTESIAN_POINT('Ctrl Pts',(-246.325822525615,-4.13823565555365,
128.142989186386));
#136677=CARTESIAN_POINT('Ctrl Pts',(-246.33359542588,-4.20899561564361,
128.260045587938));
#136678=CARTESIAN_POINT('Ctrl Pts',(-246.341085761643,-4.2771832729557,
128.372846694454));
#136679=CARTESIAN_POINT('Ctrl Pts',(-246.348576097405,-4.34074602020749,
128.488246661174));
#136680=CARTESIAN_POINT('Ctrl Pts',(-246.356066433168,-4.39950236944441,
128.60582429452));
#136681=CARTESIAN_POINT('Ctrl Pts',(-246.364388978553,-4.46478681045179,
128.736465325959));
#136682=CARTESIAN_POINT('Ctrl Pts',(-246.372711523939,-4.52432198526346,
128.870163383883));
#136683=CARTESIAN_POINT('Ctrl Pts',(-246.381034069324,-4.57783157591476,
129.006405911502));
#136684=CARTESIAN_POINT('Ctrl Pts',(-246.389336263648,-4.63121031994061,
129.142315286227));
#136685=CARTESIAN_POINT('Ctrl Pts',(-246.397638457972,-4.67859274881165,
129.280756439759));
#136686=CARTESIAN_POINT('Ctrl Pts',(-246.405940652296,-4.71974943304564,
129.42119455676));
#136687=CARTESIAN_POINT('Ctrl Pts',(-246.409102546774,-4.7354239749219,
129.474680477381));
#136688=CARTESIAN_POINT('Ctrl Pts',(-246.412264441251,-4.75019596795281,
129.528455803105));
#136689=CARTESIAN_POINT('Ctrl Pts',(-246.415426335729,-4.76405452823406,
129.582490119308));
#136690=CARTESIAN_POINT('Ctrl Pts',(-244.66511323982,-4.76405452823407,
129.582490119308));
#136691=CARTESIAN_POINT('Ctrl Pts',(-244.671869056643,-4.79358206285183,
129.69761752864));
#136692=CARTESIAN_POINT('Ctrl Pts',(-244.678624873467,-4.81889935167107,
129.813680728645));
#136693=CARTESIAN_POINT('Ctrl Pts',(-244.685380690291,-4.83996702755722,
129.930345609309));
#136694=CARTESIAN_POINT('Ctrl Pts',(-244.697240193739,-4.87695029417567,
130.135145057045));
#136695=CARTESIAN_POINT('Ctrl Pts',(-244.709099697187,-4.90094261302808,
130.342356399354));
#136696=CARTESIAN_POINT('Ctrl Pts',(-244.720959200635,-4.91170190698836,
130.550653228263));
#136697=CARTESIAN_POINT('Ctrl Pts',(-244.725686321761,-4.91599049175143,
130.633678992774));
#136698=CARTESIAN_POINT('Ctrl Pts',(-244.730413442888,-4.91817709884299,
130.716876915213));
#136699=CARTESIAN_POINT('Ctrl Pts',(-244.735140564014,-4.91824820735108,
130.800161404793));
#136700=CARTESIAN_POINT('',(-244.389859435961,-4.91824876256771,130.807849457083));
#136701=CARTESIAN_POINT('Ctrl Pts',(-244.319729366371,-4.76405452823392,
129.582490119308));
#136702=CARTESIAN_POINT('Ctrl Pts',(-244.327373776998,-4.79768114295139,
129.713599779736));
#136703=CARTESIAN_POINT('Ctrl Pts',(-244.335018187624,-4.82587144870702,
129.846021477176));
#136704=CARTESIAN_POINT('Ctrl Pts',(-244.342662598251,-4.84854502652125,
129.979258085576));
#136705=CARTESIAN_POINT('Ctrl Pts',(-244.350528737869,-4.87187625994725,
130.116359271677));
#136706=CARTESIAN_POINT('Ctrl Pts',(-244.358394877488,-4.88936580544387,
130.254322902373));
#136707=CARTESIAN_POINT('Ctrl Pts',(-244.366261017106,-4.90098345999153,
130.392603180002));
#136708=CARTESIAN_POINT('Ctrl Pts',(-244.374127156724,-4.91260111453918,
130.53088345763));
#136709=CARTESIAN_POINT('Ctrl Pts',(-244.381993296342,-4.91834691724198,
130.669479921059));
#136710=CARTESIAN_POINT('Ctrl Pts',(-244.389859435961,-4.91824876256771,
130.807849457083));
#136711=CARTESIAN_POINT('Ctrl Pts',(-244.389859435997,-4.91824876256727,
130.807849457707));
#136712=CARTESIAN_POINT('Ctrl Pts',(-244.402080311544,-4.91809626892601,
131.022821090721));
#136713=CARTESIAN_POINT('Ctrl Pts',(-244.414301187091,-4.90384922761825,
131.237299465543));
#136714=CARTESIAN_POINT('Ctrl Pts',(-244.426522062639,-4.8757015042787,
131.449897528729));
#136715=CARTESIAN_POINT('Ctrl Pts',(-244.434296396758,-4.85779527447666,
131.585142206566));
#136716=CARTESIAN_POINT('Ctrl Pts',(-244.442070730877,-4.83422918984339,
131.719855499553));
#136717=CARTESIAN_POINT('Ctrl Pts',(-244.449845064996,-4.80504265405272,
131.853526074124));
#136718=CARTESIAN_POINT('Ctrl Pts',(-244.457609817943,-4.77589208805894,
131.987031911658));
#136719=CARTESIAN_POINT('Ctrl Pts',(-244.46537457089,-4.74113493558406,
132.119497209358));
#136720=CARTESIAN_POINT('Ctrl Pts',(-244.473139323837,-4.70086229238518,
132.250416207967));
#136721=CARTESIAN_POINT('Ctrl Pts',(-244.480896364722,-4.66062964854326,
132.381205175981));
#136722=CARTESIAN_POINT('Ctrl Pts',(-244.488653405607,-4.61489252977729,
132.510450529961));
#136723=CARTESIAN_POINT('Ctrl Pts',(-244.496410446492,-4.56379289345655,
132.637657507907));
#136724=CARTESIAN_POINT('Ctrl Pts',(-244.504161637732,-4.51273179176927,
132.764768558082));
#136725=CARTESIAN_POINT('Ctrl Pts',(-244.511912828972,-4.45631636684135,
132.889843930516));
#136726=CARTESIAN_POINT('Ctrl Pts',(-244.519664020212,-4.39473802927427,
133.012405163437));
#136727=CARTESIAN_POINT('Ctrl Pts',(-244.527411916989,-4.33318586414306,
133.134914304565));
#136728=CARTESIAN_POINT('Ctrl Pts',(-244.535159813766,-4.26647532597446,
133.254911082877));
#136729=CARTESIAN_POINT('Ctrl Pts',(-244.542907710543,-4.19484537550331,
133.371938335595));
#136730=CARTESIAN_POINT('Ctrl Pts',(-244.550653986627,-4.12323040847365,
133.488941108735));
#136731=CARTESIAN_POINT('Ctrl Pts',(-244.558400262711,-4.04669827992298,
133.602975258555));
#136732=CARTESIAN_POINT('Ctrl Pts',(-244.566146538795,-3.96553300042325,
133.713609848047));
#136733=CARTESIAN_POINT('Ctrl Pts',(-244.573892872061,-3.88436712177997,
133.824245254218));
#136734=CARTESIAN_POINT('Ctrl Pts',(-244.581639205326,-3.79856825520651,
133.931480734756));
#136735=CARTESIAN_POINT('Ctrl Pts',(-244.589385538591,-3.70846243958028,
134.034916203951));
#136736=CARTESIAN_POINT('Ctrl Pts',(-244.597133606594,-3.61833644538152,
134.138374836802));
#136737=CARTESIAN_POINT('Ctrl Pts',(-244.604881674597,-3.52390183962061,
134.238031470206));
#136738=CARTESIAN_POINT('Ctrl Pts',(-244.6126297426,-3.42552318260732,134.333521139265));
#136739=CARTESIAN_POINT('Ctrl Pts',(-244.620386045342,-3.32703996758649,
134.429112295881));
#136740=CARTESIAN_POINT('Ctrl Pts',(-244.628142348084,-3.22460460876199,
134.520527368608));
#136741=CARTESIAN_POINT('Ctrl Pts',(-244.635898650826,-3.11861699298481,
134.607439779714));
#136742=CARTESIAN_POINT('Ctrl Pts',(-244.64365909334,-3.01257280842588,
134.694398578591));
#136743=CARTESIAN_POINT('Ctrl Pts',(-244.651419535854,-2.90297290135563,
134.776849692332));
#136744=CARTESIAN_POINT('Ctrl Pts',(-244.659179978368,-2.79024729589318,
134.854509144504));
#136745=CARTESIAN_POINT('Ctrl Pts',(-244.666952878634,-2.67734073328153,
134.932293262524));
#136746=CARTESIAN_POINT('Ctrl Pts',(-244.674725778899,-2.56129877656639,
135.005270139652));
#136747=CARTESIAN_POINT('Ctrl Pts',(-244.682498679164,-2.44257804042975,
135.073200691744));
#136748=CARTESIAN_POINT('Ctrl Pts',(-244.689989014927,-2.3281731020886,
135.138661797162));
#136749=CARTESIAN_POINT('Ctrl Pts',(-244.697479350689,-2.21128103703968,
135.199436958901));
#136750=CARTESIAN_POINT('Ctrl Pts',(-244.704969686451,-2.0923272727801,
135.255354848755));
#136751=CARTESIAN_POINT('Ctrl Pts',(-244.71274402057,-1.968863340396,135.313392882398));
#136752=CARTESIAN_POINT('Ctrl Pts',(-244.720518354689,-1.8427871873494,
135.366381893384));
#136753=CARTESIAN_POINT('Ctrl Pts',(-244.728292688808,-1.71455031169962,
135.414078644859));
#136754=CARTESIAN_POINT('Ctrl Pts',(-244.736057441755,-1.58647147653822,
135.46171661435));
#136755=CARTESIAN_POINT('Ctrl Pts',(-244.743822194702,-1.45623758006734,
135.504075166652));
#136756=CARTESIAN_POINT('Ctrl Pts',(-244.75158694765,-1.32432337135576,
135.54095756797));
#136757=CARTESIAN_POINT('Ctrl Pts',(-244.759343988535,-1.19254018169593,
135.577803337168));
#136758=CARTESIAN_POINT('Ctrl Pts',(-244.767101029419,-1.05908037508984,
135.609183674628));
#136759=CARTESIAN_POINT('Ctrl Pts',(-244.774858070304,-0.924436940245247,
135.634950582157));
#136760=CARTESIAN_POINT('Ctrl Pts',(-244.782609261545,-0.78989504106243,
135.660698058662));
#136761=CARTESIAN_POINT('Ctrl Pts',(-244.790360452785,-0.654171672717092,
135.680840457839));
#136762=CARTESIAN_POINT('Ctrl Pts',(-244.798111644025,-0.517772840756482,
135.695280198573));
#136763=CARTESIAN_POINT('Ctrl Pts',(-244.805859540802,-0.381431981937829,
135.709713802032));
#136764=CARTESIAN_POINT('Ctrl Pts',(-244.813607437579,-0.244416618482797,
135.718449526692));
#136765=CARTESIAN_POINT('Ctrl Pts',(-244.821355334356,-0.107240538498359,
135.721441309339));
#136766=CARTESIAN_POINT('Ctrl Pts',(-244.82910161044,0.0299068472073198,
135.724432466169));
#136767=CARTESIAN_POINT('Ctrl Pts',(-244.836847886524,0.167214491948882,
135.721682062334));
#136768=CARTESIAN_POINT('Ctrl Pts',(-244.844594162608,0.304166321564958,
135.713196111991));
#136769=CARTESIAN_POINT('Ctrl Pts',(-244.852340495874,0.441119162128515,
135.704710099007));
#136770=CARTESIAN_POINT('Ctrl Pts',(-244.860086829139,0.577715792108683,
135.690488479211));
#136771=CARTESIAN_POINT('Ctrl Pts',(-244.867833162404,0.713443376090342,
135.670589302247));
#136772=CARTESIAN_POINT('Ctrl Pts',(-244.875581230407,0.849201355323179,
135.650685669));
#136773=CARTESIAN_POINT('Ctrl Pts',(-244.88332929841,0.984089514536704,
135.62510200525));
#136774=CARTESIAN_POINT('Ctrl Pts',(-244.891077366413,1.11760374467236,
135.593947753468));
#136775=CARTESIAN_POINT('Ctrl Pts',(-244.898833669155,1.25125987532045,
135.562760390576));
#136776=CARTESIAN_POINT('Ctrl Pts',(-244.906589971897,1.38353877858307,
135.525990701823));
#136777=CARTESIAN_POINT('Ctrl Pts',(-244.914346274639,1.51394954675287,
135.483798600101));
#136778=CARTESIAN_POINT('Ctrl Pts',(-244.922106717153,1.64442991907659,
135.441583979183));
#136779=CARTESIAN_POINT('Ctrl Pts',(-244.929867159667,1.77303980310222,
135.393941314291));
#136780=CARTESIAN_POINT('Ctrl Pts',(-244.937627602181,1.89930784287381,
135.341078900697));
#136781=CARTESIAN_POINT('Ctrl Pts',(-244.945400502447,2.02577857931204,
135.288131627664));
#136782=CARTESIAN_POINT('Ctrl Pts',(-244.953173402712,2.14989960493979,
135.229948027648));
#136783=CARTESIAN_POINT('Ctrl Pts',(-244.960946302978,2.27122296010501,
135.166783032692));
#136784=CARTESIAN_POINT('Ctrl Pts',(-244.96843663874,2.38813590571619,135.105914244405));
#136785=CARTESIAN_POINT('Ctrl Pts',(-244.975926974502,2.50245078693436,
135.04042009896));
#136786=CARTESIAN_POINT('Ctrl Pts',(-244.983417310264,2.61379350653377,
134.97056591348));
#136787=CARTESIAN_POINT('Ctrl Pts',(-244.991191644383,2.72935781918755,
134.898063185326));
#136788=CARTESIAN_POINT('Ctrl Pts',(-244.998965978502,2.84208621516031,
134.820633601873));
#136789=CARTESIAN_POINT('Ctrl Pts',(-245.006740312621,2.95153000666685,
134.738525545762));
#136790=CARTESIAN_POINT('Ctrl Pts',(-245.014505065568,3.06083891848163,
134.656518680491));
#136791=CARTESIAN_POINT('Ctrl Pts',(-245.022269818515,3.16687097037143,
134.569845047159));
#136792=CARTESIAN_POINT('Ctrl Pts',(-245.030034571462,3.26920403115723,
134.478797726181));
#136793=CARTESIAN_POINT('Ctrl Pts',(-245.037791612347,3.37143545330441,
134.387840834685));
#136794=CARTESIAN_POINT('Ctrl Pts',(-245.045548653233,3.46997490535372,
134.292519158514));
#136795=CARTESIAN_POINT('Ctrl Pts',(-245.053305694118,3.56443139979751,
134.19316746639));
#136796=CARTESIAN_POINT('Ctrl Pts',(-245.061056885358,3.65881666386421,
134.09389069615));
#136797=CARTESIAN_POINT('Ctrl Pts',(-245.068808076598,3.74912483057287,
133.990590241236));
#136798=CARTESIAN_POINT('Ctrl Pts',(-245.076559267838,3.83500029380863,
133.883639073469));
#136799=CARTESIAN_POINT('Ctrl Pts',(-245.084307164615,3.9208392576816,133.776733362801));
#136800=CARTESIAN_POINT('Ctrl Pts',(-245.092055061392,4.00224902098047,
133.66618032961));
#136801=CARTESIAN_POINT('Ctrl Pts',(-245.099802958169,4.07891311439651,
133.55238734009));
#136802=CARTESIAN_POINT('Ctrl Pts',(-245.107549234253,4.15556117133711,
133.438618153609));
#136803=CARTESIAN_POINT('Ctrl Pts',(-245.115295510337,4.22746531460354,
133.321610682878));
#136804=CARTESIAN_POINT('Ctrl Pts',(-245.123041786421,4.29435165338769,
133.201802366503));
#136805=CARTESIAN_POINT('Ctrl Pts',(-245.130788119687,4.36123848591151,
133.081993165731));
#136806=CARTESIAN_POINT('Ctrl Pts',(-245.138534452952,4.42310724946262,
132.959383419429));
#136807=CARTESIAN_POINT('Ctrl Pts',(-245.146280786218,4.47972958278128,
132.834435967807));
#136808=CARTESIAN_POINT('Ctrl Pts',(-245.154028854221,4.53636459627882,
132.709460535069));
#136809=CARTESIAN_POINT('Ctrl Pts',(-245.161776922224,4.58775068028024,
132.582146711319));
#136810=CARTESIAN_POINT('Ctrl Pts',(-245.169524990227,4.63370742857589,
132.452977774113));
#136811=CARTESIAN_POINT('Ctrl Pts',(-245.177281292968,4.67971302025059,
132.323671554623));
#136812=CARTESIAN_POINT('Ctrl Pts',(-245.18503759571,4.72027761803658,132.192506652054));
#136813=CARTESIAN_POINT('Ctrl Pts',(-245.192793898452,4.75527041357106,
132.059982517787));
#136814=CARTESIAN_POINT('Ctrl Pts',(-245.200554340966,4.79028188581423,
131.9273876514));
#136815=CARTESIAN_POINT('Ctrl Pts',(-245.208314783481,4.81971554631737,
131.793432489437));
#136816=CARTESIAN_POINT('Ctrl Pts',(-245.216075225995,4.84349186038418,
131.658626185696));
#136817=CARTESIAN_POINT('Ctrl Pts',(-245.22384812626,4.86730634230103,131.523603478909));
#136818=CARTESIAN_POINT('Ctrl Pts',(-245.231621026526,4.88544527793848,
131.387727287736));
#136819=CARTESIAN_POINT('Ctrl Pts',(-245.239393926791,4.8978810157106,131.251512290314));
#136820=CARTESIAN_POINT('Ctrl Pts',(-245.246884262553,4.90986468309093,
131.120249051155));
#136821=CARTESIAN_POINT('Ctrl Pts',(-245.254374598315,4.91655258923234,
130.988671518625));
#136822=CARTESIAN_POINT('Ctrl Pts',(-245.261864934077,4.9179657442552,130.857237841703));
#136823=CARTESIAN_POINT('Ctrl Pts',(-245.269639268196,4.91943247948028,
130.720820816971));
#136824=CARTESIAN_POINT('Ctrl Pts',(-245.277413602315,4.91522122956841,
130.584126643625));
#136825=CARTESIAN_POINT('Ctrl Pts',(-245.285187936434,4.90529843916352,
130.447667072292));
#136826=CARTESIAN_POINT('Ctrl Pts',(-245.292952689381,4.895387877711,130.311375675186));
#136827=CARTESIAN_POINT('Ctrl Pts',(-245.300717442328,4.87977980928659,
130.175318691009));
#136828=CARTESIAN_POINT('Ctrl Pts',(-245.308482195276,4.85849263853231,
130.040009687804));
#136829=CARTESIAN_POINT('Ctrl Pts',(-245.31623923616,4.83722661049611,129.904835075409));
#136830=CARTESIAN_POINT('Ctrl Pts',(-245.323996277046,4.81029276547509,
129.770407349285));
#136831=CARTESIAN_POINT('Ctrl Pts',(-245.331753317931,4.77776141558045,
129.63723640897));
#136832=CARTESIAN_POINT('Ctrl Pts',(-245.339504509171,4.74525459782977,
129.504165893897));
#136833=CARTESIAN_POINT('Ctrl Pts',(-245.347255700411,4.70715876949526,
129.37235065645));
#136834=CARTESIAN_POINT('Ctrl Pts',(-245.355006891651,4.66359550854168,
129.242291478504));
#136835=CARTESIAN_POINT('Ctrl Pts',(-245.362754788428,4.62005076313615,
129.112287579179));
#136836=CARTESIAN_POINT('Ctrl Pts',(-245.370502685205,4.57104333089517,
128.984038624823));
#136837=CARTESIAN_POINT('Ctrl Pts',(-245.378250581982,4.5167448811426,128.858031061409));
#136838=CARTESIAN_POINT('Ctrl Pts',(-245.385996858066,4.46245778945517,
128.732049856059));
#136839=CARTESIAN_POINT('Ctrl Pts',(-245.39374313415,4.40288203629706,128.608309467902));
#136840=CARTESIAN_POINT('Ctrl Pts',(-245.401489410235,4.33823760648576,
128.487276775282));
#136841=CARTESIAN_POINT('Ctrl Pts',(-245.4092357435,4.27359269948386,128.366243189226));
#136842=CARTESIAN_POINT('Ctrl Pts',(-245.416982076765,4.20387922535956,
128.247917683451));
#136843=CARTESIAN_POINT('Ctrl Pts',(-245.424728410031,4.12936314985014,
128.132742561189));
#136844=CARTESIAN_POINT('Ctrl Pts',(-245.432476478034,4.05483038698237,
128.017541646257));
#136845=CARTESIAN_POINT('Ctrl Pts',(-245.440224546036,3.97549309492416,
127.905492846907));
#136846=CARTESIAN_POINT('Ctrl Pts',(-245.447972614039,3.89166035480809,
127.797009167317));
#136847=CARTESIAN_POINT('Ctrl Pts',(-245.455728916781,3.8077385162581,127.688410189981));
#136848=CARTESIAN_POINT('Ctrl Pts',(-245.463485219523,3.71931192489257,
127.583384211295));
#136849=CARTESIAN_POINT('Ctrl Pts',(-245.471241522265,3.62673007818832,
127.482311249711));
#136850=CARTESIAN_POINT('Ctrl Pts',(-245.479001964779,3.5340988177649,127.381184342445));
#136851=CARTESIAN_POINT('Ctrl Pts',(-245.486762407293,3.43730815865739,
127.284014933181));
#136852=CARTESIAN_POINT('Ctrl Pts',(-245.494522849808,3.33674347592955,
127.191145146778));
#136853=CARTESIAN_POINT('Ctrl Pts',(-245.502295750073,3.23601735784529,
127.098126277549));
#136854=CARTESIAN_POINT('Ctrl Pts',(-245.510068650338,3.13150540777764,
127.009421076986));
#136855=CARTESIAN_POINT('Ctrl Pts',(-245.517841550604,3.02362569266342,
126.925331005258));
#136856=CARTESIAN_POINT('Ctrl Pts',(-245.525331886366,2.9196676769265,126.844297819447));
#136857=CARTESIAN_POINT('Ctrl Pts',(-245.532822222128,2.81258274897094,
126.767550224307));
#136858=CARTESIAN_POINT('Ctrl Pts',(-245.54031255789,2.702767718989,126.695318184141));
#136859=CARTESIAN_POINT('Ctrl Pts',(-245.548086892009,2.58878901876726,
126.620347444217));
#136860=CARTESIAN_POINT('Ctrl Pts',(-245.555861226128,2.47150805590852,
126.550003948402));
#136861=CARTESIAN_POINT('Ctrl Pts',(-245.563635560247,2.35133724321879,
126.484592541482));
#136862=CARTESIAN_POINT('Ctrl Pts',(-245.571400313194,2.23131453031604,
126.419261748275));
#136863=CARTESIAN_POINT('Ctrl Pts',(-245.579165066141,2.10840939396299,
126.35885113496));
#136864=CARTESIAN_POINT('Ctrl Pts',(-245.586929819088,1.98306386165576,
126.303622813262));
#136865=CARTESIAN_POINT('Ctrl Pts',(-245.594686859973,1.85784282429827,
126.24844934511));
#136866=CARTESIAN_POINT('Ctrl Pts',(-245.602443900858,1.73018656998981,
126.198448082183));
#136867=CARTESIAN_POINT('Ctrl Pts',(-245.610200941743,1.60056209706517,
126.153835482064));
#136868=CARTESIAN_POINT('Ctrl Pts',(-245.617952132983,1.47103537496371,
126.109256524653));
#136869=CARTESIAN_POINT('Ctrl Pts',(-245.625703324224,1.33954375674082,
126.070058268355));
#136870=CARTESIAN_POINT('Ctrl Pts',(-245.633454515464,1.20657428023067,
126.036409111019));
#136871=CARTESIAN_POINT('Ctrl Pts',(-245.641202412241,1.07366131929493,
126.002774255473));
#136872=CARTESIAN_POINT('Ctrl Pts',(-245.648950309018,0.939272127597074,
125.974683903696));
#136873=CARTESIAN_POINT('Ctrl Pts',(-245.656698205795,0.803908757371429,
125.952256561353));
#136874=CARTESIAN_POINT('Ctrl Pts',(-245.664444481879,0.668573702245107,
125.929833910326));
#136875=CARTESIAN_POINT('Ctrl Pts',(-245.672190757963,0.532265259377637,
125.913071976405));
#136876=CARTESIAN_POINT('Ctrl Pts',(-245.679937034047,0.395495133911688,
125.902038039282));
#136877=CARTESIAN_POINT('Ctrl Pts',(-245.687683367313,0.258723998839555,
125.891004020709));
#136878=CARTESIAN_POINT('Ctrl Pts',(-245.695429700578,0.121491564067545,
125.885698114745));
#136879=CARTESIAN_POINT('Ctrl Pts',(-245.703176033843,-0.0156862871894603,
125.886135632585));
#136880=CARTESIAN_POINT('Ctrl Pts',(-245.710924101846,-0.152894858475317,
125.886573248404));
#136881=CARTESIAN_POINT('Ctrl Pts',(-245.718672169849,-0.290048431034229,
125.892756846168));
#136882=CARTESIAN_POINT('Ctrl Pts',(-245.726420237852,-0.426632466852755,
125.904649626015));
#136883=CARTESIAN_POINT('Ctrl Pts',(-245.734176540594,-0.563361665809733,
125.916555045649));
#136884=CARTESIAN_POINT('Ctrl Pts',(-245.741932843336,-0.699519728741003,
125.934181734455));
#136885=CARTESIAN_POINT('Ctrl Pts',(-245.749689146078,-0.834598023437429,
125.957441059561));
#136886=CARTESIAN_POINT('Ctrl Pts',(-245.757449588592,-0.969748413486863,
125.980712798869));
#136887=CARTESIAN_POINT('Ctrl Pts',(-245.765210031106,-1.10381750497173,
126.009623082428));
#136888=CARTESIAN_POINT('Ctrl Pts',(-245.77297047362,-1.23630915392517,
126.044032610126));
#136889=CARTESIAN_POINT('Ctrl Pts',(-245.780743373886,-1.36901349023557,
126.078497375051));
#136890=CARTESIAN_POINT('Ctrl Pts',(-245.788516274151,-1.50013494958879,
126.118478910927));
#136891=CARTESIAN_POINT('Ctrl Pts',(-245.796289174417,-1.62919392961649,
126.163788432781));
#136892=CARTESIAN_POINT('Ctrl Pts',(-245.803779510179,-1.75356129063918,
126.207450839388));
#136893=CARTESIAN_POINT('Ctrl Pts',(-245.81126984594,-1.87601323528946,
126.256060472242));
#136894=CARTESIAN_POINT('Ctrl Pts',(-245.818760181702,-1.99614180248465,
126.309407785013));
#136895=CARTESIAN_POINT('Ctrl Pts',(-245.826535047318,-2.12083360485025,
126.364781562759));
#136896=CARTESIAN_POINT('Ctrl Pts',(-245.834309912933,-2.24341704088224,
126.425435488505));
#136897=CARTESIAN_POINT('Ctrl Pts',(-245.842084778548,-2.36341261905234,
126.491187324664));
#136898=CARTESIAN_POINT('Ctrl Pts',(-245.849849942518,-2.48325846415421,
126.556857114264));
#136899=CARTESIAN_POINT('Ctrl Pts',(-245.857615106489,-2.60052253719137,
126.627611970366));
#136900=CARTESIAN_POINT('Ctrl Pts',(-245.865380270459,-2.71474531852435,
126.703221639422));
#136901=CARTESIAN_POINT('Ctrl Pts',(-245.873137602409,-2.82885289363855,
126.778755047824));
#136902=CARTESIAN_POINT('Ctrl Pts',(-245.880894934358,-2.93992495792657,
126.859133309541));
#136903=CARTESIAN_POINT('Ctrl Pts',(-245.888652266308,-3.0475269302497,
126.944080488883));
#136904=CARTESIAN_POINT('Ctrl Pts',(-245.896403235343,-3.15504064256633,
127.028957990705));
#136905=CARTESIAN_POINT('Ctrl Pts',(-245.904154204378,-3.25908962490112,
127.118396706554));
#136906=CARTESIAN_POINT('Ctrl Pts',(-245.911905173413,-3.35926898284293,
127.212077922202));
#136907=CARTESIAN_POINT('Ctrl Pts',(-245.919652672023,-3.45940348639811,
127.305717192948));
#136908=CARTESIAN_POINT('Ctrl Pts',(-245.927400170633,-3.55567152767521,
127.403594917894));
#136909=CARTESIAN_POINT('Ctrl Pts',(-245.935147669243,-3.64770209393112,
127.505352812721));
#136910=CARTESIAN_POINT('Ctrl Pts',(-245.942893376769,-3.7397113843556,
127.60708718293));
#136911=CARTESIAN_POINT('Ctrl Pts',(-245.950639084294,-3.82748488742137,
127.712699648068));
#136912=CARTESIAN_POINT('Ctrl Pts',(-245.95838479182,-3.91068948471904,
127.82179614775));
#136913=CARTESIAN_POINT('Ctrl Pts',(-245.966130386046,-3.99389286494193,
127.930891051624));
#136914=CARTESIAN_POINT('Ctrl Pts',(-245.973875980271,-4.07252723637829,
128.043469577149));
#136915=CARTESIAN_POINT('Ctrl Pts',(-245.981621574497,-4.14630095147046,
128.159106096289));
#136916=CARTESIAN_POINT('Ctrl Pts',(-245.98937223353,-4.22012290684803,
128.274818229606));
#136917=CARTESIAN_POINT('Ctrl Pts',(-245.997122892564,-4.28907764469264,
128.393592022008));
#136918=CARTESIAN_POINT('Ctrl Pts',(-246.004873551597,-4.35291776099921,
128.514974230676));
#136919=CARTESIAN_POINT('Ctrl Pts',(-246.012626773891,-4.41677899020802,
128.636396582296));
#136920=CARTESIAN_POINT('Ctrl Pts',(-246.020379996186,-4.47552205677387,
128.760428717293));
#136921=CARTESIAN_POINT('Ctrl Pts',(-246.028133218481,-4.52894684272933,
128.886595366491));
#136922=CARTESIAN_POINT('Ctrl Pts',(-246.035895555285,-4.582434433631,129.012910334292));
#136923=CARTESIAN_POINT('Ctrl Pts',(-246.043657892089,-4.63059111254368,
129.141364464471));
#136924=CARTESIAN_POINT('Ctrl Pts',(-246.051420228893,-4.67326578655212,
129.271464681522));
#136925=CARTESIAN_POINT('Ctrl Pts',(-246.057549640288,-4.7069631949169,
129.374196342493));
#136926=CARTESIAN_POINT('Ctrl Pts',(-246.063679051683,-4.7372434144468,
129.477953993567));
#136927=CARTESIAN_POINT('Ctrl Pts',(-246.069808463078,-4.7640545282341,
129.582490119308));
#136928=CARTESIAN_POINT('Origin',(213.235140564004,0.,130.804360617566));
#136929=CARTESIAN_POINT('',(-248.165132725248,-4.76405452823402,129.582490119308));
#136930=CARTESIAN_POINT('',(-247.820142267558,-4.76405452823396,129.582490119308));
#136931=CARTESIAN_POINT('',(213.235140564004,-4.76405452823405,129.582490119308));
#136932=CARTESIAN_POINT('',(-246.485140563968,-4.91824990085616,130.803373081029));
#136933=CARTESIAN_POINT('Ctrl Pts',(-246.485140564014,-4.91824990085632,
130.803373081837));
#136934=CARTESIAN_POINT('Ctrl Pts',(-246.493143038491,-4.91827842866088,
130.94545084961));
#136935=CARTESIAN_POINT('Ctrl Pts',(-246.501145512967,-4.91214612793223,
131.087450398188));
#136936=CARTESIAN_POINT('Ctrl Pts',(-246.509147987444,-4.89989941741298,
131.228823527295));
#136937=CARTESIAN_POINT('Ctrl Pts',(-246.51715723978,-4.88764233429156,
131.370316395269));
#136938=CARTESIAN_POINT('Ctrl Pts',(-246.525166492117,-4.86926054547988,
131.511181434629));
#136939=CARTESIAN_POINT('Ctrl Pts',(-246.533175744453,-4.84485207420658,
131.650877859893));
#136940=CARTESIAN_POINT('Ctrl Pts',(-246.541192936668,-4.8204194058791,
131.790712771583));
#136941=CARTESIAN_POINT('Ctrl Pts',(-246.549210128884,-4.78994820222126,
131.929376412285));
#136942=CARTESIAN_POINT('Ctrl Pts',(-246.557227321099,-4.75358708490067,
132.066340367311));
#136943=CARTESIAN_POINT('Ctrl Pts',(-246.56525935405,-4.71715865901031,
132.203557858218));
#136944=CARTESIAN_POINT('Ctrl Pts',(-246.573291387001,-4.67481862502022,
132.339069035744));
#136945=CARTESIAN_POINT('Ctrl Pts',(-246.581323419953,-4.6267651542245,
132.472361597828));
#136946=CARTESIAN_POINT('Ctrl Pts',(-246.589364048663,-4.57866025733882,
132.605796807574));
#136947=CARTESIAN_POINT('Ctrl Pts',(-246.597404677373,-4.52482986083124,
132.737008340676));
#136948=CARTESIAN_POINT('Ctrl Pts',(-246.605445306083,-4.46551925885111,
132.865506127065));
#136949=CARTESIAN_POINT('Ctrl Pts',(-246.61350054266,-4.40610090393464,
132.994237362675));
#136950=CARTESIAN_POINT('Ctrl Pts',(-246.621555779237,-4.34118261308319,
133.120244688913));
#136951=CARTESIAN_POINT('Ctrl Pts',(-246.629611015813,-4.27105485649333,
133.243063853986));
#136952=CARTESIAN_POINT('Ctrl Pts',(-246.631245362869,-4.25682646091178,
133.267982940958));
#136953=CARTESIAN_POINT('Ctrl Pts',(-246.632879709925,-4.24238375381644,
133.292770887925));
#136954=CARTESIAN_POINT('Ctrl Pts',(-246.634514056981,-4.22772936886875,
133.317423976518));
#136955=CARTESIAN_POINT('Ctrl Pts',(-246.6422883911,-4.15802074456785,133.434694875069));
#136956=CARTESIAN_POINT('Ctrl Pts',(-246.650062725219,-4.08331862959862,
133.549248904555));
#136957=CARTESIAN_POINT('Ctrl Pts',(-246.657837059338,-4.00386056780575,
133.660631545904));
#136958=CARTESIAN_POINT('Ctrl Pts',(-246.665601812285,-3.92450043097288,
133.771876918102));
#136959=CARTESIAN_POINT('Ctrl Pts',(-246.673366565232,-3.84039623438855,
133.879958363595));
#136960=CARTESIAN_POINT('Ctrl Pts',(-246.681131318179,-3.75183084408561,
133.984446839647));
#136961=CARTESIAN_POINT('Ctrl Pts',(-246.688888359064,-3.66335341817663,
134.088831536271));
#136962=CARTESIAN_POINT('Ctrl Pts',(-246.696645399949,-3.57042386743871,
134.189630068791));
#136963=CARTESIAN_POINT('Ctrl Pts',(-246.704402440834,-3.47336748156961,
134.286443528767));
#136964=CARTESIAN_POINT('Ctrl Pts',(-246.712153632074,-3.37638428667622,
134.383183980959));
#136965=CARTESIAN_POINT('Ctrl Pts',(-246.719904823314,-3.27528072673547,
134.475945067235));
#136966=CARTESIAN_POINT('Ctrl Pts',(-246.727656014554,-3.17042113259532,
134.564362333589));
#136967=CARTESIAN_POINT('Ctrl Pts',(-246.735403911332,-3.06560610657977,
134.652742020246));
#136968=CARTESIAN_POINT('Ctrl Pts',(-246.743151808109,-2.9570385197791,
134.736781307513));
#136969=CARTESIAN_POINT('Ctrl Pts',(-246.750899704886,-2.84511802668416,
134.816154041552));
#136970=CARTESIAN_POINT('Ctrl Pts',(-246.75864598097,-2.73322094494365,
134.895510172526));
#136971=CARTESIAN_POINT('Ctrl Pts',(-246.766392257054,-2.61797267065027,
134.970201465848));
#136972=CARTESIAN_POINT('Ctrl Pts',(-246.774138533138,-2.49980394381585,
135.039943612265));
#136973=CARTESIAN_POINT('Ctrl Pts',(-246.781884866404,-2.3816343446869,
135.109686273502));
#136974=CARTESIAN_POINT('Ctrl Pts',(-246.789631199669,-2.26054458669738,
135.174479516217));
#136975=CARTESIAN_POINT('Ctrl Pts',(-246.797377532934,-2.13699189672926,
135.234083938024));
#136976=CARTESIAN_POINT('Ctrl Pts',(-246.805125600937,-2.01341153799237,
135.293701707829));
#136977=CARTESIAN_POINT('Ctrl Pts',(-246.81287366894,-1.88736750180669,
135.348128174635));
#136978=CARTESIAN_POINT('Ctrl Pts',(-246.820621736943,-1.7593385973053,
135.397171386859));
#136979=CARTESIAN_POINT('Ctrl Pts',(-246.828378039685,-1.63117362216117,
135.446266722791));
#136980=CARTESIAN_POINT('Ctrl Pts',(-246.836134342427,-1.50101993034195,
135.489967234976));
#136981=CARTESIAN_POINT('Ctrl Pts',(-246.843890645169,-1.369373690359,135.528130167264));
#136982=CARTESIAN_POINT('Ctrl Pts',(-246.851651087683,-1.23765718681399,
135.566313468257));
#136983=CARTESIAN_POINT('Ctrl Pts',(-246.859411530197,-1.10444692732322,
135.598953207126));
#136984=CARTESIAN_POINT('Ctrl Pts',(-246.867171972711,-0.970250010447131,
135.62595765379));
#136985=CARTESIAN_POINT('Ctrl Pts',(-246.874944872977,-0.835837668766627,
135.65300545039));
#136986=CARTESIAN_POINT('Ctrl Pts',(-246.882717773242,-0.700435891020341,
135.674399816399));
#136987=CARTESIAN_POINT('Ctrl Pts',(-246.890490673508,-0.564558543570453,
135.690100757338));
#136988=CARTESIAN_POINT('Ctrl Pts',(-246.89798100927,-0.433620679952551,
135.705230929527));
#136989=CARTESIAN_POINT('Ctrl Pts',(-246.905471345032,-0.302241529806322,
135.715074407698));
#136990=CARTESIAN_POINT('Ctrl Pts',(-246.912961680794,-0.170879614357212,
135.719641201612));
#136991=CARTESIAN_POINT('Ctrl Pts',(-246.920736014913,-0.0345370719589941,
135.724381146904));
#136992=CARTESIAN_POINT('Ctrl Pts',(-246.928510349032,0.102218795228362,
135.723451392982));
#136993=CARTESIAN_POINT('Ctrl Pts',(-246.936284683151,0.238877189185913,
135.716806113547));
#136994=CARTESIAN_POINT('Ctrl Pts',(-246.944049436098,0.375367163886053,
135.710169023826));
#136995=CARTESIAN_POINT('Ctrl Pts',(-246.951814189045,0.511759517618411,
135.69783044261));
#136996=CARTESIAN_POINT('Ctrl Pts',(-246.959578941993,0.647540388576628,
135.679796445024));
#136997=CARTESIAN_POINT('Ctrl Pts',(-246.967335982878,0.783186400060004,
135.661780359059));
#136998=CARTESIAN_POINT('Ctrl Pts',(-246.975093023763,0.918221752336038,
135.638080165089));
#136999=CARTESIAN_POINT('Ctrl Pts',(-246.982850064648,1.05213500540984,
135.608753918795));
#137000=CARTESIAN_POINT('Ctrl Pts',(-246.990601255888,1.18594727345799,
135.579449787651));
#137001=CARTESIAN_POINT('Ctrl Pts',(-246.998352447128,1.31863874621221,
135.544528132218));
#137002=CARTESIAN_POINT('Ctrl Pts',(-247.006103638368,1.44970586847414,
135.504098478065));
#137003=CARTESIAN_POINT('Ctrl Pts',(-247.013851535145,1.5807172837126,135.463686007595));
#137004=CARTESIAN_POINT('Ctrl Pts',(-247.021599431922,1.71010534878347,
135.417770309567));
#137005=CARTESIAN_POINT('Ctrl Pts',(-247.029347328699,1.83737963821065,
135.366511330507));
#137006=CARTESIAN_POINT('Ctrl Pts',(-247.037093604784,1.96462730460019,
135.315263073721));
#137007=CARTESIAN_POINT('Ctrl Pts',(-247.044839880868,2.08976171239102,
135.258673905034));
#137008=CARTESIAN_POINT('Ctrl Pts',(-247.052586156952,2.21231083865722,
135.19695254212));
#137009=CARTESIAN_POINT('Ctrl Pts',(-247.060332490217,2.33486086955307,
135.135230723594));
#137010=CARTESIAN_POINT('Ctrl Pts',(-247.068078823482,2.45482523166445,
135.068376811107));
#137011=CARTESIAN_POINT('Ctrl Pts',(-247.075825156748,2.57175536668559,
134.996646079748));
#137012=CARTESIAN_POINT('Ctrl Pts',(-247.083573224751,2.68871168739957,
134.924899284789));
#137013=CARTESIAN_POINT('Ctrl Pts',(-247.091321292754,2.80263209571617,
134.848273702143));
#137014=CARTESIAN_POINT('Ctrl Pts',(-247.099069360757,2.9130962892978,134.767068412973));
#137015=CARTESIAN_POINT('Ctrl Pts',(-247.106825663499,3.02367788553906,
134.685776817855));
#137016=CARTESIAN_POINT('Ctrl Pts',(-247.11458196624,3.1307956137118,134.599896025063));
#137017=CARTESIAN_POINT('Ctrl Pts',(-247.122338268982,3.23406117782463,
134.509766312033));
#137018=CARTESIAN_POINT('Ctrl Pts',(-247.130098711496,3.3373818578783,134.419588494061));
#137019=CARTESIAN_POINT('Ctrl Pts',(-247.137859154011,3.43684599369009,
134.325157506169));
#137020=CARTESIAN_POINT('Ctrl Pts',(-247.145619596525,3.53210231098769,
134.226850402389));
#137021=CARTESIAN_POINT('Ctrl Pts',(-247.15339249679,3.62751154218227,134.128385487318));
#137022=CARTESIAN_POINT('Ctrl Pts',(-247.161165397056,3.71869919646961,
134.026032314337));
#137023=CARTESIAN_POINT('Ctrl Pts',(-247.168938297321,3.80535386804103,
133.920201595775));
#137024=CARTESIAN_POINT('Ctrl Pts',(-247.176428633083,3.88885842402971,
133.818218090406));
#137025=CARTESIAN_POINT('Ctrl Pts',(-247.183918968845,3.9681536607632,133.713005730932));
#137026=CARTESIAN_POINT('Ctrl Pts',(-247.191409304607,4.04300015781193,
133.604955694765));
#137027=CARTESIAN_POINT('Ctrl Pts',(-247.199183638726,4.12068448254636,
133.492808908635));
#137028=CARTESIAN_POINT('Ctrl Pts',(-247.206957972845,4.19382214090159,
133.377249769737));
#137029=CARTESIAN_POINT('Ctrl Pts',(-247.214732306964,4.26209847910996,
133.25868325668));
#137030=CARTESIAN_POINT('Ctrl Pts',(-247.222497059911,4.3302906728337,133.140262866253));
#137031=CARTESIAN_POINT('Ctrl Pts',(-247.230261812858,4.39363327377075,
133.018842811692));
#137032=CARTESIAN_POINT('Ctrl Pts',(-247.238026565806,4.45185363823772,
132.894858703241));
#137033=CARTESIAN_POINT('Ctrl Pts',(-247.245783606691,4.51001617741795,
132.770997737554));
#137034=CARTESIAN_POINT('Ctrl Pts',(-247.253540647576,4.56306643933374,
132.644578137534));
#137035=CARTESIAN_POINT('Ctrl Pts',(-247.261297688461,4.61077682206316,
132.516061572647));
#137036=CARTESIAN_POINT('Ctrl Pts',(-247.269048879701,4.65845122602164,
132.387641923102));
#137037=CARTESIAN_POINT('Ctrl Pts',(-247.276800070941,4.70079363046617,
132.257128821287));
#137038=CARTESIAN_POINT('Ctrl Pts',(-247.284551262181,4.73762399847527,
132.125005123696));
#137039=CARTESIAN_POINT('Ctrl Pts',(-247.292299158958,4.77443871259552,
131.992937582201));
#137040=CARTESIAN_POINT('Ctrl Pts',(-247.300047055735,4.80574594509449,
131.85926118226));
#137041=CARTESIAN_POINT('Ctrl Pts',(-247.307794952512,4.8314151765647,131.724474987718));
#137042=CARTESIAN_POINT('Ctrl Pts',(-247.315541228596,4.85707903858505,
131.589716987543));
#137043=CARTESIAN_POINT('Ctrl Pts',(-247.32328750468,4.87710717226894,131.453850038335));
#137044=CARTESIAN_POINT('Ctrl Pts',(-247.331033780764,4.89142003778569,
131.317384083354));
#137045=CARTESIAN_POINT('Ctrl Pts',(-247.33878011403,4.90573300895675,131.180917121011));
#137046=CARTESIAN_POINT('Ctrl Pts',(-247.346526447295,4.91433058699434,
131.043851532903));
#137047=CARTESIAN_POINT('Ctrl Pts',(-247.35427278056,4.91718508533857,130.906702686257));
#137048=CARTESIAN_POINT('Ctrl Pts',(-247.362020848563,4.92004022292792,
130.769523126077));
#137049=CARTESIAN_POINT('Ctrl Pts',(-247.369768916566,4.91714971345435,
130.632260661062));
#137050=CARTESIAN_POINT('Ctrl Pts',(-247.377516984569,4.90853799869109,
130.495430564147));
#137051=CARTESIAN_POINT('Ctrl Pts',(-247.385273287311,4.89991713129493,
130.358455042577));
#137052=CARTESIAN_POINT('Ctrl Pts',(-247.393029590053,4.8855629366223,130.221913197875));
#137053=CARTESIAN_POINT('Ctrl Pts',(-247.400785892795,4.86555181624854,
130.086315642721));
#137054=CARTESIAN_POINT('Ctrl Pts',(-247.408546335309,4.84553001533726,
129.950645715068));
#137055=CARTESIAN_POINT('Ctrl Pts',(-247.416306777823,4.81984534575211,
129.815921465078));
#137056=CARTESIAN_POINT('Ctrl Pts',(-247.424067220337,4.78862516140443,
129.682642236659));
#137057=CARTESIAN_POINT('Ctrl Pts',(-247.431840120603,4.75735485964524,
129.54914905659));
#137058=CARTESIAN_POINT('Ctrl Pts',(-247.439613020868,4.72053139094803,
129.417105910358));
#137059=CARTESIAN_POINT('Ctrl Pts',(-247.447385921134,4.67833197678282,
129.286996792535));
#137060=CARTESIAN_POINT('Ctrl Pts',(-247.454876256896,4.6376666176163,129.16161746887));
#137061=CARTESIAN_POINT('Ctrl Pts',(-247.462366592658,4.5920094921698,129.038034290196));
#137062=CARTESIAN_POINT('Ctrl Pts',(-247.46985692842,4.54156029648799,128.916660128647));
#137063=CARTESIAN_POINT('Ctrl Pts',(-247.477631262539,4.48919830421857,
128.790684028873));
#137064=CARTESIAN_POINT('Ctrl Pts',(-247.485405596658,4.43150781868713,
128.66668870827));
#137065=CARTESIAN_POINT('Ctrl Pts',(-247.493179930777,4.36865948181805,
128.545157794794));
#137066=CARTESIAN_POINT('Ctrl Pts',(-247.500944683724,4.30588859990707,
128.423776657307));
#137067=CARTESIAN_POINT('Ctrl Pts',(-247.508709436671,4.23797269224571,
128.304854227843));
#137068=CARTESIAN_POINT('Ctrl Pts',(-247.516474189618,4.16513087949918,
128.188855347233));
#137069=CARTESIAN_POINT('Ctrl Pts',(-247.524231230503,4.09236141426837,
128.072971678346));
#137070=CARTESIAN_POINT('Ctrl Pts',(-247.531988271388,4.01467598677348,
127.960006108755));
#137071=CARTESIAN_POINT('Ctrl Pts',(-247.539745312273,3.93233998821283,
127.850399670024));
#137072=CARTESIAN_POINT('Ctrl Pts',(-247.547496503513,3.85006607986883,
127.740875886361));
#137073=CARTESIAN_POINT('Ctrl Pts',(-247.555247694753,3.76314881486151,
127.634706502812));
#137074=CARTESIAN_POINT('Ctrl Pts',(-247.562998885993,3.67189711968179,
127.532303985267));
#137075=CARTESIAN_POINT('Ctrl Pts',(-247.57074678277,3.58068420890661,127.429944991524));
#137076=CARTESIAN_POINT('Ctrl Pts',(-247.578494679548,3.48514079161095,
127.331349970759));
#137077=CARTESIAN_POINT('Ctrl Pts',(-247.586242576325,3.38561619541522,
127.236898488847));
#137078=CARTESIAN_POINT('Ctrl Pts',(-247.593988852409,3.28611241761951,
127.142466764149));
#137079=CARTESIAN_POINT('Ctrl Pts',(-247.601735128493,3.18262940077015,
127.052177123273));
#137080=CARTESIAN_POINT('Ctrl Pts',(-247.609481404577,3.07555318135034,
126.966372122119));
#137081=CARTESIAN_POINT('Ctrl Pts',(-247.617227737842,2.96847617151864,
126.880566487571));
#137082=CARTESIAN_POINT('Ctrl Pts',(-247.624974071107,2.85780621128164,
126.799245803287));
#137083=CARTESIAN_POINT('Ctrl Pts',(-247.632720404373,2.74396192842133,
126.722711931327));
#137084=CARTESIAN_POINT('Ctrl Pts',(-247.640468472376,2.63009215092305,
126.646160920137));
#137085=CARTESIAN_POINT('Ctrl Pts',(-247.648216540379,2.5130469606567,126.574399072459));
#137086=CARTESIAN_POINT('Ctrl Pts',(-247.655964608381,2.39327308271081,
126.507684342342));
#137087=CARTESIAN_POINT('Ctrl Pts',(-247.663720911123,2.27337190766194,
126.440898707016));
#137088=CARTESIAN_POINT('Ctrl Pts',(-247.671477213865,2.15073659380708,
126.379171095245));
#137089=CARTESIAN_POINT('Ctrl Pts',(-247.679233516607,2.025838030973,126.322713226844));
#137090=CARTESIAN_POINT('Ctrl Pts',(-247.686993959121,1.90087280601532,
126.266225225179));
#137091=CARTESIAN_POINT('Ctrl Pts',(-247.694754401635,1.77364228761655,
126.215012717187));
#137092=CARTESIAN_POINT('Ctrl Pts',(-247.702514844149,1.64463542584875,
126.169238463993));
#137093=CARTESIAN_POINT('Ctrl Pts',(-247.710287744415,1.51542147081341,
126.123390729904));
#137094=CARTESIAN_POINT('Ctrl Pts',(-247.71806064468,1.38442584793804,126.082998811142));
#137095=CARTESIAN_POINT('Ctrl Pts',(-247.725833544946,1.25215154809811,
126.048175217154));
#137096=CARTESIAN_POINT('Ctrl Pts',(-247.733323880708,1.12468575223299,
126.014617548521));
#137097=CARTESIAN_POINT('Ctrl Pts',(-247.74081421647,0.996032932413138,
125.986230454475));
#137098=CARTESIAN_POINT('Ctrl Pts',(-247.748304552232,0.866648390248171,
125.963069092551));
#137099=CARTESIAN_POINT('Ctrl Pts',(-247.756078886351,0.732358193845027,
125.939029560551));
#137100=CARTESIAN_POINT('Ctrl Pts',(-247.76385322047,0.596854302293437,
125.920543700368));
#137101=CARTESIAN_POINT('Ctrl Pts',(-247.77162755459,0.460635841617658,
125.907729358842));
#137102=CARTESIAN_POINT('Ctrl Pts',(-247.779392307537,0.324585258020469,
125.894930809846));
#137103=CARTESIAN_POINT('Ctrl Pts',(-247.787157060484,0.187822243025281,
125.887789908473));
#137104=CARTESIAN_POINT('Ctrl Pts',(-247.794921813431,0.0508563204592624,
125.886373560124));
#137105=CARTESIAN_POINT('Ctrl Pts',(-247.802678854316,-0.0859735656223271,
125.884958618512));
#137106=CARTESIAN_POINT('Ctrl Pts',(-247.810435895201,-0.223005569805123,
125.889256919127));
#137107=CARTESIAN_POINT('Ctrl Pts',(-247.818192936086,-0.359725189316763,
125.899283569173));
#137108=CARTESIAN_POINT('Ctrl Pts',(-247.825944127326,-0.496341707498876,
125.909302658044));
#137109=CARTESIAN_POINT('Ctrl Pts',(-247.833695318566,-0.632645921560685,
125.92504146958));
#137110=CARTESIAN_POINT('Ctrl Pts',(-247.841446509806,-0.768123829952101,
125.946463043063));
#137111=CARTESIAN_POINT('Ctrl Pts',(-247.849194406583,-0.903544156619012,
125.967875511807));
#137112=CARTESIAN_POINT('Ctrl Pts',(-247.85694230336,-1.03813849077029,
125.994965877667));
#137113=CARTESIAN_POINT('Ctrl Pts',(-247.864690200137,-1.17139867277518,
126.027645406051));
#137114=CARTESIAN_POINT('Ctrl Pts',(-247.872436476222,-1.30463097962311,
126.060318098582));
#137115=CARTESIAN_POINT('Ctrl Pts',(-247.880182752306,-1.4365293099482,
126.098577535108));
#137116=CARTESIAN_POINT('Ctrl Pts',(-247.88792902839,-1.5665967996225,126.142284092034));
#137117=CARTESIAN_POINT('Ctrl Pts',(-247.895675361655,-1.69666524942494,
126.185990971593));
#137118=CARTESIAN_POINT('Ctrl Pts',(-247.903421694921,-1.82490246100744,
126.235144927253));
#137119=CARTESIAN_POINT('Ctrl Pts',(-247.911168028186,-1.95082819072668,
126.289556919423));
#137120=CARTESIAN_POINT('Ctrl Pts',(-247.918916096189,-2.0767821206405,
126.343981096782));
#137121=CARTESIAN_POINT('Ctrl Pts',(-247.926664164192,-2.20042317982122,
126.403665498695));
#137122=CARTESIAN_POINT('Ctrl Pts',(-247.934412232195,-2.32129287839771,
126.468373713158));
#137123=CARTESIAN_POINT('Ctrl Pts',(-247.942168534937,-2.44229103872771,
126.533150700281));
#137124=CARTESIAN_POINT('Ctrl Pts',(-247.949924837679,-2.56051160940061,
126.602961981097));
#137125=CARTESIAN_POINT('Ctrl Pts',(-247.957681140421,-2.67552193708478,
126.67752582239));
#137126=CARTESIAN_POINT('Ctrl Pts',(-247.965441582935,-2.79059364924404,
126.75212946065));
#137127=CARTESIAN_POINT('Ctrl Pts',(-247.973202025449,-2.90245138560497,
126.83149048763));
#137128=CARTESIAN_POINT('Ctrl Pts',(-247.980962467963,-3.0106939211645,
126.91528551215));
#137129=CARTESIAN_POINT('Ctrl Pts',(-247.988735368229,-3.11911021725144,
126.999215051883));
#137130=CARTESIAN_POINT('Ctrl Pts',(-247.996508268494,-3.22389941637474,
127.087592560679));
#137131=CARTESIAN_POINT('Ctrl Pts',(-248.00428116876,-3.32469498229554,
127.180055672173));
#137132=CARTESIAN_POINT('Ctrl Pts',(-248.011771504521,-3.42182637550397,
127.269157516662));
#137133=CARTESIAN_POINT('Ctrl Pts',(-248.019261840283,-3.51524923331697,
127.362052859884));
#137134=CARTESIAN_POINT('Ctrl Pts',(-248.026752176045,-3.60467104849656,
127.458388457695));
#137135=CARTESIAN_POINT('Ctrl Pts',(-248.034437389345,-3.69641936861804,
127.55723043769));
#137136=CARTESIAN_POINT('Ctrl Pts',(-248.042122602644,-3.78426126690538,
127.660023733442));
#137137=CARTESIAN_POINT('Ctrl Pts',(-248.049807815944,-3.86783113952899,
127.766422939043));
#137138=CARTESIAN_POINT('Ctrl Pts',(-248.057483898829,-3.95130172700292,
127.872695737115));
#137139=CARTESIAN_POINT('Ctrl Pts',(-248.065159981715,-4.03051013549663,
127.982565615255));
#137140=CARTESIAN_POINT('Ctrl Pts',(-248.0728360646,-4.10512753012237,128.095650403473));
#137141=CARTESIAN_POINT('Ctrl Pts',(-248.080527452988,-4.17989370592884,
128.208960673811));
#137142=CARTESIAN_POINT('Ctrl Pts',(-248.088218841375,-4.25005025496661,
128.325498400309));
#137143=CARTESIAN_POINT('Ctrl Pts',(-248.095910229762,-4.3153064234439,
128.444845087996));
#137144=CARTESIAN_POINT('Ctrl Pts',(-248.103572743103,-4.38031760690732,
128.563743723787));
#137145=CARTESIAN_POINT('Ctrl Pts',(-248.111235256444,-4.44046492976471,
128.685429923047));
#137146=CARTESIAN_POINT('Ctrl Pts',(-248.118897769785,-4.49550423590677,
128.809460939025));
#137147=CARTESIAN_POINT('Ctrl Pts',(-248.126603595696,-4.55085465325594,
128.934193043766));
#137148=CARTESIAN_POINT('Ctrl Pts',(-248.134309421606,-4.60103890736235,
129.061296210318));
#137149=CARTESIAN_POINT('Ctrl Pts',(-248.142015247517,-4.64585601780006,
129.19029589632));
#137150=CARTESIAN_POINT('Ctrl Pts',(-248.149721073427,-4.69067312823778,
129.319295582322));
#137151=CARTESIAN_POINT('Ctrl Pts',(-248.157426899337,-4.73012294771376,
129.450191401843));
#137152=CARTESIAN_POINT('Ctrl Pts',(-248.165132725248,-4.76405452823402,
129.582490119308));
#137153=CARTESIAN_POINT('Ctrl Pts',(-246.415426335729,-4.76405452823406,
129.582490119308));
#137154=CARTESIAN_POINT('Ctrl Pts',(-246.423702521276,-4.80032898872548,
129.723923690223));
#137155=CARTESIAN_POINT('Ctrl Pts',(-246.431978706823,-4.83034188283307,
129.867132951389));
#137156=CARTESIAN_POINT('Ctrl Pts',(-246.44025489237,-4.85393125729227,
130.011558995481));
#137157=CARTESIAN_POINT('Ctrl Pts',(-246.448509182087,-4.87745822269407,
130.155602939857));
#137158=CARTESIAN_POINT('Ctrl Pts',(-246.456763471804,-4.89459550936722,
130.300856946525));
#137159=CARTESIAN_POINT('Ctrl Pts',(-246.465017761521,-4.90523171034105,
130.446750592029));
#137160=CARTESIAN_POINT('Ctrl Pts',(-246.471725362337,-4.91387489985538,
130.565306684578));
#137161=CARTESIAN_POINT('Ctrl Pts',(-246.478432963153,-4.91822598909207,
130.684284797298));
#137162=CARTESIAN_POINT('Ctrl Pts',(-246.485140563968,-4.91824990085616,
130.803373081029));
#137163=CARTESIAN_POINT('',(-246.139859436028,-4.91824848601657,130.800501563838));
#137164=CARTESIAN_POINT('Ctrl Pts',(-246.069808463078,-4.7640545282341,
129.582490119308));
#137165=CARTESIAN_POINT('Ctrl Pts',(-246.077583997001,-4.79806606887736,
129.715100600079));
#137166=CARTESIAN_POINT('Ctrl Pts',(-246.085359530925,-4.8264933030139,
129.84896373178));
#137167=CARTESIAN_POINT('Ctrl Pts',(-246.093135064848,-4.8492767216106,
129.983569328781));
#137168=CARTESIAN_POINT('Ctrl Pts',(-246.094492645071,-4.85325462445185,
130.007070981287));
#137169=CARTESIAN_POINT('Ctrl Pts',(-246.095850225293,-4.85706061005185,
130.030595261098));
#137170=CARTESIAN_POINT('Ctrl Pts',(-246.097207805516,-4.86069452442358,
130.054139448351));
#137171=CARTESIAN_POINT('Ctrl Pts',(-246.110238294451,-4.89557399617043,
130.280124083671));
#137172=CARTESIAN_POINT('Ctrl Pts',(-246.123268783386,-4.91469973543392,
130.508600512009));
#137173=CARTESIAN_POINT('Ctrl Pts',(-246.136299272322,-4.91780024632565,
130.737848966411));
#137174=CARTESIAN_POINT('Ctrl Pts',(-246.137485993547,-4.91808261808478,
130.758727231835));
#137175=CARTESIAN_POINT('Ctrl Pts',(-246.138672714772,-4.91823209512877,
130.779611870769));
#137176=CARTESIAN_POINT('Ctrl Pts',(-246.139859435997,-4.91824848601615,
130.8005015633));
#137177=CARTESIAN_POINT('Ctrl Pts',(-246.139859436027,-4.91824848601657,
130.800501563838));
#137178=CARTESIAN_POINT('Ctrl Pts',(-246.147509209082,-4.91835414398288,
130.935159479865));
#137179=CARTESIAN_POINT('Ctrl Pts',(-246.155158982137,-4.91292539923117,
131.07002367009));
#137180=CARTESIAN_POINT('Ctrl Pts',(-246.162808755192,-4.90193805195921,
131.204593546314));
#137181=CARTESIAN_POINT('Ctrl Pts',(-246.170450973431,-4.8909615556474,
131.339030523093));
#137182=CARTESIAN_POINT('Ctrl Pts',(-246.17809319167,-4.87443740755454,
131.473173364555));
#137183=CARTESIAN_POINT('Ctrl Pts',(-246.185735409909,-4.8523934448977,
131.606520775149));
#137184=CARTESIAN_POINT('Ctrl Pts',(-246.193648744052,-4.82956744898002,
131.744598828412));
#137185=CARTESIAN_POINT('Ctrl Pts',(-246.201562078194,-4.80082273554776,
131.881823530467));
#137186=CARTESIAN_POINT('Ctrl Pts',(-246.209475412337,-4.76624899930714,
132.017642752563));
#137187=CARTESIAN_POINT('Ctrl Pts',(-246.217109079795,-4.73289714021657,
132.148661961064));
#137188=CARTESIAN_POINT('Ctrl Pts',(-246.224742747254,-4.69412137968988,
132.27837291988));
#137189=CARTESIAN_POINT('Ctrl Pts',(-246.232376414712,-4.65005427662074,
132.406290168758));
#137190=CARTESIAN_POINT('Ctrl Pts',(-246.240008934568,-4.60599379835271,
132.534188187274));
#137191=CARTESIAN_POINT('Ctrl Pts',(-246.247641454423,-4.55664369045626,
132.6602926505));
#137192=CARTESIAN_POINT('Ctrl Pts',(-246.255273974279,-4.50218607768833,
132.784134237041));
#137193=CARTESIAN_POINT('Ctrl Pts',(-246.262907113082,-4.44772404876844,
132.907985866315));
#137194=CARTESIAN_POINT('Ctrl Pts',(-246.270540251884,-4.38815385424924,
133.029573884721));
#137195=CARTESIAN_POINT('Ctrl Pts',(-246.278173390687,-4.32370512787218,
133.148450425938));
#137196=CARTESIAN_POINT('Ctrl Pts',(-246.285808915305,-4.25923625738789,
133.267364123231));
#137197=CARTESIAN_POINT('Ctrl Pts',(-246.293444439923,-4.18988601568527,
133.383564303824));
#137198=CARTESIAN_POINT('Ctrl Pts',(-246.301079964541,-4.11592890471563,
133.496629607438));
#137199=CARTESIAN_POINT('Ctrl Pts',(-246.308723686376,-4.0418923961166,
133.609816293796));
#137200=CARTESIAN_POINT('Ctrl Pts',(-246.316367408212,-3.96323936901022,
133.719861048954));
#137201=CARTESIAN_POINT('Ctrl Pts',(-246.324011130048,-3.88028651580862,
133.826373128747));
#137202=CARTESIAN_POINT('Ctrl Pts',(-246.331659746566,-3.79728054347419,
133.932953413901));
#137203=CARTESIAN_POINT('Ctrl Pts',(-246.339308363085,-3.70996952495838,
134.035996214606));
#137204=CARTESIAN_POINT('Ctrl Pts',(-246.346956979603,-3.61870806410886,
134.135146562242));
#137205=CARTESIAN_POINT('Ctrl Pts',(-246.354616228249,-3.52731974325678,
134.234434736002));
#137206=CARTESIAN_POINT('Ctrl Pts',(-246.362275476895,-3.43197030759929,
134.329819377562));
#137207=CARTESIAN_POINT('Ctrl Pts',(-246.369934725541,-3.3330486836757,
134.420984669738));
#137208=CARTESIAN_POINT('Ctrl Pts',(-246.371841626804,-3.30842044946405,
134.443681832184));
#137209=CARTESIAN_POINT('Ctrl Pts',(-246.373748528066,-3.28357094003826,
134.466117666397));
#137210=CARTESIAN_POINT('Ctrl Pts',(-246.375655429329,-3.2585064365443,
134.488287715854));
#137211=CARTESIAN_POINT('Ctrl Pts',(-246.383429763448,-3.15631980080681,
134.578673817803));
#137212=CARTESIAN_POINT('Ctrl Pts',(-246.391204097567,-3.05020769545569,
134.66494810569));
#137213=CARTESIAN_POINT('Ctrl Pts',(-246.398978431686,-2.94053510115786,
134.746750296601));
#137214=CARTESIAN_POINT('Ctrl Pts',(-246.406743184633,-2.83099766853138,
134.828451673621));
#137215=CARTESIAN_POINT('Ctrl Pts',(-246.41450793758,-2.7179087881222,134.90569168832));
#137216=CARTESIAN_POINT('Ctrl Pts',(-246.422272690527,-2.60166881959181,
134.978148155961));
#137217=CARTESIAN_POINT('Ctrl Pts',(-246.430029731412,-2.48554430223623,
135.050532658818));
#137218=CARTESIAN_POINT('Ctrl Pts',(-246.437786772297,-2.36627525465273,
135.118142864016));
#137219=CARTESIAN_POINT('Ctrl Pts',(-246.445543813182,-2.24429323315252,
135.180698235498));
#137220=CARTESIAN_POINT('Ctrl Pts',(-246.453295004422,-2.12240319924411,
135.243206433487));
#137221=CARTESIAN_POINT('Ctrl Pts',(-246.461046195662,-1.99780461008804,
135.300667207411));
#137222=CARTESIAN_POINT('Ctrl Pts',(-246.468797386903,-1.87095567857234,
135.352844750914));
#137223=CARTESIAN_POINT('Ctrl Pts',(-246.47654528368,-1.74416066123617,
135.405000117569));
#137224=CARTESIAN_POINT('Ctrl Pts',(-246.484293180457,-1.61511756467201,
135.451876571543));
#137225=CARTESIAN_POINT('Ctrl Pts',(-246.492041077234,-1.48430654412968,
135.493285563175));
#137226=CARTESIAN_POINT('Ctrl Pts',(-246.499787353318,-1.35352288643289,
135.534685892938));
#137227=CARTESIAN_POINT('Ctrl Pts',(-246.507533629402,-1.22097241283283,
135.570620917276));
#137228=CARTESIAN_POINT('Ctrl Pts',(-246.515279905486,-1.08715210297495,
135.600951424326));
#137229=CARTESIAN_POINT('Ctrl Pts',(-246.523026238751,-0.953330805285754,
135.63128215527));
#137230=CARTESIAN_POINT('Ctrl Pts',(-246.530772572017,-0.81824003392849,
135.656008199952));
#137231=CARTESIAN_POINT('Ctrl Pts',(-246.538518905282,-0.682388278878623,
135.675041196227));
#137232=CARTESIAN_POINT('Ctrl Pts',(-246.546266973285,-0.546506100770328,
135.69407845481));
#137233=CARTESIAN_POINT('Ctrl Pts',(-246.554015041288,-0.409862986968956,
135.70742007381));
#137234=CARTESIAN_POINT('Ctrl Pts',(-246.561763109291,-0.272973490629409,
135.715029465688));
#137235=CARTESIAN_POINT('Ctrl Pts',(-246.569519412033,-0.13593850650396,
135.722646944918));
#137236=CARTESIAN_POINT('Ctrl Pts',(-246.577275714774,0.0013429922648055,
135.724520005307));
#137237=CARTESIAN_POINT('Ctrl Pts',(-246.585032017516,0.138354943250946,
135.72066420585));
#137238=CARTESIAN_POINT('Ctrl Pts',(-246.59279246003,0.275440021640677,
135.716806348438));
#137239=CARTESIAN_POINT('Ctrl Pts',(-246.600552902545,0.412254875766161,
135.707213565855));
#137240=CARTESIAN_POINT('Ctrl Pts',(-246.608313345059,0.548288615183166,
135.691953343741));
#137241=CARTESIAN_POINT('Ctrl Pts',(-246.616086245324,0.68454072803519,
135.676668624564));
#137242=CARTESIAN_POINT('Ctrl Pts',(-246.62385914559,0.820008833871837,
135.655698345242));
#137243=CARTESIAN_POINT('Ctrl Pts',(-246.631632045855,0.95419139435407,
135.629161322822));
#137244=CARTESIAN_POINT('Ctrl Pts',(-246.639122381617,1.0834960807773,135.60358898801));
#137245=CARTESIAN_POINT('Ctrl Pts',(-246.646612717379,1.21160676525314,
135.572847685529));
#137246=CARTESIAN_POINT('Ctrl Pts',(-246.654103053141,1.33808987962855,
135.537086949875));
#137247=CARTESIAN_POINT('Ctrl Pts',(-246.66187738726,1.46936863972905,135.499970335061));
#137248=CARTESIAN_POINT('Ctrl Pts',(-246.669651721379,1.59930982641751,
135.457328575547));
#137249=CARTESIAN_POINT('Ctrl Pts',(-246.677426055498,1.72741304250867,
135.409273998192));
#137250=CARTESIAN_POINT('Ctrl Pts',(-246.685190808445,1.85535838283491,
135.361278643809));
#137251=CARTESIAN_POINT('Ctrl Pts',(-246.692955561393,1.98146989696326,
135.307883880514));
#137252=CARTESIAN_POINT('Ctrl Pts',(-246.70072031434,2.10526011757353,135.24925239351));
#137253=CARTESIAN_POINT('Ctrl Pts',(-246.708477355225,2.22892738799189,
135.190679140125));
#137254=CARTESIAN_POINT('Ctrl Pts',(-246.71623439611,2.35027760197344,135.126879679899));
#137255=CARTESIAN_POINT('Ctrl Pts',(-246.723991436995,2.46884146985864,
135.058065456786));
#137256=CARTESIAN_POINT('Ctrl Pts',(-246.731742628235,2.58731592780863,
134.989303127015));
#137257=CARTESIAN_POINT('Ctrl Pts',(-246.739493819475,2.70300788521343,
134.915533757005));
#137258=CARTESIAN_POINT('Ctrl Pts',(-246.747245010715,2.81547127624926,
134.837015395143));
#137259=CARTESIAN_POINT('Ctrl Pts',(-246.754992907492,2.92788686734368,
134.758530405679));
#137260=CARTESIAN_POINT('Ctrl Pts',(-246.762740804269,3.037076301428,134.675300662244));
#137261=CARTESIAN_POINT('Ctrl Pts',(-246.770488701046,3.14262141069146,
134.587628217348));
#137262=CARTESIAN_POINT('Ctrl Pts',(-246.77823497713,3.24814444219306,134.499974111639));
#137263=CARTESIAN_POINT('Ctrl Pts',(-246.785981253214,3.35002436460675,
134.407879402591));
#137264=CARTESIAN_POINT('Ctrl Pts',(-246.793727529298,3.44787542541367,
134.311686965844));
#137265=CARTESIAN_POINT('Ctrl Pts',(-246.801473862564,3.54572720853504,
134.215493819027));
#137266=CARTESIAN_POINT('Ctrl Pts',(-246.809220195829,3.63954979189833,
134.115203158233));
#137267=CARTESIAN_POINT('Ctrl Pts',(-246.816966529095,3.72899398267495,
134.011195028582));
#137268=CARTESIAN_POINT('Ctrl Pts',(-246.824714597097,3.81845820385781,
133.907163607031));
#137269=CARTESIAN_POINT('Ctrl Pts',(-246.8324626651,3.90354182648,133.799413356413));
#137270=CARTESIAN_POINT('Ctrl Pts',(-246.840210733103,3.983935939859,133.68835740841));
#137271=CARTESIAN_POINT('Ctrl Pts',(-246.847967035845,4.0644154970585,133.577183428824));
#137272=CARTESIAN_POINT('Ctrl Pts',(-246.855723338587,4.14019535918323,
133.462697050789));
#137273=CARTESIAN_POINT('Ctrl Pts',(-246.863479641329,4.21100967210949,
133.345340862255));
#137274=CARTESIAN_POINT('Ctrl Pts',(-246.871240083843,4.28186178076673,
133.22792203719));
#137275=CARTESIAN_POINT('Ctrl Pts',(-246.879000526357,4.34774287164151,
133.107630692314));
#137276=CARTESIAN_POINT('Ctrl Pts',(-246.886760968871,4.40843357354889,
132.984933131863));
#137277=CARTESIAN_POINT('Ctrl Pts',(-246.894533869137,4.46922170155901,
132.862038606395));
#137278=CARTESIAN_POINT('Ctrl Pts',(-246.902306769402,4.52480263185307,
132.736730504097));
#137279=CARTESIAN_POINT('Ctrl Pts',(-246.910079669668,4.57500523485611,
132.609495006895));
#137280=CARTESIAN_POINT('Ctrl Pts',(-246.91757000543,4.62338284678781,132.486884840502));
#137281=CARTESIAN_POINT('Ctrl Pts',(-246.925060341192,4.66676627260832,
132.362485268479));
#137282=CARTESIAN_POINT('Ctrl Pts',(-246.932550676954,4.70504696574861,
132.23674189104));
#137283=CARTESIAN_POINT('Ctrl Pts',(-246.940325011073,4.74477908300408,
132.106230915229));
#137284=CARTESIAN_POINT('Ctrl Pts',(-246.948099345192,4.77913974844341,
131.973858802142));
#137285=CARTESIAN_POINT('Ctrl Pts',(-246.955873679311,4.80795298893047,
131.840107265514));
#137286=CARTESIAN_POINT('Ctrl Pts',(-246.963638432258,4.83673071967359,
131.706520565701));
#137287=CARTESIAN_POINT('Ctrl Pts',(-246.971403185205,4.85997454692671,
131.571558203401));
#137288=CARTESIAN_POINT('Ctrl Pts',(-246.979167938152,4.87755785436409,
131.435718234002));
#137289=CARTESIAN_POINT('Ctrl Pts',(-246.986924979037,4.89512369781274,
131.300013182774));
#137290=CARTESIAN_POINT('Ctrl Pts',(-246.994682019923,4.90704015983078,
131.163432644294));
#137291=CARTESIAN_POINT('Ctrl Pts',(-247.002439060808,4.91323147168139,
131.026485735865));
#137292=CARTESIAN_POINT('Ctrl Pts',(-247.010190252048,4.91941811461557,
130.889642100166));
#137293=CARTESIAN_POINT('Ctrl Pts',(-247.017941443288,4.91988818328002,
130.752433033427));
#137294=CARTESIAN_POINT('Ctrl Pts',(-247.025692634528,4.91461767161569,
130.615373304916));
#137295=CARTESIAN_POINT('Ctrl Pts',(-247.033440531305,4.90934940005942,
130.478371830445));
#137296=CARTESIAN_POINT('Ctrl Pts',(-247.041188428082,4.89834541594072,
130.341519957818));
#137297=CARTESIAN_POINT('Ctrl Pts',(-247.048936324859,4.88163381467735,
130.205332770218));
#137298=CARTESIAN_POINT('Ctrl Pts',(-247.056682600943,4.86492570912065,
130.069174070041));
#137299=CARTESIAN_POINT('Ctrl Pts',(-247.064428877027,4.84251240876081,
129.933680166145));
#137300=CARTESIAN_POINT('Ctrl Pts',(-247.072175153112,4.81447387592537,
129.799360935709));
#137301=CARTESIAN_POINT('Ctrl Pts',(-247.079921486377,4.78643513611589,
129.665040713759));
#137302=CARTESIAN_POINT('Ctrl Pts',(-247.087667819642,4.75277116086249,
129.531895565287));
#137303=CARTESIAN_POINT('Ctrl Pts',(-247.095414152908,4.71361294563391,
129.400424699779));
#137304=CARTESIAN_POINT('Ctrl Pts',(-247.103162220911,4.67444596119468,
129.268924392283));
#137305=CARTESIAN_POINT('Ctrl Pts',(-247.110910288914,4.62978240001419,
129.139099488472));
#137306=CARTESIAN_POINT('Ctrl Pts',(-247.118658356916,4.57980286770836,
129.011433191419));
#137307=CARTESIAN_POINT('Ctrl Pts',(-247.126414659658,4.52977021656062,
128.883631209106));
#137308=CARTESIAN_POINT('Ctrl Pts',(-247.1341709624,4.47441045080083,128.757992781089));
#137309=CARTESIAN_POINT('Ctrl Pts',(-247.141927265142,4.41395223155954,
128.634980807572));
#137310=CARTESIAN_POINT('Ctrl Pts',(-247.149687707656,4.35346174394628,
128.51190317886));
#137311=CARTESIAN_POINT('Ctrl Pts',(-247.15744815017,4.28786756752669,128.391455141073));
#137312=CARTESIAN_POINT('Ctrl Pts',(-247.165208592685,4.2174434417772,128.274073306229));
#137313=CARTESIAN_POINT('Ctrl Pts',(-247.17298149295,4.14690626496909,128.156503039644));
#137314=CARTESIAN_POINT('Ctrl Pts',(-247.180754393216,4.07152386005955,
128.042009138742));
#137315=CARTESIAN_POINT('Ctrl Pts',(-247.188527293481,3.99161276595695,
127.930998372887));
#137316=CARTESIAN_POINT('Ctrl Pts',(-247.196017629243,3.91460664140931,
127.82402312799));
#137317=CARTESIAN_POINT('Ctrl Pts',(-247.203507965005,3.83339555964348,
127.720282415859));
#137318=CARTESIAN_POINT('Ctrl Pts',(-247.210998300767,3.74829574466858,
127.620108417598));
#137319=CARTESIAN_POINT('Ctrl Pts',(-247.218772634886,3.659969344343,127.516136291745));
#137320=CARTESIAN_POINT('Ctrl Pts',(-247.226546969005,3.56717371560623,
127.415677330275));
#137321=CARTESIAN_POINT('Ctrl Pts',(-247.234321303124,3.47021902008662,
127.31913996241));
#137322=CARTESIAN_POINT('Ctrl Pts',(-247.242086056071,3.37338381256389,
127.222721568222));
#137323=CARTESIAN_POINT('Ctrl Pts',(-247.249850809018,3.2724000112201,127.130215424592));
#137324=CARTESIAN_POINT('Ctrl Pts',(-247.257615561966,3.16761820494175,
127.041997268523));
#137325=CARTESIAN_POINT('Ctrl Pts',(-247.265372602851,3.06294046943085,
126.953866731971));
#137326=CARTESIAN_POINT('Ctrl Pts',(-247.273129643736,2.95447253304266,
126.87001595777));
#137327=CARTESIAN_POINT('Ctrl Pts',(-247.280886684621,2.84260177573071,
126.790783882643));
#137328=CARTESIAN_POINT('Ctrl Pts',(-247.288637875861,2.73081538102692,
126.711611557041));
#137329=CARTESIAN_POINT('Ctrl Pts',(-247.296389067101,2.61563159081257,
126.637051222871));
#137330=CARTESIAN_POINT('Ctrl Pts',(-247.304140258341,2.49747051918889,
126.567401322472));
#137331=CARTESIAN_POINT('Ctrl Pts',(-247.311888155118,2.37935966917286,
126.497781025139));
#137332=CARTESIAN_POINT('Ctrl Pts',(-247.319636051895,2.2582743906818,126.43306720868));
#137333=CARTESIAN_POINT('Ctrl Pts',(-247.327383948672,2.13466322404559,
126.373514650665));
#137334=CARTESIAN_POINT('Ctrl Pts',(-247.335130224756,2.01107791420071,
126.313974549761));
#137335=CARTESIAN_POINT('Ctrl Pts',(-247.34287650084,1.88496811914733,126.259593729453));
#137336=CARTESIAN_POINT('Ctrl Pts',(-247.350622776924,1.75680603458676,
126.21058051624));
#137337=CARTESIAN_POINT('Ctrl Pts',(-247.35836911019,1.62864300396261,126.161566941222));
#137338=CARTESIAN_POINT('Ctrl Pts',(-247.366115443455,1.49842801877366,
126.117921192016));
#137339=CARTESIAN_POINT('Ctrl Pts',(-247.373861776721,1.36665188434967,
126.079802893344));
#137340=CARTESIAN_POINT('Ctrl Pts',(-247.381609844724,1.23484623957424,
126.041676058344));
#137341=CARTESIAN_POINT('Ctrl Pts',(-247.389357912726,1.10147912537945,
126.009079245644));
#137342=CARTESIAN_POINT('Ctrl Pts',(-247.397105980729,0.967054695941718,
125.982121689686));
#137343=CARTESIAN_POINT('Ctrl Pts',(-247.404862283471,0.832487398620895,
125.955135482918));
#137344=CARTESIAN_POINT('Ctrl Pts',(-247.412618586213,0.696860925235222,
125.93380058249));
#137345=CARTESIAN_POINT('Ctrl Pts',(-247.420374888955,0.560688323761253,
125.918174818182));
#137346=CARTESIAN_POINT('Ctrl Pts',(-247.428135331469,0.424443042869429,
125.902540713934));
#137347=CARTESIAN_POINT('Ctrl Pts',(-247.435895773983,0.287651442831393,
125.892621845748));
#137348=CARTESIAN_POINT('Ctrl Pts',(-247.443656216497,0.150828820579001,
125.888423908313));
#137349=CARTESIAN_POINT('Ctrl Pts',(-247.451429116763,0.0137865585068277,
125.884219231975));
#137350=CARTESIAN_POINT('Ctrl Pts',(-247.459202017028,-0.123286434129482,
125.885753834059));
#137351=CARTESIAN_POINT('Ctrl Pts',(-247.466974917294,-0.259876833731254,
125.892981270194));
#137352=CARTESIAN_POINT('Ctrl Pts',(-247.474465253056,-0.391501828257419,
125.899945970821));
#137353=CARTESIAN_POINT('Ctrl Pts',(-247.481955588818,-0.522678400849008,
125.912196765013));
#137354=CARTESIAN_POINT('Ctrl Pts',(-247.48944592458,-0.652956151334717,
125.929647156558));
#137355=CARTESIAN_POINT('Ctrl Pts',(-247.497220258699,-0.788173422326592,
125.947759185002));
#137356=CARTESIAN_POINT('Ctrl Pts',(-247.504994592818,-0.9228506957488,
125.971530253045));
#137357=CARTESIAN_POINT('Ctrl Pts',(-247.512768926937,-1.05647669859273,
126.000920178898));
#137358=CARTESIAN_POINT('Ctrl Pts',(-247.520533679884,-1.18993801933101,
126.030273884294));
#137359=CARTESIAN_POINT('Ctrl Pts',(-247.528298432831,-1.32235026916988,
126.065232586154));
#137360=CARTESIAN_POINT('Ctrl Pts',(-247.536063185778,-1.45320782807006,
126.105704419148));
#137361=CARTESIAN_POINT('Ctrl Pts',(-247.543820226663,-1.58393541739797,
126.146136054946));
#137362=CARTESIAN_POINT('Ctrl Pts',(-247.551577267548,-1.71311101760524,
126.192069810176));
#137363=CARTESIAN_POINT('Ctrl Pts',(-247.559334308433,-1.84024008330074,
126.243362974691));
#137364=CARTESIAN_POINT('Ctrl Pts',(-247.567085499674,-1.96727327997871,
126.294617458631));
#137365=CARTESIAN_POINT('Ctrl Pts',(-247.574836690914,-2.09226265290587,
126.351223161656));
#137366=CARTESIAN_POINT('Ctrl Pts',(-247.582587882154,-2.21473003215606,
126.41298794525));
#137367=CARTESIAN_POINT('Ctrl Pts',(-247.590335778931,-2.33714535950298,
126.474726477163));
#137368=CARTESIAN_POINT('Ctrl Pts',(-247.598083675708,-2.45704047677789,
126.541619552751));
#137369=CARTESIAN_POINT('Ctrl Pts',(-247.605831572485,-2.5739585853895,
126.613427515833));
#137370=CARTESIAN_POINT('Ctrl Pts',(-247.613577848569,-2.69085223725357,
126.685220458238));
#137371=CARTESIAN_POINT('Ctrl Pts',(-247.621324124653,-2.80476978615282,
126.76192603873));
#137372=CARTESIAN_POINT('Ctrl Pts',(-247.629070400737,-2.9152807277937,
126.843259591253));
#137373=CARTESIAN_POINT('Ctrl Pts',(-247.636816734003,-3.02579248520049,
126.924593744163));
#137374=CARTESIAN_POINT('Ctrl Pts',(-247.644563067268,-3.13289727029155,
127.010555705529));
#137375=CARTESIAN_POINT('Ctrl Pts',(-247.652309400533,-3.23619549399687,
127.10081882799));
#137376=CARTESIAN_POINT('Ctrl Pts',(-247.660057468536,-3.33951685062416,
127.191102164253));
#137377=CARTESIAN_POINT('Ctrl Pts',(-247.667805536539,-3.43902965523445,
127.285688321092));
#137378=CARTESIAN_POINT('Ctrl Pts',(-247.675553604542,-3.53436949814966,
127.384212183207));
#137379=CARTESIAN_POINT('Ctrl Pts',(-247.683309907284,-3.62981066938408,
127.482840757654));
#137380=CARTESIAN_POINT('Ctrl Pts',(-247.691066210026,-3.72106974707619,
127.58541511604));
#137381=CARTESIAN_POINT('Ctrl Pts',(-247.698822512768,-3.80782076243008,
127.69153487498));
#137382=CARTESIAN_POINT('Ctrl Pts',(-247.706582955282,-3.89461807941312,
127.797711273231));
#137383=CARTESIAN_POINT('Ctrl Pts',(-247.714343397796,-3.97690230527603,
127.907436529947));
#137384=CARTESIAN_POINT('Ctrl Pts',(-247.72210384031,-4.05439011833824,
128.020280189342));
#137385=CARTESIAN_POINT('Ctrl Pts',(-247.729876740576,-4.13200232171682,
128.133304995396));
#137386=CARTESIAN_POINT('Ctrl Pts',(-247.737649640841,-4.20480251823506,
128.249457876122));
#137387=CARTESIAN_POINT('Ctrl Pts',(-247.745422541107,-4.27255231891392,
128.368281853518));
#137388=CARTESIAN_POINT('Ctrl Pts',(-247.752912876869,-4.33783924368592,
128.482786280036));
#137389=CARTESIAN_POINT('Ctrl Pts',(-247.760403212631,-4.39843644522186,
128.599770699173));
#137390=CARTESIAN_POINT('Ctrl Pts',(-247.767893548393,-4.45417324294245,
128.718809423192));
#137391=CARTESIAN_POINT('Ctrl Pts',(-247.776601668254,-4.51897176875433,
128.857201547361));
#137392=CARTESIAN_POINT('Ctrl Pts',(-247.785309788114,-4.5773862407022,
128.998765569001));
#137393=CARTESIAN_POINT('Ctrl Pts',(-247.794017907975,-4.62912257715997,
129.142913288239));
#137394=CARTESIAN_POINT('Ctrl Pts',(-247.802726027836,-4.68085891361773,
129.287061007477));
#137395=CARTESIAN_POINT('Ctrl Pts',(-247.811434147697,-4.72591691600598,
129.43379214805));
#137396=CARTESIAN_POINT('Ctrl Pts',(-247.820142267558,-4.76405452823397,
129.582490119308));
#137397=CARTESIAN_POINT('Origin',(213.235140564004,0.,130.804360617566));
#137398=CARTESIAN_POINT('',(-249.915046309122,-4.76405452823416,129.582490119309));
#137399=CARTESIAN_POINT('',(-249.569887472766,-4.76405452823394,129.582490119308));
#137400=CARTESIAN_POINT('',(213.235140564004,-4.76405452823405,129.582490119308));
#137401=CARTESIAN_POINT('',(-248.235140564067,-4.91824790393295,130.808901317858));
#137402=CARTESIAN_POINT('Ctrl Pts',(-248.235140564067,-4.91824790393295,
130.808901317859));
#137403=CARTESIAN_POINT('Ctrl Pts',(-248.245073907718,-4.91808590314736,
130.984372054252));
#137404=CARTESIAN_POINT('Ctrl Pts',(-248.255007251369,-4.90852990301773,
131.159422601792));
#137405=CARTESIAN_POINT('Ctrl Pts',(-248.26494059502,-4.88973538646957,
131.333199830189));
#137406=CARTESIAN_POINT('Ctrl Pts',(-248.275093853796,-4.87052477655029,
131.510824327155));
#137407=CARTESIAN_POINT('Ctrl Pts',(-248.285247112572,-4.84166205004334,
131.687118758878));
#137408=CARTESIAN_POINT('Ctrl Pts',(-248.295400371347,-4.80336125477624,
131.86119727411));
#137409=CARTESIAN_POINT('Ctrl Pts',(-248.298666847518,-4.79103923700606,
131.917201295518));
#137410=CARTESIAN_POINT('Ctrl Pts',(-248.301933323689,-4.77774072783249,
131.972976140221));
#137411=CARTESIAN_POINT('Ctrl Pts',(-248.30519979986,-4.7634738916458,132.028492777959));
#137412=CARTESIAN_POINT('Ctrl Pts',(-248.312974133979,-4.72951829376561,
132.160624429435));
#137413=CARTESIAN_POINT('Ctrl Pts',(-248.320748468098,-4.69000704421847,
132.291551480925));
#137414=CARTESIAN_POINT('Ctrl Pts',(-248.328522802217,-4.64504042936055,
132.420770983812));
#137415=CARTESIAN_POINT('Ctrl Pts',(-248.336287555164,-4.60012923183666,
132.549831235209));
#137416=CARTESIAN_POINT('Ctrl Pts',(-248.344052308111,-4.54977617352532,
132.677187759432));
#137417=CARTESIAN_POINT('Ctrl Pts',(-248.351817061059,-4.49413219490759,
132.802349325541));
#137418=CARTESIAN_POINT('Ctrl Pts',(-248.359574101944,-4.43854348267371,
132.927386579419));
#137419=CARTESIAN_POINT('Ctrl Pts',(-248.367331142829,-4.3776744656515,
133.050232858668));
#137420=CARTESIAN_POINT('Ctrl Pts',(-248.375088183714,-4.31172526524681,
133.170413934702));
#137421=CARTESIAN_POINT('Ctrl Pts',(-248.382839374954,-4.24582579764725,
133.290504381252));
#137422=CARTESIAN_POINT('Ctrl Pts',(-248.390590566194,-4.17485395937299,
133.407933283708));
#137423=CARTESIAN_POINT('Ctrl Pts',(-248.398341757434,-4.0990570201475,
133.522248512252));
#137424=CARTESIAN_POINT('Ctrl Pts',(-248.406089654211,-4.02329229664303,
133.636515153774));
#137425=CARTESIAN_POINT('Ctrl Pts',(-248.413837550989,-3.94270676666548,
133.747670428353));
#137426=CARTESIAN_POINT('Ctrl Pts',(-248.421585447766,-3.85759236086982,
133.855289040171));
#137427=CARTESIAN_POINT('Ctrl Pts',(-248.42933172385,-3.77249575917322,
133.962885140495));
#137428=CARTESIAN_POINT('Ctrl Pts',(-248.437077999934,-3.6828724083491,
134.066945743093));
#137429=CARTESIAN_POINT('Ctrl Pts',(-248.444824276018,-3.58905582830071,
134.167076978462));
#137430=CARTESIAN_POINT('Ctrl Pts',(-248.452570609284,-3.49523855571951,
134.267208952978));
#137431=CARTESIAN_POINT('Ctrl Pts',(-248.460316942549,-3.3972282594602,
134.363411217083));
#137432=CARTESIAN_POINT('Ctrl Pts',(-248.468063275814,-3.29539649553318,
134.455325558472));
#137433=CARTESIAN_POINT('Ctrl Pts',(-248.475811343817,-3.19354192708882,
134.547260483441));
#137434=CARTESIAN_POINT('Ctrl Pts',(-248.483559411821,-3.08786447822106,
134.634905312997));
#137435=CARTESIAN_POINT('Ctrl Pts',(-248.491307479824,-2.97876974863656,
134.717941311395));
#137436=CARTESIAN_POINT('Ctrl Pts',(-248.499063782565,-2.86955907187506,
134.80106556144));
#137437=CARTESIAN_POINT('Ctrl Pts',(-248.506820085307,-2.75692417082953,
134.879570958235));
#137438=CARTESIAN_POINT('Ctrl Pts',(-248.514576388049,-2.64130112623105,
134.953181103327));
#137439=CARTESIAN_POINT('Ctrl Pts',(-248.522336830563,-2.52561637013232,
135.02683053637));
#137440=CARTESIAN_POINT('Ctrl Pts',(-248.530097273078,-2.4069406307171,
135.095579315715));
#137441=CARTESIAN_POINT('Ctrl Pts',(-248.537857715592,-2.28573481363392,
135.159196943336));
#137442=CARTESIAN_POINT('Ctrl Pts',(-248.545630615857,-2.16433442621301,
135.22291669562));
#137443=CARTESIAN_POINT('Ctrl Pts',(-248.553403516123,-2.04039619862537,
135.281488668921));
#137444=CARTESIAN_POINT('Ctrl Pts',(-248.561176416388,-1.91440206615066,
135.33473011592));
#137445=CARTESIAN_POINT('Ctrl Pts',(-248.568666752149,-1.79298813777539,
135.386036102204));
#137446=CARTESIAN_POINT('Ctrl Pts',(-248.576157087909,-1.66966547237897,
135.432392281381));
#137447=CARTESIAN_POINT('Ctrl Pts',(-248.58364742367,-1.5448769370361,135.473679444966));
#137448=CARTESIAN_POINT('Ctrl Pts',(-248.591421757789,-1.4153570064224,
135.516532023916));
#137449=CARTESIAN_POINT('Ctrl Pts',(-248.599196091908,-1.28384757446238,
135.554059360057));
#137450=CARTESIAN_POINT('Ctrl Pts',(-248.606970426027,-1.15082599329778,
135.58607397113));
#137451=CARTESIAN_POINT('Ctrl Pts',(-248.614735178974,-1.01796834934349,
135.618049127055));
#137452=CARTESIAN_POINT('Ctrl Pts',(-248.622499931921,-0.883602640633271,
135.644524985225));
#137453=CARTESIAN_POINT('Ctrl Pts',(-248.630264684868,-0.748223740684508,
135.665363013819));
#137454=CARTESIAN_POINT('Ctrl Pts',(-248.638021725753,-0.612979300967315,
135.686180345789));
#137455=CARTESIAN_POINT('Ctrl Pts',(-248.645778766639,-0.47672405653943,
135.701370932492));
#137456=CARTESIAN_POINT('Ctrl Pts',(-248.653535807524,-0.339965159850539,
135.710846809597));
#137457=CARTESIAN_POINT('Ctrl Pts',(-248.661286998764,-0.203309394110027,
135.720315540869));
#137458=CARTESIAN_POINT('Ctrl Pts',(-248.669038190004,-0.0661511205453898,
135.724078113441));
#137459=CARTESIAN_POINT('Ctrl Pts',(-248.676789381244,0.0709956158974349,
135.722098175125));
#137460=CARTESIAN_POINT('Ctrl Pts',(-248.684537278021,0.208084061318949,
135.720119078335));
#137461=CARTESIAN_POINT('Ctrl Pts',(-248.692285174798,0.345160589265472,
135.712402330694));
#137462=CARTESIAN_POINT('Ctrl Pts',(-248.700033071575,0.48170959067201,
135.698963658953));
#137463=CARTESIAN_POINT('Ctrl Pts',(-248.707779347659,0.618230028971109,
135.685527798293));
#137464=CARTESIAN_POINT('Ctrl Pts',(-248.715525623743,0.754222771377872,
135.666372432507));
#137465=CARTESIAN_POINT('Ctrl Pts',(-248.723271899827,0.889176168671283,
135.641565265249));
#137466=CARTESIAN_POINT('Ctrl Pts',(-248.731018233092,1.0241305621602,135.616757914871));
#137467=CARTESIAN_POINT('Ctrl Pts',(-248.738764566358,1.15804521070374,
135.586298750453));
#137468=CARTESIAN_POINT('Ctrl Pts',(-248.746510899623,1.29041790504549,
135.550306750092));
#137469=CARTESIAN_POINT('Ctrl Pts',(-248.754258967626,1.42282024333416,
135.514306689572));
#137470=CARTESIAN_POINT('Ctrl Pts',(-248.762007035629,1.55367956309814,
135.472771430119));
#137471=CARTESIAN_POINT('Ctrl Pts',(-248.769755103632,1.68250846637917,
135.4258699298));
#137472=CARTESIAN_POINT('Ctrl Pts',(-248.777511406374,1.81147429055153,
135.378918582007));
#137473=CARTESIAN_POINT('Ctrl Pts',(-248.785267709116,1.93840501953951,
135.326589734343));
#137474=CARTESIAN_POINT('Ctrl Pts',(-248.793024011857,2.0628323992081,135.26910087376));
#137475=CARTESIAN_POINT('Ctrl Pts',(-248.800784454372,2.18732618951599,
135.21158132964));
#137476=CARTESIAN_POINT('Ctrl Pts',(-248.808544896886,2.30931362061622,
135.14889646352));
#137477=CARTESIAN_POINT('Ctrl Pts',(-248.8163053394,2.42835163722904,135.081309458559));
#137478=CARTESIAN_POINT('Ctrl Pts',(-248.824078239665,2.54758074423383,
135.013613956937));
#137479=CARTESIAN_POINT('Ctrl Pts',(-248.831851139931,2.66385064358805,
134.941000798226));
#137480=CARTESIAN_POINT('Ctrl Pts',(-248.839624040196,2.77674708700557,
134.863776668836));
#137481=CARTESIAN_POINT('Ctrl Pts',(-248.847114375959,2.88553946034968,
134.789359831055));
#137482=CARTESIAN_POINT('Ctrl Pts',(-248.854604711722,2.99119913977137,
134.710661627111));
#137483=CARTESIAN_POINT('Ctrl Pts',(-248.862095047485,3.09338645132278,
134.627990218518));
#137484=CARTESIAN_POINT('Ctrl Pts',(-248.869869381604,3.19944822583808,
134.54218429835));
#137485=CARTESIAN_POINT('Ctrl Pts',(-248.877643715723,3.30210509683432,
134.451826130541));
#137486=CARTESIAN_POINT('Ctrl Pts',(-248.885418049842,3.40094130968244,
134.357215986223));
#137487=CARTESIAN_POINT('Ctrl Pts',(-248.893182802789,3.49965571573175,
134.262722440453));
#137488=CARTESIAN_POINT('Ctrl Pts',(-248.900947555737,3.59455855266774,
134.163987612328));
#137489=CARTESIAN_POINT('Ctrl Pts',(-248.908712308684,3.68526577852324,
134.061352973121));
#137490=CARTESIAN_POINT('Ctrl Pts',(-248.916469349569,3.77588291268327,
133.958820272086));
#137491=CARTESIAN_POINT('Ctrl Pts',(-248.924226390454,3.86231247132771,
133.852395759161));
#137492=CARTESIAN_POINT('Ctrl Pts',(-248.931983431339,3.94420631928851,
133.742458569198));
#137493=CARTESIAN_POINT('Ctrl Pts',(-248.939734622579,4.0260384104614,133.632604283726));
#137494=CARTESIAN_POINT('Ctrl Pts',(-248.947485813819,4.10334136646626,
133.519242906031));
#137495=CARTESIAN_POINT('Ctrl Pts',(-248.955237005059,4.17580674932749,
133.402787267439));
#137496=CARTESIAN_POINT('Ctrl Pts',(-248.962984901836,4.24824133246802,
133.2863811256));
#137497=CARTESIAN_POINT('Ctrl Pts',(-248.970732798614,4.3158422257627,133.166883669836));
#137498=CARTESIAN_POINT('Ctrl Pts',(-248.978480695391,4.37834396127831,
133.044737197348));
#137499=CARTESIAN_POINT('Ctrl Pts',(-248.986226971475,4.44083262277824,
132.92261627527));
#137500=CARTESIAN_POINT('Ctrl Pts',(-248.993973247559,4.4982240701115,132.797847786463));
#137501=CARTESIAN_POINT('Ctrl Pts',(-249.001719523643,4.55029870537798,
132.670898791388));
#137502=CARTESIAN_POINT('Ctrl Pts',(-249.009465856909,4.60237372504752,
132.543948859205));
#137503=CARTESIAN_POINT('Ctrl Pts',(-249.017212190174,4.64913170595849,
132.41481875035));
#137504=CARTESIAN_POINT('Ctrl Pts',(-249.024958523439,4.69040129138085,
132.28399529826));
#137505=CARTESIAN_POINT('Ctrl Pts',(-249.032706591443,4.73168011884067,
132.153142549166));
#137506=CARTESIAN_POINT('Ctrl Pts',(-249.040454659446,4.76746798747111,
132.020596075029));
#137507=CARTESIAN_POINT('Ctrl Pts',(-249.048202727449,4.79764359597526,
131.886857263518));
#137508=CARTESIAN_POINT('Ctrl Pts',(-249.05595903019,4.82785127547527,131.752976312806));
#137509=CARTESIAN_POINT('Ctrl Pts',(-249.063715332932,4.85243469337686,
131.617900875276));
#137510=CARTESIAN_POINT('Ctrl Pts',(-249.071471635674,4.87132372481567,
131.482142463404));
#137511=CARTESIAN_POINT('Ctrl Pts',(-249.079232078188,4.89022283789929,
131.34631159318));
#137512=CARTESIAN_POINT('Ctrl Pts',(-249.086992520703,4.90342147092034,
131.20979741123));
#137513=CARTESIAN_POINT('Ctrl Pts',(-249.094752963217,4.91090156512548,
131.073114929435));
#137514=CARTESIAN_POINT('Ctrl Pts',(-249.102525863482,4.9183936670419,130.936213032786));
#137515=CARTESIAN_POINT('Ctrl Pts',(-249.110298763748,4.92014888075586,
130.799142687565));
#137516=CARTESIAN_POINT('Ctrl Pts',(-249.118071664013,4.91620131891253,
130.662418184084));
#137517=CARTESIAN_POINT('Ctrl Pts',(-249.125561999775,4.91239726088594,
130.530663960708));
#137518=CARTESIAN_POINT('Ctrl Pts',(-249.133052335536,4.90329787066862,
130.399231178461));
#137519=CARTESIAN_POINT('Ctrl Pts',(-249.140542671297,4.88897881120401,
130.268572183482));
#137520=CARTESIAN_POINT('Ctrl Pts',(-249.148317005416,4.87411684024612,
130.132959212982));
#137521=CARTESIAN_POINT('Ctrl Pts',(-249.156091339535,4.85358450089919,
129.997750283198));
#137522=CARTESIAN_POINT('Ctrl Pts',(-249.163865673654,4.82740969424021,
129.863457484159));
#137523=CARTESIAN_POINT('Ctrl Pts',(-249.171630426601,4.80126714569114,
129.729330188992));
#137524=CARTESIAN_POINT('Ctrl Pts',(-249.179395179549,4.76949603996935,
129.596117158157));
#137525=CARTESIAN_POINT('Ctrl Pts',(-249.187159932496,4.73217608246419,
129.464326070603));
#137526=CARTESIAN_POINT('Ctrl Pts',(-249.194916973381,4.69489319166695,
129.332665879815));
#137527=CARTESIAN_POINT('Ctrl Pts',(-249.202674014265,4.65207252245242,
129.202425195518));
#137528=CARTESIAN_POINT('Ctrl Pts',(-249.21043105515,4.60384487614628,129.074101845335));
#137529=CARTESIAN_POINT('Ctrl Pts',(-249.218182246391,4.5556535986833,128.945875264789));
#137530=CARTESIAN_POINT('Ctrl Pts',(-249.225933437631,4.50206359701916,
128.81956350492));
#137531=CARTESIAN_POINT('Ctrl Pts',(-249.233684628871,4.44325547958013,
128.695649208748));
#137532=CARTESIAN_POINT('Ctrl Pts',(-249.241432525648,4.38447235715986,
128.571787579457));
#137533=CARTESIAN_POINT('Ctrl Pts',(-249.249180422425,4.32047569735252,
128.450321739644));
#137534=CARTESIAN_POINT('Ctrl Pts',(-249.256928319202,4.25149412541846,
128.331714107441));
#137535=CARTESIAN_POINT('Ctrl Pts',(-249.264674595286,4.18252698294219,
128.213131285398));
#137536=CARTESIAN_POINT('Ctrl Pts',(-249.27242087137,4.10857719883152,128.097405819508));
#137537=CARTESIAN_POINT('Ctrl Pts',(-249.280167147454,4.02991902624946,
127.984974921289));
#137538=CARTESIAN_POINT('Ctrl Pts',(-249.287913480719,3.95126027303076,
127.872543193131));
#137539=CARTESIAN_POINT('Ctrl Pts',(-249.295659813985,3.86789328610782,
127.763406401521));
#137540=CARTESIAN_POINT('Ctrl Pts',(-249.30340614725,3.78013502974059,127.657971859096));
#137541=CARTESIAN_POINT('Ctrl Pts',(-249.311154215253,3.69235712052021,
127.552513705335));
#137542=CARTESIAN_POINT('Ctrl Pts',(-249.318902283256,3.60018623508184,
127.450759750993));
#137543=CARTESIAN_POINT('Ctrl Pts',(-249.326650351259,3.50397863875588,
127.353083062567));
#137544=CARTESIAN_POINT('Ctrl Pts',(-249.334406654001,3.40766879185178,
127.255302562194));
#137545=CARTESIAN_POINT('Ctrl Pts',(-249.342162956743,3.30731393858388,
127.161608263089));
#137546=CARTESIAN_POINT('Ctrl Pts',(-249.349919259484,3.20330652468301,
127.072335648273));
#137547=CARTESIAN_POINT('Ctrl Pts',(-249.357679701999,3.09924359889373,
126.983015385976));
#137548=CARTESIAN_POINT('Ctrl Pts',(-249.365440144513,2.99152453488068,
126.898121752322));
#137549=CARTESIAN_POINT('Ctrl Pts',(-249.373200587027,2.88057286552903,
126.817948317154));
#137550=CARTESIAN_POINT('Ctrl Pts',(-249.380973487292,2.76944308670791,
126.73764618047));
#137551=CARTESIAN_POINT('Ctrl Pts',(-249.388746387558,2.65507065912805,
126.662079599741));
#137552=CARTESIAN_POINT('Ctrl Pts',(-249.396519287823,2.53790670851151,
126.591497861507));
#137553=CARTESIAN_POINT('Ctrl Pts',(-249.404009623585,2.42500196261268,
126.523481947239));
#137554=CARTESIAN_POINT('Ctrl Pts',(-249.411499959348,2.30950539784452,
126.460094892698));
#137555=CARTESIAN_POINT('Ctrl Pts',(-249.41899029511,2.19183848349302,126.401517544644));
#137556=CARTESIAN_POINT('Ctrl Pts',(-249.426764629229,2.06971019232514,
126.340719218637));
#137557=CARTESIAN_POINT('Ctrl Pts',(-249.434538963348,1.94485685943472,
126.284909928026));
#137558=CARTESIAN_POINT('Ctrl Pts',(-249.442313297467,1.81772440187811,
126.234342996012));
#137559=CARTESIAN_POINT('Ctrl Pts',(-249.450078050414,1.69074862371295,
126.183838383222));
#137560=CARTESIAN_POINT('Ctrl Pts',(-249.457842803361,1.56149966938691,
126.138563417195));
#137561=CARTESIAN_POINT('Ctrl Pts',(-249.465607556308,1.43044774628691,
126.0987254524));
#137562=CARTESIAN_POINT('Ctrl Pts',(-249.473364597193,1.29952598580481,
126.058927055234));
#137563=CARTESIAN_POINT('Ctrl Pts',(-249.481121638079,1.16680519183354,
126.024555025821));
#137564=CARTESIAN_POINT('Ctrl Pts',(-249.488878678964,1.03277490216421,
125.99576840529));
#137565=CARTESIAN_POINT('Ctrl Pts',(-249.496629870204,0.898845685778742,
125.967003492974));
#137566=CARTESIAN_POINT('Ctrl Pts',(-249.504381061444,0.763609319957393,
125.943815687576));
#137567=CARTESIAN_POINT('Ctrl Pts',(-249.512132252684,0.627569489207782,
125.926313918454));
#137568=CARTESIAN_POINT('Ctrl Pts',(-249.519880149461,0.491587479015407,
125.908819588051));
#137569=CARTESIAN_POINT('Ctrl Pts',(-249.527628046238,0.354803070057864,
125.897006537039));
#137570=CARTESIAN_POINT('Ctrl Pts',(-249.535375943015,0.217728885343782,
125.890932364809));
#137571=CARTESIAN_POINT('Ctrl Pts',(-249.543122219099,0.0806833735941654,
125.884859463165));
#137572=CARTESIAN_POINT('Ctrl Pts',(-249.550868495183,-0.0566514030112906,
125.884523069839));
#137573=CARTESIAN_POINT('Ctrl Pts',(-249.558614771267,-0.193759365505211,
125.889928771383));
#137574=CARTESIAN_POINT('Ctrl Pts',(-249.566361104533,-0.330868340099152,
125.89533451283));
#137575=CARTESIAN_POINT('Ctrl Pts',(-249.574107437798,-0.467750106578944,
125.906482418326));
#137576=CARTESIAN_POINT('Ctrl Pts',(-249.581853771064,-0.603890654364946,
125.923325979288));
#137577=CARTESIAN_POINT('Ctrl Pts',(-249.589601839067,-0.740061689882508,
125.940173312249));
#137578=CARTESIAN_POINT('Ctrl Pts',(-249.597349907069,-0.875490788471238,
125.962718790783));
#137579=CARTESIAN_POINT('Ctrl Pts',(-249.605097975072,-1.00967150860756,
125.990864330333));
#137580=CARTESIAN_POINT('Ctrl Pts',(-249.612854277814,-1.14399483761019,
126.019039783297));
#137581=CARTESIAN_POINT('Ctrl Pts',(-249.620610580556,-1.27706675450334,
126.052827106273));
#137582=CARTESIAN_POINT('Ctrl Pts',(-249.628366883298,-1.40839288141555,
126.092077460319));
#137583=CARTESIAN_POINT('Ctrl Pts',(-249.636127325812,-1.53978910103584,
126.13134876346));
#137584=CARTESIAN_POINT('Ctrl Pts',(-249.643887768326,-1.66943730462585,
126.176088780145));
#137585=CARTESIAN_POINT('Ctrl Pts',(-249.65164821084,-1.79686157369262,
126.226099861833));
#137586=CARTESIAN_POINT('Ctrl Pts',(-249.659421111106,-1.92449039550829,
126.276191225748));
#137587=CARTESIAN_POINT('Ctrl Pts',(-249.667194011371,-2.04988779084198,
126.331570405567));
#137588=CARTESIAN_POINT('Ctrl Pts',(-249.674966911637,-2.17260018339459,
126.391992601907));
#137589=CARTESIAN_POINT('Ctrl Pts',(-249.682457247399,-2.29085167138406,
126.450218299215));
#137590=CARTESIAN_POINT('Ctrl Pts',(-249.689947583161,-2.40660970999656,
126.513126578891));
#137591=CARTESIAN_POINT('Ctrl Pts',(-249.697437918923,-2.5194943332875,
126.580460598977));
#137592=CARTESIAN_POINT('Ctrl Pts',(-249.705213487546,-2.63667761621944,
126.650358706415));
#137593=CARTESIAN_POINT('Ctrl Pts',(-249.712989056169,-2.75113556809579,
126.725247750044));
#137594=CARTESIAN_POINT('Ctrl Pts',(-249.720764624791,-2.86241381722082,
126.804889377329));
#137595=CARTESIAN_POINT('Ctrl Pts',(-249.728859694972,-2.97826453887508,
126.887803514343));
#137596=CARTESIAN_POINT('Ctrl Pts',(-249.736954765152,-3.09066828496617,
126.97586899289));
#137597=CARTESIAN_POINT('Ctrl Pts',(-249.745049835333,-3.19914004090874,
127.06876346836));
#137598=CARTESIAN_POINT('Ctrl Pts',(-249.752805844448,-3.30306847007098,
127.157767069616));
#137599=CARTESIAN_POINT('Ctrl Pts',(-249.760561853563,-3.40338725556096,
127.251203075515));
#137600=CARTESIAN_POINT('Ctrl Pts',(-249.768317862678,-3.49969948600923,
127.348743947545));
#137601=CARTESIAN_POINT('Ctrl Pts',(-249.776068582077,-3.59594603005828,
127.446218295224));
#137602=CARTESIAN_POINT('Ctrl Pts',(-249.783819301476,-3.68819118215815,
127.547791662028));
#137603=CARTESIAN_POINT('Ctrl Pts',(-249.791570020876,-3.77607264096405,
127.653097621137));
#137604=CARTESIAN_POINT('Ctrl Pts',(-249.799317132766,-3.86391319605633,
127.75835456644));
#137605=CARTESIAN_POINT('Ctrl Pts',(-249.807064244655,-3.94739385008372,
127.867340347028));
#137606=CARTESIAN_POINT('Ctrl Pts',(-249.814811356545,-4.02619085685783,
127.979653509448));
#137607=CARTESIAN_POINT('Ctrl Pts',(-249.822556540329,-4.10496825258799,
128.091938719303));
#137608=CARTESIAN_POINT('Ctrl Pts',(-249.830301724113,-4.17906409811855,
128.207549342181));
#137609=CARTESIAN_POINT('Ctrl Pts',(-249.838046907898,-4.24819670454866,
128.32605316651));
#137610=CARTESIAN_POINT('Ctrl Pts',(-249.845793796111,-4.31734452451827,
128.444583069164));
#137611=CARTESIAN_POINT('Ctrl Pts',(-249.853540684325,-4.38152672280169,
128.566007109581));
#137612=CARTESIAN_POINT('Ctrl Pts',(-249.861287572539,-4.44050651143091,
128.689866591933));
#137613=CARTESIAN_POINT('Ctrl Pts',(-249.86903549896,-4.4994942043001,128.813742673446));
#137614=CARTESIAN_POINT('Ctrl Pts',(-249.876783425381,-4.55327793829618,
128.940054490589));
#137615=CARTESIAN_POINT('Ctrl Pts',(-249.884531351803,-4.60166857118941,
129.068322189585));
#137616=CARTESIAN_POINT('Ctrl Pts',(-249.892284423878,-4.65009134190414,
129.196675075406));
#137617=CARTESIAN_POINT('Ctrl Pts',(-249.900037495954,-4.69311373133983,
129.32698606768));
#137618=CARTESIAN_POINT('Ctrl Pts',(-249.90779056803,-4.73059604889384,
129.45875886196));
#137619=CARTESIAN_POINT('Ctrl Pts',(-249.910209148394,-4.74228870392702,
129.499865547107));
#137620=CARTESIAN_POINT('Ctrl Pts',(-249.912627728758,-4.75344260573139,
129.541114394529));
#137621=CARTESIAN_POINT('Ctrl Pts',(-249.915046309122,-4.76405452823416,
129.582490119309));
#137622=CARTESIAN_POINT('Ctrl Pts',(-248.165132725248,-4.76405452823402,
129.582490119308));
#137623=CARTESIAN_POINT('Ctrl Pts',(-248.172792275957,-4.79778234205211,
129.713994353494));
#137624=CARTESIAN_POINT('Ctrl Pts',(-248.180451826665,-4.82605794979784,
129.84688428109));
#137625=CARTESIAN_POINT('Ctrl Pts',(-248.188111377374,-4.84878389437866,
129.980662973941));
#137626=CARTESIAN_POINT('Ctrl Pts',(-248.195949575147,-4.87203988614429,
130.117561845989));
#137627=CARTESIAN_POINT('Ctrl Pts',(-248.203787772921,-4.88948405967343,
130.255391020222));
#137628=CARTESIAN_POINT('Ctrl Pts',(-248.211625970694,-4.90106802037398,
130.393610910119));
#137629=CARTESIAN_POINT('Ctrl Pts',(-248.219464168467,-4.91265198107455,
130.531830800017));
#137630=CARTESIAN_POINT('Ctrl Pts',(-248.227302366241,-4.91837573540535,
130.670440957191));
#137631=CARTESIAN_POINT('Ctrl Pts',(-248.235140564014,-4.91824790393381,
130.808901316927));
#137632=CARTESIAN_POINT('',(-247.889859435962,-4.91824972168853,130.802706044916));
#137633=CARTESIAN_POINT('Ctrl Pts',(-247.820142267558,-4.76405452823397,
129.582490119308));
#137634=CARTESIAN_POINT('Ctrl Pts',(-247.828536217527,-4.80081621894209,
129.725823393442));
#137635=CARTESIAN_POINT('Ctrl Pts',(-247.836930167496,-4.83114800021644,
129.870983747846));
#137636=CARTESIAN_POINT('Ctrl Pts',(-247.845324117465,-4.85488130107452,
130.017397711847));
#137637=CARTESIAN_POINT('Ctrl Pts',(-247.853689943783,-4.87853508429589,
130.163321120723));
#137638=CARTESIAN_POINT('Ctrl Pts',(-247.862055770101,-4.89563442656382,
130.310489485434));
#137639=CARTESIAN_POINT('Ctrl Pts',(-247.870421596419,-4.90606132854246,
130.458318274665));
#137640=CARTESIAN_POINT('Ctrl Pts',(-247.876900876267,-4.91413689852136,
130.572810741822));
#137641=CARTESIAN_POINT('Ctrl Pts',(-247.883380156114,-4.9182110315957,
130.687698983515));
#137642=CARTESIAN_POINT('Ctrl Pts',(-247.889859435962,-4.91824972168853,
130.802706044916));
#137643=CARTESIAN_POINT('Ctrl Pts',(-247.889859435997,-4.91824972168874,
130.802706045539));
#137644=CARTESIAN_POINT('Ctrl Pts',(-247.897794815772,-4.91829710665618,
130.94355884562));
#137645=CARTESIAN_POINT('Ctrl Pts',(-247.905730195547,-4.91228935523591,
131.084363800434));
#137646=CARTESIAN_POINT('Ctrl Pts',(-247.913665575322,-4.90026508898193,
131.224580940974));
#137647=CARTESIAN_POINT('Ctrl Pts',(-247.921605586623,-4.88823380470223,
131.364879919979));
#137648=CARTESIAN_POINT('Ctrl Pts',(-247.929545597924,-4.8701790377454,
131.504590038808));
#137649=CARTESIAN_POINT('Ctrl Pts',(-247.937485609225,-4.84619113119443,
131.643177988889));
#137650=CARTESIAN_POINT('Ctrl Pts',(-247.945431595334,-4.82218517389707,
131.781870225516));
#137651=CARTESIAN_POINT('Ctrl Pts',(-247.953377581442,-4.79223724032085,
131.919438252654));
#137652=CARTESIAN_POINT('Ctrl Pts',(-247.961323567551,-4.75648844461589,
132.055360513144));
#137653=CARTESIAN_POINT('Ctrl Pts',(-247.969282639919,-4.72068077415252,
132.191506624258));
#137654=CARTESIAN_POINT('Ctrl Pts',(-247.977241712287,-4.67905324684613,
132.326001201571));
#137655=CARTESIAN_POINT('Ctrl Pts',(-247.985200784655,-4.63179671806932,
132.458338315415));
#137656=CARTESIAN_POINT('Ctrl Pts',(-247.993167071821,-4.58449735185158,
132.590795391166));
#137657=CARTESIAN_POINT('Ctrl Pts',(-248.001133358986,-4.53155894570825,
132.721090767681));
#137658=CARTESIAN_POINT('Ctrl Pts',(-248.009099646152,-4.47321970686905,
132.848740356406));
#137659=CARTESIAN_POINT('Ctrl Pts',(-248.017080531472,-4.41477356186177,
132.976623861936));
#137660=CARTESIAN_POINT('Ctrl Pts',(-248.025061416793,-4.35090697226165,
133.10185156794));
#137661=CARTESIAN_POINT('Ctrl Pts',(-248.033042302113,-4.28190365658586,
133.223964745976));
#137662=CARTESIAN_POINT('Ctrl Pts',(-248.037475258811,-4.24357599015597,
133.291792112076));
#137663=CARTESIAN_POINT('Ctrl Pts',(-248.041908215508,-4.20366430447484,
133.358659105839));
#137664=CARTESIAN_POINT('Ctrl Pts',(-248.046341172206,-4.16222272274684,
133.424491352615));
#137665=CARTESIAN_POINT('Ctrl Pts',(-248.054115506325,-4.08954420933897,
133.539945194637));
#137666=CARTESIAN_POINT('Ctrl Pts',(-248.061889840444,-4.01194316211871,
133.652555625427));
#137667=CARTESIAN_POINT('Ctrl Pts',(-248.069664174563,-3.92966864626729,
133.761874335716));
#137668=CARTESIAN_POINT('Ctrl Pts',(-248.07742892751,-3.84749552640357,
133.871058320464));
#137669=CARTESIAN_POINT('Ctrl Pts',(-248.085193680457,-3.76066063070443,
133.976958347055));
#137670=CARTESIAN_POINT('Ctrl Pts',(-248.092958433404,-3.66945768165939,
134.079152730817));
#137671=CARTESIAN_POINT('Ctrl Pts',(-248.100715474289,-3.57834531666907,
134.181245613677));
#137672=CARTESIAN_POINT('Ctrl Pts',(-248.108472515174,-3.48287379060651,
134.279639888254));
#137673=CARTESIAN_POINT('Ctrl Pts',(-248.116229556059,-3.38337846682548,
134.373945076956));
#137674=CARTESIAN_POINT('Ctrl Pts',(-248.1239807473,-3.28395817324195,134.468179149382));
#137675=CARTESIAN_POINT('Ctrl Pts',(-248.13173193854,-3.18052040429157,
134.558330005808));
#137676=CARTESIAN_POINT('Ctrl Pts',(-248.13948312978,-3.07343867253532,
134.64404260813));
#137677=CARTESIAN_POINT('Ctrl Pts',(-248.147231026557,-2.96640245337171,
134.72971878031));
#137678=CARTESIAN_POINT('Ctrl Pts',(-248.154978923334,-2.8557256563982,
134.810960206441));
#137679=CARTESIAN_POINT('Ctrl Pts',(-248.162726820111,-2.74181612894852,
134.887451037522));
#137680=CARTESIAN_POINT('Ctrl Pts',(-248.170473096195,-2.62793042891638,
134.963925868371));
#137681=CARTESIAN_POINT('Ctrl Pts',(-248.178219372279,-2.51081366781225,
135.035651862921));
#137682=CARTESIAN_POINT('Ctrl Pts',(-248.185965648363,-2.39090370055229,
135.102355796389));
#137683=CARTESIAN_POINT('Ctrl Pts',(-248.193711981629,-2.27099284814436,
135.16906022225));
#137684=CARTESIAN_POINT('Ctrl Pts',(-248.201458314894,-2.14828909009672,
135.230742322996));
#137685=CARTESIAN_POINT('Ctrl Pts',(-248.209204648159,-2.02325561360943,
135.287174441996));
#137686=CARTESIAN_POINT('Ctrl Pts',(-248.216952716162,-1.89819413674217,
135.343619198577));
#137687=CARTESIAN_POINT('Ctrl Pts',(-248.224700784165,-1.77080225954732,
135.394811473107));
#137688=CARTESIAN_POINT('Ctrl Pts',(-248.232448852168,-1.64156353356948,
135.440571595051));
#137689=CARTESIAN_POINT('Ctrl Pts',(-248.24020515491,-1.51218745113518,
135.486380351398));
#137690=CARTESIAN_POINT('Ctrl Pts',(-248.247961457652,-1.38096096804064,
135.526745291558));
#137691=CARTESIAN_POINT('Ctrl Pts',(-248.255717760394,-1.24838373415665,
135.561536367398));
#137692=CARTESIAN_POINT('Ctrl Pts',(-248.263478202908,-1.1157357398111,
135.596346012284));
#137693=CARTESIAN_POINT('Ctrl Pts',(-248.271238645422,-0.981735939945509,
135.62557578175));
#137694=CARTESIAN_POINT('Ctrl Pts',(-248.278999087936,-0.846893608806071,
135.649146916038));
#137695=CARTESIAN_POINT('Ctrl Pts',(-248.286771988202,-0.711834816785949,
135.672755888804));
#137696=CARTESIAN_POINT('Ctrl Pts',(-248.294544888467,-0.575931178582748,
135.690688023004));
#137697=CARTESIAN_POINT('Ctrl Pts',(-248.302317788733,-0.439697413820081,
135.702916450338));
#137698=CARTESIAN_POINT('Ctrl Pts',(-248.309808124495,-0.308416089557942,
135.714700343536));
#137699=CARTESIAN_POINT('Ctrl Pts',(-248.317298460257,-0.176828531537549,
135.721188003327));
#137700=CARTESIAN_POINT('Ctrl Pts',(-248.324788796019,-0.0453928562305962,
135.722401137031));
#137701=CARTESIAN_POINT('Ctrl Pts',(-248.332563130138,0.0910262426536748,
135.723660267069));
#137702=CARTESIAN_POINT('Ctrl Pts',(-248.340337464257,0.227713848903923,
135.719240996771));
#137703=CARTESIAN_POINT('Ctrl Pts',(-248.348111798376,0.364158161420716,
135.709110549619));
#137704=CARTESIAN_POINT('Ctrl Pts',(-248.355876551323,0.500434318516711,
135.698992587337));
#137705=CARTESIAN_POINT('Ctrl Pts',(-248.36364130427,0.636467392317943,
135.683177481418));
#137706=CARTESIAN_POINT('Ctrl Pts',(-248.371406057217,0.77174384338724,
135.661684418044));
#137707=CARTESIAN_POINT('Ctrl Pts',(-248.379163098102,0.906885935978272,
135.640212701885));
#137708=CARTESIAN_POINT('Ctrl Pts',(-248.386920138987,1.04127251770969,
135.613074311937));
#137709=CARTESIAN_POINT('Ctrl Pts',(-248.394677179872,1.17439379663845,
135.580340336212));
#137710=CARTESIAN_POINT('Ctrl Pts',(-248.402428371112,1.30741468777542,
135.547631045432));
#137711=CARTESIAN_POINT('Ctrl Pts',(-248.410179562353,1.43917179721702,
135.50933466086));
#137712=CARTESIAN_POINT('Ctrl Pts',(-248.417930753593,1.56916452868885,
135.465573522423));
#137713=CARTESIAN_POINT('Ctrl Pts',(-248.42567865037,1.69910200978197,135.421830983637));
#137714=CARTESIAN_POINT('Ctrl Pts',(-248.433426547147,1.8272762346577,135.37262843507));
#137715=CARTESIAN_POINT('Ctrl Pts',(-248.441174443924,1.95320101916071,
135.318138286132));
#137716=CARTESIAN_POINT('Ctrl Pts',(-248.448920720008,2.07909946291343,
135.26365953536));
#137717=CARTESIAN_POINT('Ctrl Pts',(-248.456666996092,2.20274904362696,
135.203895539383));
#137718=CARTESIAN_POINT('Ctrl Pts',(-248.464413272176,2.32368321827512,
135.139066993274));
#137719=CARTESIAN_POINT('Ctrl Pts',(-248.472159605441,2.44461828563171,
135.074237968616));
#137720=CARTESIAN_POINT('Ctrl Pts',(-248.479905938707,2.56283756234785,
135.004344503942));
#137721=CARTESIAN_POINT('Ctrl Pts',(-248.487652271972,2.67789915045646,
134.929653237791));
#137722=CARTESIAN_POINT('Ctrl Pts',(-248.495400339975,2.79298650580979,
134.85494524505));
#137723=CARTESIAN_POINT('Ctrl Pts',(-248.503148407978,2.90491443755587,
134.775437525664));
#137724=CARTESIAN_POINT('Ctrl Pts',(-248.510896475981,3.01327041236418,
134.691439788932));
#137725=CARTESIAN_POINT('Ctrl Pts',(-248.518652778723,3.12174154919241,
134.607352778406));
#137726=CARTESIAN_POINT('Ctrl Pts',(-248.526409081465,3.22663283604072,
134.518766457776));
#137727=CARTESIAN_POINT('Ctrl Pts',(-248.534165384206,3.32756478677328,
134.426030902438));
#137728=CARTESIAN_POINT('Ctrl Pts',(-248.541925826721,3.42855060792695,
134.333245851342));
#137729=CARTESIAN_POINT('Ctrl Pts',(-248.549686269235,3.52557260576337,
134.236307429017));
#137730=CARTESIAN_POINT('Ctrl Pts',(-248.557446711749,3.61828924229707,
134.135601530736));
#137731=CARTESIAN_POINT('Ctrl Pts',(-248.565219612014,3.71115471580673,
134.034733970407));
#137732=CARTESIAN_POINT('Ctrl Pts',(-248.57299251228,3.79970076425357,133.930087147147));
#137733=CARTESIAN_POINT('Ctrl Pts',(-248.580765412545,3.88362656404538,
133.822079586181));
#137734=CARTESIAN_POINT('Ctrl Pts',(-248.588255748307,3.96450144961888,
133.717998372111));
#137735=CARTESIAN_POINT('Ctrl Pts',(-248.595746084069,4.04108599085593,
133.610796771382));
#137736=CARTESIAN_POINT('Ctrl Pts',(-248.603236419831,4.11315082759725,
133.500871943694));
#137737=CARTESIAN_POINT('Ctrl Pts',(-248.61101075395,4.18794802452673,133.386779282754));
#137738=CARTESIAN_POINT('Ctrl Pts',(-248.618785088069,4.25811295722376,
133.269391404879));
#137739=CARTESIAN_POINT('Ctrl Pts',(-248.626559422189,4.32334140887819,
133.149121186319));
#137740=CARTESIAN_POINT('Ctrl Pts',(-248.634324175136,4.3884894722956,133.028999190055));
#137741=CARTESIAN_POINT('Ctrl Pts',(-248.642088928083,4.44871297496066,
132.906002261354));
#137742=CARTESIAN_POINT('Ctrl Pts',(-248.64985368103,4.50375047814352,132.780572826091));
#137743=CARTESIAN_POINT('Ctrl Pts',(-248.657610721915,4.55873331730233,
132.655267969111));
#137744=CARTESIAN_POINT('Ctrl Pts',(-248.6653677628,4.6085402512409,132.527535769216));
#137745=CARTESIAN_POINT('Ctrl Pts',(-248.673124803685,4.65295553331785,
132.397843553611));
#137746=CARTESIAN_POINT('Ctrl Pts',(-248.680875994925,4.69733732148527,
132.268249139915));
#137747=CARTESIAN_POINT('Ctrl Pts',(-248.688627186165,4.73633542453395,
132.136698020883));
#137748=CARTESIAN_POINT('Ctrl Pts',(-248.696378377405,4.76978218599676,
132.00367749006));
#137749=CARTESIAN_POINT('Ctrl Pts',(-248.704126274182,4.80321473169359,
131.870713496511));
#137750=CARTESIAN_POINT('Ctrl Pts',(-248.711874170959,4.83110053346967,
131.7362817117));
#137751=CARTESIAN_POINT('Ctrl Pts',(-248.719622067737,4.85332184983542,
131.600884367626));
#137752=CARTESIAN_POINT('Ctrl Pts',(-248.727368343821,4.87553851798082,
131.465515345758));
#137753=CARTESIAN_POINT('Ctrl Pts',(-248.735114619905,4.89209299424579,
131.329181551923));
#137754=CARTESIAN_POINT('Ctrl Pts',(-248.742860895989,4.90291877774331,
131.192394793061));
#137755=CARTESIAN_POINT('Ctrl Pts',(-248.750607229255,4.91374464115433,
131.05560702447));
#137756=CARTESIAN_POINT('Ctrl Pts',(-248.75835356252,4.91884169656952,130.918366673925));
#137757=CARTESIAN_POINT('Ctrl Pts',(-248.766099895785,4.91819541789862,
130.781189647345));
#137758=CARTESIAN_POINT('Ctrl Pts',(-248.773847963788,4.9175489944981,130.643981900921));
#137759=CARTESIAN_POINT('Ctrl Pts',(-248.781596031791,4.91115667950407,
130.506837897567));
#137760=CARTESIAN_POINT('Ctrl Pts',(-248.789344099794,4.89905605577746,
130.370272118697));
#137761=CARTESIAN_POINT('Ctrl Pts',(-248.797100402536,4.88694257136397,
130.233561196092));
#137762=CARTESIAN_POINT('Ctrl Pts',(-248.804856705278,4.86910869357656,
130.09743011565));
#137763=CARTESIAN_POINT('Ctrl Pts',(-248.81261300802,4.84564382923425,129.962387374105));
#137764=CARTESIAN_POINT('Ctrl Pts',(-248.820373450534,4.82216644098725,
129.827272556183));
#137765=CARTESIAN_POINT('Ctrl Pts',(-248.828133893048,4.79305216057069,
129.693247616478));
#137766=CARTESIAN_POINT('Ctrl Pts',(-248.835894335562,4.75844104298344,
129.560808486391));
#137767=CARTESIAN_POINT('Ctrl Pts',(-248.843667235828,4.7237743645577,129.428156753255));
#137768=CARTESIAN_POINT('Ctrl Pts',(-248.851440136093,4.68359333044033,
129.29709629083));
#137769=CARTESIAN_POINT('Ctrl Pts',(-248.859213036359,4.63808745525572,
129.16810641363));
#137770=CARTESIAN_POINT('Ctrl Pts',(-248.866703372121,4.59423583325682,
129.043805643373));
#137771=CARTESIAN_POINT('Ctrl Pts',(-248.874193707883,4.54543990567714,
128.921427816106));
#137772=CARTESIAN_POINT('Ctrl Pts',(-248.881684043645,4.49190983945131,
128.801380573546));
#137773=CARTESIAN_POINT('Ctrl Pts',(-248.889458377764,4.43635016449402,
128.676781703297));
#137774=CARTESIAN_POINT('Ctrl Pts',(-248.897232711883,4.37551427823678,
128.554298942895));
#137775=CARTESIAN_POINT('Ctrl Pts',(-248.905007046002,4.30958510854546,
128.434411408257));
#137776=CARTESIAN_POINT('Ctrl Pts',(-248.912771798949,4.24373719066353,
128.314671624291));
#137777=CARTESIAN_POINT('Ctrl Pts',(-248.920536551896,4.17280866532491,
128.197521041551));
#137778=CARTESIAN_POINT('Ctrl Pts',(-248.928301304843,4.09703044392781,
128.083418757836));
#137779=CARTESIAN_POINT('Ctrl Pts',(-248.936058345728,4.0213274865287,127.969429802119));
#137780=CARTESIAN_POINT('Ctrl Pts',(-248.943815386613,3.94078463358913,
127.858483443915));
#137781=CARTESIAN_POINT('Ctrl Pts',(-248.951572427498,3.85567844439299,
127.751013798755));
#137782=CARTESIAN_POINT('Ctrl Pts',(-248.959323618738,3.77063643443604,
127.64362519729));
#137783=CARTESIAN_POINT('Ctrl Pts',(-248.967074809978,3.68103817955354,
127.539708395561));
#137784=CARTESIAN_POINT('Ctrl Pts',(-248.974826001218,3.5872030311884,127.439667841764));
#137785=CARTESIAN_POINT('Ctrl Pts',(-248.982573897995,3.49340776526433,
127.339669807871));
#137786=CARTESIAN_POINT('Ctrl Pts',(-248.990321794772,3.39537945440582,
127.243545029701));
#137787=CARTESIAN_POINT('Ctrl Pts',(-248.99806969155,3.29347699846595,127.151664035166));
#137788=CARTESIAN_POINT('Ctrl Pts',(-249.005815967634,3.1915958583231,127.059802260155));
#137789=CARTESIAN_POINT('Ctrl Pts',(-249.013562243718,3.08584247518324,
126.97218276472));
#137790=CARTESIAN_POINT('Ctrl Pts',(-249.021308519802,2.97661150136495,
126.889138142094));
#137791=CARTESIAN_POINT('Ctrl Pts',(-249.029054853067,2.86737972122827,
126.806092906451));
#137792=CARTESIAN_POINT('Ctrl Pts',(-249.036801186332,2.75467061042075,
126.727622847623));
#137793=CARTESIAN_POINT('Ctrl Pts',(-249.044547519598,2.63891036349626,
126.654019046571));
#137794=CARTESIAN_POINT('Ctrl Pts',(-249.052295587601,2.52312419286693,
126.580398762458));
#137795=CARTESIAN_POINT('Ctrl Pts',(-249.060043655604,2.40428585632989,
126.51164711436));
#137796=CARTESIAN_POINT('Ctrl Pts',(-249.067791723607,2.28284851612436,
126.448010572525));
#137797=CARTESIAN_POINT('Ctrl Pts',(-249.075548026349,2.16128211086871,
126.384306397016));
#137798=CARTESIAN_POINT('Ctrl Pts',(-249.083304329091,2.03711153089903,
126.325728369314));
#137799=CARTESIAN_POINT('Ctrl Pts',(-249.091060631832,1.91081291549025,
126.272476123838));
#137800=CARTESIAN_POINT('Ctrl Pts',(-249.098821074346,1.78444689070799,
126.219195456034));
#137801=CARTESIAN_POINT('Ctrl Pts',(-249.106581516861,1.65595093343024,
126.171246371056));
#137802=CARTESIAN_POINT('Ctrl Pts',(-249.114341959375,1.52581798793829,
126.128779099703));
#137803=CARTESIAN_POINT('Ctrl Pts',(-249.12211485964,1.39547614148924,126.086243656115));
#137804=CARTESIAN_POINT('Ctrl Pts',(-249.129887759906,1.2634924322091,126.049207716833));
#137805=CARTESIAN_POINT('Ctrl Pts',(-249.137660660171,1.13037255825735,
126.01777091904));
#137806=CARTESIAN_POINT('Ctrl Pts',(-249.145150995933,1.00209192703174,
125.98747692803));
#137807=CARTESIAN_POINT('Ctrl Pts',(-249.152641331695,0.87275660426685,
125.962382118993));
#137808=CARTESIAN_POINT('Ctrl Pts',(-249.160131667457,0.74282315084553,
125.942530012838));
#137809=CARTESIAN_POINT('Ctrl Pts',(-249.167906001576,0.607963231046265,
125.921925208045));
#137810=CARTESIAN_POINT('Ctrl Pts',(-249.175680335695,0.472031733306959,
125.90690323831));
#137811=CARTESIAN_POINT('Ctrl Pts',(-249.183454669814,0.335530628397265,
125.897569175095));
#137812=CARTESIAN_POINT('Ctrl Pts',(-249.191219422762,0.199197748899919,
125.888246615279));
#137813=CARTESIAN_POINT('Ctrl Pts',(-249.198984175709,0.0622970452927646,
125.884598040913));
#137814=CARTESIAN_POINT('Ctrl Pts',(-249.206748928656,-0.074660417192231,
125.886677333274));
#137815=CARTESIAN_POINT('Ctrl Pts',(-249.214505969541,-0.211481851594725,
125.888754560453));
#137816=CARTESIAN_POINT('Ctrl Pts',(-249.222263010426,-0.348359544298285,
125.896548327098));
#137817=CARTESIAN_POINT('Ctrl Pts',(-249.230020051311,-0.484778774564979,
125.910060606101));
#137818=CARTESIAN_POINT('Ctrl Pts',(-249.237771242551,-0.621095130028756,
125.923562695388));
#137819=CARTESIAN_POINT('Ctrl Pts',(-249.245522433791,-0.756953323723316,
125.942774675131));
#137820=CARTESIAN_POINT('Ctrl Pts',(-249.253273625031,-0.891840464670545,
125.967646480047));
#137821=CARTESIAN_POINT('Ctrl Pts',(-249.261021521808,-1.02667027498482,
125.992507713782));
#137822=CARTESIAN_POINT('Ctrl Pts',(-249.268769418585,-1.16052946974826,
126.023023917434));
#137823=CARTESIAN_POINT('Ctrl Pts',(-249.276517315362,-1.29291231919679,
126.05909341778));
#137824=CARTESIAN_POINT('Ctrl Pts',(-249.284263591447,-1.42526747700707,
126.095155373163));
#137825=CARTESIAN_POINT('Ctrl Pts',(-249.292009867531,-1.55614652678626,
126.136768211983));
#137826=CARTESIAN_POINT('Ctrl Pts',(-249.299756143615,-1.68505632921115,
126.183779676831));
#137827=CARTESIAN_POINT('Ctrl Pts',(-249.30750247688,-1.81396708321909,
126.230791488707));
#137828=CARTESIAN_POINT('Ctrl Pts',(-249.315248810145,-1.94090819356345,
126.283201872183));
#137829=CARTESIAN_POINT('Ctrl Pts',(-249.322995143411,-2.06540439702046,
126.340809594079));
#137830=CARTESIAN_POINT('Ctrl Pts',(-249.330743211414,-2.18992848053819,
126.398430216826));
#137831=CARTESIAN_POINT('Ctrl Pts',(-249.338491279417,-2.3120062129153,
126.461250329881));
#137832=CARTESIAN_POINT('Ctrl Pts',(-249.34623934742,-2.4311852864939,126.529021898209));
#137833=CARTESIAN_POINT('Ctrl Pts',(-249.353995650161,-2.55049102501095,
126.596865494966));
#137834=CARTESIAN_POINT('Ctrl Pts',(-249.361751952903,-2.66689161024097,
126.669670865767));
#137835=CARTESIAN_POINT('Ctrl Pts',(-249.369508255645,-2.77996171918606,
126.747145328435));
#137836=CARTESIAN_POINT('Ctrl Pts',(-249.377268698159,-2.89309217705247,
126.824661141555));
#137837=CARTESIAN_POINT('Ctrl Pts',(-249.385029140673,-3.00288830383,126.906850777956));
#137838=CARTESIAN_POINT('Ctrl Pts',(-249.392789583188,-3.10895725766776,
126.993380713067));
#137839=CARTESIAN_POINT('Ctrl Pts',(-249.400562483453,-3.21519648280686,
127.080049553712));
#137840=CARTESIAN_POINT('Ctrl Pts',(-249.408335383719,-3.3176962861842,
127.171072356468));
#137841=CARTESIAN_POINT('Ctrl Pts',(-249.416108283984,-3.41609949800904,
127.26607751948));
#137842=CARTESIAN_POINT('Ctrl Pts',(-249.423598619746,-3.51092550522239,
127.357629005514));
#137843=CARTESIAN_POINT('Ctrl Pts',(-249.431088955508,-3.6019473799333,
127.452878118264));
#137844=CARTESIAN_POINT('Ctrl Pts',(-249.43857929127,-3.68888172445778,
127.551464264243));
#137845=CARTESIAN_POINT('Ctrl Pts',(-249.446285008328,-3.77831582765243,
127.652885211296));
#137846=CARTESIAN_POINT('Ctrl Pts',(-249.453990725386,-3.86371940592775,
127.758173481036));
#137847=CARTESIAN_POINT('Ctrl Pts',(-249.461696442444,-3.9447347773999,
127.866972219946));
#137848=CARTESIAN_POINT('Ctrl Pts',(-249.469392876313,-4.02565254848667,
127.975639887448));
#137849=CARTESIAN_POINT('Ctrl Pts',(-249.477089310182,-4.1021923901458,
128.087809297744));
#137850=CARTESIAN_POINT('Ctrl Pts',(-249.484785744052,-4.17403438468894,
128.203087848721));
#137851=CARTESIAN_POINT('Ctrl Pts',(-249.492473286064,-4.24579337861153,
128.318233215878));
#137852=CARTESIAN_POINT('Ctrl Pts',(-249.500160828075,-4.31286512077841,
128.436480237057));
#137853=CARTESIAN_POINT('Ctrl Pts',(-249.507848370087,-4.37497128105645,
128.557405043365));
#137854=CARTESIAN_POINT('Ctrl Pts',(-249.515530741533,-4.43703566933476,
128.678248516824));
#137855=CARTESIAN_POINT('Ctrl Pts',(-249.523213112979,-4.49414093610544,
128.801765840908));
#137856=CARTESIAN_POINT('Ctrl Pts',(-249.530895484424,-4.54605329422833,
128.927506198988));
#137857=CARTESIAN_POINT('Ctrl Pts',(-249.538574635081,-4.59794388839659,
129.053193841153));
#137858=CARTESIAN_POINT('Ctrl Pts',(-249.546253785737,-4.64464575123465,
129.181102296535));
#137859=CARTESIAN_POINT('Ctrl Pts',(-249.553932936393,-4.68597230028519,
129.310758708268));
#137860=CARTESIAN_POINT('Ctrl Pts',(-249.559251115184,-4.71459291036385,
129.40055196925));
#137861=CARTESIAN_POINT('Ctrl Pts',(-249.564569293975,-4.74063637976063,
129.49118311383));
#137862=CARTESIAN_POINT('Ctrl Pts',(-249.569887472766,-4.76405452823394,
129.582490119308));
#137863=CARTESIAN_POINT('Origin',(213.235140564004,0.,130.804360617566));
#137864=CARTESIAN_POINT('',(-251.665320902482,-4.76405452823412,129.582490119309));
#137865=CARTESIAN_POINT('',(-251.319768125496,-4.76405452823393,129.582490119308));
#137866=CARTESIAN_POINT('',(213.235140564004,-4.76405452823405,129.582490119308));
#137867=CARTESIAN_POINT('',(-249.985140564054,-4.91824989614162,130.803349873801));
#137868=CARTESIAN_POINT('Ctrl Pts',(-249.985140564054,-4.91824989614162,
130.803349873801));
#137869=CARTESIAN_POINT('Ctrl Pts',(-249.992872285789,-4.91827778423735,
130.939052540223));
#137870=CARTESIAN_POINT('Ctrl Pts',(-250.000604007523,-4.91268502623554,
131.074980544808));
#137871=CARTESIAN_POINT('Ctrl Pts',(-250.008335729258,-4.90144173251262,
131.210626546834));
#137872=CARTESIAN_POINT('Ctrl Pts',(-250.016058012704,-4.8902121637339,
131.346106962701));
#137873=CARTESIAN_POINT('Ctrl Pts',(-250.02378029615,-4.87334581320459,
131.481305670362));
#137874=CARTESIAN_POINT('Ctrl Pts',(-250.031502579596,-4.85086476716184,
131.615713853344));
#137875=CARTESIAN_POINT('Ctrl Pts',(-250.039217335718,-4.82840563460076,
131.74999102146));
#137876=CARTESIAN_POINT('Ctrl Pts',(-250.04693209184,-4.80034276065878,
131.883478810325));
#137877=CARTESIAN_POINT('Ctrl Pts',(-250.054646847962,-4.76675011339768,
132.015672476223));
#137878=CARTESIAN_POINT('Ctrl Pts',(-250.062355980694,-4.7331819522699,
132.147769784376));
#137879=CARTESIAN_POINT('Ctrl Pts',(-250.070065113426,-4.69409213639154,
132.278574464824));
#137880=CARTESIAN_POINT('Ctrl Pts',(-250.077774246158,-4.64960581892818,
132.407591353015));
#137881=CARTESIAN_POINT('Ctrl Pts',(-250.085480417393,-4.60513659108468,
132.536558678786));
#137882=CARTESIAN_POINT('Ctrl Pts',(-250.093186588627,-4.55527511194571,
132.66373920435));
#137883=CARTESIAN_POINT('Ctrl Pts',(-250.100892759861,-4.50019648316473,
132.788652600973));
#137884=CARTESIAN_POINT('Ctrl Pts',(-250.108597591538,-4.44512742865141,
132.913544284013));
#137885=CARTESIAN_POINT('Ctrl Pts',(-250.116302423215,-4.384843187584,133.036169259948));
#137886=CARTESIAN_POINT('Ctrl Pts',(-250.124007254893,-4.31956694865875,
133.156067325163));
#137887=CARTESIAN_POINT('Ctrl Pts',(-250.131712462316,-4.25428752637525,
133.275971237505));
#137888=CARTESIAN_POINT('Ctrl Pts',(-250.139417669738,-4.18401581114635,
133.393147627045));
#137889=CARTESIAN_POINT('Ctrl Pts',(-250.147122877161,-4.10902065205373,
133.507161450683));
#137890=CARTESIAN_POINT('Ctrl Pts',(-250.154830175567,-4.03400514132315,
133.621206214559));
#137891=CARTESIAN_POINT('Ctrl Pts',(-250.162537473972,-3.95426385422254,
133.732086374822));
#137892=CARTESIAN_POINT('Ctrl Pts',(-250.170244772378,-3.87010833396887,
133.839396786353));
#137893=CARTESIAN_POINT('Ctrl Pts',(-250.177960359683,-3.78586230772042,
133.946822606065));
#137894=CARTESIAN_POINT('Ctrl Pts',(-250.185675946989,-3.69719281317067,
134.050670699348));
#137895=CARTESIAN_POINT('Ctrl Pts',(-250.193391534295,-3.60445124110995,
134.150569563965));
#137896=CARTESIAN_POINT('Ctrl Pts',(-250.201111652863,-3.51165520314561,
134.250527097869));
#137897=CARTESIAN_POINT('Ctrl Pts',(-250.208831771432,-3.41478260520544,
134.346530505772));
#137898=CARTESIAN_POINT('Ctrl Pts',(-250.21655189,-3.31422006150349,134.438246753155));
#137899=CARTESIAN_POINT('Ctrl Pts',(-250.224283636345,-3.21350605397486,
134.530101140379));
#137900=CARTESIAN_POINT('Ctrl Pts',(-250.232015382689,-3.10909130424726,
134.617655217992));
#137901=CARTESIAN_POINT('Ctrl Pts',(-250.239747129033,-3.00139415167609,
134.700617309416));
#137902=CARTESIAN_POINT('Ctrl Pts',(-250.244609141538,-2.93367013703912,
134.752786988555));
#137903=CARTESIAN_POINT('Ctrl Pts',(-250.249471154044,-2.86464872179104,
134.803141697023));
#137904=CARTESIAN_POINT('Ctrl Pts',(-250.254333166549,-2.79443907615148,
134.851618122615));
#137905=CARTESIAN_POINT('Ctrl Pts',(-250.262107500668,-2.6821741975678,
134.929131689074));
#137906=CARTESIAN_POINT('Ctrl Pts',(-250.269881834787,-2.566503889421,135.002093401399));
#137907=CARTESIAN_POINT('Ctrl Pts',(-250.277656168906,-2.44783360869859,
135.070189222494));
#137908=CARTESIAN_POINT('Ctrl Pts',(-250.285420921853,-2.3293095784913,
135.138201121577));
#137909=CARTESIAN_POINT('Ctrl Pts',(-250.2931856748,-2.20779326787769,135.20135886851));
#137910=CARTESIAN_POINT('Ctrl Pts',(-250.300950427747,-2.08372070151509,
135.259390482851));
#137911=CARTESIAN_POINT('Ctrl Pts',(-250.308707468632,-1.95977136577452,
135.317364459374));
#137912=CARTESIAN_POINT('Ctrl Pts',(-250.316464509517,-1.83327117867985,
135.370222270747));
#137913=CARTESIAN_POINT('Ctrl Pts',(-250.324221550402,-1.70468215553347,
135.417737017894));
#137914=CARTESIAN_POINT('Ctrl Pts',(-250.331972741642,-1.57619010237024,
135.465215933801));
#137915=CARTESIAN_POINT('Ctrl Pts',(-250.339723932882,-1.44561271375644,
135.507359670489));
#137916=CARTESIAN_POINT('Ctrl Pts',(-250.347475124122,-1.31343311961368,
135.543988926073));
#137917=CARTESIAN_POINT('Ctrl Pts',(-250.355223020899,-1.18130970532426,
135.580602613246));
#137918=CARTESIAN_POINT('Ctrl Pts',(-250.362970917676,-1.04758581590064,
135.611706376767));
#137919=CARTESIAN_POINT('Ctrl Pts',(-250.370718814453,-0.912760713239713,
135.637170456869));
#137920=CARTESIAN_POINT('Ctrl Pts',(-250.378465090537,-0.777963813083406,
135.662629210435));
#137921=CARTESIAN_POINT('Ctrl Pts',(-250.386211366621,-0.642066541798643,
135.682450554559));
#137922=CARTESIAN_POINT('Ctrl Pts',(-250.393957642705,-0.505578963098105,
135.696555725549));
#137923=CARTESIAN_POINT('Ctrl Pts',(-250.401703975971,-0.369090376877453,
135.71066100066));
#137924=CARTESIAN_POINT('Ctrl Pts',(-250.409450309236,-0.23201186343995,
135.71904997825));
#137925=CARTESIAN_POINT('Ctrl Pts',(-250.417196642501,-0.0948588315498516,
135.721695756091));
#137926=CARTESIAN_POINT('Ctrl Pts',(-250.424944710504,0.0423249148105995,
135.724342126437));
#137927=CARTESIAN_POINT('Ctrl Pts',(-250.432692778507,0.179582822012945,
135.721242730205));
#137928=CARTESIAN_POINT('Ctrl Pts',(-250.44044084651,0.316399654915623,
135.7124227933));
#137929=CARTESIAN_POINT('Ctrl Pts',(-250.448197149252,0.453361898376639,
135.703593482461));
#137930=CARTESIAN_POINT('Ctrl Pts',(-250.455953451994,0.589881740323937,
135.689031510967));
#137931=CARTESIAN_POINT('Ctrl Pts',(-250.463709754735,0.725448684938885,
135.66881405737));
#137932=CARTESIAN_POINT('Ctrl Pts',(-250.47147019725,0.861087985714016,
135.64858581311));
#137933=CARTESIAN_POINT('Ctrl Pts',(-250.479230639764,0.995772991999703,
135.622696145893));
#137934=CARTESIAN_POINT('Ctrl Pts',(-250.486991082278,1.12900455427687,
135.591273169402));
#137935=CARTESIAN_POINT('Ctrl Pts',(-250.494763982543,1.26244999168555,
135.559799749958));
#137936=CARTESIAN_POINT('Ctrl Pts',(-250.502536882808,1.39443694596228,
135.522775376713));
#137937=CARTESIAN_POINT('Ctrl Pts',(-250.510309783074,1.524481692795,135.480378007486));
#137938=CARTESIAN_POINT('Ctrl Pts',(-250.517800118837,1.64979898552902,
135.439521889419));
#137939=CARTESIAN_POINT('Ctrl Pts',(-250.525290454599,1.77331253873323,
135.393676744279));
#137940=CARTESIAN_POINT('Ctrl Pts',(-250.532780790362,1.89460978465488,
135.3430428962));
#137941=CARTESIAN_POINT('Ctrl Pts',(-250.540555124481,2.02050605251541,
135.290489250385));
#137942=CARTESIAN_POINT('Ctrl Pts',(-250.5483294586,2.14441343443857,135.232610131886));
#137943=CARTESIAN_POINT('Ctrl Pts',(-250.55610379272,2.2658485627169,135.169576918431));
#137944=CARTESIAN_POINT('Ctrl Pts',(-250.563868545667,2.38713403305226,
135.106621387777));
#137945=CARTESIAN_POINT('Ctrl Pts',(-250.571633298614,2.50595296835785,
135.038524579066));
#137946=CARTESIAN_POINT('Ctrl Pts',(-250.579398051561,2.62184086180627,
134.965506320118));
#137947=CARTESIAN_POINT('Ctrl Pts',(-250.587155092447,2.73761365376549,
134.892560583933));
#137948=CARTESIAN_POINT('Ctrl Pts',(-250.594912133332,2.85046086855112,
134.814703332027));
#137949=CARTESIAN_POINT('Ctrl Pts',(-250.602669174217,2.95994187898805,
134.732200626466));
#137950=CARTESIAN_POINT('Ctrl Pts',(-250.610420365457,3.06934032894264,
134.649760136837));
#137951=CARTESIAN_POINT('Ctrl Pts',(-250.618171556697,3.17537731626941,
134.562681400748));
#137952=CARTESIAN_POINT('Ctrl Pts',(-250.625922747938,3.27764084568845,
134.471273972034));
#137953=CARTESIAN_POINT('Ctrl Pts',(-250.633670644715,3.37986091037994,
134.379905393915));
#137954=CARTESIAN_POINT('Ctrl Pts',(-250.641418541492,3.47831041615716,
134.284212042417));
#137955=CARTESIAN_POINT('Ctrl Pts',(-250.649166438269,3.57261032920346,
134.184543822389));
#137956=CARTESIAN_POINT('Ctrl Pts',(-250.656912714353,3.66689051674082,
134.084896450805));
#137957=CARTESIAN_POINT('Ctrl Pts',(-250.664658990438,3.75702256952765,
133.98127614832));
#137958=CARTESIAN_POINT('Ctrl Pts',(-250.672405266522,3.84266451954371,
133.874069472285));
#137959=CARTESIAN_POINT('Ctrl Pts',(-250.680151599788,3.92830710174906,
133.766862004874));
#137960=CARTESIAN_POINT('Ctrl Pts',(-250.687897933053,4.00945927102577,
133.65606841655));
#137961=CARTESIAN_POINT('Ctrl Pts',(-250.695644266319,4.085819802742,133.542107793991));
#137962=CARTESIAN_POINT('Ctrl Pts',(-250.703392334322,4.16219743486997,
133.42812165074));
#137963=CARTESIAN_POINT('Ctrl Pts',(-250.711140402325,4.2337810765948,133.310967386691));
#137964=CARTESIAN_POINT('Ctrl Pts',(-250.718888470328,4.30031345400347,
133.191092118975));
#137965=CARTESIAN_POINT('Ctrl Pts',(-250.72664477307,4.3669165428145,133.071089446398));
#137966=CARTESIAN_POINT('Ctrl Pts',(-250.734401075812,4.42845745303442,
132.948360335632));
#137967=CARTESIAN_POINT('Ctrl Pts',(-250.742157378554,4.4847251817057,132.82337599816));
#137968=CARTESIAN_POINT('Ctrl Pts',(-250.749917821068,4.54102294215796,
132.698324952784));
#137969=CARTESIAN_POINT('Ctrl Pts',(-250.757678263583,4.59204176765584,
132.571016644993));
#137970=CARTESIAN_POINT('Ctrl Pts',(-250.765438706097,4.63761964135948,
132.441940271988));
#137971=CARTESIAN_POINT('Ctrl Pts',(-250.773211606363,4.68327068071221,
132.31265669413));
#137972=CARTESIAN_POINT('Ctrl Pts',(-250.780984506628,4.72346319966091,
132.181599753318));
#137973=CARTESIAN_POINT('Ctrl Pts',(-250.788757406894,4.75808545435506,
132.049272611064));
#137974=CARTESIAN_POINT('Ctrl Pts',(-250.796247742654,4.79144910287435,
131.921755893775));
#137975=CARTESIAN_POINT('Ctrl Pts',(-250.803738078414,4.81964037634877,
131.793060022642));
#137976=CARTESIAN_POINT('Ctrl Pts',(-250.811228414174,4.84260481019838,
131.663640382685));
#137977=CARTESIAN_POINT('Ctrl Pts',(-250.819002748293,4.86643994754257,
131.529313757714));
#137978=CARTESIAN_POINT('Ctrl Pts',(-250.826777082412,4.88471957246311,
131.393781890743));
#137979=CARTESIAN_POINT('Ctrl Pts',(-250.834551416531,4.89732659784195,
131.25754408656));
#137980=CARTESIAN_POINT('Ctrl Pts',(-250.842316169478,4.90991808618873,
131.121474183296));
#137981=CARTESIAN_POINT('Ctrl Pts',(-250.850080922425,4.91685084926534,
130.984700459435));
#137982=CARTESIAN_POINT('Ctrl Pts',(-250.857845675372,4.91805875715627,
130.847732540034));
#137983=CARTESIAN_POINT('Ctrl Pts',(-250.865602716257,4.91926546533605,
130.710900659101));
#137984=CARTESIAN_POINT('Ctrl Pts',(-250.873359757142,4.91475863031501,
130.573875354883));
#137985=CARTESIAN_POINT('Ctrl Pts',(-250.881116798027,4.90452392789344,
130.437171152547));
#137986=CARTESIAN_POINT('Ctrl Pts',(-250.888867989267,4.8942969435406,130.300570039914));
#137987=CARTESIAN_POINT('Ctrl Pts',(-250.896619180507,4.87835071842023,
130.164289935484));
#137988=CARTESIAN_POINT('Ctrl Pts',(-250.904370371747,4.85672299542931,
130.028844783964));
#137989=CARTESIAN_POINT('Ctrl Pts',(-250.912118268524,4.83510446479751,
129.893457200245));
#137990=CARTESIAN_POINT('Ctrl Pts',(-250.919866165301,4.80780930064345,
129.758904248879));
#137991=CARTESIAN_POINT('Ctrl Pts',(-250.927614062078,4.77492701079141,
129.625693953867));
#137992=CARTESIAN_POINT('Ctrl Pts',(-250.935360338162,4.74205159920555,
129.492511523578));
#137993=CARTESIAN_POINT('Ctrl Pts',(-250.943106614246,4.70359148017861,
129.36067157034));
#137994=CARTESIAN_POINT('Ctrl Pts',(-250.95085289033,4.6596870332873,129.230670745223));
#137995=CARTESIAN_POINT('Ctrl Pts',(-250.958599223595,4.61578226230341,
129.10066896047));
#137996=CARTESIAN_POINT('Ctrl Pts',(-250.96634555686,4.56643320835827,128.972506701338));
#137997=CARTESIAN_POINT('Ctrl Pts',(-250.974091890126,4.51182964167352,
128.846663923229));
#137998=CARTESIAN_POINT('Ctrl Pts',(-250.981839958129,4.45721384689853,
128.720792963503));
#137999=CARTESIAN_POINT('Ctrl Pts',(-250.989588026131,4.39734135345676,
128.597242876998));
#138000=CARTESIAN_POINT('Ctrl Pts',(-250.997336094134,4.3324492708213,128.476471793275));
#138001=CARTESIAN_POINT('Ctrl Pts',(-251.005092396876,4.26748822010809,
128.355572352607));
#138002=CARTESIAN_POINT('Ctrl Pts',(-251.012848699618,4.19749710855081,
128.237458159717));
#138003=CARTESIAN_POINT('Ctrl Pts',(-251.02060500236,4.12275832746292,128.122561438687));
#138004=CARTESIAN_POINT('Ctrl Pts',(-251.028365444874,4.04797965603722,
128.007603393818));
#138005=CARTESIAN_POINT('Ctrl Pts',(-251.036125887388,3.96844849252535,
127.89586656096));
#138006=CARTESIAN_POINT('Ctrl Pts',(-251.043886329902,3.88448883832754,
127.787751672507));
#138007=CARTESIAN_POINT('Ctrl Pts',(-251.051659230167,3.80039440463922,
127.679463228437));
#138008=CARTESIAN_POINT('Ctrl Pts',(-251.059432130433,3.71185752686294,
127.574808646183));
#138009=CARTESIAN_POINT('Ctrl Pts',(-251.067205030698,3.61924112874938,
127.474153910097));
#138010=CARTESIAN_POINT('Ctrl Pts',(-251.074695366461,3.52999156997782,
127.377158227185));
#138011=CARTESIAN_POINT('Ctrl Pts',(-251.082185702224,3.43695416062381,
127.283876848435));
#138012=CARTESIAN_POINT('Ctrl Pts',(-251.089676037988,3.34048258956851,
127.194601743169));
#138013=CARTESIAN_POINT('Ctrl Pts',(-251.097450372106,3.24035326959588,
127.101941745171));
#138014=CARTESIAN_POINT('Ctrl Pts',(-251.105224706225,3.13620705522876,
127.013304294375));
#138015=CARTESIAN_POINT('Ctrl Pts',(-251.112999040344,3.0284007372799,126.929057785923));
#138016=CARTESIAN_POINT('Ctrl Pts',(-251.120763793291,2.92072728098357,
126.844915103764));
#138017=CARTESIAN_POINT('Ctrl Pts',(-251.128528546237,2.80940300125583,
126.765152835213));
#138018=CARTESIAN_POINT('Ctrl Pts',(-251.136293299184,2.69482091525471,
126.690102082033));
#138019=CARTESIAN_POINT('Ctrl Pts',(-251.144050340069,2.58035263379673,
126.615125870319));
#138020=CARTESIAN_POINT('Ctrl Pts',(-251.151807380953,2.46263331018998,
126.544852074305));
#138021=CARTESIAN_POINT('Ctrl Pts',(-251.159564421838,2.34208808644987,
126.479570858767));
#138022=CARTESIAN_POINT('Ctrl Pts',(-251.167315613078,2.22163376680053,
126.414338872302));
#138023=CARTESIAN_POINT('Ctrl Pts',(-251.175066804317,2.09835813110865,
126.354092157846));
#138024=CARTESIAN_POINT('Ctrl Pts',(-251.182817995557,1.97271397656958,
126.299076760899));
#138025=CARTESIAN_POINT('Ctrl Pts',(-251.190565892334,1.84712322414803,
126.244084746963));
#138026=CARTESIAN_POINT('Ctrl Pts',(-251.19831378911,1.71916631248399,126.194319784753));
#138027=CARTESIAN_POINT('Ctrl Pts',(-251.206061685887,1.58931903772481,
126.149981168184));
#138028=CARTESIAN_POINT('Ctrl Pts',(-251.213807961971,1.45949892421632,
126.105651826298));
#138029=CARTESIAN_POINT('Ctrl Pts',(-251.221554238055,1.32778960388612,
126.066746698588));
#138030=CARTESIAN_POINT('Ctrl Pts',(-251.229300514138,1.1946848019348,126.033416131772));
#138031=CARTESIAN_POINT('Ctrl Pts',(-251.237046847403,1.06157901743389,
126.000085318918));
#138032=CARTESIAN_POINT('Ctrl Pts',(-251.244793180668,0.927078110012168,
125.972329244041));
#138033=CARTESIAN_POINT('Ctrl Pts',(-251.252539513933,0.791688455181783,
125.950247675696));
#138034=CARTESIAN_POINT('Ctrl Pts',(-251.260287581936,0.656268480777476,
125.928161162337));
#138035=CARTESIAN_POINT('Ctrl Pts',(-251.268035649938,0.519959748713128,
125.91175174711));
#138036=CARTESIAN_POINT('Ctrl Pts',(-251.275783717941,0.383275859825544,
125.901067573318));
#138037=CARTESIAN_POINT('Ctrl Pts',(-251.283540020682,0.246446701673726,
125.890372044259));
#138038=CARTESIAN_POINT('Ctrl Pts',(-251.291296323424,0.109241980607997,
125.885413942304));
#138039=CARTESIAN_POINT('Ctrl Pts',(-251.299052626165,-0.0278220216086831,
125.886189311317));
#138040=CARTESIAN_POINT('Ctrl Pts',(-251.306813068679,-0.164959179010641,
125.886965094168));
#138041=CARTESIAN_POINT('Ctrl Pts',(-251.314573511193,-0.301955077575977,
125.893480426983));
#138042=CARTESIAN_POINT('Ctrl Pts',(-251.322333953706,-0.438297439122899,
125.905679323855));
#138043=CARTESIAN_POINT('Ctrl Pts',(-251.330106853972,-0.574858669532121,
125.917897803479));
#138044=CARTESIAN_POINT('Ctrl Pts',(-251.337879754237,-0.710763878622392,
125.935818028203));
#138045=CARTESIAN_POINT('Ctrl Pts',(-251.345652654502,-0.845508984238931,
125.959332483481));
#138046=CARTESIAN_POINT('Ctrl Pts',(-251.353142990268,-0.975355765941941,
125.981992129095));
#138047=CARTESIAN_POINT('Ctrl Pts',(-251.360633326034,-1.10412502412161,
126.009846272811));
#138048=CARTESIAN_POINT('Ctrl Pts',(-251.3681236618,-1.23137993923824,126.042755162707));
#138049=CARTESIAN_POINT('Ctrl Pts',(-251.37589799592,-1.36345976308712,
126.076911803153));
#138050=CARTESIAN_POINT('Ctrl Pts',(-251.383672330041,-1.49432653358835,
126.116622255637));
#138051=CARTESIAN_POINT('Ctrl Pts',(-251.391446664161,-1.62347745532496,
126.161785468519));
#138052=CARTESIAN_POINT('Ctrl Pts',(-251.399211417109,-1.75246921009344,
126.206893021777));
#138053=CARTESIAN_POINT('Ctrl Pts',(-251.406976170058,-1.879748958073,126.257439836739));
#138054=CARTESIAN_POINT('Ctrl Pts',(-251.414740923006,-2.00482569860016,
126.31327422553));
#138055=CARTESIAN_POINT('Ctrl Pts',(-251.422497963892,-2.12977821114571,
126.369053158819));
#138056=CARTESIAN_POINT('Ctrl Pts',(-251.430255004778,-2.2525317158745,
126.430109056492));
#138057=CARTESIAN_POINT('Ctrl Pts',(-251.438012045665,-2.37261228929872,
126.496241075681));
#138058=CARTESIAN_POINT('Ctrl Pts',(-251.445763236906,-2.49260230902894,
126.5623232242));
#138059=CARTESIAN_POINT('Ctrl Pts',(-251.453514428148,-2.60992306846137,
126.633473687105));
#138060=CARTESIAN_POINT('Ctrl Pts',(-251.461265619389,-2.72412281460433,
126.709444506893));
#138061=CARTESIAN_POINT('Ctrl Pts',(-251.469013516167,-2.83827402280803,
126.785383037055));
#138062=CARTESIAN_POINT('Ctrl Pts',(-251.476761412945,-2.94930653122269,
126.866137633138));
#138063=CARTESIAN_POINT('Ctrl Pts',(-251.484509309724,-3.05679548879321,
126.951415717597));
#138064=CARTESIAN_POINT('Ctrl Pts',(-251.492255585809,-3.16426196199071,
127.03667596372));
#138065=CARTESIAN_POINT('Ctrl Pts',(-251.500001861894,-3.26818605261292,
127.126457573303));
#138066=CARTESIAN_POINT('Ctrl Pts',(-251.50774813798,-3.3681743991748,127.220426427428));
#138067=CARTESIAN_POINT('Ctrl Pts',(-251.515494471246,-3.46816348382808,
127.314395975209));
#138068=CARTESIAN_POINT('Ctrl Pts',(-251.523240804513,-3.56421648155155,
127.412552561464));
#138069=CARTESIAN_POINT('Ctrl Pts',(-251.530987137779,-3.65597574590025,
127.514524085474));
#138070=CARTESIAN_POINT('Ctrl Pts',(-251.538735205783,-3.74775555909936,
127.616518445299));
#138071=CARTESIAN_POINT('Ctrl Pts',(-251.546483273788,-3.83523946407887,
127.722329152326));
#138072=CARTESIAN_POINT('Ctrl Pts',(-251.554231341792,-3.91810934271634,
127.831550122257));
#138073=CARTESIAN_POINT('Ctrl Pts',(-251.561987644535,-4.00106729644708,
127.940887173535));
#138074=CARTESIAN_POINT('Ctrl Pts',(-251.569743947278,-4.07940119118924,
128.053641416024));
#138075=CARTESIAN_POINT('Ctrl Pts',(-251.577500250021,-4.15283529244867,
128.169376348867));
#138076=CARTESIAN_POINT('Ctrl Pts',(-251.585260692536,-4.2263085876992,
128.285173052928));
#138077=CARTESIAN_POINT('Ctrl Pts',(-251.593021135052,-4.29487668315844,
128.403953278882));
#138078=CARTESIAN_POINT('Ctrl Pts',(-251.600781577567,-4.3583097824858,
128.525255770836));
#138079=CARTESIAN_POINT('Ctrl Pts',(-251.608554477834,-4.42184471025516,
128.646752988318));
#138080=CARTESIAN_POINT('Ctrl Pts',(-251.6163273781,-4.48022800284043,128.770780208984));
#138081=CARTESIAN_POINT('Ctrl Pts',(-251.624100278367,-4.53327764655705,
128.896855220005));
#138082=CARTESIAN_POINT('Ctrl Pts',(-251.631590614116,-4.58439880200303,
129.018347086578));
#138083=CARTESIAN_POINT('Ctrl Pts',(-251.639080949865,-4.63056725131765,
129.141740155193));
#138084=CARTESIAN_POINT('Ctrl Pts',(-251.646571285614,-4.67166446012101,
129.266591377874));
#138085=CARTESIAN_POINT('Ctrl Pts',(-251.652821157903,-4.70595562076918,
129.370766173651));
#138086=CARTESIAN_POINT('Ctrl Pts',(-251.659071030192,-4.7367771621133,
129.476136082795));
#138087=CARTESIAN_POINT('Ctrl Pts',(-251.665320902482,-4.76405452823413,
129.582490119309));
#138088=CARTESIAN_POINT('Ctrl Pts',(-249.915046309122,-4.76405452823416,
129.582490119309));
#138089=CARTESIAN_POINT('Ctrl Pts',(-249.922808577032,-4.79811276617232,
129.715282672124));
#138090=CARTESIAN_POINT('Ctrl Pts',(-249.930570844942,-4.82658446629422,
129.849382520667));
#138091=CARTESIAN_POINT('Ctrl Pts',(-249.938333112852,-4.84939694061544,
129.984279905167));
#138092=CARTESIAN_POINT('Ctrl Pts',(-249.946107049739,-4.87224370881249,
130.119380080213));
#138093=CARTESIAN_POINT('Ctrl Pts',(-249.953880986627,-4.88941421055682,
130.255279798624));
#138094=CARTESIAN_POINT('Ctrl Pts',(-249.961654923514,-4.90088768873931,
130.391464837903));
#138095=CARTESIAN_POINT('Ctrl Pts',(-249.966398463255,-4.90788863311393,
130.474562907162));
#138096=CARTESIAN_POINT('Ctrl Pts',(-249.971142002996,-4.91276945039334,
130.557767191997));
#138097=CARTESIAN_POINT('Ctrl Pts',(-249.975885542736,-4.91553494191603,
130.640961421416));
#138098=CARTESIAN_POINT('Ctrl Pts',(-249.978970549829,-4.9173335061588,
130.695067595674));
#138099=CARTESIAN_POINT('Ctrl Pts',(-249.982055556921,-4.91823876860267,
130.749203629498));
#138100=CARTESIAN_POINT('Ctrl Pts',(-249.985140564014,-4.91824989614147,
130.803349873091));
#138101=CARTESIAN_POINT('',(-249.639859436026,-4.91824799670603,130.808799693728));
#138102=CARTESIAN_POINT('Ctrl Pts',(-249.569887472766,-4.76405452823394,
129.582490119308));
#138103=CARTESIAN_POINT('Ctrl Pts',(-249.577565655275,-4.79786475257207,
129.71431567086));
#138104=CARTESIAN_POINT('Ctrl Pts',(-249.585243837783,-4.82620038099429,
129.847550331812));
#138105=CARTESIAN_POINT('Ctrl Pts',(-249.592922020292,-4.848959238378,129.98169582128));
#138106=CARTESIAN_POINT('Ctrl Pts',(-249.600744922909,-4.87214705981838,
130.118369715068));
#138107=CARTESIAN_POINT('Ctrl Pts',(-249.608567825527,-4.88954567913427,
130.25598869821));
#138108=CARTESIAN_POINT('Ctrl Pts',(-249.616390728144,-4.90110212331456,
130.394018029791));
#138109=CARTESIAN_POINT('Ctrl Pts',(-249.624213630762,-4.91265856749487,
130.532047361373));
#138110=CARTESIAN_POINT('Ctrl Pts',(-249.63203653338,-4.91837283430366,
130.670486604846));
#138111=CARTESIAN_POINT('Ctrl Pts',(-249.639859435997,-4.91824799670649,
130.808799693213));
#138112=CARTESIAN_POINT('Ctrl Pts',(-249.639859436026,-4.91824799670602,
130.808799693728));
#138113=CARTESIAN_POINT('Ctrl Pts',(-249.649450864241,-4.91809493702354,
130.978381257395));
#138114=CARTESIAN_POINT('Ctrl Pts',(-249.659042292456,-4.90916748110856,
131.147572254414));
#138115=CARTESIAN_POINT('Ctrl Pts',(-249.668633720671,-4.89160842038733,
131.315584760282));
#138116=CARTESIAN_POINT('Ctrl Pts',(-249.678384122473,-4.87375832617249,
131.486381997482));
#138117=CARTESIAN_POINT('Ctrl Pts',(-249.688134524275,-4.84698816366428,
131.655961449596));
#138118=CARTESIAN_POINT('Ctrl Pts',(-249.697884926077,-4.81149657870729,
131.823518964236));
#138119=CARTESIAN_POINT('Ctrl Pts',(-249.704265589079,-4.78827088528351,
131.933168602893));
#138120=CARTESIAN_POINT('Ctrl Pts',(-249.710646252081,-4.76131132158729,
132.041952848757));
#138121=CARTESIAN_POINT('Ctrl Pts',(-249.717026915082,-4.7306845068774,
132.14965135153));
#138122=CARTESIAN_POINT('Ctrl Pts',(-249.724801249201,-4.69336815111763,
132.280873474443));
#138123=CARTESIAN_POINT('Ctrl Pts',(-249.732575583321,-4.65052869261664,
132.410749617163));
#138124=CARTESIAN_POINT('Ctrl Pts',(-249.74034991744,-4.60227921961991,
132.538779554027));
#138125=CARTESIAN_POINT('Ctrl Pts',(-249.748114670387,-4.55408920978661,
132.666651705436));
#138126=CARTESIAN_POINT('Ctrl Pts',(-249.755879423334,-4.50050258806562,
132.792681815789));
#138127=CARTESIAN_POINT('Ctrl Pts',(-249.763644176281,-4.44168278131277,
132.91638266591));
#138128=CARTESIAN_POINT('Ctrl Pts',(-249.771401217166,-4.38292139522121,
133.039960654602));
#138129=CARTESIAN_POINT('Ctrl Pts',(-249.779158258051,-4.31893733450593,
133.161213636144));
#138130=CARTESIAN_POINT('Ctrl Pts',(-249.786915298936,-4.24994275705539,
133.279672643201));
#138131=CARTESIAN_POINT('Ctrl Pts',(-249.794666490176,-4.18100020895249,
133.398042319399));
#138132=CARTESIAN_POINT('Ctrl Pts',(-249.802417681416,-4.1070548609022,
133.51362187841));
#138133=CARTESIAN_POINT('Ctrl Pts',(-249.810168872656,-4.0283654398268,
133.625965647635));
#138134=CARTESIAN_POINT('Ctrl Pts',(-249.817916769434,-3.94970946385435,
133.73826166776));
#138135=CARTESIAN_POINT('Ctrl Pts',(-249.825664666211,-3.86631364906585,
133.847324313904));
#138136=CARTESIAN_POINT('Ctrl Pts',(-249.833412562988,-3.77848068400477,
133.952735878411));
#138137=CARTESIAN_POINT('Ctrl Pts',(-249.841158839072,-3.69066609170653,
134.058125393092));
#138138=CARTESIAN_POINT('Ctrl Pts',(-249.848905115156,-3.59841644540369,
134.159865045061));
#138139=CARTESIAN_POINT('Ctrl Pts',(-249.85665139124,-3.50207520738866,
134.257569604044));
#138140=CARTESIAN_POINT('Ctrl Pts',(-249.864397724505,-3.40573325820436,
134.355274884261));
#138141=CARTESIAN_POINT('Ctrl Pts',(-249.872144057771,-3.30529993154463,
134.448944733666));
#138142=CARTESIAN_POINT('Ctrl Pts',(-249.879890391036,-3.20115580350047,
134.5382305382));
#138143=CARTESIAN_POINT('Ctrl Pts',(-249.887638459039,-3.09698835310106,
134.627536337671));
#138144=CARTESIAN_POINT('Ctrl Pts',(-249.895386527042,-2.98910874446581,
134.712455884229));
#138145=CARTESIAN_POINT('Ctrl Pts',(-249.903134595045,-2.8779305789088,
134.792680896265));
#138146=CARTESIAN_POINT('Ctrl Pts',(-249.910890897787,-2.76663425187424,
134.872991172399));
#138147=CARTESIAN_POINT('Ctrl Pts',(-249.918647200529,-2.6520326823616,
134.948596717994));
#138148=CARTESIAN_POINT('Ctrl Pts',(-249.926403503271,-2.5345688623945,
135.019232352777));
#138149=CARTESIAN_POINT('Ctrl Pts',(-249.934163945785,-2.4170423484496,
135.089905687925));
#138150=CARTESIAN_POINT('Ctrl Pts',(-249.941924388299,-2.29665088306278,
135.155603639562));
#138151=CARTESIAN_POINT('Ctrl Pts',(-249.949684830813,-2.17386110377588,
135.21610754639));
#138152=CARTESIAN_POINT('Ctrl Pts',(-249.957457731079,-2.05087421143483,
135.276708579461));
#138153=CARTESIAN_POINT('Ctrl Pts',(-249.965230631344,-1.9254816695273,
135.332098747793));
#138154=CARTESIAN_POINT('Ctrl Pts',(-249.97300353161,-1.79816991984631,
135.382107661895));
#138155=CARTESIAN_POINT('Ctrl Pts',(-249.980493867372,-1.67548627294552,
135.430298626004));
#138156=CARTESIAN_POINT('Ctrl Pts',(-249.987984203134,-1.55102082278758,
135.473492686614));
#138157=CARTESIAN_POINT('Ctrl Pts',(-249.995474538896,-1.42521933426106,
135.511581975411));
#138158=CARTESIAN_POINT('Ctrl Pts',(-250.003248873015,-1.29464804406033,
135.551115431169));
#138159=CARTESIAN_POINT('Ctrl Pts',(-250.011023207134,-1.16222379317508,
135.585274608996));
#138160=CARTESIAN_POINT('Ctrl Pts',(-250.018797541253,-1.02842856258211,
135.613884269048));
#138161=CARTESIAN_POINT('Ctrl Pts',(-250.0265622942,-0.894798222653221,
135.642458670251));
#138162=CARTESIAN_POINT('Ctrl Pts',(-250.034327047147,-0.759800643488834,
135.665497080847));
#138163=CARTESIAN_POINT('Ctrl Pts',(-250.042091800095,-0.623934072588422,
135.682873642614));
#138164=CARTESIAN_POINT('Ctrl Pts',(-250.04984884098,-0.488202446281613,
135.700232945735));
#138165=CARTESIAN_POINT('Ctrl Pts',(-250.057605881864,-0.351603931133389,
135.711941541624));
#138166=CARTESIAN_POINT('Ctrl Pts',(-250.065362922749,-0.214647759164977,
135.717924436423));
#138167=CARTESIAN_POINT('Ctrl Pts',(-250.07311411399,-0.0777948669113959,
135.723902819475));
#138168=CARTESIAN_POINT('Ctrl Pts',(-250.08086530523,0.0594147563051551,
135.724164078753));
#138169=CARTESIAN_POINT('Ctrl Pts',(-250.08861649647,0.196466305281641,
135.718684991617));
#138170=CARTESIAN_POINT('Ctrl Pts',(-250.096364393247,0.333459603694028,
135.713208233239));
#138171=CARTESIAN_POINT('Ctrl Pts',(-250.104112290024,0.470294571658441,
135.701995996609));
#138172=CARTESIAN_POINT('Ctrl Pts',(-250.111860186801,0.606456169344113,
135.685077160981));
#138173=CARTESIAN_POINT('Ctrl Pts',(-250.119606462885,0.742589284958854,
135.668161864409));
#138174=CARTESIAN_POINT('Ctrl Pts',(-250.127352738969,0.878048922726506,
135.645542391347));
#138175=CARTESIAN_POINT('Ctrl Pts',(-250.135099015053,1.01232532774888,
135.617299479976));
#138176=CARTESIAN_POINT('Ctrl Pts',(-250.142845348319,1.14660272396899,
135.589056360123));
#138177=CARTESIAN_POINT('Ctrl Pts',(-250.150591681584,1.27969648742131,
135.555189799601));
#138178=CARTESIAN_POINT('Ctrl Pts',(-250.158338014849,1.4111076085504,135.515831553441));
#138179=CARTESIAN_POINT('Ctrl Pts',(-250.166086082852,1.54254815828874,
135.476464493274));
#138180=CARTESIAN_POINT('Ctrl Pts',(-250.173834150855,1.67230494142739,
135.431603412409));
#138181=CARTESIAN_POINT('Ctrl Pts',(-250.181582218858,1.7998950303049,135.381429651608));
#138182=CARTESIAN_POINT('Ctrl Pts',(-250.1893385216,1.92762072344738,135.331202565536));
#138183=CARTESIAN_POINT('Ctrl Pts',(-250.197094824342,2.05317475783678,
135.275651663582));
#138184=CARTESIAN_POINT('Ctrl Pts',(-250.204851127084,2.17609458179027,
135.215006311067));
#138185=CARTESIAN_POINT('Ctrl Pts',(-250.212611569598,2.29908001175517,
135.154328590302));
#138186=CARTESIAN_POINT('Ctrl Pts',(-250.220372012112,2.41942808689568,
135.08855118843));
#138187=CARTESIAN_POINT('Ctrl Pts',(-250.228132454626,2.53670261228168,
135.01794850906));
#138188=CARTESIAN_POINT('Ctrl Pts',(-250.235905354892,2.65416539714665,
134.947232492001));
#138189=CARTESIAN_POINT('Ctrl Pts',(-250.243678255157,2.76854444627906,
134.871675934157));
#138190=CARTESIAN_POINT('Ctrl Pts',(-250.251451155423,2.87943347250361,
134.791595993102));
#138191=CARTESIAN_POINT('Ctrl Pts',(-250.258941491185,2.98629140331409,
134.714427159613));
#138192=CARTESIAN_POINT('Ctrl Pts',(-250.266431826947,3.08990840587486,
134.633058296182));
#138193=CARTESIAN_POINT('Ctrl Pts',(-250.273922162709,3.18995278070627,
134.547806131977));
#138194=CARTESIAN_POINT('Ctrl Pts',(-250.281696496828,3.29379036841621,
134.459321606055));
#138195=CARTESIAN_POINT('Ctrl Pts',(-250.289470830947,3.39410799440705,
134.366373203335));
#138196=CARTESIAN_POINT('Ctrl Pts',(-250.297245165066,3.49049770194225,
134.269271706647));
#138197=CARTESIAN_POINT('Ctrl Pts',(-250.305009918014,3.58676861777726,
134.172289878875));
#138198=CARTESIAN_POINT('Ctrl Pts',(-250.312774670961,3.67912097413148,
134.071165415866));
#138199=CARTESIAN_POINT('Ctrl Pts',(-250.320539423908,3.76717956797308,
133.966249477907));
#138200=CARTESIAN_POINT('Ctrl Pts',(-250.328296464793,3.85515070077786,
133.861437743936));
#138201=CARTESIAN_POINT('Ctrl Pts',(-250.336053505678,3.93883630814634,
133.752842326548));
#138202=CARTESIAN_POINT('Ctrl Pts',(-250.343810546563,4.01789804327467,
133.640851121049));
#138203=CARTESIAN_POINT('Ctrl Pts',(-250.351561737803,4.09690015733341,
133.52894436899));
#138204=CARTESIAN_POINT('Ctrl Pts',(-250.359312929043,4.17128511504299,
133.41364724402));
#138205=CARTESIAN_POINT('Ctrl Pts',(-250.367064120283,4.24075511375156,
133.295380313933));
#138206=CARTESIAN_POINT('Ctrl Pts',(-250.37481201706,4.31019558585761,133.177163650446));
#138207=CARTESIAN_POINT('Ctrl Pts',(-250.382559913837,4.37472505619843,
133.055980028757));
#138208=CARTESIAN_POINT('Ctrl Pts',(-250.390307810615,4.43408943009937,
132.932278376405));
#138209=CARTESIAN_POINT('Ctrl Pts',(-250.398054086699,4.49344138625305,
132.808602599771));
#138210=CARTESIAN_POINT('Ctrl Pts',(-250.405800362783,4.54763022594817,
132.682410192399));
#138211=CARTESIAN_POINT('Ctrl Pts',(-250.413546638867,4.5964483415293,132.554173666481));
#138212=CARTESIAN_POINT('Ctrl Pts',(-250.421292972132,4.6452668174746,132.42593619395));
#138213=CARTESIAN_POINT('Ctrl Pts',(-250.429039305398,4.68871435109881,
132.295654938147));
#138214=CARTESIAN_POINT('Ctrl Pts',(-250.436785638663,4.72663206478553,
132.163820946756));
#138215=CARTESIAN_POINT('Ctrl Pts',(-250.444533706666,4.76455826988137,
132.031957432056));
#138216=CARTESIAN_POINT('Ctrl Pts',(-250.452281774669,4.7969520827905,131.898540865498));
#138217=CARTESIAN_POINT('Ctrl Pts',(-250.460029842672,4.82370503643262,
131.76407556691));
#138218=CARTESIAN_POINT('Ctrl Pts',(-250.467786145414,4.85048642343228,
131.629467357002));
#138219=CARTESIAN_POINT('Ctrl Pts',(-250.475542448156,4.87161489875032,
131.493808572583));
#138220=CARTESIAN_POINT('Ctrl Pts',(-250.483298750898,4.88703341344428,
131.35761234904));
#138221=CARTESIAN_POINT('Ctrl Pts',(-250.491059193412,4.90246015746378,
131.221343433472));
#138222=CARTESIAN_POINT('Ctrl Pts',(-250.498819635926,4.91217084063423,
131.084536897008));
#138223=CARTESIAN_POINT('Ctrl Pts',(-250.50658007844,4.91616055246869,130.947708044647));
#138224=CARTESIAN_POINT('Ctrl Pts',(-250.514352978706,4.92015666894279,
130.810659542465));
#138225=CARTESIAN_POINT('Ctrl Pts',(-250.522125878971,4.91841346687458,
130.67358904396));
#138226=CARTESIAN_POINT('Ctrl Pts',(-250.529898779237,4.91097817177237,
130.537009801455));
#138227=CARTESIAN_POINT('Ctrl Pts',(-250.537389114998,4.90381316837573,
130.405395558441));
#138228=CARTESIAN_POINT('Ctrl Pts',(-250.54487945076,4.89136275995624,130.274237781377));
#138229=CARTESIAN_POINT('Ctrl Pts',(-250.552369786522,4.87371412806055,
130.14398673828));
#138230=CARTESIAN_POINT('Ctrl Pts',(-250.560144120641,4.85539634292187,
130.008797187292));
#138231=CARTESIAN_POINT('Ctrl Pts',(-250.56791845476,4.83142034652068,129.874156245343));
#138232=CARTESIAN_POINT('Ctrl Pts',(-250.575692788879,4.8018270986718,129.740575123699));
#138233=CARTESIAN_POINT('Ctrl Pts',(-250.583457541826,4.77227032185607,
129.60715862885));
#138234=CARTESIAN_POINT('Ctrl Pts',(-250.591222294773,4.73711015157387,
129.474799733536));
#138235=CARTESIAN_POINT('Ctrl Pts',(-250.598987047721,4.69643922251756,
129.344003917407));
#138236=CARTESIAN_POINT('Ctrl Pts',(-250.606744088606,4.65580868840135,
129.213338009527));
#138237=CARTESIAN_POINT('Ctrl Pts',(-250.614501129491,4.60967840308756,
129.084232462259));
#138238=CARTESIAN_POINT('Ctrl Pts',(-250.622258170376,4.55819182917327,
128.957181603242));
#138239=CARTESIAN_POINT('Ctrl Pts',(-250.630009361616,4.50674408168482,
128.830226554266));
#138240=CARTESIAN_POINT('Ctrl Pts',(-250.637760552856,4.44994823165931,
128.705323470318));
#138241=CARTESIAN_POINT('Ctrl Pts',(-250.645511744096,4.38799714508469,
128.58295022837));
#138242=CARTESIAN_POINT('Ctrl Pts',(-250.653259640873,4.32607238937454,
128.460628998314));
#138243=CARTESIAN_POINT('Ctrl Pts',(-250.66100753765,4.25899693128842,128.340835819749));
#138244=CARTESIAN_POINT('Ctrl Pts',(-250.668755434427,4.18701112190058,
128.224027126023));
#138245=CARTESIAN_POINT('Ctrl Pts',(-250.676501710511,4.11504037039223,
128.107242866157));
#138246=CARTESIAN_POINT('Ctrl Pts',(-250.684247986595,4.03816151560704,
127.993442182008));
#138247=CARTESIAN_POINT('Ctrl Pts',(-250.69199426268,3.95665987842547,127.883055144159));
#138248=CARTESIAN_POINT('Ctrl Pts',(-250.699740595945,3.87515763961723,
127.772667291457));
#138249=CARTESIAN_POINT('Ctrl Pts',(-250.70748692921,3.78903278254256,127.665693449863));
#138250=CARTESIAN_POINT('Ctrl Pts',(-250.715233262476,3.69861256229198,
127.562532710882));
#138251=CARTESIAN_POINT('Ctrl Pts',(-250.722981330479,3.60817209306012,
127.459348869768));
#138252=CARTESIAN_POINT('Ctrl Pts',(-250.730729398481,3.51343460420178,
127.359980124422));
#138253=CARTESIAN_POINT('Ctrl Pts',(-250.738477466484,3.41476576516571,
127.264790328456));
#138254=CARTESIAN_POINT('Ctrl Pts',(-250.746233769226,3.31599205971319,
127.169499363641));
#138255=CARTESIAN_POINT('Ctrl Pts',(-250.753990071968,3.21327893932589,
127.078396492338));
#138256=CARTESIAN_POINT('Ctrl Pts',(-250.76174637471,3.10702728299285,126.991807073648));
#138257=CARTESIAN_POINT('Ctrl Pts',(-250.769506817224,3.00071891695165,
126.905171439579));
#138258=CARTESIAN_POINT('Ctrl Pts',(-250.777267259738,2.89086856471197,
126.823054292162));
#138259=CARTESIAN_POINT('Ctrl Pts',(-250.785027702253,2.77790711272766,
126.74573829767));
#138260=CARTESIAN_POINT('Ctrl Pts',(-250.792800602518,2.66476432499238,
126.66829818868));
#138261=CARTESIAN_POINT('Ctrl Pts',(-250.800573502783,2.54850078926418,
126.595674841375));
#138262=CARTESIAN_POINT('Ctrl Pts',(-250.808346403049,2.42957384579995,
126.528105949015));
#138263=CARTESIAN_POINT('Ctrl Pts',(-250.815836738811,2.31497019628955,
126.462993356088));
#138264=CARTESIAN_POINT('Ctrl Pts',(-250.823327074573,2.19789369399235,
126.402574255094));
#138265=CARTESIAN_POINT('Ctrl Pts',(-250.830817410335,2.07877028589902,
126.347018678589));
#138266=CARTESIAN_POINT('Ctrl Pts',(-250.838591744454,1.95513027758222,
126.289356695516));
#138267=CARTESIAN_POINT('Ctrl Pts',(-250.846366078573,1.82889342819074,
126.236751662413));
#138268=CARTESIAN_POINT('Ctrl Pts',(-250.854140412692,1.70051197402192,
126.189445440804));
#138269=CARTESIAN_POINT('Ctrl Pts',(-250.861905165639,1.57228873852158,
126.142197519886));
#138270=CARTESIAN_POINT('Ctrl Pts',(-250.869669918586,1.44192652042377,
126.100235550969));
#138271=CARTESIAN_POINT('Ctrl Pts',(-250.877434671533,1.30990066538821,
126.063754821962));
#138272=CARTESIAN_POINT('Ctrl Pts',(-250.885191712418,1.17800594029348,
126.027310326129));
#138273=CARTESIAN_POINT('Ctrl Pts',(-250.892948753303,1.04445124091266,
125.996336339765));
#138274=CARTESIAN_POINT('Ctrl Pts',(-250.900705794188,0.909730004125608,
125.970979359886));
#138275=CARTESIAN_POINT('Ctrl Pts',(-250.908456985428,0.775110361671008,
125.945641501903));
#138276=CARTESIAN_POINT('Ctrl Pts',(-250.916208176668,0.639326315453693,
125.92591229127));
#138277=CARTESIAN_POINT('Ctrl Pts',(-250.923959367908,0.50288416568047,
125.911887768545));
#138278=CARTESIAN_POINT('Ctrl Pts',(-250.931707264685,0.366500007460429,
125.897869206616));
#138279=CARTESIAN_POINT('Ctrl Pts',(-250.939455161462,0.229458690111338,
125.889550550054));
#138280=CARTESIAN_POINT('Ctrl Pts',(-250.947203058239,0.0922741395609136,
125.886976298066));
#138281=CARTESIAN_POINT('Ctrl Pts',(-250.954949334323,-0.0448817149388916,
125.884402584555));
#138282=CARTESIAN_POINT('Ctrl Pts',(-250.962695610407,-0.182180352396627,
125.887570892889));
#138283=CARTESIAN_POINT('Ctrl Pts',(-250.970441886491,-0.319105719346386,
125.896473638185));
#138284=CARTESIAN_POINT('Ctrl Pts',(-250.978188219756,-0.456032097047913,
125.905376449198));
#138285=CARTESIAN_POINT('Ctrl Pts',(-250.985934553022,-0.592584808601845,
125.920013756274));
#138286=CARTESIAN_POINT('Ctrl Pts',(-250.993680886287,-0.728251197651638,
125.940325949143));
#138287=CARTESIAN_POINT('Ctrl Pts',(-251.00142895429,-0.863947968248428,
125.960642690787));
#138288=CARTESIAN_POINT('Ctrl Pts',(-251.009177022293,-0.998757634795884,
125.986636789191));
#138289=CARTESIAN_POINT('Ctrl Pts',(-251.016925090296,-1.13217642367568,
126.018197268058));
#138290=CARTESIAN_POINT('Ctrl Pts',(-251.024681393037,-1.26573701163219,
126.049791289777));
#138291=CARTESIAN_POINT('Ctrl Pts',(-251.032437695779,-1.3979033879028,
126.086963419694));
#138292=CARTESIAN_POINT('Ctrl Pts',(-251.040193998521,-1.52818513377386,
126.129552251503));
#138293=CARTESIAN_POINT('Ctrl Pts',(-251.047954441035,-1.65853641493575,
126.172163814254));
#138294=CARTESIAN_POINT('Ctrl Pts',(-251.055714883549,-1.78700069536488,
126.220197702714));
#138295=CARTESIAN_POINT('Ctrl Pts',(-251.063475326063,-1.91310725526774,
126.27344418793));
#138296=CARTESIAN_POINT('Ctrl Pts',(-251.071248226329,-2.03941625261544,
126.326776149132));
#138297=CARTESIAN_POINT('Ctrl Pts',(-251.079021126594,-2.16335961245829,
126.38533726135));
#138298=CARTESIAN_POINT('Ctrl Pts',(-251.086794026859,-2.28449015314461,
126.448871230289));
#138299=CARTESIAN_POINT('Ctrl Pts',(-251.094284362622,-2.40121729358167,
126.510095579431));
#138300=CARTESIAN_POINT('Ctrl Pts',(-251.101774698385,-2.51533230366311,
126.575937356693));
#138301=CARTESIAN_POINT('Ctrl Pts',(-251.109265034148,-2.62646189542995,
126.646130107559));
#138302=CARTESIAN_POINT('Ctrl Pts',(-251.117040759838,-2.74182564533264,
126.718997278463));
#138303=CARTESIAN_POINT('Ctrl Pts',(-251.124816485528,-2.85433747466235,
126.796784412517));
#138304=CARTESIAN_POINT('Ctrl Pts',(-251.132592211218,-2.96354921518992,
126.879241624255));
#138305=CARTESIAN_POINT('Ctrl Pts',(-251.140391207646,-3.07308779824208,
126.961945609126));
#138306=CARTESIAN_POINT('Ctrl Pts',(-251.148190204075,-3.1793061411131,
127.049347514605));
#138307=CARTESIAN_POINT('Ctrl Pts',(-251.155989200503,-3.28177747678981,
127.141148959016));
#138308=CARTESIAN_POINT('Ctrl Pts',(-251.163745507121,-3.38368790929289,
127.232447904644));
#138309=CARTESIAN_POINT('Ctrl Pts',(-251.171501813739,-3.48189194093155,
127.328098103309));
#138310=CARTESIAN_POINT('Ctrl Pts',(-251.179258120358,-3.57599986306124,
127.42776350777));
#138311=CARTESIAN_POINT('Ctrl Pts',(-251.187009028654,-3.67004228689541,
127.527359545975));
#138312=CARTESIAN_POINT('Ctrl Pts',(-251.19475993695,-3.75999400619828,
127.63096494677));
#138313=CARTESIAN_POINT('Ctrl Pts',(-251.202510845247,-3.84550075558553,
127.738205533215));
#138314=CARTESIAN_POINT('Ctrl Pts',(-251.210258037643,-3.93096651176949,
127.845394706933));
#138315=CARTESIAN_POINT('Ctrl Pts',(-251.218005230038,-4.01199129613124,
127.956215292766));
#138316=CARTESIAN_POINT('Ctrl Pts',(-251.225752422434,-4.08826014679485,
128.070258930608));
#138317=CARTESIAN_POINT('Ctrl Pts',(-251.233587064356,-4.16538991254661,
128.185589881522));
#138318=CARTESIAN_POINT('Ctrl Pts',(-251.241421706278,-4.23765544892985,
128.30421678704));
#138319=CARTESIAN_POINT('Ctrl Pts',(-251.2492563482,-4.30477522581095,128.42568591981));
#138320=CARTESIAN_POINT('Ctrl Pts',(-251.257002773549,-4.37113924681997,
128.545787333339));
#138321=CARTESIAN_POINT('Ctrl Pts',(-251.264749198899,-4.43247263153778,
128.668666932258));
#138322=CARTESIAN_POINT('Ctrl Pts',(-251.272495624249,-4.48854916261805,
128.793860809742));
#138323=CARTESIAN_POINT('Ctrl Pts',(-251.280374374456,-4.54558359604531,
128.921193255835));
#138324=CARTESIAN_POINT('Ctrl Pts',(-251.288253124664,-4.59717974895373,
129.05091939507));
#138325=CARTESIAN_POINT('Ctrl Pts',(-251.296131874872,-4.64315073532577,
129.182530074154));
#138326=CARTESIAN_POINT('Ctrl Pts',(-251.30401062508,-4.68912172169794,
129.314140753238));
#138327=CARTESIAN_POINT('Ctrl Pts',(-251.311889375288,-4.72946743343979,
129.447635561638));
#138328=CARTESIAN_POINT('Ctrl Pts',(-251.319768125496,-4.76405452823393,
129.582490119308));
#138329=CARTESIAN_POINT('Origin',(213.235140564004,0.,130.804360617566));
#138330=CARTESIAN_POINT('',(-253.415334457588,-4.76405452823403,129.582490119308));
#138331=CARTESIAN_POINT('',(-253.070001742224,-4.7640545282341,129.582490119308));
#138332=CARTESIAN_POINT('',(213.235140564004,-4.76405452823405,129.582490119308));
#138333=CARTESIAN_POINT('',(-251.735140563966,-4.91824833132154,130.800309203871));
#138334=CARTESIAN_POINT('Ctrl Pts',(-251.735140564014,-4.91824833132224,
130.800309204721));
#138335=CARTESIAN_POINT('Ctrl Pts',(-251.74305216174,-4.91836371085688,
130.940375207723));
#138336=CARTESIAN_POINT('Ctrl Pts',(-251.750963759465,-4.91249099768164,
131.080528748395));
#138337=CARTESIAN_POINT('Ctrl Pts',(-251.75887535719,-4.90063728135767,
131.220217923703));
#138338=CARTESIAN_POINT('Ctrl Pts',(-251.766596302519,-4.8890692139637,
131.35654089196));
#138339=CARTESIAN_POINT('Ctrl Pts',(-251.774317247848,-4.8718051620345,
131.492421209125));
#138340=CARTESIAN_POINT('Ctrl Pts',(-251.782038193177,-4.84890439244957,
131.627348621964));
#138341=CARTESIAN_POINT('Ctrl Pts',(-251.789759019141,-4.82600397690774,
131.762273948842));
#138342=CARTESIAN_POINT('Ctrl Pts',(-251.797479845106,-4.79746708251017,
131.896246012727));
#138343=CARTESIAN_POINT('Ctrl Pts',(-251.80520067107,-4.76340439916263,
132.028763162703));
#138344=CARTESIAN_POINT('Ctrl Pts',(-251.812923074694,-4.72933475550731,
132.161307390996));
#138345=CARTESIAN_POINT('Ctrl Pts',(-251.820645478317,-4.68973717418013,
132.292395732819));
#138346=CARTESIAN_POINT('Ctrl Pts',(-251.828367881941,-4.6447725543266,
132.421540564595));
#138347=CARTESIAN_POINT('Ctrl Pts',(-251.836422134232,-4.59787570587356,
132.556235033804));
#138348=CARTESIAN_POINT('Ctrl Pts',(-251.844476386522,-4.54514044073534,
132.688814793964));
#138349=CARTESIAN_POINT('Ctrl Pts',(-251.852530638813,-4.48680504939182,
132.818749733713));
#138350=CARTESIAN_POINT('Ctrl Pts',(-251.860265684137,-4.43078161235955,
132.943535078385));
#138351=CARTESIAN_POINT('Ctrl Pts',(-251.86800072946,-4.36959367777433,
133.065880905503));
#138352=CARTESIAN_POINT('Ctrl Pts',(-251.875735774784,-4.30349892103463,
133.185343628667));
#138353=CARTESIAN_POINT('Ctrl Pts',(-251.883476435969,-4.23735617763905,
133.304893085136));
#138354=CARTESIAN_POINT('Ctrl Pts',(-251.891217097154,-4.16629972156714,
133.421554934597));
#138355=CARTESIAN_POINT('Ctrl Pts',(-251.898957758339,-4.0906301933765,
133.534915082054));
#138356=CARTESIAN_POINT('Ctrl Pts',(-251.906709382642,-4.01485349424142,
133.648435781776));
#138357=CARTESIAN_POINT('Ctrl Pts',(-251.914461006945,-3.93445091636207,
133.758645132567));
#138358=CARTESIAN_POINT('Ctrl Pts',(-251.922212631247,-3.8497630856514,
133.865162350259));
#138359=CARTESIAN_POINT('Ctrl Pts',(-251.923148057307,-3.83954339482556,
133.87801629897));
#138360=CARTESIAN_POINT('Ctrl Pts',(-251.924083483367,-3.82926134363088,
133.890816526164));
#138361=CARTESIAN_POINT('Ctrl Pts',(-251.925018909426,-3.81891756565244,
133.903562400163));
#138362=CARTESIAN_POINT('Ctrl Pts',(-251.932793243543,-3.73295033690651,
134.009493469825));
#138363=CARTESIAN_POINT('Ctrl Pts',(-251.94056757766,-3.64243604747541,
134.112012712167));
#138364=CARTESIAN_POINT('Ctrl Pts',(-251.948341911777,-3.54767560085317,
134.210704830004));
#138365=CARTESIAN_POINT('Ctrl Pts',(-251.956106664722,-3.45303193801269,
134.309275318626));
#138366=CARTESIAN_POINT('Ctrl Pts',(-251.963871417667,-3.35415279828997,
134.404027788042));
#138367=CARTESIAN_POINT('Ctrl Pts',(-251.971636170612,-3.25138023700927,
134.49457871639));
#138368=CARTESIAN_POINT('Ctrl Pts',(-251.979393211495,-3.14870975088558,
134.585039708279));
#138369=CARTESIAN_POINT('Ctrl Pts',(-251.987150252378,-3.04215383015814,
134.671307206829));
#138370=CARTESIAN_POINT('Ctrl Pts',(-251.994907293261,-2.93209213904093,
134.753033654255));
#138371=CARTESIAN_POINT('Ctrl Pts',(-252.002658484498,-2.82211344630132,
134.834698471131));
#138372=CARTESIAN_POINT('Ctrl Pts',(-252.010409675736,-2.70863455797444,
134.911828820889));
#138373=CARTESIAN_POINT('Ctrl Pts',(-252.018160866974,-2.5920687742975,
134.98411689417));
#138374=CARTESIAN_POINT('Ctrl Pts',(-252.025908763749,-2.47555253418798,
135.056374243092));
#138375=CARTESIAN_POINT('Ctrl Pts',(-252.033656660524,-2.35595233978666,
135.123793203315));
#138376=CARTESIAN_POINT('Ctrl Pts',(-252.041404557299,-2.23371089178026,
135.186108980314));
#138377=CARTESIAN_POINT('Ctrl Pts',(-252.049150833381,-2.1114950140499,
135.248411722195));
#138378=CARTESIAN_POINT('Ctrl Pts',(-252.056897109463,-1.9866393297505,
135.30561322667));
#138379=CARTESIAN_POINT('Ctrl Pts',(-252.064643385545,-1.85961123299061,
135.357494606879));
#138380=CARTESIAN_POINT('Ctrl Pts',(-252.072389718808,-1.73258219853835,
135.409376370064));
#138381=CARTESIAN_POINT('Ctrl Pts',(-252.080136052071,-1.60338108156755,
135.455937782793));
#138382=CARTESIAN_POINT('Ctrl Pts',(-252.087882385335,-1.47249497572673,
135.497008229412));
#138383=CARTESIAN_POINT('Ctrl Pts',(-252.095630453335,-1.34157955884983,
135.538087873472));
#138384=CARTESIAN_POINT('Ctrl Pts',(-252.103378521336,-1.20897877519691,
135.573673987504));
#138385=CARTESIAN_POINT('Ctrl Pts',(-252.111126589337,-1.0751941964541,
135.603646033377));
#138386=CARTESIAN_POINT('Ctrl Pts',(-252.118882892077,-0.941267429868731,
135.633649933896));
#138387=CARTESIAN_POINT('Ctrl Pts',(-252.126639194817,-0.806154737017025,
135.658027761528));
#138388=CARTESIAN_POINT('Ctrl Pts',(-252.134395497556,-0.670367736500607,
135.676710169924));
#138389=CARTESIAN_POINT('Ctrl Pts',(-252.142155940068,-0.534508262373896,
135.695402549683));
#138390=CARTESIAN_POINT('Ctrl Pts',(-252.14991638258,-0.397974152471628,
135.7083934161));
#138391=CARTESIAN_POINT('Ctrl Pts',(-252.157676825092,-0.261280445561837,
135.715665494202));
#138392=CARTESIAN_POINT('Ctrl Pts',(-252.165449725356,-0.124367305777813,
135.72294924609));
#138393=CARTESIAN_POINT('Ctrl Pts',(-252.173222625619,0.0127055518162359,
135.724495860071));
#138394=CARTESIAN_POINT('Ctrl Pts',(-252.180995525882,0.14942388941872,
135.720340231414));
#138395=CARTESIAN_POINT('Ctrl Pts',(-252.188485861668,0.281172171527148,
135.716335670313));
#138396=CARTESIAN_POINT('Ctrl Pts',(-252.195976197453,0.412590954282281,
135.707036272297));
#138397=CARTESIAN_POINT('Ctrl Pts',(-252.203466533239,0.543228007211834,
135.692518388616));
#138398=CARTESIAN_POINT('Ctrl Pts',(-252.211240867366,0.678818203424962,
135.677450054995));
#138399=CARTESIAN_POINT('Ctrl Pts',(-252.219015201493,0.813995730049785,
135.656711974421));
#138400=CARTESIAN_POINT('Ctrl Pts',(-252.226789535621,0.948248540112327,
135.630332827253));
#138401=CARTESIAN_POINT('Ctrl Pts',(-252.234554288576,1.08233589558552,
135.603986190027));
#138402=CARTESIAN_POINT('Ctrl Pts',(-252.242319041531,1.21550042207451,
135.572012393489));
#138403=CARTESIAN_POINT('Ctrl Pts',(-252.250083794487,1.34723456251655,
135.534491915539));
#138404=CARTESIAN_POINT('Ctrl Pts',(-252.25784083538,1.47883786275332,135.497008703456));
#138405=CARTESIAN_POINT('Ctrl Pts',(-252.265597876273,1.60901323058164,
135.453989879606));
#138406=CARTESIAN_POINT('Ctrl Pts',(-252.273354917166,1.73726303801028,
135.405567002772));
#138407=CARTESIAN_POINT('Ctrl Pts',(-252.281106108414,1.86541613126107,
135.357180642007));
#138408=CARTESIAN_POINT('Ctrl Pts',(-252.288857299663,1.99164619010694,
135.303398477313));
#138409=CARTESIAN_POINT('Ctrl Pts',(-252.296608490911,2.11547084694168,
135.244401851411));
#138410=CARTESIAN_POINT('Ctrl Pts',(-252.304356387696,2.23924287499403,
135.185430300648));
#138411=CARTESIAN_POINT('Ctrl Pts',(-252.312104284481,2.36061118221925,
135.12124886451));
#138412=CARTESIAN_POINT('Ctrl Pts',(-252.319852181266,2.47911369894876,
135.052086871715));
#138413=CARTESIAN_POINT('Ctrl Pts',(-252.327598457359,2.59759142750609,
134.982939346118));
#138414=CARTESIAN_POINT('Ctrl Pts',(-252.335344733451,2.71320422048017,
134.908813533058));
#138415=CARTESIAN_POINT('Ctrl Pts',(-252.343091009543,2.8255152842239,134.829984350743));
#138416=CARTESIAN_POINT('Ctrl Pts',(-252.350837342816,2.93782717702192,
134.751154586529));
#138417=CARTESIAN_POINT('Ctrl Pts',(-252.35858367609,3.04683697194792,134.667621608388));
#138418=CARTESIAN_POINT('Ctrl Pts',(-252.366330009363,3.15213783920438,
134.579703000073));
#138419=CARTESIAN_POINT('Ctrl Pts',(-252.374078077374,3.2574622878592,134.491764702997));
#138420=CARTESIAN_POINT('Ctrl Pts',(-252.381826145385,3.35907585601441,
134.399439071944));
#138421=CARTESIAN_POINT('Ctrl Pts',(-252.389574213396,3.45660601977891,
134.303082939576));
#138422=CARTESIAN_POINT('Ctrl Pts',(-252.397330516146,3.55423983976079,
134.206624398765));
#138423=CARTESIAN_POINT('Ctrl Pts',(-252.405086818896,3.64778130738623,
134.106127074771));
#138424=CARTESIAN_POINT('Ctrl Pts',(-252.412843121646,3.73689553725653,
134.001983923419));
#138425=CARTESIAN_POINT('Ctrl Pts',(-252.420603564168,3.82605733007419,
133.897785187731));
#138426=CARTESIAN_POINT('Ctrl Pts',(-252.42836400669,3.91078693534454,133.789937054624));
#138427=CARTESIAN_POINT('Ctrl Pts',(-252.436124449212,3.99079142810894,
133.678863503255));
#138428=CARTESIAN_POINT('Ctrl Pts',(-252.443897349485,4.07092435118573,
133.567611646763));
#138429=CARTESIAN_POINT('Ctrl Pts',(-252.451670249758,4.14631678902233,
133.453124351972));
#138430=CARTESIAN_POINT('Ctrl Pts',(-252.459443150031,4.21672014190244,
133.335853123455));
#138431=CARTESIAN_POINT('Ctrl Pts',(-252.466933485705,4.28456415470126,
133.222845000931));
#138432=CARTESIAN_POINT('Ctrl Pts',(-252.474423821378,4.34777536893473,
133.107252106937));
#138433=CARTESIAN_POINT('Ctrl Pts',(-252.481914157052,4.40617357946336,
132.989496185475));
#138434=CARTESIAN_POINT('Ctrl Pts',(-252.489688491162,4.46678597653833,
132.867275511159));
#138435=CARTESIAN_POINT('Ctrl Pts',(-252.497462825272,4.52240519695692,
132.742337390744));
#138436=CARTESIAN_POINT('Ctrl Pts',(-252.505237159382,4.57277859642071,
132.615128126281));
#138437=CARTESIAN_POINT('Ctrl Pts',(-252.51300191232,4.62308991517185,132.488075635867));
#138438=CARTESIAN_POINT('Ctrl Pts',(-252.520766665258,4.66816813384111,
132.358757930559));
#138439=CARTESIAN_POINT('Ctrl Pts',(-252.528531418196,4.70780661377364,
132.227645532757));
#138440=CARTESIAN_POINT('Ctrl Pts',(-252.536288459072,4.74740572420926,
132.096663357636));
#138441=CARTESIAN_POINT('Ctrl Pts',(-252.544045499948,4.78157573536534,
131.963890409119));
#138442=CARTESIAN_POINT('Ctrl Pts',(-252.551802540823,4.81015835128799,
131.829816466462));
#138443=CARTESIAN_POINT('Ctrl Pts',(-252.559553732055,4.83871941283779,
131.695843630007));
#138444=CARTESIAN_POINT('Ctrl Pts',(-252.567304923286,4.86170138468028,
131.560572133038));
#138445=CARTESIAN_POINT('Ctrl Pts',(-252.575056114517,4.87899610410646,
131.42450582525));
#138446=CARTESIAN_POINT('Ctrl Pts',(-252.582804011285,4.89628347281573,
131.288497349272));
#138447=CARTESIAN_POINT('Ctrl Pts',(-252.590551908053,4.90788834760884,
131.151695121396));
#138448=CARTESIAN_POINT('Ctrl Pts',(-252.598299804821,4.9137539092884,131.014611851695));
#138449=CARTESIAN_POINT('Ctrl Pts',(-252.606046080896,4.91961824401895,
130.877557256858));
#138450=CARTESIAN_POINT('Ctrl Pts',(-252.613792356972,4.91974563687403,
130.740222127488));
#138451=CARTESIAN_POINT('Ctrl Pts',(-252.621538633047,4.91413128669204,
130.603122550455));
#138452=CARTESIAN_POINT('Ctrl Pts',(-252.629284966303,4.90851689506614,
130.466021961383));
#138453=CARTESIAN_POINT('Ctrl Pts',(-252.63703129956,4.89716069182535,130.329157318756));
#138454=CARTESIAN_POINT('Ctrl Pts',(-252.644777632817,4.88010996773329,
130.19304256178));
#138455=CARTESIAN_POINT('Ctrl Pts',(-252.652525700811,4.86305542524957,
130.056897322845));
#138456=CARTESIAN_POINT('Ctrl Pts',(-252.660273768805,4.8403038729037,129.921502691585));
#138457=CARTESIAN_POINT('Ctrl Pts',(-252.668021836799,4.81195416585766,
129.787364959667));
#138458=CARTESIAN_POINT('Ctrl Pts',(-252.675778139533,4.783574328405,129.653084664569));
#138459=CARTESIAN_POINT('Ctrl Pts',(-252.683534442266,4.74958453188733,
129.520064320437));
#138460=CARTESIAN_POINT('Ctrl Pts',(-252.691290744999,4.71013436743116,
129.388798078063));
#138461=CARTESIAN_POINT('Ctrl Pts',(-252.699051187505,4.67066314723384,
129.257461774941));
#138462=CARTESIAN_POINT('Ctrl Pts',(-252.706811630011,4.62572588001987,
129.127881808272));
#138463=CARTESIAN_POINT('Ctrl Pts',(-252.714572072516,4.57552093836776,
129.000533795208));
#138464=CARTESIAN_POINT('Ctrl Pts',(-252.722344972774,4.52523540328487,
128.872981351804));
#138465=CARTESIAN_POINT('Ctrl Pts',(-252.730117873031,4.46966545428416,
128.747668379448));
#138466=CARTESIAN_POINT('Ctrl Pts',(-252.737890773288,4.40905658073008,
128.62504808137));
#138467=CARTESIAN_POINT('Ctrl Pts',(-252.745381109147,4.35065099157668,
128.506885338335));
#138468=CARTESIAN_POINT('Ctrl Pts',(-252.752871445006,4.28756661996266,
128.391223167946));
#138469=CARTESIAN_POINT('Ctrl Pts',(-252.760361780865,4.22006088580106,
128.278441144853));
#138470=CARTESIAN_POINT('Ctrl Pts',(-252.768136114974,4.14999565221084,
128.161382958746));
#138471=CARTESIAN_POINT('Ctrl Pts',(-252.775910449082,4.07494522030888,
128.047056827574));
#138472=CARTESIAN_POINT('Ctrl Pts',(-252.783684783191,3.99514851623755,
127.935916545302));
#138473=CARTESIAN_POINT('Ctrl Pts',(-252.791449536127,3.91545015447357,
127.824913233498));
#138474=CARTESIAN_POINT('Ctrl Pts',(-252.799214289064,3.83101738484741,
127.717088273015));
#138475=CARTESIAN_POINT('Ctrl Pts',(-252.806979042001,3.74213437793858,
127.612869843656));
#138476=CARTESIAN_POINT('Ctrl Pts',(-252.814736082875,3.65333965088656,
127.508754925513));
#138477=CARTESIAN_POINT('Ctrl Pts',(-252.822493123749,3.56010373468657,
127.408239705586));
#138478=CARTESIAN_POINT('Ctrl Pts',(-252.830250164624,3.46275313166815,
127.311722100396));
#138479=CARTESIAN_POINT('Ctrl Pts',(-252.838001355853,3.36547594149777,
127.215277279883));
#138480=CARTESIAN_POINT('Ctrl Pts',(-252.845752547083,3.26409051719386,
127.122824347816));
#138481=CARTESIAN_POINT('Ctrl Pts',(-252.853503738312,3.15896229718796,
127.03472664761));
#138482=CARTESIAN_POINT('Ctrl Pts',(-252.861251635079,3.05387875948159,
126.946666391279));
#138483=CARTESIAN_POINT('Ctrl Pts',(-252.868999531845,2.94505588906063,
126.862957935722));
#138484=CARTESIAN_POINT('Ctrl Pts',(-252.876747428611,2.83289433126341,
126.783926216858));
#138485=CARTESIAN_POINT('Ctrl Pts',(-252.884493704684,2.72075623524711,
126.704911029726));
#138486=CARTESIAN_POINT('Ctrl Pts',(-252.892239980758,2.60528116036644,
126.630570858501));
#138487=CARTESIAN_POINT('Ctrl Pts',(-252.899986256831,2.48690070997629,
126.561188700094));
#138488=CARTESIAN_POINT('Ctrl Pts',(-252.907732590086,2.36851938572904,
126.491806029525));
#138489=CARTESIAN_POINT('Ctrl Pts',(-252.91547892334,2.24723298047813,126.427381642497));
#138490=CARTESIAN_POINT('Ctrl Pts',(-252.923225256594,2.12349944764491,
126.368153548644));
#138491=CARTESIAN_POINT('Ctrl Pts',(-252.930973324587,1.99973820554539,
126.308912191071));
#138492=CARTESIAN_POINT('Ctrl Pts',(-252.938721392579,1.87352909795146,
126.254869611021));
#138493=CARTESIAN_POINT('Ctrl Pts',(-252.946469460571,1.74535151601177,
126.20621630186));
#138494=CARTESIAN_POINT('Ctrl Pts',(-252.954225763302,1.61703770541265,
126.157511283384));
#138495=CARTESIAN_POINT('Ctrl Pts',(-252.961982066033,1.48675160733874,
126.114207116621));
#138496=CARTESIAN_POINT('Ctrl Pts',(-252.969738368763,1.35498982250258,
126.076445046893));
#138497=CARTESIAN_POINT('Ctrl Pts',(-252.977498811267,1.22315771243448,
126.038662822411));
#138498=CARTESIAN_POINT('Ctrl Pts',(-252.98525925377,1.08984872603554,126.006428680841));
#138499=CARTESIAN_POINT('Ctrl Pts',(-252.993019696273,0.955570238710946,
125.979832808403));
#138500=CARTESIAN_POINT('Ctrl Pts',(-253.000792596528,0.821076195636046,
125.953194241909));
#138501=CARTESIAN_POINT('Ctrl Pts',(-253.008565496782,0.685609928174875,
125.932212091306));
#138502=CARTESIAN_POINT('Ctrl Pts',(-253.016338397037,0.549685422037678,
125.916924786857));
#138503=CARTESIAN_POINT('Ctrl Pts',(-253.023828732917,0.41870211182428,
125.902193214178));
#138504=CARTESIAN_POINT('Ctrl Pts',(-253.031319068797,0.287293607987546,
125.892749654319));
#138505=CARTESIAN_POINT('Ctrl Pts',(-253.038809404677,0.155918399185276,
125.888582701987));
#138506=CARTESIAN_POINT('Ctrl Pts',(-253.04658373885,0.0195620606171169,
125.884257758429));
#138507=CARTESIAN_POINT('Ctrl Pts',(-253.054358073023,-0.11719034419708,
125.885603745921));
#138508=CARTESIAN_POINT('Ctrl Pts',(-253.062132407196,-0.253827880118555,
125.892664935851));
#138509=CARTESIAN_POINT('Ctrl Pts',(-253.069897160197,-0.390297022492045,
125.899717423496));
#138510=CARTESIAN_POINT('Ctrl Pts',(-253.077661913198,-0.526651190950291,
125.912471079177));
#138511=CARTESIAN_POINT('Ctrl Pts',(-253.085426666199,-0.662376544551844,
125.930918263775));
#138512=CARTESIAN_POINT('Ctrl Pts',(-253.093183707138,-0.797967093821589,
125.949347126369));
#138513=CARTESIAN_POINT('Ctrl Pts',(-253.100940748077,-0.932929686216431,
125.973458212074));
#138514=CARTESIAN_POINT('Ctrl Pts',(-253.108697789016,-1.06675306080651,
126.003191908829));
#138515=CARTESIAN_POINT('Ctrl Pts',(-253.11644898031,-1.20047551814897,
126.032903183171));
#138516=CARTESIAN_POINT('Ctrl Pts',(-253.124200171604,-1.33306008754539,
126.068228544534));
#138517=CARTESIAN_POINT('Ctrl Pts',(-253.131951362898,-1.46400354948286,
126.109056935204));
#138518=CARTESIAN_POINT('Ctrl Pts',(-253.139699259729,-1.59489135695368,
126.149867972718));
#138519=CARTESIAN_POINT('Ctrl Pts',(-253.14744715656,-1.72413907180751,
126.196177271443));
#138520=CARTESIAN_POINT('Ctrl Pts',(-253.155195053391,-1.85125675765714,
126.247823392904));
#138521=CARTESIAN_POINT('Ctrl Pts',(-253.162941329529,-1.97834785322533,
126.299458711109));
#138522=CARTESIAN_POINT('Ctrl Pts',(-253.170687605667,-2.10330944404284,
126.356428484504));
#138523=CARTESIAN_POINT('Ctrl Pts',(-253.178433881805,-2.22567014463019,
126.418522559703));
#138524=CARTESIAN_POINT('Ctrl Pts',(-253.186180215124,-2.3480317484546,
126.480617093265));
#138525=CARTESIAN_POINT('Ctrl Pts',(-253.193926548443,-2.46779207509605,
126.547835827185));
#138526=CARTESIAN_POINT('Ctrl Pts',(-253.201672881761,-2.58450334529135,
126.619922122298));
#138527=CARTESIAN_POINT('Ctrl Pts',(-253.209420949818,-2.70124075216193,
126.692024560635));
#138528=CARTESIAN_POINT('Ctrl Pts',(-253.217169017874,-2.81492741129484,
126.76899652384));
#138529=CARTESIAN_POINT('Ctrl Pts',(-253.22491708593,-2.92514393259481,
126.850537652877));
#138530=CARTESIAN_POINT('Ctrl Pts',(-253.232673388725,-3.03547759331555,
126.932165444789));
#138531=CARTESIAN_POINT('Ctrl Pts',(-253.24042969152,-3.14233343401797,
127.018371870343));
#138532=CARTESIAN_POINT('Ctrl Pts',(-253.248185994314,-3.24532419619202,
127.108815471838));
#138533=CARTESIAN_POINT('Ctrl Pts',(-253.255946436881,-3.34836992763311,
127.199307345804));
#138534=CARTESIAN_POINT('Ctrl Pts',(-253.263706879447,-3.44754618744979,
127.294040632039));
#138535=CARTESIAN_POINT('Ctrl Pts',(-253.271467322014,-3.54250285061481,
127.392637209098));
#138536=CARTESIAN_POINT('Ctrl Pts',(-253.279240222331,-3.63761194663223,
127.491392062122));
#138537=CARTESIAN_POINT('Ctrl Pts',(-253.287013122648,-3.72848765071348,
127.594022306059));
#138538=CARTESIAN_POINT('Ctrl Pts',(-253.294786022964,-3.81481980855446,
127.700116282666));
#138539=CARTESIAN_POINT('Ctrl Pts',(-253.30227635814,-3.8980135679346,127.802353467305));
#138540=CARTESIAN_POINT('Ctrl Pts',(-253.309766693315,-3.97698820068931,
127.90780667886));
#138541=CARTESIAN_POINT('Ctrl Pts',(-253.317257028491,-4.0515054781619,
128.016084013116));
#138542=CARTESIAN_POINT('Ctrl Pts',(-253.325430147582,-4.13281540206915,
128.134231402659));
#138543=CARTESIAN_POINT('Ctrl Pts',(-253.333603266674,-4.20908046165086,
128.256123151092));
#138544=CARTESIAN_POINT('Ctrl Pts',(-253.341776385765,-4.27994506192049,
128.381293691243));
#138545=CARTESIAN_POINT('Ctrl Pts',(-253.349647985341,-4.34819535304647,
128.501846488735));
#138546=CARTESIAN_POINT('Ctrl Pts',(-253.357519584916,-4.41143630189487,
128.625440112942));
#138547=CARTESIAN_POINT('Ctrl Pts',(-253.365391184492,-4.46939190082812,
128.751626075714));
#138548=CARTESIAN_POINT('Ctrl Pts',(-253.373254756906,-4.52728839882145,
128.877683358788));
#138549=CARTESIAN_POINT('Ctrl Pts',(-253.381118329321,-4.57991011563706,
129.006327380166));
#138550=CARTESIAN_POINT('Ctrl Pts',(-253.388981901735,-4.62702611600136,
129.137083680659));
#138551=CARTESIAN_POINT('Ctrl Pts',(-253.396837413988,-4.67409382246811,
129.267705955952));
#138552=CARTESIAN_POINT('Ctrl Pts',(-253.404692926241,-4.71566692654559,
129.400435844763));
#138553=CARTESIAN_POINT('Ctrl Pts',(-253.412548438494,-4.75156215372704,
129.53477794528));
#138554=CARTESIAN_POINT('Ctrl Pts',(-253.413477111525,-4.75580566177188,
129.550659772171));
#138555=CARTESIAN_POINT('Ctrl Pts',(-253.414405784557,-4.75996987254124,
129.566564108755));
#138556=CARTESIAN_POINT('Ctrl Pts',(-253.415334457588,-4.76405452823403,
129.582490119308));
#138557=CARTESIAN_POINT('Ctrl Pts',(-251.665320902482,-4.76405452823413,
129.582490119309));
#138558=CARTESIAN_POINT('Ctrl Pts',(-251.674572419706,-4.80443247690585,
129.739923128359));
#138559=CARTESIAN_POINT('Ctrl Pts',(-251.683823936931,-4.83704222570981,
129.899513529989));
#138560=CARTESIAN_POINT('Ctrl Pts',(-251.693075454155,-4.86168099319561,
130.06055890817));
#138561=CARTESIAN_POINT('Ctrl Pts',(-251.702232760127,-4.88606885598187,
130.219964308124));
#138562=CARTESIAN_POINT('Ctrl Pts',(-251.711390066099,-4.9026471949439,
130.380795143411));
#138563=CARTESIAN_POINT('Ctrl Pts',(-251.720547372071,-4.91126596260942,
130.542349726544));
#138564=CARTESIAN_POINT('Ctrl Pts',(-251.725411769369,-4.91584428622076,
130.62816816268));
#138565=CARTESIAN_POINT('Ctrl Pts',(-251.730276166667,-4.918177390908,130.714190481682));
#138566=CARTESIAN_POINT('Ctrl Pts',(-251.735140563966,-4.91824833132153,
130.800309203871));
#138567=CARTESIAN_POINT('',(-251.389859436039,-4.91824999430341,130.804123901556));
#138568=CARTESIAN_POINT('Ctrl Pts',(-251.319768125496,-4.76405452823393,
129.582490119308));
#138569=CARTESIAN_POINT('Ctrl Pts',(-251.327528806674,-4.79812330926081,
129.715323779466));
#138570=CARTESIAN_POINT('Ctrl Pts',(-251.335289487853,-4.82660485264554,
129.849476320883));
#138571=CARTESIAN_POINT('Ctrl Pts',(-251.343050169032,-4.84942367805967,
129.984438027821));
#138572=CARTESIAN_POINT('Ctrl Pts',(-251.350823197439,-4.87227880818138,
130.119614458576));
#138573=CARTESIAN_POINT('Ctrl Pts',(-251.358596225847,-4.88945316897587,
130.255602239287));
#138574=CARTESIAN_POINT('Ctrl Pts',(-251.366369254255,-4.90092320301354,
130.391886593337));
#138575=CARTESIAN_POINT('Ctrl Pts',(-251.373483722157,-4.91142145217891,
130.516624419002));
#138576=CARTESIAN_POINT('Ctrl Pts',(-251.380598190058,-4.9171416332976,
130.6416104416));
#138577=CARTESIAN_POINT('Ctrl Pts',(-251.38771265796,-4.91810390465499,
130.766452234359));
#138578=CARTESIAN_POINT('Ctrl Pts',(-251.388428250639,-4.91820069254526,
130.779009164009));
#138579=CARTESIAN_POINT('Ctrl Pts',(-251.389143843318,-4.91824938991048,
130.791566464814));
#138580=CARTESIAN_POINT('Ctrl Pts',(-251.389859435997,-4.91824999430338,
130.804123900822));
#138581=CARTESIAN_POINT('Ctrl Pts',(-251.389859436039,-4.91824999430341,
130.804123901557));
#138582=CARTESIAN_POINT('Ctrl Pts',(-251.397623097505,-4.91825655150756,
130.940362972942));
#138583=CARTESIAN_POINT('Ctrl Pts',(-251.405386758971,-4.9125979373634,
131.076820927194));
#138584=CARTESIAN_POINT('Ctrl Pts',(-251.413150420438,-4.90124551686362,
131.212986908845));
#138585=CARTESIAN_POINT('Ctrl Pts',(-251.420904513053,-4.88990708842368,
131.348985063505));
#138586=CARTESIAN_POINT('Ctrl Pts',(-251.428658605669,-4.87288884830977,
131.484691574514));
#138587=CARTESIAN_POINT('Ctrl Pts',(-251.436412698285,-4.85021413697419,
131.619594257694));
#138588=CARTESIAN_POINT('Ctrl Pts',(-251.444159102514,-4.82756190821258,
131.754363181307));
#138589=CARTESIAN_POINT('Ctrl Pts',(-251.451905506742,-4.79926443348876,
131.888329478876));
#138590=CARTESIAN_POINT('Ctrl Pts',(-251.459651910971,-4.76539692333789,
132.020985138748));
#138591=CARTESIAN_POINT('Ctrl Pts',(-251.467392500501,-4.73155483522072,
132.15354122305));
#138592=CARTESIAN_POINT('Ctrl Pts',(-251.475133090031,-4.69215113002352,
132.284788249317));
#138593=CARTESIAN_POINT('Ctrl Pts',(-251.482873679562,-4.64731219075221,
132.414227836993));
#138594=CARTESIAN_POINT('Ctrl Pts',(-251.490611030979,-4.60249200890738,
132.543613276342));
#138595=CARTESIAN_POINT('Ctrl Pts',(-251.498348382397,-4.55224124296833,
132.671192411002));
#138596=CARTESIAN_POINT('Ctrl Pts',(-251.506085733815,-4.49673621749552,
132.796481711467));
#138597=CARTESIAN_POINT('Ctrl Pts',(-251.513821517098,-4.44124244126378,
132.921745619465));
#138598=CARTESIAN_POINT('Ctrl Pts',(-251.521557300381,-4.38049668226015,
133.044720257957));
#138599=CARTESIAN_POINT('Ctrl Pts',(-251.529293083665,-4.31472336921529,
133.16494217931));
#138600=CARTESIAN_POINT('Ctrl Pts',(-251.537028986808,-4.2489490370617,
133.285165963414));
#138601=CARTESIAN_POINT('Ctrl Pts',(-251.544764889952,-4.1781471839442,
133.402636601372));
#138602=CARTESIAN_POINT('Ctrl Pts',(-251.552500793096,-4.10258794636578,
133.516915723888));
#138603=CARTESIAN_POINT('Ctrl Pts',(-251.560238503824,-4.02701105348838,
133.631221549056));
#138604=CARTESIAN_POINT('Ctrl Pts',(-251.567976214551,-3.94667478058135,
133.742334047912));
#138605=CARTESIAN_POINT('Ctrl Pts',(-251.575713925279,-3.86189204456478,
133.849844634701));
#138606=CARTESIAN_POINT('Ctrl Pts',(-251.583459876721,-3.77701901436072,
133.957469720993));
#138607=CARTESIAN_POINT('Ctrl Pts',(-251.591205828163,-3.68769030538339,
134.061484924554));
#138608=CARTESIAN_POINT('Ctrl Pts',(-251.598951779605,-3.59425885152675,
134.161515122608));
#138609=CARTESIAN_POINT('Ctrl Pts',(-251.606701955618,-3.50077644102186,
134.261599876203));
#138610=CARTESIAN_POINT('Ctrl Pts',(-251.61445213163,-3.40318710676369,
134.35769501918));
#138611=CARTESIAN_POINT('Ctrl Pts',(-251.622202307642,-3.3018792005806,
134.449463744677));
#138612=CARTESIAN_POINT('Ctrl Pts',(-251.629964748407,-3.20041097334431,
134.541377695352));
#138613=CARTESIAN_POINT('Ctrl Pts',(-251.637727189171,-3.09521271771393,
134.628951297797));
#138614=CARTESIAN_POINT('Ctrl Pts',(-251.645489629936,-2.98670492236545,
134.711888834894));
#138615=CARTESIAN_POINT('Ctrl Pts',(-251.652379847215,-2.89038956111025,
134.78550712952));
#138616=CARTESIAN_POINT('Ctrl Pts',(-251.659270064494,-2.79146721128591,
134.855473202726));
#138617=CARTESIAN_POINT('Ctrl Pts',(-251.666160281774,-2.6902486882225,
134.921610313421));
#138618=CARTESIAN_POINT('Ctrl Pts',(-251.673934615893,-2.57604233080481,
134.996233794124));
#138619=CARTESIAN_POINT('Ctrl Pts',(-251.681708950011,-2.45854780978557,
135.066220001201));
#138620=CARTESIAN_POINT('Ctrl Pts',(-251.68948328413,-2.33817846390311,
135.131265346519));
#138621=CARTESIAN_POINT('Ctrl Pts',(-251.697248037077,-2.21795746248174,
135.196230529263));
#138622=CARTESIAN_POINT('Ctrl Pts',(-251.705012790023,-2.09486902629651,
135.2562667818));
#138623=CARTESIAN_POINT('Ctrl Pts',(-251.71277754297,-1.96935597857399,
135.311113339));
#138624=CARTESIAN_POINT('Ctrl Pts',(-251.720534583855,-1.84396759218024,
135.365905421826));
#138625=CARTESIAN_POINT('Ctrl Pts',(-251.728291624739,-1.71615974252891,
135.415517911423));
#138626=CARTESIAN_POINT('Ctrl Pts',(-251.736048665624,-1.58640008461407,
135.459735772592));
#138627=CARTESIAN_POINT('Ctrl Pts',(-251.743799856864,-1.45673827946648,
135.503920288729));
#138628=CARTESIAN_POINT('Ctrl Pts',(-251.751551048103,-1.32512796430206,
135.542718148208));
#138629=CARTESIAN_POINT('Ctrl Pts',(-251.759302239343,-1.19205668724417,
135.575962436337));
#138630=CARTESIAN_POINT('Ctrl Pts',(-251.76705013612,-1.05904196902864,
135.609192594756));
#138631=CARTESIAN_POINT('Ctrl Pts',(-251.774798032897,-0.924567902451036,
135.636873781949));
#138632=CARTESIAN_POINT('Ctrl Pts',(-251.782545929673,-0.789136898110652,
135.658889020876));
#138633=CARTESIAN_POINT('Ctrl Pts',(-251.790292205757,-0.653734223016822,
135.680899654689));
#138634=CARTESIAN_POINT('Ctrl Pts',(-251.798038481841,-0.517375393966117,
135.69724663496));
#138635=CARTESIAN_POINT('Ctrl Pts',(-251.805784757924,-0.380572318507233,
135.707864239762));
#138636=CARTESIAN_POINT('Ctrl Pts',(-251.813531091189,-0.243768233198938,
135.718481922941));
#138637=CARTESIAN_POINT('Ctrl Pts',(-251.821277424454,-0.106520284731784,
135.723370116005));
#138638=CARTESIAN_POINT('Ctrl Pts',(-251.829023757719,0.030655599466925,
135.722515078004));
#138639=CARTESIAN_POINT('Ctrl Pts',(-251.836771825722,0.167862203253604,
135.721659848522));
#138640=CARTESIAN_POINT('Ctrl Pts',(-251.844519893725,0.304996319775712,
135.715058831107));
#138641=CARTESIAN_POINT('Ctrl Pts',(-251.852267961727,0.441543525409281,
135.702750391529));
#138642=CARTESIAN_POINT('Ctrl Pts',(-251.860024264469,0.578235855037751,
135.690428870396));
#138643=CARTESIAN_POINT('Ctrl Pts',(-251.86778056721,0.714339637710827,
135.672387844934));
#138644=CARTESIAN_POINT('Ctrl Pts',(-251.875536869952,0.849346513343336,
135.648717495705));
#138645=CARTESIAN_POINT('Ctrl Pts',(-251.883297312465,0.98442544621072,
135.625034512898));
#138646=CARTESIAN_POINT('Ctrl Pts',(-251.891057754979,1.11840592373312,
135.595716303058));
#138647=CARTESIAN_POINT('Ctrl Pts',(-251.898818197493,1.25079222822346,
135.560903675746));
#138648=CARTESIAN_POINT('Ctrl Pts',(-251.906591097758,1.38339105096212,
135.526035164113));
#138649=CARTESIAN_POINT('Ctrl Pts',(-251.914363998023,1.51439021292255,
135.485654724819));
#138650=CARTESIAN_POINT('Ctrl Pts',(-251.922136898288,1.64331068855447,
135.439952601702));
#138651=CARTESIAN_POINT('Ctrl Pts',(-251.929627234054,1.76754458023938,
135.395911865851));
#138652=CARTESIAN_POINT('Ctrl Pts',(-251.93711756982,1.88984800676703,135.346929756531));
#138653=CARTESIAN_POINT('Ctrl Pts',(-251.944607905586,2.0098136467306,135.293217060795));
#138654=CARTESIAN_POINT('Ctrl Pts',(-251.952382239706,2.13432782034755,
135.237467831896));
#138655=CARTESIAN_POINT('Ctrl Pts',(-251.960156573827,2.25671785707082,
135.176445618165));
#138656=CARTESIAN_POINT('Ctrl Pts',(-251.967930907947,2.37650491992359,
135.110334076388));
#138657=CARTESIAN_POINT('Ctrl Pts',(-251.975695660895,2.49614435592709,
135.044304011178));
#138658=CARTESIAN_POINT('Ctrl Pts',(-251.983460413844,2.61318686188228,
134.973197284716));
#138659=CARTESIAN_POINT('Ctrl Pts',(-251.991225166792,2.72717369192919,
134.897245506804));
#138660=CARTESIAN_POINT('Ctrl Pts',(-251.998982207678,2.84104730864958,
134.821369165267));
#138661=CARTESIAN_POINT('Ctrl Pts',(-252.006739248564,2.95187096588072,
134.740657564109));
#138662=CARTESIAN_POINT('Ctrl Pts',(-252.01449628945,3.059210969472,134.655387922943));
#138663=CARTESIAN_POINT('Ctrl Pts',(-252.022247480692,3.16647002713174,
134.570182584277));
#138664=CARTESIAN_POINT('Ctrl Pts',(-252.029998671933,3.27025035524586,
134.480426289448));
#138665=CARTESIAN_POINT('Ctrl Pts',(-252.037749863174,3.37014799208426,
134.386439005032));
#138666=CARTESIAN_POINT('Ctrl Pts',(-252.045497759952,3.47000316976201,
134.292491667719));
#138667=CARTESIAN_POINT('Ctrl Pts',(-252.053245656731,3.56597865422714,
134.194317184808));
#138668=CARTESIAN_POINT('Ctrl Pts',(-252.060993553509,3.65770446418048,
134.092275019617));
#138669=CARTESIAN_POINT('Ctrl Pts',(-252.068739829594,3.74941108707175,
133.990254199447));
#138670=CARTESIAN_POINT('Ctrl Pts',(-252.076486105679,3.83686954240243,
133.884367596792));
#138671=CARTESIAN_POINT('Ctrl Pts',(-252.084232381765,3.91974783791985,
133.775010369661));
#138672=CARTESIAN_POINT('Ctrl Pts',(-252.091978715031,4.0026267452259,133.665652335281));
#138673=CARTESIAN_POINT('Ctrl Pts',(-252.099725048298,4.08092518910878,
133.552823936896));
#138674=CARTESIAN_POINT('Ctrl Pts',(-252.107471381564,4.15435273753924,
133.436951811542));
#138675=CARTESIAN_POINT('Ctrl Pts',(-252.115219449568,4.22779672955995,
133.32105373743));
#138676=CARTESIAN_POINT('Ctrl Pts',(-252.122967517572,4.2963674463242,133.202110910179));
#138677=CARTESIAN_POINT('Ctrl Pts',(-252.130715585577,4.35981910750697,
133.080576866589));
#138678=CARTESIAN_POINT('Ctrl Pts',(-252.13847188832,4.42333820587024,132.958913655172));
#138679=CARTESIAN_POINT('Ctrl Pts',(-252.146228191063,4.48172719924991,
132.834654073181));
#138680=CARTESIAN_POINT('Ctrl Pts',(-252.153984493806,4.53478717806245,
132.708274563148));
#138681=CARTESIAN_POINT('Ctrl Pts',(-252.161744936321,4.58787547658327,
132.581827600565));
#138682=CARTESIAN_POINT('Ctrl Pts',(-252.169505378836,4.63562895705639,
132.453258821715));
#138683=CARTESIAN_POINT('Ctrl Pts',(-252.177265821352,4.67789813903392,
132.323061398932));
#138684=CARTESIAN_POINT('Ctrl Pts',(-252.185038721618,4.72023517525472,
132.192654971689));
#138685=CARTESIAN_POINT('Ctrl Pts',(-252.192811621885,4.75707021490048,
132.060615052825));
#138686=CARTESIAN_POINT('Ctrl Pts',(-252.200584522151,4.78830439049094,
131.927447491546));
#138687=CARTESIAN_POINT('Ctrl Pts',(-252.208074857901,4.81840312506873,
131.799120906785));
#138688=CARTESIAN_POINT('Ctrl Pts',(-252.21556519365,4.84330107865172,131.66974754398));
#138689=CARTESIAN_POINT('Ctrl Pts',(-252.223055529399,4.86295542518781,
131.539784029715));
#138690=CARTESIAN_POINT('Ctrl Pts',(-252.230829863517,4.88335497227861,
131.404892909092));
#138691=CARTESIAN_POINT('Ctrl Pts',(-252.238604197635,4.89817006001821,
131.268938707896));
#138692=CARTESIAN_POINT('Ctrl Pts',(-252.246378531753,4.90729638098068,
131.132423556213));
#138693=CARTESIAN_POINT('Ctrl Pts',(-252.254143284699,4.91641145456825,
130.996076647254));
#138694=CARTESIAN_POINT('Ctrl Pts',(-252.261908037645,4.919851685145,130.859170549683));
#138695=CARTESIAN_POINT('Ctrl Pts',(-252.269672790591,4.91756396925203,
130.722216410137));
#138696=CARTESIAN_POINT('Ctrl Pts',(-252.277429831475,4.91527852555074,
130.585398295373));
#138697=CARTESIAN_POINT('Ctrl Pts',(-252.285186872359,4.90727646338769,
130.448532621974));
#138698=CARTESIAN_POINT('Ctrl Pts',(-252.292943913243,4.8935565931931,130.312134113082));
#138699=CARTESIAN_POINT('Ctrl Pts',(-252.300695104482,4.87984706925933,
130.175838463367));
#138700=CARTESIAN_POINT('Ctrl Pts',(-252.308446295721,4.86042835872714,
130.040009664371));
#138701=CARTESIAN_POINT('Ctrl Pts',(-252.31619748696,4.83535130735511,129.905160530289));
#138702=CARTESIAN_POINT('Ctrl Pts',(-252.323945383736,4.81028491439884,
129.770368710685));
#138703=CARTESIAN_POINT('Ctrl Pts',(-252.331693280512,4.77956503518677,
129.63655611141));
#138704=CARTESIAN_POINT('Ctrl Pts',(-252.339441177288,4.74329411245932,
129.504228306911));
#138705=CARTESIAN_POINT('Ctrl Pts',(-252.347187453371,4.70703077682679,
129.371928182536));
#138706=CARTESIAN_POINT('Ctrl Pts',(-252.354933729454,4.6652188105726,129.241112611982));
#138707=CARTESIAN_POINT('Ctrl Pts',(-252.362680005537,4.61801122140165,
129.11227450229));
#138708=CARTESIAN_POINT('Ctrl Pts',(-252.370426338802,4.57080328375507,
128.983435441546));
#138709=CARTESIAN_POINT('Ctrl Pts',(-252.378172672066,4.5181997782239,128.85657423789));
#138710=CARTESIAN_POINT('Ctrl Pts',(-252.38591900533,4.46040266102354,128.732165847755));
#138711=CARTESIAN_POINT('Ctrl Pts',(-252.393667073332,4.40259260055961,
128.607729597223));
#138712=CARTESIAN_POINT('Ctrl Pts',(-252.401415141334,4.33958677873817,
128.485747607737));
#138713=CARTESIAN_POINT('Ctrl Pts',(-252.409163209336,4.27163391864493,
128.366671808964));
#138714=CARTESIAN_POINT('Ctrl Pts',(-252.416919512077,4.20360883744303,
128.247469455015));
#138715=CARTESIAN_POINT('Ctrl Pts',(-252.424675814818,4.13062640909264,
128.131179801964));
#138716=CARTESIAN_POINT('Ctrl Pts',(-252.432432117559,4.05297996270192,
128.018227726903));
#138717=CARTESIAN_POINT('Ctrl Pts',(-252.440192560072,3.97529207406466,
127.905215365918));
#138718=CARTESIAN_POINT('Ctrl Pts',(-252.447953002585,3.89293544184546,
127.795544444923));
#138719=CARTESIAN_POINT('Ctrl Pts',(-252.455713445098,3.80624418806478,
127.689607297747));
#138720=CARTESIAN_POINT('Ctrl Pts',(-252.463486345363,3.71941376978695,
127.583500090857));
#138721=CARTESIAN_POINT('Ctrl Pts',(-252.471259245627,3.62823508520527,
127.481138927387));
#138722=CARTESIAN_POINT('Ctrl Pts',(-252.479032145892,3.533080279294,127.382880411199));
#138723=CARTESIAN_POINT('Ctrl Pts',(-252.486522481665,3.44138459010734,
127.288193839416));
#138724=CARTESIAN_POINT('Ctrl Pts',(-252.494012817439,3.34599706771789,
127.197317022901));
#138725=CARTESIAN_POINT('Ctrl Pts',(-252.501503153212,3.24727873647887,
127.110532810248));
#138726=CARTESIAN_POINT('Ctrl Pts',(-252.509277487329,3.14481746988947,
127.020458147957));
#138727=CARTESIAN_POINT('Ctrl Pts',(-252.517051821446,3.03844326681808,
126.934507228457));
#138728=CARTESIAN_POINT('Ctrl Pts',(-252.524826155563,2.92852220281797,
126.853039222121));
#138729=CARTESIAN_POINT('Ctrl Pts',(-252.532590908508,2.81873660670535,
126.771671617821));
#138730=CARTESIAN_POINT('Ctrl Pts',(-252.540355661453,2.70541315811351,
126.694776164561));
#138731=CARTESIAN_POINT('Ctrl Pts',(-252.548120414398,2.58895319546871,
126.622673827027));
#138732=CARTESIAN_POINT('Ctrl Pts',(-252.555877455281,2.47260890250127,
126.550643102551));
#138733=CARTESIAN_POINT('Ctrl Pts',(-252.563634496164,2.35313462519186,
126.483396224484));
#138734=CARTESIAN_POINT('Ctrl Pts',(-252.571391537047,2.2309627717077,126.421212414076));
#138735=CARTESIAN_POINT('Ctrl Pts',(-252.579142728285,2.10888304896848,
126.359075496964));
#138736=CARTESIAN_POINT('Ctrl Pts',(-252.586893919523,1.98411014615064,
126.301994224445));
#138737=CARTESIAN_POINT('Ctrl Pts',(-252.594645110761,1.85710299173296,
126.250203007141));
#138738=CARTESIAN_POINT('Ctrl Pts',(-252.602393007536,1.73014981874447,
126.198433802485));
#138739=CARTESIAN_POINT('Ctrl Pts',(-252.610140904311,1.6009646441356,126.151950328436));
#138740=CARTESIAN_POINT('Ctrl Pts',(-252.617888801086,1.47002819481218,
126.110939672354));
#138741=CARTESIAN_POINT('Ctrl Pts',(-252.625635077168,1.33911913457094,
126.069937594816));
#138742=CARTESIAN_POINT('Ctrl Pts',(-252.63338135325,1.20645990112001,126.034406174967));
#138743=CARTESIAN_POINT('Ctrl Pts',(-252.641127629332,1.0725478955156,126.004483111387));
#138744=CARTESIAN_POINT('Ctrl Pts',(-252.648873962595,0.938634901403728,
125.974559826921));
#138745=CARTESIAN_POINT('Ctrl Pts',(-252.656620295858,0.803469498240778,
125.950245066594));
#138746=CARTESIAN_POINT('Ctrl Pts',(-252.664366629121,0.667560442590652,
125.931625644475));
#138747=CARTESIAN_POINT('Ctrl Pts',(-252.672114697122,0.531620951049647,
125.913002052664));
#138748=CARTESIAN_POINT('Ctrl Pts',(-252.679862765123,0.394937862907427,
125.900076390078));
#138749=CARTESIAN_POINT('Ctrl Pts',(-252.687610833124,0.258025840295146,
125.892883677964));
#138750=CARTESIAN_POINT('Ctrl Pts',(-252.695367135864,0.120968305955731,
125.88568332135));
#138751=CARTESIAN_POINT('Ctrl Pts',(-252.703123438603,-0.0163182578508794,
125.884228107272));
#138752=CARTESIAN_POINT('Ctrl Pts',(-252.710879741343,-0.153317838445549,
125.88850090609));
#138753=CARTESIAN_POINT('Ctrl Pts',(-252.718640183855,-0.290390539841379,
125.892775985429));
#138754=CARTESIAN_POINT('Ctrl Pts',(-252.726400626367,-0.427175563086022,
125.902785140902));
#138755=CARTESIAN_POINT('Ctrl Pts',(-252.734161068879,-0.563162225504971,
125.918459332208));
#138756=CARTESIAN_POINT('Ctrl Pts',(-252.741933969142,-0.699367185787194,
125.934158685117));
#138757=CARTESIAN_POINT('Ctrl Pts',(-252.749706869406,-0.8347708377973,
125.955541185586));
#138758=CARTESIAN_POINT('Ctrl Pts',(-252.757479769669,-0.968872007157794,
125.982486490606));
#138759=CARTESIAN_POINT('Ctrl Pts',(-252.764970105454,-1.098098261668,126.008452266005));
#138760=CARTESIAN_POINT('Ctrl Pts',(-252.77246044124,-1.2261147871949,126.039583351033));
#138761=CARTESIAN_POINT('Ctrl Pts',(-252.779950777025,-1.35248847272114,
126.075728892251));
#138762=CARTESIAN_POINT('Ctrl Pts',(-252.787725111152,-1.48365365467449,
126.113244902573));
#138763=CARTESIAN_POINT('Ctrl Pts',(-252.79549944528,-1.61346445276583,
126.156281960898));
#138764=CARTESIAN_POINT('Ctrl Pts',(-252.803273779407,-1.74142081401129,
126.204726217852));
#138765=CARTESIAN_POINT('Ctrl Pts',(-252.811038532362,-1.86921948047746,
126.25311077159));
#138766=CARTESIAN_POINT('Ctrl Pts',(-252.818803285317,-1.99516789529014,
126.306889127703));
#138767=CARTESIAN_POINT('Ctrl Pts',(-252.826568038273,-2.11877908854417,
126.36589711806));
#138768=CARTESIAN_POINT('Ctrl Pts',(-252.834325079166,-2.2422675094189,
126.424846500849));
#138769=CARTESIAN_POINT('Ctrl Pts',(-252.842082120059,-2.36342297780638,
126.489015013957));
#138770=CARTESIAN_POINT('Ctrl Pts',(-252.849839160952,-2.48177684978281,
126.558189786054));
#138771=CARTESIAN_POINT('Ctrl Pts',(-252.8575903522,-2.60004147018366,126.627312392917));
#138772=CARTESIAN_POINT('Ctrl Pts',(-252.865341543449,-2.71550836321191,
126.701433547859));
#138773=CARTESIAN_POINT('Ctrl Pts',(-252.873092734697,-2.82773225051986,
126.780293846019));
#138774=CARTESIAN_POINT('Ctrl Pts',(-252.880840631482,-2.93990843968162,
126.859120626448));
#138775=CARTESIAN_POINT('Ctrl Pts',(-252.888588528267,-3.04884404536948,
126.942682319567));
#138776=CARTESIAN_POINT('Ctrl Pts',(-252.896336425053,-3.15412182105297,
127.030675601503));
#138777=CARTESIAN_POINT('Ctrl Pts',(-252.904082701145,-3.25937757489534,
127.118650477141));
#138778=CARTESIAN_POINT('Ctrl Pts',(-252.911828977237,-3.36097672084659,
127.211054847185));
#138779=CARTESIAN_POINT('Ctrl Pts',(-252.919575253329,-3.45853455176965,
127.307544663485));
#138780=CARTESIAN_POINT('Ctrl Pts',(-252.927321586603,-3.55609310284179,
127.40403519205));
#138781=CARTESIAN_POINT('Ctrl Pts',(-252.935067919876,-3.64961000138655,
127.50461095212));
#138782=CARTESIAN_POINT('Ctrl Pts',(-252.94281425315,-3.73873721291884,
127.608890837512));
#138783=CARTESIAN_POINT('Ctrl Pts',(-252.950562321161,-3.8278843838718,
127.713194075662));
#138784=CARTESIAN_POINT('Ctrl Pts',(-252.958310389172,-3.91263965770853,
127.821202792624));
#138785=CARTESIAN_POINT('Ctrl Pts',(-252.966058457183,-3.99269538260755,
127.93250291841));
#138786=CARTESIAN_POINT('Ctrl Pts',(-252.973814759933,-4.07283619168238,
128.043921335292));
#138787=CARTESIAN_POINT('Ctrl Pts',(-252.981571062683,-4.1482672456395,
128.15863783103));
#138788=CARTESIAN_POINT('Ctrl Pts',(-252.989327365432,-4.21872403867159,
128.276209010555));
#138789=CARTESIAN_POINT('Ctrl Pts',(-252.997087807955,-4.28921843661511,
128.393842941357));
#138790=CARTESIAN_POINT('Ctrl Pts',(-253.004848250477,-4.35473309682876,
128.5143342486));
#138791=CARTESIAN_POINT('Ctrl Pts',(-253.012608692999,-4.41505006841288,
128.637215962517));
#138792=CARTESIAN_POINT('Ctrl Pts',(-253.020381593272,-4.47546386615323,
128.760294937068));
#138793=CARTESIAN_POINT('Ctrl Pts',(-253.028154493545,-4.5306631441883,
128.885771628353));
#138794=CARTESIAN_POINT('Ctrl Pts',(-253.035927393818,-4.5804782535058,
129.013159335839));
#138795=CARTESIAN_POINT('Ctrl Pts',(-253.043417729492,-4.62848245750808,
129.135916177715));
#138796=CARTESIAN_POINT('Ctrl Pts',(-253.050908065165,-4.67148705231427,
129.260447216305));
#138797=CARTESIAN_POINT('Ctrl Pts',(-253.058398400839,-4.70938484811523,
129.386306523096));
#138798=CARTESIAN_POINT('Ctrl Pts',(-253.062266181301,-4.72895411183443,
129.451296423275));
#138799=CARTESIAN_POINT('Ctrl Pts',(-253.066133961763,-4.74718276800677,
129.516707382247));
#138800=CARTESIAN_POINT('Ctrl Pts',(-253.070001742224,-4.7640545282341,
129.582490119308));
#138801=CARTESIAN_POINT('Origin',(213.235140564004,0.,130.804360617566));
#138802=CARTESIAN_POINT('',(-255.165002394563,-4.76405452823405,129.582490119308));
#138803=CARTESIAN_POINT('',(-254.820081699213,-4.76405452823396,129.582490119308));
#138804=CARTESIAN_POINT('',(213.235140564004,-4.76405452823405,129.582490119308));
#138805=CARTESIAN_POINT('',(-253.485140564065,-4.91824929180127,130.806999972842));
#138806=CARTESIAN_POINT('Ctrl Pts',(-253.485140564065,-4.91824929180127,
130.806999972842));
#138807=CARTESIAN_POINT('Ctrl Pts',(-253.493706779917,-4.91816774629876,
130.958954169261));
#138808=CARTESIAN_POINT('Ctrl Pts',(-253.50227299577,-4.91103996867778,
131.110660600794));
#138809=CARTESIAN_POINT('Ctrl Pts',(-253.510839211622,-4.8969591051712,
131.261497998209));
#138810=CARTESIAN_POINT('Ctrl Pts',(-253.519452637721,-4.88280063901485,
131.413166692775));
#138811=CARTESIAN_POINT('Ctrl Pts',(-253.528066063821,-4.86161232316216,
131.563956517786));
#138812=CARTESIAN_POINT('Ctrl Pts',(-253.53667948992,-4.83353902686892,
131.713251996244));
#138813=CARTESIAN_POINT('Ctrl Pts',(-253.545317379068,-4.80538599942276,
131.86297148977));
#138814=CARTESIAN_POINT('Ctrl Pts',(-253.553955268215,-4.770308945894,132.011187921938));
#138815=CARTESIAN_POINT('Ctrl Pts',(-253.562593157362,-4.72850271380084,
132.157300064873));
#138816=CARTESIAN_POINT('Ctrl Pts',(-253.571262549868,-4.6865440096535,
132.303945095308));
#138817=CARTESIAN_POINT('Ctrl Pts',(-253.579931942374,-4.63780707281119,
132.448470249791));
#138818=CARTESIAN_POINT('Ctrl Pts',(-253.588601334879,-4.58253613751236,
132.590290518456));
#138819=CARTESIAN_POINT('Ctrl Pts',(-253.590969107354,-4.56744061620894,
132.629024273825));
#138820=CARTESIAN_POINT('Ctrl Pts',(-253.593336879829,-4.55185796435086,
132.667556402421));
#138821=CARTESIAN_POINT('Ctrl Pts',(-253.595704652304,-4.53579374871089,
132.705875311607));
#138822=CARTESIAN_POINT('Ctrl Pts',(-253.60347898638,-4.48304857138345,
132.831691455099));
#138823=CARTESIAN_POINT('Ctrl Pts',(-253.611253320455,-4.4249809543474,
132.955510610546));
#138824=CARTESIAN_POINT('Ctrl Pts',(-253.619027654531,-4.36176301072568,
133.076849671613));
#138825=CARTESIAN_POINT('Ctrl Pts',(-253.626792407435,-4.29862297757613,
133.198039193119));
#138826=CARTESIAN_POINT('Ctrl Pts',(-253.634557160338,-4.23034542602361,
133.316754358359));
#138827=CARTESIAN_POINT('Ctrl Pts',(-253.642321913241,-4.15715089052608,
133.432530995585));
#138828=CARTESIAN_POINT('Ctrl Pts',(-253.650078954082,-4.08402905288004,
133.548192641812));
#138829=CARTESIAN_POINT('Ctrl Pts',(-253.657835994922,-4.00600015747823,
133.660921239823));
#138830=CARTESIAN_POINT('Ctrl Pts',(-253.665593035762,-3.92333093663046,
133.770276567855));
#138831=CARTESIAN_POINT('Ctrl Pts',(-253.673344226957,-3.84072405729242,
133.879549430174));
#138832=CARTESIAN_POINT('Ctrl Pts',(-253.681095418152,-3.75348405247946,
133.985453775198));
#138833=CARTESIAN_POINT('Ctrl Pts',(-253.688846609347,-3.66192110264863,
134.087578079215));
#138834=CARTESIAN_POINT('Ctrl Pts',(-253.696594506078,-3.57039706952383,
134.189658977667));
#138835=CARTESIAN_POINT('Ctrl Pts',(-253.704342402809,-3.47455400621042,
134.287962740067));
#138836=CARTESIAN_POINT('Ctrl Pts',(-253.71209029954,-3.3747423939718,134.382110865533));
#138837=CARTESIAN_POINT('Ctrl Pts',(-253.719836575578,-3.27495166017714,
134.476239297235));
#138838=CARTESIAN_POINT('Ctrl Pts',(-253.727582851616,-3.17119431286658,
134.566213552931));
#138839=CARTESIAN_POINT('Ctrl Pts',(-253.735329127653,-3.06385742935098,
134.651692253273));
#138840=CARTESIAN_POINT('Ctrl Pts',(-253.743075460872,-2.95651975350517,
134.737171584594));
#138841=CARTESIAN_POINT('Ctrl Pts',(-253.75082179409,-2.84560279456388,
134.818155050787));
#138842=CARTESIAN_POINT('Ctrl Pts',(-253.758568127308,-2.73152609712807,
134.894342065349));
#138843=CARTESIAN_POINT('Ctrl Pts',(-253.766316195264,-2.61742385301241,
134.970546141461));
#138844=CARTESIAN_POINT('Ctrl Pts',(-253.77406426322,-2.50016078741905,
135.041951411448));
#138845=CARTESIAN_POINT('Ctrl Pts',(-253.781812331175,-2.38018440848479,
135.108301282132));
#138846=CARTESIAN_POINT('Ctrl Pts',(-253.789568633869,-2.26008051723188,
135.174721670246));
#138847=CARTESIAN_POINT('Ctrl Pts',(-253.797324936564,-2.13725789473119,
135.236075736524));
#138848=CARTESIAN_POINT('Ctrl Pts',(-253.805081239258,-2.01218807302497,
135.292153195357));
#138849=CARTESIAN_POINT('Ctrl Pts',(-253.812841681724,-1.88705149779281,
135.348260584417));
#138850=CARTESIAN_POINT('Ctrl Pts',(-253.82060212419,-1.75966569640479,
135.399085609535));
#138851=CARTESIAN_POINT('Ctrl Pts',(-253.828362566656,-1.63052011205161,
135.444466998533));
#138852=CARTESIAN_POINT('Ctrl Pts',(-253.836135466874,-1.50116721173979,
135.489921237767));
#138853=CARTESIAN_POINT('Ctrl Pts',(-253.843908367092,-1.37004925746463,
135.52991426423));
#138854=CARTESIAN_POINT('Ctrl Pts',(-253.851681267309,-1.23766958020655,
135.564335099927));
#138855=CARTESIAN_POINT('Ctrl Pts',(-253.859171603578,-1.11010222824022,
135.597504653996));
#138856=CARTESIAN_POINT('Ctrl Pts',(-253.866661939847,-0.981363595088982,
135.625500043834));
#138857=CARTESIAN_POINT('Ctrl Pts',(-253.874152276116,-0.851909148230417,
135.648267497932));
#138858=CARTESIAN_POINT('Ctrl Pts',(-253.881926610583,-0.717546399757441,
135.671898186431));
#138859=CARTESIAN_POINT('Ctrl Pts',(-253.88970094505,-0.581986865247745,
135.689971534245));
#138860=CARTESIAN_POINT('Ctrl Pts',(-253.897475279516,-0.445730027143223,
135.702371214268));
#138861=CARTESIAN_POINT('Ctrl Pts',(-253.905240032812,-0.309641113389513,
135.714755612795));
#138862=CARTESIAN_POINT('Ctrl Pts',(-253.913004786108,-0.172856991538168,
135.721480221007));
#138863=CARTESIAN_POINT('Ctrl Pts',(-253.920769539404,-0.0358873867344748,
135.722479684646));
#138864=CARTESIAN_POINT('Ctrl Pts',(-253.928526580638,0.10094617794333,
135.723478155603));
#138865=CARTESIAN_POINT('Ctrl Pts',(-253.936283621872,0.237964470533983,
135.718762795134));
#138866=CARTESIAN_POINT('Ctrl Pts',(-253.944040663107,0.374652944628602,
135.708320062095));
#138867=CARTESIAN_POINT('Ctrl Pts',(-253.951791854696,0.511238340890916,
135.697885204));
#138868=CARTESIAN_POINT('Ctrl Pts',(-253.959543046286,0.647494025464798,
135.681731599816));
#138869=CARTESIAN_POINT('Ctrl Pts',(-253.967294237876,0.782906111640338,
135.65989777455));
#138870=CARTESIAN_POINT('Ctrl Pts',(-253.975042135001,0.918260644054309,
135.638073229245));
#138871=CARTESIAN_POINT('Ctrl Pts',(-253.982790032127,1.05277190603047,
135.610573326714));
#138872=CARTESIAN_POINT('Ctrl Pts',(-253.990537929253,1.18593201033485,
135.577488347825));
#138873=CARTESIAN_POINT('Ctrl Pts',(-253.998284205685,1.31906426040746,
135.544410289601));
#138874=CARTESIAN_POINT('Ctrl Pts',(-254.006030482117,1.4508455357925,135.505749573001));
#138875=CARTESIAN_POINT('Ctrl Pts',(-254.013776758549,1.58077939959622,
135.461647333274));
#138876=CARTESIAN_POINT('Ctrl Pts',(-254.021523092162,1.71071422252711,
135.417544768));
#138877=CARTESIAN_POINT('Ctrl Pts',(-254.029269425775,1.83880123644463,
135.36800072511));
#138878=CARTESIAN_POINT('Ctrl Pts',(-254.037015759387,1.96456077526858,
135.313205705033));
#138879=CARTESIAN_POINT('Ctrl Pts',(-254.044763827736,2.09034847704797,
135.258398414001));
#138880=CARTESIAN_POINT('Ctrl Pts',(-254.052511896085,2.21380730821146,
135.198337961979));
#138881=CARTESIAN_POINT('Ctrl Pts',(-254.060259964434,2.33447950053559,
135.133262155379));
#138882=CARTESIAN_POINT('Ctrl Pts',(-254.068016267518,2.45527994463568,
135.068117185473));
#138883=CARTESIAN_POINT('Ctrl Pts',(-254.075772570602,2.57328748897384,
134.997946398859));
#138884=CARTESIAN_POINT('Ctrl Pts',(-254.083528873686,2.68807033968866,
134.923032844314));
#138885=CARTESIAN_POINT('Ctrl Pts',(-254.09128931654,2.80291445344082,134.848079306166));
#138886=CARTESIAN_POINT('Ctrl Pts',(-254.099049759395,2.91453012608298,
134.768378183231));
#138887=CARTESIAN_POINT('Ctrl Pts',(-254.10681020225,3.02251711872841,134.684254086399));
#138888=CARTESIAN_POINT('Ctrl Pts',(-254.114583102849,3.13067746158827,
134.599994946171));
#138889=CARTESIAN_POINT('Ctrl Pts',(-254.122356003449,3.23519718582483,
134.511298896802));
#138890=CARTESIAN_POINT('Ctrl Pts',(-254.130128904049,3.33571085978134,
134.41852941861));
#138891=CARTESIAN_POINT('Ctrl Pts',(-254.137619236009,3.43257055517851,
134.329132393845));
#138892=CARTESIAN_POINT('Ctrl Pts',(-254.145109567969,3.52571018997497,
134.235953179316));
#138893=CARTESIAN_POINT('Ctrl Pts',(-254.152599899929,3.61483833388053,
134.13934590725));
#138894=CARTESIAN_POINT('Ctrl Pts',(-254.160374233492,3.70734583879135,
134.039075697376));
#138895=CARTESIAN_POINT('Ctrl Pts',(-254.168148567055,3.79582468878446,
133.934794719803));
#138896=CARTESIAN_POINT('Ctrl Pts',(-254.175922900618,3.8799070321371,133.826860325502));
#138897=CARTESIAN_POINT('Ctrl Pts',(-254.18368765301,3.96388575151609,133.719058950695));
#138898=CARTESIAN_POINT('Ctrl Pts',(-254.191452405401,4.04347850709934,
133.607613423275));
#138899=CARTESIAN_POINT('Ctrl Pts',(-254.199217157793,4.11835479563008,
133.492917263763));
#138900=CARTESIAN_POINT('Ctrl Pts',(-254.206974198124,4.19315671598237,
133.378335022083));
#138901=CARTESIAN_POINT('Ctrl Pts',(-254.214731238455,4.26325127923338,
133.260508898578));
#138902=CARTESIAN_POINT('Ctrl Pts',(-254.222488278785,4.3283489679517,133.139864476294));
#138903=CARTESIAN_POINT('Ctrl Pts',(-254.230239469473,4.39339756600839,
133.019311032884));
#138904=CARTESIAN_POINT('Ctrl Pts',(-254.237990660161,4.4534566049638,132.895943863657));
#138905=CARTESIAN_POINT('Ctrl Pts',(-254.245741850849,4.50828072869673,
132.770216139664));
#138906=CARTESIAN_POINT('Ctrl Pts',(-254.253489747078,4.563081550746,132.644541853235));
#138907=CARTESIAN_POINT('Ctrl Pts',(-254.261237643308,4.61265172693553,
132.516509365148));
#138908=CARTESIAN_POINT('Ctrl Pts',(-254.268985539537,4.65679268767404,
132.386594774234));
#138909=CARTESIAN_POINT('Ctrl Pts',(-254.276731815076,4.70092441509108,
132.256707358604));
#138910=CARTESIAN_POINT('Ctrl Pts',(-254.284478090616,4.73962906027621,
132.124938993175));
#138911=CARTESIAN_POINT('Ctrl Pts',(-254.292224366155,4.77275702806113,
131.99178363132));
#138912=CARTESIAN_POINT('Ctrl Pts',(-254.299970698879,4.80588524040378,
131.858627286484));
#138913=CARTESIAN_POINT('Ctrl Pts',(-254.307717031603,4.83343659880648,
131.724084304192));
#138914=CARTESIAN_POINT('Ctrl Pts',(-254.315463364327,4.85531210545887,
131.588661211143));
#138915=CARTESIAN_POINT('Ctrl Pts',(-254.323211431793,4.87719251099064,
131.453207790961));
#138916=CARTESIAN_POINT('Ctrl Pts',(-254.330959499258,4.8933944731545,131.316874253714));
#138917=CARTESIAN_POINT('Ctrl Pts',(-254.338707566724,4.90387063032863,
131.180174272853));
#138918=CARTESIAN_POINT('Ctrl Pts',(-254.346463868937,4.91435792170045,
131.043329005454));
#138919=CARTESIAN_POINT('Ctrl Pts',(-254.354220171151,4.91910722179682,
130.906116906895));
#138920=CARTESIAN_POINT('Ctrl Pts',(-254.361976473364,4.91812327245555,
130.769054252261));
#138921=CARTESIAN_POINT('Ctrl Pts',(-254.369736915355,4.91713879795033,
130.631918443083));
#138922=CARTESIAN_POINT('Ctrl Pts',(-254.377497357344,4.9104149958339,130.494932627069));
#138923=CARTESIAN_POINT('Ctrl Pts',(-254.385257799334,4.89800863156218,
130.358608996546));
#138924=CARTESIAN_POINT('Ctrl Pts',(-254.393030699088,4.88558235147199,
130.222066526996));
#138925=CARTESIAN_POINT('Ctrl Pts',(-254.400803598842,4.8674553319674,130.086188754904));
#138926=CARTESIAN_POINT('Ctrl Pts',(-254.408576498596,4.84373585461035,
129.95147959816));
#138927=CARTESIAN_POINT('Ctrl Pts',(-254.416066840311,4.82087862032894,
129.821667346853));
#138928=CARTESIAN_POINT('Ctrl Pts',(-254.423557182027,4.79282852551927,
129.692940524602));
#138929=CARTESIAN_POINT('Ctrl Pts',(-254.431047523742,4.75972598709712,
129.565735738818));
#138930=CARTESIAN_POINT('Ctrl Pts',(-254.438821857757,4.72536838363919,
129.433708051632));
#138931=CARTESIAN_POINT('Ctrl Pts',(-254.446596191771,4.68545882085699,
129.302901868167));
#138932=CARTESIAN_POINT('Ctrl Pts',(-254.454370525786,4.64009911541028,
129.173819829463));
#138933=CARTESIAN_POINT('Ctrl Pts',(-254.462135278623,4.59479531177607,
129.044896872919));
#138934=CARTESIAN_POINT('Ctrl Pts',(-254.469900031461,4.54405485831362,
128.91769419862));
#138935=CARTESIAN_POINT('Ctrl Pts',(-254.477664784299,4.48803018990912,
128.792702575809));
#138936=CARTESIAN_POINT('Ctrl Pts',(-254.48542182507,4.43206116602998,128.667835096519));
#138937=CARTESIAN_POINT('Ctrl Pts',(-254.49317886584,4.3708185305596,128.545174652937));
#138938=CARTESIAN_POINT('Ctrl Pts',(-254.500935906611,4.30450384733297,
128.425194862349));
#138939=CARTESIAN_POINT('Ctrl Pts',(-254.508687097733,4.23823917256443,
128.305305549527));
#138940=CARTESIAN_POINT('Ctrl Pts',(-254.516438288854,4.16691025157994,
128.188093206812));
#138941=CARTESIAN_POINT('Ctrl Pts',(-254.524189479975,4.09076572905404,
128.074009209323));
#138942=CARTESIAN_POINT('Ctrl Pts',(-254.531937376627,4.01465357004527,
127.959973700671));
#138943=CARTESIAN_POINT('Ctrl Pts',(-254.539685273279,3.93373009693972,
127.849064217211));
#138944=CARTESIAN_POINT('Ctrl Pts',(-254.547433169931,3.84828853346442,
127.741705164253));
#138945=CARTESIAN_POINT('Ctrl Pts',(-254.555179445886,3.76286484256564,
127.63436856855));
#138946=CARTESIAN_POINT('Ctrl Pts',(-254.562925721841,3.6729251844364,127.530581231843));
#138947=CARTESIAN_POINT('Ctrl Pts',(-254.570671997796,3.57880427621025,
127.430736006694));
#138948=CARTESIAN_POINT('Ctrl Pts',(-254.578418330929,3.48468267325045,
127.330890044559));
#138949=CARTESIAN_POINT('Ctrl Pts',(-254.586164664061,3.38638002678753,
127.234986536532));
#138950=CARTESIAN_POINT('Ctrl Pts',(-254.593910997194,3.2842689813596,127.143382562377));
#138951=CARTESIAN_POINT('Ctrl Pts',(-254.60165906506,3.18213506891837,127.051758074188));
#138952=CARTESIAN_POINT('Ctrl Pts',(-254.609407132927,3.07619135137947,
126.964435296853));
#138953=CARTESIAN_POINT('Ctrl Pts',(-254.617155200794,2.96684439666846,
126.881731730142));
#138954=CARTESIAN_POINT('Ctrl Pts',(-254.624911503394,2.85738122677966,
126.798940265145));
#138955=CARTESIAN_POINT('Ctrl Pts',(-254.632667805995,2.74450790669163,
126.720778053945));
#138956=CARTESIAN_POINT('Ctrl Pts',(-254.640424108595,2.62866135635465,
126.647520166441));
#138957=CARTESIAN_POINT('Ctrl Pts',(-254.648184550965,2.51275297526742,
126.574223179024));
#138958=CARTESIAN_POINT('Ctrl Pts',(-254.655944993335,2.39386854062481,
126.505835925912));
#138959=CARTESIAN_POINT('Ctrl Pts',(-254.663705435705,2.27246965747638,
126.442587501235));
#138960=CARTESIAN_POINT('Ctrl Pts',(-254.671478335823,2.15087589411364,
126.379237544598));
#138961=CARTESIAN_POINT('Ctrl Pts',(-254.679251235941,2.02675997039196,
126.321043067199));
#138962=CARTESIAN_POINT('Ctrl Pts',(-254.687024136058,1.90060437555955,
126.268185348674));
#138963=CARTESIAN_POINT('Ctrl Pts',(-254.694514473224,1.7790348292785,126.217249130848));
#138964=CARTESIAN_POINT('Ctrl Pts',(-254.70200481039,1.65557161951262,126.171268508598));
#138965=CARTESIAN_POINT('Ctrl Pts',(-254.709495147555,1.53065797437531,
126.130361342001));
#138966=CARTESIAN_POINT('Ctrl Pts',(-254.71726948387,1.40100817808425,126.087903163711));
#138967=CARTESIAN_POINT('Ctrl Pts',(-254.725043820186,1.26938509756202,
126.050776262233));
#138968=CARTESIAN_POINT('Ctrl Pts',(-254.732818156501,1.13626665366864,
126.019166665984));
#138969=CARTESIAN_POINT('Ctrl Pts',(-254.740582911652,1.00331226618556,
125.987596025695));
#138970=CARTESIAN_POINT('Ctrl Pts',(-254.748347666802,0.868866558888896,
125.961529250959));
#138971=CARTESIAN_POINT('Ctrl Pts',(-254.756112421953,0.73342482492517,
125.94110336664));
#138972=CARTESIAN_POINT('Ctrl Pts',(-254.763869465047,0.598117613473356,
125.920697769578));
#138973=CARTESIAN_POINT('Ctrl Pts',(-254.771626508141,0.461816728131874,
125.905921971419));
#138974=CARTESIAN_POINT('Ctrl Pts',(-254.779383551234,0.32502958699541,
125.896862392393));
#138975=CARTESIAN_POINT('Ctrl Pts',(-254.787134744686,0.188345598026315,
125.887809645261));
#138976=CARTESIAN_POINT('Ctrl Pts',(-254.794885938138,0.0511764716662484,
125.884464562924));
#138977=CARTESIAN_POINT('Ctrl Pts',(-254.80263713159,-0.0859636386297147,
125.886861932733));
#138978=CARTESIAN_POINT('Ctrl Pts',(-254.810385030575,-0.223045460675289,
125.889258283595));
#138979=CARTESIAN_POINT('Ctrl Pts',(-254.81813292956,-0.360097901098543,
125.897392225423));
#138980=CARTESIAN_POINT('Ctrl Pts',(-254.825880828545,-0.49660540085496,
125.911246462108));
#138981=CARTESIAN_POINT('Ctrl Pts',(-254.833627106835,-0.633084346150557,
125.925097800782));
#138982=CARTESIAN_POINT('Ctrl Pts',(-254.841373385125,-0.769018188791224,
125.94466701483));
#138983=CARTESIAN_POINT('Ctrl Pts',(-254.849119663415,-0.903895487765914,
125.969884843535));
#138984=CARTESIAN_POINT('Ctrl Pts',(-254.856865998881,-1.03877378229616,
125.995102858377));
#138985=CARTESIAN_POINT('Ctrl Pts',(-254.864612334348,-1.17259513329347,
126.025969499218));
#138986=CARTESIAN_POINT('Ctrl Pts',(-254.872358669815,-1.30485769573404,
126.062364259872));
#138987=CARTESIAN_POINT('Ctrl Pts',(-254.880106740012,-1.43714987733809,
126.098767170847));
#138988=CARTESIAN_POINT('Ctrl Pts',(-254.88785481021,-1.56788219887774,
126.140700561361));
#138989=CARTESIAN_POINT('Ctrl Pts',(-254.895602880408,-1.69656777868186,
126.18799399057));
#138990=CARTESIAN_POINT('Ctrl Pts',(-254.903359185322,-1.82539012663506,
126.235337683646));
#138991=CARTESIAN_POINT('Ctrl Pts',(-254.911115490235,-1.95216101991438,
126.288052660099));
#138992=CARTESIAN_POINT('Ctrl Pts',(-254.918871795149,-2.07641286828906,
126.345920008687));
#138993=CARTESIAN_POINT('Ctrl Pts',(-254.926632239826,-2.20073103345476,
126.403818242746));
#138994=CARTESIAN_POINT('Ctrl Pts',(-254.934392684504,-2.32252712768721,
126.466874148827));
#138995=CARTESIAN_POINT('Ctrl Pts',(-254.942153129181,-2.44135889857268,
126.534823196386));
#138996=CARTESIAN_POINT('Ctrl Pts',(-254.949926031572,-2.56038142814344,
126.602881321431));
#138997=CARTESIAN_POINT('Ctrl Pts',(-254.957698933963,-2.67642979404177,
126.675848076281));
#138998=CARTESIAN_POINT('Ctrl Pts',(-254.965471836354,-2.7890906831194,
126.753415515021));
#138999=CARTESIAN_POINT('Ctrl Pts',(-254.972962148026,-2.89765568624046,
126.828162921133));
#139000=CARTESIAN_POINT('Ctrl Pts',(-254.980452459697,-3.00307499878199,
126.90718211095));
#139001=CARTESIAN_POINT('Ctrl Pts',(-254.987942771368,-3.10500988958206,
126.990163893733));
#139002=CARTESIAN_POINT('Ctrl Pts',(-254.995611852538,-3.2093776363245,
127.075126183109));
#139003=CARTESIAN_POINT('Ctrl Pts',(-255.003280933707,-3.31044213216741,
127.164527494784));
#139004=CARTESIAN_POINT('Ctrl Pts',(-255.010950014877,-3.40779452867065,
127.258078125595));
#139005=CARTESIAN_POINT('Ctrl Pts',(-255.018610310982,-3.50503540633297,
127.351521592552));
#139006=CARTESIAN_POINT('Ctrl Pts',(-255.026270607087,-3.59857235074418,
127.449104654649));
#139007=CARTESIAN_POINT('Ctrl Pts',(-255.033930903193,-3.68802771709246,
127.550496050554));
#139008=CARTESIAN_POINT('Ctrl Pts',(-255.041584189907,-3.77740122920827,
127.651794670416));
#139009=CARTESIAN_POINT('Ctrl Pts',(-255.049237476621,-3.8627003248688,
127.756894395887));
#139010=CARTESIAN_POINT('Ctrl Pts',(-255.056890763335,-3.9435829442897,
127.865426010603));
#139011=CARTESIAN_POINT('Ctrl Pts',(-255.064538809855,-4.02441018350123,
127.973883313883));
#139012=CARTESIAN_POINT('Ctrl Pts',(-255.072186856375,-4.10082672142748,
128.085767511594));
#139013=CARTESIAN_POINT('Ctrl Pts',(-255.079834902895,-4.17253003611261,
128.200675505991));
#139014=CARTESIAN_POINT('Ctrl Pts',(-255.087480300179,-4.24420851321359,
128.31554369697));
#139015=CARTESIAN_POINT('Ctrl Pts',(-255.095125697463,-4.31117679765856,
128.433433263226));
#139016=CARTESIAN_POINT('Ctrl Pts',(-255.102771094747,-4.37317529652245,
128.553911576067));
#139017=CARTESIAN_POINT('Ctrl Pts',(-255.11041480321,-4.43516010029642,
128.674363275983));
#139018=CARTESIAN_POINT('Ctrl Pts',(-255.118058511672,-4.49217712152607,
128.79740222569));
#139019=CARTESIAN_POINT('Ctrl Pts',(-255.125702220135,-4.54401274453013,
128.922571245705));
#139020=CARTESIAN_POINT('Ctrl Pts',(-255.133348272447,-4.59586426229855,
129.047778647281));
#139021=CARTESIAN_POINT('Ctrl Pts',(-255.14099432476,-4.64253105279218,
129.175117052467));
#139022=CARTESIAN_POINT('Ctrl Pts',(-255.148640377073,-4.68384772590579,
129.304109457584));
#139023=CARTESIAN_POINT('Ctrl Pts',(-255.154094382903,-4.71331932338101,
129.396121034376));
#139024=CARTESIAN_POINT('Ctrl Pts',(-255.159548388733,-4.74006973265035,
129.488973765347));
#139025=CARTESIAN_POINT('Ctrl Pts',(-255.165002394563,-4.76405452823405,
129.582490119308));
#139026=CARTESIAN_POINT('Ctrl Pts',(-253.415334457588,-4.76405452823403,
129.582490119308));
#139027=CARTESIAN_POINT('Ctrl Pts',(-253.423183166685,-4.79857612324911,
129.717089294334));
#139028=CARTESIAN_POINT('Ctrl Pts',(-253.431031875783,-4.82741111287845,
129.853237788276));
#139029=CARTESIAN_POINT('Ctrl Pts',(-253.43888058488,-4.85043173299432,
129.990422618661));
#139030=CARTESIAN_POINT('Ctrl Pts',(-253.446726269139,-4.87344348112395,
130.12755457897));
#139031=CARTESIAN_POINT('Ctrl Pts',(-253.454571953398,-4.89064525643546,
130.265721710007));
#139032=CARTESIAN_POINT('Ctrl Pts',(-253.462417637657,-4.90196031792918,
130.404400489619));
#139033=CARTESIAN_POINT('Ctrl Pts',(-253.469991946443,-4.91288400117358,
130.538282489468));
#139034=CARTESIAN_POINT('Ctrl Pts',(-253.477566255229,-4.91832139488876,
130.672640994209));
#139035=CARTESIAN_POINT('Ctrl Pts',(-253.485140564015,-4.91824929180175,
130.806999971948));
#139036=CARTESIAN_POINT('',(-253.13985943596,-4.91824809876146,130.800036091088));
#139037=CARTESIAN_POINT('Ctrl Pts',(-253.070001742224,-4.7640545282341,
129.582490119308));
#139038=CARTESIAN_POINT('Ctrl Pts',(-253.07954420969,-4.80568000947843,
129.744787238925));
#139039=CARTESIAN_POINT('Ctrl Pts',(-253.089086677157,-4.83904288583247,
129.909348847311));
#139040=CARTESIAN_POINT('Ctrl Pts',(-253.098629144623,-4.86393139366922,
130.075419975141));
#139041=CARTESIAN_POINT('Ctrl Pts',(-253.108045009558,-4.88848969885077,
130.2392877918));
#139042=CARTESIAN_POINT('Ctrl Pts',(-253.117460874493,-4.90479697694862,
130.404625368815));
#139043=CARTESIAN_POINT('Ctrl Pts',(-253.126876739428,-4.9126957295879,
130.570686205212));
#139044=CARTESIAN_POINT('Ctrl Pts',(-253.131204304938,-4.91632602481152,
130.647008365018));
#139045=CARTESIAN_POINT('Ctrl Pts',(-253.135531870449,-4.91818078701807,
130.723483003563));
#139046=CARTESIAN_POINT('Ctrl Pts',(-253.13985943596,-4.91824809876146,
130.800036091088));
#139047=CARTESIAN_POINT('Ctrl Pts',(-253.139859435997,-4.91824809876204,
130.800036091749));
#139048=CARTESIAN_POINT('Ctrl Pts',(-253.147555448689,-4.91836780392906,
130.936175806272));
#139049=CARTESIAN_POINT('Ctrl Pts',(-253.155251461381,-4.91283062992671,
131.072423279795));
#139050=CARTESIAN_POINT('Ctrl Pts',(-253.162947474073,-4.90163658373028,
131.208268854096));
#139051=CARTESIAN_POINT('Ctrl Pts',(-253.170640926388,-4.8904462616678,
131.344069234094));
#139052=CARTESIAN_POINT('Ctrl Pts',(-253.178334378702,-4.87360283988483,
131.479467585744));
#139053=CARTESIAN_POINT('Ctrl Pts',(-253.186027831017,-4.85115838920778,
131.613956408883));
#139054=CARTESIAN_POINT('Ctrl Pts',(-253.193720214653,-4.82871705623311,
131.748426550518));
#139055=CARTESIAN_POINT('Ctrl Pts',(-253.20141259829,-4.80067630673908,
131.881987023561));
#139056=CARTESIAN_POINT('Ctrl Pts',(-253.209104981926,-4.76713975822367,
132.014138112837));
#139057=CARTESIAN_POINT('Ctrl Pts',(-253.216798019897,-4.73360035700124,
132.146300443232));
#139058=CARTESIAN_POINT('Ctrl Pts',(-253.224491057868,-4.69456432442808,
132.277052766712));
#139059=CARTESIAN_POINT('Ctrl Pts',(-253.232184095839,-4.65018569343382,
132.40590864341));
#139060=CARTESIAN_POINT('Ctrl Pts',(-253.239879511309,-4.60579334742024,
132.534804342445));
#139061=CARTESIAN_POINT('Ctrl Pts',(-253.247574926779,-4.55605524774839,
132.661802053837));
#139062=CARTESIAN_POINT('Ctrl Pts',(-253.25527034225,-4.50117411226919,
132.786433944549));
#139063=CARTESIAN_POINT('Ctrl Pts',(-253.262974316368,-4.44623193936449,
132.911204447731));
#139064=CARTESIAN_POINT('Ctrl Pts',(-253.270678290487,-4.38613547050944,
133.033603513458));
#139065=CARTESIAN_POINT('Ctrl Pts',(-253.278382264606,-4.32113424600608,
133.153186258284));
#139066=CARTESIAN_POINT('Ctrl Pts',(-253.286091036346,-4.25609254222782,
133.272843472827));
#139067=CARTESIAN_POINT('Ctrl Pts',(-253.293799808087,-4.18614020375855,
133.389680534304));
#139068=CARTESIAN_POINT('Ctrl Pts',(-253.301508579827,-4.11157026886499,
133.503281325309));
#139069=CARTESIAN_POINT('Ctrl Pts',(-253.309228941747,-4.03688821767641,
133.61705291571));
#139070=CARTESIAN_POINT('Ctrl Pts',(-253.316949303667,-3.95757493897604,
133.727578199157));
#139071=CARTESIAN_POINT('Ctrl Pts',(-253.324669665587,-3.87396422101779,
133.834473532421));
#139072=CARTESIAN_POINT('Ctrl Pts',(-253.328728451942,-3.83000798623275,
133.890671068828));
#139073=CARTESIAN_POINT('Ctrl Pts',(-253.332787238297,-3.78486462953533,
133.945865935702));
#139074=CARTESIAN_POINT('Ctrl Pts',(-253.336846024651,-3.73858661432107,
134.000006591343));
#139075=CARTESIAN_POINT('Ctrl Pts',(-253.34462035876,-3.64994416786029,
134.103709400265));
#139076=CARTESIAN_POINT('Ctrl Pts',(-253.352394692869,-3.55684320656323,
134.203885458297));
#139077=CARTESIAN_POINT('Ctrl Pts',(-253.360169026978,-3.45959513373787,
134.300127282136));
#139078=CARTESIAN_POINT('Ctrl Pts',(-253.367933779914,-3.36246691047244,
134.396250496526));
#139079=CARTESIAN_POINT('Ctrl Pts',(-253.375698532851,-3.26120202015508,
134.488448851603));
#139080=CARTESIAN_POINT('Ctrl Pts',(-253.383463285787,-3.15615219366089,
134.576347679176));
#139081=CARTESIAN_POINT('Ctrl Pts',(-253.391220326662,-3.0512067041369,
134.664159204392));
#139082=CARTESIAN_POINT('Ctrl Pts',(-253.398977367536,-2.94248405742258,
134.747679451028));
#139083=CARTESIAN_POINT('Ctrl Pts',(-253.406734408411,-2.83037266328232,
134.826570662982));
#139084=CARTESIAN_POINT('Ctrl Pts',(-253.41448559964,-2.71834581321827,
134.905402382458));
#139085=CARTESIAN_POINT('Ctrl Pts',(-253.422236790869,-2.60293562070072,
134.979611791377));
#139086=CARTESIAN_POINT('Ctrl Pts',(-253.429987982099,-2.48456310623925,
135.048901727464));
#139087=CARTESIAN_POINT('Ctrl Pts',(-253.437735878865,-2.36624090325532,
135.118162213479));
#139088=CARTESIAN_POINT('Ctrl Pts',(-253.445483775631,-2.24495921921734,
135.182507188226));
#139089=CARTESIAN_POINT('Ctrl Pts',(-253.453231672398,-2.12116736783148,
135.241683240516));
#139090=CARTESIAN_POINT('Ctrl Pts',(-253.460977948471,-1.99740141103332,
135.300846914451));
#139091=CARTESIAN_POINT('Ctrl Pts',(-253.468724224544,-1.87112668379759,
135.354843648039));
#139092=CARTESIAN_POINT('Ctrl Pts',(-253.476470500617,-1.7428160137112,
135.403466552946));
#139093=CARTESIAN_POINT('Ctrl Pts',(-253.484216833872,-1.61450439646546,
135.452089816777));
#139094=CARTESIAN_POINT('Ctrl Pts',(-253.491963167126,-1.48415717197565,
135.495339034232));
#139095=CARTESIAN_POINT('Ctrl Pts',(-253.499709500381,-1.35226562913962,
135.533056075168));
#139096=CARTESIAN_POINT('Ctrl Pts',(-253.507457568373,-1.22034455010754,
135.570781562575));
#139097=CARTESIAN_POINT('Ctrl Pts',(-253.515205636365,-1.08687884037397,
135.602972300736));
#139098=CARTESIAN_POINT('Ctrl Pts',(-253.522953704357,-0.952372984250942,
135.629520590185));
#139099=CARTESIAN_POINT('Ctrl Pts',(-253.530710007088,-0.817724173703003,
135.656097095473));
#139100=CARTESIAN_POINT('Ctrl Pts',(-253.538466309819,-0.682033392627136,
135.677019096846));
#139101=CARTESIAN_POINT('Ctrl Pts',(-253.54622261255,-0.545813862636227,
135.69223032633));
#139102=CARTESIAN_POINT('Ctrl Pts',(-253.553983055053,-0.409521628180569,
135.707449674506));
#139103=CARTESIAN_POINT('Ctrl Pts',(-253.561743497556,-0.272700472318955,
135.7169521503));
#139104=CARTESIAN_POINT('Ctrl Pts',(-253.56950394006,-0.135865706927921,
135.720733627436));
#139105=CARTESIAN_POINT('Ctrl Pts',(-253.577276840314,0.00118871777756249,
135.724521174936));
#139106=CARTESIAN_POINT('Ctrl Pts',(-253.585049740569,0.13825640451962,
135.72256937708));
#139107=CARTESIAN_POINT('Ctrl Pts',(-253.592822640824,0.274824173439137,
135.714926240404));
#139108=CARTESIAN_POINT('Ctrl Pts',(-253.600312976704,0.406427362220847,
135.707560950871));
#139109=CARTESIAN_POINT('Ctrl Pts',(-253.607803312583,0.537566042083476,
135.694910956932));
#139110=CARTESIAN_POINT('Ctrl Pts',(-253.615293648463,0.667790078184718,
135.677064125269));
#139111=CARTESIAN_POINT('Ctrl Pts',(-253.623067982636,0.802951597001489,
135.658540625722));
#139112=CARTESIAN_POINT('Ctrl Pts',(-253.630842316809,0.937555896552514,
135.634359756279));
#139113=CARTESIAN_POINT('Ctrl Pts',(-253.638616650982,1.07109182849129,
135.604563254689));
#139114=CARTESIAN_POINT('Ctrl Pts',(-253.646381403983,1.20446318933245,
135.574803474623));
#139115=CARTESIAN_POINT('Ctrl Pts',(-253.654146156984,1.33676842441923,
135.539441916995));
#139116=CARTESIAN_POINT('Ctrl Pts',(-253.661910909985,1.46750219565566,
135.49857198565));
#139117=CARTESIAN_POINT('Ctrl Pts',(-253.669667950924,1.59810612026909,
135.457742646895));
#139118=CARTESIAN_POINT('Ctrl Pts',(-253.677424991863,1.7271413163536,135.41141593785));
#139119=CARTESIAN_POINT('Ctrl Pts',(-253.685182032802,1.85411367516457,
135.35973607323));
#139120=CARTESIAN_POINT('Ctrl Pts',(-253.692933224096,1.98099028313289,
135.308095180798));
#139121=CARTESIAN_POINT('Ctrl Pts',(-253.70068441539,2.10580678950429,135.251109314703));
#139122=CARTESIAN_POINT('Ctrl Pts',(-253.708435606684,2.22808561136653,
135.188972067959));
#139123=CARTESIAN_POINT('Ctrl Pts',(-253.716183503515,2.35031246146511,
135.126861231205));
#139124=CARTESIAN_POINT('Ctrl Pts',(-253.723931400346,2.47000342446012,
135.059603545246));
#139125=CARTESIAN_POINT('Ctrl Pts',(-253.731679297177,2.58670243330287,
134.987440055497));
#139126=CARTESIAN_POINT('Ctrl Pts',(-253.739425573315,2.70337703122698,
134.915291660796));
#139127=CARTESIAN_POINT('Ctrl Pts',(-253.747171849453,2.81706058753968,
134.838239708944));
#139128=CARTESIAN_POINT('Ctrl Pts',(-253.75491812559,2.92732346636293,134.756570174988));
#139129=CARTESIAN_POINT('Ctrl Pts',(-253.762664458909,3.03758715911975,
134.674900038169));
#139130=CARTESIAN_POINT('Ctrl Pts',(-253.770410792228,3.14442980982937,
134.588612483931));
#139131=CARTESIAN_POINT('Ctrl Pts',(-253.778157125547,3.24745282547091,
134.498035374342));
#139132=CARTESIAN_POINT('Ctrl Pts',(-253.785905193603,3.35049891239881,
134.407437980639));
#139133=CARTESIAN_POINT('Ctrl Pts',(-253.79365326166,3.449723368586,134.312549378169));
#139134=CARTESIAN_POINT('Ctrl Pts',(-253.801401329716,3.54476289732365,
134.213735789684));
#139135=CARTESIAN_POINT('Ctrl Pts',(-253.80915763251,3.63990343519483,134.114817180951));
#139136=CARTESIAN_POINT('Ctrl Pts',(-253.816913935305,3.73084988922346,
134.011965535371));
#139137=CARTESIAN_POINT('Ctrl Pts',(-253.824670238099,3.81727751074879,
133.905582226615));
#139138=CARTESIAN_POINT('Ctrl Pts',(-253.832430680666,3.9037512612951,133.799142137887));
#139139=CARTESIAN_POINT('Ctrl Pts',(-253.840191123233,3.98570114005506,
133.689166943396));
#139140=CARTESIAN_POINT('Ctrl Pts',(-253.847951565799,4.06284513681559,
133.576087959271));
#139141=CARTESIAN_POINT('Ctrl Pts',(-253.855724466116,4.14011297195755,
133.462827450737));
#139142=CARTESIAN_POINT('Ctrl Pts',(-253.863497366433,4.21255930167557,
133.346453528086));
#139143=CARTESIAN_POINT('Ctrl Pts',(-253.87127026675,4.27994712897441,133.227423892779));
#139144=CARTESIAN_POINT('Ctrl Pts',(-253.878760601925,4.34488523349815,
133.11272129427));
#139145=CARTESIAN_POINT('Ctrl Pts',(-253.886250937101,4.40512608899376,
132.99555298893));
#139146=CARTESIAN_POINT('Ctrl Pts',(-253.893741272277,4.46050031135695,
132.876345181911));
#139147=CARTESIAN_POINT('Ctrl Pts',(-253.901515606323,4.51797406815235,
132.752617566131));
#139148=CARTESIAN_POINT('Ctrl Pts',(-253.909289940369,4.57038692897968,
132.626300808125));
#139149=CARTESIAN_POINT('Ctrl Pts',(-253.917064274415,4.61749772082124,
132.497847511732));
#139150=CARTESIAN_POINT('Ctrl Pts',(-253.92482902729,4.66455045282275,132.369552522545));
#139151=CARTESIAN_POINT('Ctrl Pts',(-253.932593780164,4.70631398387226,
132.239126597573));
#139152=CARTESIAN_POINT('Ctrl Pts',(-253.940358533039,4.74259374968307,
132.107045379113));
#139153=CARTESIAN_POINT('Ctrl Pts',(-253.948115573851,4.77883748191978,
131.975095345579));
#139154=CARTESIAN_POINT('Ctrl Pts',(-253.955872614664,4.80960818491979,
131.841493664873));
#139155=CARTESIAN_POINT('Ctrl Pts',(-253.963629655476,4.83476011276247,
131.706733996241));
#139156=CARTESIAN_POINT('Ctrl Pts',(-253.971380846644,4.8598930733414,131.572075950919));
#139157=CARTESIAN_POINT('Ctrl Pts',(-253.979132037812,4.8794156211349,131.43626203859));
#139158=CARTESIAN_POINT('Ctrl Pts',(-253.98688322898,4.89323248619918,131.299798705025));
#139159=CARTESIAN_POINT('Ctrl Pts',(-253.994631125686,4.90704347872852,
131.163393372004));
#139160=CARTESIAN_POINT('Ctrl Pts',(-254.002379022391,4.9151535725004,131.026339554893));
#139161=CARTESIAN_POINT('Ctrl Pts',(-254.010126919097,4.91751905046686,
130.889151246739));
#139162=CARTESIAN_POINT('Ctrl Pts',(-254.01787319511,4.91988403362645,130.751991635413));
#139163=CARTESIAN_POINT('Ctrl Pts',(-254.025619471123,4.91650678439137,
130.614697979661));
#139164=CARTESIAN_POINT('Ctrl Pts',(-254.033365747136,4.90739567298088,
130.477786320799));
#139165=CARTESIAN_POINT('Ctrl Pts',(-254.041112080331,4.89828449431365,
130.340873651278));
#139166=CARTESIAN_POINT('Ctrl Pts',(-254.048858413526,4.88343939497198,
130.204343374377));
#139167=CARTESIAN_POINT('Ctrl Pts',(-254.056604746721,4.86292076533104,
130.068708055134));
#139168=CARTESIAN_POINT('Ctrl Pts',(-254.064352814654,4.84239754068363,
129.933042361292));
#139169=CARTESIAN_POINT('Ctrl Pts',(-254.072100882587,4.81619831596094,
129.798272410412));
#139170=CARTESIAN_POINT('Ctrl Pts',(-254.07984895052,4.78443483398994,129.664901806637));
#139171=CARTESIAN_POINT('Ctrl Pts',(-254.087605253193,4.75263759340677,
129.531389454973));
#139172=CARTESIAN_POINT('Ctrl Pts',(-254.095361555866,4.71526437292624,
129.399279802276));
#139173=CARTESIAN_POINT('Ctrl Pts',(-254.103117858539,4.67247732499925,
129.26906302105));
#139174=CARTESIAN_POINT('Ctrl Pts',(-254.110878300986,4.6296674403329,129.138776739196));
#139175=CARTESIAN_POINT('Ctrl Pts',(-254.118638743432,4.58143810801695,
129.010385707703));
#139176=CARTESIAN_POINT('Ctrl Pts',(-254.126399185878,4.52799977311575,
128.884360326638));
#139177=CARTESIAN_POINT('Ctrl Pts',(-254.134172086077,4.47447565424295,
128.758132638414));
#139178=CARTESIAN_POINT('Ctrl Pts',(-254.141944986276,4.41572599058927,
128.634278542783));
#139179=CARTESIAN_POINT('Ctrl Pts',(-254.149717886475,4.35200775668906,
128.513244830833));
#139180=CARTESIAN_POINT('Ctrl Pts',(-254.157208223013,4.29060583420141,
128.396610986097));
#139181=CARTESIAN_POINT('Ctrl Pts',(-254.164698559551,4.22459046320145,
128.282596296163));
#139182=CARTESIAN_POINT('Ctrl Pts',(-254.172188896089,4.15422866606825,
128.171573643176));
#139183=CARTESIAN_POINT('Ctrl Pts',(-254.179963230165,4.08119908798231,
128.056341545135));
#139184=CARTESIAN_POINT('Ctrl Pts',(-254.187737564241,4.00325565330251,
127.943967827592));
#139185=CARTESIAN_POINT('Ctrl Pts',(-254.195511898317,3.92064879054702,
127.834900039669));
#139186=CARTESIAN_POINT('Ctrl Pts',(-254.203276651221,3.83814373337573,
127.72596666806));
#139187=CARTESIAN_POINT('Ctrl Pts',(-254.211041404124,3.75098691724529,
127.620331428173));
#139188=CARTESIAN_POINT('Ctrl Pts',(-254.218806157027,3.65947334673958,
127.518415108736));
#139189=CARTESIAN_POINT('Ctrl Pts',(-254.226563197868,3.56805066881094,
127.416600014034));
#139190=CARTESIAN_POINT('Ctrl Pts',(-254.234320238708,3.47228010732953,
127.318496778202));
#139191=CARTESIAN_POINT('Ctrl Pts',(-254.242077279549,3.37249821256741,
127.224494856294));
#139192=CARTESIAN_POINT('Ctrl Pts',(-254.249828470744,3.27279156411731,
127.130563821975));
#139193=CARTESIAN_POINT('Ctrl Pts',(-254.257579661939,3.16907988684366,
127.040728212488));
#139194=CARTESIAN_POINT('Ctrl Pts',(-254.265330853134,3.06173777218382,
126.955341927447));
#139195=CARTESIAN_POINT('Ctrl Pts',(-254.273078749865,2.95444128079738,
126.869991933865));
#139196=CARTESIAN_POINT('Ctrl Pts',(-254.280826646596,2.84351772632847,
126.789087746387));
#139197=CARTESIAN_POINT('Ctrl Pts',(-254.288574543327,2.72937591555043,
126.712943971206));
#139198=CARTESIAN_POINT('Ctrl Pts',(-254.296320819365,2.61525798078589,
126.636816123665));
#139199=CARTESIAN_POINT('Ctrl Pts',(-254.304067095402,2.49792345375603,
126.565446924596));
#139200=CARTESIAN_POINT('Ctrl Pts',(-254.31181337144,2.37781101894459,126.499108264836));
#139201=CARTESIAN_POINT('Ctrl Pts',(-254.319559704658,2.25769769749779,
126.432769115384));
#139202=CARTESIAN_POINT('Ctrl Pts',(-254.327306037877,2.13480676958809,
126.371460768358));
#139203=CARTESIAN_POINT('Ctrl Pts',(-254.335052371095,2.00960211317238,
126.315409469555));
#139204=CARTESIAN_POINT('Ctrl Pts',(-254.342800439051,1.88436941804778,
126.259345618454));
#139205=CARTESIAN_POINT('Ctrl Pts',(-254.350548507006,1.75682232014265,
126.208541317943));
#139206=CARTESIAN_POINT('Ctrl Pts',(-254.358296574962,1.62744491561126,
126.16317476596));
#139207=CARTESIAN_POINT('Ctrl Pts',(-254.366052877656,1.49793000724005,
126.117759997867));
#139208=CARTESIAN_POINT('Ctrl Pts',(-254.373809180351,1.36658127588195,
126.077794652661));
#139209=CARTESIAN_POINT('Ctrl Pts',(-254.381565483045,1.23389876490954,
126.043407257108));
#139210=CARTESIAN_POINT('Ctrl Pts',(-254.389325925511,1.10114543728956,
126.009001507968));
#139211=CARTESIAN_POINT('Ctrl Pts',(-254.397086367977,0.967057293625354,
125.980179722764));
#139212=CARTESIAN_POINT('Ctrl Pts',(-254.404846810444,0.832143845516441,
125.957019110836));
#139213=CARTESIAN_POINT('Ctrl Pts',(-254.412619710661,0.697013822361867,
125.933821319437));
#139214=CARTESIAN_POINT('Ctrl Pts',(-254.420392610879,0.561056235268857,
125.916302911662));
#139215=CARTESIAN_POINT('Ctrl Pts',(-254.428165511096,0.424785883249542,
125.90448918906));
#139216=CARTESIAN_POINT('Ctrl Pts',(-254.435655847365,0.293469292076369,
125.893104924191));
#139217=CARTESIAN_POINT('Ctrl Pts',(-254.443146183634,0.161862588416898,
125.887017800988));
#139218=CARTESIAN_POINT('Ctrl Pts',(-254.450636519903,0.0304238206479022,
125.886204717878));
#139219=CARTESIAN_POINT('Ctrl Pts',(-254.458410854369,-0.105998484822487,
125.885360806493));
#139220=CARTESIAN_POINT('Ctrl Pts',(-254.466185188836,-0.242672013207798,
125.890196086895));
#139221=CARTESIAN_POINT('Ctrl Pts',(-254.473959523303,-0.379084865978152,
125.90074177768));
#139222=CARTESIAN_POINT('Ctrl Pts',(-254.481724276599,-0.515329602123221,
125.911274471845));
#139223=CARTESIAN_POINT('Ctrl Pts',(-254.489489029895,-0.651313915803659,
125.927503543881));
#139224=CARTESIAN_POINT('Ctrl Pts',(-254.497253783191,-0.786524328319661,
125.949408244632));
#139225=CARTESIAN_POINT('Ctrl Pts',(-254.505010824425,-0.921600447964142,
125.971291189327));
#139226=CARTESIAN_POINT('Ctrl Pts',(-254.512767865659,-1.05590381265517,
125.998838482507));
#139227=CARTESIAN_POINT('Ctrl Pts',(-254.520524906893,-1.18892484914377,
126.031977484834));
#139228=CARTESIAN_POINT('Ctrl Pts',(-254.528276098483,-1.32184557344231,
126.065091496783));
#139229=CARTESIAN_POINT('Ctrl Pts',(-254.536027290072,-1.45348551648552,
126.103788730564));
#139230=CARTESIAN_POINT('Ctrl Pts',(-254.543778481662,-1.5833444566458,
126.147945323146));
#139231=CARTESIAN_POINT('Ctrl Pts',(-254.551526378788,-1.71314820328092,
126.192083147994));
#139232=CARTESIAN_POINT('Ctrl Pts',(-254.559274275913,-1.84117208322022,
126.241675590997));
#139233=CARTESIAN_POINT('Ctrl Pts',(-254.567022173039,-1.96693043928436,
126.296548763738));
#139234=CARTESIAN_POINT('Ctrl Pts',(-254.574768449471,-2.09266248940304,
126.35141045819));
#139235=CARTESIAN_POINT('Ctrl Pts',(-254.582514725904,-2.21612960014617,
126.411550528982));
#139236=CARTESIAN_POINT('Ctrl Pts',(-254.590261002336,-2.33686590233866,
126.476746862044));
#139237=CARTESIAN_POINT('Ctrl Pts',(-254.598007335948,-2.45760309576507,
126.541943676362));
#139238=CARTESIAN_POINT('Ctrl Pts',(-254.605753669561,-2.57560909640333,
126.612196641663));
#139239=CARTESIAN_POINT('Ctrl Pts',(-254.613500003173,-2.6904428198599,
126.687237775633));
#139240=CARTESIAN_POINT('Ctrl Pts',(-254.621248071522,-2.8053022595138,
126.762295714532));
#139241=CARTESIAN_POINT('Ctrl Pts',(-254.628996139871,-2.9169876811357,
126.842143741976));
#139242=CARTESIAN_POINT('Ctrl Pts',(-254.63674420822,-3.02508749592522,
126.92647089447));
#139243=CARTESIAN_POINT('Ctrl Pts',(-254.644500511304,-3.13330220042483,
127.010887670818));
#139244=CARTESIAN_POINT('Ctrl Pts',(-254.652256814388,-3.23792337680575,
127.099792840901));
#139245=CARTESIAN_POINT('Ctrl Pts',(-254.660013117472,-3.33857260616974,
127.192835175896));
#139246=CARTESIAN_POINT('Ctrl Pts',(-254.667773560327,-3.43927555503557,
127.285927170365));
#139247=CARTESIAN_POINT('Ctrl Pts',(-254.675534003181,-3.53600205711497,
127.383160452591));
#139248=CARTESIAN_POINT('Ctrl Pts',(-254.683294446036,-3.62841175050696,
127.484148089537));
#139249=CARTESIAN_POINT('Ctrl Pts',(-254.691067346636,-3.72096978806263,
127.585297840715));
#139250=CARTESIAN_POINT('Ctrl Pts',(-254.698840247236,-3.80919691736656,
127.690213690724));
#139251=CARTESIAN_POINT('Ctrl Pts',(-254.706613147835,-3.89279359003628,
127.798476200648));
#139252=CARTESIAN_POINT('Ctrl Pts',(-254.714103479795,-3.97335126873092,
127.902803038195));
#139253=CARTESIAN_POINT('Ctrl Pts',(-254.721593811756,-4.04960912989874,
128.0102371864));
#139254=CARTESIAN_POINT('Ctrl Pts',(-254.729084143716,-4.12133902359766,
128.120380789946));
#139255=CARTESIAN_POINT('Ctrl Pts',(-254.737024238098,-4.19737599085458,
128.237138046155));
#139256=CARTESIAN_POINT('Ctrl Pts',(-254.74496433248,-4.26855771158485,
128.357297650974));
#139257=CARTESIAN_POINT('Ctrl Pts',(-254.752904426862,-4.33457263714298,
128.480427934412));
#139258=CARTESIAN_POINT('Ctrl Pts',(-254.760834559692,-4.40050474112921,
128.603403740002));
#139259=CARTESIAN_POINT('Ctrl Pts',(-254.768764692523,-4.46128277734,128.729342485631));
#139260=CARTESIAN_POINT('Ctrl Pts',(-254.776694825353,-4.5166380372809,
128.857783133188));
#139261=CARTESIAN_POINT('Ctrl Pts',(-254.784613472957,-4.57191312609647,
128.986037759917));
#139262=CARTESIAN_POINT('Ctrl Pts',(-254.792532120561,-4.62178094224067,
129.116786732569));
#139263=CARTESIAN_POINT('Ctrl Pts',(-254.800450768166,-4.66601867417977,
129.249544617293));
#139264=CARTESIAN_POINT('Ctrl Pts',(-254.806994411848,-4.70257491074876,
129.359250256068));
#139265=CARTESIAN_POINT('Ctrl Pts',(-254.813538055531,-4.73528730506565,
129.470327152778));
#139266=CARTESIAN_POINT('Ctrl Pts',(-254.820081699213,-4.76405452823395,
129.582490119308));
#139267=CARTESIAN_POINT('Origin',(213.235140564004,0.,130.804360617566));
#139268=CARTESIAN_POINT('',(-256.915106732785,-4.76405452823404,129.582490119308));
#139269=CARTESIAN_POINT('',(-256.569732696692,-4.76405452823406,129.582490119308));
#139270=CARTESIAN_POINT('',(213.235140564004,-4.76405452823405,129.582490119308));
#139271=CARTESIAN_POINT('',(-255.235140563976,-4.91824902737425,130.807453711842));
#139272=CARTESIAN_POINT('Ctrl Pts',(-255.235140564014,-4.91824902737384,
130.807453712504));
#139273=CARTESIAN_POINT('Ctrl Pts',(-255.245557174403,-4.91813385884421,
130.990580166781));
#139274=CARTESIAN_POINT('Ctrl Pts',(-255.255973784792,-4.90779148807459,
131.173384516713));
#139275=CARTESIAN_POINT('Ctrl Pts',(-255.266390395181,-4.88732539910615,
131.355027037236));
#139276=CARTESIAN_POINT('Ctrl Pts',(-255.27416472986,-4.87205073496179,
131.490594145323));
#139277=CARTESIAN_POINT('Ctrl Pts',(-255.281939064539,-4.85110695834174,
131.6257399563));
#139278=CARTESIAN_POINT('Ctrl Pts',(-255.289713399218,-4.82452352870267,
131.759952467413));
#139279=CARTESIAN_POINT('Ctrl Pts',(-255.297478152694,-4.79797286086927,
131.893999573074));
#139280=CARTESIAN_POINT('Ctrl Pts',(-255.30524290617,-4.76579644445566,
132.027115287618));
#139281=CARTESIAN_POINT('Ctrl Pts',(-255.313007659645,-4.72807552956579,
132.158792177011));
#139282=CARTESIAN_POINT('Ctrl Pts',(-255.320764701028,-4.69039207976998,
132.290338282539));
#139283=CARTESIAN_POINT('Ctrl Pts',(-255.32852174241,-4.64717519744029,
132.420448033409));
#139284=CARTESIAN_POINT('Ctrl Pts',(-255.336278783793,-4.59855719839869,
132.548624002366));
#139285=CARTESIAN_POINT('Ctrl Pts',(-255.344029975499,-4.54997586276346,
132.676703312315));
#139286=CARTESIAN_POINT('Ctrl Pts',(-255.351781167205,-4.49600165566221,
132.802851378912));
#139287=CARTESIAN_POINT('Ctrl Pts',(-255.359532358911,-4.43681665357432,
132.92658611102));
#139288=CARTESIAN_POINT('Ctrl Pts',(-255.367280256105,-4.3776568070638,
133.050268251787));
#139289=CARTESIAN_POINT('Ctrl Pts',(-255.375028153299,-4.3132907389033,
133.171538746241));
#139290=CARTESIAN_POINT('Ctrl Pts',(-255.382776050493,-4.2439484806307,
133.289935874172));
#139291=CARTESIAN_POINT('Ctrl Pts',(-255.390522326964,-4.17462072752967,
133.408308235522));
#139292=CARTESIAN_POINT('Ctrl Pts',(-255.398268603435,-4.10031905224497,
133.523808088737));
#139293=CARTESIAN_POINT('Ctrl Pts',(-255.406014879907,-4.02131903729324,
133.635999058964));
#139294=CARTESIAN_POINT('Ctrl Pts',(-255.413761213529,-3.94231843948762,
133.748190856924));
#139295=CARTESIAN_POINT('Ctrl Pts',(-255.421507547151,-3.85861965794036,
133.857073403517));
#139296=CARTESIAN_POINT('Ctrl Pts',(-255.429253880774,-3.77054089507489,
133.962240352621));
#139297=CARTESIAN_POINT('Ctrl Pts',(-255.437001949104,-3.68244240792615,
134.067430852721));
#139298=CARTESIAN_POINT('Ctrl Pts',(-255.444750017433,-3.58996223866315,
134.168903799941));
#139299=CARTESIAN_POINT('Ctrl Pts',(-255.452498085763,-3.49345778637573,
134.266287213742));
#139300=CARTESIAN_POINT('Ctrl Pts',(-255.460254388783,-3.39685076862586,
134.36377412717));
#139301=CARTESIAN_POINT('Ctrl Pts',(-255.468010691802,-3.29621119965999,
134.457162546673));
#139302=CARTESIAN_POINT('Ctrl Pts',(-255.475766994821,-3.19193254441991,
134.546118185123));
#139303=CARTESIAN_POINT('Ctrl Pts',(-255.483527437587,-3.08759823287794,
134.635121301573));
#139304=CARTESIAN_POINT('Ctrl Pts',(-255.491287880352,-2.97962127256047,
134.719686681781));
#139305=CARTESIAN_POINT('Ctrl Pts',(-255.499048323118,-2.86842608786575,
134.799522046213));
#139306=CARTESIAN_POINT('Ctrl Pts',(-255.506821223587,-2.75705240347212,
134.87948556897));
#139307=CARTESIAN_POINT('Ctrl Pts',(-255.514594124056,-2.6424504981078,
134.954703688043));
#139308=CARTESIAN_POINT('Ctrl Pts',(-255.522367024526,-2.52507225411039,
135.024928490971));
#139309=CARTESIAN_POINT('Ctrl Pts',(-255.529857356015,-2.41196107242921,
135.09260040505));
#139310=CARTESIAN_POINT('Ctrl Pts',(-255.537347687505,-2.29627217499392,
135.155635597492));
#139311=CARTESIAN_POINT('Ctrl Pts',(-255.544838018994,-2.17842757880106,
135.213854505352));
#139312=CARTESIAN_POINT('Ctrl Pts',(-255.552612366624,-2.05611458658772,
135.274280940281));
#139313=CARTESIAN_POINT('Ctrl Pts',(-255.560386714254,-1.93109174547298,
135.329710048654));
#139314=CARTESIAN_POINT('Ctrl Pts',(-255.568161061884,-1.80380574339727,
135.379889865925));
#139315=CARTESIAN_POINT('Ctrl Pts',(-255.575925828398,-1.67667660875542,
135.430007841523));
#139316=CARTESIAN_POINT('Ctrl Pts',(-255.583690594912,-1.5472902229039,
135.474889255854));
#139317=CARTESIAN_POINT('Ctrl Pts',(-255.591455361427,-1.41611742396956,
135.514328186884));
#139318=CARTESIAN_POINT('Ctrl Pts',(-255.59921241592,-1.28507490678246,
135.553727946891));
#139319=CARTESIAN_POINT('Ctrl Pts',(-255.606969470413,-1.15224987939031,
135.58769586897));
#139320=CARTESIAN_POINT('Ctrl Pts',(-255.614726524906,-1.01813236307906,
135.616074403085));
#139321=CARTESIAN_POINT('Ctrl Pts',(-255.622477729782,-0.884115985187912,
135.644431536862));
#139322=CARTESIAN_POINT('Ctrl Pts',(-255.630228934657,-0.748809439346092,
135.667207591719));
#139323=CARTESIAN_POINT('Ctrl Pts',(-255.637980139532,-0.612716740876425,
135.684295172245));
#139324=CARTESIAN_POINT('Ctrl Pts',(-255.645728049937,-0.476681885459189,
135.70137549009));
#139325=CARTESIAN_POINT('Ctrl Pts',(-255.653475960342,-0.339861929090951,
135.712772093729));
#139326=CARTESIAN_POINT('Ctrl Pts',(-255.661223870747,-0.202769669246156,
135.718428944699));
#139327=CARTESIAN_POINT('Ctrl Pts',(-255.668970160453,-0.0657060862072468,
135.724084612376));
#139328=CARTESIAN_POINT('Ctrl Pts',(-255.676716450159,0.0716292966275856,
135.724002899405));
#139329=CARTESIAN_POINT('Ctrl Pts',(-255.684462739865,0.208720384205294,
135.718179790441));
#139330=CARTESIAN_POINT('Ctrl Pts',(-255.692209086732,0.345812483418953,
135.712356638507));
#139331=CARTESIAN_POINT('Ctrl Pts',(-255.6999554336,0.482659893166817,135.700792022632));
#139332=CARTESIAN_POINT('Ctrl Pts',(-255.707701780468,0.618748745367988,
135.683534016064));
#139333=CARTESIAN_POINT('Ctrl Pts',(-255.715449862042,0.754868073110716,
135.666272144762));
#139334=CARTESIAN_POINT('Ctrl Pts',(-255.723197943616,0.890228117501376,
135.643314394903));
#139335=CARTESIAN_POINT('Ctrl Pts',(-255.730946025189,1.02432273647311,
135.614760392433));
#139336=CARTESIAN_POINT('Ctrl Pts',(-255.738702341375,1.1585598703514,135.586176042952));
#139337=CARTESIAN_POINT('Ctrl Pts',(-255.74645865756,1.2915285092558,135.551983641321));
#139338=CARTESIAN_POINT('Ctrl Pts',(-255.754214973746,1.42273472920243,
135.512333530914));
#139339=CARTESIAN_POINT('Ctrl Pts',(-255.761975429655,1.55401097692936,
135.472662258331));
#139340=CARTESIAN_POINT('Ctrl Pts',(-255.769735885565,1.68352256238016,
135.42752760136));
#139341=CARTESIAN_POINT('Ctrl Pts',(-255.777496341475,1.81079416939543,
135.377128656575));
#139342=CARTESIAN_POINT('Ctrl Pts',(-255.785269254919,1.93827008016889,
135.326648808484));
#139343=CARTESIAN_POINT('Ctrl Pts',(-255.793042168362,2.06349846970333,
135.27088794483));
#139344=CARTESIAN_POINT('Ctrl Pts',(-255.800815081806,2.18602650742093,
135.210092244816));
#139345=CARTESIAN_POINT('Ctrl Pts',(-255.808305268806,2.30409779716003,
135.151507884494));
#139346=CARTESIAN_POINT('Ctrl Pts',(-255.815795455806,2.41966149372262,
135.088248740042));
#139347=CARTESIAN_POINT('Ctrl Pts',(-255.823285642807,2.53233843750942,
135.020572792067));
#139348=CARTESIAN_POINT('Ctrl Pts',(-255.831059947351,2.64928943966847,
134.950329762112));
#139349=CARTESIAN_POINT('Ctrl Pts',(-255.838834251894,2.76350083179706,
134.875105728614));
#139350=CARTESIAN_POINT('Ctrl Pts',(-255.846608556438,2.87451918596033,
134.795140304801));
#139351=CARTESIAN_POINT('Ctrl Pts',(-255.854373279807,2.98540071936351,
134.715273431629));
#139352=CARTESIAN_POINT('Ctrl Pts',(-255.862138003176,3.09309673038082,
134.630677021003));
#139353=CARTESIAN_POINT('Ctrl Pts',(-255.869902726545,3.19717947386991,
134.541635891661));
#139354=CARTESIAN_POINT('Ctrl Pts',(-255.877659737879,3.30115884088379,
134.452683199247));
#139355=CARTESIAN_POINT('Ctrl Pts',(-255.885416749213,3.40153178697501,
134.359294825797));
#139356=CARTESIAN_POINT('Ctrl Pts',(-255.893173760547,3.49790089452245,
134.261797875796));
#139357=CARTESIAN_POINT('Ctrl Pts',(-255.900924922294,3.59419732981155,
134.164374448564));
#139358=CARTESIAN_POINT('Ctrl Pts',(-255.908676084041,3.68649566257353,
134.062848888677));
#139359=CARTESIAN_POINT('Ctrl Pts',(-255.916427245787,3.77443310740116,
133.957587184157));
#139360=CARTESIAN_POINT('Ctrl Pts',(-255.92417511326,3.86233317847696,133.852370216265));
#139361=CARTESIAN_POINT('Ctrl Pts',(-255.931922980733,3.94587579774067,
133.743420561318));
#139362=CARTESIAN_POINT('Ctrl Pts',(-255.939670848206,4.02473664074394,
133.631139355839));
#139363=CARTESIAN_POINT('Ctrl Pts',(-255.947417095106,4.10358098890874,
133.518881635531));
#139364=CARTESIAN_POINT('Ctrl Pts',(-255.955163342005,4.17774528404333,
133.403294070481));
#139365=CARTESIAN_POINT('Ctrl Pts',(-255.962909588904,4.24694718773835,
133.284808691415));
#139366=CARTESIAN_POINT('Ctrl Pts',(-255.970655893131,4.31614960357181,
133.166322435481));
#139367=CARTESIAN_POINT('Ctrl Pts',(-255.978402197357,4.380389357505,133.044938660342));
#139368=CARTESIAN_POINT('Ctrl Pts',(-255.986148501584,4.43942913845158,
132.921115678306));
#139369=CARTESIAN_POINT('Ctrl Pts',(-255.993896540721,4.4984821423154,132.797264964102));
#139370=CARTESIAN_POINT('Ctrl Pts',(-256.001644579858,4.55233268750128,
132.670974308765));
#139371=CARTESIAN_POINT('Ctrl Pts',(-256.009392618995,4.60079101177705,
132.542723389962));
#139372=CARTESIAN_POINT('Ctrl Pts',(-256.017148893306,4.64930084105,132.414336156845));
#139373=CARTESIAN_POINT('Ctrl Pts',(-256.024905167617,4.6924068622338,132.283984864543));
#139374=CARTESIAN_POINT('Ctrl Pts',(-256.032661441928,4.72996858728783,
132.152166325289));
#139375=CARTESIAN_POINT('Ctrl Pts',(-256.040421856202,4.76755036116648,
132.020277426999));
#139376=CARTESIAN_POINT('Ctrl Pts',(-256.048182270477,4.79958185098399,
131.886920101229));
#139377=CARTESIAN_POINT('Ctrl Pts',(-256.055942684752,4.82597364416927,
131.752601857063));
#139378=CARTESIAN_POINT('Ctrl Pts',(-256.063715557391,4.85240780604265,
131.618067981934));
#139379=CARTESIAN_POINT('Ctrl Pts',(-256.071488430031,4.87318411957688,
131.482570492412));
#139380=CARTESIAN_POINT('Ctrl Pts',(-256.07926130267,4.88826493817758,131.346623429018));
#139381=CARTESIAN_POINT('Ctrl Pts',(-256.086751957319,4.90279820138934,
131.215612340861));
#139382=CARTESIAN_POINT('Ctrl Pts',(-256.094242611969,4.91204236174855,
131.084184066446));
#139383=CARTESIAN_POINT('Ctrl Pts',(-256.101733266619,4.91600952625544,
130.952797136879));
#139384=CARTESIAN_POINT('Ctrl Pts',(-256.109507612938,4.92012693818049,
130.816434223354));
#139385=CARTESIAN_POINT('Ctrl Pts',(-256.117281959258,4.91857281033011,
130.679683873794));
#139386=CARTESIAN_POINT('Ctrl Pts',(-256.125056305577,4.91130364868276,
130.543057091116));
#139387=CARTESIAN_POINT('Ctrl Pts',(-256.132821070531,4.90404344579439,
130.406598691873));
#139388=CARTESIAN_POINT('Ctrl Pts',(-256.140585835484,4.89108224394783,
130.270263943168));
#139389=CARTESIAN_POINT('Ctrl Pts',(-256.148350600438,4.87242846398543,
130.134566674741));
#139390=CARTESIAN_POINT('Ctrl Pts',(-256.156107653126,4.85379321167978,
129.999004186098));
#139391=CARTESIAN_POINT('Ctrl Pts',(-256.163864705815,4.8294766860502,129.864078302512));
#139392=CARTESIAN_POINT('Ctrl Pts',(-256.171621758503,4.79953927689507,
129.730300194665));
#139393=CARTESIAN_POINT('Ctrl Pts',(-256.179372961334,4.76962444456061,
129.59662297345));
#139394=CARTESIAN_POINT('Ctrl Pts',(-256.187124164164,4.7340972510083,129.464092185079));
#139395=CARTESIAN_POINT('Ctrl Pts',(-256.194875366995,4.69306951939789,
129.333210880592));
#139396=CARTESIAN_POINT('Ctrl Pts',(-256.202623275001,4.65205922755306,
129.202385210165));
#139397=CARTESIAN_POINT('Ctrl Pts',(-256.210371183007,4.60555316471098,
129.073208001369));
#139398=CARTESIAN_POINT('Ctrl Pts',(-256.218119091014,4.55371351452655,
128.946168945505));
#139399=CARTESIAN_POINT('Ctrl Pts',(-256.225865378107,4.50188470954078,
128.819156467054));
#139400=CARTESIAN_POINT('Ctrl Pts',(-256.233611665199,4.44472468426253,
128.694281613556));
#139401=CARTESIAN_POINT('Ctrl Pts',(-256.241357952292,4.38244430899901,
128.572015451374));
#139402=CARTESIAN_POINT('Ctrl Pts',(-256.249104296336,4.32016347584558,
128.449748390282));
#139403=CARTESIAN_POINT('Ctrl Pts',(-256.25685064038,4.25276239504261,128.330090407149));
#139404=CARTESIAN_POINT('Ctrl Pts',(-256.264596984424,4.18049838674326,
128.213488891498));
#139405=CARTESIAN_POINT('Ctrl Pts',(-256.272345062966,4.10821819767546,
128.096861267386));
#139406=CARTESIAN_POINT('Ctrl Pts',(-256.280093141508,4.03107312030725,
127.983291804847));
#139407=CARTESIAN_POINT('Ctrl Pts',(-256.287841220051,3.94936415147337,
127.873199437836));
#139408=CARTESIAN_POINT('Ctrl Pts',(-256.295597532897,3.86756834608115,
127.762990069688));
#139409=CARTESIAN_POINT('Ctrl Pts',(-256.303353845743,3.78119919361253,
127.656265493271));
#139410=CARTESIAN_POINT('Ctrl Pts',(-256.311110158589,3.69059874068027,
127.553412448525));
#139411=CARTESIAN_POINT('Ctrl Pts',(-256.318870610986,3.59994993419757,
127.450504511009));
#139412=CARTESIAN_POINT('Ctrl Pts',(-256.326631063385,3.50506559784399,
127.351472504486));
#139413=CARTESIAN_POINT('Ctrl Pts',(-256.334391515782,3.40632438553531,
127.256665979776));
#139414=CARTESIAN_POINT('Ctrl Pts',(-256.342164425457,3.30742467131085,
127.16170726921));
#139415=CARTESIAN_POINT('Ctrl Pts',(-256.349937335131,3.20465600249904,
127.07098785364));
#139416=CARTESIAN_POINT('Ctrl Pts',(-256.357710244805,3.0984305090419,126.98481726225));
#139417=CARTESIAN_POINT('Ctrl Pts',(-256.365200460014,2.99606835123671,
126.901780625875));
#139418=CARTESIAN_POINT('Ctrl Pts',(-256.372690675223,2.89049669188504,
126.822967871032));
#139419=CARTESIAN_POINT('Ctrl Pts',(-256.380180890432,2.78210777718279,
126.748616619403));
#139420=CARTESIAN_POINT('Ctrl Pts',(-256.387955305096,2.6696062876589,126.671444275909));
#139421=CARTESIAN_POINT('Ctrl Pts',(-256.39572971976,2.55371319387958,126.598834247598));
#139422=CARTESIAN_POINT('Ctrl Pts',(-256.403504134424,2.43483491863965,
126.53109933589));
#139423=CARTESIAN_POINT('Ctrl Pts',(-256.411268968321,2.3161031425358,126.463447897011));
#139424=CARTESIAN_POINT('Ctrl Pts',(-256.419033802218,2.19439384106692,
126.400659812629));
#139425=CARTESIAN_POINT('Ctrl Pts',(-256.426798636115,2.07014387587007,
126.343005734159));
#139426=CARTESIAN_POINT('Ctrl Pts',(-256.434555758268,1.94601731112681,
126.28540891558));
#139427=CARTESIAN_POINT('Ctrl Pts',(-256.44231288042,1.81935545646732,126.232936119353));
#139428=CARTESIAN_POINT('Ctrl Pts',(-256.450070002572,1.69062102621373,
126.185812836258));
#139429=CARTESIAN_POINT('Ctrl Pts',(-256.45782127531,1.56198367075648,126.138725087427));
#139430=CARTESIAN_POINT('Ctrl Pts',(-256.465572548048,1.43127721614667,
126.09697895632));
#139431=CARTESIAN_POINT('Ctrl Pts',(-256.473323820785,1.29898534580503,
126.060752272236));
#139432=CARTESIAN_POINT('Ctrl Pts',(-256.481071799121,1.1667497013993,126.024540985011));
#139433=CARTESIAN_POINT('Ctrl Pts',(-256.488819777457,1.03293035773216,
125.993844582143));
#139434=CARTESIAN_POINT('Ctrl Pts',(-256.496567755794,0.898026978859469,
125.968791301783));
#139435=CARTESIAN_POINT('Ctrl Pts',(-256.504314113463,0.763151818115598,
125.94374326189));
#139436=CARTESIAN_POINT('Ctrl Pts',(-256.512060471132,0.627193457326346,
125.924336067988));
#139437=CARTESIAN_POINT('Ctrl Pts',(-256.519806828801,0.490662206737524,
125.910646929437));
#139438=CARTESIAN_POINT('Ctrl Pts',(-256.5275532436,0.354129949215721,125.896957689928));
#139439=CARTESIAN_POINT('Ctrl Pts',(-256.535299658399,0.217025182469028,
125.888986628924));
#139440=CARTESIAN_POINT('Ctrl Pts',(-256.543046073199,0.0798634036778129,
125.886759078273));
#139441=CARTESIAN_POINT('Ctrl Pts',(-256.550794222607,-0.0573290889515717,
125.88453102882));
#139442=CARTESIAN_POINT('Ctrl Pts',(-256.558542372016,-0.194578228199409,
125.88804905528));
#139443=CARTESIAN_POINT('Ctrl Pts',(-256.566290521425,-0.331368849287899,
125.897286362144));
#139444=CARTESIAN_POINT('Ctrl Pts',(-256.574046904909,-0.468304839833111,
125.906533485634));
#139445=CARTESIAN_POINT('Ctrl Pts',(-256.581803288393,-0.604780948146652,
125.921512004537));
#139446=CARTESIAN_POINT('Ctrl Pts',(-256.589559671878,-0.740286906957838,
125.942143185377));
#139447=CARTESIAN_POINT('Ctrl Pts',(-256.597320194901,-0.875865184559755,
125.962785376964));
#139448=CARTESIAN_POINT('Ctrl Pts',(-256.605080717925,-1.01047189745824,
125.989086166776));
#139449=CARTESIAN_POINT('Ctrl Pts',(-256.612841240949,-1.14360827952286,
126.020915920958));
#139450=CARTESIAN_POINT('Ctrl Pts',(-256.620614220507,-1.27695836084543,
126.052796765569));
#139451=CARTESIAN_POINT('Ctrl Pts',(-256.628387200066,-1.40883301888172,
126.090224202077));
#139452=CARTESIAN_POINT('Ctrl Pts',(-256.636160179625,-1.53874906425391,
126.133018799656));
#139453=CARTESIAN_POINT('Ctrl Pts',(-256.643649624498,-1.66392616688881,
126.174252380296));
#139454=CARTESIAN_POINT('Ctrl Pts',(-256.651139069372,-1.78728476738983,
126.220468281193));
#139455=CARTESIAN_POINT('Ctrl Pts',(-256.658628514245,-1.90841305938302,
126.271465002479));
#139456=CARTESIAN_POINT('Ctrl Pts',(-256.666403063451,-2.03415240084404,
126.3244030407));
#139457=CARTESIAN_POINT('Ctrl Pts',(-256.674177612657,-2.15788660754819,
126.382660805064));
#139458=CARTESIAN_POINT('Ctrl Pts',(-256.681952161862,-2.27913277366472,
126.446065439115));
#139459=CARTESIAN_POINT('Ctrl Pts',(-256.68971703315,-2.40022801007117,
126.50939114578));
#139460=CARTESIAN_POINT('Ctrl Pts',(-256.697481904438,-2.51884102536472,
126.577850794189));
#139461=CARTESIAN_POINT('Ctrl Pts',(-256.705246775725,-2.63450794188062,
126.651223132884));
#139462=CARTESIAN_POINT('Ctrl Pts',(-256.71300383883,-2.75005854629814,
126.724521689975));
#139463=CARTESIAN_POINT('Ctrl Pts',(-256.720760901934,-2.86266861975698,
126.802722897663));
#139464=CARTESIAN_POINT('Ctrl Pts',(-256.728517965039,-2.97189832430596,
126.885559345176));
#139465=CARTESIAN_POINT('Ctrl Pts',(-256.736292497028,-3.08137401385148,
126.968582340142));
#139466=CARTESIAN_POINT('Ctrl Pts',(-256.744067029018,-3.18745374186974,
127.056261291037));
#139467=CARTESIAN_POINT('Ctrl Pts',(-256.751841561007,-3.28972276324023,
127.148282499757));
#139468=CARTESIAN_POINT('Ctrl Pts',(-256.759588911131,-3.39163422447051,
127.23998197746));
#139469=CARTESIAN_POINT('Ctrl Pts',(-256.767336261256,-3.48976128720013,
127.335993139251));
#139470=CARTESIAN_POINT('Ctrl Pts',(-256.77508361138,-3.58372615583562,
127.435964871446));
#139471=CARTESIAN_POINT('Ctrl Pts',(-256.782829210042,-3.67766978161093,
127.535914002795));
#139472=CARTESIAN_POINT('Ctrl Pts',(-256.790574808705,-3.76745281825126,
127.639821638118));
#139473=CARTESIAN_POINT('Ctrl Pts',(-256.798320407367,-3.85273467051478,
127.747300163288));
#139474=CARTESIAN_POINT('Ctrl Pts',(-256.806065932552,-3.93801571375518,
127.854777668866));
#139475=CARTESIAN_POINT('Ctrl Pts',(-256.813811457736,-4.01879541538737,
127.965825690128));
#139476=CARTESIAN_POINT('Ctrl Pts',(-256.82155698292,-4.09477403842602,
128.080024251268));
#139477=CARTESIAN_POINT('Ctrl Pts',(-256.829352795409,-4.17124594759677,
128.194964238935));
#139478=CARTESIAN_POINT('Ctrl Pts',(-256.837148607897,-4.24285397776989,
128.313095497808));
#139479=CARTESIAN_POINT('Ctrl Pts',(-256.844944420386,-4.309337732552,128.433961628091));
#139480=CARTESIAN_POINT('Ctrl Pts',(-256.852698030591,-4.37546158048252,
128.55417345495));
#139481=CARTESIAN_POINT('Ctrl Pts',(-256.860451640795,-4.43651636272949,
128.677090242758));
#139482=CARTESIAN_POINT('Ctrl Pts',(-256.868205250999,-4.49229316026251,
128.80224043517));
#139483=CARTESIAN_POINT('Ctrl Pts',(-256.87602216463,-4.54852534081278,
128.928412401415));
#139484=CARTESIAN_POINT('Ctrl Pts',(-256.883839078261,-4.59939281359841,
129.056854029583));
#139485=CARTESIAN_POINT('Ctrl Pts',(-256.891655991892,-4.64473216300896,
129.187064665549));
#139486=CARTESIAN_POINT('Ctrl Pts',(-256.899472905523,-4.69007151241964,
129.317275301515));
#139487=CARTESIAN_POINT('Ctrl Pts',(-256.907289819154,-4.72988266582926,
129.449254546422));
#139488=CARTESIAN_POINT('Ctrl Pts',(-256.915106732785,-4.76405452823404,
129.582490119308));
#139489=CARTESIAN_POINT('Ctrl Pts',(-255.165002394563,-4.76405452823405,
129.582490119308));
#139490=CARTESIAN_POINT('Ctrl Pts',(-255.172655166336,-4.79770872156121,
129.713707308317));
#139491=CARTESIAN_POINT('Ctrl Pts',(-255.180307938108,-4.82591576732456,
129.846231170376));
#139492=CARTESIAN_POINT('Ctrl Pts',(-255.187960709881,-4.84859700324015,
129.979563574245));
#139493=CARTESIAN_POINT('Ctrl Pts',(-255.195824018897,-4.87190222808818,
130.116564117922));
#139494=CARTESIAN_POINT('Ctrl Pts',(-255.203687327913,-4.88937314622007,
130.254417878155));
#139495=CARTESIAN_POINT('Ctrl Pts',(-255.211550636929,-4.90098157013989,
130.392580686475));
#139496=CARTESIAN_POINT('Ctrl Pts',(-255.219413945945,-4.91258999405968,
130.530743494795));
#139497=CARTESIAN_POINT('Ctrl Pts',(-255.22727725496,-4.91833596597612,
130.669214894679));
#139498=CARTESIAN_POINT('Ctrl Pts',(-255.235140563976,-4.91824902737425,
130.807453711842));
#139499=CARTESIAN_POINT('',(-254.88985943604,-4.91824957686614,130.806400753838));
#139500=CARTESIAN_POINT('Ctrl Pts',(-254.820081699213,-4.76405452823395,
129.582490119308));
#139501=CARTESIAN_POINT('Ctrl Pts',(-254.827987033215,-4.79880802620788,
129.71799348045));
#139502=CARTESIAN_POINT('Ctrl Pts',(-254.835892367217,-4.8278021954462,
129.855082133978));
#139503=CARTESIAN_POINT('Ctrl Pts',(-254.843797701219,-4.85090328122655,
129.993237680715));
#139504=CARTESIAN_POINT('Ctrl Pts',(-254.851697709623,-4.87398880446313,
130.131300155994));
#139505=CARTESIAN_POINT('Ctrl Pts',(-254.859597718027,-4.89118909248049,
130.270427729865));
#139506=CARTESIAN_POINT('Ctrl Pts',(-254.867497726431,-4.90242129645858,
130.410091046676));
#139507=CARTESIAN_POINT('Ctrl Pts',(-254.874951629619,-4.91301922962145,
130.541867722008));
#139508=CARTESIAN_POINT('Ctrl Pts',(-254.882405532808,-4.91830444773814,
130.674120990215));
#139509=CARTESIAN_POINT('Ctrl Pts',(-254.889859435997,-4.91824957686646,
130.806400753076));
#139510=CARTESIAN_POINT('Ctrl Pts',(-254.88985943604,-4.91824957686614,
130.806400753838));
#139511=CARTESIAN_POINT('Ctrl Pts',(-254.898291060281,-4.91818750861372,
130.956031521351));
#139512=CARTESIAN_POINT('Ctrl Pts',(-254.906722684522,-4.91129283825743,
131.105445383408));
#139513=CARTESIAN_POINT('Ctrl Pts',(-254.915154308762,-4.8976496465132,
131.254039394594));
#139514=CARTESIAN_POINT('Ctrl Pts',(-254.923623830761,-4.88394513249381,
131.403301293691));
#139515=CARTESIAN_POINT('Ctrl Pts',(-254.932093352761,-4.86343138027049,
131.551735692772));
#139516=CARTESIAN_POINT('Ctrl Pts',(-254.94056287476,-4.8362441535837,131.698746188462));
#139517=CARTESIAN_POINT('Ctrl Pts',(-254.949051704908,-4.80899494759928,
131.8460918271));
#139518=CARTESIAN_POINT('Ctrl Pts',(-254.957540535056,-4.77504192517439,
131.992006814685));
#139519=CARTESIAN_POINT('Ctrl Pts',(-254.966029365204,-4.73457087064609,
132.135909239784));
#139520=CARTESIAN_POINT('Ctrl Pts',(-254.97454688385,-4.69396304182292,
132.280297991541));
#139521=CARTESIAN_POINT('Ctrl Pts',(-254.983064402496,-4.64679317755957,
132.422660312185));
#139522=CARTESIAN_POINT('Ctrl Pts',(-254.991581921142,-4.59329646968355,
132.56243075385));
#139523=CARTESIAN_POINT('Ctrl Pts',(-254.996898536605,-4.55990394821213,
132.649675140648));
#139524=CARTESIAN_POINT('Ctrl Pts',(-255.002215152067,-4.52404728017144,
132.7359101305));
#139525=CARTESIAN_POINT('Ctrl Pts',(-255.007531767529,-4.48579264567317,
132.821003224109));
#139526=CARTESIAN_POINT('Ctrl Pts',(-255.015306101543,-4.42985399291509,
132.945432409695));
#139527=CARTESIAN_POINT('Ctrl Pts',(-255.023080435558,-4.3686455941954,
133.067729436475));
#139528=CARTESIAN_POINT('Ctrl Pts',(-255.030854769572,-4.30235183476065,
133.187415747527));
#139529=CARTESIAN_POINT('Ctrl Pts',(-255.038619522409,-4.23613977650277,
133.306954555818));
#139530=CARTESIAN_POINT('Ctrl Pts',(-255.046384275247,-4.16485501511812,
133.423888711477));
#139531=CARTESIAN_POINT('Ctrl Pts',(-255.054149028084,-4.08872985823644,
133.537759821646));
#139532=CARTESIAN_POINT('Ctrl Pts',(-255.061906068855,-4.01268030998117,
133.651517833353));
#139533=CARTESIAN_POINT('Ctrl Pts',(-255.069663109626,-3.93180014935378,
133.762218530888));
#139534=CARTESIAN_POINT('Ctrl Pts',(-255.077420150396,-3.84636725562247,
133.869428642484));
#139535=CARTESIAN_POINT('Ctrl Pts',(-255.085171341517,-3.76099878755241,
133.976557906036));
#139536=CARTESIAN_POINT('Ctrl Pts',(-255.092922532638,-3.67108466272751,
134.080201518523));
#139537=CARTESIAN_POINT('Ctrl Pts',(-255.10067372376,-3.57694546208149,
134.179956005612));
#139538=CARTESIAN_POINT('Ctrl Pts',(-255.108421620411,-3.48284627318568,
134.279668094299));
#139539=CARTESIAN_POINT('Ctrl Pts',(-255.116169517063,-3.38452584789885,
134.375494061506));
#139540=CARTESIAN_POINT('Ctrl Pts',(-255.123917413715,-3.28234421214176,
134.467064473397));
#139541=CARTESIAN_POINT('Ctrl Pts',(-255.131663689669,-3.18018395063194,
134.558615730686));
#139542=CARTESIAN_POINT('Ctrl Pts',(-255.139409965624,-3.07416437615344,
134.645912942504));
#139543=CARTESIAN_POINT('Ctrl Pts',(-255.147156241579,-2.9646811514689,
134.72862471834));
#139544=CARTESIAN_POINT('Ctrl Pts',(-255.154902574711,-2.85519711865731,
134.811337104695));
#139545=CARTESIAN_POINT('Ctrl Pts',(-255.162648907844,-2.74224969657472,
134.889463751859));
#139546=CARTESIAN_POINT('Ctrl Pts',(-255.170395240976,-2.62626596372606,
134.962714877399));
#139547=CARTESIAN_POINT('Ctrl Pts',(-255.178143308842,-2.51025625717804,
135.035982406987));
#139548=CARTESIAN_POINT('Ctrl Pts',(-255.185891376708,-2.39120921731934,
135.104372033592));
#139549=CARTESIAN_POINT('Ctrl Pts',(-255.193639444575,-2.2695787544378,
135.16763866737));
#139550=CARTESIAN_POINT('Ctrl Pts',(-255.201395747175,-2.14781902132732,
135.230972541641));
#139551=CARTESIAN_POINT('Ctrl Pts',(-255.209152049775,-2.0234707277822,
135.289172365858));
#139552=CARTESIAN_POINT('Ctrl Pts',(-255.216908352375,-1.89701061846926,
135.342039955721));
#139553=CARTESIAN_POINT('Ctrl Pts',(-255.224668794745,-1.77048301363391,
135.394935762589));
#139554=CARTESIAN_POINT('Ctrl Pts',(-255.232429237115,-1.64184171363962,
135.442493528761));
#139555=CARTESIAN_POINT('Ctrl Pts',(-255.240189679485,-1.5115801177162,
135.484564524473));
#139556=CARTESIAN_POINT('Ctrl Pts',(-255.247962579602,-1.38110941436878,
135.526703056265));
#139557=CARTESIAN_POINT('Ctrl Pts',(-255.255735479719,-1.24901359434345,
135.563337112166));
#139558=CARTESIAN_POINT('Ctrl Pts',(-255.263508379837,-1.11579865670131,
135.594368594616));
#139559=CARTESIAN_POINT('Ctrl Pts',(-255.270998717005,-0.987426391052345,
135.624272010697));
#139560=CARTESIAN_POINT('Ctrl Pts',(-255.278489054173,-0.858015262777696,
135.648973056799));
#139561=CARTESIAN_POINT('Ctrl Pts',(-255.285979391341,-0.728021963377957,
135.668429601795));
#139562=CARTESIAN_POINT('Ctrl Pts',(-255.293753727656,-0.593099915733337,
135.688623849522));
#139563=CARTESIAN_POINT('Ctrl Pts',(-255.301528063971,-0.457123287592099,
135.703232023219));
#139564=CARTESIAN_POINT('Ctrl Pts',(-255.309302400287,-0.320594367480395,
135.712150579865));
#139565=CARTESIAN_POINT('Ctrl Pts',(-255.317067155437,-0.184233706881655,
135.721058145199));
#139566=CARTESIAN_POINT('Ctrl Pts',(-255.324831910588,-0.0473224949908735,
135.724290019907));
#139567=CARTESIAN_POINT('Ctrl Pts',(-255.332596665739,0.0896280410715395,
135.721793878603));
#139568=CARTESIAN_POINT('Ctrl Pts',(-255.340353708832,0.226442556060319,
135.7193002165));
#139569=CARTESIAN_POINT('Ctrl Pts',(-255.348110751926,0.363295929124422,
135.71108986711));
#139570=CARTESIAN_POINT('Ctrl Pts',(-255.35586779502,0.499673435663358,
135.697162424322));
#139571=CARTESIAN_POINT('Ctrl Pts',(-255.363618988471,0.63594809894258,
135.683245484318));
#139572=CARTESIAN_POINT('Ctrl Pts',(-255.371370181923,0.771747222606243,
135.663620071859));
#139573=CARTESIAN_POINT('Ctrl Pts',(-255.379121375375,0.906558070205984,
135.638337813193));
#139574=CARTESIAN_POINT('Ctrl Pts',(-255.38686927436,1.04131161955525,135.61306630017));
#139575=CARTESIAN_POINT('Ctrl Pts',(-255.394617173345,1.17507734481474,
135.582142794849));
#139576=CARTESIAN_POINT('Ctrl Pts',(-255.40236507233,1.3073498278057,135.545670509382));
#139577=CARTESIAN_POINT('Ctrl Pts',(-255.41011135062,1.43959464221113,135.509205853141));
#139578=CARTESIAN_POINT('Ctrl Pts',(-255.41785762891,1.57034645897749,135.467194829281));
#139579=CARTESIAN_POINT('Ctrl Pts',(-255.4256039072,1.69911260427714,135.419791195582));
#139580=CARTESIAN_POINT('Ctrl Pts',(-255.433350242666,1.82787970002439,
135.372387211988));
#139581=CARTESIAN_POINT('Ctrl Pts',(-255.441096578133,1.95466072816569,
135.319590674196));
#139582=CARTESIAN_POINT('Ctrl Pts',(-255.448842913599,2.07898103995985,
135.261604261118));
#139583=CARTESIAN_POINT('Ctrl Pts',(-255.456590983797,2.2033291923131,135.203604862438));
#139584=CARTESIAN_POINT('Ctrl Pts',(-255.464339053995,2.32521517752682,
135.140413440998));
#139585=CARTESIAN_POINT('Ctrl Pts',(-255.472087124192,2.44418744476934,
135.072279407484));
#139586=CARTESIAN_POINT('Ctrl Pts',(-255.479843429106,2.56328615676787,
135.004072960528));
#139587=CARTESIAN_POINT('Ctrl Pts',(-255.48759973402,2.67946462494469,134.930913602568));
#139588=CARTESIAN_POINT('Ctrl Pts',(-255.495356038933,2.79229841889414,
134.853095309089));
#139589=CARTESIAN_POINT('Ctrl Pts',(-255.503116483611,2.90519243549031,
134.775235481745));
#139590=CARTESIAN_POINT('Ctrl Pts',(-255.510876928288,3.01473790867863,
134.692711999233));
#139591=CARTESIAN_POINT('Ctrl Pts',(-255.518637372965,3.12054301335554,
134.605859580383));
#139592=CARTESIAN_POINT('Ctrl Pts',(-255.526410275356,3.22651796522496,
134.518867738775));
#139593=CARTESIAN_POINT('Ctrl Pts',(-255.534183177747,3.32874025826255,
134.427533334813));
#139594=CARTESIAN_POINT('Ctrl Pts',(-255.541956080138,3.42685385515063,
134.332229055864));
#139595=CARTESIAN_POINT('Ctrl Pts',(-255.54944639181,3.52140044571991,134.240389648003));
#139596=CARTESIAN_POINT('Ctrl Pts',(-255.556936703482,3.61213169130486,
134.144864233102));
#139597=CARTESIAN_POINT('Ctrl Pts',(-255.564427015153,3.69876529575126,
134.046014261842));
#139598=CARTESIAN_POINT('Ctrl Pts',(-255.572201345162,3.78868388130008,
133.943416088142));
#139599=CARTESIAN_POINT('Ctrl Pts',(-255.579975675171,3.87447277901351,
133.836911261055));
#139600=CARTESIAN_POINT('Ctrl Pts',(-255.58775000518,3.95577337616257,133.726866401811));
#139601=CARTESIAN_POINT('Ctrl Pts',(-255.59551475402,4.03697377756145,133.616957163061));
#139602=CARTESIAN_POINT('Ctrl Pts',(-255.603279502859,4.11369665420668,
133.503516884211));
#139603=CARTESIAN_POINT('Ctrl Pts',(-255.611044251698,4.18562165265169,
133.386947391201));
#139604=CARTESIAN_POINT('Ctrl Pts',(-255.618801288481,4.25747521419536,
133.27049367662));
#139605=CARTESIAN_POINT('Ctrl Pts',(-255.626558325265,4.32454017676951,
133.15091726347));
#139606=CARTESIAN_POINT('Ctrl Pts',(-255.634315362048,4.3865379775844,133.028650983887));
#139607=CARTESIAN_POINT('Ctrl Pts',(-255.642066549197,4.44848902543446,
132.906476906141));
#139608=CARTESIAN_POINT('Ctrl Pts',(-255.649817736346,4.50538034125497,
132.78161734675));
#139609=CARTESIAN_POINT('Ctrl Pts',(-255.657568923495,4.55697821318472,
132.654531589952));
#139610=CARTESIAN_POINT('Ctrl Pts',(-255.665316816211,4.60855415483123,
132.527499847526));
#139611=CARTESIAN_POINT('Ctrl Pts',(-255.673064708927,4.65484098057059,
132.398244151073));
#139612=CARTESIAN_POINT('Ctrl Pts',(-255.680812601643,4.6956523349151,132.267245511229));
#139613=CARTESIAN_POINT('Ctrl Pts',(-255.688558873685,4.73645515249877,
132.136274273172));
#139614=CARTESIAN_POINT('Ctrl Pts',(-255.696305145727,4.77178466061213,
132.003561189931));
#139615=CARTESIAN_POINT('Ctrl Pts',(-255.704051417769,4.80150391786348,
131.86960387112));
#139616=CARTESIAN_POINT('Ctrl Pts',(-255.711797747015,4.83122339458221,
131.735645563075));
#139617=CARTESIAN_POINT('Ctrl Pts',(-255.719544076261,4.85533245308934,
131.60044338281));
#139618=CARTESIAN_POINT('Ctrl Pts',(-255.727290405506,4.87374505372797,
131.464506217992));
#139619=CARTESIAN_POINT('Ctrl Pts',(-255.735038469516,4.89216177780544,
131.328538610512));
#139620=CARTESIAN_POINT('Ctrl Pts',(-255.742786533526,4.90487945304789,
131.191836078304));
#139621=CARTESIAN_POINT('Ctrl Pts',(-255.750534597535,4.91186384154735,
131.054913335771));
#139622=CARTESIAN_POINT('Ctrl Pts',(-255.758290896348,4.91885565319941,
130.917845068914));
#139623=CARTESIAN_POINT('Ctrl Pts',(-255.76604719516,4.92010198582534,130.780556515283));
#139624=CARTESIAN_POINT('Ctrl Pts',(-255.773803493972,4.91562075439972,
130.643563660459));
#139625=CARTESIAN_POINT('Ctrl Pts',(-255.781563932585,4.91113713118828,
130.506497687884));
#139626=CARTESIAN_POINT('Ctrl Pts',(-255.789324371199,4.90091988171353,
130.369728118281));
#139627=CARTESIAN_POINT('Ctrl Pts',(-255.797084809812,4.88503882343902,
130.233765528213));
#139628=CARTESIAN_POINT('Ctrl Pts',(-255.804857706264,4.86913227128675,
130.097584677272));
#139629=CARTESIAN_POINT('Ctrl Pts',(-255.812630602717,4.84754380299392,
129.962213780887));
#139630=CARTESIAN_POINT('Ctrl Pts',(-255.82040349917,4.82039452419987,129.828153829245));
#139631=CARTESIAN_POINT('Ctrl Pts',(-255.827893879102,4.79423202296297,
129.698966469343));
#139632=CARTESIAN_POINT('Ctrl Pts',(-255.835384259034,4.76290599817105,
129.570996711417));
#139633=CARTESIAN_POINT('Ctrl Pts',(-255.842874638966,4.72656796529398,
129.444677444192));
#139634=CARTESIAN_POINT('Ctrl Pts',(-255.850648973645,4.68885238454662,
129.313569507252));
#139635=CARTESIAN_POINT('Ctrl Pts',(-255.858423308324,4.64561782316634,
129.183824354334));
#139636=CARTESIAN_POINT('Ctrl Pts',(-255.866197643003,4.59697889127745,
129.055941864621));
#139637=CARTESIAN_POINT('Ctrl Pts',(-255.873962396479,4.54839990271601,
128.928216979149));
#139638=CARTESIAN_POINT('Ctrl Pts',(-255.881727149955,4.49442993355858,
128.802350551294));
#139639=CARTESIAN_POINT('Ctrl Pts',(-255.889491903431,4.43523389272254,
128.678829300614));
#139640=CARTESIAN_POINT('Ctrl Pts',(-255.897248944813,4.37609664646376,
128.555430733471));
#139641=CARTESIAN_POINT('Ctrl Pts',(-255.905005986196,4.31174382598289,
128.434373058433));
#139642=CARTESIAN_POINT('Ctrl Pts',(-255.912763027578,4.24238901545678,
128.316124594993));
#139643=CARTESIAN_POINT('Ctrl Pts',(-255.920514219284,4.17308650621095,
128.197965304113));
#139644=CARTESIAN_POINT('Ctrl Pts',(-255.92826541099,4.09878971197225,128.082611344041));
#139645=CARTESIAN_POINT('Ctrl Pts',(-255.936016602696,4.0197587148412,127.97050759792));
#139646=CARTESIAN_POINT('Ctrl Pts',(-255.94376449989,3.94076130849002,127.858451499587));
#139647=CARTESIAN_POINT('Ctrl Pts',(-255.951512397084,3.85703392614292,
127.749643186482));
#139648=CARTESIAN_POINT('Ctrl Pts',(-255.959260294278,3.76888052620867,
127.644499443137));
#139649=CARTESIAN_POINT('Ctrl Pts',(-255.967006570749,3.68074556640345,
127.539377693999));
#139650=CARTESIAN_POINT('Ctrl Pts',(-255.974752847221,3.58818668159333,
127.437919289294));
#139651=CARTESIAN_POINT('Ctrl Pts',(-255.982499123692,3.49154850490718,
127.340508412234));
#139652=CARTESIAN_POINT('Ctrl Pts',(-255.990245457314,3.39490961523462,
127.243096816488));
#139653=CARTESIAN_POINT('Ctrl Pts',(-255.997991790937,3.2941916489815,127.149733085528));
#139654=CARTESIAN_POINT('Ctrl Pts',(-256.005738124559,3.18977624146807,
127.060764673575));
#139655=CARTESIAN_POINT('Ctrl Pts',(-256.013486192889,3.08533745125707,
126.971776338112));
#139656=CARTESIAN_POINT('Ctrl Pts',(-256.021234261218,2.9771998696897,126.887185533782));
#139657=CARTESIAN_POINT('Ctrl Pts',(-256.028982329548,2.86577803441173,
126.807299282037));
#139658=CARTESIAN_POINT('Ctrl Pts',(-256.036738632568,2.75423777939466,
126.727328126743));
#139659=CARTESIAN_POINT('Ctrl Pts',(-256.044494935587,2.6394066162155,126.652071740293));
#139660=CARTESIAN_POINT('Ctrl Pts',(-256.052251238606,2.52172834191952,
126.58179395355));
#139661=CARTESIAN_POINT('Ctrl Pts',(-256.060011681372,2.40398725958728,
126.511478657677));
#139662=CARTESIAN_POINT('Ctrl Pts',(-256.067772124137,2.283396381839,126.446147442374));
#139663=CARTESIAN_POINT('Ctrl Pts',(-256.075532566902,2.16042300955805,
126.386017547786));
#139664=CARTESIAN_POINT('Ctrl Pts',(-256.083305467372,2.03725223025821,
126.325791127723));
#139665=CARTESIAN_POINT('Ctrl Pts',(-256.091078367841,1.91169167201454,
126.270782870492));
#139666=CARTESIAN_POINT('Ctrl Pts',(-256.098851268311,1.78422829296174,
126.221161684387));
#139667=CARTESIAN_POINT('Ctrl Pts',(-256.1063415998,1.66139860208187,126.173344381913));
#139668=CARTESIAN_POINT('Ctrl Pts',(-256.11383193129,1.53680232659375,126.130529377399));
#139669=CARTESIAN_POINT('Ctrl Pts',(-256.121322262779,1.41088555684552,
126.092823181868));
#139670=CARTESIAN_POINT('Ctrl Pts',(-256.12909661041,1.28019431282663,126.053687254135));
#139671=CARTESIAN_POINT('Ctrl Pts',(-256.13687095804,1.14766647288937,126.019931239898));
#139672=CARTESIAN_POINT('Ctrl Pts',(-256.14464530567,1.01378455099754,125.991728910625));
#139673=CARTESIAN_POINT('Ctrl Pts',(-256.152410072184,0.880067625359694,
125.963561337938));
#139674=CARTESIAN_POINT('Ctrl Pts',(-256.160174838698,0.745000317022461,
125.940933911775));
#139675=CARTESIAN_POINT('Ctrl Pts',(-256.167939605212,0.609081255968552,
125.923970972658));
#139676=CARTESIAN_POINT('Ctrl Pts',(-256.175696659705,0.473297190682827,
125.907024881251));
#139677=CARTESIAN_POINT('Ctrl Pts',(-256.183453714199,0.336663441636364,
125.895732128981));
#139678=CARTESIAN_POINT('Ctrl Pts',(-256.191210768692,0.199689468356939,
125.890166158784));
#139679=CARTESIAN_POINT('Ctrl Pts',(-256.198961973567,0.0628187875599876,
125.884604385901));
#139680=CARTESIAN_POINT('Ctrl Pts',(-256.206713178443,-0.0743912177338724,
125.88476081502));
#139681=CARTESIAN_POINT('Ctrl Pts',(-256.214464383318,-0.211425672508862,
125.890657101123));
#139682=CARTESIAN_POINT('Ctrl Pts',(-256.222212293723,-0.348401883959695,
125.896550881146));
#139683=CARTESIAN_POINT('Ctrl Pts',(-256.229960204128,-0.485202303508083,
125.908179649215));
#139684=CARTESIAN_POINT('Ctrl Pts',(-256.237708114533,-0.621311980170193,
125.925512957944));
#139685=CARTESIAN_POINT('Ctrl Pts',(-256.245454404239,-0.75739318556207,
125.942842640911));
#139686=CARTESIAN_POINT('Ctrl Pts',(-256.253200693945,-0.892783547878109,
125.965874441702));
#139687=CARTESIAN_POINT('Ctrl Pts',(-256.260946983651,-1.02697355893801,
125.994526070334));
#139688=CARTESIAN_POINT('Ctrl Pts',(-256.268693330519,-1.16116456022594,
126.023177910396));
#139689=CARTESIAN_POINT('Ctrl Pts',(-256.276439677387,-1.29415481023727,
126.057449579415));
#139690=CARTESIAN_POINT('Ctrl Pts',(-256.284186024255,-1.42544570139586,
126.09720780351));
#139691=CARTESIAN_POINT('Ctrl Pts',(-256.291934105829,-1.55676599364681,
126.136974931005));
#139692=CARTESIAN_POINT('Ctrl Pts',(-256.299682187402,-1.6863857956792,
126.182230945161));
#139693=CARTESIAN_POINT('Ctrl Pts',(-256.307430268976,-1.81382273267125,
126.232793035549));
#139694=CARTESIAN_POINT('Ctrl Pts',(-256.315186585161,-1.94139510882823,
126.283408863005));
#139695=CARTESIAN_POINT('Ctrl Pts',(-256.322942901347,-2.06677962164013,
126.339341887316));
#139696=CARTESIAN_POINT('Ctrl Pts',(-256.330699217532,-2.18951441834683,
126.400361335737));
#139697=CARTESIAN_POINT('Ctrl Pts',(-256.338459673442,-2.31231472144022,
126.461413351642));
#139698=CARTESIAN_POINT('Ctrl Pts',(-256.346220129352,-2.43246214816031,
126.527557012553));
#139699=CARTESIAN_POINT('Ctrl Pts',(-256.353980585262,-2.54952133943239,
126.598516587852));
#139700=CARTESIAN_POINT('Ctrl Pts',(-256.361753498706,-2.66676844090148,
126.669590071574));
#139701=CARTESIAN_POINT('Ctrl Pts',(-256.369526412149,-2.78091707468402,
126.745494701648));
#139702=CARTESIAN_POINT('Ctrl Pts',(-256.377299325593,-2.89156191943161,
126.825912084709));
#139703=CARTESIAN_POINT('Ctrl Pts',(-256.384789512593,-2.99818224702861,
126.903404422883));
#139704=CARTESIAN_POINT('Ctrl Pts',(-256.392279699593,-3.10154900471017,
126.985086738741));
#139705=CARTESIAN_POINT('Ctrl Pts',(-256.399769886592,-3.2013314782914,
127.070641315235));
#139706=CARTESIAN_POINT('Ctrl Pts',(-256.407430116474,-3.3033792223307,
127.15813815922));
#139707=CARTESIAN_POINT('Ctrl Pts',(-256.415090346355,-3.40202131093705,
127.249979901927));
#139708=CARTESIAN_POINT('Ctrl Pts',(-256.422750576237,-3.49685688824348,
127.345867453536));
#139709=CARTESIAN_POINT('Ctrl Pts',(-256.430402001156,-3.59158345789778,
127.441644788313));
#139710=CARTESIAN_POINT('Ctrl Pts',(-256.438053426075,-3.6825119332072,
127.541458404519));
#139711=CARTESIAN_POINT('Ctrl Pts',(-256.445704850994,-3.76927368310696,
127.644968434829));
#139712=CARTESIAN_POINT('Ctrl Pts',(-256.453349252676,-3.85595579445533,
127.748383453353));
#139713=CARTESIAN_POINT('Ctrl Pts',(-256.460993654357,-3.93847852763003,
127.855487833074));
#139714=CARTESIAN_POINT('Ctrl Pts',(-256.468638056039,-4.01650977625177,
127.965904650007));
#139715=CARTESIAN_POINT('Ctrl Pts',(-256.476277209502,-4.09448745298127,
128.076245660927));
#139716=CARTESIAN_POINT('Ctrl Pts',(-256.483916362964,-4.1679795463751,
128.189894258021));
#139717=CARTESIAN_POINT('Ctrl Pts',(-256.491555516427,-4.23669433217617,
128.306440643226));
#139718=CARTESIAN_POINT('Ctrl Pts',(-256.499191793952,-4.30538324868746,
128.422943151816));
#139719=CARTESIAN_POINT('Ctrl Pts',(-256.506828071476,-4.36929822806934,
128.542340933306));
#139720=CARTESIAN_POINT('Ctrl Pts',(-256.514464349001,-4.42819123600362,
128.664195801511));
#139721=CARTESIAN_POINT('Ctrl Pts',(-256.522098960068,-4.48707139177239,
128.786024077443));
#139722=CARTESIAN_POINT('Ctrl Pts',(-256.529733571135,-4.54093158425627,
128.910308008879));
#139723=CARTESIAN_POINT('Ctrl Pts',(-256.537368182202,-4.58957036579766,
129.036586050521));
#139724=CARTESIAN_POINT('Ctrl Pts',(-256.545004452601,-4.63821971865693,
129.162891537861));
#139725=CARTESIAN_POINT('Ctrl Pts',(-256.552640723,-4.68164525005835,129.291191624277));
#139726=CARTESIAN_POINT('Ctrl Pts',(-256.560276993399,-4.71969426905031,
129.421006335687));
#139727=CARTESIAN_POINT('Ctrl Pts',(-256.563428894497,-4.73539915356272,
129.47458787615));
#139728=CARTESIAN_POINT('Ctrl Pts',(-256.566580795594,-4.75018865139969,
129.528427275975));
#139729=CARTESIAN_POINT('Ctrl Pts',(-256.569732696692,-4.76405452823407,
129.582490119308));
#139730=CARTESIAN_POINT('Origin',(213.235140564004,0.,130.804360617566));
#139731=CARTESIAN_POINT('',(-258.665423831404,-4.76405452823398,129.582490119308));
#139732=CARTESIAN_POINT('',(-258.319801180437,-4.76405452823418,129.582490119309));
#139733=CARTESIAN_POINT('',(213.235140564004,-4.76405452823405,129.582490119308));
#139734=CARTESIAN_POINT('',(-256.985140564063,-4.91824826888146,130.800234100334));
#139735=CARTESIAN_POINT('Ctrl Pts',(-256.985140564063,-4.91824826888146,
130.800234100334));
#139736=CARTESIAN_POINT('Ctrl Pts',(-256.992787534705,-4.91836128350308,
130.934932184893));
#139737=CARTESIAN_POINT('Ctrl Pts',(-257.000434505347,-4.91293659407798,
131.069827034711));
#139738=CARTESIAN_POINT('Ctrl Pts',(-257.00808147599,-4.90195239602637,
131.204417825464));
#139739=CARTESIAN_POINT('Ctrl Pts',(-257.015721341468,-4.8909784039146,
131.338883561525));
#139740=CARTESIAN_POINT('Ctrl Pts',(-257.023361206947,-4.8744552100032,
131.47304540063));
#139741=CARTESIAN_POINT('Ctrl Pts',(-257.031001072426,-4.8524130586271,
131.606402119588));
#139742=CARTESIAN_POINT('Ctrl Pts',(-257.038689517819,-4.83023074695118,
131.740606819189));
#139743=CARTESIAN_POINT('Ctrl Pts',(-257.046377963213,-4.80245903531062,
131.873995709716));
#139744=CARTESIAN_POINT('Ctrl Pts',(-257.054066408607,-4.76918191165742,
132.006062309343));
#139745=CARTESIAN_POINT('Ctrl Pts',(-257.061698806436,-4.73614737302964,
132.13716616412));
#139746=CARTESIAN_POINT('Ctrl Pts',(-257.069331204265,-4.69768753437786,
132.26696654803));
#139747=CARTESIAN_POINT('Ctrl Pts',(-257.076963602095,-4.65393581023225,
132.394978276445));
#139748=CARTESIAN_POINT('Ctrl Pts',(-257.084595206406,-4.61018863482752,
132.522976695849));
#139749=CARTESIAN_POINT('Ctrl Pts',(-257.092226810717,-4.56115079839951,
132.64918644757));
#139750=CARTESIAN_POINT('Ctrl Pts',(-257.099858415028,-4.50700523503668,
132.773138632948));
#139751=CARTESIAN_POINT('Ctrl Pts',(-257.107490992867,-4.45285276457458,
132.897106630333));
#139752=CARTESIAN_POINT('Ctrl Pts',(-257.115123570707,-4.39359143362793,
133.018816119003));
#139753=CARTESIAN_POINT('Ctrl Pts',(-257.122756148546,-4.32945161927853,
133.137819796302));
#139754=CARTESIAN_POINT('Ctrl Pts',(-257.13048678299,-4.26448779336661,
133.258352327512));
#139755=CARTESIAN_POINT('Ctrl Pts',(-257.138217417433,-4.19451945678236,
133.376108660477));
#139756=CARTESIAN_POINT('Ctrl Pts',(-257.145948051877,-4.11983247940448,
133.490652374644));
#139757=CARTESIAN_POINT('Ctrl Pts',(-257.153591779927,-4.04598511951259,
133.603908409101));
#139758=CARTESIAN_POINT('Ctrl Pts',(-257.161235507977,-3.96752495530406,
133.71402339357));
#139759=CARTESIAN_POINT('Ctrl Pts',(-257.168879236027,-3.88476970613984,
133.820607854242));
#139760=CARTESIAN_POINT('Ctrl Pts',(-257.176653323668,-3.80060311157986,
133.929010054447));
#139761=CARTESIAN_POINT('Ctrl Pts',(-257.184427411309,-3.71199388470393,
134.03375987988));
#139762=CARTESIAN_POINT('Ctrl Pts',(-257.192201498949,-3.61931550348488,
134.134486493375));
#139763=CARTESIAN_POINT('Ctrl Pts',(-257.19997558659,-3.52663712226583,
134.235213106871));
#139764=CARTESIAN_POINT('Ctrl Pts',(-257.20774967423,-3.42988994053418,
134.331916252334));
#139765=CARTESIAN_POINT('Ctrl Pts',(-257.215523761871,-3.3294819563702,
134.424268484447));
#139766=CARTESIAN_POINT('Ctrl Pts',(-257.223298557193,-3.22906483198696,
134.516629123457));
#139767=CARTESIAN_POINT('Ctrl Pts',(-257.231073352515,-3.12464272484351,
134.604954364295));
#139768=CARTESIAN_POINT('Ctrl Pts',(-257.238848147837,-3.01657361527509,
134.688876891972));
#139769=CARTESIAN_POINT('Ctrl Pts',(-257.246613364855,-2.90863764345205,
134.772696029733));
#139770=CARTESIAN_POINT('Ctrl Pts',(-257.254378581874,-2.79706391473311,
134.852123009051));
#139771=CARTESIAN_POINT('Ctrl Pts',(-257.262143798892,-2.68224651844936,
134.926827922078));
#139772=CARTESIAN_POINT('Ctrl Pts',(-257.269901306206,-2.56754311875833,
135.00145866424));
#139773=CARTESIAN_POINT('Ctrl Pts',(-257.277658813519,-2.44960278596319,
135.071376458272));
#139774=CARTESIAN_POINT('Ctrl Pts',(-257.285416320832,-2.32885160599809,
135.136292433712));
#139775=CARTESIAN_POINT('Ctrl Pts',(-257.293167980352,-2.2081914511474,
135.201159473945));
#139776=CARTESIAN_POINT('Ctrl Pts',(-257.300919639872,-2.08472500956599,
135.261032016185));
#139777=CARTESIAN_POINT('Ctrl Pts',(-257.308671299391,-1.95890588475593,
135.315665395252));
#139778=CARTESIAN_POINT('Ctrl Pts',(-257.316419665594,-1.833140214598,135.370275563155));
#139779=CARTESIAN_POINT('Ctrl Pts',(-257.324168031796,-1.70502420705359,
135.419650839623));
#139780=CARTESIAN_POINT('Ctrl Pts',(-257.331916397999,-1.57503431937467,
135.463593382227));
#139781=CARTESIAN_POINT('Ctrl Pts',(-257.339663144139,-1.44507161054926,
135.507526737133));
#139782=CARTESIAN_POINT('Ctrl Pts',(-257.34740989028,-1.31323617099235,
135.546029492443));
#139783=CARTESIAN_POINT('Ctrl Pts',(-257.35515663642,-1.18002223567149,
135.578952808091));
#139784=CARTESIAN_POINT('Ctrl Pts',(-257.362903439926,-1.04680731388757,
135.61187636754));
#139785=CARTESIAN_POINT('Ctrl Pts',(-257.370650243432,-0.912214255464911,
135.639220311094));
#139786=CARTESIAN_POINT('Ctrl Pts',(-257.378397046938,-0.7767497900252,
135.66088641552));
#139787=CARTESIAN_POINT('Ctrl Pts',(-257.386145584919,-0.641254994689473,
135.682557370892));
#139788=CARTESIAN_POINT('Ctrl Pts',(-257.3938941229,-0.504888790033397,
135.698547895776));
#139789=CARTESIAN_POINT('Ctrl Pts',(-257.401642660881,-0.368164972862441,
135.708811414063));
#139790=CARTESIAN_POINT('Ctrl Pts',(-257.409399430516,-0.231295907226831,
135.719085835792));
#139791=CARTESIAN_POINT('Ctrl Pts',(-257.417156200152,-0.0940688606027882,
135.723621068002));
#139792=CARTESIAN_POINT('Ctrl Pts',(-257.424912969787,0.0429998485669047,
135.722422641933));
#139793=CARTESIAN_POINT('Ctrl Pts',(-257.432673878259,0.180141694477021,
135.721223576412));
#139794=CARTESIAN_POINT('Ctrl Pts',(-257.44043478673,0.317124644366466,
135.714284776344));
#139795=CARTESIAN_POINT('Ctrl Pts',(-257.448195695201,0.45343654122407,
135.701663790291));
#139796=CARTESIAN_POINT('Ctrl Pts',(-257.455969055081,0.589967133498706,
135.689022555442));
#139797=CARTESIAN_POINT('Ctrl Pts',(-257.46374241496,0.725824133687792,
135.670680969544));
#139798=CARTESIAN_POINT('Ctrl Pts',(-257.47151577484,0.860503737315126,
135.646748084567));
#139799=CARTESIAN_POINT('Ctrl Pts',(-257.479000978455,0.990190805907493,
135.623702384906));
#139800=CARTESIAN_POINT('Ctrl Pts',(-257.48648618207,1.11878592285715,135.595472640323));
#139801=CARTESIAN_POINT('Ctrl Pts',(-257.493971385684,1.24585361515672,
135.562199605184));
#139802=CARTESIAN_POINT('Ctrl Pts',(-257.501744289864,1.37780526903188,
135.527647690873));
#139803=CARTESIAN_POINT('Ctrl Pts',(-257.509517194043,1.50852789871494,
135.487547546984));
#139804=CARTESIAN_POINT('Ctrl Pts',(-257.517290098223,1.63751915163922,
135.442001622486));
#139805=CARTESIAN_POINT('Ctrl Pts',(-257.525053419543,1.76635137712096,
135.396511849485));
#139806=CARTESIAN_POINT('Ctrl Pts',(-257.532816740863,1.89345610764402,
135.345589783312));
#139807=CARTESIAN_POINT('Ctrl Pts',(-257.540580062182,2.01834292803111,
135.289388475603));
#139808=CARTESIAN_POINT('Ctrl Pts',(-257.54833567123,2.14310568281374,135.23324299964));
#139809=CARTESIAN_POINT('Ctrl Pts',(-257.556091280278,2.26565455778836,
135.171828878374));
#139810=CARTESIAN_POINT('Ctrl Pts',(-257.563846889326,2.38551635535023,
135.105348269357));
#139811=CARTESIAN_POINT('Ctrl Pts',(-257.571596649984,2.50528776691088,
135.03891779238));
#139812=CARTESIAN_POINT('Ctrl Pts',(-257.579346410642,2.62237579357889,
134.967428621133));
#139813=CARTESIAN_POINT('Ctrl Pts',(-257.5870961713,2.73632954467773,134.891129963324));
#139814=CARTESIAN_POINT('Ctrl Pts',(-257.594842644384,2.8502349547566,134.814863672636));
#139815=CARTESIAN_POINT('Ctrl Pts',(-257.602589117469,2.96100840939698,
134.733792170391));
#139816=CARTESIAN_POINT('Ctrl Pts',(-257.610335590554,3.06822605017053,
134.648209205577));
#139817=CARTESIAN_POINT('Ctrl Pts',(-257.618080447319,3.17542131973774,
134.562644097844));
#139818=CARTESIAN_POINT('Ctrl Pts',(-257.625825304084,3.27906194566963,
134.472569643717));
#139819=CARTESIAN_POINT('Ctrl Pts',(-257.633570160849,3.37875568273299,
134.378321039689));
#139820=CARTESIAN_POINT('Ctrl Pts',(-257.641315080479,3.47845022900745,
134.284071670648));
#139821=CARTESIAN_POINT('Ctrl Pts',(-257.649060000109,3.57419753827989,
134.185648352807));
#139822=CARTESIAN_POINT('Ctrl Pts',(-257.656804919739,3.66564119490863,
134.083424156549));
#139823=CARTESIAN_POINT('Ctrl Pts',(-257.664551581105,3.75710541607468,
133.981176971345));
#139824=CARTESIAN_POINT('Ctrl Pts',(-257.672298242471,3.84426379800583,
133.875127498292));
#139825=CARTESIAN_POINT('Ctrl Pts',(-257.680044903836,3.92679955720989,
133.765682670298));
#139826=CARTESIAN_POINT('Ctrl Pts',(-257.687799818904,4.00942325436452,
133.656121234012));
#139827=CARTESIAN_POINT('Ctrl Pts',(-257.695554733971,4.08741425434609,
133.543157529048));
#139828=CARTESIAN_POINT('Ctrl Pts',(-257.703309649038,4.16049825033351,
133.427228775036));
#139829=CARTESIAN_POINT('Ctrl Pts',(-257.711068711982,4.23362133680738,
133.311238014133));
#139830=CARTESIAN_POINT('Ctrl Pts',(-257.718827774927,4.30183199513327,
133.192279383277));
#139831=CARTESIAN_POINT('Ctrl Pts',(-257.726586837871,4.36490193450261,
133.070814712551));
#139832=CARTESIAN_POINT('Ctrl Pts',(-257.734358386394,4.42807336354529,
132.94915458564));
#139833=CARTESIAN_POINT('Ctrl Pts',(-257.742129934918,4.48608737743533,
132.82498071497));
#139834=CARTESIAN_POINT('Ctrl Pts',(-257.749901483442,4.53876353342889,
132.698775738419));
#139835=CARTESIAN_POINT('Ctrl Pts',(-257.75740732546,4.58963871020913,132.576885665549));
#139836=CARTESIAN_POINT('Ctrl Pts',(-257.764913167478,4.63553498217158,
132.453101406161));
#139837=CARTESIAN_POINT('Ctrl Pts',(-257.772419009496,4.67633451815619,
132.327869244651));
#139838=CARTESIAN_POINT('Ctrl Pts',(-257.780194620124,4.71860043647074,
132.198136094971));
#139839=CARTESIAN_POINT('Ctrl Pts',(-257.787970230752,4.75553046150047,
132.066437493625));
#139840=CARTESIAN_POINT('Ctrl Pts',(-257.79574584138,4.78693929394865,131.933251780854));
#139841=CARTESIAN_POINT('Ctrl Pts',(-257.803511864073,4.8183093968543,131.800230296465));
#139842=CARTESIAN_POINT('Ctrl Pts',(-257.811277886767,4.84417176442526,
131.665725725988));
#139843=CARTESIAN_POINT('Ctrl Pts',(-257.81904390946,4.86439012903196,131.530233702255));
#139844=CARTESIAN_POINT('Ctrl Pts',(-257.826802212121,4.88458839500891,
131.394876368151));
#139845=CARTESIAN_POINT('Ctrl Pts',(-257.834560514782,4.89915376608289,
131.258533918293));
#139846=CARTESIAN_POINT('Ctrl Pts',(-257.842318817444,4.90800059843263,
131.121714029845));
#139847=CARTESIAN_POINT('Ctrl Pts',(-257.850071261287,4.91684074994213,
130.984997463329));
#139848=CARTESIAN_POINT('Ctrl Pts',(-257.85782370513,4.91997093328085,130.847804564311));
#139849=CARTESIAN_POINT('Ctrl Pts',(-257.865576148974,4.91735714788234,
130.710649664788));
#139850=CARTESIAN_POINT('Ctrl Pts',(-257.873325280157,4.91474447936821,
130.573553372283));
#139851=CARTESIAN_POINT('Ctrl Pts',(-257.88107441134,4.90639273133353,130.436495436918));
#139852=CARTESIAN_POINT('Ctrl Pts',(-257.888823542523,4.89231998862875,
130.299991515257));
#139853=CARTESIAN_POINT('Ctrl Pts',(-257.896571041791,4.87825020954869,
130.163516340402));
#139854=CARTESIAN_POINT('Ctrl Pts',(-257.90431854106,4.85846187230104,130.027595335706));
#139855=CARTESIAN_POINT('Ctrl Pts',(-257.912066040328,4.83302501993536,
129.892739962261));
#139856=CARTESIAN_POINT('Ctrl Pts',(-257.91981358446,4.80758802027207,129.757883807906));
#139857=CARTESIAN_POINT('Ctrl Pts',(-257.927561128591,4.77650251262282,
129.624093681182));
#139858=CARTESIAN_POINT('Ctrl Pts',(-257.935308672723,4.7398897713283,129.491871372598));
#139859=CARTESIAN_POINT('Ctrl Pts',(-257.94305793817,4.70326889557698,129.359619687446));
#139860=CARTESIAN_POINT('Ctrl Pts',(-257.950807203617,4.66111844684277,
129.228936890161));
#139861=CARTESIAN_POINT('Ctrl Pts',(-257.958556469064,4.6136096127303,129.100309736922));
#139862=CARTESIAN_POINT('Ctrl Pts',(-257.966313941403,4.56605046418237,
128.971546360543));
#139863=CARTESIAN_POINT('Ctrl Pts',(-257.974071413743,4.51312172979363,
128.844843344298));
#139864=CARTESIAN_POINT('Ctrl Pts',(-257.981828886083,4.45504303968147,
128.720668083365));
#139865=CARTESIAN_POINT('Ctrl Pts',(-257.989590484902,4.39693345542028,
128.596426769134));
#139866=CARTESIAN_POINT('Ctrl Pts',(-257.997352083721,4.33366863695595,
128.474716236107));
#139867=CARTESIAN_POINT('Ctrl Pts',(-258.00511368254,4.26551379943042,128.355978480446));
#139868=CARTESIAN_POINT('Ctrl Pts',(-258.01288770478,4.19724987146726,128.237050669989));
#139869=CARTESIAN_POINT('Ctrl Pts',(-258.020661727019,4.12408049208502,
128.121105476245));
#139870=CARTESIAN_POINT('Ctrl Pts',(-258.028435749259,4.04631425159911,
128.008555896237));
#139871=CARTESIAN_POINT('Ctrl Pts',(-258.035912710609,3.9715196142071,127.900307060074));
#139872=CARTESIAN_POINT('Ctrl Pts',(-258.04338967196,3.89247317935221,127.795199323993));
#139873=CARTESIAN_POINT('Ctrl Pts',(-258.05086663331,3.80948286040464,127.693569175058));
#139874=CARTESIAN_POINT('Ctrl Pts',(-258.058643465866,3.72316412958299,
127.587863044745));
#139875=CARTESIAN_POINT('Ctrl Pts',(-258.066420298421,3.6323063418413,127.485585869392));
#139876=CARTESIAN_POINT('Ctrl Pts',(-258.074197130977,3.53721205379093,
127.387152115145));
#139877=CARTESIAN_POINT('Ctrl Pts',(-258.081964402288,3.44223467962177,
127.288839380493));
#139878=CARTESIAN_POINT('Ctrl Pts',(-258.0897316736,3.34303143766935,127.194360943156));
#139879=CARTESIAN_POINT('Ctrl Pts',(-258.097498944911,3.23994592104352,
127.104099344194));
#139880=CARTESIAN_POINT('Ctrl Pts',(-258.105258521243,3.13696253050272,
127.013927166754));
#139881=CARTESIAN_POINT('Ctrl Pts',(-258.113018097574,3.03010481143685,
126.927963769676));
#139882=CARTESIAN_POINT('Ctrl Pts',(-258.120777673905,2.91975383782572,
126.846555595966));
#139883=CARTESIAN_POINT('Ctrl Pts',(-258.128531414864,2.80948585058243,
126.765208642999));
#139884=CARTESIAN_POINT('Ctrl Pts',(-258.136285155823,2.69573015088393,
126.688410325789));
#139885=CARTESIAN_POINT('Ctrl Pts',(-258.144038896781,2.57890131011219,
126.616467221692));
#139886=CARTESIAN_POINT('Ctrl Pts',(-258.151789355802,2.46212191966585,
126.544554569065));
#139887=CARTESIAN_POINT('Ctrl Pts',(-258.159539814823,2.34227230728373,
126.477493246544));
#139888=CARTESIAN_POINT('Ctrl Pts',(-258.167290273843,2.21979629815279,
126.415546716612));
#139889=CARTESIAN_POINT('Ctrl Pts',(-258.175039119409,2.09734578551536,
126.353613082424));
#139890=CARTESIAN_POINT('Ctrl Pts',(-258.182787964974,1.97227031206583,
126.296792299111));
#139891=CARTESIAN_POINT('Ctrl Pts',(-258.19053681054,1.84503824287365,126.245301839174));
#139892=CARTESIAN_POINT('Ctrl Pts',(-258.198285718053,1.71780515653942,
126.193810967602));
#139893=CARTESIAN_POINT('Ctrl Pts',(-258.206034625566,1.58841580221056,
126.147650650974));
#139894=CARTESIAN_POINT('Ctrl Pts',(-258.213783533079,1.4573580867132,126.106990026523));
#139895=CARTESIAN_POINT('Ctrl Pts',(-258.221534177625,1.32627099267363,
126.066320287388));
#139896=CARTESIAN_POINT('Ctrl Pts',(-258.229284822171,1.19351516631886,
126.031152809411));
#139897=CARTESIAN_POINT('Ctrl Pts',(-258.237035466717,1.05959283264569,
126.001606606428));
#139898=CARTESIAN_POINT('Ctrl Pts',(-258.24479433493,0.925528403350393,
125.972029054035));
#139899=CARTESIAN_POINT('Ctrl Pts',(-258.252553203143,0.790295376400809,
125.948084775374));
#139900=CARTESIAN_POINT('Ctrl Pts',(-258.260312071356,0.654405862237226,
125.929841561293));
#139901=CARTESIAN_POINT('Ctrl Pts',(-258.268075077377,0.518443878131305,
125.911588618097));
#139902=CARTESIAN_POINT('Ctrl Pts',(-258.275838083398,0.381825098035721,
125.899042833517));
#139903=CARTESIAN_POINT('Ctrl Pts',(-258.283601089419,0.245064894361125,
125.892219917214));
#139904=CARTESIAN_POINT('Ctrl Pts',(-258.291376523712,0.108085742901093,
125.885386077687));
#139905=CARTESIAN_POINT('Ctrl Pts',(-258.299151958005,-0.0290348936966784,
125.884293418368));
#139906=CARTESIAN_POINT('Ctrl Pts',(-258.306927392298,-0.165782603154849,
125.888905481875));
#139907=CARTESIAN_POINT('Ctrl Pts',(-258.314389680573,-0.297022967417457,
125.893331800217));
#139908=CARTESIAN_POINT('Ctrl Pts',(-258.321851968847,-0.42791956262217,
125.903012206386));
#139909=CARTESIAN_POINT('Ctrl Pts',(-258.329314257122,-0.558025608205252,
125.917870007416));
#139910=CARTESIAN_POINT('Ctrl Pts',(-258.337078965247,-0.693404386406557,
125.933329941972));
#139911=CARTESIAN_POINT('Ctrl Pts',(-258.344843673372,-0.828357737740643,
125.95444493456));
#139912=CARTESIAN_POINT('Ctrl Pts',(-258.352608381497,-0.962374722353744,
125.981185526791));
#139913=CARTESIAN_POINT('Ctrl Pts',(-258.36036349259,-1.09622606452778,
126.007893068159));
#139914=CARTESIAN_POINT('Ctrl Pts',(-258.368118603684,-1.22914296192161,
126.040212299277));
#139915=CARTESIAN_POINT('Ctrl Pts',(-258.375873714777,-1.36061904066752,
126.078061971831));
#139916=CARTESIAN_POINT('Ctrl Pts',(-258.383621107811,-1.49196427147542,
126.115873975544));
#139917=CARTESIAN_POINT('Ctrl Pts',(-258.391368500844,-1.62187116284061,
126.159205360274));
#139918=CARTESIAN_POINT('Ctrl Pts',(-258.399115893877,-1.74984335866182,
126.20792381471));
#139919=CARTESIAN_POINT('Ctrl Pts',(-258.406857441036,-1.87771899175559,
126.25660550814));
#139920=CARTESIAN_POINT('Ctrl Pts',(-258.414598988195,-2.00366247002254,
126.310666041904));
#139921=CARTESIAN_POINT('Ctrl Pts',(-258.422340535354,-2.12719279761935,
126.369923351773));
#139922=CARTESIAN_POINT('Ctrl Pts',(-258.430078827125,-2.25067117965424,
126.429155743434));
#139923=CARTESIAN_POINT('Ctrl Pts',(-258.437817118897,-2.37173807634447,
126.493580396106));
#139924=CARTESIAN_POINT('Ctrl Pts',(-258.445555410669,-2.48993289461645,
126.562967303712));
#139925=CARTESIAN_POINT('Ctrl Pts',(-258.453292106575,-2.60810333760513,
126.632339901676));
#139926=CARTESIAN_POINT('Ctrl Pts',(-258.461028802482,-2.72340254235218,
126.706672520862));
#139927=CARTESIAN_POINT('Ctrl Pts',(-258.468765498388,-2.83539530810336,
126.785689629629));
#139928=CARTESIAN_POINT('Ctrl Pts',(-258.476502285018,-2.94738938713674,
126.86470766499));
#139929=CARTESIAN_POINT('Ctrl Pts',(-258.484239071649,-3.05607662954166,
126.948410073452));
#139930=CARTESIAN_POINT('Ctrl Pts',(-258.491975858279,-3.16105191900665,
127.03647874205));
#139931=CARTESIAN_POINT('Ctrl Pts',(-258.499714421935,-3.2660513197487,
127.124567638723));
#139932=CARTESIAN_POINT('Ctrl Pts',(-258.507452985592,-3.36733677080673,
127.217024539132));
#139933=CARTESIAN_POINT('Ctrl Pts',(-258.515191549248,-3.46453758341159,
127.313492187558));
#139934=CARTESIAN_POINT('Ctrl Pts',(-258.522938467807,-3.56184333840171,
127.410063986812));
#139935=CARTESIAN_POINT('Ctrl Pts',(-258.530685386366,-3.65505536697492,
127.510654907398));
#139936=CARTESIAN_POINT('Ctrl Pts',(-258.538432304925,-3.74384073218759,
127.614871687578));
#139937=CARTESIAN_POINT('Ctrl Pts',(-258.546183413452,-3.83267411749838,
127.719144834031));
#139938=CARTESIAN_POINT('Ctrl Pts',(-258.553934521978,-3.91707582783379,
127.827047438742));
#139939=CARTESIAN_POINT('Ctrl Pts',(-258.561685630505,-3.99675500185125,
127.93815537061));
#139940=CARTESIAN_POINT('Ctrl Pts',(-258.56944937751,-4.07656409580551,
128.049444468205));
#139941=CARTESIAN_POINT('Ctrl Pts',(-258.577213124515,-4.15163505097128,
128.163949008845));
#139942=CARTESIAN_POINT('Ctrl Pts',(-258.58497687152,-4.22172142935844,
128.281217491345));
#139943=CARTESIAN_POINT('Ctrl Pts',(-258.592571874658,-4.29028449091672,
128.395937161123));
#139944=CARTESIAN_POINT('Ctrl Pts',(-258.600166877797,-4.35407734153579,
128.513301519617));
#139945=CARTESIAN_POINT('Ctrl Pts',(-258.607761880935,-4.41291389643242,
128.632869423669));
#139946=CARTESIAN_POINT('Ctrl Pts',(-258.616142080685,-4.47783316948833,
128.764798654153));
#139947=CARTESIAN_POINT('Ctrl Pts',(-258.624522280435,-4.53690193565634,
128.899782543912));
#139948=CARTESIAN_POINT('Ctrl Pts',(-258.632902480184,-4.58984492952747,
129.037299049484));
#139949=CARTESIAN_POINT('Ctrl Pts',(-258.641261557762,-4.64265448135215,
129.174468946703));
#139950=CARTESIAN_POINT('Ctrl Pts',(-258.64962063534,-4.68936894459055,
129.314158454846));
#139951=CARTESIAN_POINT('Ctrl Pts',(-258.657979712918,-4.72976019490264,
129.455823795223));
#139952=CARTESIAN_POINT('Ctrl Pts',(-258.660461085747,-4.74175024405593,
129.497876823573));
#139953=CARTESIAN_POINT('Ctrl Pts',(-258.662942458575,-4.75318341178602,
129.54010380127));
#139954=CARTESIAN_POINT('Ctrl Pts',(-258.665423831404,-4.76405452823398,
129.582490119308));
#139955=CARTESIAN_POINT('Ctrl Pts',(-256.915106732785,-4.76405452823404,
129.582490119308));
#139956=CARTESIAN_POINT('Ctrl Pts',(-256.922429867876,-4.79606782357288,
129.707309471965));
#139957=CARTESIAN_POINT('Ctrl Pts',(-256.929753002967,-4.8231322264902,
129.833231074052));
#139958=CARTESIAN_POINT('Ctrl Pts',(-256.937076138058,-4.84519862184994,
129.959829163253));
#139959=CARTESIAN_POINT('Ctrl Pts',(-256.949180993161,-4.88167350796509,
130.169090839695));
#139960=CARTESIAN_POINT('Ctrl Pts',(-256.961285848263,-4.90459890573453,
130.380778486436));
#139961=CARTESIAN_POINT('Ctrl Pts',(-256.973390703365,-4.91372733444181,
130.593489222495));
#139962=CARTESIAN_POINT('Ctrl Pts',(-256.977307323581,-4.91668090869941,
130.66231343907));
#139963=CARTESIAN_POINT('Ctrl Pts',(-256.981223943798,-4.91819038511672,
130.731244526239));
#139964=CARTESIAN_POINT('Ctrl Pts',(-256.985140564014,-4.91824826888074,
130.800234099472));
#139965=CARTESIAN_POINT('',(-256.639859435963,-4.9182486809668,130.807962654264));
#139966=CARTESIAN_POINT('Ctrl Pts',(-256.569732696692,-4.76405452823407,
129.582490119308));
#139967=CARTESIAN_POINT('Ctrl Pts',(-256.577375070971,-4.79767494244943,
129.713575604073));
#139968=CARTESIAN_POINT('Ctrl Pts',(-256.585017445249,-4.82586170849428,
129.84597521023));
#139969=CARTESIAN_POINT('Ctrl Pts',(-256.592659819528,-4.84853379240785,
129.979192073341));
#139970=CARTESIAN_POINT('Ctrl Pts',(-256.600526422267,-4.87187107882093,
130.116317540118));
#139971=CARTESIAN_POINT('Ctrl Pts',(-256.608393025006,-4.88936503882379,
130.254308498874));
#139972=CARTESIAN_POINT('Ctrl Pts',(-256.616259627745,-4.90098477109259,
130.392618785809));
#139973=CARTESIAN_POINT('Ctrl Pts',(-256.624126230484,-4.91260450336143,
130.530929072745));
#139974=CARTESIAN_POINT('Ctrl Pts',(-256.631992833224,-4.91835004587602,
130.66955822564));
#139975=CARTESIAN_POINT('Ctrl Pts',(-256.639859435963,-4.9182486809668,
130.807962654264));
#139976=CARTESIAN_POINT('Ctrl Pts',(-256.639859435997,-4.91824868096635,
130.807962654868));
#139977=CARTESIAN_POINT('Ctrl Pts',(-256.6526454608,-4.91808392694182,131.032919032592));
#139978=CARTESIAN_POINT('Ctrl Pts',(-256.665431485602,-4.90248437098539,
131.257319986635));
#139979=CARTESIAN_POINT('Ctrl Pts',(-256.678217510405,-4.87168150318488,
131.479566063357));
#139980=CARTESIAN_POINT('Ctrl Pts',(-256.685991856725,-4.85295229175362,
131.614699382361));
#139981=CARTESIAN_POINT('Ctrl Pts',(-256.693766203044,-4.82856655252723,
131.749266871525));
#139982=CARTESIAN_POINT('Ctrl Pts',(-256.701540549363,-4.7985668010147,
131.882757445593));
#139983=CARTESIAN_POINT('Ctrl Pts',(-256.709305314317,-4.76860402220363,
132.016083501394));
#139984=CARTESIAN_POINT('Ctrl Pts',(-256.71707007927,-4.73304108255198,
132.148334905095));
#139985=CARTESIAN_POINT('Ctrl Pts',(-256.724834844224,-4.69197215476163,
132.279006460283));
#139986=CARTESIAN_POINT('Ctrl Pts',(-256.732591896912,-4.65094401822101,
132.40954822742));
#139987=CARTESIAN_POINT('Ctrl Pts',(-256.740348949601,-4.60442089308742,
132.538512898194));
#139988=CARTESIAN_POINT('Ctrl Pts',(-256.748106002289,-4.55254774579543,
132.665406582811));
#139989=CARTESIAN_POINT('Ctrl Pts',(-256.75585720512,-4.5007137178118,132.792204572575));
#139990=CARTESIAN_POINT('Ctrl Pts',(-256.76360840795,-4.4435378457051,132.916934324425));
#139991=CARTESIAN_POINT('Ctrl Pts',(-256.771359610781,-4.38121444901763,
133.039118549473));
#139992=CARTESIAN_POINT('Ctrl Pts',(-256.779107518787,-4.31891754429999,
133.161250837351));
#139993=CARTESIAN_POINT('Ctrl Pts',(-256.786855426793,-4.25147764418569,
133.280839402966));
#139994=CARTESIAN_POINT('Ctrl Pts',(-256.7946033348,-4.17913648783132,133.397428545442));
#139995=CARTESIAN_POINT('Ctrl Pts',(-256.802349621893,-4.10681046572665,
133.513993296696));
#139996=CARTESIAN_POINT('Ctrl Pts',(-256.810095908985,-4.02958543290878,
133.627559540941));
#139997=CARTESIAN_POINT('Ctrl Pts',(-256.817842196078,-3.94774801793461,
133.73769807674));
#139998=CARTESIAN_POINT('Ctrl Pts',(-256.825588540122,-3.86591000128596,
133.847837422285));
#139999=CARTESIAN_POINT('Ctrl Pts',(-256.833334884166,-3.77945976799264,
133.95454869528));
#140000=CARTESIAN_POINT('Ctrl Pts',(-256.84108122821,-3.6887257863977,134.057433800767));
#140001=CARTESIAN_POINT('Ctrl Pts',(-256.848829306752,-3.59797148838824,
134.16034194345));
#140002=CARTESIAN_POINT('Ctrl Pts',(-256.856577385294,-3.50293179196144,
134.259421920673));
#140003=CARTESIAN_POINT('Ctrl Pts',(-256.864325463836,-3.40397347246881,
134.35431099204));
#140004=CARTESIAN_POINT('Ctrl Pts',(-256.872081776682,-3.30490998459592,
134.449300907176));
#140005=CARTESIAN_POINT('Ctrl Pts',(-256.879838089528,-3.20191983719705,
134.540090748283));
#140006=CARTESIAN_POINT('Ctrl Pts',(-256.887594402374,-3.09540489790895,
134.626356376394));
#140007=CARTESIAN_POINT('Ctrl Pts',(-256.895354854772,-2.98883311149377,
134.712668044555));
#140008=CARTESIAN_POINT('Ctrl Pts',(-256.90311530717,-2.87873309846759,
134.794450455455));
#140009=CARTESIAN_POINT('Ctrl Pts',(-256.910875759568,-2.76553660397908,
134.871422254));
#140010=CARTESIAN_POINT('Ctrl Pts',(-256.918648669242,-2.65215840358668,
134.948517609642));
#140011=CARTESIAN_POINT('Ctrl Pts',(-256.926421578916,-2.53567412139693,
135.020786715443));
#140012=CARTESIAN_POINT('Ctrl Pts',(-256.93419448859,-2.41654181946556,
135.087993269565));
#140013=CARTESIAN_POINT('Ctrl Pts',(-256.9416847038,-2.30174226340984,135.15275557544));
#140014=CARTESIAN_POINT('Ctrl Pts',(-256.949174919009,-2.1844842287566,
135.212817034756));
#140015=CARTESIAN_POINT('Ctrl Pts',(-256.956665134218,-2.06519415639283,
135.268008919001));
#140016=CARTESIAN_POINT('Ctrl Pts',(-256.964439548882,-1.9413778891806,
135.325294935785));
#140017=CARTESIAN_POINT('Ctrl Pts',(-256.972213963546,-1.81498016000566,
135.377515999124));
#140018=CARTESIAN_POINT('Ctrl Pts',(-256.97998837821,-1.68645395088644,
135.424431627198));
#140019=CARTESIAN_POINT('Ctrl Pts',(-256.987753212107,-1.55808613049318,
135.471289438997));
#140020=CARTESIAN_POINT('Ctrl Pts',(-256.995518046004,-1.4275954129211,
135.512854691697));
#140021=CARTESIAN_POINT('Ctrl Pts',(-257.003282879901,-1.2954577469346,
135.5489335476));
#140022=CARTESIAN_POINT('Ctrl Pts',(-257.011040002054,-1.1634513151737,
135.584976571322));
#140023=CARTESIAN_POINT('Ctrl Pts',(-257.018797124206,-1.02980156480316,
135.61554393947));
#140024=CARTESIAN_POINT('Ctrl Pts',(-257.026554246358,-0.895002386540549,
135.640490660336));
#140025=CARTESIAN_POINT('Ctrl Pts',(-257.034305519096,-0.760304856319965,
135.665418569624));
#140026=CARTESIAN_POINT('Ctrl Pts',(-257.042056791834,-0.624460006293084,
135.68473419698));
#140027=CARTESIAN_POINT('Ctrl Pts',(-257.049808064571,-0.487974436285498,
135.698343046226));
#140028=CARTESIAN_POINT('Ctrl Pts',(-257.057556042907,-0.351546874596144,
135.711946111517));
#140029=CARTESIAN_POINT('Ctrl Pts',(-257.065304021244,-0.214479522753159,
135.719847184052));
#140030=CARTESIAN_POINT('Ctrl Pts',(-257.07305199958,-0.0772864488981899,
135.72200333205));
#140031=CARTESIAN_POINT('Ctrl Pts',(-257.080798357249,0.0598779278858586,
135.72415902904));
#140032=CARTESIAN_POINT('Ctrl Pts',(-257.088544714918,0.197167583714288,
135.720572185566));
#140033=CARTESIAN_POINT('Ctrl Pts',(-257.096291072587,0.334066481811716,
135.711251960181));
#140034=CARTESIAN_POINT('Ctrl Pts',(-257.104037487386,0.470966389553566,
135.701931666059));
#140035=CARTESIAN_POINT('Ctrl Pts',(-257.111783902185,0.607475143760713,
135.686877932206));
#140036=CARTESIAN_POINT('Ctrl Pts',(-257.119530316984,0.743080263342752,
135.666151931961));
#140037=CARTESIAN_POINT('Ctrl Pts',(-257.127278466393,0.878715748189702,
135.645421290665));
#140038=CARTESIAN_POINT('Ctrl Pts',(-257.135026615802,1.01344680937286,
135.619015914566));
#140039=CARTESIAN_POINT('Ctrl Pts',(-257.142774765211,1.14677000495776,
135.587048315736));
#140040=CARTESIAN_POINT('Ctrl Pts',(-257.150531148695,1.28023488511363,
135.555046744457));
#140041=CARTESIAN_POINT('Ctrl Pts',(-257.158287532179,1.41228853014399,
135.517471233775));
#140042=CARTESIAN_POINT('Ctrl Pts',(-257.166043915663,1.54244100652532,
135.474484684857));
#140043=CARTESIAN_POINT('Ctrl Pts',(-257.173804438687,1.67266294457373,
135.431475194252));
#140044=CARTESIAN_POINT('Ctrl Pts',(-257.181564961711,1.80098132661255,
135.383049049112));
#140045=CARTESIAN_POINT('Ctrl Pts',(-257.189325484734,1.92692606489398,
135.329417413114));
#140046=CARTESIAN_POINT('Ctrl Pts',(-257.197098464293,2.05307295901443,
135.27569969215));
#140047=CARTESIAN_POINT('Ctrl Pts',(-257.204871443852,2.1768382426607,135.21675995174));
#140048=CARTESIAN_POINT('Ctrl Pts',(-257.21264442341,2.29777550775867,135.152855849074));
#140049=CARTESIAN_POINT('Ctrl Pts',(-257.220133868284,2.41430134875486,
135.091282773974));
#140050=CARTESIAN_POINT('Ctrl Pts',(-257.227623313158,2.52820162523055,
135.02510135035));
#140051=CARTESIAN_POINT('Ctrl Pts',(-257.235112758031,2.63910399638473,
134.95457906468));
#140052=CARTESIAN_POINT('Ctrl Pts',(-257.242886884259,2.75422187852779,
134.881376155799));
#140053=CARTESIAN_POINT('Ctrl Pts',(-257.250661010486,2.86647411356299,
134.803263961844));
#140054=CARTESIAN_POINT('Ctrl Pts',(-257.258435136714,2.97541354663934,
134.720493568447));
#140055=CARTESIAN_POINT('Ctrl Pts',(-257.266199681633,3.08421871609441,
134.637825186346));
#140056=CARTESIAN_POINT('Ctrl Pts',(-257.273964226551,3.18971889900276,
134.550510262036));
#140057=CARTESIAN_POINT('Ctrl Pts',(-257.28172877147,3.29149376730582,134.458844417268));
#140058=CARTESIAN_POINT('Ctrl Pts',(-257.289485604404,3.39316754967603,
134.367269617841));
#140059=CARTESIAN_POINT('Ctrl Pts',(-257.297242437338,3.49112309215199,
134.271352757835));
#140060=CARTESIAN_POINT('Ctrl Pts',(-257.304999270271,3.58497146246548,
134.171430957759));
#140061=CARTESIAN_POINT('Ctrl Pts',(-257.312750253849,3.6787490625934,134.071584507786));
#140062=CARTESIAN_POINT('Ctrl Pts',(-257.320501237427,3.76842538871227,
133.967739412882));
#140063=CARTESIAN_POINT('Ctrl Pts',(-257.328252221005,3.85364712108406,
133.860270781275));
#140064=CARTESIAN_POINT('Ctrl Pts',(-257.335999911282,3.93883264375147,
133.752847811816));
#140065=CARTESIAN_POINT('Ctrl Pts',(-257.343747601559,4.01956709467813,
133.641804673502));
#140066=CARTESIAN_POINT('Ctrl Pts',(-257.351495291836,4.09553649901408,
133.52755063072));
#140067=CARTESIAN_POINT('Ctrl Pts',(-257.359241362153,4.17149001895948,
133.413320477238));
#140068=CARTESIAN_POINT('Ctrl Pts',(-257.366987432471,4.24268025769708,
133.295881080046));
#140069=CARTESIAN_POINT('Ctrl Pts',(-257.374733502789,4.30883600091209,
133.175671516572));
#140070=CARTESIAN_POINT('Ctrl Pts',(-257.382479631211,4.37499224037473,
133.055461051381));
#140071=CARTESIAN_POINT('Ctrl Pts',(-257.390225759633,4.43611372044746,
132.932480720985));
#140072=CARTESIAN_POINT('Ctrl Pts',(-257.397971888056,4.49197491009745,
132.807194726911));
#140073=CARTESIAN_POINT('Ctrl Pts',(-257.40571975233,4.54784861783948,132.681880657143));
#140074=CARTESIAN_POINT('Ctrl Pts',(-257.413467616605,4.59845953030864,
132.55426025259));
#140075=CARTESIAN_POINT('Ctrl Pts',(-257.421215480879,4.64363019511848,
132.424817859669));
#140076=CARTESIAN_POINT('Ctrl Pts',(-257.428971582797,4.68884888604488,
132.295237841688));
#140077=CARTESIAN_POINT('Ctrl Pts',(-257.436727684715,4.72861564582192,
132.163832335389));
#140078=CARTESIAN_POINT('Ctrl Pts',(-257.444483786632,4.7628027175212,132.031101558626));
#140079=CARTESIAN_POINT('Ctrl Pts',(-257.452244029583,4.79700804191968,
131.898299916041));
#140080=CARTESIAN_POINT('Ctrl Pts',(-257.460004272534,4.82562766072816,
131.764171975294));
#140081=CARTESIAN_POINT('Ctrl Pts',(-257.467764515485,4.84858514897815,
131.629227343534));
#140082=CARTESIAN_POINT('Ctrl Pts',(-257.475537220362,4.87157950392382,
131.494066008508));
#140083=CARTESIAN_POINT('Ctrl Pts',(-257.483309925238,4.88889350892239,
131.358085749759));
#140084=CARTESIAN_POINT('Ctrl Pts',(-257.491082630115,4.90050265488211,
131.221801382218));
#140085=CARTESIAN_POINT('Ctrl Pts',(-257.498575214025,4.91169341814975,
131.090428574991));
#140086=CARTESIAN_POINT('Ctrl Pts',(-257.506067797935,4.9175834303487,130.958773509831));
#140087=CARTESIAN_POINT('Ctrl Pts',(-257.513560381844,4.91819652859018,
130.827294624271));
#140088=CARTESIAN_POINT('Ctrl Pts',(-257.521334853192,4.91883269293202,
130.690869214703));
#140089=CARTESIAN_POINT('Ctrl Pts',(-257.52910932454,4.91378912490896,130.554201241754));
#140090=CARTESIAN_POINT('Ctrl Pts',(-257.536883795887,4.90303538749604,
130.417802664005));
#140091=CARTESIAN_POINT('Ctrl Pts',(-257.544648684898,4.89229490448109,
130.281572202787));
#140092=CARTESIAN_POINT('Ctrl Pts',(-257.552413573909,4.87585828604941,
130.145610862108));
#140093=CARTESIAN_POINT('Ctrl Pts',(-257.560178462919,4.85374706526777,
130.010432101323));
#140094=CARTESIAN_POINT('Ctrl Pts',(-257.567935638579,4.83165780894596,
129.875387622062));
#140095=CARTESIAN_POINT('Ctrl Pts',(-257.57569281424,4.8039052307422,129.741124558989));
#140096=CARTESIAN_POINT('Ctrl Pts',(-257.5834499899,4.7705627478743,129.608152386908));
#140097=CARTESIAN_POINT('Ctrl Pts',(-257.591201314504,4.73724541446206,
129.475280512629));
#140098=CARTESIAN_POINT('Ctrl Pts',(-257.598952639107,4.69834666345011,
129.343697968952));
#140099=CARTESIAN_POINT('Ctrl Pts',(-257.606703963711,4.65399112145413,
129.213904801164));
#140100=CARTESIAN_POINT('Ctrl Pts',(-257.614451991261,4.60965444625133,
129.084166841379));
#140101=CARTESIAN_POINT('Ctrl Pts',(-257.62220001881,4.55986572266236,128.956217112845));
#140102=CARTESIAN_POINT('Ctrl Pts',(-257.62994804636,4.50479958044842,128.830541020315));
#140103=CARTESIAN_POINT('Ctrl Pts',(-257.637694451625,4.44974496799959,
128.704891241882));
#140104=CARTESIAN_POINT('Ctrl Pts',(-257.64544085689,4.38941529160877,128.581514510411));
#140105=CARTESIAN_POINT('Ctrl Pts',(-257.653187262155,4.32403337665568,
128.460876369685));
#140106=CARTESIAN_POINT('Ctrl Pts',(-257.660933722896,4.25865099346387,
128.340237364997));
#140107=CARTESIAN_POINT('Ctrl Pts',(-257.668680183638,4.18821648578911,
128.222337333908));
#140108=CARTESIAN_POINT('Ctrl Pts',(-257.67642664438,4.11299850975596,128.107616966188));
#140109=CARTESIAN_POINT('Ctrl Pts',(-257.68417483804,4.03776370712001,127.992870935002));
#140110=CARTESIAN_POINT('Ctrl Pts',(-257.6919230317,3.95774352110598,127.881306309479));
#140111=CARTESIAN_POINT('Ctrl Pts',(-257.69967122536,3.87324954452746,127.77333421908));
#140112=CARTESIAN_POINT('Ctrl Pts',(-257.707427650194,3.7886658070849,127.665247426208));
#140113=CARTESIAN_POINT('Ctrl Pts',(-257.715184075027,3.69959902644132,
127.560761100655));
#140114=CARTESIAN_POINT('Ctrl Pts',(-257.72294049986,3.60640101062734,127.460253141266));
#140115=CARTESIAN_POINT('Ctrl Pts',(-257.730701062721,3.51315327398186,
127.359691561215));
#140116=CARTESIAN_POINT('Ctrl Pts',(-257.738461625581,3.41577018795562,
127.263112851648));
#140117=CARTESIAN_POINT('Ctrl Pts',(-257.746222188441,3.31463920771752,
127.170856800978));
#140118=CARTESIAN_POINT('Ctrl Pts',(-257.753995204865,3.21334594014211,
127.078452704785));
#140119=CARTESIAN_POINT('Ctrl Pts',(-257.761768221289,3.10829305956532,
126.990385380488));
#140120=CARTESIAN_POINT('Ctrl Pts',(-257.769541237712,2.99990046564037,
126.906953754182));
#140121=CARTESIAN_POINT('Ctrl Pts',(-257.777030160361,2.89546948192646,
126.826571446753));
#140122=CARTESIAN_POINT('Ctrl Pts',(-257.784519083009,2.78793889786747,
126.750492074074));
#140123=CARTESIAN_POINT('Ctrl Pts',(-257.792008005657,2.67770667734081,
126.678943061412));
#140124=CARTESIAN_POINT('Ctrl Pts',(-257.799782800979,2.56326659126626,
126.604662827117));
#140125=CARTESIAN_POINT('Ctrl Pts',(-257.807557596301,2.44555223334035,
126.535030546044));
#140126=CARTESIAN_POINT('Ctrl Pts',(-257.815332391623,2.32497793458195,
126.47034854257));
#140127=CARTESIAN_POINT('Ctrl Pts',(-257.823097608641,2.20455217956887,
126.405746225291));
#140128=CARTESIAN_POINT('Ctrl Pts',(-257.83086282566,2.08127383534646,126.34608223423));
#140129=CARTESIAN_POINT('Ctrl Pts',(-257.838628042678,1.95558658271125,
126.291615978212));
#140130=CARTESIAN_POINT('Ctrl Pts',(-257.846385549992,1.83002411881898,
126.237203799083));
#140131=CARTESIAN_POINT('Ctrl Pts',(-257.854143057305,1.70205786245693,
126.187979239617));
#140132=CARTESIAN_POINT('Ctrl Pts',(-257.861900564618,1.57215618295987,
126.144155901153));
#140133=CARTESIAN_POINT('Ctrl Pts',(-257.869652224138,1.44235242644127,
126.100365597765));
#140134=CARTESIAN_POINT('Ctrl Pts',(-257.877403883657,1.31061651968804,
126.0619685356));
#140135=CARTESIAN_POINT('Ctrl Pts',(-257.885155543177,1.17743657511444,
126.029130133696));
#140136=CARTESIAN_POINT('Ctrl Pts',(-257.89290390938,1.04431321246085,125.996305683291));
#140137=CARTESIAN_POINT('Ctrl Pts',(-257.900652275582,0.909747410954359,
125.969035289451));
#140138=CARTESIAN_POINT('Ctrl Pts',(-257.908400641785,0.774241990431667,
125.94743438766));
#140139=CARTESIAN_POINT('Ctrl Pts',(-257.916147387925,0.638764901973453,
125.925838002279));
#140140=CARTESIAN_POINT('Ctrl Pts',(-257.923894134065,0.502348971063077,
125.909908812609));
#140141=CARTESIAN_POINT('Ctrl Pts',(-257.931640880206,0.365506356057829,
125.899710969917));
#140142=CARTESIAN_POINT('Ctrl Pts',(-257.939387683711,0.228662727719137,
125.88951305171));
#140143=CARTESIAN_POINT('Ctrl Pts',(-257.947134487217,0.0913927988120277,
125.885046594219));
#140144=CARTESIAN_POINT('Ctrl Pts',(-257.954881290723,-0.0457874123577805,
125.886323755629));
#140145=CARTESIAN_POINT('Ctrl Pts',(-257.962629828704,-0.182998337571502,
125.887601202991));
#140146=CARTESIAN_POINT('Ctrl Pts',(-257.970378366685,-0.320119114255745,
125.894624824555));
#140147=CARTESIAN_POINT('Ctrl Pts',(-257.978126904666,-0.456635387480373,
125.907354676647));
#140148=CARTESIAN_POINT('Ctrl Pts',(-257.985883674301,-0.593296688685096,
125.920098052289));
#140149=CARTESIAN_POINT('Ctrl Pts',(-257.993640443937,-0.729351813734129,
125.938559731631));
#140150=CARTESIAN_POINT('Ctrl Pts',(-258.001397213572,-0.864292629606964,
125.962647975029));
#140151=CARTESIAN_POINT('Ctrl Pts',(-258.009158122043,-0.999305446825205,
125.986749071364));
#140152=CARTESIAN_POINT('Ctrl Pts',(-258.016919030515,-1.13320238870135,
126.016482629223));
#140153=CARTESIAN_POINT('Ctrl Pts',(-258.024679938986,-1.26548811816278,
126.05170631862));
#140154=CARTESIAN_POINT('Ctrl Pts',(-258.032453298865,-1.39798608355804,
126.086986520028));
#140155=CARTESIAN_POINT('Ctrl Pts',(-258.040226658745,-1.52886729747962,
126.127774338258));
#140156=CARTESIAN_POINT('Ctrl Pts',(-258.048000018625,-1.65765326508232,
126.173878060071));
#140157=CARTESIAN_POINT('Ctrl Pts',(-258.05548522224,-1.78166517308229,
126.218272729882));
#140158=CARTESIAN_POINT('Ctrl Pts',(-258.062970425854,-1.90373413762637,
126.267596055785));
#140159=CARTESIAN_POINT('Ctrl Pts',(-258.070455629469,-2.02345433243006,
126.321636487411));
#140160=CARTESIAN_POINT('Ctrl Pts',(-258.078229099559,-2.14778513240421,
126.377758097521));
#140161=CARTESIAN_POINT('Ctrl Pts',(-258.086002569648,-2.2699766705071,
126.439145286734));
#140162=CARTESIAN_POINT('Ctrl Pts',(-258.093776039737,-2.38955067604954,
126.505613052392));
#140163=CARTESIAN_POINT('Ctrl Pts',(-258.101539798875,-2.50897530461983,
126.571997783668));
#140164=CARTESIAN_POINT('Ctrl Pts',(-258.109303558012,-2.62578856848527,
126.643450274066));
#140165=CARTESIAN_POINT('Ctrl Pts',(-258.11706731715,-2.73953245162599,
126.719737622847));
#140166=CARTESIAN_POINT('Ctrl Pts',(-258.124823236471,-2.85316147660633,
126.79594793694));
#140167=CARTESIAN_POINT('Ctrl Pts',(-258.132579155793,-2.96372696652871,
126.876983176398));
#140168=CARTESIAN_POINT('Ctrl Pts',(-258.140335075115,-3.07079611464425,
126.962564906601));
#140169=CARTESIAN_POINT('Ctrl Pts',(-258.148084607211,-3.17777708819573,
127.048076157755));
#140170=CARTESIAN_POINT('Ctrl Pts',(-258.155834139307,-3.28126714906281,
127.138126200936));
#140171=CARTESIAN_POINT('Ctrl Pts',(-258.163583671403,-3.38086343512353,
127.232394003004));
#140172=CARTESIAN_POINT('Ctrl Pts',(-258.171329725354,-3.48041502037351,
127.326619495792));
#140173=CARTESIAN_POINT('Ctrl Pts',(-258.179075779304,-3.57607602433451,
127.425058713004));
#140174=CARTESIAN_POINT('Ctrl Pts',(-258.186821833255,-3.66747770404219,
127.527351256448));
#140175=CARTESIAN_POINT('Ctrl Pts',(-258.194566089714,-3.75885817376112,
127.629620062652));
#140176=CARTESIAN_POINT('Ctrl Pts',(-258.202310346174,-3.84598102601229,
127.735740124088));
#140177=CARTESIAN_POINT('Ctrl Pts',(-258.210054602633,-3.9285156279429,
127.845315497344));
#140178=CARTESIAN_POINT('Ctrl Pts',(-258.217798740691,-4.01104896800664,
127.954889195309));
#140179=CARTESIAN_POINT('Ctrl Pts',(-258.225542878749,-4.08899396318763,
128.067917786909));
#140180=CARTESIAN_POINT('Ctrl Pts',(-258.233287016807,-4.16206164266541,
128.183974015335));
#140181=CARTESIAN_POINT('Ctrl Pts',(-258.241036109274,-4.23517606810922,
128.300104492191));
#140182=CARTESIAN_POINT('Ctrl Pts',(-258.248785201742,-4.30340673492681,
128.419266144586));
#140183=CARTESIAN_POINT('Ctrl Pts',(-258.256534294209,-4.36650909341112,
128.541004392917));
#140184=CARTESIAN_POINT('Ctrl Pts',(-258.264285952437,-4.42963234537518,
128.662782949339));
#140185=CARTESIAN_POINT('Ctrl Pts',(-258.272037610665,-4.48762373703312,
128.787139448687));
#140186=CARTESIAN_POINT('Ctrl Pts',(-258.279789268892,-4.54028613560329,
128.913597578645));
#140187=CARTESIAN_POINT('Ctrl Pts',(-258.287549765891,-4.59300858208599,
129.040199901556));
#140188=CARTESIAN_POINT('Ctrl Pts',(-258.29531026289,-4.64038975854418,
129.168908276302));
#140189=CARTESIAN_POINT('Ctrl Pts',(-258.303070759888,-4.68228167746306,
129.299228943793));
#140190=CARTESIAN_POINT('Ctrl Pts',(-258.308647566738,-4.71238582419431,
129.392879284897));
#140191=CARTESIAN_POINT('Ctrl Pts',(-258.314224373587,-4.73965632075143,
129.487361878628));
#140192=CARTESIAN_POINT('Ctrl Pts',(-258.319801180436,-4.76405452823419,
129.582490119309));
#140193=CARTESIAN_POINT('Origin',(210.,0.,130.804360617566));
#140194=CARTESIAN_POINT('',(209.436623794218,-5.91986778237144,130.801550299888));
#140195=CARTESIAN_POINT('',(209.999781618288,2.5839291206855,125.481650700449));
#140196=CARTESIAN_POINT('Ctrl Pts',(209.436624807795,-5.91674932306679,
130.801530336897));
#140197=CARTESIAN_POINT('Ctrl Pts',(209.445314454709,-5.91666144223196,
130.617813974195));
#140198=CARTESIAN_POINT('Ctrl Pts',(209.454004101622,-5.90801760417395,
130.434327549234));
#140199=CARTESIAN_POINT('Ctrl Pts',(209.462693748535,-5.89087755369375,
130.251647120456));
#140200=CARTESIAN_POINT('Ctrl Pts',(209.470129292751,-5.87621118065508,
130.095331401409));
#140201=CARTESIAN_POINT('Ctrl Pts',(209.477564836966,-5.85529721592649,
129.939370695698));
#140202=CARTESIAN_POINT('Ctrl Pts',(209.485000381182,-5.82815696752497,
129.784303303299));
#140203=CARTESIAN_POINT('Ctrl Pts',(209.492427278008,-5.80104828268818,
129.629416251167));
#140204=CARTESIAN_POINT('Ctrl Pts',(209.499854174835,-5.76772779211504,
129.475420807086));
#140205=CARTESIAN_POINT('Ctrl Pts',(209.507281071662,-5.72826867527633,
129.322851742686));
#140206=CARTESIAN_POINT('Ctrl Pts',(209.51470093492,-5.68884692779981,129.170427167293));
#140207=CARTESIAN_POINT('Ctrl Pts',(209.522120798179,-5.64329822100986,
129.0194266398));
#140208=CARTESIAN_POINT('Ctrl Pts',(209.529540661437,-5.59174703436072,
128.870376215815));
#140209=CARTESIAN_POINT('Ctrl Pts',(209.536955099496,-5.54023354052269,
128.721434773403));
#140210=CARTESIAN_POINT('Ctrl Pts',(209.544369537554,-5.48272642729368,
128.574440945163));
#140211=CARTESIAN_POINT('Ctrl Pts',(209.551783975613,-5.41940037535893,
128.429906967974));
#140212=CARTESIAN_POINT('Ctrl Pts',(209.559194592598,-5.35610695887099,
128.285447477206));
#140213=CARTESIAN_POINT('Ctrl Pts',(209.566605209583,-5.28700072526885,
128.143445652368));
#140214=CARTESIAN_POINT('Ctrl Pts',(209.574015826567,-5.21230494212194,
128.004394947628));
#140215=CARTESIAN_POINT('Ctrl Pts',(209.581425300872,-5.13762067669639,
127.865365683821));
#140216=CARTESIAN_POINT('Ctrl Pts',(209.588834775176,-5.05734874775978,
127.729286964407));
#140217=CARTESIAN_POINT('Ctrl Pts',(209.596244249481,-4.97175901792443,
127.596628890911));
#140218=CARTESIAN_POINT('Ctrl Pts',(209.603653447896,-4.88617247499418,
127.463975756894));
#140219=CARTESIAN_POINT('Ctrl Pts',(209.611062646311,-4.79526872641441,
127.334743328014));
#140220=CARTESIAN_POINT('Ctrl Pts',(209.618471844726,-4.69936158985239,
127.209373662051));
#140221=CARTESIAN_POINT('Ctrl Pts',(209.625882215991,-4.60343927153547,
127.083984150522));
#140222=CARTESIAN_POINT('Ctrl Pts',(209.633292587255,-4.5025122140518,126.962458914826));
#140223=CARTESIAN_POINT('Ctrl Pts',(209.64070295852,-4.39693514121467,126.845207687146));
#140224=CARTESIAN_POINT('Ctrl Pts',(209.648115951785,-4.2913207121981,126.727914972638));
#140225=CARTESIAN_POINT('Ctrl Pts',(209.655528945051,-4.18105324043719,
126.61489955342));
#140226=CARTESIAN_POINT('Ctrl Pts',(209.662941938316,-4.06652488048987,
126.506534892987));
#140227=CARTESIAN_POINT('Ctrl Pts',(209.670363046154,-3.95187115301046,
126.398051612064));
#140228=CARTESIAN_POINT('Ctrl Pts',(209.677784153991,-3.83294749285477,
126.294229512671));
#140229=CARTESIAN_POINT('Ctrl Pts',(209.685205261829,-3.71018032603156,
126.195402762386));
#140230=CARTESIAN_POINT('Ctrl Pts',(209.692630935426,-3.58733762799181,
126.096515209975));
#140231=CARTESIAN_POINT('Ctrl Pts',(209.700056609023,-3.4606470090426,126.002629352074));
#140232=CARTESIAN_POINT('Ctrl Pts',(209.70748228262,-3.33056413386467,125.914036179176));
#140233=CARTESIAN_POINT('Ctrl Pts',(209.71491844568,-3.20029750436431,125.825317860071));
#140234=CARTESIAN_POINT('Ctrl Pts',(209.722354608741,-3.06662936267343,
125.741907354593));
#140235=CARTESIAN_POINT('Ctrl Pts',(209.729790771801,-2.93004094085217,
125.664050252673));
#140236=CARTESIAN_POINT('Ctrl Pts',(209.733574305317,-2.86054449925481,
125.624436415245));
#140237=CARTESIAN_POINT('Ctrl Pts',(209.737357838833,-2.79029240399966,
125.586259478074));
#140238=CARTESIAN_POINT('Ctrl Pts',(209.741141372349,-2.71934995185403,
125.549546976546));
#140239=CARTESIAN_POINT('Ctrl Pts',(209.748429935947,-2.58268707519309,
125.478824356781));
#140240=CARTESIAN_POINT('Ctrl Pts',(209.755718499544,-2.44301584246147,
125.413308818321));
#140241=CARTESIAN_POINT('Ctrl Pts',(209.763007063142,-2.30077949620412,
125.353274095381));
#140242=CARTESIAN_POINT('Ctrl Pts',(209.770286840669,-2.15871461013878,
125.293311741883));
#140243=CARTESIAN_POINT('Ctrl Pts',(209.777566618197,-2.01409111408332,
125.238817210897));
#140244=CARTESIAN_POINT('Ctrl Pts',(209.784846395724,-1.86737837579021,
125.190019288066));
#140245=CARTESIAN_POINT('Ctrl Pts',(209.792119116272,-1.72080786008898,
125.141268669697));
#140246=CARTESIAN_POINT('Ctrl Pts',(209.799391836819,-1.5721524963476,125.098203794501));
#140247=CARTESIAN_POINT('Ctrl Pts',(209.806664557367,-1.42190296680508,
125.061005978029));
#140248=CARTESIAN_POINT('Ctrl Pts',(209.813931941926,-1.27176367521208,
125.023835453562));
#140249=CARTESIAN_POINT('Ctrl Pts',(209.821199326485,-1.1200329197269,124.992523514836));
#140250=CARTESIAN_POINT('Ctrl Pts',(209.828466711043,-0.967217642662254,
124.967202011341));
#140251=CARTESIAN_POINT('Ctrl Pts',(209.835731111368,-0.814465116728247,
124.941890905714));
#140252=CARTESIAN_POINT('Ctrl Pts',(209.842995511692,-0.660629336190675,
124.922565407679));
#140253=CARTESIAN_POINT('Ctrl Pts',(209.850259912017,-0.506228400192777,
124.909306472833));
#140254=CARTESIAN_POINT('Ctrl Pts',(209.857522871346,-0.351858091776005,
124.896050168081));
#140255=CARTESIAN_POINT('Ctrl Pts',(209.864785830675,-0.196923236786615,
124.88885806683));
#140256=CARTESIAN_POINT('Ctrl Pts',(209.872048790004,-0.041947692904324,
124.887759316687));
#140257=CARTESIAN_POINT('Ctrl Pts',(209.879311856424,0.113030136058688,
124.886660550344));
#140258=CARTESIAN_POINT('Ctrl Pts',(209.886574922844,0.268048267459926,
124.891655316722));
#140259=CARTESIAN_POINT('Ctrl Pts',(209.893837989264,0.422582550641461,
124.90272062936));
#140260=CARTESIAN_POINT('Ctrl Pts',(209.901102710863,0.577152050615399,
124.913788463671));
#140261=CARTESIAN_POINT('Ctrl Pts',(209.908367432462,0.731237096509864,
124.930929568337));
#140262=CARTESIAN_POINT('Ctrl Pts',(209.915632154061,0.884318713515213,
124.954069088469));
#140263=CARTESIAN_POINT('Ctrl Pts',(209.922904372259,1.03755829824375,124.977232486695));
#140264=CARTESIAN_POINT('Ctrl Pts',(209.930176590457,1.18979200252811,125.006406603914));
#140265=CARTESIAN_POINT('Ctrl Pts',(209.937448808656,1.34051053729742,125.041465332911));
#140266=CARTESIAN_POINT('Ctrl Pts',(209.944724904051,1.491309427951,125.076542753539));
#140267=CARTESIAN_POINT('Ctrl Pts',(209.952000999447,1.64059116756246,125.117510930441));
#140268=CARTESIAN_POINT('Ctrl Pts',(209.959277094843,1.78786254938573,125.164194124722));
#140269=CARTESIAN_POINT('Ctrl Pts',(209.966564295703,1.93535871072363,125.210948571309));
#140270=CARTESIAN_POINT('Ctrl Pts',(209.973851496564,2.08083802164559,125.263435326559));
#140271=CARTESIAN_POINT('Ctrl Pts',(209.981138697425,2.22382735036804,125.321430517861));
#140272=CARTESIAN_POINT('Ctrl Pts',(209.987353004379,2.34576437349178,125.370887082528));
#140273=CARTESIAN_POINT('Ctrl Pts',(209.993567311334,2.46589090244907,125.42434861294));
#140274=CARTESIAN_POINT('Ctrl Pts',(209.999781618288,2.5839291206855,125.481650700449));
#140275=CARTESIAN_POINT('',(210.,-2.58391981636517,125.481646183642));
#140276=CARTESIAN_POINT('Origin',(210.,0.,130.804360617566));
#140277=CARTESIAN_POINT('',(209.688375192173,-5.9167497157184,130.802526483902));
#140278=CARTESIAN_POINT('Ctrl Pts',(209.999999999999,-2.58391981636503,
125.481646183643));
#140279=CARTESIAN_POINT('Ctrl Pts',(209.99131183034,-2.74995620526197,125.562248801129));
#140280=CARTESIAN_POINT('Ctrl Pts',(209.982623660682,-2.91209254072039,
125.650562775723));
#140281=CARTESIAN_POINT('Ctrl Pts',(209.973935491023,-3.06969027976343,
125.746205603252));
#140282=CARTESIAN_POINT('Ctrl Pts',(209.965231695902,-3.22757145453489,
125.842020442098));
#140283=CARTESIAN_POINT('Ctrl Pts',(209.95652790078,-3.38089761558052,125.94519044461));
#140284=CARTESIAN_POINT('Ctrl Pts',(209.947824105658,-3.52905730190805,
126.05528859007));
#140285=CARTESIAN_POINT('Ctrl Pts',(209.939119990154,-3.67722244191973,
126.165390788187));
#140286=CARTESIAN_POINT('Ctrl Pts',(209.93041587465,-3.82022064776757,126.282421571801));
#140287=CARTESIAN_POINT('Ctrl Pts',(209.921711759146,-3.9574720567728,126.405912540987));
#140288=CARTESIAN_POINT('Ctrl Pts',(209.913018683697,-4.09454937995234,
126.529246877702));
#140289=CARTESIAN_POINT('Ctrl Pts',(209.904325608248,-4.22589438898566,
126.659024962998));
#140290=CARTESIAN_POINT('Ctrl Pts',(209.895632532799,-4.35096223417733,
126.794739912404));
#140291=CARTESIAN_POINT('Ctrl Pts',(209.886971363206,-4.47557104773246,
126.929956752522));
#140292=CARTESIAN_POINT('Ctrl Pts',(209.878310193613,-4.59394860132631,
127.071066895327));
#140293=CARTESIAN_POINT('Ctrl Pts',(209.86964902402,-4.70558990066976,127.217529948408));
#140294=CARTESIAN_POINT('Ctrl Pts',(209.866691412045,-4.74371311720728,
127.267544080455));
#140295=CARTESIAN_POINT('Ctrl Pts',(209.863733800069,-4.78105112881579,
127.318182073746));
#140296=CARTESIAN_POINT('Ctrl Pts',(209.860776188094,-4.81758476774297,
127.369421379659));
#140297=CARTESIAN_POINT('Ctrl Pts',(209.853352615767,-4.90928378479419,
127.498031453132));
#140298=CARTESIAN_POINT('Ctrl Pts',(209.84592904344,-4.99586157637515,127.63036143513));
#140299=CARTESIAN_POINT('Ctrl Pts',(209.838505471113,-5.07701336223303,
127.765962045586));
#140300=CARTESIAN_POINT('Ctrl Pts',(209.831082830258,-5.15815496558327,
127.901545641577));
#140301=CARTESIAN_POINT('Ctrl Pts',(209.823660189402,-5.23387172917773,
128.040398730499));
#140302=CARTESIAN_POINT('Ctrl Pts',(209.816237548547,-5.30390330506813,
128.182044791242));
#140303=CARTESIAN_POINT('Ctrl Pts',(209.808814397566,-5.37393969391849,
128.323700586692));
#140304=CARTESIAN_POINT('Ctrl Pts',(209.801391246585,-5.43828995410957,
128.468149403269));
#140305=CARTESIAN_POINT('Ctrl Pts',(209.793968095605,-5.4967406783166,128.614892079806));
#140306=CARTESIAN_POINT('Ctrl Pts',(209.786540360911,-5.55522749519685,
128.761725368317));
#140307=CARTESIAN_POINT('Ctrl Pts',(209.779112626217,-5.60780736360233,
128.910855000888));
#140308=CARTESIAN_POINT('Ctrl Pts',(209.771684891523,-5.65431567064078,
129.061763458368));
#140309=CARTESIAN_POINT('Ctrl Pts',(209.764254403954,-5.70084121463515,
129.212727845693));
#140310=CARTESIAN_POINT('Ctrl Pts',(209.756823916385,-5.74129061476954,
129.365472014495));
#140311=CARTESIAN_POINT('Ctrl Pts',(209.749393428817,-5.77554982777,129.519465777727));
#140312=CARTESIAN_POINT('Ctrl Pts',(209.74195603147,-5.80984089918891,129.673602743248));
#140313=CARTESIAN_POINT('Ctrl Pts',(209.734518634122,-5.8379302216951,129.828991259508));
#140314=CARTESIAN_POINT('Ctrl Pts',(209.727081236775,-5.85975521629992,
129.985093037623));
#140315=CARTESIAN_POINT('Ctrl Pts',(209.725238283246,-5.86516335155979,
130.023774354418));
#140316=CARTESIAN_POINT('Ctrl Pts',(209.723395329716,-5.87018709070327,
130.062499450682));
#140317=CARTESIAN_POINT('Ctrl Pts',(209.721552376187,-5.87482597569107,
130.101260114192));
#140318=CARTESIAN_POINT('Ctrl Pts',(209.71049331486,-5.90266265890184,130.333852281056));
#140319=CARTESIAN_POINT('Ctrl Pts',(209.699434253533,-5.91667702418257,
130.568030238081));
#140320=CARTESIAN_POINT('Ctrl Pts',(209.688375192206,-5.91674971571818,
130.802526483197));
#140321=CARTESIAN_POINT('',(207.938375235231,-5.91423241434992,130.80143089854));
#140322=CARTESIAN_POINT('Ctrl Pts',(209.688375192173,-5.9167497157184,130.802526483902));
#140323=CARTESIAN_POINT('Ctrl Pts',(209.680943409138,-5.91679856502823,
130.960109950051));
#140324=CARTESIAN_POINT('Ctrl Pts',(209.673511626102,-5.9105476477549,131.117854987543));
#140325=CARTESIAN_POINT('Ctrl Pts',(209.666079843067,-5.8979845522807,131.27522023949));
#140326=CARTESIAN_POINT('Ctrl Pts',(209.658653719117,-5.88543102323509,
131.432465662415));
#140327=CARTESIAN_POINT('Ctrl Pts',(209.651227595166,-5.8665749164667,131.589331507636));
#140328=CARTESIAN_POINT('Ctrl Pts',(209.643801471216,-5.8414558785676,131.745277075732));
#140329=CARTESIAN_POINT('Ctrl Pts',(209.636379410181,-5.81635058357617,
131.901137324257));
#140330=CARTESIAN_POINT('Ctrl Pts',(209.628957349147,-5.78498924065305,
132.056077933289));
#140331=CARTESIAN_POINT('Ctrl Pts',(209.621535288112,-5.74746325356225,
132.20956405887));
#140332=CARTESIAN_POINT('Ctrl Pts',(209.614100682456,-5.70987384078865,
132.36330960367));
#140333=CARTESIAN_POINT('Ctrl Pts',(209.606666076801,-5.66609898337391,
132.515595374754));
#140334=CARTESIAN_POINT('Ctrl Pts',(209.599231471145,-5.61628193033324,
132.665894351215));
#140335=CARTESIAN_POINT('Ctrl Pts',(209.59181124687,-5.56656124259613,132.815902591761));
#140336=CARTESIAN_POINT('Ctrl Pts',(209.584391022596,-5.51082184033433,
132.963931367112));
#140337=CARTESIAN_POINT('Ctrl Pts',(209.576970798321,-5.4492558567059,133.109472582451));
#140338=CARTESIAN_POINT('Ctrl Pts',(209.569549627897,-5.38768202282445,
133.25503235569));
#140339=CARTESIAN_POINT('Ctrl Pts',(209.562128457473,-5.32028027222218,
133.398103595494));
#140340=CARTESIAN_POINT('Ctrl Pts',(209.554707287049,-5.24729052265184,
133.538199079032));
#140341=CARTESIAN_POINT('Ctrl Pts',(209.547283729025,-5.17427729022698,
133.678339635224));
#140342=CARTESIAN_POINT('Ctrl Pts',(209.539860171002,-5.09567264996152,
133.815502199823));
#140343=CARTESIAN_POINT('Ctrl Pts',(209.532436612979,-5.01176195446012,
133.94922510977));
#140344=CARTESIAN_POINT('Ctrl Pts',(209.524992291262,-4.92761656072304,
134.083322042729));
#140345=CARTESIAN_POINT('Ctrl Pts',(209.517547969545,-4.83813559558281,
134.213959741109));
#140346=CARTESIAN_POINT('Ctrl Pts',(209.510103647828,-4.74364932018439,
134.340703600029));
#140347=CARTESIAN_POINT('Ctrl Pts',(209.50266720501,-4.64926304689699,134.467313316149));
#140348=CARTESIAN_POINT('Ctrl Pts',(209.495230762193,-4.54988231892117,
134.590037168706));
#140349=CARTESIAN_POINT('Ctrl Pts',(209.487794319376,-4.44587511023585,
134.708477043428));
#140350=CARTESIAN_POINT('Ctrl Pts',(209.480345730974,-4.3416980315738,134.827110360307));
#140351=CARTESIAN_POINT('Ctrl Pts',(209.472897142572,-4.23287962656979,
134.941445447219));
#140352=CARTESIAN_POINT('Ctrl Pts',(209.46544855417,-4.11982451206075,135.05112133043));
#140353=CARTESIAN_POINT('Ctrl Pts',(209.458000620238,-4.00677933114232,
135.160787576966));
#140354=CARTESIAN_POINT('Ctrl Pts',(209.450552686306,-3.88949849868325,
135.265795238245));
#140355=CARTESIAN_POINT('Ctrl Pts',(209.443104752375,-3.76841686049243,
135.365825834802));
#140356=CARTESIAN_POINT('Ctrl Pts',(209.435742893708,-3.64873455454395,
135.464700384571));
#140357=CARTESIAN_POINT('Ctrl Pts',(209.428381035041,-3.52494699684348,
135.559035800125));
#140358=CARTESIAN_POINT('Ctrl Pts',(209.421019176375,-3.39743599074722,
135.648466236901));
#140359=CARTESIAN_POINT('Ctrl Pts',(209.413666779922,-3.27008887484194,
135.73778172853));
#140360=CARTESIAN_POINT('Ctrl Pts',(209.406314383469,-3.13902814043842,
135.822204569766));
#140361=CARTESIAN_POINT('Ctrl Pts',(209.398961987017,-3.00467057976207,
135.901407337934));
#140362=CARTESIAN_POINT('Ctrl Pts',(209.391617367729,-2.87045513886034,
135.980526327567));
#140363=CARTESIAN_POINT('Ctrl Pts',(209.384272748441,-2.73295013636556,
136.054436040991));
#140364=CARTESIAN_POINT('Ctrl Pts',(209.376928129154,-2.59260326520279,
136.122850898817));
#140365=CARTESIAN_POINT('Ctrl Pts',(209.369589609032,-2.45237294179964,
136.191208943132));
#140366=CARTESIAN_POINT('Ctrl Pts',(209.362251088911,-2.309305786928,136.254081048402));
#140367=CARTESIAN_POINT('Ctrl Pts',(209.35491256879,-2.16387596942645,136.311226454995));
#140368=CARTESIAN_POINT('Ctrl Pts',(209.34757847529,-2.01853387570421,136.368337391276));
#140369=CARTESIAN_POINT('Ctrl Pts',(209.34024438179,-1.87083230938491,136.419728367192));
#140370=CARTESIAN_POINT('Ctrl Pts',(209.33291028829,-1.7212672027132,136.465205941311));
#140371=CARTESIAN_POINT('Ctrl Pts',(209.325578014926,-1.57173921429979,
136.510672229051));
#140372=CARTESIAN_POINT('Ctrl Pts',(209.318245741561,-1.42034896766245,
136.550227919959));
#140373=CARTESIAN_POINT('Ctrl Pts',(209.310913468197,-1.26760940802185,
136.58372883141));
#140374=CARTESIAN_POINT('Ctrl Pts',(209.303581889688,-1.11488432301136,
136.61722656809));
#140375=CARTESIAN_POINT('Ctrl Pts',(209.296250311179,-0.960810550721905,
136.644670584959));
#140376=CARTESIAN_POINT('Ctrl Pts',(209.288918732671,-0.805912813346689,
136.665967487681));
#140377=CARTESIAN_POINT('Ctrl Pts',(209.281586340522,-0.650997885813834,
136.68726675388));
#140378=CARTESIAN_POINT('Ctrl Pts',(209.274253948373,-0.495259187985151,
136.702417496254));
#140379=CARTESIAN_POINT('Ctrl Pts',(209.266921556224,-0.339227930045618,
136.711378052277));
#140380=CARTESIAN_POINT('Ctrl Pts',(209.259586841621,-0.183147250917642,
136.720341446458));
#140381=CARTESIAN_POINT('Ctrl Pts',(209.252252127018,-0.0267742067296978,
136.723110730372));
#140382=CARTESIAN_POINT('Ctrl Pts',(209.244917412414,0.129358863151292,
136.719696351658));
#140383=CARTESIAN_POINT('Ctrl Pts',(209.237574655162,0.285663135787447,
136.716278229015));
#140384=CARTESIAN_POINT('Ctrl Pts',(209.230231897911,0.441726528171486,
136.706662911789));
#140385=CARTESIAN_POINT('Ctrl Pts',(209.222889140659,0.597020032079499,
136.690912888955));
#140386=CARTESIAN_POINT('Ctrl Pts',(209.215541982281,0.752406616329664,
136.67515342582));
#140387=CARTESIAN_POINT('Ctrl Pts',(209.208194823903,0.907022017350668,
136.653251986223));
#140388=CARTESIAN_POINT('Ctrl Pts',(209.200847665525,1.06034700512894,136.625322289937));
#140389=CARTESIAN_POINT('Ctrl Pts',(209.193489593897,1.21389973726609,136.597351107714));
#140390=CARTESIAN_POINT('Ctrl Pts',(209.186131522269,1.36615785808255,136.563333868863));
#140391=CARTESIAN_POINT('Ctrl Pts',(209.178773450641,1.51661609478376,136.523434509687));
#140392=CARTESIAN_POINT('Ctrl Pts',(209.174068009948,1.61283319423839,136.497919119542));
#140393=CARTESIAN_POINT('Ctrl Pts',(209.169362569255,1.70831457266076,136.469999222647));
#140394=CARTESIAN_POINT('Ctrl Pts',(209.164657128562,1.80293258570797,136.439727921823));
#140395=CARTESIAN_POINT('Ctrl Pts',(209.157221130164,1.95245724009132,136.391890246442));
#140396=CARTESIAN_POINT('Ctrl Pts',(209.149785131767,2.10029751050973,136.338026748851));
#140397=CARTESIAN_POINT('Ctrl Pts',(209.14234913337,2.24593212653075,136.278273244336));
#140398=CARTESIAN_POINT('Ctrl Pts',(209.134921860703,2.39139584842722,136.218589857237));
#140399=CARTESIAN_POINT('Ctrl Pts',(209.127494588036,2.53465872740355,136.15303036157));
#140400=CARTESIAN_POINT('Ctrl Pts',(209.12006731537,2.67521401390798,136.081780493063));
#140401=CARTESIAN_POINT('Ctrl Pts',(209.112647154316,2.81563471872803,136.010598846304));
#140402=CARTESIAN_POINT('Ctrl Pts',(209.105226993263,2.95335266314768,135.93373784144));
#140403=CARTESIAN_POINT('Ctrl Pts',(209.09780683221,3.08788056468555,135.851431469133));
#140404=CARTESIAN_POINT('Ctrl Pts',(209.090392174166,3.22230869637828,135.769186137651));
#140405=CARTESIAN_POINT('Ctrl Pts',(209.082977516123,3.35355118035611,135.681503673601));
#140406=CARTESIAN_POINT('Ctrl Pts',(209.075562858079,3.48114495184259,135.588664160064));
#140407=CARTESIAN_POINT('Ctrl Pts',(209.06815209874,3.60867163319029,135.495873462514));
#140408=CARTESIAN_POINT('Ctrl Pts',(209.060741339401,3.73255312323486,135.397931334398));
#140409=CARTESIAN_POINT('Ctrl Pts',(209.053330580062,3.85235507996995,135.295161314583));
#140410=CARTESIAN_POINT('Ctrl Pts',(209.045921079812,3.97213668232604,135.192408755417));
#140411=CARTESIAN_POINT('Ctrl Pts',(209.038511579563,4.08783984546415,135.084830174857));
#140412=CARTESIAN_POINT('Ctrl Pts',(209.031102079314,4.19906299594078,134.972789640426));
#140413=CARTESIAN_POINT('Ctrl Pts',(209.023692927238,4.31028092002014,134.860754370801));
#140414=CARTESIAN_POINT('Ctrl Pts',(209.016283775163,4.41701898816564,134.744257828168));
#140415=CARTESIAN_POINT('Ctrl Pts',(209.008874623087,4.51891240724618,134.6237010342));
#140416=CARTESIAN_POINT('Ctrl Pts',(209.001464370453,4.62082096162604,134.503126332667));
#140417=CARTESIAN_POINT('Ctrl Pts',(208.994054117818,4.71788319396834,134.378490462857));
#140418=CARTESIAN_POINT('Ctrl Pts',(208.986643865183,4.80977462402228,134.250227508293));
#140419=CARTESIAN_POINT('Ctrl Pts',(208.979231062888,4.90169767134631,134.121920422035));
#140420=CARTESIAN_POINT('Ctrl Pts',(208.971818260593,4.98844615751906,133.989984068232));
#140421=CARTESIAN_POINT('Ctrl Pts',(208.964405458297,5.0697390257851,133.85488135556));
#140422=CARTESIAN_POINT('Ctrl Pts',(208.956984650393,5.15111968796501,133.71963273592));
#140423=CARTESIAN_POINT('Ctrl Pts',(208.949563842489,5.22703277370046,133.58121124698));
#140424=CARTESIAN_POINT('Ctrl Pts',(208.942143034584,5.29724293660821,133.440104883054));
#140425=CARTESIAN_POINT('Ctrl Pts',(208.93471772318,5.36749570828399,133.298912885253));
#140426=CARTESIAN_POINT('Ctrl Pts',(208.927292411775,5.43203850821355,133.155033103922));
#140427=CARTESIAN_POINT('Ctrl Pts',(208.919867100371,5.49068441292632,133.008972882829));
#140428=CARTESIAN_POINT('Ctrl Pts',(208.912431393417,5.54941242279996,132.862708175199));
#140429=CARTESIAN_POINT('Ctrl Pts',(208.904995686463,5.60222692426299,132.714257280312));
#140430=CARTESIAN_POINT('Ctrl Pts',(208.897559979509,5.64899080795368,132.564142824021));
#140431=CARTESIAN_POINT('Ctrl Pts',(208.893776487922,5.67278555425194,132.487760472487));
#140432=CARTESIAN_POINT('Ctrl Pts',(208.889992996336,5.69501458077322,132.410947592297));
#140433=CARTESIAN_POINT('Ctrl Pts',(208.886209504749,5.71566493562994,132.33377387307));
#140434=CARTESIAN_POINT('Ctrl Pts',(208.878777025297,5.75623152197345,132.182169972497));
#140435=CARTESIAN_POINT('Ctrl Pts',(208.871344545846,5.79082171676416,132.028728443607));
#140436=CARTESIAN_POINT('Ctrl Pts',(208.863912066394,5.81926846734694,131.873961041763));
#140437=CARTESIAN_POINT('Ctrl Pts',(208.856488197357,5.84768226280323,131.719372935591));
#140438=CARTESIAN_POINT('Ctrl Pts',(208.849064328319,5.86996671485046,131.56346237674));
#140439=CARTESIAN_POINT('Ctrl Pts',(208.841640459282,5.88600463401675,131.406755845662));
#140440=CARTESIAN_POINT('Ctrl Pts',(208.834223583446,5.90202744564246,131.250196930385));
#140441=CARTESIAN_POINT('Ctrl Pts',(208.82680670761,5.91181540164507,131.092843903578));
#140442=CARTESIAN_POINT('Ctrl Pts',(208.819389831774,5.91530244428613,130.935232903106));
#140443=CARTESIAN_POINT('Ctrl Pts',(208.811978337368,5.91878695684913,130.777736259749));
#140444=CARTESIAN_POINT('Ctrl Pts',(208.804566842962,5.91597965131232,130.619982386042));
#140445=CARTESIAN_POINT('Ctrl Pts',(208.797155348556,5.90686634525875,130.46251190578));
#140446=CARTESIAN_POINT('Ctrl Pts',(208.78974762803,5.89775767963602,130.30512160837));
#140447=CARTESIAN_POINT('Ctrl Pts',(208.782339907505,5.88234943013702,130.148014787699));
#140448=CARTESIAN_POINT('Ctrl Pts',(208.774932186979,5.86067950054184,129.991731332819));
#140449=CARTESIAN_POINT('Ctrl Pts',(208.767525527194,5.8390126739486,129.835470256778));
#140450=CARTESIAN_POINT('Ctrl Pts',(208.760118867408,5.81108599671315,129.680032681036));
#140451=CARTESIAN_POINT('Ctrl Pts',(208.752712207623,5.77698917900472,129.525952784297));
#140452=CARTESIAN_POINT('Ctrl Pts',(208.745305772146,5.74289339390685,129.371877553816));
#140453=CARTESIAN_POINT('Ctrl Pts',(208.737899336669,5.70262792010967,129.219160284054));
#140454=CARTESIAN_POINT('Ctrl Pts',(208.730492901192,5.65633342585285,129.068324115047));
#140455=CARTESIAN_POINT('Ctrl Pts',(208.723085238113,5.61003125837413,128.917462945239));
#140456=CARTESIAN_POINT('Ctrl Pts',(208.715677575033,5.55769818979722,128.768483852881));
#140457=CARTESIAN_POINT('Ctrl Pts',(208.708269911954,5.49952447183615,128.621893860391));
#140458=CARTESIAN_POINT('Ctrl Pts',(208.700859568914,5.44132970765705,128.475250834244));
#140459=CARTESIAN_POINT('Ctrl Pts',(208.693449225874,5.37729022396487,128.330998974698));
#140460=CARTESIAN_POINT('Ctrl Pts',(208.686038882833,5.30764396275474,128.189624277678));
#140461=CARTESIAN_POINT('Ctrl Pts',(208.678620321859,5.23792046511928,128.048092798713));
#140462=CARTESIAN_POINT('Ctrl Pts',(208.671201760884,5.16257793705867,127.909445188496));
#140463=CARTESIAN_POINT('Ctrl Pts',(208.66378319991,5.08190010003917,127.77414248421));
#140464=CARTESIAN_POINT('Ctrl Pts',(208.656360018143,5.0011720112898,127.638755504053));
#140465=CARTESIAN_POINT('Ctrl Pts',(208.648936836376,4.91510219414187,127.506717892626));
#140466=CARTESIAN_POINT('Ctrl Pts',(208.641513654609,4.82401676740594,127.378460328549));
#140467=CARTESIAN_POINT('Ctrl Pts',(208.634079874691,4.73280129709001,127.250019649858));
#140468=CARTESIAN_POINT('Ctrl Pts',(208.626646094773,4.63655614217903,127.125370091038));
#140469=CARTESIAN_POINT('Ctrl Pts',(208.619212314855,4.53564714939468,127.004908617779));
#140470=CARTESIAN_POINT('Ctrl Pts',(208.615395503548,4.4838362821366,126.943058695106));
#140471=CARTESIAN_POINT('Ctrl Pts',(208.611578692242,4.43079651974987,126.882312244135));
#140472=CARTESIAN_POINT('Ctrl Pts',(208.607761880936,4.37658094580437,126.822719023032));
#140473=CARTESIAN_POINT('Ctrl Pts',(208.600347300224,4.27126116010103,126.706952559281));
#140474=CARTESIAN_POINT('Ctrl Pts',(208.592932719512,4.16118202673538,126.59518870569));
#140475=CARTESIAN_POINT('Ctrl Pts',(208.585518138801,4.04668003584927,126.487844516593));
#140476=CARTESIAN_POINT('Ctrl Pts',(208.578112433415,3.93231510497043,126.380628819544));
#140477=CARTESIAN_POINT('Ctrl Pts',(208.570706728029,3.81353812445766,126.277822510432));
#140478=CARTESIAN_POINT('Ctrl Pts',(208.563301022643,3.69072512918956,126.179808900559));
#140479=CARTESIAN_POINT('Ctrl Pts',(208.555902556337,3.56803218366444,126.081891099022));
#140480=CARTESIAN_POINT('Ctrl Pts',(208.548504090031,3.44131136762011,125.988756902431));
#140481=CARTESIAN_POINT('Ctrl Pts',(208.541105623725,3.31097468788467,125.900752030139));
#140482=CARTESIAN_POINT('Ctrl Pts',(208.53371276603,3.18073681346501,125.812813872368));
#140483=CARTESIAN_POINT('Ctrl Pts',(208.526319908335,3.04688884180788,125.729997505443));
#140484=CARTESIAN_POINT('Ctrl Pts',(208.51892705064,2.90987480129162,125.652607595214));
#140485=CARTESIAN_POINT('Ctrl Pts',(208.511538175579,2.77293457211052,125.575259375987));
#140486=CARTESIAN_POINT('Ctrl Pts',(208.504149300517,2.63283199574196,125.503331975456));
#140487=CARTESIAN_POINT('Ctrl Pts',(208.496760425456,2.49003883636241,125.437085968742));
#140488=CARTESIAN_POINT('Ctrl Pts',(208.489372864132,2.34727106551612,125.370851740526));
#140489=CARTESIAN_POINT('Ctrl Pts',(208.481985302808,2.20181400050144,125.310297058228));
#140490=CARTESIAN_POINT('Ctrl Pts',(208.474597741484,2.05416277777801,125.255635913196));
#140491=CARTESIAN_POINT('Ctrl Pts',(208.467210559759,1.90651914189565,125.200977576845));
#140492=CARTESIAN_POINT('Ctrl Pts',(208.459823378033,1.75668192351523,125.152212305522));
#140493=CARTESIAN_POINT('Ctrl Pts',(208.452436196308,1.60516468869492,125.109505317853));
#140494=CARTESIAN_POINT('Ctrl Pts',(208.445047926206,1.45362513034552,125.066792038024));
#140495=CARTESIAN_POINT('Ctrl Pts',(208.437659656103,1.30040542302256,125.030138920576));
#140496=CARTESIAN_POINT('Ctrl Pts',(208.430271386,1.14603252496013,124.999660796366));
#140497=CARTESIAN_POINT('Ctrl Pts',(208.42288055916,0.991606205605298,124.969172125093));
#140498=CARTESIAN_POINT('Ctrl Pts',(208.41548973232,0.836026268007994,124.94486277379));
#140499=CARTESIAN_POINT('Ctrl Pts',(208.40809890548,0.679827884668699,124.926796104119));
#140500=CARTESIAN_POINT('Ctrl Pts',(208.400699950783,0.523457726470988,
124.908709566127));
#140501=CARTESIAN_POINT('Ctrl Pts',(208.393300996085,0.366468136359524,
124.896879462965));
#140502=CARTESIAN_POINT('Ctrl Pts',(208.385902041387,0.209398135492758,
124.891317155579));
#140503=CARTESIAN_POINT('Ctrl Pts',(208.378498546358,0.0522317494068543,
124.88575143491));
#140504=CARTESIAN_POINT('Ctrl Pts',(208.371095051329,-0.105014772330601,
124.886461171952));
#140505=CARTESIAN_POINT('Ctrl Pts',(208.3636915563,-0.261804959028031,124.893405641767));
#140506=CARTESIAN_POINT('Ctrl Pts',(208.356277419713,-0.418820511142279,
124.900360093349));
#140507=CARTESIAN_POINT('Ctrl Pts',(208.348863283127,-0.575378046221946,
124.91356714454));
#140508=CARTESIAN_POINT('Ctrl Pts',(208.341449146541,-0.730947916145645,
124.932934410384));
#140509=CARTESIAN_POINT('Ctrl Pts',(208.337404183401,-0.81582285500014,
124.943500694878));
#140510=CARTESIAN_POINT('Ctrl Pts',(208.333359220262,-0.900404006088913,
124.955899684651));
#140511=CARTESIAN_POINT('Ctrl Pts',(208.329314257123,-0.984607096318311,
124.970110072005));
#140512=CARTESIAN_POINT('Ctrl Pts',(208.321888582056,-1.13918570830919,
124.996197261288));
#140513=CARTESIAN_POINT('Ctrl Pts',(208.31446290699,-1.2929594256917,125.028471290496));
#140514=CARTESIAN_POINT('Ctrl Pts',(208.307037231924,-1.44539418231598,
125.066872820609));
#140515=CARTESIAN_POINT('Ctrl Pts',(208.299620316285,-1.59764912481468,
125.105229051752));
#140516=CARTESIAN_POINT('Ctrl Pts',(208.292203400647,-1.74856789230455,
125.149698305817));
#140517=CARTESIAN_POINT('Ctrl Pts',(208.284786485008,-1.89762360100986,
125.200169754347));
#140518=CARTESIAN_POINT('Ctrl Pts',(208.277376703944,-2.04653592813962,
125.250592652735));
#140519=CARTESIAN_POINT('Ctrl Pts',(208.26996692288,-2.19358841336712,125.307006132278));
#140520=CARTESIAN_POINT('Ctrl Pts',(208.262557141816,-2.3382665050408,125.369248814309));
#140521=CARTESIAN_POINT('Ctrl Pts',(208.255152876074,-2.48283690848986,
125.431445167253));
#140522=CARTESIAN_POINT('Ctrl Pts',(208.247748610331,-2.62503609623895,
125.49946193655));
#140523=CARTESIAN_POINT('Ctrl Pts',(208.240344344589,-2.76436687577973,
125.57308865574));
#140524=CARTESIAN_POINT('Ctrl Pts',(208.232943979269,-2.90362425857356,
125.646676589805));
#140525=CARTESIAN_POINT('Ctrl Pts',(208.22554361395,-3.04001591349676,125.725868414398));
#140526=CARTESIAN_POINT('Ctrl Pts',(208.218143248631,-3.17306685816016,
125.810406545276));
#140527=CARTESIAN_POINT('Ctrl Pts',(208.210744110281,-3.30609574317275,
125.894930659855));
#140528=CARTESIAN_POINT('Ctrl Pts',(208.203344971931,-3.43578470271374,
125.984799121566));
#140529=CARTESIAN_POINT('Ctrl Pts',(208.195945833582,-3.56168539721341,
126.079709551744));
#140530=CARTESIAN_POINT('Ctrl Pts',(208.188547021966,-3.68758053213906,
126.174615790828));
#140531=CARTESIAN_POINT('Ctrl Pts',(208.181148210351,-3.80968743678457,
126.274563331131));
#140532=CARTESIAN_POINT('Ctrl Pts',(208.173749398735,-3.92758891228548,
126.37920797629));
#140533=CARTESIAN_POINT('Ctrl Pts',(208.166349455627,-4.04550841834104,
126.48386862465));
#140534=CARTESIAN_POINT('Ctrl Pts',(208.158949512519,-4.15922093567722,
126.593227560529));
#140535=CARTESIAN_POINT('Ctrl Pts',(208.15154956941,-4.26834446912122,126.706902130232));
#140536=CARTESIAN_POINT('Ctrl Pts',(208.144147036186,-4.37750619780807,
126.820616488125));
#140537=CARTESIAN_POINT('Ctrl Pts',(208.136744502961,-4.48207548641057,
126.938649218448));
#140538=CARTESIAN_POINT('Ctrl Pts',(208.129341969737,-4.5817092353704,127.060582973926));
#140539=CARTESIAN_POINT('Ctrl Pts',(208.121931316487,-4.68145227509573,
127.182650481607));
#140540=CARTESIAN_POINT('Ctrl Pts',(208.114520663238,-4.77624872702756,
127.308627271148));
#140541=CARTESIAN_POINT('Ctrl Pts',(208.107110009989,-4.86579718354771,
127.438064681217));
#140542=CARTESIAN_POINT('Ctrl Pts',(208.099694803174,-4.95540066419993,
127.567581625668));
#140543=CARTESIAN_POINT('Ctrl Pts',(208.092279596359,-5.03974952437945,
127.700563113604));
#140544=CARTESIAN_POINT('Ctrl Pts',(208.084864389544,-5.1185875629994,127.836534490178));
#140545=CARTESIAN_POINT('Ctrl Pts',(208.077438621532,-5.1975378876451,127.972699525621));
#140546=CARTESIAN_POINT('Ctrl Pts',(208.070012853519,-5.27096154115178,
128.111862625628));
#140547=CARTESIAN_POINT('Ctrl Pts',(208.062587085507,-5.33864947802633,
128.25352696692));
#140548=CARTESIAN_POINT('Ctrl Pts',(208.058680268108,-5.37426120317554,
128.328058882332));
#140549=CARTESIAN_POINT('Ctrl Pts',(208.054773450709,-5.40828610965599,
128.403282833115));
#140550=CARTESIAN_POINT('Ctrl Pts',(208.05086663331,-5.44069928145357,128.479124738931));
#140551=CARTESIAN_POINT('Ctrl Pts',(208.042629123207,-5.50904233485686,
128.639037118127));
#140552=CARTESIAN_POINT('Ctrl Pts',(208.034391613105,-5.57039277901538,
128.802108281298));
#140553=CARTESIAN_POINT('Ctrl Pts',(208.026154103002,-5.62447863771873,
128.967741273133));
#140554=CARTESIAN_POINT('Ctrl Pts',(208.01794965263,-5.67834743278805,129.132709527456));
#140555=CARTESIAN_POINT('Ctrl Pts',(208.009745202257,-5.72500972152271,
129.300218882322));
#140556=CARTESIAN_POINT('Ctrl Pts',(208.001540751885,-5.76424268442704,
129.469655842146));
#140557=CARTESIAN_POINT('Ctrl Pts',(207.993357644752,-5.80337358582728,
129.638652024886));
#140558=CARTESIAN_POINT('Ctrl Pts',(207.98517453762,-5.83511364888881,129.80956558809));
#140559=CARTESIAN_POINT('Ctrl Pts',(207.976991430487,-5.85928927127411,
129.981767280593));
#140560=CARTESIAN_POINT('Ctrl Pts',(207.968843187868,-5.88336189228223,
130.153235299679));
#140561=CARTESIAN_POINT('Ctrl Pts',(207.960694945248,-5.8999343002241,130.325980274811));
#140562=CARTESIAN_POINT('Ctrl Pts',(207.952546702629,-5.90888377768745,
130.49936379089));
#140563=CARTESIAN_POINT('Ctrl Pts',(207.947822886293,-5.91407209740434,
130.599880175086));
#140564=CARTESIAN_POINT('Ctrl Pts',(207.943099069957,-5.91669932500736,
130.700610864797));
#140565=CARTESIAN_POINT('Ctrl Pts',(207.938375253621,-5.91674927385308,
130.801429259683));
#140566=CARTESIAN_POINT('',(206.188375157632,-5.91498635325863,130.809335103955));
#140567=CARTESIAN_POINT('Ctrl Pts',(207.938375192211,-5.90834445110727,
130.801434732496));
#140568=CARTESIAN_POINT('Ctrl Pts',(207.88305646464,-5.90301392988973,131.980404529528));
#140569=CARTESIAN_POINT('Ctrl Pts',(207.734921862463,-4.98909168451827,
135.145083942105));
#140570=CARTESIAN_POINT('Ctrl Pts',(207.493971385684,0.173518526030102,
137.800670327432));
#140571=CARTESIAN_POINT('Ctrl Pts',(207.21552376187,5.97986291472846,134.440038130778));
#140572=CARTESIAN_POINT('Ctrl Pts',(206.937076138059,6.29112482667552,127.7385118325));
#140573=CARTESIAN_POINT('Ctrl Pts',(206.658628514245,0.821087121814331,
123.854289400871));
#140574=CARTESIAN_POINT('Ctrl Pts',(206.409061532297,-4.75784521223805,
126.09730669271));
#140575=CARTESIAN_POINT('Ctrl Pts',(206.252310424952,-5.90151704252715,
129.448939722285));
#140576=CARTESIAN_POINT('Ctrl Pts',(206.188375192211,-5.91227720962736,
130.809332089608));
#140577=CARTESIAN_POINT('',(204.438375192211,-5.92105141345348,130.805327648265));
#140578=CARTESIAN_POINT('Ctrl Pts',(206.188375135149,-5.91674790721062,
130.80933706396));
#140579=CARTESIAN_POINT('Ctrl Pts',(206.179566065341,-5.91659014051484,
130.996913839284));
#140580=CARTESIAN_POINT('Ctrl Pts',(206.170756995534,-5.90750858188079,
131.184105581818));
#140581=CARTESIAN_POINT('Ctrl Pts',(206.161947925727,-5.88963571160845,
131.370153642484));
#140582=CARTESIAN_POINT('Ctrl Pts',(206.153074186251,-5.87163163195439,
131.557567530276));
#140583=CARTESIAN_POINT('Ctrl Pts',(206.144200446775,-5.84470678641371,
131.74382085212));
#140584=CARTESIAN_POINT('Ctrl Pts',(206.135326707299,-5.80904529038186,
131.928159254686));
#140585=CARTESIAN_POINT('Ctrl Pts',(206.126381804847,-5.77309780689119,
132.113975959543));
#140586=CARTESIAN_POINT('Ctrl Pts',(206.117436902394,-5.72827303913071,
132.297846882214));
#140587=CARTESIAN_POINT('Ctrl Pts',(206.108491999942,-5.67480770886274,
132.479021189124));
#140588=CARTESIAN_POINT('Ctrl Pts',(206.106239088835,-5.66134164402378,
132.524652721779));
#140589=CARTESIAN_POINT('Ctrl Pts',(206.103986177728,-5.64732768966758,
132.570113299786));
#140590=CARTESIAN_POINT('Ctrl Pts',(206.101733266621,-5.63277009911369,
132.615391145478));
#140591=CARTESIAN_POINT('Ctrl Pts',(206.094310026419,-5.58480349665586,
132.764579599188));
#140592=CARTESIAN_POINT('Ctrl Pts',(206.086886786216,-5.53083319938669,
132.91208669215));
#140593=CARTESIAN_POINT('Ctrl Pts',(206.079463546014,-5.47099418136574,
133.057392625763));
#140594=CARTESIAN_POINT('Ctrl Pts',(206.072049079851,-5.41122589119732,
133.202526812296));
#140595=CARTESIAN_POINT('Ctrl Pts',(206.064634613687,-5.34560282846522,
133.345464676374));
#140596=CARTESIAN_POINT('Ctrl Pts',(206.057220147523,-5.274309902267,133.485700882685));
#140597=CARTESIAN_POINT('Ctrl Pts',(206.049812828053,-5.20308569425869,
133.625801917405));
#140598=CARTESIAN_POINT('Ctrl Pts',(206.042405508582,-5.12620267075052,
133.763206148049));
#140599=CARTESIAN_POINT('Ctrl Pts',(206.034998189112,-5.04389400946855,
133.897427668851));
#140600=CARTESIAN_POINT('Ctrl Pts',(206.027596394619,-4.96164674063805,
134.031549076396));
#140601=CARTESIAN_POINT('Ctrl Pts',(206.020194600126,-4.87398208622341,
134.162492184038));
#140602=CARTESIAN_POINT('Ctrl Pts',(206.012792805633,-4.78117932515222,
134.289795285328));
#140603=CARTESIAN_POINT('Ctrl Pts',(206.005394918777,-4.68842555753051,
134.417031179371));
#140604=CARTESIAN_POINT('Ctrl Pts',(205.99799703192,-4.59053930480269,134.540630593273));
#140605=CARTESIAN_POINT('Ctrl Pts',(205.990599145064,-4.48784330175735,
134.660160542533));
#140606=CARTESIAN_POINT('Ctrl Pts',(205.983202487927,-4.38516436944237,
134.779670622824));
#140607=CARTESIAN_POINT('Ctrl Pts',(205.975805830791,-4.27767751662466,
134.895112298157));
#140608=CARTESIAN_POINT('Ctrl Pts',(205.968409173654,-4.16574599834706,
135.0060853634));
#140609=CARTESIAN_POINT('Ctrl Pts',(205.961012844691,-4.05381944622384,
135.117053505014));
#140610=CARTESIAN_POINT('Ctrl Pts',(205.953616515728,-3.93744888583708,
135.223553167924));
#140611=CARTESIAN_POINT('Ctrl Pts',(205.946220186765,-3.81703449993298,
135.325220954805));
#140612=CARTESIAN_POINT('Ctrl Pts',(205.938822725573,-3.69660168102824,
135.426904304962));
#140613=CARTESIAN_POINT('Ctrl Pts',(205.931425264382,-3.5721240892894,135.523754065483));
#140614=CARTESIAN_POINT('Ctrl Pts',(205.924027803191,-3.44403492469912,
135.61544718922));
#140615=CARTESIAN_POINT('Ctrl Pts',(205.916627748971,-3.31590086107405,
135.707172454105));
#140616=CARTESIAN_POINT('Ctrl Pts',(205.909227694752,-3.18415300742791,
135.793737266225));
#140617=CARTESIAN_POINT('Ctrl Pts',(205.901827640532,-3.04925332393586,
135.874862045331));
#140618=CARTESIAN_POINT('Ctrl Pts',(205.894419449247,-2.9142053053851,135.956076028864));
#140619=CARTESIAN_POINT('Ctrl Pts',(205.887011257962,-2.77599885578924,
136.031837840764));
#140620=CARTESIAN_POINT('Ctrl Pts',(205.879603066678,-2.63512094888712,
136.10191365149));
#140621=CARTESIAN_POINT('Ctrl Pts',(205.872190315849,-2.49415633539396,
136.172032592006));
#140622=CARTESIAN_POINT('Ctrl Pts',(205.864777565021,-2.35051732811826,
136.236458405575));
#140623=CARTESIAN_POINT('Ctrl Pts',(205.857364814192,-2.20471013894131,
136.295005731371));
#140624=CARTESIAN_POINT('Ctrl Pts',(205.849941471535,-2.05869461081846,
136.353636713455));
#140625=CARTESIAN_POINT('Ctrl Pts',(205.842518128878,-1.91050506407407,
136.406372307113));
#140626=CARTESIAN_POINT('Ctrl Pts',(205.835094786222,-1.76066288435223,
136.453077000087));
#140627=CARTESIAN_POINT('Ctrl Pts',(205.831158405083,-1.68120596618447,
136.477843130523));
#140628=CARTESIAN_POINT('Ctrl Pts',(205.827222023945,-1.60128453480154,
136.500914311524));
#140629=CARTESIAN_POINT('Ctrl Pts',(205.823285642806,-1.5209772722179,136.52227620805));
#140630=CARTESIAN_POINT('Ctrl Pts',(205.815862363887,-1.36953278846232,
136.562560751281));
#140631=CARTESIAN_POINT('Ctrl Pts',(205.808439084968,-1.21625774237482,
136.596885322964));
#140632=CARTESIAN_POINT('Ctrl Pts',(205.801015806049,-1.06166241873887,
136.625082520486));
#140633=CARTESIAN_POINT('Ctrl Pts',(205.793601300696,-0.907249811172222,
136.653246391767));
#140634=CARTESIAN_POINT('Ctrl Pts',(205.786186795344,-0.751520395763363,
136.675297237676));
#140635=CARTESIAN_POINT('Ctrl Pts',(205.778772289991,-0.594999279427515,
136.691117485314));
#140636=CARTESIAN_POINT('Ctrl Pts',(205.771364930901,-0.438629021562489,
136.706922485052));
#140637=CARTESIAN_POINT('Ctrl Pts',(205.76395757181,-0.281468950781068,
136.716508804378));
#140638=CARTESIAN_POINT('Ctrl Pts',(205.75655021272,-0.124053917183144,
136.719809982418));
#140639=CARTESIAN_POINT('Ctrl Pts',(205.749148378216,0.0332437125062621,
136.723108698361));
#140640=CARTESIAN_POINT('Ctrl Pts',(205.741746543712,0.190795554774945,
136.720131598888));
#140641=CARTESIAN_POINT('Ctrl Pts',(205.734344709207,0.348062200778197,
136.710864089747));
#140642=CARTESIAN_POINT('Ctrl Pts',(205.726946781988,0.505245828778614,
136.701601472745));
#140643=CARTESIAN_POINT('Ctrl Pts',(205.719548854768,0.662144188633564,
136.686055081083));
#140644=CARTESIAN_POINT('Ctrl Pts',(205.712150927548,0.818218547581937,
136.664262406068));
#140645=CARTESIAN_POINT('Ctrl Pts',(205.704754229649,0.97426697149117,136.642473352365));
#140646=CARTESIAN_POINT('Ctrl Pts',(205.697357531751,1.12949129690173,136.614440126908));
#140647=CARTESIAN_POINT('Ctrl Pts',(205.689960833853,1.28335846744775,136.580252029853));
#140648=CARTESIAN_POINT('Ctrl Pts',(205.682564463884,1.43721881635304,136.546065448514));
#140649=CARTESIAN_POINT('Ctrl Pts',(205.675168093915,1.5897217656208,136.505724619111));
#140650=CARTESIAN_POINT('Ctrl Pts',(205.667771723946,1.74034526633639,136.459369805573));
#140651=CARTESIAN_POINT('Ctrl Pts',(205.66037422154,1.89099182858503,136.413007894781));
#140652=CARTESIAN_POINT('Ctrl Pts',(205.652976719135,2.03975801251326,136.360630276258));
#140653=CARTESIAN_POINT('Ctrl Pts',(205.645579216729,2.18613787059475,136.30242680244));
#140654=CARTESIAN_POINT('Ctrl Pts',(205.63817912112,2.3325690423081,136.244202925325));
#140655=CARTESIAN_POINT('Ctrl Pts',(205.630779025511,2.47661187598612,136.180149264629));
#140656=CARTESIAN_POINT('Ctrl Pts',(205.623378929902,2.61778144864533,136.110503364386));
#140657=CARTESIAN_POINT('Ctrl Pts',(205.61597069717,2.75910625094721,136.040780881718));
#140658=CARTESIAN_POINT('Ctrl Pts',(205.608562464438,2.89755114766472,135.965454044387));
#140659=CARTESIAN_POINT('Ctrl Pts',(205.601154231705,3.03265618688166,135.884806170337));
#140660=CARTESIAN_POINT('Ctrl Pts',(205.593741439334,3.16784438091394,135.804108658914));
#140661=CARTESIAN_POINT('Ctrl Pts',(205.586328646963,3.29968830944655,135.718083788424));
#140662=CARTESIAN_POINT('Ctrl Pts',(205.578915854592,3.4277584000582,135.627057260869));
#140663=CARTESIAN_POINT('Ctrl Pts',(205.571492470601,3.55601148104427,135.535900671891));
#140664=CARTESIAN_POINT('Ctrl Pts',(205.56406908661,3.68047966012121,135.439728380284));
#140665=CARTESIAN_POINT('Ctrl Pts',(205.55664570262,3.80076710215312,135.338905798473));
#140666=CARTESIAN_POINT('Ctrl Pts',(205.552709808078,3.86454376885181,135.285449443535));
#140667=CARTESIAN_POINT('Ctrl Pts',(205.548773913536,3.92714579463605,135.230686447014));
#140668=CARTESIAN_POINT('Ctrl Pts',(205.544838018994,3.98851860995265,135.174675235595));
#140669=CARTESIAN_POINT('Ctrl Pts',(205.537414752403,4.10427038243128,135.069035678946));
#140670=CARTESIAN_POINT('Ctrl Pts',(205.529991485813,4.21599734533866,134.958634520244));
#140671=CARTESIAN_POINT('Ctrl Pts',(205.522568219222,4.32328283706097,134.843810589193));
#140672=CARTESIAN_POINT('Ctrl Pts',(205.515153726284,4.43044152670348,134.729122369998));
#140673=CARTESIAN_POINT('Ctrl Pts',(205.507739233346,4.53316894181514,134.610022053583));
#140674=CARTESIAN_POINT('Ctrl Pts',(205.500324740408,4.63108233208609,134.486887874212));
#140675=CARTESIAN_POINT('Ctrl Pts',(205.492917393806,4.7289013501625,134.363872375674));
#140676=CARTESIAN_POINT('Ctrl Pts',(205.485510047204,4.82191534978399,134.236831044588));
#140677=CARTESIAN_POINT('Ctrl Pts',(205.478102700602,4.90977931610782,134.106177939833));
#140678=CARTESIAN_POINT('Ctrl Pts',(205.470700878647,4.99757775054161,133.975622280541));
#140679=CARTESIAN_POINT('Ctrl Pts',(205.463299056693,5.08023359234056,133.841460519697));
#140680=CARTESIAN_POINT('Ctrl Pts',(205.455897234738,5.15744299933014,133.704138586853));
#140681=CARTESIAN_POINT('Ctrl Pts',(205.448499320116,5.23461164839757,133.566889144614));
#140682=CARTESIAN_POINT('Ctrl Pts',(205.441101405494,5.30633940608169,133.426483177278));
#140683=CARTESIAN_POINT('Ctrl Pts',(205.433703490873,5.37236661664779,133.283394199192));
#140684=CARTESIAN_POINT('Ctrl Pts',(205.426306805605,5.4383828550952,133.140328999019));
#140685=CARTESIAN_POINT('Ctrl Pts',(205.418910120337,5.49870027026613,132.994582011598));
#140686=CARTESIAN_POINT('Ctrl Pts',(205.411513435069,5.55310586287155,132.846649979591));
#140687=CARTESIAN_POINT('Ctrl Pts',(205.40411707775,5.60750904328352,132.698724506482));
#140688=CARTESIAN_POINT('Ctrl Pts',(205.396720720431,5.6560007934494,132.548614531768));
#140689=CARTESIAN_POINT('Ctrl Pts',(205.389324363111,5.6984169411165,132.396835084456));
#140690=CARTESIAN_POINT('Ctrl Pts',(205.381926873363,5.74083958296442,132.245032398749));
#140691=CARTESIAN_POINT('Ctrl Pts',(205.374529383615,5.77718466965693,132.091560091043));
#140692=CARTESIAN_POINT('Ctrl Pts',(205.367131893866,5.80733845234025,131.936946447634));
#140693=CARTESIAN_POINT('Ctrl Pts',(205.359731810911,5.83750280549823,131.782278604073));
#140694=CARTESIAN_POINT('Ctrl Pts',(205.352331727957,5.8614714620337,131.626468994384));
#140695=CARTESIAN_POINT('Ctrl Pts',(205.344931645002,5.87918216165979,131.470053994821));
#140696=CARTESIAN_POINT('Ctrl Pts',(205.337523424855,5.89691233611661,131.313467000041));
#140697=CARTESIAN_POINT('Ctrl Pts',(205.330115204709,5.90837076922905,131.156273657112));
#140698=CARTESIAN_POINT('Ctrl Pts',(205.322706984562,5.91354720906745,130.999014075358));
#140699=CARTESIAN_POINT('Ctrl Pts',(205.315294204756,5.91872683493454,130.84165770246));
#140700=CARTESIAN_POINT('Ctrl Pts',(205.30788142495,5.91761676570394,130.684235381923));
#140701=CARTESIAN_POINT('Ctrl Pts',(205.300468645144,5.91025882921648,130.527284573548));
#140702=CARTESIAN_POINT('Ctrl Pts',(205.293045273578,5.90289037933228,130.370109505815));
#140703=CARTESIAN_POINT('Ctrl Pts',(205.285621902013,5.88925626469626,130.213407666724));
#140704=CARTESIAN_POINT('Ctrl Pts',(205.278198530447,5.86944995847761,130.057709596387));
#140705=CARTESIAN_POINT('Ctrl Pts',(205.274262485358,5.85894819204549,129.975154840818));
#140706=CARTESIAN_POINT('Ctrl Pts',(205.270326440269,5.84671205599,129.892882092421));
#140707=CARTESIAN_POINT('Ctrl Pts',(205.266390395181,5.8327612125786,129.810968852179));
#140708=CARTESIAN_POINT('Ctrl Pts',(205.258967132391,5.80645034102074,129.656482941948));
#140709=CARTESIAN_POINT('Ctrl Pts',(205.251543869601,5.77395789796265,129.502809451314));
#140710=CARTESIAN_POINT('Ctrl Pts',(205.244120606812,5.73534373383937,129.350482074768));
#140711=CARTESIAN_POINT('Ctrl Pts',(205.236706117758,5.69677520874019,129.198334737669));
#140712=CARTESIAN_POINT('Ctrl Pts',(205.229291628704,5.65209945553443,129.047530706073));
#140713=CARTESIAN_POINT('Ctrl Pts',(205.22187713965,5.60142780672731,128.898596443141));
#140714=CARTESIAN_POINT('Ctrl Pts',(205.214469797011,5.55080499751139,128.749805729682));
#140715=CARTESIAN_POINT('Ctrl Pts',(205.207062454371,5.49419791719723,128.602881548161));
#140716=CARTESIAN_POINT('Ctrl Pts',(205.199655111732,5.43176843551374,128.458337977979));
#140717=CARTESIAN_POINT('Ctrl Pts',(205.192253293815,5.36938551648445,128.313902214751));
#140718=CARTESIAN_POINT('Ctrl Pts',(205.184851475898,5.30118899017215,128.171843868699));
#140719=CARTESIAN_POINT('Ctrl Pts',(205.17744965798,5.22738979486144,128.03265960644));
#140720=CARTESIAN_POINT('Ctrl Pts',(205.170051747467,5.15362955798969,127.893548819258));
#140721=CARTESIAN_POINT('Ctrl Pts',(205.162653836954,5.07427271682429,127.757309423218));
#140722=CARTESIAN_POINT('Ctrl Pts',(205.155255926441,4.98957730139766,127.624415819951));
#140723=CARTESIAN_POINT('Ctrl Pts',(205.147859245375,4.90489596136757,127.491544302061));
#140724=CARTESIAN_POINT('Ctrl Pts',(205.140462564308,4.81487800835612,127.362017787878));
#140725=CARTESIAN_POINT('Ctrl Pts',(205.133065883242,4.7198262340098,127.236283981162));
#140726=CARTESIAN_POINT('Ctrl Pts',(205.125669530182,4.62477867473806,127.110555750117));
#140727=CARTESIAN_POINT('Ctrl Pts',(205.118273177122,4.52469796309431,126.988620189907));
#140728=CARTESIAN_POINT('Ctrl Pts',(205.110876824062,4.41992866778351,126.870893808985));
#140729=CARTESIAN_POINT('Ctrl Pts',(205.103479338627,4.31514333238748,126.753149404261));
#140730=CARTESIAN_POINT('Ctrl Pts',(205.096081853192,4.20566823223877,126.639615740833));
#140731=CARTESIAN_POINT('Ctrl Pts',(205.088684367756,4.0918863448901,126.53067407045));
#140732=CARTESIAN_POINT('Ctrl Pts',(205.081284289166,3.97806457180816,126.42169421105));
#140733=CARTESIAN_POINT('Ctrl Pts',(205.073884210575,3.85993327514114,126.317309807603));
#140734=CARTESIAN_POINT('Ctrl Pts',(205.066484131984,3.73791006961344,126.217863165917));
#140735=CARTESIAN_POINT('Ctrl Pts',(205.059075916258,3.61575268720724,126.118307172572));
#140736=CARTESIAN_POINT('Ctrl Pts',(205.051667700531,3.48969513894966,126.02370002017));
#140737=CARTESIAN_POINT('Ctrl Pts',(205.044259484804,3.36018629211852,125.93434227625));
#140738=CARTESIAN_POINT('Ctrl Pts',(205.036846709456,3.23059773496496,125.844929534275));
#140739=CARTESIAN_POINT('Ctrl Pts',(205.029433934108,3.09755396123104,125.76077283788));
#140740=CARTESIAN_POINT('Ctrl Pts',(205.02202115876,2.9615297594948,125.682127506302));
#140741=CARTESIAN_POINT('Ctrl Pts',(205.014597791674,2.82531119969063,125.603369802408));
#140742=CARTESIAN_POINT('Ctrl Pts',(205.007174424588,2.68610403603951,125.530139364625));
#140743=CARTESIAN_POINT('Ctrl Pts',(204.999751057502,2.5444051509773,125.462644321264));
#140744=CARTESIAN_POINT('Ctrl Pts',(204.995814962124,2.46927208532876,125.42685639307));
#140745=CARTESIAN_POINT('Ctrl Pts',(204.991878866746,2.39343879236606,125.39268011218));
#140746=CARTESIAN_POINT('Ctrl Pts',(204.987942771368,2.31698110677334,125.360140828344));
#140747=CARTESIAN_POINT('Ctrl Pts',(204.980519502944,2.17278594159917,125.298773454077));
#140748=CARTESIAN_POINT('Ctrl Pts',(204.97309623452,2.02593299682858,125.243045954815));
#140749=CARTESIAN_POINT('Ctrl Pts',(204.965672966097,1.87690363642786,125.193196451186));
#140750=CARTESIAN_POINT('Ctrl Pts',(204.958258471337,1.7280504158966,125.143405865378));
#140751=CARTESIAN_POINT('Ctrl Pts',(204.950843976577,1.57702625054469,125.099479563857));
#140752=CARTESIAN_POINT('Ctrl Pts',(204.943429481818,1.42433424764934,125.061608445177));
#140753=CARTESIAN_POINT('Ctrl Pts',(204.936022133407,1.27178941463677,125.023773828004));
#140754=CARTESIAN_POINT('Ctrl Pts',(204.928614784996,1.11758030422428,124.991982864216));
#140755=CARTESIAN_POINT('Ctrl Pts',(204.921207436585,0.962226921405626,
124.966377240215));
#140756=CARTESIAN_POINT('Ctrl Pts',(204.913805612837,0.80698940662729,124.940790713794));
#140757=CARTESIAN_POINT('Ctrl Pts',(204.906403789088,0.650609685497499,
124.921380402016));
#140758=CARTESIAN_POINT('Ctrl Pts',(204.899001965339,0.493619635819424,
124.908237296465));
#140759=CARTESIAN_POINT('Ctrl Pts',(204.89160404894,0.336712459641496,124.89510112903));
#140760=CARTESIAN_POINT('Ctrl Pts',(204.884206132541,0.179195967619653,
124.888225610057));
#140761=CARTESIAN_POINT('Ctrl Pts',(204.876808216143,0.0216087595666902,
124.887650076733));
#140762=CARTESIAN_POINT('Ctrl Pts',(204.869411529128,-0.135952260670864,
124.88707463905));
#140763=CARTESIAN_POINT('Ctrl Pts',(204.862014842114,-0.293583600686453,
124.89279711053));
#140764=CARTESIAN_POINT('Ctrl Pts',(204.854618155099,-0.450744927651624,
124.90480473829));
#140765=CARTESIAN_POINT('Ctrl Pts',(204.847221796053,-0.607899286109743,
124.916811833635));
#140766=CARTESIAN_POINT('Ctrl Pts',(204.839825437006,-0.764583300742472,
124.935103502707));
#140767=CARTESIAN_POINT('Ctrl Pts',(204.83242907796,-0.920260302747,124.95961498258));
#140768=CARTESIAN_POINT('Ctrl Pts',(204.825031586505,-1.07596113944049,
124.984130215246));
#140769=CARTESIAN_POINT('Ctrl Pts',(204.81763409505,-1.23065428774014,125.014867096753));
#140770=CARTESIAN_POINT('Ctrl Pts',(204.810236603595,-1.38381198042967,
125.051709492622));
#140771=CARTESIAN_POINT('Ctrl Pts',(204.802836518957,-1.53702336240519,
125.088564803558));
#140772=CARTESIAN_POINT('Ctrl Pts',(204.795436434318,-1.68869785439576,
125.131529802889));
#140773=CARTESIAN_POINT('Ctrl Pts',(204.78803634968,-1.83832173330245,125.180438163676));
#140774=CARTESIAN_POINT('Ctrl Pts',(204.780628127893,-1.98811013894526,
125.229400304201));
#140775=CARTESIAN_POINT('Ctrl Pts',(204.773219906105,-2.13584307336326,
125.284318741618));
#140776=CARTESIAN_POINT('Ctrl Pts',(204.765811684318,-2.2810250362999,125.344978294787));
#140777=CARTESIAN_POINT('Ctrl Pts',(204.758398902893,-2.42629635631982,
125.405675182902));
#140778=CARTESIAN_POINT('Ctrl Pts',(204.750986121469,-2.56901323864276,
125.47212007064));
#140779=CARTESIAN_POINT('Ctrl Pts',(204.743573340044,-2.70870424060689,
125.544051510734));
#140780=CARTESIAN_POINT('Ctrl Pts',(204.736149966909,-2.84859483927297,
125.616085729662));
#140781=CARTESIAN_POINT('Ctrl Pts',(204.728726593773,-2.98545059862428,
125.693621974519));
#140782=CARTESIAN_POINT('Ctrl Pts',(204.721303220637,-3.11882783680492,
125.77635470201));
#140783=CARTESIAN_POINT('Ctrl Pts',(204.717367196277,-3.18954717814477,
125.820221287307));
#140784=CARTESIAN_POINT('Ctrl Pts',(204.713431171916,-3.25928911964002,
125.865548075032));
#140785=CARTESIAN_POINT('Ctrl Pts',(204.709495147555,-3.3279913467505,125.912284968268));
#140786=CARTESIAN_POINT('Ctrl Pts',(204.702104411593,-3.45699461857756,
126.000043580996));
#140787=CARTESIAN_POINT('Ctrl Pts',(204.694713675631,-3.58272775527118,
126.093046915379));
#140788=CARTESIAN_POINT('Ctrl Pts',(204.68732293967,-3.70473253445668,126.191022627494));
#140789=CARTESIAN_POINT('Ctrl Pts',(204.679940958213,-3.82659279604236,
126.288882285019));
#140790=CARTESIAN_POINT('Ctrl Pts',(204.672558976756,-3.94473319850045,
126.391702364622));
#140791=CARTESIAN_POINT('Ctrl Pts',(204.665176995299,-4.05872330506565,
126.499166580659));
#140792=CARTESIAN_POINT('Ctrl Pts',(204.657802110667,-4.17260382482097,
126.60652748369));
#140793=CARTESIAN_POINT('Ctrl Pts',(204.650427226035,-4.28234171832161,
126.71852337928));
#140794=CARTESIAN_POINT('Ctrl Pts',(204.643052341403,-4.38753867962024,
126.83479705247));
#140795=CARTESIAN_POINT('Ctrl Pts',(204.635682901836,-4.49265797131831,
126.950984877841));
#140796=CARTESIAN_POINT('Ctrl Pts',(204.628313462269,-4.59324275370197,
127.071443914587));
#140797=CARTESIAN_POINT('Ctrl Pts',(204.620944022703,-4.68893086223868,
127.195779465417));
#140798=CARTESIAN_POINT('Ctrl Pts',(204.613336988099,-4.78770401129907,
127.324123667047));
#140799=CARTESIAN_POINT('Ctrl Pts',(204.605729953495,-4.88125914129115,
127.45659826124));
#140800=CARTESIAN_POINT('Ctrl Pts',(204.598122918891,-4.96924186267879,
127.592730833064));
#140801=CARTESIAN_POINT('Ctrl Pts',(204.590758398115,-5.05441967681546,
127.724523470504));
#140802=CARTESIAN_POINT('Ctrl Pts',(204.583393877339,-5.13437472757324,
127.859744080796));
#140803=CARTESIAN_POINT('Ctrl Pts',(204.576029356562,-5.20882895299715,
127.997933796692));
#140804=CARTESIAN_POINT('Ctrl Pts',(204.568664962593,-5.283281896423,128.136121133155));
#140805=CARTESIAN_POINT('Ctrl Pts',(204.561300568623,-5.35223402382612,
128.277277141798));
#140806=CARTESIAN_POINT('Ctrl Pts',(204.553936174654,-5.41545310427121,
128.420918099287));
#140807=CARTESIAN_POINT('Ctrl Pts',(204.54657042013,-5.47868386429348,128.564585594107));
#140808=CARTESIAN_POINT('Ctrl Pts',(204.539204665606,-5.53617931718692,
128.710738606591));
#140809=CARTESIAN_POINT('Ctrl Pts',(204.531838911082,-5.58775535548524,
128.858873365039));
#140810=CARTESIAN_POINT('Ctrl Pts',(204.524470308052,-5.63935133941324,
129.007065410574));
#140811=CARTESIAN_POINT('Ctrl Pts',(204.517101705023,-5.68502322819046,
129.157240371933));
#140812=CARTESIAN_POINT('Ctrl Pts',(204.509733101994,-5.7246368129675,129.308879450143));
#140813=CARTESIAN_POINT('Ctrl Pts',(204.502356410778,-5.76429387980796,
129.460684975799));
#140814=CARTESIAN_POINT('Ctrl Pts',(204.494979719562,-5.79787927133109,
129.613957462062));
#140815=CARTESIAN_POINT('Ctrl Pts',(204.487603028346,-5.82530980176946,
129.768167452221));
#140816=CARTESIAN_POINT('Ctrl Pts',(204.480221494494,-5.85275833974991,
129.922478677858));
#140817=CARTESIAN_POINT('Ctrl Pts',(204.472839960642,-5.87404391676752,
130.077728261269));
#140818=CARTESIAN_POINT('Ctrl Pts',(204.465458426791,-5.88913528604936,
130.233382382334));
#140819=CARTESIAN_POINT('Ctrl Pts',(204.458067024258,-5.90424683161207,
130.389244603885));
#140820=CARTESIAN_POINT('Ctrl Pts',(204.450675621726,-5.91314761819259,
130.545512068223));
#140821=CARTESIAN_POINT('Ctrl Pts',(204.443284219194,-5.91585846087386,
130.701651156428));
#140822=CARTESIAN_POINT('Ctrl Pts',(204.441647876866,-5.91645859956244,
130.736217938293));
#140823=CARTESIAN_POINT('Ctrl Pts',(204.440011534539,-5.91675556357633,
130.770778450004));
#140824=CARTESIAN_POINT('Ctrl Pts',(204.438375192211,-5.91674992108927,
130.805326945742));
#140825=CARTESIAN_POINT('',(202.688375192211,-5.91520709160217,130.79891930971));
#140826=CARTESIAN_POINT('Ctrl Pts',(204.438375192211,-5.92634035306676,
130.805328512059));
#140827=CARTESIAN_POINT('Ctrl Pts',(204.435932636055,-5.9264572190019,130.856982408026));
#140828=CARTESIAN_POINT('Ctrl Pts',(204.433490079899,-5.92584057372106,
130.908633442257));
#140829=CARTESIAN_POINT('Ctrl Pts',(204.338231649138,-5.87285210044721,
132.922235594029));
#140830=CARTESIAN_POINT('Ctrl Pts',(204.152599899928,-3.62660601729001,
136.789783698913));
#140831=CARTESIAN_POINT('Ctrl Pts',(203.874152276118,3.07543675800755,137.09079434209));
#140832=CARTESIAN_POINT('Ctrl Pts',(203.595704652303,6.95130345427144,131.614879558226));
#140833=CARTESIAN_POINT('Ctrl Pts',(203.317257028491,4.43926183532277,125.394137434058));
#140834=CARTESIAN_POINT('Ctrl Pts',(203.038809404678,-2.1522445239837,124.145126127266));
#140835=CARTESIAN_POINT('Ctrl Pts',(202.829182125918,-5.62563427618384,
127.811846704057));
#140836=CARTESIAN_POINT('Ctrl Pts',(202.712370721762,-5.91979598762536,
130.288990713325));
#140837=CARTESIAN_POINT('Ctrl Pts',(202.688375192211,-5.91520709160217,
130.79891930971));
#140838=CARTESIAN_POINT('',(200.938375192211,-5.90723919874194,130.805767413591));
#140839=CARTESIAN_POINT('Ctrl Pts',(202.688375192211,-5.91520709160217,
130.79891930971));
#140840=CARTESIAN_POINT('Ctrl Pts',(202.619554847158,-5.90204591476485,
132.26141930917));
#140841=CARTESIAN_POINT('Ctrl Pts',(202.457918627501,-4.61506249001968,
135.717037067151));
#140842=CARTESIAN_POINT('Ctrl Pts',(202.203466533238,1.18549267223545,137.701618597998));
#140843=CARTESIAN_POINT('Ctrl Pts',(201.925018909427,6.44364622673833,133.535108470905));
#140844=CARTESIAN_POINT('Ctrl Pts',(201.646571285612,5.78040368780743,126.859174470383));
#140845=CARTESIAN_POINT('Ctrl Pts',(201.368123661802,-0.194747451439191,
123.808673806412));
#140846=CARTESIAN_POINT('Ctrl Pts',(201.132058297333,-5.10870273655874,
126.672675766875));
#140847=CARTESIAN_POINT('Ctrl Pts',(200.98880880747,-5.90496142391559,129.730359660658));
#140848=CARTESIAN_POINT('Ctrl Pts',(200.938375192211,-5.90723919874194,
130.805767413591));
#140849=CARTESIAN_POINT('',(199.188375192211,-5.92038509218979,130.80931765918));
#140850=CARTESIAN_POINT('Ctrl Pts',(200.938375192211,-5.90723919874194,
130.805767413591));
#140851=CARTESIAN_POINT('Ctrl Pts',(200.895992932866,-5.90915334356233,
131.70949422463));
#140852=CARTESIAN_POINT('Ctrl Pts',(200.760794798915,-5.28885804543136,
134.58986393661));
#140853=CARTESIAN_POINT('Ctrl Pts',(200.532780790362,-0.799939293036777,
137.756889485374));
#140854=CARTESIAN_POINT('Ctrl Pts',(200.254333166548,5.41697271486199,135.235383878266));
#140855=CARTESIAN_POINT('Ctrl Pts',(199.975885542736,6.65595143161651,128.641984362081));
#140856=CARTESIAN_POINT('Ctrl Pts',(199.697437918923,1.77843594402775,124.035702986741));
#140857=CARTESIAN_POINT('Ctrl Pts',(199.434934468748,-4.36050283967217,
125.557080494142));
#140858=CARTESIAN_POINT('Ctrl Pts',(199.265246893177,-5.90575828303711,
129.179380091958));
#140859=CARTESIAN_POINT('Ctrl Pts',(199.188375192211,-5.92038509218979,
130.80931765918));
#140860=CARTESIAN_POINT('',(197.438375192211,-5.92351700154912,130.800613675003));
#140861=CARTESIAN_POINT('Ctrl Pts',(199.188375192211,-5.92038509218979,
130.80931765918));
#140862=CARTESIAN_POINT('Ctrl Pts',(199.172431018573,-5.92341887942187,
131.147387550494));
#140863=CARTESIAN_POINT('Ctrl Pts',(199.06367097033,-5.7429796640639,133.450227209526));
#140864=CARTESIAN_POINT('Ctrl Pts',(198.862095047485,-2.72093855833704,
137.252155115847));
#140865=CARTESIAN_POINT('Ctrl Pts',(198.583647423671,3.9539783690358,136.578753710139));
#140866=CARTESIAN_POINT('Ctrl Pts',(198.305199799859,6.99538233784591,130.598967147137));
#140867=CARTESIAN_POINT('Ctrl Pts',(198.026752176046,3.60837168160217,124.807927149431));
#140868=CARTESIAN_POINT('Ctrl Pts',(197.748304552233,-3.09455627127803,
124.527316566881));
#140869=CARTESIAN_POINT('Ctrl Pts',(197.552178890954,-5.81278598755467,
128.392589611084));
#140870=CARTESIAN_POINT('Ctrl Pts',(197.448869104281,-5.92515660607875,
130.578413788211));
#140871=CARTESIAN_POINT('Ctrl Pts',(197.438375192211,-5.92351700154912,
130.800613675003));
#140872=CARTESIAN_POINT('',(195.688375192211,-5.90858988324653,130.801212225252));
#140873=CARTESIAN_POINT('Ctrl Pts',(197.438375192211,-5.92351700154912,
130.800613675003));
#140874=CARTESIAN_POINT('Ctrl Pts',(197.356053229677,-5.91065473800382,
132.543712972427));
#140875=CARTESIAN_POINT('Ctrl Pts',(197.180915392537,-4.17421686252449,
136.274385756281));
#140876=CARTESIAN_POINT('Ctrl Pts',(196.912961680794,2.17250297652081,137.457013573142));
#140877=CARTESIAN_POINT('Ctrl Pts',(196.634514056981,6.77135626959459,132.57249375751));
#140878=CARTESIAN_POINT('Ctrl Pts',(196.356066433169,5.14766395005485,126.063145964373));
#140879=CARTESIAN_POINT('Ctrl Pts',(196.077618809355,-1.20648006222068,
123.910742816309));
#140880=CARTESIAN_POINT('Ctrl Pts',(195.85505506237,-5.39917704206329,127.253819372125));
#140881=CARTESIAN_POINT('Ctrl Pts',(195.725307189988,-5.91237200604756,
130.014152192806));
#140882=CARTESIAN_POINT('Ctrl Pts',(195.688375192211,-5.90858988324653,
130.801212225252));
#140883=CARTESIAN_POINT('',(193.938375192211,-5.91196518873725,130.809243212275));
#140884=CARTESIAN_POINT('Ctrl Pts',(195.688375192211,-5.90858988324653,
130.801212225252));
#140885=CARTESIAN_POINT('Ctrl Pts',(195.632491315384,-5.90286694115081,
131.992156895353));
#140886=CARTESIAN_POINT('Ctrl Pts',(195.483791563953,-4.97462506172764,
135.169312250667));
#140887=CARTESIAN_POINT('Ctrl Pts',(195.242275937916,0.216039013678407,
137.799422280975));
#140888=CARTESIAN_POINT('Ctrl Pts',(194.963828314104,6.00191785180767,134.403602569768));
#140889=CARTESIAN_POINT('Ctrl Pts',(194.685380690291,6.27232739411319,127.70025533723));
#140890=CARTESIAN_POINT('Ctrl Pts',(194.406933066478,0.778774481457,123.849429213348));
#140891=CARTESIAN_POINT('Ctrl Pts',(194.157931233786,-4.77381132895269,
126.121196694781));
#140892=CARTESIAN_POINT('Ctrl Pts',(194.001745275696,-5.90152936629919,
129.46069533092));
#140893=CARTESIAN_POINT('Ctrl Pts',(193.938375192211,-5.91196518873725,
130.809243212275));
#140894=CARTESIAN_POINT('',(192.188375873533,-5.92197168067619,130.805533319426));
#140895=CARTESIAN_POINT('Ctrl Pts',(193.938375192211,-5.91196518873725,
130.809243212275));
#140896=CARTESIAN_POINT('Ctrl Pts',(193.908929401091,-5.91681433885312,
131.435864751108));
#140897=CARTESIAN_POINT('Ctrl Pts',(193.78666773537,-5.53611148477146,134.031915457605));
#140898=CARTESIAN_POINT('Ctrl Pts',(193.571590195038,-1.75782624092181,
137.578399843691));
#140899=CARTESIAN_POINT('Ctrl Pts',(193.293142571227,4.74904303118782,135.944803285106));
#140900=CARTESIAN_POINT('Ctrl Pts',(193.014694947413,6.89177376128537,129.587391039638));
#140901=CARTESIAN_POINT('Ctrl Pts',(192.736247323601,2.70130108662762,124.348314384016));
#140902=CARTESIAN_POINT('Ctrl Pts',(192.46080781812,-3.8994475031143,125.034534503354));
#140903=CARTESIAN_POINT('Ctrl Pts',(192.278184187244,-5.92103596021112,
128.906232297951));
#140904=CARTESIAN_POINT('Ctrl Pts',(192.188376430972,-5.92624401559878,
130.805522386918));
#140905=CARTESIAN_POINT('',(190.438375193894,-5.91568182138061,130.798900870218));
#140906=CARTESIAN_POINT('Ctrl Pts',(192.188375192211,-5.91674988112158,
130.805546681526));
#140907=CARTESIAN_POINT('Ctrl Pts',(192.185367486799,-5.91673715075054,
130.869052886841));
#140908=CARTESIAN_POINT('Ctrl Pts',(192.182359781387,-5.91570200665032,
130.932547687523));
#140909=CARTESIAN_POINT('Ctrl Pts',(192.179352075975,-5.91364535475517,
130.996009204001));
#140910=CARTESIAN_POINT('Ctrl Pts',(192.17192880957,-5.90856936730653,131.152637489943));
#140911=CARTESIAN_POINT('Ctrl Pts',(192.164505543164,-5.89725874201999,
131.309300813403));
#140912=CARTESIAN_POINT('Ctrl Pts',(192.157082276759,-5.87970025871574,
131.465462296703));
#140913=CARTESIAN_POINT('Ctrl Pts',(192.149667784038,-5.86216252808058,
131.621439210099));
#140914=CARTESIAN_POINT('Ctrl Pts',(192.142253291317,-5.83839167951754,
131.776915096634));
#140915=CARTESIAN_POINT('Ctrl Pts',(192.134838798596,-5.80842648002977,
131.931353247794));
#140916=CARTESIAN_POINT('Ctrl Pts',(192.127431452242,-5.77849016212943,
132.08564254565));
#140917=CARTESIAN_POINT('Ctrl Pts',(192.120024105888,-5.74237144971965,
132.238895735347));
#140918=CARTESIAN_POINT('Ctrl Pts',(192.112616759534,-5.70016086098663,
132.390581510562));
#140919=CARTESIAN_POINT('Ctrl Pts',(192.105214937859,-5.65798175450327,
132.542154152802));
#140920=CARTESIAN_POINT('Ctrl Pts',(192.097813116184,-5.60971991816693,
132.692161350184));
#140921=CARTESIAN_POINT('Ctrl Pts',(192.090411294508,-5.55551684961682,
132.84008238051));
#140922=CARTESIAN_POINT('Ctrl Pts',(192.083013380197,-5.5013423944446,132.987925324475));
#140923=CARTESIAN_POINT('Ctrl Pts',(192.075615465886,-5.44123308132258,
133.133683944999));
#140924=CARTESIAN_POINT('Ctrl Pts',(192.068217551574,-5.37538008816079,
133.2768531798));
#140925=CARTESIAN_POINT('Ctrl Pts',(192.060820866662,-5.30953803857184,
133.419998622472));
#140926=CARTESIAN_POINT('Ctrl Pts',(192.05342418175,-5.23795435917514,133.560555194648));
#140927=CARTESIAN_POINT('Ctrl Pts',(192.046027496837,-5.16086820194777,
133.69803820234));
#140928=CARTESIAN_POINT('Ctrl Pts',(192.038631139902,-5.08378546280139,
133.835515113891));
#140929=CARTESIAN_POINT('Ctrl Pts',(192.031234782967,-5.00120091351712,
133.969918406331));
#140930=CARTESIAN_POINT('Ctrl Pts',(192.023838426031,-4.91339933435241,
134.100788615215));
#140931=CARTESIAN_POINT('Ctrl Pts',(192.016440936695,-4.82558431254177,
134.231678860662));
#140932=CARTESIAN_POINT('Ctrl Pts',(192.009043447358,-4.73255087844258,
134.359034635486));
#140933=CARTESIAN_POINT('Ctrl Pts',(192.001645958021,-4.63462665546448,
134.482426186171));
#140934=CARTESIAN_POINT('Ctrl Pts',(191.994245875506,-4.53666810530159,
134.605860991573));
#140935=CARTESIAN_POINT('Ctrl Pts',(191.986845792991,-4.43381558469625,
134.725328513823));
#140936=CARTESIAN_POINT('Ctrl Pts',(191.979445710476,-4.32643632479157,
134.840432877824));
#140937=CARTESIAN_POINT('Ctrl Pts',(191.97203749081,-4.21893899035197,134.955663810906));
#140938=CARTESIAN_POINT('Ctrl Pts',(191.964629271143,-4.10690523078763,
135.066521731207));
#140939=CARTESIAN_POINT('Ctrl Pts',(191.957221051477,-3.99073891115741,
135.172647868363));
#140940=CARTESIAN_POINT('Ctrl Pts',(191.949808272175,-3.8745010930958,135.278839324385));
#140941=CARTESIAN_POINT('Ctrl Pts',(191.942395492873,-3.75412593146085,
135.380292954059));
#140942=CARTESIAN_POINT('Ctrl Pts',(191.934982713571,-3.63004912034786,
135.476691293616));
#140943=CARTESIAN_POINT('Ctrl Pts',(191.927559342542,-3.50579502246853,
135.573227371642));
#140944=CARTESIAN_POINT('Ctrl Pts',(191.920135971513,-3.37782901450236,
135.664693516634));
#140945=CARTESIAN_POINT('Ctrl Pts',(191.912712600484,-3.24661509159063,
135.750816016087));
#140946=CARTESIAN_POINT('Ctrl Pts',(191.908776551044,-3.17704232122627,
135.796480231779));
#140947=CARTESIAN_POINT('Ctrl Pts',(191.904840501603,-3.10655685573822,
135.84064292555));
#140948=CARTESIAN_POINT('Ctrl Pts',(191.900904452162,-3.03523037952588,
135.883268679906));
#140949=CARTESIAN_POINT('Ctrl Pts',(191.893481185756,-2.90071087141565,
135.963659522316));
#140950=CARTESIAN_POINT('Ctrl Pts',(191.886057919351,-2.76279191120802,
136.038823925974));
#140951=CARTESIAN_POINT('Ctrl Pts',(191.878634652946,-2.62191804346816,
136.108460572868));
#140952=CARTESIAN_POINT('Ctrl Pts',(191.871220160225,-2.48121067694097,
136.178014915029));
#140953=CARTESIAN_POINT('Ctrl Pts',(191.863805667504,-2.33755568601003,
136.242054341289));
#140954=CARTESIAN_POINT('Ctrl Pts',(191.856391174783,-2.19142557325891,
136.300321363365));
#140955=CARTESIAN_POINT('Ctrl Pts',(191.848983828429,-2.04543630621208,
136.358532225492));
#140956=CARTESIAN_POINT('Ctrl Pts',(191.841576482075,-1.89697701105787,
136.410981622255));
#140957=CARTESIAN_POINT('Ctrl Pts',(191.834169135721,-1.74654361814439,
136.457458525122));
#140958=CARTESIAN_POINT('Ctrl Pts',(191.826767314046,-1.59622242413098,
136.503900763762));
#140959=CARTESIAN_POINT('Ctrl Pts',(191.819365492371,-1.44393041914754,
136.544379268321));
#140960=CARTESIAN_POINT('Ctrl Pts',(191.811963670695,-1.29018218445807,
136.578731621702));
#140961=CARTESIAN_POINT('Ctrl Pts',(191.804565756384,-1.1365151122651,136.613065840743));
#140962=CARTESIAN_POINT('Ctrl Pts',(191.797167842073,-0.981393704726121,
136.641280267975));
#140963=CARTESIAN_POINT('Ctrl Pts',(191.789769927761,-0.825346221371544,
136.663262748287));
#140964=CARTESIAN_POINT('Ctrl Pts',(191.782373242849,-0.669324670277544,
136.68524157551));
#140965=CARTESIAN_POINT('Ctrl Pts',(191.774976557937,-0.512377718094195,
136.700990459225));
#140966=CARTESIAN_POINT('Ctrl Pts',(191.767579873025,-0.355042419086338,
136.710448615822));
#140967=CARTESIAN_POINT('Ctrl Pts',(191.760183516089,-0.19771409649043,
136.719906353036));
#140968=CARTESIAN_POINT('Ctrl Pts',(191.752787159154,-0.0399978339334864,
136.723073895353));
#140969=CARTESIAN_POINT('Ctrl Pts',(191.745390802218,0.117565877448984,
136.719942484716));
#140970=CARTESIAN_POINT('Ctrl Pts',(191.737993312882,0.275153712237935,
136.716810594653));
#140971=CARTESIAN_POINT('Ctrl Pts',(191.730595823545,0.432588576099383,
136.707377838831));
#140972=CARTESIAN_POINT('Ctrl Pts',(191.723198334209,0.589331816772684,
136.691687563833));
#140973=CARTESIAN_POINT('Ctrl Pts',(191.715798251694,0.746130003545964,
136.675991788633));
#140974=CARTESIAN_POINT('Ctrl Pts',(191.708398169179,0.902235713210191,
136.654034164045));
#140975=CARTESIAN_POINT('Ctrl Pts',(191.700998086664,1.0571173874321,136.625909671872));
#140976=CARTESIAN_POINT('Ctrl Pts',(191.693589866998,1.21216936997707,136.597754253928));
#140977=CARTESIAN_POINT('Ctrl Pts',(191.686181647331,1.36599426160672,136.563418492823));
#140978=CARTESIAN_POINT('Ctrl Pts',(191.678773427665,1.51807191972469,136.523048247525));
#140979=CARTESIAN_POINT('Ctrl Pts',(191.671360648363,1.67024317910383,136.482653155014));
#140980=CARTESIAN_POINT('Ctrl Pts',(191.663947869061,1.82066470625482,136.43621628731));
#140981=CARTESIAN_POINT('Ctrl Pts',(191.656535089759,1.96883390661907,136.383932609274));
#140982=CARTESIAN_POINT('Ctrl Pts',(191.64911171873,2.11721481808522,136.331574225866));
#140983=CARTESIAN_POINT('Ctrl Pts',(191.641688347701,2.26333662937201,136.273352484731));
#140984=CARTESIAN_POINT('Ctrl Pts',(191.634264976672,2.40671825768975,136.209509809827));
#140985=CARTESIAN_POINT('Ctrl Pts',(191.630328927231,2.48274263741927,136.175658891709));
#140986=CARTESIAN_POINT('Ctrl Pts',(191.626392877791,2.55799707823944,136.140228488059));
#140987=CARTESIAN_POINT('Ctrl Pts',(191.62245682835,2.63241303524121,136.103259764973));
#140988=CARTESIAN_POINT('Ctrl Pts',(191.615033561944,2.77275920770318,136.033537906988));
#140989=CARTESIAN_POINT('Ctrl Pts',(191.607610295539,2.91054571611699,135.958130975866));
#140990=CARTESIAN_POINT('Ctrl Pts',(191.600187029134,3.04527876591065,135.877250109798));
#140991=CARTESIAN_POINT('Ctrl Pts',(191.592772536413,3.17985257242841,135.796464838196));
#140992=CARTESIAN_POINT('Ctrl Pts',(191.585358043692,3.31137978699819,135.710218699948));
#140993=CARTESIAN_POINT('Ctrl Pts',(191.577943550971,3.43938837824726,135.618770046154));
#140994=CARTESIAN_POINT('Ctrl Pts',(191.570536204617,3.56727358999668,135.527409534016));
#140995=CARTESIAN_POINT('Ctrl Pts',(191.563128858263,3.69164662828833,135.430856704515));
#140996=CARTESIAN_POINT('Ctrl Pts',(191.555721511909,3.81206188637452,135.329414731823));
#140997=CARTESIAN_POINT('Ctrl Pts',(191.548319690234,3.93238733421826,135.228048418381));
#140998=CARTESIAN_POINT('Ctrl Pts',(191.540917868558,4.04876059514704,135.121800461911));
#140999=CARTESIAN_POINT('Ctrl Pts',(191.533516046883,4.16076687931502,135.011016003796));
#141000=CARTESIAN_POINT('Ctrl Pts',(191.526118132572,4.27271403623751,134.900290027933));
#141001=CARTESIAN_POINT('Ctrl Pts',(191.51872021826,4.38029854276746,134.785032581598));
#141002=CARTESIAN_POINT('Ctrl Pts',(191.511322303949,4.48314050245561,134.665627481918));
#141003=CARTESIAN_POINT('Ctrl Pts',(191.503925619037,4.58596537167568,134.546242225199));
#141004=CARTESIAN_POINT('Ctrl Pts',(191.496528934124,4.68404901487392,134.422710965694));
#141005=CARTESIAN_POINT('Ctrl Pts',(191.489132249212,4.77705000213056,134.295452687341));
#141006=CARTESIAN_POINT('Ctrl Pts',(191.481735892277,4.87004686562598,134.168200051753));
#141007=CARTESIAN_POINT('Ctrl Pts',(191.474339535341,4.95796130103329,134.037221027301));
#141008=CARTESIAN_POINT('Ctrl Pts',(191.466943178406,5.04049379128799,133.902965610541));
#141009=CARTESIAN_POINT('Ctrl Pts',(191.459545689069,5.12303891747765,133.768689638933));
#141010=CARTESIAN_POINT('Ctrl Pts',(191.452148199733,5.20020026233308,133.63113659425));
#141011=CARTESIAN_POINT('Ctrl Pts',(191.444750710396,5.27172313985551,133.490783089779));
#141012=CARTESIAN_POINT('Ctrl Pts',(191.437350627881,5.34327108961184,133.350380384605));
#141013=CARTESIAN_POINT('Ctrl Pts',(191.429950545366,5.40917646734144,133.207175597486));
#141014=CARTESIAN_POINT('Ctrl Pts',(191.422550462851,5.4692318636611,133.061667283488));
#141015=CARTESIAN_POINT('Ctrl Pts',(191.415142243184,5.52935329706284,132.915998968139));
#141016=CARTESIAN_POINT('Ctrl Pts',(191.407734023518,5.58361176011364,132.768022412689));
#141017=CARTESIAN_POINT('Ctrl Pts',(191.400325803851,5.63184881831531,132.618254068169));
#141018=CARTESIAN_POINT('Ctrl Pts',(191.392913024549,5.68011556562145,132.468393543732));
#141019=CARTESIAN_POINT('Ctrl Pts',(191.385500245247,5.72235342333643,132.316739391503));
#141020=CARTESIAN_POINT('Ctrl Pts',(191.378087465945,5.75845475628461,132.163819841788));
#141021=CARTESIAN_POINT('Ctrl Pts',(191.370664094916,5.79460767251027,132.01068179345));
#141022=CARTESIAN_POINT('Ctrl Pts',(191.363240723888,5.82460648099202,131.856275102001));
#141023=CARTESIAN_POINT('Ctrl Pts',(191.355817352859,5.84839510287327,131.701135552089));
#141024=CARTESIAN_POINT('Ctrl Pts',(191.351881303418,5.86100840099461,131.618876840204));
#141025=CARTESIAN_POINT('Ctrl Pts',(191.347945253977,5.87187666241779,131.536412149219));
#141026=CARTESIAN_POINT('Ctrl Pts',(191.344009204537,5.88099747114688,131.453821399187));
#141027=CARTESIAN_POINT('Ctrl Pts',(191.336585938131,5.89819903175955,131.298057822193));
#141028=CARTESIAN_POINT('Ctrl Pts',(191.329162671726,5.90923401839223,131.14137484216));
#141029=CARTESIAN_POINT('Ctrl Pts',(191.32173940532,5.91401315955457,130.984302027795));
#141030=CARTESIAN_POINT('Ctrl Pts',(191.314324912599,5.91878665216895,130.827414860453));
#141031=CARTESIAN_POINT('Ctrl Pts',(191.306910419878,5.91731900564953,130.67013914539));
#141032=CARTESIAN_POINT('Ctrl Pts',(191.299495927157,5.90957243360595,130.513011661047));
#141033=CARTESIAN_POINT('Ctrl Pts',(191.292088580803,5.90183332800017,130.35603562209));
#141034=CARTESIAN_POINT('Ctrl Pts',(191.28468123445,5.88782736319993,130.199207899769));
#141035=CARTESIAN_POINT('Ctrl Pts',(191.277273888096,5.86756874689005,130.043067268706));
#141036=CARTESIAN_POINT('Ctrl Pts',(191.269872066421,5.84732524022051,129.887043093216));
#141037=CARTESIAN_POINT('Ctrl Pts',(191.262470244745,5.82083841545084,129.731705357212));
#141038=CARTESIAN_POINT('Ctrl Pts',(191.25506842307,5.78817444575804,129.577589592487));
#141039=CARTESIAN_POINT('Ctrl Pts',(191.247670508758,5.7555277191206,129.423555184274));
#141040=CARTESIAN_POINT('Ctrl Pts',(191.240272594447,5.71671041893551,129.270741826916));
#141041=CARTESIAN_POINT('Ctrl Pts',(191.232874680136,5.67184011811256,129.119676600586));
#141042=CARTESIAN_POINT('Ctrl Pts',(191.225477995223,5.6269772739196,128.968636478556));
#141043=CARTESIAN_POINT('Ctrl Pts',(191.218081310311,5.57606353168593,128.819344268479));
#141044=CARTESIAN_POINT('Ctrl Pts',(191.210684625399,5.51926684325338,128.672313696069));
#141045=CARTESIAN_POINT('Ctrl Pts',(191.203288268464,5.46247267324549,128.525289643149));
#141046=CARTESIAN_POINT('Ctrl Pts',(191.195891911528,5.39979621022294,128.380527376718));
#141047=CARTESIAN_POINT('Ctrl Pts',(191.188495554593,5.33145415274227,128.238522123095));
#141048=CARTESIAN_POINT('Ctrl Pts',(191.181098065256,5.26310163191814,128.096495128106));
#141049=CARTESIAN_POINT('Ctrl Pts',(191.17370057592,5.18908195138688,127.957226322785));
#141050=CARTESIAN_POINT('Ctrl Pts',(191.166303086583,5.10965843540239,127.821187602801));
#141051=CARTESIAN_POINT('Ctrl Pts',(191.158903004068,5.03020707762741,127.685101194655));
#141052=CARTESIAN_POINT('Ctrl Pts',(191.151502921553,4.94534830094565,127.552247448424));
#141053=CARTESIAN_POINT('Ctrl Pts',(191.144102839038,4.8553894440146,127.423070344689));
#141054=CARTESIAN_POINT('Ctrl Pts',(191.136694619372,4.7653316680724,127.293751197449));
#141055=CARTESIAN_POINT('Ctrl Pts',(191.129286399705,4.67016282567414,127.168117073055));
#141056=CARTESIAN_POINT('Ctrl Pts',(191.121878180039,4.5702317839837,127.046580421338));
#141057=CARTESIAN_POINT('Ctrl Pts',(191.114465400737,4.47023923640445,126.924968965839));
#141058=CARTESIAN_POINT('Ctrl Pts',(191.107052621435,4.3654788968777,126.807460286267));
#141059=CARTESIAN_POINT('Ctrl Pts',(191.099639842133,4.25633700107888,126.694430460526));
#141060=CARTESIAN_POINT('Ctrl Pts',(191.092216471104,4.14703915822113,126.58123913247));
#141061=CARTESIAN_POINT('Ctrl Pts',(191.084793100075,4.03334752442669,126.472539696962));
#141062=CARTESIAN_POINT('Ctrl Pts',(191.077369729046,3.91568255850171,126.368668939423));
#141063=CARTESIAN_POINT('Ctrl Pts',(191.073433679605,3.85329377023497,126.31359417143));
#141064=CARTESIAN_POINT('Ctrl Pts',(191.069497630165,3.78978845095696,126.259876215498));
#141065=CARTESIAN_POINT('Ctrl Pts',(191.065561580724,3.72523253376711,126.207560303014));
#141066=CARTESIAN_POINT('Ctrl Pts',(191.058138314318,3.60348208867042,126.108894124795));
#141067=CARTESIAN_POINT('Ctrl Pts',(191.050715047913,3.47762493989561,126.014919100111));
#141068=CARTESIAN_POINT('Ctrl Pts',(191.043291781507,3.34805837517246,125.925996580418));
#141069=CARTESIAN_POINT('Ctrl Pts',(191.035877288786,3.2186449473689,125.837179159759));
#141070=CARTESIAN_POINT('Ctrl Pts',(191.028462796065,3.08553113521307,125.753402566677));
#141071=CARTESIAN_POINT('Ctrl Pts',(191.021048303344,2.94914812114376,125.674988733792));
#141072=CARTESIAN_POINT('Ctrl Pts',(191.013640956991,2.81289655815807,125.596650479111));
#141073=CARTESIAN_POINT('Ctrl Pts',(191.006233610637,2.67338238768785,125.523664879322));
#141074=CARTESIAN_POINT('Ctrl Pts',(190.998826264283,2.53106657568212,125.456311201941));
#141075=CARTESIAN_POINT('Ctrl Pts',(190.991424442608,2.38885690817838,125.389007759474));
#141076=CARTESIAN_POINT('Ctrl Pts',(190.984022620932,2.24385009572029,125.327328034653));
#141077=CARTESIAN_POINT('Ctrl Pts',(190.976620799257,2.09653246459078,125.271505822127));
#141078=CARTESIAN_POINT('Ctrl Pts',(190.969222884945,1.94929260129213,125.215713077712));
#141079=CARTESIAN_POINT('Ctrl Pts',(190.961824970634,1.79974469693171,125.165771819394));
#141080=CARTESIAN_POINT('Ctrl Pts',(190.954427056323,1.64839575001803,125.121868029465));
#141081=CARTESIAN_POINT('Ctrl Pts',(190.94703037141,1.49707195455342,125.077971535549));
#141082=CARTESIAN_POINT('Ctrl Pts',(190.939633686498,1.34394806872582,125.040110622631));
#141083=CARTESIAN_POINT('Ctrl Pts',(190.932237001586,1.18954708660089,125.008421669366));
#141084=CARTESIAN_POINT('Ctrl Pts',(190.924840644651,1.03515295077734,124.976734121223));
#141085=CARTESIAN_POINT('Ctrl Pts',(190.917444287715,0.879482196927022,
124.951218063633));
#141086=CARTESIAN_POINT('Ctrl Pts',(190.91004793078,0.723068603840397,124.931958863885));
#141087=CARTESIAN_POINT('Ctrl Pts',(190.902650441443,0.566631063433394,
124.912696715504));
#141088=CARTESIAN_POINT('Ctrl Pts',(190.895252952107,0.409450827861063,
124.899693377976));
#141089=CARTESIAN_POINT('Ctrl Pts',(190.88785546277,0.252067249504715,124.892982380283));
#141090=CARTESIAN_POINT('Ctrl Pts',(190.880455380255,0.0946285005788653,
124.88626903006));
#141091=CARTESIAN_POINT('Ctrl Pts',(190.87305529774,-0.0630133603256108,
124.885852427237));
#141092=CARTESIAN_POINT('Ctrl Pts',(190.865655215225,-0.220318675722416,
124.891713981445));
#141093=CARTESIAN_POINT('Ctrl Pts',(190.858246995558,-0.377796964484852,
124.897581981035));
#141094=CARTESIAN_POINT('Ctrl Pts',(190.850838775892,-0.534937595424837,
124.909741910448));
#141095=CARTESIAN_POINT('Ctrl Pts',(190.843430556225,-0.691204991596928,
124.928123197065));
#141096=CARTESIAN_POINT('Ctrl Pts',(190.836017776923,-0.84756856774404,
124.946515797058));
#141097=CARTESIAN_POINT('Ctrl Pts',(190.828604997621,-1.00305747031484,
124.971137326051));
#141098=CARTESIAN_POINT('Ctrl Pts',(190.821192218319,-1.15714652449987,
125.001866112326));
#141099=CARTESIAN_POINT('Ctrl Pts',(190.81376884729,-1.31145574835155,125.032638805332));
#141100=CARTESIAN_POINT('Ctrl Pts',(190.806345476262,-1.46436076711051,
125.069536096735));
#141101=CARTESIAN_POINT('Ctrl Pts',(190.798922105233,-1.61535096541017,
125.112386283379));
#141102=CARTESIAN_POINT('Ctrl Pts',(190.794986055792,-1.69540959150786,
125.135106480513));
#141103=CARTESIAN_POINT('Ctrl Pts',(190.791050006351,-1.77493020547604,
125.15949943687));
#141104=CARTESIAN_POINT('Ctrl Pts',(190.787113956911,-1.85383911441731,
125.185534129735));
#141105=CARTESIAN_POINT('Ctrl Pts',(190.779690690505,-2.0026588540193,125.234634747963));
#141106=CARTESIAN_POINT('Ctrl Pts',(190.7722674241,-2.14975156694095,125.289726135378));
#141107=CARTESIAN_POINT('Ctrl Pts',(190.764844157694,-2.29459849424747,
125.350669361848));
#141108=CARTESIAN_POINT('Ctrl Pts',(190.757429664973,-2.4392742245148,125.411540558485));
#141109=CARTESIAN_POINT('Ctrl Pts',(190.750015172252,-2.58170911190695,
125.478249683713));
#141110=CARTESIAN_POINT('Ctrl Pts',(190.742600679531,-2.72139924075281,
125.550607983978));
#141111=CARTESIAN_POINT('Ctrl Pts',(190.735193333178,-2.86095473099336,
125.62289654259));
#141112=CARTESIAN_POINT('Ctrl Pts',(190.727785986824,-2.99777040011747,
125.700823265995));
#141113=CARTESIAN_POINT('Ctrl Pts',(190.72037864047,-3.13136212909958,125.784151281399));
#141114=CARTESIAN_POINT('Ctrl Pts',(190.712976818795,-3.26485422033005,
125.867417147625));
#141115=CARTESIAN_POINT('Ctrl Pts',(190.705574997119,-3.39512684380415,
125.956076087876));
#141116=CARTESIAN_POINT('Ctrl Pts',(190.698173175444,-3.5217204302287,126.049845313793));
#141117=CARTESIAN_POINT('Ctrl Pts',(190.690775261132,-3.6482471888842,126.143565039666));
#141118=CARTESIAN_POINT('Ctrl Pts',(190.683377346821,-3.77109847913389,
126.242389457018));
#141119=CARTESIAN_POINT('Ctrl Pts',(190.67597943251,-3.88984378373164,126.345992541614));
#141120=CARTESIAN_POINT('Ctrl Pts',(190.668582747597,-4.0085693550141,126.449578409258));
#141121=CARTESIAN_POINT('Ctrl Pts',(190.661186062685,-4.12319001387754,
126.557941122862));
#141122=CARTESIAN_POINT('Ctrl Pts',(190.653789377773,-4.23330833002912,
126.670714388701));
#141123=CARTESIAN_POINT('Ctrl Pts',(190.646393020838,-4.34342176341914,
126.783482654056));
#141124=CARTESIAN_POINT('Ctrl Pts',(190.638996663902,-4.44903299024769,
126.900660815703));
#141125=CARTESIAN_POINT('Ctrl Pts',(190.631600306967,-4.54978166812228,
127.021845933534));
#141126=CARTESIAN_POINT('Ctrl Pts',(190.62420281763,-4.65054577087687,127.143049605116));
#141127=CARTESIAN_POINT('Ctrl Pts',(190.616805328294,-4.7464456036807,127.268261167321));
#141128=CARTESIAN_POINT('Ctrl Pts',(190.609407838957,-4.83716142451464,
127.397044970948));
#141129=CARTESIAN_POINT('Ctrl Pts',(190.602007756442,-4.92790904563891,
127.525873919538));
#141130=CARTESIAN_POINT('Ctrl Pts',(190.594607673927,-5.01346882182785,
127.658277297765));
#141131=CARTESIAN_POINT('Ctrl Pts',(190.587207591412,-5.09356469563254,
127.793791027952));
#141132=CARTESIAN_POINT('Ctrl Pts',(190.579799371746,-5.17374864308446,
127.929453769417));
#141133=CARTESIAN_POINT('Ctrl Pts',(190.572391152079,-5.24845649947873,
128.068233371551));
#141134=CARTESIAN_POINT('Ctrl Pts',(190.564982932413,-5.31745814713684,
128.209641092078));
#141135=CARTESIAN_POINT('Ctrl Pts',(190.557570153111,-5.38650226415769,
128.351135846697));
#141136=CARTESIAN_POINT('Ctrl Pts',(190.550157373809,-5.44983302436487,
128.495261601939));
#141137=CARTESIAN_POINT('Ctrl Pts',(190.542744594507,-5.50726892380859,
128.641510746828));
#141138=CARTESIAN_POINT('Ctrl Pts',(190.535321223478,-5.56478689035895,
128.787968859353));
#141139=CARTESIAN_POINT('Ctrl Pts',(190.527897852449,-5.61639305166817,
128.9365560694));
#141140=CARTESIAN_POINT('Ctrl Pts',(190.52047448142,-5.66195586638615,129.086749972048));
#141141=CARTESIAN_POINT('Ctrl Pts',(190.516538431979,-5.68611436401442,
129.166386383086));
#141142=CARTESIAN_POINT('Ctrl Pts',(190.512602382539,-5.70857471323609,
129.246474316501));
#141143=CARTESIAN_POINT('Ctrl Pts',(190.508666333098,-5.72932318152839,
129.326935003837));
#141144=CARTESIAN_POINT('Ctrl Pts',(190.498971765574,-5.78042706879116,
129.525111266141));
#141145=CARTESIAN_POINT('Ctrl Pts',(190.48927719805,-5.82126881850071,129.726034303134));
#141146=CARTESIAN_POINT('Ctrl Pts',(190.479582630525,-5.85160626396125,
129.928783839625));
#141147=CARTESIAN_POINT('Ctrl Pts',(190.470087632604,-5.88131919141924,
130.127359631965));
#141148=CARTESIAN_POINT('Ctrl Pts',(190.460592634683,-5.90095589270113,
130.327687736164));
#141149=CARTESIAN_POINT('Ctrl Pts',(190.451097636761,-5.91033348368092,
130.528881627115));
#141150=CARTESIAN_POINT('Ctrl Pts',(190.446856827631,-5.91452185462971,
130.618742088053));
#141151=CARTESIAN_POINT('Ctrl Pts',(190.4426160185,-5.9166642962425,130.708774942494));
#141152=CARTESIAN_POINT('Ctrl Pts',(190.438375209369,-5.91674747976679,
130.798899557834));
#141153=CARTESIAN_POINT('',(188.688375158851,-5.91280930184219,130.805575254198));
#141154=CARTESIAN_POINT('Ctrl Pts',(190.438375192211,-5.91556591356672,
130.798901012961));
#141155=CARTESIAN_POINT('Ctrl Pts',(190.368989697902,-5.90218450277572,
132.273183331429));
#141156=CARTESIAN_POINT('Ctrl Pts',(190.206788328991,-4.59798200865986,
135.740709904657));
#141157=CARTESIAN_POINT('Ctrl Pts',(189.951771085471,1.22745627517318,137.694274377758));
#141158=CARTESIAN_POINT('Ctrl Pts',(189.673323461659,6.46014967796433,133.495833572777));
#141159=CARTESIAN_POINT('Ctrl Pts',(189.394875837845,5.75628112256356,126.824060607722));
#141160=CARTESIAN_POINT('Ctrl Pts',(189.116428214034,-0.237328574507486,
123.809988903246));
#141161=CARTESIAN_POINT('Ctrl Pts',(188.880927998822,-5.12203658652489,
126.696922428952));
#141162=CARTESIAN_POINT('Ctrl Pts',(188.738243658214,-5.90521979014647,
129.742180863919));
#141163=CARTESIAN_POINT('Ctrl Pts',(188.688375192211,-5.90715995150835,
130.805573381844));
#141164=CARTESIAN_POINT('',(186.938375192211,-5.91753456722523,130.809401790279));
#141165=CARTESIAN_POINT('Ctrl Pts',(188.688375135582,-5.9167498750567,130.805576560215));
#141166=CARTESIAN_POINT('Ctrl Pts',(188.680495520896,-5.916715288546,130.97387375165));
#141167=CARTESIAN_POINT('Ctrl Pts',(188.67261590621,-5.90949584186738,131.141986835927));
#141168=CARTESIAN_POINT('Ctrl Pts',(188.664736291524,-5.89516395080611,
131.309308689764));
#141169=CARTESIAN_POINT('Ctrl Pts',(188.656841930411,-5.88080523810475,
131.476943680682));
#141170=CARTESIAN_POINT('Ctrl Pts',(188.648947569298,-5.85930751799326,
131.643784192002));
#141171=CARTESIAN_POINT('Ctrl Pts',(188.641053208185,-5.83079446595158,
131.809231981636));
#141172=CARTESIAN_POINT('Ctrl Pts',(188.633135901846,-5.80219853976692,
131.975160650825));
#141173=CARTESIAN_POINT('Ctrl Pts',(188.625218595508,-5.76654654061531,
132.139688210389));
#141174=CARTESIAN_POINT('Ctrl Pts',(188.617301289169,-5.72401296888253,
132.30222779945));
#141175=CARTESIAN_POINT('Ctrl Pts',(188.609371641021,-5.68141309414261,
132.465020761625));
#141176=CARTESIAN_POINT('Ctrl Pts',(188.601441992874,-5.63191030844115,
132.625819284766));
#141177=CARTESIAN_POINT('Ctrl Pts',(188.593512344726,-5.5757279961427,132.784054501865));
#141178=CARTESIAN_POINT('Ctrl Pts',(188.585563505692,-5.51940971458834,
132.94267267089));
#141179=CARTESIAN_POINT('Ctrl Pts',(188.577614666658,-5.45637968482179,
133.098714854591));
#141180=CARTESIAN_POINT('Ctrl Pts',(188.569665827625,-5.38690907388433,
133.251632811704));
#141181=CARTESIAN_POINT('Ctrl Pts',(188.566288207219,-5.35738962430293,
133.316610704718));
#141182=CARTESIAN_POINT('Ctrl Pts',(188.562910586813,-5.32670783786975,
133.381024824207));
#141183=CARTESIAN_POINT('Ctrl Pts',(188.559532966408,-5.29488692684622,
133.444834626984));
#141184=CARTESIAN_POINT('Ctrl Pts',(188.552109700002,-5.22495156661437,
133.585074532128));
#141185=CARTESIAN_POINT('Ctrl Pts',(188.544686433597,-5.14933503520301,
133.722746124474));
#141186=CARTESIAN_POINT('Ctrl Pts',(188.537263167192,-5.06824922202705,
133.857355931339));
#141187=CARTESIAN_POINT('Ctrl Pts',(188.529848674471,-4.98725924554844,
133.991806640591));
#141188=CARTESIAN_POINT('Ctrl Pts',(188.52243418175,-4.90081304514209,134.123202450914));
#141189=CARTESIAN_POINT('Ctrl Pts',(188.515019689029,-4.80916968995939,
134.251071724647));
#141190=CARTESIAN_POINT('Ctrl Pts',(188.507612342675,-4.71761466409284,
134.37881775316));
#141191=CARTESIAN_POINT('Ctrl Pts',(188.500204996321,-4.62087267180682,
134.503043710459));
#141192=CARTESIAN_POINT('Ctrl Pts',(188.492797649967,-4.51924756505893,
134.623304451692));
#141193=CARTESIAN_POINT('Ctrl Pts',(188.485395828292,-4.41769825414966,
134.743475497927));
#141194=CARTESIAN_POINT('Ctrl Pts',(188.477994006617,-4.31127332042061,
134.859686932794));
#141195=CARTESIAN_POINT('Ctrl Pts',(188.470592184941,-4.2003185360947,134.971524492174));
#141196=CARTESIAN_POINT('Ctrl Pts',(188.46319427063,-4.08942232393587,135.083303013377));
#141197=CARTESIAN_POINT('Ctrl Pts',(188.455796356319,-3.97400128576268,
135.190711993113));
#141198=CARTESIAN_POINT('Ctrl Pts',(188.448398442007,-3.85443981639646,
135.293372119476));
#141199=CARTESIAN_POINT('Ctrl Pts',(188.441001757095,-3.73489821597734,
135.396015185588));
#141200=CARTESIAN_POINT('Ctrl Pts',(188.433605072183,-3.61121783291183,
135.493910721659));
#141201=CARTESIAN_POINT('Ctrl Pts',(188.426208387271,-3.483818170251,135.586717935786));
#141202=CARTESIAN_POINT('Ctrl Pts',(188.418812030335,-3.35642415662479,
135.679521034743));
#141203=CARTESIAN_POINT('Ctrl Pts',(188.4114156734,-3.22531149304034,135.767236040568));
#141204=CARTESIAN_POINT('Ctrl Pts',(188.404019316464,-3.09093063134526,
135.849564121362));
#141205=CARTESIAN_POINT('Ctrl Pts',(188.396621827128,-2.95652919559707,
135.931904806795));
#141206=CARTESIAN_POINT('Ctrl Pts',(188.389224337791,-2.81885888376706,
136.00885672998));
#141207=CARTESIAN_POINT('Ctrl Pts',(188.381826848455,-2.67839669617966,
136.080165930539));
#141208=CARTESIAN_POINT('Ctrl Pts',(188.37442676594,-2.53788526979019,136.151500128428));
#141209=CARTESIAN_POINT('Ctrl Pts',(188.367026683425,-2.39458035173523,
136.217187496532));
#141210=CARTESIAN_POINT('Ctrl Pts',(188.35962660091,-2.24898081214349,136.277021384424));
#141211=CARTESIAN_POINT('Ctrl Pts',(188.352218381243,-2.10322117088992,
136.336921065828));
#141212=CARTESIAN_POINT('Ctrl Pts',(188.344810161577,-1.95516221465031,
136.390954270921));
#141213=CARTESIAN_POINT('Ctrl Pts',(188.33740194191,-1.80532063496924,136.43896335134));
#141214=CARTESIAN_POINT('Ctrl Pts',(188.329989162608,-1.65538683029596,
136.487001980547));
#141215=CARTESIAN_POINT('Ctrl Pts',(188.322576383306,-1.50366857485122,
136.529008997548));
#141216=CARTESIAN_POINT('Ctrl Pts',(188.315163604004,-1.35069426213214,
136.564877571169));
#141217=CARTESIAN_POINT('Ctrl Pts',(188.307740232975,-1.19750137254131,
136.600797395489));
#141218=CARTESIAN_POINT('Ctrl Pts',(188.300316861946,-1.04304920681346,
136.630561188534));
#141219=CARTESIAN_POINT('Ctrl Pts',(188.292893490918,-0.887873634317857,
136.654113686883));
#141220=CARTESIAN_POINT('Ctrl Pts',(188.288957441477,-0.805595822389184,
136.666601786643));
#141221=CARTESIAN_POINT('Ctrl Pts',(188.285021392036,-0.72311468724722,
136.67734453826));
#141222=CARTESIAN_POINT('Ctrl Pts',(188.281085342595,-0.640510152529407,
136.686339647366));
#141223=CARTESIAN_POINT('Ctrl Pts',(188.273662076189,-0.484720578059533,
136.703304142411));
#141224=CARTESIAN_POINT('Ctrl Pts',(188.266238809784,-0.328020986091857,
136.714100671442));
#141225=CARTESIAN_POINT('Ctrl Pts',(188.258815543378,-0.170941080575582,
136.718640768985));
#141226=CARTESIAN_POINT('Ctrl Pts',(188.251401050657,-0.014046830462841,
136.72317550051));
#141227=CARTESIAN_POINT('Ctrl Pts',(188.243986557936,0.143226468969914,
136.721468508825));
#141228=CARTESIAN_POINT('Ctrl Pts',(188.236572065215,0.300341982397618,
136.713482824469));
#141229=CARTESIAN_POINT('Ctrl Pts',(188.229164718861,0.457306061978129,
136.705504837015));
#141230=CARTESIAN_POINT('Ctrl Pts',(188.221757372508,0.61411228800125,136.691260223337));
#141231=CARTESIAN_POINT('Ctrl Pts',(188.214350026154,0.770221908090596,
136.670764011026));
#141232=CARTESIAN_POINT('Ctrl Pts',(188.206948204478,0.926215095735712,
136.650283085563));
#141233=CARTESIAN_POINT('Ctrl Pts',(188.199546382803,1.08151234342266,136.623559893873));
#141234=CARTESIAN_POINT('Ctrl Pts',(188.192144561128,1.23557822068304,136.590661424046));
#141235=CARTESIAN_POINT('Ctrl Pts',(188.184746646816,1.38956276776613,136.557780321065));
#141236=CARTESIAN_POINT('Ctrl Pts',(188.177348732505,1.54231687484672,136.518730509913));
#141237=CARTESIAN_POINT('Ctrl Pts',(188.169950818194,1.69331364128615,136.473630365491));
#141238=CARTESIAN_POINT('Ctrl Pts',(188.162554133281,1.84428531480222,136.428537715894));
#141239=CARTESIAN_POINT('Ctrl Pts',(188.155157448369,1.99349986995265,136.377396835288));
#141240=CARTESIAN_POINT('Ctrl Pts',(188.147760763457,2.14044383721241,136.320376457123));
#141241=CARTESIAN_POINT('Ctrl Pts',(188.140364406522,2.28738128882264,136.263358607301));
#141242=CARTESIAN_POINT('Ctrl Pts',(188.132968049586,2.43204800471394,136.20046191333));
#141243=CARTESIAN_POINT('Ctrl Pts',(188.125571692651,2.57394908891939,136.131903827166));
#141244=CARTESIAN_POINT('Ctrl Pts',(188.118174203314,2.71587189854313,136.063335244583));
#141245=CARTESIAN_POINT('Ctrl Pts',(188.110776713978,2.85502789723953,135.989103706352));
#141246=CARTESIAN_POINT('Ctrl Pts',(188.103379224641,2.99094559062203,135.909473254564));
#141247=CARTESIAN_POINT('Ctrl Pts',(188.095979142126,3.12691092974114,135.829814888445));
#141248=CARTESIAN_POINT('Ctrl Pts',(188.088579059611,3.25963538151613,135.744754029243));
#141249=CARTESIAN_POINT('Ctrl Pts',(188.081178977096,3.38867543359986,135.65459869092));
#141250=CARTESIAN_POINT('Ctrl Pts',(188.07377075743,3.51785737848661,135.564344217535));
#141251=CARTESIAN_POINT('Ctrl Pts',(188.066362537763,3.64334652662018,135.46898429159));
#141252=CARTESIAN_POINT('Ctrl Pts',(188.058954318097,3.76473095956622,135.368868407524));
#141253=CARTESIAN_POINT('Ctrl Pts',(188.051541538795,3.88619010260547,135.268690903801));
#141254=CARTESIAN_POINT('Ctrl Pts',(188.044128759492,4.0035392187013,135.163751857378));
#141255=CARTESIAN_POINT('Ctrl Pts',(188.03671598019,4.11640281816916,135.054438075809));
#141256=CARTESIAN_POINT('Ctrl Pts',(188.029292609162,4.22942768244064,134.944968101584));
#141257=CARTESIAN_POINT('Ctrl Pts',(188.021869238133,4.33795397276301,134.831111177405));
#141258=CARTESIAN_POINT('Ctrl Pts',(188.014445867104,4.44164554397361,134.713288274123));
#141259=CARTESIAN_POINT('Ctrl Pts',(188.010509817663,4.49662530307466,134.650815743681));
#141260=CARTESIAN_POINT('Ctrl Pts',(188.006573768223,4.55024655251569,134.587228748358));
#141261=CARTESIAN_POINT('Ctrl Pts',(188.002637718782,4.60246416130131,134.522593290011));
#141262=CARTESIAN_POINT('Ctrl Pts',(187.995214452376,4.70094494181516,134.400692832772));
#141263=CARTESIAN_POINT('Ctrl Pts',(187.987791185971,4.79472832452141,134.274692815747));
#141264=CARTESIAN_POINT('Ctrl Pts',(187.980367919565,4.88345356298841,134.144991076123));
#141265=CARTESIAN_POINT('Ctrl Pts',(187.972953426844,4.9720739355918,134.015442633183));
#141266=CARTESIAN_POINT('Ctrl Pts',(187.965538934123,5.05564785509995,133.882201481457));
#141267=CARTESIAN_POINT('Ctrl Pts',(187.958124441402,5.13385404545199,133.745699292812));
#141268=CARTESIAN_POINT('Ctrl Pts',(187.950717095049,5.21198485773338,133.609328670115));
#141269=CARTESIAN_POINT('Ctrl Pts',(187.943309748695,5.28475805618814,133.469703589541));
#141270=CARTESIAN_POINT('Ctrl Pts',(187.935902402341,5.3518950751355,133.327285441504));
#141271=CARTESIAN_POINT('Ctrl Pts',(187.928500580666,5.41898202076117,133.184973514294));
#141272=CARTESIAN_POINT('Ctrl Pts',(187.92109875899,5.48044099847369,133.03987300371));
#141273=CARTESIAN_POINT('Ctrl Pts',(187.913696937315,5.53603895400241,132.892470591267));
#141274=CARTESIAN_POINT('Ctrl Pts',(187.906299023003,5.59160755980321,132.74514599141));
#141275=CARTESIAN_POINT('Ctrl Pts',(187.898901108692,5.64132117383657,132.595522258129));
#141276=CARTESIAN_POINT('Ctrl Pts',(187.891503194381,5.68499458559291,132.44410667238));
#141277=CARTESIAN_POINT('Ctrl Pts',(187.884106509468,5.72866073962051,132.292716249155));
#141278=CARTESIAN_POINT('Ctrl Pts',(187.876709824556,5.76628858020843,132.139534922778));
#141279=CARTESIAN_POINT('Ctrl Pts',(187.869313139644,5.79774252476681,131.985085894254));
#141280=CARTESIAN_POINT('Ctrl Pts',(187.861916782709,5.82919507462433,131.830643714162));
#141281=CARTESIAN_POINT('Ctrl Pts',(187.854520425773,5.85447419827982,131.67493430948));
#141282=CARTESIAN_POINT('Ctrl Pts',(187.847124068838,5.87349534086361,131.518491588294));
#141283=CARTESIAN_POINT('Ctrl Pts',(187.839726579501,5.8925193956329,131.362024915329));
#141284=CARTESIAN_POINT('Ctrl Pts',(187.832329090164,5.90528351654167,131.204825072902));
#141285=CARTESIAN_POINT('Ctrl Pts',(187.824931600828,5.91175499544869,131.047431463797));
#141286=CARTESIAN_POINT('Ctrl Pts',(187.817531518313,5.9182287429226,130.889982680606));
#141287=CARTESIAN_POINT('Ctrl Pts',(187.810131435798,5.91840544118585,130.73234036825));
#141288=CARTESIAN_POINT('Ctrl Pts',(187.802731353283,5.91230450185313,130.575044155298));
#141289=CARTESIAN_POINT('Ctrl Pts',(187.795323133616,5.90619685391042,130.417574978989));
#141290=CARTESIAN_POINT('Ctrl Pts',(187.78791491395,5.89379779728831,130.260453035358));
#141291=CARTESIAN_POINT('Ctrl Pts',(187.780506694283,5.87517871958054,130.10421379333));
#141292=CARTESIAN_POINT('Ctrl Pts',(187.773093914981,5.8565481821411,129.947878388655));
#141293=CARTESIAN_POINT('Ctrl Pts',(187.765681135679,5.83169005401839,129.792427135914));
#141294=CARTESIAN_POINT('Ctrl Pts',(187.758268356377,5.80072680601682,129.638385024143));
#141295=CARTESIAN_POINT('Ctrl Pts',(187.750844985348,5.76971931627449,129.484122809779));
#141296=CARTESIAN_POINT('Ctrl Pts',(187.74342161432,5.73258937218858,129.331274119478));
#141297=CARTESIAN_POINT('Ctrl Pts',(187.735998243291,5.68950945378594,129.180349306712));
#141298=CARTESIAN_POINT('Ctrl Pts',(187.73206219385,5.66666744736085,129.100325349594));
#141299=CARTESIAN_POINT('Ctrl Pts',(187.728126144409,5.64215350241321,129.020841949638));
#141300=CARTESIAN_POINT('Ctrl Pts',(187.724190094969,5.61599875376964,128.941972752443));
#141301=CARTESIAN_POINT('Ctrl Pts',(187.716766828563,5.56667171408872,128.793227907954));
#141302=CARTESIAN_POINT('Ctrl Pts',(187.709343562158,5.51135654039937,128.646219205077));
#141303=CARTESIAN_POINT('Ctrl Pts',(187.701920295752,5.45019295213473,128.501465190717));
#141304=CARTESIAN_POINT('Ctrl Pts',(187.694505803031,5.38910165415207,128.356882263581));
#141305=CARTESIAN_POINT('Ctrl Pts',(187.68709131031,5.32217584452053,128.214549061059));
#141306=CARTESIAN_POINT('Ctrl Pts',(187.679676817589,5.24960504344817,128.074969210988));
#141307=CARTESIAN_POINT('Ctrl Pts',(187.672269471236,5.17710418884611,127.935523893231));
#141308=CARTESIAN_POINT('Ctrl Pts',(187.664862124882,5.09896934552089,127.798826973745));
#141309=CARTESIAN_POINT('Ctrl Pts',(187.657454778528,5.01543812273929,127.665362210514));
#141310=CARTESIAN_POINT('Ctrl Pts',(187.650052956853,4.9319692006951,127.53199699034));
#141311=CARTESIAN_POINT('Ctrl Pts',(187.642651135177,4.84311211035346,127.401859441534));
#141312=CARTESIAN_POINT('Ctrl Pts',(187.635249313502,4.74915033913089,127.275408702502));
#141313=CARTESIAN_POINT('Ctrl Pts',(187.62785139919,4.65523816959588,127.149024715831));
#141314=CARTESIAN_POINT('Ctrl Pts',(187.620453484879,4.55622690793055,127.026323961781));
#141315=CARTESIAN_POINT('Ctrl Pts',(187.613055570568,4.45244323316465,126.907736460947));
#141316=CARTESIAN_POINT('Ctrl Pts',(187.605658885656,4.34867680536279,126.789168667204));
#141317=CARTESIAN_POINT('Ctrl Pts',(187.598262200743,4.24013978411027,126.674713050673));
#141318=CARTESIAN_POINT('Ctrl Pts',(187.590865515831,4.12719906752894,126.56476648375));
#141319=CARTESIAN_POINT('Ctrl Pts',(187.583469158896,4.01426335885729,126.454824791973));
#141320=CARTESIAN_POINT('Ctrl Pts',(187.57607280196,3.89692461059156,126.349392012655));
#141321=CARTESIAN_POINT('Ctrl Pts',(187.568676445025,3.77558631075384,126.248827874566));
#141322=CARTESIAN_POINT('Ctrl Pts',(187.561278955688,3.65422943371256,126.14824833985));
#141323=CARTESIAN_POINT('Ctrl Pts',(187.553881466352,3.52887207328063,126.05253916878));
#141324=CARTESIAN_POINT('Ctrl Pts',(187.546483977015,3.39995036474609,125.962019440019));
#141325=CARTESIAN_POINT('Ctrl Pts',(187.5390838945,3.27098346290651,125.871467979709));
#141326=CARTESIAN_POINT('Ctrl Pts',(187.531683811985,3.13845003058641,125.786109797999));
#141327=CARTESIAN_POINT('Ctrl Pts',(187.52428372947,3.00281456503668,125.706220245773));
#141328=CARTESIAN_POINT('Ctrl Pts',(187.516875509804,2.86702995434889,125.626242846772));
#141329=CARTESIAN_POINT('Ctrl Pts',(187.509467290137,2.72813682027947,125.551746275818));
#141330=CARTESIAN_POINT('Ctrl Pts',(187.502059070471,2.58662425473907,125.482959906541));
#141331=CARTESIAN_POINT('Ctrl Pts',(187.494646291169,2.44502459057584,125.414131200402));
#141332=CARTESIAN_POINT('Ctrl Pts',(187.487233511867,2.3008026235927,125.351019848396));
#141333=CARTESIAN_POINT('Ctrl Pts',(187.479820732564,2.15446624039682,125.293806581764));
#141334=CARTESIAN_POINT('Ctrl Pts',(187.472397361536,2.00792076491405,125.236511566134));
#141335=CARTESIAN_POINT('Ctrl Pts',(187.464973990507,1.85925519113648,125.185131589024));
#141336=CARTESIAN_POINT('Ctrl Pts',(187.457550619478,1.7089921235619,125.139797396619));
#141337=CARTESIAN_POINT('Ctrl Pts',(187.453614570037,1.62931903962022,125.115760120027));
#141338=CARTESIAN_POINT('Ctrl Pts',(187.449678520597,1.54919701811686,125.093421677015));
#141339=CARTESIAN_POINT('Ctrl Pts',(187.445742471156,1.46870484831581,125.072795680218));
#141340=CARTESIAN_POINT('Ctrl Pts',(187.43831920475,1.31689912814708,125.033895693975));
#141341=CARTESIAN_POINT('Ctrl Pts',(187.430895938345,1.1633173403862,125.000972121415));
#141342=CARTESIAN_POINT('Ctrl Pts',(187.423472671939,1.00847127499773,124.97418769989));
#141343=CARTESIAN_POINT('Ctrl Pts',(187.416058179218,0.853808224799215,
124.947434935327));
#141344=CARTESIAN_POINT('Ctrl Pts',(187.408643686497,0.697884235571734,
124.926806941762));
#141345=CARTESIAN_POINT('Ctrl Pts',(187.401229193776,0.541225463979645,
124.912416493625));
#141346=CARTESIAN_POINT('Ctrl Pts',(187.393821847423,0.384717686009742,
124.898039915544));
#141347=CARTESIAN_POINT('Ctrl Pts',(187.386414501069,0.227476904821062,
124.889888948137));
#141348=CARTESIAN_POINT('Ctrl Pts',(187.379007154715,0.0700385533196246,
124.888025167006));
#141349=CARTESIAN_POINT('Ctrl Pts',(187.37160533304,-0.0872823747195095,
124.886162775954));
#141350=CARTESIAN_POINT('Ctrl Pts',(187.364203511364,-0.244800208001704,
124.890578238706));
#141351=CARTESIAN_POINT('Ctrl Pts',(187.356801689689,-0.401975428509942,
124.901281224794));
#141352=CARTESIAN_POINT('Ctrl Pts',(187.349403775377,-0.559067677442723,
124.911978560858));
#141353=CARTESIAN_POINT('Ctrl Pts',(187.342005861066,-0.715817302305466,
124.928956784745));
#141354=CARTESIAN_POINT('Ctrl Pts',(187.334607946755,-0.871685936598251,
124.952173488771));
#141355=CARTESIAN_POINT('Ctrl Pts',(187.327211261842,-1.02752866835165,
124.975386334601));
#141356=CARTESIAN_POINT('Ctrl Pts',(187.31981457693,-1.18249033124199,125.00483554804));
#141357=CARTESIAN_POINT('Ctrl Pts',(187.312417892018,-1.33603870788574,
125.040426966531));
#141358=CARTESIAN_POINT('Ctrl Pts',(187.305021535083,-1.48958027603362,
125.076016806862));
#141359=CARTESIAN_POINT('Ctrl Pts',(187.297625178147,-1.64170831888113,
125.117748226424));
#141360=CARTESIAN_POINT('Ctrl Pts',(187.290228821212,-1.79190209129523,
125.165476201504));
#141361=CARTESIAN_POINT('Ctrl Pts',(187.282831331875,-1.94211885875933,
125.213211483858));
#141362=CARTESIAN_POINT('Ctrl Pts',(187.275433842538,-2.09040041034268,
125.266945036705));
#141363=CARTESIAN_POINT('Ctrl Pts',(187.268036353202,-2.2362425543513,125.326482396885));
#141364=CARTESIAN_POINT('Ctrl Pts',(187.260636270687,-2.38213582309748,
125.386040627795));
#141365=CARTESIAN_POINT('Ctrl Pts',(187.253236188172,-2.52558763631716,
125.451406575745));
#141366=CARTESIAN_POINT('Ctrl Pts',(187.245836105657,-2.66611526140484,
125.522338279919));
#141367=CARTESIAN_POINT('Ctrl Pts',(187.23842788599,-2.80679741106287,125.593347980794));
#141368=CARTESIAN_POINT('Ctrl Pts',(187.231019666324,-2.94454861767688,
125.669935491864));
#141369=CARTESIAN_POINT('Ctrl Pts',(187.223611446657,-3.07891153659171,
125.751813308303));
#141370=CARTESIAN_POINT('Ctrl Pts',(187.216198667355,-3.2133571536413,125.833741519172));
#141371=CARTESIAN_POINT('Ctrl Pts',(187.208785888053,-3.34441001746257,
125.920966317233));
#141372=CARTESIAN_POINT('Ctrl Pts',(187.201373108751,-3.47164354862595,
126.013158092752));
#141373=CARTESIAN_POINT('Ctrl Pts',(187.193949737723,-3.59905887702523,
126.105481596203));
#141374=CARTESIAN_POINT('Ctrl Pts',(187.186526366694,-3.72264368091018,
126.202786021196));
#141375=CARTESIAN_POINT('Ctrl Pts',(187.179102995665,-3.84200547931489,
126.304702357274));
#141376=CARTESIAN_POINT('Ctrl Pts',(187.175166946224,-3.90529396887533,
126.358740844111));
#141377=CARTESIAN_POINT('Ctrl Pts',(187.171230896784,-3.96739584334917,
126.414075295879));
#141378=CARTESIAN_POINT('Ctrl Pts',(187.167294847343,-4.02825706251959,
126.470646782902));
#141379=CARTESIAN_POINT('Ctrl Pts',(187.159982110724,-4.14133035410826,
126.57575023523));
#141380=CARTESIAN_POINT('Ctrl Pts',(187.152669374104,-4.25048290247324,
126.685464074864));
#141381=CARTESIAN_POINT('Ctrl Pts',(187.145356637485,-4.355306958856,126.799459637936));
#141382=CARTESIAN_POINT('Ctrl Pts',(187.138052644169,-4.4600056848014,126.913318904872));
#141383=CARTESIAN_POINT('Ctrl Pts',(187.130748650852,-4.56038595696257,
127.03144942948));
#141384=CARTESIAN_POINT('Ctrl Pts',(187.123444657536,-4.65607377997443,
127.153482980896));
#141385=CARTESIAN_POINT('Ctrl Pts',(187.11614769061,-4.75166955197894,127.275399136901));
#141386=CARTESIAN_POINT('Ctrl Pts',(187.108850723683,-4.84258162128955,
127.401210547057));
#141387=CARTESIAN_POINT('Ctrl Pts',(187.101553756756,-4.92847369766666,
127.530513099139));
#141388=CARTESIAN_POINT('Ctrl Pts',(187.094262461591,-5.01429901214382,
127.659715147376));
#141389=CARTESIAN_POINT('Ctrl Pts',(187.086971166426,-5.09511188989882,
127.792402615212));
#141390=CARTESIAN_POINT('Ctrl Pts',(187.079679871261,-5.1706173282255,127.92813965812));
#141391=CARTESIAN_POINT('Ctrl Pts',(187.072391625532,-5.24609118793796,
128.063819931771));
#141392=CARTESIAN_POINT('Ctrl Pts',(187.065103379803,-5.31626183691263,
128.202546907271));
#141393=CARTESIAN_POINT('Ctrl Pts',(187.057815134074,-5.38087854125002,
128.343857277431));
#141394=CARTESIAN_POINT('Ctrl Pts',(187.050528398168,-5.44548185967987,
128.48513837393));
#141395=CARTESIAN_POINT('Ctrl Pts',(187.043241662262,-5.50453336306754,
128.629001449778));
#141396=CARTESIAN_POINT('Ctrl Pts',(187.035954926356,-5.55782922554555,
128.774960493842));
#141397=CARTESIAN_POINT('Ctrl Pts',(187.028668162023,-5.61112529593695,
128.920920107308));
#141398=CARTESIAN_POINT('Ctrl Pts',(187.021381397691,-5.65866555016246,
129.068975342758));
#141399=CARTESIAN_POINT('Ctrl Pts',(187.014094633358,-5.7002951840503,129.218622500097));
#141400=CARTESIAN_POINT('Ctrl Pts',(187.006803471584,-5.74194994073617,
129.368359967031));
#141401=CARTESIAN_POINT('Ctrl Pts',(186.999512309809,-5.77768684994215,
129.519690902912));
#141402=CARTESIAN_POINT('Ctrl Pts',(186.992221148034,-5.80740158088912,
129.672098527418));
#141403=CARTESIAN_POINT('Ctrl Pts',(186.984927500083,-5.8371264441105,129.824558120621));
#141404=CARTESIAN_POINT('Ctrl Pts',(186.977633852133,-5.86082497829701,
129.97809475339));
#141405=CARTESIAN_POINT('Ctrl Pts',(186.970340204182,-5.87844452383703,
130.132184641597));
#141406=CARTESIAN_POINT('Ctrl Pts',(186.963039152689,-5.89608195439748,
130.286430941374));
#141407=CARTESIAN_POINT('Ctrl Pts',(186.955738101197,-5.90762804625571,
130.441231234208));
#141408=CARTESIAN_POINT('Ctrl Pts',(186.948437049704,-5.91308220639865,
130.596059434488));
#141409=CARTESIAN_POINT('Ctrl Pts',(186.945083097206,-5.91558773509581,
130.66718431692));
#141410=CARTESIAN_POINT('Ctrl Pts',(186.941729144709,-5.91680841145624,
130.738315114615));
#141411=CARTESIAN_POINT('Ctrl Pts',(186.938375192211,-5.91674785298769,
130.809401120074));
#141412=CARTESIAN_POINT('',(185.188375192211,-5.92379981193959,130.800775453898));
#141413=CARTESIAN_POINT('Ctrl Pts',(186.938375192211,-5.9200304115163,130.809403916499));
#141414=CARTESIAN_POINT('Ctrl Pts',(186.921865869317,-5.92320279675294,
131.159511089235));
#141415=CARTESIAN_POINT('Ctrl Pts',(186.812540671824,-5.73530460751272,
133.474529816069));
#141416=CARTESIAN_POINT('Ctrl Pts',(186.610399599713,-2.68163859043372,
137.268598778454));
#141417=CARTESIAN_POINT('Ctrl Pts',(186.331951975907,3.98905548069682,136.554577735401));
#141418=CARTESIAN_POINT('Ctrl Pts',(186.05350435209,6.99400244126163,130.556388074787));
#141419=CARTESIAN_POINT('Ctrl Pts',(185.775056728279,3.57180283432081,124.78607306685));
#141420=CARTESIAN_POINT('Ctrl Pts',(185.496609104465,-3.13270908509169,
124.546270308331));
#141421=CARTESIAN_POINT('Ctrl Pts',(185.301048592443,-5.81959460894973,
128.416832856216));
#141422=CARTESIAN_POINT('Ctrl Pts',(185.198303955025,-5.92529888389735,
130.590568476525));
#141423=CARTESIAN_POINT('Ctrl Pts',(185.188375192211,-5.92379981193959,
130.800775453898));
#141424=CARTESIAN_POINT('',(183.438375192211,-5.90878783959383,130.801050019915));
#141425=CARTESIAN_POINT('Ctrl Pts',(185.188375192211,-5.92379981193959,
130.800775453898));
#141426=CARTESIAN_POINT('Ctrl Pts',(185.105488080421,-5.9112852874943,132.555621405934));
#141427=CARTESIAN_POINT('Ctrl Pts',(184.929785094025,-4.15424292220225,
136.29728126716));
#141428=CARTESIAN_POINT('Ctrl Pts',(184.661266233027,2.21295931186131,137.443665672644));
#141429=CARTESIAN_POINT('Ctrl Pts',(184.382818609213,6.78199394032505,132.531241830544));
#141430=CARTESIAN_POINT('Ctrl Pts',(184.104370985402,5.11870745645332,126.031898516554));
#141431=CARTESIAN_POINT('Ctrl Pts',(183.825923361588,-1.24842111713792,
123.918214725658));
#141432=CARTESIAN_POINT('Ctrl Pts',(183.603924763859,-5.41009564609318,
127.278197857111));
#141433=CARTESIAN_POINT('Ctrl Pts',(183.474742040733,-5.91271172097454,
130.026098884935));
#141434=CARTESIAN_POINT('Ctrl Pts',(183.438375192211,-5.90878783959383,
130.801050019915));
#141435=CARTESIAN_POINT('',(181.688375192211,-5.9116597264178,130.809147953816));
#141436=CARTESIAN_POINT('Ctrl Pts',(183.438375192211,-5.90878783959383,
130.801050019915));
#141437=CARTESIAN_POINT('Ctrl Pts',(183.381926166128,-5.90269714734493,
132.003937776489));
#141438=CARTESIAN_POINT('Ctrl Pts',(183.232661265441,-4.96014564476939,
135.193432897632));
#141439=CARTESIAN_POINT('Ctrl Pts',(182.99058049015,0.258615936756311,137.79797758789));
#141440=CARTESIAN_POINT('Ctrl Pts',(182.712132866336,6.02371625752071,134.36700050664));
#141441=CARTESIAN_POINT('Ctrl Pts',(182.433685242524,6.2533156125226,127.662131411966));
#141442=CARTESIAN_POINT('Ctrl Pts',(182.155237618711,0.736423411067356,
123.844817450807));
#141443=CARTESIAN_POINT('Ctrl Pts',(181.906800935273,-4.78965977321783,
126.145110250613));
#141444=CARTESIAN_POINT('Ctrl Pts',(181.75118012644,-5.90155441818334,129.472452618097));
#141445=CARTESIAN_POINT('Ctrl Pts',(181.688375192211,-5.9116597264178,130.809147953816));
#141446=CARTESIAN_POINT('',(179.938376004444,-5.92191450869858,130.805748116515));
#141447=CARTESIAN_POINT('Ctrl Pts',(181.688375192211,-5.9116597264178,130.809147953816));
#141448=CARTESIAN_POINT('Ctrl Pts',(181.658364251836,-5.91648848400863,
131.447879361033));
#141449=CARTESIAN_POINT('Ctrl Pts',(181.535537436858,-5.52634643860716,
134.05629721562));
#141450=CARTESIAN_POINT('Ctrl Pts',(181.31989474727,-1.71655817300176,137.588974723689));
#141451=CARTESIAN_POINT('Ctrl Pts',(181.041447123461,4.78024637596874,135.91579927174));
#141452=CARTESIAN_POINT('Ctrl Pts',(180.762999499646,6.88423803344246,129.54546140426));
#141453=CARTESIAN_POINT('Ctrl Pts',(180.484551875834,2.66195125190711,124.331990413167));
#141454=CARTESIAN_POINT('Ctrl Pts',(180.209677598402,-3.92096128402385,
125.056887831312));
#141455=CARTESIAN_POINT('Ctrl Pts',(180.027619195576,-5.92009025890988,
128.918301208267));
#141456=CARTESIAN_POINT('Ctrl Pts',(179.938376667353,-5.92612969673344,
130.805735096168));
#141457=CARTESIAN_POINT('',(178.188375192211,-5.91592736650928,130.798890494443));
#141458=CARTESIAN_POINT('Ctrl Pts',(179.938375192211,-5.91674983355068,
130.805764069745));
#141459=CARTESIAN_POINT('Ctrl Pts',(179.934802337543,-5.91673193815412,
130.881208453364));
#141460=CARTESIAN_POINT('Ctrl Pts',(179.931229482876,-5.91527111751309,
130.956633994371));
#141461=CARTESIAN_POINT('Ctrl Pts',(179.927656628208,-5.91236916926149,
131.032003690964));
#141462=CARTESIAN_POINT('Ctrl Pts',(179.920233361803,-5.90633983502618,
131.18859817597));
#141463=CARTESIAN_POINT('Ctrl Pts',(179.912810095397,-5.89407576518302,
131.345189745836));
#141464=CARTESIAN_POINT('Ctrl Pts',(179.905386828992,-5.87556700792397,
131.501241452354));
#141465=CARTESIAN_POINT('Ctrl Pts',(179.897972336271,-5.85708012647892,
131.657108718716));
#141466=CARTESIAN_POINT('Ctrl Pts',(179.89055784355,-5.83236329248394,131.81243702474));
#141467=CARTESIAN_POINT('Ctrl Pts',(179.883143350829,-5.80145853932096,
131.966689907845));
#141468=CARTESIAN_POINT('Ctrl Pts',(179.875736004475,-5.77058357332259,
132.120794116214));
#141469=CARTESIAN_POINT('Ctrl Pts',(179.868328658121,-5.73353263444466,
132.27382460163));
#141470=CARTESIAN_POINT('Ctrl Pts',(179.860921311767,-5.69039947340868,
132.425250618624));
#141471=CARTESIAN_POINT('Ctrl Pts',(179.853519490092,-5.64729848271151,
132.576563696382));
#141472=CARTESIAN_POINT('Ctrl Pts',(179.846117668417,-5.59812440416739,
132.726274330983));
#141473=CARTESIAN_POINT('Ctrl Pts',(179.838715846741,-5.54302190257774,
132.873862671212));
#141474=CARTESIAN_POINT('Ctrl Pts',(179.83131793243,-5.48794848916994,133.021373100704));
#141475=CARTESIAN_POINT('Ctrl Pts',(179.823920018118,-5.42695301563993,
133.166763118208));
#141476=CARTESIAN_POINT('Ctrl Pts',(179.816522103807,-5.3602297308131,133.309528834554));
#141477=CARTESIAN_POINT('Ctrl Pts',(179.809125418895,-5.2935175341856,133.452270825829));
#141478=CARTESIAN_POINT('Ctrl Pts',(179.801728733983,-5.22107957331895,
133.592389043643));
#141479=CARTESIAN_POINT('Ctrl Pts',(179.79433204907,-5.1431579462292,133.729400258774));
#141480=CARTESIAN_POINT('Ctrl Pts',(179.786935692135,-5.06523977426604,
133.866405398685));
#141481=CARTESIAN_POINT('Ctrl Pts',(179.779539335199,-4.98183860409271,
134.000303485351));
#141482=CARTESIAN_POINT('Ctrl Pts',(179.772142978264,-4.89324200758084,
134.13063679638));
#141483=CARTESIAN_POINT('Ctrl Pts',(179.764745488927,-4.80463184670375,
134.260990061772));
#141484=CARTESIAN_POINT('Ctrl Pts',(179.757347999591,-4.71082488554907,
134.387777156069));
#141485=CARTESIAN_POINT('Ctrl Pts',(179.749950510254,-4.61215135748797,
134.510570328055));
#141486=CARTESIAN_POINT('Ctrl Pts',(179.742550427739,-4.51344323957483,
134.633406544996));
#141487=CARTESIAN_POINT('Ctrl Pts',(179.735150345224,-4.4098653918718,134.752245761303));
#141488=CARTESIAN_POINT('Ctrl Pts',(179.727750262709,-4.30178744852212,
134.866694344654));
#141489=CARTESIAN_POINT('Ctrl Pts',(179.720342043042,-4.19359066236287,
134.981268775988));
#141490=CARTESIAN_POINT('Ctrl Pts',(179.712933823376,-4.08088415489833,
135.091442661055));
#141491=CARTESIAN_POINT('Ctrl Pts',(179.70552560371,-3.96407396764172,135.19685969458));
#141492=CARTESIAN_POINT('Ctrl Pts',(179.698112824407,-3.84719188566385,
135.30234161053));
#141493=CARTESIAN_POINT('Ctrl Pts',(179.690700045105,-3.72620137726176,
135.403060602727));
#141494=CARTESIAN_POINT('Ctrl Pts',(179.683287265803,-3.60154006095042,
135.49870186548));
#141495=CARTESIAN_POINT('Ctrl Pts',(179.675863894774,-3.47670062270434,
135.594479784955));
#141496=CARTESIAN_POINT('Ctrl Pts',(179.668440523746,-3.34818020526591,
135.685165269879));
#141497=CARTESIAN_POINT('Ctrl Pts',(179.661017152717,-3.21644446134536,
135.77048743729));
#141498=CARTESIAN_POINT('Ctrl Pts',(179.657081103276,-3.14659500896289,
135.815727297728));
#141499=CARTESIAN_POINT('Ctrl Pts',(179.653145053835,-3.07584201855703,
135.859460108231));
#141500=CARTESIAN_POINT('Ctrl Pts',(179.649209004394,-3.00425738879533,
135.901650888324));
#141501=CARTESIAN_POINT('Ctrl Pts',(179.641785737989,-2.86925101114459,
135.981221382851));
#141502=CARTESIAN_POINT('Ctrl Pts',(179.634362471584,-2.73087705919654,
136.05554484203));
#141503=CARTESIAN_POINT('Ctrl Pts',(179.626939205178,-2.58958190348824,
136.124322659501));
#141504=CARTESIAN_POINT('Ctrl Pts',(179.619524712457,-2.44845374692,136.193019187303));
#141505=CARTESIAN_POINT('Ctrl Pts',(179.612110219736,-2.30441159141906,
136.256182958357));
#141506=CARTESIAN_POINT('Ctrl Pts',(179.604695727015,-2.15792949821889,
136.313559365407));
#141507=CARTESIAN_POINT('Ctrl Pts',(179.597288380661,-2.01158858997503,
136.370880470916));
#141508=CARTESIAN_POINT('Ctrl Pts',(179.589881034308,-1.86281277106264,
136.422425182046));
#141509=CARTESIAN_POINT('Ctrl Pts',(179.582473687954,-1.71209924723198,
136.467985493044));
#141510=CARTESIAN_POINT('Ctrl Pts',(179.575071866278,-1.5614981312336,136.513511823442));
#141511=CARTESIAN_POINT('Ctrl Pts',(179.567670044603,-1.40896254372182,
136.553062533368));
#141512=CARTESIAN_POINT('Ctrl Pts',(179.560268222928,-1.25500804510559,
136.586478341136));
#141513=CARTESIAN_POINT('Ctrl Pts',(179.552870308616,-1.10113481787052,
136.619876508959));
#141514=CARTESIAN_POINT('Ctrl Pts',(179.545472394305,-0.945844535144645,
136.647146145406));
#141515=CARTESIAN_POINT('Ctrl Pts',(179.538074479993,-0.789666129390942,
136.668178313112));
#141516=CARTESIAN_POINT('Ctrl Pts',(179.530677795081,-0.633513677655301,
136.689206985652));
#141517=CARTESIAN_POINT('Ctrl Pts',(179.523281110169,-0.476473765410261,
136.704000196932));
#141518=CARTESIAN_POINT('Ctrl Pts',(179.515884425257,-0.319083806977362,
136.712500433669));
#141519=CARTESIAN_POINT('Ctrl Pts',(179.508488068321,-0.161700827380124,
136.721000293498));
#141520=CARTESIAN_POINT('Ctrl Pts',(179.501091711386,-0.0039682052111765,
136.723207713473));
#141521=CARTESIAN_POINT('Ctrl Pts',(179.493695354451,0.153573525095219,
136.71911722582));
#141522=CARTESIAN_POINT('Ctrl Pts',(179.486297865114,0.311139375442765,
136.715026111904));
#141523=CARTESIAN_POINT('Ctrl Pts',(179.478900375777,0.468513902538733,
136.704635180148));
#141524=CARTESIAN_POINT('Ctrl Pts',(179.471502886441,0.625158727965406,
136.687991055259));
#141525=CARTESIAN_POINT('Ctrl Pts',(179.464102803926,0.781858464992578,
136.671341095798));
#141526=CARTESIAN_POINT('Ctrl Pts',(179.456702721411,0.937827620086148,
136.648433618271));
#141527=CARTESIAN_POINT('Ctrl Pts',(179.449302638896,1.09253522294258,136.619366838468));
#141528=CARTESIAN_POINT('Ctrl Pts',(179.44189441923,1.24741294271294,136.590268096752));
#141529=CARTESIAN_POINT('Ctrl Pts',(179.434486199563,1.40102597280012,136.554996596033));
#141530=CARTESIAN_POINT('Ctrl Pts',(179.427077979897,1.55285506812971,136.513701358832));
#141531=CARTESIAN_POINT('Ctrl Pts',(179.419665200595,1.70477761173422,136.472380705102));
#141532=CARTESIAN_POINT('Ctrl Pts',(179.412252421292,1.85491367752859,136.425029039235));
#141533=CARTESIAN_POINT('Ctrl Pts',(179.40483964199,2.0027618670726,136.371844381916));
#141534=CARTESIAN_POINT('Ctrl Pts',(179.397416270962,2.15082130904315,136.318583731865));
#141535=CARTESIAN_POINT('Ctrl Pts',(179.389992899933,2.29658600076753,136.259473584504));
#141536=CARTESIAN_POINT('Ctrl Pts',(179.382569528904,2.43957634407283,136.194759287789));
#141537=CARTESIAN_POINT('Ctrl Pts',(179.378633479463,2.51539325509978,136.160446214872));
#141538=CARTESIAN_POINT('Ctrl Pts',(179.374697430023,2.59043062670582,136.124558372525));
#141539=CARTESIAN_POINT('Ctrl Pts',(179.370761380582,2.66462016584161,136.087137343332));
#141540=CARTESIAN_POINT('Ctrl Pts',(179.363338114176,2.80453932127499,136.016562450144));
#141541=CARTESIAN_POINT('Ctrl Pts',(179.355914847771,2.94186425343108,135.940318170553));
#141542=CARTESIAN_POINT('Ctrl Pts',(179.348491581365,3.07610246214482,135.858618644704));
#141543=CARTESIAN_POINT('Ctrl Pts',(179.341077088644,3.21018201244378,135.777015680909));
#141544=CARTESIAN_POINT('Ctrl Pts',(179.333662595923,3.3411817853958,135.689970497116));
#141545=CARTESIAN_POINT('Ctrl Pts',(179.326248103202,3.46863133103027,135.597744313025));
#141546=CARTESIAN_POINT('Ctrl Pts',(179.318840756849,3.59595803599425,135.505607020003));
#141547=CARTESIAN_POINT('Ctrl Pts',(179.311433410495,3.71974102546335,135.408298885418));
#141548=CARTESIAN_POINT('Ctrl Pts',(179.304026064141,3.83953654645319,135.306125790357));
#141549=CARTESIAN_POINT('Ctrl Pts',(179.296624242466,3.95924271942392,135.204028899845));
#141550=CARTESIAN_POINT('Ctrl Pts',(179.28922242079,4.07496706275787,135.097074514833));
#141551=CARTESIAN_POINT('Ctrl Pts',(179.281820599115,4.18629689526787,134.985610295255));
#141552=CARTESIAN_POINT('Ctrl Pts',(179.274422684804,4.29756795762586,134.87420491677));
#141553=CARTESIAN_POINT('Ctrl Pts',(179.267024770492,4.40444886607418,134.758294708461));
#141554=CARTESIAN_POINT('Ctrl Pts',(179.259626856181,4.50656206760595,134.638265792882));
#141555=CARTESIAN_POINT('Ctrl Pts',(179.252230171269,4.6086582997761,134.518256823932));
#141556=CARTESIAN_POINT('Ctrl Pts',(179.244833486356,4.70598815587262,134.394130790199));
#141557=CARTESIAN_POINT('Ctrl Pts',(179.237436801444,4.79821276277581,134.266308746241));
#141558=CARTESIAN_POINT('Ctrl Pts',(179.230040444509,4.89043328034328,134.138492370046));
#141559=CARTESIAN_POINT('Ctrl Pts',(179.222644087573,4.97754878040159,134.006980612211));
#141560=CARTESIAN_POINT('Ctrl Pts',(179.215247730638,5.05926249069234,133.872225284199));
#141561=CARTESIAN_POINT('Ctrl Pts',(179.207850241301,5.14098871156078,133.737449324802));
#141562=CARTESIAN_POINT('Ctrl Pts',(179.200452751965,5.21731130237002,133.599429125651));
#141563=CARTESIAN_POINT('Ctrl Pts',(179.193055262628,5.28797848312044,133.45864284155));
#141564=CARTESIAN_POINT('Ctrl Pts',(179.185655180113,5.3586704361415,133.317807205035));
#141565=CARTESIAN_POINT('Ctrl Pts',(179.178255097598,5.42370286461153,133.174203886429));
#141566=CARTESIAN_POINT('Ctrl Pts',(179.170855015083,5.4828713978363,133.028332694119));
#141567=CARTESIAN_POINT('Ctrl Pts',(179.163446795416,5.54210499294605,132.882301101438));
#141568=CARTESIAN_POINT('Ctrl Pts',(179.15603857575,5.59546167541947,132.733997000985));
#141569=CARTESIAN_POINT('Ctrl Pts',(179.148630356084,5.64278615747782,132.583937798662));
#141570=CARTESIAN_POINT('Ctrl Pts',(179.141217576781,5.69013976696525,132.433786237403));
#141571=CARTESIAN_POINT('Ctrl Pts',(179.133804797479,5.73145368024142,132.281877781146));
#141572=CARTESIAN_POINT('Ctrl Pts',(179.126392018177,5.76662347961273,132.128741305616));
#141573=CARTESIAN_POINT('Ctrl Pts',(179.118968647149,5.80184353124267,131.975386021508));
#141574=CARTESIAN_POINT('Ctrl Pts',(179.11154527612,5.83090186655938,131.820799579596));
#141575=CARTESIAN_POINT('Ctrl Pts',(179.104121905091,5.85374566921849,131.665518095967));
#141576=CARTESIAN_POINT('Ctrl Pts',(179.10018585565,5.86585800151788,131.583184127419));
#141577=CARTESIAN_POINT('Ctrl Pts',(179.096249806209,5.87622407559727,131.50065480612));
#141578=CARTESIAN_POINT('Ctrl Pts',(179.092313756769,5.88484196200156,131.41801006535));
#141579=CARTESIAN_POINT('Ctrl Pts',(179.084890490363,5.90109502680501,131.262144663512));
#141580=CARTESIAN_POINT('Ctrl Pts',(179.077467223958,5.91117603521354,131.105397413357));
#141581=CARTESIAN_POINT('Ctrl Pts',(179.070043957552,5.91499894102585,130.948298417199));
#141582=CARTESIAN_POINT('Ctrl Pts',(179.062629464831,5.91881732848096,130.791385099008));
#141583=CARTESIAN_POINT('Ctrl Pts',(179.05521497211,5.91639232723587,130.63412123188));
#141584=CARTESIAN_POINT('Ctrl Pts',(179.047800479389,5.90768941912305,130.477043814329));
#141585=CARTESIAN_POINT('Ctrl Pts',(179.040393133036,5.89899489920073,130.320117793906));
#141586=CARTESIAN_POINT('Ctrl Pts',(179.032985786682,5.88403453903981,130.163378235523));
#141587=CARTESIAN_POINT('Ctrl Pts',(179.025578440328,5.8628258257359,130.007363817331));
#141588=CARTESIAN_POINT('Ctrl Pts',(179.018176618653,5.84163293069053,129.851465760579));
#141589=CARTESIAN_POINT('Ctrl Pts',(179.010774796977,5.81420101177123,129.696292135444));
#141590=CARTESIAN_POINT('Ctrl Pts',(179.003372975302,5.78059950086301,129.542378060982));
#141591=CARTESIAN_POINT('Ctrl Pts',(178.99597506099,5.74701572793086,129.388545236562));
#141592=CARTESIAN_POINT('Ctrl Pts',(178.988577146679,5.70726892866063,129.235971002404));
#141593=CARTESIAN_POINT('Ctrl Pts',(178.981179232368,5.66147988227038,129.08518171322));
#141594=CARTESIAN_POINT('Ctrl Pts',(178.973782547456,5.61569844518896,128.93441748248));
#141595=CARTESIAN_POINT('Ctrl Pts',(178.966385862543,5.56387686221214,128.785437964842));
#141596=CARTESIAN_POINT('Ctrl Pts',(178.958989177631,5.5061862092642,128.638755854132));
#141597=CARTESIAN_POINT('Ctrl Pts',(178.951592820696,5.44849811438028,128.49208024746));
#141598=CARTESIAN_POINT('Ctrl Pts',(178.94419646376,5.38494160360329,128.347702192559));
#141599=CARTESIAN_POINT('Ctrl Pts',(178.936800106825,5.31573638605803,128.206115587466));
#141600=CARTESIAN_POINT('Ctrl Pts',(178.929402617488,5.24652057301731,128.064507305103));
#141601=CARTESIAN_POINT('Ctrl Pts',(178.922005128152,5.17165449515218,127.925691658915));
#141602=CARTESIAN_POINT('Ctrl Pts',(178.914607638815,5.09140434440064,127.790138932899));
#141603=CARTESIAN_POINT('Ctrl Pts',(178.9072075563,5.01112606208312,127.654538689084));
#141604=CARTESIAN_POINT('Ctrl Pts',(178.899807473785,4.9254601391764,127.522203963786));
#141605=CARTESIAN_POINT('Ctrl Pts',(178.89240739127,4.8347166112795,127.393576858499));
#141606=CARTESIAN_POINT('Ctrl Pts',(178.884999171604,4.743873301545,127.264808314486));
#141607=CARTESIAN_POINT('Ctrl Pts',(178.877590951937,4.64794145183068,127.139755837558));
#141608=CARTESIAN_POINT('Ctrl Pts',(178.870182732271,4.54727243353588,127.018829746248));
#141609=CARTESIAN_POINT('Ctrl Pts',(178.862769952969,4.44654145513995,126.897829226946));
#141610=CARTESIAN_POINT('Ctrl Pts',(178.855357173667,4.34106774789423,126.780960430458));
#141611=CARTESIAN_POINT('Ctrl Pts',(178.847944394365,4.23123982961107,126.668597076596));
#141612=CARTESIAN_POINT('Ctrl Pts',(178.840521023336,4.12125498404791,126.556073172705));
#141613=CARTESIAN_POINT('Ctrl Pts',(178.833097652307,4.00690377237975,126.448067824391));
#141614=CARTESIAN_POINT('Ctrl Pts',(178.825674281278,3.88860869573101,126.344915251381));
#141615=CARTESIAN_POINT('Ctrl Pts',(178.821738231838,3.82588580763872,126.290221282058));
#141616=CARTESIAN_POINT('Ctrl Pts',(178.817802182397,3.76205466852198,126.236890896299));
#141617=CARTESIAN_POINT('Ctrl Pts',(178.813866132956,3.69718148559496,126.184968923298));
#141618=CARTESIAN_POINT('Ctrl Pts',(178.80644286655,3.57483268722024,126.08704570265));
#141619=CARTESIAN_POINT('Ctrl Pts',(178.799019600145,3.44840581763817,125.993838547293));
#141620=CARTESIAN_POINT('Ctrl Pts',(178.791596333739,3.31830035686659,125.905706383583));
#141621=CARTESIAN_POINT('Ctrl Pts',(178.784181841018,3.18834866994496,125.817678384771));
#141622=CARTESIAN_POINT('Ctrl Pts',(178.776767348297,3.05472735217882,125.734713645432));
#141623=CARTESIAN_POINT('Ctrl Pts',(178.769352855576,2.91786953771339,125.657131467491));
#141624=CARTESIAN_POINT('Ctrl Pts',(178.761945509222,2.7811436319621,125.579624066173));
#141625=CARTESIAN_POINT('Ctrl Pts',(178.754538162869,2.64118776230442,125.507489080993));
#141626=CARTESIAN_POINT('Ctrl Pts',(178.747130816515,2.49846458612938,125.441002968261));
#141627=CARTESIAN_POINT('Ctrl Pts',(178.73972899484,2.3558478582839,125.374566443381));
#141628=CARTESIAN_POINT('Ctrl Pts',(178.732327173164,2.2104682704742,125.313770558968));
#141629=CARTESIAN_POINT('Ctrl Pts',(178.724925351489,2.06281356314709,125.258846144932));
#141630=CARTESIAN_POINT('Ctrl Pts',(178.717527437177,1.91523680159044,125.203950725066));
#141631=CARTESIAN_POINT('Ctrl Pts',(178.710129522866,1.7653876613914,125.154920732585));
#141632=CARTESIAN_POINT('Ctrl Pts',(178.702731608555,1.61377426379196,125.11193906009));
#141633=CARTESIAN_POINT('Ctrl Pts',(178.695334923642,1.46218606158879,125.068964530368));
#141634=CARTESIAN_POINT('Ctrl Pts',(178.68793823873,1.30883454266877,125.03203642748));
#141635=CARTESIAN_POINT('Ctrl Pts',(178.680541553818,1.15424352158327,125.00128794394));
#141636=CARTESIAN_POINT('Ctrl Pts',(178.673145196882,0.999659355225655,
124.970540823821));
#141637=CARTESIAN_POINT('Ctrl Pts',(178.665748839947,0.84383616210872,124.945972851047));
#141638=CARTESIAN_POINT('Ctrl Pts',(178.658352483011,0.687308230788165,
124.927666142064));
#141639=CARTESIAN_POINT('Ctrl Pts',(178.650954993675,0.530756334641783,
124.909356630278));
#141640=CARTESIAN_POINT('Ctrl Pts',(178.643557504338,0.373499856248618,
124.897310334378));
#141641=CARTESIAN_POINT('Ctrl Pts',(178.636160015002,0.216078342097464,
124.891557499537));
#141642=CARTESIAN_POINT('Ctrl Pts',(178.628759932487,0.0586016440782505,
124.885802648048));
#141643=CARTESIAN_POINT('Ctrl Pts',(178.621359849972,-0.0990398320677371,
124.886345663696));
#141644=CARTESIAN_POINT('Ctrl Pts',(178.613959767457,-0.256306552017657,
124.893164671406));
#141645=CARTESIAN_POINT('Ctrl Pts',(178.60655154779,-0.413746202893404,
124.899991177317));
#141646=CARTESIAN_POINT('Ctrl Pts',(178.599143328124,-0.570809901440018,
124.913107441057));
#141647=CARTESIAN_POINT('Ctrl Pts',(178.591735108457,-0.726962510230612,
124.932439631107));
#141648=CARTESIAN_POINT('Ctrl Pts',(178.584322329155,-0.883211228346482,
124.951783719797));
#141649=CARTESIAN_POINT('Ctrl Pts',(178.576909549853,-1.0385473718329,124.977351297693));
#141650=CARTESIAN_POINT('Ctrl Pts',(178.569496770551,-1.19244651626097,
125.009017498444));
#141651=CARTESIAN_POINT('Ctrl Pts',(178.562073399522,-1.34656555900366,
125.040728945347));
#141652=CARTESIAN_POINT('Ctrl Pts',(178.554650028493,-1.49924314050149,
125.078556329378));
#141653=CARTESIAN_POINT('Ctrl Pts',(178.547226657465,-1.64996970005422,
125.1223248423));
#141654=CARTESIAN_POINT('Ctrl Pts',(178.543290608024,-1.72988853855967,
125.145531958061));
#141655=CARTESIAN_POINT('Ctrl Pts',(178.539354558583,-1.8092591923436,125.17040852702));
#141656=CARTESIAN_POINT('Ctrl Pts',(178.535418509143,-1.88800815871802,
125.196923078448));
#141657=CARTESIAN_POINT('Ctrl Pts',(178.527995242737,-2.0365262516354,125.246928694951));
#141658=CARTESIAN_POINT('Ctrl Pts',(178.520571976332,-2.18328088235783,
125.302914456743));
#141659=CARTESIAN_POINT('Ctrl Pts',(178.513148709927,-2.32775414726904,
125.364738278435));
#141660=CARTESIAN_POINT('Ctrl Pts',(178.505734217206,-2.47205665677897,
125.426489029504));
#141661=CARTESIAN_POINT('Ctrl Pts',(178.498319724485,-2.61408282780302,
125.494063960354));
#141662=CARTESIAN_POINT('Ctrl Pts',(178.490905231764,-2.7533299030029,125.567271253451));
#141663=CARTESIAN_POINT('Ctrl Pts',(178.48349788541,-2.89244276662918,125.640407986602));
#141664=CARTESIAN_POINT('Ctrl Pts',(178.476090539056,-3.02878153879216,
125.719166102016));
#141665=CARTESIAN_POINT('Ctrl Pts',(178.468683192702,-3.16186355134782,
125.803305784318));
#141666=CARTESIAN_POINT('Ctrl Pts',(178.461281371027,-3.29484630631761,
125.887382712069));
#141667=CARTESIAN_POINT('Ctrl Pts',(178.453879549352,-3.42457682400798,
125.97683301611));
#141668=CARTESIAN_POINT('Ctrl Pts',(178.446477727676,-3.55059726505351,
126.071371115793));
#141669=CARTESIAN_POINT('Ctrl Pts',(178.439079813365,-3.6765511808892,126.165859309549));
#141670=CARTESIAN_POINT('Ctrl Pts',(178.431681899054,-3.79879862271108,
126.265429726586));
#141671=CARTESIAN_POINT('Ctrl Pts',(178.424283984742,-3.91691106585152,
126.369753728031));
#141672=CARTESIAN_POINT('Ctrl Pts',(178.41688729983,-4.03500388084664,126.47406039272));
#141673=CARTESIAN_POINT('Ctrl Pts',(178.409490614918,-4.14896278146007,
126.583118827097));
#141674=CARTESIAN_POINT('Ctrl Pts',(178.402093930006,-4.25839257449629,
126.696560324955));
#141675=CARTESIAN_POINT('Ctrl Pts',(178.39469757307,-4.36781751530079,126.809996792698));
#141676=CARTESIAN_POINT('Ctrl Pts',(178.387301216135,-4.47271348866885,
126.927815668819));
#141677=CARTESIAN_POINT('Ctrl Pts',(178.379904859199,-4.57272261169512,
127.049611827168));
#141678=CARTESIAN_POINT('Ctrl Pts',(178.372507369863,-4.67274704637341,
127.171426632821));
#141679=CARTESIAN_POINT('Ctrl Pts',(178.365109880526,-4.76788290405682,
127.297219644647));
#141680=CARTESIAN_POINT('Ctrl Pts',(178.35771239119,-4.85781310057062,127.426553275158));
#141681=CARTESIAN_POINT('Ctrl Pts',(178.350312308675,-4.94777482197532,
127.555932243373));
#141682=CARTESIAN_POINT('Ctrl Pts',(178.34291222616,-5.03252703599572,127.688853995114));
#141683=CARTESIAN_POINT('Ctrl Pts',(178.335512143645,-5.11179651527014,
127.824852780863));
#141684=CARTESIAN_POINT('Ctrl Pts',(178.328103923978,-5.19115315948626,
127.961001111259));
#141685=CARTESIAN_POINT('Ctrl Pts',(178.320695704312,-5.26501484088846,
128.100232910055));
#141686=CARTESIAN_POINT('Ctrl Pts',(178.313287484645,-5.33315442117471,
128.242058043239));
#141687=CARTESIAN_POINT('Ctrl Pts',(178.305874705343,-5.40133594023571,
128.383970467425));
#141688=CARTESIAN_POINT('Ctrl Pts',(178.298461926041,-5.46378819269074,
128.528479064664));
#141689=CARTESIAN_POINT('Ctrl Pts',(178.291049146739,-5.52033276792493,
128.675075128517));
#141690=CARTESIAN_POINT('Ctrl Pts',(178.28362577571,-5.57695813669991,128.821880655701));
#141691=CARTESIAN_POINT('Ctrl Pts',(178.276202404682,-5.62765884934485,
128.970779254122));
#141692=CARTESIAN_POINT('Ctrl Pts',(178.268779033653,-5.67230654697386,
129.121247727812));
#141693=CARTESIAN_POINT('Ctrl Pts',(178.264842984212,-5.6959798275633,129.201029723002));
#141694=CARTESIAN_POINT('Ctrl Pts',(178.260906934771,-5.71795224266406,
129.281252895093));
#141695=CARTESIAN_POINT('Ctrl Pts',(178.256970885331,-5.73821053949377,
129.361838393494));
#141696=CARTESIAN_POINT('Ctrl Pts',(178.247172129819,-5.7886433657853,129.562455181598));
#141697=CARTESIAN_POINT('Ctrl Pts',(178.237373374307,-5.82857446158366,
129.765810079928));
#141698=CARTESIAN_POINT('Ctrl Pts',(178.227574618795,-5.85776135301345,
129.970956457724));
#141699=CARTESIAN_POINT('Ctrl Pts',(178.217994260588,-5.88629771913801,
130.171530477743));
#141700=CARTESIAN_POINT('Ctrl Pts',(178.208413902381,-5.90456354448022,
130.373817290485));
#141701=CARTESIAN_POINT('Ctrl Pts',(178.198833544173,-5.91237657174734,
130.576909883663));
#141702=CARTESIAN_POINT('Ctrl Pts',(178.195347434847,-5.91521958310837,
130.650811398403));
#141703=CARTESIAN_POINT('Ctrl Pts',(178.19186132552,-5.91667897563865,130.724819368428));
#141704=CARTESIAN_POINT('Ctrl Pts',(178.188375216193,-5.91674747022219,
130.798889226584));
#141705=CARTESIAN_POINT('',(176.438375192211,-5.90709253321605,130.805377784422));
#141706=CARTESIAN_POINT('Ctrl Pts',(178.188375192211,-5.91592736650928,
130.798890494443));
#141707=CARTESIAN_POINT('Ctrl Pts',(178.118424548647,-5.90234026736635,
132.284949550647));
#141708=CARTESIAN_POINT('Ctrl Pts',(177.955658030477,-4.58078385458697,
135.76435699672));
#141709=CARTESIAN_POINT('Ctrl Pts',(177.700075637705,1.26937439390032,137.686674848873));
#141710=CARTESIAN_POINT('Ctrl Pts',(177.421628013892,6.47641374616305,133.456458941318));
#141711=CARTESIAN_POINT('Ctrl Pts',(177.143180390079,5.73194525610269,126.789094236441));
#141712=CARTESIAN_POINT('Ctrl Pts',(176.864732766266,-0.279900903224888,
123.811563179148));
#141713=CARTESIAN_POINT('Ctrl Pts',(176.62979770031,-5.13526498310803,126.721178580489));
#141714=CARTESIAN_POINT('Ctrl Pts',(176.487678508958,-5.90548474499912,
129.754006561336));
#141715=CARTESIAN_POINT('Ctrl Pts',(176.438375192211,-5.90709253321605,
130.805377784422));
#141716=CARTESIAN_POINT('',(174.688376076494,-5.9186848337546,130.809462800912));
#141717=CARTESIAN_POINT('Ctrl Pts',(176.438375192211,-5.90709253321605,
130.805377784422));
#141718=CARTESIAN_POINT('Ctrl Pts',(176.394862634354,-5.90851148395661,
131.733263658879));
#141719=CARTESIAN_POINT('Ctrl Pts',(176.258534201893,-5.26482177762399,
134.63854442458));
#141720=CARTESIAN_POINT('Ctrl Pts',(176.029389894828,-0.715237544583954,
137.76611296774));
#141721=CARTESIAN_POINT('Ctrl Pts',(175.750942271015,5.47051605577885,135.169107415928));
#141722=CARTESIAN_POINT('Ctrl Pts',(175.472494647202,6.6291326504466,128.561112786155));
#141723=CARTESIAN_POINT('Ctrl Pts',(175.194047023389,1.69590019048836,124.0145533247));
#141724=CARTESIAN_POINT('Ctrl Pts',(174.932674316708,-4.3976998989599,125.603680783644));
#141725=CARTESIAN_POINT('Ctrl Pts',(174.764117484631,-5.9049897404614,129.202992274976));
#141726=CARTESIAN_POINT('Ctrl Pts',(174.688376527159,-5.91967202939123,
130.80945409654));
#141727=CARTESIAN_POINT('',(172.938373760814,-5.92088540128737,130.800975483928));
#141728=CARTESIAN_POINT('Ctrl Pts',(174.688375192211,-5.91674778536724,
130.809479880392));
#141729=CARTESIAN_POINT('Ctrl Pts',(174.677234495542,-5.91654344322708,
131.045654686463));
#141730=CARTESIAN_POINT('Ctrl Pts',(174.666093798872,-5.90219520381266,
131.281241271787));
#141731=CARTESIAN_POINT('Ctrl Pts',(174.654953102203,-5.8739315365935,131.514894829207));
#141732=CARTESIAN_POINT('Ctrl Pts',(174.649019326723,-5.85887769745775,
131.639343756504));
#141733=CARTESIAN_POINT('Ctrl Pts',(174.643085551242,-5.83987696246974,
131.763245004832));
#141734=CARTESIAN_POINT('Ctrl Pts',(174.637151775762,-5.81696862578434,
131.886398772688));
#141735=CARTESIAN_POINT('Ctrl Pts',(174.629728509357,-5.78830985925462,
132.040466487369));
#141736=CARTESIAN_POINT('Ctrl Pts',(174.622305242951,-5.7534825938637,132.193627803463));
#141737=CARTESIAN_POINT('Ctrl Pts',(174.614881976545,-5.71255479535126,
132.345349998649));
#141738=CARTESIAN_POINT('Ctrl Pts',(174.607467483824,-5.67167537009779,
132.496892870799));
#141739=CARTESIAN_POINT('Ctrl Pts',(174.600052991103,-5.6247098601858,132.64699965084));
#141740=CARTESIAN_POINT('Ctrl Pts',(174.592638498382,-5.57177759741108,
132.795145630441));
#141741=CARTESIAN_POINT('Ctrl Pts',(174.585231152028,-5.51889635274405,
132.94314882137));
#141742=CARTESIAN_POINT('Ctrl Pts',(174.577823805674,-5.46005992904419,
133.089194625093));
#141743=CARTESIAN_POINT('Ctrl Pts',(174.57041645932,-5.39543800101284,133.232771484723));
#141744=CARTESIAN_POINT('Ctrl Pts',(174.563014637645,-5.33086427045342,
133.376241259315));
#141745=CARTESIAN_POINT('Ctrl Pts',(174.555612815969,-5.26051377995737,
133.517245417411));
#141746=CARTESIAN_POINT('Ctrl Pts',(174.548210994294,-5.1846050020994,133.655290559656));
#141747=CARTESIAN_POINT('Ctrl Pts',(174.540813079983,-5.10873629589451,
133.793262828945));
#141748=CARTESIAN_POINT('Ctrl Pts',(174.533415165671,-5.0273153252958,133.928278866984));
#141749=CARTESIAN_POINT('Ctrl Pts',(174.52601725136,-4.94060731033035,134.059868253498));
#141750=CARTESIAN_POINT('Ctrl Pts',(174.518620566448,-4.85391370466393,
134.191435772243));
#141751=CARTESIAN_POINT('Ctrl Pts',(174.511223881535,-4.76193500360776,
134.31957745824));
#141752=CARTESIAN_POINT('Ctrl Pts',(174.503827196623,-4.66498077731926,
134.443850267193));
#141753=CARTESIAN_POINT('Ctrl Pts',(174.496430839688,-4.5680308500827,134.56811756576));
#141754=CARTESIAN_POINT('Ctrl Pts',(174.489034482753,-4.46610606590234,
134.688516034061));
#141755=CARTESIAN_POINT('Ctrl Pts',(174.481638125817,-4.35955729241333,
134.804634455276));
#141756=CARTESIAN_POINT('Ctrl Pts',(174.474240636481,-4.25299220603502,
134.920770654517));
#141757=CARTESIAN_POINT('Ctrl Pts',(174.466843147144,-4.14180197313662,
135.032625226841));
#141758=CARTESIAN_POINT('Ctrl Pts',(174.459445657808,-4.02637532920606,
135.139822792567));
#141759=CARTESIAN_POINT('Ctrl Pts',(174.452045575293,-3.91090822264448,
135.247057936233));
#141760=CARTESIAN_POINT('Ctrl Pts',(174.444645492778,-3.79120202165373,
135.349632569119));
#141761=CARTESIAN_POINT('Ctrl Pts',(174.437245410263,-3.6676795021956,135.447210780093));
#141762=CARTESIAN_POINT('Ctrl Pts',(174.429837190596,-3.54402115702884,
135.54489628834));
#141763=CARTESIAN_POINT('Ctrl Pts',(174.42242897093,-3.41653840594465,135.637574171094));
#141764=CARTESIAN_POINT('Ctrl Pts',(174.415020751264,-3.28568463866214,
135.724950726258));
#141765=CARTESIAN_POINT('Ctrl Pts',(174.407607971962,-3.15475033306937,
135.812381060234));
#141766=CARTESIAN_POINT('Ctrl Pts',(174.40019519266,-3.02044119471371,135.894503370643));
#141767=CARTESIAN_POINT('Ctrl Pts',(174.392782413358,-2.8832358430249,135.971069592919));
#141768=CARTESIAN_POINT('Ctrl Pts',(174.385359042329,-2.74583444589511,
136.047745216605));
#141769=CARTESIAN_POINT('Ctrl Pts',(174.3779356713,-2.60552890252608,136.118848728295));
#141770=CARTESIAN_POINT('Ctrl Pts',(174.370512300271,-2.462819205497,136.184179585109));
#141771=CARTESIAN_POINT('Ctrl Pts',(174.366576250831,-2.38715109986894,
136.21881957298));
#141772=CARTESIAN_POINT('Ctrl Pts',(174.362640201391,-2.31080738998295,
136.251837482137));
#141773=CARTESIAN_POINT('Ctrl Pts',(174.35870415195,-2.23386428477683,136.283209120646));
#141774=CARTESIAN_POINT('Ctrl Pts',(174.351280885545,-2.08875198965366,
136.342375051804));
#141775=CARTESIAN_POINT('Ctrl Pts',(174.34385761914,-1.94106804902361,136.395861319592));
#141776=CARTESIAN_POINT('Ctrl Pts',(174.336434352734,-1.79129739440587,
136.443437156087));
#141777=CARTESIAN_POINT('Ctrl Pts',(174.329019860013,-1.64170375626399,
136.490956761893));
#141778=CARTESIAN_POINT('Ctrl Pts',(174.321605367292,-1.49002866566799,
136.532579729446));
#141779=CARTESIAN_POINT('Ctrl Pts',(174.314190874571,-1.33677807634548,
136.568122838295));
#141780=CARTESIAN_POINT('Ctrl Pts',(174.306783528217,-1.18367519571074,
136.603631689358));
#141781=CARTESIAN_POINT('Ctrl Pts',(174.299376181864,-1.02900020063819,
136.633072264044));
#141782=CARTESIAN_POINT('Ctrl Pts',(174.29196883551,-0.873275191744421,
136.656310805493));
#141783=CARTESIAN_POINT('Ctrl Pts',(174.284567013834,-0.717666328437618,
136.679532014762));
#141784=CARTESIAN_POINT('Ctrl Pts',(174.277165192159,-0.561009378267391,
136.696560346347));
#141785=CARTESIAN_POINT('Ctrl Pts',(174.269763370484,-0.403837541848953,
136.70731291301));
#141786=CARTESIAN_POINT('Ctrl Pts',(174.262365456172,-0.246748675219313,
136.718059803478));
#141787=CARTESIAN_POINT('Ctrl Pts',(174.254967541861,-0.0891458351376757,
136.722537501462));
#141788=CARTESIAN_POINT('Ctrl Pts',(174.247569627549,0.0684318425907609,
136.720714870433));
#141789=CARTESIAN_POINT('Ctrl Pts',(174.240172942637,0.225983333767741,
136.718892542293));
#141790=CARTESIAN_POINT('Ctrl Pts',(174.232776257725,0.383509297983157,
136.710771967438));
#141791=CARTESIAN_POINT('Ctrl Pts',(174.225379572813,0.540469659291495,
136.696374119747));
#141792=CARTESIAN_POINT('Ctrl Pts',(174.217983215877,0.69742306081293,136.681976910472));
#141793=CARTESIAN_POINT('Ctrl Pts',(174.210586858942,0.853810537556758,
136.661303015894));
#141794=CARTESIAN_POINT('Ctrl Pts',(174.203190502006,1.00909646863808,136.634425358157));
#141795=CARTESIAN_POINT('Ctrl Pts',(174.195793012669,1.16440617439188,136.607543585382));
#141796=CARTESIAN_POINT('Ctrl Pts',(174.188395523333,1.31861363082728,136.574456221915));
#141797=CARTESIAN_POINT('Ctrl Pts',(174.180998033996,1.47119289936138,136.535287420045));
#141798=CARTESIAN_POINT('Ctrl Pts',(174.173597951481,1.62382565432149,136.496104887612));
#141799=CARTESIAN_POINT('Ctrl Pts',(174.166197868966,1.77482872365539,136.450836765063));
#141800=CARTESIAN_POINT('Ctrl Pts',(174.158797786451,1.92369097507765,136.399657177616));
#141801=CARTESIAN_POINT('Ctrl Pts',(174.151389566784,2.07271691584888,136.34842131295));
#141802=CARTESIAN_POINT('Ctrl Pts',(174.143981347118,2.21959698428384,136.291261123376));
#141803=CARTESIAN_POINT('Ctrl Pts',(174.136573127451,2.36383901227271,136.228399305348));
#141804=CARTESIAN_POINT('Ctrl Pts',(174.129160348149,2.5081698188232,136.16549879692));
#141805=CARTESIAN_POINT('Ctrl Pts',(174.121747568847,2.64985901435945,136.096889829714));
#141806=CARTESIAN_POINT('Ctrl Pts',(174.114334789545,2.78843918964349,136.022840994856));
#141807=CARTESIAN_POINT('Ctrl Pts',(174.106911418516,2.9272173747806,135.94868635555));
#141808=CARTESIAN_POINT('Ctrl Pts',(174.099488047487,3.0628773462658,135.869076513123));
#141809=CARTESIAN_POINT('Ctrl Pts',(174.092064676459,3.1949801234916,135.784323727168));
#141810=CARTESIAN_POINT('Ctrl Pts',(174.088128627018,3.26502418573835,135.73938576644));
#141811=CARTESIAN_POINT('Ctrl Pts',(174.084192577577,3.33406872782739,135.693002627549));
#141812=CARTESIAN_POINT('Ctrl Pts',(174.080256528136,3.40205220360581,135.6452253509));
#141813=CARTESIAN_POINT('Ctrl Pts',(174.072833261731,3.53026691723385,135.555118898219));
#141814=CARTESIAN_POINT('Ctrl Pts',(174.065409995325,3.65509320642557,135.459778850555));
#141815=CARTESIAN_POINT('Ctrl Pts',(174.05798672892,3.77607480225818,135.359488458829));
#141816=CARTESIAN_POINT('Ctrl Pts',(174.050572236199,3.89691340789153,135.259316602018));
#141817=CARTESIAN_POINT('Ctrl Pts',(174.043157743478,4.01391608065393,135.154206283297));
#141818=CARTESIAN_POINT('Ctrl Pts',(174.035743250757,4.12665519164441,135.04448414074));
#141819=CARTESIAN_POINT('Ctrl Pts',(174.028335904403,4.23928564043516,134.934867752515));
#141820=CARTESIAN_POINT('Ctrl Pts',(174.020928558049,4.34766044270246,134.820648648281));
#141821=CARTESIAN_POINT('Ctrl Pts',(174.013521211696,4.45138485687511,134.702193787224));
#141822=CARTESIAN_POINT('Ctrl Pts',(174.00611939002,4.55503190946633,134.583827274271));
#141823=CARTESIAN_POINT('Ctrl Pts',(173.998717568345,4.65403523522225,134.461231574499));
#141824=CARTESIAN_POINT('Ctrl Pts',(173.991315746669,4.7480368908042,134.334810482111));
#141825=CARTESIAN_POINT('Ctrl Pts',(173.983917832358,4.84198892364395,134.208456126432));
#141826=CARTESIAN_POINT('Ctrl Pts',(173.976519918047,4.93094432250053,134.078280698662));
#141827=CARTESIAN_POINT('Ctrl Pts',(173.969122003735,5.01458547525733,133.944720958966));
#141828=CARTESIAN_POINT('Ctrl Pts',(173.961725318823,5.09821272837186,133.811183414476));
#141829=CARTESIAN_POINT('Ctrl Pts',(173.954328633911,5.17652729020417,133.67426299035));
#141830=CARTESIAN_POINT('Ctrl Pts',(173.946931948999,5.24925488243041,133.534425404669));
#141831=CARTESIAN_POINT('Ctrl Pts',(173.939535592063,5.321979249839,133.394594019533));
#141832=CARTESIAN_POINT('Ctrl Pts',(173.932139235128,5.38911696797228,133.251846061218));
#141833=CARTESIAN_POINT('Ctrl Pts',(173.924742878193,5.4504398721223,133.106671578944));
#141834=CARTESIAN_POINT('Ctrl Pts',(173.917345388856,5.51177216496549,132.961474870085));
#141835=CARTESIAN_POINT('Ctrl Pts',(173.909947899519,5.56728772592756,132.813851241446));
#141836=CARTESIAN_POINT('Ctrl Pts',(173.902550410183,5.61680672519481,132.664310287398));
#141837=CARTESIAN_POINT('Ctrl Pts',(173.895150327668,5.6663430832705,132.514716911999));
#141838=CARTESIAN_POINT('Ctrl Pts',(173.887750245153,5.70987857714054,132.363205227167));
#141839=CARTESIAN_POINT('Ctrl Pts',(173.880350162638,5.747283423796,132.210299381901));
#141840=CARTESIAN_POINT('Ctrl Pts',(173.872941942972,5.78472940092567,132.057225400939));
#141841=CARTESIAN_POINT('Ctrl Pts',(173.865533723305,5.81603117931075,131.902754560826));
#141842=CARTESIAN_POINT('Ctrl Pts',(173.858125503639,5.84111009089988,131.747421309403));
#141843=CARTESIAN_POINT('Ctrl Pts',(173.850712724337,5.86620443814064,131.591992452956));
#141844=CARTESIAN_POINT('Ctrl Pts',(173.843299945035,5.88506824206225,131.435700497263));
#141845=CARTESIAN_POINT('Ctrl Pts',(173.835887165733,5.89767482987402,131.279083867018));
#141846=CARTESIAN_POINT('Ctrl Pts',(173.828463794704,5.91029943056965,131.122243455587));
#141847=CARTESIAN_POINT('Ctrl Pts',(173.821040423675,5.91664894373514,130.965077815077));
#141848=CARTESIAN_POINT('Ctrl Pts',(173.813617052647,5.91674880246757,130.808125056241));
#141849=CARTESIAN_POINT('Ctrl Pts',(173.809681003206,5.91680174996359,130.724904937476));
#141850=CARTESIAN_POINT('Ctrl Pts',(173.805744953765,5.91509856308171,130.64174458923));
#141851=CARTESIAN_POINT('Ctrl Pts',(173.801808904324,5.91164891636172,130.55872338061));
#141852=CARTESIAN_POINT('Ctrl Pts',(173.794385637919,5.90514299030768,130.402147972159));
#141853=CARTESIAN_POINT('Ctrl Pts',(173.786962371513,5.89240236639736,130.245594455225));
#141854=CARTESIAN_POINT('Ctrl Pts',(173.779539105108,5.87341872715443,130.089599805817));
#141855=CARTESIAN_POINT('Ctrl Pts',(173.772124612387,5.85445752499658,129.933789529131));
#141856=CARTESIAN_POINT('Ctrl Pts',(173.764710119666,5.82926803955538,129.778537172117));
#141857=CARTESIAN_POINT('Ctrl Pts',(173.757295626945,5.79789393682564,129.624379066939));
#141858=CARTESIAN_POINT('Ctrl Pts',(173.749888280591,5.76655007363732,129.470369545146));
#141859=CARTESIAN_POINT('Ctrl Pts',(173.742480934237,5.72903353421945,129.31745253887));
#141860=CARTESIAN_POINT('Ctrl Pts',(173.735073587884,5.68543968426595,129.166158505776));
#141861=CARTESIAN_POINT('Ctrl Pts',(173.727671766208,5.64187834825044,129.01497731348));
#141862=CARTESIAN_POINT('Ctrl Pts',(173.720269944533,5.59224882980388,128.865417041309));
#141863=CARTESIAN_POINT('Ctrl Pts',(173.712868122858,5.53669737530587,128.717997097759));
#141864=CARTESIAN_POINT('Ctrl Pts',(173.705470208546,5.4811752459883,128.57065497605));
#141865=CARTESIAN_POINT('Ctrl Pts',(173.698072294235,5.41973753778378,128.425451281223));
#141866=CARTESIAN_POINT('Ctrl Pts',(173.690674379924,5.35258003228326,128.282889308885));
#141867=CARTESIAN_POINT('Ctrl Pts',(173.683277695011,5.28543368714182,128.14035102776));
#141868=CARTESIAN_POINT('Ctrl Pts',(173.675881010099,5.21256959014646,128.000453935199));
#141869=CARTESIAN_POINT('Ctrl Pts',(173.668484325187,5.13423130897537,127.863680521323));
#141870=CARTESIAN_POINT('Ctrl Pts',(173.661087968252,5.05589650140576,127.726913172124));
#141871=CARTESIAN_POINT('Ctrl Pts',(173.653691611316,4.97208817782416,127.593269550138));
#141872=CARTESIAN_POINT('Ctrl Pts',(173.646295254381,4.88309530191968,127.463206500368));
#141873=CARTESIAN_POINT('Ctrl Pts',(173.638897765044,4.79408880097865,127.333123537613));
#141874=CARTESIAN_POINT('Ctrl Pts',(173.631500275708,4.69989637802937,127.206622546706));
#141875=CARTESIAN_POINT('Ctrl Pts',(173.624102786371,4.60084956684095,127.084130271768));
#141876=CARTESIAN_POINT('Ctrl Pts',(173.616702703856,4.50176803494637,126.961595057352));
#141877=CARTESIAN_POINT('Ctrl Pts',(173.609302621341,4.39782896131317,126.843071646839));
#141878=CARTESIAN_POINT('Ctrl Pts',(173.601902538826,4.28940317645384,126.728952545688));
#141879=CARTESIAN_POINT('Ctrl Pts',(173.59449431916,4.18085816629766,126.614707958854));
#141880=CARTESIAN_POINT('Ctrl Pts',(173.587086099493,4.06781684947402,126.504877623945));
#141881=CARTESIAN_POINT('Ctrl Pts',(173.579677879827,3.95068635008608,126.399816608733));
#141882=CARTESIAN_POINT('Ctrl Pts',(173.572265100525,3.83348375883016,126.29469093022));
#141883=CARTESIAN_POINT('Ctrl Pts',(173.564852321222,3.71218725688151,126.194340658035));
#141884=CARTESIAN_POINT('Ctrl Pts',(173.55743954192,3.5872354188883,126.099079264451));
#141885=CARTESIAN_POINT('Ctrl Pts',(173.550016170892,3.46210504384931,126.00368175692));
#141886=CARTESIAN_POINT('Ctrl Pts',(173.542592799863,3.33330920628706,125.913387863986));
#141887=CARTESIAN_POINT('Ctrl Pts',(173.535169428834,3.20131438122949,125.828467050071));
#141888=CARTESIAN_POINT('Ctrl Pts',(173.531233379393,3.13132755781107,125.783439996887));
#141889=CARTESIAN_POINT('Ctrl Pts',(173.527297329953,3.06044178749597,125.739922736716));
#141890=CARTESIAN_POINT('Ctrl Pts',(173.523361280512,2.98872907508726,125.697950031036));
#141891=CARTESIAN_POINT('Ctrl Pts',(173.515938014106,2.85348113756254,125.618790818047));
#141892=CARTESIAN_POINT('Ctrl Pts',(173.508514747701,2.71488161150959,125.544888865841));
#141893=CARTESIAN_POINT('Ctrl Pts',(173.501091481295,2.57337777425295,125.476541420795));
#141894=CARTESIAN_POINT('Ctrl Pts',(173.493676988574,2.43204118278068,125.408274756753));
#141895=CARTESIAN_POINT('Ctrl Pts',(173.486262495853,2.28780744568151,125.345549693042));
#141896=CARTESIAN_POINT('Ctrl Pts',(173.478848003132,2.14115139693,125.28861939286));
#141897=CARTESIAN_POINT('Ctrl Pts',(173.471440656779,1.99463670079973,125.231743964244));
#141898=CARTESIAN_POINT('Ctrl Pts',(173.464033310425,1.84570468663678,125.180652314282));
#141899=CARTESIAN_POINT('Ctrl Pts',(173.456625964071,1.69485319098633,125.13555093444));
#141900=CARTESIAN_POINT('Ctrl Pts',(173.449224142396,1.54411420607265,125.090483192909));
#141901=CARTESIAN_POINT('Ctrl Pts',(173.44182232072,1.3914589463391,125.051396932038));
#141902=CARTESIAN_POINT('Ctrl Pts',(173.434420499045,1.23740345460525,125.018449863585));
#141903=CARTESIAN_POINT('Ctrl Pts',(173.427022584733,1.08342928756632,124.985520187633));
#141904=CARTESIAN_POINT('Ctrl Pts',(173.419624670422,0.928056724741681,
124.958723327701));
#141905=CARTESIAN_POINT('Ctrl Pts',(173.412226756111,0.771815027712196,
124.938166610759));
#141906=CARTESIAN_POINT('Ctrl Pts',(173.404830071199,0.615599295218299,
124.917613309971));
#141907=CARTESIAN_POINT('Ctrl Pts',(173.397433386286,0.45851508492483,124.903298142686));
#141908=CARTESIAN_POINT('Ctrl Pts',(173.390036701374,0.301099983714709,
124.895276986214));
#141909=CARTESIAN_POINT('Ctrl Pts',(173.382640344439,0.143691862455135,
124.887256185409));
#141910=CARTESIAN_POINT('Ctrl Pts',(173.375243987503,-0.0140467477342156,
124.885528859503));
#141911=CARTESIAN_POINT('Ctrl Pts',(173.367847630568,-0.171575298280786,
124.890098831044));
#141912=CARTESIAN_POINT('Ctrl Pts',(173.360450141231,-0.329127966850539,
124.894669502258));
#141913=CARTESIAN_POINT('Ctrl Pts',(173.353052651895,-0.486470138576459,
124.90553937981));
#141914=CARTESIAN_POINT('Ctrl Pts',(173.345655162558,-0.643063579444112,
124.92266020057));
#141915=CARTESIAN_POINT('Ctrl Pts',(173.338255080043,-0.799711913899935,
124.939787023007));
#141916=CARTESIAN_POINT('Ctrl Pts',(173.330854997528,-0.955610624073656,
124.963169110885));
#141917=CARTESIAN_POINT('Ctrl Pts',(173.323454915013,-1.11022904105624,
124.992706632779));
#141918=CARTESIAN_POINT('Ctrl Pts',(173.316046695347,-1.26501747688335,
125.022276634214));
#141919=CARTESIAN_POINT('Ctrl Pts',(173.30863847568,-1.41852244113016,125.058015516781));
#141920=CARTESIAN_POINT('Ctrl Pts',(173.301230256014,-1.57022514470069,
125.099772678245));
#141921=CARTESIAN_POINT('Ctrl Pts',(173.293817476711,-1.72202121875402,
125.141555540544));
#141922=CARTESIAN_POINT('Ctrl Pts',(173.286404697409,-1.87201246694569,
125.189363949622));
#141923=CARTESIAN_POINT('Ctrl Pts',(173.278991918107,-2.01969809586478,
125.242998359624));
#141924=CARTESIAN_POINT('Ctrl Pts',(173.271568547079,-2.16759474493629,
125.296709404987));
#141925=CARTESIAN_POINT('Ctrl Pts',(173.26414517605,-2.31317885053309,125.356262936134));
#141926=CARTESIAN_POINT('Ctrl Pts',(173.256721805021,-2.45597156345851,
125.421412146516));
#141927=CARTESIAN_POINT('Ctrl Pts',(173.25278575558,-2.53168368611545,125.455955821094));
#141928=CARTESIAN_POINT('Ctrl Pts',(173.248849706139,-2.60661147990583,
125.492071885158));
#141929=CARTESIAN_POINT('Ctrl Pts',(173.244913656699,-2.68068677865969,
125.529718548457));
#141930=CARTESIAN_POINT('Ctrl Pts',(173.237490390293,-2.82039048029919,
125.600718980525));
#141931=CARTESIAN_POINT('Ctrl Pts',(173.230067123888,-2.95748271501561,
125.677380876813));
#141932=CARTESIAN_POINT('Ctrl Pts',(173.222643857482,-3.09147163669408,
125.759488599168));
#141933=CARTESIAN_POINT('Ctrl Pts',(173.215229364761,-3.22530219459432,
125.841499277013));
#141934=CARTESIAN_POINT('Ctrl Pts',(173.20781487204,-3.35603642516729,125.928942775866));
#141935=CARTESIAN_POINT('Ctrl Pts',(173.200400379319,-3.4832046756844,126.021556445348));
#141936=CARTESIAN_POINT('Ctrl Pts',(173.192993032965,-3.61025035665381,
126.114080850287));
#141937=CARTESIAN_POINT('Ctrl Pts',(173.185585686612,-3.73373660027955,
126.211765286989));
#141938=CARTESIAN_POINT('Ctrl Pts',(173.178178340258,-3.8532205866295,126.31430252515));
#141939=CARTESIAN_POINT('Ctrl Pts',(173.170776518582,-3.97261545731455,
126.416763287169));
#141940=CARTESIAN_POINT('Ctrl Pts',(173.163374696907,-4.08801373226404,
126.524069401869));
#141941=CARTESIAN_POINT('Ctrl Pts',(173.155972875232,-4.19900379035953,
126.635871954867));
#141942=CARTESIAN_POINT('Ctrl Pts',(173.14857496092,-4.30993525766733,126.747615488169));
#141943=CARTESIAN_POINT('Ctrl Pts',(173.141177046609,-4.41646288024796,
126.863850468309));
#141944=CARTESIAN_POINT('Ctrl Pts',(173.133779132297,-4.51821028206757,
126.984189625383));
#141945=CARTESIAN_POINT('Ctrl Pts',(173.126382447385,-4.61994077531485,
127.104508784271));
#141946=CARTESIAN_POINT('Ctrl Pts',(173.118985762473,-4.71689238363702,
127.228930481662));
#141947=CARTESIAN_POINT('Ctrl Pts',(173.111589077561,-4.80872751702927,
127.357032633538));
#141948=CARTESIAN_POINT('Ctrl Pts',(173.104192720625,-4.90055857835549,
127.485129105229));
#141949=CARTESIAN_POINT('Ctrl Pts',(173.09679636369,-4.98727339834807,127.616905403527));
#141950=CARTESIAN_POINT('Ctrl Pts',(173.089400006754,-5.06857658128193,
127.751908815788));
#141951=CARTESIAN_POINT('Ctrl Pts',(173.082002517418,-5.14989221194058,
127.886932897415));
#141952=CARTESIAN_POINT('Ctrl Pts',(173.074605028081,-5.22579436321945,
128.025184756979));
#141953=CARTESIAN_POINT('Ctrl Pts',(173.067207538745,-5.29603271162384,
128.166185475558));
#141954=CARTESIAN_POINT('Ctrl Pts',(173.05980745623,-5.36629568197261,128.30723562172));
#141955=CARTESIAN_POINT('Ctrl Pts',(173.052407373714,-5.43089073011257,
128.451036211508));
#141956=CARTESIAN_POINT('Ctrl Pts',(173.045007291199,-5.48961500754095,
128.597086816815));
#141957=CARTESIAN_POINT('Ctrl Pts',(173.037599071533,-5.5484038583492,128.743298019777));
#141958=CARTESIAN_POINT('Ctrl Pts',(173.030190851866,-5.6013089070106,128.891763832682));
#141959=CARTESIAN_POINT('Ctrl Pts',(173.0227826322,-5.6481764412713,129.041966379387));
#141960=CARTESIAN_POINT('Ctrl Pts',(173.015369852898,-5.69507282171727,
129.192261373252));
#141961=CARTESIAN_POINT('Ctrl Pts',(173.007957073596,-5.73592418654342,
129.34429487122));
#141962=CARTESIAN_POINT('Ctrl Pts',(173.000544294294,-5.77062772825557,
129.497537682204));
#141963=CARTESIAN_POINT('Ctrl Pts',(172.993120923265,-5.80538085601562,
129.650999453703));
#141964=CARTESIAN_POINT('Ctrl Pts',(172.985697552236,-5.8339685487822,129.805673623159));
#141965=CARTESIAN_POINT('Ctrl Pts',(172.978274181207,-5.85633962220855,
129.961023916212));
#141966=CARTESIAN_POINT('Ctrl Pts',(172.974338131767,-5.86820130212529,
130.043394369165));
#141967=CARTESIAN_POINT('Ctrl Pts',(172.970402082326,-5.87831613732414,
130.125954858955));
#141968=CARTESIAN_POINT('Ctrl Pts',(172.966466032885,-5.88668244164833,
130.208625446799));
#141969=CARTESIAN_POINT('Ctrl Pts',(172.957102419327,-5.90658535236688,
130.40529356514));
#141970=CARTESIAN_POINT('Ctrl Pts',(172.947738805769,-5.91663481636451,
130.602975526734));
#141971=CARTESIAN_POINT('Ctrl Pts',(172.938375192211,-5.91674901559961,
130.800947568913));
#141972=CARTESIAN_POINT('',(171.188376356001,-5.9123977248154,130.800865364339));
#141973=CARTESIAN_POINT('Ctrl Pts',(172.938372658076,-5.92407204290102,
130.800996989454));
#141974=CARTESIAN_POINT('Ctrl Pts',(172.854921241741,-5.9119229449166,132.567576623035));
#141975=CARTESIAN_POINT('Ctrl Pts',(172.678653950803,-4.13412436784543,
136.320139871475));
#141976=CARTESIAN_POINT('Ctrl Pts',(172.40957078526,2.25333364517889,137.430071750254));
#141977=CARTESIAN_POINT('Ctrl Pts',(172.131123161447,6.79238030177618,132.489925913362));
#141978=CARTESIAN_POINT('Ctrl Pts',(171.852675537634,5.08956128726442,126.000827914072));
#141979=CARTESIAN_POINT('Ctrl Pts',(171.574227913821,-1.29031591135152,
123.925941803677));
#141980=CARTESIAN_POINT('Ctrl Pts',(171.352795156532,-5.42090502035294,
127.302567481839));
#141981=CARTESIAN_POINT('Ctrl Pts',(171.224178273849,-5.91304630517759,
130.038021817468));
#141982=CARTESIAN_POINT('Ctrl Pts',(171.188377265769,-5.90899622223902,
130.800847976222));
#141983=CARTESIAN_POINT('',(169.438373999605,-5.91358019339441,130.809073357389));
#141984=CARTESIAN_POINT('Ctrl Pts',(171.188375192211,-5.91674898070731,
130.800887607493));
#141985=CARTESIAN_POINT('Ctrl Pts',(171.18090496395,-5.91684253313628,130.960267000919));
#141986=CARTESIAN_POINT('Ctrl Pts',(171.173434735688,-5.9104919442183,131.119659794272));
#141987=CARTESIAN_POINT('Ctrl Pts',(171.165964507427,-5.89772060551839,
131.278514834824));
#141988=CARTESIAN_POINT('Ctrl Pts',(171.158493173355,-5.88494737628981,
131.437393390531));
#141989=CARTESIAN_POINT('Ctrl Pts',(171.151021839283,-5.86575153204893,
131.595733673016));
#141990=CARTESIAN_POINT('Ctrl Pts',(171.143550505211,-5.84020840133279,
131.752989307572));
#141991=CARTESIAN_POINT('Ctrl Pts',(171.136076702404,-5.81465683046071,
131.910296903733));
#141992=CARTESIAN_POINT('Ctrl Pts',(171.128602899596,-5.78275385258358,
132.066518779791));
#141993=CARTESIAN_POINT('Ctrl Pts',(171.121129096789,-5.74462599973562,
132.22111842526));
#141994=CARTESIAN_POINT('Ctrl Pts',(171.113651461089,-5.7064785932572,132.375797356188));
#141995=CARTESIAN_POINT('Ctrl Pts',(171.106173825389,-5.66210003830098,
132.528852047103));
#141996=CARTESIAN_POINT('Ctrl Pts',(171.098696189689,-5.61166682707188,
132.67976083737));
#141997=CARTESIAN_POINT('Ctrl Pts',(171.091208645838,-5.56116678992481,
132.830869587509));
#141998=CARTESIAN_POINT('Ctrl Pts',(171.083721101987,-5.50459618557524,
132.979826412699));
#141999=CARTESIAN_POINT('Ctrl Pts',(171.076233558136,-5.44218016527434,
133.126128394755));
#142000=CARTESIAN_POINT('Ctrl Pts',(171.068740561995,-5.37971869479419,
133.27253691118));
#142001=CARTESIAN_POINT('Ctrl Pts',(171.061247565855,-5.31140347855277,
133.416286403861));
#142002=CARTESIAN_POINT('Ctrl Pts',(171.053754569714,-5.23750565751984,
133.55689854645));
#142003=CARTESIAN_POINT('Ctrl Pts',(171.046249473471,-5.1634885022134,133.697737757276));
#142004=CARTESIAN_POINT('Ctrl Pts',(171.038744377227,-5.08387091193248,
133.83542918238));
#142005=CARTESIAN_POINT('Ctrl Pts',(171.031239280983,-4.99896796735605,
133.969522512927));
#142006=CARTESIAN_POINT('Ctrl Pts',(171.026603742721,-4.94652748752451,
134.05234553669));
#142007=CARTESIAN_POINT('Ctrl Pts',(171.021968204458,-4.89207150365022,
134.133796524639));
#142008=CARTESIAN_POINT('Ctrl Pts',(171.017332666195,-4.83568178337217,
134.213775853712));
#142009=CARTESIAN_POINT('Ctrl Pts',(171.00990939979,-4.74538031406421,134.341853292187));
#142010=CARTESIAN_POINT('Ctrl Pts',(171.002486133384,-4.64985041243972,
134.466534345509));
#142011=CARTESIAN_POINT('Ctrl Pts',(170.995062866979,-4.54937602345474,
134.587363176343));
#142012=CARTESIAN_POINT('Ctrl Pts',(170.987648374258,-4.44902038685363,
134.708049197534));
#142013=CARTESIAN_POINT('Ctrl Pts',(170.980233881537,-4.34373213169881,
134.824891774797));
#142014=CARTESIAN_POINT('Ctrl Pts',(170.972819388816,-4.23383854646287,
134.937463776814));
#142015=CARTESIAN_POINT('Ctrl Pts',(170.965412042462,-4.12405088080163,
135.049927277698));
#142016=CARTESIAN_POINT('Ctrl Pts',(170.958004696108,-4.0096669808313,135.158128132436));
#142017=CARTESIAN_POINT('Ctrl Pts',(170.950597349755,-3.89105440604151,
135.261672158363));
#142018=CARTESIAN_POINT('Ctrl Pts',(170.943195528079,-3.7725302969849,135.36513895725));
#142019=CARTESIAN_POINT('Ctrl Pts',(170.935793706404,-3.64978407296881,
135.463955598576));
#142020=CARTESIAN_POINT('Ctrl Pts',(170.928391884729,-3.52322007245554,
135.557764753924));
#142021=CARTESIAN_POINT('Ctrl Pts',(170.920993970417,-3.39672288409311,
135.651524388149));
#142022=CARTESIAN_POINT('Ctrl Pts',(170.913596056106,-3.26641223208966,
135.740281579155));
#142023=CARTESIAN_POINT('Ctrl Pts',(170.906198141795,-3.13272535945786,
135.823719379869));
#142024=CARTESIAN_POINT('Ctrl Pts',(170.898801456882,-2.99906070315902,
135.907143314734));
#142025=CARTESIAN_POINT('Ctrl Pts',(170.89140477197,-2.86202125615291,135.985249416302));
#142026=CARTESIAN_POINT('Ctrl Pts',(170.884008087058,-2.72207315338673,
136.05776411531));
#142027=CARTESIAN_POINT('Ctrl Pts',(170.876611730123,-2.58213125606608,
136.130275598941));
#142028=CARTESIAN_POINT('Ctrl Pts',(170.869215373187,-2.43928129087289,
136.197196001237));
#142029=CARTESIAN_POINT('Ctrl Pts',(170.861819016252,-2.2940136536867,136.258297903527));
#142030=CARTESIAN_POINT('Ctrl Pts',(170.854421526915,-2.14872377565441,
136.319409160675));
#142031=CARTESIAN_POINT('Ctrl Pts',(170.847024037579,-2.00101583272812,
136.374699999318));
#142032=CARTESIAN_POINT('Ctrl Pts',(170.839626548242,-1.85139969235813,
136.423991365368));
#142033=CARTESIAN_POINT('Ctrl Pts',(170.832226465727,-1.70173110428202,
136.473300010429));
#142034=CARTESIAN_POINT('Ctrl Pts',(170.824826383212,-1.55015334128703,
136.516604878893));
#142035=CARTESIAN_POINT('Ctrl Pts',(170.817426300697,-1.39719074927454,
136.553776985567));
#142036=CARTESIAN_POINT('Ctrl Pts',(170.810018081031,-1.24405995916715,
136.590989966794));
#142037=CARTESIAN_POINT('Ctrl Pts',(170.802609861364,-1.08954166194996,
136.622056630609));
#142038=CARTESIAN_POINT('Ctrl Pts',(170.795201641698,-0.934170424566269,
136.646899122391));
#142039=CARTESIAN_POINT('Ctrl Pts',(170.787788862396,-0.778703558778695,
136.671756904312));
#142040=CARTESIAN_POINT('Ctrl Pts',(170.780376083094,-0.622383076571657,
136.690382836639));
#142041=CARTESIAN_POINT('Ctrl Pts',(170.772963303792,-0.465747442605949,
136.702751066002));
#142042=CARTESIAN_POINT('Ctrl Pts',(170.765539932763,-0.30888800030067,
136.715136967672));
#142043=CARTESIAN_POINT('Ctrl Pts',(170.758116561734,-0.151712878907354,
136.721247294134));
#142044=CARTESIAN_POINT('Ctrl Pts',(170.750693190705,0.00523985014762619,
136.72110829737));
#142045=CARTESIAN_POINT('Ctrl Pts',(170.746757141265,0.0884599531236234,
136.721034597951));
#142046=CARTESIAN_POINT('Ctrl Pts',(170.742821091824,0.171617613112122,
136.719204857148));
#142047=CARTESIAN_POINT('Ctrl Pts',(170.738885042383,0.254633475820528,
136.715628870276));
#142048=CARTESIAN_POINT('Ctrl Pts',(170.731461775977,0.411198802048661,
136.708884670637));
#142049=CARTESIAN_POINT('Ctrl Pts',(170.724038509572,0.567732748635394,
136.695905813678));
#142050=CARTESIAN_POINT('Ctrl Pts',(170.716615243167,0.723698327536533,
136.676684799116));
#142051=CARTESIAN_POINT('Ctrl Pts',(170.709200750446,0.879479568075601,
136.657486502198));
#142052=CARTESIAN_POINT('Ctrl Pts',(170.701786257724,1.03469341120078,136.632060778267));
#142053=CARTESIAN_POINT('Ctrl Pts',(170.694371765003,1.18880359182316,136.600452109474));
#142054=CARTESIAN_POINT('Ctrl Pts',(170.68696441865,1.34276523525142,136.568873906306));
#142055=CARTESIAN_POINT('Ctrl Pts',(170.679557072296,1.4956249706662,136.531124696679));
#142056=CARTESIAN_POINT('Ctrl Pts',(170.672149725942,1.64685248614557,136.487300653443));
#142057=CARTESIAN_POINT('Ctrl Pts',(170.664747904267,1.79796721043819,136.443509295832));
#142058=CARTESIAN_POINT('Ctrl Pts',(170.657346082591,1.94745178174247,136.393652229581));
#142059=CARTESIAN_POINT('Ctrl Pts',(170.649944260916,2.09478701472477,136.337876491352));
#142060=CARTESIAN_POINT('Ctrl Pts',(170.642546346605,2.24204447058444,136.282130196701));
#142061=CARTESIAN_POINT('Ctrl Pts',(170.635148432293,2.3871544995349,136.220471584335));
#142062=CARTESIAN_POINT('Ctrl Pts',(170.627750517982,2.52961410449764,136.153097201548));
#142063=CARTESIAN_POINT('Ctrl Pts',(170.62035383307,2.67205003525861,136.085734015161));
#142064=CARTESIAN_POINT('Ctrl Pts',(170.612957148157,2.81183607906894,136.012657102981));
#142065=CARTESIAN_POINT('Ctrl Pts',(170.605560463245,2.94849011703518,135.934110766671));
#142066=CARTESIAN_POINT('Ctrl Pts',(170.59816410631,3.08513809561822,135.855567913188));
#142067=CARTESIAN_POINT('Ctrl Pts',(170.590767749374,3.21865402084596,135.771556303813));
#142068=CARTESIAN_POINT('Ctrl Pts',(170.583371392439,3.34858148799712,135.682365597139));
#142069=CARTESIAN_POINT('Ctrl Pts',(170.575973903102,3.47852884737482,135.593161235141));
#142070=CARTESIAN_POINT('Ctrl Pts',(170.568576413766,3.60488634696185,135.498776408292));
#142071=CARTESIAN_POINT('Ctrl Pts',(170.561178924429,3.72722774767048,135.399543299407));
#142072=CARTESIAN_POINT('Ctrl Pts',(170.553778841914,3.84961203496816,135.30027540451));
#142073=CARTESIAN_POINT('Ctrl Pts',(170.546378759399,3.96797713065668,135.196156078782));
#142074=CARTESIAN_POINT('Ctrl Pts',(170.538978676884,4.08193109407247,135.087556749632));
#142075=CARTESIAN_POINT('Ctrl Pts',(170.531570457217,4.1960103615853,134.978838004356));
#142076=CARTESIAN_POINT('Ctrl Pts',(170.524162237551,4.30566853967162,134.865629675359));
#142077=CARTESIAN_POINT('Ctrl Pts',(170.516754017884,4.41055118054293,134.748339426626));
#142078=CARTESIAN_POINT('Ctrl Pts',(170.509341238582,4.51549837492998,134.630976987701));
#142079=CARTESIAN_POINT('Ctrl Pts',(170.50192845928,4.61566393828353,134.50952791018));
#142080=CARTESIAN_POINT('Ctrl Pts',(170.494515679978,4.7107350661301,134.384431245254));
#142081=CARTESIAN_POINT('Ctrl Pts',(170.487092308949,4.80594203606249,134.259155836346));
#142082=CARTESIAN_POINT('Ctrl Pts',(170.479668937921,4.89603981909766,134.130222735993));
#142083=CARTESIAN_POINT('Ctrl Pts',(170.472245566892,4.98075966102131,133.99809882876));
#142084=CARTESIAN_POINT('Ctrl Pts',(170.468309517451,5.02568015403342,133.928043562877));
#142085=CARTESIAN_POINT('Ctrl Pts',(170.46437346801,5.06908948773575,133.857091648785));
#142086=CARTESIAN_POINT('Ctrl Pts',(170.46043741857,5.11095301027064,133.785315144107));
#142087=CARTESIAN_POINT('Ctrl Pts',(170.453014152164,5.18990630725628,133.649946896351));
#142088=CARTESIAN_POINT('Ctrl Pts',(170.445590885759,5.26359724900008,133.511235064603));
#142089=CARTESIAN_POINT('Ctrl Pts',(170.438167619353,5.33172927014896,133.369627378029));
#142090=CARTESIAN_POINT('Ctrl Pts',(170.430753126632,5.39978076490694,133.228187059981));
#142091=CARTESIAN_POINT('Ctrl Pts',(170.423338633911,5.46228625678789,133.083858033033));
#142092=CARTESIAN_POINT('Ctrl Pts',(170.41592414119,5.51899330550528,132.937115515881));
#142093=CARTESIAN_POINT('Ctrl Pts',(170.408516794837,5.57564569783404,132.790514434693));
#142094=CARTESIAN_POINT('Ctrl Pts',(170.401109448483,5.62651063945996,132.641504840197));
#142095=CARTESIAN_POINT('Ctrl Pts',(170.393702102129,5.6713823967779,132.490584882608));
#142096=CARTESIAN_POINT('Ctrl Pts',(170.386300280454,5.71622068704628,132.339777486818));
#142097=CARTESIAN_POINT('Ctrl Pts',(170.378898458778,5.75507458733743,132.187062921222));
#142098=CARTESIAN_POINT('Ctrl Pts',(170.371496637103,5.7877871714044,132.032957468053));
#142099=CARTESIAN_POINT('Ctrl Pts',(170.364098722792,5.82048248675273,131.878933365954));
#142100=CARTESIAN_POINT('Ctrl Pts',(170.35670080848,5.84704286506366,131.72352020279));
#142101=CARTESIAN_POINT('Ctrl Pts',(170.349302894169,5.8673617849352,131.567247402864));
#142102=CARTESIAN_POINT('Ctrl Pts',(170.341906209257,5.88767732817102,131.41100057264));
#142103=CARTESIAN_POINT('Ctrl Pts',(170.334509524345,5.90175342345177,131.253894759001));
#142104=CARTESIAN_POINT('Ctrl Pts',(170.327112839432,5.90953501164803,131.09646763324));
#142105=CARTESIAN_POINT('Ctrl Pts',(170.319716482497,5.91731625480052,130.939047487964));
#142106=CARTESIAN_POINT('Ctrl Pts',(170.312320125562,5.9188035273941,130.781306431737));
#142107=CARTESIAN_POINT('Ctrl Pts',(170.304923768626,5.91399382950801,130.623785018325));
#142108=CARTESIAN_POINT('Ctrl Pts',(170.29752627929,5.90918339524489,130.466239487983));
#142109=CARTESIAN_POINT('Ctrl Pts',(170.290128789953,5.89807408227965,130.30891404056));
#142110=CARTESIAN_POINT('Ctrl Pts',(170.282731300617,5.88071497278581,130.152346835999));
#142111=CARTESIAN_POINT('Ctrl Pts',(170.275331218102,5.86334977808317,129.995724747049));
#142112=CARTESIAN_POINT('Ctrl Pts',(170.267931135587,5.83973046598384,129.839861800962));
#142113=CARTESIAN_POINT('Ctrl Pts',(170.260531053072,5.80995767538453,129.685288514107));
#142114=CARTESIAN_POINT('Ctrl Pts',(170.253122833405,5.78015214654102,129.530545258031));
#142115=CARTESIAN_POINT('Ctrl Pts',(170.245714613739,5.74417969693544,129.377094860036));
#142116=CARTESIAN_POINT('Ctrl Pts',(170.238306394072,5.70219171813597,129.225455879426));
#142117=CARTESIAN_POINT('Ctrl Pts',(170.23089361477,5.66017789643608,129.073723567553));
#142118=CARTESIAN_POINT('Ctrl Pts',(170.223480835468,5.61214128157387,128.923805249309));
#142119=CARTESIAN_POINT('Ctrl Pts',(170.216068056166,5.55828218129294,128.776201413849));
#142120=CARTESIAN_POINT('Ctrl Pts',(170.208644685137,5.50434612460392,128.628386675108));
#142121=CARTESIAN_POINT('Ctrl Pts',(170.201221314109,5.44457110819336,128.482893368432));
#142122=CARTESIAN_POINT('Ctrl Pts',(170.19379794308,5.3792046670526,128.340199966866));
#142123=CARTESIAN_POINT('Ctrl Pts',(170.189861893639,5.34454581151123,128.264540501469));
#142124=CARTESIAN_POINT('Ctrl Pts',(170.185925844198,5.30831576191901,128.18966775694));
#142125=CARTESIAN_POINT('Ctrl Pts',(170.181989794757,5.27055641221757,128.115649835773));
#142126=CARTESIAN_POINT('Ctrl Pts',(170.174566528351,5.199343457114,127.976054346479));
#142127=CARTESIAN_POINT('Ctrl Pts',(170.167143261946,5.122473018555,127.839078936869));
#142128=CARTESIAN_POINT('Ctrl Pts',(170.15971999554,5.04016148295009,127.705215124323));
#142129=CARTESIAN_POINT('Ctrl Pts',(170.152305502819,4.95794723274491,127.571509527688));
#142130=CARTESIAN_POINT('Ctrl Pts',(170.144891010098,4.87030487990625,127.440908522623));
#142131=CARTESIAN_POINT('Ctrl Pts',(170.137476517377,4.77749778924088,127.313881361604));
#142132=CARTESIAN_POINT('Ctrl Pts',(170.130069171024,4.68478014954309,127.186976634145));
#142133=CARTESIAN_POINT('Ctrl Pts',(170.12266182467,4.58690790091625,127.063639192598));
#142134=CARTESIAN_POINT('Ctrl Pts',(170.115254478316,4.48418894720447,126.94431138883));
#142135=CARTESIAN_POINT('Ctrl Pts',(170.107852656641,4.38154660516425,126.82507258424));
#142136=CARTESIAN_POINT('Ctrl Pts',(170.100450834965,4.27406499819322,126.70983774456));
#142137=CARTESIAN_POINT('Ctrl Pts',(170.09304901329,4.16209366668581,126.599017959442));
#142138=CARTESIAN_POINT('Ctrl Pts',(170.085651098978,4.05018144397212,126.488256675227));
#142139=CARTESIAN_POINT('Ctrl Pts',(170.078253184667,3.93378448152172,126.381906065856));
#142140=CARTESIAN_POINT('Ctrl Pts',(170.070855270356,3.8132906215737,126.28034191757));
#142141=CARTESIAN_POINT('Ctrl Pts',(170.063458585443,3.69281678551975,126.178794647402));
#142142=CARTESIAN_POINT('Ctrl Pts',(170.056061900531,3.568247688363,126.082032499992));
#142143=CARTESIAN_POINT('Ctrl Pts',(170.048665215619,3.44000592738821,125.990392422611));
#142144=CARTESIAN_POINT('Ctrl Pts',(170.041268858683,3.31176985278735,125.898756408648));
#142145=CARTESIAN_POINT('Ctrl Pts',(170.033872501748,3.17986174189001,125.812242230164));
#142146=CARTESIAN_POINT('Ctrl Pts',(170.026476144812,3.04473475635657,125.731144593589));
#142147=CARTESIAN_POINT('Ctrl Pts',(170.019078655476,2.90958708253732,125.65003454076));
#142148=CARTESIAN_POINT('Ctrl Pts',(170.011681166139,2.77121987291441,125.574342873171));
#142149=CARTESIAN_POINT('Ctrl Pts',(170.004283676803,2.63011242680299,125.504319185192));
#142150=CARTESIAN_POINT('Ctrl Pts',(169.996883594288,2.48895551569434,125.434270950519));
#142151=CARTESIAN_POINT('Ctrl Pts',(169.989483511773,2.34505678975826,125.369894817197));
#142152=CARTESIAN_POINT('Ctrl Pts',(169.982083429258,2.19891698522216,125.31139287193));
#142153=CARTESIAN_POINT('Ctrl Pts',(169.974675209591,2.05261648494759,125.252826597759));
#142154=CARTESIAN_POINT('Ctrl Pts',(169.967266989925,1.90407033148488,125.200147550055));
#142155=CARTESIAN_POINT('Ctrl Pts',(169.959858770258,1.75379663430364,125.153508652773));
#142156=CARTESIAN_POINT('Ctrl Pts',(169.952445990956,1.60343044616849,125.106841050028));
#142157=CARTESIAN_POINT('Ctrl Pts',(169.945033211654,1.45133495542855,125.06622110161));
#142158=CARTESIAN_POINT('Ctrl Pts',(169.937620432352,1.29803950901369,125.031750809555));
#142159=CARTESIAN_POINT('Ctrl Pts',(169.930197061323,1.14452502687665,124.997231264731));
#142160=CARTESIAN_POINT('Ctrl Pts',(169.922773690294,0.989807530928758,
124.968878992825));
#142161=CARTESIAN_POINT('Ctrl Pts',(169.915350319265,0.834423372802704,
124.946744362004));
#142162=CARTESIAN_POINT('Ctrl Pts',(169.911414269825,0.752034963776186,
124.935008049631));
#142163=CARTESIAN_POINT('Ctrl Pts',(169.907478220384,0.669459176533651,
124.925018869156));
#142164=CARTESIAN_POINT('Ctrl Pts',(169.903542170944,0.586775952330272,
124.916778385082));
#142165=CARTESIAN_POINT('Ctrl Pts',(169.896118904538,0.430837971931043,
124.901237089293));
#142166=CARTESIAN_POINT('Ctrl Pts',(169.888695638133,0.274046330774959,
124.891871811632));
#142167=CARTESIAN_POINT('Ctrl Pts',(169.881272371727,0.116931518494834,
124.888766177234));
#142168=CARTESIAN_POINT('Ctrl Pts',(169.873857879006,-0.0399975971249745,
124.885664213438));
#142169=CARTESIAN_POINT('Ctrl Pts',(169.866443386285,-0.197248753992104,
124.888807173698));
#142170=CARTESIAN_POINT('Ctrl Pts',(169.859028893564,-0.354284801597808,
124.898227124166));
#142171=CARTESIAN_POINT('Ctrl Pts',(169.85162154721,-0.511169491949031,
124.907637995332));
#142172=CARTESIAN_POINT('Ctrl Pts',(169.844214200856,-0.667839115666281,
124.923313790147));
#142173=CARTESIAN_POINT('Ctrl Pts',(169.836806854503,-0.823755080046966,
124.945234562377));
#142174=CARTESIAN_POINT('Ctrl Pts',(169.829405032827,-0.979554756418378,
124.967138985267));
#142175=CARTESIAN_POINT('Ctrl Pts',(169.822003211152,-1.13460152461393,
124.995279059635));
#142176=CARTESIAN_POINT('Ctrl Pts',(169.814601389476,-1.28836058814432,
125.029582911245));
#142177=CARTESIAN_POINT('Ctrl Pts',(169.807203475165,-1.44203848346232,
125.06386865412));
#142178=CARTESIAN_POINT('Ctrl Pts',(169.799805560854,-1.59442966448984,
125.10431161304));
#142179=CARTESIAN_POINT('Ctrl Pts',(169.792407646542,-1.74500833341729,
125.150788606987));
#142180=CARTESIAN_POINT('Ctrl Pts',(169.78501096163,-1.8955619789013,125.1972578773));
#142181=CARTESIAN_POINT('Ctrl Pts',(169.777614276718,-2.04430335374695,
125.249759082496));
#142182=CARTESIAN_POINT('Ctrl Pts',(169.770217591806,-2.19072055051497,
125.308118807743));
#142183=CARTESIAN_POINT('Ctrl Pts',(169.76282123487,-2.33713125499116,125.366475945258));
#142184=CARTESIAN_POINT('Ctrl Pts',(169.755424877935,-2.48121763953383,
125.43069094809));
#142185=CARTESIAN_POINT('Ctrl Pts',(169.748028520999,-2.62248681432916,
125.500541854527));
#142186=CARTESIAN_POINT('Ctrl Pts',(169.740631031663,-2.76377761779588,
125.570403455315));
#142187=CARTESIAN_POINT('Ctrl Pts',(169.733233542326,-2.90225001804727,
125.64590251233));
#142188=CARTESIAN_POINT('Ctrl Pts',(169.725836052989,-3.03743495128211,
125.726770689339));
#142189=CARTESIAN_POINT('Ctrl Pts',(169.718435970474,-3.17266727338555,
125.807667214562));
#142190=CARTESIAN_POINT('Ctrl Pts',(169.711035887959,-3.30460951386572,
125.893936415581));
#142191=CARTESIAN_POINT('Ctrl Pts',(169.703635805444,-3.43282099129518,
125.985266241625));
#142192=CARTESIAN_POINT('Ctrl Pts',(169.696227585778,-3.56117345042462,
126.076696494202));
#142193=CARTESIAN_POINT('Ctrl Pts',(169.688819366111,-3.68578664959458,
126.173198268115));
#142194=CARTESIAN_POINT('Ctrl Pts',(169.681411146445,-3.80625187872553,
126.274418322327));
#142195=CARTESIAN_POINT('Ctrl Pts',(169.673998367143,-3.92679125219456,
126.375700675793));
#142196=CARTESIAN_POINT('Ctrl Pts',(169.666585587841,-4.0431772930982,126.481706845402));
#142197=CARTESIAN_POINT('Ctrl Pts',(169.659172808539,-4.15503805928876,
126.592046611184));
#142198=CARTESIAN_POINT('Ctrl Pts',(169.65174943751,-4.2670586573882,126.702544035598));
#142199=CARTESIAN_POINT('Ctrl Pts',(169.644326066481,-4.37454081246608,
126.817387151258));
#142200=CARTESIAN_POINT('Ctrl Pts',(169.636902695452,-4.47715223719654,
126.93615193557));
#142201=CARTESIAN_POINT('Ctrl Pts',(169.632966646012,-4.5315592767123,126.999123873931));
#142202=CARTESIAN_POINT('Ctrl Pts',(169.629030596571,-4.58459768718307,
127.063197826358));
#142203=CARTESIAN_POINT('Ctrl Pts',(169.625094547131,-4.63622294214824,
127.128307381662));
#142204=CARTESIAN_POINT('Ctrl Pts',(169.617314574009,-4.73826512990403,
127.257002561406));
#142205=CARTESIAN_POINT('Ctrl Pts',(169.609534600887,-4.83511364716786,
127.390162962955));
#142206=CARTESIAN_POINT('Ctrl Pts',(169.601754627766,-4.92635568212228,
127.527326858857));
#142207=CARTESIAN_POINT('Ctrl Pts',(169.594350421438,-5.0131907960697,127.657865842737));
#142208=CARTESIAN_POINT('Ctrl Pts',(169.586946215111,-5.09494797384064,
127.792030342425));
#142209=CARTESIAN_POINT('Ctrl Pts',(169.579542008784,-5.17131070252216,
127.929386499338));
#142210=CARTESIAN_POINT('Ctrl Pts',(169.572144764004,-5.24760163379818,
128.066613511892));
#142211=CARTESIAN_POINT('Ctrl Pts',(169.564747519225,-5.31850802957858,
128.207025885231));
#142212=CARTESIAN_POINT('Ctrl Pts',(169.557350274446,-5.38375627541832,
128.350160354875));
#142213=CARTESIAN_POINT('Ctrl Pts',(169.549958517475,-5.4489561154119,128.493188637064));
#142214=CARTESIAN_POINT('Ctrl Pts',(169.542566760505,-5.50850600673006,
128.638934657115));
#142215=CARTESIAN_POINT('Ctrl Pts',(169.535175003534,-5.56217803209591,
128.786910221207));
#142216=CARTESIAN_POINT('Ctrl Pts',(169.527787264386,-5.61582088379647,
128.93480535253));
#142217=CARTESIAN_POINT('Ctrl Pts',(169.520399525237,-5.66359210391255,
129.084927264337));
#142218=CARTESIAN_POINT('Ctrl Pts',(169.513011786088,-5.70531179041672,
129.236767578339));
#142219=CARTESIAN_POINT('Ctrl Pts',(169.505625960535,-5.74702067055978,
129.388568562198));
#142220=CARTESIAN_POINT('Ctrl Pts',(169.498240134981,-5.78268103618175,
129.542086702717));
#142221=CARTESIAN_POINT('Ctrl Pts',(169.490854309427,-5.81216278083217,
129.696798261936));
#142222=CARTESIAN_POINT('Ctrl Pts',(169.483469578459,-5.84164015626333,
129.851486892771));
#142223=CARTESIAN_POINT('Ctrl Pts',(169.476084847491,-5.86494066769169,
130.007368222288));
#142224=CARTESIAN_POINT('Ctrl Pts',(169.468700116523,-5.88198533934066,
130.163908409918));
#142225=CARTESIAN_POINT('Ctrl Pts',(169.461313667309,-5.89903397686634,
130.320485020607));
#142226=CARTESIAN_POINT('Ctrl Pts',(169.453927218095,-5.90982382871627,
130.477720423684));
#142227=CARTESIAN_POINT('Ctrl Pts',(169.446540768881,-5.91432778501902,
130.635075609807));
#142228=CARTESIAN_POINT('Ctrl Pts',(169.443818909991,-5.9159874638645,130.693059980898));
#142229=CARTESIAN_POINT('Ctrl Pts',(169.441097051101,-5.91679410654643,
130.751060598256));
#142230=CARTESIAN_POINT('Ctrl Pts',(169.438375192211,-5.91674814130737,
130.80905048279));
#142231=CARTESIAN_POINT('',(167.688376105063,-5.921848643152,130.805960821993));
#142232=CARTESIAN_POINT('Ctrl Pts',(169.438373164445,-5.91136173808653,
130.809089376048));
#142233=CARTESIAN_POINT('Ctrl Pts',(169.407797750736,-5.91615588573312,
131.459917301021));
#142234=CARTESIAN_POINT('Ctrl Pts',(169.284406462423,-5.51647731895877,
134.080691029829));
#142235=CARTESIAN_POINT('Ctrl Pts',(169.068199299504,-1.67522649738779,
137.599298197324));
#142236=CARTESIAN_POINT('Ctrl Pts',(168.789751675692,4.81127258696239,135.886605852133));
#142237=CARTESIAN_POINT('Ctrl Pts',(168.51130405188,6.87644720762614,129.50357841786));
#142238=CARTESIAN_POINT('Ctrl Pts',(168.232856428066,2.6225027776035,124.315906278371));
#142239=CARTESIAN_POINT('Ctrl Pts',(167.958547360081,-3.94234836512363,
125.079289384233));
#142240=CARTESIAN_POINT('Ctrl Pts',(167.777054166701,-5.91917198462181,
128.930354853733));
#142241=CARTESIAN_POINT('Ctrl Pts',(167.688376847924,-5.92599799601691,
130.805946244722));
#142242=CARTESIAN_POINT('',(165.938375192211,-5.91629100133431,130.79888781122));
#142243=CARTESIAN_POINT('Ctrl Pts',(167.688375192211,-5.91674977873797,
130.805978735034));
#142244=CARTESIAN_POINT('Ctrl Pts',(167.684237188288,-5.91672588056883,
130.893363915518));
#142245=CARTESIAN_POINT('Ctrl Pts',(167.680099184364,-5.91476617950728,
130.980720247118));
#142246=CARTESIAN_POINT('Ctrl Pts',(167.67596118044,-5.91087389875397,131.06798974253));
#142247=CARTESIAN_POINT('Ctrl Pts',(167.668537914035,-5.90389144115121,
131.224544623933));
#142248=CARTESIAN_POINT('Ctrl Pts',(167.66111464763,-5.89067438120114,131.381058637645));
#142249=CARTESIAN_POINT('Ctrl Pts',(167.653691381224,-5.8712160358362,131.536994784828));
#142250=CARTESIAN_POINT('Ctrl Pts',(167.646276888503,-5.85178068861954,
131.692746628435));
#142251=CARTESIAN_POINT('Ctrl Pts',(167.638862395782,-5.82611878508409,
131.847921598201));
#142252=CARTESIAN_POINT('Ctrl Pts',(167.631447903061,-5.79427562343302,
132.001983497353));
#142253=CARTESIAN_POINT('Ctrl Pts',(167.624040556707,-5.76246315341997,
132.155896905847));
#142254=CARTESIAN_POINT('Ctrl Pts',(167.616633210354,-5.72448136101022,
132.308699016381));
#142255=CARTESIAN_POINT('Ctrl Pts',(167.609225864,-5.6804272259866,132.459859664008));
#142256=CARTESIAN_POINT('Ctrl Pts',(167.601824042324,-5.63640594819903,
132.61090757032));
#142257=CARTESIAN_POINT('Ctrl Pts',(167.594422220649,-5.58632144961113,
132.760316094556));
#142258=CARTESIAN_POINT('Ctrl Pts',(167.587020398974,-5.53032155682588,
132.907566275748));
#142259=CARTESIAN_POINT('Ctrl Pts',(167.579622484662,-5.47435122594817,
133.054738724714));
#142260=CARTESIAN_POINT('Ctrl Pts',(167.572224570351,-5.41247185221993,
133.199754751718));
#142261=CARTESIAN_POINT('Ctrl Pts',(167.56482665604,-5.34488074818397,133.342111659373));
#142262=CARTESIAN_POINT('Ctrl Pts',(167.557429971127,-5.27730087656324,
133.484444909893));
#142263=CARTESIAN_POINT('Ctrl Pts',(167.550033286215,-5.2040113184423,133.624119581212));
#142264=CARTESIAN_POINT('Ctrl Pts',(167.542636601303,-5.12525710890511,
133.760653926782));
#142265=CARTESIAN_POINT('Ctrl Pts',(167.535240244368,-5.04650639141215,
133.897182218276));
#142266=CARTESIAN_POINT('Ctrl Pts',(167.527843887432,-4.96229169081128,
134.030570137526));
#142267=CARTESIAN_POINT('Ctrl Pts',(167.520447530497,-4.87290335993222,
134.160361721151));
#142268=CARTESIAN_POINT('Ctrl Pts',(167.51305004116,-4.78350134347127,134.290173176198));
#142269=CARTESIAN_POINT('Ctrl Pts',(167.505652551824,-4.68892433131307,
134.416386891826));
#142270=CARTESIAN_POINT('Ctrl Pts',(167.498255062487,-4.58950515455338,
134.538577134967));
#142271=CARTESIAN_POINT('Ctrl Pts',(167.490854979972,-4.49005112655565,
134.660810211707));
#142272=CARTESIAN_POINT('Ctrl Pts',(167.483454897457,-4.38575178987019,
134.779016718441));
#142273=CARTESIAN_POINT('Ctrl Pts',(167.476054814942,-4.27697916794346,
134.892805280207));
#142274=CARTESIAN_POINT('Ctrl Pts',(167.468646595276,-4.1680869393367,135.006718964195));
#142275=CARTESIAN_POINT('Ctrl Pts',(167.461238375609,-4.05471186035349,
135.116204731494));
#142276=CARTESIAN_POINT('Ctrl Pts',(167.453830155943,-3.9372621339154,135.22090875512));
#142277=CARTESIAN_POINT('Ctrl Pts',(167.446417376641,-3.81974011913044,
135.325677222327));
#142278=CARTESIAN_POINT('Ctrl Pts',(167.439004597339,-3.69813874730967,
135.425657844868));
#142279=CARTESIAN_POINT('Ctrl Pts',(167.431591818037,-3.57289754517158,
135.520538486795));
#142280=CARTESIAN_POINT('Ctrl Pts',(167.424168447008,-3.4474773925306,135.615554698633));
#142281=CARTESIAN_POINT('Ctrl Pts',(167.416745075979,-3.3184073279918,135.705456163106));
#142282=CARTESIAN_POINT('Ctrl Pts',(167.409321704951,-3.18615464457944,
135.78997483683));
#142283=CARTESIAN_POINT('Ctrl Pts',(167.40538565551,-3.11603109847216,135.834788665638));
#142284=CARTESIAN_POINT('Ctrl Pts',(167.401449606069,-3.0450132049226,135.878089972339));
#142285=CARTESIAN_POINT('Ctrl Pts',(167.397513556628,-2.97317307420229,
135.919844214777));
#142286=CARTESIAN_POINT('Ctrl Pts',(167.390090290222,-2.83768482972203,
135.998591412907));
#142287=CARTESIAN_POINT('Ctrl Pts',(167.382667023817,-2.69886101353126,
136.072071173523));
#142288=CARTESIAN_POINT('Ctrl Pts',(167.375243757411,-2.55714980559849,
136.139987612983));
#142289=CARTESIAN_POINT('Ctrl Pts',(167.36782926469,-2.41560608854492,136.207823780852));
#142290=CARTESIAN_POINT('Ctrl Pts',(167.360414771969,-2.27118210600901,
136.270109556143));
#142291=CARTESIAN_POINT('Ctrl Pts',(167.353000279248,-2.1243534603076,136.326593222064));
#142292=CARTESIAN_POINT('Ctrl Pts',(167.345592932895,-1.97766633358292,
136.383022446901));
#142293=CARTESIAN_POINT('Ctrl Pts',(167.338185586541,-1.8285795038551,136.433660562389));
#142294=CARTESIAN_POINT('Ctrl Pts',(167.330778240187,-1.67759143385237,
136.478302593262));
#142295=CARTESIAN_POINT('Ctrl Pts',(167.323376418512,-1.5267159764487,136.522911328424));
#142296=CARTESIAN_POINT('Ctrl Pts',(167.315974596836,-1.37394245867082,
136.561532778151));
#142297=CARTESIAN_POINT('Ctrl Pts',(167.308572775161,-1.21978740096834,
136.594010802071));
#142298=CARTESIAN_POINT('Ctrl Pts',(167.301174860849,-1.06571372052088,
136.626471681095));
#142299=CARTESIAN_POINT('Ctrl Pts',(167.293776946538,-0.910260316947344,
136.652795516271));
#142300=CARTESIAN_POINT('Ctrl Pts',(167.286379032227,-0.753956776043483,
136.672876592015));
#142301=CARTESIAN_POINT('Ctrl Pts',(167.278982347315,-0.597679209952597,
136.692954330647));
#142302=CARTESIAN_POINT('Ctrl Pts',(167.271585662402,-0.440552156817429,
136.706791321324));
#142303=CARTESIAN_POINT('Ctrl Pts',(167.26418897749,-0.283113371102142,
136.714333323222));
#142304=CARTESIAN_POINT('Ctrl Pts',(167.256792620555,-0.125681566387597,
136.721874990701));
#142305=CARTESIAN_POINT('Ctrl Pts',(167.249396263619,0.0320615705531974,
136.723122206536));
#142306=CARTESIAN_POINT('Ctrl Pts',(167.241999906684,0.189575482016936,
136.718072793443));
#142307=CARTESIAN_POINT('Ctrl Pts',(167.234602417347,0.347113509262802,
136.713022607272));
#142308=CARTESIAN_POINT('Ctrl Pts',(167.227204928011,0.504421868022577,
136.701673884621));
#142309=CARTESIAN_POINT('Ctrl Pts',(167.219807438674,0.660962473671266,
136.684076526596));
#142310=CARTESIAN_POINT('Ctrl Pts',(167.212407356159,0.817557954386651,
136.666472999844));
#142311=CARTESIAN_POINT('Ctrl Pts',(167.205007273644,0.97338477541586,136.642616518223));
#142312=CARTESIAN_POINT('Ctrl Pts',(167.197607191129,1.12791257416039,136.61260852787));
#142313=CARTESIAN_POINT('Ctrl Pts',(167.190198971462,1.28261029210532,136.582567540647));
#142314=CARTESIAN_POINT('Ctrl Pts',(167.182790751796,1.43600576846275,136.546361607312));
#142315=CARTESIAN_POINT('Ctrl Pts',(167.175382532129,1.58758067492107,136.504142908419));
#142316=CARTESIAN_POINT('Ctrl Pts',(167.167969752827,1.73924887320532,136.46189822462));
#142317=CARTESIAN_POINT('Ctrl Pts',(167.160556973525,1.88909391429604,136.413633515224));
#142318=CARTESIAN_POINT('Ctrl Pts',(167.153144194223,2.03661561445089,136.359549849399));
#142319=CARTESIAN_POINT('Ctrl Pts',(167.145720823194,2.18434810052894,136.305388906297));
#142320=CARTESIAN_POINT('Ctrl Pts',(167.138297452166,2.32975027132682,136.245392543059));
#142321=CARTESIAN_POINT('Ctrl Pts',(167.130874081137,2.47234403106011,136.179809022544));
#142322=CARTESIAN_POINT('Ctrl Pts',(167.126938031696,2.54795066396015,136.145035066313));
#142323=CARTESIAN_POINT('Ctrl Pts',(167.123001982255,2.62276818581389,136.108691115105));
#142324=CARTESIAN_POINT('Ctrl Pts',(167.119065932815,2.69672855796225,136.070819166455));
#142325=CARTESIAN_POINT('Ctrl Pts',(167.111642666409,2.83621551161134,135.999393853244));
#142326=CARTESIAN_POINT('Ctrl Pts',(167.104219400004,2.97307377888389,135.922315050444));
#142327=CARTESIAN_POINT('Ctrl Pts',(167.096796133598,3.10681217227156,135.83979989222));
#142328=CARTESIAN_POINT('Ctrl Pts',(167.089381640877,3.24039249798464,135.75738226006));
#142329=CARTESIAN_POINT('Ctrl Pts',(167.081967148156,3.3708599750741,135.669541256212));
#142330=CARTESIAN_POINT('Ctrl Pts',(167.074552655435,3.49774575240416,135.576540959301));
#142331=CARTESIAN_POINT('Ctrl Pts',(167.067145309082,3.6245092324449,135.483630299577));
#142332=CARTESIAN_POINT('Ctrl Pts',(167.059737962728,3.74769758626735,135.385570465694));
#142333=CARTESIAN_POINT('Ctrl Pts',(167.052330616374,3.86686893109385,135.282670034326));
#142334=CARTESIAN_POINT('Ctrl Pts',(167.044928794699,3.98595139343525,135.179846349981));
#142335=CARTESIAN_POINT('Ctrl Pts',(167.037526973023,4.10102253096623,135.072189499663));
#142336=CARTESIAN_POINT('Ctrl Pts',(167.030125151348,4.21167178645031,134.960049648968));
#142337=CARTESIAN_POINT('Ctrl Pts',(167.022727237036,4.32226263105375,134.847968996028));
#142338=CARTESIAN_POINT('Ctrl Pts',(167.015329322725,4.42843598090915,134.731410320841));
#142339=CARTESIAN_POINT('Ctrl Pts',(167.007931408414,4.52981664044239,134.610762037079));
#142340=CARTESIAN_POINT('Ctrl Pts',(167.000534723502,4.63118045234922,134.490133802873));
#142341=CARTESIAN_POINT('Ctrl Pts',(166.993138038589,4.72775291475044,134.365417594449));
#142342=CARTESIAN_POINT('Ctrl Pts',(166.985741353677,4.81919772388348,134.237036521379));
#142343=CARTESIAN_POINT('Ctrl Pts',(166.978344996742,4.91063847825786,134.108661140859));
#142344=CARTESIAN_POINT('Ctrl Pts',(166.970948639806,4.9969518148703,133.976621522858));
#142345=CARTESIAN_POINT('Ctrl Pts',(166.963552282871,5.07784371726555,133.841371277002));
#142346=CARTESIAN_POINT('Ctrl Pts',(166.956154793534,5.15874800441759,133.706100323988));
#142347=CARTESIAN_POINT('Ctrl Pts',(166.948757304198,5.23422901301899,133.567618084759));
#142348=CARTESIAN_POINT('Ctrl Pts',(166.941359814861,5.30403787839899,133.426404237914));
#142349=CARTESIAN_POINT('Ctrl Pts',(166.933959732346,5.37387121516852,133.285140888775));
#142350=CARTESIAN_POINT('Ctrl Pts',(166.926559649831,5.43802828457844,133.141144359955));
#142351=CARTESIAN_POINT('Ctrl Pts',(166.919159567316,5.49630776219657,132.994915694645));
#142352=CARTESIAN_POINT('Ctrl Pts',(166.91175134765,5.55465132409161,132.848526235885));
#142353=CARTESIAN_POINT('Ctrl Pts',(166.904343127983,5.60710424883609,132.699900085894));
#142354=CARTESIAN_POINT('Ctrl Pts',(166.896934908317,5.65351440112497,132.549555586265));
#142355=CARTESIAN_POINT('Ctrl Pts',(166.889522129015,5.69995311808823,132.399118552105));
#142356=CARTESIAN_POINT('Ctrl Pts',(166.882109349713,5.7403415560233,132.246961420844));
#142357=CARTESIAN_POINT('Ctrl Pts',(166.87469657041,5.77457851858784,132.093613694027));
#142358=CARTESIAN_POINT('Ctrl Pts',(166.867273199382,5.80886440053004,131.940046856787));
#142359=CARTESIAN_POINT('Ctrl Pts',(166.859849828353,5.83698118591433,131.785286392668));
#142360=CARTESIAN_POINT('Ctrl Pts',(166.852426457324,5.85887932286573,131.629868729335));
#142361=CARTESIAN_POINT('Ctrl Pts',(166.848490407883,5.87049024051603,131.547462555039));
#142362=CARTESIAN_POINT('Ctrl Pts',(166.844554358443,5.88035374313279,131.464871661582));
#142363=CARTESIAN_POINT('Ctrl Pts',(166.840618309002,5.88846838787322,131.382175992507));
#142364=CARTESIAN_POINT('Ctrl Pts',(166.833195042596,5.90377235460417,131.226214541475));
#142365=CARTESIAN_POINT('Ctrl Pts',(166.825771776191,5.91289901123309,131.069408829523));
#142366=CARTESIAN_POINT('Ctrl Pts',(166.818348509785,5.91576554003616,130.912289472932));
#142367=CARTESIAN_POINT('Ctrl Pts',(166.810934017064,5.91862868084023,130.755355818374));
#142368=CARTESIAN_POINT('Ctrl Pts',(166.803519524343,5.91524641472873,130.598109626652));
#142369=CARTESIAN_POINT('Ctrl Pts',(166.796105031622,5.90558749303605,130.441088096452));
#142370=CARTESIAN_POINT('Ctrl Pts',(166.788697685269,5.89593788097574,130.284217909516));
#142371=CARTESIAN_POINT('Ctrl Pts',(166.781290338915,5.88002367981568,130.127572323112));
#142372=CARTESIAN_POINT('Ctrl Pts',(166.773882992561,5.85786565541429,129.971689898964));
#142373=CARTESIAN_POINT('Ctrl Pts',(166.766481170886,5.83572415730347,129.815923737809));
#142374=CARTESIAN_POINT('Ctrl Pts',(166.75907934921,5.80734816073423,129.660919973558));
#142375=CARTESIAN_POINT('Ctrl Pts',(166.751677527535,5.77281035372675,129.507213292701));
#142376=CARTESIAN_POINT('Ctrl Pts',(166.744279613223,5.73829077895876,129.353587752404));
#142377=CARTESIAN_POINT('Ctrl Pts',(166.736881698912,5.69761595343543,129.201258295142));
#142378=CARTESIAN_POINT('Ctrl Pts',(166.729483784601,5.65090985820759,129.050750530656));
#142379=CARTESIAN_POINT('Ctrl Pts',(166.722087099688,5.60421152468545,128.90026777783));
#142380=CARTESIAN_POINT('Ctrl Pts',(166.714690414776,5.55148402123303,128.751606473121));
#142381=CARTESIAN_POINT('Ctrl Pts',(166.707293729864,5.4929015415178,128.605278259469));
#142382=CARTESIAN_POINT('Ctrl Pts',(166.699897372929,5.43432165941111,128.458956534164));
#142383=CARTESIAN_POINT('Ctrl Pts',(166.692501015993,5.36988745598924,128.314968040774));
#142384=CARTESIAN_POINT('Ctrl Pts',(166.685104659058,5.29982164280383,128.173805330755));
#142385=CARTESIAN_POINT('Ctrl Pts',(166.677707169721,5.22974510236354,128.032621008365));
#142386=CARTESIAN_POINT('Ctrl Pts',(166.670309680384,5.15403540135419,127.894263665175));
#142387=CARTESIAN_POINT('Ctrl Pts',(166.662912191048,5.07296158953401,127.759201956082));
#142388=CARTESIAN_POINT('Ctrl Pts',(166.655512108533,4.99185935741483,127.624092901316));
#142389=CARTESIAN_POINT('Ctrl Pts',(166.648112026018,4.90538946266501,127.492282100661));
#142390=CARTESIAN_POINT('Ctrl Pts',(166.640711943503,4.81386462633662,127.364209760146));
#142391=CARTESIAN_POINT('Ctrl Pts',(166.633303723836,4.72223914904163,127.235996590927));
#142392=CARTESIAN_POINT('Ctrl Pts',(166.62589550417,4.62554784680075,127.11153039533));
#142393=CARTESIAN_POINT('Ctrl Pts',(166.618487284503,4.52414458222861,126.991219345387));
#142394=CARTESIAN_POINT('Ctrl Pts',(166.611074505201,4.42267890563909,126.870834246001));
#142395=CARTESIAN_POINT('Ctrl Pts',(166.603661725899,4.31649573904106,126.754609663215));
#142396=CARTESIAN_POINT('Ctrl Pts',(166.596248946597,4.20598586798708,126.642916944897));
#142397=CARTESIAN_POINT('Ctrl Pts',(166.588825575568,4.09531809524689,126.531064634786));
#142398=CARTESIAN_POINT('Ctrl Pts',(166.58140220454,3.98031154303065,126.423757375843));
#142399=CARTESIAN_POINT('Ctrl Pts',(166.573978833511,3.86139073912517,126.321326809719));
#142400=CARTESIAN_POINT('Ctrl Pts',(166.57004278407,3.79833607542974,126.267015665773));
#142401=CARTESIAN_POINT('Ctrl Pts',(166.566106734629,3.73418148176345,126.214074826365));
#142402=CARTESIAN_POINT('Ctrl Pts',(166.562170685189,3.66899343700182,126.162548716838));
#142403=CARTESIAN_POINT('Ctrl Pts',(166.554747418783,3.54605081902921,126.065372082344));
#142404=CARTESIAN_POINT('Ctrl Pts',(166.547324152378,3.41905891343449,125.972936250139));
#142405=CARTESIAN_POINT('Ctrl Pts',(166.539900885972,3.28841937772064,125.885597708182));
#142406=CARTESIAN_POINT('Ctrl Pts',(166.532486393251,3.15793424708902,125.798362393129));
#142407=CARTESIAN_POINT('Ctrl Pts',(166.52507190053,3.0238103751002,125.716212581821));
#142408=CARTESIAN_POINT('Ctrl Pts',(166.517657407809,2.88648283155587,125.63946493366));
#142409=CARTESIAN_POINT('Ctrl Pts',(166.510250061456,2.7492876494682,125.562791257771));
#142410=CARTESIAN_POINT('Ctrl Pts',(166.502842715102,2.6088952667398,125.491509560188));
#142411=CARTESIAN_POINT('Ctrl Pts',(166.495435368748,2.46577001505577,125.425893475773));
#142412=CARTESIAN_POINT('Ctrl Pts',(166.488033547073,2.3227515115844,125.360326330309));
#142413=CARTESIAN_POINT('Ctrl Pts',(166.480631725397,2.17700453551775,125.300416539118));
#142414=CARTESIAN_POINT('Ctrl Pts',(166.473229903722,2.0290182233931,125.246391958817));
#142415=CARTESIAN_POINT('Ctrl Pts',(166.46583198941,1.88111003209069,125.192395897671));
#142416=CARTESIAN_POINT('Ctrl Pts',(166.458434075099,1.7309652087691,125.144278987851));
#142417=CARTESIAN_POINT('Ctrl Pts',(166.451036160788,1.57909297857519,125.102221025491));
#142418=CARTESIAN_POINT('Ctrl Pts',(166.443639475876,1.42724598679064,125.0601700524));
#142419=CARTESIAN_POINT('Ctrl Pts',(166.436242790963,1.27367251727574,125.024176127926));
#142420=CARTESIAN_POINT('Ctrl Pts',(166.428846106051,1.11889718565743,124.994369253508));
#142421=CARTESIAN_POINT('Ctrl Pts',(166.421449749116,0.964128716939459,
124.964563700758));
#142422=CARTESIAN_POINT('Ctrl Pts',(166.41405339218,0.808158858642217,124.940944723177));
#142423=CARTESIAN_POINT('Ctrl Pts',(166.406657035245,0.65152238928837,124.923591183321));
#142424=CARTESIAN_POINT('Ctrl Pts',(166.399259545908,0.49486193849108,124.906234986593));
#142425=CARTESIAN_POINT('Ctrl Pts',(166.391862056572,0.337535044474101,
124.895146178702));
#142426=CARTESIAN_POINT('Ctrl Pts',(166.384464567235,0.180081427840616,
124.890351719885));
#142427=CARTESIAN_POINT('Ctrl Pts',(166.37706448472,0.0225726160860165,
124.885555580378));
#142428=CARTESIAN_POINT('Ctrl Pts',(166.369664402205,-0.135062633837593,
124.887058194374));
#142429=CARTESIAN_POINT('Ctrl Pts',(166.36226431969,-0.292284930763479,
124.894834402906));
#142430=CARTESIAN_POINT('Ctrl Pts',(166.354856100024,-0.449680109767736,
124.902619162179));
#142431=CARTESIAN_POINT('Ctrl Pts',(166.347447880357,-0.606661055867241,
124.916691274218));
#142432=CARTESIAN_POINT('Ctrl Pts',(166.340039660691,-0.76269309098338,
124.936973651338));
#142433=CARTESIAN_POINT('Ctrl Pts',(166.332626881389,-0.918821161213655,
124.957268511922));
#142434=CARTESIAN_POINT('Ctrl Pts',(166.325214102086,-1.07399878957714,
124.983781191305));
#142435=CARTESIAN_POINT('Ctrl Pts',(166.317801322784,-1.22770232145825,
125.016383633128));
#142436=CARTESIAN_POINT('Ctrl Pts',(166.310377951756,-1.38162547215363,
125.049032658848));
#142437=CARTESIAN_POINT('Ctrl Pts',(166.302954580727,-1.53406995886588,
125.087788733798));
#142438=CARTESIAN_POINT('Ctrl Pts',(166.295531209698,-1.68452729444312,
125.13247395114));
#142439=CARTESIAN_POINT('Ctrl Pts',(166.291595160257,-1.76430338394073,
125.156167125582));
#142440=CARTESIAN_POINT('Ctrl Pts',(166.287659110816,-1.84352113643791,
125.181526385335));
#142441=CARTESIAN_POINT('Ctrl Pts',(166.283723061376,-1.92210724217974,
125.20851981282));
#142442=CARTESIAN_POINT('Ctrl Pts',(166.27629979497,-2.07031818501966,125.259428574621));
#142443=CARTESIAN_POINT('Ctrl Pts',(166.268876528565,-2.21672929549576,
125.316306636218));
#142444=CARTESIAN_POINT('Ctrl Pts',(166.261453262159,-2.36082354450143,
125.379008762227));
#142445=CARTESIAN_POINT('Ctrl Pts',(166.254038769438,-2.50474748607107,
125.441636779531));
#142446=CARTESIAN_POINT('Ctrl Pts',(166.246624276717,-2.64635967789469,
125.510075011988));
#142447=CARTESIAN_POINT('Ctrl Pts',(166.239209783996,-2.78515853959671,
125.584128585193));
#142448=CARTESIAN_POINT('Ctrl Pts',(166.231802437643,-2.92382362173009,
125.658110782776));
#142449=CARTESIAN_POINT('Ctrl Pts',(166.224395091289,-3.05968044484829,
125.737697371788));
#142450=CARTESIAN_POINT('Ctrl Pts',(166.216987744935,-3.19224780957431,
125.822645603159));
#142451=CARTESIAN_POINT('Ctrl Pts',(166.20958592326,-3.32471630055828,125.907530476934));
#142452=CARTESIAN_POINT('Ctrl Pts',(166.202184101584,-3.45389990525267,
125.997768830151));
#142453=CARTESIAN_POINT('Ctrl Pts',(166.194782279909,-3.5793425311852,126.093072300455));
#142454=CARTESIAN_POINT('Ctrl Pts',(166.187384365598,-3.70471893693221,
126.188325460799));
#142455=CARTESIAN_POINT('Ctrl Pts',(166.179986451286,-3.82635800040218,
126.288638187903));
#142456=CARTESIAN_POINT('Ctrl Pts',(166.172588536975,-3.94383320538515,
126.393679240431));
#142457=CARTESIAN_POINT('Ctrl Pts',(166.165191852063,-4.06128888812006,
126.498702837042));
#142458=CARTESIAN_POINT('Ctrl Pts',(166.157795167151,-4.17458180769433,
126.608452950993));
#142459=CARTESIAN_POINT('Ctrl Pts',(166.150398482238,-4.28331902265383,
126.722558477252));
#142460=CARTESIAN_POINT('Ctrl Pts',(166.143002125303,-4.39205141609135,
126.836658943953));
#142461=CARTESIAN_POINT('Ctrl Pts',(166.135605768367,-4.49622824904004,
126.955114168725));
#142462=CARTESIAN_POINT('Ctrl Pts',(166.128209411432,-4.59549411134317,
127.077516854392));
#142463=CARTESIAN_POINT('Ctrl Pts',(166.120811922095,-4.69477517150308,
127.199938280222));
#142464=CARTESIAN_POINT('Ctrl Pts',(166.113414432759,-4.78914352877203,
127.326308080363));
#142465=CARTESIAN_POINT('Ctrl Pts',(166.106016943422,-4.87828476856935,
127.456186745252));
#142466=CARTESIAN_POINT('Ctrl Pts',(166.098616860907,-4.96745725669013,
127.586110938907));
#142467=CARTESIAN_POINT('Ctrl Pts',(166.091216778392,-5.05139876801785,
127.719546138697));
#142468=CARTESIAN_POINT('Ctrl Pts',(166.083816695877,-5.12983891540261,
127.856024940524));
#142469=CARTESIAN_POINT('Ctrl Pts',(166.076408476211,-5.20836531579331,
127.992653814823));
#142470=CARTESIAN_POINT('Ctrl Pts',(166.069000256545,-5.2813780852317,128.132332650995));
#142471=CARTESIAN_POINT('Ctrl Pts',(166.061592036878,-5.34865307320897,
128.274569941452));
#142472=CARTESIAN_POINT('Ctrl Pts',(166.054179257576,-5.41596946781898,
128.416894776589));
#142473=CARTESIAN_POINT('Ctrl Pts',(166.046766478274,-5.47754089833081,
128.561780861005));
#142474=CARTESIAN_POINT('Ctrl Pts',(166.039353698972,-5.53319205407562,
128.70871841165));
#142475=CARTESIAN_POINT('Ctrl Pts',(166.031930327943,-5.58892272680148,
128.855865913559));
#142476=CARTESIAN_POINT('Ctrl Pts',(166.024506956914,-5.63871611204877,
129.005070382862));
#142477=CARTESIAN_POINT('Ctrl Pts',(166.017083585886,-5.68244703815218,
129.155807851927));
#142478=CARTESIAN_POINT('Ctrl Pts',(166.013147536445,-5.70563422448215,
129.235732474924));
#142479=CARTESIAN_POINT('Ctrl Pts',(166.009211487004,-5.7271178912674,129.316087912996));
#142480=CARTESIAN_POINT('Ctrl Pts',(166.005275437563,-5.74688526595699,
129.39679523634));
#142481=CARTESIAN_POINT('Ctrl Pts',(165.99536581659,-5.79665272791137,129.599988564085));
#142482=CARTESIAN_POINT('Ctrl Pts',(165.985456195617,-5.8356617089951,129.805912698135));
#142483=CARTESIAN_POINT('Ctrl Pts',(165.975546574645,-5.86366917150755,
130.013592377427));
#142484=CARTESIAN_POINT('Ctrl Pts',(165.965876951706,-5.89099832997878,
130.216242327029));
#142485=CARTESIAN_POINT('Ctrl Pts',(165.956207328768,-5.90785247295491,
130.420564146172));
#142486=CARTESIAN_POINT('Ctrl Pts',(165.94653770583,-5.91404984588532,130.625629023034));
#142487=CARTESIAN_POINT('Ctrl Pts',(165.943816872408,-5.91579365942388,
130.683330070328));
#142488=CARTESIAN_POINT('Ctrl Pts',(165.941096038987,-5.91669400065677,
130.741089791547));
#142489=CARTESIAN_POINT('Ctrl Pts',(165.938375205566,-5.91674746826018,
130.798887105275));
#142490=CARTESIAN_POINT('',(164.188375192211,-5.90703701052902,130.805180874694));
#142491=CARTESIAN_POINT('Ctrl Pts',(165.938375192211,-5.91629100133431,
130.79888781122));
#142492=CARTESIAN_POINT('Ctrl Pts',(165.867859399391,-5.90251351537856,
132.296718260267));
#142493=CARTESIAN_POINT('Ctrl Pts',(165.704527731967,-4.56346770795856,
135.787977784439));
#142494=CARTESIAN_POINT('Ctrl Pts',(165.448380189937,1.31124547549227,137.678820293304));
#142495=CARTESIAN_POINT('Ctrl Pts',(165.169932566125,6.49243782846852,133.41698603538));
#142496=CARTESIAN_POINT('Ctrl Pts',(164.891484942312,5.70739699030252,126.754276652334));
#142497=CARTESIAN_POINT('Ctrl Pts',(164.613037318499,-0.322462860107947,
123.813396575733));
#142498=CARTESIAN_POINT('Ctrl Pts',(164.378667401798,-5.14838830328745,
126.745443838765));
#142499=CARTESIAN_POINT('Ctrl Pts',(164.237113359703,-5.9057559966609,129.765836853127));
#142500=CARTESIAN_POINT('Ctrl Pts',(164.188375192211,-5.90703701052902,
130.805180874694));
#142501=CARTESIAN_POINT('',(162.438375999696,-5.91850430126774,130.80953524169));
#142502=CARTESIAN_POINT('Ctrl Pts',(164.188375192211,-5.90703701052902,
130.805180874694));
#142503=CARTESIAN_POINT('Ctrl Pts',(164.144297485099,-5.90819553078106,
131.745140330083));
#142504=CARTESIAN_POINT('Ctrl Pts',(164.007403903381,-5.25265206602396,
134.662876630279));
#142505=CARTESIAN_POINT('Ctrl Pts',(163.777694447059,-0.672846130350174,
137.770337836536));
#142506=CARTESIAN_POINT('Ctrl Pts',(163.499246823248,5.49698415240917,135.13572596333));
#142507=CARTESIAN_POINT('Ctrl Pts',(163.220799199434,6.61535454171388,128.520800936328));
#142508=CARTESIAN_POINT('Ctrl Pts',(162.942351575622,1.65453728521643,124.004355698289));
#142509=CARTESIAN_POINT('Ctrl Pts',(162.681543965991,-4.41612301327428,
125.627031304092));
#142510=CARTESIAN_POINT('Ctrl Pts',(162.513552230965,-5.90464145011147,
129.214801166862));
#142511=CARTESIAN_POINT('Ctrl Pts',(162.438376370543,-5.91931103223556,
130.809528082525));
#142512=CARTESIAN_POINT('',(160.688373776686,-5.92101633406598,130.801148899096));
#142513=CARTESIAN_POINT('Ctrl Pts',(162.438375192211,-5.91674772355508,
130.809550830069));
#142514=CARTESIAN_POINT('Ctrl Pts',(162.42743056777,-5.91654415116547,131.041619646537));
#142515=CARTESIAN_POINT('Ctrl Pts',(162.41648594333,-5.90268400911373,131.273113435323));
#142516=CARTESIAN_POINT('Ctrl Pts',(162.405541318889,-5.87538811168766,
131.502748117124));
#142517=CARTESIAN_POINT('Ctrl Pts',(162.398846321925,-5.85869078676843,
131.643219222907));
#142518=CARTESIAN_POINT('Ctrl Pts',(162.39215132496,-5.83696670312851,131.782995481317));
#142519=CARTESIAN_POINT('Ctrl Pts',(162.385456327996,-5.81027417745911,
131.921788264106));
#142520=CARTESIAN_POINT('Ctrl Pts',(162.378033061591,-5.78067808800102,
132.075678670223));
#142521=CARTESIAN_POINT('Ctrl Pts',(162.370609795185,-5.74491913147518,
132.228625145143));
#142522=CARTESIAN_POINT('Ctrl Pts',(162.36318652878,-5.70306851519399,132.380095390141));
#142523=CARTESIAN_POINT('Ctrl Pts',(162.355772036059,-5.66126736286574,
132.531386609889));
#142524=CARTESIAN_POINT('Ctrl Pts',(162.348357543338,-5.61338898054029,
132.681204716409));
#142525=CARTESIAN_POINT('Ctrl Pts',(162.340943050617,-5.55955589185102,
132.829025737502));
#142526=CARTESIAN_POINT('Ctrl Pts',(162.333535704263,-5.50577468951937,
132.976704283129));
#142527=CARTESIAN_POINT('Ctrl Pts',(162.326128357909,-5.44605033366204,
133.12238922695));
#142528=CARTESIAN_POINT('Ctrl Pts',(162.318721011555,-5.38055560982868,
133.265570054416));
#142529=CARTESIAN_POINT('Ctrl Pts',(162.31131918988,-5.31510973443136,133.408644092219));
#142530=CARTESIAN_POINT('Ctrl Pts',(162.303917368204,-5.24390221503485,
133.549217394432));
#142531=CARTESIAN_POINT('Ctrl Pts',(162.296515546529,-5.16715452362796,
133.686797900743));
#142532=CARTESIAN_POINT('Ctrl Pts',(162.289117632217,-5.09044734672991,
133.824305779377));
#142533=CARTESIAN_POINT('Ctrl Pts',(162.281719717906,-5.0082060037273,133.958823683324));
#142534=CARTESIAN_POINT('Ctrl Pts',(162.274321803595,-4.92069857331505,
134.089882815494));
#142535=CARTESIAN_POINT('Ctrl Pts',(162.266925118682,-4.83320568505026,
134.220920168013));
#142536=CARTESIAN_POINT('Ctrl Pts',(162.25952843377,-4.74044865333258,134.348499579381));
#142537=CARTESIAN_POINT('Ctrl Pts',(162.252131748858,-4.64273973952022,
134.472179897953));
#142538=CARTESIAN_POINT('Ctrl Pts',(162.244735391922,-4.54503515822351,
134.59585473241));
#142539=CARTESIAN_POINT('Ctrl Pts',(162.237339034987,-4.44237936282352,
134.715630524915));
#142540=CARTESIAN_POINT('Ctrl Pts',(162.229942678051,-4.33512571764814,
134.831098202098));
#142541=CARTESIAN_POINT('Ctrl Pts',(162.222545188714,-4.22785565166576,
134.946583557678));
#142542=CARTESIAN_POINT('Ctrl Pts',(162.215147699378,-4.11598658833484,
135.057759211088));
#142543=CARTESIAN_POINT('Ctrl Pts',(162.207750210041,-3.99990954098363,
135.164252155947));
#142544=CARTESIAN_POINT('Ctrl Pts',(162.200350127526,-3.8837918030032,135.270782431743));
#142545=CARTESIAN_POINT('Ctrl Pts',(162.192950045011,-3.7634634189861,135.372626478538));
#142546=CARTESIAN_POINT('Ctrl Pts',(162.185549962496,-3.63934920184748,
135.469450964978));
#142547=CARTESIAN_POINT('Ctrl Pts',(162.178141742829,-3.51509850836809,
135.566381919893));
#142548=CARTESIAN_POINT('Ctrl Pts',(162.170733523163,-3.38705396266636,
135.658282061851));
#142549=CARTESIAN_POINT('Ctrl Pts',(162.163325303496,-3.25567073390916,
135.744860454108));
#142550=CARTESIAN_POINT('Ctrl Pts',(162.155912524194,-3.12420664096672,
135.83149213392));
#142551=CARTESIAN_POINT('Ctrl Pts',(162.148499744892,-2.98940008923525,
135.912795344946));
#142552=CARTESIAN_POINT('Ctrl Pts',(162.14108696559,-2.85173119931621,135.988524940709));
#142553=CARTESIAN_POINT('Ctrl Pts',(162.133663594561,-2.71386560163142,
136.064362742469));
#142554=CARTESIAN_POINT('Ctrl Pts',(162.126240223532,-2.57312983054176,
136.13461085711));
#142555=CARTESIAN_POINT('Ctrl Pts',(162.118816852503,-2.43002509012415,
136.199071789062));
#142556=CARTESIAN_POINT('Ctrl Pts',(162.114880803063,-2.35414752301458,
136.233250521898));
#142557=CARTESIAN_POINT('Ctrl Pts',(162.110944753623,-2.27760423821805,
136.265803093478));
#142558=CARTESIAN_POINT('Ctrl Pts',(162.107008704182,-2.20047159052352,
136.296705776221));
#142559=CARTESIAN_POINT('Ctrl Pts',(162.099585437777,-2.05500182417906,
136.354987271443));
#142560=CARTESIAN_POINT('Ctrl Pts',(162.092162171372,-1.90699503369736,
136.407573554191));
#142561=CARTESIAN_POINT('Ctrl Pts',(162.084738904966,-1.75693754636281,
136.45423681273));
#142562=CARTESIAN_POINT('Ctrl Pts',(162.077324412245,-1.60705741451664,
136.500844919173));
#142563=CARTESIAN_POINT('Ctrl Pts',(162.069909919524,-1.45513176329157,
136.541543826221));
#142564=CARTESIAN_POINT('Ctrl Pts',(162.062495426803,-1.30166765235591,
136.576153396704));
#142565=CARTESIAN_POINT('Ctrl Pts',(162.055088080449,-1.14835145590825,
136.61072960918));
#142566=CARTESIAN_POINT('Ctrl Pts',(162.047680734095,-0.993500113471112,
136.639228087804));
#142567=CARTESIAN_POINT('Ctrl Pts',(162.040273387742,-0.837636530203736,
136.661518256367));
#142568=CARTESIAN_POINT('Ctrl Pts',(162.032871566066,-0.681889195877158,
136.683791800082));
#142569=CARTESIAN_POINT('Ctrl Pts',(162.025469744391,-0.525131491909981,
136.699866200852));
#142570=CARTESIAN_POINT('Ctrl Pts',(162.018067922716,-0.367897113596595,
136.709661818716));
#142571=CARTESIAN_POINT('Ctrl Pts',(162.010670008404,-0.210745738087498,
136.71945226555));
#142572=CARTESIAN_POINT('Ctrl Pts',(162.003272094093,-0.0531185610031907,
136.722970507353));
#142573=CARTESIAN_POINT('Ctrl Pts',(161.995874179782,0.104445102303171,
136.720188690043));
#142574=CARTESIAN_POINT('Ctrl Pts',(161.988477494869,0.261982581387019,
136.717407335021));
#142575=CARTESIAN_POINT('Ctrl Pts',(161.981080809957,0.419456194766861,
136.708328005366));
#142576=CARTESIAN_POINT('Ctrl Pts',(161.973684125045,0.57632600417748,136.692974962164));
#142577=CARTESIAN_POINT('Ctrl Pts',(161.96628776811,0.733188857816362,136.677622599732));
#142578=CARTESIAN_POINT('Ctrl Pts',(161.958891411174,0.889447589197945,
136.655997113235));
#142579=CARTESIAN_POINT('Ctrl Pts',(161.951495054239,1.04456703125893,136.628174683941));
#142580=CARTESIAN_POINT('Ctrl Pts',(161.944097564902,1.19971022250251,136.600347994962));
#142581=CARTESIAN_POINT('Ctrl Pts',(161.936700075566,1.35371340965791,136.56632253997));
#142582=CARTESIAN_POINT('Ctrl Pts',(161.929302586229,1.5060514196369,136.526225670493));
#142583=CARTESIAN_POINT('Ctrl Pts',(161.921902503714,1.65844283146914,136.486114745121));
#142584=CARTESIAN_POINT('Ctrl Pts',(161.914502421199,1.80916754315514,136.439928262743));
#142585=CARTESIAN_POINT('Ctrl Pts',(161.907102338684,1.95771549182921,136.387843456758));
#142586=CARTESIAN_POINT('Ctrl Pts',(161.899694119018,2.106426784244,136.335701378175));
#142587=CARTESIAN_POINT('Ctrl Pts',(161.892285899351,2.25295618103334,136.277648146981));
#142588=CARTESIAN_POINT('Ctrl Pts',(161.884877679685,2.39681287882266,136.213909451472));
#142589=CARTESIAN_POINT('Ctrl Pts',(161.877464900383,2.5407581180093,136.150131525859));
#142590=CARTESIAN_POINT('Ctrl Pts',(161.870052121081,2.6820270461158,136.08066132747));
#142591=CARTESIAN_POINT('Ctrl Pts',(161.862639341779,2.82015389755464,136.005770287704));
#142592=CARTESIAN_POINT('Ctrl Pts',(161.85521597075,2.95847811111618,135.930772240109));
#142593=CARTESIAN_POINT('Ctrl Pts',(161.847792599721,3.09365096142933,135.850338071918));
#142594=CARTESIAN_POINT('Ctrl Pts',(161.840369228692,3.22523537683267,135.764782709135));
#142595=CARTESIAN_POINT('Ctrl Pts',(161.836433179252,3.29500459120555,135.719419202914));
#142596=CARTESIAN_POINT('Ctrl Pts',(161.832497129811,3.3637655067298,135.672616629669));
#142597=CARTESIAN_POINT('Ctrl Pts',(161.82856108037,3.43145688909021,135.624426403509));
#142598=CARTESIAN_POINT('Ctrl Pts',(161.821137813964,3.55912072364372,135.533541140937));
#142599=CARTESIAN_POINT('Ctrl Pts',(161.813714547559,3.68336433816243,135.437443006652));
#142600=CARTESIAN_POINT('Ctrl Pts',(161.806291281154,3.80373319640592,135.336418023762));
#142601=CARTESIAN_POINT('Ctrl Pts',(161.798876788433,3.92395978865511,135.235512444013));
#142602=CARTESIAN_POINT('Ctrl Pts',(161.791462295712,4.04032045728496,135.129691844265));
#142603=CARTESIAN_POINT('Ctrl Pts',(161.784047802991,4.15238956965613,135.019285459637));
#142604=CARTESIAN_POINT('Ctrl Pts',(161.776640456637,4.26435066559748,134.90898548884));
#142605=CARTESIAN_POINT('Ctrl Pts',(161.769233110283,4.37202817582391,134.79410879264));
#142606=CARTESIAN_POINT('Ctrl Pts',(161.761825763929,4.47502959986258,134.675024726327));
#142607=CARTESIAN_POINT('Ctrl Pts',(161.754423942254,4.57795420155314,134.556029477404));
#142608=CARTESIAN_POINT('Ctrl Pts',(161.747022120578,4.67620941818536,134.432833387703));
#142609=CARTESIAN_POINT('Ctrl Pts',(161.739620298903,4.76943977106237,134.305842422846));
#142610=CARTESIAN_POINT('Ctrl Pts',(161.732222384592,4.86262090836165,134.178918495531));
#142611=CARTESIAN_POINT('Ctrl Pts',(161.72482447028,4.95078224430348,134.048203982849));
#142612=CARTESIAN_POINT('Ctrl Pts',(161.717426555969,5.03360883133898,133.91413757027));
#142613=CARTESIAN_POINT('Ctrl Pts',(161.710029871057,5.11642165409845,133.780093437095));
#142614=CARTESIAN_POINT('Ctrl Pts',(161.702633186145,5.19390129145906,133.642698826822));
#142615=CARTESIAN_POINT('Ctrl Pts',(161.695236501232,5.26577630513684,133.502421118511));
#142616=CARTESIAN_POINT('Ctrl Pts',(161.687840144297,5.33764813180117,133.362149630261));
#142617=CARTESIAN_POINT('Ctrl Pts',(161.680443787362,5.40391565868912,133.218995630389));
#142618=CARTESIAN_POINT('Ctrl Pts',(161.673047430426,5.46435370838878,133.073450547938));
#142619=CARTESIAN_POINT('Ctrl Pts',(161.66564994109,5.52480101130816,132.927883182164));
#142620=CARTESIAN_POINT('Ctrl Pts',(161.658252451753,5.57941691676746,132.779924349673));
#142621=CARTESIAN_POINT('Ctrl Pts',(161.650854962416,5.62802470033038,132.630084730068));
#142622=CARTESIAN_POINT('Ctrl Pts',(161.643454879901,5.67664952327648,132.480192584417));
#142623=CARTESIAN_POINT('Ctrl Pts',(161.636054797386,5.71926191590507,132.328418693837));
#142624=CARTESIAN_POINT('Ctrl Pts',(161.628654714871,5.7557352882555,132.175287987645));
#142625=CARTESIAN_POINT('Ctrl Pts',(161.621246495205,5.79224876682841,132.021988898498));
#142626=CARTESIAN_POINT('Ctrl Pts',(161.613838275538,5.82260965741637,131.867330377562));
#142627=CARTESIAN_POINT('Ctrl Pts',(161.606430055872,5.84674254676127,131.711847341652));
#142628=CARTESIAN_POINT('Ctrl Pts',(161.59901727657,5.8708902894969,131.556268608527));
#142629=CARTESIAN_POINT('Ctrl Pts',(161.591604497268,5.88880235042085,131.399864719234));
#142630=CARTESIAN_POINT('Ctrl Pts',(161.584191717966,5.90045533478054,131.243174250855));
#142631=CARTESIAN_POINT('Ctrl Pts',(161.576768346937,5.91212496947076,131.086259895786));
#142632=CARTESIAN_POINT('Ctrl Pts',(161.569344975908,5.91751765313196,130.929058515902));
#142633=CARTESIAN_POINT('Ctrl Pts',(161.56192160488,5.91666209402293,130.772108057169));
#142634=CARTESIAN_POINT('Ctrl Pts',(161.557985555439,5.91620845605445,130.688889157971));
#142635=CARTESIAN_POINT('Ctrl Pts',(161.554049505998,5.91399908008518,130.605740718273));
#142636=CARTESIAN_POINT('Ctrl Pts',(161.550113456557,5.91004412361794,130.52274204682));
#142637=CARTESIAN_POINT('Ctrl Pts',(161.542690190151,5.902585199151,130.366209142766));
#142638=CARTESIAN_POINT('Ctrl Pts',(161.535266923746,5.88889182560213,130.2097360822));
#142639=CARTESIAN_POINT('Ctrl Pts',(161.52784365734,5.86895895437449,130.053859881812));
#142640=CARTESIAN_POINT('Ctrl Pts',(161.520429164619,5.8490496421453,129.898167914148));
#142641=CARTESIAN_POINT('Ctrl Pts',(161.513014671898,5.8229155582438,129.743071769148));
#142642=CARTESIAN_POINT('Ctrl Pts',(161.505600179177,5.79060363266186,129.58910750323));
#142643=CARTESIAN_POINT('Ctrl Pts',(161.498192832823,5.75832285053032,129.435291633868));
#142644=CARTESIAN_POINT('Ctrl Pts',(161.49078548647,5.71987615698665,129.282605834613));
#142645=CARTESIAN_POINT('Ctrl Pts',(161.483378140116,5.67536214500421,129.131579972785));
#142646=CARTESIAN_POINT('Ctrl Pts',(161.47597631844,5.63088133325133,128.980666751743));
#142647=CARTESIAN_POINT('Ctrl Pts',(161.468574496765,5.5803423184976,128.831411359542));
#142648=CARTESIAN_POINT('Ctrl Pts',(161.46117267509,5.52389450619997,128.684332304813));
#142649=CARTESIAN_POINT('Ctrl Pts',(161.453774760778,5.46747649226303,128.537330891972));
#142650=CARTESIAN_POINT('Ctrl Pts',(161.446376846467,5.40515602625247,128.392503876201));
#142651=CARTESIAN_POINT('Ctrl Pts',(161.438978932155,5.33713194983506,128.250353352003));
#142652=CARTESIAN_POINT('Ctrl Pts',(161.431582247243,5.26911917778517,128.108226450643));
#142653=CARTESIAN_POINT('Ctrl Pts',(161.424185562331,5.19540483748249,127.968775494491));
#142654=CARTESIAN_POINT('Ctrl Pts',(161.416788877419,5.11623542914677,127.832481482062));
#142655=CARTESIAN_POINT('Ctrl Pts',(161.409392520483,5.03706953126555,127.696193513052));
#142656=CARTESIAN_POINT('Ctrl Pts',(161.401996163548,4.95244923379804,127.563062532226));
#142657=CARTESIAN_POINT('Ctrl Pts',(161.394599806612,4.86266627602476,127.433543617118));
#142658=CARTESIAN_POINT('Ctrl Pts',(161.387202317276,4.77286957225141,127.304004872333));
#142659=CARTESIAN_POINT('Ctrl Pts',(161.379804827939,4.67790884703223,127.17807960121));
#142660=CARTESIAN_POINT('Ctrl Pts',(161.372407338603,4.57811822570637,127.056192521822));
#142661=CARTESIAN_POINT('Ctrl Pts',(161.365007256088,4.47829262293286,126.934262715107));
#142662=CARTESIAN_POINT('Ctrl Pts',(161.357607173573,4.37363398940875,126.816374207201));
#142663=CARTESIAN_POINT('Ctrl Pts',(161.350207091058,4.26451553806804,126.70291723894));
#142664=CARTESIAN_POINT('Ctrl Pts',(161.342798871391,4.15527709977247,126.589335513079));
#142665=CARTESIAN_POINT('Ctrl Pts',(161.335390651725,4.04156930891996,126.480195327652));
#142666=CARTESIAN_POINT('Ctrl Pts',(161.327982432058,3.92380144346892,126.375849265573));
#142667=CARTESIAN_POINT('Ctrl Pts',(161.320569652756,3.80596109386171,126.271438980234));
#142668=CARTESIAN_POINT('Ctrl Pts',(161.313156873454,3.68405597866619,126.171828933543));
#142669=CARTESIAN_POINT('Ctrl Pts',(161.305744094152,3.55852657259944,126.077329922235));
#142670=CARTESIAN_POINT('Ctrl Pts',(161.298320723123,3.43281780423052,125.982695886308));
#142671=CARTESIAN_POINT('Ctrl Pts',(161.290897352094,3.30347470840148,125.893187683131));
#142672=CARTESIAN_POINT('Ctrl Pts',(161.283473981066,3.17096539180398,125.809071932567));
#142673=CARTESIAN_POINT('Ctrl Pts',(161.279537931625,3.10070577263001,125.76447174329));
#142674=CARTESIAN_POINT('Ctrl Pts',(161.275601882185,3.02955641375347,125.721386791199));
#142675=CARTESIAN_POINT('Ctrl Pts',(161.271665832744,2.9575895302463,125.679851398814));
#142676=CARTESIAN_POINT('Ctrl Pts',(161.264242566338,2.82186223395502,125.601516945046));
#142677=CARTESIAN_POINT('Ctrl Pts',(161.256819299933,2.68281541367125,125.528460056726));
#142678=CARTESIAN_POINT('Ctrl Pts',(161.249396033528,2.54089814785558,125.460975252021));
#142679=CARTESIAN_POINT('Ctrl Pts',(161.241981540807,2.39914861646251,125.39357020875));
#142680=CARTESIAN_POINT('Ctrl Pts',(161.234567048086,2.25453572641405,125.331724298886));
#142681=CARTESIAN_POINT('Ctrl Pts',(161.227152555365,2.10753584396342,125.275687790484));
#142682=CARTESIAN_POINT('Ctrl Pts',(161.219745209011,1.96067764553395,125.21970529218));
#142683=CARTESIAN_POINT('Ctrl Pts',(161.212337862657,1.8114373813614,125.16952118027));
#142684=CARTESIAN_POINT('Ctrl Pts',(161.204930516303,1.66031413573936,125.125338911923));
#142685=CARTESIAN_POINT('Ctrl Pts',(161.197528694628,1.50930360353531,125.081189596379));
#142686=CARTESIAN_POINT('Ctrl Pts',(161.190126872953,1.35641324298605,125.04303331558));
#142687=CARTESIAN_POINT('Ctrl Pts',(161.182725051277,1.2021600473863,125.011024637065));
#142688=CARTESIAN_POINT('Ctrl Pts',(161.175327136966,1.04798828084787,124.979032855682));
#142689=CARTESIAN_POINT('Ctrl Pts',(161.167929222655,0.892455476624556,
124.953182289123));
#142690=CARTESIAN_POINT('Ctrl Pts',(161.160531308343,0.736091539820999,
124.933577040606));
#142691=CARTESIAN_POINT('Ctrl Pts',(161.153134623431,0.579753587867119,
124.913975050126));
#142692=CARTESIAN_POINT('Ctrl Pts',(161.145737938519,0.422585147493782,
124.900616364242));
#142693=CARTESIAN_POINT('Ctrl Pts',(161.138341253607,0.265124135764709,
124.893553586785));
#142694=CARTESIAN_POINT('Ctrl Pts',(161.130944896671,0.107670106021902,
124.886491122498));
#142695=CARTESIAN_POINT('Ctrl Pts',(161.123548539736,-0.0500760963594786,
124.885724028287));
#142696=CARTESIAN_POINT('Ctrl Pts',(161.1161521828,-0.207573909553045,124.891252836156));
#142697=CARTESIAN_POINT('Ctrl Pts',(161.108754693464,-0.365095836063884,
124.896782490499));
#142698=CARTESIAN_POINT('Ctrl Pts',(161.101357204127,-0.522368924573997,
124.908609953116));
#142699=CARTESIAN_POINT('Ctrl Pts',(161.093959714791,-0.67885524483256,
124.926683685388));
#142700=CARTESIAN_POINT('Ctrl Pts',(161.086559632276,-0.835396421127937,
124.944763753378));
#142701=CARTESIAN_POINT('Ctrl Pts',(161.079159549761,-0.991149909453824,
124.969094407738));
#142702=CARTESIAN_POINT('Ctrl Pts',(161.071759467246,-1.14558565843546,
124.99957258856));
#142703=CARTESIAN_POINT('Ctrl Pts',(161.064351247579,-1.30019122539966,
125.030084283276));
#142704=CARTESIAN_POINT('Ctrl Pts',(161.056943027913,-1.45347579283293,
125.066756931971));
#142705=CARTESIAN_POINT('Ctrl Pts',(161.049534808246,-1.60492149800979,
125.109436777186));
#142706=CARTESIAN_POINT('Ctrl Pts',(161.042122028944,-1.75646041549145,
125.152142891134));
#142707=CARTESIAN_POINT('Ctrl Pts',(161.034709249642,-1.9061578613372,125.200863453733));
#142708=CARTESIAN_POINT('Ctrl Pts',(161.02729647034,-2.05351426610689,125.255395874355));
#142709=CARTESIAN_POINT('Ctrl Pts',(161.019873099311,-2.20108122061784,
125.310006213458));
#142710=CARTESIAN_POINT('Ctrl Pts',(161.012449728283,-2.34630010963088,
125.370444852988));
#142711=CARTESIAN_POINT('Ctrl Pts',(161.005026357254,-2.48869359520285,
125.436462076079));
#142712=CARTESIAN_POINT('Ctrl Pts',(161.001090307813,-2.56419403793659,
125.471465991823));
#142713=CARTESIAN_POINT('Ctrl Pts',(160.997154258372,-2.63890059475449,
125.508037493488));
#142714=CARTESIAN_POINT('Ctrl Pts',(160.993218208932,-2.71274535513869,
125.546134376648));
#142715=CARTESIAN_POINT('Ctrl Pts',(160.985794942526,-2.85201426860962,
125.617983909328));
#142716=CARTESIAN_POINT('Ctrl Pts',(160.978371676121,-2.9886373006023,125.695478904593));
#142717=CARTESIAN_POINT('Ctrl Pts',(160.970948409715,-3.12212392676529,
125.778400734278));
#142718=CARTESIAN_POINT('Ctrl Pts',(160.963533916994,-3.25545278282157,
125.861224557247));
#142719=CARTESIAN_POINT('Ctrl Pts',(160.956119424273,-3.3856522977949,125.949462252342));
#142720=CARTESIAN_POINT('Ctrl Pts',(160.948704931552,-3.51225442648564,
126.042848315142));
#142721=CARTESIAN_POINT('Ctrl Pts',(160.941297585199,-3.63873453127822,
126.136144368939));
#142722=CARTESIAN_POINT('Ctrl Pts',(160.933890238845,-3.76162385409736,
126.234578691589));
#142723=CARTESIAN_POINT('Ctrl Pts',(160.926482892491,-3.88048145341341,
126.33784136291));
#142724=CARTESIAN_POINT('Ctrl Pts',(160.919081070816,-3.99925040424752,
126.441027017035));
#142725=CARTESIAN_POINT('Ctrl Pts',(160.91167924914,-4.11399333835672,126.549033605654));
#142726=CARTESIAN_POINT('Ctrl Pts',(160.904277427465,-4.22430076618984,
126.661509715196));
#142727=CARTESIAN_POINT('Ctrl Pts',(160.896879513154,-4.33454996359047,
126.773926449476));
#142728=CARTESIAN_POINT('Ctrl Pts',(160.889481598842,-4.44036805714527,
126.890807739926));
#142729=CARTESIAN_POINT('Ctrl Pts',(160.882083684531,-4.5413810352156,127.011764032707));
#142730=CARTESIAN_POINT('Ctrl Pts',(160.874686999619,-4.64237722676158,
127.132700224747));
#142731=CARTESIAN_POINT('Ctrl Pts',(160.867290314706,-4.73856964860784,
127.25770978885));
#142732=CARTESIAN_POINT('Ctrl Pts',(160.859893629794,-4.82962328634955,
127.386368593811));
#142733=CARTESIAN_POINT('Ctrl Pts',(160.852497272859,-4.92067288667764,
127.515021693907));
#142734=CARTESIAN_POINT('Ctrl Pts',(160.845100915923,-5.00658394031519,
127.647323408416));
#142735=CARTESIAN_POINT('Ctrl Pts',(160.837704558988,-5.08706381280048,
127.782819234928));
#142736=CARTESIAN_POINT('Ctrl Pts',(160.830307069651,-5.16755600695972,
127.918335806196));
#142737=CARTESIAN_POINT('Ctrl Pts',(160.822909580314,-5.24261517363796,
128.057047142211));
#142738=CARTESIAN_POINT('Ctrl Pts',(160.815512090978,-5.31199390929384,
128.198472809136));
#142739=CARTESIAN_POINT('Ctrl Pts',(160.808112008463,-5.38139696555798,
128.339948052609));
#142740=CARTESIAN_POINT('Ctrl Pts',(160.800711925948,-5.4451154618958,128.484139186497));
#142741=CARTESIAN_POINT('Ctrl Pts',(160.793311843433,-5.50294959981077,
128.630544557168));
#142742=CARTESIAN_POINT('Ctrl Pts',(160.785903623766,-5.56084733230582,
128.777110915596));
#142743=CARTESIAN_POINT('Ctrl Pts',(160.7784954041,-5.61284764721661,128.925896025821));
#142744=CARTESIAN_POINT('Ctrl Pts',(160.771087184433,-5.65879998759627,
129.076381085604));
#142745=CARTESIAN_POINT('Ctrl Pts',(160.763674405131,-5.70478061087473,
129.22695876643));
#142746=CARTESIAN_POINT('Ctrl Pts',(160.756261625829,-5.74470574776557,
129.379238121422));
#142747=CARTESIAN_POINT('Ctrl Pts',(160.748848846527,-5.77847581401576,
129.53268934348));
#142748=CARTESIAN_POINT('Ctrl Pts',(160.741425475498,-5.81229413252025,
129.68635982384));
#142749=CARTESIAN_POINT('Ctrl Pts',(160.734002104469,-5.83993975005202,
129.841205148942));
#142750=CARTESIAN_POINT('Ctrl Pts',(160.72657873344,-5.86136474766689,129.996688742788));
#142751=CARTESIAN_POINT('Ctrl Pts',(160.722642683999,-5.87272479548808,
130.079129875023));
#142752=CARTESIAN_POINT('Ctrl Pts',(160.718706634559,-5.88233687414806,
130.161750407033));
#142753=CARTESIAN_POINT('Ctrl Pts',(160.714770585118,-5.89019978413138,
130.244470391255));
#142754=CARTESIAN_POINT('Ctrl Pts',(160.705972120815,-5.90777617229443,
130.429378848125));
#142755=CARTESIAN_POINT('Ctrl Pts',(160.697173656513,-5.91664728421935,
130.615127793757));
#142756=CARTESIAN_POINT('Ctrl Pts',(160.688375192211,-5.91674911325059,
130.801121273744));
#142757=CARTESIAN_POINT('',(158.938376379574,-5.91250676172561,130.8007115422));
#142758=CARTESIAN_POINT('Ctrl Pts',(160.688372676203,-5.9243338325154,130.801170376087));
#142759=CARTESIAN_POINT('Ctrl Pts',(160.60435610457,-5.91260203390904,132.579506857946));
#142760=CARTESIAN_POINT('Ctrl Pts',(160.427523658333,-4.11390117656668,
136.342953783282));
#142761=CARTESIAN_POINT('Ctrl Pts',(160.157875337493,2.29362448039243,137.416232309703));
#142762=CARTESIAN_POINT('Ctrl Pts',(159.879427713679,6.80251496907736,132.448547536935));
#142763=CARTESIAN_POINT('Ctrl Pts',(159.600980089867,5.0602265225104,125.969935308263));
#142764=CARTESIAN_POINT('Ctrl Pts',(159.322532466054,-1.33216289243681,
123.933923764033));
#142765=CARTESIAN_POINT('Ctrl Pts',(159.101664869801,-5.43163117945458,
127.326948799706));
#142766=CARTESIAN_POINT('Ctrl Pts',(158.973613148154,-5.91338609833529,
130.049979290673));
#142767=CARTESIAN_POINT('Ctrl Pts',(158.93837730111,-5.90921436344405,130.800693926467));
#142768=CARTESIAN_POINT('',(157.188373977522,-5.91343480873076,130.808965839466));
#142769=CARTESIAN_POINT('Ctrl Pts',(158.938375192211,-5.91674888869566,
130.800734239386));
#142770=CARTESIAN_POINT('Ctrl Pts',(158.930915454658,-5.91684642256871,
130.959869168598));
#142771=CARTESIAN_POINT('Ctrl Pts',(158.923455717105,-5.91051955951184,
131.119024896707));
#142772=CARTESIAN_POINT('Ctrl Pts',(158.915995979553,-5.89778993384828,
131.27765171055));
#142773=CARTESIAN_POINT('Ctrl Pts',(158.908535435224,-5.88505893146643,
131.436295679998));
#142774=CARTESIAN_POINT('Ctrl Pts',(158.901074890895,-5.86592381531385,
131.594410257938));
#142775=CARTESIAN_POINT('Ctrl Pts',(158.893614346566,-5.84045817256563,
131.751450316069));
#142776=CARTESIAN_POINT('Ctrl Pts',(158.886151617577,-5.81498507275002,
131.908536360014));
#142777=CARTESIAN_POINT('Ctrl Pts',(158.878688888587,-5.78317781144301,
132.064546897695));
#142778=CARTESIAN_POINT('Ctrl Pts',(158.871226159598,-5.74516121293526,
132.218946493321));
#142779=CARTESIAN_POINT('Ctrl Pts',(158.863759867021,-5.70712646081542,
132.373419817541));
#142780=CARTESIAN_POINT('Ctrl Pts',(158.856293574443,-5.66287655157163,
132.526280313815));
#142781=CARTESIAN_POINT('Ctrl Pts',(158.848827281866,-5.61258631675067,
132.677007247212));
#142782=CARTESIAN_POINT('Ctrl Pts',(158.841351300495,-5.56223082172863,
132.827929774644));
#142783=CARTESIAN_POINT('Ctrl Pts',(158.833875319123,-5.50581945828213,
132.976712862554));
#142784=CARTESIAN_POINT('Ctrl Pts',(158.826399337751,-5.44357577420364,
133.122854385727));
#142785=CARTESIAN_POINT('Ctrl Pts',(158.818918114411,-5.38128844643688,
133.26909837962));
#142786=CARTESIAN_POINT('Ctrl Pts',(158.811436891071,-5.31316080199116,
133.412696788273));
#142787=CARTESIAN_POINT('Ctrl Pts',(158.803955667732,-5.23946244456385,
133.553171970588));
#142788=CARTESIAN_POINT('Ctrl Pts',(158.796462266502,-5.16564412139993,
133.693875817549));
#142789=CARTESIAN_POINT('Ctrl Pts',(158.788968865273,-5.08623714866151,
133.831445965049));
#142790=CARTESIAN_POINT('Ctrl Pts',(158.781475464043,-5.0015551708291,133.965432656551));
#142791=CARTESIAN_POINT('Ctrl Pts',(158.776196048838,-4.94189316853013,
134.059831895929));
#142792=CARTESIAN_POINT('Ctrl Pts',(158.770916633633,-4.87961366328841,
134.1524530099));
#142793=CARTESIAN_POINT('Ctrl Pts',(158.765637218427,-4.81483811113869,
134.24314885269));
#142794=CARTESIAN_POINT('Ctrl Pts',(158.758213952022,-4.72375867118721,
134.370674227512));
#142795=CARTESIAN_POINT('Ctrl Pts',(158.750790685616,-4.62747157055039,
134.494771453157));
#142796=CARTESIAN_POINT('Ctrl Pts',(158.743367419211,-4.52626352373467,
134.614986429189));
#142797=CARTESIAN_POINT('Ctrl Pts',(158.73595292649,-4.42517509642523,134.735059321103));
#142798=CARTESIAN_POINT('Ctrl Pts',(158.728538433769,-4.31917753808615,
134.85125881405));
#142799=CARTESIAN_POINT('Ctrl Pts',(158.721123941048,-4.20860073119569,
134.963159776924));
#142800=CARTESIAN_POINT('Ctrl Pts',(158.713716594694,-4.09813050239493,
135.074952885437));
#142801=CARTESIAN_POINT('Ctrl Pts',(158.70630924834,-3.98309007237963,135.182455448199));
#142802=CARTESIAN_POINT('Ctrl Pts',(158.698901901987,-3.86384939333115,
135.285275527286));
#142803=CARTESIAN_POINT('Ctrl Pts',(158.691500080311,-3.74469764847946,
135.38801891928));
#142804=CARTESIAN_POINT('Ctrl Pts',(158.684098258636,-3.62135217372323,
135.486086538658));
#142805=CARTESIAN_POINT('Ctrl Pts',(158.67669643696,-3.49421947519282,135.579123524945));
#142806=CARTESIAN_POINT('Ctrl Pts',(158.669298522649,-3.36715388902532,
135.672111397731));
#142807=CARTESIAN_POINT('Ctrl Pts',(158.661900608338,-3.23630536116322,
135.760073706346));
#142808=CARTESIAN_POINT('Ctrl Pts',(158.654502694027,-3.10211305586488,
135.842696171212));
#142809=CARTESIAN_POINT('Ctrl Pts',(158.647106009114,-2.96794305089252,
135.925304905723));
#142810=CARTESIAN_POINT('Ctrl Pts',(158.639709324202,-2.8304306889006,136.002575362156));
#142811=CARTESIAN_POINT('Ctrl Pts',(158.63231263929,-2.69004376149368,136.074236813811));
#142812=CARTESIAN_POINT('Ctrl Pts',(158.624916282355,-2.54966305899033,
136.145895087922));
#142813=CARTESIAN_POINT('Ctrl Pts',(158.617519925419,-2.40640837699323,
136.211944682055));
#142814=CARTESIAN_POINT('Ctrl Pts',(158.610123568484,-2.26077148665801,
136.272161166929));
#142815=CARTESIAN_POINT('Ctrl Pts',(158.602726079147,-2.11511229894314,
136.332386871101));
#142816=CARTESIAN_POINT('Ctrl Pts',(158.595328589811,-1.96707052167487,
136.38677754516));
#142817=CARTESIAN_POINT('Ctrl Pts',(158.587931100474,-1.81715710280992,
136.435157242042));
#142818=CARTESIAN_POINT('Ctrl Pts',(158.580531017959,-1.66719113202903,
136.483553898351));
#142819=CARTESIAN_POINT('Ctrl Pts',(158.573130935444,-1.51535256839407,
136.52593526761));
#142820=CARTESIAN_POINT('Ctrl Pts',(158.565730852929,-1.36216653326101,
136.562175558858));
#142821=CARTESIAN_POINT('Ctrl Pts',(158.558322633263,-1.2088120543336,136.598455700031));
#142822=CARTESIAN_POINT('Ctrl Pts',(158.550914413597,-1.0541075083823,136.628581191521));
#142823=CARTESIAN_POINT('Ctrl Pts',(158.54350619393,-0.898587926369288,
136.652477434207));
#142824=CARTESIAN_POINT('Ctrl Pts',(158.536093414628,-0.742972624648474,
136.676388384633));
#142825=CARTESIAN_POINT('Ctrl Pts',(158.528680635326,-0.586541657361018,
136.69406240472));
#142826=CARTESIAN_POINT('Ctrl Pts',(158.521267856024,-0.429833636567998,
136.705476919366));
#142827=CARTESIAN_POINT('Ctrl Pts',(158.513844484995,-0.272901704006047,
136.716907743607));
#142828=CARTESIAN_POINT('Ctrl Pts',(158.506421113967,-0.115692299412364,
136.722061187283));
#142829=CARTESIAN_POINT('Ctrl Pts',(158.498997742938,0.0412566755591604,
136.720966777285));
#142830=CARTESIAN_POINT('Ctrl Pts',(158.495061693497,0.12447478803224,136.720386494843));
#142831=CARTESIAN_POINT('Ctrl Pts',(158.491125644056,0.207619769152417,
136.718050583662));
#142832=CARTESIAN_POINT('Ctrl Pts',(158.487189594615,0.290612325724202,
136.713969321925));
#142833=CARTESIAN_POINT('Ctrl Pts',(158.47976632821,0.447133697301818,136.706272189662));
#142834=CARTESIAN_POINT('Ctrl Pts',(158.472343061804,0.603585737690694,
136.692340706608));
#142835=CARTESIAN_POINT('Ctrl Pts',(158.464919795399,0.759431423139469,
136.672170641421));
#142836=CARTESIAN_POINT('Ctrl Pts',(158.457505302678,0.915092911930112,
136.652024415575));
#142837=CARTESIAN_POINT('Ctrl Pts',(158.450090809957,1.07014910570366,136.625654332006));
#142838=CARTESIAN_POINT('Ctrl Pts',(158.442676317236,1.22406402008241,136.593108136437));
#142839=CARTESIAN_POINT('Ctrl Pts',(158.435268970882,1.37783058547173,136.560593310118));
#142840=CARTESIAN_POINT('Ctrl Pts',(158.427861624529,1.53045769859553,136.5219142993));
#142841=CARTESIAN_POINT('Ctrl Pts',(158.420454278175,1.68141564278876,136.477170503212));
#142842=CARTESIAN_POINT('Ctrl Pts',(158.413052456499,1.83226099685249,136.432460078735));
#142843=CARTESIAN_POINT('Ctrl Pts',(158.405650634824,1.98143930444071,136.381693981206));
#142844=CARTESIAN_POINT('Ctrl Pts',(158.398248813149,2.12843228489295,136.32502240499));
#142845=CARTESIAN_POINT('Ctrl Pts',(158.390850898837,2.27534766889573,136.268380745258));
#142846=CARTESIAN_POINT('Ctrl Pts',(158.383452984526,2.42007967582008,136.20583994935));
#142847=CARTESIAN_POINT('Ctrl Pts',(158.376055070214,2.56212651434601,136.137599622803));
#142848=CARTESIAN_POINT('Ctrl Pts',(158.368658385302,2.70414974726347,136.069370636562));
#142849=CARTESIAN_POINT('Ctrl Pts',(158.36126170039,2.84348836125589,135.995444161003));
#142850=CARTESIAN_POINT('Ctrl Pts',(158.353865015478,2.97966173349597,135.916067428059));
#142851=CARTESIAN_POINT('Ctrl Pts',(158.346468658543,3.11582906766606,135.836694214762));
#142852=CARTESIAN_POINT('Ctrl Pts',(158.339072301607,3.24883111664123,135.751871412594));
#142853=CARTESIAN_POINT('Ctrl Pts',(158.331675944672,3.37821324739038,135.661891453048));
#142854=CARTESIAN_POINT('Ctrl Pts',(158.324278455335,3.50761518687414,135.57189771734));
#142855=CARTESIAN_POINT('Ctrl Pts',(158.316880965998,3.63339579811905,135.476745465258));
#142856=CARTESIAN_POINT('Ctrl Pts',(158.309483476662,3.75513087202569,135.376769468102));
#142857=CARTESIAN_POINT('Ctrl Pts',(158.302083394147,3.87690861997383,135.276758424516));
#142858=CARTESIAN_POINT('Ctrl Pts',(158.294683311632,3.99463771874266,135.171920505944));
#142859=CARTESIAN_POINT('Ctrl Pts',(158.287283229117,4.10792849591445,135.062629518769));
#142860=CARTESIAN_POINT('Ctrl Pts',(158.279875009451,4.22134384794215,134.953218354919));
#142861=CARTESIAN_POINT('Ctrl Pts',(158.272466789784,4.33031086308549,134.839344602955));
#142862=CARTESIAN_POINT('Ctrl Pts',(158.265058570118,4.43447758168943,134.721418076934));
#142863=CARTESIAN_POINT('Ctrl Pts',(158.257645790816,4.53870841317052,134.603418969105));
#142864=CARTESIAN_POINT('Ctrl Pts',(158.250233011514,4.63813282568165,134.481362405539));
#142865=CARTESIAN_POINT('Ctrl Pts',(158.242820232211,4.73244069317407,134.355689333426));
#142866=CARTESIAN_POINT('Ctrl Pts',(158.235396861183,4.82688331217036,134.229836693733));
#142867=CARTESIAN_POINT('Ctrl Pts',(158.227973490154,4.91619457352484,134.100357531433));
#142868=CARTESIAN_POINT('Ctrl Pts',(158.220550119125,5.00010857006147,133.967720358427));
#142869=CARTESIAN_POINT('Ctrl Pts',(158.216614069684,5.04460178451412,133.897392946713));
#142870=CARTESIAN_POINT('Ctrl Pts',(158.212678020244,5.0875784095031,133.82617810226));
#142871=CARTESIAN_POINT('Ctrl Pts',(158.208741970803,5.12900423244793,133.754148092289));
#142872=CARTESIAN_POINT('Ctrl Pts',(158.201318704397,5.20713204166579,133.618301741464));
#142873=CARTESIAN_POINT('Ctrl Pts',(158.193895437992,5.27997723979626,133.479143902046));
#142874=CARTESIAN_POINT('Ctrl Pts',(158.186472171586,5.34724599243546,133.337124100184));
#142875=CARTESIAN_POINT('Ctrl Pts',(158.179057678865,5.41443523899529,133.195272153933));
#142876=CARTESIAN_POINT('Ctrl Pts',(158.171643186144,5.4760610010417,133.050565312398));
#142877=CARTESIAN_POINT('Ctrl Pts',(158.164228693423,5.53187373575638,132.903480322144));
#142878=CARTESIAN_POINT('Ctrl Pts',(158.15682134707,5.58763267605594,132.756537097942));
#142879=CARTESIAN_POINT('Ctrl Pts',(158.149414000716,5.63758961157662,132.607220634913));
#142880=CARTESIAN_POINT('Ctrl Pts',(158.142006654362,5.68154184490677,132.456030326398));
#142881=CARTESIAN_POINT('Ctrl Pts',(158.134604832687,5.72546129700346,132.304952781318));
#142882=CARTESIAN_POINT('Ctrl Pts',(158.127203011011,5.76338486051576,132.152004530449));
#142883=CARTESIAN_POINT('Ctrl Pts',(158.119801189336,5.7951587548607,131.997702801712));
#142884=CARTESIAN_POINT('Ctrl Pts',(158.112403275024,5.82691587601384,131.843482527657));
#142885=CARTESIAN_POINT('Ctrl Pts',(158.105005360713,5.85252971818674,131.687910563377));
#142886=CARTESIAN_POINT('Ctrl Pts',(158.097607446402,5.87189698470698,131.53151697179));
#142887=CARTESIAN_POINT('Ctrl Pts',(158.09021076149,5.89126103273897,131.375149369981));
#142888=CARTESIAN_POINT('Ctrl Pts',(158.082814076577,5.90438051954253,131.21796078196));
#142889=CARTESIAN_POINT('Ctrl Pts',(158.075417391665,5.91120365996612,131.060489204223));
#142890=CARTESIAN_POINT('Ctrl Pts',(158.06802103473,5.91802649784452,130.903024608941));
#142891=CARTESIAN_POINT('Ctrl Pts',(158.060624677794,5.91855352830065,130.745277421841));
#142892=CARTESIAN_POINT('Ctrl Pts',(158.053228320859,5.91278504197351,130.587788204932));
#142893=CARTESIAN_POINT('Ctrl Pts',(158.045830831522,5.90701567247639,130.430274876021));
#142894=CARTESIAN_POINT('Ctrl Pts',(158.038433342186,5.89494888068794,130.273019969015));
#142895=CARTESIAN_POINT('Ctrl Pts',(158.031035852849,5.87663702380465,130.116561335109));
#142896=CARTESIAN_POINT('Ctrl Pts',(158.023635770334,5.85831874772836,129.960047854871));
#142897=CARTESIAN_POINT('Ctrl Pts',(158.016235687819,5.83375109124769,129.80433157402));
#142898=CARTESIAN_POINT('Ctrl Pts',(158.008835605304,5.80303792079846,129.649942386475));
#142899=CARTESIAN_POINT('Ctrl Pts',(158.001427385638,5.77229097806086,129.495383432147));
#142900=CARTESIAN_POINT('Ctrl Pts',(157.994019165971,5.73538509881401,129.342154851743));
#142901=CARTESIAN_POINT('Ctrl Pts',(157.986610946305,5.69247482843885,129.190774273397));
#142902=CARTESIAN_POINT('Ctrl Pts',(157.979198167002,5.6495381475081,129.03930052283));
#142903=CARTESIAN_POINT('Ctrl Pts',(157.9717853877,5.60058982729749,128.889677394733));
#142904=CARTESIAN_POINT('Ctrl Pts',(157.964372608398,5.54583321845891,128.74240414966));
#142905=CARTESIAN_POINT('Ctrl Pts',(157.95694923737,5.49099837081001,128.594920473669));
#142906=CARTESIAN_POINT('Ctrl Pts',(157.949525866341,5.43033880283783,128.449793730138));
#142907=CARTESIAN_POINT('Ctrl Pts',(157.942102495312,5.36410495754869,128.307500876431));
#142908=CARTESIAN_POINT('Ctrl Pts',(157.938166445871,5.32898618351717,128.232053791125));
#142909=CARTESIAN_POINT('Ctrl Pts',(157.93423039643,5.29230103353882,128.157402976415));
#142910=CARTESIAN_POINT('Ctrl Pts',(157.93029434699,5.25409181533825,128.083616278512));
#142911=CARTESIAN_POINT('Ctrl Pts',(157.922871080584,5.18203042228066,127.94445686907));
#142912=CARTESIAN_POINT('Ctrl Pts',(157.915447814179,5.10432759975642,127.807951929475));
#142913=CARTESIAN_POINT('Ctrl Pts',(157.908024547773,5.02120272217172,127.674591650796));
#142914=CARTESIAN_POINT('Ctrl Pts',(157.900610055052,4.9381760912894,127.541388992892));
#142915=CARTESIAN_POINT('Ctrl Pts',(157.893195562331,4.84974035687387,127.411323911439));
#142916=CARTESIAN_POINT('Ctrl Pts',(157.88578106961,4.75616173532534,127.284864047042));
#142917=CARTESIAN_POINT('Ctrl Pts',(157.878373723257,4.66267330837544,127.158526069424));
#142918=CARTESIAN_POINT('Ctrl Pts',(157.870966376903,4.56405208308138,127.035786689192));
#142919=CARTESIAN_POINT('Ctrl Pts',(157.863559030549,4.4606086503039,126.917086375718));
#142920=CARTESIAN_POINT('Ctrl Pts',(157.856157208874,4.35724236954085,126.798474593416));
#142921=CARTESIAN_POINT('Ctrl Pts',(157.848755387198,4.24906128677821,126.683896159819));
#142922=CARTESIAN_POINT('Ctrl Pts',(157.841353565523,4.13641743835362,126.573760029212));
#142923=CARTESIAN_POINT('Ctrl Pts',(157.833955651211,4.02383305374083,126.463682038611));
#142924=CARTESIAN_POINT('Ctrl Pts',(157.8265577369,3.90679086151295,126.35804194102));
#142925=CARTESIAN_POINT('Ctrl Pts',(157.819159822589,3.78568098424077,126.257213154809));
#142926=CARTESIAN_POINT('Ctrl Pts',(157.811763137677,3.66459123323212,126.156401124512));
#142927=CARTESIAN_POINT('Ctrl Pts',(157.804366452764,3.53943542539678,126.060399057331));
#142928=CARTESIAN_POINT('Ctrl Pts',(157.796969767852,3.41063820128344,125.969541321827));
#142929=CARTESIAN_POINT('Ctrl Pts',(157.789573410917,3.2818466881739,125.878687615051));
#142930=CARTESIAN_POINT('Ctrl Pts',(157.782177053981,3.14941438486853,125.792978001585));
#142931=CARTESIAN_POINT('Ctrl Pts',(157.774780697046,3.01379623859334,125.712704423876));
#142932=CARTESIAN_POINT('Ctrl Pts',(157.767383207709,2.87815732883389,125.632418556078));
#142933=CARTESIAN_POINT('Ctrl Pts',(157.759985718373,2.73933192617019,125.557570571358));
#142934=CARTESIAN_POINT('Ctrl Pts',(157.752588229036,2.59780084038886,125.488407141831));
#142935=CARTESIAN_POINT('Ctrl Pts',(157.745188146521,2.45622014110446,125.419219467172));
#142936=CARTESIAN_POINT('Ctrl Pts',(157.737788064006,2.31193220548298,125.355720478979));
#142937=CARTESIAN_POINT('Ctrl Pts',(157.730387981491,2.16543899063345,125.298109212087));
#142938=CARTESIAN_POINT('Ctrl Pts',(157.722979761825,2.01878469143474,125.240434595684));
#142939=CARTESIAN_POINT('Ctrl Pts',(157.715571542158,1.86992061787313,125.188660766598));
#142940=CARTESIAN_POINT('Ctrl Pts',(157.708163322492,1.71936580071042,125.142937492075));
#142941=CARTESIAN_POINT('Ctrl Pts',(157.70075054319,1.56871831956924,125.097186075638));
#142942=CARTESIAN_POINT('Ctrl Pts',(157.693337763888,1.41637838165166,125.057492728236));
#142943=CARTESIAN_POINT('Ctrl Pts',(157.685924984585,1.26287594499535,125.023956227729));
#142944=CARTESIAN_POINT('Ctrl Pts',(157.678501613557,1.1091541768597,124.990371808697));
#142945=CARTESIAN_POINT('Ctrl Pts',(157.671078242528,0.95426695914299,124.962961871404));
#142946=CARTESIAN_POINT('Ctrl Pts',(157.663654871499,0.798750940145906,
124.94177351816));
#142947=CARTESIAN_POINT('Ctrl Pts',(157.659718822058,0.716292615317222,
124.930538944863));
#142948=CARTESIAN_POINT('Ctrl Pts',(157.655782772618,0.633657551031939,
124.921052611719));
#142949=CARTESIAN_POINT('Ctrl Pts',(157.651846723177,0.550925696587703,
124.913315596575));
#142950=CARTESIAN_POINT('Ctrl Pts',(157.644423456771,0.394896001079837,
124.898723827478));
#142951=CARTESIAN_POINT('Ctrl Pts',(157.637000190366,0.238050255806775,
124.890313158557));
#142952=CARTESIAN_POINT('Ctrl Pts',(157.62957692396,0.0809194496225133,
124.888163984156));
#142953=CARTESIAN_POINT('Ctrl Pts',(157.622162431239,-0.0760256409977402,
124.886017349901));
#142954=CARTESIAN_POINT('Ctrl Pts',(157.614747938518,-0.233254752273388,
124.890117484353));
#142955=CARTESIAN_POINT('Ctrl Pts',(157.607333445797,-0.390230548452075,
124.900493183286));
#142956=CARTESIAN_POINT('Ctrl Pts',(157.599926099444,-0.547055045447757,
124.910858881729));
#142957=CARTESIAN_POINT('Ctrl Pts',(157.59251875309,-0.703626343425722,
124.927488078575));
#142958=CARTESIAN_POINT('Ctrl Pts',(157.585111406736,-0.859405981080647,
124.950357549393));
#142959=CARTESIAN_POINT('Ctrl Pts',(157.577709585061,-1.01506943240597,
124.973209963296));
#142960=CARTESIAN_POINT('Ctrl Pts',(157.570307763385,-1.16994203132464,
125.002293329978));
#142961=CARTESIAN_POINT('Ctrl Pts',(157.56290594171,-1.32348942877478,125.03753252108));
#142962=CARTESIAN_POINT('Ctrl Pts',(157.555508027398,-1.47695576974743,
125.072753109686));
#142963=CARTESIAN_POINT('Ctrl Pts',(157.548110113087,-1.62909793954779,
125.114122967664));
#142964=CARTESIAN_POINT('Ctrl Pts',(157.540712198776,-1.7793908999459,125.161515715596));
#142965=CARTESIAN_POINT('Ctrl Pts',(157.533315513864,-1.92965888438154,
125.208900587713));
#142966=CARTESIAN_POINT('Ctrl Pts',(157.525918828951,-2.07807791365631,
125.26230625115));
#142967=CARTESIAN_POINT('Ctrl Pts',(157.518522144039,-2.22413714544071,
125.32155617816));
#142968=CARTESIAN_POINT('Ctrl Pts',(157.511125787104,-2.37018990080557,
125.380803477966));
#142969=CARTESIAN_POINT('Ctrl Pts',(157.503729430168,-2.51388272081235,
125.445894385763));
#142970=CARTESIAN_POINT('Ctrl Pts',(157.496333073233,-2.65472407592328,
125.516603943587));
#142971=CARTESIAN_POINT('Ctrl Pts',(157.488935583896,-2.79558699420534,
125.587324327225));
#142972=CARTESIAN_POINT('Ctrl Pts',(157.48153809456,-2.9335972446944,125.66366490622));
#142973=CARTESIAN_POINT('Ctrl Pts',(157.474140605223,-3.06828740571877,
125.745354493987));
#142974=CARTESIAN_POINT('Ctrl Pts',(157.466740522708,-3.2030247821701,125.827072717912));
#142975=CARTESIAN_POINT('Ctrl Pts',(157.459340440193,-3.33443943295326,
125.91414349043));
#142976=CARTESIAN_POINT('Ctrl Pts',(157.451940357678,-3.46209258434725,
126.006252083997));
#142977=CARTESIAN_POINT('Ctrl Pts',(157.444532138012,-3.58988610350434,
126.098461960432));
#142978=CARTESIAN_POINT('Ctrl Pts',(157.437123918345,-3.71390956019198,
126.195720502302));
#142979=CARTESIAN_POINT('Ctrl Pts',(157.429715698679,-3.83375640218153,
126.297671987182));
#142980=CARTESIAN_POINT('Ctrl Pts',(157.422302919377,-3.95367700790322,
126.3996862215));
#142981=CARTESIAN_POINT('Ctrl Pts',(157.414890140075,-4.06941560280145,
126.506398901927));
#142982=CARTESIAN_POINT('Ctrl Pts',(157.407477360772,-4.18060262699952,
126.617417551602));
#142983=CARTESIAN_POINT('Ctrl Pts',(157.400053989744,-4.29194852043124,
126.728594829929));
#142984=CARTESIAN_POINT('Ctrl Pts',(157.392630618715,-4.39872960147221,
126.844090092197));
#142985=CARTESIAN_POINT('Ctrl Pts',(157.385207247686,-4.50061617009897,
126.963477300939));
#142986=CARTESIAN_POINT('Ctrl Pts',(157.381271198245,-4.55463887352011,
127.026779263672));
#142987=CARTESIAN_POINT('Ctrl Pts',(157.377335148805,-4.60728626498116,
127.091174888821));
#142988=CARTESIAN_POINT('Ctrl Pts',(157.373399099364,-4.65851422311026,
127.15659749538));
#142989=CARTESIAN_POINT('Ctrl Pts',(157.365689769899,-4.75885168404861,
127.284737254798));
#142990=CARTESIAN_POINT('Ctrl Pts',(157.357980440434,-4.85406153169077,
127.41722862095));
#142991=CARTESIAN_POINT('Ctrl Pts',(157.35027111097,-4.94374546843798,127.553620500947));
#142992=CARTESIAN_POINT('Ctrl Pts',(157.342858577229,-5.02997673020698,
127.684761531701));
#142993=CARTESIAN_POINT('Ctrl Pts',(157.335446043488,-5.11109935062457,
127.819508015262));
#142994=CARTESIAN_POINT('Ctrl Pts',(157.328033509748,-5.18679860691237,
127.957423531181));
#142995=CARTESIAN_POINT('Ctrl Pts',(157.320628026987,-5.26242585625219,
128.095207858554));
#142996=CARTESIAN_POINT('Ctrl Pts',(157.313222544226,-5.33263983071511,
128.236154894347));
#142997=CARTESIAN_POINT('Ctrl Pts',(157.305817061465,-5.39716886407673,
128.37979904583));
#142998=CARTESIAN_POINT('Ctrl Pts',(157.298417163401,-5.4616492341606,128.523334870953));
#142999=CARTESIAN_POINT('Ctrl Pts',(157.291017265337,-5.52045304536111,
128.669563424275));
#143000=CARTESIAN_POINT('Ctrl Pts',(157.283617367272,-5.57335445625534,
128.817994420854));
#143001=CARTESIAN_POINT('Ctrl Pts',(157.276221591408,-5.62622639779663,
128.966342732202));
#143002=CARTESIAN_POINT('Ctrl Pts',(157.268825815544,-5.67320236126874,
129.116890693481));
#143003=CARTESIAN_POINT('Ctrl Pts',(157.26143003968,-5.71410461872065,129.269128072049));
#143004=CARTESIAN_POINT('Ctrl Pts',(157.254036397143,-5.75499507783323,
129.421321537436));
#143005=CARTESIAN_POINT('Ctrl Pts',(157.246642754605,-5.78981522071373,
129.575203090644));
#143006=CARTESIAN_POINT('Ctrl Pts',(157.239249112068,-5.81843719116697,
129.730247394975));
#143007=CARTESIAN_POINT('Ctrl Pts',(157.231856662052,-5.84705454517623,
129.885266692176));
#143008=CARTESIAN_POINT('Ctrl Pts',(157.224464212037,-5.8694756532606,130.041447999862));
#143009=CARTESIAN_POINT('Ctrl Pts',(157.217071762022,-5.8856238307037,130.198256100215));
#143010=CARTESIAN_POINT('Ctrl Pts',(157.209677888262,-5.90177511819504,
130.355094400928));
#143011=CARTESIAN_POINT('Ctrl Pts',(157.202284014502,-5.91165102567913,
130.512559364308));
#143012=CARTESIAN_POINT('Ctrl Pts',(157.194890140743,-5.91522675507618,
130.670110855812));
#143013=CARTESIAN_POINT('Ctrl Pts',(157.192718491232,-5.91627698006614,
130.716385194614));
#143014=CARTESIAN_POINT('Ctrl Pts',(157.190546841722,-5.91678406166311,
130.762666987724));
#143015=CARTESIAN_POINT('Ctrl Pts',(157.188375192211,-5.91674822587776,
130.808942546454));
#143016=CARTESIAN_POINT('',(155.438375192211,-5.9258497230187,130.806193117355));
#143017=CARTESIAN_POINT('Ctrl Pts',(157.188373110924,-5.9110709125586,130.808982457434));
#143018=CARTESIAN_POINT('Ctrl Pts',(157.157232565799,-5.91582530741731,
131.471921867218));
#143019=CARTESIAN_POINT('Ctrl Pts',(157.033276146074,-5.5065273811508,134.105074895486));
#143020=CARTESIAN_POINT('Ctrl Pts',(156.816503851736,-1.63383274564036,
137.60936988204));
#143021=CARTESIAN_POINT('Ctrl Pts',(156.538056227926,4.84212051448032,135.857224108064));
#143022=CARTESIAN_POINT('Ctrl Pts',(156.259608604111,6.86840157253082,129.461743632418));
#143023=CARTESIAN_POINT('Ctrl Pts',(155.981160980299,2.58295712549506,124.300062575641));
#143024=CARTESIAN_POINT('Ctrl Pts',(155.707416509666,-3.96362314909615,
125.101740191743));
#143025=CARTESIAN_POINT('Ctrl Pts',(155.526487913636,-5.91829371355799,
128.942418927956));
#143026=CARTESIAN_POINT('Ctrl Pts',(155.438375192211,-5.9258497230187,130.806193117355));
#143027=CARTESIAN_POINT('',(153.688375192211,-5.91665636044548,130.798893010347));
#143028=CARTESIAN_POINT('Ctrl Pts',(155.438375192211,-5.9258497230187,130.806193117355));
#143029=CARTESIAN_POINT('Ctrl Pts',(155.433672039032,-5.92625303674393,
130.905674955648));
#143030=CARTESIAN_POINT('Ctrl Pts',(155.428968885853,-5.92396577613154,
131.005137856645));
#143031=CARTESIAN_POINT('Ctrl Pts',(155.331449858069,-5.81954753850361,
133.064593445196));
#143032=CARTESIAN_POINT('Ctrl Pts',(155.145818108861,-3.47980464159975,
136.876305955482));
#143033=CARTESIAN_POINT('Ctrl Pts',(154.867370485047,3.22758017148122,137.014053586386));
#143034=CARTESIAN_POINT('Ctrl Pts',(154.588922861235,6.96897648302375,131.44539673931));
#143035=CARTESIAN_POINT('Ctrl Pts',(154.310475237422,4.30622386010103,125.287659012708));
#143036=CARTESIAN_POINT('Ctrl Pts',(154.032027613609,-2.31373811952758,
124.199500555112));
#143037=CARTESIAN_POINT('Ctrl Pts',(153.824660931872,-5.66034222041055,
127.909258680071));
#143038=CARTESIAN_POINT('Ctrl Pts',(153.710110124739,-5.92092250522073,
130.337292720254));
#143039=CARTESIAN_POINT('Ctrl Pts',(153.688375192211,-5.91665636044548,
130.798893010347));
#143040=CARTESIAN_POINT('',(151.938375192211,-5.9069934382874,130.80498290727));
#143041=CARTESIAN_POINT('Ctrl Pts',(153.688375192211,-5.91665636044548,
130.798893010347));
#143042=CARTESIAN_POINT('Ctrl Pts',(153.617294250135,-5.90270455317563,
132.308489759256));
#143043=CARTESIAN_POINT('Ctrl Pts',(153.453397433455,-4.5460332507832,135.811571704644));
#143044=CARTESIAN_POINT('Ctrl Pts',(153.196684742169,1.35306796840206,137.670711002101));
#143045=CARTESIAN_POINT('Ctrl Pts',(152.918237118358,6.50822133110401,133.377416317647));
#143046=CARTESIAN_POINT('Ctrl Pts',(152.639789494545,5.68263723480749,126.719609145577));
#143047=CARTESIAN_POINT('Ctrl Pts',(152.361341870732,-0.365012868011487,
123.81548902506));
#143048=CARTESIAN_POINT('Ctrl Pts',(152.127537103287,-5.16140692478195,
126.769717825966));
#143049=CARTESIAN_POINT('Ctrl Pts',(151.986548210447,-5.90603325491028,
129.777671834643));
#143050=CARTESIAN_POINT('Ctrl Pts',(151.938375192211,-5.9069934382874,130.80498290727));
#143051=CARTESIAN_POINT('',(150.188375920137,-5.91832258703425,130.809599870259));
#143052=CARTESIAN_POINT('Ctrl Pts',(151.938375192211,-5.9069934382874,130.80498290727));
#143053=CARTESIAN_POINT('Ctrl Pts',(151.893732335843,-5.90788325856775,
131.75701170556));
#143054=CARTESIAN_POINT('Ctrl Pts',(151.756273604869,-5.24038079272229,
134.687203035383));
#143055=CARTESIAN_POINT('Ctrl Pts',(151.525998999293,-0.63042978355948,
137.774304578484));
#143056=CARTESIAN_POINT('Ctrl Pts',(151.247551375479,5.52324855627425,135.102184010395));
#143057=CARTESIAN_POINT('Ctrl Pts',(150.969103751667,6.60133129858417,128.480573704642));
#143058=CARTESIAN_POINT('Ctrl Pts',(150.690656127853,1.61311307045599,123.994410048561));
#143059=CARTESIAN_POINT('Ctrl Pts',(150.430413613649,-4.43442532867792,
125.650413545519));
#143060=CARTESIAN_POINT('Ctrl Pts',(150.262986974047,-5.90431344697162,
129.226604649882));
#143061=CARTESIAN_POINT('Ctrl Pts',(150.188376209049,-5.91894766702673,
130.809594295568));
#143062=CARTESIAN_POINT('',(148.438373822973,-5.92114154475418,130.801327303241));
#143063=CARTESIAN_POINT('Ctrl Pts',(150.188375192211,-5.91674766787937,
130.809613915962));
#143064=CARTESIAN_POINT('Ctrl Pts',(150.177611091204,-5.91654497524426,
131.037904998178));
#143065=CARTESIAN_POINT('Ctrl Pts',(150.166846990196,-5.90312653602111,
131.265633413056));
#143066=CARTESIAN_POINT('Ctrl Pts',(150.156082889189,-5.87670615149839,
131.491569007678));
#143067=CARTESIAN_POINT('Ctrl Pts',(150.148642219535,-5.8584430979265,131.647746669091));
#143068=CARTESIAN_POINT('Ctrl Pts',(150.141201549882,-5.833968323526,131.803068599181));
#143069=CARTESIAN_POINT('Ctrl Pts',(150.133760880228,-5.80336442728749,
131.957136348831));
#143070=CARTESIAN_POINT('Ctrl Pts',(150.126337613823,-5.77283211159509,
132.110843743918));
#143071=CARTESIAN_POINT('Ctrl Pts',(150.118914347417,-5.73614278899573,
132.263569710176));
#143072=CARTESIAN_POINT('Ctrl Pts',(150.111491081012,-5.69337090573593,
132.414782392201));
#143073=CARTESIAN_POINT('Ctrl Pts',(150.104076588291,-5.65064957529008,
132.565816353394));
#143074=CARTESIAN_POINT('Ctrl Pts',(150.096662095569,-5.60186009470238,
132.715340234829));
#143075=CARTESIAN_POINT('Ctrl Pts',(150.089247602848,-5.54712817490362,
132.86283081985));
#143076=CARTESIAN_POINT('Ctrl Pts',(150.081840256495,-5.49244900778982,
133.010179247892));
#143077=CARTESIAN_POINT('Ctrl Pts',(150.074432910141,-5.43183893288328,
133.155497933402));
#143078=CARTESIAN_POINT('Ctrl Pts',(150.067025563787,-5.36547384017928,
133.298277423085));
#143079=CARTESIAN_POINT('Ctrl Pts',(150.059623742112,-5.29915824506516,
133.440950422439));
#143080=CARTESIAN_POINT('Ctrl Pts',(150.052221920436,-5.22709633538908,
133.581087659771));
#143081=CARTESIAN_POINT('Ctrl Pts',(150.044820098761,-5.14951257434729,
133.718198432054));
#143082=CARTESIAN_POINT('Ctrl Pts',(150.037422184449,-5.07196976916916,
133.855236824627));
#143083=CARTESIAN_POINT('Ctrl Pts',(150.030024270138,-4.98891110124634,
133.989251609871));
#143084=CARTESIAN_POINT('Ctrl Pts',(150.022626355827,-4.90060749800784,
134.119775631251));
#143085=CARTESIAN_POINT('Ctrl Pts',(150.015229670914,-4.81231856922621,
134.250277961907));
#143086=CARTESIAN_POINT('Ctrl Pts',(150.007832986002,-4.71878664399335,
134.377290371145));
#143087=CARTESIAN_POINT('Ctrl Pts',(150.00043630109,-4.62032666329727,134.500373616315));
#143088=CARTESIAN_POINT('Ctrl Pts',(149.993039944155,-4.52187104841988,
134.623451403846));
#143089=CARTESIAN_POINT('Ctrl Pts',(149.985643587219,-4.41848804574877,
134.742600082219));
#143090=CARTESIAN_POINT('Ctrl Pts',(149.978247230284,-4.31053350321053,
134.857412736673));
#143091=CARTESIAN_POINT('Ctrl Pts',(149.970849740947,-4.20256243255607,
134.972242969238));
#143092=CARTESIAN_POINT('Ctrl Pts',(149.963452251611,-4.0900186841422,135.08273558408));
#143093=CARTESIAN_POINT('Ctrl Pts',(149.956054762274,-3.97329553464828,
135.188519961938));
#143094=CARTESIAN_POINT('Ctrl Pts',(149.948654679759,-3.8565314680353,135.294341422345));
#143095=CARTESIAN_POINT('Ctrl Pts',(149.941254597244,-3.73558535980521,
135.395451109179));
#143096=CARTESIAN_POINT('Ctrl Pts',(149.933854514729,-3.61088404408494,
135.491518283217));
#143097=CARTESIAN_POINT('Ctrl Pts',(149.926446295062,-3.48604560644852,
135.587691092989));
#143098=CARTESIAN_POINT('Ctrl Pts',(149.919038075396,-3.35744401086744,
135.678810088757));
#143099=CARTESIAN_POINT('Ctrl Pts',(149.911629855729,-3.22553618908989,
135.764587109912));
#143100=CARTESIAN_POINT('Ctrl Pts',(149.904217076427,-3.09354718024895,
135.850416925392));
#143101=CARTESIAN_POINT('Ctrl Pts',(149.896804297125,-2.9582482104489,135.930898024315));
#143102=CARTESIAN_POINT('Ctrl Pts',(149.889391517823,-2.82012088367187,
136.005788187376));
#143103=CARTESIAN_POINT('Ctrl Pts',(149.881968146794,-2.68179619409281,
136.080785357013));
#143104=CARTESIAN_POINT('Ctrl Pts',(149.874544775766,-2.54063541029859,
136.150175471535));
#143105=CARTESIAN_POINT('Ctrl Pts',(149.867121404737,-2.39714092929154,
136.213764090003));
#143106=CARTESIAN_POINT('Ctrl Pts',(149.863185355297,-2.3210567123676,136.247480301299));
#143107=CARTESIAN_POINT('Ctrl Pts',(149.859249305856,-2.24431668899597,
136.279566329056));
#143108=CARTESIAN_POINT('Ctrl Pts',(149.855313256416,-2.16699735698748,
136.309998910926));
#143109=CARTESIAN_POINT('Ctrl Pts',(149.84788999001,-2.02117550985723,136.36739381057));
#143110=CARTESIAN_POINT('Ctrl Pts',(149.840466723605,-1.87285135396975,
136.419078159672));
#143111=CARTESIAN_POINT('Ctrl Pts',(149.8330434572,-1.72251259435359,136.464827111133));
#143112=CARTESIAN_POINT('Ctrl Pts',(149.825628964479,-1.57235152266629,
136.510521991132));
#143113=CARTESIAN_POINT('Ctrl Pts',(149.818214471758,-1.42018094047277,
136.550295329563));
#143114=CARTESIAN_POINT('Ctrl Pts',(149.810799979037,-1.2665089945928,136.583970079209));
#143115=CARTESIAN_POINT('Ctrl Pts',(149.803392632683,-1.11298516351992,
136.617612371864));
#143116=CARTESIAN_POINT('Ctrl Pts',(149.795985286329,-0.957963211791275,
136.645167698403));
#143117=CARTESIAN_POINT('Ctrl Pts',(149.788577939975,-0.80196682973234,
136.666508668111));
#143118=CARTESIAN_POINT('Ctrl Pts',(149.7811761183,-0.64608679566044,136.687833720919));
#143119=CARTESIAN_POINT('Ctrl Pts',(149.773774296625,-0.489234146610383,
136.70295359523));
#143120=CARTESIAN_POINT('Ctrl Pts',(149.766372474949,-0.331943052779465,
136.711791901315));
#143121=CARTESIAN_POINT('Ctrl Pts',(149.758974560638,-0.174734991692686,
136.720625541726));
#143122=CARTESIAN_POINT('Ctrl Pts',(149.751576646326,-0.0170893185384864,
136.723184196977));
#143123=CARTESIAN_POINT('Ctrl Pts',(149.744178732015,0.140454491766542,
136.719443296468));
#143124=CARTESIAN_POINT('Ctrl Pts',(149.736782047103,0.297972121148322,
136.715703017628));
#143125=CARTESIAN_POINT('Ctrl Pts',(149.729385362191,0.455387548450213,
136.705665269612));
#143126=CARTESIAN_POINT('Ctrl Pts',(149.721988677278,0.612160993094913,
136.689357599811));
#143127=CARTESIAN_POINT('Ctrl Pts',(149.714592320343,0.768927486240734,
136.673050653109));
#143128=CARTESIAN_POINT('Ctrl Pts',(149.707195963407,0.925051682035538,
136.650474376033));
#143129=CARTESIAN_POINT('Ctrl Pts',(149.699799606472,1.07999888706843,136.621708206152));
#143130=CARTESIAN_POINT('Ctrl Pts',(149.692402117135,1.23496981491403,136.592937632097));
#143131=CARTESIAN_POINT('Ctrl Pts',(149.685004627799,1.38876302614496,136.557975346407));
#143132=CARTESIAN_POINT('Ctrl Pts',(149.677607138462,1.54085413262811,136.516951895127));
#143133=CARTESIAN_POINT('Ctrl Pts',(149.670207055947,1.69299855441292,136.475914063139));
#143134=CARTESIAN_POINT('Ctrl Pts',(149.662806973432,1.84343932329165,136.428810932389));
#143135=CARTESIAN_POINT('Ctrl Pts',(149.655406890917,1.99166746471887,136.375822837888));
#143136=CARTESIAN_POINT('Ctrl Pts',(149.647998671251,2.14005859822582,136.322776477531));
#143137=CARTESIAN_POINT('Ctrl Pts',(149.640590451584,2.28623189366907,136.263832355901));
#143138=CARTESIAN_POINT('Ctrl Pts',(149.633182231918,2.42969793059621,136.199219144771));
#143139=CARTESIAN_POINT('Ctrl Pts',(149.625769452616,2.57325226847531,136.134566165288));
#143140=CARTESIAN_POINT('Ctrl Pts',(149.618356673314,2.71409569438009,136.064237309958));
#143141=CARTESIAN_POINT('Ctrl Pts',(149.610943894012,2.85176410363253,135.988506840401));
#143142=CARTESIAN_POINT('Ctrl Pts',(149.603520522983,2.98962921996412,135.912668163597));
#143143=CARTESIAN_POINT('Ctrl Pts',(149.596097151954,3.12430994022576,135.831412650158));
#143144=CARTESIAN_POINT('Ctrl Pts',(149.588673780925,3.25537111789792,135.745057880833));
#143145=CARTESIAN_POINT('Ctrl Pts',(149.584737731484,3.32486289907089,135.699270510082));
#143146=CARTESIAN_POINT('Ctrl Pts',(149.580801682043,3.39333764006722,135.652050236771));
#143147=CARTESIAN_POINT('Ctrl Pts',(149.576865632603,3.46073442067854,135.603448846806));
#143148=CARTESIAN_POINT('Ctrl Pts',(149.569442366197,3.58784264552746,135.511788142132));
#143149=CARTESIAN_POINT('Ctrl Pts',(149.562019099792,3.71149898148062,135.414935482176));
#143150=CARTESIAN_POINT('Ctrl Pts',(149.554595833386,3.83125064182295,135.31317965164));
#143151=CARTESIAN_POINT('Ctrl Pts',(149.547181340665,3.95086076564756,135.211544088046));
#143152=CARTESIAN_POINT('Ctrl Pts',(149.539766847944,4.06657511835765,135.105017128492));
#143153=CARTESIAN_POINT('Ctrl Pts',(149.532352355223,4.1779700793475,134.993930592943));
#143154=CARTESIAN_POINT('Ctrl Pts',(149.524945008869,4.28925767368004,134.882951126779));
#143155=CARTESIAN_POINT('Ctrl Pts',(149.517537662516,4.39623390183603,134.76742109541));
#143156=CARTESIAN_POINT('Ctrl Pts',(149.510130316162,4.49850851898521,134.647712236546));
#143157=CARTESIAN_POINT('Ctrl Pts',(149.502728494487,4.60070685586633,134.528092661065));
#143158=CARTESIAN_POINT('Ctrl Pts',(149.495326672811,4.69821032249184,134.40430074651));
#143159=CARTESIAN_POINT('Ctrl Pts',(149.487924851136,4.790665917979,134.276744614882));
#143160=CARTESIAN_POINT('Ctrl Pts',(149.480526936824,4.88307270687708,134.149255819142));
#143161=CARTESIAN_POINT('Ctrl Pts',(149.473129022513,4.97043671305392,134.018007065221));
#143162=CARTESIAN_POINT('Ctrl Pts',(149.465731108202,5.05244566519888,133.883438947637));
#143163=CARTESIAN_POINT('Ctrl Pts',(149.458334423289,5.13444098894366,133.748893192833));
#143164=CARTESIAN_POINT('Ctrl Pts',(149.450937738377,5.21108283079605,133.611029487619));
#143165=CARTESIAN_POINT('Ctrl Pts',(149.443541053465,5.28210260257023,133.47031685472));
#143166=CARTESIAN_POINT('Ctrl Pts',(149.43614469653,5.3531192252533,133.329610461167));
#143167=CARTESIAN_POINT('Ctrl Pts',(149.428748339594,5.41851410532828,133.186055724362));
#143168=CARTESIAN_POINT('Ctrl Pts',(149.421351982659,5.47806506102332,133.040145434961));
#143169=CARTESIAN_POINT('Ctrl Pts',(149.413954493322,5.53762513412174,132.894212806323));
#143170=CARTESIAN_POINT('Ctrl Pts',(149.406557003986,5.59133936026565,132.745924252647));
#143171=CARTESIAN_POINT('Ctrl Pts',(149.399159514649,5.63903412694477,132.595791519848));
#143172=CARTESIAN_POINT('Ctrl Pts',(149.391759432134,5.68674561295041,132.445606158253));
#143173=CARTESIAN_POINT('Ctrl Pts',(149.384359349619,5.72843332531943,132.293575685963));
#143174=CARTESIAN_POINT('Ctrl Pts',(149.376959267104,5.76397387183037,132.140225793157));
#143175=CARTESIAN_POINT('Ctrl Pts',(149.369551047438,5.79955349882585,131.98670727638));
#143176=CARTESIAN_POINT('Ctrl Pts',(149.362142827771,5.82897237658241,131.831866805549));
#143177=CARTESIAN_POINT('Ctrl Pts',(149.354734608105,5.85215834942968,131.676239746632));
#143178=CARTESIAN_POINT('Ctrl Pts',(149.347321828803,5.87535859285637,131.520516901856));
#143179=CARTESIAN_POINT('Ctrl Pts',(149.339909049501,5.89231824704431,131.364006874566));
#143180=CARTESIAN_POINT('Ctrl Pts',(149.332496270198,5.90301719614591,131.207248374275));
#143181=CARTESIAN_POINT('Ctrl Pts',(149.32507289917,5.91373143240772,131.050265890087));
#143182=CARTESIAN_POINT('Ctrl Pts',(149.317649528141,5.91816708673635,130.893034595984));
#143183=CARTESIAN_POINT('Ctrl Pts',(149.310226157112,5.91635614148846,130.73609225321));
#143184=CARTESIAN_POINT('Ctrl Pts',(149.306290107671,5.91539593486498,130.652877657291));
#143185=CARTESIAN_POINT('Ctrl Pts',(149.302354058231,5.91268045167756,130.569744207242));
#143186=CARTESIAN_POINT('Ctrl Pts',(149.29841800879,5.90822033201568,130.486771148508));
#143187=CARTESIAN_POINT('Ctrl Pts',(149.290994742384,5.89980868552901,130.330286549237));
#143188=CARTESIAN_POINT('Ctrl Pts',(149.283571475979,5.88516306975464,130.173899743206));
#143189=CARTESIAN_POINT('Ctrl Pts',(149.276148209573,5.86428170516227,130.018147767888));
#143190=CARTESIAN_POINT('Ctrl Pts',(149.268733716852,5.84342502060875,129.86257987847));
#143191=CARTESIAN_POINT('Ctrl Pts',(149.261319224131,5.81634730665521,129.707645692629));
#143192=CARTESIAN_POINT('Ctrl Pts',(149.25390473141,5.7830987555516,129.553880971175));
#143193=CARTESIAN_POINT('Ctrl Pts',(149.246497385057,5.74988225065333,129.400264453949));
#143194=CARTESIAN_POINT('Ctrl Pts',(149.239090038703,5.7105068276405,129.247815519545));
#143195=CARTESIAN_POINT('Ctrl Pts',(149.231682692349,5.66507430311255,129.097063425302));
#143196=CARTESIAN_POINT('Ctrl Pts',(149.224280870674,5.61967566387543,128.946423767658));
#143197=CARTESIAN_POINT('Ctrl Pts',(149.216879048998,5.56822902555666,128.797478786142));
#143198=CARTESIAN_POINT('Ctrl Pts',(149.209477227323,5.51088694715425,128.650746070303));
#143199=CARTESIAN_POINT('Ctrl Pts',(149.202079313011,5.45357513918877,128.504090813522));
#143200=CARTESIAN_POINT('Ctrl Pts',(149.1946813987,5.39037422468059,128.359645843425));
#143201=CARTESIAN_POINT('Ctrl Pts',(149.187283484389,5.32148609800419,128.217912034809));
#143202=CARTESIAN_POINT('Ctrl Pts',(149.179886799476,5.25260941928464,128.076201779779));
#143203=CARTESIAN_POINT('Ctrl Pts',(149.172490114564,5.17804756718716,127.937202127442));
#143204=CARTESIAN_POINT('Ctrl Pts',(149.165093429652,5.09804996533892,127.801392566885));
#143205=CARTESIAN_POINT('Ctrl Pts',(149.157697072717,5.01805591066821,127.665589028267));
#143206=CARTESIAN_POINT('Ctrl Pts',(149.150300715781,4.93262677495175,127.532975621818));
#143207=CARTESIAN_POINT('Ctrl Pts',(149.142904358846,4.84205706225094,127.404005640743));
#143208=CARTESIAN_POINT('Ctrl Pts',(149.135506869509,4.75147348309586,127.275015914035));
#143209=CARTESIAN_POINT('Ctrl Pts',(149.128109380173,4.65574797441214,127.149671028903));
#143210=CARTESIAN_POINT('Ctrl Pts',(149.120711890836,4.5552172407278,127.028393661636));
#143211=CARTESIAN_POINT('Ctrl Pts',(149.113311808321,4.45465126615065,126.907073780776));
#143212=CARTESIAN_POINT('Ctrl Pts',(149.105911725806,4.3492769509007,126.789824543879));
#143213=CARTESIAN_POINT('Ctrl Pts',(149.098511643291,4.23946987650391,126.677033912698));
#143214=CARTESIAN_POINT('Ctrl Pts',(149.091103423624,4.1295420579403,126.564119256623));
#143215=CARTESIAN_POINT('Ctrl Pts',(149.083695203958,4.0151720065438,126.455673264908));
#143216=CARTESIAN_POINT('Ctrl Pts',(149.076286984291,3.89677113896211,126.352046022543));
#143217=CARTESIAN_POINT('Ctrl Pts',(149.068874204989,3.77829739762201,126.24835499934));
#143218=CARTESIAN_POINT('Ctrl Pts',(149.061461425687,3.65578818641941,126.149488869229));
#143219=CARTESIAN_POINT('Ctrl Pts',(149.054048646385,3.52968586381837,126.055755741893));
#143220=CARTESIAN_POINT('Ctrl Pts',(149.046625275356,3.40340336030519,125.96188868427));
#143221=CARTESIAN_POINT('Ctrl Pts',(149.039201904328,3.27351779906642,125.873169487608));
#143222=CARTESIAN_POINT('Ctrl Pts',(149.031778533299,3.14049890111156,125.789861917335));
#143223=CARTESIAN_POINT('Ctrl Pts',(149.027842483858,3.06996908967165,125.745690244639));
#143224=CARTESIAN_POINT('Ctrl Pts',(149.023906434417,2.99855877869273,125.703039197153));
#143225=CARTESIAN_POINT('Ctrl Pts',(149.019970384977,2.92634039083971,125.661942657166));
#143226=CARTESIAN_POINT('Ctrl Pts',(149.012547118571,2.79013876520704,125.584435865331));
#143227=CARTESIAN_POINT('Ctrl Pts',(149.005123852166,2.65064980312381,125.512226748048));
#143228=CARTESIAN_POINT('Ctrl Pts',(148.99770058576,2.5083243675459,125.445607084357));
#143229=CARTESIAN_POINT('Ctrl Pts',(148.990286093039,2.3661671488134,125.379066159577));
#143230=CARTESIAN_POINT('Ctrl Pts',(148.982871600318,2.22118046449983,125.318101695282));
#143231=CARTESIAN_POINT('Ctrl Pts',(148.975457107597,2.07384219548515,125.262961055116));
#143232=CARTESIAN_POINT('Ctrl Pts',(148.968049761244,1.92664593664134,125.207873561574));
#143233=CARTESIAN_POINT('Ctrl Pts',(148.96064241489,1.77710295261238,125.158598847307));
#143234=CARTESIAN_POINT('Ctrl Pts',(148.953235068536,1.62571355694652,125.115337327645));
#143235=CARTESIAN_POINT('Ctrl Pts',(148.945833246861,1.47443707320333,125.072108074057));
#143236=CARTESIAN_POINT('Ctrl Pts',(148.938431425185,1.32131727724733,125.034883187226));
#143237=CARTESIAN_POINT('Ctrl Pts',(148.93102960351,1.16687209369101,125.003814084741));
#143238=CARTESIAN_POINT('Ctrl Pts',(148.923631689198,1.01250844054517,124.972761383394));
#143239=CARTESIAN_POINT('Ctrl Pts',(148.916233774887,0.856821158249057,
124.947858068111));
#143240=CARTESIAN_POINT('Ctrl Pts',(148.908835860576,0.700340775795215,
124.929205014498));
#143241=CARTESIAN_POINT('Ctrl Pts',(148.901439175664,0.543886397541983,
124.910555060685));
#143242=CARTESIAN_POINT('Ctrl Pts',(148.894042490751,0.386639551023458,
124.898153351213));
#143243=CARTESIAN_POINT('Ctrl Pts',(148.886645805839,0.229138463551447,
124.892049214483));
#143244=CARTESIAN_POINT('Ctrl Pts',(148.879249448904,0.0716443598427598,
124.885945348418));
#143245=CARTESIAN_POINT('Ctrl Pts',(148.871853091968,-0.0861035893867342,
124.886138514327));
#143246=CARTESIAN_POINT('Ctrl Pts',(148.864456735033,-0.243564829087545,
124.892625953651));
#143247=CARTESIAN_POINT('Ctrl Pts',(148.857059245696,-0.401050176506133,
124.899114386219));
#143248=CARTESIAN_POINT('Ctrl Pts',(148.84966175636,-0.558248353987908,
124.911898995629));
#143249=CARTESIAN_POINT('Ctrl Pts',(148.842264267023,-0.714621754978833,
124.930924969684));
#143250=CARTESIAN_POINT('Ctrl Pts',(148.834864184508,-0.871049972423344,
124.949957613264));
#143251=CARTESIAN_POINT('Ctrl Pts',(148.827464101993,-1.02665246739904,
124.975235932525));
#143252=CARTESIAN_POINT('Ctrl Pts',(148.820064019478,-1.1808998257067,125.006653642895));
#143253=CARTESIAN_POINT('Ctrl Pts',(148.812655799812,-1.33531679484166,
125.038105900268));
#143254=CARTESIAN_POINT('Ctrl Pts',(148.805247580145,-1.48837528544521,
125.075710956173));
#143255=CARTESIAN_POINT('Ctrl Pts',(148.797839360479,-1.63955838035195,
125.119311903622));
#143256=CARTESIAN_POINT('Ctrl Pts',(148.790426581177,-1.79083452593109,
125.162939686727));
#143257=CARTESIAN_POINT('Ctrl Pts',(148.783013801875,-1.94023262233649,
125.212570597488));
#143258=CARTESIAN_POINT('Ctrl Pts',(148.775601022573,-2.08725434261052,
125.267999008011));
#143259=CARTESIAN_POINT('Ctrl Pts',(148.768177651544,-2.23448613441307,
125.323506617247));
#143260=CARTESIAN_POINT('Ctrl Pts',(148.760754280515,-2.37933442570295,
125.384828125585));
#143261=CARTESIAN_POINT('Ctrl Pts',(148.753330909486,-2.52132340747843,
125.451710915091));
#143262=CARTESIAN_POINT('Ctrl Pts',(148.749394860046,-2.59660937259654,
125.487173774919));
#143263=CARTESIAN_POINT('Ctrl Pts',(148.745458810605,-2.67109192416717,
125.524199359016));
#143264=CARTESIAN_POINT('Ctrl Pts',(148.741522761164,-2.74470340984099,
125.562745050348));
#143265=CARTESIAN_POINT('Ctrl Pts',(148.734099494758,-2.88353237448325,
125.635441021227));
#143266=CARTESIAN_POINT('Ctrl Pts',(148.726676228353,-3.01968114113617,
125.713766243864));
#143267=CARTESIAN_POINT('Ctrl Pts',(148.719252961947,-3.15266052538826,
125.797499108181));
#143268=CARTESIAN_POINT('Ctrl Pts',(148.711838469226,-3.28548273905141,
125.881133007207));
#143269=CARTESIAN_POINT('Ctrl Pts',(148.704423976505,-3.41514271383474,
125.970161628865));
#143270=CARTESIAN_POINT('Ctrl Pts',(148.697009483784,-3.5411740294112,126.064316624529));
#143271=CARTESIAN_POINT('Ctrl Pts',(148.68960213743,-3.66708387126062,126.158380870064));
#143272=CARTESIAN_POINT('Ctrl Pts',(148.682194791077,-3.78937171956451,
126.257561431142));
#143273=CARTESIAN_POINT('Ctrl Pts',(148.674787444723,-3.90759852753498,
126.361545709188));
#143274=CARTESIAN_POINT('Ctrl Pts',(148.667385623047,-4.02573715749167,
126.465452431836));
#143275=CARTESIAN_POINT('Ctrl Pts',(148.659983801372,-4.13982049891955,
126.574155492152));
#143276=CARTESIAN_POINT('Ctrl Pts',(148.652581979697,-4.24944120900851,
126.687300990395));
#143277=CARTESIAN_POINT('Ctrl Pts',(148.645184065385,-4.35900405117806,
126.800386760011));
#143278=CARTESIAN_POINT('Ctrl Pts',(148.637786151074,-4.4641086945792,126.917910029692));
#143279=CARTESIAN_POINT('Ctrl Pts',(148.630388236762,-4.56438350582768,
127.039478976103));
#143280=CARTESIAN_POINT('Ctrl Pts',(148.62299155185,-4.66464165322159,127.161027719959));
#143281=CARTESIAN_POINT('Ctrl Pts',(148.615594866938,-4.76007132414656,
127.2866205185));
#143282=CARTESIAN_POINT('Ctrl Pts',(148.608198182026,-4.85034009221182,
127.415831209049));
#143283=CARTESIAN_POINT('Ctrl Pts',(148.60080182509,-4.94060485766535,127.545036170261));
#143284=CARTESIAN_POINT('Ctrl Pts',(148.593405468155,-5.02570896148213,
127.677858398495));
#143285=CARTESIAN_POINT('Ctrl Pts',(148.586009111219,-5.10536254130746,
127.81384161841));
#143286=CARTESIAN_POINT('Ctrl Pts',(148.578611621883,-5.18502831629924,
127.949845657703));
#143287=CARTESIAN_POINT('Ctrl Pts',(148.571214132546,-5.25924171703161,
128.08901133017));
#143288=CARTESIAN_POINT('Ctrl Pts',(148.56381664321,-5.32775826908414,128.230856704861));
#143289=CARTESIAN_POINT('Ctrl Pts',(148.556416560695,-5.39629883950763,
128.372751803229));
#143290=CARTESIAN_POINT('Ctrl Pts',(148.54901647818,-5.45913842293072,128.517328138161));
#143291=CARTESIAN_POINT('Ctrl Pts',(148.541616395665,-5.51608027826669,
128.664082849094));
#143292=CARTESIAN_POINT('Ctrl Pts',(148.534208175998,-5.57308474702654,
128.810998931918));
#143293=CARTESIAN_POINT('Ctrl Pts',(148.526799956332,-5.62417840129561,
128.960097826176));
#143294=CARTESIAN_POINT('Ctrl Pts',(148.519391736665,-5.66921384501301,
129.110859822759));
#143295=CARTESIAN_POINT('Ctrl Pts',(148.511978957363,-5.7142770072945,129.261714610834));
#143296=CARTESIAN_POINT('Ctrl Pts',(148.504566178061,-5.75327443680885,
129.414234180084));
#143297=CARTESIAN_POINT('Ctrl Pts',(148.497153398759,-5.78610977623428,
129.567888127024));
#143298=CARTESIAN_POINT('Ctrl Pts',(148.48973002773,-5.81899203233256,129.721761621931));
#143299=CARTESIAN_POINT('Ctrl Pts',(148.482306656701,-5.84569455021054,
129.876772364828));
#143300=CARTESIAN_POINT('Ctrl Pts',(148.474883285673,-5.86617267810224,
130.032383497965));
#143301=CARTESIAN_POINT('Ctrl Pts',(148.470947236232,-5.87703067287567,
130.114892254587));
#143302=CARTESIAN_POINT('Ctrl Pts',(148.467011186792,-5.88613963881658,
130.197569767277));
#143303=CARTESIAN_POINT('Ctrl Pts',(148.463075137351,-5.89349886309523,
130.280336082649));
#143304=CARTESIAN_POINT('Ctrl Pts',(148.454841822305,-5.90889267684155,
130.453464281364));
#143305=CARTESIAN_POINT('Ctrl Pts',(148.446608507258,-5.91665920916557,
130.627280655751));
#143306=CARTESIAN_POINT('Ctrl Pts',(148.438375192211,-5.91674920870991,
130.801300596218));
#143307=CARTESIAN_POINT('',(146.688376397846,-5.91262067511285,130.80056261765));
#143308=CARTESIAN_POINT('Ctrl Pts',(148.438372749788,-5.92458418098038,
130.801348235738));
#143309=CARTESIAN_POINT('Ctrl Pts',(148.353791004372,-5.91330618353133,
132.591447999183));
#143310=CARTESIAN_POINT('Ctrl Pts',(148.17639338435,-4.09355336934731,136.365725888165));
#143311=CARTESIAN_POINT('Ctrl Pts',(147.906179889726,2.33383032450629,137.402147863814));
#143312=CARTESIAN_POINT('Ctrl Pts',(147.627732265912,6.81239756668457,132.407108234558));
#143313=CARTESIAN_POINT('Ctrl Pts',(147.3492846421,5.03070424920177,125.939221843861));
#143314=CARTESIAN_POINT('Ctrl Pts',(147.070837018287,-1.3739605097317,123.942160310955));
#143315=CARTESIAN_POINT('Ctrl Pts',(146.850534579625,-5.44226183250563,
127.351331318721));
#143316=CARTESIAN_POINT('Ctrl Pts',(146.723048015568,-5.91372560248277,
130.061942539049));
#143317=CARTESIAN_POINT('Ctrl Pts',(146.688377326116,-5.90944225702956,
130.800544870309));
#143318=CARTESIAN_POINT('',(144.938373961035,-5.91329332165665,130.808852035354));
#143319=CARTESIAN_POINT('Ctrl Pts',(146.688375192211,-5.91674879577075,
130.800585667847));
#143320=CARTESIAN_POINT('Ctrl Pts',(146.680925564612,-5.91685017423445,
130.959483387732));
#143321=CARTESIAN_POINT('Ctrl Pts',(146.673475937013,-5.91054628583829,
131.118409240451));
#143322=CARTESIAN_POINT('Ctrl Pts',(146.666026309415,-5.89785702676342,
131.27681490568));
#143323=CARTESIAN_POINT('Ctrl Pts',(146.658576163893,-5.88516688548858,
131.435231583804));
#143324=CARTESIAN_POINT('Ctrl Pts',(146.651126018371,-5.86609051749853,
131.593127637726));
#143325=CARTESIAN_POINT('Ctrl Pts',(146.643675872849,-5.84069978669513,
131.749959139244));
#143326=CARTESIAN_POINT('Ctrl Pts',(146.636223817714,-5.81530254776845,
131.906830839634));
#143327=CARTESIAN_POINT('Ctrl Pts',(146.62877176258,-5.78358778015593,132.062637083029));
#143328=CARTESIAN_POINT('Ctrl Pts',(146.621319707445,-5.7456786176807,132.216843461648));
#143329=CARTESIAN_POINT('Ctrl Pts',(146.613864350142,-5.70775265683128,
132.371118172467));
#143330=CARTESIAN_POINT('Ctrl Pts',(146.60640899284,-5.66362692050174,132.523791251461));
#143331=CARTESIAN_POINT('Ctrl Pts',(146.598953635537,-5.6134745963873,132.674342841603));
#143332=CARTESIAN_POINT('Ctrl Pts',(146.591488802704,-5.56325853020448,
132.825085778207));
#143333=CARTESIAN_POINT('Ctrl Pts',(146.584023969871,-5.50700069033317,
132.973701492184));
#143334=CARTESIAN_POINT('Ctrl Pts',(146.576559137038,-5.44492303782663,
133.119688601815));
#143335=CARTESIAN_POINT('Ctrl Pts',(146.569089267876,-5.38280350314429,
133.265774205147));
#143336=CARTESIAN_POINT('Ctrl Pts',(146.561619398714,-5.31485648538662,
133.40922733926));
#143337=CARTESIAN_POINT('Ctrl Pts',(146.554149529553,-5.24135006816218,
133.549570996658));
#143338=CARTESIAN_POINT('Ctrl Pts',(146.54666740051,-5.16772300893682,133.690144992309));
#143339=CARTESIAN_POINT('Ctrl Pts',(146.539185271466,-5.08851850020001,
133.827598996989));
#143340=CARTESIAN_POINT('Ctrl Pts',(146.531703142423,-5.00404876843835,
133.961483751939));
#143341=CARTESIAN_POINT('Ctrl Pts',(146.525782685169,-4.93720957958121,
134.067424048357));
#143342=CARTESIAN_POINT('Ctrl Pts',(146.519862227915,-4.86707459463988,
134.171130098108));
#143343=CARTESIAN_POINT('Ctrl Pts',(146.513941770661,-4.79381602330894,
134.272394426105));
#143344=CARTESIAN_POINT('Ctrl Pts',(146.506518504255,-4.70196198769583,
134.399363011775));
#143345=CARTESIAN_POINT('Ctrl Pts',(146.49909523785,-4.60492125600033,134.522871811275));
#143346=CARTESIAN_POINT('Ctrl Pts',(146.491671971445,-4.50298330165497,
134.642468477895));
#143347=CARTESIAN_POINT('Ctrl Pts',(146.484257478724,-4.40116582950608,
134.761923791186));
#143348=CARTESIAN_POINT('Ctrl Pts',(146.476842986003,-4.29446289576129,
134.877475894003));
#143349=CARTESIAN_POINT('Ctrl Pts',(146.469428493282,-4.18320696468062,
134.988701671202));
#143350=CARTESIAN_POINT('Ctrl Pts',(146.462021146928,-4.07205826625514,
135.09982024481));
#143351=CARTESIAN_POINT('Ctrl Pts',(146.454613800574,-3.95636556906017,
135.206620532048));
#143352=CARTESIAN_POINT('Ctrl Pts',(146.44720645422,-3.83650120426009,135.30871285426));
#143353=CARTESIAN_POINT('Ctrl Pts',(146.439804632545,-3.7167262388252,135.410729032166));
#143354=CARTESIAN_POINT('Ctrl Pts',(146.432402810869,-3.59278608394093,
135.508043995664));
#143355=CARTESIAN_POINT('Ctrl Pts',(146.425000989194,-3.46508939834247,
135.600305365371));
#143356=CARTESIAN_POINT('Ctrl Pts',(146.417603074883,-3.33746012283026,
135.692518031019));
#143357=CARTESIAN_POINT('Ctrl Pts',(146.410205160571,-3.20607856774808,
135.779682197768));
#143358=CARTESIAN_POINT('Ctrl Pts',(146.40280724626,-3.0713858023266,135.861486265181));
#143359=CARTESIAN_POINT('Ctrl Pts',(146.395410561348,-2.93671542039964,
135.943276738242));
#143360=CARTESIAN_POINT('Ctrl Pts',(146.388013876436,-2.79873523899313,
136.019708686253));
#143361=CARTESIAN_POINT('Ctrl Pts',(146.380617191523,-2.65791468903476,
136.090514235114));
#143362=CARTESIAN_POINT('Ctrl Pts',(146.373220834588,-2.51710038320706,
136.161316644382));
#143363=CARTESIAN_POINT('Ctrl Pts',(146.365824477652,-2.37344629276073,
136.226492982859));
#143364=CARTESIAN_POINT('Ctrl Pts',(146.358428120717,-2.22744554590481,
136.285821818973));
#143365=CARTESIAN_POINT('Ctrl Pts',(146.35103063138,-2.08142244596171,136.345159738483));
#143366=CARTESIAN_POINT('Ctrl Pts',(146.343633142044,-1.93305232009356,
136.398648232491));
#143367=CARTESIAN_POINT('Ctrl Pts',(146.336235652707,-1.78284717783012,
136.446114467479));
#143368=CARTESIAN_POINT('Ctrl Pts',(146.328835570192,-1.63258938138722,
136.493597341681));
#143369=CARTESIAN_POINT('Ctrl Pts',(146.321435487677,-1.48049564354469,
136.535053641277));
#143370=CARTESIAN_POINT('Ctrl Pts',(146.314035405162,-1.32709184165449,
136.570360774201));
#143371=CARTESIAN_POINT('Ctrl Pts',(146.306627185496,-1.17351935651349,
136.605706730947));
#143372=CARTESIAN_POINT('Ctrl Pts',(146.299218965829,-1.01863429446173,
136.634889933799));
#143373=CARTESIAN_POINT('Ctrl Pts',(146.291810746163,-0.862972130654549,
136.657839041906));
#143374=CARTESIAN_POINT('Ctrl Pts',(146.284397966861,-0.707214159382685,
136.680802274806));
#143375=CARTESIAN_POINT('Ctrl Pts',(146.276985187559,-0.550678503621795,
136.697523727736));
#143376=CARTESIAN_POINT('Ctrl Pts',(146.269572408257,-0.393903902874796,
136.707984104697));
#143377=CARTESIAN_POINT('Ctrl Pts',(146.262149037228,-0.236905295226194,
136.718459427934));
#143378=CARTESIAN_POINT('Ctrl Pts',(146.254725666199,-0.0796674328840097,
136.722655797862));
#143379=CARTESIAN_POINT('Ctrl Pts',(146.24730229517,0.0772719722024892,
136.720606015182));
#143380=CARTESIAN_POINT('Ctrl Pts',(146.243366245729,0.16048501049027,136.719519171221));
#143381=CARTESIAN_POINT('Ctrl Pts',(146.239430196289,0.243614231769653,
136.716677176219));
#143382=CARTESIAN_POINT('Ctrl Pts',(146.235494146848,0.326580406880512,
136.712090790851));
#143383=CARTESIAN_POINT('Ctrl Pts',(146.228070880442,0.483052023851161,
136.703441011183));
#143384=CARTESIAN_POINT('Ctrl Pts',(146.220647614037,0.639416360654844,
136.688557418271));
#143385=CARTESIAN_POINT('Ctrl Pts',(146.213224347631,0.795136377732586,
136.667439049866));
#143386=CARTESIAN_POINT('Ctrl Pts',(146.20580985491,0.950672346682217,136.646345641619));
#143387=CARTESIAN_POINT('Ctrl Pts',(146.198395362189,1.10556514544094,136.619032175565));
#143388=CARTESIAN_POINT('Ctrl Pts',(146.190980869468,1.2592790902034,136.585549659232));
#143389=CARTESIAN_POINT('Ctrl Pts',(146.183573523114,1.41284487967899,136.552099414609));
#143390=CARTESIAN_POINT('Ctrl Pts',(146.176166176761,1.56523371485981,136.512492035865));
#143391=CARTESIAN_POINT('Ctrl Pts',(146.168758830407,1.71591649396653,136.466830144922));
#143392=CARTESIAN_POINT('Ctrl Pts',(146.161357008731,1.86648688817112,136.42120231034));
#143393=CARTESIAN_POINT('Ctrl Pts',(146.153955187056,2.01535340418601,136.369529062689));
#143394=CARTESIAN_POINT('Ctrl Pts',(146.146553365381,2.16199868522904,136.311963748472));
#143395=CARTESIAN_POINT('Ctrl Pts',(146.139155451069,2.30856655337047,136.254428822537));
#143396=CARTESIAN_POINT('Ctrl Pts',(146.131757536758,2.45291517517011,136.191008160558));
#143397=CARTESIAN_POINT('Ctrl Pts',(146.124359622446,2.59454398366055,136.121904418923));
#143398=CARTESIAN_POINT('Ctrl Pts',(146.116962937534,2.73614925601171,136.052812161077));
#143399=CARTESIAN_POINT('Ctrl Pts',(146.109566252622,2.87503527694299,135.978038861511));
#143400=CARTESIAN_POINT('Ctrl Pts',(146.10216956771,3.01072293750282,135.897834673267));
#143401=CARTESIAN_POINT('Ctrl Pts',(146.094773210774,3.14640458152964,135.817634041359));
#143402=CARTESIAN_POINT('Ctrl Pts',(146.087376853839,3.27888782581267,135.732003189538));
#143403=CARTESIAN_POINT('Ctrl Pts',(146.079980496903,3.40771982585763,135.641237311359));
#143404=CARTESIAN_POINT('Ctrl Pts',(146.072583007567,3.5365715504106,135.550457536692));
#143405=CARTESIAN_POINT('Ctrl Pts',(146.06518551823,3.6617706124662,135.454541385279));
#143406=CARTESIAN_POINT('Ctrl Pts',(146.057788028894,3.78289484863255,135.353826204499));
#143407=CARTESIAN_POINT('Ctrl Pts',(146.050387946379,3.90406154471191,135.253075718169));
#143408=CARTESIAN_POINT('Ctrl Pts',(146.042987863864,4.02115028406602,135.147523091562));
#143409=CARTESIAN_POINT('Ctrl Pts',(146.035587781349,4.13377367696238,135.037544496179));
#143410=CARTESIAN_POINT('Ctrl Pts',(146.028179561682,4.24652091085759,134.927444968025));
#143411=CARTESIAN_POINT('Ctrl Pts',(146.020771342016,4.35479272524531,134.812910012728));
#143412=CARTESIAN_POINT('Ctrl Pts',(146.013363122349,4.45823966164598,134.69435157923));
#143413=CARTESIAN_POINT('Ctrl Pts',(146.005950343047,4.56175026791007,134.575720174994));
#143414=CARTESIAN_POINT('Ctrl Pts',(145.998537563745,4.66042984537124,134.453060648234));
#143415=CARTESIAN_POINT('Ctrl Pts',(145.991124784443,4.75397095789735,134.326815825793));
#143416=CARTESIAN_POINT('Ctrl Pts',(145.983701413414,4.84764572635165,134.20039061883));
#143417=CARTESIAN_POINT('Ctrl Pts',(145.976278042385,4.93616715656382,134.070370192481));
#143418=CARTESIAN_POINT('Ctrl Pts',(145.968854671357,5.01927219824941,133.937224668619));
#143419=CARTESIAN_POINT('Ctrl Pts',(145.964918621916,5.06333648542698,133.866627717088));
#143420=CARTESIAN_POINT('Ctrl Pts',(145.960982572476,5.10587880918495,133.79515258117));
#143421=CARTESIAN_POINT('Ctrl Pts',(145.957046523035,5.14686539748783,133.72287173501));
#143422=CARTESIAN_POINT('Ctrl Pts',(145.949623256629,5.22416482388311,133.586552314953));
#143423=CARTESIAN_POINT('Ctrl Pts',(145.942199990224,5.29616157909455,133.446953624411));
#143424=CARTESIAN_POINT('Ctrl Pts',(145.934776723819,5.3625645705556,133.304526969856));
#143425=CARTESIAN_POINT('Ctrl Pts',(145.927362231098,5.42888907919511,133.162268651779));
#143426=CARTESIAN_POINT('Ctrl Pts',(145.919947738377,5.48963282784175,133.017189357821));
#143427=CARTESIAN_POINT('Ctrl Pts',(145.912533245656,5.54454918039234,132.869767344753));
#143428=CARTESIAN_POINT('Ctrl Pts',(145.905125899302,5.59941260249481,132.722487422573));
#143429=CARTESIAN_POINT('Ctrl Pts',(145.897718552948,5.64845968073772,132.572869623985));
#143430=CARTESIAN_POINT('Ctrl Pts',(145.890311206594,5.69149076141396,132.421414566957));
#143431=CARTESIAN_POINT('Ctrl Pts',(145.882909384919,5.73448974788684,132.270072470824));
#143432=CARTESIAN_POINT('Ctrl Pts',(145.875507563244,5.77148156934821,132.116896202237));
#143433=CARTESIAN_POINT('Ctrl Pts',(145.868105741568,5.80231559657743,131.96240391564));
#143434=CARTESIAN_POINT('Ctrl Pts',(145.860707827257,5.83313334676377,131.807993184319));
#143435=CARTESIAN_POINT('Ctrl Pts',(145.853309912946,5.85779970366842,131.652268183698));
#143436=CARTESIAN_POINT('Ctrl Pts',(145.845911998634,5.8762145991763,131.495759595673));
#143437=CARTESIAN_POINT('Ctrl Pts',(145.838515313722,5.89462643446256,131.339277016536));
#143438=CARTESIAN_POINT('Ctrl Pts',(145.83111862881,5.90678882664155,131.182011478816));
#143439=CARTESIAN_POINT('Ctrl Pts',(145.823721943898,5.91265326645856,131.02450128427));
#143440=CARTESIAN_POINT('Ctrl Pts',(145.816325586962,5.91851744624016,130.866998073892));
#143441=CARTESIAN_POINT('Ctrl Pts',(145.808929230027,5.9180842150296,130.709250601297));
#143442=CARTESIAN_POINT('Ctrl Pts',(145.801532873091,5.91135715401488,130.551799416711));
#143443=CARTESIAN_POINT('Ctrl Pts',(145.794135383755,5.90462906306994,130.394324125948));
#143444=CARTESIAN_POINT('Ctrl Pts',(145.786737894418,5.89160523959781,130.237145586498));
#143445=CARTESIAN_POINT('Ctrl Pts',(145.779340405082,5.87234131387779,130.080801320878));
#143446=CARTESIAN_POINT('Ctrl Pts',(145.771940322567,5.85307063521842,129.924402249017));
#143447=CARTESIAN_POINT('Ctrl Pts',(145.764540240052,5.82755554472008,129.768838403525));
#143448=CARTESIAN_POINT('Ctrl Pts',(145.757140157537,5.79590313250887,129.61463903624));
#143449=CARTESIAN_POINT('Ctrl Pts',(145.74973193787,5.76421591521665,129.460270110899));
#143450=CARTESIAN_POINT('Ctrl Pts',(145.742323718204,5.72637797388972,129.307269026028));
#143451=CARTESIAN_POINT('Ctrl Pts',(145.734915498537,5.682547001995,129.156152459408));
#143452=CARTESIAN_POINT('Ctrl Pts',(145.727502719235,5.63868905286833,129.004942883063));
#143453=CARTESIAN_POINT('Ctrl Pts',(145.720089939933,5.58883084110783,128.855620489456));
#143454=CARTESIAN_POINT('Ctrl Pts',(145.712677160631,5.53317875273848,128.708683292035));
#143455=CARTESIAN_POINT('Ctrl Pts',(145.705253789602,5.4774471460555,128.561536143857));
#143456=CARTESIAN_POINT('Ctrl Pts',(145.697830418573,5.41590527428469,128.416781341196));
#143457=CARTESIAN_POINT('Ctrl Pts',(145.690407047545,5.34880647916707,128.274894308061));
#143458=CARTESIAN_POINT('Ctrl Pts',(145.686470998104,5.3132290879834,128.199662398563));
#143459=CARTESIAN_POINT('Ctrl Pts',(145.682534948663,5.27609019699943,128.125236279882));
#143460=CARTESIAN_POINT('Ctrl Pts',(145.678598899223,5.23743252615506,128.051683539434));
#143461=CARTESIAN_POINT('Ctrl Pts',(145.671175632817,5.16452536540489,127.912965366447));
#143462=CARTESIAN_POINT('Ctrl Pts',(145.663752366412,5.0859930382221,127.776935955108));
#143463=CARTESIAN_POINT('Ctrl Pts',(145.656329100007,5.00205789888053,127.64408415201));
#143464=CARTESIAN_POINT('Ctrl Pts',(145.648914607286,4.91822196390334,127.511389368711));
#143465=CARTESIAN_POINT('Ctrl Pts',(145.641500114565,4.8289961249295,127.381865030479));
#143466=CARTESIAN_POINT('Ctrl Pts',(145.634085621844,4.73464944008796,127.255977148721));
#143467=CARTESIAN_POINT('Ctrl Pts',(145.62667827549,4.64039369013352,127.130210602443));
#143468=CARTESIAN_POINT('Ctrl Pts',(145.619270929136,4.5410271426175,127.008073831677));
#143469=CARTESIAN_POINT('Ctrl Pts',(145.611863582782,4.4368630639082,126.890005406982));
#143470=CARTESIAN_POINT('Ctrl Pts',(145.604461761107,4.3327766746982,126.772025042172));
#143471=CARTESIAN_POINT('Ctrl Pts',(145.597059939431,4.22390012483411,126.658107260404));
#143472=CARTESIAN_POINT('Ctrl Pts',(145.589658117756,4.11058793355197,126.548658865441));
#143473=CARTESIAN_POINT('Ctrl Pts',(145.582260203445,3.99733555889367,126.439268247435));
#143474=CARTESIAN_POINT('Ctrl Pts',(145.574862289133,3.87965247392742,126.334342576154));
#143475=CARTESIAN_POINT('Ctrl Pts',(145.567464374822,3.75793106709958,126.234252888264));
#143476=CARTESIAN_POINT('Ctrl Pts',(145.56006768991,3.63622988816143,126.134179833464));
#143477=CARTESIAN_POINT('Ctrl Pts',(145.552671004998,3.51049200734194,126.038941403905));
#143478=CARTESIAN_POINT('Ctrl Pts',(145.545274320085,3.3811440927185,125.948869377045));
#143479=CARTESIAN_POINT('Ctrl Pts',(145.53787796315,3.25180191351725,125.858801344073));
#143480=CARTESIAN_POINT('Ctrl Pts',(145.530481606214,3.11885032513162,125.773899471627));
#143481=CARTESIAN_POINT('Ctrl Pts',(145.523085249279,2.98274604349509,125.694452927351));
#143482=CARTESIAN_POINT('Ctrl Pts',(145.515687759942,2.84662092394524,125.614994219607));
#143483=CARTESIAN_POINT('Ctrl Pts',(145.508290270606,2.70734247246724,125.540992691276));
#143484=CARTESIAN_POINT('Ctrl Pts',(145.500892781269,2.56539299150256,125.472692083078));
#143485=CARTESIAN_POINT('Ctrl Pts',(145.493492698754,2.42339375036843,125.404367532208));
#143486=CARTESIAN_POINT('Ctrl Pts',(145.486092616239,2.27872195170525,125.341748042123));
#143487=CARTESIAN_POINT('Ctrl Pts',(145.478692533724,2.13188075490347,125.285029588413));
#143488=CARTESIAN_POINT('Ctrl Pts',(145.471284314058,1.98487809110943,125.228248766932));
#143489=CARTESIAN_POINT('Ctrl Pts',(145.463876094391,1.83570161366175,125.177382074964));
#143490=CARTESIAN_POINT('Ctrl Pts',(145.456467874725,1.68487125538148,125.132576117491));
#143491=CARTESIAN_POINT('Ctrl Pts',(145.449055095423,1.53394806353227,125.087742582699));
#143492=CARTESIAN_POINT('Ctrl Pts',(145.441642316121,1.38136932344967,125.048977307164));
#143493=CARTESIAN_POINT('Ctrl Pts',(145.434229536819,1.22766558464131,125.016375840911));
#143494=CARTESIAN_POINT('Ctrl Pts',(145.42680616579,1.07374222672317,124.983727792155));
#143495=CARTESIAN_POINT('Ctrl Pts',(145.419382794761,0.918691026639936,
124.957261205161));
#143496=CARTESIAN_POINT('Ctrl Pts',(145.411959423733,0.763048909474546,
124.937019914637));
#143497=CARTESIAN_POINT('Ctrl Pts',(145.408023374292,0.680523724368401,
124.926287496717));
#143498=CARTESIAN_POINT('Ctrl Pts',(145.404087324851,0.597832445114237,
124.917304362424));
#143499=CARTESIAN_POINT('Ctrl Pts',(145.40015127541,0.5150550260896,124.910071102909));
#143500=CARTESIAN_POINT('Ctrl Pts',(145.392728009004,0.358939397210291,
124.896429401206));
#143501=CARTESIAN_POINT('Ctrl Pts',(145.385304742599,0.202045359796482,
124.888973652685));
#143502=CARTESIAN_POINT('Ctrl Pts',(145.377881476193,0.0449043822473605,
124.887781017919));
#143503=CARTESIAN_POINT('Ctrl Pts',(145.370466983472,-0.112050867716212,
124.886589792749));
#143504=CARTESIAN_POINT('Ctrl Pts',(145.363052490751,-0.269252107218764,
124.891646949463));
#143505=CARTESIAN_POINT('Ctrl Pts',(145.35563799803,-0.426161835175479,
124.902978012384));
#143506=CARTESIAN_POINT('Ctrl Pts',(145.348230651676,-0.582920327628564,
124.914298154001));
#143507=CARTESIAN_POINT('Ctrl Pts',(145.340823305323,-0.739387498062542,
124.931880136678));
#143508=CARTESIAN_POINT('Ctrl Pts',(145.333415958969,-0.895025036522239,
124.955697458647));
#143509=CARTESIAN_POINT('Ctrl Pts',(145.326014137293,-1.05054649463355,
124.979497016758));
#143510=CARTESIAN_POINT('Ctrl Pts',(145.318612315618,-1.20523918541278,
125.009522598061));
#143511=CARTESIAN_POINT('Ctrl Pts',(145.311210493943,-1.35856922702592,
125.045695822852));
#143512=CARTESIAN_POINT('Ctrl Pts',(145.303812579631,-1.51181832690372,
125.081849952079));
#143513=CARTESIAN_POINT('Ctrl Pts',(145.29641466532,-1.663705847795,125.12414517614));
#143514=CARTESIAN_POINT('Ctrl Pts',(145.289016751009,-1.81370753050493,
125.172451921903));
#143515=CARTESIAN_POINT('Ctrl Pts',(145.281620066096,-1.96368428565677,
125.22075063996));
#143516=CARTESIAN_POINT('Ctrl Pts',(145.274223381184,-2.11177546963895,
125.275058782671));
#143517=CARTESIAN_POINT('Ctrl Pts',(145.266826696272,-2.25747132416115,
125.335196715918));
#143518=CARTESIAN_POINT('Ctrl Pts',(145.259430339337,-2.4031607183768,125.395331982586));
#143519=CARTESIAN_POINT('Ctrl Pts',(145.252033982401,-2.54645464925804,
125.461296383379));
#143520=CARTESIAN_POINT('Ctrl Pts',(145.244637625466,-2.68686296575698,
125.532861972423));
#143521=CARTESIAN_POINT('Ctrl Pts',(145.237240136129,-2.82729277912728,
125.604438518341));
#143522=CARTESIAN_POINT('Ctrl Pts',(145.229842646792,-2.96483576583358,
125.68161779049));
#143523=CARTESIAN_POINT('Ctrl Pts',(145.222445157456,-3.09902616365413,
125.764125761978));
#143524=CARTESIAN_POINT('Ctrl Pts',(145.215045074941,-3.23326360171076,
125.846662656507));
#143525=CARTESIAN_POINT('Ctrl Pts',(145.207644992426,-3.36414579317909,
125.934531774084));
#143526=CARTESIAN_POINT('Ctrl Pts',(145.200244909911,-3.49123588830347,
126.027415722058));
#143527=CARTESIAN_POINT('Ctrl Pts',(145.192836690244,-3.6184657320528,126.120401805481));
#143528=CARTESIAN_POINT('Ctrl Pts',(145.185428470578,-3.74189485052367,
126.218413511359));
#143529=CARTESIAN_POINT('Ctrl Pts',(145.178020250911,-3.86111886440333,
126.321092649058));
#143530=CARTESIAN_POINT('Ctrl Pts',(145.170607471609,-3.98041625867358,
126.423834984053));
#143531=CARTESIAN_POINT('Ctrl Pts',(145.163194692307,-4.09550311882838,
126.531250221017));
#143532=CARTESIAN_POINT('Ctrl Pts',(145.155781913005,-4.20601228095614,
126.642943640748));
#143533=CARTESIAN_POINT('Ctrl Pts',(145.148358541976,-4.31667934375759,
126.754796653276));
#143534=CARTESIAN_POINT('Ctrl Pts',(145.140935170948,-4.42275539394983,
126.870939782432));
#143535=CARTESIAN_POINT('Ctrl Pts',(145.133511799919,-4.52391333102896,
126.990944991669));
#143536=CARTESIAN_POINT('Ctrl Pts',(145.129575750478,-4.57754969651935,
127.054574633091));
#143537=CARTESIAN_POINT('Ctrl Pts',(145.125639701037,-4.6298041180975,127.119289544752));
#143538=CARTESIAN_POINT('Ctrl Pts',(145.121703651597,-4.68063288111521,
127.185022778303));
#143539=CARTESIAN_POINT('Ctrl Pts',(145.114064965789,-4.77927619251906,
127.312591175442));
#143540=CARTESIAN_POINT('Ctrl Pts',(145.106426279981,-4.87285827794634,
127.444399281556));
#143541=CARTESIAN_POINT('Ctrl Pts',(145.098787594173,-4.96099500290015,
127.580006551447));
#143542=CARTESIAN_POINT('Ctrl Pts',(145.091366378611,-5.04662251151985,
127.7117531381));
#143543=CARTESIAN_POINT('Ctrl Pts',(145.083945163049,-5.12711022034083,
127.847085199565));
#143544=CARTESIAN_POINT('Ctrl Pts',(145.076523947486,-5.20214519205127,
127.985563717589));
#143545=CARTESIAN_POINT('Ctrl Pts',(145.069109876635,-5.2771079244886,128.123908916612));
#143546=CARTESIAN_POINT('Ctrl Pts',(145.061695805784,-5.34662819244207,
128.265394218518));
#143547=CARTESIAN_POINT('Ctrl Pts',(145.054281734933,-5.41043627226524,
128.409551667721));
#143548=CARTESIAN_POINT('Ctrl Pts',(145.046873350587,-5.47419541204351,
128.553598549861));
#143549=CARTESIAN_POINT('Ctrl Pts',(145.039464966241,-5.53225093573288,
128.700313160822));
#143550=CARTESIAN_POINT('Ctrl Pts',(145.032056581895,-5.58437907086082,
128.849203090554));
#143551=CARTESIAN_POINT('Ctrl Pts',(145.024652429676,-5.63647742717881,
128.998007965163));
#143552=CARTESIAN_POINT('Ctrl Pts',(145.017248277456,-5.68265501508533,
129.148985333991));
#143553=CARTESIAN_POINT('Ctrl Pts',(145.009844125237,-5.72273627239586,
129.301623075909));
#143554=CARTESIAN_POINT('Ctrl Pts',(145.002442331162,-5.76280476424999,
129.454212204321));
#143555=CARTESIAN_POINT('Ctrl Pts',(144.995040537086,-5.79678069627863,
129.608460293921));
#143556=CARTESIAN_POINT('Ctrl Pts',(144.987638743011,-5.82453845256294,
129.763840374074));
#143557=CARTESIAN_POINT('Ctrl Pts',(144.980238245299,-5.85229134730386,
129.919193240681));
#143558=CARTESIAN_POINT('Ctrl Pts',(144.972837747588,-5.87382817296325,
130.075677336557));
#143559=CARTESIAN_POINT('Ctrl Pts',(144.965437249876,-5.88907452469448,
130.232756029503));
#143560=CARTESIAN_POINT('Ctrl Pts',(144.958035619644,-5.90432320962045,
130.389858760671));
#143561=CARTESIAN_POINT('Ctrl Pts',(144.950633989412,-5.91327946377241,
130.547555900412));
#143562=CARTESIAN_POINT('Ctrl Pts',(144.94323235918,-5.91592078837946,130.705306147098));
#143563=CARTESIAN_POINT('Ctrl Pts',(144.941613303524,-5.91649855995291,
130.73981292752));
#143564=CARTESIAN_POINT('Ctrl Pts',(144.939994247867,-5.91677436921867,
130.774322244405));
#143565=CARTESIAN_POINT('Ctrl Pts',(144.938375192211,-5.91674831314815,
130.808828431186));
#143566=CARTESIAN_POINT('',(143.188375192211,-5.92568524777546,130.806401493052));
#143567=CARTESIAN_POINT('Ctrl Pts',(144.938373068227,-5.91078788040133,
130.808869152286));
#143568=CARTESIAN_POINT('Ctrl Pts',(144.90666738808,-5.91549280454811,131.483920819572));
#143569=CARTESIAN_POINT('Ctrl Pts',(144.782145833326,-5.49648468611223,
134.129459311167));
#143570=CARTESIAN_POINT('Ctrl Pts',(144.564808403972,-1.59237845161755,
137.619189404644));
#143571=CARTESIAN_POINT('Ctrl Pts',(144.286360780157,4.87278901544506,135.827655128273));
#143572=CARTESIAN_POINT('Ctrl Pts',(144.007913156345,6.86010142628747,129.419958598146));
#143573=CARTESIAN_POINT('Ctrl Pts',(143.729465532532,2.54331576096232,124.284459892064));
#143574=CARTESIAN_POINT('Ctrl Pts',(143.456286211154,-3.98475800102683,
125.1242362306));
#143575=CARTESIAN_POINT('Ctrl Pts',(143.275922764381,-5.91742993572983,
128.954444514574));
#143576=CARTESIAN_POINT('Ctrl Pts',(143.188375192211,-5.92568524777546,
130.806401493052));
#143577=CARTESIAN_POINT('',(141.438375192211,-5.91702297748046,130.798906129064));
#143578=CARTESIAN_POINT('Ctrl Pts',(143.188375192211,-5.92568524777546,
130.806401493052));
#143579=CARTESIAN_POINT('Ctrl Pts',(143.183106889776,-5.92618202317967,
130.917845696673));
#143580=CARTESIAN_POINT('Ctrl Pts',(143.177838587341,-5.92331160393294,
131.02926379799));
#143581=CARTESIAN_POINT('Ctrl Pts',(143.079754410302,-5.80568103701415,
133.099976805968));
#143582=CARTESIAN_POINT('Ctrl Pts',(142.894122661094,-3.44277851418379,
136.897376014938));
#143583=CARTESIAN_POINT('Ctrl Pts',(142.615675037281,3.26532053551612,136.994291338557));
#143584=CARTESIAN_POINT('Ctrl Pts',(142.337227413468,6.97274953285437,131.402962724511));
#143585=CARTESIAN_POINT('Ctrl Pts',(142.058779789655,4.27256234724961,125.261548017523));
#143586=CARTESIAN_POINT('Ctrl Pts',(141.780332165842,-2.35390090920024,
124.213707308521));
#143587=CARTESIAN_POINT('Ctrl Pts',(141.57353063336,-5.66880166132113,127.933602662797));
#143588=CARTESIAN_POINT('Ctrl Pts',(141.459544975484,-5.92119195072286,
130.349379528659));
#143589=CARTESIAN_POINT('Ctrl Pts',(141.438375192211,-5.91702297748046,
130.798906129064));
#143590=CARTESIAN_POINT('',(139.688375192172,-5.9167499847919,130.804784840391));
#143591=CARTESIAN_POINT('Ctrl Pts',(141.438375192211,-5.91674748606238,
130.79890638302));
#143592=CARTESIAN_POINT('Ctrl Pts',(141.431065800626,-5.91689055543903,
130.954107881506));
#143593=CARTESIAN_POINT('Ctrl Pts',(141.423756409041,-5.91092284628539,
131.109486426606));
#143594=CARTESIAN_POINT('Ctrl Pts',(141.416447017456,-5.89882942285099,
131.264514942339));
#143595=CARTESIAN_POINT('Ctrl Pts',(141.409142780344,-5.88674452751565,
131.419434134311));
#143596=CARTESIAN_POINT('Ctrl Pts',(141.401838543231,-5.86854254517654,
131.574003406929));
#143597=CARTESIAN_POINT('Ctrl Pts',(141.394534306118,-5.84426061148494,
131.727696129471));
#143598=CARTESIAN_POINT('Ctrl Pts',(141.387232856437,-5.81998794422667,
131.881330200039));
#143599=CARTESIAN_POINT('Ctrl Pts',(141.379931406756,-5.78963999913602,
132.034088007126));
#143600=CARTESIAN_POINT('Ctrl Pts',(141.372629957075,-5.75330570620068,
132.185448599376));
#143601=CARTESIAN_POINT('Ctrl Pts',(141.365329820798,-5.71697794917513,
132.336781964477));
#143602=CARTESIAN_POINT('Ctrl Pts',(141.358029684521,-5.67466607556131,
132.486718241348));
#143603=CARTESIAN_POINT('Ctrl Pts',(141.350729548244,-5.6265099594955,132.634747526992));
#143604=CARTESIAN_POINT('Ctrl Pts',(141.34342919449,-5.57835240881922,132.782781222551));
#143605=CARTESIAN_POINT('Ctrl Pts',(141.336128840736,-5.52435038797274,
132.928907448565));
#143606=CARTESIAN_POINT('Ctrl Pts',(141.328828486982,-5.46469329765204,
133.07263258651));
#143607=CARTESIAN_POINT('Ctrl Pts',(141.321526384877,-5.40502192013949,
133.216392144984));
#143608=CARTESIAN_POINT('Ctrl Pts',(141.314224282772,-5.33969292580351,
133.357749116711));
#143609=CARTESIAN_POINT('Ctrl Pts',(141.306922180666,-5.26894327268043,
133.496231222141));
#143610=CARTESIAN_POINT('Ctrl Pts',(141.299612578507,-5.19812095195867,
133.634855563775));
#143611=CARTESIAN_POINT('Ctrl Pts',(141.292302976348,-5.12186702820574,
133.770598799663));
#143612=CARTESIAN_POINT('Ctrl Pts',(141.284993374188,-5.04046402047297,
133.903014038137));
#143613=CARTESIAN_POINT('Ctrl Pts',(141.277679838574,-4.95901720801798,
134.035500532121));
#143614=CARTESIAN_POINT('Ctrl Pts',(141.270366302959,-4.87241600671399,
134.164655143615));
#143615=CARTESIAN_POINT('Ctrl Pts',(141.263052767344,-4.78098497342835,
134.290061873605));
#143616=CARTESIAN_POINT('Ctrl Pts',(141.255728307744,-4.68941737264306,
134.415655919466));
#143617=CARTESIAN_POINT('Ctrl Pts',(141.248403848144,-4.59300576799819,
134.537490601409));
#143618=CARTESIAN_POINT('Ctrl Pts',(141.241079388544,-4.4921140771244,134.655184124376));
#143619=CARTESIAN_POINT('Ctrl Pts',(141.235198565101,-4.41110793424951,
134.749680492256));
#143620=CARTESIAN_POINT('Ctrl Pts',(141.229317741659,-4.32721448582552,
134.841507901096));
#143621=CARTESIAN_POINT('Ctrl Pts',(141.223436918216,-4.24063787803311,
134.930487245518));
#143622=CARTESIAN_POINT('Ctrl Pts',(141.216013651811,-4.13135365442037,
135.042804403935));
#143623=CARTESIAN_POINT('Ctrl Pts',(141.208590385405,-4.01743886492291,
135.150946661614));
#143624=CARTESIAN_POINT('Ctrl Pts',(141.201167119,-3.89924547964,135.254508396237));
#143625=CARTESIAN_POINT('Ctrl Pts',(141.193752626279,-3.78119178912335,
135.357947729489));
#143626=CARTESIAN_POINT('Ctrl Pts',(141.186338133558,-3.65886984672371,
135.456817072274));
#143627=CARTESIAN_POINT('Ctrl Pts',(141.178923640837,-3.53266992342586,
135.550745955339));
#143628=CARTESIAN_POINT('Ctrl Pts',(141.171516294483,-3.40659163636524,
135.64458430621));
#143629=CARTESIAN_POINT('Ctrl Pts',(141.164108948129,-3.2766431069661,135.733491455784));
#143630=CARTESIAN_POINT('Ctrl Pts',(141.156701601776,-3.14324920679138,
135.817135795699));
#143631=CARTESIAN_POINT('Ctrl Pts',(141.1492997801,-3.00995479681998,135.900717750509));
#143632=CARTESIAN_POINT('Ctrl Pts',(141.141897958425,-2.873220447571,135.979044513807));
#143633=CARTESIAN_POINT('Ctrl Pts',(141.134496136749,-2.73350156943249,
136.051826647224));
#143634=CARTESIAN_POINT('Ctrl Pts',(141.127098222438,-2.59385644780272,
136.124570359518));
#143635=CARTESIAN_POINT('Ctrl Pts',(141.119700308127,-2.45123026521982,
136.191775099103));
#143636=CARTESIAN_POINT('Ctrl Pts',(141.112302393815,-2.30610459091035,
136.253196472892));
#143637=CARTESIAN_POINT('Ctrl Pts',(141.104905708903,-2.16100303385463,
136.314607639563));
#143638=CARTESIAN_POINT('Ctrl Pts',(141.097509023991,-2.01340315289902,
136.370237202565));
#143639=CARTESIAN_POINT('Ctrl Pts',(141.090112339079,-1.86380824292428,
136.419888143641));
#143640=CARTESIAN_POINT('Ctrl Pts',(141.082715982143,-1.71421996614457,
136.469536883143));
#143641=CARTESIAN_POINT('Ctrl Pts',(141.075319625208,-1.56263719053038,
136.513207410233));
#143642=CARTESIAN_POINT('Ctrl Pts',(141.067923268272,-1.40957992781836,
136.550752093057));
#143643=CARTESIAN_POINT('Ctrl Pts',(141.060525778935,-1.25649923164864,
136.588302524067));
#143644=CARTESIAN_POINT('Ctrl Pts',(141.053128289599,-1.1019439614603,136.619725154422));
#143645=CARTESIAN_POINT('Ctrl Pts',(141.045730800262,-0.946445768353029,
136.644923173525));
#143646=CARTESIAN_POINT('Ctrl Pts',(141.038330717747,-0.790893065595329,
136.670130025753));
#143647=CARTESIAN_POINT('Ctrl Pts',(141.030930635232,-0.634397150076889,
136.689107862652));
#143648=CARTESIAN_POINT('Ctrl Pts',(141.023530552717,-0.47749611352947,
136.701811594392));
#143649=CARTESIAN_POINT('Ctrl Pts',(141.016122333051,-0.320422548162493,
136.714529295191));
#143650=CARTESIAN_POINT('Ctrl Pts',(141.008714113384,-0.162943344437875,
136.720959082884));
#143651=CARTESIAN_POINT('Ctrl Pts',(141.001305893718,-0.005598663443887,
136.721107968727));
#143652=CARTESIAN_POINT('Ctrl Pts',(140.993893114416,0.151842860575984,
136.721256946206));
#143653=CARTESIAN_POINT('Ctrl Pts',(140.986480335114,0.309149324733783,
136.715117333287));
#143654=CARTESIAN_POINT('Ctrl Pts',(140.979067555811,0.465784880194546,
136.702748109744));
#143655=CARTESIAN_POINT('Ctrl Pts',(140.971644184783,0.622644243882486,
136.690361212474));
#143656=CARTESIAN_POINT('Ctrl Pts',(140.964220813754,0.778830414595473,
136.671726971074));
#143657=CARTESIAN_POINT('Ctrl Pts',(140.956797442725,0.933816109861406,
136.646955763172));
#143658=CARTESIAN_POINT('Ctrl Pts',(140.952861393284,1.01599324432282,136.633821474366));
#143659=CARTESIAN_POINT('Ctrl Pts',(140.948925343844,1.09783309672732,136.618962708455));
#143660=CARTESIAN_POINT('Ctrl Pts',(140.944989294403,1.1792588336594,136.602401594115));
#143661=CARTESIAN_POINT('Ctrl Pts',(140.937566027997,1.33282523230163,136.571167849323));
#143662=CARTESIAN_POINT('Ctrl Pts',(140.930142761592,1.48538210268091,136.533781642481));
#143663=CARTESIAN_POINT('Ctrl Pts',(140.922719495186,1.63639793481917,136.490319847232));
#143664=CARTESIAN_POINT('Ctrl Pts',(140.915305002465,1.78723527878503,136.446909420215));
#143665=CARTESIAN_POINT('Ctrl Pts',(140.907890509744,1.93653485474148,136.397437800529));
#143666=CARTESIAN_POINT('Ctrl Pts',(140.900476017023,2.08377402541546,136.342033086528));
#143667=CARTESIAN_POINT('Ctrl Pts',(140.89306867067,2.23087128143318,136.286681773677));
#143668=CARTESIAN_POINT('Ctrl Pts',(140.885661324316,2.37591173866099,136.225408881583));
#143669=CARTESIAN_POINT('Ctrl Pts',(140.878253977962,2.51838675213341,136.158392624304));
#143670=CARTESIAN_POINT('Ctrl Pts',(140.870852156287,2.66075550236602,136.091426350279));
#143671=CARTESIAN_POINT('Ctrl Pts',(140.863450334611,2.80056228234905,136.018725398538));
#143672=CARTESIAN_POINT('Ctrl Pts',(140.856048512936,2.93731741894727,135.940516470229));
#143673=CARTESIAN_POINT('Ctrl Pts',(140.848650598625,3.0740003635726,135.862348827806));
#143674=CARTESIAN_POINT('Ctrl Pts',(140.841252684313,3.20763454984633,135.778679184328));
#143675=CARTESIAN_POINT('Ctrl Pts',(140.833854770002,3.33775406301456,135.689780597192));
#143676=CARTESIAN_POINT('Ctrl Pts',(140.82645808509,3.46785195268059,135.600896783388));
#143677=CARTESIAN_POINT('Ctrl Pts',(140.819061400178,3.59443602052922,135.506785960925));
#143678=CARTESIAN_POINT('Ctrl Pts',(140.811664715266,3.71706846634464,135.407765072858));
#143679=CARTESIAN_POINT('Ctrl Pts',(140.80426835833,3.83969547450895,135.308748575482));
#143680=CARTESIAN_POINT('Ctrl Pts',(140.796872001395,3.95837091859831,135.204822679915));
#143681=CARTESIAN_POINT('Ctrl Pts',(140.789475644459,4.07268951270544,135.096345088134));
#143682=CARTESIAN_POINT('Ctrl Pts',(140.782078155123,4.18702560928126,134.987850888157));
#143683=CARTESIAN_POINT('Ctrl Pts',(140.774680665786,4.29700325689377,134.874803861363));
#143684=CARTESIAN_POINT('Ctrl Pts',(140.76728317645,4.40225363563843,134.757598972385));
#143685=CARTESIAN_POINT('Ctrl Pts',(140.759883093935,4.50754090974044,134.640352997414));
#143686=CARTESIAN_POINT('Ctrl Pts',(140.75248301142,4.60809736636642,134.518946535896));
#143687=CARTESIAN_POINT('Ctrl Pts',(140.745082928905,4.70359421844273,134.393807927492));
#143688=CARTESIAN_POINT('Ctrl Pts',(140.737674709238,4.79919607912508,134.268531716323));
#143689=CARTESIAN_POINT('Ctrl Pts',(140.730266489572,4.88972699786911,134.139515459491));
#143690=CARTESIAN_POINT('Ctrl Pts',(140.722858269905,4.97490090317974,134.007217399572));
#143691=CARTESIAN_POINT('Ctrl Pts',(140.715445490603,5.06012723160788,133.874837912405));
#143692=CARTESIAN_POINT('Ctrl Pts',(140.708032711301,5.13998978767766,133.739172918207));
#143693=CARTESIAN_POINT('Ctrl Pts',(140.700619931999,5.21424855335885,133.600705121788));
#143694=CARTESIAN_POINT('Ctrl Pts',(140.693196560971,5.28861342344689,133.462039476089));
#143695=CARTESIAN_POINT('Ctrl Pts',(140.685773189942,5.35735834873741,133.320563364602));
#143696=CARTESIAN_POINT('Ctrl Pts',(140.678349818913,5.42029118399987,133.17678006681));
#143697=CARTESIAN_POINT('Ctrl Pts',(140.674413769472,5.45365968330849,133.100542712289));
#143698=CARTESIAN_POINT('Ctrl Pts',(140.670477720031,5.48539502199948,133.023657000717));
#143699=CARTESIAN_POINT('Ctrl Pts',(140.666541670591,5.51547428721513,132.946199535311));
#143700=CARTESIAN_POINT('Ctrl Pts',(140.659118404185,5.57220284267034,132.800117172921));
#143701=CARTESIAN_POINT('Ctrl Pts',(140.65169513778,5.62320948287038,132.651558599229));
#143702=CARTESIAN_POINT('Ctrl Pts',(140.644271871374,5.66827158966255,132.501012540715));
#143703=CARTESIAN_POINT('Ctrl Pts',(140.636857378653,5.71328043678675,132.35064441514));
#143704=CARTESIAN_POINT('Ctrl Pts',(140.629442885932,5.7523586296856,132.198293834652));
#143705=CARTESIAN_POINT('Ctrl Pts',(140.622028393211,5.7853314429195,132.044469749081));
#143706=CARTESIAN_POINT('Ctrl Pts',(140.614621046857,5.81827247571454,131.890793924955));
#143707=CARTESIAN_POINT('Ctrl Pts',(140.607213700504,5.84511976619896,131.73564778568));
#143708=CARTESIAN_POINT('Ctrl Pts',(140.59980635415,5.86574831587934,131.579555597722));
#143709=CARTESIAN_POINT('Ctrl Pts',(140.592404532474,5.88636148000912,131.423579829206));
#143710=CARTESIAN_POINT('Ctrl Pts',(140.585002710799,5.90076508986235,131.266659785438));
#143711=CARTESIAN_POINT('Ctrl Pts',(140.577600889124,5.90888519524603,131.109329979801));
#143712=CARTESIAN_POINT('Ctrl Pts',(140.570202974812,5.91700101408927,130.952083227345));
#143713=CARTESIAN_POINT('Ctrl Pts',(140.562805060501,5.91883991526116,130.794427515672));
#143714=CARTESIAN_POINT('Ctrl Pts',(140.555407146189,5.9143797913781,130.636902426251));
#143715=CARTESIAN_POINT('Ctrl Pts',(140.548010461277,5.9099204086867,130.479403514643));
#143716=CARTESIAN_POINT('Ctrl Pts',(140.540613776365,5.89916408905104,130.322035554988));
#143717=CARTESIAN_POINT('Ctrl Pts',(140.533217091453,5.88214084393088,130.165338196473));
#143718=CARTESIAN_POINT('Ctrl Pts',(140.525820734517,5.86511835363928,130.008647786082));
#143719=CARTESIAN_POINT('Ctrl Pts',(140.518424377582,5.84182953070357,129.852628288822));
#143720=CARTESIAN_POINT('Ctrl Pts',(140.511028020646,5.81235625299531,129.697814029859));
#143721=CARTESIAN_POINT('Ctrl Pts',(140.50363053131,5.78287846285299,129.542976068438));
#143722=CARTESIAN_POINT('Ctrl Pts',(140.496233041973,5.74721440244067,129.389344079463));
#143723=CARTESIAN_POINT('Ctrl Pts',(140.488835552636,5.70549701052338,129.237441849598));
#143724=CARTESIAN_POINT('Ctrl Pts',(140.481435470121,5.66376499463898,129.085486370643));
#143725=CARTESIAN_POINT('Ctrl Pts',(140.474035387606,5.61597552118902,128.935262217809));
#143726=CARTESIAN_POINT('Ctrl Pts',(140.466635305091,5.56231124701649,128.787277537023));
#143727=CARTESIAN_POINT('Ctrl Pts',(140.459227085425,5.50858796345766,128.639130131867));
#143728=CARTESIAN_POINT('Ctrl Pts',(140.451818865758,5.44897710557661,128.493227467744));
#143729=CARTESIAN_POINT('Ctrl Pts',(140.444410646092,5.38370957720002,128.35005791601));
#143730=CARTESIAN_POINT('Ctrl Pts',(140.43699786679,5.31840187774888,128.206800245806));
#143731=CARTESIAN_POINT('Ctrl Pts',(140.429585087488,5.24743073820561,128.066279372394));
#143732=CARTESIAN_POINT('Ctrl Pts',(140.422172308186,5.17107253618896,127.928958143481));
#143733=CARTESIAN_POINT('Ctrl Pts',(140.414748937157,5.09460522999219,127.791440703556));
#143734=CARTESIAN_POINT('Ctrl Pts',(140.407325566128,5.01273568189467,127.657132356947));
#143735=CARTESIAN_POINT('Ctrl Pts',(140.399902195099,4.92578345598751,127.526466795732));
#143736=CARTESIAN_POINT('Ctrl Pts',(140.395966145658,4.87967929942065,127.457184779897));
#143737=CARTESIAN_POINT('Ctrl Pts',(140.392030096218,4.83214689849864,127.38892633552));
#143738=CARTESIAN_POINT('Ctrl Pts',(140.388094046777,4.78323831671844,127.321752145748));
#143739=CARTESIAN_POINT('Ctrl Pts',(140.380670780371,4.69099825786723,127.195063720275));
#143740=CARTESIAN_POINT('Ctrl Pts',(140.373247513966,4.59358205735704,127.071850851466));
#143741=CARTESIAN_POINT('Ctrl Pts',(140.36582424756,4.49128056406732,126.952565002878));
#143742=CARTESIAN_POINT('Ctrl Pts',(140.358409754839,4.38909998264718,126.833420140257));
#143743=CARTESIAN_POINT('Ctrl Pts',(140.350995262118,4.2820458422903,126.718193339696));
#143744=CARTESIAN_POINT('Ctrl Pts',(140.343580769397,4.17045189353369,126.60730670247));
#143745=CARTESIAN_POINT('Ctrl Pts',(140.336173423044,4.05896550322618,126.49652694196));
#143746=CARTESIAN_POINT('Ctrl Pts',(140.32876607669,3.94294827857493,126.390079278187));
#143747=CARTESIAN_POINT('Ctrl Pts',(140.321358730336,3.8227737350675,126.288352254755));
#143748=CARTESIAN_POINT('Ctrl Pts',(140.313956908661,3.70268882226875,126.186701103175));
#143749=CARTESIAN_POINT('Ctrl Pts',(140.306555086985,3.57845304819304,126.089763821632));
#143750=CARTESIAN_POINT('Ctrl Pts',(140.29915326531,3.45047614220427,125.997891544059));
#143751=CARTESIAN_POINT('Ctrl Pts',(140.291755350999,3.32256679422905,125.906067765147));
#143752=CARTESIAN_POINT('Ctrl Pts',(140.284357436688,3.19092054995827,125.819303882397));
#143753=CARTESIAN_POINT('Ctrl Pts',(140.276959522376,3.05597942498416,125.737910152342));
#143754=CARTESIAN_POINT('Ctrl Pts',(140.269562837464,2.92106072477569,125.656529948447));
#143755=CARTESIAN_POINT('Ctrl Pts',(140.262166152552,2.7828485499254,125.580518318672));
#143756=CARTESIAN_POINT('Ctrl Pts',(140.25476946764,2.64181314450327,125.510141707091));
#143757=CARTESIAN_POINT('Ctrl Pts',(140.247373110704,2.50078399273881,125.439768216083));
#143758=CARTESIAN_POINT('Ctrl Pts',(140.239976753769,2.35693219333363,125.375029413135));
#143759=CARTESIAN_POINT('Ctrl Pts',(140.232580396834,2.2107515461741,125.31614522788));
#143760=CARTESIAN_POINT('Ctrl Pts',(140.225182907497,2.06454851838484,125.257252027305));
#143761=CARTESIAN_POINT('Ctrl Pts',(140.217785418161,1.9160162791809,125.204215368678));
#143762=CARTESIAN_POINT('Ctrl Pts',(140.210387928824,1.76566736176624,125.157206526336));
#143763=CARTESIAN_POINT('Ctrl Pts',(140.202987846309,1.61526573977063,125.110181205117));
#143764=CARTESIAN_POINT('Ctrl Pts',(140.195587763794,1.46304652769936,125.069188018563));
#143765=CARTESIAN_POINT('Ctrl Pts',(140.188187681279,1.30953597359666,125.034347957584));
#143766=CARTESIAN_POINT('Ctrl Pts',(140.180779461613,1.15585661885894,124.999469586376));
#143767=CARTESIAN_POINT('Ctrl Pts',(140.173371241946,1.00088345059321,124.970757935549));
#143768=CARTESIAN_POINT('Ctrl Pts',(140.16596302228,0.845152158611476,124.948282715822));
#143769=CARTESIAN_POINT('Ctrl Pts',(140.158550242978,0.689325016618268,
124.925793662972));
#143770=CARTESIAN_POINT('Ctrl Pts',(140.151137463676,0.532739191569369,
124.909548728185));
#143771=CARTESIAN_POINT('Ctrl Pts',(140.143724684374,0.375933479202662,
124.899565567633));
#143772=CARTESIAN_POINT('Ctrl Pts',(140.136301313345,0.218903715480498,
124.889568142673));
#143773=CARTESIAN_POINT('Ctrl Pts',(140.128877942316,0.06165380914696,124.885850370148));
#143774=CARTESIAN_POINT('Ctrl Pts',(140.121454571288,-0.0952786301733748,
124.888377812898));
#143775=CARTESIAN_POINT('Ctrl Pts',(140.117518521847,-0.17848797504547,
124.889717923689));
#143776=CARTESIAN_POINT('Ctrl Pts',(140.113582472406,-0.261608161221388,
124.892812922281));
#143777=CARTESIAN_POINT('Ctrl Pts',(140.109646422965,-0.344559992659762,
124.897651806903));
#143778=CARTESIAN_POINT('Ctrl Pts',(140.10222315656,-0.501004557910546,
124.906777792284));
#143779=CARTESIAN_POINT('Ctrl Pts',(140.094799890154,-0.657322869908095,
124.922137235511));
#143780=CARTESIAN_POINT('Ctrl Pts',(140.087376623749,-0.812977888652229,
124.943729464263));
#143781=CARTESIAN_POINT('Ctrl Pts',(140.079962131028,-0.96844893609033,
124.965296172795));
#143782=CARTESIAN_POINT('Ctrl Pts',(140.072547638307,-1.1232578846003,124.993080952733));
#143783=CARTESIAN_POINT('Ctrl Pts',(140.065133145586,-1.2768692081074,125.02703116635));
#143784=CARTESIAN_POINT('Ctrl Pts',(140.057725799232,-1.43033247523699,
125.060948657473));
#143785=CARTESIAN_POINT('Ctrl Pts',(140.050318452878,-1.5826000533251,125.101019671952));
#143786=CARTESIAN_POINT('Ctrl Pts',(140.042911106524,-1.73314315538902,
125.147139977938));
#143787=CARTESIAN_POINT('Ctrl Pts',(140.035509284849,-1.88357397672872,
125.193225885661));
#143788=CARTESIAN_POINT('Ctrl Pts',(140.028107463174,-2.03228252761314,
125.245351992432));
#143789=CARTESIAN_POINT('Ctrl Pts',(140.020705641498,-2.17875192039045,
125.303363377802));
#143790=CARTESIAN_POINT('Ctrl Pts',(140.013307727187,-2.32514399311632,
125.361344139413));
#143791=CARTESIAN_POINT('Ctrl Pts',(140.005909812875,-2.46929891562388,
125.425203855182));
#143792=CARTESIAN_POINT('Ctrl Pts',(139.998511898564,-2.61071674008065,
125.494738346108));
#143793=CARTESIAN_POINT('Ctrl Pts',(139.991115213652,-2.75211106345952,
125.564261281663));
#143794=CARTESIAN_POINT('Ctrl Pts',(139.983718528739,-2.8907688568771,125.639456956156));
#143795=CARTESIAN_POINT('Ctrl Pts',(139.976321843827,-3.02621177498084,
125.720073759464));
#143796=CARTESIAN_POINT('Ctrl Pts',(139.968925486892,-3.16164868740332,
125.800686988139));
#143797=CARTESIAN_POINT('Ctrl Pts',(139.961529129956,-3.29387068717532,
125.886720676746));
#143798=CARTESIAN_POINT('Ctrl Pts',(139.954132773021,-3.42242583036773,
125.977878254796));
#143799=CARTESIAN_POINT('Ctrl Pts',(139.946735283684,-3.5510006556812,126.069049789303));
#143800=CARTESIAN_POINT('Ctrl Pts',(139.939337794348,-3.67590720205223,
126.165346559318));
#143801=CARTESIAN_POINT('Ctrl Pts',(139.931940305011,-3.79672433481373,
126.266429934101));
#143802=CARTESIAN_POINT('Ctrl Pts',(139.924540222496,-3.9175838198334,126.367548743504));
#143803=CARTESIAN_POINT('Ctrl Pts',(139.917140139981,-4.03435075095351,
126.473457259045));
#143804=CARTESIAN_POINT('Ctrl Pts',(139.909740057466,-4.14663888517259,
126.583778131881));
#143805=CARTESIAN_POINT('Ctrl Pts',(139.902331837799,-4.25905049173922,
126.694220313858));
#143806=CARTESIAN_POINT('Ctrl Pts',(139.894923618133,-4.36697319961371,
126.809084280795));
#143807=CARTESIAN_POINT('Ctrl Pts',(139.887515398466,-4.47005880576604,
126.927957022029));
#143808=CARTESIAN_POINT('Ctrl Pts',(139.880102619164,-4.57320785938891,
127.046902927451));
#143809=CARTESIAN_POINT('Ctrl Pts',(139.872689839862,-4.67151364636655,
127.169862232749));
#143810=CARTESIAN_POINT('Ctrl Pts',(139.86527706056,-4.7646700798034,127.296391177402));
#143811=CARTESIAN_POINT('Ctrl Pts',(139.857853689531,-4.85795961952092,
127.423100912544));
#143812=CARTESIAN_POINT('Ctrl Pts',(139.850430318503,-4.94608490225515,
127.55339016543));
#143813=CARTESIAN_POINT('Ctrl Pts',(139.843006947474,-5.02878430982933,
127.686788015731));
#143814=CARTESIAN_POINT('Ctrl Pts',(139.839070898033,-5.07263352006995,
127.757518756797));
#143815=CARTESIAN_POINT('Ctrl Pts',(139.835134848592,-5.11495810104929,
127.82912304585));
#143816=CARTESIAN_POINT('Ctrl Pts',(139.831198799151,-5.15572450147464,
127.901528306289));
#143817=CARTESIAN_POINT('Ctrl Pts',(139.823436577619,-5.23611928206174,
128.044317587796));
#143818=CARTESIAN_POINT('Ctrl Pts',(139.815674356087,-5.31067601333723,
128.190622135892));
#143819=CARTESIAN_POINT('Ctrl Pts',(139.807912134555,-5.37908850597535,
128.339946405753));
#143820=CARTESIAN_POINT('Ctrl Pts',(139.800162163852,-5.44739302568525,
128.489035002596));
#143821=CARTESIAN_POINT('Ctrl Pts',(139.79241219315,-5.5095724986194,128.641133529821));
#143822=CARTESIAN_POINT('Ctrl Pts',(139.784662222447,-5.5653656799586,128.795720428075));
#143823=CARTESIAN_POINT('Ctrl Pts',(139.776638303261,-5.62313105680892,
128.955771714261));
#143824=CARTESIAN_POINT('Ctrl Pts',(139.768614384074,-5.67405018060018,
129.11849024006));
#143825=CARTESIAN_POINT('Ctrl Pts',(139.760590464888,-5.71788537890809,
129.283269773412));
#143826=CARTESIAN_POINT('Ctrl Pts',(139.752866423857,-5.7600823231272,129.441890996669));
#143827=CARTESIAN_POINT('Ctrl Pts',(139.745142382826,-5.79571510917827,
129.602421614688));
#143828=CARTESIAN_POINT('Ctrl Pts',(139.737418341795,-5.82462070112284,
129.764300883439));
#143829=CARTESIAN_POINT('Ctrl Pts',(139.729702869658,-5.85349422579409,
129.926000566637));
#143830=CARTESIAN_POINT('Ctrl Pts',(139.721987397521,-5.87565537091717,
130.089045600889));
#143831=CARTESIAN_POINT('Ctrl Pts',(139.714271925383,-5.89099142555501,
130.252862125694));
#143832=CARTESIAN_POINT('Ctrl Pts',(139.706566454259,-5.90630760116474,
130.416466306882));
#143833=CARTESIAN_POINT('Ctrl Pts',(139.698860983135,-5.91481629810642,
130.580839661933));
#143834=CARTESIAN_POINT('Ctrl Pts',(139.691155512011,-5.91645622347929,
130.745400307584));
#143835=CARTESIAN_POINT('Ctrl Pts',(139.690228738744,-5.9166534650198,130.765192790701));
#143836=CARTESIAN_POINT('Ctrl Pts',(139.689301965478,-5.91675140419712,
130.784987974349));
#143837=CARTESIAN_POINT('Ctrl Pts',(139.688375192211,-5.91674998479196,
130.804784839551));
#143838=CARTESIAN_POINT('',(137.938375192211,-5.917008063288,130.809669329993));
#143839=CARTESIAN_POINT('Ctrl Pts',(139.688375192172,-5.9167499847919,130.80478484039));
#143840=CARTESIAN_POINT('Ctrl Pts',(139.680584137911,-5.91673805233238,
130.971210067061));
#143841=CARTESIAN_POINT('Ctrl Pts',(139.672793083651,-5.90970006480498,
131.137483867577));
#143842=CARTESIAN_POINT('Ctrl Pts',(139.665002029391,-5.89569994840646,
131.303011478249));
#143843=CARTESIAN_POINT('Ctrl Pts',(139.657199697439,-5.88167956658594,
131.468778693135));
#143844=CARTESIAN_POINT('Ctrl Pts',(139.649397365486,-5.86067696226432,
131.633797253035));
#143845=CARTESIAN_POINT('Ctrl Pts',(139.641595033534,-5.83280745341976,
131.797480838804));
#143846=CARTESIAN_POINT('Ctrl Pts',(139.633773170766,-5.80486818155786,
131.961574157693));
#143847=CARTESIAN_POINT('Ctrl Pts',(139.625951307999,-5.77002767955835,
132.124325512147));
#143848=CARTESIAN_POINT('Ctrl Pts',(139.618129445232,-5.72845218244328,
132.285159778817));
#143849=CARTESIAN_POINT('Ctrl Pts',(139.610297413009,-5.68682263168829,
132.446203151285));
#143850=CARTESIAN_POINT('Ctrl Pts',(139.602465380787,-5.63844069455175,
132.605324163508));
#143851=CARTESIAN_POINT('Ctrl Pts',(139.594633348564,-5.58352163616306,
132.761965455371));
#143852=CARTESIAN_POINT('Ctrl Pts',(139.586782860964,-5.5284731666656,132.918975856317));
#143853=CARTESIAN_POINT('Ctrl Pts',(139.578932373364,-5.46685688233304,
133.073494561328));
#143854=CARTESIAN_POINT('Ctrl Pts',(139.571081885763,-5.39893602997023,
133.224984567458));
#143855=CARTESIAN_POINT('Ctrl Pts',(139.564971648955,-5.34607148024038,
133.342893143161));
#143856=CARTESIAN_POINT('Ctrl Pts',(139.558861412147,-5.28938863651094,
133.458967410419));
#143857=CARTESIAN_POINT('Ctrl Pts',(139.552751175339,-5.22903006457896,
133.572965888497));
#143858=CARTESIAN_POINT('Ctrl Pts',(139.545327908933,-5.15570103112815,
133.711461514633));
#143859=CARTESIAN_POINT('Ctrl Pts',(139.537904642528,-5.07675504096567,
133.847251270503));
#143860=CARTESIAN_POINT('Ctrl Pts',(139.530481376123,-4.99241593521631,
133.979846988549));
#143861=CARTESIAN_POINT('Ctrl Pts',(139.523066883402,-4.90817651128592,
134.112285989467));
#143862=CARTESIAN_POINT('Ctrl Pts',(139.515652390681,-4.81855685806873,
134.24153815499));
#143863=CARTESIAN_POINT('Ctrl Pts',(139.50823789796,-4.72382745082585,134.36713829479));
#143864=CARTESIAN_POINT('Ctrl Pts',(139.500830551606,-4.62918934735203,
134.492617376446));
#143865=CARTESIAN_POINT('Ctrl Pts',(139.493423205252,-4.52945151777752,
134.614451143893));
#143866=CARTESIAN_POINT('Ctrl Pts',(139.486015858898,-4.4249285618775,134.732201982079));
#143867=CARTESIAN_POINT('Ctrl Pts',(139.478614037223,-4.32048356314145,
134.849864997248));
#143868=CARTESIAN_POINT('Ctrl Pts',(139.471212215547,-4.21126079104434,
134.96345086859));
#143869=CARTESIAN_POINT('Ctrl Pts',(139.463810393872,-4.09761600135079,
135.072553873263));
#143870=CARTESIAN_POINT('Ctrl Pts',(139.456412479561,-3.98403120385755,
135.181599283308));
#143871=CARTESIAN_POINT('Ctrl Pts',(139.449014565249,-3.86602930634111,
135.28616628175));
#143872=CARTESIAN_POINT('Ctrl Pts',(139.441616650938,-3.74400382473826,
135.385885027939));
#143873=CARTESIAN_POINT('Ctrl Pts',(139.434219966026,-3.62199862155639,
135.485587202682));
#143874=CARTESIAN_POINT('Ctrl Pts',(139.426823281113,-3.49597145012708,
135.580442488246));
#143875=CARTESIAN_POINT('Ctrl Pts',(139.419426596201,-3.36634998636792,
135.67012040734));
#143876=CARTESIAN_POINT('Ctrl Pts',(139.412030239266,-3.23673427016026,
135.759794350021));
#143877=CARTESIAN_POINT('Ctrl Pts',(139.40463388233,-3.10352488550231,135.844291170306));
#143878=CARTESIAN_POINT('Ctrl Pts',(139.397237525395,-2.96717942633891,
135.923323091975));
#143879=CARTESIAN_POINT('Ctrl Pts',(139.389840036058,-2.83081309233788,
136.002367113633));
#143880=CARTESIAN_POINT('Ctrl Pts',(139.382442546722,-2.69131005079165,
136.075944383498));
#143881=CARTESIAN_POINT('Ctrl Pts',(139.375045057385,-2.54915334377066,
136.14381262994));
#143882=CARTESIAN_POINT('Ctrl Pts',(139.36764497487,-2.40694680393599,136.211704667491));
#143883=CARTESIAN_POINT('Ctrl Pts',(139.360244892355,-2.26208508319391,
136.273883536337));
#143884=CARTESIAN_POINT('Ctrl Pts',(139.35284480984,-2.11507193508654,136.33015479324));
#143885=CARTESIAN_POINT('Ctrl Pts',(139.345436590174,-1.96789713090972,
136.386487926174));
#143886=CARTESIAN_POINT('Ctrl Pts',(139.338028370507,-1.81856652372409,
136.436900340648));
#143887=CARTESIAN_POINT('Ctrl Pts',(139.330620150841,-1.66760049015753,
136.481247014855));
#143888=CARTESIAN_POINT('Ctrl Pts',(139.323207371539,-1.51654153951631,
136.525620983701));
#143889=CARTESIAN_POINT('Ctrl Pts',(139.315794592236,-1.36384551800387,
136.563921682478));
#143890=CARTESIAN_POINT('Ctrl Pts',(139.308381812934,-1.2100432634918,136.596055176413));
#143891=CARTESIAN_POINT('Ctrl Pts',(139.300958441906,-1.05602124910576,
136.628234584191));
#143892=CARTESIAN_POINT('Ctrl Pts',(139.293535070877,-0.900890212021972,
136.654229126076));
#143893=CARTESIAN_POINT('Ctrl Pts',(139.286111699848,-0.745187208254172,
136.673996601778));
#143894=CARTESIAN_POINT('Ctrl Pts',(139.282175650407,-0.662629739613447,
136.684477791709));
#143895=CARTESIAN_POINT('Ctrl Pts',(139.278239600966,-0.579911501811691,
136.693209200584));
#143896=CARTESIAN_POINT('Ctrl Pts',(139.274303551526,-0.497112450655344,
136.700190480605));
#143897=CARTESIAN_POINT('Ctrl Pts',(139.26688028512,-0.34095602424579,136.713356956847));
#143898=CARTESIAN_POINT('Ctrl Pts',(139.259457018715,-0.184040020820868,
136.720335139353));
#143899=CARTESIAN_POINT('Ctrl Pts',(139.252033752309,-0.0268961411683008,
136.721049485513));
#143900=CARTESIAN_POINT('Ctrl Pts',(139.244619259588,0.130062007468616,
136.721762987375));
#143901=CARTESIAN_POINT('Ctrl Pts',(139.237204766867,0.287247126580009,
136.716227387588));
#143902=CARTESIAN_POINT('Ctrl Pts',(139.229790274146,0.444121639883464,
136.704418797914));
#143903=CARTESIAN_POINT('Ctrl Pts',(139.222382927792,0.600844951624832,
136.692621589803));
#143904=CARTESIAN_POINT('Ctrl Pts',(139.214975581439,0.757257883806268,
136.67456345632));
#143905=CARTESIAN_POINT('Ctrl Pts',(139.207568235085,0.912822209628291,
136.650272537541));
#143906=CARTESIAN_POINT('Ctrl Pts',(139.200166413409,1.06827050970707,136.625999735846));
#143907=CARTESIAN_POINT('Ctrl Pts',(139.192764591734,1.22287109641961,136.595503462281));
#143908=CARTESIAN_POINT('Ctrl Pts',(139.185362770059,1.37609032896568,136.558863721139));
#143909=CARTESIAN_POINT('Ctrl Pts',(139.177964855747,1.5292286782716,136.52224332183));
#143910=CARTESIAN_POINT('Ctrl Pts',(139.170566941436,1.68098676351751,136.479486000311));
#143911=CARTESIAN_POINT('Ctrl Pts',(139.163169027125,1.83084072231294,136.430722924778));
#143912=CARTESIAN_POINT('Ctrl Pts',(139.155772342212,1.98066977809889,136.381967952784));
#143913=CARTESIAN_POINT('Ctrl Pts',(139.1483756573,2.12859498082751,136.327209323002));
#143914=CARTESIAN_POINT('Ctrl Pts',(139.140978972388,2.27410712131415,136.266628220246));
#143915=CARTESIAN_POINT('Ctrl Pts',(139.133582615453,2.41961280963993,136.20604980372));
#143916=CARTESIAN_POINT('Ctrl Pts',(139.126186258517,2.5627053038478,136.139649571035));
#143917=CARTESIAN_POINT('Ctrl Pts',(139.118789901582,2.70289514894905,136.067656958861));
#143918=CARTESIAN_POINT('Ctrl Pts',(139.111392412245,2.84310645747352,135.995653324434));
#143919=CARTESIAN_POINT('Ctrl Pts',(139.103994922909,2.98041389993418,135.918055776236));
#143920=CARTESIAN_POINT('Ctrl Pts',(139.096597433572,3.11435255031025,135.835139757508));
#143921=CARTESIAN_POINT('Ctrl Pts',(139.089197351057,3.24833815267259,135.752194672698));
#143922=CARTESIAN_POINT('Ctrl Pts',(139.081797268542,3.37895229453517,135.663927601756));
#143923=CARTESIAN_POINT('Ctrl Pts',(139.074397186027,3.50575909419982,135.570657265482));
#143924=CARTESIAN_POINT('Ctrl Pts',(139.066988966361,3.63270533097677,135.477284368885));
#143925=CARTESIAN_POINT('Ctrl Pts',(139.059580746694,3.75583556381397,135.378897441212));
#143926=CARTESIAN_POINT('Ctrl Pts',(139.052172527028,3.87474650548079,135.275855902229));
#143927=CARTESIAN_POINT('Ctrl Pts',(139.044759747726,3.99373063484815,135.172750942898));
#143928=CARTESIAN_POINT('Ctrl Pts',(139.037346968424,4.10849002689675,135.064985918659));
#143929=CARTESIAN_POINT('Ctrl Pts',(139.029934189121,4.21865872080517,134.952956664408));
#143930=CARTESIAN_POINT('Ctrl Pts',(139.022510818093,4.32898482890984,134.840767337505));
#143931=CARTESIAN_POINT('Ctrl Pts',(139.015087447064,4.43470688803128,134.724301887308));
#143932=CARTESIAN_POINT('Ctrl Pts',(139.007664076035,4.53549910197673,134.603989343964));
#143933=CARTESIAN_POINT('Ctrl Pts',(139.003728026594,4.58894155228695,134.540196746623));
#143934=CARTESIAN_POINT('Ctrl Pts',(138.999791977154,4.64099876189668,134.475323090231));
#143935=CARTESIAN_POINT('Ctrl Pts',(138.995855927713,4.69162722012794,134.409435455881));
#143936=CARTESIAN_POINT('Ctrl Pts',(138.988432661307,4.78711091229139,134.285173433781));
#143937=CARTESIAN_POINT('Ctrl Pts',(138.981009394902,4.87779878760417,134.156927434104));
#143938=CARTESIAN_POINT('Ctrl Pts',(138.973586128496,4.96333989266453,134.025103959154));
#143939=CARTESIAN_POINT('Ctrl Pts',(138.966171635775,5.04877989524251,133.893436288605));
#143940=CARTESIAN_POINT('Ctrl Pts',(138.958757143054,5.12908503470471,133.758199869283));
#143941=CARTESIAN_POINT('Ctrl Pts',(138.951342650333,5.2039446400889,133.619834067164));
#143942=CARTESIAN_POINT('Ctrl Pts',(138.94393530398,5.278732092967,133.481601627214));
#143943=CARTESIAN_POINT('Ctrl Pts',(138.936527957626,5.34808428427725,133.340246135284));
#143944=CARTESIAN_POINT('Ctrl Pts',(138.929120611272,5.41173396433075,133.19623562722));
#143945=CARTESIAN_POINT('Ctrl Pts',(138.921718789597,5.47533617205153,133.052332527627));
#143946=CARTESIAN_POINT('Ctrl Pts',(138.914316967921,5.53324418684925,132.905778694735));
#143947=CARTESIAN_POINT('Ctrl Pts',(138.906915146246,5.58523687271368,132.757066339937));
#143948=CARTESIAN_POINT('Ctrl Pts',(138.899517231935,5.63720211204399,132.608432489233));
#143949=CARTESIAN_POINT('Ctrl Pts',(138.892119317623,5.68325811847254,132.457642737417));
#143950=CARTESIAN_POINT('Ctrl Pts',(138.884721403312,5.72323208709994,132.305208724368));
#143951=CARTESIAN_POINT('Ctrl Pts',(138.8773247184,5.7631994127789,132.152800043086));
#143952=CARTESIAN_POINT('Ctrl Pts',(138.869928033487,5.79708661204707,131.99874800362));
#143953=CARTESIAN_POINT('Ctrl Pts',(138.862531348575,5.82477088081715,131.843578952895));
#143954=CARTESIAN_POINT('Ctrl Pts',(138.85513499164,5.85245392203775,131.688416782529));
#143955=CARTESIAN_POINT('Ctrl Pts',(138.847738634704,5.87393451407551,131.53213806688));
#143956=CARTESIAN_POINT('Ctrl Pts',(138.840342277769,5.88914112612127,131.375278614416));
#143957=CARTESIAN_POINT('Ctrl Pts',(138.832944788432,5.90435006633816,131.218395146369));
#143958=CARTESIAN_POINT('Ctrl Pts',(138.825547299096,5.91328307793312,131.060931136052));
#143959=CARTESIAN_POINT('Ctrl Pts',(138.818149809759,5.91592059523523,130.903426622692));
#143960=CARTESIAN_POINT('Ctrl Pts',(138.810749727244,5.91855903711495,130.745866896369));
#143961=CARTESIAN_POINT('Ctrl Pts',(138.803349644729,5.91489758458202,130.588267011748));
#143962=CARTESIAN_POINT('Ctrl Pts',(138.795949562214,5.90496878176886,130.431165964824));
#143963=CARTESIAN_POINT('Ctrl Pts',(138.788541342548,5.8950290612163,130.273892169149));
#143964=CARTESIAN_POINT('Ctrl Pts',(138.781133122881,5.8788082509739,130.117118679392));
#143965=CARTESIAN_POINT('Ctrl Pts',(138.773724903215,5.85639075447156,129.961379067685));
#143966=CARTESIAN_POINT('Ctrl Pts',(138.766312123912,5.83395946037415,129.805543600845));
#143967=CARTESIAN_POINT('Ctrl Pts',(138.75889934461,5.80532394797405,129.650743646252));
#143968=CARTESIAN_POINT('Ctrl Pts',(138.751486565308,5.77061943361669,129.497501055537));
#143969=CARTESIAN_POINT('Ctrl Pts',(138.74406319428,5.73586533182175,129.344039504623));
#143970=CARTESIAN_POINT('Ctrl Pts',(138.736639823251,5.6950250054579,129.192140121422));
#143971=CARTESIAN_POINT('Ctrl Pts',(138.729216452222,5.64828330893846,129.042308908771));
#143972=CARTESIAN_POINT('Ctrl Pts',(138.725280402781,5.62349973989224,128.962864804673));
#143973=CARTESIAN_POINT('Ctrl Pts',(138.72134435334,5.597057888815,128.884001803985));
#143974=CARTESIAN_POINT('Ctrl Pts',(138.7174083039,5.56899067434469,128.805792772442));
#143975=CARTESIAN_POINT('Ctrl Pts',(138.709985037494,5.51605678380148,128.658292979773));
#143976=CARTESIAN_POINT('Ctrl Pts',(138.702561771089,5.45717880393865,128.51267460645));
#143977=CARTESIAN_POINT('Ctrl Pts',(138.695138504683,5.39250903777161,128.369452643935));
#143978=CARTESIAN_POINT('Ctrl Pts',(138.687724011962,5.32791570589757,128.226399957886));
#143979=CARTESIAN_POINT('Ctrl Pts',(138.680309519241,5.25754436566888,128.08573838172));
#143980=CARTESIAN_POINT('Ctrl Pts',(138.67289502652,5.18159674288067,127.947966779758));
#143981=CARTESIAN_POINT('Ctrl Pts',(138.665487680167,5.10572232127067,127.810327967253));
#143982=CARTESIAN_POINT('Ctrl Pts',(138.658080333813,5.02428249593846,127.675573908359));
#143983=CARTESIAN_POINT('Ctrl Pts',(138.650672987459,4.93752658371395,127.544182432617));
#143984=CARTESIAN_POINT('Ctrl Pts',(138.643271165784,4.8508353773219,127.412888953594));
#143985=CARTESIAN_POINT('Ctrl Pts',(138.635869344108,4.75883618356946,127.28495337425));
#143986=CARTESIAN_POINT('Ctrl Pts',(138.628467522433,4.66182358442672,127.160827794854));
#143987=CARTESIAN_POINT('Ctrl Pts',(138.621069608121,4.56486219748007,127.036767740384));
#143988=CARTESIAN_POINT('Ctrl Pts',(138.61367169381,4.46289290514456,126.916513973701));
#143989=CARTESIAN_POINT('Ctrl Pts',(138.606273779499,4.35625275927245,126.800488434312));
#143990=CARTESIAN_POINT('Ctrl Pts',(138.598877094586,4.24963033505785,126.684482176264));
#143991=CARTESIAN_POINT('Ctrl Pts',(138.591480409674,4.13833885021982,126.572703025522));
#143992=CARTESIAN_POINT('Ctrl Pts',(138.584083724762,4.02275475672535,126.465538804015));
#143993=CARTESIAN_POINT('Ctrl Pts',(138.576687367827,3.90717578835071,126.358379334282));
#143994=CARTESIAN_POINT('Ctrl Pts',(138.569291010891,3.78730486352086,126.255834640711));
#143995=CARTESIAN_POINT('Ctrl Pts',(138.561894653956,3.66355410892532,126.158254521761));
#143996=CARTESIAN_POINT('Ctrl Pts',(138.554497164619,3.53978440777332,126.060659463046));
#143997=CARTESIAN_POINT('Ctrl Pts',(138.547099675283,3.41213398724868,125.968030723546));
#143998=CARTESIAN_POINT('Ctrl Pts',(138.539702185946,3.28104662192607,125.880676668809));
#143999=CARTESIAN_POINT('Ctrl Pts',(138.532302103431,3.14991330413065,125.793291992243));
#144000=CARTESIAN_POINT('Ctrl Pts',(138.524902020916,3.01534095320797,125.711185888728));
#144001=CARTESIAN_POINT('Ctrl Pts',(138.517501938401,2.8778006326532,125.634622318464));
#144002=CARTESIAN_POINT('Ctrl Pts',(138.510093718734,2.74010907237648,125.557974558684));
#144003=CARTESIAN_POINT('Ctrl Pts',(138.502685499068,2.59944335123651,125.486881685119));
#144004=CARTESIAN_POINT('Ctrl Pts',(138.495277279402,2.45629800069497,125.421561095544));
#144005=CARTESIAN_POINT('Ctrl Pts',(138.487864500099,2.31306454657868,125.356200302236));
#144006=CARTESIAN_POINT('Ctrl Pts',(138.480451720797,2.16734876670303,125.296619013161));
#144007=CARTESIAN_POINT('Ctrl Pts',(138.473038941495,2.01966279736456,125.242985540533));
#144008=CARTESIAN_POINT('Ctrl Pts',(138.465615570467,1.87176580738731,125.189275433885));
#144009=CARTESIAN_POINT('Ctrl Pts',(138.458192199438,1.7218933603057,125.141530230144));
#144010=CARTESIAN_POINT('Ctrl Pts',(138.450768828409,1.57057108896393,125.099867912951));
#144011=CARTESIAN_POINT('Ctrl Pts',(138.446832778968,1.49033638977069,125.077777552701));
#144012=CARTESIAN_POINT('Ctrl Pts',(138.442896729527,1.40969424739082,125.057396452677));
#144013=CARTESIAN_POINT('Ctrl Pts',(138.438960680087,1.32872375915806,125.038736303205));
#144014=CARTESIAN_POINT('Ctrl Pts',(138.431537413681,1.1760159453532,125.003543843664));
#144015=CARTESIAN_POINT('Ctrl Pts',(138.424114147276,1.02167809745959,124.974369267926));
#144016=CARTESIAN_POINT('Ctrl Pts',(138.41669088087,0.866225815879054,124.951362804615));
#144017=CARTESIAN_POINT('Ctrl Pts',(138.409276388149,0.710957265985616,
124.928383533034));
#144018=CARTESIAN_POINT('Ctrl Pts',(138.401861895428,0.554577269905189,
124.91155791682));
#144019=CARTESIAN_POINT('Ctrl Pts',(138.394447402707,0.397614574039386,
124.900985886701));
#144020=CARTESIAN_POINT('Ctrl Pts',(138.387040056354,0.240803164729622,
124.890424046303));
#144021=CARTESIAN_POINT('Ctrl Pts',(138.37963271,0.0834105436789232,124.886103817468));
#144022=CARTESIAN_POINT('Ctrl Pts',(138.372225363646,-0.0740265157508794,
124.888073721424));
#144023=CARTESIAN_POINT('Ctrl Pts',(138.364823541971,-0.231346152682223,
124.890042156151));
#144024=CARTESIAN_POINT('Ctrl Pts',(138.357421720295,-0.388709790336678,
124.898291377771));
#144025=CARTESIAN_POINT('Ctrl Pts',(138.35001989862,-0.545577835203225,
124.91281791737));
#144026=CARTESIAN_POINT('Ctrl Pts',(138.342621984309,-0.702363070649498,
124.927336788521));
#144027=CARTESIAN_POINT('Ctrl Pts',(138.335224069997,-0.858652863569166,
124.948126343829));
#144028=CARTESIAN_POINT('Ctrl Pts',(138.327826155686,-1.01391003954467,
124.975131080637));
#144029=CARTESIAN_POINT('Ctrl Pts',(138.320429470774,-1.1691414145945,125.002131329746));
#144030=CARTESIAN_POINT('Ctrl Pts',(138.313032785861,-1.32334014586377,
125.035344646546));
#144031=CARTESIAN_POINT('Ctrl Pts',(138.305636100949,-1.47597646629815,
125.074663938558));
#144032=CARTESIAN_POINT('Ctrl Pts',(138.298239744014,-1.62860601867814,
125.113981487112));
#144033=CARTESIAN_POINT('Ctrl Pts',(138.290843387078,-1.77967293647711,
125.159404379423));
#144034=CARTESIAN_POINT('Ctrl Pts',(138.283447030143,-1.92866015980101,
125.210774956249));
#144035=CARTESIAN_POINT('Ctrl Pts',(138.276049540806,-2.07767019344926,
125.26215339804));
#144036=CARTESIAN_POINT('Ctrl Pts',(138.26865205147,-2.2245995457011,125.319481215793));
#144037=CARTESIAN_POINT('Ctrl Pts',(138.261254562133,-2.36894890889079,
125.382551728499));
#144038=CARTESIAN_POINT('Ctrl Pts',(138.253854479618,-2.51334887352568,
125.445644350475));
#144039=CARTESIAN_POINT('Ctrl Pts',(138.246454397103,-2.6551667065646,125.51448352609));
#144040=CARTESIAN_POINT('Ctrl Pts',(138.239054314588,-2.79392570948898,
125.58881561322));
#144041=CARTESIAN_POINT('Ctrl Pts',(138.231646094922,-2.93283729220205,
125.663229436122));
#144042=CARTESIAN_POINT('Ctrl Pts',(138.224237875255,-3.0686829984143,125.743148056475));
#144043=CARTESIAN_POINT('Ctrl Pts',(138.216829655589,-3.20101261888635,
125.828272919763));
#144044=CARTESIAN_POINT('Ctrl Pts',(138.209416876287,-3.33342368603194,
125.913450175983));
#144045=CARTESIAN_POINT('Ctrl Pts',(138.202004096985,-3.46231405028907,
126.003839846379));
#144046=CARTESIAN_POINT('Ctrl Pts',(138.194591317683,-3.58726528364737,
126.099102033042));
#144047=CARTESIAN_POINT('Ctrl Pts',(138.187167946654,-3.71239505318744,
126.194500334784));
#144048=CARTESIAN_POINT('Ctrl Pts',(138.179744575625,-3.83357416379487,
126.294784820258));
#144049=CARTESIAN_POINT('Ctrl Pts',(138.172321204596,-3.9504192350998,126.399577032706));
#144050=CARTESIAN_POINT('Ctrl Pts',(138.168385155156,-4.01237329556604,
126.455140378201));
#144051=CARTESIAN_POINT('Ctrl Pts',(138.164449105715,-4.07310953999066,
126.511970414092));
#144052=CARTESIAN_POINT('Ctrl Pts',(138.160513056274,-4.13257537892972,
126.570006912458));
#144053=CARTESIAN_POINT('Ctrl Pts',(138.15319622246,-4.24311811160658,126.67789260345));
#144054=CARTESIAN_POINT('Ctrl Pts',(138.145879388645,-4.34962365026246,
126.79029608547));
#144055=CARTESIAN_POINT('Ctrl Pts',(138.138562554831,-4.4516921232071,126.906878378649));
#144056=CARTESIAN_POINT('Ctrl Pts',(138.131254509615,-4.55363799684109,
127.023320639275));
#144057=CARTESIAN_POINT('Ctrl Pts',(138.123946464399,-4.65115715751967,
127.143931437888));
#144058=CARTESIAN_POINT('Ctrl Pts',(138.116638419182,-4.74388446255217,
127.268333076885));
#144059=CARTESIAN_POINT('Ctrl Pts',(138.109210784725,-4.83812916213939,
127.394770430923));
#144060=CARTESIAN_POINT('Ctrl Pts',(138.101783150268,-4.92742349399904,
127.525123525742));
#144061=CARTESIAN_POINT('Ctrl Pts',(138.094355515811,-5.01142397125429,
127.65895756822));
#144062=CARTESIAN_POINT('Ctrl Pts',(138.087060421163,-5.09392553154876,
127.790403456215));
#144063=CARTESIAN_POINT('Ctrl Pts',(138.079765326516,-5.17132035816477,
127.925206767697));
#144064=CARTESIAN_POINT('Ctrl Pts',(138.072470231869,-5.2433247161891,128.062923679918));
#144065=CARTESIAN_POINT('Ctrl Pts',(138.065178223667,-5.31529861023819,
128.200582326158));
#144066=CARTESIAN_POINT('Ctrl Pts',(138.057886215466,-5.38188639496685,
128.341151780288));
#144067=CARTESIAN_POINT('Ctrl Pts',(138.050594207265,-5.4428493125588,128.484161935712));
#144068=CARTESIAN_POINT('Ctrl Pts',(138.043303748025,-5.50379928046742,
128.627141713059));
#144069=CARTESIAN_POINT('Ctrl Pts',(138.036013288785,-5.55912660869075,
128.772560805855));
#144070=CARTESIAN_POINT('Ctrl Pts',(138.028722829545,-5.60864002550062,
128.919927645329));
#144071=CARTESIAN_POINT('Ctrl Pts',(138.021193859767,-5.65977329522876,
129.07211565491));
#144072=CARTESIAN_POINT('Ctrl Pts',(138.013664889989,-5.7047055945997,129.226380625873));
#144073=CARTESIAN_POINT('Ctrl Pts',(138.006135920212,-5.74328164631964,
129.382162848777));
#144074=CARTESIAN_POINT('Ctrl Pts',(137.998841500885,-5.78065593596289,
129.533091978651));
#144075=CARTESIAN_POINT('Ctrl Pts',(137.991547081559,-5.81206404154171,
129.685444843784));
#144076=CARTESIAN_POINT('Ctrl Pts',(137.984252662233,-5.83741664668609,
129.838701539272));
#144077=CARTESIAN_POINT('Ctrl Pts',(137.97660641723,-5.86399206300757,129.999350137845));
#144078=CARTESIAN_POINT('Ctrl Pts',(137.968960172226,-5.88391324967551,
130.160991447785));
#144079=CARTESIAN_POINT('Ctrl Pts',(137.961313927222,-5.89713851398654,
130.323020914906));
#144080=CARTESIAN_POINT('Ctrl Pts',(137.953667682218,-5.91036377829757,
130.485050382027));
#144081=CARTESIAN_POINT('Ctrl Pts',(137.946021437215,-5.91689314513619,
130.647467521529));
#144082=CARTESIAN_POINT('Ctrl Pts',(137.938375192211,-5.91674761862911,
130.809669096323));
#144083=CARTESIAN_POINT('',(136.188375192211,-5.92482275393929,130.801481359489));
#144084=CARTESIAN_POINT('Ctrl Pts',(137.938375192211,-5.91858262641488,
130.809670742684));
#144085=CARTESIAN_POINT('Ctrl Pts',(137.919605272295,-5.92227655107304,
131.20796854486));
#144086=CARTESIAN_POINT('Ctrl Pts',(137.808019477772,-5.70376707825749,
133.571789017959));
#144087=CARTESIAN_POINT('Ctrl Pts',(137.60361780865,-2.52345964543731,137.331972121637));
#144088=CARTESIAN_POINT('Ctrl Pts',(137.325170184835,4.12787285265972,136.455752149097));
#144089=CARTESIAN_POINT('Ctrl Pts',(137.046722561023,6.98589185696212,130.386179444888));
#144090=CARTESIAN_POINT('Ctrl Pts',(136.768274937209,3.42421752450535,124.700894809093));
#144091=CARTESIAN_POINT('Ctrl Pts',(136.489827313397,-3.28414543064536,
124.624397080398));
#144092=CARTESIAN_POINT('Ctrl Pts',(136.296527398397,-5.84603763581142,
128.513744555582));
#144093=CARTESIAN_POINT('Ctrl Pts',(136.196043358002,-5.92579277232221,
130.639208488848));
#144094=CARTESIAN_POINT('Ctrl Pts',(136.188375192211,-5.92482275393929,
130.801481359489));
#144095=CARTESIAN_POINT('',(134.438375192211,-5.90967939056383,130.800446782654));
#144096=CARTESIAN_POINT('Ctrl Pts',(136.188375192211,-5.92482275393929,
130.801481359489));
#144097=CARTESIAN_POINT('Ctrl Pts',(136.103227483398,-5.91405161973785,
132.603367692488));
#144098=CARTESIAN_POINT('Ctrl Pts',(135.925263899979,-4.07309906563022,
136.388452668));
#144099=CARTESIAN_POINT('Ctrl Pts',(135.654484441958,2.37394968768175,137.387818934492));
#144100=CARTESIAN_POINT('Ctrl Pts',(135.376036818145,6.82202772839269,132.365609541781));
#144101=CARTESIAN_POINT('Ctrl Pts',(135.097589194333,5.00099556129847,125.908688658965));
#144102=CARTESIAN_POINT('Ctrl Pts',(134.819141570519,-1.41570721441751,
123.950651139233));
#144103=CARTESIAN_POINT('Ctrl Pts',(134.599403569813,-5.45281051817537,
127.375725945688));
#144104=CARTESIAN_POINT('Ctrl Pts',(134.47248144371,-5.91406978814998,130.073942001419));
#144105=CARTESIAN_POINT('Ctrl Pts',(134.438375192211,-5.90967939056383,
130.800446782654));
#144106=CARTESIAN_POINT('',(132.688375175112,-5.91363808545199,130.808706388299));
#144107=CARTESIAN_POINT('Ctrl Pts',(134.438375192211,-5.90967939056383,
130.800446782654));
#144108=CARTESIAN_POINT('Ctrl Pts',(134.379665569105,-5.90212187321015,
132.051033405842));
#144109=CARTESIAN_POINT('Ctrl Pts',(134.228140071397,-4.90112661354537,
135.289767902303));
#144110=CARTESIAN_POINT('Ctrl Pts',(133.98379869908,0.428812026623837,137.789607984421));
#144111=CARTESIAN_POINT('Ctrl Pts',(133.705351075268,6.10866981692772,134.219285740918));
#144112=CARTESIAN_POINT('Ctrl Pts',(133.426903451454,6.17495847058624,127.510814137418));
#144113=CARTESIAN_POINT('Ctrl Pts',(133.148455827642,0.566761953268891,
123.828950850487));
#144114=CARTESIAN_POINT('Ctrl Pts',(132.902279741227,-4.85191927268251,
126.240955591494));
#144115=CARTESIAN_POINT('Ctrl Pts',(132.748919529417,-5.90178715204232,
129.519491859617));
#144116=CARTESIAN_POINT('Ctrl Pts',(132.688375192211,-5.91051263528418,
130.808703727191));
#144117=CARTESIAN_POINT('',(130.938375192211,-5.92111984587309,130.806604383885));
#144118=CARTESIAN_POINT('Ctrl Pts',(132.688375158095,-5.91674840209997,
130.808709036521));
#144119=CARTESIAN_POINT('Ctrl Pts',(132.679863463167,-5.91661505896896,
130.990144580226));
#144120=CARTESIAN_POINT('Ctrl Pts',(132.671351768239,-5.90813228569475,
131.171242140953));
#144121=CARTESIAN_POINT('Ctrl Pts',(132.662840073311,-5.89141688080036,
131.351295439204));
#144122=CARTESIAN_POINT('Ctrl Pts',(132.654286777509,-5.87461977943247,
131.532228747219));
#144123=CARTESIAN_POINT('Ctrl Pts',(132.645733481707,-5.84950948183229,
131.71210743218));
#144124=CARTESIAN_POINT('Ctrl Pts',(132.637180185905,-5.8162539680182,131.89023369579));
#144125=CARTESIAN_POINT('Ctrl Pts',(132.628572394587,-5.78278657372961,
132.069494853226));
#144126=CARTESIAN_POINT('Ctrl Pts',(132.619964603269,-5.74106992332052,
132.246981060688));
#144127=CARTESIAN_POINT('Ctrl Pts',(132.611356811951,-5.69132379711266,
132.42200211027));
#144128=CARTESIAN_POINT('Ctrl Pts',(132.604758067973,-5.65318835230238,
132.556173473667));
#144129=CARTESIAN_POINT('Ctrl Pts',(132.598159323995,-5.61033516103908,
132.688896533316));
#144130=CARTESIAN_POINT('Ctrl Pts',(132.591560580017,-5.56288192611719,
132.819869297423));
#144131=CARTESIAN_POINT('Ctrl Pts',(132.584137313612,-5.50949934212925,
132.967207294329));
#144132=CARTESIAN_POINT('Ctrl Pts',(132.576714047206,-5.45017842274767,
133.112645788839));
#144133=CARTESIAN_POINT('Ctrl Pts',(132.569290780801,-5.38507303773925,
133.255670255436));
#144134=CARTESIAN_POINT('Ctrl Pts',(132.56187628808,-5.32004460188919,133.398525678991));
#144135=CARTESIAN_POINT('Ctrl Pts',(132.554461795359,-5.24924546216386,
133.538972417469));
#144136=CARTESIAN_POINT('Ctrl Pts',(132.547047302638,-5.17287886179537,
133.676512222842));
#144137=CARTESIAN_POINT('Ctrl Pts',(132.539639956284,-5.09658586643148,
133.813919462173));
#144138=CARTESIAN_POINT('Ctrl Pts',(132.53223260993,-5.01473627332167,133.948425022081));
#144139=CARTESIAN_POINT('Ctrl Pts',(132.524825263577,-4.92758085248979,
134.079551834072));
#144140=CARTESIAN_POINT('Ctrl Pts',(132.517423441901,-4.84049043545895,
134.210580846739));
#144141=CARTESIAN_POINT('Ctrl Pts',(132.510021620226,-4.74810227594555,
134.338235819595));
#144142=CARTESIAN_POINT('Ctrl Pts',(132.502619798551,-4.65071233059291,
134.462065551069));
#144143=CARTESIAN_POINT('Ctrl Pts',(132.495221884239,-4.55337379663426,
134.585829913792));
#144144=CARTESIAN_POINT('Ctrl Pts',(132.487823969928,-4.45103896551377,
134.705772764018));
#144145=CARTESIAN_POINT('Ctrl Pts',(132.480426055617,-4.34404617176119,
134.821473190062));
#144146=CARTESIAN_POINT('Ctrl Pts',(132.473029370704,-4.23707115826996,
134.937154388795));
#144147=CARTESIAN_POINT('Ctrl Pts',(132.465632685792,-4.12543997164268,
135.048594288785));
#144148=CARTESIAN_POINT('Ctrl Pts',(132.45823600088,-4.00953024249916,135.155406215693));
#144149=CARTESIAN_POINT('Ctrl Pts',(132.450839643945,-3.8936256529145,135.262213406449));
#144150=CARTESIAN_POINT('Ctrl Pts',(132.443443287009,-3.77344317254592,
135.364392779179));
#144151=CARTESIAN_POINT('Ctrl Pts',(132.436046930074,-3.64939599084017,
135.461595791415));
#144152=CARTESIAN_POINT('Ctrl Pts',(132.428649440737,-3.52532981719431,
135.558813685681));
#144153=CARTESIAN_POINT('Ctrl Pts',(132.4212519514,-3.39739805791841,135.651053472161));
#144154=CARTESIAN_POINT('Ctrl Pts',(132.413854462064,-3.26604542409023,
135.738008137432));
#144155=CARTESIAN_POINT('Ctrl Pts',(132.406454379549,-3.13464674480017,
135.824993284526));
#144156=CARTESIAN_POINT('Ctrl Pts',(132.399054297034,-2.99982511447287,
135.906689415786));
#144157=CARTESIAN_POINT('Ctrl Pts',(132.391654214519,-2.86205239782559,
135.982834005989));
#144158=CARTESIAN_POINT('Ctrl Pts',(132.384245994852,-2.72412818591259,
136.059062324996));
#144159=CARTESIAN_POINT('Ctrl Pts',(132.376837775186,-2.58324673407528,
136.129726731196));
#144160=CARTESIAN_POINT('Ctrl Pts',(132.36942955552,-2.43990323316877,136.194611333003));
#144161=CARTESIAN_POINT('Ctrl Pts',(132.362016776217,-2.29647150672927,
136.259535870201));
#144162=CARTESIAN_POINT('Ctrl Pts',(132.354603996915,-2.15057505685119,
136.31867337459));
#144163=CARTESIAN_POINT('Ctrl Pts',(132.347191217613,-2.00272652974338,
136.371857093502));
#144164=CARTESIAN_POINT('Ctrl Pts',(132.339767846585,-1.85466674972663,
136.425116803806));
#144165=CARTESIAN_POINT('Ctrl Pts',(132.332344475556,-1.7046496768683,136.47240562622));
#144166=CARTESIAN_POINT('Ctrl Pts',(132.324921104527,-1.55320130067954,
136.513607177496));
#144167=CARTESIAN_POINT('Ctrl Pts',(132.320985055086,-1.47289973766145,
136.535453228602));
#144168=CARTESIAN_POINT('Ctrl Pts',(132.317049005645,-1.39219593574406,
136.555588787283));
#144169=CARTESIAN_POINT('Ctrl Pts',(132.313112956203,-1.31116902747609,
136.574002404011));
#144170=CARTESIAN_POINT('Ctrl Pts',(132.305689689798,-1.15835480726222,
136.608729910486));
#144171=CARTESIAN_POINT('Ctrl Pts',(132.298266423393,-1.00392887687804,
136.637434599771));
#144172=CARTESIAN_POINT('Ctrl Pts',(132.290843156987,-0.848407291581399,
136.659967813245));
#144173=CARTESIAN_POINT('Ctrl Pts',(132.283428664266,-0.693069519883096,
136.682474394333));
#144174=CARTESIAN_POINT('Ctrl Pts',(132.276014171545,-0.536639036756118,
136.698823965696));
#144175=CARTESIAN_POINT('Ctrl Pts',(132.268599678824,-0.37964489030772,
136.708918206392));
#144176=CARTESIAN_POINT('Ctrl Pts',(132.26119233247,-0.222802060728393,
136.719002717879));
#144177=CARTESIAN_POINT('Ctrl Pts',(132.253784986117,-0.0653970194188368,
136.722843877706));
#144178=CARTESIAN_POINT('Ctrl Pts',(132.246377639763,0.0920333150634869,
136.720394798622));
#144179=CARTESIAN_POINT('Ctrl Pts',(132.238975818087,0.249346232062847,
136.717947546153));
#144180=CARTESIAN_POINT('Ctrl Pts',(132.231573996412,0.40668403302671,136.70921940196));
#144181=CARTESIAN_POINT('Ctrl Pts',(132.224172174737,0.563507137501594,
136.694215477279));
#144182=CARTESIAN_POINT('Ctrl Pts',(132.216774260425,0.720247456280445,
136.679219473053));
#144183=CARTESIAN_POINT('Ctrl Pts',(132.209376346114,0.876473249021992,
136.657954321672));
#144184=CARTESIAN_POINT('Ctrl Pts',(132.201978431803,1.03164751272782,136.630477160511));
#144185=CARTESIAN_POINT('Ctrl Pts',(132.19458174689,1.18679598928595,136.603004565556));
#144186=CARTESIAN_POINT('Ctrl Pts',(132.187185061978,1.3408929164058,136.569322074703));
#144187=CARTESIAN_POINT('Ctrl Pts',(132.179788377066,1.49340885543957,136.52953839236));
#144188=CARTESIAN_POINT('Ctrl Pts',(132.17239202013,1.64591803175678,136.489756474067));
#144189=CARTESIAN_POINT('Ctrl Pts',(132.164995663195,1.79684599816473,136.443873996419));
#144190=CARTESIAN_POINT('Ctrl Pts',(132.15759930626,1.94567617702488,136.39205019168));
#144191=CARTESIAN_POINT('Ctrl Pts',(132.150201816923,2.09452914216546,136.340218452584));
#144192=CARTESIAN_POINT('Ctrl Pts',(132.142804327586,2.24128332769327,136.282443697963));
#144193=CARTESIAN_POINT('Ctrl Pts',(132.13540683825,2.38544005732124,136.218934127588));
#144194=CARTESIAN_POINT('Ctrl Pts',(132.128006755735,2.52964732086721,136.155402294031));
#144195=CARTESIAN_POINT('Ctrl Pts',(132.12060667322,2.67125497424492,136.086131792574));
#144196=CARTESIAN_POINT('Ctrl Pts',(132.113206590705,2.8097870931432,136.011377715071));
#144197=CARTESIAN_POINT('Ctrl Pts',(132.105798371039,2.94847154234775,135.936541437775));
#144198=CARTESIAN_POINT('Ctrl Pts',(132.098390151372,3.08407337454253,135.856209719998));
#144199=CARTESIAN_POINT('Ctrl Pts',(132.090981931706,3.21614329127075,135.770682485157));
#144200=CARTESIAN_POINT('Ctrl Pts',(132.083569152404,3.3482944948291,135.68510260973));
#144201=CARTESIAN_POINT('Ctrl Pts',(132.076156373101,3.47690914701088,135.594321060081));
#144202=CARTESIAN_POINT('Ctrl Pts',(132.068743593799,3.60156985627617,135.498679006093));
#144203=CARTESIAN_POINT('Ctrl Pts',(132.061320222771,3.72640868660878,135.402900294253));
#144204=CARTESIAN_POINT('Ctrl Pts',(132.053896851742,3.84728200444542,135.302247445761));
#144205=CARTESIAN_POINT('Ctrl Pts',(132.046473480713,3.96380758308421,135.1971000825));
#144206=CARTESIAN_POINT('Ctrl Pts',(132.042537431272,4.02559224087191,135.141348427522));
#144207=CARTESIAN_POINT('Ctrl Pts',(132.038601381832,4.08615523288903,135.084333794629));
#144208=CARTESIAN_POINT('Ctrl Pts',(132.034665332391,4.14544415324828,135.026116571526));
#144209=CARTESIAN_POINT('Ctrl Pts',(132.027242065985,4.25726120670123,134.916320705653));
#144210=CARTESIAN_POINT('Ctrl Pts',(132.01981879958,4.36488226219099,134.80191338256));
#144211=CARTESIAN_POINT('Ctrl Pts',(132.012395533174,4.46790330853993,134.683248420537));
#144212=CARTESIAN_POINT('Ctrl Pts',(132.004981040453,4.57080259256751,134.564723710644));
#144213=CARTESIAN_POINT('Ctrl Pts',(131.997566547732,4.66911244715607,134.44195165753));
#144214=CARTESIAN_POINT('Ctrl Pts',(131.990152055011,4.76246418868836,134.315324219479));
#144215=CARTESIAN_POINT('Ctrl Pts',(131.982744708658,4.85572595429752,134.188818829721));
#144216=CARTESIAN_POINT('Ctrl Pts',(131.975337362304,4.94403890050665,134.058465751236));
#144217=CARTESIAN_POINT('Ctrl Pts',(131.96793001595,5.02707336214907,133.92469136511));
#144218=CARTESIAN_POINT('Ctrl Pts',(131.960528194275,5.11004589355733,133.791016752969));
#144219=CARTESIAN_POINT('Ctrl Pts',(131.953126372599,5.18774758326425,133.653926229846));
#144220=CARTESIAN_POINT('Ctrl Pts',(131.945724550924,5.25989107508295,133.513876522809));
#144221=CARTESIAN_POINT('Ctrl Pts',(131.938326636612,5.33199648291384,133.373900746921));
#144222=CARTESIAN_POINT('Ctrl Pts',(131.930928722301,5.39854936580052,133.230969229192));
#144223=CARTESIAN_POINT('Ctrl Pts',(131.92353080799,5.45930753179741,133.085564649598));
#144224=CARTESIAN_POINT('Ctrl Pts',(131.916134123077,5.52005560088938,132.940184233608));
#144225=CARTESIAN_POINT('Ctrl Pts',(131.908737438165,5.57501072053143,132.792331915523));
#144226=CARTESIAN_POINT('Ctrl Pts',(131.901340753253,5.62397817230058,132.642511884461));
#144227=CARTESIAN_POINT('Ctrl Pts',(131.893944396317,5.67294345280161,132.492698496576));
#144228=CARTESIAN_POINT('Ctrl Pts',(131.886548039382,5.71592147736038,132.340917924023));
#144229=CARTESIAN_POINT('Ctrl Pts',(131.879151682447,5.75276698976015,132.18769084713));
#144230=CARTESIAN_POINT('Ctrl Pts',(131.87175419311,5.78961814330195,132.03444031078));
#144231=CARTESIAN_POINT('Ctrl Pts',(131.864356703773,5.82033482792118,131.879743192101));
#144232=CARTESIAN_POINT('Ctrl Pts',(131.856959214437,5.84482266126758,131.724131578639));
#144233=CARTESIAN_POINT('Ctrl Pts',(131.849559131922,5.86931907878599,131.568465415767));
#144234=CARTESIAN_POINT('Ctrl Pts',(131.842159049407,5.8875822396772,131.411884488379));
#144235=CARTESIAN_POINT('Ctrl Pts',(131.834758966892,5.89956951122791,131.254927088456));
#144236=CARTESIAN_POINT('Ctrl Pts',(131.827350747225,5.91156996401602,131.097797097736));
#144237=CARTESIAN_POINT('Ctrl Pts',(131.819942527559,5.91728071729803,130.940290180197));
#144238=CARTESIAN_POINT('Ctrl Pts',(131.812534307892,5.91671124834779,130.782946459289));
#144239=CARTESIAN_POINT('Ctrl Pts',(131.80512152859,5.91614142889891,130.625505895945));
#144240=CARTESIAN_POINT('Ctrl Pts',(131.797708749288,5.90928370120321,130.46822910146));
#144241=CARTESIAN_POINT('Ctrl Pts',(131.790295969986,5.89619949082419,130.311651649813));
#144242=CARTESIAN_POINT('Ctrl Pts',(131.782872598957,5.8830965851118,130.15485047296));
#144243=CARTESIAN_POINT('Ctrl Pts',(131.775449227928,5.86374947382362,129.998751004161));
#144244=CARTESIAN_POINT('Ctrl Pts',(131.7680258569,5.83827094073324,129.843880016466));
#144245=CARTESIAN_POINT('Ctrl Pts',(131.764089807459,5.82476161114022,129.761763702715));
#144246=CARTESIAN_POINT('Ctrl Pts',(131.760153758018,5.80952936226843,129.679992540563));
#144247=CARTESIAN_POINT('Ctrl Pts',(131.756217708578,5.79259667334227,129.598643261597));
#144248=CARTESIAN_POINT('Ctrl Pts',(131.748794442172,5.76066215047756,129.445221060287));
#144249=CARTESIAN_POINT('Ctrl Pts',(131.741371175767,5.72257983865848,129.292836465631));
#144250=CARTESIAN_POINT('Ctrl Pts',(131.733947909361,5.67842903732282,129.142020631104));
#144251=CARTESIAN_POINT('Ctrl Pts',(131.72653341664,5.63433041856781,128.991383048369));
#144252=CARTESIAN_POINT('Ctrl Pts',(131.719118923919,5.58417769095449,128.842310889842));
#144253=CARTESIAN_POINT('Ctrl Pts',(131.711704431198,5.52810133758869,128.69532620252));
#144254=CARTESIAN_POINT('Ctrl Pts',(131.704297084845,5.47207903272345,128.548483184572));
#144255=CARTESIAN_POINT('Ctrl Pts',(131.696889738491,5.41014460059332,128.403723978802));
#144256=CARTESIAN_POINT('Ctrl Pts',(131.689482392137,5.34247857560552,128.261556411243));
#144257=CARTESIAN_POINT('Ctrl Pts',(131.682080570462,5.2748630184921,128.119494877619));
#144258=CARTESIAN_POINT('Ctrl Pts',(131.674678748786,5.20152454004015,127.980021469073));
#144259=CARTESIAN_POINT('Ctrl Pts',(131.667276927111,5.12269207462701,127.843624818638));
#144260=CARTESIAN_POINT('Ctrl Pts',(131.6598790128,5.04390122425867,127.707300170934));
#144261=CARTESIAN_POINT('Ctrl Pts',(131.652481098488,4.95962234920705,127.574049369056));
#144262=CARTESIAN_POINT('Ctrl Pts',(131.645083184177,4.87013063114568,127.444337076268));
#144263=CARTESIAN_POINT('Ctrl Pts',(131.637686499265,4.78065378498436,127.31464633931));
#144264=CARTESIAN_POINT('Ctrl Pts',(131.630289814352,4.68596602690469,127.188493251327));
#144265=CARTESIAN_POINT('Ctrl Pts',(131.62289312944,4.5863862954267,127.066314160976));
#144266=CARTESIAN_POINT('Ctrl Pts',(131.615496772505,4.48681097941837,126.944140488175));
#144267=CARTESIAN_POINT('Ctrl Pts',(131.608100415569,4.38234435715202,126.825940752002));
#144268=CARTESIAN_POINT('Ctrl Pts',(131.600704058634,4.27334597719978,126.712118601061));
#144269=CARTESIAN_POINT('Ctrl Pts',(131.593306569297,4.16433090931738,126.598279023658));
#144270=CARTESIAN_POINT('Ctrl Pts',(131.585909079961,4.05078296045702,126.488818635613));
#144271=CARTESIAN_POINT('Ctrl Pts',(131.578511590624,3.93309877497434,126.384104449786));
#144272=CARTESIAN_POINT('Ctrl Pts',(131.571111508109,3.8153733354828,126.279353556564));
#144273=CARTESIAN_POINT('Ctrl Pts',(131.563711425594,3.69350905123402,126.179352426111));
#144274=CARTESIAN_POINT('Ctrl Pts',(131.556311343079,3.56793575849341,126.084427886503));
#144275=CARTESIAN_POINT('Ctrl Pts',(131.548903123413,3.44222438500809,125.989398967604));
#144276=CARTESIAN_POINT('Ctrl Pts',(131.541494903746,3.31279615609758,125.899458012881));
#144277=CARTESIAN_POINT('Ctrl Pts',(131.53408668408,3.18011061561469,125.814888998752));
#144278=CARTESIAN_POINT('Ctrl Pts',(131.526673904778,3.04734340939542,125.730267933805));
#144279=CARTESIAN_POINT('Ctrl Pts',(131.519261125476,2.91131521855655,125.651025585218));
#144280=CARTESIAN_POINT('Ctrl Pts',(131.511848346174,2.77250983867293,125.577399764741));
#144281=CARTESIAN_POINT('Ctrl Pts',(131.504424975145,2.6335061271533,125.50366874424));
#144282=CARTESIAN_POINT('Ctrl Pts',(131.497001604116,2.49171763685584,125.435570441078));
#144283=CARTESIAN_POINT('Ctrl Pts',(131.489578233088,2.34764851925148,125.373294700772));
#144284=CARTESIAN_POINT('Ctrl Pts',(131.485642183647,2.27125961620314,125.340274608975));
#144285=CARTESIAN_POINT('Ctrl Pts',(131.481706134206,2.19422981901554,125.308890620834));
#144286=CARTESIAN_POINT('Ctrl Pts',(131.477770084765,2.11663583471571,125.279165299236));
#144287=CARTESIAN_POINT('Ctrl Pts',(131.470346818359,1.97029600195762,125.2231042704));
#144288=CARTESIAN_POINT('Ctrl Pts',(131.462923551954,1.82150610696681,125.172776402269));
#144289=CARTESIAN_POINT('Ctrl Pts',(131.455500285548,1.67075588748716,125.128402079405));
#144290=CARTESIAN_POINT('Ctrl Pts',(131.448085792827,1.52018384224779,125.084080203305));
#144291=CARTESIAN_POINT('Ctrl Pts',(131.440671300106,1.36765643901191,125.045697970471));
#144292=CARTESIAN_POINT('Ctrl Pts',(131.433256807385,1.21368342000861,125.013427780924));
#144293=CARTESIAN_POINT('Ctrl Pts',(131.425849461032,1.059858805998,124.981188694601));
#144294=CARTESIAN_POINT('Ctrl Pts',(131.418442114678,0.90459171299056,124.955049999767));
#144295=CARTESIAN_POINT('Ctrl Pts',(131.411034768324,0.748406972666796,
124.935134300089));
#144296=CARTESIAN_POINT('Ctrl Pts',(131.403632946648,0.592338720814656,
124.915233454291));
#144297=CARTESIAN_POINT('Ctrl Pts',(131.396231124973,0.435354553116601,
124.90154640912));
#144298=CARTESIAN_POINT('Ctrl Pts',(131.388829303298,0.277989315005478,
124.89414467369));
#144299=CARTESIAN_POINT('Ctrl Pts',(131.381431388986,0.120707148778738,
124.886746845579));
#144300=CARTESIAN_POINT('Ctrl Pts',(131.374033474675,-0.036955315291354,
124.885627736816));
#144301=CARTESIAN_POINT('Ctrl Pts',(131.366635560363,-0.194458400426787,
124.890806991107));
#144302=CARTESIAN_POINT('Ctrl Pts',(131.359238875451,-0.351935311406643,
124.895985384701));
#144303=CARTESIAN_POINT('Ctrl Pts',(131.351842190539,-0.509252523287558,
124.907460051755));
#144304=CARTESIAN_POINT('Ctrl Pts',(131.344445505627,-0.665870529525372,
124.925198517368));
#144305=CARTESIAN_POINT('Ctrl Pts',(131.337049148691,-0.822481591156665,
124.942936196438));
#144306=CARTESIAN_POINT('Ctrl Pts',(131.329652791756,-0.978393137864227,
124.966937079809));
#144307=CARTESIAN_POINT('Ctrl Pts',(131.32225643482,-1.13307122385995,124.997116851014));
#144308=CARTESIAN_POINT('Ctrl Pts',(131.314858945484,-1.28777299146552,
125.027301242818));
#144309=CARTESIAN_POINT('Ctrl Pts',(131.307461456147,-1.44124055592927,
125.063666334583));
#144310=CARTESIAN_POINT('Ctrl Pts',(131.300063966811,-1.59295074297537,
125.106076797594));
#144311=CARTESIAN_POINT('Ctrl Pts',(131.292663884296,-1.74471411179257,
125.148502127527));
#144312=CARTESIAN_POINT('Ctrl Pts',(131.285263801781,-1.89471851735897,
125.196976947569));
#144313=CARTESIAN_POINT('Ctrl Pts',(131.277863719266,-2.0424566529597,125.251316282854));
#144314=CARTESIAN_POINT('Ctrl Pts',(131.270455499599,-2.19035724182826,
125.305715369823));
#144315=CARTESIAN_POINT('Ctrl Pts',(131.263047279933,-2.33598623348387,
125.365991721447));
#144316=CARTESIAN_POINT('Ctrl Pts',(131.255639060266,-2.4788563158455,125.431912206656));
#144317=CARTESIAN_POINT('Ctrl Pts',(131.248226280964,-2.62181433235911,
125.497873264823));
#144318=CARTESIAN_POINT('Ctrl Pts',(131.240813501662,-2.76200972430766,
125.569485209282));
#144319=CARTESIAN_POINT('Ctrl Pts',(131.23340072236,-2.89898091060348,125.646469552173));
#144320=CARTESIAN_POINT('Ctrl Pts',(131.225977351331,-3.0361478077535,125.723563893904));
#144321=CARTESIAN_POINT('Ctrl Pts',(131.218553980302,-3.17008098123058,
125.806045770198));
#144322=CARTESIAN_POINT('Ctrl Pts',(131.211130609274,-3.30034820243907,
125.893593640285));
#144323=CARTESIAN_POINT('Ctrl Pts',(131.207194559833,-3.3694190088398,125.940013621685));
#144324=CARTESIAN_POINT('Ctrl Pts',(131.203258510392,-3.43745973383563,
125.987857159465));
#144325=CARTESIAN_POINT('Ctrl Pts',(131.199322460952,-3.50440993260739,
126.037071913623));
#144326=CARTESIAN_POINT('Ctrl Pts',(131.191967172959,-3.62951963982809,
126.129039429726));
#144327=CARTESIAN_POINT('Ctrl Pts',(131.184611884967,-3.7512127270936,126.226086955291));
#144328=CARTESIAN_POINT('Ctrl Pts',(131.177256596974,-3.86904358294745,
126.327929861288));
#144329=CARTESIAN_POINT('Ctrl Pts',(131.169910034406,-3.98673465851265,
126.429651953168));
#144330=CARTESIAN_POINT('Ctrl Pts',(131.162563471839,-4.10057233439905,
126.536157859477));
#144331=CARTESIAN_POINT('Ctrl Pts',(131.155216909271,-4.21014017975913,
126.647119918583));
#144332=CARTESIAN_POINT('Ctrl Pts',(131.147877385571,-4.319603046289,126.757975663039));
#144333=CARTESIAN_POINT('Ctrl Pts',(131.140537861871,-4.42480395838242,
126.87327879409));
#144334=CARTESIAN_POINT('Ctrl Pts',(131.133198338171,-4.52535995253196,
126.992661801746));
#144335=CARTESIAN_POINT('Ctrl Pts',(131.125864173213,-4.62584252861205,
127.11195764533));
#144336=CARTESIAN_POINT('Ctrl Pts',(131.118530008255,-4.72168669313732,
127.23532714599));
#144337=CARTESIAN_POINT('Ctrl Pts',(131.111195843297,-4.81254688099806,
127.362366561689));
#144338=CARTESIAN_POINT('Ctrl Pts',(131.10386482153,-4.90336812906279,127.489351532321));
#144339=CARTESIAN_POINT('Ctrl Pts',(131.096533799763,-4.98920942880024,
127.620002979867));
#144340=CARTESIAN_POINT('Ctrl Pts',(131.089202777995,-5.06976607935129,
127.753884841042));
#144341=CARTESIAN_POINT('Ctrl Pts',(131.081873298667,-5.15030578086776,
127.887738533614));
#144342=CARTESIAN_POINT('Ctrl Pts',(131.074543819339,-5.22556284885647,
128.024820961599));
#144343=CARTESIAN_POINT('Ctrl Pts',(131.067214340011,-5.29527657013599,
128.164668096027));
#144344=CARTESIAN_POINT('Ctrl Pts',(131.059884890251,-5.36499001018411,
128.304514666299));
#144345=CARTESIAN_POINT('Ctrl Pts',(131.052555440491,-5.42915997803113,
128.447125579991));
#144346=CARTESIAN_POINT('Ctrl Pts',(131.045225990731,-5.48757240378098,
128.592013520983));
#144347=CARTESIAN_POINT('Ctrl Pts',(131.037895057908,-5.5459966488725,128.736930779025));
#144348=CARTESIAN_POINT('Ctrl Pts',(131.030564125085,-5.59866089133872,
128.884125627996));
#144349=CARTESIAN_POINT('Ctrl Pts',(131.023233192263,-5.64539984928383,
129.033092398406));
#144350=CARTESIAN_POINT('Ctrl Pts',(131.015895152461,-5.69218411835187,
129.18220358478));
#144351=CARTESIAN_POINT('Ctrl Pts',(131.008557112659,-5.73303151523554,
129.33308975983));
#144352=CARTESIAN_POINT('Ctrl Pts',(131.001219072857,-5.76782697643615,
129.485231157507));
#144353=CARTESIAN_POINT('Ctrl Pts',(130.993877359742,-5.80263985572723,
129.637448714906));
#144354=CARTESIAN_POINT('Ctrl Pts',(130.986535646627,-5.83139469385814,
129.790922372803));
#144355=CARTESIAN_POINT('Ctrl Pts',(130.979193933511,-5.85402801498565,
129.945124583485));
#144356=CARTESIAN_POINT('Ctrl Pts',(130.971841575104,-5.87669415383726,
130.099550383342));
#144357=CARTESIAN_POINT('Ctrl Pts',(130.964489216696,-5.89322100286484,
130.254706467999));
#144358=CARTESIAN_POINT('Ctrl Pts',(130.957136858289,-5.90359711718267,
130.410061694802));
#144359=CARTESIAN_POINT('Ctrl Pts',(130.950882969596,-5.91242300139681,
130.542206272419));
#144360=CARTESIAN_POINT('Ctrl Pts',(130.944629080904,-5.91679963655113,
130.674494784546));
#144361=CARTESIAN_POINT('Ctrl Pts',(130.938375192211,-5.91674957518414,
130.806602727802));
#144362=CARTESIAN_POINT('',(129.188375192211,-5.91739037745531,130.798927194587));
#144363=CARTESIAN_POINT('Ctrl Pts',(130.938375192211,-5.92550534701643,
130.80660604574));
#144364=CARTESIAN_POINT('Ctrl Pts',(130.932541740521,-5.9261030892962,130.930015222463));
#144365=CARTESIAN_POINT('Ctrl Pts',(130.92670828883,-5.92258319844409,131.053389657062));
#144366=CARTESIAN_POINT('Ctrl Pts',(130.828058962535,-5.79159940387876,
133.135275101838));
#144367=CARTESIAN_POINT('Ctrl Pts',(130.642427213325,-3.40562481334391,
136.918220295468));
#144368=CARTESIAN_POINT('Ctrl Pts',(130.363979589513,3.30293990190001,136.97429972057));
#144369=CARTESIAN_POINT('Ctrl Pts',(130.085531965701,6.97626420488279,131.360506528292));
#144370=CARTESIAN_POINT('Ctrl Pts',(129.807084341888,4.23874251303069,125.235642413295));
#144371=CARTESIAN_POINT('Ctrl Pts',(129.528636718075,-2.39397647421211,
124.228158281014));
#144372=CARTESIAN_POINT('Ctrl Pts',(129.322400334849,-5.67717480651475,
127.95794273319));
#144373=CARTESIAN_POINT('Ctrl Pts',(129.208979826228,-5.92145620834998,
130.361470692854));
#144374=CARTESIAN_POINT('Ctrl Pts',(129.188375192211,-5.91739037745531,
130.798927194587));
#144375=CARTESIAN_POINT('',(127.438375192169,-5.91674999573792,130.804585195673));
#144376=CARTESIAN_POINT('Ctrl Pts',(129.188375192211,-5.91674750575255,
130.79892778488));
#144377=CARTESIAN_POINT('Ctrl Pts',(129.181067794371,-5.91688994338944,
130.954052667514));
#144378=CARTESIAN_POINT('Ctrl Pts',(129.173760396532,-5.91092763526548,
131.109359430848));
#144379=CARTESIAN_POINT('Ctrl Pts',(129.166452998692,-5.89884451512316,
131.26432142992));
#144380=CARTESIAN_POINT('Ctrl Pts',(129.159150918755,-5.88677018837911,
131.419170656582));
#144381=CARTESIAN_POINT('Ctrl Pts',(129.151848838819,-5.86858394450736,
131.573675236878));
#144382=CARTESIAN_POINT('Ctrl Pts',(129.144546758882,-5.84432178705686,
131.727308834874));
#144383=CARTESIAN_POINT('Ctrl Pts',(129.137247681465,-5.8200696058889,131.88087926074));
#144384=CARTESIAN_POINT('Ctrl Pts',(129.129948604049,-5.7897465394639,132.033579037759));
#144385=CARTESIAN_POINT('Ctrl Pts',(129.122649526632,-5.75344039640455,
132.184887389317));
#144386=CARTESIAN_POINT('Ctrl Pts',(129.115351907255,-5.71714150574178,
132.336165516012));
#144387=CARTESIAN_POINT('Ctrl Pts',(129.108054287878,-5.67486200501293,
132.486052396529));
#144388=CARTESIAN_POINT('Ctrl Pts',(129.100756668501,-5.62674067312069,
132.634038173845));
#144389=CARTESIAN_POINT('Ctrl Pts',(129.09345897469,-5.57861885040187,132.782025460581));
#144390=CARTESIAN_POINT('Ctrl Pts',(129.086161280879,-5.52465519666547,
132.928111239962));
#144391=CARTESIAN_POINT('Ctrl Pts',(129.078863587068,-5.46503805690862,
133.071801818356));
#144392=CARTESIAN_POINT('Ctrl Pts',(129.071564286455,-5.40540779068163,
133.215524034465));
#144393=CARTESIAN_POINT('Ctrl Pts',(129.064264985841,-5.34012170915914,
133.356849645448));
#144394=CARTESIAN_POINT('Ctrl Pts',(129.056965685228,-5.26941576627111,
133.495306184588));
#144395=CARTESIAN_POINT('Ctrl Pts',(129.049658966624,-5.19863796772325,
133.633903431645));
#144396=CARTESIAN_POINT('Ctrl Pts',(129.042352248019,-5.1224294819203,133.769625440692));
#144397=CARTESIAN_POINT('Ctrl Pts',(129.035045529415,-5.04107189146871,
133.902025019586));
#144398=CARTESIAN_POINT('Ctrl Pts',(129.027735001506,-4.95967188583252,
134.034493624032));
#144399=CARTESIAN_POINT('Ctrl Pts',(129.020424473597,-4.87311764274452,
134.163636029777));
#144400=CARTESIAN_POINT('Ctrl Pts',(129.013113945688,-4.78173285762243,
134.28903584502));
#144401=CARTESIAN_POINT('Ctrl Pts',(129.005792346453,-4.69020967609837,
134.414625570249));
#144402=CARTESIAN_POINT('Ctrl Pts',(128.998470747218,-4.59384157672553,
134.536461081353));
#144403=CARTESIAN_POINT('Ctrl Pts',(128.991149147983,-4.49299173791707,
134.654160067603));
#144404=CARTESIAN_POINT('Ctrl Pts',(128.984679922138,-4.40388273826438,
134.758156653506));
#144405=CARTESIAN_POINT('Ctrl Pts',(128.978210696293,-4.31127545703475,
134.858924203103));
#144406=CARTESIAN_POINT('Ctrl Pts',(128.971741470448,-4.21544240491636,
134.956224764348));
#144407=CARTESIAN_POINT('Ctrl Pts',(128.964318204043,-4.10547649966461,
135.067874597701));
#144408=CARTESIAN_POINT('Ctrl Pts',(128.956894937638,-3.99090552812758,
135.175321420097));
#144409=CARTESIAN_POINT('Ctrl Pts',(128.949471671232,-3.87208392302154,
135.278161759277));
#144410=CARTESIAN_POINT('Ctrl Pts',(128.942057178511,-3.7534027551848,135.380880549717));
#144411=CARTESIAN_POINT('Ctrl Pts',(128.93464268579,-3.63048123337495,135.4790034523));
#144412=CARTESIAN_POINT('Ctrl Pts',(128.927228193069,-3.50371187649744,
135.572162380327));
#144413=CARTESIAN_POINT('Ctrl Pts',(128.919820846715,-3.37706470469924,
135.665231518273));
#144414=CARTESIAN_POINT('Ctrl Pts',(128.912413500361,-3.24657737989109,
135.753345987021));
#144415=CARTESIAN_POINT('Ctrl Pts',(128.905006154008,-3.11267678435826,
135.836176770668));
#144416=CARTESIAN_POINT('Ctrl Pts',(128.897604332332,-2.97887605694135,
135.918945775991));
#144417=CARTESIAN_POINT('Ctrl Pts',(128.890202510657,-2.84166744382333,
135.996438747281));
#144418=CARTESIAN_POINT('Ctrl Pts',(128.882800688982,-2.70150810884803,
136.068369023746));
#144419=CARTESIAN_POINT('Ctrl Pts',(128.87540277467,-2.56142276289497,136.140261328777));
#144420=CARTESIAN_POINT('Ctrl Pts',(128.868004860359,-2.41839012851996,
136.206596617157));
#144421=CARTESIAN_POINT('Ctrl Pts',(128.860606946048,-2.27289325371729,
136.267133431779));
#144422=CARTESIAN_POINT('Ctrl Pts',(128.853210261135,-2.12742055785532,
136.327660186281));
#144423=CARTESIAN_POINT('Ctrl Pts',(128.845813576223,-1.97948477864414,
136.382390236227));
#144424=CARTESIAN_POINT('Ctrl Pts',(128.838416891311,-1.82959040094573,
136.431129630709));
#144425=CARTESIAN_POINT('Ctrl Pts',(128.831020534376,-1.67970266972099,
136.479866864036));
#144426=CARTESIAN_POINT('Ctrl Pts',(128.82362417744,-1.52785686769099,136.522613854633));
#144427=CARTESIAN_POINT('Ctrl Pts',(128.816227820505,-1.37457389563478,
136.559226138839));
#144428=CARTESIAN_POINT('Ctrl Pts',(128.808830331168,-1.22126745556424,
136.59584402848));
#144429=CARTESIAN_POINT('Ctrl Pts',(128.801432841832,-1.06652377045739,
136.626325254849));
#144430=CARTESIAN_POINT('Ctrl Pts',(128.794035352495,-0.910875070877245,
136.650576245453));
#144431=CARTESIAN_POINT('Ctrl Pts',(128.78663526998,-0.75517180888686,136.674835737205));
#144432=CARTESIAN_POINT('Ctrl Pts',(128.779235187465,-0.598563269395612,
136.692860587431));
#144433=CARTESIAN_POINT('Ctrl Pts',(128.77183510495,-0.441587808640241,
136.704608982657));
#144434=CARTESIAN_POINT('Ctrl Pts',(128.764426885284,-0.284439737228188,
136.716370296452));
#144435=CARTESIAN_POINT('Ctrl Pts',(128.757018665617,-0.126924311285822,
136.721841344405));
#144436=CARTESIAN_POINT('Ctrl Pts',(128.749610445951,0.0304183607859964,
136.721032425756));
#144437=CARTESIAN_POINT('Ctrl Pts',(128.742197666649,0.187857874647408,
136.720223009231));
#144438=CARTESIAN_POINT('Ctrl Pts',(128.734784887347,0.345124050714408,
136.713125940969));
#144439=CARTESIAN_POINT('Ctrl Pts',(128.727372108045,0.501681409106723,
136.699803461514));
#144440=CARTESIAN_POINT('Ctrl Pts',(128.719948737016,0.658462463994298,
136.686461946276));
#144441=CARTESIAN_POINT('Ctrl Pts',(128.712525365987,0.814532309022712,
136.666877300573));
#144442=CARTESIAN_POINT('Ctrl Pts',(128.705101994958,0.969364343389114,
136.641163109707));
#144443=CARTESIAN_POINT('Ctrl Pts',(128.701165945517,1.0514600031544,136.627528828707));
#144444=CARTESIAN_POINT('Ctrl Pts',(128.697229896077,1.13320788973021,136.612172155684));
#144445=CARTESIAN_POINT('Ctrl Pts',(128.693293846636,1.21453130582814,136.59511568661));
#144446=CARTESIAN_POINT('Ctrl Pts',(128.68587058023,1.36790473057144,136.562947718252));
#144447=CARTESIAN_POINT('Ctrl Pts',(128.678447313825,1.52023119397322,136.524633547119));
#144448=CARTESIAN_POINT('Ctrl Pts',(128.671024047419,1.67097966385473,136.480253280882));
#144449=CARTESIAN_POINT('Ctrl Pts',(128.663609554698,1.82154996156415,136.435925468434));
#144450=CARTESIAN_POINT('Ctrl Pts',(128.656195061977,1.97054562355525,136.385545936448));
#144451=CARTESIAN_POINT('Ctrl Pts',(128.648780569256,2.11744480200929,136.329245962344));
#144452=CARTESIAN_POINT('Ctrl Pts',(128.641373222902,2.26420239350458,136.273000252275));
#144453=CARTESIAN_POINT('Ctrl Pts',(128.633965876549,2.40886717798405,136.210845592995));
#144454=CARTESIAN_POINT('Ctrl Pts',(128.626558530195,2.55093160474578,136.142963291526));
#144455=CARTESIAN_POINT('Ctrl Pts',(128.619156708519,2.69289007449794,136.075131619238));
#144456=CARTESIAN_POINT('Ctrl Pts',(128.611754886844,2.83225171285692,136.001580970925));
#144457=CARTESIAN_POINT('Ctrl Pts',(128.604353065169,2.96852823575426,135.922541024315));
#144458=CARTESIAN_POINT('Ctrl Pts',(128.596955150857,3.10473281933593,135.843542802277));
#144459=CARTESIAN_POINT('Ctrl Pts',(128.589557236546,3.23785520881031,135.759061239781));
#144460=CARTESIAN_POINT('Ctrl Pts',(128.582159322234,3.36743116023369,135.669372225321));
#144461=CARTESIAN_POINT('Ctrl Pts',(128.574762637322,3.49698557848459,135.579698115547));
#144462=CARTESIAN_POINT('Ctrl Pts',(128.56736595241,3.62299442173573,135.484818483589));
#144463=CARTESIAN_POINT('Ctrl Pts',(128.559969267498,3.74502182720505,135.385052931644));
#144464=CARTESIAN_POINT('Ctrl Pts',(128.552572910562,3.86704382185134,135.28529180341));
#144465=CARTESIAN_POINT('Ctrl Pts',(128.545176553627,3.98508444073574,135.180645422236));
#144466=CARTESIAN_POINT('Ctrl Pts',(128.537780196691,4.09874058289344,135.071473950563));
#144467=CARTESIAN_POINT('Ctrl Pts',(128.530382707355,4.21241412609649,134.96228576446));
#144468=CARTESIAN_POINT('Ctrl Pts',(128.522985218018,4.3217015867391,134.848571367008));
#144469=CARTESIAN_POINT('Ctrl Pts',(128.515587728681,4.42623655601193,134.730727960636));
#144470=CARTESIAN_POINT('Ctrl Pts',(128.508187646166,4.53080816985605,134.61284324444));
#144471=CARTESIAN_POINT('Ctrl Pts',(128.500787563651,4.63062372781277,134.49082691661));
#144472=CARTESIAN_POINT('Ctrl Pts',(128.493387481136,4.72535705632517,134.36510931029));
#144473=CARTESIAN_POINT('Ctrl Pts',(128.48597926147,4.82019455387149,134.239253464538));
#144474=CARTESIAN_POINT('Ctrl Pts',(128.478571041803,4.90993843671278,134.10968851068));
#144475=CARTESIAN_POINT('Ctrl Pts',(128.471162822137,4.99430542810679,133.9768744242));
#144476=CARTESIAN_POINT('Ctrl Pts',(128.463750042835,5.07872434597632,133.843978592866));
#144477=CARTESIAN_POINT('Ctrl Pts',(128.456337263533,5.15775959105189,133.707829966179));
#144478=CARTESIAN_POINT('Ctrl Pts',(128.448924484231,5.23117408811143,133.568912701064));
#144479=CARTESIAN_POINT('Ctrl Pts',(128.441501113202,5.30469348324712,133.429796944445));
#144480=CARTESIAN_POINT('Ctrl Pts',(128.434077742173,5.37257592960687,133.28790498431));
#144481=CARTESIAN_POINT('Ctrl Pts',(128.426654371144,5.4346323491252,133.143741260459));
#144482=CARTESIAN_POINT('Ctrl Pts',(128.422718321704,5.4675361517749,133.067302194917));
#144483=CARTESIAN_POINT('Ctrl Pts',(128.418782272263,5.49880287733247,132.99022472585));
#144484=CARTESIAN_POINT('Ctrl Pts',(128.414846222823,5.52841007967023,132.912585594531));
#144485=CARTESIAN_POINT('Ctrl Pts',(128.407422956417,5.58424833927361,132.76616061589));
#144486=CARTESIAN_POINT('Ctrl Pts',(128.399999690012,5.63434971623466,132.617294302748));
#144487=CARTESIAN_POINT('Ctrl Pts',(128.392576423606,5.67849457154205,132.46647672767));
#144488=CARTESIAN_POINT('Ctrl Pts',(128.385161930885,5.7225872512966,132.31583740644));
#144489=CARTESIAN_POINT('Ctrl Pts',(128.377747438164,5.76073731894136,132.163251768604));
#144490=CARTESIAN_POINT('Ctrl Pts',(128.370332945443,5.79277315039603,132.009229818164));
#144491=CARTESIAN_POINT('Ctrl Pts',(128.362925599089,5.82477810451019,131.855356319879));
#144492=CARTESIAN_POINT('Ctrl Pts',(128.355518252736,5.85068047899101,131.700049628025));
#144493=CARTESIAN_POINT('Ctrl Pts',(128.348110906382,5.87035846901979,131.543834760256));
#144494=CARTESIAN_POINT('Ctrl Pts',(128.340709084707,5.89002178246118,131.38773640343));
#144495=CARTESIAN_POINT('Ctrl Pts',(128.333307263031,5.90346990860321,131.230731588165));
#144496=CARTESIAN_POINT('Ctrl Pts',(128.325905441356,5.91063215235769,131.073355268099));
#144497=CARTESIAN_POINT('Ctrl Pts',(128.318507527044,5.91779061521941,130.916062025769));
#144498=CARTESIAN_POINT('Ctrl Pts',(128.311109612733,5.91866978725571,130.758398041177));
#144499=CARTESIAN_POINT('Ctrl Pts',(128.303711698422,5.91325084607816,130.600903020372));
#144500=CARTESIAN_POINT('Ctrl Pts',(128.29631501351,5.90783280543032,130.443434172382));
#144501=CARTESIAN_POINT('Ctrl Pts',(128.288918328597,5.8961187416476,130.286134605162));
#144502=CARTESIAN_POINT('Ctrl Pts',(128.281521643685,5.8781419506315,130.129543775211));
#144503=CARTESIAN_POINT('Ctrl Pts',(128.27412528675,5.86016595672518,129.972959888661));
#144504=CARTESIAN_POINT('Ctrl Pts',(128.266728929814,5.83592783031404,129.817085047756));
#144505=CARTESIAN_POINT('Ctrl Pts',(128.259332572879,5.8055127003416,129.66245306935));
#144506=CARTESIAN_POINT('Ctrl Pts',(128.251935083542,5.77509291373494,129.507797416392));
#144507=CARTESIAN_POINT('Ctrl Pts',(128.244537594206,5.73849431257206,129.354385371121));
#144508=CARTESIAN_POINT('Ctrl Pts',(128.237140104869,5.69585302159305,129.202739901257));
#144509=CARTESIAN_POINT('Ctrl Pts',(128.229740022354,5.65319678277553,129.051041272309));
#144510=CARTESIAN_POINT('Ctrl Pts',(128.222339939839,5.60449373769657,128.90111081087));
#144511=CARTESIAN_POINT('Ctrl Pts',(128.214939857324,5.54992963304343,128.753455541565));
#144512=CARTESIAN_POINT('Ctrl Pts',(128.207531637658,5.49530552954812,128.605637910113));
#144513=CARTESIAN_POINT('Ctrl Pts',(128.200123417991,5.4348076251895,128.46010081744));
#144514=CARTESIAN_POINT('Ctrl Pts',(128.192715198325,5.36866979237122,128.317331220277));
#144515=CARTESIAN_POINT('Ctrl Pts',(128.185302419023,5.30249125282027,128.174473750808));
#144516=CARTESIAN_POINT('Ctrl Pts',(128.177889639721,5.23066603776645,128.034387502393));
#144517=CARTESIAN_POINT('Ctrl Pts',(128.170476860419,5.15347333719323,127.897533631772));
#144518=CARTESIAN_POINT('Ctrl Pts',(128.16305348939,5.07617034006962,127.760484217924));
#144519=CARTESIAN_POINT('Ctrl Pts',(128.155630118361,4.99348473579819,127.626676722914));
#144520=CARTESIAN_POINT('Ctrl Pts',(128.148206747332,4.90573872255601,127.496542885508));
#144521=CARTESIAN_POINT('Ctrl Pts',(128.144270697892,4.8592136808981,127.427542802397));
#144522=CARTESIAN_POINT('Ctrl Pts',(128.140334648451,4.81126665211715,127.359574965908));
#144523=CARTESIAN_POINT('Ctrl Pts',(128.13639859901,4.76195006814101,127.292699741138));
#144524=CARTESIAN_POINT('Ctrl Pts',(128.128975332605,4.66894052988033,127.166575154328));
#144525=CARTESIAN_POINT('Ctrl Pts',(128.121552066199,4.57077610256248,127.043957568431));
#144526=CARTESIAN_POINT('Ctrl Pts',(128.114128799794,4.46775037786499,126.925296668159));
#144527=CARTESIAN_POINT('Ctrl Pts',(128.106714307073,4.36484642101827,126.806776015218));
#144528=CARTESIAN_POINT('Ctrl Pts',(128.099299814352,4.25709284588642,126.69220301848));
#144529=CARTESIAN_POINT('Ctrl Pts',(128.091885321631,4.14482596627309,126.581997739768));
#144530=CARTESIAN_POINT('Ctrl Pts',(128.084477975277,4.03266729370517,126.471898681052));
#144531=CARTESIAN_POINT('Ctrl Pts',(128.077070628923,3.91600424144183,126.366159219284));
#144532=CARTESIAN_POINT('Ctrl Pts',(128.06966328257,3.79521268322544,126.265165617174));
#144533=CARTESIAN_POINT('Ctrl Pts',(128.062261460894,3.67451121591021,126.164247339902));
#144534=CARTESIAN_POINT('Ctrl Pts',(128.054859639219,3.54968765888871,126.068068112802));
#144535=CARTESIAN_POINT('Ctrl Pts',(128.047457817543,3.42115387138544,125.97697656916));
#144536=CARTESIAN_POINT('Ctrl Pts',(128.040059903232,3.29268793586909,125.885933112036));
#144537=CARTESIAN_POINT('Ctrl Pts',(128.032661988921,3.16051597431732,125.799972204874));
#144538=CARTESIAN_POINT('Ctrl Pts',(128.02526407461,3.02508188275239,125.719401407784));
#144539=CARTESIAN_POINT('Ctrl Pts',(128.017867389697,2.88967029787569,125.638844000099));
#144540=CARTESIAN_POINT('Ctrl Pts',(128.010470704785,2.75099797941207,125.563675115381));
#144541=CARTESIAN_POINT('Ctrl Pts',(128.003074019873,2.60953678463971,125.49415833026));
#144542=CARTESIAN_POINT('Ctrl Pts',(127.995677662938,2.46808186240486,125.424644627585));
#144543=CARTESIAN_POINT('Ctrl Pts',(127.988281306002,2.32383864477195,125.360782690831));
#144544=CARTESIAN_POINT('Ctrl Pts',(127.980884949067,2.17730226125249,125.302789439653));
#144545=CARTESIAN_POINT('Ctrl Pts',(127.97348745973,2.03074344263884,125.24478730956));
#144546=CARTESIAN_POINT('Ctrl Pts',(127.966089970394,1.88189110619851,125.192655791478));
#144547=CARTESIAN_POINT('Ctrl Pts',(127.958692481057,1.73125881823492,125.146563036635));
#144548=CARTESIAN_POINT('Ctrl Pts',(127.951292398542,1.58057372635705,125.100454124049));
#144549=CARTESIAN_POINT('Ctrl Pts',(127.943892316027,1.42810779739511,125.060388298553));
#144550=CARTESIAN_POINT('Ctrl Pts',(127.936492233512,1.27438800614917,125.026483345394));
#144551=CARTESIAN_POINT('Ctrl Pts',(127.929084013846,1.12049918418889,124.992541110253));
#144552=CARTESIAN_POINT('Ctrl Pts',(127.92167579418,0.965354111249209,124.964773357049));
#144553=CARTESIAN_POINT('Ctrl Pts',(127.914267574513,0.809488891566029,
124.943246534311));
#144554=CARTESIAN_POINT('Ctrl Pts',(127.906854795211,0.653527739440219,
124.921706462173));
#144555=CARTESIAN_POINT('Ctrl Pts',(127.899442015909,0.496845928034274,
124.906415010728));
#144556=CARTESIAN_POINT('Ctrl Pts',(127.892029236607,0.339982350581597,
124.897386556019));
#144557=CARTESIAN_POINT('Ctrl Pts',(127.884605865578,0.182894639093508,
124.88834520103));
#144558=CARTESIAN_POINT('Ctrl Pts',(127.877182494549,0.0256250150995326,
124.885584722199));
#144559=CARTESIAN_POINT('Ctrl Pts',(127.869759123521,-0.131289131365203,
124.889067410422));
#144560=CARTESIAN_POINT('Ctrl Pts',(127.86582307408,-0.214488776927516,
124.890914015284));
#144561=CARTESIAN_POINT('Ctrl Pts',(127.861887024639,-0.297588582945411,
124.894514932699));
#144562=CARTESIAN_POINT('Ctrl Pts',(127.857950975198,-0.380509421815742,
124.89985867901));
#144563=CARTESIAN_POINT('Ctrl Pts',(127.850527708792,-0.536895536047933,
124.909936817781));
#144564=CARTESIAN_POINT('Ctrl Pts',(127.843104442387,-0.693117454538892,
124.926247530366));
#144565=CARTESIAN_POINT('Ctrl Pts',(127.835681175981,-0.848638151331146,
124.948786875344));
#144566=CARTESIAN_POINT('Ctrl Pts',(127.82826668326,-1.00397503557443,124.971299580687));
#144567=CARTESIAN_POINT('Ctrl Pts',(127.82085219054,-1.15861198199119,125.000026211848));
#144568=CARTESIAN_POINT('Ctrl Pts',(127.813437697819,-1.31201379484953,
125.034910872172));
#144569=CARTESIAN_POINT('Ctrl Pts',(127.806030351465,-1.4652677532656,125.069761909347));
#144570=CARTESIAN_POINT('Ctrl Pts',(127.798623005111,-1.61728858655028,
125.11075907737));
#144571=CARTESIAN_POINT('Ctrl Pts',(127.791215658757,-1.76754815200689,
125.157794927446));
#144572=CARTESIAN_POINT('Ctrl Pts',(127.783813837082,-1.91769564821019,
125.204795696411));
#144573=CARTESIAN_POINT('Ctrl Pts',(127.776412015406,-2.06608413746188,
125.257826068563));
#144574=CARTESIAN_POINT('Ctrl Pts',(127.769010193731,-2.21219768473163,
125.316727979883));
#144575=CARTESIAN_POINT('Ctrl Pts',(127.76161227942,-2.35823409979941,125.375598797342));
#144576=CARTESIAN_POINT('Ctrl Pts',(127.754214365108,-2.50199761923544,
125.440334841869));
#144577=CARTESIAN_POINT('Ctrl Pts',(127.746816450797,-2.64298954736569,
125.510728894919));
#144578=CARTESIAN_POINT('Ctrl Pts',(127.739419765884,-2.78395804519353,
125.581111249753));
#144579=CARTESIAN_POINT('Ctrl Pts',(127.732023080972,-2.92215553218961,
125.657149580389));
#144580=CARTESIAN_POINT('Ctrl Pts',(127.72462639606,-3.05710520348624,125.738589369541));
#144581=CARTESIAN_POINT('Ctrl Pts',(127.717230039125,-3.19204889097331,
125.820025547567));
#144582=CARTESIAN_POINT('Ctrl Pts',(127.709833682189,-3.32374472949663,
125.906862515012));
#144583=CARTESIAN_POINT('Ctrl Pts',(127.702437325254,-3.45174258880932,
125.998800955768));
#144584=CARTESIAN_POINT('Ctrl Pts',(127.695039835917,-3.57976004492076,
126.090753472534));
#144585=CARTESIAN_POINT('Ctrl Pts',(127.68764234658,-3.70407809129121,126.187808799992));
#144586=CARTESIAN_POINT('Ctrl Pts',(127.680244857244,-3.82427766239768,
126.289625750114));
#144587=CARTESIAN_POINT('Ctrl Pts',(127.672844774729,-3.94451936927671,
126.391478392009));
#144588=CARTESIAN_POINT('Ctrl Pts',(127.665444692214,-4.06063944178101,
126.498095738762));
#144589=CARTESIAN_POINT('Ctrl Pts',(127.658044609699,-4.17225394109482,
126.609098097351));
#144590=CARTESIAN_POINT('Ctrl Pts',(127.650636390032,-4.28399117202575,
126.720222514446));
#144591=CARTESIAN_POINT('Ctrl Pts',(127.643228170366,-4.39121267077332,
126.835741309375));
#144592=CARTESIAN_POINT('Ctrl Pts',(127.635819950699,-4.49357275487206,
126.955239359516));
#144593=CARTESIAN_POINT('Ctrl Pts',(127.628407171397,-4.59599583989401,
127.074810958712));
#144594=CARTESIAN_POINT('Ctrl Pts',(127.620994392095,-4.69355131730112,
127.198366401086));
#144595=CARTESIAN_POINT('Ctrl Pts',(127.613581612793,-4.78593580716516,
127.325460071101));
#144596=CARTESIAN_POINT('Ctrl Pts',(127.606158241765,-4.87845230032126,
127.452735338512));
#144597=CARTESIAN_POINT('Ctrl Pts',(127.598734870736,-4.96578284263531,
127.583558621049));
#144598=CARTESIAN_POINT('Ctrl Pts',(127.591311499707,-5.04766868740341,
127.717457414563));
#144599=CARTESIAN_POINT('Ctrl Pts',(127.587375450266,-5.09108652712324,
127.788453767742));
#144600=CARTESIAN_POINT('Ctrl Pts',(127.583439400825,-5.13297444829509,
127.860314371871));
#144601=CARTESIAN_POINT('Ctrl Pts',(127.579503351385,-5.17329934204225,
127.932966447459));
#144602=CARTESIAN_POINT('Ctrl Pts',(127.571720884375,-5.25303084948161,
128.076616162733));
#144603=CARTESIAN_POINT('Ctrl Pts',(127.563938417365,-5.32687085259762,
128.223760860196));
#144604=CARTESIAN_POINT('Ctrl Pts',(127.556155950355,-5.39451514061434,
128.373900381277));
#144605=CARTESIAN_POINT('Ctrl Pts',(127.548386021547,-5.4620504480527,128.523798015092));
#144606=CARTESIAN_POINT('Ctrl Pts',(127.540616092739,-5.52340980383546,
128.676680565061));
#144607=CARTESIAN_POINT('Ctrl Pts',(127.532846163931,-5.57833413430794,
128.83202219617));
#144608=CARTESIAN_POINT('Ctrl Pts',(127.524973582954,-5.63398409583541,
128.989416118326));
#144609=CARTESIAN_POINT('Ctrl Pts',(127.517101001978,-5.68302759259376,
129.149334291285));
#144610=CARTESIAN_POINT('Ctrl Pts',(127.509228421001,-5.72524371990631,
129.31120459418));
#144611=CARTESIAN_POINT('Ctrl Pts',(127.501485147885,-5.76676644347643,
129.470416162583));
#144612=CARTESIAN_POINT('Ctrl Pts',(127.493741874769,-5.80168422650777,
129.631515907992));
#144613=CARTESIAN_POINT('Ctrl Pts',(127.485998601653,-5.82983536458688,
129.793939821901));
#144614=CARTESIAN_POINT('Ctrl Pts',(127.478061366746,-5.85869166249726,
129.960432303816));
#144615=CARTESIAN_POINT('Ctrl Pts',(127.470124131839,-5.88043772876022,
130.128315857805));
#144616=CARTESIAN_POINT('Ctrl Pts',(127.462186896932,-5.89495394412328,
130.296966728004));
#144617=CARTESIAN_POINT('Ctrl Pts',(127.454249662025,-5.90947015948635,
130.465617598202));
#144618=CARTESIAN_POINT('Ctrl Pts',(127.446312427118,-5.91675643119916,
130.635035426966));
#144619=CARTESIAN_POINT('Ctrl Pts',(127.438375192211,-5.91674999573795,
130.804585194783));
#144620=CARTESIAN_POINT('',(125.688375192211,-5.91687709322784,130.809716457862));
#144621=CARTESIAN_POINT('Ctrl Pts',(127.438375192169,-5.91674999573792,
130.804585195673));
#144622=CARTESIAN_POINT('Ctrl Pts',(127.430604669703,-5.91674369542117,
130.970573766693));
#144623=CARTESIAN_POINT('Ctrl Pts',(127.422834147236,-5.90974812859556,
131.136419067381));
#144624=CARTESIAN_POINT('Ctrl Pts',(127.415063624769,-5.89582513269253,
131.301529167669));
#144625=CARTESIAN_POINT('Ctrl Pts',(127.407282577955,-5.88188327957108,
131.466862892042));
#144626=CARTESIAN_POINT('Ctrl Pts',(127.399501531142,-5.86099529452708,
131.6314591157));
#144627=CARTESIAN_POINT('Ctrl Pts',(127.391720484328,-5.83327443974951,
131.794734220337));
#144628=CARTESIAN_POINT('Ctrl Pts',(127.383920661007,-5.80548669155154,
131.958403325458));
#144629=CARTESIAN_POINT('Ctrl Pts',(127.376120837686,-5.77083315191996,
132.120744625218));
#144630=CARTESIAN_POINT('Ctrl Pts',(127.368321014365,-5.72947802711713,
132.281185623883));
#144631=CARTESIAN_POINT('Ctrl Pts',(127.360511508761,-5.68807156627945,
132.441825785402));
#144632=CARTESIAN_POINT('Ctrl Pts',(127.352702003157,-5.63994700459161,
132.600560636575));
#144633=CARTESIAN_POINT('Ctrl Pts',(127.344892497554,-5.58531762056006,
132.756835365152));
#144634=CARTESIAN_POINT('Ctrl Pts',(127.337064695576,-5.53056024895637,
132.913476219459));
#144635=CARTESIAN_POINT('Ctrl Pts',(127.329236893598,-5.4692676909672,133.067645130788));
#144636=CARTESIAN_POINT('Ctrl Pts',(127.32140909162,-5.4017012640059,133.218807555674));
#144637=CARTESIAN_POINT('Ctrl Pts',(127.314624636937,-5.34314058974658,
133.349821935478));
#144638=CARTESIAN_POINT('Ctrl Pts',(127.307840182254,-5.27986784560114,
133.478578151947));
#144639=CARTESIAN_POINT('Ctrl Pts',(127.301055727571,-5.21207989665515,
133.604745182833));
#144640=CARTESIAN_POINT('Ctrl Pts',(127.293632461166,-5.13790915963536,
133.742791868326));
#144641=CARTESIAN_POINT('Ctrl Pts',(127.28620919476,-5.05813804137341,133.878098541676));
#144642=CARTESIAN_POINT('Ctrl Pts',(127.278785928355,-4.97299335046132,
134.010178406956));
#144643=CARTESIAN_POINT('Ctrl Pts',(127.271371435634,-4.88794929350306,
134.142102164803));
#144644=CARTESIAN_POINT('Ctrl Pts',(127.263956942913,-4.79754450611277,
134.270806395316));
#144645=CARTESIAN_POINT('Ctrl Pts',(127.256542450192,-4.70205229028583,
134.395827563247));
#144646=CARTESIAN_POINT('Ctrl Pts',(127.249135103838,-4.60665211345173,
134.520728231069));
#144647=CARTESIAN_POINT('Ctrl Pts',(127.241727757484,-4.50617449506531,
134.64195260874));
#144648=CARTESIAN_POINT('Ctrl Pts',(127.234320411131,-4.40093669295999,
134.759065004377));
#144649=CARTESIAN_POINT('Ctrl Pts',(127.226918589455,-4.29577738117766,
134.87609005317));
#144650=CARTESIAN_POINT('Ctrl Pts',(127.21951676778,-4.18586520328702,134.989008950014));
#144651=CARTESIAN_POINT('Ctrl Pts',(127.212114946104,-4.07155837821149,
135.09741814517));
#144652=CARTESIAN_POINT('Ctrl Pts',(127.204717031793,-3.95731189481916,
135.205770111955));
#144653=CARTESIAN_POINT('Ctrl Pts',(127.197319117482,-3.83867565460476,
135.309616861971));
#144654=CARTESIAN_POINT('Ctrl Pts',(127.18992120317,-3.71604541753918,135.408590956861));
#144655=CARTESIAN_POINT('Ctrl Pts',(127.182524518258,-3.59343555939452,
135.507548604052));
#144656=CARTESIAN_POINT('Ctrl Pts',(127.175127833346,-3.46683331191033,
135.601634969004));
#144657=CARTESIAN_POINT('Ctrl Pts',(127.167731148434,-3.33666835478942,
135.690522183933));
#144658=CARTESIAN_POINT('Ctrl Pts',(127.160334791498,-3.20650916931911,
135.77940545751));
#144659=CARTESIAN_POINT('Ctrl Pts',(127.152938434563,-3.07278789659433,
135.863089828931));
#144660=CARTESIAN_POINT('Ctrl Pts',(127.145542077627,-2.93596387385731,
135.941290312812));
#144661=CARTESIAN_POINT('Ctrl Pts',(127.138144588291,-2.79911890301292,
136.019502769387));
#144662=CARTESIAN_POINT('Ctrl Pts',(127.130747098954,-2.65917056040906,
136.092229481426));
#144663=CARTESIAN_POINT('Ctrl Pts',(127.123349609618,-2.51660335394268,
136.159231122202));
#144664=CARTESIAN_POINT('Ctrl Pts',(127.115949527103,-2.37398617076349,
136.2262562503));
#144665=CARTESIAN_POINT('Ctrl Pts',(127.108549444588,-2.22874863355076,
136.287552152705));
#144666=CARTESIAN_POINT('Ctrl Pts',(127.101149362073,-2.0813956701444,136.342927456271));
#144667=CARTESIAN_POINT('Ctrl Pts',(127.093741142406,-1.93388067700622,
136.398363650677));
#144668=CARTESIAN_POINT('Ctrl Pts',(127.08633292274,-1.78424596189502,136.447866113334));
#144669=CARTESIAN_POINT('Ctrl Pts',(127.078924703073,-1.63301277458622,
136.491292992805));
#144670=CARTESIAN_POINT('Ctrl Pts',(127.071511923771,-1.48168650577378,
136.534746600795));
#144671=CARTESIAN_POINT('Ctrl Pts',(127.064099144469,-1.32876016613994,
136.572117085926));
#144672=CARTESIAN_POINT('Ctrl Pts',(127.056686365167,-1.17476515552874,
136.603313746524));
#144673=CARTESIAN_POINT('Ctrl Pts',(127.049262994138,-1.02055010962506,
136.634554982375));
#144674=CARTESIAN_POINT('Ctrl Pts',(127.04183962311,-0.865263710605422,
136.659604715986));
#144675=CARTESIAN_POINT('Ctrl Pts',(127.034416252081,-0.709443261418309,
136.678424017065));
#144676=CARTESIAN_POINT('Ctrl Pts',(127.03048020264,-0.626823520400057,
136.688402462059));
#144677=CARTESIAN_POINT('Ctrl Pts',(127.0265441532,-0.544053664613397,136.696630179769));
#144678=CARTESIAN_POINT('Ctrl Pts',(127.022608103759,-0.461213650500511,
136.703107309118));
#144679=CARTESIAN_POINT('Ctrl Pts',(127.015184837353,-0.304979969229936,
136.715322972925));
#144680=CARTESIAN_POINT('Ctrl Pts',(127.007761570948,-0.148024394917613,
136.721345833891));
#144681=CARTESIAN_POINT('Ctrl Pts',(127.000338304543,0.00912092165060211,
136.721103587418));
#144682=CARTESIAN_POINT('Ctrl Pts',(126.992923811822,0.166080505504851,
136.720861627259));
#144683=CARTESIAN_POINT('Ctrl Pts',(126.985509319101,0.323229015572892,
136.714369299599));
#144684=CARTESIAN_POINT('Ctrl Pts',(126.97809482638,0.480028740117872,136.701605989022));
#144685=CARTESIAN_POINT('Ctrl Pts',(126.970687480026,0.63667733518493,136.688854980204));
#144686=CARTESIAN_POINT('Ctrl Pts',(126.963280133672,0.792977444412863,
136.669845051384));
#144687=CARTESIAN_POINT('Ctrl Pts',(126.955872787318,0.948391022270923,
136.644607618454));
#144688=CARTESIAN_POINT('Ctrl Pts',(126.948470965643,1.1036886868192,136.619389008553));
#144689=CARTESIAN_POINT('Ctrl Pts',(126.941069143967,1.2581007696677,136.587952202361));
#144690=CARTESIAN_POINT('Ctrl Pts',(126.933667322292,1.41109412691216,136.550380451111));
#144691=CARTESIAN_POINT('Ctrl Pts',(126.926269407981,1.56400672015455,136.512828533696));
#144692=CARTESIAN_POINT('Ctrl Pts',(126.918871493669,1.71550171772267,136.469148209832));
#144693=CARTESIAN_POINT('Ctrl Pts',(126.911473579358,1.86505606539004,136.419473834185));
#144694=CARTESIAN_POINT('Ctrl Pts',(126.904076894446,2.01458555983769,136.369807713518));
#144695=CARTESIAN_POINT('Ctrl Pts',(126.896680209533,2.16217469053301,136.314149635592));
#144696=CARTESIAN_POINT('Ctrl Pts',(126.889283524621,2.30731536064919,136.252683881563));
#144697=CARTESIAN_POINT('Ctrl Pts',(126.881887167686,2.45244959507596,136.19122085299));
#144698=CARTESIAN_POINT('Ctrl Pts',(126.87449081075,2.59513524104833,136.123950805921));
#144699=CARTESIAN_POINT('Ctrl Pts',(126.867094453815,2.73488424929218,136.051106152226));
#144700=CARTESIAN_POINT('Ctrl Pts',(126.859696964478,2.87465465346605,135.978250345828));
#144701=CARTESIAN_POINT('Ctrl Pts',(126.852299475142,3.01148719363715,135.899818405958));
#144702=CARTESIAN_POINT('Ctrl Pts',(126.844901985805,3.14491862909991,135.816088600891));
#144703=CARTESIAN_POINT('Ctrl Pts',(126.83750190329,3.27839683874543,135.73232944447));
#144704=CARTESIAN_POINT('Ctrl Pts',(126.830101820775,3.40847125391639,135.643268923558));
#144705=CARTESIAN_POINT('Ctrl Pts',(126.82270173826,3.53470794113451,135.549228406386));
#144706=CARTESIAN_POINT('Ctrl Pts',(126.815293518594,3.66108343856776,135.455084481998));
#144707=CARTESIAN_POINT('Ctrl Pts',(126.807885298927,3.78361248093266,135.355949848531));
#144708=CARTESIAN_POINT('Ctrl Pts',(126.800477079261,3.9018939763607,135.252186374016));
#144709=CARTESIAN_POINT('Ctrl Pts',(126.793064299959,4.02024827207562,135.148359034814));
#144710=CARTESIAN_POINT('Ctrl Pts',(126.785651520657,4.1343495416086,135.039897434219));
#144711=CARTESIAN_POINT('Ctrl Pts',(126.778238741354,4.24383424047797,134.927199627502));
#144712=CARTESIAN_POINT('Ctrl Pts',(126.770815370326,4.35347537621934,134.814340792873));
#144713=CARTESIAN_POINT('Ctrl Pts',(126.763391999297,4.45848651830365,134.697233940329));
#144714=CARTESIAN_POINT('Ctrl Pts',(126.755968628268,4.55854448820266,134.576310075284));
#144715=CARTESIAN_POINT('Ctrl Pts',(126.752032578827,4.61159762470175,134.512193340508));
#144716=CARTESIAN_POINT('Ctrl Pts',(126.748096529387,4.66325896545235,134.447003999064));
#144717=CARTESIAN_POINT('Ctrl Pts',(126.744160479946,4.7134854089243,134.380809395664));
#144718=CARTESIAN_POINT('Ctrl Pts',(126.73673721354,4.80821091379789,134.255968439515));
#144719=CARTESIAN_POINT('Ctrl Pts',(126.729313947135,4.89811643907389,134.127172773102));
#144720=CARTESIAN_POINT('Ctrl Pts',(126.721890680729,4.9828535123478,133.99483102755));
#144721=CARTESIAN_POINT('Ctrl Pts',(126.714476188008,5.06749043343813,133.862645698951));
#144722=CARTESIAN_POINT('Ctrl Pts',(126.707061695287,5.14697086256309,133.726922945069));
#144723=CARTESIAN_POINT('Ctrl Pts',(126.699647202566,5.22098680906185,133.588104014882));
#144724=CARTESIAN_POINT('Ctrl Pts',(126.692239856213,5.29493141620472,133.449418883607));
#144725=CARTESIAN_POINT('Ctrl Pts',(126.684832509859,5.36342185157869,133.307643844193));
#144726=CARTESIAN_POINT('Ctrl Pts',(126.677425163505,5.42619371951346,133.163248550642));
#144727=CARTESIAN_POINT('Ctrl Pts',(126.67002334183,5.48891876982088,133.018960952549));
#144728=CARTESIAN_POINT('Ctrl Pts',(126.662621520154,5.54593359693948,132.872057332438));
#144729=CARTESIAN_POINT('Ctrl Pts',(126.655219698479,5.59702006518662,132.723031238699));
#144730=CARTESIAN_POINT('Ctrl Pts',(126.647821784167,5.64807956528488,132.574083814675));
#144731=CARTESIAN_POINT('Ctrl Pts',(126.640423869856,5.69321681838378,132.42301650066));
#144732=CARTESIAN_POINT('Ctrl Pts',(126.633025955545,5.73226213728277,132.270341978967));
#144733=CARTESIAN_POINT('Ctrl Pts',(126.625629270632,5.77130096755809,132.117692829009));
#144734=CARTESIAN_POINT('Ctrl Pts',(126.61823258572,5.80424978048555,131.96343736277));
#144735=CARTESIAN_POINT('Ctrl Pts',(126.610835900808,5.83098897827627,131.808102664967));
#144736=CARTESIAN_POINT('Ctrl Pts',(126.603439543872,5.85772699042292,131.652774854867));
#144737=CARTESIAN_POINT('Ctrl Pts',(126.596043186937,5.87825587157571,131.49636827624));
#144738=CARTESIAN_POINT('Ctrl Pts',(126.588646830002,5.89250735386897,131.339419163054));
#144739=CARTESIAN_POINT('Ctrl Pts',(126.581249340665,5.90676101810057,131.182446020559));
#144740=CARTESIAN_POINT('Ctrl Pts',(126.573851851328,5.91473533606307,131.024930549908));
#144741=CARTESIAN_POINT('Ctrl Pts',(126.566454361992,5.91641402982012,130.867412899425));
#144742=CARTESIAN_POINT('Ctrl Pts',(126.559054279477,5.91809331204067,130.709840031374));
#144743=CARTESIAN_POINT('Ctrl Pts',(126.551654196962,5.91347257211605,130.552265355014));
#144744=CARTESIAN_POINT('Ctrl Pts',(126.544254114447,5.90258763459732,130.39522765825));
#144745=CARTESIAN_POINT('Ctrl Pts',(126.53684589478,5.8916907279708,130.238017282394));
#144746=CARTESIAN_POINT('Ctrl Pts',(126.529437675114,5.87451589353259,130.081345437962));
#144747=CARTESIAN_POINT('Ctrl Pts',(126.522029455447,5.85115078115382,129.925745173414));
#144748=CARTESIAN_POINT('Ctrl Pts',(126.514616676145,5.82777128793821,129.770049139498));
#144749=CARTESIAN_POINT('Ctrl Pts',(126.507203896843,5.79819399482663,129.615426365481));
#144750=CARTESIAN_POINT('Ctrl Pts',(126.499791117541,5.7625572923183,129.462397870226));
#144751=CARTESIAN_POINT('Ctrl Pts',(126.492367746512,5.72686967041826,129.309150720681));
#144752=CARTESIAN_POINT('Ctrl Pts',(126.484944375484,5.6851054460712,129.157502758481));
#144753=CARTESIAN_POINT('Ctrl Pts',(126.477521004455,5.6374525504484,129.007958851829));
#144754=CARTESIAN_POINT('Ctrl Pts',(126.473584955014,5.6121858417739,128.928667084266));
#144755=CARTESIAN_POINT('Ctrl Pts',(126.469648905573,5.58526441913393,128.849966503781));
#144756=CARTESIAN_POINT('Ctrl Pts',(126.465712856133,5.55672164411094,128.771929774371));
#144757=CARTESIAN_POINT('Ctrl Pts',(126.458289589727,5.50289086120658,128.624754938147));
#144758=CARTESIAN_POINT('Ctrl Pts',(126.450866323322,5.44312755184637,128.47949766977));
#144759=CARTESIAN_POINT('Ctrl Pts',(126.443443056916,5.37758715112309,128.336672024049));
#144760=CARTESIAN_POINT('Ctrl Pts',(126.436028564195,5.31212421371066,128.194015186379));
#144761=CARTESIAN_POINT('Ctrl Pts',(126.428614071474,5.24089793036124,128.053784586668));
#144762=CARTESIAN_POINT('Ctrl Pts',(126.421199578753,5.16411305986116,127.916477852031));
#144763=CARTESIAN_POINT('Ctrl Pts',(126.413792232399,5.08740219751015,127.779303458795));
#144764=CARTESIAN_POINT('Ctrl Pts',(126.406384886046,5.005143594865,127.645047643914));
#144765=CARTESIAN_POINT('Ctrl Pts',(126.398977539692,4.9175894728204,127.514186710414));
#144766=CARTESIAN_POINT('Ctrl Pts',(126.391575718017,4.83010065194325,127.383423377935));
#144767=CARTESIAN_POINT('Ctrl Pts',(126.384173896341,4.73732438253885,127.256050194145));
#144768=CARTESIAN_POINT('Ctrl Pts',(126.376772074666,4.63955799318205,127.132517457735));
#144769=CARTESIAN_POINT('Ctrl Pts',(126.369374160354,4.5418432139411,127.009049933294));
#144770=CARTESIAN_POINT('Ctrl Pts',(126.361976246043,4.43914379205028,126.889419110659));
#144771=CARTESIAN_POINT('Ctrl Pts',(126.354578331732,4.33179934158259,126.774044869791));
#144772=CARTESIAN_POINT('Ctrl Pts',(126.347181646819,4.22447272981522,126.658689802029));
#144773=CARTESIAN_POINT('Ctrl Pts',(126.339784961907,4.11250287553328,126.547590185152));
#144774=CARTESIAN_POINT('Ctrl Pts',(126.332388276995,3.99626858451111,126.441131542334));
#144775=CARTESIAN_POINT('Ctrl Pts',(126.324991920059,3.88003944743921,126.334677620003));
#144776=CARTESIAN_POINT('Ctrl Pts',(126.317595563124,3.75954652488443,126.23286451469));
#144777=CARTESIAN_POINT('Ctrl Pts',(126.310199206189,3.63520406522306,126.136039509642));
#144778=CARTESIAN_POINT('Ctrl Pts',(126.302801716852,3.5108425684136,126.039199680439));
#144779=CARTESIAN_POINT('Ctrl Pts',(126.295404227515,3.3826306555269,125.947349701476));
#144780=CARTESIAN_POINT('Ctrl Pts',(126.288006738179,3.25101397002412,125.860795231207));
#144781=CARTESIAN_POINT('Ctrl Pts',(126.280606655664,3.11935114649618,125.774210419402));
#144782=CARTESIAN_POINT('Ctrl Pts',(126.273206573149,2.98428148573068,125.692925017219));
#144783=CARTESIAN_POINT('Ctrl Pts',(126.265806490634,2.84627764929576,125.617200112471));
#144784=CARTESIAN_POINT('Ctrl Pts',(126.258398270967,2.70812206345563,125.541391940405));
#144785=CARTESIAN_POINT('Ctrl Pts',(126.250990051301,2.56702618602561,125.471156656197));
#144786=CARTESIAN_POINT('Ctrl Pts',(126.243581831634,2.42348586266683,125.406708643239));
#144787=CARTESIAN_POINT('Ctrl Pts',(126.236169052332,2.27985719263392,125.342220963605));
#144788=CARTESIAN_POINT('Ctrl Pts',(126.22875627303,2.13378142431607,125.283527791744));
#144789=CARTESIAN_POINT('Ctrl Pts',(126.221343493728,1.98577170908535,125.230794319235));
#144790=CARTESIAN_POINT('Ctrl Pts',(126.213920122699,1.83755051063265,125.177985498666));
#144791=CARTESIAN_POINT('Ctrl Pts',(126.20649675167,1.68739020173327,125.131153495658));
#144792=CARTESIAN_POINT('Ctrl Pts',(126.199073380642,1.53581712369258,125.090413091987));
#144793=CARTESIAN_POINT('Ctrl Pts',(126.195137331201,1.45544944077159,125.068811552409));
#144794=CARTESIAN_POINT('Ctrl Pts',(126.19120128176,1.3746847269651,125.048921721609));
#144795=CARTESIAN_POINT('Ctrl Pts',(126.18726523232,1.29360214930372,125.030754808211));
#144796=CARTESIAN_POINT('Ctrl Pts',(126.179841965914,1.14068293833117,124.996492576511));
#144797=CARTESIAN_POINT('Ctrl Pts',(126.172418699509,0.986170356037416,
124.968258039597));
#144798=CARTESIAN_POINT('Ctrl Pts',(126.164995433103,0.83058090775567,124.946198284703));
#144799=CARTESIAN_POINT('Ctrl Pts',(126.157580940382,0.675175353280782,
124.924164602608));
#144800=CARTESIAN_POINT('Ctrl Pts',(126.150166447661,0.518695832258268,
124.908291227556));
#144801=CARTESIAN_POINT('Ctrl Pts',(126.14275195494,0.361671689599985,124.898674869794));
#144802=CARTESIAN_POINT('Ctrl Pts',(126.135344608587,0.204798892722251,
124.889067780639));
#144803=CARTESIAN_POINT('Ctrl Pts',(126.127937262233,0.0473828893332454,
124.885705725405));
#144804=CARTESIAN_POINT('Ctrl Pts',(126.120529915879,-0.110039261787883,
124.88863395693));
#144805=CARTESIAN_POINT('Ctrl Pts',(126.113128094204,-0.267344001529506,
124.891560004469));
#144806=CARTESIAN_POINT('Ctrl Pts',(126.105726272528,-0.4246545082465,124.900766990378));
#144807=CARTESIAN_POINT('Ctrl Pts',(126.098324450853,-0.581431219541534,
124.916248161147));
#144808=CARTESIAN_POINT('Ctrl Pts',(126.090926536542,-0.738125169631245,
124.931721159526));
#144809=CARTESIAN_POINT('Ctrl Pts',(126.08352862223,-0.894285514939462,
124.953461709982));
#144810=CARTESIAN_POINT('Ctrl Pts',(126.076130707919,-1.04937542886165,
124.981411040951));
#144811=CARTESIAN_POINT('Ctrl Pts',(126.068734023007,-1.20443956965344,
125.009355727248));
#144812=CARTESIAN_POINT('Ctrl Pts',(126.061337338095,-1.35843326509065,
125.043507080126));
#144813=CARTESIAN_POINT('Ctrl Pts',(126.053940653182,-1.51082740983665,
125.083754784248));
#144814=CARTESIAN_POINT('Ctrl Pts',(126.046544296247,-1.66321479726657,
125.124000703746));
#144815=CARTESIAN_POINT('Ctrl Pts',(126.039147939311,-1.81400241410713,
125.170342341682));
#144816=CARTESIAN_POINT('Ctrl Pts',(126.031751582376,-1.96267416976077,
125.222618894246));
#144817=CARTESIAN_POINT('Ctrl Pts',(126.024354093039,-2.11136868743985,
125.274903450483));
#144818=CARTESIAN_POINT('Ctrl Pts',(126.016956603703,-2.25794634673264,
125.333124606754));
#144819=CARTESIAN_POINT('Ctrl Pts',(126.009559114366,-2.40190910735036,
125.397072646454));
#144820=CARTESIAN_POINT('Ctrl Pts',(126.002159031851,-2.54592233389065,
125.461043103041));
#144821=CARTESIAN_POINT('Ctrl Pts',(125.994758949336,-2.68731849577285,
125.530744288628));
#144822=CARTESIAN_POINT('Ctrl Pts',(125.987358866821,-2.82562244730206,
125.605919663991));
#144823=CARTESIAN_POINT('Ctrl Pts',(125.979950647155,-2.96407847824398,
125.681177702409));
#144824=CARTESIAN_POINT('Ctrl Pts',(125.972542427489,-3.09943518022415,
125.761921773426));
#144825=CARTESIAN_POINT('Ctrl Pts',(125.965134207822,-3.2312441697306,125.847850587506));
#144826=CARTESIAN_POINT('Ctrl Pts',(125.95772142852,-3.36313428547102,125.933832289338));
#144827=CARTESIAN_POINT('Ctrl Pts',(125.950308649218,-3.49147203410891,
126.025004877253));
#144828=CARTESIAN_POINT('Ctrl Pts',(125.942895869916,-3.61584106444145,
126.121025912551));
#144829=CARTESIAN_POINT('Ctrl Pts',(125.935472498887,-3.74038779907668,
126.217184147207));
#144830=CARTESIAN_POINT('Ctrl Pts',(125.928049127858,-3.86095420438861,
126.318204426282));
#144831=CARTESIAN_POINT('Ctrl Pts',(125.92062575683,-3.97715921088422,126.423705966286));
#144832=CARTESIAN_POINT('Ctrl Pts',(125.916689707389,-4.03877389363215,
126.479645414274));
#144833=CARTESIAN_POINT('Ctrl Pts',(125.912753657948,-4.09916307219774,
126.536844115996));
#144834=CARTESIAN_POINT('Ctrl Pts',(125.908817608507,-4.15827452473585,
126.595241524521));
#144835=CARTESIAN_POINT('Ctrl Pts',(125.90149902863,-4.26818470079762,126.703824027184));
#144836=CARTESIAN_POINT('Ctrl Pts',(125.894180448753,-4.37402795947477,
126.816901451091));
#144837=CARTESIAN_POINT('Ctrl Pts',(125.886861868876,-4.47540639748585,
126.934132182468));
#144838=CARTESIAN_POINT('Ctrl Pts',(125.879552092185,-4.57666289199929,
127.051221902347));
#144839=CARTESIAN_POINT('Ctrl Pts',(125.872242315493,-4.67346500209269,
127.172454701838));
#144840=CARTESIAN_POINT('Ctrl Pts',(125.864932538802,-4.76544979670491,
127.297450467935));
#144841=CARTESIAN_POINT('Ctrl Pts',(125.857575982694,-4.85802325431277,
127.423246153001));
#144842=CARTESIAN_POINT('Ctrl Pts',(125.850219426586,-4.94571721874585,
127.552852884212));
#144843=CARTESIAN_POINT('Ctrl Pts',(125.842862870478,-5.02820048573112,
127.685846478141));
#144844=CARTESIAN_POINT('Ctrl Pts',(125.835566061488,-5.11001385535975,
127.817759949273));
#144845=CARTESIAN_POINT('Ctrl Pts',(125.828269252498,-5.18670063628449,
127.953005146424));
#144846=CARTESIAN_POINT('Ctrl Pts',(125.820972443509,-5.25797928195931,
128.091136625156));
#144847=CARTESIAN_POINT('Ctrl Pts',(125.8136787567,-5.32922742870997,128.229208999771));
#144848=CARTESIAN_POINT('Ctrl Pts',(125.806385069891,-5.39507186801401,
128.37016485772));
#144849=CARTESIAN_POINT('Ctrl Pts',(125.799091383082,-5.45527616356596,
128.513532701347));
#144850=CARTESIAN_POINT('Ctrl Pts',(125.791799281877,-5.51546737106253,
128.656869377658));
#144851=CARTESIAN_POINT('Ctrl Pts',(125.784507180672,-5.57002072663485,
128.802616641396));
#144852=CARTESIAN_POINT('Ctrl Pts',(125.777215079467,-5.61874738739333,
128.95028177373));
#144853=CARTESIAN_POINT('Ctrl Pts',(125.769811755529,-5.66821725127364,
129.100199167673));
#144854=CARTESIAN_POINT('Ctrl Pts',(125.762408431591,-5.71168106557502,
129.252093037716));
#144855=CARTESIAN_POINT('Ctrl Pts',(125.755005107653,-5.7489934610278,129.405430759582));
#144856=CARTESIAN_POINT('Ctrl Pts',(125.747709255647,-5.7857642031293,129.556542521685));
#144857=CARTESIAN_POINT('Ctrl Pts',(125.740413403641,-5.81656087769184,
129.709056107196));
#144858=CARTESIAN_POINT('Ctrl Pts',(125.733117551634,-5.84129583934044,
129.862451131573));
#144859=CARTESIAN_POINT('Ctrl Pts',(125.725660491731,-5.86657734047008,
130.019235546166));
#144860=CARTESIAN_POINT('Ctrl Pts',(125.718203431827,-5.88552606068901,
130.176940386491));
#144861=CARTESIAN_POINT('Ctrl Pts',(125.710746371923,-5.89810441933159,
130.335004866391));
#144862=CARTESIAN_POINT('Ctrl Pts',(125.703289312019,-5.91068277797417,
130.493069346291));
#144863=CARTESIAN_POINT('Ctrl Pts',(125.695832252115,-5.91689079666146,
130.6514930386));
#144864=CARTESIAN_POINT('Ctrl Pts',(125.688375192211,-5.91674757605312,
130.809716340626));
#144865=CARTESIAN_POINT('',(123.938375192211,-5.92504829577756,130.801671299475));
#144866=CARTESIAN_POINT('Ctrl Pts',(125.688375192211,-5.91821605979866,
130.809717669868));
#144867=CARTESIAN_POINT('Ctrl Pts',(125.669040123039,-5.92203015439028,
131.220073233809));
#144868=CARTESIAN_POINT('Ctrl Pts',(125.556889179265,-5.69567161983018,
133.596115399124));
#144869=CARTESIAN_POINT('Ctrl Pts',(125.351922360878,-2.48367746759114,
137.347212195226));
#144870=CARTESIAN_POINT('Ctrl Pts',(125.07347473707,4.16219799704592,136.430519908213));
#144871=CARTESIAN_POINT('Ctrl Pts',(124.795027113255,6.98321683707467,130.343662086251));
#144872=CARTESIAN_POINT('Ctrl Pts',(124.516579489443,3.38700055293948,124.680163708199));
#144873=CARTESIAN_POINT('Ctrl Pts',(124.238131865629,-3.32170377516985,
124.644503106196));
#144874=CARTESIAN_POINT('Ctrl Pts',(124.045397099886,-5.8524521295715,128.537956850714));
#144875=CARTESIAN_POINT('Ctrl Pts',(123.945478208746,-5.92589711076374,
130.651373189507));
#144876=CARTESIAN_POINT('Ctrl Pts',(123.938375192211,-5.92504829577756,
130.801671299475));
#144877=CARTESIAN_POINT('',(122.188375192211,-5.90992605862746,130.800308419121));
#144878=CARTESIAN_POINT('Ctrl Pts',(123.938375192211,-5.92504829577756,
130.801671299475));
#144879=CARTESIAN_POINT('Ctrl Pts',(123.852662334142,-5.91480555481291,
132.615334621827));
#144880=CARTESIAN_POINT('Ctrl Pts',(123.674133601469,-4.05249985999765,
136.411139468064));
#144881=CARTESIAN_POINT('Ctrl Pts',(123.40278899419,2.4139810832736,137.373246052702));
#144882=CARTESIAN_POINT('Ctrl Pts',(123.124341370378,6.83140509735844,132.324052996348));
#144883=CARTESIAN_POINT('Ctrl Pts',(122.845893746565,4.97110155966289,125.878336884994));
#144884=CARTESIAN_POINT('Ctrl Pts',(122.567446122753,-1.45740145955266,
123.959395934234));
#144885=CARTESIAN_POINT('Ctrl Pts',(122.348273271301,-5.4632512585378,127.400110204618));
#144886=CARTESIAN_POINT('Ctrl Pts',(122.221916294454,-5.91440793099423,
130.08591681752));
#144887=CARTESIAN_POINT('Ctrl Pts',(122.188375192211,-5.90992605862746,
130.800308419121));
#144888=CARTESIAN_POINT('',(120.438375158672,-5.91341329990167,130.808580694715));
#144889=CARTESIAN_POINT('Ctrl Pts',(122.188375192211,-5.90992605862746,
130.800308419121));
#144890=CARTESIAN_POINT('Ctrl Pts',(122.12910041985,-5.90200556864557,132.062801203515));
#144891=CARTESIAN_POINT('Ctrl Pts',(121.977009772883,-4.8860947069906,135.313812493445));
#144892=CARTESIAN_POINT('Ctrl Pts',(121.732103251314,0.471325265101819,
137.786868263448));
#144893=CARTESIAN_POINT('Ctrl Pts',(121.4536556275,6.12934425592135,134.182037263242));
#144894=CARTESIAN_POINT('Ctrl Pts',(121.175208003688,6.15479531066329,127.473286434335));
#144895=CARTESIAN_POINT('Ctrl Pts',(120.896760379875,0.524290153371079,
123.825630047797));
#144896=CARTESIAN_POINT('Ctrl Pts',(120.651149442716,-4.86720232846028,
126.264962262151));
#144897=CARTESIAN_POINT('Ctrl Pts',(120.498354380162,-5.90187691199983,
129.531255255228));
#144898=CARTESIAN_POINT('Ctrl Pts',(120.438375192211,-5.91024609870193,
130.808577719811));
#144899=CARTESIAN_POINT('',(118.688375192211,-5.92111403471271,130.806804712595));
#144900=CARTESIAN_POINT('Ctrl Pts',(120.438375123354,-5.91674849279557,
130.80858382741));
#144901=CARTESIAN_POINT('Ctrl Pts',(120.429906845386,-5.91661962929804,
130.989122548634));
#144902=CARTESIAN_POINT('Ctrl Pts',(120.421438567417,-5.90822361023152,
131.16933121331));
#144903=CARTESIAN_POINT('Ctrl Pts',(120.412970289449,-5.89167472838423,
131.348510833424));
#144904=CARTESIAN_POINT('Ctrl Pts',(120.404463212892,-5.87505002554334,
131.528511389778));
#144905=CARTESIAN_POINT('Ctrl Pts',(120.395956136335,-5.85019768804956,
131.707473309596));
#144906=CARTESIAN_POINT('Ctrl Pts',(120.387449059779,-5.81728316216418,
131.884706475938));
#144907=CARTESIAN_POINT('Ctrl Pts',(120.378889667413,-5.78416622243705,
132.063029569755));
#144908=CARTESIAN_POINT('Ctrl Pts',(120.370330275048,-5.74288771416499,
132.239602441887));
#144909=CARTESIAN_POINT('Ctrl Pts',(120.361770882682,-5.69366480443984,
132.413743001334));
#144910=CARTESIAN_POINT('Ctrl Pts',(120.354468965871,-5.6516733199206,132.562300261501));
#144911=CARTESIAN_POINT('Ctrl Pts',(120.34716704906,-5.60390106750741,132.709087690254));
#144912=CARTESIAN_POINT('Ctrl Pts',(120.339865132249,-5.55050988539579,
132.853694795933));
#144913=CARTESIAN_POINT('Ctrl Pts',(120.332441865844,-5.49623140225706,
133.000705108066));
#144914=CARTESIAN_POINT('Ctrl Pts',(120.325018599438,-5.43602625655856,
133.145779804663));
#144915=CARTESIAN_POINT('Ctrl Pts',(120.317595333033,-5.3700514472791,133.28840530639));
#144916=CARTESIAN_POINT('Ctrl Pts',(120.310180840312,-5.30415461474539,
133.430862236618));
#144917=CARTESIAN_POINT('Ctrl Pts',(120.302766347591,-5.23250184760396,
133.570875398483));
#144918=CARTESIAN_POINT('Ctrl Pts',(120.29535185487,-5.15529941829848,133.707947790391));
#144919=CARTESIAN_POINT('Ctrl Pts',(120.287944508517,-5.07817139960087,
133.844888066766));
#144920=CARTESIAN_POINT('Ctrl Pts',(120.280537162163,-4.9955045494545,133.978892892891));
#144921=CARTESIAN_POINT('Ctrl Pts',(120.273129815809,-4.90755253728837,
134.109486735622));
#144922=CARTESIAN_POINT('Ctrl Pts',(120.265727994134,-4.81966612305121,
134.239983176537));
#144923=CARTESIAN_POINT('Ctrl Pts',(120.258326172459,-4.72650260322443,
134.367073391291));
#144924=CARTESIAN_POINT('Ctrl Pts',(120.250924350783,-4.62836067555996,
134.490307988247));
#144925=CARTESIAN_POINT('Ctrl Pts',(120.243526436472,-4.53027055625502,
134.613477530618));
#144926=CARTESIAN_POINT('Ctrl Pts',(120.236128522161,-4.42720749498932,
134.732795217418));
#144927=CARTESIAN_POINT('Ctrl Pts',(120.228730607849,-4.31951238223295,
134.847842204297));
#144928=CARTESIAN_POINT('Ctrl Pts',(120.221333922937,-4.21183516645075,
134.962870072455));
#144929=CARTESIAN_POINT('Ctrl Pts',(120.213937238025,-4.09952768178991,
135.073628377004));
#144930=CARTESIAN_POINT('Ctrl Pts',(120.206540553113,-3.98296990567007,
135.179732749514));
#144931=CARTESIAN_POINT('Ctrl Pts',(120.199144196178,-3.86641729784416,
135.285832417245));
#144932=CARTESIAN_POINT('Ctrl Pts',(120.191747839242,-3.74561504933562,
135.387278311958));
#144933=CARTESIAN_POINT('Ctrl Pts',(120.184351482307,-3.62097846361268,
135.483724412843));
#144934=CARTESIAN_POINT('Ctrl Pts',(120.17695399297,-3.4963227957102,135.580185279874));
#144935=CARTESIAN_POINT('Ctrl Pts',(120.169556503634,-3.36783191695308,
135.671644600433));
#144936=CARTESIAN_POINT('Ctrl Pts',(120.162159014297,-3.23595239905746,
135.757798073872));
#144937=CARTESIAN_POINT('Ctrl Pts',(120.154758931782,-3.10402665100148,
135.843981748277));
#144938=CARTESIAN_POINT('Ctrl Pts',(120.147358849268,-2.96871021106818,
135.924855668366));
#144939=CARTESIAN_POINT('Ctrl Pts',(120.139958766753,-2.83047653329784,
136.000160186155));
#144940=CARTESIAN_POINT('Ctrl Pts',(120.132550547086,-2.69209085338783,
136.075547509003));
#144941=CARTESIAN_POINT('Ctrl Pts',(120.12514232742,-2.55078185746082,136.145353020571));
#144942=CARTESIAN_POINT('Ctrl Pts',(120.117734107753,-2.40704604139051,
136.209363847641));
#144943=CARTESIAN_POINT('Ctrl Pts',(120.110321328452,-2.26322175832377,
136.273414072308));
#144944=CARTESIAN_POINT('Ctrl Pts',(120.10290854915,-2.11696802479533,136.331662367916));
#144945=CARTESIAN_POINT('Ctrl Pts',(120.095495769848,-1.96879849258671,
136.383945105508));
#144946=CARTESIAN_POINT('Ctrl Pts',(120.088072398819,-1.82041724880191,
136.436302547129));
#144947=CARTESIAN_POINT('Ctrl Pts',(120.08064902779,-1.67011509492895,136.482677296888));
#144948=CARTESIAN_POINT('Ctrl Pts',(120.073225656761,-1.51841871919148,
136.522956175543));
#144949=CARTESIAN_POINT('Ctrl Pts',(120.06928960732,-1.43798566085437,136.544313003488));
#144950=CARTESIAN_POINT('Ctrl Pts',(120.065353557878,-1.35716078332332,
136.563956922157));
#144951=CARTESIAN_POINT('Ctrl Pts',(120.061417508437,-1.27602328737747,
136.581876963936));
#144952=CARTESIAN_POINT('Ctrl Pts',(120.053994242031,-1.1230005022684,136.615673603459));
#144953=CARTESIAN_POINT('Ctrl Pts',(120.046570975626,-0.968402699448,136.643437726442));
#144954=CARTESIAN_POINT('Ctrl Pts',(120.03914770922,-0.812746829540018,
136.665023818397));
#144955=CARTESIAN_POINT('Ctrl Pts',(120.031733216499,-0.657274931943631,
136.686584397383));
#144956=CARTESIAN_POINT('Ctrl Pts',(120.024318723778,-0.500747822629744,
136.701981429075));
#144957=CARTESIAN_POINT('Ctrl Pts',(120.016904231057,-0.343695138411051,
136.711119814819));
#144958=CARTESIAN_POINT('Ctrl Pts',(120.009496884704,-0.186793827482337,
136.720249392643));
#144959=CARTESIAN_POINT('Ctrl Pts',(120.00208953835,-0.0293683202935072,
136.723132312138));
#144960=CARTESIAN_POINT('Ctrl Pts',(119.994682191996,0.128044189129835,
136.7197249553));
#144961=CARTESIAN_POINT('Ctrl Pts',(119.987280370321,0.285339294364816,
136.716320139796));
#144962=CARTESIAN_POINT('Ctrl Pts',(119.979878548645,0.442621049532602,
136.706634397463));
#144963=CARTESIAN_POINT('Ctrl Pts',(119.97247672697,0.599349915290433,136.690676124022));
#144964=CARTESIAN_POINT('Ctrl Pts',(119.965078812659,0.755996045100118,
136.674726274828));
#144965=CARTESIAN_POINT('Ctrl Pts',(119.957680898347,0.912089496327345,
136.652510526699));
#144966=CARTESIAN_POINT('Ctrl Pts',(119.950282984036,1.06709362373455,136.624089284839));
#144967=CARTESIAN_POINT('Ctrl Pts',(119.942886299124,1.22207199226762,136.595672766075));
#144968=CARTESIAN_POINT('Ctrl Pts',(119.935489614211,1.37596102944626,136.561052867546));
#144969=CARTESIAN_POINT('Ctrl Pts',(119.928092929299,1.52823196814656,136.520341514493));
#144970=CARTESIAN_POINT('Ctrl Pts',(119.920696572364,1.68049615499387,136.479631966624));
#144971=CARTESIAN_POINT('Ctrl Pts',(119.913300215428,1.83114202539174,136.432831597701));
#144972=CARTESIAN_POINT('Ctrl Pts',(119.905903858493,1.97965398056459,136.380102781595));
#144973=CARTESIAN_POINT('Ctrl Pts',(119.898506369156,2.12818867329702,136.327365892573));
#144974=CARTESIAN_POINT('Ctrl Pts',(119.89110887982,2.27458844847988,136.268698874004));
#144975=CARTESIAN_POINT('Ctrl Pts',(119.883711390483,2.4183559064365,136.204312957384));
#144976=CARTESIAN_POINT('Ctrl Pts',(119.876311307968,2.56217376185254,136.139904470381));
#144977=CARTESIAN_POINT('Ctrl Pts',(119.868911225453,2.70335712236475,136.069773246366));
#144978=CARTESIAN_POINT('Ctrl Pts',(119.861511142938,2.84143162529623,135.994177269555));
#144979=CARTESIAN_POINT('Ctrl Pts',(119.854102923272,2.97965795533809,135.918498167197));
#144980=CARTESIAN_POINT('Ctrl Pts',(119.846694703605,3.11476827317795,135.83734249094));
#144981=CARTESIAN_POINT('Ctrl Pts',(119.839286483939,3.24631511440242,135.751012893652));
#144982=CARTESIAN_POINT('Ctrl Pts',(119.831873704637,3.37794292051287,135.664630161937));
#144983=CARTESIAN_POINT('Ctrl Pts',(119.824460925334,3.50600257670346,135.573067380366));
#144984=CARTESIAN_POINT('Ctrl Pts',(119.817048146032,3.63007877596548,135.476668253284));
#144985=CARTESIAN_POINT('Ctrl Pts',(119.809624775004,3.75433226111951,135.380131386608));
#144986=CARTESIAN_POINT('Ctrl Pts',(119.802201403975,3.87459063699609,135.278744612786));
#144987=CARTESIAN_POINT('Ctrl Pts',(119.794778032946,3.99047399484126,135.172889873391));
#144988=CARTESIAN_POINT('Ctrl Pts',(119.790841983505,4.05191813175439,135.116763150613));
#144989=CARTESIAN_POINT('Ctrl Pts',(119.786905934064,4.11213293742652,135.059380909947));
#144990=CARTESIAN_POINT('Ctrl Pts',(119.782969884624,4.17106637453843,135.000803856989));
#144991=CARTESIAN_POINT('Ctrl Pts',(119.775546618218,4.2822129976811,134.890329363237));
#144992=CARTESIAN_POINT('Ctrl Pts',(119.768123351813,4.38913562935371,134.775269039935));
#144993=CARTESIAN_POINT('Ctrl Pts',(119.760700085407,4.49143241965637,134.655979158149));
#144994=CARTESIAN_POINT('Ctrl Pts',(119.753285592686,4.59360830364818,134.536830267096));
#144995=CARTESIAN_POINT('Ctrl Pts',(119.745871099965,4.69116898844872,134.413462048675));
#144996=CARTESIAN_POINT('Ctrl Pts',(119.738456607244,4.78374818323294,134.28626869819));
#144997=CARTESIAN_POINT('Ctrl Pts',(119.73104926089,4.87623814670367,134.159197941445));
#144998=CARTESIAN_POINT('Ctrl Pts',(119.723641914537,4.96375596049115,134.028309692132));
#144999=CARTESIAN_POINT('Ctrl Pts',(119.716234568183,5.04597456103929,133.894032330199));
#145000=CARTESIAN_POINT('Ctrl Pts',(119.708832746507,5.12813183985327,133.759855117389));
#145001=CARTESIAN_POINT('Ctrl Pts',(119.701430924832,5.2049975810027,133.622294141996));
#145002=CARTESIAN_POINT('Ctrl Pts',(119.694029103157,5.27628721385202,133.481807871844));
#145003=CARTESIAN_POINT('Ctrl Pts',(119.686631188845,5.34753921345904,133.3413957633));
#145004=CARTESIAN_POINT('Ctrl Pts',(119.679233274534,5.41322079855772,133.198061767473));
#145005=CARTESIAN_POINT('Ctrl Pts',(119.671835360222,5.4730927198998,133.052290029687));
#145006=CARTESIAN_POINT('Ctrl Pts',(119.66443867531,5.53295469161473,132.90654251652));
#145007=CARTESIAN_POINT('Ctrl Pts',(119.657041990398,5.58700877404001,132.758358410385));
#145008=CARTESIAN_POINT('Ctrl Pts',(119.649645305486,5.63506332150261,132.608243076363));
#145009=CARTESIAN_POINT('Ctrl Pts',(119.64224894855,5.68311573817622,132.458134398613));
#145010=CARTESIAN_POINT('Ctrl Pts',(119.634852591615,5.72516903502612,132.306095018769));
#145011=CARTESIAN_POINT('Ctrl Pts',(119.627456234679,5.76108112805576,132.152646491726));
#145012=CARTESIAN_POINT('Ctrl Pts',(119.620058745343,5.79699871931853,131.999174471322));
#145013=CARTESIAN_POINT('Ctrl Pts',(119.612661256006,5.826773149559,131.844293237645));
#145014=CARTESIAN_POINT('Ctrl Pts',(119.60526376667,5.85031327714352,131.688535442913));
#145015=CARTESIAN_POINT('Ctrl Pts',(119.597863684155,5.87386165668326,131.532723047528));
#145016=CARTESIAN_POINT('Ctrl Pts',(119.59046360164,5.89117132665236,131.376033848179));
#145017=CARTESIAN_POINT('Ctrl Pts',(119.583063519125,5.90220293186348,131.219006386388));
#145018=CARTESIAN_POINT('Ctrl Pts',(119.575655299458,5.91324666745862,131.061806256761));
#145019=CARTESIAN_POINT('Ctrl Pts',(119.568247079792,5.91799852562069,130.904267494484));
#145020=CARTESIAN_POINT('Ctrl Pts',(119.560838860125,5.91647127133269,130.74693015531));
#145021=CARTESIAN_POINT('Ctrl Pts',(119.553426080823,5.91494307704515,130.589495977628));
#145022=CARTESIAN_POINT('Ctrl Pts',(119.546013301521,5.90712808791871,130.432263842053));
#145023=CARTESIAN_POINT('Ctrl Pts',(119.538600522219,5.89309098856959,130.275768938725));
#145024=CARTESIAN_POINT('Ctrl Pts',(119.53117715119,5.87903383235464,130.119050428141));
#145025=CARTESIAN_POINT('Ctrl Pts',(119.523753780161,5.85873685775066,129.963071622861));
#145026=CARTESIAN_POINT('Ctrl Pts',(119.516330409133,5.83231605305868,129.808358599629));
#145027=CARTESIAN_POINT('Ctrl Pts',(119.512394359692,5.81830710845317,129.726326042428));
#145028=CARTESIAN_POINT('Ctrl Pts',(119.508458310251,5.80257737752639,129.64464911833));
#145029=CARTESIAN_POINT('Ctrl Pts',(119.504522260811,5.78514980617318,129.563404420662));
#145030=CARTESIAN_POINT('Ctrl Pts',(119.497098994405,5.75228195049539,129.410179456414));
#145031=CARTESIAN_POINT('Ctrl Pts',(119.489675728,5.71327273597372,129.258029502933));
#145032=CARTESIAN_POINT('Ctrl Pts',(119.482252461594,5.66820469385868,129.107485221133));
#145033=CARTESIAN_POINT('Ctrl Pts',(119.474837968873,5.62318991842674,128.957118870173));
#145034=CARTESIAN_POINT('Ctrl Pts',(119.467423476152,5.57213067548659,128.808354767496));
#145035=CARTESIAN_POINT('Ctrl Pts',(119.460008983431,5.51516062357471,128.661714156138));
#145036=CARTESIAN_POINT('Ctrl Pts',(119.452601637078,5.45824548154374,128.515214882522));
#145037=CARTESIAN_POINT('Ctrl Pts',(119.445194290724,5.39543100654209,128.370835371273));
#145038=CARTESIAN_POINT('Ctrl Pts',(119.43778694437,5.3269008209133,128.229082340049));
#145039=CARTESIAN_POINT('Ctrl Pts',(119.430385122695,5.25842174768234,128.087435033583));
#145040=CARTESIAN_POINT('Ctrl Pts',(119.422983301019,5.18423561379725,127.94841064129));
#145041=CARTESIAN_POINT('Ctrl Pts',(119.415581479344,5.10457432384171,127.812496393562));
#145042=CARTESIAN_POINT('Ctrl Pts',(119.408183565033,5.02495508646112,127.676653893907));
#145043=CARTESIAN_POINT('Ctrl Pts',(119.400785650721,4.93986663744964,127.543918590292));
#145044=CARTESIAN_POINT('Ctrl Pts',(119.39338773641,4.84958698191946,127.414753462261));
#145045=CARTESIAN_POINT('Ctrl Pts',(119.385991051498,4.75932232923027,127.28560979913));
#145046=CARTESIAN_POINT('Ctrl Pts',(119.378594366585,4.66386839584224,127.160035439731));
#145047=CARTESIAN_POINT('Ctrl Pts',(119.371197681673,4.56354677054439,127.038464783166));
#145048=CARTESIAN_POINT('Ctrl Pts',(119.363801324738,4.46322959361246,126.916899517171));
#145049=CARTESIAN_POINT('Ctrl Pts',(119.356404967802,4.35804539152727,126.799337888946));
#145050=CARTESIAN_POINT('Ctrl Pts',(119.349008610867,4.24835616332295,126.686181350942));
#145051=CARTESIAN_POINT('Ctrl Pts',(119.34161112153,4.13865014141778,126.573007488382));
#145052=CARTESIAN_POINT('Ctrl Pts',(119.334213632194,4.02443797988699,126.464240326978));
#145053=CARTESIAN_POINT('Ctrl Pts',(119.326816142857,3.90611854984878,126.360244458302));
#145054=CARTESIAN_POINT('Ctrl Pts',(119.319416060342,3.78775764311796,126.256212134036));
#145055=CARTESIAN_POINT('Ctrl Pts',(119.312015977827,3.66528688146725,126.156954678861));
#145056=CARTESIAN_POINT('Ctrl Pts',(119.304615895312,3.53913808269339,126.062796298259));
#145057=CARTESIAN_POINT('Ctrl Pts',(119.297207675646,3.4128505703467,125.968534380837));
#145058=CARTESIAN_POINT('Ctrl Pts',(119.289799455979,3.2828772433216,125.879382958877));
#145059=CARTESIAN_POINT('Ctrl Pts',(119.282391236313,3.14967936560169,125.795623206162));
#145060=CARTESIAN_POINT('Ctrl Pts',(119.274978457011,3.01639950681047,125.711811900716));
#145061=CARTESIAN_POINT('Ctrl Pts',(119.267565677709,2.87989146559127,125.633399062513));
#145062=CARTESIAN_POINT('Ctrl Pts',(119.260152898407,2.74064047618298,125.560619553897));
#145063=CARTESIAN_POINT('Ctrl Pts',(119.252729527378,2.60119051843079,125.487736054507));
#145064=CARTESIAN_POINT('Ctrl Pts',(119.245306156349,2.45899012144547,125.420502119833));
#145065=CARTESIAN_POINT('Ctrl Pts',(119.23788278532,2.31454458300072,125.359104522964));
#145066=CARTESIAN_POINT('Ctrl Pts',(119.233946735879,2.2379560925923,125.326550043888));
#145067=CARTESIAN_POINT('Ctrl Pts',(119.230010686439,2.16073667934626,125.295635539458));
#145068=CARTESIAN_POINT('Ctrl Pts',(119.226074636998,2.08296318621513,125.266383105209));
#145069=CARTESIAN_POINT('Ctrl Pts',(119.218651370592,1.93628480540107,125.211213927153));
#145070=CARTESIAN_POINT('Ctrl Pts',(119.211228104187,1.78719130712475,125.161792717803));
#145071=CARTESIAN_POINT('Ctrl Pts',(119.203804837781,1.63617376159973,125.118336876466));
#145072=CARTESIAN_POINT('Ctrl Pts',(119.19639034506,1.48533470627207,125.074932396325));
#145073=CARTESIAN_POINT('Ctrl Pts',(119.188975852339,1.33257648547059,125.037479352221));
#145074=CARTESIAN_POINT('Ctrl Pts',(119.181561359618,1.17840988142788,125.006147038035));
#145075=CARTESIAN_POINT('Ctrl Pts',(119.174154013265,1.02439186896254,124.974844923114));
#145076=CARTESIAN_POINT('Ctrl Pts',(119.166746666911,0.868968539040656,
124.949651867435));
#145077=CARTESIAN_POINT('Ctrl Pts',(119.159339320557,0.712665459942137,
124.930687277593));
#145078=CARTESIAN_POINT('Ctrl Pts',(119.151937498882,0.556478957576876,
124.911736832258));
#145079=CARTESIAN_POINT('Ctrl Pts',(119.144535677206,0.399414381503607,
124.899005647863));
#145080=CARTESIAN_POINT('Ctrl Pts',(119.137133855531,0.242007002542,124.89256197644));
#145081=CARTESIAN_POINT('Ctrl Pts',(119.129735941219,0.0846827177107159,
124.886121706581));
#145082=CARTESIAN_POINT('Ctrl Pts',(119.122338026908,-0.072983637571102,
124.885962354721));
#145083=CARTESIAN_POINT('Ctrl Pts',(119.114940112597,-0.230452276947585,
124.892100279036));
#145084=CARTESIAN_POINT('Ctrl Pts',(119.107543427685,-0.387894747893087,
124.89823718334));
#145085=CARTESIAN_POINT('Ctrl Pts',(119.100146742772,-0.545139195494856,
124.910669272316));
#145086=CARTESIAN_POINT('Ctrl Pts',(119.09275005786,-0.701646320888489,
124.929360787533));
#145087=CARTESIAN_POINT('Ctrl Pts',(119.085353700925,-0.858146506592173,
124.948051473949));
#145088=CARTESIAN_POINT('Ctrl Pts',(119.077957343989,-1.01390906443024,
124.973000990477));
#145089=CARTESIAN_POINT('Ctrl Pts',(119.070560987054,-1.16840057176563,
125.004121771932));
#145090=CARTESIAN_POINT('Ctrl Pts',(119.063163497717,-1.32291573214497,
125.035247318059));
#145091=CARTESIAN_POINT('Ctrl Pts',(119.055766008381,-1.47615908857449,
125.072545936687));
#145092=CARTESIAN_POINT('Ctrl Pts',(119.048368519044,-1.62760830025584,
125.115879116898));
#145093=CARTESIAN_POINT('Ctrl Pts',(119.040968436529,-1.77911060222412,
125.159227487489));
#145094=CARTESIAN_POINT('Ctrl Pts',(119.033568354014,-1.92881714856776,
125.208614528798));
#145095=CARTESIAN_POINT('Ctrl Pts',(119.026168271499,-2.07622176796565,
125.263852181265));
#145096=CARTESIAN_POINT('Ctrl Pts',(119.018760051833,-2.22378847389583,
125.319150573209));
#145097=CARTESIAN_POINT('Ctrl Pts',(119.011351832166,-2.36904784812238,
125.380312293057));
#145098=CARTESIAN_POINT('Ctrl Pts',(119.0039436125,-2.51151400672803,125.447101247654));
#145099=CARTESIAN_POINT('Ctrl Pts',(118.996530833198,-2.65406785087714,
125.513931309738));
#145100=CARTESIAN_POINT('Ctrl Pts',(118.989118053896,-2.79382472309748,
125.586395336536));
#145101=CARTESIAN_POINT('Ctrl Pts',(118.981705274593,-2.93032474608807,
125.664212035573));
#145102=CARTESIAN_POINT('Ctrl Pts',(118.974281903565,-3.06701980671292,
125.742139922759));
#145103=CARTESIAN_POINT('Ctrl Pts',(118.966858532536,-3.20044840812621,
125.825435560096));
#145104=CARTESIAN_POINT('Ctrl Pts',(118.959435161507,-3.33018028705042,
125.913774781673));
#145105=CARTESIAN_POINT('Ctrl Pts',(118.955499112066,-3.39896724213075,
125.960614356624));
#145106=CARTESIAN_POINT('Ctrl Pts',(118.951563062626,-3.46671546929933,
126.008871191182));
#145107=CARTESIAN_POINT('Ctrl Pts',(118.947627013185,-3.53336484346536,
126.05849257837));
#145108=CARTESIAN_POINT('Ctrl Pts',(118.940276572164,-3.65783032623298,
126.151158863527));
#145109=CARTESIAN_POINT('Ctrl Pts',(118.932926131144,-3.77885418607313,
126.248878586329));
#145110=CARTESIAN_POINT('Ctrl Pts',(118.925575690124,-3.89599287290778,
126.351364985775));
#145111=CARTESIAN_POINT('Ctrl Pts',(118.918233970298,-4.01299257634084,
126.453729786551));
#145112=CARTESIAN_POINT('Ctrl Pts',(118.910892250472,-4.12611599515914,
126.560849761971));
#145113=CARTESIAN_POINT('Ctrl Pts',(118.903550530647,-4.23494899655388,
126.672395279003));
#145114=CARTESIAN_POINT('Ctrl Pts',(118.896215841812,-4.34367777115461,
126.783833971529));
#145115=CARTESIAN_POINT('Ctrl Pts',(118.888881152978,-4.44812404099511,
126.899689499942));
#145116=CARTESIAN_POINT('Ctrl Pts',(118.881546464144,-4.54790736508967,
127.019592571693));
#145117=CARTESIAN_POINT('Ctrl Pts',(118.874217122619,-4.64761794278351,
127.139408228868));
#145118=CARTESIAN_POINT('Ctrl Pts',(118.866887781093,-4.74267209858175,
127.263265263788));
#145119=CARTESIAN_POINT('Ctrl Pts',(118.859558439568,-4.83272699882416,
127.390758368133));
#145120=CARTESIAN_POINT('Ctrl Pts',(118.852232235997,-4.92274334332396,
127.518196888093));
#145121=CARTESIAN_POINT('Ctrl Pts',(118.844906032426,-5.00776447083573,
127.649268069622));
#145122=CARTESIAN_POINT('Ctrl Pts',(118.837579828855,-5.08748860375037,
127.783534527039));
#145123=CARTESIAN_POINT('Ctrl Pts',(118.830255153022,-5.16719611173853,
127.917772985782));
#145124=CARTESIAN_POINT('Ctrl Pts',(118.82293047719,-5.24160862790158,128.05520506719));
#145125=CARTESIAN_POINT('Ctrl Pts',(118.815605801357,-5.31046853091582,
128.195365687588));
#145126=CARTESIAN_POINT('Ctrl Pts',(118.808281137258,-5.37932832362041,
128.335526083456));
#145127=CARTESIAN_POINT('Ctrl Pts',(118.800956473159,-5.44263535269792,
128.478414667306));
#145128=CARTESIAN_POINT('Ctrl Pts',(118.79363180906,-5.50017878311434,128.623543358766));
#145129=CARTESIAN_POINT('Ctrl Pts',(118.786305640915,-5.5577340294947,128.768701850942));
#145130=CARTESIAN_POINT('Ctrl Pts',(118.77897947277,-5.60952318185033,128.916101011511));
#145131=CARTESIAN_POINT('Ctrl Pts',(118.771653304625,-5.65538430752652,
129.065234717384));
#145132=CARTESIAN_POINT('Ctrl Pts',(118.764320097234,-5.70128949822011,
129.214511716281));
#145133=CARTESIAN_POINT('Ctrl Pts',(118.756986889844,-5.74125517395969,
129.365526224171));
#145134=CARTESIAN_POINT('Ctrl Pts',(118.749653682453,-5.7751697130392,129.517758368192));
#145135=CARTESIAN_POINT('Ctrl Pts',(118.742316774607,-5.80910136594485,
129.67006733102));
#145136=CARTESIAN_POINT('Ctrl Pts',(118.734979866761,-5.8369757312481,129.82359477925));
#145137=CARTESIAN_POINT('Ctrl Pts',(118.727642958916,-5.85873282046703,
129.9778134012));
#145138=CARTESIAN_POINT('Ctrl Pts',(118.720295637506,-5.88052079038378,
130.132250911744));
#145139=CARTESIAN_POINT('Ctrl Pts',(118.712948316096,-5.89617410202407,
130.287381176658));
#145140=CARTESIAN_POINT('Ctrl Pts',(118.705600994687,-5.90568481511976,
130.442673699135));
#145141=CARTESIAN_POINT('Ctrl Pts',(118.699859060528,-5.91311744061035,
130.564034857805));
#145142=CARTESIAN_POINT('Ctrl Pts',(118.69411712637,-5.91679956894418,130.685495037937));
#145143=CARTESIAN_POINT('Ctrl Pts',(118.688375192211,-5.9167494959397,130.806802911017));
#145144=CARTESIAN_POINT('',(116.938375192211,-5.91775807691223,130.798956223901));
#145145=CARTESIAN_POINT('Ctrl Pts',(118.688375192211,-5.92531066698449,
130.806806444865));
#145146=CARTESIAN_POINT('Ctrl Pts',(118.681976591265,-5.92601627665423,
130.942183404842));
#145147=CARTESIAN_POINT('Ctrl Pts',(118.675577990318,-5.92178053373525,
131.077515423935));
#145148=CARTESIAN_POINT('Ctrl Pts',(118.576363514767,-5.7773031608978,133.170487024815));
#145149=CARTESIAN_POINT('Ctrl Pts',(118.390731765559,-3.36834491582461,
136.938838024679));
#145150=CARTESIAN_POINT('Ctrl Pts',(118.112284141745,3.34043687663362,136.95407947322));
#145151=CARTESIAN_POINT('Ctrl Pts',(117.833836517933,6.9795203688748,131.318029723882));
#145152=CARTESIAN_POINT('Ctrl Pts',(117.55538889412,4.20476561065067,125.209943159972));
#145153=CARTESIAN_POINT('Ctrl Pts',(117.276941270308,-2.43396332954512,
124.242852937102));
#145154=CARTESIAN_POINT('Ctrl Pts',(117.071270036338,-5.68546201478638,
127.982278744742));
#145155=CARTESIAN_POINT('Ctrl Pts',(116.958414676972,-5.92171512746286,
130.37356612518));
#145156=CARTESIAN_POINT('Ctrl Pts',(116.938375192211,-5.91775807691223,
130.798956223901));
#145157=CARTESIAN_POINT('',(115.188375192211,-5.90693479489549,130.80438521844));
#145158=CARTESIAN_POINT('Ctrl Pts',(116.938375192211,-5.91775807691223,
130.798956223901));
#145159=CARTESIAN_POINT('Ctrl Pts',(116.865598802368,-5.90338745526516,
132.343824070018));
#145160=CARTESIAN_POINT('Ctrl Pts',(116.700006537921,-4.49301687389813,
135.882186555631));
#145161=CARTESIAN_POINT('Ctrl Pts',(116.441598398868,1.4782284268974,137.64485776677));
#145162=CARTESIAN_POINT('Ctrl Pts',(116.163150775056,6.55412255704564,133.258140973988));
#145163=CARTESIAN_POINT('Ctrl Pts',(115.884703151243,5.60709824395641,126.616519907489));
#145164=CARTESIAN_POINT('Ctrl Pts',(115.60625552743,-0.492575433349502,
123.823319866161));
#145165=CARTESIAN_POINT('Ctrl Pts',(115.374146207752,-5.19983838450488,
126.842588456896));
#145166=CARTESIAN_POINT('Ctrl Pts',(115.23485276268,-5.90689819190348,129.813205798887));
#145167=CARTESIAN_POINT('Ctrl Pts',(115.188375192211,-5.90693479489549,
130.80438521844));
#145168=CARTESIAN_POINT('',(113.438375192211,-5.91784867649587,130.809756633416));
#145169=CARTESIAN_POINT('Ctrl Pts',(115.188375192211,-5.90693479489549,
130.80438521844));
#145170=CARTESIAN_POINT('Ctrl Pts',(115.142036888076,-5.90697128820956,
131.79259464792));
#145171=CARTESIAN_POINT('Ctrl Pts',(115.002882709335,-5.20295378394123,
134.760144048991));
#145172=CARTESIAN_POINT('Ctrl Pts',(114.770912655992,-0.503046869620426,
137.78465462121));
#145173=CARTESIAN_POINT('Ctrl Pts',(114.492465032178,5.60080991683228,135.000607608133));
#145174=CARTESIAN_POINT('Ctrl Pts',(114.214017408366,6.55779600449193,128.360414608787));
#145175=CARTESIAN_POINT('Ctrl Pts',(113.935569784553,1.48848793016878,123.96608859811));
#145176=CARTESIAN_POINT('Ctrl Pts',(113.677022379168,-4.48861432852338,
125.720745735417));
#145177=CARTESIAN_POINT('Ctrl Pts',(113.511290848388,-5.90345104083902,
129.261993258066));
#145178=CARTESIAN_POINT('Ctrl Pts',(113.438375192211,-5.91784867649587,
130.809756633416));
#145179=CARTESIAN_POINT('',(111.688375192211,-5.92147968542167,130.801867673062));
#145180=CARTESIAN_POINT('Ctrl Pts',(113.438375192211,-5.91784867649587,
130.809756633416));
#145181=CARTESIAN_POINT('Ctrl Pts',(113.418474973783,-5.92177809453099,
131.232173859838));
#145182=CARTESIAN_POINT('Ctrl Pts',(113.305758880752,-5.68749102524069,
133.620446152917));
#145183=CARTESIAN_POINT('Ctrl Pts',(113.100226913113,-2.44380325616413,
137.36220982104));
#145184=CARTESIAN_POINT('Ctrl Pts',(112.821779289301,4.19636890965415,136.40507918793));
#145185=CARTESIAN_POINT('Ctrl Pts',(112.543331665489,6.98028305151762,130.30116179897));
#145186=CARTESIAN_POINT('Ctrl Pts',(112.264884041676,3.34965807482215,124.65965954167));
#145187=CARTESIAN_POINT('Ctrl Pts',(111.986436417863,-3.35913903274104,
124.664837387781));
#145188=CARTESIAN_POINT('Ctrl Pts',(111.794266801375,-5.85878875116337,
128.562162782962));
#145189=CARTESIAN_POINT('Ctrl Pts',(111.694913059491,-5.92599367912675,
130.663539518991));
#145190=CARTESIAN_POINT('Ctrl Pts',(111.688375192211,-5.92526049744177,
130.801866081339));
#145191=CARTESIAN_POINT('',(109.938375221708,-5.91299038747931,130.800172818778));
#145192=CARTESIAN_POINT('Ctrl Pts',(111.688375192211,-5.91674947565407,
130.801869664481));
#145193=CARTESIAN_POINT('Ctrl Pts',(111.681028256843,-5.91681482372276,
130.957090633337));
#145194=CARTESIAN_POINT('Ctrl Pts',(111.673681321476,-5.91076783778976,
131.112561170285));
#145195=CARTESIAN_POINT('Ctrl Pts',(111.666334386108,-5.89857585866385,
131.267753973246));
#145196=CARTESIAN_POINT('Ctrl Pts',(111.658995738555,-5.88639763287252,
131.422771708769));
#145197=CARTESIAN_POINT('Ctrl Pts',(111.651657091002,-5.86808823697625,
131.577511957074));
#145198=CARTESIAN_POINT('Ctrl Pts',(111.644318443448,-5.8436669866875,131.731445679035));
#145199=CARTESIAN_POINT('Ctrl Pts',(111.636986394494,-5.81926769494539,
131.885240990358));
#145200=CARTESIAN_POINT('Ctrl Pts',(111.62965434554,-5.78876754528707,132.038230844198));
#145201=CARTESIAN_POINT('Ctrl Pts',(111.622322296585,-5.75223777418,132.189889813143));
#145202=CARTESIAN_POINT('Ctrl Pts',(111.614995163127,-5.71573249308259,
132.341447108042));
#145203=CARTESIAN_POINT('Ctrl Pts',(111.607668029669,-5.6732057261156,132.491674924627));
#145204=CARTESIAN_POINT('Ctrl Pts',(111.600340896211,-5.62478001587141,
132.640056762235));
#145205=CARTESIAN_POINT('Ctrl Pts',(111.59301624978,-5.57637074262402,132.788388235031));
#145206=CARTESIAN_POINT('Ctrl Pts',(111.585691603349,-5.52206662529805,
132.934874612607));
#145207=CARTESIAN_POINT('Ctrl Pts',(111.578366956918,-5.46204039978975,
133.079013389653));
#145208=CARTESIAN_POINT('Ctrl Pts',(111.571043435937,-5.40202339745138,
133.223130019439));
#145209=CARTESIAN_POINT('Ctrl Pts',(111.563719914955,-5.3362861823376,133.364899414094));
#145210=CARTESIAN_POINT('Ctrl Pts',(111.556396393973,-5.26504997945334,
133.503838210797));
#145211=CARTESIAN_POINT('Ctrl Pts',(111.549072481829,-5.19380997170936,
133.642784428484));
#145212=CARTESIAN_POINT('Ctrl Pts',(111.541748569684,-5.11707056565635,
133.778899407751));
#145213=CARTESIAN_POINT('Ctrl Pts',(111.534424657539,-5.03509924458978,
133.911723834126));
#145214=CARTESIAN_POINT('Ctrl Pts',(111.52709883756,-4.95310657048997,134.044582860461));
#145215=CARTESIAN_POINT('Ctrl Pts',(111.51977301758,-4.86587946962067,134.174149303627));
#145216=CARTESIAN_POINT('Ctrl Pts',(111.5124471976,-4.77372894444798,134.299992538613));
#145217=CARTESIAN_POINT('Ctrl Pts',(111.505113740359,-4.68148235115796,
134.425966966802));
#145218=CARTESIAN_POINT('Ctrl Pts',(111.497780283117,-4.58430230842726,
134.548210126812));
#145219=CARTESIAN_POINT('Ctrl Pts',(111.490446825875,-4.48254073891411,
134.666323730605));
#145220=CARTESIAN_POINT('Ctrl Pts',(111.483109318504,-4.38072296842701,
134.784502566289));
#145221=CARTESIAN_POINT('Ctrl Pts',(111.475771811134,-4.27431889094365,
134.898547024507));
#145222=CARTESIAN_POINT('Ctrl Pts',(111.468434303764,-4.16371701420639,
135.008096002686));
#145223=CARTESIAN_POINT('Ctrl Pts',(111.46108589296,-4.05295078462652,135.117807769115));
#145224=CARTESIAN_POINT('Ctrl Pts',(111.453737482156,-3.93797457691017,
135.223010454999));
#145225=CARTESIAN_POINT('Ctrl Pts',(111.446389071352,-3.81921032087068,
135.323382977264));
#145226=CARTESIAN_POINT('Ctrl Pts',(111.440773104314,-3.72844564194221,
135.40009191361));
#145227=CARTESIAN_POINT('Ctrl Pts',(111.435157137275,-3.63546917588325,
135.473980540481));
#145228=CARTESIAN_POINT('Ctrl Pts',(111.429541170237,-3.54047996203196,
135.544923052652));
#145229=CARTESIAN_POINT('Ctrl Pts',(111.422117903832,-3.41492184617205,
135.638695890656));
#145230=CARTESIAN_POINT('Ctrl Pts',(111.414694637426,-3.28544581013673,
135.727618796898));
#145231=CARTESIAN_POINT('Ctrl Pts',(111.407271371021,-3.15246312477616,
135.811346418367));
#145232=CARTESIAN_POINT('Ctrl Pts',(111.3998568783,-3.01963761390607,135.894975080742));
#145233=CARTESIAN_POINT('Ctrl Pts',(111.392442385579,-2.88331401631127,
135.973420483882));
#145234=CARTESIAN_POINT('Ctrl Pts',(111.385027892858,-2.74393591172043,
136.046378003542));
#145235=CARTESIAN_POINT('Ctrl Pts',(111.377620546504,-2.60469214499458,
136.119265203997));
#145236=CARTESIAN_POINT('Ctrl Pts',(111.37021320015,-2.46240006080196,136.186674879226));
#145237=CARTESIAN_POINT('Ctrl Pts',(111.362805853797,-2.31753131135518,
136.248346214846));
#145238=CARTESIAN_POINT('Ctrl Pts',(111.355404032121,-2.1727706104869,136.309971553657));
#145239=CARTESIAN_POINT('Ctrl Pts',(111.348002210446,-2.02543741286825,
136.365866929071));
#145240=CARTESIAN_POINT('Ctrl Pts',(111.34060038877,-1.87602691241399,136.415817967168));
#145241=CARTESIAN_POINT('Ctrl Pts',(111.333202474459,-1.72669528459959,
136.465742636501));
#145242=CARTESIAN_POINT('Ctrl Pts',(111.325804560148,-1.57528889100536,
136.509729099871));
#145243=CARTESIAN_POINT('Ctrl Pts',(111.318406645836,-1.42232169026551,
136.54761157603));
#145244=CARTESIAN_POINT('Ctrl Pts',(111.311009960924,-1.26937990989975,
136.585487756809));
#145245=CARTESIAN_POINT('Ctrl Pts',(111.303613276012,-1.11487819917337,
136.617261873957));
#145246=CARTESIAN_POINT('Ctrl Pts',(111.296216591099,-0.959344537573924,
136.642818343775));
#145247=CARTESIAN_POINT('Ctrl Pts',(111.288820234164,-0.803817772499801,
136.668373680392));
#145248=CARTESIAN_POINT('Ctrl Pts',(111.281423877228,-0.647259515892521,
136.687711857333));
#145249=CARTESIAN_POINT('Ctrl Pts',(111.274027520293,-0.490206505653107,
136.700768688953));
#145250=CARTESIAN_POINT('Ctrl Pts',(111.266630030956,-0.333129450197,136.713827519607));
#145251=CARTESIAN_POINT('Ctrl Pts',(111.25923254162,-0.175557862322717,
136.720603059159));
#145252=CARTESIAN_POINT('Ctrl Pts',(111.251835052283,-0.0180319985780747,
136.721083140173));
#145253=CARTESIAN_POINT('Ctrl Pts',(111.244434969768,0.139549085614132,
136.721563389479));
#145254=CARTESIAN_POINT('Ctrl Pts',(111.237034887253,0.297084040700731,
136.715743785263));
#145255=CARTESIAN_POINT('Ctrl Pts',(111.229634804738,0.454034366966793,
136.703664250717));
#145256=CARTESIAN_POINT('Ctrl Pts',(111.222226585072,0.611157276251357,
136.691571433482));
#145257=CARTESIAN_POINT('Ctrl Pts',(111.214818365405,0.767693900457209,
136.673204967905));
#145258=CARTESIAN_POINT('Ctrl Pts',(111.207410145739,0.923111873492083,
136.648656557328));
#145259=CARTESIAN_POINT('Ctrl Pts',(111.199997366436,1.07862550369607,136.624093037614));
#145260=CARTESIAN_POINT('Ctrl Pts',(111.192584587134,1.23301874552727,136.593340063945));
#145261=CARTESIAN_POINT('Ctrl Pts',(111.185171807832,1.38577164822839,136.556539987289));
#145262=CARTESIAN_POINT('Ctrl Pts',(111.177748436803,1.53874281144028,136.519687328957));
#145263=CARTESIAN_POINT('Ctrl Pts',(111.170325065775,1.69006859625799,136.476770412435));
#145264=CARTESIAN_POINT('Ctrl Pts',(111.162901694746,1.8392455790784,136.427981005034));
#145265=CARTESIAN_POINT('Ctrl Pts',(111.158965645305,1.91834279482255,136.402111690544));
#145266=CARTESIAN_POINT('Ctrl Pts',(111.155029595864,1.99683624975567,136.37459220838));
#145267=CARTESIAN_POINT('Ctrl Pts',(111.151093546423,2.07465353583313,136.345456472066));
#145268=CARTESIAN_POINT('Ctrl Pts',(111.143670280018,2.2214145087805,136.290507382672));
#145269=CARTESIAN_POINT('Ctrl Pts',(111.136247013613,2.36621282833455,136.22964052949));
#145270=CARTESIAN_POINT('Ctrl Pts',(111.128823747207,2.50853563728656,136.163015254596));
#145271=CARTESIAN_POINT('Ctrl Pts',(111.121409254486,2.65069023249767,136.096468725244));
#145272=CARTESIAN_POINT('Ctrl Pts',(111.113994761765,2.79037480623799,136.024177478235));
#145273=CARTESIAN_POINT('Ctrl Pts',(111.106580269044,2.92709330382308,135.946350052912));
#145274=CARTESIAN_POINT('Ctrl Pts',(111.09917292269,3.06368002697254,135.868597640592));
#145275=CARTESIAN_POINT('Ctrl Pts',(111.091765576337,3.19730604306728,135.785319856274));
#145276=CARTESIAN_POINT('Ctrl Pts',(111.084358229983,3.32749698203934,135.696772537777));
#145277=CARTESIAN_POINT('Ctrl Pts',(111.076956408307,3.45759081969766,135.60829126121));
#145278=CARTESIAN_POINT('Ctrl Pts',(111.069554586632,3.58425437419898,135.514548485092));
#145279=CARTESIAN_POINT('Ctrl Pts',(111.062152764957,3.70703962228686,135.415844955748));
#145280=CARTESIAN_POINT('Ctrl Pts',(111.054754850645,3.82976005299812,135.317193531228));
#145281=CARTESIAN_POINT('Ctrl Pts',(111.047356936334,3.9486059644373,135.213586802126));
#145282=CARTESIAN_POINT('Ctrl Pts',(111.039959022022,4.0631600729491,135.105367567583));
#145283=CARTESIAN_POINT('Ctrl Pts',(111.03256233711,4.1776951446462,134.997166317113));
#145284=CARTESIAN_POINT('Ctrl Pts',(111.025165652198,4.28793955785393,134.884354338607));
#145285=CARTESIAN_POINT('Ctrl Pts',(111.017768967286,4.39351068292429,134.767313360349));
#145286=CARTESIAN_POINT('Ctrl Pts',(111.01037261035,4.4990771268601,134.650277571811));
#145287=CARTESIAN_POINT('Ctrl Pts',(111.002976253415,4.59997044464968,134.529013433565));
#145288=CARTESIAN_POINT('Ctrl Pts',(110.99557989648,4.69584651514763,134.4039378245));
#145289=CARTESIAN_POINT('Ctrl Pts',(110.988182407143,4.79173726451681,134.278843066039));
#145290=CARTESIAN_POINT('Ctrl Pts',(110.980784917806,4.88260900998074,134.149935971131));
#145291=CARTESIAN_POINT('Ctrl Pts',(110.97338742847,4.96815949287188,134.017664496113));
#145292=CARTESIAN_POINT('Ctrl Pts',(110.965987345955,5.05373996535192,133.885346653536));
#145293=CARTESIAN_POINT('Ctrl Pts',(110.95858726344,5.13399525873404,133.749662395969));
#145294=CARTESIAN_POINT('Ctrl Pts',(110.951187180925,5.20866788928199,133.611086357937));
#145295=CARTESIAN_POINT('Ctrl Pts',(110.943778961259,5.28342263006397,133.472357941305));
#145296=CARTESIAN_POINT('Ctrl Pts',(110.936370741592,5.35258227141165,133.330731722743));
#145297=CARTESIAN_POINT('Ctrl Pts',(110.928962521926,5.41593620906649,133.186705164818));
#145298=CARTESIAN_POINT('Ctrl Pts',(110.921549742624,5.47932914001303,133.04258996095));
#145299=CARTESIAN_POINT('Ctrl Pts',(110.914136963322,5.5369091107708,132.896071820502));
#145300=CARTESIAN_POINT('Ctrl Pts',(110.906724184019,5.5885148391545,132.747665136948));
#145301=CARTESIAN_POINT('Ctrl Pts',(110.899300812991,5.64019430422286,132.599046402965));
#145302=CARTESIAN_POINT('Ctrl Pts',(110.891877441962,5.68588236991391,132.448534092744));
#145303=CARTESIAN_POINT('Ctrl Pts',(110.884454070933,5.72546826274446,132.296655405738));
#145304=CARTESIAN_POINT('Ctrl Pts',(110.880518021492,5.74645765297392,132.216125681608));
#145305=CARTESIAN_POINT('Ctrl Pts',(110.876581972052,5.76573236293829,132.135211962611));
#145306=CARTESIAN_POINT('Ctrl Pts',(110.872645922611,5.78328178672794,132.053993498776));
#145307=CARTESIAN_POINT('Ctrl Pts',(110.865222656205,5.81637945229606,131.900818010725));
#145308=CARTESIAN_POINT('Ctrl Pts',(110.8577993898,5.84343747348966,131.746095062683));
#145309=CARTESIAN_POINT('Ctrl Pts',(110.850376123395,5.86431269746181,131.590342264227));
#145310=CARTESIAN_POINT('Ctrl Pts',(110.842961630674,5.88516324865282,131.434773552645));
#145311=CARTESIAN_POINT('Ctrl Pts',(110.835547137953,5.89984549924196,131.278177779864));
#145312=CARTESIAN_POINT('Ctrl Pts',(110.828132645232,5.90826676961038,131.12108501135));
#145313=CARTESIAN_POINT('Ctrl Pts',(110.820725298878,5.91667992324135,130.96414365476));
#145314=CARTESIAN_POINT('Ctrl Pts',(110.813317952524,5.91884409044083,130.806706626337));
#145315=CARTESIAN_POINT('Ctrl Pts',(110.80591060617,5.91471810620367,130.649311313645));
#145316=CARTESIAN_POINT('Ctrl Pts',(110.798508784495,5.91059519928123,130.492033392315));
#145317=CARTESIAN_POINT('Ctrl Pts',(110.791106962819,5.90019149193709,130.334797496329));
#145318=CARTESIAN_POINT('Ctrl Pts',(110.783705141144,5.88351784305867,130.178143121076));
#145319=CARTESIAN_POINT('Ctrl Pts',(110.776307226833,5.86685299606959,130.021571442447));
#145320=CARTESIAN_POINT('Ctrl Pts',(110.768909312521,5.84392483868674,129.865581043447));
#145321=CARTESIAN_POINT('Ctrl Pts',(110.76151139821,5.81479622552752,129.710708287943));
#145322=CARTESIAN_POINT('Ctrl Pts',(110.754114713298,5.78567245301547,129.555861269481));
#145323=CARTESIAN_POINT('Ctrl Pts',(110.746718028385,5.75035033870547,129.402131892397));
#145324=CARTESIAN_POINT('Ctrl Pts',(110.739321343473,5.7089442207431,129.250048407312));
#145325=CARTESIAN_POINT('Ctrl Pts',(110.731924986538,5.66753993877138,129.097971665769));
#145326=CARTESIAN_POINT('Ctrl Pts',(110.724528629602,5.62005228760751,128.947541031302));
#145327=CARTESIAN_POINT('Ctrl Pts',(110.717132272667,5.56664599338309,128.799271355999));
#145328=CARTESIAN_POINT('Ctrl Pts',(110.70973478333,5.51323152251866,128.65097898023));
#145329=CARTESIAN_POINT('Ctrl Pts',(110.702337293994,5.4538967308225,128.504848573621));
#145330=CARTESIAN_POINT('Ctrl Pts',(110.694939804657,5.38885511845664,128.361376566291));
#145331=CARTESIAN_POINT('Ctrl Pts',(110.687539722142,5.32379070585452,128.217854265072));
#145332=CARTESIAN_POINT('Ctrl Pts',(110.680139639627,5.25301564360368,128.076992558315));
#145333=CARTESIAN_POINT('Ctrl Pts',(110.672739557112,5.17679007892136,127.939264625931));
#145334=CARTESIAN_POINT('Ctrl Pts',(110.665331337446,5.10048069639449,127.801385247528));
#145335=CARTESIAN_POINT('Ctrl Pts',(110.657923117779,5.01870902312205,127.666646852014));
#145336=CARTESIAN_POINT('Ctrl Pts',(110.650514898113,4.93177975170426,127.535495517385));
#145337=CARTESIAN_POINT('Ctrl Pts',(110.643102118811,4.84479697677027,127.404263461299));
#145338=CARTESIAN_POINT('Ctrl Pts',(110.635689339509,4.75265049626616,127.276623167334));
#145339=CARTESIAN_POINT('Ctrl Pts',(110.628276560207,4.65568590702782,127.152988368999));
#145340=CARTESIAN_POINT('Ctrl Pts',(110.620853189178,4.55858277023719,127.029176915467));
#145341=CARTESIAN_POINT('Ctrl Pts',(110.613429818149,4.4566480164177,126.909382671706));
#145342=CARTESIAN_POINT('Ctrl Pts',(110.60600644712,4.35026531762562,126.793983798767));
#145343=CARTESIAN_POINT('Ctrl Pts',(110.602070397679,4.29385865810708,126.732796547375));
#145344=CARTESIAN_POINT('Ctrl Pts',(110.598134348239,4.23620210626621,126.672844346448));
#145345=CARTESIAN_POINT('Ctrl Pts',(110.594198298798,4.1773566046412,126.614178955614));
#145346=CARTESIAN_POINT('Ctrl Pts',(110.586775032392,4.0663758250838,126.503537859386));
#145347=CARTESIAN_POINT('Ctrl Pts',(110.579351765987,3.9508285482978,126.397141647097));
#145348=CARTESIAN_POINT('Ctrl Pts',(110.571928499581,3.831072876271,126.295390537914));
#145349=CARTESIAN_POINT('Ctrl Pts',(110.56451400686,3.71145874550318,126.193759690091));
#145350=CARTESIAN_POINT('Ctrl Pts',(110.557099514139,3.58764640191728,126.096763256595));
#145351=CARTESIAN_POINT('Ctrl Pts',(110.549685021418,3.46003170900208,126.004765724744));
#145352=CARTESIAN_POINT('Ctrl Pts',(110.542277675064,3.33254001593298,125.912856863579));
#145353=CARTESIAN_POINT('Ctrl Pts',(110.534870328711,3.20125357030618,125.825937528946));
#145354=CARTESIAN_POINT('Ctrl Pts',(110.527462982357,3.06660224080808,125.744332825234));
#145355=CARTESIAN_POINT('Ctrl Pts',(110.520061160682,2.93205133935162,125.662788985389));
#145356=CARTESIAN_POINT('Ctrl Pts',(110.512659339006,2.79414086896212,125.586552076545));
#145357=CARTESIAN_POINT('Ctrl Pts',(110.505257517331,2.65333059188378,125.515904573249));
#145358=CARTESIAN_POINT('Ctrl Pts',(110.497859603019,2.51259464745525,125.44529436422));
#145359=CARTESIAN_POINT('Ctrl Pts',(110.490461688708,2.36896227778349,125.380267851449));
#145360=CARTESIAN_POINT('Ctrl Pts',(110.483063774397,2.22291871543582,125.321062071338));
#145361=CARTESIAN_POINT('Ctrl Pts',(110.475667089485,2.07689942287797,125.261866130153));
#145362=CARTESIAN_POINT('Ctrl Pts',(110.468270404572,1.9284700785201,125.208489141934));
#145363=CARTESIAN_POINT('Ctrl Pts',(110.46087371966,1.77813691713127,125.161120443124));
#145364=CARTESIAN_POINT('Ctrl Pts',(110.453477362725,1.62781042167225,125.113753844692));
#145365=CARTESIAN_POINT('Ctrl Pts',(110.446081005789,1.47558063307365,125.072395118134));
#145366=CARTESIAN_POINT('Ctrl Pts',(110.438684648854,1.32196974947645,125.037183964821));
#145367=CARTESIAN_POINT('Ctrl Pts',(110.431287159517,1.16833534766071,125.00196742059));
#145368=CARTESIAN_POINT('Ctrl Pts',(110.423889670181,1.01331979370737,124.972900407086));
#145369=CARTESIAN_POINT('Ctrl Pts',(110.416492180844,0.857456150389222,
124.950071633184));
#145370=CARTESIAN_POINT('Ctrl Pts',(110.409092098329,0.7015378693113,124.92723485669));
#145371=CARTESIAN_POINT('Ctrl Pts',(110.401692015814,0.544771276080293,
124.910640727774));
#145372=CARTESIAN_POINT('Ctrl Pts',(110.394291933299,0.3876950862832,124.900326142517));
#145373=CARTESIAN_POINT('Ctrl Pts',(110.386883713632,0.230446175068722,
124.890000215312));
#145374=CARTESIAN_POINT('Ctrl Pts',(110.379475493966,0.0728873601448385,
124.885967645987));
#145375=CARTESIAN_POINT('Ctrl Pts',(110.372067274299,-0.084441366644023,
124.88821320408));
#145376=CARTESIAN_POINT('Ctrl Pts',(110.364654494997,-0.241866926639501,
124.890460144276));
#145377=CARTESIAN_POINT('Ctrl Pts',(110.357241715695,-0.399061744428589,
124.898992891373));
#145378=CARTESIAN_POINT('Ctrl Pts',(110.349828936393,-0.555490930763011,
124.913744318032));
#145379=CARTESIAN_POINT('Ctrl Pts',(110.342405565364,-0.712143630454446,
124.92851682222));
#145380=CARTESIAN_POINT('Ctrl Pts',(110.334982194336,-0.868028144814353,
124.949525702661));
#145381=CARTESIAN_POINT('Ctrl Pts',(110.327558823307,-1.02261893212332,
124.976652570472));
#145382=CARTESIAN_POINT('Ctrl Pts',(110.323622773866,-1.10458667690795,
124.991035886685));
#145383=CARTESIAN_POINT('Ctrl Pts',(110.319686724425,-1.18619093608855,
125.007138347652));
#145384=CARTESIAN_POINT('Ctrl Pts',(110.315750674985,-1.26735522189452,
125.024936658032));
#145385=CARTESIAN_POINT('Ctrl Pts',(110.308327408579,-1.42042853187652,
125.058503715942));
#145386=CARTESIAN_POINT('Ctrl Pts',(110.300904142174,-1.57239880407388,
125.098207160757));
#145387=CARTESIAN_POINT('Ctrl Pts',(110.293480875768,-1.72273575989662,
125.143962039367));
#145388=CARTESIAN_POINT('Ctrl Pts',(110.286066383047,-1.87289502992315,
125.189662839511));
#145389=CARTESIAN_POINT('Ctrl Pts',(110.278651890326,-2.02142447249822,
125.241400729143));
#145390=CARTESIAN_POINT('Ctrl Pts',(110.271237397605,-2.16780346023257,
125.299039671399));
#145391=CARTESIAN_POINT('Ctrl Pts',(110.263830051251,-2.31404136238737,
125.356623059072));
#145392=CARTESIAN_POINT('Ctrl Pts',(110.256422704898,-2.45813259100948,
125.420096040512));
#145393=CARTESIAN_POINT('Ctrl Pts',(110.249015358544,-2.59957127204351,
125.489272681881));
#145394=CARTESIAN_POINT('Ctrl Pts',(110.241613536868,-2.74090446277334,
125.558397728701));
#145395=CARTESIAN_POINT('Ctrl Pts',(110.234211715193,-2.87958871122211,
125.633217801848));
#145396=CARTESIAN_POINT('Ctrl Pts',(110.226809893518,-3.01513785083059,
125.713498774716));
#145397=CARTESIAN_POINT('Ctrl Pts',(110.219411979206,-3.15061543510308,
125.793737367883));
#145398=CARTESIAN_POINT('Ctrl Pts',(110.212014064895,-3.28296088616804,
125.879430929855));
#145399=CARTESIAN_POINT('Ctrl Pts',(110.204616150583,-3.41171249853264,
125.970299344697));
#145400=CARTESIAN_POINT('Ctrl Pts',(110.197219465671,-3.54044271471451,
126.061152658855));
#145401=CARTESIAN_POINT('Ctrl Pts',(110.189822780759,-3.66557997283185,
126.157178904063));
#145402=CARTESIAN_POINT('Ctrl Pts',(110.182426095847,-3.78669134651391,
126.258054511645));
#145403=CARTESIAN_POINT('Ctrl Pts',(110.175029738911,-3.90779734999058,
126.358925646296));
#145404=CARTESIAN_POINT('Ctrl Pts',(110.167633381976,-4.02487753714001,
126.464645476868));
#145405=CARTESIAN_POINT('Ctrl Pts',(110.16023702504,-4.13753211239265,126.574850175278));
#145406=CARTESIAN_POINT('Ctrl Pts',(110.152839535704,-4.25020393534867,
126.68507174631));
#145407=CARTESIAN_POINT('Ctrl Pts',(110.145442046367,-4.35844853040673,
126.79977929132));
#145408=CARTESIAN_POINT('Ctrl Pts',(110.138044557031,-4.46190313082993,
126.918572278813));
#145409=CARTESIAN_POINT('Ctrl Pts',(110.130644474516,-4.565393997103,127.037406909004));
#145410=CARTESIAN_POINT('Ctrl Pts',(110.123244392001,-4.66409128060714,
127.160329551736));
#145411=CARTESIAN_POINT('Ctrl Pts',(110.115844309486,-4.75767275069233,
127.286906913561));
#145412=CARTESIAN_POINT('Ctrl Pts',(110.108436089819,-4.85135712322395,
127.413623460207));
#145413=CARTESIAN_POINT('Ctrl Pts',(110.101027870153,-4.93991422605951,
127.544002451278));
#145414=CARTESIAN_POINT('Ctrl Pts',(110.093619650486,-5.02306499423533,
127.677581343906));
#145415=CARTESIAN_POINT('Ctrl Pts',(110.086206871184,-5.10626694032159,
127.811242452114));
#145416=CARTESIAN_POINT('Ctrl Pts',(110.078794091882,-5.18405573724024,
127.948107062538));
#145417=CARTESIAN_POINT('Ctrl Pts',(110.07138131258,-5.25619874041902,128.087688873737));
#145418=CARTESIAN_POINT('Ctrl Pts',(110.063957941551,-5.32844482490401,
128.227470125975));
#145419=CARTESIAN_POINT('Ctrl Pts',(110.056534570523,-5.39502884648885,
128.369975995833));
#145420=CARTESIAN_POINT('Ctrl Pts',(110.049111199494,-5.45576634095696,
128.514700338096));
#145421=CARTESIAN_POINT('Ctrl Pts',(110.045175150053,-5.48797081789958,
128.591436656976));
#145422=CARTESIAN_POINT('Ctrl Pts',(110.041239100613,-5.51853245682477,
128.668796404854));
#145423=CARTESIAN_POINT('Ctrl Pts',(110.037303051172,-5.54742951325403,
128.746702638703));
#145424=CARTESIAN_POINT('Ctrl Pts',(110.028756344549,-5.61017635301933,
128.915867618672));
#145425=CARTESIAN_POINT('Ctrl Pts',(110.020209637926,-5.66522896920832,
129.088032641139));
#145426=CARTESIAN_POINT('Ctrl Pts',(110.011662931303,-5.71232982365823,
129.262537492741));
#145427=CARTESIAN_POINT('Ctrl Pts',(110.003146762702,-5.75926238323207,
129.436418825455));
#145428=CARTESIAN_POINT('Ctrl Pts',(109.994630594102,-5.79829980958457,
129.612623168292));
#145429=CARTESIAN_POINT('Ctrl Pts',(109.986114425501,-5.82923382386852,
129.790475225045));
#145430=CARTESIAN_POINT('Ctrl Pts',(109.977658406563,-5.85994935133939,
129.967071113468));
#145431=CARTESIAN_POINT('Ctrl Pts',(109.969202387625,-5.88267545579212,
130.145291379479));
#145432=CARTESIAN_POINT('Ctrl Pts',(109.960746368688,-5.89725540094682,
130.324455107592));
#145433=CARTESIAN_POINT('Ctrl Pts',(109.953289332851,-5.91011289030673,
130.482452665433));
#145434=CARTESIAN_POINT('Ctrl Pts',(109.945832297014,-5.91663589330626,
130.641183591745));
#145435=CARTESIAN_POINT('Ctrl Pts',(109.938375261177,-5.9167485154848,130.800169316047));
#145436=CARTESIAN_POINT('',(108.188375192211,-5.90998823786883,130.808446092953));
#145437=CARTESIAN_POINT('Ctrl Pts',(109.938375192211,-5.91018173940183,
130.800175436554));
#145438=CARTESIAN_POINT('Ctrl Pts',(109.878535270594,-5.90190088737836,
132.074566921819));
#145439=CARTESIAN_POINT('Ctrl Pts',(109.725879474373,-4.87095122287221,
135.337840497513));
#145440=CARTESIAN_POINT('Ctrl Pts',(109.480407803546,0.513821038447506,
137.783869803085));
#145441=CARTESIAN_POINT('Ctrl Pts',(109.201960179734,6.14979156980978,134.144663624517));
#145442=CARTESIAN_POINT('Ctrl Pts',(108.923512555921,6.13440408253642,127.435882165428));
#145443=CARTESIAN_POINT('Ctrl Pts',(108.645064932108,0.481798925711525,
123.822567844538));
#145444=CARTESIAN_POINT('Ctrl Pts',(108.400019144205,-4.8823733627542,126.288986106739));
#145445=CARTESIAN_POINT('Ctrl Pts',(108.247789230906,-5.9019786814506,129.543020490365));
#145446=CARTESIAN_POINT('Ctrl Pts',(108.188375192211,-5.90998823786883,
130.808446092953));
#145447=CARTESIAN_POINT('',(106.438375192211,-5.92510185054946,130.807002374807));
#145448=CARTESIAN_POINT('Ctrl Pts',(108.188375192211,-5.90998823786883,
130.808446092953));
#145449=CARTESIAN_POINT('Ctrl Pts',(108.154973356302,-5.91449111118078,
131.519852677365));
#145450=CARTESIAN_POINT('Ctrl Pts',(108.028755645787,-5.4658095909918,134.202602094435));
#145451=CARTESIAN_POINT('Ctrl Pts',(107.809722060669,-1.46766768783018,
137.647131407855));
#145452=CARTESIAN_POINT('Ctrl Pts',(107.531274436856,4.96370662816406,135.737835765966));
#145453=CARTESIAN_POINT('Ctrl Pts',(107.252826813044,6.83367704342109,129.294917476357));
#145454=CARTESIAN_POINT('Ctrl Pts',(106.97437918923,2.42383209946288,124.239103693122));
#145455=CARTESIAN_POINT('Ctrl Pts',(106.70289531562,-4.04740441513389,125.191997893739));
#145456=CARTESIAN_POINT('Ctrl Pts',(106.524227316613,-5.91499524236282,
128.990435688002));
#145457=CARTESIAN_POINT('Ctrl Pts',(106.438375192211,-5.92510185054946,
130.807002374807));
#145458=CARTESIAN_POINT('',(104.688375192211,-5.91791127406073,130.79899341794));
#145459=CARTESIAN_POINT('Ctrl Pts',(106.438375192211,-5.92510185054946,
130.807002374807));
#145460=CARTESIAN_POINT('Ctrl Pts',(106.431411442009,-5.92592163101843,
130.954350116296));
#145461=CARTESIAN_POINT('Ctrl Pts',(106.424447691807,-5.92090358124783,
131.101641088351));
#145462=CARTESIAN_POINT('Ctrl Pts',(106.324668067,-5.76279283782334,133.205611270108));
#145463=CARTESIAN_POINT('Ctrl Pts',(106.139036317792,-3.33094020304525,
136.959228438572));
#145464=CARTESIAN_POINT('Ctrl Pts',(105.860588693979,3.37781007024566,136.933631345777));
#145465=CARTESIAN_POINT('Ctrl Pts',(105.582141070166,6.98251790417742,131.275533885272));
#145466=CARTESIAN_POINT('Ctrl Pts',(105.303693446353,4.17063289913194,125.184451209843));
#145467=CARTESIAN_POINT('Ctrl Pts',(105.02524582254,-2.47385999346925,124.257790732271));
#145468=CARTESIAN_POINT('Ctrl Pts',(104.820139737826,-5.69366364351441,
128.006610555169));
#145469=CARTESIAN_POINT('Ctrl Pts',(104.707849527717,-5.9219685611791,130.385665735681));
#145470=CARTESIAN_POINT('Ctrl Pts',(104.688375192211,-5.91812558406999,
130.798993223573));
#145471=CARTESIAN_POINT('',(102.938375192243,-5.91674999740235,130.804185291264));
#145472=CARTESIAN_POINT('Ctrl Pts',(104.688375192211,-5.91674756661093,
130.798994473354));
#145473=CARTESIAN_POINT('Ctrl Pts',(104.681070929629,-5.91688813321788,
130.95398418232));
#145474=CARTESIAN_POINT('Ctrl Pts',(104.673766667046,-5.91093459052331,
131.109165024354));
#145475=CARTESIAN_POINT('Ctrl Pts',(104.666462404463,-5.89886870365173,
131.264011114768));
#145476=CARTESIAN_POINT('Ctrl Pts',(104.659163775948,-5.88681212367718,
131.418737766252));
#145477=CARTESIAN_POINT('Ctrl Pts',(104.651865147433,-5.86865261192464,
131.573129798245));
#145478=CARTESIAN_POINT('Ctrl Pts',(104.644566518918,-5.84442399892119,
131.726661372924));
#145479=CARTESIAN_POINT('Ctrl Pts',(104.637224187918,-5.82005031063467,
131.881112258859));
#145480=CARTESIAN_POINT('Ctrl Pts',(104.629881856918,-5.78953459696489,
132.03469195511));
#145481=CARTESIAN_POINT('Ctrl Pts',(104.622539525918,-5.75296435337207,
132.186869825973));
#145482=CARTESIAN_POINT('Ctrl Pts',(104.615246064261,-5.716637515284,132.338034826047));
#145483=CARTESIAN_POINT('Ctrl Pts',(104.607952602604,-5.67433660502426,
132.487816229281));
#145484=CARTESIAN_POINT('Ctrl Pts',(104.600659140947,-5.62619862320037,
132.635704281327));
#145485=CARTESIAN_POINT('Ctrl Pts',(104.593365872807,-5.5780619186232,132.783588409455));
#145486=CARTESIAN_POINT('Ctrl Pts',(104.586072604668,-5.52408856948681,
132.92957892035));
#145487=CARTESIAN_POINT('Ctrl Pts',(104.578779336528,-5.46446520768868,
133.07318202007));
#145488=CARTESIAN_POINT('Ctrl Pts',(104.571484727083,-5.40483088054543,
133.216811529867));
#145489=CARTESIAN_POINT('Ctrl Pts',(104.564190117637,-5.33954462106144,
133.358052399635));
#145490=CARTESIAN_POINT('Ctrl Pts',(104.556895508191,-5.26884075583047,
133.496431874461));
#145491=CARTESIAN_POINT('Ctrl Pts',(104.549516763751,-5.19732140221541,
133.636407398583));
#145492=CARTESIAN_POINT('Ctrl Pts',(104.542138019311,-5.12025887064447,
133.773454747819));
#145493=CARTESIAN_POINT('Ctrl Pts',(104.534759274872,-5.03794240410383,
133.907112121543));
#145494=CARTESIAN_POINT('Ctrl Pts',(104.527453780949,-4.956443112324,134.039442647348));
#145495=CARTESIAN_POINT('Ctrl Pts',(104.520148287026,-4.86979399565266,
134.168449915169));
#145496=CARTESIAN_POINT('Ctrl Pts',(104.512842793103,-4.77831778963543,
134.293717243615));
#145497=CARTESIAN_POINT('Ctrl Pts',(104.505427423405,-4.68546576712084,
134.420868612344));
#145498=CARTESIAN_POINT('Ctrl Pts',(104.498012053707,-4.58764055265885,
134.544166319473));
#145499=CARTESIAN_POINT('Ctrl Pts',(104.490596684009,-4.48521962585023,
134.663212191595));
#145500=CARTESIAN_POINT('Ctrl Pts',(104.48318131431,-4.38279869904161,134.782258063717));
#145501=CARTESIAN_POINT('Ctrl Pts',(104.475765944612,-4.27578238614007,
134.897051848695));
#145502=CARTESIAN_POINT('Ctrl Pts',(104.468350574914,-4.16458378379214,
135.007237307439));
#145503=CARTESIAN_POINT('Ctrl Pts',(104.460927308509,-4.05326676485245,
135.117540103867));
#145504=CARTESIAN_POINT('Ctrl Pts',(104.453504042103,-3.93739618980244,
135.223584137171));
#145505=CARTESIAN_POINT('Ctrl Pts',(104.446080775698,-3.81733137710063,
135.324970279979));
#145506=CARTESIAN_POINT('Ctrl Pts',(104.438666282977,-3.69740847103641,
135.426236592786));
#145507=CARTESIAN_POINT('Ctrl Pts',(104.431251790256,-3.57330147716299,
135.522855734817));
#145508=CARTESIAN_POINT('Ctrl Pts',(104.423837297535,-3.44540736650959,
135.614464425313));
#145509=CARTESIAN_POINT('Ctrl Pts',(104.416429951181,-3.31763652501516,
135.705984819904));
#145510=CARTESIAN_POINT('Ctrl Pts',(104.409022604827,-3.18608613494249,
135.792504161153));
#145511=CARTESIAN_POINT('Ctrl Pts',(104.401615258474,-3.05118705249279,
135.873698654549));
#145512=CARTESIAN_POINT('Ctrl Pts',(104.394213436798,-2.91638858286824,
135.954832590028));
#145513=CARTESIAN_POINT('Ctrl Pts',(104.386811615123,-2.77824671234438,
136.030649393715));
#145514=CARTESIAN_POINT('Ctrl Pts',(104.379409793448,-2.63722206079119,
136.10086799173));
#145515=CARTESIAN_POINT('Ctrl Pts',(104.372011879136,-2.49627185505403,
136.171049521894));
#145516=CARTESIAN_POINT('Ctrl Pts',(104.364613964825,-2.35244223234035,
136.235638565941));
#145517=CARTESIAN_POINT('Ctrl Pts',(104.357216050514,-2.20621914442719,
136.294399565448));
#145518=CARTESIAN_POINT('Ctrl Pts',(104.349819365601,-2.06002035613838,
136.353150799943));
#145519=CARTESIAN_POINT('Ctrl Pts',(104.342422680689,-1.91142923810393,
136.406075773057));
#145520=CARTESIAN_POINT('Ctrl Pts',(104.335025995777,-1.76095259902307,
136.452986690028));
#145521=CARTESIAN_POINT('Ctrl Pts',(104.327629638842,-1.61048263223418,
136.499895526919));
#145522=CARTESIAN_POINT('Ctrl Pts',(104.320233281906,-1.458127667017,136.540790726794));
#145523=CARTESIAN_POINT('Ctrl Pts',(104.312836924971,-1.30441032429665,
136.575534178322));
#145524=CARTESIAN_POINT('Ctrl Pts',(104.305439435634,-1.15066944705815,
136.610282949161));
#145525=CARTESIAN_POINT('Ctrl Pts',(104.298041946298,-0.995566141135667,
136.638878014005));
#145526=CARTESIAN_POINT('Ctrl Pts',(104.290644456961,-0.839633736832117,
136.661232286851));
#145527=CARTESIAN_POINT('Ctrl Pts',(104.283244374446,-0.683646670666186,
136.683594395953));
#145528=CARTESIAN_POINT('Ctrl Pts',(104.275844291931,-0.526830296748347,
136.699711304421));
#145529=CARTESIAN_POINT('Ctrl Pts',(104.268444209416,-0.369723440469288,
136.709547756012));
#145530=CARTESIAN_POINT('Ctrl Pts',(104.26103598975,-0.212443829050997,
136.719395023793));
#145531=CARTESIAN_POINT('Ctrl Pts',(104.253627770083,-0.0548734701753229,
136.722948019605));
#145532=CARTESIAN_POINT('Ctrl Pts',(104.246219550417,0.10244769317082,136.720223617388));
#145533=CARTESIAN_POINT('Ctrl Pts',(104.238806771115,0.259865685068295,
136.717497538347));
#145534=CARTESIAN_POINT('Ctrl Pts',(104.231393991813,0.41703380399418,136.708486383821));
#145535=CARTESIAN_POINT('Ctrl Pts',(104.223981212511,0.573417367490317,
136.693258908856));
#145536=CARTESIAN_POINT('Ctrl Pts',(104.216557841482,0.730024379155305,
136.678009676161));
#145537=CARTESIAN_POINT('Ctrl Pts',(104.209134470453,0.885844227662873,
136.656526434193));
#145538=CARTESIAN_POINT('Ctrl Pts',(104.201711099424,1.04035173406291,136.628929170852));
#145539=CARTESIAN_POINT('Ctrl Pts',(104.197775049984,1.12227532131508,136.614296439642));
#145540=CARTESIAN_POINT('Ctrl Pts',(104.193839000543,1.20383019216157,136.597945677965));
#145541=CARTESIAN_POINT('Ctrl Pts',(104.189902951102,1.28493993008904,136.579900413859));
#145542=CARTESIAN_POINT('Ctrl Pts',(104.182479684696,1.43791036446801,136.545867608928));
#145543=CARTESIAN_POINT('Ctrl Pts',(104.175056418291,1.58975908912062,136.505701802784));
#145544=CARTESIAN_POINT('Ctrl Pts',(104.167633151886,1.73995608648117,136.459489562127));
#145545=CARTESIAN_POINT('Ctrl Pts',(104.160218659165,1.88997556346436,136.413331940502));
#145546=CARTESIAN_POINT('Ctrl Pts',(104.152804166444,2.03834684572162,136.361142217985));
#145547=CARTESIAN_POINT('Ctrl Pts',(104.145389673722,2.18454972232464,136.303058015422));
#145548=CARTESIAN_POINT('Ctrl Pts',(104.137982327369,2.33061168309022,136.245029796601));
#145549=CARTESIAN_POINT('Ctrl Pts',(104.130574981015,2.4745090543689,136.18111854503));
#145550=CARTESIAN_POINT('Ctrl Pts',(104.123167634661,2.61573653036711,136.111511733391));
#145551=CARTESIAN_POINT('Ctrl Pts',(104.115765812986,2.75685867358603,136.041956837138));
#145552=CARTESIAN_POINT('Ctrl Pts',(104.10836399131,2.89531455309249,135.966715003406));
#145553=CARTESIAN_POINT('Ctrl Pts',(104.100962169635,3.03061871718004,135.886021837441));
#145554=CARTESIAN_POINT('Ctrl Pts',(104.093564255324,3.16585145525257,135.805371268769));
#145555=CARTESIAN_POINT('Ctrl Pts',(104.086166341012,3.2979354715768,135.719275289696));
#145556=CARTESIAN_POINT('Ctrl Pts',(104.078768426701,3.42640991537508,135.628015420132));
#145557=CARTESIAN_POINT('Ctrl Pts',(104.071371741789,3.55486300905146,135.536770716303));
#145558=CARTESIAN_POINT('Ctrl Pts',(104.063975056876,3.67970741668296,135.440364041114));
#145559=CARTESIAN_POINT('Ctrl Pts',(104.056578371964,3.80051119873585,135.339120279421));
#145560=CARTESIAN_POINT('Ctrl Pts',(104.049182015029,3.92130962422245,135.237881006982));
#145561=CARTESIAN_POINT('Ctrl Pts',(104.041785658093,4.03806749426662,135.131805314281));
#145562=CARTESIAN_POINT('Ctrl Pts',(104.034389301158,4.15038612251815,135.021258244555));
#145563=CARTESIAN_POINT('Ctrl Pts',(104.026991811821,4.26272194703856,134.910694249791));
#145564=CARTESIAN_POINT('Ctrl Pts',(104.019594322485,4.37061691040595,134.795657776786));
#145565=CARTESIAN_POINT('Ctrl Pts',(104.012196833148,4.47370946664381,134.676550459317));
#145566=CARTESIAN_POINT('Ctrl Pts',(104.004796750633,4.57683816181694,134.557401388963));
#145567=CARTESIAN_POINT('Ctrl Pts',(103.997396668118,4.67516085392078,134.434178915021));
#145568=CARTESIAN_POINT('Ctrl Pts',(103.989996585603,4.76835663259408,134.30731730969));
#145569=CARTESIAN_POINT('Ctrl Pts',(103.982588365937,4.86165488960713,134.180316206982));
#145570=CARTESIAN_POINT('Ctrl Pts',(103.97518014627,4.94981475345225,134.049668282459));
#145571=CARTESIAN_POINT('Ctrl Pts',(103.967771926604,5.03255856827978,133.915836926223));
#145572=CARTESIAN_POINT('Ctrl Pts',(103.960359147302,5.1153533105451,133.78192319902));
#145573=CARTESIAN_POINT('Ctrl Pts',(103.952946368,5.19272517835729,133.644822460204));
#145574=CARTESIAN_POINT('Ctrl Pts',(103.945533588698,5.264443008356,133.505021717051));
#145575=CARTESIAN_POINT('Ctrl Pts',(103.938110217669,5.33626331215313,133.365021220041));
#145576=CARTESIAN_POINT('Ctrl Pts',(103.93068684664,5.40241328647759,133.222313351403));
#145577=CARTESIAN_POINT('Ctrl Pts',(103.923263475611,5.46271000849914,133.077404815452));
#145578=CARTESIAN_POINT('Ctrl Pts',(103.91932742617,5.49468077731558,133.000570832657));
#145579=CARTESIAN_POINT('Ctrl Pts',(103.915391376729,5.52500681822054,132.923118423985));
#145580=CARTESIAN_POINT('Ctrl Pts',(103.911455327289,5.55366662102438,132.84512459829));
#145581=CARTESIAN_POINT('Ctrl Pts',(103.904032060883,5.60771811466959,132.698030677136));
#145582=CARTESIAN_POINT('Ctrl Pts',(103.896608794478,5.65600342919169,132.548565445181));
#145583=CARTESIAN_POINT('Ctrl Pts',(103.889185528072,5.69830890816788,132.397221612629));
#145584=CARTESIAN_POINT('Ctrl Pts',(103.881771035351,5.74056438558124,132.24605665592));
#145585=CARTESIAN_POINT('Ctrl Pts',(103.87435654263,5.77685399616787,132.093017874238));
#145586=CARTESIAN_POINT('Ctrl Pts',(103.866942049909,5.80701233752974,131.938617323201));
#145587=CARTESIAN_POINT('Ctrl Pts',(103.859534703555,5.83714161114672,131.784365589228));
#145588=CARTESIAN_POINT('Ctrl Pts',(103.852127357202,5.86115130920403,131.628755062792));
#145589=CARTESIAN_POINT('Ctrl Pts',(103.844720010848,5.87892602765447,131.472312205532));
#145590=CARTESIAN_POINT('Ctrl Pts',(103.837318189173,5.89668748904934,131.315986029258));
#145591=CARTESIAN_POINT('Ctrl Pts',(103.829916367497,5.90822318821751,131.158829127538));
#145592=CARTESIAN_POINT('Ctrl Pts',(103.822514545822,5.91346894801861,131.001377275033));
#145593=CARTESIAN_POINT('Ctrl Pts',(103.81511663151,5.91871193862392,130.844008540137));
#145594=CARTESIAN_POINT('Ctrl Pts',(103.807718717199,5.91767159021922,130.686345536689));
#145595=CARTESIAN_POINT('Ctrl Pts',(103.800320802888,5.91033565237705,130.528928159891));
#145596=CARTESIAN_POINT('Ctrl Pts',(103.792924117975,5.90300093363465,130.371536943005));
#145597=CARTESIAN_POINT('Ctrl Pts',(103.785527433063,5.88937271923794,130.214391644283));
#145598=CARTESIAN_POINT('Ctrl Pts',(103.778130748151,5.86949087014882,130.05803127489));
#145599=CARTESIAN_POINT('Ctrl Pts',(103.770734391216,5.84960990264173,129.901677838679));
#145600=CARTESIAN_POINT('Ctrl Pts',(103.76333803428,5.82347589888097,129.746109632908));
#145601=CARTESIAN_POINT('Ctrl Pts',(103.755941677345,5.79118048037017,129.591859398482));
#145602=CARTESIAN_POINT('Ctrl Pts',(103.748544188008,5.75888011734825,129.437585547951));
#145603=CARTESIAN_POINT('Ctrl Pts',(103.741146698671,5.72041653778777,129.284630435945));
#145604=CARTESIAN_POINT('Ctrl Pts',(103.733749209335,5.67593222312858,129.133515334199));
#145605=CARTESIAN_POINT('Ctrl Pts',(103.72634912682,5.63143231456174,128.982347259288));
#145606=CARTESIAN_POINT('Ctrl Pts',(103.718949044305,5.5809075741387,128.833020836734));
#145607=CARTESIAN_POINT('Ctrl Pts',(103.71154896179,5.52454990747228,128.686040792245));
#145608=CARTESIAN_POINT('Ctrl Pts',(103.704140742123,5.4681302697579,128.538899128088));
#145609=CARTESIAN_POINT('Ctrl Pts',(103.696732522457,5.40586503054713,128.39410934336));
#145610=CARTESIAN_POINT('Ctrl Pts',(103.68932430279,5.33799397328917,128.252155511461));
#145611=CARTESIAN_POINT('Ctrl Pts',(103.681911523488,5.27008114252791,128.110114309347));
#145612=CARTESIAN_POINT('Ctrl Pts',(103.674498744186,5.19655579253233,127.97091286747));
#145613=CARTESIAN_POINT('Ctrl Pts',(103.667085964884,5.11770270687505,127.835008909441));
#145614=CARTESIAN_POINT('Ctrl Pts',(103.659662593855,5.03873695223119,127.698910765464));
#145615=CARTESIAN_POINT('Ctrl Pts',(103.652239222827,4.9544284575738,127.566119829768));
#145616=CARTESIAN_POINT('Ctrl Pts',(103.644815851798,4.86510465333724,127.43706388657));
#145617=CARTESIAN_POINT('Ctrl Pts',(103.640879802357,4.81774302903664,127.368635328833));
#145618=CARTESIAN_POINT('Ctrl Pts',(103.636943752916,4.76897208992012,127.301256252977));
#145619=CARTESIAN_POINT('Ctrl Pts',(103.633007703476,4.71884499893512,127.234986381299));
#145620=CARTESIAN_POINT('Ctrl Pts',(103.62558443707,4.62430686974852,127.110003471525));
#145621=CARTESIAN_POINT('Ctrl Pts',(103.618161170665,4.52465692896269,126.988590060143));
#145622=CARTESIAN_POINT('Ctrl Pts',(103.610737904259,4.42019422111259,126.871192224255));
#145623=CARTESIAN_POINT('Ctrl Pts',(103.603323411538,4.31585497950823,126.753933142859));
#145624=CARTESIAN_POINT('Ctrl Pts',(103.595908918817,4.20671453914133,126.640680466018));
#145625=CARTESIAN_POINT('Ctrl Pts',(103.588494426096,4.0931143028676,126.531850130023));
#145626=CARTESIAN_POINT('Ctrl Pts',(103.581087079743,3.97962355877872,126.423124688804));
#145627=CARTESIAN_POINT('Ctrl Pts',(103.573679733389,3.8616818440389,126.318813359302));
#145628=CARTESIAN_POINT('Ctrl Pts',(103.566272387035,3.73966970702886,126.219297799585));
#145629=CARTESIAN_POINT('Ctrl Pts',(103.55887056536,3.61774857127317,126.119856462327));
#145630=CARTESIAN_POINT('Ctrl Pts',(103.551468743684,3.49176334611748,126.025204007759));
#145631=CARTESIAN_POINT('Ctrl Pts',(103.544066922009,3.36213010464429,125.935684029216));
#145632=CARTESIAN_POINT('Ctrl Pts',(103.536669007698,3.23256529555132,125.846211307574));
#145633=CARTESIAN_POINT('Ctrl Pts',(103.529271093386,3.09935661177866,125.761865877655));
#145634=CARTESIAN_POINT('Ctrl Pts',(103.521873179075,2.96295166079344,125.682949872634));
#145635=CARTESIAN_POINT('Ctrl Pts',(103.514476494163,2.82656937783547,125.604046982021));
#145636=CARTESIAN_POINT('Ctrl Pts',(103.50707980925,2.68699220466574,125.530571912318));
#145637=CARTESIAN_POINT('Ctrl Pts',(103.499683124338,2.54469517246507,125.462782476068));
#145638=CARTESIAN_POINT('Ctrl Pts',(103.492286767403,2.40240444986392,125.394996045672));
#145639=CARTESIAN_POINT('Ctrl Pts',(103.484890410467,2.25739444503718,125.332894908006));
#145640=CARTESIAN_POINT('Ctrl Pts',(103.477494053532,2.11016289165644,125.276689938774));
#145641=CARTESIAN_POINT('Ctrl Pts',(103.470096564195,1.96290879674932,125.220476364418));
#145642=CARTESIAN_POINT('Ctrl Pts',(103.462699074859,1.81343282482721,125.170160889072));
#145643=CARTESIAN_POINT('Ctrl Pts',(103.455301585522,1.66225055126366,125.12590539917));
#145644=CARTESIAN_POINT('Ctrl Pts',(103.447901503007,1.51101528098924,125.081634395576));
#145645=CARTESIAN_POINT('Ctrl Pts',(103.440501420492,1.35807287621826,125.043427711738));
#145646=CARTESIAN_POINT('Ctrl Pts',(103.433101337977,1.20395170665455,125.011396708603));
#145647=CARTESIAN_POINT('Ctrl Pts',(103.425693118311,1.04966106501999,124.979330484088));
#145648=CARTESIAN_POINT('Ctrl Pts',(103.418284898644,0.894189435762269,
124.953453577946));
#145649=CARTESIAN_POINT('Ctrl Pts',(103.410876678978,0.738073692353686,
124.933825907069));
#145650=CARTESIAN_POINT('Ctrl Pts',(103.403463899676,0.581861862309744,
124.914186155687));
#145651=CARTESIAN_POINT('Ctrl Pts',(103.396051120374,0.425005499239751,
124.900803335466));
#145652=CARTESIAN_POINT('Ctrl Pts',(103.388638341072,0.268043631458563,
124.893685260711));
#145653=CARTESIAN_POINT('Ctrl Pts',(103.381214970043,0.110857489199907,
124.886557015317));
#145654=CARTESIAN_POINT('Ctrl Pts',(103.373791599014,-0.0464340865480609,
124.88571139527));
#145655=CARTESIAN_POINT('Ctrl Pts',(103.366368227985,-0.203294204659716,
124.891104151891));
#145656=CARTESIAN_POINT('Ctrl Pts',(103.362432178544,-0.286465203090883,
124.893963520848));
#145657=CARTESIAN_POINT('Ctrl Pts',(103.358496129104,-0.369515011775571,
124.898575856866));
#145658=CARTESIAN_POINT('Ctrl Pts',(103.354560079663,-0.452364648780765,
124.904928713812));
#145659=CARTESIAN_POINT('Ctrl Pts',(103.347136813257,-0.608616478520997,
124.916910003745));
#145660=CARTESIAN_POINT('Ctrl Pts',(103.339713546852,-0.764628247202771,
124.935121406622));
#145661=CARTESIAN_POINT('Ctrl Pts',(103.332290280446,-0.919863016651839,
124.959552443374));
#145662=CARTESIAN_POINT('Ctrl Pts',(103.324875787725,-1.07491431149509,
124.98395460467));
#145663=CARTESIAN_POINT('Ctrl Pts',(103.317461295004,-1.22919006992554,
125.014561709986));
#145664=CARTESIAN_POINT('Ctrl Pts',(103.310046802283,-1.38215581637968,
125.051311351155));
#145665=CARTESIAN_POINT('Ctrl Pts',(103.30263945593,-1.53497412868833,125.088025571637));
#145666=CARTESIAN_POINT('Ctrl Pts',(103.295232109576,-1.68648458215299,
125.130870454988));
#145667=CARTESIAN_POINT('Ctrl Pts',(103.287824763222,-1.83616038133609,
125.179732130589));
#145668=CARTESIAN_POINT('Ctrl Pts',(103.280422941547,-1.985724546661,125.228557363309));
#145669=CARTESIAN_POINT('Ctrl Pts',(103.273021119871,-2.13345642894244,
125.28339033761));
#145670=CARTESIAN_POINT('Ctrl Pts',(103.265619298196,-2.27884205571151,
125.344066720016));
#145671=CARTESIAN_POINT('Ctrl Pts',(103.258221383884,-2.42415093453936,
125.404711071832));
#145672=CARTESIAN_POINT('Ctrl Pts',(103.250823469573,-2.56711568089916,
125.471192545033));
#145673=CARTESIAN_POINT('Ctrl Pts',(103.243425555262,-2.70724015882465,
125.543297865142));
#145674=CARTESIAN_POINT('Ctrl Pts',(103.23602887035,-2.84734135060463,125.615391202654));
#145675=CARTESIAN_POINT('Ctrl Pts',(103.228632185437,-2.98460287912828,
125.69310636157));
#145676=CARTESIAN_POINT('Ctrl Pts',(103.221235500525,-3.11855107344445,
125.776183038679));
#145677=CARTESIAN_POINT('Ctrl Pts',(103.21383914359,-3.25249332835751,125.859256032082));
#145678=CARTESIAN_POINT('Ctrl Pts',(103.206442786654,-3.38312222394707,
125.947689874226));
#145679=CARTESIAN_POINT('Ctrl Pts',(103.199046429719,-3.50999130730211,
126.041179791147));
#145680=CARTESIAN_POINT('Ctrl Pts',(103.191648940382,-3.63687981463743,
126.134684021613));
#145681=CARTESIAN_POINT('Ctrl Pts',(103.184251451046,-3.76000706303217,
126.233245646722));
#145682=CARTESIAN_POINT('Ctrl Pts',(103.176853961709,-3.87895817176008,
126.336518401883));
#145683=CARTESIAN_POINT('Ctrl Pts',(103.169453879194,-3.99795097861475,
126.439827359149));
#145684=CARTESIAN_POINT('Ctrl Pts',(103.162053796679,-4.11276444940223,
126.547850489973));
#145685=CARTESIAN_POINT('Ctrl Pts',(103.154653714164,-4.22301929627321,
126.660203455271));
#145686=CARTESIAN_POINT('Ctrl Pts',(103.147245494498,-4.33339537968287,
126.772679964204));
#145687=CARTESIAN_POINT('Ctrl Pts',(103.139837274831,-4.43920256691127,
126.889495549236));
#145688=CARTESIAN_POINT('Ctrl Pts',(103.132429055165,-4.54010025495626,
127.010230910051));
#145689=CARTESIAN_POINT('Ctrl Pts',(103.125016275863,-4.64106004384467,
127.131040581467));
#145690=CARTESIAN_POINT('Ctrl Pts',(103.117603496561,-4.7371040851871,127.255774540897));
#145691=CARTESIAN_POINT('Ctrl Pts',(103.110190717259,-4.82793444661485,
127.383983512379));
#145692=CARTESIAN_POINT('Ctrl Pts',(103.10276734623,-4.91889459072227,127.512375674851));
#145693=CARTESIAN_POINT('Ctrl Pts',(103.095343975201,-5.00462597356885,
127.644252453965));
#145694=CARTESIAN_POINT('Ctrl Pts',(103.087920604172,-5.08487562005356,
127.77913823052));
#145695=CARTESIAN_POINT('Ctrl Pts',(103.083984554731,-5.12742590818442,
127.85065790579));
#145696=CARTESIAN_POINT('Ctrl Pts',(103.080048505291,-5.16843586946286,
127.92302314221));
#145697=CARTESIAN_POINT('Ctrl Pts',(103.07611245585,-5.20787328350828,127.996160762602));
#145698=CARTESIAN_POINT('Ctrl Pts',(103.068287579489,-5.28627496354613,
128.141558539092));
#145699=CARTESIAN_POINT('Ctrl Pts',(103.060462703129,-5.35867507229847,
128.290410856979));
#145700=CARTESIAN_POINT('Ctrl Pts',(103.052637826769,-5.42477333902216,
128.442208043592));
#145701=CARTESIAN_POINT('Ctrl Pts',(103.044826119433,-5.49076036440746,
128.593749760234));
#145702=CARTESIAN_POINT('Ctrl Pts',(103.037014412098,-5.550466563893,128.74822618012));
#145703=CARTESIAN_POINT('Ctrl Pts',(103.029202704763,-5.60363718529675,
128.905102641919));
#145704=CARTESIAN_POINT('Ctrl Pts',(103.021408952776,-5.65668559307875,
129.061618520372));
#145705=CARTESIAN_POINT('Ctrl Pts',(103.013615200789,-5.7032282856301,129.220523141253));
#145706=CARTESIAN_POINT('Ctrl Pts',(103.005821448802,-5.74305852531664,
129.381262118766));
#145707=CARTESIAN_POINT('Ctrl Pts',(102.998038259748,-5.78283478276906,
129.54178324549));
#145708=CARTESIAN_POINT('Ctrl Pts',(102.990255070694,-5.81591664255203,
129.704133471243));
#145709=CARTESIAN_POINT('Ctrl Pts',(102.98247188164,-5.84214646079905,129.867741541808));
#145710=CARTESIAN_POINT('Ctrl Pts',(102.974703271238,-5.86832714810848,
130.031043158938));
#145711=CARTESIAN_POINT('Ctrl Pts',(102.966934660835,-5.88768134387658,
130.195597612681));
#145712=CARTESIAN_POINT('Ctrl Pts',(102.959166050433,-5.90010205343943,
130.360822207166));
#145713=CARTESIAN_POINT('Ctrl Pts',(102.95223576437,-5.91118242250353,130.508217126603));
#145714=CARTESIAN_POINT('Ctrl Pts',(102.945305478307,-5.91674561064366,
130.656145013206));
#145715=CARTESIAN_POINT('Ctrl Pts',(102.938375192243,-5.91674999740235,
130.804185291264));
#145716=CARTESIAN_POINT('',(101.188375192211,-5.91674751171398,130.809786953944));
#145717=CARTESIAN_POINT('Ctrl Pts',(102.938375192211,-5.91674999740237,
130.804185291958));
#145718=CARTESIAN_POINT('Ctrl Pts',(102.930643930825,-5.91675489114609,
130.969335485603));
#145719=CARTESIAN_POINT('Ctrl Pts',(102.922912669439,-5.90984088281348,
131.134358686294));
#145720=CARTESIAN_POINT('Ctrl Pts',(102.915181408053,-5.89606567339422,
131.298668353215));
#145721=CARTESIAN_POINT('Ctrl Pts',(102.90744101397,-5.88227419175061,131.46317211401));
#145722=CARTESIAN_POINT('Ctrl Pts',(102.899700619886,-5.86160536074397,
131.626960339075));
#145723=CARTESIAN_POINT('Ctrl Pts',(102.891960225803,-5.83416837114592,
131.789454511375));
#145724=CARTESIAN_POINT('Ctrl Pts',(102.884102276323,-5.80631468878351,
131.954416525332));
#145725=CARTESIAN_POINT('Ctrl Pts',(102.876244326842,-5.77148569305193,
132.118044524203));
#145726=CARTESIAN_POINT('Ctrl Pts',(102.868386377361,-5.72984819340822,
132.279748784455));
#145727=CARTESIAN_POINT('Ctrl Pts',(102.860619727974,-5.68869447234087,
132.439574232159));
#145728=CARTESIAN_POINT('Ctrl Pts',(102.852853078587,-5.6408897815955,132.597520124815));
#145729=CARTESIAN_POINT('Ctrl Pts',(102.8450864292,-5.5866440981802,132.753036650869));
#145730=CARTESIAN_POINT('Ctrl Pts',(102.837182829673,-5.53144189496007,
132.911295416079));
#145731=CARTESIAN_POINT('Ctrl Pts',(102.829279230146,-5.46956958395598,
133.067038018644));
#145732=CARTESIAN_POINT('Ctrl Pts',(102.821375630618,-5.40129765077299,
133.219710333498));
#145733=CARTESIAN_POINT('Ctrl Pts',(102.813472031091,-5.33302571758999,
133.372382648353));
#145734=CARTESIAN_POINT('Ctrl Pts',(102.805568431564,-5.25835437312984,
133.521984396406));
#145735=CARTESIAN_POINT('Ctrl Pts',(102.797664832036,-5.17760078944642,
133.667991289916));
#145736=CARTESIAN_POINT('Ctrl Pts',(102.790241565631,-5.10175492164865,
133.805124764836));
#145737=CARTESIAN_POINT('Ctrl Pts',(102.782818299225,-5.02034244549844,
133.939450249718));
#145738=CARTESIAN_POINT('Ctrl Pts',(102.77539503282,-4.93359607919921,134.070483745957));
#145739=CARTESIAN_POINT('Ctrl Pts',(102.767980540099,-4.84695223990111,
134.201362371485));
#145740=CARTESIAN_POINT('Ctrl Pts',(102.760566047378,-4.75498726308215,
134.328956444911));
#145741=CARTESIAN_POINT('Ctrl Pts',(102.753151554657,-4.65798007372,134.452805792614));
#145742=CARTESIAN_POINT('Ctrl Pts',(102.745744208303,-4.561066383539,134.576535769652));
#145743=CARTESIAN_POINT('Ctrl Pts',(102.738336861949,-4.45912038450908,
134.696527914479));
#145744=CARTESIAN_POINT('Ctrl Pts',(102.730929515596,-4.35246461521372,
134.812350429905));
#145745=CARTESIAN_POINT('Ctrl Pts',(102.72352769392,-4.24588839381515,134.928086560529));
#145746=CARTESIAN_POINT('Ctrl Pts',(102.716125872245,-4.13460964824198,
135.039658980494));
#145747=CARTESIAN_POINT('Ctrl Pts',(102.708724050569,-4.0189914838226,135.146668531045));
#145748=CARTESIAN_POINT('Ctrl Pts',(102.701326136258,-3.90343435333242,
135.253621592087));
#145749=CARTESIAN_POINT('Ctrl Pts',(102.693928221947,-3.78354263939548,
135.356016327841));
#145750=CARTESIAN_POINT('Ctrl Pts',(102.686530307636,-3.65971654597314,
135.453490145298));
#145751=CARTESIAN_POINT('Ctrl Pts',(102.679133622723,-3.53591103020099,
135.550947764375));
#145752=CARTESIAN_POINT('Ctrl Pts',(102.671736937811,-3.40817272562196,
135.64348585751));
#145753=CARTESIAN_POINT('Ctrl Pts',(102.664340252899,-3.2769352716698,135.730781812286));
#145754=CARTESIAN_POINT('Ctrl Pts',(102.656943895964,-3.14570363692396,
135.818073896267));
#145755=CARTESIAN_POINT('Ctrl Pts',(102.649547539028,-3.01097347212354,
135.900124097315));
#145756=CARTESIAN_POINT('Ctrl Pts',(102.642151182093,-2.87320754997878,
135.976653043294));
#145757=CARTESIAN_POINT('Ctrl Pts',(102.634753692756,-2.73542053551983,
136.05319370605));
#145758=CARTESIAN_POINT('Ctrl Pts',(102.62735620342,-2.59459716462314,136.124211249309));
#145759=CARTESIAN_POINT('Ctrl Pts',(102.619958714083,-2.45122482292418,
136.189472262646));
#145760=CARTESIAN_POINT('Ctrl Pts',(102.612558631568,-2.30780222227279,
136.254756153131));
#145761=CARTESIAN_POINT('Ctrl Pts',(102.605158549053,-2.16182921133596,
136.31427934143));
#145762=CARTESIAN_POINT('Ctrl Pts',(102.597758466538,-2.01381301037555,
136.367856615744));
#145763=CARTESIAN_POINT('Ctrl Pts',(102.590350246872,-1.86563405038554,
136.421492803779));
#145764=CARTESIAN_POINT('Ctrl Pts',(102.582942027205,-1.71540776479546,
136.469169893595));
#145765=CARTESIAN_POINT('Ctrl Pts',(102.575533807539,-1.5636570916988,136.510752390138));
#145766=CARTESIAN_POINT('Ctrl Pts',(102.568121028237,-1.41181301859527,
136.552360480014));
#145767=CARTESIAN_POINT('Ctrl Pts',(102.560708248935,-1.25844305127042,
136.587866418042));
#145768=CARTESIAN_POINT('Ctrl Pts',(102.553295469633,-1.10407965441939,
136.617185978713));
#145769=CARTESIAN_POINT('Ctrl Pts',(102.545872098604,-0.949495695907687,
136.646547432548));
#145770=CARTESIAN_POINT('Ctrl Pts',(102.538448727576,-0.793915841144419,
136.669704799978));
#145771=CARTESIAN_POINT('Ctrl Pts',(102.531025356547,-0.637877827209255,
136.686625694903));
#145772=CARTESIAN_POINT('Ctrl Pts',(102.527089307106,-0.555142728135863,
136.695597559403));
#145773=CARTESIAN_POINT('Ctrl Pts',(102.523153257665,-0.472278839371946,
136.702816998817));
#145774=CARTESIAN_POINT('Ctrl Pts',(102.519217208224,-0.389366109742821,
136.708285125475));
#145775=CARTESIAN_POINT('Ctrl Pts',(102.511793941818,-0.232995289287956,
136.718597841695));
#145776=CARTESIAN_POINT('Ctrl Pts',(102.504370675413,-0.0759780225912232,
136.72270942545));
#145777=CARTESIAN_POINT('Ctrl Pts',(102.496947409008,0.08115269873832,136.720554056086));
#145778=CARTESIAN_POINT('Ctrl Pts',(102.489532916287,0.238097704604704,
136.718401234189));
#145779=CARTESIAN_POINT('Ctrl Pts',(102.482118423566,0.395155528571331,
136.709996207954));
#145780=CARTESIAN_POINT('Ctrl Pts',(102.474703930845,0.551788247772069,
136.695324909778));
#145781=CARTESIAN_POINT('Ctrl Pts',(102.467296584491,0.708269998460256,
136.680667752353));
#145782=CARTESIAN_POINT('Ctrl Pts',(102.459889238137,0.864327090902323,
136.659756381358));
#145783=CARTESIAN_POINT('Ctrl Pts',(102.452481891783,1.01942190190995,136.632628760712));
#145784=CARTESIAN_POINT('Ctrl Pts',(102.445080070108,1.17440103735679,136.605521372868));
#145785=CARTESIAN_POINT('Ctrl Pts',(102.437678248432,1.32841895428545,136.572207030938));
#145786=CARTESIAN_POINT('Ctrl Pts',(102.430276426757,1.48094356183199,136.532775470662));
#145787=CARTESIAN_POINT('Ctrl Pts',(102.422878512446,1.63338765282512,136.493364725999));
#145788=CARTESIAN_POINT('Ctrl Pts',(102.415480598134,1.78433964388543,136.44784328736));
#145789=CARTESIAN_POINT('Ctrl Pts',(102.408082683823,1.93327815522968,136.396351867292));
#145790=CARTESIAN_POINT('Ctrl Pts',(102.400685998911,2.08219191569537,136.344869004164));
#145791=CARTESIAN_POINT('Ctrl Pts',(102.393289313998,2.22909250807164,136.287418250493));
#145792=CARTESIAN_POINT('Ctrl Pts',(102.385892629086,2.37347411668863,136.224190059523));
#145793=CARTESIAN_POINT('Ctrl Pts',(102.378496272151,2.51784932327399,136.160964672158));
#145794=CARTESIAN_POINT('Ctrl Pts',(102.371099915215,2.6597054262402,136.091962506608));
#145795=CARTESIAN_POINT('Ctrl Pts',(102.36370355828,2.79855724194409,136.017421899199));
#145796=CARTESIAN_POINT('Ctrl Pts',(102.356306068943,2.93743031621535,135.942869879433));
#145797=CARTESIAN_POINT('Ctrl Pts',(102.348908579607,3.07329785845258,135.862777906003));
#145798=CARTESIAN_POINT('Ctrl Pts',(102.34151109027,3.2057000500142,135.777429866213));
#145799=CARTESIAN_POINT('Ctrl Pts',(102.334111007755,3.33814865495844,135.6920519078));
#145800=CARTESIAN_POINT('Ctrl Pts',(102.32671092524,3.46712917705859,135.601414416739));
#145801=CARTESIAN_POINT('Ctrl Pts',(102.319310842725,3.592211627442,135.505844020299));
#145802=CARTESIAN_POINT('Ctrl Pts',(102.311902623059,3.71743161883874,135.410168534382));
#145803=CARTESIAN_POINT('Ctrl Pts',(102.304494403392,3.83874468162846,135.309549537309));
#145804=CARTESIAN_POINT('Ctrl Pts',(102.297086183726,3.95575415917278,135.204353753321));
#145805=CARTESIAN_POINT('Ctrl Pts',(102.289673404424,4.07283565409778,135.099093223083));
#145806=CARTESIAN_POINT('Ctrl Pts',(102.282260625122,4.18560801894928,134.989250552694));
#145807=CARTESIAN_POINT('Ctrl Pts',(102.27484784582,4.29371258224892,134.875228193837));
#145808=CARTESIAN_POINT('Ctrl Pts',(102.267424474791,4.40197161041875,134.761042914487));
#145809=CARTESIAN_POINT('Ctrl Pts',(102.260001103762,4.50554927123721,134.64266629917));
#145810=CARTESIAN_POINT('Ctrl Pts',(102.252577732733,4.60412765733418,134.520533255842));
#145811=CARTESIAN_POINT('Ctrl Pts',(102.248641683293,4.65639628299939,134.455775385726));
#145812=CARTESIAN_POINT('Ctrl Pts',(102.244705633852,4.70726015778164,134.389961932632));
#145813=CARTESIAN_POINT('Ctrl Pts',(102.240769584411,4.75667700322258,134.323160761012));
#145814=CARTESIAN_POINT('Ctrl Pts',(102.233346318005,4.84987563147594,134.19717583613));
#145815=CARTESIAN_POINT('Ctrl Pts',(102.2259230516,4.93820649134497,134.067295174149));
#145816=CARTESIAN_POINT('Ctrl Pts',(102.218499785195,5.02132611106557,133.933931618331));
#145817=CARTESIAN_POINT('Ctrl Pts',(102.211085292474,5.10434749029832,133.800725687162));
#145818=CARTESIAN_POINT('Ctrl Pts',(102.203670799753,5.18216969388803,133.664045369766));
#145819=CARTESIAN_POINT('Ctrl Pts',(102.196256307032,5.25449012591507,133.524335632003));
#145820=CARTESIAN_POINT('Ctrl Pts',(102.188848960678,5.32674085278701,133.384760551745));
#145821=CARTESIAN_POINT('Ctrl Pts',(102.181441614324,5.39350019450025,133.242162193296));
#145822=CARTESIAN_POINT('Ctrl Pts',(102.17403426797,5.45450949270733,133.097013394692));
#145823=CARTESIAN_POINT('Ctrl Pts',(102.166632446295,5.51547328787797,132.95197285354));
#145824=CARTESIAN_POINT('Ctrl Pts',(102.15923062462,5.57069543469773,132.804386002453));
#145825=CARTESIAN_POINT('Ctrl Pts',(102.151828802944,5.61996382227698,132.654749008904));
#145826=CARTESIAN_POINT('Ctrl Pts',(102.144430888633,5.66920620145778,132.50519100756));
#145827=CARTESIAN_POINT('Ctrl Pts',(102.137032974322,5.71250096427134,132.353585372791));
#145828=CARTESIAN_POINT('Ctrl Pts',(102.12963506001,5.74968467766248,132.200446814745));
#145829=CARTESIAN_POINT('Ctrl Pts',(102.122238375098,5.78686221179517,132.047333705549));
#145830=CARTESIAN_POINT('Ctrl Pts',(102.114841690186,5.81793062406755,131.892688541069));
#145831=CARTESIAN_POINT('Ctrl Pts',(102.107445005274,5.84277674246381,131.737039822987));
#145832=CARTESIAN_POINT('Ctrl Pts',(102.100048648338,5.86762175915711,131.581398006531));
#145833=CARTESIAN_POINT('Ctrl Pts',(102.092652291403,5.88624497171845,131.424753093581));
#145834=CARTESIAN_POINT('Ctrl Pts',(102.085255934467,5.89858464563732,131.267642109482));
#145835=CARTESIAN_POINT('Ctrl Pts',(102.077858445131,5.91092620879179,131.110507071289));
#145836=CARTESIAN_POINT('Ctrl Pts',(102.070460955794,5.91698228855131,130.952906192042));
#145837=CARTESIAN_POINT('Ctrl Pts',(102.063063466458,5.91674318413639,130.795379778208));
#145838=CARTESIAN_POINT('Ctrl Pts',(102.055663383943,5.91650399590379,130.637798143734));
#145839=CARTESIAN_POINT('Ctrl Pts',(102.048263301428,5.90996523040597,130.480291399709));
#145840=CARTESIAN_POINT('Ctrl Pts',(102.040863218913,5.89716926892732,130.323397857969));
#145841=CARTESIAN_POINT('Ctrl Pts',(102.033454999246,5.88435923697359,130.166331795651));
#145842=CARTESIAN_POINT('Ctrl Pts',(102.02604677958,5.86527829873151,130.009880654487));
#145843=CARTESIAN_POINT('Ctrl Pts',(102.018638559913,5.84002058709075,129.854576376353));
#145844=CARTESIAN_POINT('Ctrl Pts',(102.011225780611,5.81474732974995,129.699176511027));
#145845=CARTESIAN_POINT('Ctrl Pts',(102.003813001309,5.78328979806562,129.544925280196));
#145846=CARTESIAN_POINT('Ctrl Pts',(101.996400222007,5.74579271534276,129.392341979299));
#145847=CARTESIAN_POINT('Ctrl Pts',(101.988976850979,5.70824205502964,129.239540660225));
#145848=CARTESIAN_POINT('Ctrl Pts',(101.98155347995,5.66463471166064,129.088412388619));
#145849=CARTESIAN_POINT('Ctrl Pts',(101.974130108921,5.61516474891769,128.939459707326));
#145850=CARTESIAN_POINT('Ctrl Pts',(101.97019405948,5.58893458765602,128.860481421635));
#145851=CARTESIAN_POINT('Ctrl Pts',(101.96625801004,5.56105703237352,128.782114424262));
#145852=CARTESIAN_POINT('Ctrl Pts',(101.962321960599,5.5315663268166,128.704430967666));
#145853=CARTESIAN_POINT('Ctrl Pts',(101.954898694193,5.47594777650948,128.557922392943));
#145854=CARTESIAN_POINT('Ctrl Pts',(101.947475427788,5.41442048453332,128.413403468563));
#145855=CARTESIAN_POINT('Ctrl Pts',(101.940052161383,5.3471461327407,128.271386318917));
#145856=CARTESIAN_POINT('Ctrl Pts',(101.932637668662,5.27995129364506,128.129537021748));
#145857=CARTESIAN_POINT('Ctrl Pts',(101.925223175941,5.20702307358521,127.990183947674));
#145858=CARTESIAN_POINT('Ctrl Pts',(101.91780868322,5.12857227445554,127.853822194128));
#145859=CARTESIAN_POINT('Ctrl Pts',(101.910401336866,5.05019708915963,127.717591871173));
#145860=CARTESIAN_POINT('Ctrl Pts',(101.902993990512,4.96631010648422,127.584347450367));
#145861=CARTESIAN_POINT('Ctrl Pts',(101.895586644158,4.87716932730788,127.454562128811));
#145862=CARTESIAN_POINT('Ctrl Pts',(101.888184822483,4.78809503268775,127.324873606044));
#145863=CARTESIAN_POINT('Ctrl Pts',(101.880783000807,4.69377495422336,127.19863935193));
#145864=CARTESIAN_POINT('Ctrl Pts',(101.873381179132,4.5945118805448,127.076306012007));
#145865=CARTESIAN_POINT('Ctrl Pts',(101.865983264821,4.49530120707003,126.954037250901));
#145866=CARTESIAN_POINT('Ctrl Pts',(101.858585350509,4.39115296967782,126.835665592008));
#145867=CARTESIAN_POINT('Ctrl Pts',(101.851187436198,4.28241186903464,126.721606749593));
#145868=CARTESIAN_POINT('Ctrl Pts',(101.843790751286,4.17368883918985,126.607566861688));
#145869=CARTESIAN_POINT('Ctrl Pts',(101.836394066373,4.06037471825631,126.497838637721));
#145870=CARTESIAN_POINT('Ctrl Pts',(101.828997381461,3.94285297742602,126.392802960581));
#145871=CARTESIAN_POINT('Ctrl Pts',(101.821601024526,3.82533644763288,126.287771940833));
#145872=CARTESIAN_POINT('Ctrl Pts',(101.81420466759,3.70361294724021,126.187433302954));
#145873=CARTESIAN_POINT('Ctrl Pts',(101.806808310655,3.5781009218694,126.092129261253));
#145874=CARTESIAN_POINT('Ctrl Pts',(101.799410821318,3.45256968028745,125.996810628261));
#145875=CARTESIAN_POINT('Ctrl Pts',(101.792013331982,3.32324905612667,125.906528351994));
#145876=CARTESIAN_POINT('Ctrl Pts',(101.784615842645,3.19058838101215,125.821582642836));
#145877=CARTESIAN_POINT('Ctrl Pts',(101.77721576013,3.05788120190286,125.736607156092));
#145878=CARTESIAN_POINT('Ctrl Pts',(101.769815677615,2.92183195486256,125.656972162231));
#145879=CARTESIAN_POINT('Ctrl Pts',(101.7624155951,2.78291644500274,125.582932975375));
#145880=CARTESIAN_POINT('Ctrl Pts',(101.755007375434,2.64384818325936,125.508812374822));
#145881=CARTESIAN_POINT('Ctrl Pts',(101.747599155767,2.5019076940745,125.440300045235));
#145882=CARTESIAN_POINT('Ctrl Pts',(101.740190936101,2.35759339633895,125.377604317525));
#145883=CARTESIAN_POINT('Ctrl Pts',(101.732778156799,2.21319027556084,125.31487000164));
#145884=CARTESIAN_POINT('Ctrl Pts',(101.725365377496,2.06641078217233,125.257959555909));
#145885=CARTESIAN_POINT('Ctrl Pts',(101.717952598194,1.91777004061455,125.207031912387));
#145886=CARTESIAN_POINT('Ctrl Pts',(101.710529227166,1.76891691419489,125.156031501059));
#145887=CARTESIAN_POINT('Ctrl Pts',(101.703105856137,1.61819758485778,125.111031071743));
#145888=CARTESIAN_POINT('Ctrl Pts',(101.695682485108,1.46613975229401,125.072138989851));
#145889=CARTESIAN_POINT('Ctrl Pts',(101.691746435667,1.38551504089039,125.051517474829));
#145890=CARTESIAN_POINT('Ctrl Pts',(101.687810386226,1.30451416695347,125.032612375321));
#145891=CARTESIAN_POINT('Ctrl Pts',(101.683874336786,1.2232164281044,125.015433935312));
#145892=CARTESIAN_POINT('Ctrl Pts',(101.67645107038,1.06989142985194,124.983035933576));
#145893=CARTESIAN_POINT('Ctrl Pts',(101.669027803975,0.915046561581508,
124.95668457816));
#145894=CARTESIAN_POINT('Ctrl Pts',(101.661604537569,0.759200081038398,
124.936520657287));
#145895=CARTESIAN_POINT('Ctrl Pts',(101.654190044848,0.603537798092602,
124.916380568493));
#145896=CARTESIAN_POINT('Ctrl Pts',(101.646775552127,0.446876625876293,
124.902413405039));
#145897=CARTESIAN_POINT('Ctrl Pts',(101.639361059406,0.289747047455172,
124.894709425576));
#145898=CARTESIAN_POINT('Ctrl Pts',(101.631953713052,0.132768916437669,
124.887012871498));
#145899=CARTESIAN_POINT('Ctrl Pts',(101.624546366699,-0.024676351654649,
124.885567501704));
#145900=CARTESIAN_POINT('Ctrl Pts',(101.617139020345,-0.182051186920557,
124.89041202734));
#145901=CARTESIAN_POINT('Ctrl Pts',(101.609737198669,-0.339308646096463,
124.895252939745));
#145902=CARTESIAN_POINT('Ctrl Pts',(101.602335376994,-0.496495405527897,
124.906374395249));
#145903=CARTESIAN_POINT('Ctrl Pts',(101.594933555319,-0.653072025024084,
124.923763072024));
#145904=CARTESIAN_POINT('Ctrl Pts',(101.587535641007,-0.809565988942297,
124.941142569453));
#145905=CARTESIAN_POINT('Ctrl Pts',(101.580137726696,-0.965450084301358,
124.964782658182));
#145906=CARTESIAN_POINT('Ctrl Pts',(101.572739812385,-1.1201882397861,124.994618035494));
#145907=CARTESIAN_POINT('Ctrl Pts',(101.565343127472,-1.27490068059598,
125.024448454707));
#145908=CARTESIAN_POINT('Ctrl Pts',(101.55794644256,-1.42846719329978,125.060472048556));
#145909=CARTESIAN_POINT('Ctrl Pts',(101.550549757648,-1.58036005478951,
125.102572068371));
#145910=CARTESIAN_POINT('Ctrl Pts',(101.543153400713,-1.7322461811907,125.144670221428));
#145911=CARTESIAN_POINT('Ctrl Pts',(101.535757043777,-1.88245844419995,
125.192844165016));
#145912=CARTESIAN_POINT('Ctrl Pts',(101.528360686842,-2.03048274914784,
125.246926824176));
#145913=CARTESIAN_POINT('Ctrl Pts',(101.520963197505,-2.17852971699439,
125.301017763529));
#145914=CARTESIAN_POINT('Ctrl Pts',(101.513565708169,-2.32438770913538,
125.361019091596));
#145915=CARTESIAN_POINT('Ctrl Pts',(101.506168218832,-2.46756127535356,
125.426715044002));
#145916=CARTESIAN_POINT('Ctrl Pts',(101.498768136317,-2.61078503084301,
125.492434026021));
#145917=CARTESIAN_POINT('Ctrl Pts',(101.491368053802,-2.75132214776985,
125.563851451296));
#145918=CARTESIAN_POINT('Ctrl Pts',(101.483967971287,-2.88870063884851,
125.640705015029));
#145919=CARTESIAN_POINT('Ctrl Pts',(101.476559751621,-3.02623019170205,
125.717643087156));
#145920=CARTESIAN_POINT('Ctrl Pts',(101.469151531954,-3.16059385644758,
125.800029053022));
#145921=CARTESIAN_POINT('Ctrl Pts',(101.461743312288,-3.29134695080476,
125.887556186645));
#145922=CARTESIAN_POINT('Ctrl Pts',(101.454330532986,-3.42218052150978,
125.975137191757));
#145923=CARTESIAN_POINT('Ctrl Pts',(101.446917753684,-3.54939879275536,
126.067865450524));
#145924=CARTESIAN_POINT('Ctrl Pts',(101.439504974382,-3.67258961316041,
126.16539348082));
#145925=CARTESIAN_POINT('Ctrl Pts',(101.432081603353,-3.79595645438663,
126.26306086374));
#145926=CARTESIAN_POINT('Ctrl Pts',(101.424658232324,-3.91528406907986,
126.365541472862));
#145927=CARTESIAN_POINT('Ctrl Pts',(101.417234861295,-4.03019605177665,
126.472449913645));
#145928=CARTESIAN_POINT('Ctrl Pts',(101.413298811855,-4.09112514227896,
126.529135334182));
#145929=CARTESIAN_POINT('Ctrl Pts',(101.409362762414,-4.15081348883542,
126.587064995423));
#145930=CARTESIAN_POINT('Ctrl Pts',(101.405426712973,-4.2092096105901,126.646177719158));
#145931=CARTESIAN_POINT('Ctrl Pts',(101.398103766296,-4.31785450750161,
126.756155840706));
#145932=CARTESIAN_POINT('Ctrl Pts',(101.390780819619,-4.42237227151351,
126.870583452434));
#145933=CARTESIAN_POINT('Ctrl Pts',(101.383457872942,-4.52236893674723,
126.989113605583));
#145934=CARTESIAN_POINT('Ctrl Pts',(101.37614376298,-4.62224493444518,127.107500726547));
#145935=CARTESIAN_POINT('Ctrl Pts',(101.368829653017,-4.71761044316818,
127.229980248052));
#145936=CARTESIAN_POINT('Ctrl Pts',(101.361515543054,-4.80810695455015,
127.356167166481));
#145937=CARTESIAN_POINT('Ctrl Pts',(101.35420977717,-4.89850022574951,127.482210128415));
#145938=CARTESIAN_POINT('Ctrl Pts',(101.346904011286,-4.98403533882533,
127.611951754446));
#145939=CARTESIAN_POINT('Ctrl Pts',(101.339598245403,-5.06439317574481,
127.744973044216));
#145940=CARTESIAN_POINT('Ctrl Pts',(101.332297196746,-5.14469912677806,
127.877908444074));
#145941=CARTESIAN_POINT('Ctrl Pts',(101.324996148089,-5.21983425330153,
128.01411896797));
#145942=CARTESIAN_POINT('Ctrl Pts',(101.317695099432,-5.2895219147003,128.153155518671));
#145943=CARTESIAN_POINT('Ctrl Pts',(101.310397231159,-5.35917921969485,
128.292131504136));
#145944=CARTESIAN_POINT('Ctrl Pts',(101.303099362887,-5.42339360907288,
128.433930724259));
#145945=CARTESIAN_POINT('Ctrl Pts',(101.295801494615,-5.48193384866948,
128.578078550686));
#145946=CARTESIAN_POINT('Ctrl Pts',(101.288505272512,-5.54046088343661,
128.722193861915));
#145947=CARTESIAN_POINT('Ctrl Pts',(101.281209050408,-5.59331617186153,
128.868656369036));
#145948=CARTESIAN_POINT('Ctrl Pts',(101.273912828305,-5.64031631067929,
129.016970766978));
#145949=CARTESIAN_POINT('Ctrl Pts',(101.266614230649,-5.68733175211061,
129.165333454095));
#145950=CARTESIAN_POINT('Ctrl Pts',(101.259315632994,-5.72848811293174,
129.315548871925));
#145951=CARTESIAN_POINT('Ctrl Pts',(101.252017035339,-5.76365158385039,
129.467105599823));
#145952=CARTESIAN_POINT('Ctrl Pts',(101.244717423453,-5.79881994116889,
129.618683388405));
#145953=CARTESIAN_POINT('Ctrl Pts',(101.237417811567,-5.82799367149967,
129.771602481803));
#145954=CARTESIAN_POINT('Ctrl Pts',(101.230118199681,-5.8510901061574,129.925341202464));
#145955=CARTESIAN_POINT('Ctrl Pts',(101.222812013546,-5.87420734215359,
130.079218384805));
#145956=CARTESIAN_POINT('Ctrl Pts',(101.215505827412,-5.89123629851133,
130.233916287517));
#145957=CARTESIAN_POINT('Ctrl Pts',(101.208199641278,-5.90214615682664,
130.388907484281));
#145958=CARTESIAN_POINT('Ctrl Pts',(101.201591491589,-5.91201368216852,
130.529090749511));
#145959=CARTESIAN_POINT('Ctrl Pts',(101.1949833419,-5.91687615839487,130.669513687404));
#145960=CARTESIAN_POINT('Ctrl Pts',(101.188375192211,-5.91674751171398,
130.809786953944));
#145961=CARTESIAN_POINT('',(99.4383751922114,-5.92157883723614,130.802066910743));
#145962=CARTESIAN_POINT('Ctrl Pts',(101.188375192211,-5.91748097844663,
130.809787626617));
#145963=CARTESIAN_POINT('Ctrl Pts',(101.167909824527,-5.92152051365936,
131.244270330207));
#145964=CARTESIAN_POINT('Ctrl Pts',(101.054628582244,-5.67922493894598,
133.644781142275));
#145965=CARTESIAN_POINT('Ctrl Pts',(100.848531465343,-2.40383848871005,
137.376964443327));
#145966=CARTESIAN_POINT('Ctrl Pts',(100.570083841535,4.23038432426813,136.379430930968));
#145967=CARTESIAN_POINT('Ctrl Pts',(100.29163621772,6.97709060900665,130.258680157901));
#145968=CARTESIAN_POINT('Ctrl Pts',(100.013188593908,3.3121914738928,124.6393830693));
#145969=CARTESIAN_POINT('Ctrl Pts',(99.7347409700951,-3.39644981617912,
124.685399171656));
#145970=CARTESIAN_POINT('Ctrl Pts',(99.543136502863,-5.86504781316068,128.586362303126));
#145971=CARTESIAN_POINT('Ctrl Pts',(99.444347910235,-5.92608242641807,130.675707350711));
#145972=CARTESIAN_POINT('Ctrl Pts',(99.4383751922114,-5.92545872057778,
130.802065407881));
#145973=CARTESIAN_POINT('',(97.688375206741,-5.91312254842892,130.800045764439));
#145974=CARTESIAN_POINT('Ctrl Pts',(99.4383751922114,-5.91674955613188,
130.802068781351));
#145975=CARTESIAN_POINT('Ctrl Pts',(99.431023129912,-5.91680971516,130.95737913934));
#145976=CARTESIAN_POINT('Ctrl Pts',(99.4236710676126,-5.91075049538843,
131.112939264388));
#145977=CARTESIAN_POINT('Ctrl Pts',(99.4163190053132,-5.89853912438324,
131.268221330087));
#145978=CARTESIAN_POINT('Ctrl Pts',(99.408975301965,-5.88634163713612,131.423326847334));
#145979=CARTESIAN_POINT('Ctrl Pts',(99.4016315986168,-5.86800594686994,
131.578154558207));
#145980=CARTESIAN_POINT('Ctrl Pts',(99.3942878952686,-5.84355125337422,
131.732174883294));
#145981=CARTESIAN_POINT('Ctrl Pts',(99.3869508649334,-5.8191187811586,131.88605525452));
#145982=CARTESIAN_POINT('Ctrl Pts',(99.3796138345983,-5.78857843098604,
132.039129326219));
#145983=CARTESIAN_POINT('Ctrl Pts',(99.3722768042632,-5.75200132330698,
132.190871107672));
#145984=CARTESIAN_POINT('Ctrl Pts',(99.3649447671003,-5.71544910796076,
132.34250962216));
#145985=CARTESIAN_POINT('Ctrl Pts',(99.3576127299374,-5.6728684020007,132.492817282297));
#145986=CARTESIAN_POINT('Ctrl Pts',(99.3502806927746,-5.62438163597361,
132.641276994384));
#145987=CARTESIAN_POINT('Ctrl Pts',(99.3429512462964,-5.57591200214526,
132.789684250069));
#145988=CARTESIAN_POINT('Ctrl Pts',(99.3356217998181,-5.52154057596112,
132.936244494583));
#145989=CARTESIAN_POINT('Ctrl Pts',(99.3282923533399,-5.46143998898768,
133.080454598312));
#145990=CARTESIAN_POINT('Ctrl Pts',(99.3209641084283,-5.40134925471783,
133.224641060683));
#145991=CARTESIAN_POINT('Ctrl Pts',(99.3136358635168,-5.33553137435344,
133.36647779707));
#145992=CARTESIAN_POINT('Ctrl Pts',(99.3063076186053,-5.2642074849828,133.505480777343));
#145993=CARTESIAN_POINT('Ctrl Pts',(99.2989790617049,-5.19288055910685,
133.644489675454));
#145994=CARTESIAN_POINT('Ctrl Pts',(99.2916505048046,-5.11604733151058,
133.780664238252));
#145995=CARTESIAN_POINT('Ctrl Pts',(99.2843219479042,-5.0339752224617,133.913544436857));
#145996=CARTESIAN_POINT('Ctrl Pts',(99.2769915654631,-4.9518826692811,134.04645773587));
#145997=CARTESIAN_POINT('Ctrl Pts',(99.269661183022,-4.86454883783369,134.176074713569));
#145998=CARTESIAN_POINT('Ctrl Pts',(99.2623308005808,-4.77228470195073,
134.301963980732));
#145999=CARTESIAN_POINT('Ctrl Pts',(99.2549928040885,-4.67992473152374,
134.427984008784));
#146000=CARTESIAN_POINT('Ctrl Pts',(99.2476548075961,-4.58262445388987,
134.550268285244));
#146001=CARTESIAN_POINT('Ctrl Pts',(99.2403168111037,-4.48073581656695,
134.668417695901));
#146002=CARTESIAN_POINT('Ctrl Pts',(99.2329748443228,-4.37879205148796,
134.786631032352));
#146003=CARTESIAN_POINT('Ctrl Pts',(99.225632877542,-4.27225524109257,134.900704768478));
#146004=CARTESIAN_POINT('Ctrl Pts',(99.2182909107612,-4.16151397634769,
135.010276925241));
#146005=CARTESIAN_POINT('Ctrl Pts',(99.2109378862937,-4.05060592493055,
135.12001410789));
#146006=CARTESIAN_POINT('Ctrl Pts',(99.2035848618261,-3.93548105011751,
135.225235910576));
#146007=CARTESIAN_POINT('Ctrl Pts',(99.1962318373586,-3.81656147570949,
135.325620294319));
#146008=CARTESIAN_POINT('Ctrl Pts',(99.1901031323955,-3.71744267240554,
135.40929011938));
#146009=CARTESIAN_POINT('Ctrl Pts',(99.1839744274325,-3.61568830166646,
135.489600015005));
#146010=CARTESIAN_POINT('Ctrl Pts',(99.1778457224694,-3.51155721606452,
135.566387127447));
#146011=CARTESIAN_POINT('Ctrl Pts',(99.1704224560639,-3.38543060462471,
135.659393920168));
#146012=CARTESIAN_POINT('Ctrl Pts',(99.1629991896585,-3.25541566851069,
135.747527021494));
#146013=CARTESIAN_POINT('Ctrl Pts',(99.1555759232531,-3.12192577321451,
135.830443588334));
#146014=CARTESIAN_POINT('Ctrl Pts',(99.148161430532,-2.98859365188864,135.913262154677));
#146015=CARTESIAN_POINT('Ctrl Pts',(99.140746937811,-2.85179506061965,135.990876263974));
#146016=CARTESIAN_POINT('Ctrl Pts',(99.13333244509,-2.71197542525192,136.062983997818));
#146017=CARTESIAN_POINT('Ctrl Pts',(99.1259250987362,-2.57229055331288,
136.135022231512));
#146018=CARTESIAN_POINT('Ctrl Pts',(99.1185177523824,-2.42959076363607,
136.201564485492));
#146019=CARTESIAN_POINT('Ctrl Pts',(99.1111104060286,-2.28434928734665,
136.262352821289));
#146020=CARTESIAN_POINT('Ctrl Pts',(99.1037085843533,-2.13921613763021,
136.323095818851));
#146021=CARTESIAN_POINT('Ctrl Pts',(99.0963067626779,-1.99154541873936,
136.378093299661));
#146022=CARTESIAN_POINT('Ctrl Pts',(99.0889049410025,-1.84183362036898,
136.427133908157));
#146023=CARTESIAN_POINT('Ctrl Pts',(99.0815070266911,-1.69220085369213,
136.476148628497));
#146024=CARTESIAN_POINT('Ctrl Pts',(99.0741091123798,-1.54052950722125,
136.519212623207));
#146025=CARTESIAN_POINT('Ctrl Pts',(99.0667111980685,-1.38733453922557,
136.556163242724));
#146026=CARTESIAN_POINT('Ctrl Pts',(99.0593145131563,-1.23416502945379,
136.593107721718));
#146027=CARTESIAN_POINT('Ctrl Pts',(99.0519178282441,-1.07947276321659,
136.623940754398));
#146028=CARTESIAN_POINT('Ctrl Pts',(99.0445211433319,-0.923786413810061,
136.64854997317));
#146029=CARTESIAN_POINT('Ctrl Pts',(99.0371247863964,-0.768106967699302,
136.673158100744));
#146030=CARTESIAN_POINT('Ctrl Pts',(99.029728429461,-0.611433894782134,
136.691542904848));
#146031=CARTESIAN_POINT('Ctrl Pts',(99.0223320725256,-0.454304313731296,
136.703643468305));
#146032=CARTESIAN_POINT('Ctrl Pts',(99.014934583189,-0.297150675740802,
136.715745884389));
#146033=CARTESIAN_POINT('Ctrl Pts',(99.0075370938524,-0.139540762671032,
136.721562115426));
#146034=CARTESIAN_POINT('Ctrl Pts',(99.0001396045159,0.0179851048732815,
136.721083282902));
#146035=CARTESIAN_POINT('Ctrl Pts',(98.9927395220009,0.175566192866603,
136.720604282524));
#146036=CARTESIAN_POINT('Ctrl Pts',(98.9853394394859,0.333062803612473,
136.713825826146));
#146037=CARTESIAN_POINT('Ctrl Pts',(98.9779393569709,0.489936690396937,
136.700791114223));
#146038=CARTESIAN_POINT('Ctrl Pts',(98.9705311373045,0.646983076146948,
136.687742069293));
#146039=CARTESIAN_POINT('Ctrl Pts',(98.963122917638,0.803404998202632,136.668423061143));
#146040=CARTESIAN_POINT('Ctrl Pts',(98.9557146979715,0.958670658559488,
136.642929032076));
#146041=CARTESIAN_POINT('Ctrl Pts',(98.9483019186694,1.11403188233977,136.61741931186));
#146042=CARTESIAN_POINT('Ctrl Pts',(98.9408891393674,1.26823506154246,136.585727072488));
#146043=CARTESIAN_POINT('Ctrl Pts',(98.9334763600653,1.42076112157449,136.547997827377));
#146044=CARTESIAN_POINT('Ctrl Pts',(98.9260529890365,1.57350511799364,136.510214672951));
#146045=CARTESIAN_POINT('Ctrl Pts',(98.9186296180078,1.72456685164282,136.466377388575));
#146046=CARTESIAN_POINT('Ctrl Pts',(98.911206246979,1.87344407558823,136.416680802493));
#146047=CARTESIAN_POINT('Ctrl Pts',(98.9072701975382,1.95238235198493,136.390330480099));
#146048=CARTESIAN_POINT('Ctrl Pts',(98.9033341480973,2.03070683371787,136.362333695868));
#146049=CARTESIAN_POINT('Ctrl Pts',(98.8993980986565,2.10834532052523,136.332724803464));
#146050=CARTESIAN_POINT('Ctrl Pts',(98.8919748322511,2.25476908362792,136.276883356452));
#146051=CARTESIAN_POINT('Ctrl Pts',(98.8845515658457,2.39919420659289,136.215136202522));
#146052=CARTESIAN_POINT('Ctrl Pts',(98.8771282994402,2.54110881167391,136.147645802706));
#146053=CARTESIAN_POINT('Ctrl Pts',(98.8697138067192,2.68285568547721,136.080235170937));
#146054=CARTESIAN_POINT('Ctrl Pts',(98.8622993139982,2.82209761384657,136.007094963671));
#146055=CARTESIAN_POINT('Ctrl Pts',(98.8548848212772,2.95833982072648,135.92843673601));
#146056=CARTESIAN_POINT('Ctrl Pts',(98.8474774749235,3.09445071223768,135.84985432211));
#146057=CARTESIAN_POINT('Ctrl Pts',(98.8400701285697,3.22756731704156,135.765764661248));
#146058=CARTESIAN_POINT('Ctrl Pts',(98.832662782216,3.35721683121657,135.67642647413));
#146059=CARTESIAN_POINT('Ctrl Pts',(98.8252609605406,3.48676964789279,135.587154918802));
#146060=CARTESIAN_POINT('Ctrl Pts',(98.8178591388652,3.61286021672606,135.492642842513));
#146061=CARTESIAN_POINT('Ctrl Pts',(98.8104573171898,3.73504235348902,135.393193713261));
#146062=CARTESIAN_POINT('Ctrl Pts',(98.8030594028784,3.85715999125305,135.29379708243));
#146063=CARTESIAN_POINT('Ctrl Pts',(98.7956614885671,3.97537301718541,135.189468824126));
#146064=CARTESIAN_POINT('Ctrl Pts',(98.7882635742557,4.08926624207776,135.080554271261));
#146065=CARTESIAN_POINT('Ctrl Pts',(98.7808668893435,4.20314053998237,134.97165781802));
#146066=CARTESIAN_POINT('Ctrl Pts',(98.7734702044313,4.31269619208334,134.858176840624));
#146067=CARTESIAN_POINT('Ctrl Pts',(98.7660735195191,4.41755289951034,134.740495389462));
#146068=CARTESIAN_POINT('Ctrl Pts',(98.7586771625837,4.52240495748097,134.622819156418));
#146069=CARTESIAN_POINT('Ctrl Pts',(98.7512808056482,4.62255823672275,134.500943098654));
#146070=CARTESIAN_POINT('Ctrl Pts',(98.7438844487128,4.71767116012618,134.375286182096));
#146071=CARTESIAN_POINT('Ctrl Pts',(98.7364869593762,4.81279864556113,134.249610027143));
#146072=CARTESIAN_POINT('Ctrl Pts',(98.7290894700397,4.90288401330732,134.120152158478));
#146073=CARTESIAN_POINT('Ctrl Pts',(98.7216919807031,4.98762773713472,133.987362364073));
#146074=CARTESIAN_POINT('Ctrl Pts',(98.7142918981881,5.07240116774308,133.854526020411));
#146075=CARTESIAN_POINT('Ctrl Pts',(98.7068918156731,5.15182902559318,133.71835574001));
#146076=CARTESIAN_POINT('Ctrl Pts',(98.6994917331581,5.22565672095441,133.579327715973));
#146077=CARTESIAN_POINT('Ctrl Pts',(98.6920835134917,5.29956559745636,133.440146816332));
#146078=CARTESIAN_POINT('Ctrl Pts',(98.6846752938252,5.3678618384454,133.29810222741));
#146079=CARTESIAN_POINT('Ctrl Pts',(98.6772670741587,5.43033787176085,133.153692684563));
#146080=CARTESIAN_POINT('Ctrl Pts',(98.6698542948567,5.49285235803233,133.009194260052));
#146081=CARTESIAN_POINT('Ctrl Pts',(98.6624415155546,5.54953936445879,132.862328328622));
#146082=CARTESIAN_POINT('Ctrl Pts',(98.6550287362526,5.60024074310215,132.713610255984));
#146083=CARTESIAN_POINT('Ctrl Pts',(98.6476053652238,5.65101456625302,132.564679687989));
#146084=CARTESIAN_POINT('Ctrl Pts',(98.6401819941951,5.6957855742973,132.41389205019));
#146085=CARTESIAN_POINT('Ctrl Pts',(98.6327586231663,5.73444620501691,132.261775206579));
#146086=CARTESIAN_POINT('Ctrl Pts',(98.6288225737255,5.75494499907408,132.1811192061));
#146087=CARTESIAN_POINT('Ctrl Pts',(98.6248865242845,5.77372680714943,132.100089655617));
#146088=CARTESIAN_POINT('Ctrl Pts',(98.6209504748437,5.79078150594723,132.018765868246));
#146089=CARTESIAN_POINT('Ctrl Pts',(98.6135272084382,5.82294613562024,131.865391743297));
#146090=CARTESIAN_POINT('Ctrl Pts',(98.6061039420328,5.84906181299111,131.710506952057));
#146091=CARTESIAN_POINT('Ctrl Pts',(98.5986806756273,5.86898853870163,131.554629965926));
#146092=CARTESIAN_POINT('Ctrl Pts',(98.5912661829063,5.88889171267715,131.398937213448));
#146093=CARTESIAN_POINT('Ctrl Pts',(98.5838516901853,5.90262044832208,131.242254966998));
#146094=CARTESIAN_POINT('Ctrl Pts',(98.5764371974642,5.91008529439362,131.085113846385));
#146095=CARTESIAN_POINT('Ctrl Pts',(98.5690298511104,5.91754294556548,130.9281241843));
#146096=CARTESIAN_POINT('Ctrl Pts',(98.5616225047566,5.91874870878988,130.77067689892));
#146097=CARTESIAN_POINT('Ctrl Pts',(98.5542151584028,5.913664691055,130.613309618434));
#146098=CARTESIAN_POINT('Ctrl Pts',(98.5468133367274,5.90858446517237,130.456059708404));
#146099=CARTESIAN_POINT('Ctrl Pts',(98.539411515052,5.89722381105688,130.298890055954));
#146100=CARTESIAN_POINT('Ctrl Pts',(98.5320096933766,5.87959687145631,130.142340080376));
#146101=CARTESIAN_POINT('Ctrl Pts',(98.5246117790652,5.86197923697987,129.985872746311));
#146102=CARTESIAN_POINT('Ctrl Pts',(98.5172138647539,5.83810194656837,129.830024807654));
#146103=CARTESIAN_POINT('Ctrl Pts',(98.5098159504425,5.80803111867375,129.675332235718));
#146104=CARTESIAN_POINT('Ctrl Pts',(98.5024192655302,5.77796528800529,129.520665370882));
#146105=CARTESIAN_POINT('Ctrl Pts',(98.495022580618,5.74170803378008,129.367153857783));
#146106=CARTESIAN_POINT('Ctrl Pts',(98.4876258957058,5.69937690763675,129.215325241246));
#146107=CARTESIAN_POINT('Ctrl Pts',(98.4802295387703,5.65704765849982,129.063503356948));
#146108=CARTESIAN_POINT('Ctrl Pts',(98.4728331818348,5.60864517320242,128.913364580423));
#146109=CARTESIAN_POINT('Ctrl Pts',(98.4654368248993,5.55433730887498,128.765422751485));
#146110=CARTESIAN_POINT('Ctrl Pts',(98.4580393355627,5.50002112987499,128.617458272275));
#146111=CARTESIAN_POINT('Ctrl Pts',(98.4506418462262,5.43979790025302,128.471691760842));
#146112=CARTESIAN_POINT('Ctrl Pts',(98.4432443568896,5.37388413812647,128.328618338472));
#146113=CARTESIAN_POINT('Ctrl Pts',(98.4358442743745,5.30794727003245,128.185494761935));
#146114=CARTESIAN_POINT('Ctrl Pts',(98.4284441918595,5.23631605388839,128.04506649291));
#146115=CARTESIAN_POINT('Ctrl Pts',(98.4210441093444,5.15925351247204,127.907805118953));
#146116=CARTESIAN_POINT('Ctrl Pts',(98.4136358896779,5.08210623286946,127.770392812005));
#146117=CARTESIAN_POINT('Ctrl Pts',(98.4062276700114,4.99951588377923,127.636154680266));
#146118=CARTESIAN_POINT('Ctrl Pts',(98.398819450345,4.9117898675597,127.505534938716));
#146119=CARTESIAN_POINT('Ctrl Pts',(98.3914066710429,4.82400985744078,127.374834802895));
#146120=CARTESIAN_POINT('Ctrl Pts',(98.3839938917408,4.73108810149869,127.247757795591));
#146121=CARTESIAN_POINT('Ctrl Pts',(98.3765811124387,4.63337270867953,127.124715538898));
#146122=CARTESIAN_POINT('Ctrl Pts',(98.3691577414099,4.53551769552477,127.00149747366));
#146123=CARTESIAN_POINT('Ctrl Pts',(98.3617343703811,4.43285560875591,126.882325955187));
#146124=CARTESIAN_POINT('Ctrl Pts',(98.3543109993523,4.32577241529428,126.767576802005));
#146125=CARTESIAN_POINT('Ctrl Pts',(98.3503749499117,4.26899433669849,126.706734047623));
#146126=CARTESIAN_POINT('Ctrl Pts',(98.3464389004712,4.21097390704092,126.647133929272));
#146127=CARTESIAN_POINT('Ctrl Pts',(98.3425028510307,4.15177238280614,126.588827834647));
#146128=CARTESIAN_POINT('Ctrl Pts',(98.3350795846252,4.0401201557092,126.478864359847));
#146129=CARTESIAN_POINT('Ctrl Pts',(98.3276563182197,3.92392735580368,126.373173487904));
#146130=CARTESIAN_POINT('Ctrl Pts',(98.3202330518143,3.80355451469021,126.272153250699));
#146131=CARTESIAN_POINT('Ctrl Pts',(98.3128185590933,3.68332394427833,126.171252411025));
#146132=CARTESIAN_POINT('Ctrl Pts',(98.3054040663723,3.55892344982694,126.075011455526));
#146133=CARTESIAN_POINT('Ctrl Pts',(98.2979895736513,3.43075110622816,125.983792455034));
#146134=CARTESIAN_POINT('Ctrl Pts',(98.2905822272975,3.30270229995984,125.892661374849));
#146135=CARTESIAN_POINT('Ctrl Pts',(98.2831748809437,3.17088918410599,125.806542828488));
#146136=CARTESIAN_POINT('Ctrl Pts',(98.27576753459,3.0357435983912,125.725759297584));
#146137=CARTESIAN_POINT('Ctrl Pts',(98.2683657129146,2.90069880935358,125.645036018085));
#146138=CARTESIAN_POINT('Ctrl Pts',(98.2609638912392,2.76232681842323,125.569640021911));
#146139=CARTESIAN_POINT('Ctrl Pts',(98.2535620695638,2.62108909882881,125.499850979673));
#146140=CARTESIAN_POINT('Ctrl Pts',(98.2461641552525,2.47992593752656,125.430098778526));
#146141=CARTESIAN_POINT('Ctrl Pts',(98.2387662409411,2.33590039418907,125.365947801548));
#146142=CARTESIAN_POINT('Ctrl Pts',(98.2313683266298,2.18949913530127,125.307632126999));
#146143=CARTESIAN_POINT('Ctrl Pts',(98.2239716417176,2.0431222056468,125.249326143457));
#146144=CARTESIAN_POINT('Ctrl Pts',(98.2165749568053,1.89437069046328,125.196853675738));
#146145=CARTESIAN_POINT('Ctrl Pts',(98.2091782718931,1.74375196768514,125.150400975183));
#146146=CARTESIAN_POINT('Ctrl Pts',(98.2017819149577,1.59313992349878,125.10395033439));
#146147=CARTESIAN_POINT('Ctrl Pts',(98.1943855580222,1.44066119305779,125.063519040045));
#146148=CARTESIAN_POINT('Ctrl Pts',(98.1869892010868,1.28683881522993,125.029243612161));
#146149=CARTESIAN_POINT('Ctrl Pts',(98.1795917117502,1.13299288680343,124.994962936622));
#146150=CARTESIAN_POINT('Ctrl Pts',(98.1721942224136,0.977803265767891,
124.966840085338));
#146151=CARTESIAN_POINT('Ctrl Pts',(98.164796733077,0.82180354501573,124.944960520636));
#146152=CARTESIAN_POINT('Ctrl Pts',(98.157396650562,0.665749138803402,124.923073286087));
#146153=CARTESIAN_POINT('Ctrl Pts',(98.149996568047,0.508884436922934,124.907433747371));
#146154=CARTESIAN_POINT('Ctrl Pts',(98.142596485532,0.351748369577102,124.89807552057));
#146155=CARTESIAN_POINT('Ctrl Pts',(98.1351882658656,0.194439514970794,
124.888707003436));
#146156=CARTESIAN_POINT('Ctrl Pts',(98.1277800461991,0.036859071852575,
124.885633614052));
#146157=CARTESIAN_POINT('Ctrl Pts',(98.1203718265326,-0.120453070650101,
124.888836835155));
#146158=CARTESIAN_POINT('Ctrl Pts',(98.1129590472305,-0.277862036151929,
124.892042027787));
#146159=CARTESIAN_POINT('Ctrl Pts',(98.1055462679284,-0.435002000231745,
124.901531506265));
#146160=CARTESIAN_POINT('Ctrl Pts',(98.0981334886263,-0.591338492174717,
124.917234888471));
#146161=CARTESIAN_POINT('Ctrl Pts',(98.0907101175975,-0.747898365028274,
124.932960708406));
#146162=CARTESIAN_POINT('Ctrl Pts',(98.0832867465688,-0.903652104190678,
124.954918112885));
#146163=CARTESIAN_POINT('Ctrl Pts',(98.07586337554,-1.05807489834628,124.982985516098));
#146164=CARTESIAN_POINT('Ctrl Pts',(98.0719273260993,-1.13995356913028,
124.99786752675));
#146165=CARTESIAN_POINT('Ctrl Pts',(98.0679912766585,-1.22145829612271,
125.014466437663));
#146166=CARTESIAN_POINT('Ctrl Pts',(98.0640552272178,-1.3025127347755,125.032758488326));
#146167=CARTESIAN_POINT('Ctrl Pts',(98.0566319608124,-1.4553788764545,125.067256725002));
#146168=CARTESIAN_POINT('Ctrl Pts',(98.049208694407,-1.60710464685679,125.107884520385));
#146169=CARTESIAN_POINT('Ctrl Pts',(98.0417854280016,-1.75716029435094,
125.154553694984));
#146170=CARTESIAN_POINT('Ctrl Pts',(98.0343709352805,-1.90703858853163,
125.201167710494));
#146171=CARTESIAN_POINT('Ctrl Pts',(98.0269564425595,-2.05525033598057,
125.253808782418));
#146172=CARTESIAN_POINT('Ctrl Pts',(98.0195419498385,-2.2012757470495,125.312337707203));
#146173=CARTESIAN_POINT('Ctrl Pts',(98.0121346034847,-2.34716041332917,
125.370810219607));
#146174=CARTESIAN_POINT('Ctrl Pts',(98.0047272571309,-2.49086259422015,
125.435159149245));
#146175=CARTESIAN_POINT('Ctrl Pts',(97.9973199107772,-2.63187755687176,
125.505195486327));
#146176=CARTESIAN_POINT('Ctrl Pts',(97.9899180891017,-2.77278734524423,
125.575179587667));
#146177=CARTESIAN_POINT('Ctrl Pts',(97.9825162674263,-2.91101357317273,
125.650842484954));
#146178=CARTESIAN_POINT('Ctrl Pts',(97.9751144457509,-3.0460715083007,125.731947096488));
#146179=CARTESIAN_POINT('Ctrl Pts',(97.9677165314396,-3.18105814739561,
125.813008893528));
#146180=CARTESIAN_POINT('Ctrl Pts',(97.9603186171283,-3.31287950537079,
125.899506492121));
#146181=CARTESIAN_POINT('Ctrl Pts',(97.9529207028169,-3.44107559043296,
125.991156970989));
#146182=CARTESIAN_POINT('Ctrl Pts',(97.9455240179047,-3.5692503716316,126.082792219209));
#146183=CARTESIAN_POINT('Ctrl Pts',(97.9381273329925,-3.69380077223537,
126.179578431282));
#146184=CARTESIAN_POINT('Ctrl Pts',(97.9307306480803,-3.81429584354901,
126.281189409179));
#146185=CARTESIAN_POINT('Ctrl Pts',(97.9233342911449,-3.934785571985,126.382795881538));
#146186=CARTESIAN_POINT('Ctrl Pts',(97.9159379342095,-4.05122004329452,
126.489226453697));
#146187=CARTESIAN_POINT('Ctrl Pts',(97.908541577274,-4.16320168404008,126.600114870645));
#146188=CARTESIAN_POINT('Ctrl Pts',(97.9011440879375,-4.27520046946032,
126.711020264891));
#146189=CARTESIAN_POINT('Ctrl Pts',(97.8937465986009,-4.38274480161207,
126.826384600209));
#146190=CARTESIAN_POINT('Ctrl Pts',(97.8863491092644,-4.48547435862851,
126.945805144259));
#146191=CARTESIAN_POINT('Ctrl Pts',(97.8789490267493,-4.58823992733302,
127.065267550997));
#146192=CARTESIAN_POINT('Ctrl Pts',(97.8715489442343,-4.68618711718988,
127.188788714636));
#146193=CARTESIAN_POINT('Ctrl Pts',(97.8641488617193,-4.77899634109947,
127.315933388246));
#146194=CARTESIAN_POINT('Ctrl Pts',(97.8567406420528,-4.87190761829117,
127.443217870495));
#146195=CARTESIAN_POINT('Ctrl Pts',(97.8493324223863,-4.95966942644447,
127.574133518166));
#146196=CARTESIAN_POINT('Ctrl Pts',(97.8419242027199,-5.04200552139587,
127.708216098214));
#146197=CARTESIAN_POINT('Ctrl Pts',(97.8345114234178,-5.12439229284004,
127.842381203853));
#146198=CARTESIAN_POINT('Ctrl Pts',(97.8270986441157,-5.20134651478244,
127.979716800978));
#146199=CARTESIAN_POINT('Ctrl Pts',(97.8196858648136,-5.27263850721605,
128.119735180988));
#146200=CARTESIAN_POINT('Ctrl Pts',(97.8122624937849,-5.34403236499151,
128.259953625824));
#146201=CARTESIAN_POINT('Ctrl Pts',(97.8048391227562,-5.40974767925094,
128.402862171217));
#146202=CARTESIAN_POINT('Ctrl Pts',(97.7974157517274,-5.46960307024504,
128.547953558442));
#146203=CARTESIAN_POINT('Ctrl Pts',(97.7934797022866,-5.50133983476077,
128.624884493369));
#146204=CARTESIAN_POINT('Ctrl Pts',(97.7895436528458,-5.53142999670768,
128.702428845323));
#146205=CARTESIAN_POINT('Ctrl Pts',(97.785607603405,-5.55985228038424,128.780509540336));
#146206=CARTESIAN_POINT('Ctrl Pts',(97.7770139152604,-5.62190745675972,
128.950985331644));
#146207=CARTESIAN_POINT('Ctrl Pts',(97.7684202271159,-5.67616396084671,
129.124443100668));
#146208=CARTESIAN_POINT('Ctrl Pts',(97.7598265389713,-5.72236577378178,
129.300212847714));
#146209=CARTESIAN_POINT('Ctrl Pts',(97.7512653268184,-5.768392987678,129.475318351802));
#146210=CARTESIAN_POINT('Ctrl Pts',(97.7427041146655,-5.80642618331576,
129.65271827668));
#146211=CARTESIAN_POINT('Ctrl Pts',(97.7341429025126,-5.83625879841363,
129.831728209901));
#146212=CARTESIAN_POINT('Ctrl Pts',(97.7256452108506,-5.86587006841195,
130.009409966851));
#146213=CARTESIAN_POINT('Ctrl Pts',(97.7171475191885,-5.88740192283493,
130.188677798431));
#146214=CARTESIAN_POINT('Ctrl Pts',(97.7086498275265,-5.9006995006581,130.368842574962));
#146215=CARTESIAN_POINT('Ctrl Pts',(97.7018916271594,-5.91127504268765,
130.512127328907));
#146216=CARTESIAN_POINT('Ctrl Pts',(97.6951334267924,-5.91664328977992,
130.65597899437));
#146217=CARTESIAN_POINT('Ctrl Pts',(97.6883752264253,-5.91674842443727,
130.800042699191));
#146218=CARTESIAN_POINT('',(95.9383751922114,-5.90973932447518,130.808309037287));
#146219=CARTESIAN_POINT('Ctrl Pts',(97.6883751922114,-5.91044616388941,
130.800048027004));
#146220=CARTESIAN_POINT('Ctrl Pts',(97.6279701213383,-5.90180813919648,
132.086330752508));
#146221=CARTESIAN_POINT('Ctrl Pts',(97.4747491758607,-4.85569580484173,
135.361851444278));
#146222=CARTESIAN_POINT('Ctrl Pts',(97.2287123557792,0.556297771968347,
137.780612714447));
#146223=CARTESIAN_POINT('Ctrl Pts',(96.9502647319661,6.17001100091076,134.107166209633));
#146224=CARTESIAN_POINT('Ctrl Pts',(96.6718171081533,6.11378554181002,127.398602716729));
#146225=CARTESIAN_POINT('Ctrl Pts',(96.3933694843406,0.439289844815531,
123.819764354175));
#146226=CARTESIAN_POINT('Ctrl Pts',(96.1488888456932,-4.89743273152406,
126.313026653818));
#146227=CARTESIAN_POINT('Ctrl Pts',(95.9972240816501,-5.90209215049429,
129.554787758123));
#146228=CARTESIAN_POINT('Ctrl Pts',(95.9383751922114,-5.90973932447518,
130.808309037287));
#146229=CARTESIAN_POINT('',(94.1883751922115,-5.92487953698549,130.807193534747));
#146230=CARTESIAN_POINT('Ctrl Pts',(95.9383751922114,-5.90973932447518,
130.808309037287));
#146231=CARTESIAN_POINT('Ctrl Pts',(95.9044082070458,-5.91415319613265,
131.531828870885));
#146232=CARTESIAN_POINT('Ctrl Pts',(95.7776253472764,-5.45539215556061,
134.226986472583));
#146233=CARTESIAN_POINT('Ctrl Pts',(95.5580266129015,-1.42598660733677,
137.655938736953));
#146234=CARTESIAN_POINT('Ctrl Pts',(95.2795789890891,4.99364612569024,135.707528868983));
#146235=CARTESIAN_POINT('Ctrl Pts',(95.0011313652761,6.82436202238293,129.25334691105));
#146236=CARTESIAN_POINT('Ctrl Pts',(94.7226837414632,2.38382260912524,124.224470778171));
#146237=CARTESIAN_POINT('Ctrl Pts',(94.4517650171081,-4.06803459211089,
125.214673966664));
#146238=CARTESIAN_POINT('Ctrl Pts',(94.2736621673578,-5.91423505740828,
129.002405790779));
#146239=CARTESIAN_POINT('Ctrl Pts',(94.1883751922115,-5.92487953698549,
130.807193534747));
#146240=CARTESIAN_POINT('',(92.4383751922114,-5.91809470196727,130.799038547181));
#146241=CARTESIAN_POINT('Ctrl Pts',(94.1883751922115,-5.92487953698549,
130.807193534747));
#146242=CARTESIAN_POINT('Ctrl Pts',(94.1808462927535,-5.92581920234919,
130.966515230048));
#146243=CARTESIAN_POINT('Ctrl Pts',(94.0805015186906,-5.84762556849407,
133.089009600992));
#146244=CARTESIAN_POINT('Ctrl Pts',(93.8873408700248,-3.29341206105117,
136.979390781575));
#146245=CARTESIAN_POINT('Ctrl Pts',(93.6088932462115,3.41505809786538,136.912956095953));
#146246=CARTESIAN_POINT('Ctrl Pts',(93.3304456223988,6.98525669970749,131.233020587166));
#146247=CARTESIAN_POINT('Ctrl Pts',(93.0519979985858,4.1363456432787,125.159167507523));
#146248=CARTESIAN_POINT('Ctrl Pts',(92.7735503747728,-2.51366498760439,
124.272971112994));
#146249=CARTESIAN_POINT('Ctrl Pts',(92.5690094393148,-5.70178004860599,
128.030938026362));
#146250=CARTESIAN_POINT('Ctrl Pts',(92.457284378461,-5.9222163663983,130.397769432159));
#146251=CARTESIAN_POINT('Ctrl Pts',(92.4383751922115,-5.91849239897776,
130.799038189537));
#146252=CARTESIAN_POINT('',(90.6883751922462,-5.91674998811213,130.803985550795));
#146253=CARTESIAN_POINT('Ctrl Pts',(92.4383751922115,-5.9167476075087,130.799039758607));
#146254=CARTESIAN_POINT('Ctrl Pts',(92.431072074229,-5.91688693521948,130.953970927748));
#146255=CARTESIAN_POINT('Ctrl Pts',(92.4237689562464,-5.91093675709542,
131.109097642124));
#146256=CARTESIAN_POINT('Ctrl Pts',(92.4164658382639,-5.89887780130397,
131.263894346234));
#146257=CARTESIAN_POINT('Ctrl Pts',(92.4091685072242,-5.88682840095014,
131.418568390449));
#146258=CARTESIAN_POINT('Ctrl Pts',(92.4018711761846,-5.86867988553666,
131.572912562971));
#146259=CARTESIAN_POINT('Ctrl Pts',(92.3945738451449,-5.84446504588668,
131.72640122942));
#146260=CARTESIAN_POINT('Ctrl Pts',(92.3871605652284,-5.8198654513932,131.882328710609));
#146261=CARTESIAN_POINT('Ctrl Pts',(92.3797472853118,-5.7890051060506,132.037372864326));
#146262=CARTESIAN_POINT('Ctrl Pts',(92.3723340053952,-5.75197330847544,
132.190987323311));
#146263=CARTESIAN_POINT('Ctrl Pts',(92.3650421934528,-5.71554828381093,
132.342084780733));
#146264=CARTESIAN_POINT('Ctrl Pts',(92.3577503815105,-5.67315260666512,
132.491798652156));
#146265=CARTESIAN_POINT('Ctrl Pts',(92.3504585695681,-5.62492277146484,
132.639619285317));
#146266=CARTESIAN_POINT('Ctrl Pts',(92.3431670707937,-5.5766950076346,132.787433569893));
#146267=CARTESIAN_POINT('Ctrl Pts',(92.3358755720193,-5.52263370339903,
132.933354411886));
#146268=CARTESIAN_POINT('Ctrl Pts',(92.3285840732449,-5.46292500449768,
133.076888055846));
#146269=CARTESIAN_POINT('Ctrl Pts',(92.3212913518392,-5.40320629370073,
133.220445767385));
#146270=CARTESIAN_POINT('Ctrl Pts',(92.3139986304335,-5.33783845222892,
133.361615129123));
#146271=CARTESIAN_POINT('Ctrl Pts',(92.3067059090278,-5.26705534710743,
133.49992336642));
#146272=CARTESIAN_POINT('Ctrl Pts',(92.2992016772044,-5.19421932328822,
133.642242950292));
#146273=CARTESIAN_POINT('Ctrl Pts',(92.291697445381,-5.11564935180377,133.781532541102));
#146274=CARTESIAN_POINT('Ctrl Pts',(92.2841932135576,-5.03164988115286,
133.917306173787));
#146275=CARTESIAN_POINT('Ctrl Pts',(92.276889709559,-4.94989728019178,134.049448049538));
#146276=CARTESIAN_POINT('Ctrl Pts',(92.2695862055604,-4.86300220249854,
134.178259375424));
#146277=CARTESIAN_POINT('Ctrl Pts',(92.2622827015618,-4.77128770943318,
134.303323914932));
#146278=CARTESIAN_POINT('Ctrl Pts',(92.254678105826,-4.67579222630446,134.433544322017));
#146279=CARTESIAN_POINT('Ctrl Pts',(92.2470735100902,-4.57507179766996,
134.559702064348));
#146280=CARTESIAN_POINT('Ctrl Pts',(92.2394689143544,-4.46953475600557,
134.681368436408));
#146281=CARTESIAN_POINT('Ctrl Pts',(92.2318643186186,-4.36399771434125,
134.803034808467));
#146282=CARTESIAN_POINT('Ctrl Pts',(92.2242597228828,-4.25364443123981,
134.920209524872));
#146283=CARTESIAN_POINT('Ctrl Pts',(92.216655127147,-4.13892252036997,135.03251044141));
#146284=CARTESIAN_POINT('Ctrl Pts',(92.2092318607415,-4.02693611944722,
135.142133575893));
#146285=CARTESIAN_POINT('Ctrl Pts',(92.2018085943361,-3.91042217108091,
135.247470307369));
#146286=CARTESIAN_POINT('Ctrl Pts',(92.1943853279307,-3.78974241667382,
135.348123703133));
#146287=CARTESIAN_POINT('Ctrl Pts',(92.1869708352097,-3.66920529571444,
135.448658134942));
#146288=CARTESIAN_POINT('Ctrl Pts',(92.1795563424887,-3.54451245311485,
135.544520012347));
#146289=CARTESIAN_POINT('Ctrl Pts',(92.1721418497677,-3.4160630639424,135.635348477794));
#146290=CARTESIAN_POINT('Ctrl Pts',(92.1647345034139,-3.28773747912728,
135.726089399346));
#146291=CARTESIAN_POINT('Ctrl Pts',(92.1573271570602,-3.15566285859136,
135.811806353029));
#146292=CARTESIAN_POINT('Ctrl Pts',(92.1499198107064,-3.02027202158217,
135.892178173075));
#146293=CARTESIAN_POINT('Ctrl Pts',(92.142517989031,-2.88498216416675,135.972490048786));
#146294=CARTESIAN_POINT('Ctrl Pts',(92.1351161673556,-2.74638133468789,
136.047464538988));
#146295=CARTESIAN_POINT('Ctrl Pts',(92.1277143456801,-2.60493185545782,
136.116823378934));
#146296=CARTESIAN_POINT('Ctrl Pts',(92.1203164313688,-2.4635570463081,136.186145604888));
#146297=CARTESIAN_POINT('Ctrl Pts',(92.1129185170575,-2.31933691658116,
136.249857920511));
#146298=CARTESIAN_POINT('Ctrl Pts',(92.1055206027462,-2.17275884296142,
136.307727729874));
#146299=CARTESIAN_POINT('Ctrl Pts',(92.098123917834,-2.0262051279577,136.365587922324));
#146300=CARTESIAN_POINT('Ctrl Pts',(92.0907272329219,-1.87729459363938,
136.41760739855));
#146301=CARTESIAN_POINT('Ctrl Pts',(92.0833305480097,-1.72653518247573,
136.463601452358));
#146302=CARTESIAN_POINT('Ctrl Pts',(92.0759341910742,-1.57578245614237,
136.50959346674));
#146303=CARTESIAN_POINT('Ctrl Pts',(92.0685378341388,-1.42318137302075,
136.549560481005));
#146304=CARTESIAN_POINT('Ctrl Pts',(92.0611414772034,-1.26925538507593,
136.583367567722));
#146305=CARTESIAN_POINT('Ctrl Pts',(92.0537439878668,-1.11530583066928,
136.617179830391));
#146306=CARTESIAN_POINT('Ctrl Pts',(92.0463464985303,-0.960031332176321,
136.644830207587));
#146307=CARTESIAN_POINT('Ctrl Pts',(92.0389490091937,-0.803965740135812,
136.666234861457));
#146308=CARTESIAN_POINT('Ctrl Pts',(92.0315489266788,-0.647845439544837,
136.687647018694));
#146309=CARTESIAN_POINT('Ctrl Pts',(92.0241488441638,-0.490933862875954,
136.702809042775));
#146310=CARTESIAN_POINT('Ctrl Pts',(92.0167487616488,-0.333770040151441,
136.711688958093));
#146311=CARTESIAN_POINT('Ctrl Pts',(92.0093405419824,-0.176433399646112,
136.720578637791));
#146312=CARTESIAN_POINT('Ctrl Pts',(92.001932322316,-0.0188443320902763,
136.723172392277));
#146313=CARTESIAN_POINT('Ctrl Pts',(91.9945241026495,0.138457332249514,
136.719490381962));
#146314=CARTESIAN_POINT('Ctrl Pts',(91.9871113233474,0.29585581313921,136.715806105432));
#146315=CARTESIAN_POINT('Ctrl Pts',(91.9796985440454,0.452966166648504,
136.705838390912));
#146316=CARTESIAN_POINT('Ctrl Pts',(91.9722857647433,0.609254138757135,
136.68965924694));
#146317=CARTESIAN_POINT('Ctrl Pts',(91.9648623937146,0.765765422449383,
136.673456985448));
#146318=CARTESIAN_POINT('Ctrl Pts',(91.9574390226858,0.92145160938465,136.651025621869));
#146319=CARTESIAN_POINT('Ctrl Pts',(91.9500156516571,1.0757882607436,136.622488338796));
#146320=CARTESIAN_POINT('Ctrl Pts',(91.9460796022161,1.15762125655496,136.607357186567));
#146321=CARTESIAN_POINT('Ctrl Pts',(91.9421435527752,1.239075084653,136.590510280186));
#146322=CARTESIAN_POINT('Ctrl Pts',(91.9382075033342,1.32007347316205,136.571971612419));
#146323=CARTESIAN_POINT('Ctrl Pts',(91.9307842369288,1.4728339060101,136.537008263585));
#146324=CARTESIAN_POINT('Ctrl Pts',(91.9233609705233,1.62443531659534,136.495918855334));
#146325=CARTESIAN_POINT('Ctrl Pts',(91.9159377041179,1.77434822412814,136.448793179129));
#146326=CARTESIAN_POINT('Ctrl Pts',(91.9085232113969,1.92408394705383,136.40172320156));
#146327=CARTESIAN_POINT('Ctrl Pts',(91.9011087186759,2.0721347866806,136.34863126789));
#146328=CARTESIAN_POINT('Ctrl Pts',(91.8936942259549,2.21798137945556,136.289658163086));
#146329=CARTESIAN_POINT('Ctrl Pts',(91.8862868796011,2.36368739979317,136.230741898781));
#146330=CARTESIAN_POINT('Ctrl Pts',(91.8788795332474,2.50719305905855,136.165955887195));
#146331=CARTESIAN_POINT('Ctrl Pts',(91.8714721868936,2.6479942020197,136.095490673478));
#146332=CARTESIAN_POINT('Ctrl Pts',(91.8640703652182,2.788690330177,136.025078015374));
#146333=CARTESIAN_POINT('Ctrl Pts',(91.8566685435428,2.92668562601896,135.948994755462));
#146334=CARTESIAN_POINT('Ctrl Pts',(91.8492667218674,3.06149608102939,135.867479449703));
#146335=CARTESIAN_POINT('Ctrl Pts',(91.841868807556,3.19623537064901,135.78600717524));
#146336=CARTESIAN_POINT('Ctrl Pts',(91.8344708932447,3.32779284910019,135.699108758429));
#146337=CARTESIAN_POINT('Ctrl Pts',(91.8270729789334,3.45570938783534,135.607068519295));
#146338=CARTESIAN_POINT('Ctrl Pts',(91.8196762940212,3.58360466916295,135.515043575578));
#146339=CARTESIAN_POINT('Ctrl Pts',(91.812279609109,3.70785990892144,135.417878723237));
#146340=CARTESIAN_POINT('Ctrl Pts',(91.8048829241967,3.82804515324628,135.315901470446));
#146341=CARTESIAN_POINT('Ctrl Pts',(91.7974865672613,3.94822506843153,135.213928739434));
#146342=CARTESIAN_POINT('Ctrl Pts',(91.7900902103259,4.06433506237359,135.107144273775));
#146343=CARTESIAN_POINT('Ctrl Pts',(91.7826938533904,4.17597867823078,134.995915536861));
#146344=CARTESIAN_POINT('Ctrl Pts',(91.7752963640539,4.28763938701026,134.884669770543));
#146345=CARTESIAN_POINT('Ctrl Pts',(91.7678988747173,4.39483209167113,134.768978641631));
#146346=CARTESIAN_POINT('Ctrl Pts',(91.7605013853807,4.49719769779428,134.649245977294));
#146347=CARTESIAN_POINT('Ctrl Pts',(91.7531013028658,4.59959918802175,134.529471340858));
#146348=CARTESIAN_POINT('Ctrl Pts',(91.7457012203508,4.69716996826024,134.405652631808));
#146349=CARTESIAN_POINT('Ctrl Pts',(91.7383011378358,4.78959177763234,134.278226067772));
#146350=CARTESIAN_POINT('Ctrl Pts',(91.7308929181693,4.8821152142855,134.150659385129));
#146351=CARTESIAN_POINT('Ctrl Pts',(91.7234846985029,4.96947815373376,134.019477227095));
#146352=CARTESIAN_POINT('Ctrl Pts',(91.7160764788364,5.05140576605887,133.885144665358));
#146353=CARTESIAN_POINT('Ctrl Pts',(91.7086636995343,5.13338380346227,133.75072942417));
#146354=CARTESIAN_POINT('Ctrl Pts',(91.7012509202323,5.20991966664164,133.613160240993));
#146355=CARTESIAN_POINT('Ctrl Pts',(91.6938381409302,5.28078516107104,133.472925521238));
#146356=CARTESIAN_POINT('Ctrl Pts',(91.6864147699014,5.35175191144219,133.332490427539));
#146357=CARTESIAN_POINT('Ctrl Pts',(91.6789913988727,5.41703195685918,133.189382529278));
#146358=CARTESIAN_POINT('Ctrl Pts',(91.671568027844,5.47644546233392,133.044109634885));
#146359=CARTESIAN_POINT('Ctrl Pts',(91.6676319784031,5.50794792854484,132.967082460501));
#146360=CARTESIAN_POINT('Ctrl Pts',(91.6636959289622,5.53780193278343,132.889446883624));
#146361=CARTESIAN_POINT('Ctrl Pts',(91.6597598795213,5.56598643403332,132.81128004262));
#146362=CARTESIAN_POINT('Ctrl Pts',(91.6523366131159,5.61914152378125,132.663859819992));
#146363=CARTESIAN_POINT('Ctrl Pts',(91.6449133467104,5.66651610639811,132.514103430867));
#146364=CARTESIAN_POINT('Ctrl Pts',(91.637490080305,5.70789952868653,132.362504876908));
#146365=CARTESIAN_POINT('Ctrl Pts',(91.630075587584,5.74923403920651,132.21108549985));
#146366=CARTESIAN_POINT('Ctrl Pts',(91.622661094863,5.78459138692901,132.057828648463));
#146367=CARTESIAN_POINT('Ctrl Pts',(91.615246602142,5.81380928954839,131.903247375727));
#146368=CARTESIAN_POINT('Ctrl Pts',(91.6078392557882,5.84299903085316,131.748815094241));
#146369=CARTESIAN_POINT('Ctrl Pts',(91.6004319094344,5.86606103862443,131.593061297061));
#146370=CARTESIAN_POINT('Ctrl Pts',(91.5930245630806,5.88288311567461,131.436513138569));
#146371=CARTESIAN_POINT('Ctrl Pts',(91.5856227414052,5.89969264618515,131.280081739599));
#146372=CARTESIAN_POINT('Ctrl Pts',(91.5782209197298,5.91027147295635,131.122857528558));
#146373=CARTESIAN_POINT('Ctrl Pts',(91.5708190980544,5.91455868144933,130.965376660842));
#146374=CARTESIAN_POINT('Ctrl Pts',(91.563421183743,5.91884362675829,130.807978926052));
#146375=CARTESIAN_POINT('Ctrl Pts',(91.5560232694317,5.91684355817676,130.650325176631));
#146376=CARTESIAN_POINT('Ctrl Pts',(91.5486253551204,5.90854951199959,130.492955372348));
#146377=CARTESIAN_POINT('Ctrl Pts',(91.5412286702081,5.9002568441424,130.335611720071));
#146378=CARTESIAN_POINT('Ctrl Pts',(91.5338319852959,5.88567229420846,130.178552291697));
#146379=CARTESIAN_POINT('Ctrl Pts',(91.5264353003837,5.86483900353505,130.022315845757));
#146380=CARTESIAN_POINT('Ctrl Pts',(91.5190389434483,5.84400663663162,129.866086327505));
#146381=CARTESIAN_POINT('Ctrl Pts',(91.5116425865128,5.81692612924937,129.710680089151));
#146382=CARTESIAN_POINT('Ctrl Pts',(91.5042462295773,5.78369234413948,129.556629304004));
#146383=CARTESIAN_POINT('Ctrl Pts',(91.4968487402407,5.7504534708521,129.402554933288));
#146384=CARTESIAN_POINT('Ctrl Pts',(91.4894512509041,5.71105952275197,129.249836793911));
#146385=CARTESIAN_POINT('Ctrl Pts',(91.4820537615675,5.6656561517681,129.098995280627));
#146386=CARTESIAN_POINT('Ctrl Pts',(91.4746536790525,5.6202368647031,128.948100890085));
#146387=CARTESIAN_POINT('Ctrl Pts',(91.4672535965375,5.56880406806876,128.799084792641));
#146388=CARTESIAN_POINT('Ctrl Pts',(91.4598535140225,5.51155273633097,128.652450536465));
#146389=CARTESIAN_POINT('Ctrl Pts',(91.4524452943561,5.45423845086832,128.505655040851));
#146390=CARTESIAN_POINT('Ctrl Pts',(91.4450370746896,5.39109298877237,128.361246964927));
#146391=CARTESIAN_POINT('Ctrl Pts',(91.4376288550231,5.32235907574186,128.219708913493));
#146392=CARTESIAN_POINT('Ctrl Pts',(91.430216075721,5.25358285813457,128.07808374775));
#146393=CARTESIAN_POINT('Ctrl Pts',(91.4228032964189,5.1792115117065,127.939332454627));
#146394=CARTESIAN_POINT('Ctrl Pts',(91.4153905171168,5.09953260104743,127.803911015697));
#146395=CARTESIAN_POINT('Ctrl Pts',(91.4079671460881,5.01973984142452,127.668296080265));
#146396=CARTESIAN_POINT('Ctrl Pts',(91.4005437750593,4.93462457269217,127.536020814614));
#146397=CARTESIAN_POINT('Ctrl Pts',(91.3931204040306,4.84451682326219,127.407511001874));
#146398=CARTESIAN_POINT('Ctrl Pts',(91.3891843545899,4.79673953240945,127.339372015609));
#146399=CARTESIAN_POINT('Ctrl Pts',(91.3852483051492,4.74755934134621,127.27229107068));
#146400=CARTESIAN_POINT('Ctrl Pts',(91.3813122557084,4.6970297755815,127.20632756466));
#146401=CARTESIAN_POINT('Ctrl Pts',(91.373888989303,4.60173259152136,127.081922450956));
#146402=CARTESIAN_POINT('Ctrl Pts',(91.3664657228975,4.50134541912187,126.961117886557));
#146403=CARTESIAN_POINT('Ctrl Pts',(91.3590424564921,4.39617001277534,126.844358119931));
#146404=CARTESIAN_POINT('Ctrl Pts',(91.3516279637711,4.29111891502469,126.727736353653));
#146405=CARTESIAN_POINT('Ctrl Pts',(91.3442134710501,4.18129109558825,126.61515014396));
#146406=CARTESIAN_POINT('Ctrl Pts',(91.3367989783291,4.06703048291858,126.507013341221));
#146407=CARTESIAN_POINT('Ctrl Pts',(91.3293916319753,3.95287999892924,126.398980764803));
#146408=CARTESIAN_POINT('Ctrl Pts',(91.3219842856215,3.834305496706,126.295389312641));
#146409=CARTESIAN_POINT('Ctrl Pts',(91.3145769392677,3.71168984083991,126.196618319227));
#146410=CARTESIAN_POINT('Ctrl Pts',(91.3071751175923,3.58916563635607,126.097920992945));
#146411=CARTESIAN_POINT('Ctrl Pts',(91.2997732959169,3.4626065690586,126.004037199892));
#146412=CARTESIAN_POINT('Ctrl Pts',(91.2923714742415,3.33243079587129,125.915307994283));
#146413=CARTESIAN_POINT('Ctrl Pts',(91.2849735599302,3.20232374146136,125.826625628131));
#146414=CARTESIAN_POINT('Ctrl Pts',(91.2775756456189,3.06860409116429,125.743092640004));
#146415=CARTESIAN_POINT('Ctrl Pts',(91.2701777313075,2.93172128332445,125.665008432767));
#146416=CARTESIAN_POINT('Ctrl Pts',(91.2627810463953,2.79486122292416,125.586937201708));
#146417=CARTESIAN_POINT('Ctrl Pts',(91.2553843614831,2.65483937219252,125.514313139197));
#146418=CARTESIAN_POINT('Ctrl Pts',(91.2479876765709,2.51213232288727,125.447391161352));
#146419=CARTESIAN_POINT('Ctrl Pts',(91.2405913196355,2.36943160136182,125.380472150898));
#146420=CARTESIAN_POINT('Ctrl Pts',(91.2331949627,2.2240462559833,125.31925488088));
#146421=CARTESIAN_POINT('Ctrl Pts',(91.2257986057645,2.07647529486173,125.263947193251));
#146422=CARTESIAN_POINT('Ctrl Pts',(91.218401116428,1.9288817402496,125.208631037874));
#146423=CARTESIAN_POINT('Ctrl Pts',(91.2110036270914,1.77910225319146,125.159226397424));
#146424=CARTESIAN_POINT('Ctrl Pts',(91.2036061377549,1.62765338495715,125.115892016885));
#146425=CARTESIAN_POINT('Ctrl Pts',(91.1962060552398,1.47615142655567,125.072542445545));
#146426=CARTESIAN_POINT('Ctrl Pts',(91.1888059727248,1.32297928052248,125.035267473416));
#146427=CARTESIAN_POINT('Ctrl Pts',(91.1814058902097,1.16866598465761,125.004175243045));
#146428=CARTESIAN_POINT('Ctrl Pts',(91.1739976705433,1.01418300546115,124.973048823571));
#146429=CARTESIAN_POINT('Ctrl Pts',(91.1665894508768,0.858556736660159,
124.948118796804));
#146430=CARTESIAN_POINT('Ctrl Pts',(91.1591812312104,0.702324406511077,
124.929441810423));
#146431=CARTESIAN_POINT('Ctrl Pts',(91.1517684519083,0.545995917969107,
124.910753328669));
#146432=CARTESIAN_POINT('Ctrl Pts',(91.1443556726062,0.389060996058686,
124.898325585603));
#146433=CARTESIAN_POINT('Ctrl Pts',(91.1369428933041,0.232058706675651,
124.892163114171));
#146434=CARTESIAN_POINT('Ctrl Pts',(91.1295195222753,0.0748320850588696,
124.88599183751));
#146435=CARTESIAN_POINT('Ctrl Pts',(91.1220961512465,-0.0824617239700671,
124.886103711596));
#146436=CARTESIAN_POINT('Ctrl Pts',(91.1146727802177,-0.239286108587151,
124.892451220363));
#146437=CARTESIAN_POINT('Ctrl Pts',(91.110736730777,-0.322438160258785,
124.895816821817));
#146438=CARTESIAN_POINT('Ctrl Pts',(91.1068006813363,-0.405458353621252,
124.900934620137));
#146439=CARTESIAN_POINT('Ctrl Pts',(91.1028646318956,-0.488267783968064,
124.907791688635));
#146440=CARTESIAN_POINT('Ctrl Pts',(91.0954413654902,-0.644443785211036,
124.92072390582));
#146441=CARTESIAN_POINT('Ctrl Pts',(91.0880180990847,-0.800341805377526,
124.939884659199));
#146442=CARTESIAN_POINT('Ctrl Pts',(91.0805948326793,-0.955424980030571,
124.965260201403));
#146443=CARTESIAN_POINT('Ctrl Pts',(91.0731803399583,-1.11032485925025,
124.990605751824));
#146444=CARTESIAN_POINT('Ctrl Pts',(91.0657658472373,-1.26441144517061,
125.022151410391));
#146445=CARTESIAN_POINT('Ctrl Pts',(91.0583513545163,-1.41715065202697,
125.05983151659));
#146446=CARTESIAN_POINT('Ctrl Pts',(91.0509440081626,-1.56974264308468,
125.097475305284));
#146447=CARTESIAN_POINT('Ctrl Pts',(91.0435366618088,-1.72098948044506,
125.141241681953));
#146448=CARTESIAN_POINT('Ctrl Pts',(91.036129315455,-1.87036507159359,125.191013571332));
#146449=CARTESIAN_POINT('Ctrl Pts',(91.0287274937796,-2.01962925279147,
125.240748338959));
#146450=CARTESIAN_POINT('Ctrl Pts',(91.0213256721042,-2.16702461406562,
125.296479583231));
#146451=CARTESIAN_POINT('Ctrl Pts',(91.0139238504288,-2.31203819281439,
125.35803984502));
#146452=CARTESIAN_POINT('Ctrl Pts',(91.0065259361174,-2.45697522002445,
125.419567609626));
#146453=CARTESIAN_POINT('Ctrl Pts',(90.999128021806,-2.5995326259831,125.486918118069));
#146454=CARTESIAN_POINT('Ctrl Pts',(90.9917301074946,-2.73921558217862,
125.559875079703));
#146455=CARTESIAN_POINT('Ctrl Pts',(90.9843334225824,-2.87887532560003,
125.632819917213));
#146456=CARTESIAN_POINT('Ctrl Pts',(90.9769367376702,-3.01566123675495,
125.711369186131));
#146457=CARTESIAN_POINT('Ctrl Pts',(90.969540052758,-3.14910123800777,125.7952597047));
#146458=CARTESIAN_POINT('Ctrl Pts',(90.9621436958225,-3.28253532239091,
125.879146503475));
#146459=CARTESIAN_POINT('Ctrl Pts',(90.9547473388871,-3.41262347583157,
125.968373882309));
#146460=CARTESIAN_POINT('Ctrl Pts',(90.9473509819516,-3.53892110893609,
126.062634355198));
#146461=CARTESIAN_POINT('Ctrl Pts',(90.9399534926151,-3.66523807853076,
126.156909259607));
#146462=CARTESIAN_POINT('Ctrl Pts',(90.9325560032785,-3.7877630730756,126.256218569106));
#146463=CARTESIAN_POINT('Ctrl Pts',(90.9251585139419,-3.90608332734201,
126.360213500024));
#146464=CARTESIAN_POINT('Ctrl Pts',(90.917758431427,-4.02444505858962,126.464244886203));
#146465=CARTESIAN_POINT('Ctrl Pts',(90.910358348912,-4.13859883469101,126.572964917792));
#146466=CARTESIAN_POINT('Ctrl Pts',(90.902958266397,-4.24816771440527,126.685986953996));
#146467=CARTESIAN_POINT('Ctrl Pts',(90.8955500467306,-4.3578570763672,126.799133269549));
#146468=CARTESIAN_POINT('Ctrl Pts',(90.8881418270641,-4.46295121361114,
126.916590768638));
#146469=CARTESIAN_POINT('Ctrl Pts',(90.8807336073976,-4.56311208184558,
127.037938085373));
#146470=CARTESIAN_POINT('Ctrl Pts',(90.8733208280956,-4.66333459742306,
127.159360089355));
#146471=CARTESIAN_POINT('Ctrl Pts',(90.8659080487935,-4.75861756827702,
127.284676385094));
#146472=CARTESIAN_POINT('Ctrl Pts',(90.8584952694914,-4.84866580242902,
127.413435891351));
#146473=CARTESIAN_POINT('Ctrl Pts',(90.8510718984627,-4.93884270172108,
127.542379375229));
#146474=CARTESIAN_POINT('Ctrl Pts',(90.843648527434,-5.02376972477853,127.674775582234));
#146475=CARTESIAN_POINT('Ctrl Pts',(90.8362251564052,-5.10319679641646,
127.810147362044));
#146476=CARTESIAN_POINT('Ctrl Pts',(90.8322891069644,-5.14531093562596,
127.881924727902));
#146477=CARTESIAN_POINT('Ctrl Pts',(90.8283530575235,-5.18587962935102,
127.954538262835));
#146478=CARTESIAN_POINT('Ctrl Pts',(90.8244170080826,-5.22487110325824,
128.027914594889));
#146479=CARTESIAN_POINT('Ctrl Pts',(90.8165699274292,-5.30260621434947,
128.174200866019));
#146480=CARTESIAN_POINT('Ctrl Pts',(90.8087228467758,-5.37428305171831,
128.323921525479));
#146481=CARTESIAN_POINT('Ctrl Pts',(90.8008757661224,-5.4396033048784,128.476561990525));
#146482=CARTESIAN_POINT('Ctrl Pts',(90.7930422008072,-5.50481105437651,
128.628939556845));
#146483=CARTESIAN_POINT('Ctrl Pts',(90.7852086354919,-5.56368392285292,
128.784226620248));
#146484=CARTESIAN_POINT('Ctrl Pts',(90.7773750701766,-5.61596930729451,
128.94188395945));
#146485=CARTESIAN_POINT('Ctrl Pts',(90.7695601035074,-5.66813055447299,
129.099166984667));
#146486=CARTESIAN_POINT('Ctrl Pts',(90.7617451368382,-5.71373541680176,
129.258808767443));
#146487=CARTESIAN_POINT('Ctrl Pts',(90.753930170169,-5.75257945854759,129.42025074635));
#146488=CARTESIAN_POINT('Ctrl Pts',(90.7461262213542,-5.79136873640084,
129.581465117862));
#146489=CARTESIAN_POINT('Ctrl Pts',(90.7383222725393,-5.82341611818608,
129.744474327453));
#146490=CARTESIAN_POINT('Ctrl Pts',(90.7305183237245,-5.84856635671517,
129.90870324245));
#146491=CARTESIAN_POINT('Ctrl Pts',(90.7227297011632,-5.87366720243783,
130.072609626629));
#146492=CARTESIAN_POINT('Ctrl Pts',(90.7149410786019,-5.89189787549124,
130.237730632963));
#146493=CARTESIAN_POINT('Ctrl Pts',(90.7071524560406,-5.90315384345051,
130.403480008088));
#146494=CARTESIAN_POINT('Ctrl Pts',(90.7008933681091,-5.91219935729549,
130.536679415985));
#146495=CARTESIAN_POINT('Ctrl Pts',(90.6946342801777,-5.91674151269891,
130.670284287664));
#146496=CARTESIAN_POINT('Ctrl Pts',(90.6883751922462,-5.91674998811213,
130.803985550795));
#146497=CARTESIAN_POINT('',(88.9383751922115,-5.91674749024185,130.809810316349));
#146498=CARTESIAN_POINT('Ctrl Pts',(90.6883751922114,-5.91674998811218,
130.803985551538));
#146499=CARTESIAN_POINT('Ctrl Pts',(90.6806626928907,-5.91676043156495,
130.96873334105));
#146500=CARTESIAN_POINT('Ctrl Pts',(90.67295019357,-5.90988562066363,131.133362254122));
#146501=CARTESIAN_POINT('Ctrl Pts',(90.6652376942492,-5.89618120901639,
131.297288313016));
#146502=CARTESIAN_POINT('Ctrl Pts',(90.6575167057358,-5.88246171284378,
131.461394806274));
#146503=CARTESIAN_POINT('Ctrl Pts',(90.6497957172224,-5.86189764216194,
131.624796578391));
#146504=CARTESIAN_POINT('Ctrl Pts',(90.6420747287089,-5.83459617221082,
131.786917521629));
#146505=CARTESIAN_POINT('Ctrl Pts',(90.6340659500057,-5.80627707411455,
131.955081320255));
#146506=CARTESIAN_POINT('Ctrl Pts',(90.6260571713024,-5.77070874452146,
132.121866580596));
#146507=CARTESIAN_POINT('Ctrl Pts',(90.6180483925991,-5.72806756474608,
132.286646870691));
#146508=CARTESIAN_POINT('Ctrl Pts',(90.6103020467591,-5.68682365755272,
132.446027615496));
#146509=CARTESIAN_POINT('Ctrl Pts',(90.602555700919,-5.63896326188491,132.603532434554));
#146510=CARTESIAN_POINT('Ctrl Pts',(90.5948093550789,-5.58469548427981,
132.758614160575));
#146511=CARTESIAN_POINT('Ctrl Pts',(90.586669359944,-5.52766995833463,132.921576739497));
#146512=CARTESIAN_POINT('Ctrl Pts',(90.5785293648092,-5.46356904828496,
133.081863137164));
#146513=CARTESIAN_POINT('Ctrl Pts',(90.5703893696743,-5.39269046322379,
133.238866754415));
#146514=CARTESIAN_POINT('Ctrl Pts',(90.5622493745395,-5.32181187816262,
133.395870371666));
#146515=CARTESIAN_POINT('Ctrl Pts',(90.5541093794046,-5.24415586832495,
133.549590877696));
#146516=CARTESIAN_POINT('Ctrl Pts',(90.5459693842698,-5.1600731277978,133.699455759056));
#146517=CARTESIAN_POINT('Ctrl Pts',(90.5385461178643,-5.08339389486299,
133.836124997886));
#146518=CARTESIAN_POINT('Ctrl Pts',(90.5311228514589,-5.00116524974444,
133.969952413179));
#146519=CARTESIAN_POINT('Ctrl Pts',(90.5236995850534,-4.91362285257071,
134.100455431918));
#146520=CARTESIAN_POINT('Ctrl Pts',(90.5162850923324,-4.82618392324049,
134.230804206926));
#146521=CARTESIAN_POINT('Ctrl Pts',(90.5088705996114,-4.73344394897865,
134.357836099414));
#146522=CARTESIAN_POINT('Ctrl Pts',(90.5014561068903,-4.63568465080247,
134.481092642179));
#146523=CARTESIAN_POINT('Ctrl Pts',(90.4940487605366,-4.53801957671838,
134.604230385648));
#146524=CARTESIAN_POINT('Ctrl Pts',(90.4866414141827,-4.43534504026797,
134.723599733067));
#146525=CARTESIAN_POINT('Ctrl Pts',(90.479234067829,-4.32798620253089,134.83877085863));
#146526=CARTESIAN_POINT('Ctrl Pts',(90.4718322461535,-4.22070743706488,
134.953856085223));
#146527=CARTESIAN_POINT('Ctrl Pts',(90.4644304244781,-4.10875158023966,
135.064749052701));
#146528=CARTESIAN_POINT('Ctrl Pts',(90.4570286028026,-3.99248416044879,
135.171052820031));
#146529=CARTESIAN_POINT('Ctrl Pts',(90.4496306884912,-3.87627811732363,
135.277300470429));
#146530=CARTESIAN_POINT('Ctrl Pts',(90.4422327741798,-3.75576531888127,
135.378963494154));
#146531=CARTESIAN_POINT('Ctrl Pts',(90.4348348598683,-3.63134816887476,
135.475681741072));
#146532=CARTESIAN_POINT('Ctrl Pts',(90.4274381749561,-3.50695169474222,
135.57238391517));
#146533=CARTESIAN_POINT('Ctrl Pts',(90.4200414900439,-3.37865245121897,
135.664142714472));
#146534=CARTESIAN_POINT('Ctrl Pts',(90.4126448051317,-3.24688603353782,
135.750638172224));
#146535=CARTESIAN_POINT('Ctrl Pts',(90.4052484481962,-3.11512545851761,
135.837129794677));
#146536=CARTESIAN_POINT('Ctrl Pts',(90.3978520912607,-2.9798983270917,135.918358334771));
#146537=CARTESIAN_POINT('Ctrl Pts',(90.3904557343252,-2.84166910401371,
135.994047242575));
#146538=CARTESIAN_POINT('Ctrl Pts',(90.3830582449886,-2.70341871768888,
136.069747738544));
#146539=CARTESIAN_POINT('Ctrl Pts',(90.375660755652,-2.56216565197898,136.139906734183));
#146540=CARTESIAN_POINT('Ctrl Pts',(90.3682632663154,-2.41839870432485,
136.204293790247));
#146541=CARTESIAN_POINT('Ctrl Pts',(90.3608631838004,-2.27458135939049,
136.268703417093));
#146542=CARTESIAN_POINT('Ctrl Pts',(90.3534631012855,-2.12824871845321,
136.327336923415));
#146543=CARTESIAN_POINT('Ctrl Pts',(90.3460630187705,-1.97990911981401,
136.380012188439));
#146544=CARTESIAN_POINT('Ctrl Pts',(90.338654799104,-1.831406406536,136.432745375332));
#146545=CARTESIAN_POINT('Ctrl Pts',(90.3312465794375,-1.68089268031238,
136.479507111761));
#146546=CARTESIAN_POINT('Ctrl Pts',(90.323838359771,-1.52889169434468,136.520165088458));
#146547=CARTESIAN_POINT('Ctrl Pts',(90.3164255804689,-1.37679715430617,
136.56084808946));
#146548=CARTESIAN_POINT('Ctrl Pts',(90.3090128011668,-1.22321389384794,
136.595419763122));
#146549=CARTESIAN_POINT('Ctrl Pts',(90.3016000218647,-1.06867488050435,
136.623799126759));
#146550=CARTESIAN_POINT('Ctrl Pts',(90.2941766508359,-0.913915054571438,
136.652219040162));
#146551=CARTESIAN_POINT('Ctrl Pts',(90.2867532798072,-0.758197116873509,
136.674428919804));
#146552=CARTESIAN_POINT('Ctrl Pts',(90.2793299087784,-0.602058991670594,
136.690399653543));
#146553=CARTESIAN_POINT('Ctrl Pts',(90.2753938593379,-0.51927081121063,
136.698867719784));
#146554=CARTESIAN_POINT('Ctrl Pts',(90.2714578098973,-0.43636451095525,
136.705582609427));
#146555=CARTESIAN_POINT('Ctrl Pts',(90.2675217604568,-0.353420031477407,
136.710545921453));
#146556=CARTESIAN_POINT('Ctrl Pts',(90.2600984940514,-0.196989331781025,
136.719906573035));
#146557=CARTESIAN_POINT('Ctrl Pts',(90.252675227646,-0.0399499458733333,
136.723062271943));
#146558=CARTESIAN_POINT('Ctrl Pts',(90.2452519612405,0.1171647438427,136.719950443213));
#146559=CARTESIAN_POINT('Ctrl Pts',(90.2378374685195,0.274093737043611,
136.716842292406));
#146560=CARTESIAN_POINT('Ctrl Pts',(90.2304229757985,0.4310974873121,136.707481366344));
#146561=CARTESIAN_POINT('Ctrl Pts',(90.2230084830775,0.587637996115035,
136.691856872174));
#146562=CARTESIAN_POINT('Ctrl Pts',(90.2156011367237,0.744027625281383,
136.67624743748));
#146563=CARTESIAN_POINT('Ctrl Pts',(90.20819379037,0.899954532896394,136.654386490109));
#146564=CARTESIAN_POINT('Ctrl Pts',(90.2007864440162,1.05488133682979,136.626315265939));
#146565=CARTESIAN_POINT('Ctrl Pts',(90.1933846223408,1.20969259050831,136.598264978346));
#146566=CARTESIAN_POINT('Ctrl Pts',(90.1859828006654,1.36350485998654,136.564013702878));
#146567=CARTESIAN_POINT('Ctrl Pts',(90.17858097899,1.51578661050585,136.5236544126));
#146568=CARTESIAN_POINT('Ctrl Pts',(90.1711830646786,1.6679879726742,136.483316427676));
#146569=CARTESIAN_POINT('Ctrl Pts',(90.1637851503673,1.81866006502622,136.436876944829));
#146570=CARTESIAN_POINT('Ctrl Pts',(90.1563872360559,1.96728237399586,136.384479847785));
#146571=CARTESIAN_POINT('Ctrl Pts',(90.1489905511438,2.11587998463392,136.332091458189));
#146572=CARTESIAN_POINT('Ctrl Pts',(90.1415938662316,2.26242813623829,136.273747543346));
#146573=CARTESIAN_POINT('Ctrl Pts',(90.1341971813194,2.40642218185364,136.209641632017));
#146574=CARTESIAN_POINT('Ctrl Pts',(90.1268008243839,2.55040984262232,136.145538563211));
#146575=CARTESIAN_POINT('Ctrl Pts',(90.1194044674485,2.69184328155654,136.075674157749));
#146576=CARTESIAN_POINT('Ctrl Pts',(90.1120081105131,2.83023877482334,136.000289700991));
#146577=CARTESIAN_POINT('Ctrl Pts',(90.1046106211765,2.96865545679327,135.924893702681));
#146578=CARTESIAN_POINT('Ctrl Pts',(90.0972131318399,3.10403293914437,135.843976148877));
#146579=CARTESIAN_POINT('Ctrl Pts',(90.0898156425034,3.23591313985699,135.757823720669));
#146580=CARTESIAN_POINT('Ctrl Pts',(90.0824155599884,3.36783957096878,135.671641091861));
#146581=CARTESIAN_POINT('Ctrl Pts',(90.0750154774735,3.49626596722398,135.580220139055));
#146582=CARTESIAN_POINT('Ctrl Pts',(90.0676153949586,3.62076433598955,135.483890100936));
#146583=CARTESIAN_POINT('Ctrl Pts',(90.0602071752921,3.74539960351103,135.387454138036));
#146584=CARTESIAN_POINT('Ctrl Pts',(90.0527989556256,3.86609792225628,135.286098538153));
#146585=CARTESIAN_POINT('Ctrl Pts',(90.0453907359591,3.98246487529061,135.180192433298));
#146586=CARTESIAN_POINT('Ctrl Pts',(90.0379779566571,4.09890345024309,135.074221145003));
#146587=CARTESIAN_POINT('Ctrl Pts',(90.030565177355,4.21100508217256,134.96369403235));
#146588=CARTESIAN_POINT('Ctrl Pts',(90.023152398053,4.31841355608367,134.849015722904));
#146589=CARTESIAN_POINT('Ctrl Pts',(90.0157290270242,4.42597550025919,134.73417355571));
#146590=CARTESIAN_POINT('Ctrl Pts',(90.0083056559955,4.5288306499666,134.615168627018));
#146591=CARTESIAN_POINT('Ctrl Pts',(90.0008822849668,4.626663751134,134.492437771917));
#146592=CARTESIAN_POINT('Ctrl Pts',(89.9969462355258,4.67853720884777,134.427362927653));
#146593=CARTESIAN_POINT('Ctrl Pts',(89.9930101860849,4.72899951607211,134.361241071086));
#146594=CARTESIAN_POINT('Ctrl Pts',(89.989074136644,4.77800880824216,134.294140322771));
#146595=CARTESIAN_POINT('Ctrl Pts',(89.9816508702386,4.87043880374435,134.167590405595));
#146596=CARTESIAN_POINT('Ctrl Pts',(89.9742276038331,4.95797740659319,134.037174454986));
#146597=CARTESIAN_POINT('Ctrl Pts',(89.9668043374277,5.04028366448247,133.903307397369));
#146598=CARTESIAN_POINT('Ctrl Pts',(89.9593898447067,5.12249264320998,133.769598559497));
#146599=CARTESIAN_POINT('Ctrl Pts',(89.9519753519856,5.19948139304801,133.632447048629));
#146600=CARTESIAN_POINT('Ctrl Pts',(89.9445608592646,5.27095003231685,133.492299664367));
#146601=CARTESIAN_POINT('Ctrl Pts',(89.9371535129108,5.34234978742056,133.352287359431));
#146602=CARTESIAN_POINT('Ctrl Pts',(89.929746166557,5.40823985555575,133.209285259937));
#146603=CARTESIAN_POINT('Ctrl Pts',(89.9223388202033,5.46836446146664,133.06376776969));
#146604=CARTESIAN_POINT('Ctrl Pts',(89.9149369985278,5.52844422417803,132.918358811877));
#146605=CARTESIAN_POINT('Ctrl Pts',(89.9075351768524,5.58276694480667,132.770438542351));
#146606=CARTESIAN_POINT('Ctrl Pts',(89.900133355177,5.63112353670508,132.62050441057));
#146607=CARTESIAN_POINT('Ctrl Pts',(89.8927354408656,5.6794546015352,132.470649427849));
#146608=CARTESIAN_POINT('Ctrl Pts',(89.8853375265543,5.72182569566769,132.31878305447));
#146609=CARTESIAN_POINT('Ctrl Pts',(89.8779396122429,5.75807652226219,132.165420985909));
#146610=CARTESIAN_POINT('Ctrl Pts',(89.8705429273306,5.79432132462683,132.012084403341));
#146611=CARTESIAN_POINT('Ctrl Pts',(89.8631462424184,5.82444779226367,131.857252981835));
#146612=CARTESIAN_POINT('Ctrl Pts',(89.8557495575062,5.84834597239345,131.701455902187));
#146613=CARTESIAN_POINT('Ctrl Pts',(89.8483532005708,5.87224309285286,131.545665730745));
#146614=CARTESIAN_POINT('Ctrl Pts',(89.8409568436353,5.88991241832283,131.388910355282));
#146615=CARTESIAN_POINT('Ctrl Pts',(89.8335604866999,5.90129548446236,131.231727166987));
#146616=CARTESIAN_POINT('Ctrl Pts',(89.8261629973633,5.9126802933784,131.074519913545));
#146617=CARTESIAN_POINT('Ctrl Pts',(89.8187655080266,5.9177768996482,130.9168850892));
#146618=CARTESIAN_POINT('Ctrl Pts',(89.81136801869,5.91657889167082,130.759363049462));
#146619=CARTESIAN_POINT('Ctrl Pts',(89.803967936175,5.9153804637336,130.601785790617));
#146620=CARTESIAN_POINT('Ctrl Pts',(89.79656785366,5.90788303112719,130.444321768149));
#146621=CARTESIAN_POINT('Ctrl Pts',(89.789167771145,5.89413225120764,130.287509025933));
#146622=CARTESIAN_POINT('Ctrl Pts',(89.7817595514785,5.88036635089195,130.130523851985));
#146623=CARTESIAN_POINT('Ctrl Pts',(89.7743513318121,5.86033340367287,129.974191760586));
#146624=CARTESIAN_POINT('Ctrl Pts',(89.7669431121456,5.83413077877718,129.819044110739));
#146625=CARTESIAN_POINT('Ctrl Pts',(89.7595303328435,5.80791202660307,129.663800970104));
#146626=CARTESIAN_POINT('Ctrl Pts',(89.7521175535414,5.77551610672988,129.509744088114));
#146627=CARTESIAN_POINT('Ctrl Pts',(89.7447047742394,5.73709090087995,129.357391869617));
#146628=CARTESIAN_POINT('Ctrl Pts',(89.7372814032106,5.69861079129397,129.204821963126));
#146629=CARTESIAN_POINT('Ctrl Pts',(89.7298580321818,5.65408429518321,129.053961941852));
#146630=CARTESIAN_POINT('Ctrl Pts',(89.7224346611531,5.60370853175498,128.905313158013));
#146631=CARTESIAN_POINT('Ctrl Pts',(89.7184986117124,5.57699809323635,128.826496006045));
#146632=CARTESIAN_POINT('Ctrl Pts',(89.7145625622717,5.54864401230487,128.748300159224));
#146633=CARTESIAN_POINT('Ctrl Pts',(89.7106265128311,5.51868097189372,128.67079766022));
#146634=CARTESIAN_POINT('Ctrl Pts',(89.7032032464256,5.46217161279101,128.524630365864));
#146635=CARTESIAN_POINT('Ctrl Pts',(89.6957799800202,5.39976573306095,128.380488653174));
#146636=CARTESIAN_POINT('Ctrl Pts',(89.6883567136147,5.33162812900701,128.238883652851));
#146637=CARTESIAN_POINT('Ctrl Pts',(89.6809422208937,5.26357105794249,128.097446017879));
#146638=CARTESIAN_POINT('Ctrl Pts',(89.6735277281727,5.18979590735851,127.958539460469));
#146639=CARTESIAN_POINT('Ctrl Pts',(89.6661132354517,5.11051648904238,127.822657785672));
#146640=CARTESIAN_POINT('Ctrl Pts',(89.6587058890979,5.03131348321451,127.686907078748));
#146641=CARTESIAN_POINT('Ctrl Pts',(89.6512985427442,4.94661695816185,127.554175770526));
#146642=CARTESIAN_POINT('Ctrl Pts',(89.6438911963904,4.8566877904679,127.424935478815));
#146643=CARTESIAN_POINT('Ctrl Pts',(89.636489374715,4.76682569534005,127.29579157939));
#146644=CARTESIAN_POINT('Ctrl Pts',(89.6290875530396,4.6717389406739,127.170133817194));
#146645=CARTESIAN_POINT('Ctrl Pts',(89.6216857313642,4.57173302834773,127.048406986327));
#146646=CARTESIAN_POINT('Ctrl Pts',(89.6142878170529,4.47177990836459,126.926744414108));
#146647=CARTESIAN_POINT('Ctrl Pts',(89.6068899027416,4.36691303871298,126.80900892825));
#146648=CARTESIAN_POINT('Ctrl Pts',(89.5994919884303,4.25747964424359,126.695614137026));
#146649=CARTESIAN_POINT('Ctrl Pts',(89.5920953035181,4.14806443561865,126.582238189958));
#146650=CARTESIAN_POINT('Ctrl Pts',(89.5846986186058,4.03408446728941,126.473201774218));
#146651=CARTESIAN_POINT('Ctrl Pts',(89.5773019336936,3.91592552188532,126.368883431338));
#146652=CARTESIAN_POINT('Ctrl Pts',(89.5699055767581,3.79777181577235,126.264569714043));
#146653=CARTESIAN_POINT('Ctrl Pts',(89.5625092198227,3.67543978086556,126.164973900703));
#146654=CARTESIAN_POINT('Ctrl Pts',(89.5551128628872,3.54934993818911,126.070435652088));
#146655=CARTESIAN_POINT('Ctrl Pts',(89.5477153735506,3.42324079083603,125.975882929426));
#146656=CARTESIAN_POINT('Ctrl Pts',(89.540317884214,3.29337298884547,125.886389537225));
#146657=CARTESIAN_POINT('Ctrl Pts',(89.5329203948774,3.16019768298323,125.802252945098));
#146658=CARTESIAN_POINT('Ctrl Pts',(89.5255203123625,3.02697569272453,125.718086859018));
#146659=CARTESIAN_POINT('Ctrl Pts',(89.5181202298475,2.89044420555162,125.639281510992));
#146660=CARTESIAN_POINT('Ctrl Pts',(89.5107201473325,2.75108057192996,125.566089314049));
#146661=CARTESIAN_POINT('Ctrl Pts',(89.503311927666,2.6115636936656,125.49281663476));
#146662=CARTESIAN_POINT('Ctrl Pts',(89.4959037079995,2.46920878031269,125.425169606593));
#146663=CARTESIAN_POINT('Ctrl Pts',(89.4884954883331,2.32451550969679,125.363353522581));
#146664=CARTESIAN_POINT('Ctrl Pts',(89.481082709031,2.17973318278706,125.3014993918));
#146665=CARTESIAN_POINT('Ctrl Pts',(89.4736699297289,2.03260997884623,125.245483488926));
#146666=CARTESIAN_POINT('Ctrl Pts',(89.4662571504268,1.88366198023594,125.195461607358));
#146667=CARTESIAN_POINT('Ctrl Pts',(89.458833779398,1.73450115774015,125.14536825218));
#146668=CARTESIAN_POINT('Ctrl Pts',(89.4514104083693,1.58351069049682,125.101286127954));
#146669=CARTESIAN_POINT('Ctrl Pts',(89.4439870373405,1.43121892807072,125.063320385828));
#146670=CARTESIAN_POINT('Ctrl Pts',(89.4400509878997,1.35047018144233,125.043190038378));
#146671=CARTESIAN_POINT('Ctrl Pts',(89.436114938459,1.2693557275585,125.024778364448));
#146672=CARTESIAN_POINT('Ctrl Pts',(89.4321788890182,1.18795492492918,125.008095125127));
#146673=CARTESIAN_POINT('Ctrl Pts',(89.4247556226128,1.03443555160173,124.976631056434));
#146674=CARTESIAN_POINT('Ctrl Pts',(89.4173323562074,0.879433144068388,
124.951222773912));
#146675=CARTESIAN_POINT('Ctrl Pts',(89.4099090898019,0.72346680749017,124.932007908391));
#146676=CARTESIAN_POINT('Ctrl Pts',(89.4024945970809,0.567684810169257,
124.912815753245));
#146677=CARTESIAN_POINT('Ctrl Pts',(89.3950801043599,0.410941518433562,
124.89980248959));
#146678=CARTESIAN_POINT('Ctrl Pts',(89.3876656116389,0.253767954950186,
124.893055145207));
#146679=CARTESIAN_POINT('Ctrl Pts',(89.3802582652851,0.0967458812652225,
124.886314304168));
#146680=CARTESIAN_POINT('Ctrl Pts',(89.3728509189314,-0.0607052681065663,
124.885827375188));
#146681=CARTESIAN_POINT('Ctrl Pts',(89.3654435725776,-0.218047697578145,
124.891629796356));
#146682=CARTESIAN_POINT('Ctrl Pts',(89.3580417509023,-0.375272775129521,
124.89742788986));
#146683=CARTESIAN_POINT('Ctrl Pts',(89.3506399292269,-0.532388922797885,
124.909505979728));
#146684=CARTESIAN_POINT('Ctrl Pts',(89.3432381075515,-0.688856791480747,
124.927847460656));
#146685=CARTESIAN_POINT('Ctrl Pts',(89.3358401932401,-0.845242061994901,
124.94617925926));
#146686=CARTESIAN_POINT('Ctrl Pts',(89.3284422789287,-1.00097936525315,
124.970767820726));
#146687=CARTESIAN_POINT('Ctrl Pts',(89.3210443646174,-1.15553303738866,
125.00154458033));
#146688=CARTESIAN_POINT('Ctrl Pts',(89.3136476797051,-1.3100610255072,125.032316225394));
#146689=CARTESIAN_POINT('Ctrl Pts',(89.3062509947929,-1.46340540713921,
125.06927395476));
#146690=CARTESIAN_POINT('Ctrl Pts',(89.2988543098807,-1.61503917963648,
125.11229780952));
#146691=CARTESIAN_POINT('Ctrl Pts',(89.2914579529453,-1.76666622853337,
125.155319756558));
#146692=CARTESIAN_POINT('Ctrl Pts',(89.2840615960098,-1.91658245998966,
125.204407192274));
#146693=CARTESIAN_POINT('Ctrl Pts',(89.2766652390744,-2.06427480589359,
125.259389915366));
#146694=CARTESIAN_POINT('Ctrl Pts',(89.2692677497378,-2.21198976387168,
125.314381056453));
#146695=CARTESIAN_POINT('Ctrl Pts',(89.2618702604013,-2.35747980848721,
125.375269151832));
#146696=CARTESIAN_POINT('Ctrl Pts',(89.2544727710648,-2.50025081212146,
125.441835425179));
#146697=CARTESIAN_POINT('Ctrl Pts',(89.2470726885498,-2.64307186391052,
125.50842503323));
#146698=CARTESIAN_POINT('Ctrl Pts',(89.2396726060348,-2.78317163887261,
125.580696624625));
#146699=CARTESIAN_POINT('Ctrl Pts',(89.2322725235198,-2.92007975519077,
125.658385026308));
#146700=CARTESIAN_POINT('Ctrl Pts',(89.2248643038533,-3.05713841605742,
125.736158854375));
#146701=CARTESIAN_POINT('Ctrl Pts',(89.2174560841868,-3.19099808459716,
125.819361203584));
#146702=CARTESIAN_POINT('Ctrl Pts',(89.2100478645204,-3.32121595389669,
125.907682646729));
#146703=CARTESIAN_POINT('Ctrl Pts',(89.2026350852183,-3.45151397012132,
125.996058450248));
#146704=CARTESIAN_POINT('Ctrl Pts',(89.1952223059163,-3.57816542107575,
126.0895594047));
#146705=CARTESIAN_POINT('Ctrl Pts',(89.1878095266143,-3.70076027823738,
126.187835525517));
#146706=CARTESIAN_POINT('Ctrl Pts',(89.1803861555856,-3.82353030468065,
126.286252067864));
#146707=CARTESIAN_POINT('Ctrl Pts',(89.1729627845568,-3.94223187995439,
126.389457159318));
#146708=CARTESIAN_POINT('Ctrl Pts',(89.1655394135281,-4.05649095157504,
126.49706312119));
#146709=CARTESIAN_POINT('Ctrl Pts',(89.1616033640871,-4.11707385295909,
126.554118384145));
#146710=CARTESIAN_POINT('Ctrl Pts',(89.1576673146462,-4.17640845933906,
126.612410311992));
#146711=CARTESIAN_POINT('Ctrl Pts',(89.1537312652053,-4.23444366322195,
126.671877414273));
#146712=CARTESIAN_POINT('Ctrl Pts',(89.1464056947544,-4.34245576547198,
126.782554491329));
#146713=CARTESIAN_POINT('Ctrl Pts',(89.1390801243036,-4.44631023157514,
126.897658490166));
#146714=CARTESIAN_POINT('Ctrl Pts',(89.1317545538528,-4.54561506504811,
127.016839760474));
#146715=CARTESIAN_POINT('Ctrl Pts',(89.1244378391925,-4.64479985014911,
127.135876954034));
#146716=CARTESIAN_POINT('Ctrl Pts',(89.1171211245321,-4.73944570272937,
127.25898131977));
#146717=CARTESIAN_POINT('Ctrl Pts',(89.1098044098719,-4.82919632579842,
127.385765378379));
#146718=CARTESIAN_POINT('Ctrl Pts',(89.1024960821167,-4.91884407073205,
127.512404108664));
#146719=CARTESIAN_POINT('Ctrl Pts',(89.0951877543616,-5.0036075403914,127.642713820679));
#146720=CARTESIAN_POINT('Ctrl Pts',(89.0878794266064,-5.08317004454765,
127.776273290438));
#146721=CARTESIAN_POINT('Ctrl Pts',(89.080575841019,-5.16268092283848,127.909746097224));
#146722=CARTESIAN_POINT('Ctrl Pts',(89.0732722554317,-5.23699735301651,
128.046464138771));
#146723=CARTESIAN_POINT('Ctrl Pts',(89.0659686698443,-5.30584530870804,
128.185976359562));
#146724=CARTESIAN_POINT('Ctrl Pts',(89.0586682910363,-5.37466303538422,
128.325427324838));
#146725=CARTESIAN_POINT('Ctrl Pts',(89.0513679122282,-5.43801689537401,
128.467669684678));
#146726=CARTESIAN_POINT('Ctrl Pts',(89.0440675334202,-5.49567842461156,
128.612227132634));
#146727=CARTESIAN_POINT('Ctrl Pts',(89.0367688286363,-5.55332673168708,
128.756751432632));
#146728=CARTESIAN_POINT('Ctrl Pts',(89.0294701238524,-5.60528516440204,
128.903589407486));
#146729=CARTESIAN_POINT('Ctrl Pts',(89.0221714190685,-5.65137321380395,
129.052244365487));
#146730=CARTESIAN_POINT('Ctrl Pts',(89.0148704812603,-5.69747536375345,
129.200944804179));
#146731=CARTESIAN_POINT('Ctrl Pts',(89.0075695434521,-5.73770342247987,
129.351462971357));
#146732=CARTESIAN_POINT('Ctrl Pts',(89.0002686056439,-5.77192657573628,
129.503286381863));
#146733=CARTESIAN_POINT('Ctrl Pts',(88.9929666749589,-5.80615438310364,
129.655130439298));
#146734=CARTESIAN_POINT('Ctrl Pts',(88.9856647442739,-5.83437558247517,
129.808279716939));
#146735=CARTESIAN_POINT('Ctrl Pts',(88.9783628135889,-5.85651055570804,
129.962211774795));
#146736=CARTESIAN_POINT('Ctrl Pts',(88.9710546158251,-5.87866452687827,
130.116275948988));
#146737=CARTESIAN_POINT('Ctrl Pts',(88.9637464180612,-5.89472179038301,
130.271123863905));
#146738=CARTESIAN_POINT('Ctrl Pts',(88.9564382202974,-5.90465460925057,
130.426227693906));
#146739=CARTESIAN_POINT('Ctrl Pts',(88.9504172109355,-5.91283796680676,
130.554013181203));
#146740=CARTESIAN_POINT('Ctrl Pts',(88.9443962015735,-5.91686523723295,
130.681972202389));
#146741=CARTESIAN_POINT('Ctrl Pts',(88.9383751922115,-5.91674749024185,
130.809810316349));
#146742=CARTESIAN_POINT('',(87.1883751922115,-5.92167067617498,130.802270369068));
#146743=CARTESIAN_POINT('Ctrl Pts',(88.9383751922115,-5.91711345945967,
130.80981065343));
#146744=CARTESIAN_POINT('Ctrl Pts',(88.9173446752718,-5.92125755772848,
131.2563625544));
#146745=CARTESIAN_POINT('Ctrl Pts',(88.8034982837279,-5.67087300393402,
133.669120225896));
#146746=CARTESIAN_POINT('Ctrl Pts',(88.5968360175794,-2.36378464613456,
137.391475515387));
#146747=CARTESIAN_POINT('Ctrl Pts',(88.3183883937666,4.26424298043648,136.353576087713));
#146748=CARTESIAN_POINT('Ctrl Pts',(88.0399407699536,6.97363962783762,130.216218737225));
#146749=CARTESIAN_POINT('Ctrl Pts',(87.7614931461409,3.27460213849075,124.619335042443));
#146750=CARTESIAN_POINT('Ctrl Pts',(87.483045522328,-3.43363474291932,124.706187695898));
#146751=CARTESIAN_POINT('Ctrl Pts',(87.2920062043515,-5.8712296258447,128.610555365562));
#146752=CARTESIAN_POINT('Ctrl Pts',(87.1937827609793,-5.92616330583837,
130.687876557329));
#146753=CARTESIAN_POINT('Ctrl Pts',(87.1883751922115,-5.92564232318124,
130.802268967144));
#146754=CARTESIAN_POINT('',(85.4383751922433,-5.91674833501214,130.799921852979));
#146755=CARTESIAN_POINT('Ctrl Pts',(87.1883751922115,-5.9167496313956,130.802272106112));
#146756=CARTESIAN_POINT('Ctrl Pts',(87.181017727412,-5.9168044873817,130.957679027627));
#146757=CARTESIAN_POINT('Ctrl Pts',(87.1736602626125,-5.91073235004027,
131.113335685801));
#146758=CARTESIAN_POINT('Ctrl Pts',(87.166302797813,-5.89850038482534,131.268713686594));
#146759=CARTESIAN_POINT('Ctrl Pts',(87.158953758399,-5.88628242701996,131.423913756591));
#146760=CARTESIAN_POINT('Ctrl Pts',(87.151604718985,-5.86791870763707,131.578835428669));
#146761=CARTESIAN_POINT('Ctrl Pts',(87.144255679571,-5.84342836198335,131.732948546019));
#146762=CARTESIAN_POINT('Ctrl Pts',(87.1369133832024,-5.81896048722727,
131.886920258257));
#146763=CARTESIAN_POINT('Ctrl Pts',(87.1295710868338,-5.78837723357423,
132.04008451902));
#146764=CARTESIAN_POINT('Ctrl Pts',(87.1222287904652,-5.75174965655959,
132.191914742913));
#146765=CARTESIAN_POINT('Ctrl Pts',(87.1148915608766,-5.71514735554355,
132.343640191638));
#146766=CARTESIAN_POINT('Ctrl Pts',(87.1075543312879,-5.67250912311375,
132.494033067684));
#146767=CARTESIAN_POINT('Ctrl Pts',(87.1002171016993,-5.62395732798598,
132.642575658167));
#146768=CARTESIAN_POINT('Ctrl Pts',(87.0928825618798,-5.57542333155484,
132.791063794134));
#146769=CARTESIAN_POINT('Ctrl Pts',(87.0855480220604,-5.52098020160226,
132.937702632535));
#146770=CARTESIAN_POINT('Ctrl Pts',(87.0782134822409,-5.4608005143236,133.081988397793));
#146771=CARTESIAN_POINT('Ctrl Pts',(87.0708802169912,-5.40063128485238,
133.226249089595));
#146772=CARTESIAN_POINT('Ctrl Pts',(87.0635469517414,-5.33472762736758,
133.368157170652));
#146773=CARTESIAN_POINT('Ctrl Pts',(87.0562136864917,-5.2633106383249,133.507227925999));
#146774=CARTESIAN_POINT('Ctrl Pts',(87.0488801855783,-5.19189135420766,
133.646303150559));
#146775=CARTESIAN_POINT('Ctrl Pts',(87.0415466846648,-5.1149585595205,133.782540529362));
#146776=CARTESIAN_POINT('Ctrl Pts',(87.0342131837514,-5.03277965687032,
133.915479305095));
#146777=CARTESIAN_POINT('Ctrl Pts',(87.0268779370043,-4.95058119048251,
134.048449728602));
#146778=CARTESIAN_POINT('Ctrl Pts',(87.0195426902574,-4.86313433070873,
134.178119662737));
#146779=CARTESIAN_POINT('Ctrl Pts',(87.0122074435103,-4.77075006606631,
134.30405694291));
#146780=CARTESIAN_POINT('Ctrl Pts',(87.0048646043054,-4.67827017769559,
134.430124576367));
#146781=CARTESIAN_POINT('Ctrl Pts',(86.9975217651005,-4.58084290189408,
134.55245153159));
#146782=CARTESIAN_POINT('Ctrl Pts',(86.9901789258955,-4.47882025222901,
134.6706378594));
#146783=CARTESIAN_POINT('Ctrl Pts',(86.9828321944078,-4.37674352252813,
134.788886835267));
#146784=CARTESIAN_POINT('Ctrl Pts',(86.97548546292,-4.27006682580401,134.902990533726));
#146785=CARTESIAN_POINT('Ctrl Pts',(86.9681387314323,-4.15917887539443,
135.012586092154));
#146786=CARTESIAN_POINT('Ctrl Pts',(86.9607807868572,-4.04812168016111,
135.122348922868));
#146787=CARTESIAN_POINT('Ctrl Pts',(86.953422842282,-3.93284067045875,135.22758961038));
#146788=CARTESIAN_POINT('Ctrl Pts',(86.9460648977068,-3.81375820132093,
135.327985153749));
#146789=CARTESIAN_POINT('Ctrl Pts',(86.9394266900386,-3.70632410043697,
135.41856024018));
#146790=CARTESIAN_POINT('Ctrl Pts',(86.9327884823704,-3.59579644350382,
135.505192137477));
#146791=CARTESIAN_POINT('Ctrl Pts',(86.9261502747022,-3.48250434805229,
135.587674743598));
#146792=CARTESIAN_POINT('Ctrl Pts',(86.9187270082967,-3.35581391470071,
135.679912044636));
#146793=CARTESIAN_POINT('Ctrl Pts',(86.9113037418913,-3.22526489625941,
135.767252075241));
#146794=CARTESIAN_POINT('Ctrl Pts',(86.9038804754859,-3.09127273754494,
135.849354514947));
#146795=CARTESIAN_POINT('Ctrl Pts',(86.8964659827649,-2.95743894643452,
135.931359916388));
#146796=CARTESIAN_POINT('Ctrl Pts',(86.8890514900438,-2.82017043061389,
136.008139855822));
#146797=CARTESIAN_POINT('Ctrl Pts',(86.8816369973228,-2.67991444553776,
136.07939513187));
#146798=CARTESIAN_POINT('Ctrl Pts',(86.874229650969,-2.53979364446059,136.1505817294));
#146799=CARTESIAN_POINT('Ctrl Pts',(86.8668223046153,-2.39669143709357,
136.216254096383));
#146800=CARTESIAN_POINT('Ctrl Pts',(86.8594149582615,-2.25108261593864,
136.276157179822));
#146801=CARTESIAN_POINT('Ctrl Pts',(86.8520131365861,-2.10558239533646,
136.336015585281));
#146802=CARTESIAN_POINT('Ctrl Pts',(86.8446113149108,-1.9575796271664,136.390113133535));
#146803=CARTESIAN_POINT('Ctrl Pts',(86.8372094932354,-1.80757207850582,
136.438241495212));
#146804=CARTESIAN_POINT('Ctrl Pts',(86.829811578924,-1.65764371766262,136.486344450301));
#146805=CARTESIAN_POINT('Ctrl Pts',(86.8224136646127,-1.50571303855146,
136.528484380601));
#146806=CARTESIAN_POINT('Ctrl Pts',(86.8150157503013,-1.35229597999468,
136.564501774256));
#146807=CARTESIAN_POINT('Ctrl Pts',(86.8076190653891,-1.19890441656933,
136.600513182473));
#146808=CARTESIAN_POINT('Ctrl Pts',(86.8002223804769,-1.04402732700005,
136.630403988158));
#146809=CARTESIAN_POINT('Ctrl Pts',(86.7928256955647,-0.888194058801287,
136.65406504398));
#146810=CARTESIAN_POINT('Ctrl Pts',(86.7854293386293,-0.732367700412934,
136.677725050647));
#146811=CARTESIAN_POINT('Ctrl Pts',(86.7780329816938,-0.575585616764118,
136.695155800659));
#146812=CARTESIAN_POINT('Ctrl Pts',(86.7706366247584,-0.418385287396174,
136.706299647562));
#146813=CARTESIAN_POINT('Ctrl Pts',(86.7632391354218,-0.261160890256827,
136.717445200616));
#146814=CARTESIAN_POINT('Ctrl Pts',(86.7558416460852,-0.103518492284539,
136.722301907616));
#146815=CARTESIAN_POINT('Ctrl Pts',(86.7484441567487,0.054001541880814,
136.720864179297));
#146816=CARTESIAN_POINT('Ctrl Pts',(86.7410440742336,0.211576794450855,
136.719425946984));
#146817=CARTESIAN_POINT('Ctrl Pts',(86.7336439917187,0.369029224761944,
136.711688889623));
#146818=CARTESIAN_POINT('Ctrl Pts',(86.7262439092036,0.525820859046008,
136.697699483327));
#146819=CARTESIAN_POINT('Ctrl Pts',(86.7188356895372,0.682784901850091,
136.683694694241));
#146820=CARTESIAN_POINT('Ctrl Pts',(86.7114274698707,0.839086325483952,
136.66342385939));
#146821=CARTESIAN_POINT('Ctrl Pts',(86.7040192502042,0.99419391973684,136.636985156524));
#146822=CARTESIAN_POINT('Ctrl Pts',(86.6966064709022,1.14939698012588,136.610530181078));
#146823=CARTESIAN_POINT('Ctrl Pts',(86.6891936916001,1.30340438264431,136.57789985037));
#146824=CARTESIAN_POINT('Ctrl Pts',(86.681780912298,1.45569794809776,136.539242834875));
#146825=CARTESIAN_POINT('Ctrl Pts',(86.6743575412692,1.60820911773939,136.500530584423));
#146826=CARTESIAN_POINT('Ctrl Pts',(86.6669341702405,1.75900120257212,136.455774556602));
#146827=CARTESIAN_POINT('Ctrl Pts',(86.6595107992117,1.90757315094241,136.405172633364));
#146828=CARTESIAN_POINT('Ctrl Pts',(86.6555747497709,1.98634956290362,136.378342279486));
#146829=CARTESIAN_POINT('Ctrl Pts',(86.6516387003301,2.06450216909274,136.34986923062));
#146830=CARTESIAN_POINT('Ctrl Pts',(86.6477026508893,2.14195897970616,136.319788279294));
#146831=CARTESIAN_POINT('Ctrl Pts',(86.6402793844839,2.28804010717831,136.263056543888));
#146832=CARTESIAN_POINT('Ctrl Pts',(86.6328561180785,2.43208668182863,136.200431377274));
#146833=CARTESIAN_POINT('Ctrl Pts',(86.625432851673,2.57358782434125,136.132078353417));
#146834=CARTESIAN_POINT('Ctrl Pts',(86.618018358952,2.71492172425416,136.063806117158));
#146835=CARTESIAN_POINT('Ctrl Pts',(86.610603866231,2.85371584759169,135.989819659871));
#146836=CARTESIAN_POINT('Ctrl Pts',(86.60318937351,2.9894767152613,135.910333544581));
#146837=CARTESIAN_POINT('Ctrl Pts',(86.5957820271562,3.12510673149553,135.830924041002));
#146838=CARTESIAN_POINT('Ctrl Pts',(86.5883746808025,3.25770899232424,135.74602561957));
#146839=CARTESIAN_POINT('Ctrl Pts',(86.5809673344487,3.38681227749217,135.655899874289));
#146840=CARTESIAN_POINT('Ctrl Pts',(86.5735655127733,3.51581927255932,135.56584134819));
#146841=CARTESIAN_POINT('Ctrl Pts',(86.5661636910979,3.64133218339242,135.470563473909));
#146842=CARTESIAN_POINT('Ctrl Pts',(86.5587618694225,3.76290668132671,135.370372429873));
#146843=CARTESIAN_POINT('Ctrl Pts',(86.5513639551112,3.88441700102952,135.27023427591));
#146844=CARTESIAN_POINT('Ctrl Pts',(86.5439660407998,4.00199276102789,135.165188354324));
#146845=CARTESIAN_POINT('Ctrl Pts',(86.5365681264885,4.11522088194545,135.055582519008));
#146846=CARTESIAN_POINT('Ctrl Pts',(86.5291714415763,4.22843018640389,134.945994898192));
#146847=CARTESIAN_POINT('Ctrl Pts',(86.5217747566641,4.3372930177734,134.831849126987));
#146848=CARTESIAN_POINT('Ctrl Pts',(86.5143780717518,4.44143142205343,134.713531563649));
#146849=CARTESIAN_POINT('Ctrl Pts',(86.5069817148164,4.54556520872726,134.595219246636));
#146850=CARTESIAN_POINT('Ctrl Pts',(86.4995853578809,4.64497473820458,134.472735785514));
#146851=CARTESIAN_POINT('Ctrl Pts',(86.4921890009455,4.73932099006906,134.346502217727));
#146852=CARTESIAN_POINT('Ctrl Pts',(86.4847915116089,4.83368168658562,134.220249323258));
#146853=CARTESIAN_POINT('Ctrl Pts',(86.4773940222723,4.92297733846744,134.090245477944));
#146854=CARTESIAN_POINT('Ctrl Pts',(86.4699965329358,5.00691116302107,133.956942284726));
#146855=CARTESIAN_POINT('Ctrl Pts',(86.4625964504208,5.0908744104469,133.82359236228));
#146856=CARTESIAN_POINT('Ctrl Pts',(86.4551963679058,5.16947188953632,133.686941104884));
#146857=CARTESIAN_POINT('Ctrl Pts',(86.4477962853908,5.24245191399824,133.547466246578));
#146858=CARTESIAN_POINT('Ctrl Pts',(86.4403880657243,5.31551218749959,133.407838021327));
#146859=CARTESIAN_POINT('Ctrl Pts',(86.4329798460578,5.38294249738766,133.265380325557));
#146860=CARTESIAN_POINT('Ctrl Pts',(86.4255716263913,5.44453831129131,133.120593148937));
#146861=CARTESIAN_POINT('Ctrl Pts',(86.4181588470893,5.50617203639054,132.975716858225));
#146862=CARTESIAN_POINT('Ctrl Pts',(86.4107460677872,5.56196397792784,132.828508577983));
#146863=CARTESIAN_POINT('Ctrl Pts',(86.4033332884852,5.61175912807262,132.679484627063));
#146864=CARTESIAN_POINT('Ctrl Pts',(86.3959099174564,5.66162542786313,132.530247743734));
#146865=CARTESIAN_POINT('Ctrl Pts',(86.3884865464276,5.7054777192543,132.379190365847));
#146866=CARTESIAN_POINT('Ctrl Pts',(86.3810631753989,5.74321165527887,132.226841002376));
#146867=CARTESIAN_POINT('Ctrl Pts',(86.3771271259581,5.76321909357249,132.146061714291));
#146868=CARTESIAN_POINT('Ctrl Pts',(86.3731910765173,5.78150730379123,132.064919334902));
#146869=CARTESIAN_POINT('Ctrl Pts',(86.3692550270765,5.7980666456284,131.983493237483));
#146870=CARTESIAN_POINT('Ctrl Pts',(86.3618317606711,5.82929704753391,131.829926158971));
#146871=CARTESIAN_POINT('Ctrl Pts',(86.3544084942657,5.85446941335588,131.674885263847));
#146872=CARTESIAN_POINT('Ctrl Pts',(86.3469852278602,5.87344690241255,131.518889866121));
#146873=CARTESIAN_POINT('Ctrl Pts',(86.3395707351392,5.89240196165317,131.363078842));
#146874=CARTESIAN_POINT('Ctrl Pts',(86.3321562424181,5.90517667363057,131.206315927798));
#146875=CARTESIAN_POINT('Ctrl Pts',(86.3247417496971,5.91168481879268,131.049132278009));
#146876=CARTESIAN_POINT('Ctrl Pts',(86.3173344033434,5.91818669115943,130.892100127741));
#146877=CARTESIAN_POINT('Ctrl Pts',(86.3099270569896,5.9184340057289,130.734648419672));
#146878=CARTESIAN_POINT('Ctrl Pts',(86.3025197106359,5.91239214288674,130.577315002697));
#146879=CARTESIAN_POINT('Ctrl Pts',(86.2951178889605,5.90635478629382,130.420098930921));
#146880=CARTESIAN_POINT('Ctrl Pts',(86.287716067285,5.8940376063805,130.263001345986));
#146881=CARTESIAN_POINT('Ctrl Pts',(86.2803142456096,5.87545802923088,130.106561571102));
#146882=CARTESIAN_POINT('Ctrl Pts',(86.2729163312983,5.85688826009538,129.950204379556));
#146883=CARTESIAN_POINT('Ctrl Pts',(86.2655184169869,5.83206272143745,129.794504676245));
#146884=CARTESIAN_POINT('Ctrl Pts',(86.2581205026755,5.80105079309351,129.639998020069));
#146885=CARTESIAN_POINT('Ctrl Pts',(86.2507238177633,5.77004401836949,129.485517040097));
#146886=CARTESIAN_POINT('Ctrl Pts',(86.2433271328511,5.73285296775542,129.332229079408));
#146887=CARTESIAN_POINT('Ctrl Pts',(86.2359304479389,5.68959840202705,129.180660957484));
#146888=CARTESIAN_POINT('Ctrl Pts',(86.2285340910034,5.64634575425143,129.029099556248));
#146889=CARTESIAN_POINT('Ctrl Pts',(86.221137734068,5.5970302283931,128.879258201114));
#146890=CARTESIAN_POINT('Ctrl Pts',(86.2137413771325,5.54182280636129,128.73164970058));
#146891=CARTESIAN_POINT('Ctrl Pts',(86.2063438877959,5.48660693193224,128.584018600808));
#146892=CARTESIAN_POINT('Ctrl Pts',(86.1989463984593,5.42549749597888,128.438621385983));
#146893=CARTESIAN_POINT('Ctrl Pts',(86.1915489091227,5.35871402655086,128.29595185021));
#146894=CARTESIAN_POINT('Ctrl Pts',(86.1841488266077,5.29190714628125,128.153232301854));
#146895=CARTESIAN_POINT('Ctrl Pts',(86.1767487440927,5.2194224305666,128.013242674184));
#146896=CARTESIAN_POINT('Ctrl Pts',(86.1693486615777,5.14152576799876,127.876452944926));
#146897=CARTESIAN_POINT('Ctrl Pts',(86.1619404419113,5.06354345004241,127.739512801298));
#146898=CARTESIAN_POINT('Ctrl Pts',(86.1545322222448,4.98013748555134,127.605779907578));
#146899=CARTESIAN_POINT('Ctrl Pts',(86.1471240025784,4.89161797525111,127.47569659927));
#146900=CARTESIAN_POINT('Ctrl Pts',(86.1397112232763,4.80304398266932,127.345533226856));
#146901=CARTESIAN_POINT('Ctrl Pts',(86.1322984439742,4.7093503945407,127.219024215098));
#146902=CARTESIAN_POINT('Ctrl Pts',(86.1248856646721,4.61088781902221,127.096579059425));
#146903=CARTESIAN_POINT('Ctrl Pts',(86.1174622936434,4.51228455555823,126.973958948371));
#146904=CARTESIAN_POINT('Ctrl Pts',(86.1100389226146,4.40889894002283,126.855414571132));
#146905=CARTESIAN_POINT('Ctrl Pts',(86.1026155515859,4.30111921990029,126.741319389778));
#146906=CARTESIAN_POINT('Ctrl Pts',(86.0986795021451,4.24397182615247,126.680823386948));
#146907=CARTESIAN_POINT('Ctrl Pts',(86.0947434527043,4.18558966863885,126.621577559669));
#146908=CARTESIAN_POINT('Ctrl Pts',(86.0908074032635,4.12603431552053,126.563632921799));
#146909=CARTESIAN_POINT('Ctrl Pts',(86.0833841368581,4.01371477819838,126.454351143165));
#146910=CARTESIAN_POINT('Ctrl Pts',(86.0759608704526,3.89688076074025,126.349369527982));
#146911=CARTESIAN_POINT('Ctrl Pts',(86.0685376040472,3.77589521099997,126.249083906097));
#146912=CARTESIAN_POINT('Ctrl Pts',(86.0611231113261,3.65505265613192,126.14891681349));
#146913=CARTESIAN_POINT('Ctrl Pts',(86.0537086186051,3.53006862052098,126.053434902231));
#146914=CARTESIAN_POINT('Ctrl Pts',(86.0462941258841,3.40134337571183,125.962997813251));
#146915=CARTESIAN_POINT('Ctrl Pts',(86.0388867795303,3.27274220114004,125.872647890943));
#146916=CARTESIAN_POINT('Ctrl Pts',(86.0314794331765,3.14040729944275,125.787333324008));
#146917=CARTESIAN_POINT('Ctrl Pts',(86.0240720868227,3.00477246538082,125.707373959374));
#146918=CARTESIAN_POINT('Ctrl Pts',(86.0166702651474,2.86923879289573,125.627474231451));
#146919=CARTESIAN_POINT('Ctrl Pts',(86.009268443472,2.73041040884894,125.552921941774));
#146920=CARTESIAN_POINT('Ctrl Pts',(86.0018666217966,2.5887504803534,125.483993946652));
#146921=CARTESIAN_POINT('Ctrl Pts',(85.9944687074853,2.44716533303143,125.415102338082));
#146922=CARTESIAN_POINT('Ctrl Pts',(85.9870707931739,2.30275195294887,125.351829274035));
#146923=CARTESIAN_POINT('Ctrl Pts',(85.9796728788626,2.15599842247466,125.294405865956));
#146924=CARTESIAN_POINT('Ctrl Pts',(85.9722761939504,2.00926927977482,125.236992000607));
#146925=CARTESIAN_POINT('Ctrl Pts',(85.9648795090382,1.86020110580809,125.185425997775));
#146926=CARTESIAN_POINT('Ctrl Pts',(85.957482824126,1.70930240287311,125.139891016797));
#146927=CARTESIAN_POINT('Ctrl Pts',(85.9500864671905,1.55841039094474,125.094358054889));
#146928=CARTESIAN_POINT('Ctrl Pts',(85.9426901102551,1.40568836881746,125.054855690953));
#146929=CARTESIAN_POINT('Ctrl Pts',(85.9352937533197,1.25166019670436,125.021517258587));
#146930=CARTESIAN_POINT('Ctrl Pts',(85.9278962639831,1.09760844248501,124.988173722022));
#146931=CARTESIAN_POINT('Ctrl Pts',(85.9204987746466,0.942250504976168,
124.960996075062));
#146932=CARTESIAN_POINT('Ctrl Pts',(85.91310128531,0.786120487417467,124.940066530315));
#146933=CARTESIAN_POINT('Ctrl Pts',(85.905701202795,0.629935738723143,124.91912964875));
#146934=CARTESIAN_POINT('Ctrl Pts',(85.8983011202801,0.472978740871434,
124.904445279762));
#146935=CARTESIAN_POINT('Ctrl Pts',(85.8909010377651,0.315788618710606,
124.896043758189));
#146936=CARTESIAN_POINT('Ctrl Pts',(85.8834928180986,0.158425649850476,
124.88763299828));
#146937=CARTESIAN_POINT('Ctrl Pts',(85.8760845984321,0.000829417739716704,
124.885518902723));
#146938=CARTESIAN_POINT('Ctrl Pts',(85.8686763787657,-0.156460311216934,
124.889679668139));
#146939=CARTESIAN_POINT('Ctrl Pts',(85.8612635994636,-0.313846849377126,
124.893842994437));
#146940=CARTESIAN_POINT('Ctrl Pts',(85.8538508201616,-0.470926136867647,
124.90428885266));
#146941=CARTESIAN_POINT('Ctrl Pts',(85.8464380408595,-0.627164141312106,
124.920943608518));
#146942=CARTESIAN_POINT('Ctrl Pts',(85.8390146698307,-0.78362538594404,
124.937622161473));
#146943=CARTESIAN_POINT('Ctrl Pts',(85.831591298802,-0.939242578396752,
124.96052727635));
#146944=CARTESIAN_POINT('Ctrl Pts',(85.8241679277732,-1.09349165720549,
124.989534174918));
#146945=CARTESIAN_POINT('Ctrl Pts',(85.8202318783324,-1.17527821994747,
125.004914328549));
#146946=CARTESIAN_POINT('Ctrl Pts',(85.8162958288915,-1.25668039456697,
125.022009074331));
#146947=CARTESIAN_POINT('Ctrl Pts',(85.8123597794507,-1.33762198256737,
125.040794187459));
#146948=CARTESIAN_POINT('Ctrl Pts',(85.8049365130452,-1.4902752914328,125.076222324556));
#146949=CARTESIAN_POINT('Ctrl Pts',(85.7975132466398,-1.64175093778632,
125.11777296503));
#146950=CARTESIAN_POINT('Ctrl Pts',(85.7900899802343,-1.79151971658515,
125.165354706274));
#146951=CARTESIAN_POINT('Ctrl Pts',(85.7826754875133,-1.94111148112497,
125.212880209852));
#146952=CARTESIAN_POINT('Ctrl Pts',(85.7752609947923,-2.08900004140721,
125.266422513432));
#146953=CARTESIAN_POINT('Ctrl Pts',(85.7678465020713,-2.23466646478566,
125.325839251936));
#146954=CARTESIAN_POINT('Ctrl Pts',(85.7604391557175,-2.38019248938183,
125.385198722351));
#146955=CARTESIAN_POINT('Ctrl Pts',(85.7530318093637,-2.52350029760603,
125.450421215716));
#146956=CARTESIAN_POINT('Ctrl Pts',(85.7456244630099,-2.66408631651537,
125.52131465329));
#146957=CARTESIAN_POINT('Ctrl Pts',(85.7382226413345,-2.8045674810671,125.592155215863));
#146958=CARTESIAN_POINT('Ctrl Pts',(85.7308208196591,-2.94233056645227,
125.668658133575));
#146959=CARTESIAN_POINT('Ctrl Pts',(85.7234189979836,-3.07689229247884,
125.750583378413));
#146960=CARTESIAN_POINT('Ctrl Pts',(85.7160210836722,-3.21138298441854,
125.832465375552));
#146961=CARTESIAN_POINT('Ctrl Pts',(85.7086231693608,-3.34267536461682,
125.919763805567));
#146962=CARTESIAN_POINT('Ctrl Pts',(85.7012252550494,-3.47031117202516,
126.012192952321));
#146963=CARTESIAN_POINT('Ctrl Pts',(85.6938285701372,-3.59792576867703,
126.104606739027));
#146964=CARTESIAN_POINT('Ctrl Pts',(85.686431885225,-3.72188469650641,126.202149331515));
#146965=CARTESIAN_POINT('Ctrl Pts',(85.6790352003128,-3.84175900046248,
126.304491914496));
#146966=CARTESIAN_POINT('Ctrl Pts',(85.6716388433773,-3.96162798906637,
126.4068299595));
#146967=CARTESIAN_POINT('Ctrl Pts',(85.6642424864419,-4.07741243001356,
126.513967329422));
#146968=CARTESIAN_POINT('Ctrl Pts',(85.6568461295064,-4.18871698673091,
126.625535355896));
#146969=CARTESIAN_POINT('Ctrl Pts',(85.6494486401698,-4.30003858445971,
126.737120463719));
#146970=CARTESIAN_POINT('Ctrl Pts',(85.6420511508333,-4.40687866861079,
126.853137314478));
#146971=CARTESIAN_POINT('Ctrl Pts',(85.6346536614967,-4.50887937553932,
126.973180989914));
#146972=CARTESIAN_POINT('Ctrl Pts',(85.6272535789817,-4.61091583865813,
127.093266746475));
#146973=CARTESIAN_POINT('Ctrl Pts',(85.6198534964666,-4.70810930539743,
127.217381853899));
#146974=CARTESIAN_POINT('Ctrl Pts',(85.6124534139516,-4.80014284405043,
127.345089127901));
#146975=CARTESIAN_POINT('Ctrl Pts',(85.6050451942851,-4.89227758304025,
127.472936829179));
#146976=CARTESIAN_POINT('Ctrl Pts',(85.5976369746186,-4.97924084446482,
127.604384282323));
#146977=CARTESIAN_POINT('Ctrl Pts',(85.5902287549521,-5.06075921519709,
127.738965581311));
#146978=CARTESIAN_POINT('Ctrl Pts',(85.58281597565,-5.14232775912674,127.873629712844));
#146979=CARTESIAN_POINT('Ctrl Pts',(85.5754031963479,-5.21844455452554,
128.011431207651));
#146980=CARTESIAN_POINT('Ctrl Pts',(85.5679904170458,-5.28888289446262,
128.151880968038));
#146981=CARTESIAN_POINT('Ctrl Pts',(85.560567046017,-5.35942188000269,128.292531409628));
#146982=CARTESIAN_POINT('Ctrl Pts',(85.5531436749882,-5.4242660518313,128.435837335027));
#146983=CARTESIAN_POINT('Ctrl Pts',(85.5457203039595,-5.48323712138758,
128.581290390799));
#146984=CARTESIAN_POINT('Ctrl Pts',(85.5417842545189,-5.51450499745621,
128.658413091064));
#146985=CARTESIAN_POINT('Ctrl Pts',(85.5378482050782,-5.54412256742039,
128.736139173653));
#146986=CARTESIAN_POINT('Ctrl Pts',(85.5339121556376,-5.57206902514388,
128.814391436515));
#146987=CARTESIAN_POINT('Ctrl Pts',(85.5252696428826,-5.6334319782717,128.986212494686));
#146988=CARTESIAN_POINT('Ctrl Pts',(85.5166271301276,-5.68688789089793,
129.160997686617));
#146989=CARTESIAN_POINT('Ctrl Pts',(85.5079846173726,-5.73218221780913,
129.338066791509));
#146990=CARTESIAN_POINT('Ctrl Pts',(85.4993767151302,-5.77729515535862,
129.514426790998));
#146991=CARTESIAN_POINT('Ctrl Pts',(85.4907688128877,-5.81431165938518,
129.693052344244));
#146992=CARTESIAN_POINT('Ctrl Pts',(85.4821609106453,-5.84302684476834,
129.873249531918));
#146993=CARTESIAN_POINT('Ctrl Pts',(85.4736201635406,-5.87151800666975,
130.052040898914));
#146994=CARTESIAN_POINT('Ctrl Pts',(85.465079416436,-5.89183680036727,130.232379354862));
#146995=CARTESIAN_POINT('Ctrl Pts',(85.4565386693314,-5.90383020450548,
130.413567220912));
#146996=CARTESIAN_POINT('Ctrl Pts',(85.4504841769687,-5.9123322679512,130.542010381418));
#146997=CARTESIAN_POINT('Ctrl Pts',(85.444429684606,-5.91665152736383,130.670879980918));
#146998=CARTESIAN_POINT('Ctrl Pts',(85.4383751922433,-5.91674833501214,
130.799921852979));
#146999=CARTESIAN_POINT('',(83.6883739829004,-5.91264948157148,130.808194539386));
#147000=CARTESIAN_POINT('Ctrl Pts',(85.4383751922114,-5.91674833501265,
130.799921853659));
#147001=CARTESIAN_POINT('Ctrl Pts',(85.4307539146953,-5.91687019458339,
130.962357258523));
#147002=CARTESIAN_POINT('Ctrl Pts',(85.4231326371792,-5.91029809451247,
131.124860175597));
#147003=CARTESIAN_POINT('Ctrl Pts',(85.4155113596631,-5.8970454115672,131.286839608211));
#147004=CARTESIAN_POINT('Ctrl Pts',(85.4081075734955,-5.88417092556854,
131.444196571015));
#147005=CARTESIAN_POINT('Ctrl Pts',(85.400703787328,-5.86499199036885,131.601059130023));
#147006=CARTESIAN_POINT('Ctrl Pts',(85.3933000011605,-5.83957365415491,
131.756888884968));
#147007=CARTESIAN_POINT('Ctrl Pts',(85.3858955184429,-5.81415292657773,
131.912733300414));
#147008=CARTESIAN_POINT('Ctrl Pts',(85.3784910357254,-5.78249168839217,
132.067544351286));
#147009=CARTESIAN_POINT('Ctrl Pts',(85.3710865530078,-5.74470638305384,
132.220792449671));
#147010=CARTESIAN_POINT('Ctrl Pts',(85.3636799272186,-5.70691014155405,
132.374084902494));
#147011=CARTESIAN_POINT('Ctrl Pts',(85.3562733014294,-5.66298639222918,
132.525813141182));
#147012=CARTESIAN_POINT('Ctrl Pts',(85.3488666756402,-5.61310181538212,
132.675461516143));
#147013=CARTESIAN_POINT('Ctrl Pts',(85.3410831636556,-5.56067886155875,
132.832724749514));
#147014=CARTESIAN_POINT('Ctrl Pts',(85.3332996516709,-5.50167272599804,
132.987690471323));
#147015=CARTESIAN_POINT('Ctrl Pts',(85.3255161396863,-5.43633420588795,
133.139783697951));
#147016=CARTESIAN_POINT('Ctrl Pts',(85.3180966545036,-5.37405150075683,
133.284763681742));
#147017=CARTESIAN_POINT('Ctrl Pts',(85.3106771693208,-5.30601546554471,
133.427133436658));
#147018=CARTESIAN_POINT('Ctrl Pts',(85.303257684138,-5.23249040253982,133.566420491977));
#147019=CARTESIAN_POINT('Ctrl Pts',(85.2958327199148,-5.15891104374737,
133.705810406103));
#147020=CARTESIAN_POINT('Ctrl Pts',(85.2884077556916,-5.07983476653098,
133.84211276473));
#147021=CARTESIAN_POINT('Ctrl Pts',(85.2809827914684,-4.99556937636149,
133.974883787085));
#147022=CARTESIAN_POINT('Ctrl Pts',(85.2735474374655,-4.91118607332156,
134.107840596421));
#147023=CARTESIAN_POINT('Ctrl Pts',(85.2661120834625,-4.82159937344177,
134.237255901933));
#147024=CARTESIAN_POINT('Ctrl Pts',(85.2586767294596,-4.7271578877185,134.36271822566));
#147025=CARTESIAN_POINT('Ctrl Pts',(85.2576059969147,-4.71355778578472,
134.380785501693));
#147026=CARTESIAN_POINT('Ctrl Pts',(85.2565352643698,-4.69985707014519,
134.398770864142));
#147027=CARTESIAN_POINT('Ctrl Pts',(85.2554645318249,-4.68605684431754,
134.416673147556));
#147028=CARTESIAN_POINT('Ctrl Pts',(85.2480412654194,-4.59038145529484,
134.540787633177));
#147029=CARTESIAN_POINT('Ctrl Pts',(85.240617999014,-4.48962706034283,134.661286093997));
#147030=CARTESIAN_POINT('Ctrl Pts',(85.2331947326086,-4.38409676459561,
134.777725202041));
#147031=CARTESIAN_POINT('Ctrl Pts',(85.2257802398875,-4.27869119689414,
134.89402668873));
#147032=CARTESIAN_POINT('Ctrl Pts',(85.2183657471666,-4.16852121247841,
135.006278098828));
#147033=CARTESIAN_POINT('Ctrl Pts',(85.2109512544455,-4.0539319978261,135.114066630684));
#147034=CARTESIAN_POINT('Ctrl Pts',(85.2035439080918,-3.93945322857323,
135.221751271894));
#147035=CARTESIAN_POINT('Ctrl Pts',(85.196136561738,-3.82056397883278,135.324981344231));
#147036=CARTESIAN_POINT('Ctrl Pts',(85.1887292153843,-3.6976482659861,135.423378680266));
#147037=CARTESIAN_POINT('Ctrl Pts',(85.1813273937089,-3.57482422831567,
135.521702627856));
#147038=CARTESIAN_POINT('Ctrl Pts',(85.1739255720335,-3.4479799972602,135.615200783779));
#147039=CARTESIAN_POINT('Ctrl Pts',(85.1665237503581,-3.31753476585832,
135.703533368125));
#147040=CARTESIAN_POINT('Ctrl Pts',(85.1591258360468,-3.18715839547835,
135.791819322388));
#147041=CARTESIAN_POINT('Ctrl Pts',(85.1517279217354,-3.05318511887992,
135.874944926978));
#147042=CARTESIAN_POINT('Ctrl Pts',(85.1443300074241,-2.916065283605,135.952612148353));
#147043=CARTESIAN_POINT('Ctrl Pts',(85.1369333225119,-2.77896823515908,
136.030266462846));
#147044=CARTESIAN_POINT('Ctrl Pts',(85.1295366375997,-2.63872599033432,
136.102464010618));
#147045=CARTESIAN_POINT('Ctrl Pts',(85.1221399526875,-2.49581591455787,
136.168951327316));
#147046=CARTESIAN_POINT('Ctrl Pts',(85.114743595752,-2.35291217556375,136.235435695897));
#147047=CARTESIAN_POINT('Ctrl Pts',(85.1073472388166,-2.20734117928812,
136.29621017938));
#147048=CARTESIAN_POINT('Ctrl Pts',(85.0999508818811,-2.05960256412904,
136.351068455584));
#147049=CARTESIAN_POINT('Ctrl Pts',(85.0925533925445,-1.91184132981071,
136.405935130731));
#147050=CARTESIAN_POINT('Ctrl Pts',(85.085155903208,-1.76191216578942,136.454883665105));
#147051=CARTESIAN_POINT('Ctrl Pts',(85.0777584138714,-1.61033210410749,
136.497756886664));
#147052=CARTESIAN_POINT('Ctrl Pts',(85.0703583313564,-1.45869890627057,
136.540645137364));
#147053=CARTESIAN_POINT('Ctrl Pts',(85.0629582488414,-1.30541401752857,
136.577453733514));
#147054=CARTESIAN_POINT('Ctrl Pts',(85.0555581663265,-1.1510068023798,136.608076143277));
#147055=CARTESIAN_POINT('Ctrl Pts',(85.04814994666,-0.996429800624187,136.638732225527));
#147056=CARTESIAN_POINT('Ctrl Pts',(85.0407417269935,-0.840728374247625,
136.663188463991));
#147057=CARTESIAN_POINT('Ctrl Pts',(85.0333335073271,-0.68443992143418,
136.68138984639));
#147058=CARTESIAN_POINT('Ctrl Pts',(85.025920728025,-0.52805527568584,136.699602431436));
#147059=CARTESIAN_POINT('Ctrl Pts',(85.0185079487229,-0.371083254912988,
136.711552461018));
#147060=CARTESIAN_POINT('Ctrl Pts',(85.0110951694209,-0.214062936311232,
136.717237042945));
#147061=CARTESIAN_POINT('Ctrl Pts',(85.0036717983921,-0.0568182597147348,
136.722929747268));
#147062=CARTESIAN_POINT('Ctrl Pts',(84.9962484273634,0.100474480233154,
136.722339125452));
#147063=CARTESIAN_POINT('Ctrl Pts',(84.9888250563346,0.257278818816543,
136.715514326605));
#147064=CARTESIAN_POINT('Ctrl Pts',(84.9848890068938,0.340420241603923,
136.711895654498));
#147065=CARTESIAN_POINT('Ctrl Pts',(84.9809529574529,0.423424473608377,
136.706525194973));
#147066=CARTESIAN_POINT('Ctrl Pts',(84.977016908012,0.506212649833241,136.699416114815));
#147067=CARTESIAN_POINT('Ctrl Pts',(84.9695936416066,0.662348566459157,
136.686008611506));
#147068=CARTESIAN_POINT('Ctrl Pts',(84.9621703752011,0.818187545774523,
136.666373446931));
#147069=CARTESIAN_POINT('Ctrl Pts',(84.9547471087957,0.97319276767137,136.640526002427));
#147070=CARTESIAN_POINT('Ctrl Pts',(84.9473326160747,1.12801478626865,136.614709107456));
#147071=CARTESIAN_POINT('Ctrl Pts',(84.9399181233537,1.28200464433728,136.582694608442));
#147072=CARTESIAN_POINT('Ctrl Pts',(84.9325036306326,1.43462845843442,136.544549791169));
#147073=CARTESIAN_POINT('Ctrl Pts',(84.9250962842789,1.58710516795292,136.506441739307));
#147074=CARTESIAN_POINT('Ctrl Pts',(84.9176889379251,1.73821809495301,136.462215222015));
#147075=CARTESIAN_POINT('Ctrl Pts',(84.9102815915713,1.88744150569384,136.411988915259));
#147076=CARTESIAN_POINT('Ctrl Pts',(84.9028797698959,2.03655361998528,136.361800069177));
#147077=CARTESIAN_POINT('Ctrl Pts',(84.8954779482205,2.18377867179703,136.30562046227));
#147078=CARTESIAN_POINT('Ctrl Pts',(84.8880761265451,2.32860421059144,136.243619114173));
#147079=CARTESIAN_POINT('Ctrl Pts',(84.8806782122337,2.47335329711207,136.181650496105));
#147080=CARTESIAN_POINT('Ctrl Pts',(84.8732802979223,2.61570505097423,136.113866403918));
#147081=CARTESIAN_POINT('Ctrl Pts',(84.865882383611,2.75516530427255,136.040484633346));
#147082=CARTESIAN_POINT('Ctrl Pts',(84.8584856986987,2.89460238180624,135.967115057494));
#147083=CARTESIAN_POINT('Ctrl Pts',(84.8510890137866,3.03114858242346,135.88814982315));
#147084=CARTESIAN_POINT('Ctrl Pts',(84.8436923288743,3.16433263170998,135.803853547694));
#147085=CARTESIAN_POINT('Ctrl Pts',(84.8362959719389,3.2975107754758,135.719561010023));
#147086=CARTESIAN_POINT('Ctrl Pts',(84.8288996150035,3.42732674890866,135.629938100893));
#147087=CARTESIAN_POINT('Ctrl Pts',(84.821503258068,3.55333690055581,135.535293658061));
#147088=CARTESIAN_POINT('Ctrl Pts',(84.8141057687314,3.67936634467932,135.440634724923));
#147089=CARTESIAN_POINT('Ctrl Pts',(84.8067082793948,3.80158850831983,135.340952951481));
#147090=CARTESIAN_POINT('Ctrl Pts',(84.7993107900582,3.91959168973813,135.236598376107));
#147091=CARTESIAN_POINT('Ctrl Pts',(84.7919107075432,4.03763623698866,135.132207219398));
#147092=CARTESIAN_POINT('Ctrl Pts',(84.7845106250282,4.15145857796007,135.023140246564));
#147093=CARTESIAN_POINT('Ctrl Pts',(84.7771105425132,4.260682949959,134.90978524389));
#147094=CARTESIAN_POINT('Ctrl Pts',(84.7697023228468,4.37002742538333,134.796305595737));
#147095=CARTESIAN_POINT('Ctrl Pts',(84.7622941031803,4.47476357561472,134.6785287703));
#147096=CARTESIAN_POINT('Ctrl Pts',(84.7548858835139,4.57455464042029,134.556877160409));
#147097=CARTESIAN_POINT('Ctrl Pts',(84.7474731042118,4.67440712496108,134.435150675982));
#147098=CARTESIAN_POINT('Ctrl Pts',(84.7400603249097,4.76930823477344,134.309544952112));
#147099=CARTESIAN_POINT('Ctrl Pts',(84.7326475456077,4.85896415218238,134.180511966411));
#147100=CARTESIAN_POINT('Ctrl Pts',(84.7252241745789,4.94874817417062,134.051294612328));
#147101=CARTESIAN_POINT('Ctrl Pts',(84.7178008035501,5.03327183533983,133.91864052993));
#147102=CARTESIAN_POINT('Ctrl Pts',(84.7103774325214,5.11228651394487,133.783027628468));
#147103=CARTESIAN_POINT('Ctrl Pts',(84.7064413830806,5.15418199247268,133.711122414126));
#147104=CARTESIAN_POINT('Ctrl Pts',(84.7025053336398,5.19452948766344,133.638385738386));
#147105=CARTESIAN_POINT('Ctrl Pts',(84.698569284199,5.23329744864993,133.564891069572));
#147106=CARTESIAN_POINT('Ctrl Pts',(84.6911460177936,5.30641261316367,133.42628241788));
#147107=CARTESIAN_POINT('Ctrl Pts',(84.6837227513881,5.37412776800918,133.284557384925));
#147108=CARTESIAN_POINT('Ctrl Pts',(84.6762994849827,5.43616568955871,133.140175926653));
#147109=CARTESIAN_POINT('Ctrl Pts',(84.6688849922617,5.49813028743685,132.995965115275));
#147110=CARTESIAN_POINT('Ctrl Pts',(84.6614704995407,5.55443086241595,132.849104467748));
#147111=CARTESIAN_POINT('Ctrl Pts',(84.6540560068196,5.60483544689032,132.700079524942));
#147112=CARTESIAN_POINT('Ctrl Pts',(84.6466486604658,5.65519144952862,132.551198217986));
#147113=CARTESIAN_POINT('Ctrl Pts',(84.639241314112,5.69966265615239,132.40015711987));
#147114=CARTESIAN_POINT('Ctrl Pts',(84.6318339677582,5.73806474028561,132.247462692539));
#147115=CARTESIAN_POINT('Ctrl Pts',(84.6244321460828,5.77643818269558,132.094882150473));
#147116=CARTESIAN_POINT('Ctrl Pts',(84.6170303244074,5.80875142499177,131.940651094957));
#147117=CARTESIAN_POINT('Ctrl Pts',(84.609628502732,5.83486967614705,131.785292024383));
#147118=CARTESIAN_POINT('Ctrl Pts',(84.6022305884206,5.86097413968081,131.630014966653));
#147119=CARTESIAN_POINT('Ctrl Pts',(84.5948326741093,5.88089006327614,131.473611446973));
#147120=CARTESIAN_POINT('Ctrl Pts',(84.5874347597979,5.89453357482782,131.316614946711));
#147121=CARTESIAN_POINT('Ctrl Pts',(84.5800380748857,5.9081748190754,131.159644536419));
#147122=CARTESIAN_POINT('Ctrl Pts',(84.5726413899735,5.91554568777026,131.002081712654));
#147123=CARTESIAN_POINT('Ctrl Pts',(84.5652447050612,5.91661407567471,130.844466004086));
#147124=CARTESIAN_POINT('Ctrl Pts',(84.5578483481258,5.91768241620572,130.686857284363));
#147125=CARTESIAN_POINT('Ctrl Pts',(84.5504519911903,5.9124488290741,130.529196057789));
#147126=CARTESIAN_POINT('Ctrl Pts',(84.5430556342549,5.90093334378395,130.372022515245));
#147127=CARTESIAN_POINT('Ctrl Pts',(84.5356581449183,5.88941609544361,130.21482490903));
#147128=CARTESIAN_POINT('Ctrl Pts',(84.5282606555817,5.87161506120222,130.05811550784));
#147129=CARTESIAN_POINT('Ctrl Pts',(84.5208631662451,5.84760220340926,129.902429892298));
#147130=CARTESIAN_POINT('Ctrl Pts',(84.5134630837301,5.82358092794618,129.746689701403));
#147131=CARTESIAN_POINT('Ctrl Pts',(84.5060630012151,5.79334355032403,129.591974379402));
#147132=CARTESIAN_POINT('Ctrl Pts',(84.4986629187001,5.75701321721257,129.438809674049));
#147133=CARTESIAN_POINT('Ctrl Pts',(84.4912546990337,5.72064293516506,129.285476548357));
#147134=CARTESIAN_POINT('Ctrl Pts',(84.4838464793672,5.67816640383382,129.133697807877));
#147135=CARTESIAN_POINT('Ctrl Pts',(84.4764382597007,5.62975696713954,128.983985092175));
#147136=CARTESIAN_POINT('Ctrl Pts',(84.4690254803986,5.58131773524458,128.834180230793));
#147137=CARTESIAN_POINT('Ctrl Pts',(84.4616127010965,5.52693845035551,128.686444277526));
#147138=CARTESIAN_POINT('Ctrl Pts',(84.4541999217945,5.46684055840752,128.541268734444));
#147139=CARTESIAN_POINT('Ctrl Pts',(84.4467765507657,5.40665679577329,128.395885757739));
#147140=CARTESIAN_POINT('Ctrl Pts',(84.4393531797369,5.34073826275935,128.25307083597));
#147141=CARTESIAN_POINT('Ctrl Pts',(84.4319298087082,5.26935265182927,128.113291463278));
#147142=CARTESIAN_POINT('Ctrl Pts',(84.4279937592675,5.23150228804109,128.039177085919));
#147143=CARTESIAN_POINT('Ctrl Pts',(84.4240577098268,5.19211566942541,127.965915645588));
#147144=CARTESIAN_POINT('Ctrl Pts',(84.4201216603861,5.15123755295005,127.893573398346));
#147145=CARTESIAN_POINT('Ctrl Pts',(84.4126983939807,5.07414270103757,127.757138177767));
#147146=CARTESIAN_POINT('Ctrl Pts',(84.4052751275753,4.99150711217917,127.623561658064));
#147147=CARTESIAN_POINT('Ctrl Pts',(84.3978518611698,4.90356791419812,127.493325692751));
#147148=CARTESIAN_POINT('Ctrl Pts',(84.3904373684488,4.81573265304605,127.363243655533));
#147149=CARTESIAN_POINT('Ctrl Pts',(84.3830228757278,4.72260646696588,127.236494620028));
#147150=CARTESIAN_POINT('Ctrl Pts',(84.3756083830068,4.62447247108644,127.113536193855));
#147151=CARTESIAN_POINT('Ctrl Pts',(84.368201036653,4.52643306044697,126.990696279642));
#147152=CARTESIAN_POINT('Ctrl Pts',(84.3607936902993,4.423395680346,126.871639991104));
#147153=CARTESIAN_POINT('Ctrl Pts',(84.3533863439455,4.31568679859894,126.756796162378));
#147154=CARTESIAN_POINT('Ctrl Pts',(84.3459845222701,4.20805825019905,126.642037988512));
#147155=CARTESIAN_POINT('Ctrl Pts',(84.3385827005946,4.09576539189862,126.5314862898));
#147156=CARTESIAN_POINT('Ctrl Pts',(84.3311808789192,3.97917495855005,126.425536892894));
#147157=CARTESIAN_POINT('Ctrl Pts',(84.3237829646078,3.86264607238379,126.31964342585));
#147158=CARTESIAN_POINT('Ctrl Pts',(84.3163850502965,3.74182440487551,126.218347672525));
#147159=CARTESIAN_POINT('Ctrl Pts',(84.3089871359851,3.61711345408748,126.122008556608));
#147160=CARTESIAN_POINT('Ctrl Pts',(84.3015904510729,3.49242322799751,126.025685450504));
#147161=CARTESIAN_POINT('Ctrl Pts',(84.2941937661606,3.36384529652664,125.934317574987));
#147162=CARTESIAN_POINT('Ctrl Pts',(84.2867970812484,3.23181622675876,125.848223569526));
#147163=CARTESIAN_POINT('Ctrl Pts',(84.279400724313,3.0997930112981,125.762133381563));
#147164=CARTESIAN_POINT('Ctrl Pts',(84.2720043673776,2.96431927450088,125.681316802586));
#147165=CARTESIAN_POINT('Ctrl Pts',(84.2646080104421,2.82586032069221,125.606048967575));
#147166=CARTESIAN_POINT('Ctrl Pts',(84.2572105211056,2.68738016846453,125.530769608865));
#147167=CARTESIAN_POINT('Ctrl Pts',(84.249813031769,2.54591421718082,125.461040863941));
#147168=CARTESIAN_POINT('Ctrl Pts',(84.2424155424324,2.40195196339562,125.397091683248));
#147169=CARTESIAN_POINT('Ctrl Pts',(84.2350154599174,2.25793924386471,125.333120085269));
#147170=CARTESIAN_POINT('Ctrl Pts',(84.2276153774024,2.11142882050549,125.274932236756));
#147171=CARTESIAN_POINT('Ctrl Pts',(84.2202152948874,1.96292958357739,125.222708710432));
#147172=CARTESIAN_POINT('Ctrl Pts',(84.2128070752209,1.81426705647262,125.170427758972));
#147173=CARTESIAN_POINT('Ctrl Pts',(84.2053988555544,1.66361170077824,125.124124351147));
#147174=CARTESIAN_POINT('Ctrl Pts',(84.197990635888,1.51148766997368,125.083929201491));
#147175=CARTESIAN_POINT('Ctrl Pts',(84.1905778565859,1.35927000936616,125.043709312391));
#147176=CARTESIAN_POINT('Ctrl Pts',(84.1831650772838,1.20558223601278,125.009605253477));
#147177=CARTESIAN_POINT('Ctrl Pts',(84.1757522979817,1.05095756146268,124.981696384888));
#147178=CARTESIAN_POINT('Ctrl Pts',(84.1683289269529,0.896111951926617,
124.953747638799));
#147179=CARTESIAN_POINT('Ctrl Pts',(84.1609055559242,0.740327136270051,
124.932011813869));
#147180=CARTESIAN_POINT('Ctrl Pts',(84.1534821848955,0.584141124868732,
124.916516384849));
#147181=CARTESIAN_POINT('Ctrl Pts',(84.1495461354548,0.501327553993802,
124.908300336575));
#147182=CARTESIAN_POINT('Ctrl Pts',(84.145610086014,0.418401199937062,124.901837816294));
#147183=CARTESIAN_POINT('Ctrl Pts',(84.1416740365733,0.335441998034453,
124.897126981721));
#147184=CARTESIAN_POINT('Ctrl Pts',(84.1342507701679,0.178983532310491,
124.888242494737));
#147185=CARTESIAN_POINT('Ctrl Pts',(84.1268275037625,0.0219352689361514,
124.885564784318));
#147186=CARTESIAN_POINT('Ctrl Pts',(84.119404237357,-0.135169221699544,
124.889154801704));
#147187=CARTESIAN_POINT('Ctrl Pts',(84.111989744636,-0.292088027874135,
124.892740575988));
#147188=CARTESIAN_POINT('Ctrl Pts',(84.104575251915,-0.449062559473018,
124.902579324101));
#147189=CARTESIAN_POINT('Ctrl Pts',(84.097160759194,-0.605554787605303,
124.91868020136));
#147190=CARTESIAN_POINT('Ctrl Pts',(84.0897534128402,-0.761896182635618,
124.934765559988));
#147191=CARTESIAN_POINT('Ctrl Pts',(84.0823460664865,-0.917755830803735,
124.957100993971));
#147192=CARTESIAN_POINT('Ctrl Pts',(84.0749387201327,-1.07259647797631,
124.985643632016));
#147193=CARTESIAN_POINT('Ctrl Pts',(84.0675368984573,-1.22732163915297,
125.014164981884));
#147194=CARTESIAN_POINT('Ctrl Pts',(84.0601350767819,-1.38102894708251,
125.048884250342));
#147195=CARTESIAN_POINT('Ctrl Pts',(84.0527332551065,-1.53318715244639,
125.089706846945));
#147196=CARTESIAN_POINT('Ctrl Pts',(84.0453353407952,-1.68526503467741,
125.130507893617));
#147197=CARTESIAN_POINT('Ctrl Pts',(84.0379374264838,-1.83579508331474,
125.17740575538));
#147198=CARTESIAN_POINT('Ctrl Pts',(84.0305395121725,-1.98425722513587,
125.230254964908));
#147199=CARTESIAN_POINT('Ctrl Pts',(84.0231428272603,-2.13269469524325,
125.283095391856));
#147200=CARTESIAN_POINT('Ctrl Pts',(84.0157461423481,-2.27906458923966,
125.341885078617));
#147201=CARTESIAN_POINT('Ctrl Pts',(84.0083494574359,-2.4228628515422,125.406428961356));
#147202=CARTESIAN_POINT('Ctrl Pts',(84.0009531005004,-2.56665473767931,
125.470969982151));
#147203=CARTESIAN_POINT('Ctrl Pts',(83.9935567435649,-2.70787487828596,
125.541264538743));
#147204=CARTESIAN_POINT('Ctrl Pts',(83.9861603866295,-2.84604028615942,
125.6170698746));
#147205=CARTESIAN_POINT('Ctrl Pts',(83.9787628972929,-2.98422684750905,
125.692886816448));
#147206=CARTESIAN_POINT('Ctrl Pts',(83.9713654079563,-3.11935741760163,
125.774216037936));
#147207=CARTESIAN_POINT('Ctrl Pts',(83.9639679186197,-3.25097478909792,
125.860769465059));
#147208=CARTESIAN_POINT('Ctrl Pts',(83.9565678361047,-3.38263829885985,
125.947353233351));
#147209=CARTESIAN_POINT('Ctrl Pts',(83.9491677535897,-3.51078584632074,
126.039164648475));
#147210=CARTESIAN_POINT('Ctrl Pts',(83.9417676710747,-3.63499044291924,
126.13587317061));
#147211=CARTESIAN_POINT('Ctrl Pts',(83.9343594514083,-3.75933161524051,
126.232688033707));
#147212=CARTESIAN_POINT('Ctrl Pts',(83.9269512317417,-3.87972088333852,
126.334410528282));
#147213=CARTESIAN_POINT('Ctrl Pts',(83.9195430120753,-3.99576495561633,
126.440670323564));
#147214=CARTESIAN_POINT('Ctrl Pts',(83.9121302327732,-4.11188045108458,
126.546995519977));
#147215=CARTESIAN_POINT('Ctrl Pts',(83.9047174534711,-4.22364515725599,
126.657863319483));
#147216=CARTESIAN_POINT('Ctrl Pts',(83.897304674169,-4.33070409233231,126.772868012196));
#147217=CARTESIAN_POINT('Ctrl Pts',(83.8898813031402,-4.43791599823532,
126.888037029007));
#147218=CARTESIAN_POINT('Ctrl Pts',(83.8824579321115,-4.54040846145767,
127.007354462172));
#147219=CARTESIAN_POINT('Ctrl Pts',(83.8750345610827,-4.63786755896348,
127.130382519099));
#147220=CARTESIAN_POINT('Ctrl Pts',(83.8710985116419,-4.68954271095976,
127.195614946899));
#147221=CARTESIAN_POINT('Ctrl Pts',(83.8671624622012,-4.73980353225777,
127.261890087097));
#147222=CARTESIAN_POINT('Ctrl Pts',(83.8632264127604,-4.78860836582211,
127.329139692031));
#147223=CARTESIAN_POINT('Ctrl Pts',(83.8557474286246,-4.88134362778165,
127.456922316716));
#147224=CARTESIAN_POINT('Ctrl Pts',(83.8482684444889,-4.96909931432236,
127.588610453369));
#147225=CARTESIAN_POINT('Ctrl Pts',(83.8407894603531,-5.05153140075413,
127.723782576079));
#147226=CARTESIAN_POINT('Ctrl Pts',(83.833319537821,-5.13386361173786,127.858790923043));
#147227=CARTESIAN_POINT('Ctrl Pts',(83.8258496152888,-5.21088487347303,
127.99727454451));
#147228=CARTESIAN_POINT('Ctrl Pts',(83.8183796927567,-5.2822922066956,128.138780079375));
#147229=CARTESIAN_POINT('Ctrl Pts',(83.8109174203979,-5.35362640951029,
128.280140694145));
#147230=CARTESIAN_POINT('Ctrl Pts',(83.8034551480392,-5.41935796657825,
128.424516736713));
#147231=CARTESIAN_POINT('Ctrl Pts',(83.7959928756804,-5.4792279555501,128.571427216495));
#147232=CARTESIAN_POINT('Ctrl Pts',(83.7885368470923,-5.53904785060169,
128.71821477456));
#147233=CARTESIAN_POINT('Ctrl Pts',(83.7810808185041,-5.59301580618984,
128.867532210053));
#147234=CARTESIAN_POINT('Ctrl Pts',(83.7736247899159,-5.64091952462577,
129.018875395226));
#147235=CARTESIAN_POINT('Ctrl Pts',(83.766173990919,-5.68878964382549,129.170112429653));
#147236=CARTESIAN_POINT('Ctrl Pts',(83.7587231919221,-5.73060389010518,
129.323372035202));
#147237=CARTESIAN_POINT('Ctrl Pts',(83.7512723929252,-5.76619871155417,
129.478131760479));
#147238=CARTESIAN_POINT('Ctrl Pts',(83.7438247346584,-5.80177852874236,
129.632826249994));
#147239=CARTESIAN_POINT('Ctrl Pts',(83.7363770763917,-5.83114406078232,
129.789019243894));
#147240=CARTESIAN_POINT('Ctrl Pts',(83.728929418125,-5.85418205790248,129.946174742925));
#147241=CARTESIAN_POINT('Ctrl Pts',(83.7214825419909,-5.8772176356355,130.103313737918));
#147242=CARTESIAN_POINT('Ctrl Pts',(83.7140356658568,-5.89392694270054,
130.261414675845));
#147243=CARTESIAN_POINT('Ctrl Pts',(83.7065887897227,-5.90424811944369,
130.41993285251));
#147244=CARTESIAN_POINT('Ctrl Pts',(83.7005175905523,-5.9126626436754,130.549167635705));
#147245=CARTESIAN_POINT('Ctrl Pts',(83.6944463913818,-5.91683217465459,
130.67867949077));
#147246=CARTESIAN_POINT('Ctrl Pts',(83.6883751922114,-5.91674877278903,
130.808171417949));
#147247=CARTESIAN_POINT('',(81.9383765539627,-5.9211714837301,130.807349049409));
#147248=CARTESIAN_POINT('Ctrl Pts',(83.6883730537543,-5.90949988628817,
130.808212304205));
#147249=CARTESIAN_POINT('Ctrl Pts',(83.6538416321521,-5.91380919305711,
131.543829778501));
#147250=CARTESIAN_POINT('Ctrl Pts',(83.5264943359454,-5.4448668572003,134.25138132363));
#147251=CARTESIAN_POINT('Ctrl Pts',(83.3063311651348,-1.38425268638609,
137.664492178298));
#147252=CARTESIAN_POINT('Ctrl Pts',(83.0278835413217,5.02340058182423,135.677040283301));
#147253=CARTESIAN_POINT('Ctrl Pts',(82.7494359175088,6.81479412209936,129.211833819126));
#147254=CARTESIAN_POINT('Ctrl Pts',(82.4709882936959,2.34372478536503,124.210081683459));
#147255=CARTESIAN_POINT('Ctrl Pts',(82.2006355289506,-4.08851989451056,
125.237390232203));
#147256=CARTESIAN_POINT('Ctrl Pts',(82.0230986388097,-5.91348347804172,
129.014328708923));
#147257=CARTESIAN_POINT('Ctrl Pts',(81.9383776232731,-5.92464404173536,
130.807328188564));
#147258=CARTESIAN_POINT('',(80.1883744842576,-5.91827765709797,130.799106644454));
#147259=CARTESIAN_POINT('Ctrl Pts',(81.9383751922115,-5.91674923182385,
130.807375615392));
#147260=CARTESIAN_POINT('Ctrl Pts',(81.9302811434977,-5.91666205962317,
130.97844573922));
#147261=CARTESIAN_POINT('Ctrl Pts',(81.9221870947839,-5.90915640203312,
131.149321703326));
#147262=CARTESIAN_POINT('Ctrl Pts',(81.9140930460701,-5.8942783013915,131.319543952162));
#147263=CARTESIAN_POINT('Ctrl Pts',(81.9066697796646,-5.88063320132161,
131.475659284047));
#147264=CARTESIAN_POINT('Ctrl Pts',(81.8992465132592,-5.86076089908632,
131.631468201526));
#147265=CARTESIAN_POINT('Ctrl Pts',(81.8918232468537,-5.83467759295216,
131.786433908518));
#147266=CARTESIAN_POINT('Ctrl Pts',(81.8844087541327,-5.80862511511972,
131.941216458915));
#147267=CARTESIAN_POINT('Ctrl Pts',(81.8769942614116,-5.77637630682767,
132.095157418048));
#147268=CARTESIAN_POINT('Ctrl Pts',(81.8695797686906,-5.73799926626215,
132.24772300549));
#147269=CARTESIAN_POINT('Ctrl Pts',(81.8621724223368,-5.69965921493319,
132.400141544476));
#147270=CARTESIAN_POINT('Ctrl Pts',(81.854765075983,-5.65520278070317,132.551186991259));
#147271=CARTESIAN_POINT('Ctrl Pts',(81.8473577296292,-5.60474943947957,
132.700333793313));
#147272=CARTESIAN_POINT('Ctrl Pts',(81.8399559079538,-5.55433372826142,
132.849369356055));
#147273=CARTESIAN_POINT('Ctrl Pts',(81.8325540862784,-5.49793013494314,
132.996508741584));
#147274=CARTESIAN_POINT('Ctrl Pts',(81.825152264603,-5.43570845882643,133.141239757176));
#147275=CARTESIAN_POINT('Ctrl Pts',(81.8177543502917,-5.37351962904817,
133.285894370391));
#147276=CARTESIAN_POINT('Ctrl Pts',(81.8103564359804,-5.30551898021813,
133.428142803561));
#147277=CARTESIAN_POINT('Ctrl Pts',(81.802958521669,-5.23192505985641,133.567491220803));
#147278=CARTESIAN_POINT('Ctrl Pts',(81.7955618367569,-5.15834336946914,
133.706816480866));
#147279=CARTESIAN_POINT('Ctrl Pts',(81.7881651518447,-5.07917042649308,
133.843242351721));
#147280=CARTESIAN_POINT('Ctrl Pts',(81.7807684669325,-4.99467156519957,
133.9762979622));
#147281=CARTESIAN_POINT('Ctrl Pts',(81.7733721099971,-4.91017645067413,
134.109347672855));
#147282=CARTESIAN_POINT('Ctrl Pts',(81.7659757530617,-4.82035608751353,
134.239027105152));
#147283=CARTESIAN_POINT('Ctrl Pts',(81.7585793961263,-4.72551998827836,
134.364893078151));
#147284=CARTESIAN_POINT('Ctrl Pts',(81.7511819067897,-4.63066936939443,
134.490778321552));
#147285=CARTESIAN_POINT('Ctrl Pts',(81.7437844174532,-4.53080171005563,
134.61284864497));
#147286=CARTESIAN_POINT('Ctrl Pts',(81.7363869281167,-4.42626767476855,
134.730692879843));
#147287=CARTESIAN_POINT('Ctrl Pts',(81.7289868456017,-4.32169699523714,
134.84857842483));
#147288=CARTESIAN_POINT('Ctrl Pts',(81.7215867630867,-4.21245693047433,
134.962234652631));
#147289=CARTESIAN_POINT('Ctrl Pts',(81.7141866805717,-4.09893583816266,
135.071286391132));
#147290=CARTESIAN_POINT('Ctrl Pts',(81.7067784609053,-3.98528991773983,
135.180458043231));
#147291=CARTESIAN_POINT('Ctrl Pts',(81.6993702412389,-3.86735383809443,
135.285014835901));
#147292=CARTESIAN_POINT('Ctrl Pts',(81.6919620215724,-3.74555050406112,
135.384620652109));
#147293=CARTESIAN_POINT('Ctrl Pts',(81.6845492422704,-3.62367220210819,
135.484287774034));
#147294=CARTESIAN_POINT('Ctrl Pts',(81.6771364629684,-3.49792220035367,
135.578997623423));
#147295=CARTESIAN_POINT('Ctrl Pts',(81.6697236836664,-3.36875292302638,
135.668457070773));
#147296=CARTESIAN_POINT('Ctrl Pts',(81.6623003126377,-3.23939908257802,
135.758044341977));
#147297=CARTESIAN_POINT('Ctrl Pts',(81.6548769416089,-3.10661652316693,
135.842366028338));
#147298=CARTESIAN_POINT('Ctrl Pts',(81.6474535705802,-2.97088353185277,
135.921174235695));
#147299=CARTESIAN_POINT('Ctrl Pts',(81.6435175211393,-2.89891464298731,
135.962960238214));
#147300=CARTESIAN_POINT('Ctrl Pts',(81.6395814716984,-2.82611664945376,
136.003196993845));
#147301=CARTESIAN_POINT('Ctrl Pts',(81.6356454222575,-2.75256306750672,
136.041853063565));
#147302=CARTESIAN_POINT('Ctrl Pts',(81.6282221558521,-2.61384330748768,
136.11475720464));
#147303=CARTESIAN_POINT('Ctrl Pts',(81.6207988894467,-2.47201538770909,
136.182256599698));
#147304=CARTESIAN_POINT('Ctrl Pts',(81.6133756230412,-2.32753968547343,
136.244074725407));
#147305=CARTESIAN_POINT('Ctrl Pts',(81.6059611303202,-2.18323474151975,
136.305819787225));
#147306=CARTESIAN_POINT('Ctrl Pts',(81.5985466375992,-2.03628858416384,
136.361896800104));
#147307=CARTESIAN_POINT('Ctrl Pts',(81.5911321448782,-1.88718710672944,
136.412074535616));
#147308=CARTESIAN_POINT('Ctrl Pts',(81.5837247985244,-1.73822933891236,
136.462203907938));
#147309=CARTESIAN_POINT('Ctrl Pts',(81.5763174521706,-1.58712073809383,
136.506445204225));
#147310=CARTESIAN_POINT('Ctrl Pts',(81.5689101058169,-1.43436804614598,
136.544614868964));
#147311=CARTESIAN_POINT('Ctrl Pts',(81.5615082841415,-1.28172928291891,
136.582756065327));
#147312=CARTESIAN_POINT('Ctrl Pts',(81.5541064624661,-1.12744923074613,
136.614834556794));
#147313=CARTESIAN_POINT('Ctrl Pts',(81.5467046407907,-0.972050592543462,
136.640716347646));
#147314=CARTESIAN_POINT('Ctrl Pts',(81.5393067264793,-0.81673398807239,
136.666584475702));
#147315=CARTESIAN_POINT('Ctrl Pts',(81.5319088121679,-0.660300340859842,
136.686262356703));
#147316=CARTESIAN_POINT('Ctrl Pts',(81.5245108978566,-0.503283259295052,
136.699666930508));
#147317=CARTESIAN_POINT('Ctrl Pts',(81.5171142129443,-0.346292271120638,
136.713069276716));
#147318=CARTESIAN_POINT('Ctrl Pts',(81.5097175280321,-0.188718412604161,
136.72020035308));
#147319=CARTESIAN_POINT('Ctrl Pts',(81.5023208431199,-0.031101260648081,
136.72102887547));
#147320=CARTESIAN_POINT('Ctrl Pts',(81.4949244861845,0.12650890239831,136.721857361122));
#147321=CARTESIAN_POINT('Ctrl Pts',(81.487528129249,0.28416198177493,136.716383846503));
#147322=CARTESIAN_POINT('Ctrl Pts',(81.4801317723135,0.441317817705747,
136.704629183172));
#147323=CARTESIAN_POINT('Ctrl Pts',(81.4727342829769,0.598497714596358,
136.692872720172));
#147324=CARTESIAN_POINT('Ctrl Pts',(81.4653367936403,0.755179844175743,
136.674833221512));
#147325=CARTESIAN_POINT('Ctrl Pts',(81.4579393043037,0.91082873595516,136.650583464521));
#147326=CARTESIAN_POINT('Ctrl Pts',(81.4505392217887,1.06653219021208,136.626325206816));
#147327=CARTESIAN_POINT('Ctrl Pts',(81.4431391392738,1.22120131691355,136.595852413825));
#147328=CARTESIAN_POINT('Ctrl Pts',(81.4357390567588,1.37431055632145,136.559289032176));
#147329=CARTESIAN_POINT('Ctrl Pts',(81.4283308370923,1.5275881550782,136.522685445329));
#147330=CARTESIAN_POINT('Ctrl Pts',(81.4209226174258,1.67930207775057,136.47997798178));
#147331=CARTESIAN_POINT('Ctrl Pts',(81.4135143977593,1.82894094916629,136.431340763876));
#147332=CARTESIAN_POINT('Ctrl Pts',(81.4061016184573,1.9786719208105,136.382673610575));
#147333=CARTESIAN_POINT('Ctrl Pts',(81.3986888391551,2.12632494698645,136.328069559685));
#147334=CARTESIAN_POINT('Ctrl Pts',(81.3912760598531,2.2714088631957,136.267750804867));
#147335=CARTESIAN_POINT('Ctrl Pts',(81.3838526888243,2.4167000821083,136.207345863783));
#147336=CARTESIAN_POINT('Ctrl Pts',(81.3764293177956,2.55941452171377,136.141210067103));
#147337=CARTESIAN_POINT('Ctrl Pts',(81.3690059467669,2.69908509579542,136.069611818426));
#147338=CARTESIAN_POINT('Ctrl Pts',(81.365069897326,2.77314178552418,136.031648709));
#147339=CARTESIAN_POINT('Ctrl Pts',(81.3611338478852,2.84634320129484,135.992150644551));
#147340=CARTESIAN_POINT('Ctrl Pts',(81.3571977984443,2.91862315523441,135.951162482825));
#147341=CARTESIAN_POINT('Ctrl Pts',(81.3497745320389,3.05494089258252,135.873860089006));
#147342=CARTESIAN_POINT('Ctrl Pts',(81.3423512656334,3.18839150030732,135.791021315114));
#147343=CARTESIAN_POINT('Ctrl Pts',(81.3349279992279,3.31849348632067,135.702884021996));
#147344=CARTESIAN_POINT('Ctrl Pts',(81.3275135065069,3.44844170259093,135.614850899839));
#147345=CARTESIAN_POINT('Ctrl Pts',(81.3200990137859,3.57504886911983,135.521531931141));
#147346=CARTESIAN_POINT('Ctrl Pts',(81.3126845210649,3.69785780967332,135.423210927106));
#147347=CARTESIAN_POINT('Ctrl Pts',(81.3052771747111,3.82054838234622,135.324984688556));
#147348=CARTESIAN_POINT('Ctrl Pts',(81.2978698283573,3.93944772766662,135.221766244366));
#147349=CARTESIAN_POINT('Ctrl Pts',(81.2904624820035,4.05412750882253,135.113882714587));
#147350=CARTESIAN_POINT('Ctrl Pts',(81.2830606603281,4.16872175747112,135.006079648414));
#147351=CARTESIAN_POINT('Ctrl Pts',(81.2756588386526,4.27910243755128,134.89361867928));
#147352=CARTESIAN_POINT('Ctrl Pts',(81.2682570169772,4.38487428097723,134.776867143995));
#147353=CARTESIAN_POINT('Ctrl Pts',(81.2608591026659,4.49059028827021,134.660177240937));
#147354=CARTESIAN_POINT('Ctrl Pts',(81.2534611883546,4.5917020542855,134.539201558446));
#147355=CARTESIAN_POINT('Ctrl Pts',(81.2460632740432,4.68785126980622,134.414344140337));
#147356=CARTESIAN_POINT('Ctrl Pts',(81.238666589131,4.78398450707171,134.289507471265));
#147357=CARTESIAN_POINT('Ctrl Pts',(81.2312699042187,4.87515660306296,134.160790642332));
#147358=CARTESIAN_POINT('Ctrl Pts',(81.2238732193065,4.96104958305994,134.028630705031));
#147359=CARTESIAN_POINT('Ctrl Pts',(81.2164768623711,5.04693875447212,133.89647662784));
#147360=CARTESIAN_POINT('Ctrl Pts',(81.2090805054357,5.12754907189866,133.760880058843));
#147361=CARTESIAN_POINT('Ctrl Pts',(81.2016841485002,5.20260610879401,133.622306720535));
#147362=CARTESIAN_POINT('Ctrl Pts',(81.1942866591636,5.27767463711337,133.483712166296));
#147363=CARTESIAN_POINT('Ctrl Pts',(81.186889169827,5.34718801419711,133.342140263547));
#147364=CARTESIAN_POINT('Ctrl Pts',(81.1794916804904,5.41091803479427,133.1980808567));
#147365=CARTESIAN_POINT('Ctrl Pts',(81.1720915979754,5.4746703958513,133.053970950051));
#147366=CARTESIAN_POINT('Ctrl Pts',(81.1646915154604,5.53263521305975,132.907372144349));
#147367=CARTESIAN_POINT('Ctrl Pts',(81.1572914329454,5.58463268835026,132.758793604064));
#147368=CARTESIAN_POINT('Ctrl Pts',(81.149883213279,5.63668734021036,132.610051686399));
#147369=CARTESIAN_POINT('Ctrl Pts',(81.1424749936125,5.68276142261082,132.459326039256));
#147370=CARTESIAN_POINT('Ctrl Pts',(81.1350667739461,5.722725018843,132.307141014433));
#147371=CARTESIAN_POINT('Ctrl Pts',(81.127653994644,5.76271321200183,132.154862322267));
#147372=CARTESIAN_POINT('Ctrl Pts',(81.1202412153419,5.79658334479457,132.001122826309));
#147373=CARTESIAN_POINT('Ctrl Pts',(81.1128284360398,5.82425686863249,131.846455858265));
#147374=CARTESIAN_POINT('Ctrl Pts',(81.1054050650111,5.85196993369905,131.691567894803));
#147375=CARTESIAN_POINT('Ctrl Pts',(81.0979816939823,5.87346865548916,131.535750181317));
#147376=CARTESIAN_POINT('Ctrl Pts',(81.0905583229536,5.88872637804382,131.379540769371));
#147377=CARTESIAN_POINT('Ctrl Pts',(81.0866222735129,5.89681638864603,131.296714790967));
#147378=CARTESIAN_POINT('Ctrl Pts',(81.0826862240723,5.90315270164919,131.213778698083));
#147379=CARTESIAN_POINT('Ctrl Pts',(81.0787501746316,5.90773728098375,131.130812423159));
#147380=CARTESIAN_POINT('Ctrl Pts',(81.0713269082262,5.91638365452921,130.974340617934));
#147381=CARTESIAN_POINT('Ctrl Pts',(81.0639036418207,5.91882236112527,130.8172884614));
#147382=CARTESIAN_POINT('Ctrl Pts',(81.0564803754153,5.91499326160493,130.660189616084));
#147383=CARTESIAN_POINT('Ctrl Pts',(81.0490658826943,5.91116868776223,130.503276448557));
#147384=CARTESIAN_POINT('Ctrl Pts',(81.0416513899733,5.90109106252754,130.346317071632));
#147385=CARTESIAN_POINT('Ctrl Pts',(81.0342368972523,5.8847520493813,130.189849527509));
#147386=CARTESIAN_POINT('Ctrl Pts',(81.0268295508985,5.86842878439108,130.033532792697));
#147387=CARTESIAN_POINT('Ctrl Pts',(81.0194222045447,5.84585618441963,129.877707315739));
#147388=CARTESIAN_POINT('Ctrl Pts',(81.0120148581909,5.8170779383199,129.722910284905));
#147389=CARTESIAN_POINT('Ctrl Pts',(81.0046130365155,5.78832115612185,129.568228707537));
#147390=CARTESIAN_POINT('Ctrl Pts',(80.99721121484,5.75336801151136,129.414574414414));
#147391=CARTESIAN_POINT('Ctrl Pts',(80.9898093931646,5.71231390329363,129.26247851029));
#147392=CARTESIAN_POINT('Ctrl Pts',(80.9824114788533,5.67128146722006,129.110462896409));
#147393=CARTESIAN_POINT('Ctrl Pts',(80.9750135645419,5.62415457865414,128.960004392645));
#147394=CARTESIAN_POINT('Ctrl Pts',(80.9676156502305,5.5710794962173,128.81162285024));
#147395=CARTESIAN_POINT('Ctrl Pts',(80.9602189653183,5.51801323389632,128.663265966156));
#147396=CARTESIAN_POINT('Ctrl Pts',(80.9528222804061,5.45900086515061,128.516985709549));
#147397=CARTESIAN_POINT('Ctrl Pts',(80.9454255954939,5.39423822067638,128.373285838565));
#147398=CARTESIAN_POINT('Ctrl Pts',(80.9380292385584,5.32947844784568,128.229592339384));
#147399=CARTESIAN_POINT('Ctrl Pts',(80.930632881623,5.25896905963994,128.088479338657));
#147400=CARTESIAN_POINT('Ctrl Pts',(80.9232365246875,5.18295354733297,127.950429453594));
#147401=CARTESIAN_POINT('Ctrl Pts',(80.9158390353509,5.10692639685695,127.812358432742));
#147402=CARTESIAN_POINT('Ctrl Pts',(80.9084415460144,5.02539162382225,127.677351788358));
#147403=CARTESIAN_POINT('Ctrl Pts',(80.9010440566778,4.93863799769287,127.545866288855));
#147404=CARTESIAN_POINT('Ctrl Pts',(80.8936439741628,4.85185396021446,127.414334697313));
#147405=CARTESIAN_POINT('Ctrl Pts',(80.8862438916478,4.75984763265399,127.28632701959));
#147406=CARTESIAN_POINT('Ctrl Pts',(80.8788438091327,4.66295020425295,127.162269740727));
#147407=CARTESIAN_POINT('Ctrl Pts',(80.8714355894663,4.56594622716795,127.038076048131));
#147408=CARTESIAN_POINT('Ctrl Pts',(80.8640273697998,4.46404063841445,126.917841723763));
#147409=CARTESIAN_POINT('Ctrl Pts',(80.8566191501333,4.35760436685586,126.801959495182));
#147410=CARTESIAN_POINT('Ctrl Pts',(80.8492063708312,4.25110258554804,126.686005943023));
#147411=CARTESIAN_POINT('Ctrl Pts',(80.8417935915291,4.14006482756889,126.574410088192));
#147412=CARTESIAN_POINT('Ctrl Pts',(80.834380812227,4.02489734255513,126.467526294653));
#147413=CARTESIAN_POINT('Ctrl Pts',(80.8269574411983,3.90956530083796,126.360489780538));
#147414=CARTESIAN_POINT('Ctrl Pts',(80.8195340701695,3.79009202975858,126.258179016823));
#147415=CARTESIAN_POINT('Ctrl Pts',(80.8121106991407,3.66691579913976,126.160907259932));
#147416=CARTESIAN_POINT('Ctrl Pts',(80.8081746496999,3.60160480609316,126.109331440426));
#147417=CARTESIAN_POINT('Ctrl Pts',(80.8042386002592,3.53525325422705,126.059171536811));
#147418=CARTESIAN_POINT('Ctrl Pts',(80.8003025508184,3.46792945451917,126.010469102212));
#147419=CARTESIAN_POINT('Ctrl Pts',(80.792879284413,3.34095886937311,125.918617830511));
#147420=CARTESIAN_POINT('Ctrl Pts',(80.7854560180076,3.21014462261667,125.831675550765));
#147421=CARTESIAN_POINT('Ctrl Pts',(80.7780327516022,3.07590319296048,125.749981317391));
#147422=CARTESIAN_POINT('Ctrl Pts',(80.7706182588811,2.94182042552591,125.668383639817));
#147423=CARTESIAN_POINT('Ctrl Pts',(80.7632037661601,2.80431885379939,125.592021854166));
#147424=CARTESIAN_POINT('Ctrl Pts',(80.7557892734391,2.66384664183009,125.521193799141));
#147425=CARTESIAN_POINT('Ctrl Pts',(80.7483819270854,2.52350982226747,125.450434010861));
#147426=CARTESIAN_POINT('Ctrl Pts',(80.7409745807316,2.38020839364564,125.385197501962));
#147427=CARTESIAN_POINT('Ctrl Pts',(80.7335672343779,2.23441792256095,125.325737879155));
#147428=CARTESIAN_POINT('Ctrl Pts',(80.7261654127025,2.08873618750994,125.266322603577));
#147429=CARTESIAN_POINT('Ctrl Pts',(80.7187635910271,1.94056945055037,125.212675775415));
#147430=CARTESIAN_POINT('Ctrl Pts',(80.7113617693517,1.7904161105369,125.165004208043));
#147431=CARTESIAN_POINT('Ctrl Pts',(80.7039638550404,1.64034203530273,125.11735780612));
#147432=CARTESIAN_POINT('Ctrl Pts',(80.696565940729,1.48828380047146,125.075680495735));
#147433=CARTESIAN_POINT('Ctrl Pts',(80.6891680264177,1.33475782797484,125.040130217664));
#147434=CARTESIAN_POINT('Ctrl Pts',(80.6817713415055,1.18125736870972,125.004585847403));
#147435=CARTESIAN_POINT('Ctrl Pts',(80.6743746565933,1.02629001919024,124.975166572756));
#147436=CARTESIAN_POINT('Ctrl Pts',(80.6669779716811,0.870385456685874,
124.951979929394));
#147437=CARTESIAN_POINT('Ctrl Pts',(80.6595816147457,0.714487807153293,
124.928794314152));
#147438=CARTESIAN_POINT('Ctrl Pts',(80.6521852578102,0.557653396501586,
124.91184083561));
#147439=CARTESIAN_POINT('Ctrl Pts',(80.6447889008748,0.4004198772385,124.901175504052));
#147440=CARTESIAN_POINT('Ctrl Pts',(80.6373914115382,0.243162285121993,
124.890508539605));
#147441=CARTESIAN_POINT('Ctrl Pts',(80.6299939222017,0.0855058351928214,
124.886131664334));
#147442=CARTESIAN_POINT('Ctrl Pts',(80.6225964328652,-0.0720090934002857,
124.888048822793));
#147443=CARTESIAN_POINT('Ctrl Pts',(80.6151963503502,-0.229579238607319,
124.889966653309));
#147444=CARTESIAN_POINT('Ctrl Pts',(80.6077962678352,-0.387007390667567,
124.89818290587));
#147445=CARTESIAN_POINT('Ctrl Pts',(80.6003961853202,-0.543755719762117,
124.912649467168));
#147446=CARTESIAN_POINT('Ctrl Pts',(80.5929879656537,-0.700676409758626,
124.927131935937));
#147447=CARTESIAN_POINT('Ctrl Pts',(80.5855797459873,-0.856915411966237,
124.947878404664));
#147448=CARTESIAN_POINT('Ctrl Pts',(80.5781715263208,-1.01194181745404,
124.974789079229));
#147449=CARTESIAN_POINT('Ctrl Pts',(80.5707587470188,-1.1670636391079,125.001716316865));
#147450=CARTESIAN_POINT('Ctrl Pts',(80.5633459677167,-1.32097101277216,
125.034815241989));
#147451=CARTESIAN_POINT('Ctrl Pts',(80.5559331884147,-1.47314621415442,
125.073935607654));
#147452=CARTESIAN_POINT('Ctrl Pts',(80.5485098173859,-1.62553885060062,
125.113111870332));
#147453=CARTESIAN_POINT('Ctrl Pts',(80.5410864463572,-1.77619401502127,
125.158326650082));
#147454=CARTESIAN_POINT('Ctrl Pts',(80.5336630753285,-1.92461126036826,
125.20938054084));
#147455=CARTESIAN_POINT('Ctrl Pts',(80.5297270258876,-2.00330564507659,
125.236450538742));
#147456=CARTESIAN_POINT('Ctrl Pts',(80.5257909764466,-2.08137122710373,
125.265161325373));
#147457=CARTESIAN_POINT('Ctrl Pts',(80.5218549270057,-2.15873612287603,
125.295477889254));
#147458=CARTESIAN_POINT('Ctrl Pts',(80.5144316606003,-2.30464390182277,
125.352653982585));
#147459=CARTESIAN_POINT('Ctrl Pts',(80.5070083941949,-2.44849919979424,
125.415717287347));
#147460=CARTESIAN_POINT('Ctrl Pts',(80.4995851277895,-2.58979164379113,
125.484500675401));
#147461=CARTESIAN_POINT('Ctrl Pts',(80.4921706350684,-2.73091709185292,
125.553202767203));
#147462=CARTESIAN_POINT('Ctrl Pts',(80.4847561423474,-2.86948538298017,
125.627611323359));
#147463=CARTESIAN_POINT('Ctrl Pts',(80.4773416496263,-3.00500369342217,
125.707510279856));
#147464=CARTESIAN_POINT('Ctrl Pts',(80.4699343032726,-3.14039138621438,
125.78733222673));
#147465=CARTESIAN_POINT('Ctrl Pts',(80.4625269569188,-3.27273463124757,
125.872633850587));
#147466=CARTESIAN_POINT('Ctrl Pts',(80.455119610565,-3.40156300665132,125.963152124402));
#147467=CARTESIAN_POINT('Ctrl Pts',(80.4477177888896,-3.53029529699237,
126.053602886274));
#147468=CARTESIAN_POINT('Ctrl Pts',(80.4403159672142,-3.65551763338324,
126.14926233736));
#147469=CARTESIAN_POINT('Ctrl Pts',(80.4329141455387,-3.77678662111905,
126.24982294827));
#147470=CARTESIAN_POINT('Ctrl Pts',(80.4255162312274,-3.89799159190011,
126.350330474016));
#147471=CARTESIAN_POINT('Ctrl Pts',(80.418118316916,-4.01524708364486,126.455733769205));
#147472=CARTESIAN_POINT('Ctrl Pts',(80.4107204026046,-4.12814107763788,
126.565683724287));
#147473=CARTESIAN_POINT('Ctrl Pts',(80.4033237176924,-4.24101631069721,
126.675615407681));
#147474=CARTESIAN_POINT('Ctrl Pts',(80.3959270327802,-4.34953121735832,
126.790091991183));
#147475=CARTESIAN_POINT('Ctrl Pts',(80.388530347868,-4.45330902131296,126.908725967962));
#147476=CARTESIAN_POINT('Ctrl Pts',(80.3811339909325,-4.55708222365094,
127.027354684387));
#147477=CARTESIAN_POINT('Ctrl Pts',(80.3737376339971,-4.65611849514698,
127.150140146586));
#147478=CARTESIAN_POINT('Ctrl Pts',(80.3663412770616,-4.75008009844821,
127.276660287205));
#147479=CARTESIAN_POINT('Ctrl Pts',(80.358943787725,-4.84405608751084,127.403199798381));
#147480=CARTESIAN_POINT('Ctrl Pts',(80.3515462983884,-4.93295563879555,
127.533474826775));
#147481=CARTESIAN_POINT('Ctrl Pts',(80.3441488090518,-5.01648334550757,
127.667032868231));
#147482=CARTESIAN_POINT('Ctrl Pts',(80.3367487265368,-5.10004033272776,
127.800637728253));
#147483=CARTESIAN_POINT('Ctrl Pts',(80.3293486440218,-5.17822152833742,
127.937527576381));
#147484=CARTESIAN_POINT('Ctrl Pts',(80.3219485615068,-5.25077670126935,
128.077223914739));
#147485=CARTESIAN_POINT('Ctrl Pts',(80.3145403418403,-5.32341165607266,
128.217073863582));
#147486=CARTESIAN_POINT('Ctrl Pts',(80.3071321221738,-5.39040806140536,
128.359736134166));
#147487=CARTESIAN_POINT('Ctrl Pts',(80.2997239025073,-5.45156290764021,
128.504710116611));
#147488=CARTESIAN_POINT('Ctrl Pts',(80.2923111232052,-5.51275539366258,
128.649773328124));
#147489=CARTESIAN_POINT('Ctrl Pts',(80.2848983439031,-5.56809902540777,
128.797150737987));
#147490=CARTESIAN_POINT('Ctrl Pts',(80.2774855646011,-5.61744036726017,
128.946325557946));
#147491=CARTESIAN_POINT('Ctrl Pts',(80.2700621935723,-5.66685221033565,
129.095713525884));
#147492=CARTESIAN_POINT('Ctrl Pts',(80.2626388225435,-5.71024453190905,
129.246903675374));
#147493=CARTESIAN_POINT('Ctrl Pts',(80.2552154515147,-5.74751459409594,
129.399367182295));
#147494=CARTESIAN_POINT('Ctrl Pts',(80.251279402074,-5.76727607534973,129.480206991974));
#147495=CARTESIAN_POINT('Ctrl Pts',(80.2473433526334,-5.78531723136706,
129.561404658535));
#147496=CARTESIAN_POINT('Ctrl Pts',(80.2434073031927,-5.80162866347082,
129.642880779733));
#147497=CARTESIAN_POINT('Ctrl Pts',(80.2326855063625,-5.8460609968706,129.864821695657));
#147498=CARTESIAN_POINT('Ctrl Pts',(80.2219637095323,-5.87776907583713,
130.089387932859));
#147499=CARTESIAN_POINT('Ctrl Pts',(80.2112419127021,-5.89651005129167,
130.315382317929));
#147500=CARTESIAN_POINT('Ctrl Pts',(80.2036196725385,-5.90983321139959,
130.476044145968));
#147501=CARTESIAN_POINT('Ctrl Pts',(80.195997432375,-5.9166037256679,130.637427484151));
#147502=CARTESIAN_POINT('Ctrl Pts',(80.1883751922114,-5.9167476551358,130.799092985738));
#147503=CARTESIAN_POINT('',(78.4383751922115,-5.90698454152535,130.803787244568));
#147504=CARTESIAN_POINT('Ctrl Pts',(80.1883742158069,-5.91885782199598,
130.799111823733));
#147505=CARTESIAN_POINT('Ctrl Pts',(80.1139027036646,-5.9042356999513,132.379208715788));
#147506=CARTESIAN_POINT('Ctrl Pts',(79.946615316918,-4.43891693990135,135.952540942315));
#147507=CARTESIAN_POINT('Ctrl Pts',(79.686512055567,1.60289591088837,137.616723293554));
#147508=CARTESIAN_POINT('Ctrl Pts',(79.4080644317542,6.59783804819266,133.138047318943));
#147509=CARTESIAN_POINT('Ctrl Pts',(79.1296168079412,5.52968934151192,126.514827272704));
#147510=CARTESIAN_POINT('Ctrl Pts',(78.8511691841285,-0.619973729671027,
123.833478815034));
#147511=CARTESIAN_POINT('Ctrl Pts',(78.6207553122183,-5.23734121523145,
126.915524519283));
#147512=CARTESIAN_POINT('Ctrl Pts',(78.4831573149128,-5.90780690404512,
129.84878494448));
#147513=CARTESIAN_POINT('Ctrl Pts',(78.4383751922115,-5.90698454152535,
130.803787244568));
#147514=CARTESIAN_POINT('',(76.6883751922115,-5.91674660505805,130.809825728295));
#147515=CARTESIAN_POINT('Ctrl Pts',(78.4383751922115,-5.90698454152535,
130.803787244568));
#147516=CARTESIAN_POINT('Ctrl Pts',(78.3903414403085,-5.90610246727639,
131.828132246147));
#147517=CARTESIAN_POINT('Ctrl Pts',(78.2494918138015,-5.16459899004978,
134.833020418668));
#147518=CARTESIAN_POINT('Ctrl Pts',(78.0158263126896,-0.375496194544659,
137.79267680519));
#147519=CARTESIAN_POINT('Ctrl Pts',(77.7373786888769,5.67650346289202,134.897631799166));
#147520=CARTESIAN_POINT('Ctrl Pts',(77.4589310650639,6.5120737505428,128.241070544663));
#147521=CARTESIAN_POINT('Ctrl Pts',(77.180483441251,1.36336639393345,123.940047643478));
#147522=CARTESIAN_POINT('Ctrl Pts',(76.9236314836335,-4.5417187762996,125.791339613774));
#147523=CARTESIAN_POINT('Ctrl Pts',(76.7595954006204,-5.90275439660642,
129.297330232585));
#147524=CARTESIAN_POINT('Ctrl Pts',(76.6883751922115,-5.91674660505805,
130.809825728295));
#147525=CARTESIAN_POINT('',(74.9383751922115,-5.92581065981966,130.802476432268));
#147526=CARTESIAN_POINT('Ctrl Pts',(76.6883751922115,-5.91674660505805,
130.809825728295));
#147527=CARTESIAN_POINT('Ctrl Pts',(76.6667795260161,-5.92098937645411,
131.268450444188));
#147528=CARTESIAN_POINT('Ctrl Pts',(76.5523679852163,-5.66243486174998,
133.693463258362));
#147529=CARTESIAN_POINT('Ctrl Pts',(76.3451405698123,-2.32364321265071,
137.405742499465));
#147530=CARTESIAN_POINT('Ctrl Pts',(76.0666929459994,4.29794362351234,136.327515616246));
#147531=CARTESIAN_POINT('Ctrl Pts',(75.7882453221866,6.96993023588617,130.173779110365));
#147532=CARTESIAN_POINT('Ctrl Pts',(75.5097976983735,3.23689146150164,124.599516203979));
#147533=CARTESIAN_POINT('Ctrl Pts',(75.2313500745608,-3.47069243506588,
124.72720219018));
#147534=CARTESIAN_POINT('Ctrl Pts',(75.04087590584,-5.87733449716643,128.63474192815));
#147535=CARTESIAN_POINT('Ctrl Pts',(74.9432176117236,-5.9262362747903,130.700047010826));
#147536=CARTESIAN_POINT('Ctrl Pts',(74.9383751922115,-5.92581065981966,
130.802476432268));
#147537=CARTESIAN_POINT('',(73.1883764114855,-5.91339957507466,130.799782862282));
#147538=CARTESIAN_POINT('Ctrl Pts',(74.9383751922115,-5.92581065981966,
130.802476432268));
#147539=CARTESIAN_POINT('Ctrl Pts',(74.8504017371193,-5.91807840543484,
132.663337533789));
#147540=CARTESIAN_POINT('Ctrl Pts',(74.6696124074228,-3.96884304173467,
136.501441794556));
#147541=CARTESIAN_POINT('Ctrl Pts',(74.3960072031221,2.57319737235008,137.312525936093));
#147542=CARTESIAN_POINT('Ctrl Pts',(74.1175595793092,6.86637983689192,132.15727911691));
#147543=CARTESIAN_POINT('Ctrl Pts',(73.8391119554963,4.84969467263334,125.758766290573));
#147544=CARTESIAN_POINT('Ctrl Pts',(73.5606643316834,-1.62362297501932,
123.996908159756));
#147545=CARTESIAN_POINT('Ctrl Pts',(73.3437527748612,-5.50406124702534,
127.497637476799));
#147546=CARTESIAN_POINT('Ctrl Pts',(73.2196570926434,-5.91574354109244,
130.13384201527));
#147547=CARTESIAN_POINT('Ctrl Pts',(73.1883772850298,-5.91100043112035,
130.79976611199));
#147548=CARTESIAN_POINT('',(71.4383739998493,-5.91253438439088,130.808046854168));
#147549=CARTESIAN_POINT('Ctrl Pts',(73.1883751922115,-5.91674824715087,
130.799806241969));
#147550=CARTESIAN_POINT('Ctrl Pts',(73.1806832710384,-5.91687441850351,
130.963719848506));
#147551=CARTESIAN_POINT('Ctrl Pts',(73.1729913498653,-5.91018413384904,
131.127709820108));
#147552=CARTESIAN_POINT('Ctrl Pts',(73.1652994286922,-5.89668968518873,
131.291167888556));
#147553=CARTESIAN_POINT('Ctrl Pts',(73.1579038379578,-5.88371510871657,
131.448328752439));
#147554=CARTESIAN_POINT('Ctrl Pts',(73.1505082472235,-5.86445090490816,
131.604997533534));
#147555=CARTESIAN_POINT('Ctrl Pts',(73.1431126564891,-5.83896106797313,
131.7606368377));
#147556=CARTESIAN_POINT('Ctrl Pts',(73.1357165832859,-5.81346956814847,
131.916286295364));
#147557=CARTESIAN_POINT('Ctrl Pts',(73.1283205100827,-5.78175168615157,
132.070905774352));
#147558=CARTESIAN_POINT('Ctrl Pts',(73.1209244368795,-5.74392283019527,
132.223966578127));
#147559=CARTESIAN_POINT('Ctrl Pts',(73.1135264262367,-5.70608406477466,
132.377067476971));
#147560=CARTESIAN_POINT('Ctrl Pts',(73.1061284155939,-5.66213122723873,
132.528608525751));
#147561=CARTESIAN_POINT('Ctrl Pts',(73.0987304049511,-5.61222999085755,
132.678074867984));
#147562=CARTESIAN_POINT('Ctrl Pts',(73.091329001014,-5.56230586594768,132.827609766928));
#147563=CARTESIAN_POINT('Ctrl Pts',(73.0839275970769,-5.5064280273273,132.975067711307));
#147564=CARTESIAN_POINT('Ctrl Pts',(73.0765261931398,-5.44481073729842,
133.119952679545));
#147565=CARTESIAN_POINT('Ctrl Pts',(73.0691159044766,-5.38311948120155,
133.265011569282));
#147566=CARTESIAN_POINT('Ctrl Pts',(73.0617056158135,-5.31567516287439,
133.407490972847));
#147567=CARTESIAN_POINT('Ctrl Pts',(73.0542953271503,-5.24273888727034,
133.546917731357));
#147568=CARTESIAN_POINT('Ctrl Pts',(73.0468797846426,-5.16975090034057,
133.686443342494));
#147569=CARTESIAN_POINT('Ctrl Pts',(73.0394642421349,-5.09126338328313,
133.822911674498));
#147570=CARTESIAN_POINT('Ctrl Pts',(73.0320486996272,-5.00758113594549,
133.955877986933));
#147571=CARTESIAN_POINT('Ctrl Pts',(73.0246225841321,-4.92377957550955,
134.089033881069));
#147572=CARTESIAN_POINT('Ctrl Pts',(73.0171964686369,-4.83476870784311,
134.218677481322));
#147573=CARTESIAN_POINT('Ctrl Pts',(73.0097703531418,-4.74089440338404,
134.344396043725));
#147574=CARTESIAN_POINT('Ctrl Pts',(73.0077699301137,-4.71560684618082,
134.378261704372));
#147575=CARTESIAN_POINT('Ctrl Pts',(73.0057695070856,-4.68996659012072,
134.41184275205));
#147576=CARTESIAN_POINT('Ctrl Pts',(73.0037690840576,-4.6639808508712,134.445131577844));
#147577=CARTESIAN_POINT('Ctrl Pts',(72.9963458176522,-4.56755171438989,
134.568661360663));
#147578=CARTESIAN_POINT('Ctrl Pts',(72.9889225512467,-4.46606567785079,
134.688544268325));
#147579=CARTESIAN_POINT('Ctrl Pts',(72.9814992848412,-4.35982853943538,
134.80433882616));
#147580=CARTESIAN_POINT('Ctrl Pts',(72.9740847921202,-4.25371696449499,
134.919996524443));
#147581=CARTESIAN_POINT('Ctrl Pts',(72.9666702993992,-4.14286571507969,
135.031575218817));
#147582=CARTESIAN_POINT('Ctrl Pts',(72.9592558066782,-4.02762248411247,
135.138664216528));
#147583=CARTESIAN_POINT('Ctrl Pts',(72.9518484603244,-3.91249032891033,
135.24564999783));
#147584=CARTESIAN_POINT('Ctrl Pts',(72.9444411139707,-3.79297489116168,
135.348154444944));
#147585=CARTESIAN_POINT('Ctrl Pts',(72.9370337676169,-3.6694624831454,135.445801735073));
#147586=CARTESIAN_POINT('Ctrl Pts',(72.9296319459415,-3.54604219534296,
135.54337619617));
#147587=CARTESIAN_POINT('Ctrl Pts',(72.9222301242662,-3.41863116460394,
135.636100482951));
#147588=CARTESIAN_POINT('Ctrl Pts',(72.9148283025908,-3.28765064453706,
135.723637373551));
#147589=CARTESIAN_POINT('Ctrl Pts',(72.9074303882794,-3.15673926806736,
135.811128054108));
#147590=CARTESIAN_POINT('Ctrl Pts',(72.9000324739681,-3.02226246453471,
135.893436585211));
#147591=CARTESIAN_POINT('Ctrl Pts',(72.8926345596568,-2.88467238735192,
135.970267680237));
#147592=CARTESIAN_POINT('Ctrl Pts',(72.8852378747446,-2.74710517514343,
136.047086007328));
#147593=CARTESIAN_POINT('Ctrl Pts',(72.8778411898323,-2.60642604171713,
136.118428523097));
#147594=CARTESIAN_POINT('Ctrl Pts',(72.8704445049201,-2.46311388656519,
136.184044673745));
#147595=CARTESIAN_POINT('Ctrl Pts',(72.8630481479847,-2.31980808602419,
136.249657914904));
#147596=CARTESIAN_POINT('Ctrl Pts',(72.8556517910492,-2.17386983531104,
136.309545140405));
#147597=CARTESIAN_POINT('Ctrl Pts',(72.8482554341138,-2.02580001950833,
136.363503073328));
#147598=CARTESIAN_POINT('Ctrl Pts',(72.8408579447772,-1.87770753383881,
136.417469267349));
#147599=CARTESIAN_POINT('Ctrl Pts',(72.8334604554406,-1.7274831840357,136.465504233444));
#147600=CARTESIAN_POINT('Ctrl Pts',(72.826062966104,-1.57564494931275,136.507453949803));
#147601=CARTESIAN_POINT('Ctrl Pts',(72.8186628835891,-1.42375348793298,
136.549418371569));
#147602=CARTESIAN_POINT('Ctrl Pts',(72.8112628010742,-1.27024737483301,
136.585293197116));
#147603=CARTESIAN_POINT('Ctrl Pts',(72.8038627185592,-1.11565661319277,
136.614975118971));
#147604=CARTESIAN_POINT('Ctrl Pts',(72.7964544988927,-0.960895863117023,
136.644689679151));
#147605=CARTESIAN_POINT('Ctrl Pts',(72.7890462792262,-0.805048449462165,
136.668197665722));
#147606=CARTESIAN_POINT('Ctrl Pts',(72.7816380595598,-0.648652095330869,
136.685447338719));
#147607=CARTESIAN_POINT('Ctrl Pts',(72.7742252802577,-0.492159481853218,
136.702707628602));
#147608=CARTESIAN_POINT('Ctrl Pts',(72.7668125009557,-0.335117626186382,
136.713701903534));
#147609=CARTESIAN_POINT('Ctrl Pts',(72.7593997216537,-0.17806561314373,
136.718430552891));
#147610=CARTESIAN_POINT('Ctrl Pts',(72.7519763506249,-0.0207891968196094,
136.723165958764));
#147611=CARTESIAN_POINT('Ctrl Pts',(72.7445529795961,0.136497033575762,
136.721617862338));
#147612=CARTESIAN_POINT('Ctrl Pts',(72.7371296085674,0.29325692245052,136.713838677423));
#147613=CARTESIAN_POINT('Ctrl Pts',(72.7331935591265,0.376374776934647,
136.709713966923));
#147614=CARTESIAN_POINT('Ctrl Pts',(72.7292575096857,0.459344779550445,
136.70383833658));
#147615=CARTESIAN_POINT('Ctrl Pts',(72.7253214602449,0.542088146912409,
136.696225433011));
#147616=CARTESIAN_POINT('Ctrl Pts',(72.7178981938394,0.698139555423767,
136.68186773447));
#147617=CARTESIAN_POINT('Ctrl Pts',(72.710474927434,0.85385612258439,136.66128429759));
#147618=CARTESIAN_POINT('Ctrl Pts',(72.7030516610285,1.00870113186288,136.634493771198));
#147619=CARTESIAN_POINT('Ctrl Pts',(72.6956371683075,1.16336312719937,136.607734908983));
#147620=CARTESIAN_POINT('Ctrl Pts',(72.6882226755865,1.31715525085031,136.57478362315));
#147621=CARTESIAN_POINT('Ctrl Pts',(72.6808081828655,1.46954403885216,136.535710448136));
#147622=CARTESIAN_POINT('Ctrl Pts',(72.6734008365117,1.62178594880344,136.496674933319));
#147623=CARTESIAN_POINT('Ctrl Pts',(72.6659934901579,1.77262685666831,136.451529368163));
#147624=CARTESIAN_POINT('Ctrl Pts',(72.6585861438041,1.92154176086084,136.400395626728));
#147625=CARTESIAN_POINT('Ctrl Pts',(72.6511843221286,2.07034559869916,136.349300022767));
#147626=CARTESIAN_POINT('Ctrl Pts',(72.6437825004533,2.21722594155913,136.29222525606));
#147627=CARTESIAN_POINT('Ctrl Pts',(72.6363806787778,2.36167137726813,136.229343462543));
#147628=CARTESIAN_POINT('Ctrl Pts',(72.6289827644665,2.50604056135599,136.166494863835));
#147629=CARTESIAN_POINT('Ctrl Pts',(72.6215848501551,2.64797705676082,136.097845492001));
#147630=CARTESIAN_POINT('Ctrl Pts',(72.6141869358437,2.78698803051749,136.023616146878));
#147631=CARTESIAN_POINT('Ctrl Pts',(72.6067902509315,2.92597590317223,135.949399137325));
#147632=CARTESIAN_POINT('Ctrl Pts',(72.5993935660192,3.06203889011029,135.869604170545));
#147633=CARTESIAN_POINT('Ctrl Pts',(72.591996881107,3.1947073364501,135.784498727793));
#147634=CARTESIAN_POINT('Ctrl Pts',(72.5846005241715,3.32736990013198,135.699397058705));
#147635=CARTESIAN_POINT('Ctrl Pts',(72.5772041672361,3.45663790829007,135.608985583404));
#147636=CARTESIAN_POINT('Ctrl Pts',(72.5698078103006,3.58206959767457,135.513575834554));
#147637=CARTESIAN_POINT('Ctrl Pts',(72.562410320964,3.70752049097066,135.418151478229));
#147638=CARTESIAN_POINT('Ctrl Pts',(72.5550128316274,3.82913359886926,135.317727550659));
#147639=CARTESIAN_POINT('Ctrl Pts',(72.5476153422908,3.94649935804197,135.212656589875));
#147640=CARTESIAN_POINT('Ctrl Pts',(72.5402152597758,4.0639062596002,135.107548796628));
#147641=CARTESIAN_POINT('Ctrl Pts',(72.5328151772608,4.17706257008706,134.997790975656));
#147642=CARTESIAN_POINT('Ctrl Pts',(72.5254150947457,4.2855948943364,134.883773193433));
#147643=CARTESIAN_POINT('Ctrl Pts',(72.5180068750793,4.39424656103326,134.769630036937));
#147644=CARTESIAN_POINT('Ctrl Pts',(72.5105986554128,4.49826382978093,134.651217834956));
#147645=CARTESIAN_POINT('Ctrl Pts',(72.5031904357463,4.59731251781099,134.528961022452));
#147646=CARTESIAN_POINT('Ctrl Pts',(72.4957776564442,4.69642216865595,134.40662896292));
#147647=CARTESIAN_POINT('Ctrl Pts',(72.4883648771421,4.79055692247838,134.280447876241));
#147648=CARTESIAN_POINT('Ctrl Pts',(72.48095209784,4.87942571836309,134.150871520204));
#147649=CARTESIAN_POINT('Ctrl Pts',(72.4735287268113,4.96842149415095,134.021110019394));
#147650=CARTESIAN_POINT('Ctrl Pts',(72.4661053557825,5.05213608624131,133.887943875251));
#147651=CARTESIAN_POINT('Ctrl Pts',(72.4586819847537,5.13032378666469,133.751852501606));
#147652=CARTESIAN_POINT('Ctrl Pts',(72.4547459353131,5.17178078151535,133.679693589835));
#147653=CARTESIAN_POINT('Ctrl Pts',(72.4508098858724,5.21168476036814,133.606712655085));
#147654=CARTESIAN_POINT('Ctrl Pts',(72.4468738364318,5.25000462016293,133.532983356379));
#147655=CARTESIAN_POINT('Ctrl Pts',(72.4394505700264,5.32227467981709,133.393932200026));
#147656=CARTESIAN_POINT('Ctrl Pts',(72.432027303621,5.38912585955543,133.25179759154));
#147657=CARTESIAN_POINT('Ctrl Pts',(72.4246040372155,5.45028374076894,133.107041165886));
#147658=CARTESIAN_POINT('Ctrl Pts',(72.4171895444945,5.51136933844579,132.962455830305));
#147659=CARTESIAN_POINT('Ctrl Pts',(72.4097750517735,5.56677488786008,132.815255186186));
#147660=CARTESIAN_POINT('Ctrl Pts',(72.4023605590525,5.61627138132904,132.665926177455));
#147661=CARTESIAN_POINT('Ctrl Pts',(72.3949532126988,5.66572016821398,132.516741097645));
#147662=CARTESIAN_POINT('Ctrl Pts',(72.387545866345,5.70927112085429,132.365432089115));
#147663=CARTESIAN_POINT('Ctrl Pts',(72.3801385199912,5.7467429991667,132.212506726472));
#147664=CARTESIAN_POINT('Ctrl Pts',(72.3727366983158,5.78418692953865,132.059695421335));
#147665=CARTESIAN_POINT('Ctrl Pts',(72.3653348766404,5.81556072493446,131.905270523486));
#147666=CARTESIAN_POINT('Ctrl Pts',(72.357933054965,5.84073277742038,131.749755342148));
#147667=CARTESIAN_POINT('Ctrl Pts',(72.3505351406537,5.8658915417755,131.594322256065));
#147668=CARTESIAN_POINT('Ctrl Pts',(72.3431372263424,5.88485502375799,131.437800400301));
#147669=CARTESIAN_POINT('Ctrl Pts',(72.3357393120311,5.8975426002691,131.280723756895));
#147670=CARTESIAN_POINT('Ctrl Pts',(72.3283426271189,5.91022806833525,131.123673216776));
#147671=CARTESIAN_POINT('Ctrl Pts',(72.3209459422067,5.91663967083529,130.966068443716));
#147672=CARTESIAN_POINT('Ctrl Pts',(72.3135492572945,5.91674858739051,130.808449151822));
#147673=CARTESIAN_POINT('Ctrl Pts',(72.3061529003591,5.91685749911626,130.650836848932));
#147674=CARTESIAN_POINT('Ctrl Pts',(72.2987565434237,5.91066428031545,130.493210401786));
#147675=CARTESIAN_POINT('Ctrl Pts',(72.2913601864883,5.89819224841629,130.336109869332));
#147676=CARTESIAN_POINT('Ctrl Pts',(72.2839626971517,5.88571830701719,130.178985284385));
#147677=CARTESIAN_POINT('Ctrl Pts',(72.2765652078152,5.86696366798362,130.022387146605));
#147678=CARTESIAN_POINT('Ctrl Pts',(72.2691677184786,5.84200355256304,129.866850588638));
#147679=CARTESIAN_POINT('Ctrl Pts',(72.2617676359636,5.8170346874127,129.711259507571));
#147680=CARTESIAN_POINT('Ctrl Pts',(72.2543675534486,5.78585607394117,129.556731115587));
#147681=CARTESIAN_POINT('Ctrl Pts',(72.2469674709336,5.7485940569124,129.403790401072));
#147682=CARTESIAN_POINT('Ctrl Pts',(72.2395592512672,5.7112910664652,129.250681512517));
#147683=CARTESIAN_POINT('Ctrl Pts',(72.2321510316007,5.66789140185292,129.099164150849));
#147684=CARTESIAN_POINT('Ctrl Pts',(72.2247428119342,5.61857151827982,128.949748890957));
#147685=CARTESIAN_POINT('Ctrl Pts',(72.2173300326322,5.56922127914133,128.800241668467));
#147686=CARTESIAN_POINT('Ctrl Pts',(72.2099172533302,5.51394369109511,128.652839474547));
#147687=CARTESIAN_POINT('Ctrl Pts',(72.2025044740281,5.45296318788609,128.508032454158));
#147688=CARTESIAN_POINT('Ctrl Pts',(72.1950811029994,5.39189555287429,128.363018526708));
#147689=CARTESIAN_POINT('Ctrl Pts',(72.1876577319706,5.32510888621411,128.220607515789));
#147690=CARTESIAN_POINT('Ctrl Pts',(72.1802343609418,5.25287372117891,128.081265277361));
#147691=CARTESIAN_POINT('Ctrl Pts',(72.1762983115009,5.21457290341656,128.007382679071));
#147692=CARTESIAN_POINT('Ctrl Pts',(72.1723622620599,5.1747410513595,127.934362353626));
#147693=CARTESIAN_POINT('Ctrl Pts',(72.168426212619,5.13342332446577,127.862270283411));
#147694=CARTESIAN_POINT('Ctrl Pts',(72.1610029462135,5.05549938102976,127.726306888907));
#147695=CARTESIAN_POINT('Ctrl Pts',(72.1535796798081,4.97205220502848,127.593235870351));
#147696=CARTESIAN_POINT('Ctrl Pts',(72.1461564134027,4.88332185307086,127.463537628867));
#147697=CARTESIAN_POINT('Ctrl Pts',(72.1387419206817,4.79469637302071,127.333992679933));
#147698=CARTESIAN_POINT('Ctrl Pts',(72.1313274279606,4.70080035499852,127.207812878322));
#147699=CARTESIAN_POINT('Ctrl Pts',(72.1239129352396,4.60191969447509,127.08545409977));
#147700=CARTESIAN_POINT('Ctrl Pts',(72.1165055888859,4.50313433885499,126.963213255216));
#147701=CARTESIAN_POINT('Ctrl Pts',(72.1090982425321,4.3993741383776,126.844786390294));
#147702=CARTESIAN_POINT('Ctrl Pts',(72.1016908961784,4.29096816524474,126.730600343893));
#147703=CARTESIAN_POINT('Ctrl Pts',(72.0942890745029,4.18264304537642,126.616499461753));
#147704=CARTESIAN_POINT('Ctrl Pts',(72.0868872528275,4.06967930803466,126.50663336981));
#147705=CARTESIAN_POINT('Ctrl Pts',(72.0794854311521,3.95244609078626,126.401395654961));
#147706=CARTESIAN_POINT('Ctrl Pts',(72.0720875168408,3.83527476004097,126.296213494283));
#147707=CARTESIAN_POINT('Ctrl Pts',(72.0646896025295,3.71383871507738,126.195655093518));
#147708=CARTESIAN_POINT('Ctrl Pts',(72.0572916882181,3.58854363135225,126.100076913496));
#147709=CARTESIAN_POINT('Ctrl Pts',(72.0498950033059,3.46326936939703,126.004514616833));
#147710=CARTESIAN_POINT('Ctrl Pts',(72.0424983183937,3.33413763798613,125.913931124515));
#147711=CARTESIAN_POINT('Ctrl Pts',(72.0351016334815,3.20158693576376,125.828642412598));
#147712=CARTESIAN_POINT('Ctrl Pts',(72.0277052765461,3.06904211097796,125.743357482472));
#147713=CARTESIAN_POINT('Ctrl Pts',(72.0203089196106,2.93307893074048,125.663367067928));
#147714=CARTESIAN_POINT('Ctrl Pts',(72.0129125626752,2.79416436558012,125.588943466405));
#147715=CARTESIAN_POINT('Ctrl Pts',(72.0055150733386,2.655228532246,125.51450847044));
#147716=CARTESIAN_POINT('Ctrl Pts',(71.9981175840021,2.51334074333734,125.445642160826));
#147717=CARTESIAN_POINT('Ctrl Pts',(71.9907200946655,2.36899188002583,125.382570504064));
#147718=CARTESIAN_POINT('Ctrl Pts',(71.9833200121505,2.22459241544302,125.319476737629));
#147719=CARTESIAN_POINT('Ctrl Pts',(71.9759199296355,2.07773050063319,125.262181817734));
#147720=CARTESIAN_POINT('Ctrl Pts',(71.9685198471205,1.92891611562463,125.210863215995));
#147721=CARTESIAN_POINT('Ctrl Pts',(71.961111627454,1.77993809390178,125.159488184178));
#147722=CARTESIAN_POINT('Ctrl Pts',(71.9537034077875,1.62900366751656,125.114102716159));
#147723=CARTESIAN_POINT('Ctrl Pts',(71.9462951881211,1.47663777593351,125.074834333379));
#147724=CARTESIAN_POINT('Ctrl Pts',(71.938882408819,1.32417810568568,125.035541781565));
#147725=CARTESIAN_POINT('Ctrl Pts',(71.9314696295169,1.17028557872398,125.002373895618));
#147726=CARTESIAN_POINT('Ctrl Pts',(71.9240568502148,1.01549387980607,124.975406788398));
#147727=CARTESIAN_POINT('Ctrl Pts',(71.916633479186,0.860481007250513,124.94840114931));
#147728=CARTESIAN_POINT('Ctrl Pts',(71.9092101081573,0.704566765790298,
124.927614033484));
#147729=CARTESIAN_POINT('Ctrl Pts',(71.9017867371286,0.548289323079683,
124.91306964014));
#147730=CARTESIAN_POINT('Ctrl Pts',(71.8978506876878,0.465427273128251,
124.905357853802));
#147731=CARTESIAN_POINT('Ctrl Pts',(71.8939146382469,0.382463116307205,
124.89940024951));
#147732=CARTESIAN_POINT('Ctrl Pts',(71.8899785888061,0.299476775256987,
124.895194498427));
#147733=CARTESIAN_POINT('Ctrl Pts',(71.8825553224006,0.142967125951911,
124.88726258314));
#147734=CARTESIAN_POINT('Ctrl Pts',(71.8751320559953,-0.0140945276653115,
124.885540919688));
#147735=CARTESIAN_POINT('Ctrl Pts',(71.8677087895898,-0.171174254063978,
124.890087210186));
#147736=CARTESIAN_POINT('Ctrl Pts',(71.8602942968688,-0.328068325271036,
124.894628127346));
#147737=CARTESIAN_POINT('Ctrl Pts',(71.8528798041477,-0.484980057243426,
124.905422241698));
#147738=CARTESIAN_POINT('Ctrl Pts',(71.8454653114267,-0.641371375327656,
124.922475433256));
#147739=CARTESIAN_POINT('Ctrl Pts',(71.8380579650729,-0.797611957571487,
124.939512188305));
#147740=CARTESIAN_POINT('Ctrl Pts',(71.8306506187191,-0.953332755896087,
124.962795970381));
#147741=CARTESIAN_POINT('Ctrl Pts',(71.8232432723653,-1.10799678709192,
124.992280638566));
#147742=CARTESIAN_POINT('Ctrl Pts',(71.8158414506899,-1.26254546401804,
125.021743315973));
#147743=CARTESIAN_POINT('Ctrl Pts',(71.8084396290145,-1.41603857806588,
125.057397601174));
#147744=CARTESIAN_POINT('Ctrl Pts',(71.8010378073391,-1.56794546555856,
125.099145671612));
#147745=CARTESIAN_POINT('Ctrl Pts',(71.7936398930277,-1.71977216258702,
125.140871703569));
#147746=CARTESIAN_POINT('Ctrl Pts',(71.7862419787163,-1.8700139416556,125.188685015556));
#147747=CARTESIAN_POINT('Ctrl Pts',(71.778844064405,-2.01815162467847,125.242436977106));
#147748=CARTESIAN_POINT('Ctrl Pts',(71.7714473794928,-2.16626468990654,
125.296180006056));
#147749=CARTESIAN_POINT('Ctrl Pts',(71.7640506945806,-2.31227400249792,
125.35585959867));
#147750=CARTESIAN_POINT('Ctrl Pts',(71.7566540096684,-2.45567670361769,
125.421277626397));
#147751=CARTESIAN_POINT('Ctrl Pts',(71.7492576527329,-2.59907304611172,
125.486692753421));
#147752=CARTESIAN_POINT('Ctrl Pts',(71.7418612957974,-2.73986266731835,
125.557845654697));
#147753=CARTESIAN_POINT('Ctrl Pts',(71.7344649388619,-2.87756406671134,
125.634490638111));
#147754=CARTESIAN_POINT('Ctrl Pts',(71.7270674495253,-3.01528654854002,
125.711147356068));
#147755=CARTESIAN_POINT('Ctrl Pts',(71.7196699601888,-3.1499195409213,125.793297648849));
#147756=CARTESIAN_POINT('Ctrl Pts',(71.7122724708522,-3.28100759857521,
125.880650664635));
#147757=CARTESIAN_POINT('Ctrl Pts',(71.7048723883372,-3.41214160894424,
125.968034301885));
#147758=CARTESIAN_POINT('Ctrl Pts',(71.6974723058222,-3.5397278999848,126.060624086451));
#147759=CARTESIAN_POINT('Ctrl Pts',(71.6900722233072,-3.66334150313637,
126.158086885434));
#147760=CARTESIAN_POINT('Ctrl Pts',(71.6826640036407,-3.78709103215239,
126.255656854785));
#147761=CARTESIAN_POINT('Ctrl Pts',(71.6752557839742,-3.90685885601902,
126.358110308322));
#147762=CARTESIAN_POINT('Ctrl Pts',(71.6678475643077,-4.02225394473465,
126.465074528062));
#147763=CARTESIAN_POINT('Ctrl Pts',(71.6604347850057,-4.13772005720158,
126.572104582493));
#147764=CARTESIAN_POINT('Ctrl Pts',(71.6530220057036,-4.24880780886742,
126.683650671363));
#147765=CARTESIAN_POINT('Ctrl Pts',(71.6456092264016,-4.3551646941821,126.79930493143));
#147766=CARTESIAN_POINT('Ctrl Pts',(71.6381858553728,-4.46167354720263,
126.915124443728));
#147767=CARTESIAN_POINT('Ctrl Pts',(71.6307624843441,-4.56343779239502,
127.035063566932));
#147768=CARTESIAN_POINT('Ctrl Pts',(71.6233391133153,-4.66014617750741,
127.158682605623));
#147769=CARTESIAN_POINT('Ctrl Pts',(71.6194030638746,-4.71142328377854,
127.224228386134));
#147770=CARTESIAN_POINT('Ctrl Pts',(71.6154670144339,-4.7612797382694,127.29080825029));
#147771=CARTESIAN_POINT('Ctrl Pts',(71.6115309649932,-4.80967430015931,
127.358353698117));
#147772=CARTESIAN_POINT('Ctrl Pts',(71.6040410472673,-4.90176442565088,
127.486886089441));
#147773=CARTESIAN_POINT('Ctrl Pts',(71.5965511295414,-4.98883527277445,
127.619302996982));
#147774=CARTESIAN_POINT('Ctrl Pts',(71.5890612118156,-5.07054482348986,
127.755179456093));
#147775=CARTESIAN_POINT('Ctrl Pts',(71.5815804528749,-5.15215445852537,
127.890889763406));
#147776=CARTESIAN_POINT('Ctrl Pts',(71.5740996939342,-5.22841566190887,
128.030050891975));
#147777=CARTESIAN_POINT('Ctrl Pts',(71.5666189349935,-5.29902767983761,
128.172206326721));
#147778=CARTESIAN_POINT('Ctrl Pts',(71.5591459364582,-5.36956644612311,
128.314214291964));
#147779=CARTESIAN_POINT('Ctrl Pts',(71.5516729379229,-5.43446753397698,
128.459210054913));
#147780=CARTESIAN_POINT('Ctrl Pts',(71.5441999393877,-5.49347442677738,
128.606709761574));
#147781=CARTESIAN_POINT('Ctrl Pts',(71.5367333079833,-5.55243104462984,
128.754083795797));
#147782=CARTESIAN_POINT('Ctrl Pts',(71.5292666765789,-5.60550333329829,
128.903957188612));
#147783=CARTESIAN_POINT('Ctrl Pts',(71.5218000451745,-5.65248154376742,
129.055823240251));
#147784=CARTESIAN_POINT('Ctrl Pts',(71.5143389009662,-5.69942523014719,
129.207577686167));
#147785=CARTESIAN_POINT('Ctrl Pts',(71.5068777567579,-5.74028365480453,
129.361321525862));
#147786=CARTESIAN_POINT('Ctrl Pts',(71.4994166125495,-5.77489592895132,
129.516530049408));
#147787=CARTESIAN_POINT('Ctrl Pts',(71.4919587331199,-5.80949305777818,
129.67167065824));
#147788=CARTESIAN_POINT('Ctrl Pts',(71.4845008536903,-5.8378494005576,129.828274319361));
#147789=CARTESIAN_POINT('Ctrl Pts',(71.4770429742607,-5.85985444105077,
129.985803049525));
#147790=CARTESIAN_POINT('Ctrl Pts',(71.4695862429928,-5.88185609380548,
130.143307527693));
#147791=CARTESIAN_POINT('Ctrl Pts',(71.4621295117249,-5.89750833699887,
130.301736431149));
#147792=CARTESIAN_POINT('Ctrl Pts',(71.454672780457,-5.90675209166039,130.4605433839));
#147793=CARTESIAN_POINT('Ctrl Pts',(71.4492402510418,-5.91348653967805,
130.576240652738));
#147794=CARTESIAN_POINT('Ctrl Pts',(71.4438077216267,-5.91682061820416,
130.692138378587));
#147795=CARTESIAN_POINT('Ctrl Pts',(71.4383751922115,-5.91674886586254,
130.808024060528));
#147796=CARTESIAN_POINT('',(69.688376602423,-5.92104773189643,130.807528757205));
#147797=CARTESIAN_POINT('Ctrl Pts',(71.4383730761828,-5.90926962530269,
130.80806451132));
#147798=CARTESIAN_POINT('Ctrl Pts',(71.4032764978486,-5.91346979626751,
131.55579444876));
#147799=CARTESIAN_POINT('Ctrl Pts',(71.27536404491,-5.43425968048745,134.275764099217));
#147800=CARTESIAN_POINT('Ctrl Pts',(71.0546357173675,-1.34246747144102,
137.67279141495));
#147801=CARTESIAN_POINT('Ctrl Pts',(70.7761880935544,5.05296889400591,135.646371138679));
#147802=CARTESIAN_POINT('Ctrl Pts',(70.4977404697419,6.8049736971114,129.170379738871));
#147803=CARTESIAN_POINT('Ctrl Pts',(70.2192928459285,2.30354011402361,124.195936942177));
#147804=CARTESIAN_POINT('Ctrl Pts',(69.9495052563708,-4.10889852220346,
125.260151943503));
#147805=CARTESIAN_POINT('Ctrl Pts',(69.7725335414168,-5.91277317614864,
129.026272740359));
#147806=CARTESIAN_POINT('Ctrl Pts',(69.6883777010673,-5.92439661000214,
130.807507312234));
#147807=CARTESIAN_POINT('',(67.9383744040955,-5.9184596220467,130.79916933959));
#147808=CARTESIAN_POINT('Ctrl Pts',(69.6883751922115,-5.91674913700228,
130.807556283809));
#147809=CARTESIAN_POINT('Ctrl Pts',(69.679715994242,-5.91665027484425,130.99059873685));
#147810=CARTESIAN_POINT('Ctrl Pts',(69.6710567962725,-5.90805820439472,
131.173407171725));
#147811=CARTESIAN_POINT('Ctrl Pts',(69.662397598303,-5.89103302688227,131.355414552025));
#147812=CARTESIAN_POINT('Ctrl Pts',(69.6549743318976,-5.87643786128845,
131.511443929858));
#147813=CARTESIAN_POINT('Ctrl Pts',(69.6475510654921,-5.85561747413632,
131.667128992214));
#147814=CARTESIAN_POINT('Ctrl Pts',(69.6401277990867,-5.82859133102236,
131.821933051563));
#147815=CARTESIAN_POINT('Ctrl Pts',(69.6327133063656,-5.80159713056516,
131.97655414537));
#147816=CARTESIAN_POINT('Ctrl Pts',(69.6252988136446,-5.7684118374569,132.130295944685));
#147817=CARTESIAN_POINT('Ctrl Pts',(69.6178843209236,-5.72910679789495,
132.282625093502));
#147818=CARTESIAN_POINT('Ctrl Pts',(69.6104769745698,-5.68983964200995,
132.43480742175));
#147819=CARTESIAN_POINT('Ctrl Pts',(69.6030696282161,-5.64446457494824,
132.585579451078));
#147820=CARTESIAN_POINT('Ctrl Pts',(69.5956622818623,-5.59310426959112,
132.734416365979));
#147821=CARTESIAN_POINT('Ctrl Pts',(69.5882604601869,-5.5417822706874,132.883142272693));
#147822=CARTESIAN_POINT('Ctrl Pts',(69.5808586385115,-5.48448404319401,
133.029935587389));
#147823=CARTESIAN_POINT('Ctrl Pts',(69.5734568168361,-5.42138250112914,
133.174285160447));
#147824=CARTESIAN_POINT('Ctrl Pts',(69.5660589025248,-5.35831426987715,
133.318558532489));
#147825=CARTESIAN_POINT('Ctrl Pts',(69.5586609882133,-5.28944897435379,
133.460390390876));
#147826=CARTESIAN_POINT('Ctrl Pts',(69.551263073902,-5.21500816414918,133.599288239233));
#147827=CARTESIAN_POINT('Ctrl Pts',(69.5438663889898,-5.14057972465685,
133.738163005287));
#147828=CARTESIAN_POINT('Ctrl Pts',(69.5364697040776,-5.06057778557375,
133.87410440031));
#147829=CARTESIAN_POINT('Ctrl Pts',(69.5290730191654,-4.97527054258163,
134.006643177026));
#147830=CARTESIAN_POINT('Ctrl Pts',(69.52167666223,-4.88996708220199,134.139176076833));
#147831=CARTESIAN_POINT('Ctrl Pts',(69.5142803052945,-4.79935898769267,
134.268306344426));
#147832=CARTESIAN_POINT('Ctrl Pts',(69.506883948359,-4.70375846364788,134.393592691166));
#147833=CARTESIAN_POINT('Ctrl Pts',(69.4994864590224,-4.60814330291887,
134.518898219566));
#147834=CARTESIAN_POINT('Ctrl Pts',(69.492088969686,-4.50753441718986,134.640358358516));
#147835=CARTESIAN_POINT('Ctrl Pts',(69.4846914803494,-4.40228496737017,
134.757564081665));
#147836=CARTESIAN_POINT('Ctrl Pts',(69.4772913978344,-4.29699862251869,
134.874810891099));
#147837=CARTESIAN_POINT('Ctrl Pts',(69.4698913153193,-4.18706872400283,
134.987800037833));
#147838=CARTESIAN_POINT('Ctrl Pts',(69.4624912328043,-4.07288590608889,
135.096158720749));
#147839=CARTESIAN_POINT('Ctrl Pts',(69.4550830131379,-3.95857753242862,
135.204636555175));
#147840=CARTESIAN_POINT('Ctrl Pts',(69.4476747934714,-3.8400071709917,135.308473500258));
#147841=CARTESIAN_POINT('Ctrl Pts',(69.4402665738049,-3.71759976481711,
135.407336019535));
#147842=CARTESIAN_POINT('Ctrl Pts',(69.4328537945029,-3.59511701892641,
135.506259387043));
#147843=CARTESIAN_POINT('Ctrl Pts',(69.4254410152008,-3.46879282129271,
135.600202005724));
#147844=CARTESIAN_POINT('Ctrl Pts',(69.4180282358987,-3.33908137212494,
135.688873505545));
#147845=CARTESIAN_POINT('Ctrl Pts',(69.41060486487,-3.20918458515573,135.777671703362));
#147846=CARTESIAN_POINT('Ctrl Pts',(69.4031814938412,-3.0758911958595,135.86118354231));
#147847=CARTESIAN_POINT('Ctrl Pts',(69.3957581228125,-2.93968099143647,
135.939164044289));
#147848=CARTESIAN_POINT('Ctrl Pts',(69.3918220733717,-2.86745907273259,
135.980511177555));
#147849=CARTESIAN_POINT('Ctrl Pts',(69.3878860239309,-2.79441749542759,
136.020304045642));
#147850=CARTESIAN_POINT('Ctrl Pts',(69.3839499744901,-2.72062996579226,
136.058511657623));
#147851=CARTESIAN_POINT('Ctrl Pts',(69.3765267080847,-2.58146898772969,
136.130570021401));
#147852=CARTESIAN_POINT('Ctrl Pts',(69.3691034416792,-2.43923280771762,
136.197204819048));
#147853=CARTESIAN_POINT('Ctrl Pts',(69.3616801752738,-2.29438347780483,
136.258142334804));
#147854=CARTESIAN_POINT('Ctrl Pts',(69.3542656825528,-2.1497053477709,136.319007827476));
#147855=CARTESIAN_POINT('Ctrl Pts',(69.3468511898318,-2.00242055629298,
136.37418929841));
#147856=CARTESIAN_POINT('Ctrl Pts',(69.3394366971108,-1.85301639524541,
136.423458481232));
#147857=CARTESIAN_POINT('Ctrl Pts',(69.332029350757,-1.70375623555302,136.47268017656));
#147858=CARTESIAN_POINT('Ctrl Pts',(69.3246220044032,-1.55238112509918,
136.516000812216));
#147859=CARTESIAN_POINT('Ctrl Pts',(69.3172146580494,-1.39939891372179,
136.553239920767));
#147860=CARTESIAN_POINT('Ctrl Pts',(69.309812836374,-1.24653080224944,136.590451254986));
#147861=CARTESIAN_POINT('Ctrl Pts',(69.3024110146986,-1.09205833764615,
136.621590005645));
#147862=CARTESIAN_POINT('Ctrl Pts',(69.2950091930232,-0.936505028813258,
136.64652536135));
#147863=CARTESIAN_POINT('Ctrl Pts',(69.2876112787119,-0.781033835361272,
136.671447553874));
#147864=CARTESIAN_POINT('Ctrl Pts',(69.2802133644006,-0.624483301654845,
136.690172814277));
#147865=CARTESIAN_POINT('Ctrl Pts',(69.2728154500892,-0.46738753180734,
136.702621332184));
#147866=CARTESIAN_POINT('Ctrl Pts',(69.265418765177,-0.310317868426777,
136.715067781374));
#147867=CARTESIAN_POINT('Ctrl Pts',(69.2580220802647,-0.152703520502925,
136.721239528814));
#147868=CARTESIAN_POINT('Ctrl Pts',(69.2506253953525,0.00491575462348875,
136.721108575512));
#147869=CARTESIAN_POINT('Ctrl Pts',(69.2432290384171,0.162528040745957,
136.720977628017));
#147870=CARTESIAN_POINT('Ctrl Pts',(69.2358326814816,0.320144880339142,
136.714544535768));
#147871=CARTESIAN_POINT('Ctrl Pts',(69.2284363245462,0.477226250564283,
136.701833438044));
#147872=CARTESIAN_POINT('Ctrl Pts',(69.2210388352096,0.634331670348327,
136.689120394218));
#147873=CARTESIAN_POINT('Ctrl Pts',(69.213641345873,0.790901085422228,136.670127461194));
#147874=CARTESIAN_POINT('Ctrl Pts',(69.2062438565364,0.946399478234522,
136.644930674512));
#147875=CARTESIAN_POINT('Ctrl Pts',(69.1988437740214,1.10195238076725,136.619725055136));
#147876=CARTESIAN_POINT('Ctrl Pts',(69.1914436915064,1.25643314526804,136.588311311862));
#147877=CARTESIAN_POINT('Ctrl Pts',(69.1840436089914,1.40931697623449,136.550816588249));
#147878=CARTESIAN_POINT('Ctrl Pts',(69.176635389325,1.56236891869003,136.513280635333));
#147879=CARTESIAN_POINT('Ctrl Pts',(69.1692271696585,1.7138200580025,136.469650437345));
#147880=CARTESIAN_POINT('Ctrl Pts',(69.161818949992,1.86316008840639,136.420103226293));
#147881=CARTESIAN_POINT('Ctrl Pts',(69.15440617069,2.01259203510712,136.370525519759));
#147882=CARTESIAN_POINT('Ctrl Pts',(69.1469933913879,2.15990993525838,136.315023674676));
#147883=CARTESIAN_POINT('Ctrl Pts',(69.1395806120859,2.30462398601776,136.253822870447));
#147884=CARTESIAN_POINT('Ctrl Pts',(69.1321572410571,2.44954481099938,136.192534619638));
#147885=CARTESIAN_POINT('Ctrl Pts',(69.1247338700283,2.59185401907099,136.125531305));
#147886=CARTESIAN_POINT('Ctrl Pts',(69.1173104989996,2.73108616651883,136.053084168445));
#147887=CARTESIAN_POINT('Ctrl Pts',(69.1133744495587,2.80491039192578,136.014670958298));
#147888=CARTESIAN_POINT('Ctrl Pts',(69.1094384001179,2.87787001551399,135.974728027862));
#147889=CARTESIAN_POINT('Ctrl Pts',(69.1055023506771,2.94989912369862,135.933300636956));
#147890=CARTESIAN_POINT('Ctrl Pts',(69.0980790842717,3.08574377378226,135.855169870613));
#147891=CARTESIAN_POINT('Ctrl Pts',(69.0906558178662,3.21868764584694,135.771520279805));
#147892=CARTESIAN_POINT('Ctrl Pts',(69.0832325514608,3.34825070465196,135.682592651951));
#147893=CARTESIAN_POINT('Ctrl Pts',(69.0758180587398,3.47766063068111,135.593770129168));
#147894=CARTESIAN_POINT('Ctrl Pts',(69.0684035660188,3.60369739242263,135.499682195697));
#147895=CARTESIAN_POINT('Ctrl Pts',(69.0609890732977,3.72590554975223,135.400615440444));
#147896=CARTESIAN_POINT('Ctrl Pts',(69.053581726944,3.84799591825892,135.301644169459));
#147897=CARTESIAN_POINT('Ctrl Pts',(69.0461743805902,3.96626474068308,135.197703863605));
#147898=CARTESIAN_POINT('Ctrl Pts',(69.0387670342364,4.08028567942142,135.08912424428));
#147899=CARTESIAN_POINT('Ctrl Pts',(69.031365212561,4.19422157704181,134.980625607731));
#147900=CARTESIAN_POINT('Ctrl Pts',(69.0239633908856,4.30391563018407,134.86749480371));
#147901=CARTESIAN_POINT('Ctrl Pts',(69.0165615692102,4.40897481416923,134.750101568328));
#147902=CARTESIAN_POINT('Ctrl Pts',(69.0091636548988,4.51397853822902,134.632770303922));
#147903=CARTESIAN_POINT('Ctrl Pts',(69.0017657405875,4.61435201756119,134.511181366811));
#147904=CARTESIAN_POINT('Ctrl Pts',(68.9943678262761,4.70973940911688,134.385740974455));
#147905=CARTESIAN_POINT('Ctrl Pts',(68.9869711413639,4.80511094901846,134.260321428017));
#147906=CARTESIAN_POINT('Ctrl Pts',(68.9795744564518,4.89549781992989,134.131051993483));
#147907=CARTESIAN_POINT('Ctrl Pts',(68.9721777715395,4.98058471347895,133.998371649851));
#147908=CARTESIAN_POINT('Ctrl Pts',(68.9647814146041,5.06566783418599,133.865697189405));
#147909=CARTESIAN_POINT('Ctrl Pts',(68.9573850576686,5.14545124328763,133.729612434816));
#147910=CARTESIAN_POINT('Ctrl Pts',(68.9499887007332,5.21966335430782,133.590584770465));
#147911=CARTESIAN_POINT('Ctrl Pts',(68.9425912113966,5.29388682739167,133.451535820623));
#147912=CARTESIAN_POINT('Ctrl Pts',(68.93519372206,5.36253712819855,133.309543393217));
#147913=CARTESIAN_POINT('Ctrl Pts',(68.9277962327235,5.4253890375276,133.165098712734));
#147914=CARTESIAN_POINT('Ctrl Pts',(68.9203961502085,5.48826297949603,133.020603397391));
#147915=CARTESIAN_POINT('Ctrl Pts',(68.9129960676935,5.54533433421071,132.873654459531));
#147916=CARTESIAN_POINT('Ctrl Pts',(68.9055959851785,5.59642640636216,132.724762148671));
#147917=CARTESIAN_POINT('Ctrl Pts',(68.898187765512,5.64757465949938,132.57570611541));
#147918=CARTESIAN_POINT('Ctrl Pts',(68.8907795458456,5.6927303784587,132.424702794848));
#147919=CARTESIAN_POINT('Ctrl Pts',(68.8833713261791,5.73176684081676,132.272277319908));
#147920=CARTESIAN_POINT('Ctrl Pts',(68.875958546877,5.77082732946607,132.119758029631));
#147921=CARTESIAN_POINT('Ctrl Pts',(68.868545767575,5.80376097877548,131.965815204999));
#147922=CARTESIAN_POINT('Ctrl Pts',(68.8611329882729,5.83049248815307,131.810982645981));
#147923=CARTESIAN_POINT('Ctrl Pts',(68.8537096172442,5.85726219276484,131.655928854942));
#147924=CARTESIAN_POINT('Ctrl Pts',(68.8462862462154,5.87781200958529,131.499983159576));
#147925=CARTESIAN_POINT('Ctrl Pts',(68.8388628751866,5.89211855842186,131.343683763742));
#147926=CARTESIAN_POINT('Ctrl Pts',(68.8349268257459,5.89970423389587,131.260810073718));
#147927=CARTESIAN_POINT('Ctrl Pts',(68.8309907763051,5.9055355739646,131.17783694651));
#147928=CARTESIAN_POINT('Ctrl Pts',(68.8270547268644,5.90961502909356,131.094844301121));
#147929=CARTESIAN_POINT('Ctrl Pts',(68.819631460459,5.91730875415144,130.938322762026));
#147930=CARTESIAN_POINT('Ctrl Pts',(68.8122081940535,5.91879139451045,130.781258670205));
#147931=CARTESIAN_POINT('Ctrl Pts',(68.804784927648,5.91400606067311,130.624186044383));
#147932=CARTESIAN_POINT('Ctrl Pts',(68.797370434927,5.90922638270297,130.46729906536));
#147933=CARTESIAN_POINT('Ctrl Pts',(68.789955942206,5.89819348790567,130.310403941893));
#147934=CARTESIAN_POINT('Ctrl Pts',(68.782541449485,5.8809023151317,130.154038756963));
#147935=CARTESIAN_POINT('Ctrl Pts',(68.7751341031312,5.86362780824105,129.997824282684));
#147936=CARTESIAN_POINT('Ctrl Pts',(68.7677267567775,5.84010707258086,129.842139098635));
#147937=CARTESIAN_POINT('Ctrl Pts',(68.7603194104237,5.8103870662121,129.687520117183));
#147938=CARTESIAN_POINT('Ctrl Pts',(68.7529175887483,5.78068922614536,129.533016456402));
#147939=CARTESIAN_POINT('Ctrl Pts',(68.7455157670729,5.7448013918412,129.379577779849));
#147940=CARTESIAN_POINT('Ctrl Pts',(68.7381139453975,5.70282219332268,129.227734601719));
#147941=CARTESIAN_POINT('Ctrl Pts',(68.7307160310861,5.66086515529631,129.07597158042));
#147942=CARTESIAN_POINT('Ctrl Pts',(68.7233181167747,5.61282325626493,128.92580273905));
#147943=CARTESIAN_POINT('Ctrl Pts',(68.7159202024634,5.55884591662218,128.777747028903));
#147944=CARTESIAN_POINT('Ctrl Pts',(68.7085235175512,5.50487754703404,128.629715922929));
#147945=CARTESIAN_POINT('Ctrl Pts',(68.7011268326389,5.44497582220963,128.483797601595));
#147946=CARTESIAN_POINT('Ctrl Pts',(68.6937301477267,5.37933963573566,128.340494621635));
#147947=CARTESIAN_POINT('Ctrl Pts',(68.6863337907913,5.31370635963893,128.19719799588));
#147948=CARTESIAN_POINT('Ctrl Pts',(68.6789374338559,5.24233928292074,128.056516820309));
#147949=CARTESIAN_POINT('Ctrl Pts',(68.6715410769204,5.16548483017149,127.91893222099));
#147950=CARTESIAN_POINT('Ctrl Pts',(68.6641435875838,5.08861861080932,127.781326557117));
#147951=CARTESIAN_POINT('Ctrl Pts',(68.6567460982472,5.0062635246613,127.6468187394));
#147952=CARTESIAN_POINT('Ctrl Pts',(68.6493486089106,4.91871111632016,127.515863769964));
#147953=CARTESIAN_POINT('Ctrl Pts',(68.6419485263956,4.83112801661799,127.384862894466));
#147954=CARTESIAN_POINT('Ctrl Pts',(68.6345484438806,4.7383441746543,127.257417657059));
#147955=CARTESIAN_POINT('Ctrl Pts',(68.6271483613656,4.64069336966992,127.133952518839));
#147956=CARTESIAN_POINT('Ctrl Pts',(68.6197401416991,4.54293518758671,127.010351618007));
#147957=CARTESIAN_POINT('Ctrl Pts',(68.6123319220326,4.44029958644868,126.890739849545));
#147958=CARTESIAN_POINT('Ctrl Pts',(68.6049237023661,4.33315987889097,126.775507675788));
#147959=CARTESIAN_POINT('Ctrl Pts',(68.597510923064,4.22595422863083,126.660204578552));
#147960=CARTESIAN_POINT('Ctrl Pts',(68.590098143762,4.11423921228098,126.549286709682));
#147961=CARTESIAN_POINT('Ctrl Pts',(68.5826853644599,3.99842322906532,126.443105953622));
#147962=CARTESIAN_POINT('Ctrl Pts',(68.5752619934312,3.8824417625417,126.336773481519));
#147963=CARTESIAN_POINT('Ctrl Pts',(68.5678386224024,3.76234791036724,126.235191881096));
#147964=CARTESIAN_POINT('Ctrl Pts',(68.5604152513737,3.6385818411254,126.138671735104));
#147965=CARTESIAN_POINT('Ctrl Pts',(68.5564792019329,3.57295810148776,126.08749443773));
#147966=CARTESIAN_POINT('Ctrl Pts',(68.5525431524921,3.50630244139167,126.03773936419));
#147967=CARTESIAN_POINT('Ctrl Pts',(68.5486071030514,3.43868342349489,125.989447651013));
#147968=CARTESIAN_POINT('Ctrl Pts',(68.5411838366459,3.31115606605807,125.898370987093));
#147969=CARTESIAN_POINT('Ctrl Pts',(68.5337605702405,3.17981500065238,125.812226621635));
#147970=CARTESIAN_POINT('Ctrl Pts',(68.526337303835,3.04507876219255,125.731351067551));
#147971=CARTESIAN_POINT('Ctrl Pts',(68.518922811114,2.91050177077733,125.650571101655));
#147972=CARTESIAN_POINT('Ctrl Pts',(68.511508318393,2.77253791077296,125.575047741906));
#147973=CARTESIAN_POINT('Ctrl Pts',(68.504093825672,2.63163715095387,125.505076093385));
#147974=CARTESIAN_POINT('Ctrl Pts',(68.4966864793182,2.49087219659181,125.435171886174));
#147975=CARTESIAN_POINT('Ctrl Pts',(68.4892791329644,2.34717630986715,125.370808902426));
#147976=CARTESIAN_POINT('Ctrl Pts',(68.4818717866106,2.20102659234113,125.312237849245));
#147977=CARTESIAN_POINT('Ctrl Pts',(68.4744699649352,2.05498587878835,125.253710480566));
#147978=CARTESIAN_POINT('Ctrl Pts',(68.4670681432598,1.90649532354502,125.200966579338));
#147979=CARTESIAN_POINT('Ctrl Pts',(68.4596663215844,1.75605457516337,125.154209921209));
#147980=CARTESIAN_POINT('Ctrl Pts',(68.452268407273,1.60569324328165,125.107477945556));
#147981=CARTESIAN_POINT('Ctrl Pts',(68.4448704929616,1.45338412411913,125.06672702899));
#147982=CARTESIAN_POINT('Ctrl Pts',(68.4374725786503,1.29964459146979,125.032111965752));
#147983=CARTESIAN_POINT('Ctrl Pts',(68.4300758937381,1.14593060754188,124.997502654911));
#147984=CARTESIAN_POINT('Ctrl Pts',(68.4226792088259,0.990787045733209,
124.969027255577));
#147985=CARTESIAN_POINT('Ctrl Pts',(68.4152825239136,0.8347442280997,124.946790077133));
#147986=CARTESIAN_POINT('Ctrl Pts',(68.4078861669782,0.678708329568245,
124.924553884708));
#147987=CARTESIAN_POINT('Ctrl Pts',(68.4004898100427,0.521773624058667,
124.908555415847));
#147988=CARTESIAN_POINT('Ctrl Pts',(68.3930934531073,0.364478095067757,
124.898847406954));
#147989=CARTESIAN_POINT('Ctrl Pts',(68.3856959637707,0.207158483729802,
124.889137911739));
#147990=CARTESIAN_POINT('Ctrl Pts',(68.3782984744341,0.0494783115272505,
124.885720817121));
#147991=CARTESIAN_POINT('Ctrl Pts',(68.3709009850975,-0.108022028391509,
124.888596778138));
#147992=CARTESIAN_POINT('Ctrl Pts',(68.3635009025825,-0.26557757981027,
124.891473747319));
#147993=CARTESIAN_POINT('Ctrl Pts',(68.3561008200676,-0.422952800430353,
124.900648157497));
#147994=CARTESIAN_POINT('Ctrl Pts',(68.3487007375525,-0.579610163276937,
124.916068622333));
#147995=CARTESIAN_POINT('Ctrl Pts',(68.3412925178861,-0.73643978699885,
124.931506043556));
#147996=CARTESIAN_POINT('Ctrl Pts',(68.3338842982196,-0.892549604816276,
124.953203199051));
#147997=CARTESIAN_POINT('Ctrl Pts',(68.3264760785531,-1.04740932510994,
124.981057064756));
#147998=CARTESIAN_POINT('Ctrl Pts',(68.3190632992511,-1.20236435897748,
125.00892807405));
#147999=CARTESIAN_POINT('Ctrl Pts',(68.311650519949,-1.35606739854285,125.042963263795));
#148000=CARTESIAN_POINT('Ctrl Pts',(68.3042377406469,-1.50800164370169,
125.083009238294));
#148001=CARTESIAN_POINT('Ctrl Pts',(68.2968143696182,-1.66015297963503,
125.12311243236));
#148002=CARTESIAN_POINT('Ctrl Pts',(68.2893909985894,-1.81053011756679,
125.169243455132));
#148003=CARTESIAN_POINT('Ctrl Pts',(68.2819676275606,-1.95863383356228,
125.221199857878));
#148004=CARTESIAN_POINT('Ctrl Pts',(68.2780315781199,-2.03716197748134,
125.24874838929));
#148005=CARTESIAN_POINT('Ctrl Pts',(68.2740955286792,-2.11505134242283,
125.277933851331));
#148006=CARTESIAN_POINT('Ctrl Pts',(68.2701594792385,-2.19223025926975,
125.308720795594));
#148007=CARTESIAN_POINT('Ctrl Pts',(68.2627362128331,-2.33778728777455,
125.366784011648));
#148008=CARTESIAN_POINT('Ctrl Pts',(68.2553129464276,-2.48125603620484,
125.430721836023));
#148009=CARTESIAN_POINT('Ctrl Pts',(68.2478896800222,-2.62212715837375,
125.50036403689));
#148010=CARTESIAN_POINT('Ctrl Pts',(68.2404751873012,-2.76283178257508,
125.56992392646));
#148011=CARTESIAN_POINT('Ctrl Pts',(68.2330606945801,-2.90094456035185,
125.645174608516));
#148012=CARTESIAN_POINT('Ctrl Pts',(68.2256462018591,-3.03597399232721,
125.725897023091));
#148013=CARTESIAN_POINT('Ctrl Pts',(68.2182388555054,-3.17087327785188,
125.806541634363));
#148014=CARTESIAN_POINT('Ctrl Pts',(68.2108315091516,-3.30269481567501,
125.892647288674));
#148015=CARTESIAN_POINT('Ctrl Pts',(68.2034241627978,-3.43096979376216,
125.983948100282));
#148016=CARTESIAN_POINT('Ctrl Pts',(68.1960223411224,-3.55914909953138,
126.0751808163));
#148017=CARTESIAN_POINT('Ctrl Pts',(68.188620519447,-3.6837868096121,126.171600758942));
#148018=CARTESIAN_POINT('Ctrl Pts',(68.1812186977716,-3.80444140953322,
126.272897705445));
#148019=CARTESIAN_POINT('Ctrl Pts',(68.1738207834603,-3.92503231683004,
126.374141178078));
#148020=CARTESIAN_POINT('Ctrl Pts',(68.1664228691489,-4.04164401632709,
126.480256287848));
#148021=CARTESIAN_POINT('Ctrl Pts',(68.1590249548376,-4.15386662207163,
126.590891423595));
#148022=CARTESIAN_POINT('Ctrl Pts',(68.1516282699254,-4.26607057845517,
126.701508173791));
#148023=CARTESIAN_POINT('Ctrl Pts',(68.1442315850131,-4.37388662313031,
126.816643197344));
#148024=CARTESIAN_POINT('Ctrl Pts',(68.1368349001009,-4.47694034563364,
126.935906701059));
#148025=CARTESIAN_POINT('Ctrl Pts',(68.1294385431655,-4.57998949862684,
127.055164916505));
#148026=CARTESIAN_POINT('Ctrl Pts',(68.12204218623,-4.67827650525111,127.178550965669));
#148027=CARTESIAN_POINT('Ctrl Pts',(68.1146458292945,-4.77146620365485,
127.305640733111));
#148028=CARTESIAN_POINT('Ctrl Pts',(68.1072483399579,-4.86467016963959,
127.432749958322));
#148029=CARTESIAN_POINT('Ctrl Pts',(68.0998508506213,-4.95277505274746,
127.563563729822));
#148030=CARTESIAN_POINT('Ctrl Pts',(68.0924533612847,-5.03548820617812,
127.697627753617));
#148031=CARTESIAN_POINT('Ctrl Pts',(68.0850532787697,-5.11823035457643,
127.831738773347));
#148032=CARTESIAN_POINT('Ctrl Pts',(68.0776531962548,-5.19557681431019,
127.969101996351));
#148033=CARTESIAN_POINT('Ctrl Pts',(68.0702531137398,-5.26728027170078,
128.109237410391));
#148034=CARTESIAN_POINT('Ctrl Pts',(68.0628448940733,-5.33906257441396,
128.249526917725));
#148035=CARTESIAN_POINT('Ctrl Pts',(68.0554366744068,-5.40518931272512,
128.392594371242));
#148036=CARTESIAN_POINT('Ctrl Pts',(68.0480284547403,-5.46546052812274,
128.537937934563));
#148037=CARTESIAN_POINT('Ctrl Pts',(68.0406156754382,-5.52576883944781,
128.683370954421));
#148038=CARTESIAN_POINT('Ctrl Pts',(68.0332028961361,-5.58021431767922,
128.831082526117));
#148039=CARTESIAN_POINT('Ctrl Pts',(68.0257901168341,-5.62864667588095,
128.980554936964));
#148040=CARTESIAN_POINT('Ctrl Pts',(68.0183667458053,-5.67714823650737,
129.130240921002));
#148041=CARTESIAN_POINT('Ctrl Pts',(68.0109433747765,-5.71961941676884,
129.281692410668));
#148042=CARTESIAN_POINT('Ctrl Pts',(68.0035200037478,-5.75596069978699,
129.43437996624));
#148043=CARTESIAN_POINT('Ctrl Pts',(67.999583954307,-5.77522972003999,129.515338571891));
#148044=CARTESIAN_POINT('Ctrl Pts',(67.9956479048663,-5.79277626855372,
129.596644555686));
#148045=CARTESIAN_POINT('Ctrl Pts',(67.9917118554256,-5.80859143016921,
129.678218459637));
#148046=CARTESIAN_POINT('Ctrl Pts',(67.9808130884996,-5.85238299400481,
129.904093408566));
#148047=CARTESIAN_POINT('Ctrl Pts',(67.9699143215737,-5.88300986694146,
130.132596655975));
#148048=CARTESIAN_POINT('Ctrl Pts',(67.9590155546477,-5.90022621487157,
130.362476949796));
#148049=CARTESIAN_POINT('Ctrl Pts',(67.9521354338356,-5.91109446762949,
130.507594668574));
#148050=CARTESIAN_POINT('Ctrl Pts',(67.9452553130236,-5.91661932922891,
130.65326080399));
#148051=CARTESIAN_POINT('Ctrl Pts',(67.9383751922115,-5.91674770925342,
130.799154126957));
#148052=CARTESIAN_POINT('',(66.1883751922116,-5.90702516183033,130.803589055723));
#148053=CARTESIAN_POINT('Ctrl Pts',(67.9383740532611,-5.91922168982187,
130.79917611158));
#148054=CARTESIAN_POINT('Ctrl Pts',(67.8633374460449,-5.90455875036985,
132.391010917394));
#148055=CARTESIAN_POINT('Ctrl Pts',(67.6954849642247,-4.42064434812357,
135.975930907562));
#148056=CARTESIAN_POINT('Ctrl Pts',(67.4348166077997,1.6443349981276,137.606839793888));
#148057=CARTESIAN_POINT('Ctrl Pts',(67.156368983987,6.61192161886336,133.097841168245));
#148058=CARTESIAN_POINT('Ctrl Pts',(66.8779213601741,5.50347528219203,126.481245959285));
#148059=CARTESIAN_POINT('Ctrl Pts',(66.599473736361,-0.662395979099899,
123.837381925391));
#148060=CARTESIAN_POINT('Ctrl Pts',(66.369625013707,-5.24963757446116,126.939849443361));
#148061=CARTESIAN_POINT('Ctrl Pts',(66.2325921656571,-5.90811822702256,
129.860655023505));
#148062=CARTESIAN_POINT('Ctrl Pts',(66.1883751922116,-5.90702516183033,
130.803589055723));
#148063=CARTESIAN_POINT('',(64.4383751922115,-5.91638089232767,130.809832875924));
#148064=CARTESIAN_POINT('Ctrl Pts',(66.1883751922116,-5.90702516183033,
130.803589055723));
#148065=CARTESIAN_POINT('Ctrl Pts',(66.1397762910528,-5.90582377324359,
131.839968397412));
#148066=CARTESIAN_POINT('Ctrl Pts',(65.9983615152899,-5.15160611073396,
134.857296499428));
#148067=CARTESIAN_POINT('Ctrl Pts',(65.7641308649225,-0.332949373316311,
137.794833079793));
#148068=CARTESIAN_POINT('Ctrl Pts',(65.4856832411095,5.7013151939231,134.863001472567));
#148069=CARTESIAN_POINT('Ctrl Pts',(65.2072356172968,6.49634962267588,128.201477195226));
#148070=CARTESIAN_POINT('Ctrl Pts',(64.9287879934838,1.32155611251496,123.931875625089));
#148071=CARTESIAN_POINT('Ctrl Pts',(64.6725011851222,-4.55918243657943,
125.814926826125));
#148072=CARTESIAN_POINT('Ctrl Pts',(64.5090302513647,-5.9025589280303,129.309102465528));
#148073=CARTESIAN_POINT('Ctrl Pts',(64.4383751922115,-5.91638089232767,
130.809832875924));
#148074=CARTESIAN_POINT('',(62.6883751922116,-5.92596308185693,130.80268746135));
#148075=CARTESIAN_POINT('Ctrl Pts',(64.4383751922115,-5.91638089232767,
130.809832875924));
#148076=CARTESIAN_POINT('Ctrl Pts',(64.4162143767604,-5.92071612328831,
131.280533913689));
#148077=CARTESIAN_POINT('Ctrl Pts',(64.3012376867048,-5.65391015254493,
133.717810089976));
#148078=CARTESIAN_POINT('Ctrl Pts',(64.0934451220452,-2.28341567571408,
137.419764866907));
#148079=CARTESIAN_POINT('Ctrl Pts',(63.8149974982322,4.33148500470616,136.30125048224));
#148080=CARTESIAN_POINT('Ctrl Pts',(63.5365498744195,6.96596257060751,130.13136284993));
#148081=CARTESIAN_POINT('Ctrl Pts',(63.2581022506065,3.19906084031009,124.579927288311));
#148082=CARTESIAN_POINT('Ctrl Pts',(62.9796546267936,-3.50762151942191,
124.748441875803));
#148083=CARTESIAN_POINT('Ctrl Pts',(62.7897456073286,-5.88336273271958,
128.658921952266));
#148084=CARTESIAN_POINT('Ctrl Pts',(62.6926524624679,-5.92630129488592,
130.712218582565));
#148085=CARTESIAN_POINT('Ctrl Pts',(62.6883751922116,-5.92596308185693,
130.80268746135));
#148086=CARTESIAN_POINT('',(60.9383763907753,-5.91354401369683,130.799673779747));
#148087=CARTESIAN_POINT('Ctrl Pts',(62.6883751922116,-5.92596308185693,
130.80268746135));
#148088=CARTESIAN_POINT('Ctrl Pts',(62.5998365878636,-5.91896214252789,
132.675374428599));
#148089=CARTESIAN_POINT('Ctrl Pts',(62.4184821089114,-3.94761271390423,
136.523902656696));
#148090=CARTESIAN_POINT('Ctrl Pts',(62.1443117553548,2.61276674649605,137.296741572097));
#148091=CARTESIAN_POINT('Ctrl Pts',(61.8658641315421,6.87448821768475,132.115456447487));
#148092=CARTESIAN_POINT('Ctrl Pts',(61.5874165077291,4.81889085424591,125.729338305771));
#148093=CARTESIAN_POINT('Ctrl Pts',(61.3089688839162,-1.66503178834267,
124.006917739971));
#148094=CARTESIAN_POINT('Ctrl Pts',(61.0926224593943,-5.51403400753928,
127.522021498947));
#148095=CARTESIAN_POINT('Ctrl Pts',(60.9690919094768,-5.91607461361271,
130.14584520162));
#148096=CARTESIAN_POINT('Ctrl Pts',(60.9383772341634,-5.91128936499411,
130.799657604163));
#148097=CARTESIAN_POINT('',(59.1883740221267,-5.91242413515847,130.807894219129));
#148098=CARTESIAN_POINT('Ctrl Pts',(60.9383751922115,-5.91674816187077,
130.799696767348));
#148099=CARTESIAN_POINT('Ctrl Pts',(60.9306126273815,-5.91687853020878,
130.965087289821));
#148100=CARTESIAN_POINT('Ctrl Pts',(60.9228500625514,-5.91006894075129,
131.130563255582));
#148101=CARTESIAN_POINT('Ctrl Pts',(60.9150874977214,-5.89633053957049,
131.295498816679));
#148102=CARTESIAN_POINT('Ctrl Pts',(60.90769975758,-5.88325551345419,131.452470267759));
#148103=CARTESIAN_POINT('Ctrl Pts',(60.9003120174386,-5.86390512345827,
131.608951866011));
#148104=CARTESIAN_POINT('Ctrl Pts',(60.8929242772972,-5.83834232962341,
131.764407181347));
#148105=CARTESIAN_POINT('Ctrl Pts',(60.8855362623704,-5.81277858498592,
131.91986827881));
#148106=CARTESIAN_POINT('Ctrl Pts',(60.8781482474435,-5.78100203643834,
132.074302648395));
#148107=CARTESIAN_POINT('Ctrl Pts',(60.8707602325167,-5.74312707618287,
132.227182443838));
#148108=CARTESIAN_POINT('Ctrl Pts',(60.8633704800293,-5.70524320825183,
132.38009819453));
#148109=CARTESIAN_POINT('Ctrl Pts',(60.8559807275417,-5.66125816267149,
132.531458280336));
#148110=CARTESIAN_POINT('Ctrl Pts',(60.8485909750543,-5.61133662443686,
132.680748597104));
#148111=CARTESIAN_POINT('Ctrl Pts',(60.8411980214569,-5.56139346107563,
132.830103583794));
#148112=CARTESIAN_POINT('Ctrl Pts',(60.8338050678595,-5.50550880325984,
132.977386662192));
#148113=CARTESIAN_POINT('Ctrl Pts',(60.8264121142621,-5.44389595922857,
133.122102481449));
#148114=CARTESIAN_POINT('Ctrl Pts',(60.8190104148024,-5.38221022721806,
133.266989499484));
#148115=CARTESIAN_POINT('Ctrl Pts',(60.8116087153427,-5.31478292445014,
133.409302850196));
#148116=CARTESIAN_POINT('Ctrl Pts',(60.804207015883,-5.2418742434211,133.54856997158));
#148117=CARTESIAN_POINT('Ctrl Pts',(60.7968002188792,-5.16891535024621,
133.68793300611));
#148118=CARTESIAN_POINT('Ctrl Pts',(60.7893934218755,-5.09046774340257,
133.824245308697));
#148119=CARTESIAN_POINT('Ctrl Pts',(60.7819866248717,-5.00683535243619,
133.957062683429));
#148120=CARTESIAN_POINT('Ctrl Pts',(60.7745691702738,-4.92308262334171,
134.090071168256));
#148121=CARTESIAN_POINT('Ctrl Pts',(60.7671517156758,-4.83413042530598,
134.219574377895));
#148122=CARTESIAN_POINT('Ctrl Pts',(60.7597342610779,-4.74032383136926,
134.345160038072));
#148123=CARTESIAN_POINT('Ctrl Pts',(60.7571807194821,-4.70802986361868,
134.388394304337));
#148124=CARTESIAN_POINT('Ctrl Pts',(60.7546271778862,-4.67516090251069,
134.431164592743));
#148125=CARTESIAN_POINT('Ctrl Pts',(60.7520736362904,-4.64173203189925,
134.473455098026));
#148126=CARTESIAN_POINT('Ctrl Pts',(60.744650369885,-4.54455272117663,134.5963956006));
#148127=CARTESIAN_POINT('Ctrl Pts',(60.7372271034796,-4.44233880365307,
134.7156585128));
#148128=CARTESIAN_POINT('Ctrl Pts',(60.7298038370742,-4.33539875922592,
134.830804229614));
#148129=CARTESIAN_POINT('Ctrl Pts',(60.7223893443532,-4.22858510905032,
134.945813853753));
#148130=CARTESIAN_POINT('Ctrl Pts',(60.7149748516321,-4.11705670226956,
135.056715697814));
#148131=CARTESIAN_POINT('Ctrl Pts',(60.7075603589111,-4.00116372536805,
135.163101193156));
#148132=CARTESIAN_POINT('Ctrl Pts',(60.7001530125573,-3.88538245048097,
135.269384150153));
#148133=CARTESIAN_POINT('Ctrl Pts',(60.6927456662036,-3.76524525341261,
135.371159173705));
#148134=CARTESIAN_POINT('Ctrl Pts',(60.6853383198498,-3.64114072702438,
135.468052799572));
#148135=CARTESIAN_POINT('Ctrl Pts',(60.6779364981744,-3.51712876247431,
135.564874158517));
#148136=CARTESIAN_POINT('Ctrl Pts',(60.670534676499,-3.38915565331457,135.656821140224));
#148137=CARTESIAN_POINT('Ctrl Pts',(60.6631328548236,-3.25764469811424,
135.743559093366));
#148138=CARTESIAN_POINT('Ctrl Pts',(60.6557349405123,-3.12620316652367,
135.830251258218));
#148139=CARTESIAN_POINT('Ctrl Pts',(60.6483370262009,-2.99122781914384,
135.911739665863));
#148140=CARTESIAN_POINT('Ctrl Pts',(60.6409391118896,-2.85317259850371,
135.987731787533));
#148141=CARTESIAN_POINT('Ctrl Pts',(60.6335424269774,-2.71514032013647,
136.063711280692));
#148142=CARTESIAN_POINT('Ctrl Pts',(60.6261457420651,-2.57402951102585,
136.134196120835));
#148143=CARTESIAN_POINT('Ctrl Pts',(60.6187490571529,-2.43032058698322,
136.198938674002));
#148144=CARTESIAN_POINT('Ctrl Pts',(60.6113527002175,-2.28661803514468,
136.263678356417));
#148145=CARTESIAN_POINT('Ctrl Pts',(60.603956343282,-2.14031793778975,136.322676104791));
#148146=CARTESIAN_POINT('Ctrl Pts',(60.5965599863466,-1.99192240812506,
136.375731695004));
#148147=CARTESIAN_POINT('Ctrl Pts',(60.58916249701,-1.84350415872615,136.428795408162));
#148148=CARTESIAN_POINT('Ctrl Pts',(60.5817650076735,-1.69299018976002,
136.475915026024));
#148149=CARTESIAN_POINT('Ctrl Pts',(60.5743675183369,-1.54089940841796,
136.51693968272));
#148150=CARTESIAN_POINT('Ctrl Pts',(60.5669674358219,-1.38875531188827,
136.557978720546));
#148151=CARTESIAN_POINT('Ctrl Pts',(60.5595673533069,-1.23503366265474,
136.592918446134));
#148152=CARTESIAN_POINT('Ctrl Pts',(60.552167270792,-1.08026508293948,136.621658780208));
#148153=CARTESIAN_POINT('Ctrl Pts',(60.5447590511255,-0.92532631926001,
136.650430717234));
#148154=CARTESIAN_POINT('Ctrl Pts',(60.537350831459,-0.769338693309987,
136.672989580815));
#148155=CARTESIAN_POINT('Ctrl Pts',(60.5299426117925,-0.612840233185152,
136.689286905217));
#148156=CARTESIAN_POINT('Ctrl Pts',(60.5225298324904,-0.456245450869427,
136.705594260351));
#148157=CARTESIAN_POINT('Ctrl Pts',(60.5151170531884,-0.299139579552217,
136.715632373235));
#148158=CARTESIAN_POINT('Ctrl Pts',(60.5077042738863,-0.14206169168865,
136.719404914801));
#148159=CARTESIAN_POINT('Ctrl Pts',(60.5002809028576,0.0152406364275426,
136.723182846752));
#148160=CARTESIAN_POINT('Ctrl Pts',(60.4928575318288,0.172514528971182,
136.72067733308));
#148161=CARTESIAN_POINT('Ctrl Pts',(60.4854341608,0.329224159341883,136.711944050359));
#148162=CARTESIAN_POINT('Ctrl Pts',(60.4814981113592,0.412315365560495,
136.707313454307));
#148163=CARTESIAN_POINT('Ctrl Pts',(60.4775620619184,0.495248064304087,
136.700932870871));
#148164=CARTESIAN_POINT('Ctrl Pts',(60.4736260124776,0.577943556717647,
136.692816425989));
#148165=CARTESIAN_POINT('Ctrl Pts',(60.4662027460722,0.733904674571259,
136.677509064247));
#148166=CARTESIAN_POINT('Ctrl Pts',(60.4587794796667,0.88949305944162,136.655978117788));
#148167=CARTESIAN_POINT('Ctrl Pts',(60.4513562132613,1.04417211826217,136.628245502241));
#148168=CARTESIAN_POINT('Ctrl Pts',(60.4439417205403,1.19866835928114,136.600545664342));
#148169=CARTESIAN_POINT('Ctrl Pts',(60.4365272278193,1.35225704969109,136.566658812711));
#148170=CARTESIAN_POINT('Ctrl Pts',(60.4291127350982,1.50440516477545,136.526658727827));
#148171=CARTESIAN_POINT('Ctrl Pts',(60.4217053887444,1.656406633778,136.486697196531));
#148172=CARTESIAN_POINT('Ctrl Pts',(60.4142980423906,1.80696993304082,136.440634256398));
#148173=CARTESIAN_POINT('Ctrl Pts',(60.4068906960368,1.95557081258704,136.388594975064));
#148174=CARTESIAN_POINT('Ctrl Pts',(60.3994888743614,2.10406085999091,136.336594506589));
#148175=CARTESIAN_POINT('Ctrl Pts',(60.392087052686,2.25059105119362,136.278626695009));
#148176=CARTESIAN_POINT('Ctrl Pts',(60.3846852310106,2.39465103133813,136.21486678618));
#148177=CARTESIAN_POINT('Ctrl Pts',(60.3772873166992,2.53863496334027,136.151140535711));
#148178=CARTESIAN_POINT('Ctrl Pts',(60.3698894023878,2.68015094077902,136.081628428057));
#148179=CARTESIAN_POINT('Ctrl Pts',(60.3624914880765,2.81870748389155,136.006554258979));
#148180=CARTESIAN_POINT('Ctrl Pts',(60.3550948031642,2.95724100142048,135.931492565865));
#148181=CARTESIAN_POINT('Ctrl Pts',(60.347698118252,3.09281573281521,135.85087082348));
#148182=CARTESIAN_POINT('Ctrl Pts',(60.3403014333398,3.22496366013016,135.764959367046));
#148183=CARTESIAN_POINT('Ctrl Pts',(60.3329050764043,3.35710572786734,135.679051720016));
#148184=CARTESIAN_POINT('Ctrl Pts',(60.3255087194688,3.48582098067647,135.587855028773));
#148185=CARTESIAN_POINT('Ctrl Pts',(60.3181123625334,3.61066955988036,135.491683509351));
#148186=CARTESIAN_POINT('Ctrl Pts',(60.3107148731968,3.73553725372099,135.395497265823));
#148187=CARTESIAN_POINT('Ctrl Pts',(60.3033173838602,3.85653679946014,135.294334905369));
#148188=CARTESIAN_POINT('Ctrl Pts',(60.2959198945235,3.97326078735673,135.188551452618));
#148189=CARTESIAN_POINT('Ctrl Pts',(60.2885198120085,4.09002569266584,135.082730917641));
#148190=CARTESIAN_POINT('Ctrl Pts',(60.2811197294935,4.20251177961862,134.972286315649));
#148191=CARTESIAN_POINT('Ctrl Pts',(60.2737196469785,4.31034803441242,134.857609978849));
#148192=CARTESIAN_POINT('Ctrl Pts',(60.266311427312,4.4183028662545,134.742807543627));
#148193=CARTESIAN_POINT('Ctrl Pts',(60.2589032076455,4.52159739912048,134.623764352912));
#148194=CARTESIAN_POINT('Ctrl Pts',(60.251494987979,4.61990004008962,134.500906868065));
#148195=CARTESIAN_POINT('Ctrl Pts',(60.2440822086769,4.71826318469429,134.377973766487));
#148196=CARTESIAN_POINT('Ctrl Pts',(60.2366694293748,4.81162809432899,134.251221992685));
#148197=CARTESIAN_POINT('Ctrl Pts',(60.2292566500727,4.89970647562366,134.121107067814));
#148198=CARTESIAN_POINT('Ctrl Pts',(60.2218332790439,4.98791070743961,133.990806228636));
#148199=CARTESIAN_POINT('Ctrl Pts',(60.2144099080152,5.07081312837586,133.857132957271));
#148200=CARTESIAN_POINT('Ctrl Pts',(60.2069865369864,5.14817095334338,133.72056815436));
#148201=CARTESIAN_POINT('Ctrl Pts',(60.2030504875458,5.18918792831466,133.648158219032));
#148202=CARTESIAN_POINT('Ctrl Pts',(60.1991144381052,5.22864691217467,133.574935729605));
#148203=CARTESIAN_POINT('Ctrl Pts',(60.1951783886646,5.26651725082294,133.500974533069));
#148204=CARTESIAN_POINT('Ctrl Pts',(60.1877551222592,5.33793952762424,133.361486024646));
#148205=CARTESIAN_POINT('Ctrl Pts',(60.1803318558537,5.40392425506068,133.218947107479));
#148206=CARTESIAN_POINT('Ctrl Pts',(60.1729085894483,5.46419982971065,133.073821078444));
#148207=CARTESIAN_POINT('Ctrl Pts',(60.1654940967273,5.52440416363705,132.928866576324));
#148208=CARTESIAN_POINT('Ctrl Pts',(60.1580796040063,5.57891263441363,132.781331390186));
#148209=CARTESIAN_POINT('Ctrl Pts',(60.1506651112852,5.62749920276649,132.631703848971));
#148210=CARTESIAN_POINT('Ctrl Pts',(60.1432577649315,5.67603894155552,132.482220524414));
#148211=CARTESIAN_POINT('Ctrl Pts',(60.1358504185777,5.71866802641614,132.330649212279));
#148212=CARTESIAN_POINT('Ctrl Pts',(60.1284430722239,5.75520831037373,132.17749858103));
#148213=CARTESIAN_POINT('Ctrl Pts',(60.1210412505485,5.79172134120881,132.0244621753));
#148214=CARTESIAN_POINT('Ctrl Pts',(60.1136394288732,5.82215452713652,131.86984915739));
#148215=CARTESIAN_POINT('Ctrl Pts',(60.1062376071978,5.84637944819327,131.714183627961));
#148216=CARTESIAN_POINT('Ctrl Pts',(60.0988396928864,5.87059158110293,131.558600273151));
#148217=CARTESIAN_POINT('Ctrl Pts',(60.0914417785751,5.88860191877396,131.401965881276));
#148218=CARTESIAN_POINT('Ctrl Pts',(60.0840438642637,5.90033309010159,131.244814915254));
#148219=CARTESIAN_POINT('Ctrl Pts',(60.0766471793515,5.91206231192133,131.087690064873));
#148220=CARTESIAN_POINT('Ctrl Pts',(60.0692504944393,5.91751441064191,130.93004918262));
#148221=CARTESIAN_POINT('Ctrl Pts',(60.0618538095271,5.91666385181157,130.77243214804));
#148222=CARTESIAN_POINT('Ctrl Pts',(60.0544574525917,5.9158133306959,130.614822102365));
#148223=CARTESIAN_POINT('Ctrl Pts',(60.0470610956562,5.90866070971744,130.457236275552));
#148224=CARTESIAN_POINT('Ctrl Pts',(60.0396647387208,5.89523259336448,130.300214574605));
#148225=CARTESIAN_POINT('Ctrl Pts',(60.0322672493842,5.88180242113266,130.143168833235));
#148226=CARTESIAN_POINT('Ctrl Pts',(60.0248697600477,5.86209487226647,129.986687761667));
#148227=CARTESIAN_POINT('Ctrl Pts',(60.0174722707112,5.83618842412403,129.83130602474));
#148228=CARTESIAN_POINT('Ctrl Pts',(60.0100721881962,5.81027289451631,129.675869818984));
#148229=CARTESIAN_POINT('Ctrl Pts',(60.0026721056812,5.77815420052971,129.521534083123));
#148230=CARTESIAN_POINT('Ctrl Pts',(59.9952720231662,5.73996188034063,129.368823026718));
#148231=CARTESIAN_POINT('Ctrl Pts',(59.9878638034998,5.70172756376917,129.215944048808));
#148232=CARTESIAN_POINT('Ctrl Pts',(59.9804555838333,5.65740637406578,129.064693680482));
#148233=CARTESIAN_POINT('Ctrl Pts',(59.9730473641668,5.60717787117967,128.915581413039));
#148234=CARTESIAN_POINT('Ctrl Pts',(59.9656345848648,5.55691845348793,128.766377369483));
#148235=CARTESIAN_POINT('Ctrl Pts',(59.9582218055627,5.50074461061487,128.619314396953));
#148236=CARTESIAN_POINT('Ctrl Pts',(59.9508090262606,5.43888375579863,128.474881265133));
#148237=CARTESIAN_POINT('Ctrl Pts',(59.9433856552319,5.3769345112923,128.330241760483));
#148238=CARTESIAN_POINT('Ctrl Pts',(59.9359622842031,5.30928218578974,128.188239937507));
#148239=CARTESIAN_POINT('Ctrl Pts',(59.9285389131744,5.23620014334941,128.04933999672));
#148240=CARTESIAN_POINT('Ctrl Pts',(59.9246028637335,5.19745029086743,127.975691915255));
#148241=CARTESIAN_POINT('Ctrl Pts',(59.9206668142927,5.1571746813569,127.902915410499));
#148242=CARTESIAN_POINT('Ctrl Pts',(59.9167307648518,5.11541887509268,127.831076188715));
#148243=CARTESIAN_POINT('Ctrl Pts',(59.9093074984464,5.03666872763349,127.695589658459));
#148244=CARTESIAN_POINT('Ctrl Pts',(59.901884232041,4.95241305665509,127.563029072047));
#148245=CARTESIAN_POINT('Ctrl Pts',(59.8944609656355,4.86289483865671,127.433873360408));
#148246=CARTESIAN_POINT('Ctrl Pts',(59.8870464729145,4.77348242375785,127.304870300094));
#148247=CARTESIAN_POINT('Ctrl Pts',(59.8796319801935,4.67882005314467,127.179264408014));
#148248=CARTESIAN_POINT('Ctrl Pts',(59.8722174874725,4.57919639203602,127.057509811133));
#148249=CARTESIAN_POINT('Ctrl Pts',(59.8648101411187,4.47966875196327,126.935872565918));
#148250=CARTESIAN_POINT('Ctrl Pts',(59.857402794765,4.37518957598218,126.818079512962));
#148251=CARTESIAN_POINT('Ctrl Pts',(59.8499954484113,4.2660905284871,126.704555480093));
#148252=CARTESIAN_POINT('Ctrl Pts',(59.8425936267359,4.15707285117726,126.591116117729));
#148253=CARTESIAN_POINT('Ctrl Pts',(59.8351918050605,4.0434424207067,126.481939703682));
#148254=CARTESIAN_POINT('Ctrl Pts',(59.8277899833851,3.92557076367819,126.377417570513));
#148255=CARTESIAN_POINT('Ctrl Pts',(59.8203920690737,3.80776133017958,126.272950613763));
#148256=CARTESIAN_POINT('Ctrl Pts',(59.8129941547624,3.68571540761689,126.173133291785));
#148257=CARTESIAN_POINT('Ctrl Pts',(59.805596240451,3.5598408338089,126.078319589343));
#148258=CARTESIAN_POINT('Ctrl Pts',(59.7981995555388,3.43398717807202,125.983521643218));
#148259=CARTESIAN_POINT('Ctrl Pts',(59.7908028706266,3.30430643174462,125.893725890703));
#148260=CARTESIAN_POINT('Ctrl Pts',(59.7834061857144,3.17123900878252,125.809245632736));
#148261=CARTESIAN_POINT('Ctrl Pts',(59.7760098287789,3.03817748616901,125.724769120711));
#148262=CARTESIAN_POINT('Ctrl Pts',(59.7686134718435,2.90172990065716,125.645607834673));
#148263=CARTESIAN_POINT('Ctrl Pts',(59.761217114908,2.76236487167567,125.572031224434));
#148264=CARTESIAN_POINT('Ctrl Pts',(59.7538196255715,2.62297850555287,125.498443349429));
#148265=CARTESIAN_POINT('Ctrl Pts',(59.7464221362348,2.4806741367228,125.430442026992));
#148266=CARTESIAN_POINT('Ctrl Pts',(59.7390246468983,2.33594401278453,125.368250231303));
#148267=CARTESIAN_POINT('Ctrl Pts',(59.7316245643832,2.19116315392443,125.306036634376));
#148268=CARTESIAN_POINT('Ctrl Pts',(59.7242244818682,2.04395518968559,125.249636766183));
#148269=CARTESIAN_POINT('Ctrl Pts',(59.7168243993532,1.89483117096766,125.199224990658));
#148270=CARTESIAN_POINT('Ctrl Pts',(59.7094161796867,1.74554317506188,125.148757782205));
#148271=CARTESIAN_POINT('Ctrl Pts',(59.7020079600203,1.59433527091627,125.104291935768));
#148272=CARTESIAN_POINT('Ctrl Pts',(59.6945997403538,1.44173316452865,125.065951774969));
#148273=CARTESIAN_POINT('Ctrl Pts',(59.6871869610517,1.28903713409041,125.02758801644));
#148274=CARTESIAN_POINT('Ctrl Pts',(59.6797741817496,1.13494555606537,124.99535753251));
#148275=CARTESIAN_POINT('Ctrl Pts',(59.6723614024475,0.979992568643787,
124.969333185934));
#148276=CARTESIAN_POINT('Ctrl Pts',(59.6649380314188,0.824818177127207,
124.943271654551));
#148277=CARTESIAN_POINT('Ctrl Pts',(59.6575146603901,0.668780287322377,
124.923434018103));
#148278=CARTESIAN_POINT('Ctrl Pts',(59.6500912893613,0.512417204220075,
124.909841199384));
#148279=CARTESIAN_POINT('Ctrl Pts',(59.6461552399205,0.429509745678901,
124.902633960745));
#148280=CARTESIAN_POINT('Ctrl Pts',(59.6422191904797,0.346510860363946,
124.897181493204));
#148281=CARTESIAN_POINT('Ctrl Pts',(59.6382831410389,0.263500455258547,
124.893480981456));
#148282=CARTESIAN_POINT('Ctrl Pts',(59.6308598746335,0.106945421894931,
124.886501931788));
#148283=CARTESIAN_POINT('Ctrl Pts',(59.623436608228,-0.0501238019878781,
124.885736379098));
#148284=CARTESIAN_POINT('Ctrl Pts',(59.6160133418226,-0.207172943502528,
124.891238774243));
#148285=CARTESIAN_POINT('Ctrl Pts',(59.6085988491015,-0.364036465974028,
124.896734666014));
#148286=CARTESIAN_POINT('Ctrl Pts',(59.6011843563805,-0.520879583897477,
124.908483746625));
#148287=CARTESIAN_POINT('Ctrl Pts',(59.5937698636595,-0.677164196795334,
124.926488620569));
#148288=CARTESIAN_POINT('Ctrl Pts',(59.5863625173057,-0.833298176699715,
124.944476140738));
#148289=CARTESIAN_POINT('Ctrl Pts',(59.5789551709519,-0.988874354888629,
124.968707408117));
#148290=CARTESIAN_POINT('Ctrl Pts',(59.5715478245981,-1.14335603897445,
124.999133013876));
#148291=CARTESIAN_POINT('Ctrl Pts',(59.5641460029227,-1.29772250479158,
125.02953592707));
#148292=CARTESIAN_POINT('Ctrl Pts',(59.5567441812472,-1.45099573721353,
125.066123907832));
#148293=CARTESIAN_POINT('Ctrl Pts',(59.5493423595718,-1.60264567786908,
125.108795905116));
#148294=CARTESIAN_POINT('Ctrl Pts',(59.5419444452604,-1.75421556370291,
125.151445376185));
#148295=CARTESIAN_POINT('Ctrl Pts',(59.5345465309489,-1.90416350594036,
125.200172366655));
#148296=CARTESIAN_POINT('Ctrl Pts',(59.5271486166375,-2.05197124087056,
125.25482508843));
#148297=CARTESIAN_POINT('Ctrl Pts',(59.5197519317252,-2.19975441283546,
125.309468727914));
#148298=CARTESIAN_POINT('Ctrl Pts',(59.5123552468131,-2.34539773359331,
125.370036014932));
#148299=CARTESIAN_POINT('Ctrl Pts',(59.5049585619008,-2.48839955969069,
125.436325763559));
#148300=CARTESIAN_POINT('Ctrl Pts',(59.4975622049654,-2.63139504493705,
125.50261257283));
#148301=CARTESIAN_POINT('Ctrl Pts',(59.4901658480299,-2.77174892973205,
125.574621182192));
#148302=CARTESIAN_POINT('Ctrl Pts',(59.4827694910944,-2.90898121806823,
125.652102973055));
#148303=CARTESIAN_POINT('Ctrl Pts',(59.4753720017579,-3.04623451701808,
125.729596626577));
#148304=CARTESIAN_POINT('Ctrl Pts',(59.4679745124212,-3.18036494281243,
125.812564946542));
#148305=CARTESIAN_POINT('Ctrl Pts',(59.4605770230846,-3.31091882910719,
125.900714314093));
#148306=CARTESIAN_POINT('Ctrl Pts',(59.4531769405696,-3.44151848086477,
125.988894582269));
#148307=CARTESIAN_POINT('Ctrl Pts',(59.4457768580546,-3.56853878772847,
126.082259305327));
#148308=CARTESIAN_POINT('Ctrl Pts',(59.4383767755396,-3.69155681688597,
126.180472769639));
#148309=CARTESIAN_POINT('Ctrl Pts',(59.4309685558731,-3.81471011701257,
126.278794229752));
#148310=CARTESIAN_POINT('Ctrl Pts',(59.4235603362066,-3.93385205860722,
126.381974845803));
#148311=CARTESIAN_POINT('Ctrl Pts',(59.4161521165401,-4.04859388775333,
126.489639526401));
#148312=CARTESIAN_POINT('Ctrl Pts',(59.408739337238,-4.1634063385812,126.597370472814));
#148313=CARTESIAN_POINT('Ctrl Pts',(59.401326557936,-4.27381301934535,126.709590717669));
#148314=CARTESIAN_POINT('Ctrl Pts',(59.3939137786339,-4.37946391380618,
126.82589025948));
#148315=CARTESIAN_POINT('Ctrl Pts',(59.3864904076051,-4.48526576721925,
126.942355975529));
#148316=CARTESIAN_POINT('Ctrl Pts',(59.3790670365763,-4.58629802346991,
127.062912344384));
#148317=CARTESIAN_POINT('Ctrl Pts',(59.3716436655476,-4.68225211262389,
127.187117784091));
#148318=CARTESIAN_POINT('Ctrl Pts',(59.367707616107,-4.73312927307716,127.252974488488));
#148319=CARTESIAN_POINT('Ctrl Pts',(59.3637715666664,-4.78257951331099,
127.319856609461));
#148320=CARTESIAN_POINT('Ctrl Pts',(59.3598355172259,-4.83056201024757,
127.387695397259));
#148321=CARTESIAN_POINT('Ctrl Pts',(59.3523342649679,-4.92200619023678,
127.516981339379));
#148322=CARTESIAN_POINT('Ctrl Pts',(59.3448330127099,-5.00839086364624,
127.650130842641));
#148323=CARTESIAN_POINT('Ctrl Pts',(59.3373317604519,-5.08937601999078,
127.786715461216));
#148324=CARTESIAN_POINT('Ctrl Pts',(59.3298397696976,-5.17026118711969,
127.923131444087));
#148325=CARTESIAN_POINT('Ctrl Pts',(59.3223477789434,-5.24575992574497,
128.062973789982));
#148326=CARTESIAN_POINT('Ctrl Pts',(59.3148557881892,-5.31557370710274,
128.205782789819));
#148327=CARTESIAN_POINT('Ctrl Pts',(59.307371674703,-5.38531408448924,128.34844163667));
#148328=CARTESIAN_POINT('Ctrl Pts',(59.2998875612169,-5.44938124783879,
128.49406060307));
#148329=CARTESIAN_POINT('Ctrl Pts',(59.2924034477308,-5.50752108409904,
128.642152933114));
#148330=CARTESIAN_POINT('Ctrl Pts',(59.2849258324734,-5.5656104393027,128.790116679079));
#148331=CARTESIAN_POINT('Ctrl Pts',(59.2774482172161,-5.61778258458526,
128.940549175663));
#148332=CARTESIAN_POINT('Ctrl Pts',(59.2699706019587,-5.6638303154753,129.092941113177));
#148333=CARTESIAN_POINT('Ctrl Pts',(59.262498739361,-5.70984262104381,129.245215812919));
#148334=CARTESIAN_POINT('Ctrl Pts',(59.2550268767634,-5.74973979688954,
129.399446603185));
#148335=CARTESIAN_POINT('Ctrl Pts',(59.2475550141657,-5.7833636108455,129.555106477189));
#148336=CARTESIAN_POINT('Ctrl Pts',(59.2400865491107,-5.81697213566247,
129.71069557084));
#148337=CARTESIAN_POINT('Ctrl Pts',(59.2326180840558,-5.84431290373922,
129.867712099814));
#148338=CARTESIAN_POINT('Ctrl Pts',(59.2251496190009,-5.86527812398675,
130.02561605689));
#148339=CARTESIAN_POINT('Ctrl Pts',(59.2176826651325,-5.88623910208314,
130.183488063315));
#148340=CARTESIAN_POINT('Ctrl Pts',(59.210215711264,-5.90082705133702,130.342246780994));
#148341=CARTESIAN_POINT('Ctrl Pts',(59.2027487573956,-5.90898566277173,
130.501344116929));
#148342=CARTESIAN_POINT('Ctrl Pts',(59.1979575690009,-5.91422065485974,
130.603429294231));
#148343=CARTESIAN_POINT('Ctrl Pts',(59.1931663806062,-5.91680961849877,
130.705653731667));
#148344=CARTESIAN_POINT('Ctrl Pts',(59.1883751922115,-5.91674895814525,
130.807871854834));
#148345=CARTESIAN_POINT('',(57.4383766205357,-5.92091818089423,130.807703535762));
#148346=CARTESIAN_POINT('Ctrl Pts',(59.1883731089969,-5.90904905956648,
130.807911672142));
#148347=CARTESIAN_POINT('Ctrl Pts',(59.152711370469,-5.91313005239658,131.56775334573));
#148348=CARTESIAN_POINT('Ctrl Pts',(59.0242337573369,-5.42355709184765,
134.300145737045));
#148349=CARTESIAN_POINT('Ctrl Pts',(58.8029402696001,-1.30063251087169,
137.680836139373));
#148350=CARTESIAN_POINT('Ctrl Pts',(58.5244926457873,5.08234996656148,135.615522571577));
#148351=CARTESIAN_POINT('Ctrl Pts',(58.2460450219744,6.79490111132396,129.128986206374));
#148352=CARTESIAN_POINT('Ctrl Pts',(57.9675973981615,2.26327008415277,124.182037078465));
#148353=CARTESIAN_POINT('Ctrl Pts',(57.6983749653315,-4.12915247357771,
125.282955627744));
#148354=CARTESIAN_POINT('Ctrl Pts',(57.521968407106,-5.91208800052518,129.038205754648));
#148355=CARTESIAN_POINT('Ctrl Pts',(57.4383777234847,-5.92413758308925,
130.807682022349));
#148356=CARTESIAN_POINT('',(55.688374326571,-5.91864047034299,130.799239860638));
#148357=CARTESIAN_POINT('Ctrl Pts',(57.4383751922116,-5.91674903983214,
130.807731395733));
#148358=CARTESIAN_POINT('Ctrl Pts',(57.4291508449863,-5.91663793686835,
131.002751157247));
#148359=CARTESIAN_POINT('Ctrl Pts',(57.419926497761,-5.90688570138042,131.19749249288));
#148360=CARTESIAN_POINT('Ctrl Pts',(57.4107021505358,-5.88756945797795,
131.39126473238));
#148361=CARTESIAN_POINT('Ctrl Pts',(57.4032788841304,-5.87202476768945,
131.547202374434));
#148362=CARTESIAN_POINT('Ctrl Pts',(57.3958556177249,-5.85025706712759,
131.702757812701));
#148363=CARTESIAN_POINT('Ctrl Pts',(57.3884323513195,-5.82228908849752,
131.857394488086));
#148364=CARTESIAN_POINT('Ctrl Pts',(57.3810178585985,-5.79435416569555,
132.011848395763));
#148365=CARTESIAN_POINT('Ctrl Pts',(57.3736033658774,-5.76023361746424,
132.1653853383));
#148366=CARTESIAN_POINT('Ctrl Pts',(57.3661888731564,-5.72000203536849,
132.317472403879));
#148367=CARTESIAN_POINT('Ctrl Pts',(57.3587815268026,-5.67980922998637,
132.469412882218));
#148368=CARTESIAN_POINT('Ctrl Pts',(57.3513741804489,-5.63351721148281,
132.619905907178));
#148369=CARTESIAN_POINT('Ctrl Pts',(57.3439668340951,-5.58125184516721,
132.768427419719));
#148370=CARTESIAN_POINT('Ctrl Pts',(57.3365650124197,-5.52902546033351,
132.916838159313));
#148371=CARTESIAN_POINT('Ctrl Pts',(57.3291631907442,-5.47083472187195,
133.063279963694));
#148372=CARTESIAN_POINT('Ctrl Pts',(57.3217613690688,-5.40685565210983,
133.207242745293));
#148373=CARTESIAN_POINT('Ctrl Pts',(57.3143634547574,-5.3429103564008,133.351129530059));
#148374=CARTESIAN_POINT('Ctrl Pts',(57.3069655404461,-5.2731829660132,133.492539558029));
#148375=CARTESIAN_POINT('Ctrl Pts',(57.2995676261347,-5.19789802439756,
133.63098169059));
#148376=CARTESIAN_POINT('Ctrl Pts',(57.2921709412225,-5.1226255937733,133.76940081658));
#148377=CARTESIAN_POINT('Ctrl Pts',(57.2847742563103,-5.04179762308435,
133.904852698414));
#148378=CARTESIAN_POINT('Ctrl Pts',(57.2773775713981,-4.95568515948476,
134.036869730092));
#148379=CARTESIAN_POINT('Ctrl Pts',(57.2699812144626,-4.86957651420206,
134.168880907996));
#148380=CARTESIAN_POINT('Ctrl Pts',(57.2625848575272,-4.7781840458603,134.297457225916));
#148381=CARTESIAN_POINT('Ctrl Pts',(57.2551885005917,-4.68182263951849,
134.422159303866));
#148382=CARTESIAN_POINT('Ctrl Pts',(57.2477910112551,-4.58544647999936,
134.546880474022));
#148383=CARTESIAN_POINT('Ctrl Pts',(57.2403935219185,-4.48410009597941,
134.667725927754));
#148384=CARTESIAN_POINT('Ctrl Pts',(57.232996032582,-4.37813913168417,134.784288796078));
#148385=CARTESIAN_POINT('Ctrl Pts',(57.2255959500669,-4.27214102293702,
134.900892525335));
#148386=CARTESIAN_POINT('Ctrl Pts',(57.218195867552,-4.16152536416108,135.013210404148));
#148387=CARTESIAN_POINT('Ctrl Pts',(57.2107957850369,-4.04668505173136,
135.120872016207));
#148388=CARTESIAN_POINT('Ctrl Pts',(57.2033875653705,-3.93171846057242,
135.228652013275));
#148389=CARTESIAN_POINT('Ctrl Pts',(57.1959793457039,-3.81251821101225,
135.331765263056));
#148390=CARTESIAN_POINT('Ctrl Pts',(57.1885711260375,-3.68951126854774,
135.429880822014));
#148391=CARTESIAN_POINT('Ctrl Pts',(57.1811583467354,-3.56642861736263,
135.528056769462));
#148392=CARTESIAN_POINT('Ctrl Pts',(57.1737455674333,-3.43953490483952,
135.621228676359));
#148393=CARTESIAN_POINT('Ctrl Pts',(57.1663327881313,-3.30928609033689,
135.709108942893));
#148394=CARTESIAN_POINT('Ctrl Pts',(57.1589094171025,-3.17885117022004,
135.797114776874));
#148395=CARTESIAN_POINT('Ctrl Pts',(57.1514860460737,-3.04505189027421,
135.879813673847));
#148396=CARTESIAN_POINT('Ctrl Pts',(57.144062675045,-2.90836952006152,135.956963580853));
#148397=CARTESIAN_POINT('Ctrl Pts',(57.1401266256043,-2.83589724772816,
135.997870312733));
#148398=CARTESIAN_POINT('Ctrl Pts',(57.1361905761636,-2.76261479323338,
136.037217818737));
#148399=CARTESIAN_POINT('Ctrl Pts',(57.1322545267229,-2.68859605013294,
136.074975557183));
#148400=CARTESIAN_POINT('Ctrl Pts',(57.1248312603175,-2.5489990106882,136.146185473513));
#148401=CARTESIAN_POINT('Ctrl Pts',(57.117407993912,-2.40635984105677,136.211953204573));
#148402=CARTESIAN_POINT('Ctrl Pts',(57.1099847275066,-2.26114225091217,
136.272007852313));
#148403=CARTESIAN_POINT('Ctrl Pts',(57.1025702347856,-2.11609629589936,
136.331991520447));
#148404=CARTESIAN_POINT('Ctrl Pts',(57.0951557420646,-1.96847832799159,
136.386275404666));
#148405=CARTESIAN_POINT('Ctrl Pts',(57.0877412493436,-1.81877701955703,
136.434634209109));
#148406=CARTESIAN_POINT('Ctrl Pts',(57.0803339029898,-1.66921999887947,
136.482946403517));
#148407=CARTESIAN_POINT('Ctrl Pts',(57.0729265566361,-1.51758398805077,
136.525344773279));
#148408=CARTESIAN_POINT('Ctrl Pts',(57.0655192102823,-1.364377926056,136.561651945733));
#148409=CARTESIAN_POINT('Ctrl Pts',(57.0581173886069,-1.21128613092261,
136.597932038929));
#148410=CARTESIAN_POINT('Ctrl Pts',(57.0507155669315,-1.05662697792297,
136.628129894922));
#148411=CARTESIAN_POINT('Ctrl Pts',(57.0433137452561,-0.90092476254508,
136.65211789149));
#148412=CARTESIAN_POINT('Ctrl Pts',(57.0359158309448,-0.745304741154928,
136.676093224981));
#148413=CARTESIAN_POINT('Ctrl Pts',(57.0285179166334,-0.588643121992735,
136.693865170916));
#148414=CARTESIAN_POINT('Ctrl Pts',(57.021120002322,-0.431474485104551,
136.705357171641));
#148415=CARTESIAN_POINT('Ctrl Pts',(57.0137233174098,-0.274331966792264,
136.716847262604));
#148416=CARTESIAN_POINT('Ctrl Pts',(57.0063266324977,-0.116682969918951,
136.722059452423));
#148417=CARTESIAN_POINT('Ctrl Pts',(56.9989299475855,0.0409325877373028,
136.720969028282));
#148418=CARTESIAN_POINT('Ctrl Pts',(56.99153359065,0.198541156554561,136.719878652492));
#148419=CARTESIAN_POINT('Ctrl Pts',(56.9841372337145,0.356115915814296,
136.712486220994));
#148420=CARTESIAN_POINT('Ctrl Pts',(56.9767408767791,0.513116999625759,
136.698819159892));
#148421=CARTESIAN_POINT('Ctrl Pts',(56.9693433874425,0.670142120704182,
136.685150006327));
#148422=CARTESIAN_POINT('Ctrl Pts',(56.961945898106,0.826593019535393,136.665204342729));
#148423=CARTESIAN_POINT('Ctrl Pts',(56.9545484087694,0.981935151330484,
136.639061460033));
#148424=CARTESIAN_POINT('Ctrl Pts',(56.9471483262544,1.13733173806884,136.61290941299));
#148425=CARTESIAN_POINT('Ctrl Pts',(56.9397482437394,1.29161841602725,136.580555883478));
#148426=CARTESIAN_POINT('Ctrl Pts',(56.9323481612244,1.44427117338549,136.542131207284));
#148427=CARTESIAN_POINT('Ctrl Pts',(56.924939941558,1.59709178814353,136.503664279207));
#148428=CARTESIAN_POINT('Ctrl Pts',(56.9175317218915,1.74827453201818,136.459112963514));
#148429=CARTESIAN_POINT('Ctrl Pts',(56.910123502225,1.89731018756023,136.408657595304));
#148430=CARTESIAN_POINT('Ctrl Pts',(56.902710722923,2.04643757206169,136.358171172656));
#148431=CARTESIAN_POINT('Ctrl Pts',(56.8952979436209,2.19341488726924,136.301773590022));
#148432=CARTESIAN_POINT('Ctrl Pts',(56.8878851643188,2.33775371014633,136.2396930042));
#148433=CARTESIAN_POINT('Ctrl Pts',(56.8804617932901,2.48229877110237,136.177523714726));
#148434=CARTESIAN_POINT('Ctrl Pts',(56.8730384222613,2.62419747431995,136.109655364962));
#148435=CARTESIAN_POINT('Ctrl Pts',(56.8656150512325,2.76298603583541,136.036362025085));
#148436=CARTESIAN_POINT('Ctrl Pts',(56.8616790017917,2.83657506133772,135.997500137632));
#148437=CARTESIAN_POINT('Ctrl Pts',(56.8577429523508,2.90929018919875,135.957113821308));
#148438=CARTESIAN_POINT('Ctrl Pts',(56.85380690291,2.98106578256428,135.91524873633));
#148439=CARTESIAN_POINT('Ctrl Pts',(56.8463836365046,3.11643231161008,135.836292492627));
#148440=CARTESIAN_POINT('Ctrl Pts',(56.8389603700992,3.24886452173071,135.751835184569));
#148441=CARTESIAN_POINT('Ctrl Pts',(56.8315371036937,3.37788385232074,135.662120517225));
#148442=CARTESIAN_POINT('Ctrl Pts',(56.8241226109727,3.50675069277659,135.572511885166));
#148443=CARTESIAN_POINT('Ctrl Pts',(56.8167081182517,3.63221237939239,135.477658473385));
#148444=CARTESIAN_POINT('Ctrl Pts',(56.8092936255307,3.7538152250301,135.377849637869));
#148445=CARTESIAN_POINT('Ctrl Pts',(56.801886279177,3.87530086526675,135.278137001867));
#148446=CARTESIAN_POINT('Ctrl Pts',(56.7944789328232,3.99293478229969,135.173478685896));
#148447=CARTESIAN_POINT('Ctrl Pts',(56.7870715864694,4.1062926535324,135.064207000482));
#148448=CARTESIAN_POINT('Ctrl Pts',(56.779669764794,4.21956597818814,134.955016814015));
#148449=CARTESIAN_POINT('Ctrl Pts',(56.7722679431187,4.32856933963917,134.841220367209));
#148450=CARTESIAN_POINT('Ctrl Pts',(56.7648661214433,4.432911971177,134.72318978178));
#148451=CARTESIAN_POINT('Ctrl Pts',(56.7574682071319,4.53719952105183,134.605221503779));
#148452=CARTESIAN_POINT('Ctrl Pts',(56.7500702928206,4.63683099432456,134.483023817571));
#148453=CARTESIAN_POINT('Ctrl Pts',(56.7426723785092,4.73145302730025,134.357005099209));
#148454=CARTESIAN_POINT('Ctrl Pts',(56.735275693597,4.82605933581067,134.231007322872));
#148455=CARTESIAN_POINT('Ctrl Pts',(56.7278790086848,4.91565763232375,134.101190072864));
#148456=CARTESIAN_POINT('Ctrl Pts',(56.7204823237726,4.99993528649898,133.96799423942));
#148457=CARTESIAN_POINT('Ctrl Pts',(56.7130859668372,5.0842092037147,133.834804312018));
#148458=CARTESIAN_POINT('Ctrl Pts',(56.7056896099017,5.16316274808802,133.698236414509));
#148459=CARTESIAN_POINT('Ctrl Pts',(56.6982932529663,5.23652718327612,133.558759575834));
#148460=CARTESIAN_POINT('Ctrl Pts',(56.6908957636297,5.30990285074653,133.4192613829));
#148461=CARTESIAN_POINT('Ctrl Pts',(56.6834982742931,5.37768753141459,133.276853692419));
#148462=CARTESIAN_POINT('Ctrl Pts',(56.6761007849565,5.43965900047506,133.132029090749));
#148463=CARTESIAN_POINT('Ctrl Pts',(56.6687007024415,5.50165219353794,132.98715372104));
#148464=CARTESIAN_POINT('Ctrl Pts',(56.6613006199266,5.55782797095889,132.839860096268));
#148465=CARTESIAN_POINT('Ctrl Pts',(56.6539005374116,5.60801274673584,132.690659532094));
#148466=CARTESIAN_POINT('Ctrl Pts',(56.6464923177451,5.65825270583287,132.541294906561));
#148467=CARTESIAN_POINT('Ctrl Pts',(56.6390840980787,5.70248838808931,132.390019508063));
#148468=CARTESIAN_POINT('Ctrl Pts',(56.6316758784122,5.74059627006279,132.237359231188));
#148469=CARTESIAN_POINT('Ctrl Pts',(56.6242630991101,5.77872760680182,132.084604994459));
#148470=CARTESIAN_POINT('Ctrl Pts',(56.616850319808,5.81072355225942,131.93046454556));
#148471=CARTESIAN_POINT('Ctrl Pts',(56.609437540506,5.83651205663076,131.775472132946));
#148472=CARTESIAN_POINT('Ctrl Pts',(56.6020141694772,5.86233740882646,131.620258259905));
#148473=CARTESIAN_POINT('Ctrl Pts',(56.5945907984485,5.88193755919618,131.464190361284));
#148474=CARTESIAN_POINT('Ctrl Pts',(56.5871674274198,5.8952924041802,131.307806773292));
#148475=CARTESIAN_POINT('Ctrl Pts',(56.5832313779789,5.90237346343602,131.224888442564));
#148476=CARTESIAN_POINT('Ctrl Pts',(56.579295328538,5.90769961448785,131.14188135563));
#148477=CARTESIAN_POINT('Ctrl Pts',(56.5753592790971,5.91127379424545,131.058865415098));
#148478=CARTESIAN_POINT('Ctrl Pts',(56.5679360126917,5.9180145857218,130.902299942097));
#148479=CARTESIAN_POINT('Ctrl Pts',(56.5605127462863,5.91854110490386,130.745229735058));
#148480=CARTESIAN_POINT('Ctrl Pts',(56.5530894798808,5.91279971407171,130.588189149112));
#148481=CARTESIAN_POINT('Ctrl Pts',(56.5456749871598,5.90706510908673,130.431334172098));
#148482=CARTESIAN_POINT('Ctrl Pts',(56.5382604944388,5.89507735355469,130.274509115897));
#148483=CARTESIAN_POINT('Ctrl Pts',(56.5308460017177,5.87683466188365,130.118252084327));
#148484=CARTESIAN_POINT('Ctrl Pts',(56.523438655364,5.85860955320567,129.962145659168));
#148485=CARTESIAN_POINT('Ctrl Pts',(56.5160313090102,5.83414155342617,129.806606536998));
#148486=CARTESIAN_POINT('Ctrl Pts',(56.5086239626564,5.80348088807406,129.652171334393));
#148487=CARTESIAN_POINT('Ctrl Pts',(56.501222140981,5.77284309060293,129.497851315388));
#148488=CARTESIAN_POINT('Ctrl Pts',(56.4938203193056,5.73602189644192,129.344633941132));
#148489=CARTESIAN_POINT('Ctrl Pts',(56.4864184976302,5.69311916317717,129.193049115601));
#148490=CARTESIAN_POINT('Ctrl Pts',(56.4790205833188,5.65023907793129,129.041544310519));
#148491=CARTESIAN_POINT('Ctrl Pts',(56.4716226690074,5.60128394864446,128.891670696105));
#148492=CARTESIAN_POINT('Ctrl Pts',(56.4642247546961,5.54640635194575,128.743946304474));
#148493=CARTESIAN_POINT('Ctrl Pts',(56.4568280697838,5.49153787490811,128.596246461957));
#148494=CARTESIAN_POINT('Ctrl Pts',(56.4494313848717,5.4307490136853,128.450695482952));
#148495=CARTESIAN_POINT('Ctrl Pts',(56.4420346999594,5.3642417173845,128.307794704162));
#148496=CARTESIAN_POINT('Ctrl Pts',(56.434638343024,5.29773737008691,128.164900261742));
#148497=CARTESIAN_POINT('Ctrl Pts',(56.4272419860885,5.22551524938953,128.02465612432));
#148498=CARTESIAN_POINT('Ctrl Pts',(56.4198456291531,5.14782470406803,127.887541908992));
#148499=CARTESIAN_POINT('Ctrl Pts',(56.4124481398165,5.0701222641257,127.750406701128));
#148500=CARTESIAN_POINT('Ctrl Pts',(56.4050506504799,4.98694991656233,127.616402694314));
#148501=CARTESIAN_POINT('Ctrl Pts',(56.3976531611433,4.89860197029609,127.48598310753));
#148502=CARTESIAN_POINT('Ctrl Pts',(56.3902530786283,4.81022305379425,127.355517802362));
#148503=CARTESIAN_POINT('Ctrl Pts',(56.3828529961133,4.71666513556686,127.228639727802));
#148504=CARTESIAN_POINT('Ctrl Pts',(56.3754529135983,4.61826457248577,127.105771305271));
#148505=CARTESIAN_POINT('Ctrl Pts',(56.3680446939318,4.51975580786975,126.982767776279));
#148506=CARTESIAN_POINT('Ctrl Pts',(56.3606364742654,4.41639399754719,126.863782995981));
#148507=CARTESIAN_POINT('Ctrl Pts',(56.3532282545989,4.30855482409166,126.74920514702));
#148508=CARTESIAN_POINT('Ctrl Pts',(56.3458154752968,4.20064927742411,126.634556777305));
#148509=CARTESIAN_POINT('Ctrl Pts',(56.3384026959947,4.08826114234471,126.524321004499));
#148510=CARTESIAN_POINT('Ctrl Pts',(56.3309899166927,3.97180095253115,126.418847220485));
#148511=CARTESIAN_POINT('Ctrl Pts',(56.3235665456639,3.85517435893695,126.313222730583));
#148512=CARTESIAN_POINT('Ctrl Pts',(56.3161431746351,3.73446437578927,126.212374057597));
#148513=CARTESIAN_POINT('Ctrl Pts',(56.3087198036064,3.61011305412161,126.116609099091));
#148514=CARTESIAN_POINT('Ctrl Pts',(56.3047837541656,3.54417899960593,126.065832220244));
#148515=CARTESIAN_POINT('Ctrl Pts',(56.3008477047249,3.47722170123107,126.016483820474));
#148516=CARTESIAN_POINT('Ctrl Pts',(56.2969116552842,3.40930997079423,125.968604618186));
#148517=CARTESIAN_POINT('Ctrl Pts',(56.2894883888788,3.28123056664013,125.878305936926));
#148518=CARTESIAN_POINT('Ctrl Pts',(56.2820651224733,3.14936754947702,125.792962677869));
#148519=CARTESIAN_POINT('Ctrl Pts',(56.2746418560679,3.01414149491475,125.712908799947));
#148520=CARTESIAN_POINT('Ctrl Pts',(56.2672273633469,2.87907526631916,125.632949539062));
#148521=CARTESIAN_POINT('Ctrl Pts',(56.2598128706259,2.74065423033887,125.55826740376));
#148522=CARTESIAN_POINT('Ctrl Pts',(56.2523983779049,2.59933014379981,125.489154754569));
#148523=CARTESIAN_POINT('Ctrl Pts',(56.2449910315511,2.45814227073612,125.420108718752));
#148524=CARTESIAN_POINT('Ctrl Pts',(56.2375836851973,2.31405725061324,125.356621645149));
#148525=CARTESIAN_POINT('Ctrl Pts',(56.2301763388435,2.16755370227811,125.298941331967));
#148526=CARTESIAN_POINT('Ctrl Pts',(56.2227745171681,2.02115942181659,125.241304038939));
#148527=CARTESIAN_POINT('Ctrl Pts',(56.2153726954928,1.87235055066234,125.18946501909));
#148528=CARTESIAN_POINT('Ctrl Pts',(56.2079708738174,1.72162796855045,125.143625002789));
#148529=CARTESIAN_POINT('Ctrl Pts',(56.2005729595061,1.57098495171644,125.097809185076));
#148530=CARTESIAN_POINT('Ctrl Pts',(56.1931750451947,1.41843059209391,125.057986172369));
#148531=CARTESIAN_POINT('Ctrl Pts',(56.1857771308833,1.26448319616759,125.02430760664));
#148532=CARTESIAN_POINT('Ctrl Pts',(56.1783804459711,1.11056138350559,124.990634637679));
#148533=CARTESIAN_POINT('Ctrl Pts',(56.1709837610589,0.95524735830994,124.963104168823));
#148534=CARTESIAN_POINT('Ctrl Pts',(56.1635870761467,0.799072067771759,
124.941817279303));
#148535=CARTESIAN_POINT('Ctrl Pts',(56.1561907192113,0.642903702209399,
124.920531333667));
#148536=CARTESIAN_POINT('Ctrl Pts',(56.1487943622758,0.485874517115526,
124.905488467316));
#148537=CARTESIAN_POINT('Ctrl Pts',(56.1413980053404,0.32852280704081,124.89673814082));
#148538=CARTESIAN_POINT('Ctrl Pts',(56.1340005160038,0.171147006017805,
124.887986474627));
#148539=CARTESIAN_POINT('Ctrl Pts',(56.1266030266673,0.0134489544389833,
124.885529287282));
#148540=CARTESIAN_POINT('Ctrl Pts',(56.1192055373307,-0.14403096057209,
124.889363944287));
#148541=CARTESIAN_POINT('Ctrl Pts',(56.1118054548157,-0.301566079923245,
124.893199945526));
#148542=CARTESIAN_POINT('Ctrl Pts',(56.1044053723007,-0.458882537506066,
124.903332173359));
#148543=CARTESIAN_POINT('Ctrl Pts',(56.0970052897857,-0.615443129108086,
124.919705970322));
#148544=CARTESIAN_POINT('Ctrl Pts',(56.0895970701192,-0.772175875175615,
124.936097771958));
#148545=CARTESIAN_POINT('Ctrl Pts',(56.0821888504527,-0.92815072389576,
124.958744810225));
#148546=CARTESIAN_POINT('Ctrl Pts',(56.0747806307862,-1.08283802061103,
124.987540834934));
#148547=CARTESIAN_POINT('Ctrl Pts',(56.0673678514841,-1.23762052477633,
125.016354583116));
#148548=CARTESIAN_POINT('Ctrl Pts',(56.0599550721821,-1.39111353472003,
125.051324776295));
#148549=CARTESIAN_POINT('Ctrl Pts',(56.05254229288,-1.542801193676,125.092294875709));
#148550=CARTESIAN_POINT('Ctrl Pts',(56.0451189218513,-1.69470559107253,
125.133323515123));
#148551=CARTESIAN_POINT('Ctrl Pts',(56.0376955508226,-1.84479913023503,
125.180369071514));
#148552=CARTESIAN_POINT('Ctrl Pts',(56.0302721797938,-1.99258382884118,
125.233226060984));
#148553=CARTESIAN_POINT('Ctrl Pts',(56.026336130353,-2.07094282208795,125.261252105087));
#148554=CARTESIAN_POINT('Ctrl Pts',(56.0224000809121,-2.14865308373086,
125.290911161063));
#148555=CARTESIAN_POINT('Ctrl Pts',(56.0184640314713,-2.22564316176527,
125.322167344889));
#148556=CARTESIAN_POINT('Ctrl Pts',(56.0110407650659,-2.37084404615895,
125.381115532112));
#148557=CARTESIAN_POINT('Ctrl Pts',(56.0036174986605,-2.51392092876084,
125.445925506861));
#148558=CARTESIAN_POINT('Ctrl Pts',(55.996194232255,-2.65436550907055,125.516423939924));
#148559=CARTESIAN_POINT('Ctrl Pts',(55.988779739534,-2.79464409554954,125.586839049693));
#148560=CARTESIAN_POINT('Ctrl Pts',(55.981365246813,-2.93229624215579,125.662929069208));
#148561=CARTESIAN_POINT('Ctrl Pts',(55.973950754092,-3.06683179209899,125.744471950661));
#148562=CARTESIAN_POINT('Ctrl Pts',(55.9665434077382,-3.20123767161417,
125.825936238016));
#148563=CARTESIAN_POINT('Ctrl Pts',(55.9591360613844,-3.33253261753232,
125.912842732105));
#148564=CARTESIAN_POINT('Ctrl Pts',(55.9517287150307,-3.46024944502699,
126.004922698321));
#148565=CARTESIAN_POINT('Ctrl Pts',(55.9443268933553,-3.58787101649304,
126.096933987824));
#148566=CARTESIAN_POINT('Ctrl Pts',(55.9369250716799,-3.7119194817674,126.194110849145));
#148567=CARTESIAN_POINT('Ctrl Pts',(55.9295232500045,-3.8319552229732,126.296140377646));
#148568=CARTESIAN_POINT('Ctrl Pts',(55.9221253356931,-3.95192759824541,
126.398116045552));
#148569=CARTESIAN_POINT('Ctrl Pts',(55.9147274213818,-4.06789118440539,
126.504939037767));
#148570=CARTESIAN_POINT('Ctrl Pts',(55.9073295070704,-4.17943824345153,
126.616255254556));
#148571=CARTESIAN_POINT('Ctrl Pts',(55.8999328221582,-4.29096676540029,
126.727552972609));
#148572=CARTESIAN_POINT('Ctrl Pts',(55.892536137246,-4.39807995292613,126.843342169842));
#148573=CARTESIAN_POINT('Ctrl Pts',(55.8851394523338,-4.50040577528442,
126.963230781139));
#148574=CARTESIAN_POINT('Ctrl Pts',(55.8777430953984,-4.60272706040851,
127.08311407645));
#148575=CARTESIAN_POINT('Ctrl Pts',(55.870346738463,-4.70026116009976,127.207096140462));
#148576=CARTESIAN_POINT('Ctrl Pts',(55.8629503815275,-4.79267550042741,
127.33475082537));
#148577=CARTESIAN_POINT('Ctrl Pts',(55.855552892191,-4.88510398962636,127.462425054536));
#148578=CARTESIAN_POINT('Ctrl Pts',(55.8481554028543,-4.97241093979794,
127.59377272179));
#148579=CARTESIAN_POINT('Ctrl Pts',(55.8407579135178,-5.05430647498039,
127.72833776013));
#148580=CARTESIAN_POINT('Ctrl Pts',(55.8333578310028,-5.13623071851609,
127.862949970035));
#148581=CARTESIAN_POINT('Ctrl Pts',(55.8259577484878,-5.21273957627244,
128.000781477871));
#148582=CARTESIAN_POINT('Ctrl Pts',(55.8185576659728,-5.28358866112371,
128.141350774823));
#148583=CARTESIAN_POINT('Ctrl Pts',(55.8111494463063,-5.35451565182703,
128.282074642168));
#148584=CARTESIAN_POINT('Ctrl Pts',(55.8037412266398,-5.41977027276596,
128.425541977201));
#148585=CARTESIAN_POINT('Ctrl Pts',(55.7963330069734,-5.47915562395426,
128.571249735637));
#148586=CARTESIAN_POINT('Ctrl Pts',(55.7889202276713,-5.53857752583539,
128.717047174767));
#148587=CARTESIAN_POINT('Ctrl Pts',(55.7815074483693,-5.59212283305584,
128.865087434788));
#148588=CARTESIAN_POINT('Ctrl Pts',(55.7740946690672,-5.63964441292811,
129.014851897769));
#148589=CARTESIAN_POINT('Ctrl Pts',(55.7666712980385,-5.68723389386225,
129.164830351238));
#148590=CARTESIAN_POINT('Ctrl Pts',(55.7592479270097,-5.72878235902658,
129.316537568987));
#148591=CARTESIAN_POINT('Ctrl Pts',(55.7518245559809,-5.7641935162364,129.469443515316));
#148592=CARTESIAN_POINT('Ctrl Pts',(55.7478885065401,-5.78296936146829,
129.550517916989));
#148593=CARTESIAN_POINT('Ctrl Pts',(55.7439524570992,-5.80002065228488,
129.631929205196));
#148594=CARTESIAN_POINT('Ctrl Pts',(55.7400164076584,-5.81533895737569,
129.713597869152));
#148595=CARTESIAN_POINT('Ctrl Pts',(55.7289255750963,-5.85850222538121,
129.943720353922));
#148596=CARTESIAN_POINT('Ctrl Pts',(55.7178347425342,-5.88801578371597,
130.176477191147));
#148597=CARTESIAN_POINT('Ctrl Pts',(55.7067439099721,-5.90363014035041,
130.410556442314));
#148598=CARTESIAN_POINT('Ctrl Pts',(55.7006210040519,-5.91225034412153,
130.539784363187));
#148599=CARTESIAN_POINT('Ctrl Pts',(55.6944980981317,-5.91663505796375,
130.669414956629));
#148600=CARTESIAN_POINT('Ctrl Pts',(55.6883751922115,-5.91674776958239,
130.799223143303));
#148601=CARTESIAN_POINT('',(53.9383751922116,-5.90707774427615,130.803391861671));
#148602=CARTESIAN_POINT('Ctrl Pts',(55.6883738953519,-5.91958331968349,
130.799248188382));
#148603=CARTESIAN_POINT('Ctrl Pts',(55.6127721915164,-5.90490201336922,
132.402818445112));
#148604=CARTESIAN_POINT('Ctrl Pts',(55.4443546130767,-4.40225102814146,
135.999289301185));
#148605=CARTESIAN_POINT('Ctrl Pts',(55.1831211600325,1.68571315393122,137.596704225852));
#148606=CARTESIAN_POINT('Ctrl Pts',(54.90467353622,6.62576018234721,133.057550031782));
#148607=CARTESIAN_POINT('Ctrl Pts',(54.6262259124067,5.47705728957188,126.447824840472));
#148608=CARTESIAN_POINT('Ctrl Pts',(54.3477782885941,-0.704793683201028,
123.841543199704));
#148609=CARTESIAN_POINT('Ctrl Pts',(54.1184947151954,-5.26183227781015,
126.964180250712));
#148610=CARTESIAN_POINT('Ctrl Pts',(53.9820270164014,-5.9084332985456,129.872530384689));
#148611=CARTESIAN_POINT('Ctrl Pts',(53.9383751922116,-5.90707774427615,
130.803391861671));
#148612=CARTESIAN_POINT('',(52.1883751922116,-5.91601678976896,130.809832131107));
#148613=CARTESIAN_POINT('Ctrl Pts',(53.9383751922116,-5.90707774427615,
130.803391861671));
#148614=CARTESIAN_POINT('Ctrl Pts',(53.8892111417971,-5.9055510145305,131.851799836197));
#148615=CARTESIAN_POINT('Ctrl Pts',(53.7472312167785,-5.13850862592351,
134.881563943613));
#148616=CARTESIAN_POINT('Ctrl Pts',(53.5124354171551,-0.290390214522944,
137.796730319866));
#148617=CARTESIAN_POINT('Ctrl Pts',(53.2339877933425,5.72591566061874,134.828220751543));
#148618=CARTESIAN_POINT('Ctrl Pts',(52.9555401695295,6.48038477018695,128.16198029659));
#148619=CARTESIAN_POINT('Ctrl Pts',(52.6770925457166,1.27969686034724,123.923958269158));
#148620=CARTESIAN_POINT('Ctrl Pts',(52.4213708866106,-4.57652770833536,
125.838541045522));
#148621=CARTESIAN_POINT('Ctrl Pts',(52.258465102109,-5.90238132460186,129.320871834531));
#148622=CARTESIAN_POINT('Ctrl Pts',(52.1883751922116,-5.91601678976896,
130.809832131107));
#148623=CARTESIAN_POINT('',(50.4383743543751,-5.92189907249208,130.802920451297));
#148624=CARTESIAN_POINT('Ctrl Pts',(52.1883751708118,-5.91674746906338,
130.809833261547));
#148625=CARTESIAN_POINT('Ctrl Pts',(52.1787920763061,-5.91655914876486,
131.013435698233));
#148626=CARTESIAN_POINT('Ctrl Pts',(52.1692089818004,-5.90585813140058,
131.21656877425));
#148627=CARTESIAN_POINT('Ctrl Pts',(52.1596258872947,-5.88480997411137,
131.418316748816));
#148628=CARTESIAN_POINT('Ctrl Pts',(52.1498159990139,-5.86326369055945,
131.624839296434));
#148629=CARTESIAN_POINT('Ctrl Pts',(52.1400061107331,-5.83087469838739,
131.829910702615));
#148630=CARTESIAN_POINT('Ctrl Pts',(52.1301962224523,-5.78786844693692,
132.032574525422));
#148631=CARTESIAN_POINT('Ctrl Pts',(52.1268632476651,-5.77325678698019,
132.1014309071));
#148632=CARTESIAN_POINT('Ctrl Pts',(52.123530272878,-5.75741993033894,132.170009565731));
#148633=CARTESIAN_POINT('Ctrl Pts',(52.1201972980909,-5.74036795552583,
132.238273549955));
#148634=CARTESIAN_POINT('Ctrl Pts',(52.1127740316855,-5.70238946488,132.390312426081));
#148635=CARTESIAN_POINT('Ctrl Pts',(52.1053507652801,-5.6583090420052,132.54107131796));
#148636=CARTESIAN_POINT('Ctrl Pts',(52.0979274988747,-5.60822693525101,
132.69002262472));
#148637=CARTESIAN_POINT('Ctrl Pts',(52.0905130061538,-5.55820402138787,
132.838797883405));
#148638=CARTESIAN_POINT('Ctrl Pts',(52.0830985134328,-5.50219366108803,
132.98576945914));
#148639=CARTESIAN_POINT('Ctrl Pts',(52.0756840207118,-5.44034688608054,
133.130420875086));
#148640=CARTESIAN_POINT('Ctrl Pts',(52.0682766743581,-5.37855972132337,
133.274932870551));
#148641=CARTESIAN_POINT('Ctrl Pts',(52.0608693280044,-5.31094748660528,
133.417128817239));
#148642=CARTESIAN_POINT('Ctrl Pts',(52.0534619816507,-5.23771066323937,
133.556508428039));
#148643=CARTESIAN_POINT('Ctrl Pts',(52.0460601599753,-5.1645284626593,133.695784084266));
#148644=CARTESIAN_POINT('Ctrl Pts',(52.0386583382999,-5.08573019919347,
133.832247258008));
#148645=CARTESIAN_POINT('Ctrl Pts',(52.0312565166245,-5.00156395702014,
133.965418754699));
#148646=CARTESIAN_POINT('Ctrl Pts',(52.0238586023132,-4.9174421455509,134.098519951195));
#148647=CARTESIAN_POINT('Ctrl Pts',(52.0164606880019,-4.82795819778345,
134.228332616496));
#148648=CARTESIAN_POINT('Ctrl Pts',(52.0090627736906,-4.73340546081606,
134.354403336466));
#148649=CARTESIAN_POINT('Ctrl Pts',(52.0016660887784,-4.63886843679818,
134.48045310577));
#148650=CARTESIAN_POINT('Ctrl Pts',(51.9942694038662,-4.53926451913656,
134.602761865571));
#148651=CARTESIAN_POINT('Ctrl Pts',(51.986872718954,-4.43492965747943,134.720906225076));
#148652=CARTESIAN_POINT('Ctrl Pts',(51.9794763620186,-4.3305994221394,134.839045345937));
#148653=CARTESIAN_POINT('Ctrl Pts',(51.9720800050832,-4.2215389070088,134.953020153849));
#148654=CARTESIAN_POINT('Ctrl Pts',(51.9646836481478,-4.10812334647795,
135.062441538899));
#148655=CARTESIAN_POINT('Ctrl Pts',(51.9572861588113,-3.99469042173525,
135.171879676643));
#148656=CARTESIAN_POINT('Ctrl Pts',(51.9498886694747,-3.87690139263427,
135.276762744222));
#148657=CARTESIAN_POINT('Ctrl Pts',(51.9424911801381,-3.75516711110429,
135.3767397062));
#148658=CARTESIAN_POINT('Ctrl Pts',(51.9350910976232,-3.63339015581062,
135.476751714948));
#148659=CARTESIAN_POINT('Ctrl Pts',(51.9276910151082,-3.50766548284016,
135.571853957159));
#148660=CARTESIAN_POINT('Ctrl Pts',(51.9202909325932,-3.37843552045251,
135.661736863714));
#148661=CARTESIAN_POINT('Ctrl Pts',(51.9128827129268,-3.24906345643605,
135.751718605766));
#148662=CARTESIAN_POINT('Ctrl Pts',(51.9054744932604,-3.11617871210872,
135.836469337328));
#148663=CARTESIAN_POINT('Ctrl Pts',(51.8980662735939,-2.98025170497133,
135.915723482548));
#148664=CARTESIAN_POINT('Ctrl Pts',(51.8906534942919,-2.8442410370291,135.995026407372));
#148665=CARTESIAN_POINT('Ctrl Pts',(51.8832407149899,-2.7051847041352,136.068825830096));
#148666=CARTESIAN_POINT('Ctrl Pts',(51.8758279356878,-2.56357553038275,
136.136903262733));
#148667=CARTESIAN_POINT('Ctrl Pts',(51.8684045646591,-2.42176401880202,
136.205077967598));
#148668=CARTESIAN_POINT('Ctrl Pts',(51.8609811936304,-2.27739272297172,
136.267514205589));
#148669=CARTESIAN_POINT('Ctrl Pts',(51.8535578226017,-2.13097290953555,
136.324042222634));
#148670=CARTESIAN_POINT('Ctrl Pts',(51.8496217731604,-2.05333761114648,
136.354014733646));
#148671=CARTESIAN_POINT('Ctrl Pts',(51.8456857237191,-1.97512664002955,
136.382327069553));
#148672=CARTESIAN_POINT('Ctrl Pts',(51.8417496742778,-1.89641753569978,
136.408959719446));
#148673=CARTESIAN_POINT('Ctrl Pts',(51.8343264078724,-1.74797462137917,
136.459188065961));
#148674=CARTESIAN_POINT('Ctrl Pts',(51.826903141467,-1.59731035063802,136.503590821326));
#148675=CARTESIAN_POINT('Ctrl Pts',(51.8194798750616,-1.44492279571566,
136.541967146156));
#148676=CARTESIAN_POINT('Ctrl Pts',(51.8120653823406,-1.292715350228,136.580298113358));
#148677=CARTESIAN_POINT('Ctrl Pts',(51.8046508896195,-1.13878903323905,
136.612616737607));
#148678=CARTESIAN_POINT('Ctrl Pts',(51.7972363968985,-0.983660007678643,
136.638770917827));
#148679=CARTESIAN_POINT('Ctrl Pts',(51.7898290505447,-0.828680501313577,
136.664899889664));
#148680=CARTESIAN_POINT('Ctrl Pts',(51.782421704191,-0.672500959779303,
136.684876184232));
#148681=CARTESIAN_POINT('Ctrl Pts',(51.7750143578372,-0.515650653838979,
136.698598054733));
#148682=CARTESIAN_POINT('Ctrl Pts',(51.7676125361618,-0.358917332774448,
136.712309690944));
#148683=CARTESIAN_POINT('Ctrl Pts',(51.7602107144864,-0.201514613708668,
136.719776158913));
#148684=CARTESIAN_POINT('Ctrl Pts',(51.752808892811,-0.0439797521587122,
136.720947162517));
#148685=CARTESIAN_POINT('Ctrl Pts',(51.7454109784996,0.11347194796408,136.722117547958));
#148686=CARTESIAN_POINT('Ctrl Pts',(51.7380130641883,0.271055279303985,
136.716999084829));
#148687=CARTESIAN_POINT('Ctrl Pts',(51.7306151498769,0.428230210433925,
136.705593492938));
#148688=CARTESIAN_POINT('Ctrl Pts',(51.7232184649647,0.585379021941531,
136.694189796449));
#148689=CARTESIAN_POINT('Ctrl Pts',(51.7158217800525,0.742119195984115,
136.67650107182));
#148690=CARTESIAN_POINT('Ctrl Pts',(51.7084250951403,0.897912932904884,
136.65258110994));
#148691=CARTESIAN_POINT('Ctrl Pts',(51.7010287382049,1.05369976176832,136.628662208695));
#148692=CARTESIAN_POINT('Ctrl Pts',(51.6936323812694,1.20853986797863,136.598512676227));
#148693=CARTESIAN_POINT('Ctrl Pts',(51.6862360243339,1.36190305899322,136.562237884442));
#148694=CARTESIAN_POINT('Ctrl Pts',(51.6788385349974,1.51528973030366,136.525957538894));
#148695=CARTESIAN_POINT('Ctrl Pts',(51.6714410456609,1.66719867288674,136.483550152689));
#148696=CARTESIAN_POINT('Ctrl Pts',(51.6640435563243,1.81711247518638,136.435171643965));
#148697=CARTESIAN_POINT('Ctrl Pts',(51.6566434738093,1.96707882953745,136.386776176231));
#148698=CARTESIAN_POINT('Ctrl Pts',(51.6492433912943,2.11504829608217,136.332405533068));
#148699=CARTESIAN_POINT('Ctrl Pts',(51.6418433087793,2.26052128227204,136.272264612233));
#148700=CARTESIAN_POINT('Ctrl Pts',(51.6344350891128,2.406154230965,136.212057560273));
#148701=CARTESIAN_POINT('Ctrl Pts',(51.6270268694463,2.54928487189358,136.146067701939));
#148702=CARTESIAN_POINT('Ctrl Pts',(51.6196186497799,2.68943549642102,136.074547262562));
#148703=CARTESIAN_POINT('Ctrl Pts',(51.6122058704778,2.82967238131952,136.002982803547));
#148704=CARTESIAN_POINT('Ctrl Pts',(51.6047930911757,2.96692527033519,135.925881163036));
#148705=CARTESIAN_POINT('Ctrl Pts',(51.5973803118736,3.10074395987572,135.843538869801));
#148706=CARTESIAN_POINT('Ctrl Pts',(51.5899569408449,3.23475385583515,135.761078922035));
#148707=CARTESIAN_POINT('Ctrl Pts',(51.5825335698162,3.36531944300499,135.673363573769));
#148708=CARTESIAN_POINT('Ctrl Pts',(51.5751101987874,3.49202155036641,135.580731211885));
#148709=CARTESIAN_POINT('Ctrl Pts',(51.5711741493467,3.55920204786404,135.531615310932));
#148710=CARTESIAN_POINT('Ctrl Pts',(51.5672380999059,3.62529695819835,135.481117715013));
#148711=CARTESIAN_POINT('Ctrl Pts',(51.5633020504651,3.69024795428735,135.429293114195));
#148712=CARTESIAN_POINT('Ctrl Pts',(51.5558787840597,3.81274350586153,135.331553534442));
#148713=CARTESIAN_POINT('Ctrl Pts',(51.5484555176542,3.93153852001657,135.228796190306));
#148714=CARTESIAN_POINT('Ctrl Pts',(51.5410322512488,4.04619480467912,135.121331565475));
#148715=CARTESIAN_POINT('Ctrl Pts',(51.5336177585278,4.16071557513481,135.013993954905));
#148716=CARTESIAN_POINT('Ctrl Pts',(51.5262032658068,4.27110708321817,134.901960390835));
#148717=CARTESIAN_POINT('Ctrl Pts',(51.5187887730858,4.37696236331513,134.78558292141));
#148718=CARTESIAN_POINT('Ctrl Pts',(51.511381426732,4.48271561610775,134.669317620971));
#148719=CARTESIAN_POINT('Ctrl Pts',(51.5039740803782,4.58394109558224,134.548717024605));
#148720=CARTESIAN_POINT('Ctrl Pts',(51.4965667340244,4.68026711550046,134.424171426167));
#148721=CARTESIAN_POINT('Ctrl Pts',(51.489164912349,4.77652129183885,134.299718718535));
#148722=CARTESIAN_POINT('Ctrl Pts',(51.4817630906735,4.86788305723269,134.171327161424));
#148723=CARTESIAN_POINT('Ctrl Pts',(51.4743612689981,4.9540196963999,134.039421576834));
#148724=CARTESIAN_POINT('Ctrl Pts',(51.4669633546868,5.0401108647059,133.907585624176));
#148725=CARTESIAN_POINT('Ctrl Pts',(51.4595654403754,5.12098219648986,133.772239650181));
#148726=CARTESIAN_POINT('Ctrl Pts',(51.452167526064,5.19634323849538,133.633838928181));
#148727=CARTESIAN_POINT('Ctrl Pts',(51.4447708411518,5.2716917568628,133.495461205871));
#148728=CARTESIAN_POINT('Ctrl Pts',(51.4373741562396,5.34153162452368,133.354030070604));
#148729=CARTESIAN_POINT('Ctrl Pts',(51.4299774713274,5.40561740342432,133.21002706375));
#148730=CARTESIAN_POINT('Ctrl Pts',(51.4225811143919,5.46970034069436,133.066030442141));
#148731=CARTESIAN_POINT('Ctrl Pts',(51.4151847574565,5.5280295447358,132.919462516744));
#148732=CARTESIAN_POINT('Ctrl Pts',(51.407788400521,5.58040708589907,132.770826309651));
#148733=CARTESIAN_POINT('Ctrl Pts',(51.4003909111844,5.63279264619761,132.622167345976));
#148734=CARTESIAN_POINT('Ctrl Pts',(51.3929934218478,5.67922460519249,132.471439822194));
#148735=CARTESIAN_POINT('Ctrl Pts',(51.3855959325112,5.71955446764392,132.319163328864));
#148736=CARTESIAN_POINT('Ctrl Pts',(51.3781958499962,5.75989846766612,132.166833455245));
#148737=CARTESIAN_POINT('Ctrl Pts',(51.3707957674812,5.79413601673944,132.012953891622));
#148738=CARTESIAN_POINT('Ctrl Pts',(51.3633956849662,5.82216945917212,131.858055711596));
#148739=CARTESIAN_POINT('Ctrl Pts',(51.3559874652997,5.85023372725667,131.702987205098));
#148740=CARTESIAN_POINT('Ctrl Pts',(51.3485792456332,5.87208019809251,131.546898212893));
#148741=CARTESIAN_POINT('Ctrl Pts',(51.3411710259668,5.88766286280675,131.390326978739));
#148742=CARTESIAN_POINT('Ctrl Pts',(51.3337582466647,5.90325511839111,131.233659377603));
#148743=CARTESIAN_POINT('Ctrl Pts',(51.3263454673626,5.91257586369814,131.076509314862));
#148744=CARTESIAN_POINT('Ctrl Pts',(51.3189326880606,5.91563123074403,130.919415840593));
#148745=CARTESIAN_POINT('Ctrl Pts',(51.3115093170318,5.91869096344165,130.762097903802));
#148746=CARTESIAN_POINT('Ctrl Pts',(51.304085946003,5.91546744582428,130.604837089201));
#148747=CARTESIAN_POINT('Ctrl Pts',(51.2966625749742,5.90601880018665,130.448168963618));
#148748=CARTESIAN_POINT('Ctrl Pts',(51.2927265255335,5.90100890155253,130.365099764236));
#148749=CARTESIAN_POINT('Ctrl Pts',(51.2887904760928,5.8942497574333,130.282197060201));
#148750=CARTESIAN_POINT('Ctrl Pts',(51.2848544266521,5.88575585291891,130.199539485056));
#148751=CARTESIAN_POINT('Ctrl Pts',(51.2774311602467,5.86973661409017,130.043649877984));
#148752=CARTESIAN_POINT('Ctrl Pts',(51.2700078938412,5.84749555710952,129.888161413633));
#148753=CARTESIAN_POINT('Ctrl Pts',(51.2625846274358,5.81905704717815,129.733610579422));
#148754=CARTESIAN_POINT('Ctrl Pts',(51.2551701347148,5.79065214920381,129.579242411461));
#148755=CARTESIAN_POINT('Ctrl Pts',(51.2477556419938,5.75606444537802,129.425810031309));
#148756=CARTESIAN_POINT('Ctrl Pts',(51.2403411492728,5.71537014892045,129.273846121284));
#148757=CARTESIAN_POINT('Ctrl Pts',(51.232933802919,5.67471507515792,129.122028679797));
#148758=CARTESIAN_POINT('Ctrl Pts',(51.2255264565653,5.62796522207529,128.971677248892));
#148759=CARTESIAN_POINT('Ctrl Pts',(51.2181191102115,5.57524804945439,128.823315502089));
#148760=CARTESIAN_POINT('Ctrl Pts',(51.2107172885361,5.52257019528973,128.675064409074));
#148761=CARTESIAN_POINT('Ctrl Pts',(51.2033154668607,5.46393400788523,128.528800395592));
#148762=CARTESIAN_POINT('Ctrl Pts',(51.1959136451853,5.39951706128397,128.385033011101));
#148763=CARTESIAN_POINT('Ctrl Pts',(51.1885157308739,5.3351341198874,128.241341520293));
#148764=CARTESIAN_POINT('Ctrl Pts',(51.1811178165626,5.26497664899024,128.100144373515));
#148765=CARTESIAN_POINT('Ctrl Pts',(51.1737199022513,5.18927068585997,127.961932023674));
#148766=CARTESIAN_POINT('Ctrl Pts',(51.1663232173391,5.11357730368743,127.823742642219));
#148767=CARTESIAN_POINT('Ctrl Pts',(51.1589265324269,5.03233743845365,127.688537400328));
#148768=CARTESIAN_POINT('Ctrl Pts',(51.1515298475147,4.94582355928902,127.556783076863));
#148769=CARTESIAN_POINT('Ctrl Pts',(51.1441334905793,4.85931351624045,127.425034595522));
#148770=CARTESIAN_POINT('Ctrl Pts',(51.1367371336438,4.76753012913943,127.296737040395));
#148771=CARTESIAN_POINT('Ctrl Pts',(51.1293407767083,4.67078961890795,127.172328831031));
#148772=CARTESIAN_POINT('Ctrl Pts',(51.1219432873718,4.57403429745725,127.047901574452));
#148773=CARTESIAN_POINT('Ctrl Pts',(51.1145457980352,4.4723205708751,126.927365144));
#148774=CARTESIAN_POINT('Ctrl Pts',(51.1071483086987,4.36600532010895,126.811125324313));
#148775=CARTESIAN_POINT('Ctrl Pts',(51.0997482261837,4.25965280069645,126.694844756938));
#148776=CARTESIAN_POINT('Ctrl Pts',(51.0923481436687,4.14869579729786,126.582864074389));
#148777=CARTESIAN_POINT('Ctrl Pts',(51.0849480611537,4.03352833188814,126.47555249542));
#148778=CARTESIAN_POINT('Ctrl Pts',(51.0775398414873,3.9182342280107,126.368122916338));
#148779=CARTESIAN_POINT('Ctrl Pts',(51.0701316218208,3.79872068931553,126.265372948727));
#148780=CARTESIAN_POINT('Ctrl Pts',(51.0627234021543,3.67541568660011,126.167632235054));
#148781=CARTESIAN_POINT('Ctrl Pts',(51.0553106228523,3.55203479171279,126.069831363602));
#148782=CARTESIAN_POINT('Ctrl Pts',(51.0478978435503,3.4248580837182,125.977046109082));
#148783=CARTESIAN_POINT('Ctrl Pts',(51.0404850642482,3.2943423952177,125.889562682191));
#148784=CARTESIAN_POINT('Ctrl Pts',(51.0330616932195,3.16364021978109,125.801954254876));
#148785=CARTESIAN_POINT('Ctrl Pts',(51.0256383221907,3.02958985258975,125.719662979942));
#148786=CARTESIAN_POINT('Ctrl Pts',(51.018214951162,2.89267329770254,125.642929444407));
#148787=CARTESIAN_POINT('Ctrl Pts',(51.0142789017211,2.82007685503185,125.602243482669));
#148788=CARTESIAN_POINT('Ctrl Pts',(51.0103428522802,2.7466749796996,125.563119205502));
#148789=CARTESIAN_POINT('Ctrl Pts',(51.0064068028393,2.67254165787765,125.525586929539));
#148790=CARTESIAN_POINT('Ctrl Pts',(50.9989835364339,2.53272852654616,125.454802228416));
#148791=CARTESIAN_POINT('Ctrl Pts',(50.9915602700284,2.38988984325885,125.389468946554));
#148792=CARTESIAN_POINT('Ctrl Pts',(50.9841370036229,2.24449014006184,125.329856569374));
#148793=CARTESIAN_POINT('Ctrl Pts',(50.9767225109019,2.09926228723931,125.270314649074));
#148794=CARTESIAN_POINT('Ctrl Pts',(50.9693080181809,1.95147978161683,125.216480314611));
#148795=CARTESIAN_POINT('Ctrl Pts',(50.9618935254599,1.80163197902212,125.168577373449));
#148796=CARTESIAN_POINT('Ctrl Pts',(50.9544861791061,1.65192860538102,125.120720602946));
#148797=CARTESIAN_POINT('Ctrl Pts',(50.9470788327523,1.50016425086646,125.078783957427));
#148798=CARTESIAN_POINT('Ctrl Pts',(50.9396714863985,1.34684839196752,125.042943259697));
#148799=CARTESIAN_POINT('Ctrl Pts',(50.9322696647231,1.19364688182042,125.007129293311));
#148800=CARTESIAN_POINT('Ctrl Pts',(50.9248678430477,1.03889653330481,124.977402306454));
#148801=CARTESIAN_POINT('Ctrl Pts',(50.9174660213723,0.883122027918332,
124.953888324981));
#148802=CARTESIAN_POINT('Ctrl Pts',(50.9100681070609,0.727429754680704,
124.930386756356));
#148803=CARTESIAN_POINT('Ctrl Pts',(50.9026701927495,0.57071476947349,124.913091716819));
#148804=CARTESIAN_POINT('Ctrl Pts',(50.8952722784381,0.413511882881774,
124.902078136592));
#148805=CARTESIAN_POINT('Ctrl Pts',(50.8878755935259,0.256335120558084,
124.891066386622));
#148806=CARTESIAN_POINT('Ctrl Pts',(50.8804789086137,0.0986709897909217,
124.886334050262));
#148807=CARTESIAN_POINT('Ctrl Pts',(50.8730822237015,-0.0589405189251695,
124.887904196892));
#148808=CARTESIAN_POINT('Ctrl Pts',(50.865685866766,-0.216545038981799,
124.889474273901));
#148809=CARTESIAN_POINT('Ctrl Pts',(50.8582895098306,-0.374096568347735,
124.897346274522));
#148810=CARTESIAN_POINT('Ctrl Pts',(50.8508931528951,-0.531055327108481,
124.911491129613));
#148811=CARTESIAN_POINT('Ctrl Pts',(50.8434956635586,-0.688038116655891,
124.925638150317));
#148812=CARTESIAN_POINT('Ctrl Pts',(50.8360981742219,-0.844427583078323,
124.946059904248));
#148813=CARTESIAN_POINT('Ctrl Pts',(50.8287006848853,-0.999689425397175,
124.972675473866));
#148814=CARTESIAN_POINT('Ctrl Pts',(50.8213006023703,-1.15500569451439,
124.999300373531));
#148815=CARTESIAN_POINT('Ctrl Pts',(50.8139005198553,-1.30919318481324,
125.032123348759));
#148816=CARTESIAN_POINT('Ctrl Pts',(50.8065004373403,-1.461728283598,125.071012469457));
#148817=CARTESIAN_POINT('Ctrl Pts',(50.7990922176738,-1.61443111040486,
125.109944352741));
#148818=CARTESIAN_POINT('Ctrl Pts',(50.7916839980073,-1.76547755513184,
125.154955610344));
#148819=CARTESIAN_POINT('Ctrl Pts',(50.7842757783408,-1.91435895156643,
125.205864358118));
#148820=CARTESIAN_POINT('Ctrl Pts',(50.7768629990387,-2.0633319820163,125.256804439376));
#148821=CARTESIAN_POINT('Ctrl Pts',(50.7694502197367,-2.21013696159357,
125.313649109171));
#148822=CARTESIAN_POINT('Ctrl Pts',(50.7620374404346,-2.35428616395485,
125.376168725167));
#148823=CARTESIAN_POINT('Ctrl Pts',(50.7546140694058,-2.49864133345638,
125.438777672122));
#148824=CARTESIAN_POINT('Ctrl Pts',(50.747190698377,-2.64033281149806,125.507077598366));
#148825=CARTESIAN_POINT('Ctrl Pts',(50.7397673273483,-2.77889765043978,
125.580793023394));
#148826=CARTESIAN_POINT('Ctrl Pts',(50.7358312779076,-2.85236805286118,
125.61987871052));
#148827=CARTESIAN_POINT('Ctrl Pts',(50.731895228467,-2.92495992185215,125.660486159611));
#148828=CARTESIAN_POINT('Ctrl Pts',(50.7279591790264,-2.99660775983645,
125.702569510887));
#148829=CARTESIAN_POINT('Ctrl Pts',(50.7205359126209,-3.13173334622803,
125.781937398021));
#148830=CARTESIAN_POINT('Ctrl Pts',(50.7131126462155,-3.26390788393835,
125.866797392972));
#148831=CARTESIAN_POINT('Ctrl Pts',(50.7056893798101,-3.39265355633307,
125.956904335226));
#148832=CARTESIAN_POINT('Ctrl Pts',(50.6982748870891,-3.52124706203486,
126.046904778557));
#148833=CARTESIAN_POINT('Ctrl Pts',(50.690860394368,-3.64641946636367,126.142139613201));
#148834=CARTESIAN_POINT('Ctrl Pts',(50.683445901647,-3.767717964983,126.242318103643));
#148835=CARTESIAN_POINT('Ctrl Pts',(50.6760385552932,-3.88889955154256,
126.342400038283));
#148836=CARTESIAN_POINT('Ctrl Pts',(50.6686312089394,-4.00621437979071,
126.447415906663));
#148837=CARTESIAN_POINT('Ctrl Pts',(50.6612238625856,-4.11923914053527,
126.557032108305));
#148838=CARTESIAN_POINT('Ctrl Pts',(50.6538220409102,-4.23217960314893,
126.666566554047));
#148839=CARTESIAN_POINT('Ctrl Pts',(50.6464202192348,-4.34083610246405,
126.780694242492));
#148840=CARTESIAN_POINT('Ctrl Pts',(50.6390183975594,-4.44481900619264,
126.89904186429));
#148841=CARTESIAN_POINT('Ctrl Pts',(50.6316204832481,-4.54874701815576,
127.017327011299));
#148842=CARTESIAN_POINT('Ctrl Pts',(50.6242225689366,-4.64800610221966,
127.139827375428));
#148843=CARTESIAN_POINT('Ctrl Pts',(50.6168246546253,-4.74224413928239,
127.266133507));
#148844=CARTESIAN_POINT('Ctrl Pts',(50.6094279697131,-4.83646651569314,
127.392418648785));
#148845=CARTESIAN_POINT('Ctrl Pts',(50.6020312848009,-4.92566927813927,
127.522508003883));
#148846=CARTESIAN_POINT('Ctrl Pts',(50.5946345998886,-5.00954113964657,
127.655959732563));
#148847=CARTESIAN_POINT('Ctrl Pts',(50.5872382429532,-5.09340928218753,
127.789405543853));
#148848=CARTESIAN_POINT('Ctrl Pts',(50.5798418860178,-5.17194679515063,
127.926213116219));
#148849=CARTESIAN_POINT('Ctrl Pts',(50.5724455290823,-5.24488637100059,
128.065912604952));
#148850=CARTESIAN_POINT('Ctrl Pts',(50.5650480397457,-5.31783711408582,
128.205633482032));
#148851=CARTESIAN_POINT('Ctrl Pts',(50.5576505504091,-5.38518804075603,
128.348246826142));
#148852=CARTESIAN_POINT('Ctrl Pts',(50.5502530610725,-5.44671842649877,
128.493259376828));
#148853=CARTESIAN_POINT('Ctrl Pts',(50.5428529785575,-5.50827038162302,
128.63832276144));
#148854=CARTESIAN_POINT('Ctrl Pts',(50.5354528960425,-5.56399758771458,
128.785786683702));
#148855=CARTESIAN_POINT('Ctrl Pts',(50.5280528135274,-5.61372801584443,
128.935139301985));
#148856=CARTESIAN_POINT('Ctrl Pts',(50.520644593861,-5.66351312769235,129.084656148825));
#148857=CARTESIAN_POINT('Ctrl Pts',(50.5132363741945,-5.7072881747754,129.236065484827));
#148858=CARTESIAN_POINT('Ctrl Pts',(50.505828154528,-5.74493123486562,129.388841041875));
#148859=CARTESIAN_POINT('Ctrl Pts',(50.4984153752259,-5.78259746363116,
129.541710629728));
#148860=CARTESIAN_POINT('Ctrl Pts',(50.4910025959238,-5.81412411038098,
129.695947749312));
#148861=CARTESIAN_POINT('Ctrl Pts',(50.4835898166218,-5.83944075171248,
129.851017935347));
#148862=CARTESIAN_POINT('Ctrl Pts',(50.476166445593,-5.86479356664839,130.006309692938));
#148863=CARTESIAN_POINT('Ctrl Pts',(50.4687430745643,-5.8839186092329,130.162436524779));
#148864=CARTESIAN_POINT('Ctrl Pts',(50.4613197035355,-5.89679741450964,
130.318860035968));
#148865=CARTESIAN_POINT('Ctrl Pts',(50.4573836540948,-5.90362606608985,
130.401799534928));
#148866=CARTESIAN_POINT('Ctrl Pts',(50.4534476046541,-5.90869954745151,
130.484822448345));
#148867=CARTESIAN_POINT('Ctrl Pts',(50.4495115552134,-5.91202103868685,
130.567848882922));
#148868=CARTESIAN_POINT('Ctrl Pts',(50.4457994342128,-5.91515356472693,
130.646151804683));
#148869=CARTESIAN_POINT('Ctrl Pts',(50.4420873132122,-5.91673052304171,
130.724517373101));
#148870=CARTESIAN_POINT('Ctrl Pts',(50.4383751922116,-5.91674982070073,
130.802903998923));
#148871=CARTESIAN_POINT('',(48.6883751922117,-5.91158553941399,130.799597756573));
#148872=CARTESIAN_POINT('Ctrl Pts',(50.438373671031,-5.92609883128946,130.802933869946));
#148873=CARTESIAN_POINT('Ctrl Pts',(50.3492704244875,-5.91986146368452,
132.687448269669));
#148874=CARTESIAN_POINT('Ctrl Pts',(50.1673513033397,-3.92624335915797,
136.546317570673));
#148875=CARTESIAN_POINT('Ctrl Pts',(49.8926163075878,2.65223930360469,137.280716630537));
#148876=CARTESIAN_POINT('Ctrl Pts',(49.6141686837748,6.88234186179267,132.073585194923));
#148877=CARTESIAN_POINT('Ctrl Pts',(49.3357210599618,4.78790847008234,125.700098377784));
#148878=CARTESIAN_POINT('Ctrl Pts',(49.0572734361491,-1.70637890329801,
124.017179201934));
#148879=CARTESIAN_POINT('Ctrl Pts',(48.8414914802322,-5.52392597259,127.546415598653));
#148880=CARTESIAN_POINT('Ctrl Pts',(48.7185253989198,-5.9164078143733,130.157882010726));
#148881=CARTESIAN_POINT('Ctrl Pts',(48.6883751922117,-5.91158553941399,
130.799597756573));
#148882=CARTESIAN_POINT('',(46.9383751922116,-5.90883819398982,130.807710527577));
#148883=CARTESIAN_POINT('Ctrl Pts',(48.6883751922117,-5.91158553941399,
130.799597756573));
#148884=CARTESIAN_POINT('Ctrl Pts',(48.6257095243155,-5.90156268670095,
132.133371226262));
#148885=CARTESIAN_POINT('Ctrl Pts',(48.4702279818151,-4.79354772380148,
135.457715080396));
#148886=CARTESIAN_POINT('Ctrl Pts',(48.2219305647104,0.725982839758202,
137.765000634599));
#148887=CARTESIAN_POINT('Ctrl Pts',(47.9434829408974,6.24859503990529,133.955966645865));
#148888=CARTESIAN_POINT('Ctrl Pts',(47.6650353170847,6.02905365921741,127.250760681639));
#148889=CARTESIAN_POINT('Ctrl Pts',(47.3865876932715,0.269106501353806,
123.81113945552));
#148890=CARTESIAN_POINT('Ctrl Pts',(47.1443676516474,-4.95656072458745,
126.409346611893));
#148891=CARTESIAN_POINT('Ctrl Pts',(46.9949634846273,-5.90265684270682,
129.601880827053));
#148892=CARTESIAN_POINT('Ctrl Pts',(46.9383751922116,-5.90883819398982,
130.807710527577));
#148893=CARTESIAN_POINT('',(45.1883751922116,-5.92386795880746,130.807904967694));
#148894=CARTESIAN_POINT('Ctrl Pts',(46.9383751922116,-5.90883819398982,
130.807710527577));
#148895=CARTESIAN_POINT('Ctrl Pts',(46.902147610023,-5.91279546857935,131.579677531993));
#148896=CARTESIAN_POINT('Ctrl Pts',(46.7731041532299,-5.41277144263418,
134.324515665972));
#148897=CARTESIAN_POINT('Ctrl Pts',(46.5512448218333,-1.25874935488714,
137.688626053462));
#148898=CARTESIAN_POINT('Ctrl Pts',(46.27279719802,5.11154271077221,135.584495725102));
#148899=CARTESIAN_POINT('Ctrl Pts',(45.9943495742072,6.78457673797554,129.087654755492));
#148900=CARTESIAN_POINT('Ctrl Pts',(45.7159019503944,2.22291618797788,124.168382607389));
#148901=CARTESIAN_POINT('Ctrl Pts',(45.4472438230623,-4.14930174401023,
125.305804141896));
#148902=CARTESIAN_POINT('Ctrl Pts',(45.2714015703349,-5.9114443679371,129.050163660677));
#148903=CARTESIAN_POINT('Ctrl Pts',(45.1883751922116,-5.92386795880746,
130.807904967694));
#148904=CARTESIAN_POINT('',(43.4383751922116,-5.91881984665077,130.799298212246));
#148905=CARTESIAN_POINT('Ctrl Pts',(45.1883751922116,-5.92386795880746,
130.807904967694));
#148906=CARTESIAN_POINT('Ctrl Pts',(45.1785856957306,-5.92533280289505,
131.015157201605));
#148907=CARTESIAN_POINT('Ctrl Pts',(45.1687961992496,-5.91540331898639,
131.222267486992));
#148908=CARTESIAN_POINT('Ctrl Pts',(45.0661908281642,-5.68704911656536,
133.379871893754));
#148909=CARTESIAN_POINT('Ctrl Pts',(44.8805590789556,-3.14209308084078,
137.057744629576));
#148910=CARTESIAN_POINT('Ctrl Pts',(44.6021114551428,3.56277101426011,136.827999321065));
#148911=CARTESIAN_POINT('Ctrl Pts',(44.32366383133,6.9936225982931,131.06282431515));
#148912=CARTESIAN_POINT('Ctrl Pts',(44.045216207517,3.99767667195677,125.060133797806));
#148913=CARTESIAN_POINT('Ctrl Pts',(43.7667685837041,-2.67193881854835,
124.336107106742));
#148914=CARTESIAN_POINT('Ctrl Pts',(43.564488245269,-5.73340049741501,128.128201901887));
#148915=CARTESIAN_POINT('Ctrl Pts',(43.4550237814381,-5.92314857408724,
130.446223158808));
#148916=CARTESIAN_POINT('Ctrl Pts',(43.4383751922116,-5.91994246001312,
130.799297252068));
#148917=CARTESIAN_POINT('',(41.6883752167573,-5.91147118309346,130.803194539491));
#148918=CARTESIAN_POINT('Ctrl Pts',(43.4383751922116,-5.9167478358041,130.799299984451));
#148919=CARTESIAN_POINT('Ctrl Pts',(43.4310738632198,-5.91688020106165,
130.954057666618));
#148920=CARTESIAN_POINT('Ctrl Pts',(43.423772534228,-5.91093669250362,131.109027043208));
#148921=CARTESIAN_POINT('Ctrl Pts',(43.4164712052362,-5.89889422020681,
131.263683533727));
#148922=CARTESIAN_POINT('Ctrl Pts',(43.4091762411837,-5.8868622459447,131.418205202329));
#148923=CARTESIAN_POINT('Ctrl Pts',(43.4018812771311,-5.86874191729228,
131.572414145738));
#148924=CARTESIAN_POINT('Ctrl Pts',(43.3945863130785,-5.84456219308604,
131.725785239361));
#148925=CARTESIAN_POINT('Ctrl Pts',(43.3872960069955,-5.82039790808101,
131.879058402702));
#148926=CARTESIAN_POINT('Ctrl Pts',(43.3800057009126,-5.790181987833,132.031494401671));
#148927=CARTESIAN_POINT('Ctrl Pts',(43.3727153948296,-5.75399524481711,
132.18257296881));
#148928=CARTESIAN_POINT('Ctrl Pts',(43.365427232522,-5.71781914281539,132.333607110034));
#148929=CARTESIAN_POINT('Ctrl Pts',(43.3581390702143,-5.6756757968219,132.483284238412));
#148930=CARTESIAN_POINT('Ctrl Pts',(43.3508509079067,-5.62769715383045,
132.631094125024));
#148931=CARTESIAN_POINT('Ctrl Pts',(43.3435635977204,-5.57972412043198,
132.778886729919));
#148932=CARTESIAN_POINT('Ctrl Pts',(43.3362762875341,-5.52591726582878,
132.924812160688));
#148933=CARTESIAN_POINT('Ctrl Pts',(43.3289889773478,-5.46645834994697,
133.06837556248));
#148934=CARTESIAN_POINT('Ctrl Pts',(43.3217009811613,-5.40699383682384,
133.211952478798));
#148935=CARTESIAN_POINT('Ctrl Pts',(43.3144129849747,-5.34187635144991,
133.35316656767));
#148936=CARTESIAN_POINT('Ctrl Pts',(43.3071249887881,-5.27133559294232,
133.491543460076));
#148937=CARTESIAN_POINT('Ctrl Pts',(43.2998347680968,-5.20077330337891,
133.629962589065));
#148938=CARTESIAN_POINT('Ctrl Pts',(43.2925445474055,-5.12478462248862,
133.765542455605));
#148939=CARTESIAN_POINT('Ctrl Pts',(43.2852543267141,-5.04364477738988,
133.897834057246));
#148940=CARTESIAN_POINT('Ctrl Pts',(43.2779564503192,-4.96241972463731,
134.030264582705));
#148941=CARTESIAN_POINT('Ctrl Pts',(43.2706585739243,-4.87603291001786,
134.159399620895));
#148942=CARTESIAN_POINT('Ctrl Pts',(43.2633606975294,-4.78480268829636,
134.284819466134));
#148943=CARTESIAN_POINT('Ctrl Pts',(43.2560584445036,-4.6935177546307,134.410314527276));
#148944=CARTESIAN_POINT('Ctrl Pts',(43.2487561914779,-4.5973838684373,134.53208965766));
#148945=CARTESIAN_POINT('Ctrl Pts',(43.2414539384521,-4.4967585403759,134.64975958153));
#148946=CARTESIAN_POINT('Ctrl Pts',(43.2341415377505,-4.39599337695109,
134.767593027019));
#148947=CARTESIAN_POINT('Ctrl Pts',(43.2268291370489,-4.290724572944,134.881309596506));
#148948=CARTESIAN_POINT('Ctrl Pts',(43.2195167363474,-4.18134561707234,
134.990561686924));
#148949=CARTESIAN_POINT('Ctrl Pts',(43.216302269591,-4.13326359423922,135.038587940823));
#148950=CARTESIAN_POINT('Ctrl Pts',(43.2130878028346,-4.08438774511687,
135.085752009502));
#148951=CARTESIAN_POINT('Ctrl Pts',(43.2098733360782,-4.03475336763297,
135.132026943067));
#148952=CARTESIAN_POINT('Ctrl Pts',(43.2024500696728,-3.92013118148087,
135.238891062617));
#148953=CARTESIAN_POINT('Ctrl Pts',(43.1950268032674,-3.80108715052099,
135.341359818122));
#148954=CARTESIAN_POINT('Ctrl Pts',(43.187603536862,-3.67799257299818,135.439045201814));
#148955=CARTESIAN_POINT('Ctrl Pts',(43.180189044141,-3.55504348304345,135.536615129496));
#148956=CARTESIAN_POINT('Ctrl Pts',(43.17277455142,-3.4280536654459,135.629412708999));
#148957=CARTESIAN_POINT('Ctrl Pts',(43.165360058699,-3.29743096270113,135.717086908407));
#148958=CARTESIAN_POINT('Ctrl Pts',(43.1579527123452,-3.16693415903493,
135.804676604121));
#148959=CARTESIAN_POINT('Ctrl Pts',(43.1505453659914,-3.03281174891307,
135.887152543895));
#148960=CARTESIAN_POINT('Ctrl Pts',(43.1431380196376,-2.89550424266712,
135.964204194962));
#148961=CARTESIAN_POINT('Ctrl Pts',(43.1357361979622,-2.75829914553965,
136.041198378001));
#148962=CARTESIAN_POINT('Ctrl Pts',(43.1283343762869,-2.61791400650058,
136.112776145849));
#148963=CARTESIAN_POINT('Ctrl Pts',(43.1209325546114,-2.47481778569465,
136.178670572352));
#148964=CARTESIAN_POINT('Ctrl Pts',(43.1135346403001,-2.33179710427043,
136.244530213699));
#148965=CARTESIAN_POINT('Ctrl Pts',(43.1061367259887,-2.18606852951715,
136.30471233298));
#148966=CARTESIAN_POINT('Ctrl Pts',(43.0987388116774,-2.03812495663172,
136.358996269313));
#148967=CARTESIAN_POINT('Ctrl Pts',(43.0913421267652,-1.89020596928393,
136.41327118464));
#148968=CARTESIAN_POINT('Ctrl Pts',(43.0839454418531,-1.74007306446702,
136.461649733906));
#148969=CARTESIAN_POINT('Ctrl Pts',(43.0765487569409,-1.5882385311008,136.503959632482));
#148970=CARTESIAN_POINT('Ctrl Pts',(43.0691524000054,-1.43641073023689,
136.546267654992));
#148971=CARTESIAN_POINT('Ctrl Pts',(43.0617560430699,-1.28288181044486,
136.582507461651));
#148972=CARTESIAN_POINT('Ctrl Pts',(43.0543596861345,-1.12817835358521,
136.612556909445));
#148973=CARTESIAN_POINT('Ctrl Pts',(43.0469621967979,-0.97345121123072,
136.642610957887));
#148974=CARTESIAN_POINT('Ctrl Pts',(43.0395647074613,-0.817549540226447,
136.666472689166));
#148975=CARTESIAN_POINT('Ctrl Pts',(43.0321672181248,-0.661009074052499,
136.684071287873));
#148976=CARTESIAN_POINT('Ctrl Pts',(43.0247671356097,-0.504413732859909,
136.701676055741));
#148977=CARTESIAN_POINT('Ctrl Pts',(43.0173670530946,-0.34717952138695,
136.713013278072));
#148978=CARTESIAN_POINT('Ctrl Pts',(43.0099669705796,-0.189846088377888,
136.718064112435));
#148979=CARTESIAN_POINT('Ctrl Pts',(43.0025587509131,-0.032339651086311,
136.72312050071));
#148980=CARTESIAN_POINT('Ctrl Pts',(42.9951505312467,0.125265852295126,
136.721876684258));
#148981=CARTESIAN_POINT('Ctrl Pts',(42.9877423115802,0.282431242364485,
136.714365960697));
#148982=CARTESIAN_POINT('Ctrl Pts',(42.9803295322782,0.439693365108987,
136.706850614411));
#148983=CARTESIAN_POINT('Ctrl Pts',(42.9729167529761,0.59651446377348,136.693060707733));
#148984=CARTESIAN_POINT('Ctrl Pts',(42.9655039736741,0.752362195889403,
136.673081235273));
#148985=CARTESIAN_POINT('Ctrl Pts',(42.9580806026453,0.908432610553728,
136.653073215205));
#148986=CARTESIAN_POINT('Ctrl Pts',(42.9506572316165,1.06352651384456,136.62685802807));
#148987=CARTESIAN_POINT('Ctrl Pts',(42.9432338605878,1.21712262151333,136.594571588394));
#148988=CARTESIAN_POINT('Ctrl Pts',(42.939297811147,1.29856296328754,136.577452543376));
#148989=CARTESIAN_POINT('Ctrl Pts',(42.9353617617062,1.37958247648485,136.558627484354));
#148990=CARTESIAN_POINT('Ctrl Pts',(42.9314257122654,1.46010549598786,136.538122253969));
#148991=CARTESIAN_POINT('Ctrl Pts',(42.92400244586,1.61196939773252,136.499450029408));
#148992=CARTESIAN_POINT('Ctrl Pts',(42.9165791794545,1.76252547035062,136.454681779949));
#148993=CARTESIAN_POINT('Ctrl Pts',(42.9091559130491,1.9112465761481,136.403920161643));
#148994=CARTESIAN_POINT('Ctrl Pts',(42.9017414203281,2.05979190594948,136.353218539354));
#148995=CARTESIAN_POINT('Ctrl Pts',(42.8943269276071,2.20650623605967,136.296537767699));
#148996=CARTESIAN_POINT('Ctrl Pts',(42.8869124348861,2.350873784555,136.234031234794));
#148997=CARTESIAN_POINT('Ctrl Pts',(42.8795050885323,2.49510218617154,136.171584948039));
#148998=CARTESIAN_POINT('Ctrl Pts',(42.8720977421785,2.6369879689361,136.103324225895));
#148999=CARTESIAN_POINT('Ctrl Pts',(42.8646903958248,2.77603176624284,136.029451831632));
#149000=CARTESIAN_POINT('Ctrl Pts',(42.8572885741494,2.91497185943954,135.955634534188));
#149001=CARTESIAN_POINT('Ctrl Pts',(42.849886752474,3.05107385946634,135.876214072708));
#149002=CARTESIAN_POINT('Ctrl Pts',(42.8424849307986,3.1838597093746,135.791440716534));
#149003=CARTESIAN_POINT('Ctrl Pts',(42.8350870164872,3.31657546266687,135.706712111554));
#149004=CARTESIAN_POINT('Ctrl Pts',(42.8276891021759,3.44597823833732,135.616636439868));
#149005=CARTESIAN_POINT('Ctrl Pts',(42.8202911878645,3.57161596624295,135.521509115565));
#149006=CARTESIAN_POINT('Ctrl Pts',(42.8128945029523,3.69723281543698,135.426397599699));
#149007=CARTESIAN_POINT('Ctrl Pts',(42.8054978180401,3.8190855613395,135.326236322482));
#149008=CARTESIAN_POINT('Ctrl Pts',(42.7981011331279,3.936752351339,135.22136316304));
#149009=CARTESIAN_POINT('Ctrl Pts',(42.7907047761925,4.05441392387007,135.116494653784));
#149010=CARTESIAN_POINT('Ctrl Pts',(42.783308419257,4.16788963087681,135.006914926103));
#149011=CARTESIAN_POINT('Ctrl Pts',(42.7759120623216,4.27679207962592,134.893000986949));
#149012=CARTESIAN_POINT('Ctrl Pts',(42.768514572985,4.38571120161748,134.77906960728));
#149013=CARTESIAN_POINT('Ctrl Pts',(42.7611170836484,4.49005541322899,134.660802964712));
#149014=CARTESIAN_POINT('Ctrl Pts',(42.7537195943119,4.58947555841892,134.538613509535));
#149015=CARTESIAN_POINT('Ctrl Pts',(42.7463195117969,4.68893055518748,134.416381221032));
#149016=CARTESIAN_POINT('Ctrl Pts',(42.7389194292818,4.78345781338101,134.290223671413));
#149017=CARTESIAN_POINT('Ctrl Pts',(42.7315193467668,4.87274978700204,134.160584697655));
#149018=CARTESIAN_POINT('Ctrl Pts',(42.7241111271003,4.96213994632701,134.03080317252));
#149019=CARTESIAN_POINT('Ctrl Pts',(42.7167029074339,5.04628311262473,133.897532885731));
#149020=CARTESIAN_POINT('Ctrl Pts',(42.7092946877674,5.12491586048902,133.761245462366));
#149021=CARTESIAN_POINT('Ctrl Pts',(42.7018819084654,5.20359700549757,133.624874156366));
#149022=CARTESIAN_POINT('Ctrl Pts',(42.6944691291633,5.27676080085523,133.485482343259));
#149023=CARTESIAN_POINT('Ctrl Pts',(42.6870563498613,5.34419101082741,133.343563839502));
#149024=CARTESIAN_POINT('Ctrl Pts',(42.6796329788325,5.41171756824586,133.201442555932));
#149025=CARTESIAN_POINT('Ctrl Pts',(42.6722096078038,5.47349403196441,133.056787713618));
#149026=CARTESIAN_POINT('Ctrl Pts',(42.664786236775,5.52935298385414,132.910111348883));
#149027=CARTESIAN_POINT('Ctrl Pts',(42.6608501873342,5.55897074046346,132.832340020849));
#149028=CARTESIAN_POINT('Ctrl Pts',(42.6569141378934,5.58692571105045,132.754000605576));
#149029=CARTESIAN_POINT('Ctrl Pts',(42.6529780884526,5.61319873891446,132.675170730846));
#149030=CARTESIAN_POINT('Ctrl Pts',(42.6455548220471,5.66274884951259,132.526500047301));
#149031=CARTESIAN_POINT('Ctrl Pts',(42.6381315556416,5.70646328812605,132.375634627079));
#149032=CARTESIAN_POINT('Ctrl Pts',(42.6307082892362,5.74414349140036,132.223073454155));
#149033=CARTESIAN_POINT('Ctrl Pts',(42.6232937965152,5.78177915980349,132.070692595868));
#149034=CARTESIAN_POINT('Ctrl Pts',(42.6158793037942,5.8133947004483,131.916620333196));
#149035=CARTESIAN_POINT('Ctrl Pts',(42.6084648110732,5.83884037037358,131.761373518104));
#149036=CARTESIAN_POINT('Ctrl Pts',(42.6010574647194,5.86426151480434,131.606276335736));
#149037=CARTESIAN_POINT('Ctrl Pts',(42.5936501183655,5.88352456735708,131.4500072206));
#149038=CARTESIAN_POINT('Ctrl Pts',(42.5862427720117,5.89653019866703,131.293095902467));
#149039=CARTESIAN_POINT('Ctrl Pts',(42.5788409503363,5.90952612988641,131.136301614717));
#149040=CARTESIAN_POINT('Ctrl Pts',(42.5714391286609,5.91627390182893,130.978866448102));
#149041=CARTESIAN_POINT('Ctrl Pts',(42.5640373069855,5.91672567172351,130.821327882166));
#149042=CARTESIAN_POINT('Ctrl Pts',(42.5566393926741,5.91717720313227,130.663872479614));
#149043=CARTESIAN_POINT('Ctrl Pts',(42.5492414783628,5.91133935055484,130.506314158799));
#149044=CARTESIAN_POINT('Ctrl Pts',(42.5418435640514,5.89921629927872,130.349192937667));
#149045=CARTESIAN_POINT('Ctrl Pts',(42.5344468791392,5.88709526263374,130.192097827232));
#149046=CARTESIAN_POINT('Ctrl Pts',(42.5270501942269,5.8686911289748,130.035440044143));
#149047=CARTESIAN_POINT('Ctrl Pts',(42.5196535093147,5.84406014394001,129.879757136872));
#149048=CARTESIAN_POINT('Ctrl Pts',(42.5122571523792,5.81943025106894,129.724081132744));
#149049=CARTESIAN_POINT('Ctrl Pts',(42.5048607954438,5.78857411414706,129.569380287195));
#149050=CARTESIAN_POINT('Ctrl Pts',(42.4974644385084,5.75159952456495,129.416184306169));
#149051=CARTESIAN_POINT('Ctrl Pts',(42.4900669491718,5.71461927407879,129.262964870447));
#149052=CARTESIAN_POINT('Ctrl Pts',(42.4826694598351,5.67151879332518,129.111251120904));
#149053=CARTESIAN_POINT('Ctrl Pts',(42.4752719704985,5.62245636104609,128.961559751864));
#149054=CARTESIAN_POINT('Ctrl Pts',(42.4678718879835,5.57337673000736,128.811815908746));
#149055=CARTESIAN_POINT('Ctrl Pts',(42.4604718054685,5.51833110255527,128.664096212138));
#149056=CARTESIAN_POINT('Ctrl Pts',(42.4530717229535,5.45752665518637,128.518899313927));
#149057=CARTESIAN_POINT('Ctrl Pts',(42.445663503287,5.39665534707674,128.3735427568));
#149058=CARTESIAN_POINT('Ctrl Pts',(42.4382552836205,5.3300127170849,128.230714882618));
#149059=CARTESIAN_POINT('Ctrl Pts',(42.430847063954,5.25785316887965,128.09089224351));
#149060=CARTESIAN_POINT('Ctrl Pts',(42.4234342846519,5.18564920767632,127.950983545901));
#149061=CARTESIAN_POINT('Ctrl Pts',(42.4160215053498,5.10792174604282,127.81408409294));
#149062=CARTESIAN_POINT('Ctrl Pts',(42.4086087260477,5.02496936505489,127.680642729734));
#149063=CARTESIAN_POINT('Ctrl Pts',(42.4011853550189,4.94189845781504,127.547010699251));
#149064=CARTESIAN_POINT('Ctrl Pts',(42.3937619839902,4.85358792975135,127.416846935062));
#149065=CARTESIAN_POINT('Ctrl Pts',(42.3863386129614,4.76037807793621,127.290569058921));
#149066=CARTESIAN_POINT('Ctrl Pts',(42.3824025635208,4.71095597796659,127.223613498998));
#149067=CARTESIAN_POINT('Ctrl Pts',(42.3784665140802,4.66015715365228,127.157749823019));
#149068=CARTESIAN_POINT('Ctrl Pts',(42.3745304646396,4.60803656078139,127.093036107771));
#149069=CARTESIAN_POINT('Ctrl Pts',(42.3671071982341,4.50973874925041,126.970988060455));
#149070=CARTESIAN_POINT('Ctrl Pts',(42.3596839318287,4.40644012034219,126.852663420469));
#149071=CARTESIAN_POINT('Ctrl Pts',(42.3522606654233,4.29845315506421,126.738498957817));
#149072=CARTESIAN_POINT('Ctrl Pts',(42.3448461727022,4.19059382141112,126.624469428078));
#149073=CARTESIAN_POINT('Ctrl Pts',(42.3374316799813,4.07805743524288,126.514590556936));
#149074=CARTESIAN_POINT('Ctrl Pts',(42.3300171872602,3.96119789902671,126.409267698497));
#149075=CARTESIAN_POINT('Ctrl Pts',(42.3226098409065,3.8444509964314,126.304046354195));
#149076=CARTESIAN_POINT('Ctrl Pts',(42.3152024945526,3.7233895145285,126.203372528709));
#149077=CARTESIAN_POINT('Ctrl Pts',(42.3077951481988,3.59840544002805,126.107616122527));
#149078=CARTESIAN_POINT('Ctrl Pts',(42.3003933265235,3.47351458336627,126.011931135086));
#149079=CARTESIAN_POINT('Ctrl Pts',(42.2929915048481,3.34470725445664,125.921156490321));
#149080=CARTESIAN_POINT('Ctrl Pts',(42.2855896831728,3.21240978987496,125.835622960533));
#149081=CARTESIAN_POINT('Ctrl Pts',(42.2781917688614,3.08018216409485,125.750134583229));
#149082=CARTESIAN_POINT('Ctrl Pts',(42.2707938545501,2.94446838459398,125.669882012963));
#149083=CARTESIAN_POINT('Ctrl Pts',(42.2633959402388,2.80572504601558,125.595153621423));
#149084=CARTESIAN_POINT('Ctrl Pts',(42.2559992553266,2.66700476406279,125.520437648387));
#149085=CARTESIAN_POINT('Ctrl Pts',(42.2486025704143,2.52525625058312,125.451244208928));
#149086=CARTESIAN_POINT('Ctrl Pts',(42.2412058855021,2.38096216247064,125.387816540077));
#149087=CARTESIAN_POINT('Ctrl Pts',(42.2338095285666,2.23667447250883,125.324391683675));
#149088=CARTESIAN_POINT('Ctrl Pts',(42.2264131716312,2.08984177408347,125.266732239761));
#149089=CARTESIAN_POINT('Ctrl Pts',(42.2190168146957,1.94096798768702,125.215033839387));
#149090=CARTESIAN_POINT('Ctrl Pts',(42.2116193253592,1.79207140833466,125.163327523855));
#149091=CARTESIAN_POINT('Ctrl Pts',(42.2042218360226,1.64113347145343,125.11758419154));
#149092=CARTESIAN_POINT('Ctrl Pts',(42.1968243466861,1.48867444013729,125.077949963956));
#149093=CARTESIAN_POINT('Ctrl Pts',(42.1894242641711,1.33616196454341,125.038301842654));
#149094=CARTESIAN_POINT('Ctrl Pts',(42.1820241816561,1.18212769394658,125.004767183732));
#149095=CARTESIAN_POINT('Ctrl Pts',(42.1746240991411,1.02710314225816,124.97744121726));
#149096=CARTESIAN_POINT('Ctrl Pts',(42.1672158794746,0.871908125138678,
124.950085203079));
#149097=CARTESIAN_POINT('Ctrl Pts',(42.1598076598081,0.715721020147045,
124.928951580348));
#149098=CARTESIAN_POINT('Ctrl Pts',(42.1523994401417,0.559080275483776,
124.914083900122));
#149099=CARTESIAN_POINT('Ctrl Pts',(42.1449866608396,0.402343121054518,
124.899207069086));
#149100=CARTESIAN_POINT('Ctrl Pts',(42.1375738815375,0.245152142473199,
124.890603885634));
#149101=CARTESIAN_POINT('Ctrl Pts',(42.1301611022354,0.0880463562037916,
124.888265756793));
#149102=CARTESIAN_POINT('Ctrl Pts',(42.1227377312066,-0.0692839101796727,
124.885924287124));
#149103=CARTESIAN_POINT('Ctrl Pts',(42.1153143601779,-0.226528368943481,
124.889865741497));
#149104=CARTESIAN_POINT('Ctrl Pts',(42.1078909891491,-0.383151724199011,
124.900029553106));
#149105=CARTESIAN_POINT('Ctrl Pts',(42.1039549397083,-0.466197185281535,
124.905418649899));
#149106=CARTESIAN_POINT('Ctrl Pts',(42.1000188902675,-0.549068166615232,
124.912556213816));
#149107=CARTESIAN_POINT('Ctrl Pts',(42.0960828408267,-0.631686101607738,
124.921427400918));
#149108=CARTESIAN_POINT('Ctrl Pts',(42.0886595744213,-0.787500948585284,
124.938158182934));
#149109=CARTESIAN_POINT('Ctrl Pts',(42.0812363080159,-0.942886251466519,
124.961108886852));
#149110=CARTESIAN_POINT('Ctrl Pts',(42.0738130416105,-1.09730563966232,
124.990252698404));
#149111=CARTESIAN_POINT('Ctrl Pts',(42.0663985488895,-1.25154251696522,
125.019362064391));
#149112=CARTESIAN_POINT('Ctrl Pts',(42.0589840561685,-1.40481538876541,
125.054649899477));
#149113=CARTESIAN_POINT('Ctrl Pts',(42.0515695634475,-1.55659192624549,
125.09603755929));
#149114=CARTESIAN_POINT('Ctrl Pts',(42.0441622170937,-1.70822217578466,
125.137385328118));
#149115=CARTESIAN_POINT('Ctrl Pts',(42.03675487074,-1.85835860445632,125.184821119712));
#149116=CARTESIAN_POINT('Ctrl Pts',(42.0293475243862,-2.00647812611256,
125.2382150848));
#149117=CARTESIAN_POINT('Ctrl Pts',(42.0219457027108,-2.15448717464132,
125.291569226655));
#149118=CARTESIAN_POINT('Ctrl Pts',(42.0145438810354,-2.30048196172353,
125.35087256769));
#149119=CARTESIAN_POINT('Ctrl Pts',(42.00714205936,-2.44395375392194,125.415945209379));
#149120=CARTESIAN_POINT('Ctrl Pts',(41.9997441450487,-2.58734980847783,
125.480983499726));
#149121=CARTESIAN_POINT('Ctrl Pts',(41.9923462307374,-2.72822518152775,
125.551784871527));
#149122=CARTESIAN_POINT('Ctrl Pts',(41.984948316426,-2.866090457244,125.628121050719));
#149123=CARTESIAN_POINT('Ctrl Pts',(41.9775516315138,-3.00393282225275,
125.704444544223));
#149124=CARTESIAN_POINT('Ctrl Pts',(41.9701549466016,-3.1387657564655,125.786300838968));
#149125=CARTESIAN_POINT('Ctrl Pts',(41.9627582616894,-3.27012372983875,
125.873415337597));
#149126=CARTESIAN_POINT('Ctrl Pts',(41.955361904754,-3.40147587866162,125.960525973478));
#149127=CARTESIAN_POINT('Ctrl Pts',(41.9479655478186,-3.52935306191335,
126.052894143335));
#149128=CARTESIAN_POINT('Ctrl Pts',(41.9405691908831,-3.65331830831435,
126.150201627949));
#149129=CARTESIAN_POINT('Ctrl Pts',(41.9331717015466,-3.77730253411086,
126.247524010587));
#149130=CARTESIAN_POINT('Ctrl Pts',(41.92577421221,-3.89737333685454,126.34978698321));
#149131=CARTESIAN_POINT('Ctrl Pts',(41.9183767228735,-4.01312656546657,
126.456631815991));
#149132=CARTESIAN_POINT('Ctrl Pts',(41.9109766403586,-4.12892037119295,
126.563514103062));
#149133=CARTESIAN_POINT('Ctrl Pts',(41.9035765578436,-4.24039331524811,
126.674981195114));
#149134=CARTESIAN_POINT('Ctrl Pts',(41.8961764753286,-4.34717798162448,
126.79063738862));
#149135=CARTESIAN_POINT('Ctrl Pts',(41.8887682556622,-4.45408006872018,
126.906420758002));
#149136=CARTESIAN_POINT('Ctrl Pts',(41.8813600359958,-4.55628332938965,
127.026402153576));
#149137=CARTESIAN_POINT('Ctrl Pts',(41.8739518163293,-4.65346007849235,
127.150152104033));
#149138=CARTESIAN_POINT('Ctrl Pts',(41.8665390370272,-4.75069663826223,
127.273978220518));
#149139=CARTESIAN_POINT('Ctrl Pts',(41.8591262577252,-4.84290030368096,
127.401577211877));
#149140=CARTESIAN_POINT('Ctrl Pts',(41.8517134784232,-4.9297869526943,127.532490943581));
#149141=CARTESIAN_POINT('Ctrl Pts',(41.8442901073945,-5.01679774942646,
127.663591730964));
#149142=CARTESIAN_POINT('Ctrl Pts',(41.8368667363657,-5.09847616310607,
127.79801639988));
#149143=CARTESIAN_POINT('Ctrl Pts',(41.829443365337,-5.17458380979925,127.935281852899));
#149144=CARTESIAN_POINT('Ctrl Pts',(41.8255073158959,-5.21493791025638,
128.008063289734));
#149145=CARTESIAN_POINT('Ctrl Pts',(41.8215712664549,-5.25372666523621,
128.081643021004));
#149146=CARTESIAN_POINT('Ctrl Pts',(41.8176352170139,-5.29092009620234,
128.155946922899));
#149147=CARTESIAN_POINT('Ctrl Pts',(41.8096921274624,-5.36597777962749,
128.305894873405));
#149148=CARTESIAN_POINT('Ctrl Pts',(41.8017490379109,-5.43473806517258,
128.459197098472));
#149149=CARTESIAN_POINT('Ctrl Pts',(41.7938059483595,-5.49691040210597,
128.615318225624));
#149150=CARTESIAN_POINT('Ctrl Pts',(41.7858780055998,-5.55896418171488,
128.77114164315));
#149151=CARTESIAN_POINT('Ctrl Pts',(41.7779500628403,-5.61445495316443,
128.929772973799));
#149152=CARTESIAN_POINT('Ctrl Pts',(41.7700221200806,-5.66313861815877,
129.090653654862));
#149153=CARTESIAN_POINT('Ctrl Pts',(41.7621157324991,-5.7116899177838,129.251096919582));
#149154=CARTESIAN_POINT('Ctrl Pts',(41.7542093449176,-5.7534709436117,129.413777056059));
#149155=CARTESIAN_POINT('Ctrl Pts',(41.7463029573361,-5.78828636125568,
129.578117753121));
#149156=CARTESIAN_POINT('Ctrl Pts',(41.7384097906993,-5.82304356107211,
129.742183642095));
#149157=CARTESIAN_POINT('Ctrl Pts',(41.7305166240624,-5.8508583106983,129.907904271569));
#149158=CARTESIAN_POINT('Ctrl Pts',(41.7226234574255,-5.87158482744633,
130.074687967262));
#149159=CARTESIAN_POINT('Ctrl Pts',(41.7147488404953,-5.89226263487094,
130.241079705103));
#149160=CARTESIAN_POINT('Ctrl Pts',(41.7068742235651,-5.90588539747435,
130.408529236549));
#149161=CARTESIAN_POINT('Ctrl Pts',(41.698999606635,-5.91235828421885,130.576435012316));
#149162=CARTESIAN_POINT('Ctrl Pts',(41.6954581533194,-5.91526933708988,
130.651947316161));
#149163=CARTESIAN_POINT('Ctrl Pts',(41.6919167000038,-5.91673495586757,
130.727551735458));
#149164=CARTESIAN_POINT('Ctrl Pts',(41.6883752466882,-5.91674988476282,
130.803192859412));
#149165=CARTESIAN_POINT('',(39.9383751911717,-5.91572623955714,130.809823626609));
#149166=CARTESIAN_POINT('Ctrl Pts',(41.6883751922116,-5.90714223694013,
130.803195917287));
#149167=CARTESIAN_POINT('Ctrl Pts',(41.6386459925414,-5.90528448095996,
131.86362665666));
#149168=CARTESIAN_POINT('Ctrl Pts',(41.496100918267,-5.12530615771963,134.905822374616));
#149169=CARTESIAN_POINT('Ctrl Pts',(41.2607399693881,-0.247820295217642,
137.79836845511));
#149170=CARTESIAN_POINT('Ctrl Pts',(40.9822923455752,5.75030395140879,134.793290924898));
#149171=CARTESIAN_POINT('Ctrl Pts',(40.7038447217622,6.4641797846552,128.122581312326));
#149172=CARTESIAN_POINT('Ctrl Pts',(40.4253970979495,1.23779018854298,123.916295869069));
#149173=CARTESIAN_POINT('Ctrl Pts',(40.1702405880992,-4.59375490894458,
125.86218170759));
#149174=CARTESIAN_POINT('Ctrl Pts',(40.0078999528533,-5.90222128016794,
129.332638640001));
#149175=CARTESIAN_POINT('Ctrl Pts',(39.9383751922116,-5.91565475715166,
130.809823538498));
#149176=CARTESIAN_POINT('',(38.1883744840812,-5.92195841769095,130.803134636241));
#149177=CARTESIAN_POINT('Ctrl Pts',(39.9383751763149,-5.91674747680489,
130.809824885406));
#149178=CARTESIAN_POINT('Ctrl Pts',(39.9288809276006,-5.91656114752689,
131.011583532271));
#149179=CARTESIAN_POINT('Ctrl Pts',(39.9193866788863,-5.90605155807218,
131.212880654709));
#149180=CARTESIAN_POINT('Ctrl Pts',(39.909892430172,-5.88538083791949,131.412820111));
#149181=CARTESIAN_POINT('Ctrl Pts',(39.9001899609273,-5.86425678349646,
131.617144485033));
#149182=CARTESIAN_POINT('Ctrl Pts',(39.8904874916825,-5.83252101133659,
131.820051237144));
#149183=CARTESIAN_POINT('Ctrl Pts',(39.8807850224378,-5.79039458226029,
132.020609417866));
#149184=CARTESIAN_POINT('Ctrl Pts',(39.8766906317331,-5.77261745199748,
132.105243909375));
#149185=CARTESIAN_POINT('Ctrl Pts',(39.8725962410283,-5.75299053662962,
132.189460452012));
#149186=CARTESIAN_POINT('Ctrl Pts',(39.8685018503236,-5.73153296479048,
132.273190231926));
#149187=CARTESIAN_POINT('Ctrl Pts',(39.8610785839182,-5.69262967400549,
132.424995105271));
#149188=CARTESIAN_POINT('Ctrl Pts',(39.8536553175129,-5.64763235567367,
132.575482873891));
#149189=CARTESIAN_POINT('Ctrl Pts',(39.8462320511075,-5.59664446794347,
132.724126556929));
#149190=CARTESIAN_POINT('Ctrl Pts',(39.8388175583866,-5.54571684366221,
132.872594555478));
#149191=CARTESIAN_POINT('Ctrl Pts',(39.8314030656656,-5.48881286340787,
133.019222457208));
#149192=CARTESIAN_POINT('Ctrl Pts',(39.8239885729446,-5.42608670005231,
133.163494714224));
#149193=CARTESIAN_POINT('Ctrl Pts',(39.8165812265909,-5.36342099453469,
133.307627916207));
#149194=CARTESIAN_POINT('Ctrl Pts',(39.8091738802373,-5.2949444254275,133.44940965347));
#149195=CARTESIAN_POINT('Ctrl Pts',(39.8017665338836,-5.22086051571906,
133.588340868557));
#149196=CARTESIAN_POINT('Ctrl Pts',(39.7943647122082,-5.1468318605854,133.727168463501));
#149197=CARTESIAN_POINT('Ctrl Pts',(39.7869628905328,-5.06720436699781,
133.863149441501));
#149198=CARTESIAN_POINT('Ctrl Pts',(39.7795610688575,-4.98222903153145,
133.995806127028));
#149199=CARTESIAN_POINT('Ctrl Pts',(39.7721631545462,-4.89729855388323,
134.128392784123));
#149200=CARTESIAN_POINT('Ctrl Pts',(39.7647652402349,-4.80702605750756,
134.257658330108));
#149201=CARTESIAN_POINT('Ctrl Pts',(39.7573673259236,-4.71170764412821,
134.383151144932));
#149202=CARTESIAN_POINT('Ctrl Pts',(39.7499706410115,-4.61640507094005,
134.508623105127));
#149203=CARTESIAN_POINT('Ctrl Pts',(39.7425739560993,-4.51605847057263,
134.630323281512));
#149204=CARTESIAN_POINT('Ctrl Pts',(39.7351772711872,-4.41100636374977,
134.747830336159));
#149205=CARTESIAN_POINT('Ctrl Pts',(39.7277809142518,-4.30595891504757,
134.86533218042));
#149206=CARTESIAN_POINT('Ctrl Pts',(39.7203845573165,-4.19620662355086,
134.978640994331));
#149207=CARTESIAN_POINT('Ctrl Pts',(39.7129882003811,-4.08212708532021,
135.087369959348));
#149208=CARTESIAN_POINT('Ctrl Pts',(39.7055907110446,-3.96803008122102,
135.196115571048));
#149209=CARTESIAN_POINT('Ctrl Pts',(39.6981932217081,-3.84960478147709,
135.300279680133));
#149210=CARTESIAN_POINT('Ctrl Pts',(39.6907957323716,-3.72726416725788,
135.399513758646));
#149211=CARTESIAN_POINT('Ctrl Pts',(39.6833956498567,-3.60488066672601,
135.498782623511));
#149212=CARTESIAN_POINT('Ctrl Pts',(39.6759955673418,-3.4785794088019,135.593117781928));
#149213=CARTESIAN_POINT('Ctrl Pts',(39.6685954848269,-3.34880469798308,
135.6822123637));
#149214=CARTESIAN_POINT('Ctrl Pts',(39.6611872651605,-3.21888728652836,
135.771404914125));
#149215=CARTESIAN_POINT('Ctrl Pts',(39.6537790454941,-3.0854891024902,135.855345168296));
#149216=CARTESIAN_POINT('Ctrl Pts',(39.6463708258277,-2.94908217128925,
135.933770418848));
#149217=CARTESIAN_POINT('Ctrl Pts',(39.6389580465257,-2.81259128389822,
136.012243938832));
#149218=CARTESIAN_POINT('Ctrl Pts',(39.6315452672237,-2.67308828936398,
136.085195518857));
#149219=CARTESIAN_POINT('Ctrl Pts',(39.6241324879217,-2.5310673326472,136.152409674943));
#149220=CARTESIAN_POINT('Ctrl Pts',(39.616709116893,-2.38884344972733,136.219719869767));
#149221=CARTESIAN_POINT('Ctrl Pts',(39.6092857458643,-2.24409476166139,
136.281276121904));
#149222=CARTESIAN_POINT('Ctrl Pts',(39.6018623748356,-2.09733355896172,
136.336911792653));
#149223=CARTESIAN_POINT('Ctrl Pts',(39.5979263253939,-2.01951724778617,
136.36641116025));
#149224=CARTESIAN_POINT('Ctrl Pts',(39.5939902759524,-1.94113538050561,
136.394246879217));
#149225=CARTESIAN_POINT('Ctrl Pts',(39.5900542265107,-1.86226561396691,
136.420399911013));
#149226=CARTESIAN_POINT('Ctrl Pts',(39.5826309601053,-1.71351969574773,
136.46972371276));
#149227=CARTESIAN_POINT('Ctrl Pts',(39.5752076936998,-1.56258792429142,
136.513208509265));
#149228=CARTESIAN_POINT('Ctrl Pts',(39.5677844272944,-1.40996958517554,
136.550656496772));
#149229=CARTESIAN_POINT('Ctrl Pts',(39.5603699345734,-1.25753162826233,
136.588060223867));
#149230=CARTESIAN_POINT('Ctrl Pts',(39.5529554418523,-1.10341143053259,
136.619441256146));
#149231=CARTESIAN_POINT('Ctrl Pts',(39.5455409491313,-0.948126071235282,
136.64465063738));
#149232=CARTESIAN_POINT('Ctrl Pts',(39.5381336027775,-0.792990381813435,
136.669835720864));
#149233=CARTESIAN_POINT('Ctrl Pts',(39.5307262564237,-0.636692132549131,
136.688860936119));
#149234=CARTESIAN_POINT('Ctrl Pts',(39.5233189100699,-0.479761203760998,
136.701627760054));
#149235=CARTESIAN_POINT('Ctrl Pts',(39.5159170883945,-0.32294731998022,
136.714385062009));
#149236=CARTESIAN_POINT('Ctrl Pts',(39.5085152667191,-0.165502066712273,
136.720893236615));
#149237=CARTESIAN_POINT('Ctrl Pts',(39.5011134450436,-0.0079629956869028,
136.721105259107));
#149238=CARTESIAN_POINT('Ctrl Pts',(39.4937155307323,0.14949291168893,136.721317169674));
#149239=CARTESIAN_POINT('Ctrl Pts',(39.4863176164209,0.307042165836828,
136.715239546913));
#149240=CARTESIAN_POINT('Ctrl Pts',(39.4789197021096,0.464144755804185,
136.702877397924));
#149241=CARTESIAN_POINT('Ctrl Pts',(39.4715230171974,0.62122123817122,136.690517303299));
#149242=CARTESIAN_POINT('Ctrl Pts',(39.4641263322851,0.777850831894141,
136.671874784474));
#149243=CARTESIAN_POINT('Ctrl Pts',(39.4567296473729,0.933496074720745,
136.647006905078));
#149244=CARTESIAN_POINT('Ctrl Pts',(39.4493332904375,1.08913441607418,136.622140128351));
#149245=CARTESIAN_POINT('Ctrl Pts',(39.4419369335021,1.24378812469433,136.591048598808));
#149246=CARTESIAN_POINT('Ctrl Pts',(39.4345405765666,1.39692765929057,136.553840913837));
#149247=CARTESIAN_POINT('Ctrl Pts',(39.42714308723,1.55009063994051,136.516627532275));
#149248=CARTESIAN_POINT('Ctrl Pts',(39.4197455978935,1.70173862220643,136.47329621893));
#149249=CARTESIAN_POINT('Ctrl Pts',(39.4123481085569,1.85135515323665,136.424006038683));
#149250=CARTESIAN_POINT('Ctrl Pts',(39.4049480260419,2.0010241321101,136.37469857984));
#149251=CARTESIAN_POINT('Ctrl Pts',(39.3975479435268,2.14865988758613,136.319428211898));
#149252=CARTESIAN_POINT('Ctrl Pts',(39.3901478610118,2.2937640836433,136.258402869977));
#149253=CARTESIAN_POINT('Ctrl Pts',(39.3827396413453,2.4390278366809,136.19731042442));
#149254=CARTESIAN_POINT('Ctrl Pts',(39.3753314216789,2.58175412673234,136.130450511889));
#149255=CARTESIAN_POINT('Ctrl Pts',(39.3679232020125,2.72146678937886,136.058078260988));
#149256=CARTESIAN_POINT('Ctrl Pts',(39.3605104227104,2.86126544283821,135.985661466175));
#149257=CARTESIAN_POINT('Ctrl Pts',(39.3530976434082,2.99804644930585,135.907725756886));
#149258=CARTESIAN_POINT('Ctrl Pts',(39.3456848641062,3.1313614185855,135.824570396917));
#149259=CARTESIAN_POINT('Ctrl Pts',(39.3382614930774,3.26486687454492,135.74129622067));
#149260=CARTESIAN_POINT('Ctrl Pts',(39.3308381220487,3.3948960944153,135.652787707778));
#149261=CARTESIAN_POINT('Ctrl Pts',(39.3234147510199,3.52103197480109,135.559385790468));
#149262=CARTESIAN_POINT('Ctrl Pts',(39.3194787015792,3.58791224516892,135.509861852763));
#149263=CARTESIAN_POINT('Ctrl Pts',(39.3155426521385,3.65369853771744,135.458962853969));
#149264=CARTESIAN_POINT('Ctrl Pts',(39.3116066026978,3.7183328593593,135.406743838193));
#149265=CARTESIAN_POINT('Ctrl Pts',(39.3041833362924,3.84023117281087,135.308260404137));
#149266=CARTESIAN_POINT('Ctrl Pts',(39.296760069887,3.95839847284968,135.204781824887));
#149267=CARTESIAN_POINT('Ctrl Pts',(39.2893368034815,4.07239846552338,135.096621245778));
#149268=CARTESIAN_POINT('Ctrl Pts',(39.2819223107605,4.18626371967286,134.988588503492));
#149269=CARTESIAN_POINT('Ctrl Pts',(39.2745078180395,4.29597120235384,134.875885030702));
#149270=CARTESIAN_POINT('Ctrl Pts',(39.2670933253185,4.40111609850937,134.758865346346));
#149271=CARTESIAN_POINT('Ctrl Pts',(39.2596859789647,4.5061596520555,134.641958449967));
#149272=CARTESIAN_POINT('Ctrl Pts',(39.2522786326109,4.60664912599584,134.520743899827));
#149273=CARTESIAN_POINT('Ctrl Pts',(39.2448712862571,4.70221521680818,134.395614245106));
#149274=CARTESIAN_POINT('Ctrl Pts',(39.2374694645817,4.79771003082449,134.270577916802));
#149275=CARTESIAN_POINT('Ctrl Pts',(39.2300676429062,4.88828854764652,134.141632593492));
#149276=CARTESIAN_POINT('Ctrl Pts',(39.2226658212308,4.97362064416872,134.009205114636));
#149277=CARTESIAN_POINT('Ctrl Pts',(39.2152679069195,5.05890769454127,133.876847543215));
#149278=CARTESIAN_POINT('Ctrl Pts',(39.2078699926081,5.13895363860715,133.741011790118));
#149279=CARTESIAN_POINT('Ctrl Pts',(39.2004720782968,5.21347079986936,133.60215488831));
#149280=CARTESIAN_POINT('Ctrl Pts',(39.1930753933846,5.28797557773124,133.463321062001));
#149281=CARTESIAN_POINT('Ctrl Pts',(39.1856787084723,5.3569532199578,133.321467412027));
#149282=CARTESIAN_POINT('Ctrl Pts',(39.1782820235601,5.42016122432172,133.17707696489));
#149283=CARTESIAN_POINT('Ctrl Pts',(39.1708856666247,5.48336642597648,133.032692920177));
#149284=CARTESIAN_POINT('Ctrl Pts',(39.1634893096892,5.54080234875001,132.885772643923));
#149285=CARTESIAN_POINT('Ctrl Pts',(39.1560929527538,5.59227412869818,132.736820353755));
#149286=CARTESIAN_POINT('Ctrl Pts',(39.1486954634172,5.64375378910726,132.587845258612));
#149287=CARTESIAN_POINT('Ctrl Pts',(39.1412979740807,5.68926736660663,132.436837882949));
#149288=CARTESIAN_POINT('Ctrl Pts',(39.1339004847441,5.72866953160297,132.284318711629));
#149289=CARTESIAN_POINT('Ctrl Pts',(39.1265004022291,5.76808550896718,132.131746074951));
#149290=CARTESIAN_POINT('Ctrl Pts',(39.1191003197141,5.80138571511799,131.977660948681));
#149291=CARTESIAN_POINT('Ctrl Pts',(39.1117002371991,5.82847572896873,131.822594991039));
#149292=CARTESIAN_POINT('Ctrl Pts',(39.1042920175326,5.85559553107463,131.667358522436));
#149293=CARTESIAN_POINT('Ctrl Pts',(39.0968837978661,5.87649143914705,131.51113943653));
#149294=CARTESIAN_POINT('Ctrl Pts',(39.0894755781997,5.89112072160808,131.354476247175));
#149295=CARTESIAN_POINT('Ctrl Pts',(39.0820627988976,5.90575900814838,131.197716634241));
#149296=CARTESIAN_POINT('Ctrl Pts',(39.0746500195955,5.91412296372715,131.040512745104));
#149297=CARTESIAN_POINT('Ctrl Pts',(39.0672372402934,5.91622200159782,130.883403582527));
#149298=CARTESIAN_POINT('Ctrl Pts',(39.0598138692646,5.91832403867224,130.726069935011));
#149299=CARTESIAN_POINT('Ctrl Pts',(39.0523904982359,5.91414328956474,130.568831656556));
#149300=CARTESIAN_POINT('Ctrl Pts',(39.0449671272071,5.90374113564045,130.412223950259));
#149301=CARTESIAN_POINT('Ctrl Pts',(39.0410310777664,5.89822566403367,130.329186786632));
#149302=CARTESIAN_POINT('Ctrl Pts',(39.0370950283257,5.8909619928557,130.246326763421));
#149303=CARTESIAN_POINT('Ctrl Pts',(39.033158978885,5.88196508559281,130.163722424537));
#149304=CARTESIAN_POINT('Ctrl Pts',(39.0257357124796,5.86499719927847,130.007933219393));
#149305=CARTESIAN_POINT('Ctrl Pts',(39.0183124460742,5.8418100519577,129.852583023509));
#149306=CARTESIAN_POINT('Ctrl Pts',(39.0108891796687,5.81243127413145,129.698208166048));
#149307=CARTESIAN_POINT('Ctrl Pts',(39.0034746869477,5.78308721958079,129.544015766849));
#149308=CARTESIAN_POINT('Ctrl Pts',(38.9960601942267,5.74756617013776,129.390796774614));
#149309=CARTESIAN_POINT('Ctrl Pts',(38.9886457015057,5.70594758019843,129.239083397861));
#149310=CARTESIAN_POINT('Ctrl Pts',(38.981238355152,5.66436910382299,129.087516248173));
#149311=CARTESIAN_POINT('Ctrl Pts',(38.9738310087982,5.61670488507211,128.937452182556));
#149312=CARTESIAN_POINT('Ctrl Pts',(38.9664236624444,5.56308556911545,128.789414088946));
#149313=CARTESIAN_POINT('Ctrl Pts',(38.959021840769,5.50950624446756,128.64148640773));
#149314=CARTESIAN_POINT('Ctrl Pts',(38.9516200190936,5.44998079289106,128.495582039298));
#149315=CARTESIAN_POINT('Ctrl Pts',(38.9442181974182,5.38468988691117,128.35220944272));
#149316=CARTESIAN_POINT('Ctrl Pts',(38.9368202831068,5.31943344749233,128.208912531421));
#149317=CARTESIAN_POINT('Ctrl Pts',(38.9294223687955,5.24841776934164,128.068145069138));
#149318=CARTESIAN_POINT('Ctrl Pts',(38.9220244544841,5.17187187106469,127.930396123737));
#149319=CARTESIAN_POINT('Ctrl Pts',(38.9146277695719,5.09533869332735,127.792670069712));
#149320=CARTESIAN_POINT('Ctrl Pts',(38.9072310846597,5.01327730059677,127.65796186298));
#149321=CARTESIAN_POINT('Ctrl Pts',(38.8998343997475,4.92596299837052,127.526736615154));
#149322=CARTESIAN_POINT('Ctrl Pts',(38.8924380428121,4.83865256775205,127.395517185994));
#149323=CARTESIAN_POINT('Ctrl Pts',(38.8850416858767,4.74608989755134,127.267780719453));
#149324=CARTESIAN_POINT('Ctrl Pts',(38.8776453289412,4.64859387161577,127.143963702029));
#149325=CARTESIAN_POINT('Ctrl Pts',(38.8702478396046,4.55108291878959,127.020127727903));
#149326=CARTESIAN_POINT('Ctrl Pts',(38.8628503502681,4.44863733726269,126.900212691035));
#149327=CARTESIAN_POINT('Ctrl Pts',(38.8554528609315,4.34161647149663,126.78462219611));
#149328=CARTESIAN_POINT('Ctrl Pts',(38.8480527784165,4.23455808973198,126.668991181117));
#149329=CARTESIAN_POINT('Ctrl Pts',(38.8406526959015,4.12292148391106,126.557688000084));
#149330=CARTESIAN_POINT('Ctrl Pts',(38.8332526133865,4.00710291624785,126.4510794664));
#149331=CARTESIAN_POINT('Ctrl Pts',(38.82584439372,3.89115699416305,126.344353705674));
#149332=CARTESIAN_POINT('Ctrl Pts',(38.8184361740536,3.77102020156013,126.242333154614));
#149333=CARTESIAN_POINT('Ctrl Pts',(38.8110279543871,3.64712250793451,126.145344844399));
#149334=CARTESIAN_POINT('Ctrl Pts',(38.803615175085,3.52314855734582,126.048296839498));
#149335=CARTESIAN_POINT('Ctrl Pts',(38.796202395783,3.39540939546134,125.956287464793));
#149336=CARTESIAN_POINT('Ctrl Pts',(38.7887896164809,3.26436358866415,125.869600144807));
#149337=CARTESIAN_POINT('Ctrl Pts',(38.7813662454522,3.13313053747277,125.782788961913));
#149338=CARTESIAN_POINT('Ctrl Pts',(38.7739428744234,2.99858172357663,125.701315214279));
#149339=CARTESIAN_POINT('Ctrl Pts',(38.7665195033946,2.86120060662562,125.62541655037));
#149340=CARTESIAN_POINT('Ctrl Pts',(38.7625834539538,2.78835784200169,125.585173257601));
#149341=CARTESIAN_POINT('Ctrl Pts',(38.7586474045129,2.71471916605623,125.546496523365));
#149342=CARTESIAN_POINT('Ctrl Pts',(38.754711355072,2.64035874813627,125.509416213359));
#149343=CARTESIAN_POINT('Ctrl Pts',(38.7472880886666,2.50011732065159,125.439483905927));
#149344=CARTESIAN_POINT('Ctrl Pts',(38.7398648222612,2.35688358160388,125.375021334148));
#149345=CARTESIAN_POINT('Ctrl Pts',(38.7324415558557,2.21112369486684,125.31629515071));
#149346=CARTESIAN_POINT('Ctrl Pts',(38.7250270631347,2.0655360842111,125.257638376744));
#149347=CARTESIAN_POINT('Ctrl Pts',(38.7176125704137,1.9174286117822,125.204704633764));
#149348=CARTESIAN_POINT('Ctrl Pts',(38.7101980776927,1.76729198672081,125.157714746239));
#149349=CARTESIAN_POINT('Ctrl Pts',(38.7027907313389,1.6173000689914,125.110770149337));
#149350=CARTESIAN_POINT('Ctrl Pts',(38.6953833849851,1.46528324605487,125.069758113509));
#149351=CARTESIAN_POINT('Ctrl Pts',(38.6879760386313,1.31175205524416,125.034851356973));
#149352=CARTESIAN_POINT('Ctrl Pts',(38.6805742169559,1.15833537378774,124.999970635214));
#149353=CARTESIAN_POINT('Ctrl Pts',(38.6731723952805,1.00340693583127,124.971186208423));
#149354=CARTESIAN_POINT('Ctrl Pts',(38.6657705736051,0.847492180306439,
124.948620906238));
#149355=CARTESIAN_POINT('Ctrl Pts',(38.6583726592937,0.691659730967629,
124.926067516101));
#149356=CARTESIAN_POINT('Ctrl Pts',(38.6509747449823,0.5348423695119,124.909726765597));
#149357=CARTESIAN_POINT('Ctrl Pts',(38.643576830671,0.377575352737061,124.899670328016));
#149358=CARTESIAN_POINT('Ctrl Pts',(38.6361801457588,0.220334470887072,
124.889615561632));
#149359=CARTESIAN_POINT('Ctrl Pts',(38.6287834608465,0.0626444541963754,
124.885843059267));
#149360=CARTESIAN_POINT('Ctrl Pts',(38.6213867759343,-0.0949545764154013,
124.888372602795));
#149361=CARTESIAN_POINT('Ctrl Pts',(38.6139904189989,-0.252546618921009,
124.89090203416));
#149362=CARTESIAN_POINT('Ctrl Pts',(38.6065940620634,-0.41004731011999,
124.899732949809));
#149363=CARTESIAN_POINT('Ctrl Pts',(38.5991977051279,-0.566917057050841,
124.914832995343));
#149364=CARTESIAN_POINT('Ctrl Pts',(38.5918002157913,-0.723810821140417,
124.929935352733));
#149365=CARTESIAN_POINT('Ctrl Pts',(38.5844027264547,-0.880073077015787,
124.951308715367));
#149366=CARTESIAN_POINT('Ctrl Pts',(38.5770052371182,-1.03517002616573,
124.978868914763));
#149367=CARTESIAN_POINT('Ctrl Pts',(38.5696051546031,-1.190321344311,125.006438775344));
#149368=CARTESIAN_POINT('Ctrl Pts',(38.5622050720881,-1.34430617510638,
125.040199725455));
#149369=CARTESIAN_POINT('Ctrl Pts',(38.5548049895731,-1.4966017186534,125.080016650069));
#149370=CARTESIAN_POINT('Ctrl Pts',(38.5473967699066,-1.64906472680669,
125.119877357484));
#149371=CARTESIAN_POINT('Ctrl Pts',(38.5399885502401,-1.79983437669202,
125.165807243714));
#149372=CARTESIAN_POINT('Ctrl Pts',(38.5325803305736,-1.94840311870171,
125.217621331584));
#149373=CARTESIAN_POINT('Ctrl Pts',(38.5251675512716,-2.0970633022931,125.269467310161));
#149374=CARTESIAN_POINT('Ctrl Pts',(38.5177547719695,-2.24351953227452,
125.327204570334));
#149375=CARTESIAN_POINT('Ctrl Pts',(38.5103419926675,-2.38728548923707,
125.390600505095));
#149376=CARTESIAN_POINT('Ctrl Pts',(38.5029186216387,-2.53125686574089,
125.454087022941));
#149377=CARTESIAN_POINT('Ctrl Pts',(38.4954952506099,-2.67252995753066,
125.52324819999));
#149378=CARTESIAN_POINT('Ctrl Pts',(38.4880718795811,-2.81064350247165,
125.597805742746));
#149379=CARTESIAN_POINT('Ctrl Pts',(38.4841358301405,-2.88387461798553,
125.637337940897));
#149380=CARTESIAN_POINT('Ctrl Pts',(38.4801997806998,-2.95621795294915,
125.678386524937));
#149381=CARTESIAN_POINT('Ctrl Pts',(38.4762637312592,-3.0276082901613,125.720905237232));
#149382=CARTESIAN_POINT('Ctrl Pts',(38.4688404648538,-3.16224823813214,
125.80109420166));
#149383=CARTESIAN_POINT('Ctrl Pts',(38.4614171984484,-3.29390376007871,
125.886757208278));
#149384=CARTESIAN_POINT('Ctrl Pts',(38.4539939320429,-3.42209854058113,
125.977646192509));
#149385=CARTESIAN_POINT('Ctrl Pts',(38.4465794393219,-3.5501418054991,126.068427753509));
#149386=CARTESIAN_POINT('Ctrl Pts',(38.439164946601,-3.67473216920356,126.164422783625));
#149387=CARTESIAN_POINT('Ctrl Pts',(38.4317504538799,-3.79541860553706,
126.26533779638));
#149388=CARTESIAN_POINT('Ctrl Pts',(38.4243431075262,-3.91598871973946,
126.366155543447));
#149389=CARTESIAN_POINT('Ctrl Pts',(38.4169357611724,-4.03266211301745,
126.471883594784));
#149390=CARTESIAN_POINT('Ctrl Pts',(38.4095284148186,-4.14501751474261,
126.582185779289));
#149391=CARTESIAN_POINT('Ctrl Pts',(38.4021265931432,-4.2572891175704,126.692405696264));
#149392=CARTESIAN_POINT('Ctrl Pts',(38.3947247714678,-4.36524887609951,
126.807192693139));
#149393=CARTESIAN_POINT('Ctrl Pts',(38.3873229497923,-4.46850943770092,
126.926171095679));
#149394=CARTESIAN_POINT('Ctrl Pts',(38.379925035481,-4.5717154888555,127.045086690445));
#149395=CARTESIAN_POINT('Ctrl Pts',(38.3725271211697,-4.67022703939225,
127.168189003144));
#149396=CARTESIAN_POINT('Ctrl Pts',(38.3651292068583,-4.76369446916959,
127.295066448235));
#149397=CARTESIAN_POINT('Ctrl Pts',(38.3577325219461,-4.85714636635578,
127.421922808596));
#149398=CARTESIAN_POINT('Ctrl Pts',(38.3503358370339,-4.94555558525297,
127.552552755974));
#149399=CARTESIAN_POINT('Ctrl Pts',(38.3429391521217,-5.02861353425828,
127.686512563928));
#149400=CARTESIAN_POINT('Ctrl Pts',(38.3355427951862,-5.11166780038709,
127.820466431964));
#149401=CARTESIAN_POINT('Ctrl Pts',(38.3281464382508,-5.18937107170843,
127.957749549736));
#149402=CARTESIAN_POINT('Ctrl Pts',(38.3207500813153,-5.2614589057177,128.097890454061));
#149403=CARTESIAN_POINT('Ctrl Pts',(38.3133525919788,-5.33355777655829,
128.238052814316));
#149404=CARTESIAN_POINT('Ctrl Pts',(38.3059551026421,-5.40003932746775,
128.381073500337));
#149405=CARTESIAN_POINT('Ctrl Pts',(38.2985576133056,-5.46068584063949,
128.526457917199));
#149406=CARTESIAN_POINT('Ctrl Pts',(38.2911575307906,-5.52135361335258,
128.671893298343));
#149407=CARTESIAN_POINT('Ctrl Pts',(38.2837574482756,-5.5761821321981,128.81969371576));
#149408=CARTESIAN_POINT('Ctrl Pts',(38.2763573657606,-5.62500248715958,
128.969346290116));
#149409=CARTESIAN_POINT('Ctrl Pts',(38.2689491460942,-5.67387652512014,
129.119163422861));
#149410=CARTESIAN_POINT('Ctrl Pts',(38.2615409264277,-5.71672908954976,
129.270836424734));
#149411=CARTESIAN_POINT('Ctrl Pts',(38.2541327067612,-5.75344146402281,
129.423838295196));
#149412=CARTESIAN_POINT('Ctrl Pts',(38.2467199274591,-5.79017643434988,
129.576934335755));
#149413=CARTESIAN_POINT('Ctrl Pts',(38.2393071481571,-5.82076361185966,
129.731360509329));
#149414=CARTESIAN_POINT('Ctrl Pts',(38.231894368855,-5.84513582789617,129.886581931855));
#149415=CARTESIAN_POINT('Ctrl Pts',(38.2244709978262,-5.86954286809787,
130.042025142029));
#149416=CARTESIAN_POINT('Ctrl Pts',(38.2170476267974,-5.88771716800039,
130.198265500764));
#149417=CARTESIAN_POINT('Ctrl Pts',(38.2096242557687,-5.89964354035209,
130.35476451073));
#149418=CARTESIAN_POINT('Ctrl Pts',(38.2056882063279,-5.90596718914241,
130.437744040958));
#149419=CARTESIAN_POINT('Ctrl Pts',(38.2017521568871,-5.9105351924658,130.520796299877));
#149420=CARTESIAN_POINT('Ctrl Pts',(38.1978161074462,-5.91335121668874,
130.60384141503));
#149421=CARTESIAN_POINT('Ctrl Pts',(38.1946691357013,-5.91560269975465,
130.670238099032));
#149422=CARTESIAN_POINT('Ctrl Pts',(38.1915221639564,-5.91673594582547,
130.73667291686));
#149423=CARTESIAN_POINT('Ctrl Pts',(38.1883751922115,-5.91674987009191,
130.80312075171));
#149424=CARTESIAN_POINT('',(36.4383751922116,-5.91188926911274,130.799500886255));
#149425=CARTESIAN_POINT('Ctrl Pts',(38.1883739050364,-5.92621749523645,
130.803145989751));
#149426=CARTESIAN_POINT('Ctrl Pts',(38.0987054312354,-5.92080046752888,
132.699513211106));
#149427=CARTESIAN_POINT('Ctrl Pts',(37.9162210828302,-3.90476091023743,
136.568682839027));
#149428=CARTESIAN_POINT('Ctrl Pts',(37.6409208598204,2.69161358101603,137.264451705223));
#149429=CARTESIAN_POINT('Ctrl Pts',(37.3624732360077,6.88994047818806,132.031666910778));
#149430=CARTESIAN_POINT('Ctrl Pts',(37.0840256121947,4.75674866821361,125.671047590115));
#149431=CARTESIAN_POINT('Ctrl Pts',(36.8055779883818,-1.74766278776102,
124.027692165396));
#149432=CARTESIAN_POINT('Ctrl Pts',(36.5903611817208,-5.53371367076097,
127.570797637055));
#149433=CARTESIAN_POINT('Ctrl Pts',(36.4679602496641,-5.91673427114246,
130.169895298242));
#149434=CARTESIAN_POINT('Ctrl Pts',(36.4383751922116,-5.91188926911274,
130.799500886255));
#149435=CARTESIAN_POINT('',(34.6883751922117,-5.90863770699821,130.807549372269));
#149436=CARTESIAN_POINT('Ctrl Pts',(36.4383751922116,-5.91188926911274,
130.799500886255));
#149437=CARTESIAN_POINT('Ctrl Pts',(36.3751443750598,-5.90153426345037,
132.145128687637));
#149438=CARTESIAN_POINT('Ctrl Pts',(36.2190976833036,-4.77772734883998,
135.481633513835));
#149439=CARTESIAN_POINT('Ctrl Pts',(35.970235116943,0.768340780429054,137.760452406458));
#149440=CARTESIAN_POINT('Ctrl Pts',(35.6917874931303,6.26766398833651,133.917871282335));
#149441=CARTESIAN_POINT('Ctrl Pts',(35.4133398693173,6.00731018337622,127.214125960743));
#149442=CARTESIAN_POINT('Ctrl Pts',(35.1348922455045,0.226531793307069,
123.809630896056));
#149443=CARTESIAN_POINT('Ctrl Pts',(34.8932373531359,-4.97106715849222,
126.433463773508));
#149444=CARTESIAN_POINT('Ctrl Pts',(34.7443983353716,-5.90282418023302,
129.613660964501));
#149445=CARTESIAN_POINT('Ctrl Pts',(34.6883751922117,-5.90863770699821,
130.807549372269));
#149446=CARTESIAN_POINT('',(32.9383751922116,-5.9235876075816,130.808068272843));
#149447=CARTESIAN_POINT('Ctrl Pts',(34.6883751922117,-5.90863770699821,
130.807549372269));
#149448=CARTESIAN_POINT('Ctrl Pts',(34.6515824607673,-5.9124556921549,131.591625614405));
#149449=CARTESIAN_POINT('Ctrl Pts',(34.5219738547188,-5.40187661372055,
134.348894589915));
#149450=CARTESIAN_POINT('Ctrl Pts',(34.2995493740658,-1.21681955547966,
137.696160868569));
#149451=CARTESIAN_POINT('Ctrl Pts',(34.0211017502528,5.14054604489025,135.553291748959));
#149452=CARTESIAN_POINT('Ctrl Pts',(33.7426541264402,6.77400095963935,129.046386917784));
#149453=CARTESIAN_POINT('Ctrl Pts',(33.4642065026269,2.18247992082522,124.154974034912));
#149454=CARTESIAN_POINT('Ctrl Pts',(33.196113524551,-4.16930635618508,125.328689761559));
#149455=CARTESIAN_POINT('Ctrl Pts',(33.0208364210792,-5.91080789301554,
129.062074719763));
#149456=CARTESIAN_POINT('Ctrl Pts',(32.9383751922116,-5.9235876075816,130.808068272843));
#149457=CARTESIAN_POINT('',(31.1883751922117,-5.91899767233231,130.79938269648));
#149458=CARTESIAN_POINT('Ctrl Pts',(32.9383751922116,-5.9235876075816,130.808068272843));
#149459=CARTESIAN_POINT('Ctrl Pts',(32.9280205464749,-5.92519235467021,
131.02731245522));
#149460=CARTESIAN_POINT('Ctrl Pts',(32.8248500261334,-5.81447119154423,
133.21015694754));
#149461=CARTESIAN_POINT('Ctrl Pts',(32.6288636311887,-3.10396874173013,
137.076755581275));
#149462=CARTESIAN_POINT('Ctrl Pts',(32.3504160073755,3.5993726028644,136.806200118591));
#149463=CARTESIAN_POINT('Ctrl Pts',(32.0719683835628,6.99506636455412,131.020247360633));
#149464=CARTESIAN_POINT('Ctrl Pts',(31.7935207597497,3.96263586520661,125.035905232443));
#149465=CARTESIAN_POINT('Ctrl Pts',(31.515073135937,-2.71126340873828,124.352491798475));
#149466=CARTESIAN_POINT('Ctrl Pts',(31.3133579467576,-5.74109606907425,
128.152505750201));
#149467=CARTESIAN_POINT('Ctrl Pts',(31.2044586321825,-5.92336622444082,
130.458345827985));
#149468=CARTESIAN_POINT('Ctrl Pts',(31.1883751922117,-5.92029803960656,
130.799381602861));
#149469=CARTESIAN_POINT('',(29.4383752206225,-5.91150934056856,130.802999882248));
#149470=CARTESIAN_POINT('Ctrl Pts',(31.1883751922117,-5.91674790756165,
130.799384588548));
#149471=CARTESIAN_POINT('Ctrl Pts',(31.1810736186236,-5.91687803629541,
130.954114175227));
#149472=CARTESIAN_POINT('Ctrl Pts',(31.1737720450354,-5.91093449718433,
131.109059102874));
#149473=CARTESIAN_POINT('Ctrl Pts',(31.1664704714473,-5.89889333136726,
131.263694948583));
#149474=CARTESIAN_POINT('Ctrl Pts',(31.1591753990885,-5.88686288685281,
131.41819310848));
#149475=CARTESIAN_POINT('Ctrl Pts',(31.1518803267297,-5.86874564859868,
131.572382352231));
#149476=CARTESIAN_POINT('Ctrl Pts',(31.1445852543709,-5.84456970245775,
131.725737606433));
#149477=CARTESIAN_POINT('Ctrl Pts',(31.1372949755956,-5.82040964230286,
131.878992091076));
#149478=CARTESIAN_POINT('Ctrl Pts',(31.1300046968204,-5.79019885757158,
132.031413297529));
#149479=CARTESIAN_POINT('Ctrl Pts',(31.1227144180451,-5.75401729566393,
132.182480903934));
#149480=CARTESIAN_POINT('Ctrl Pts',(31.1154264573996,-5.71784723860511,
132.333500474548));
#149481=CARTESIAN_POINT('Ctrl Pts',(31.108138496754,-5.67571026758409,132.483166926363));
#149482=CARTESIAN_POINT('Ctrl Pts',(31.1008505361085,-5.62773748163055,
132.63096988075));
#149483=CARTESIAN_POINT('Ctrl Pts',(31.0935635496382,-5.57977110815652,
132.778753078448));
#149484=CARTESIAN_POINT('Ctrl Pts',(31.0862765631679,-5.52597059006752,
132.924672907551));
#149485=CARTESIAN_POINT('Ctrl Pts',(31.0789895766976,-5.46651687014971,
133.068234260433));
#149486=CARTESIAN_POINT('Ctrl Pts',(31.0717020260758,-5.40705854738212,
133.211806727697));
#149487=CARTESIAN_POINT('Ctrl Pts',(31.064414475454,-5.34194629960161,133.353019999323));
#149488=CARTESIAN_POINT('Ctrl Pts',(31.0571269248322,-5.27140905118794,
133.491399355202));
#149489=CARTESIAN_POINT('Ctrl Pts',(31.0498372714414,-5.20085144977045,
133.629818639424));
#149490=CARTESIAN_POINT('Ctrl Pts',(31.0425476180504,-5.12486590861082,
133.765402037925));
#149491=CARTESIAN_POINT('Ctrl Pts',(31.0352579646596,-5.04372693339733,
133.897700104887));
#149492=CARTESIAN_POINT('Ctrl Pts',(31.0279607119279,-4.96250337216937,
134.030136090356));
#149493=CARTESIAN_POINT('Ctrl Pts',(31.0206634591962,-4.87611585245031,
134.15927957765));
#149494=CARTESIAN_POINT('Ctrl Pts',(31.0133662064645,-4.78488207870418,
134.284710320598));
#149495=CARTESIAN_POINT('Ctrl Pts',(31.0060646862501,-4.69359495083073,
134.410214416292));
#149496=CARTESIAN_POINT('Ctrl Pts',(30.9987631660356,-4.59745616387367,
134.532001142695));
#149497=CARTESIAN_POINT('Ctrl Pts',(30.9914616458212,-4.49682265436147,
134.64968460622));
#149498=CARTESIAN_POINT('Ctrl Pts',(30.9841498323878,-4.39604727812509,
134.767533972411));
#149499=CARTESIAN_POINT('Ctrl Pts',(30.9768380189543,-4.29076478995553,
134.881268245521));
#149500=CARTESIAN_POINT('Ctrl Pts',(30.9695262055209,-4.18136822975938,
134.990539100342));
#149501=CARTESIAN_POINT('Ctrl Pts',(30.9657434331176,-4.12477183370912,
135.047070462619));
#149502=CARTESIAN_POINT('Ctrl Pts',(30.9619606607143,-4.06707483665724,
135.102407846852));
#149503=CARTESIAN_POINT('Ctrl Pts',(30.958177888311,-4.00833487973587,135.156507450382));
#149504=CARTESIAN_POINT('Ctrl Pts',(30.9507546219056,-3.89306430504004,
135.262671852207));
#149505=CARTESIAN_POINT('Ctrl Pts',(30.9433313555002,-3.77339872329145,
135.364414054398));
#149506=CARTESIAN_POINT('Ctrl Pts',(30.9359080890948,-3.64971178776911,
135.461348316575));
#149507=CARTESIAN_POINT('Ctrl Pts',(30.9284935963738,-3.52617103993263,
135.558168010504));
#149508=CARTESIAN_POINT('Ctrl Pts',(30.9210791036528,-3.39861868995656,
135.650190847619));
#149509=CARTESIAN_POINT('Ctrl Pts',(30.9136646109318,-3.26746470961103,
135.737068285161));
#149510=CARTESIAN_POINT('Ctrl Pts',(30.906257264578,-3.13643714040962,135.823861986957));
#149511=CARTESIAN_POINT('Ctrl Pts',(30.8988499182242,-3.00181516081051,
135.905519957464));
#149512=CARTESIAN_POINT('Ctrl Pts',(30.8914425718704,-2.86404116328473,
135.981734351179));
#149513=CARTESIAN_POINT('Ctrl Pts',(30.8840407501951,-2.7263699228048,136.057891901324));
#149514=CARTESIAN_POINT('Ctrl Pts',(30.8766389285197,-2.58555167058872,
136.128613778815));
#149515=CARTESIAN_POINT('Ctrl Pts',(30.8692371068443,-2.4420569829478,136.193635917134));
#149516=CARTESIAN_POINT('Ctrl Pts',(30.8618391925329,-2.29863804503449,
136.258623730773));
#149517=CARTESIAN_POINT('Ctrl Pts',(30.8544412782215,-2.15254582465138,
136.317917643822));
#149518=CARTESIAN_POINT('Ctrl Pts',(30.8470433639101,-2.00427455108857,
136.37129999988));
#149519=CARTESIAN_POINT('Ctrl Pts',(30.8396466789979,-1.85602791752194,
136.424673484759));
#149520=CARTESIAN_POINT('Ctrl Pts',(30.8322499940857,-1.70560330035875,
136.472137236077));
#149521=CARTESIAN_POINT('Ctrl Pts',(30.8248533091735,-1.55351402777272,
136.513522090849));
#149522=CARTESIAN_POINT('Ctrl Pts',(30.8174569522381,-1.40143149898463,
136.554905110572));
#149523=CARTESIAN_POINT('Ctrl Pts',(30.8100605953026,-1.24768482173847,
136.590209671679));
#149524=CARTESIAN_POINT('Ctrl Pts',(30.8026642383672,-1.09280131165758,
136.619316838875));
#149525=CARTESIAN_POINT('Ctrl Pts',(30.7952667490306,-0.937894088515456,
136.648428462453));
#149526=CARTESIAN_POINT('Ctrl Pts',(30.787869259694,-0.781850052877025,
136.671340733907));
#149527=CARTESIAN_POINT('Ctrl Pts',(30.7804717703574,-0.625205359369967,
136.687986100303));
#149528=CARTESIAN_POINT('Ctrl Pts',(30.7730716878424,-0.468505754308653,
136.704637301707));
#149529=CARTESIAN_POINT('Ctrl Pts',(30.7656716053274,-0.311205443132389,
136.715017184711));
#149530=CARTESIAN_POINT('Ctrl Pts',(30.7582715228124,-0.153844179286222,
136.719110192231));
#149531=CARTESIAN_POINT('Ctrl Pts',(30.750863303146,0.00369011944644976,
136.723207700434));
#149532=CARTESIAN_POINT('Ctrl Pts',(30.7434550834795,0.161285131299126,
136.721004517593));
#149533=CARTESIAN_POINT('Ctrl Pts',(30.736046863813,0.31840188955168,136.71253722285));
#149534=CARTESIAN_POINT('Ctrl Pts',(30.728634084511,0.475615350547304,136.704064716629));
#149535=CARTESIAN_POINT('Ctrl Pts',(30.7212213052089,0.632349600604035,
136.689320450907));
#149536=CARTESIAN_POINT('Ctrl Pts',(30.7138085259068,0.788072824502699,
136.66839265924));
#149537=CARTESIAN_POINT('Ctrl Pts',(30.7063851548781,0.944018553046586,
136.647434964963));
#149538=CARTESIAN_POINT('Ctrl Pts',(30.6989617838493,1.09895000352174,136.620276162924));
#149539=CARTESIAN_POINT('Ctrl Pts',(30.6915384128206,1.25234672868807,136.587055338338));
#149540=CARTESIAN_POINT('Ctrl Pts',(30.6876023633798,1.33368135307515,136.56944086002));
#149541=CARTESIAN_POINT('Ctrl Pts',(30.683666313939,1.41458477169084,136.55012296101));
#149542=CARTESIAN_POINT('Ctrl Pts',(30.6797302644982,1.49498147813114,136.529127944064));
#149543=CARTESIAN_POINT('Ctrl Pts',(30.6723069980928,1.64660715738226,136.489531997337));
#149544=CARTESIAN_POINT('Ctrl Pts',(30.6648837316873,1.79688792350402,136.443848099782));
#149545=CARTESIAN_POINT('Ctrl Pts',(30.6574604652819,1.94529727346557,136.392182114388));
#149546=CARTESIAN_POINT('Ctrl Pts',(30.6500459725609,2.0935312159003,136.340577193899));
#149547=CARTESIAN_POINT('Ctrl Pts',(30.6426314798399,2.23989779578875,136.283004380637));
#149548=CARTESIAN_POINT('Ctrl Pts',(30.6352169871188,2.38388217448049,136.219620199589));
#149549=CARTESIAN_POINT('Ctrl Pts',(30.6278096407651,2.52772777560693,136.156297110602));
#149550=CARTESIAN_POINT('Ctrl Pts',(30.6204022944114,2.66919540716613,136.087173954138));
#149551=CARTESIAN_POINT('Ctrl Pts',(30.6129949480576,2.80778694608197,136.012456529501));
#149552=CARTESIAN_POINT('Ctrl Pts',(30.6055931263822,2.94627511819893,135.937794831938));
#149553=CARTESIAN_POINT('Ctrl Pts',(30.5981913047068,3.08189114167944,135.85754735043));
#149554=CARTESIAN_POINT('Ctrl Pts',(30.5907894830314,3.21415849189268,135.771967259752));
#149555=CARTESIAN_POINT('Ctrl Pts',(30.58339156872,3.34635601920263,135.686432346138));
#149556=CARTESIAN_POINT('Ctrl Pts',(30.5759936544085,3.47520808115981,135.59557063192));
#149557=CARTESIAN_POINT('Ctrl Pts',(30.5685957400972,3.60026441426646,135.499680277596));
#149558=CARTESIAN_POINT('Ctrl Pts',(30.5611990551849,3.72529996527858,135.403805858511));
#149559=CARTESIAN_POINT('Ctrl Pts',(30.5538023702728,3.84654074340866,135.302904684799));
#149560=CARTESIAN_POINT('Ctrl Pts',(30.5464056853606,3.96356696062728,135.197317197265));
#149561=CARTESIAN_POINT('Ctrl Pts',(30.5390093284251,4.08058798878063,135.091734391592));
#149562=CARTESIAN_POINT('Ctrl Pts',(30.5316129714896,4.19339455044032,134.981465935333));
#149563=CARTESIAN_POINT('Ctrl Pts',(30.5242166145542,4.30160155499882,134.866891186624));
#149564=CARTESIAN_POINT('Ctrl Pts',(30.5168191252176,4.40982512632628,134.752298896229));
#149565=CARTESIAN_POINT('Ctrl Pts',(30.509421635881,4.51344748206035,134.633399272034));
#149566=CARTESIAN_POINT('Ctrl Pts',(30.5020241465444,4.61212198333057,134.510606882101));
#149567=CARTESIAN_POINT('Ctrl Pts',(30.4946240640294,4.71083107479424,134.387771447486));
#149568=CARTESIAN_POINT('Ctrl Pts',(30.4872239815144,4.80458862480395,134.261040821023));
#149569=CARTESIAN_POINT('Ctrl Pts',(30.4798238989994,4.89308979482202,134.130860703589));
#149570=CARTESIAN_POINT('Ctrl Pts',(30.472415679333,4.98168828097442,134.000537439732));
#149571=CARTESIAN_POINT('Ctrl Pts',(30.4650074596664,5.0650186342318,133.866757418797));
#149572=CARTESIAN_POINT('Ctrl Pts',(30.45759924,5.14282030498432,133.729993860668));
#149573=CARTESIAN_POINT('Ctrl Pts',(30.4501864606979,5.22066986136723,133.59314612685));
#149574=CARTESIAN_POINT('Ctrl Pts',(30.4427736813959,5.29298378363884,133.453311527561));
#149575=CARTESIAN_POINT('Ctrl Pts',(30.4353609020938,5.35954884607186,133.310985186398));
#149576=CARTESIAN_POINT('Ctrl Pts',(30.427937531065,5.42620901978758,133.168455482684));
#149577=CARTESIAN_POINT('Ctrl Pts',(30.4205141600363,5.48710378384813,133.02342726962));
#149578=CARTESIAN_POINT('Ctrl Pts',(30.4130907890076,5.54206884013689,132.876413593164));
#149579=CARTESIAN_POINT('Ctrl Pts',(30.4091547395668,5.57121263184922,132.798463414363));
#149580=CARTESIAN_POINT('Ctrl Pts',(30.405218690126,5.5986902102386,132.719955280698));
#149581=CARTESIAN_POINT('Ctrl Pts',(30.4012826406853,5.62448289150163,132.640966935127));
#149582=CARTESIAN_POINT('Ctrl Pts',(30.3938593742799,5.67312708340229,132.49199738052));
#149583=CARTESIAN_POINT('Ctrl Pts',(30.3864361078745,5.71592235145471,132.34086865329));
#149584=CARTESIAN_POINT('Ctrl Pts',(30.3790128414691,5.75267317344041,132.188080936879));
#149585=CARTESIAN_POINT('Ctrl Pts',(30.3715983487481,5.78938055900654,132.03547380286));
#149586=CARTESIAN_POINT('Ctrl Pts',(30.3641838560271,5.82005763229482,131.881211942021));
#149587=CARTESIAN_POINT('Ctrl Pts',(30.3567693633061,5.84455779934302,131.725813108278));
#149588=CARTESIAN_POINT('Ctrl Pts',(30.3493620169523,5.86903435220777,131.570564053781));
#149589=CARTESIAN_POINT('Ctrl Pts',(30.3419546705985,5.88734579340239,131.414180574283));
#149590=CARTESIAN_POINT('Ctrl Pts',(30.3345473242447,5.89939602001794,131.257192994386));
#149591=CARTESIAN_POINT('Ctrl Pts',(30.3271455025693,5.91143725911992,131.100322501748));
#149592=CARTESIAN_POINT('Ctrl Pts',(30.319743680894,5.91722655349739,130.942849176438));
#149593=CARTESIAN_POINT('Ctrl Pts',(30.3123418592185,5.91671933305621,130.785310779276));
#149594=CARTESIAN_POINT('Ctrl Pts',(30.3049439449072,5.91621238037276,130.627855545408));
#149595=CARTESIAN_POINT('Ctrl Pts',(30.2975460305958,5.90941553373817,130.470335680449));
#149596=CARTESIAN_POINT('Ctrl Pts',(30.2901481162845,5.89633626560493,130.313291166865));
#149597=CARTESIAN_POINT('Ctrl Pts',(30.2827514313723,5.88325917100875,130.156272751229));
#149598=CARTESIAN_POINT('Ctrl Pts',(30.2753547464601,5.86390175794559,129.999729901832));
#149599=CARTESIAN_POINT('Ctrl Pts',(30.2679580615479,5.83832354322159,129.844199814802));
#149600=CARTESIAN_POINT('Ctrl Pts',(30.2605617046125,5.81274646266239,129.688676624139));
#149601=CARTESIAN_POINT('Ctrl Pts',(30.253165347677,5.78094918947733,129.534166474902));
#149602=CARTESIAN_POINT('Ctrl Pts',(30.2457689907415,5.74304273753031,129.381198407064));
#149603=CARTESIAN_POINT('Ctrl Pts',(30.238371501405,5.70513048200873,129.228206919425));
#149604=CARTESIAN_POINT('Ctrl Pts',(30.2309740120684,5.66110727515254,129.076758345647));
#149605=CARTESIAN_POINT('Ctrl Pts',(30.2235765227319,5.61113453803621,128.927368406992));
#149606=CARTESIAN_POINT('Ctrl Pts',(30.2161764402169,5.56114428305427,128.777926099925));
#149607=CARTESIAN_POINT('Ctrl Pts',(30.2087763577018,5.50520046374941,128.630544218579));
#149608=CARTESIAN_POINT('Ctrl Pts',(30.2013762751868,5.44351328821527,128.48572014446));
#149609=CARTESIAN_POINT('Ctrl Pts',(30.1939680555204,5.38175828129011,128.340736821384));
#149610=CARTESIAN_POINT('Ctrl Pts',(30.1865598358539,5.31424745222283,128.198317266076));
#149611=CARTESIAN_POINT('Ctrl Pts',(30.1791516161874,5.24123810087678,128.058936473209));
#149612=CARTESIAN_POINT('Ctrl Pts',(30.1717388368853,5.168183813493,127.91946989379));
#149613=CARTESIAN_POINT('Ctrl Pts',(30.1643260575833,5.08962444614304,127.78304612638));
#149614=CARTESIAN_POINT('Ctrl Pts',(30.1569132782812,5.00586130661822,127.650112190222));
#149615=CARTESIAN_POINT('Ctrl Pts',(30.1494899072524,4.92197848239179,127.516988311822));
#149616=CARTESIAN_POINT('Ctrl Pts',(30.1420665362237,4.83287724674095,127.387364530517));
#149617=CARTESIAN_POINT('Ctrl Pts',(30.134643165195,4.73890043261532,127.261656388836));
#149618=CARTESIAN_POINT('Ctrl Pts',(30.1307071157541,4.68907167082233,127.195002915791));
#149619=CARTESIAN_POINT('Ctrl Pts',(30.1267710663133,4.63787285679946,127.129449686971));
#149620=CARTESIAN_POINT('Ctrl Pts',(30.1228350168724,4.58535929884655,127.065054443557));
#149621=CARTESIAN_POINT('Ctrl Pts',(30.115411750467,4.48632036744083,126.943607024187));
#149622=CARTESIAN_POINT('Ctrl Pts',(30.1079884840615,4.38230337674868,126.825913384557));
#149623=CARTESIAN_POINT('Ctrl Pts',(30.1005652176561,4.27362346073099,126.712408384415));
#149624=CARTESIAN_POINT('Ctrl Pts',(30.0931507249351,4.16507199534872,126.599037537757));
#149625=CARTESIAN_POINT('Ctrl Pts',(30.085736232214,4.05186883034323,126.489845743341));
#149626=CARTESIAN_POINT('Ctrl Pts',(30.078321739493,3.93437032913027,126.385236193457));
#149627=CARTESIAN_POINT('Ctrl Pts',(30.0709143931392,3.81698507739635,126.280727470195));
#149628=CARTESIAN_POINT('Ctrl Pts',(30.0635070467855,3.69531300833176,126.180792445563));
#149629=CARTESIAN_POINT('Ctrl Pts',(30.0560997004317,3.56974835307321,126.085798627062));
#149630=CARTESIAN_POINT('Ctrl Pts',(30.0486978787563,3.44427734867218,125.990875658534));
#149631=CARTESIAN_POINT('Ctrl Pts',(30.0412960570808,3.31491983523602,125.900886782384));
#149632=CARTESIAN_POINT('Ctrl Pts',(30.0338942354055,3.1821041549464,125.816160169551));
#149633=CARTESIAN_POINT('Ctrl Pts',(30.0264963210942,3.04935858702152,125.731478283239));
#149634=CARTESIAN_POINT('Ctrl Pts',(30.0190984067829,2.91315880180979,125.652053328163));
#149635=CARTESIAN_POINT('Ctrl Pts',(30.0117004924716,2.77396314089516,125.57817089125));
#149636=CARTESIAN_POINT('Ctrl Pts',(30.0043038075593,2.63479061177271,125.504300732257));
#149637=CARTESIAN_POINT('Ctrl Pts',(29.9969071226471,2.49262352445887,125.435971438226));
#149638=CARTESIAN_POINT('Ctrl Pts',(29.9895104377349,2.34794600755799,125.373423303612));
#149639=CARTESIAN_POINT('Ctrl Pts',(29.9821140807995,2.20327490581003,125.310877942449));
#149640=CARTESIAN_POINT('Ctrl Pts',(29.974717723864,2.05609393845387,125.254113379142));
#149641=CARTESIAN_POINT('Ctrl Pts',(29.9673213669285,1.90690820750723,125.203322173613));
#149642=CARTESIAN_POINT('Ctrl Pts',(29.9599238775919,1.75769963584433,125.15252319182));
#149643=CARTESIAN_POINT('Ctrl Pts',(29.9525263882554,1.6064860428455,125.107699509086));
#149644=CARTESIAN_POINT('Ctrl Pts',(29.9451288989188,1.45378857144856,125.068994077228));
#149645=CARTESIAN_POINT('Ctrl Pts',(29.9377288164038,1.3010375721893,125.030275077241));
#149646=CARTESIAN_POINT('Ctrl Pts',(29.9303287338888,1.14680202050313,124.997678689964));
#149647=CARTESIAN_POINT('Ctrl Pts',(29.9229286513738,0.991614000146153,
124.971296908226));
#149648=CARTESIAN_POINT('Ctrl Pts',(29.9155204317073,0.836255334607523,
124.944886117008));
#149649=CARTESIAN_POINT('Ctrl Pts',(29.9081122120408,0.679942477040716,
124.924703641073));
#149650=CARTESIAN_POINT('Ctrl Pts',(29.9007039923743,0.523214130777668,
124.910789752984));
#149651=CARTESIAN_POINT('Ctrl Pts',(29.8932912130722,0.366389320832201,
124.896867301128));
#149652=CARTESIAN_POINT('Ctrl Pts',(29.8858784337702,0.209148884616497,
124.889221143176));
#149653=CARTESIAN_POINT('Ctrl Pts',(29.8784656544681,0.052031776299944,
124.887839405168));
#149654=CARTESIAN_POINT('Ctrl Pts',(29.8710422834393,-0.105309828308809,
124.886455692868));
#149655=CARTESIAN_POINT('Ctrl Pts',(29.8636189124105,-0.262527380945767,
124.891354265867));
#149656=CARTESIAN_POINT('Ctrl Pts',(29.8561955413817,-0.419085964327446,
124.902471299983));
#149657=CARTESIAN_POINT('Ctrl Pts',(29.852259491941,-0.502097081807044,
124.90836581822));
#149658=CARTESIAN_POINT('Ctrl Pts',(29.8483234425003,-0.584923079354862,
124.91600770908));
#149659=CARTESIAN_POINT('Ctrl Pts',(29.8443873930595,-0.667485482193467,
124.92538165064));
#149660=CARTESIAN_POINT('Ctrl Pts',(29.8369641266541,-0.823195597264386,
124.943060611872));
#149661=CARTESIAN_POINT('Ctrl Pts',(29.8295408602487,-0.978438313767397,
124.966956765008));
#149662=CARTESIAN_POINT('Ctrl Pts',(29.8221175938432,-1.13267743427713,
124.997040031239));
#149663=CARTESIAN_POINT('Ctrl Pts',(29.8147031011222,-1.28673425695539,
125.027087741547));
#149664=CARTESIAN_POINT('Ctrl Pts',(29.8072886084012,-1.43978948189665,
125.063307938306));
#149665=CARTESIAN_POINT('Ctrl Pts',(29.7998741156802,-1.59131126887694,
125.105618738164));
#149666=CARTESIAN_POINT('Ctrl Pts',(29.7924667693264,-1.74268701345381,
125.14788875728));
#149667=CARTESIAN_POINT('Ctrl Pts',(29.7850594229726,-1.89253190531764,
125.196237593054));
#149668=CARTESIAN_POINT('Ctrl Pts',(29.7776520766189,-2.04032365844145,
125.250532214446));
#149669=CARTESIAN_POINT('Ctrl Pts',(29.7702502549434,-2.18800518290161,
125.304786340861));
#149670=CARTESIAN_POINT('Ctrl Pts',(29.7628484332679,-2.33363626877076,
125.364977294851));
#149671=CARTESIAN_POINT('Ctrl Pts',(29.7554466115925,-2.47670928713071,
125.430922084416));
#149672=CARTESIAN_POINT('Ctrl Pts',(29.7480486972811,-2.61970677835692,
125.49683206224));
#149673=CARTESIAN_POINT('Ctrl Pts',(29.7406507829698,-2.76014855326697,
125.568489670636));
#149674=CARTESIAN_POINT('Ctrl Pts',(29.7332528686584,-2.89754659466987,
125.645663660561));
#149675=CARTESIAN_POINT('Ctrl Pts',(29.7258561837462,-3.03492180301074,
125.722824825567));
#149676=CARTESIAN_POINT('Ctrl Pts',(29.7184594988339,-3.1692539565818,125.805500370047));
#149677=CARTESIAN_POINT('Ctrl Pts',(29.7110628139217,-3.30007920551684,
125.893412867914));
#149678=CARTESIAN_POINT('Ctrl Pts',(29.7036664569863,-3.43089865352306,
125.981321467648));
#149679=CARTESIAN_POINT('Ctrl Pts',(29.6962701000508,-3.55821119623962,
126.074466350848));
#149680=CARTESIAN_POINT('Ctrl Pts',(29.6888737431154,-3.68158180757366,
126.17252664422));
#149681=CARTESIAN_POINT('Ctrl Pts',(29.6814762537788,-3.80497130726343,
126.270601950873));
#149682=CARTESIAN_POINT('Ctrl Pts',(29.6740787644423,-3.92441738163343,
126.373593933858));
#149683=CARTESIAN_POINT('Ctrl Pts',(29.6666812751057,-4.03951807078312,
126.481141409809));
#149684=CARTESIAN_POINT('Ctrl Pts',(29.6592811925907,-4.15465910829997,
126.588726586361));
#149685=CARTESIAN_POINT('Ctrl Pts',(29.6518811100758,-4.26545145519191,
126.700870180637));
#149686=CARTESIAN_POINT('Ctrl Pts',(29.6444810275608,-4.37153011101842,
126.817174259875));
#149687=CARTESIAN_POINT('Ctrl Pts',(29.6370728078944,-4.47772541123308,
126.933606227405));
#149688=CARTESIAN_POINT('Ctrl Pts',(29.6296645882279,-4.5791964175029,127.054207540259));
#149689=CARTESIAN_POINT('Ctrl Pts',(29.6222563685614,-4.67561806507234,
127.17854674037));
#149690=CARTESIAN_POINT('Ctrl Pts',(29.6148435892594,-4.77209905855644,
127.302962469182));
#149691=CARTESIAN_POINT('Ctrl Pts',(29.6074308099574,-4.86352428437705,
127.431120366309));
#149692=CARTESIAN_POINT('Ctrl Pts',(29.6000180306554,-4.94961241453897,
127.562560576178));
#149693=CARTESIAN_POINT('Ctrl Pts',(29.5925946596266,-5.03582355145902,
127.694188593984));
#149694=CARTESIAN_POINT('Ctrl Pts',(29.5851712885978,-5.11668217071284,
127.82910797201));
#149695=CARTESIAN_POINT('Ctrl Pts',(29.5777479175691,-5.19195283353445,
127.966834170667));
#149696=CARTESIAN_POINT('Ctrl Pts',(29.5738118681283,-5.23186314505729,
128.039859905889));
#149697=CARTESIAN_POINT('Ctrl Pts',(29.5698758186875,-5.27020328066042,
128.113674392054));
#149698=CARTESIAN_POINT('Ctrl Pts',(29.5659397692467,-5.30694371357554,
128.188203324237));
#149699=CARTESIAN_POINT('Ctrl Pts',(29.5579707528573,-5.38132924060183,
128.339096317574));
#149700=CARTESIAN_POINT('Ctrl Pts',(29.5500017364678,-5.44935422305597,
128.493323694942));
#149701=CARTESIAN_POINT('Ctrl Pts',(29.5420327200784,-5.51073002588949,
128.650344567426));
#149702=CARTESIAN_POINT('Ctrl Pts',(29.5340793302799,-5.5719854757813,128.807057534791));
#149703=CARTESIAN_POINT('Ctrl Pts',(29.5261259404815,-5.6266176400274,128.966552807321));
#149704=CARTESIAN_POINT('Ctrl Pts',(29.518172550683,-5.67438451996701,129.128266681637));
#149705=CARTESIAN_POINT('Ctrl Pts',(29.5102415681632,-5.72201682511289,
129.289524955518));
#149706=CARTESIAN_POINT('Ctrl Pts',(29.5023105856434,-5.76282234525453,
129.45298908768));
#149707=CARTESIAN_POINT('Ctrl Pts',(29.4943796031236,-5.79660799173531,
129.6180780405));
#149708=CARTESIAN_POINT('Ctrl Pts',(29.4864625062504,-5.8303344859551,129.782877953866));
#149709=CARTESIAN_POINT('Ctrl Pts',(29.4785454093773,-5.85706554950225,
129.949296736362));
#149710=CARTESIAN_POINT('Ctrl Pts',(29.4706283125042,-5.87665773256306,
130.116738296225));
#149711=CARTESIAN_POINT('Ctrl Pts',(29.4627306403779,-5.89620184583215,
130.283769035054));
#149712=CARTESIAN_POINT('Ctrl Pts',(29.4548329682517,-5.90864197837242,
130.451817261117));
#149713=CARTESIAN_POINT('Ctrl Pts',(29.4469352961255,-5.91388568523945,
130.620277309197));
#149714=CARTESIAN_POINT('Ctrl Pts',(29.444081949191,-5.91578018208298,130.68114017538));
#149715=CARTESIAN_POINT('Ctrl Pts',(29.4412286022565,-5.91673580774773,
130.742056685041));
#149716=CARTESIAN_POINT('Ctrl Pts',(29.438375255322,-5.91674984308085,130.8029979354));
#149717=CARTESIAN_POINT('',(27.6883751922116,-5.91529524537258,130.809807152419));
#149718=CARTESIAN_POINT('Ctrl Pts',(29.4383751922116,-5.90721857606676,
130.803001476268));
#149719=CARTESIAN_POINT('Ctrl Pts',(29.3880808432857,-5.90502446395126,
131.875448957813));
#149720=CARTESIAN_POINT('Ctrl Pts',(29.2449706197554,-5.11199832894571,
134.930071410922));
#149721=CARTESIAN_POINT('Ctrl Pts',(29.009044521621,-0.205241192839764,
137.799747424816));
#149722=CARTESIAN_POINT('Ctrl Pts',(28.730596897808,5.77447916256885,134.758213286979));
#149723=CARTESIAN_POINT('Ctrl Pts',(28.4521492739951,6.44773526656473,128.083281702383));
#149724=CARTESIAN_POINT('Ctrl Pts',(28.1737016501822,1.195837649966,123.90888870875));
#149725=CARTESIAN_POINT('Ctrl Pts',(27.9191102895877,-4.61086435825437,
125.885848252815));
#149726=CARTESIAN_POINT('Ctrl Pts',(27.7573348035975,-5.90207848774965,
129.344403176503));
#149727=CARTESIAN_POINT('Ctrl Pts',(27.6883751922116,-5.91529524537258,
130.809807152419));
#149728=CARTESIAN_POINT('',(25.9383751922117,-5.92200882025382,130.803339028211));
#149729=CARTESIAN_POINT('Ctrl Pts',(27.6883751922116,-5.91529524537258,
130.809807152419));
#149730=CARTESIAN_POINT('Ctrl Pts',(27.6645189289932,-5.9198675224259,131.316756978095));
#149731=CARTESIAN_POINT('Ctrl Pts',(27.5478467911706,-5.62781300415635,
133.790871818885));
#149732=CARTESIAN_POINT('Ctrl Pts',(27.3383587787435,-2.16223136626054,
137.460359118851));
#149733=CARTESIAN_POINT('Ctrl Pts',(27.0599111549305,4.4311411779048,136.22123687532));
#149734=CARTESIAN_POINT('Ctrl Pts',(26.7814635311178,6.95251145285309,130.004269980034));
#149735=CARTESIAN_POINT('Ctrl Pts',(26.503015907305,3.08486335170113,124.522547294034));
#149736=CARTESIAN_POINT('Ctrl Pts',(26.224568283492,-3.61762346571424,124.813504168722));
#149737=CARTESIAN_POINT('Ctrl Pts',(26.0363547117943,-5.90099064463134,
128.731422459272));
#149738=CARTESIAN_POINT('Ctrl Pts',(25.9409570147008,-5.92644834143233,
130.748738712938));
#149739=CARTESIAN_POINT('Ctrl Pts',(25.9383751922117,-5.9263183307278,130.803338284789));
#149740=CARTESIAN_POINT('',(24.1883752150562,-5.91399912579995,130.799408621223));
#149741=CARTESIAN_POINT('Ctrl Pts',(25.9383751922117,-5.91674991196247,
130.80333993541));
#149742=CARTESIAN_POINT('Ctrl Pts',(25.9309865517842,-5.91677682314269,
130.959340236106));
#149743=CARTESIAN_POINT('Ctrl Pts',(25.9235979113567,-5.91062985096164,
131.115586525969));
#149744=CARTESIAN_POINT('Ctrl Pts',(25.9162092709292,-5.89827665873343,
131.271546896838));
#149745=CARTESIAN_POINT('Ctrl Pts',(25.9088293095786,-5.88593797719979,
131.42732406864));
#149746=CARTESIAN_POINT('Ctrl Pts',(25.9014493482279,-5.86740761380681,
131.582815617648));
#149747=CARTESIAN_POINT('Ctrl Pts',(25.8940693868772,-5.8427051950539,131.737487921952));
#149748=CARTESIAN_POINT('Ctrl Pts',(25.8866964457628,-5.81802627463759,
131.892013093219));
#149749=CARTESIAN_POINT('Ctrl Pts',(25.8793235046484,-5.78718704453997,
132.045720201084));
#149750=CARTESIAN_POINT('Ctrl Pts',(25.871950563534,-5.75025904433928,132.198079199452));
#149751=CARTESIAN_POINT('Ctrl Pts',(25.8645829896906,-5.71335792657033,
132.350327285224));
#149752=CARTESIAN_POINT('Ctrl Pts',(25.8572154158473,-5.67037695146818,
132.501228850292));
#149753=CARTESIAN_POINT('Ctrl Pts',(25.8498478420039,-5.62143897356322,
132.650262681329));
#149754=CARTESIAN_POINT('Ctrl Pts',(25.8422572250815,-5.5710194662557,132.803808304886));
#149755=CARTESIAN_POINT('Ctrl Pts',(25.8346666081591,-5.51427664135492,
132.955370916967));
#149756=CARTESIAN_POINT('Ctrl Pts',(25.8270759912367,-5.45140084465804,
133.104395268036));
#149757=CARTESIAN_POINT('Ctrl Pts',(25.8197131383383,-5.39041169889071,
133.248947994962));
#149758=CARTESIAN_POINT('Ctrl Pts',(25.81235028544,-5.3236525039499,133.391112229823));
#149759=CARTESIAN_POINT('Ctrl Pts',(25.8049874325417,-5.25134636247009,
133.530400225472));
#149760=CARTESIAN_POINT('Ctrl Pts',(25.7976246335066,-5.17904074994853,
133.669687202154));
#149761=CARTESIAN_POINT('Ctrl Pts',(25.7902618344715,-5.1011884450187,133.806097646521));
#149762=CARTESIAN_POINT('Ctrl Pts',(25.7828990354363,-5.01805886634146,
133.93916775301));
#149763=CARTESIAN_POINT('Ctrl Pts',(25.7755348016019,-4.93491308808304,
134.072263791063));
#149764=CARTESIAN_POINT('Ctrl Pts',(25.7681705677676,-4.84648818882913,
134.20201787566));
#149765=CARTESIAN_POINT('Ctrl Pts',(25.7608063339332,-4.75309721281873,
134.327994742726));
#149766=CARTESIAN_POINT('Ctrl Pts',(25.7534391759961,-4.65966915422614,
134.454021631195));
#149767=CARTESIAN_POINT('Ctrl Pts',(25.7460720180589,-4.56127131814642,
134.576268013992));
#149768=CARTESIAN_POINT('Ctrl Pts',(25.7387048601218,-4.45825721635506,
134.694331460043));
#149769=CARTESIAN_POINT('Ctrl Pts',(25.731329522749,-4.35512874247756,134.812525986813));
#149770=CARTESIAN_POINT('Ctrl Pts',(25.7239541853762,-4.24737401883896,
134.926528021219));
#149771=CARTESIAN_POINT('Ctrl Pts',(25.7165788480033,-4.13538404176333,
135.035971349856));
#149772=CARTESIAN_POINT('Ctrl Pts',(25.7091985999226,-4.02331949859767,
135.145487548952));
#149773=CARTESIAN_POINT('Ctrl Pts',(25.7018183518418,-3.90701436365152,
135.250438744274));
#149774=CARTESIAN_POINT('Ctrl Pts',(25.694438103761,-3.7868924195254,135.350499239016));
#149775=CARTESIAN_POINT('Ctrl Pts',(25.6870479415286,-3.66660911128828,
135.450694148606));
#149776=CARTESIAN_POINT('Ctrl Pts',(25.6796577792962,-3.54249905746435,
135.545985015808));
#149777=CARTESIAN_POINT('Ctrl Pts',(25.6722676170638,-3.41501511222522,
135.636089329505));
#149778=CARTESIAN_POINT('Ctrl Pts',(25.6707360899979,-3.38859551459576,
135.654762423659));
#149779=CARTESIAN_POINT('Ctrl Pts',(25.6692045629321,-3.36203109940731,
135.673212924242));
#149780=CARTESIAN_POINT('Ctrl Pts',(25.6676730358662,-3.33532602361916,
135.691438566471));
#149781=CARTESIAN_POINT('Ctrl Pts',(25.6602497694608,-3.20588731086571,
135.779777715472));
#149782=CARTESIAN_POINT('Ctrl Pts',(25.6528265030553,-3.0727408334396,135.863104438142));
#149783=CARTESIAN_POINT('Ctrl Pts',(25.6454032366499,-2.93631220034191,
135.941091214417));
#149784=CARTESIAN_POINT('Ctrl Pts',(25.6379887439289,-2.80004481455865,
136.018985816799));
#149785=CARTESIAN_POINT('Ctrl Pts',(25.6305742512079,-2.66050331566374,
136.091552852161));
#149786=CARTESIAN_POINT('Ctrl Pts',(25.6231597584869,-2.51814385723093,
136.158506868537));
#149787=CARTESIAN_POINT('Ctrl Pts',(25.6157524121331,-2.37592161020409,
136.225396352112));
#149788=CARTESIAN_POINT('Ctrl Pts',(25.6083450657794,-2.23088714630567,
136.286683429217));
#149789=CARTESIAN_POINT('Ctrl Pts',(25.6009377194256,-2.08352279988314,
136.342127613826));
#149790=CARTESIAN_POINT('Ctrl Pts',(25.5935358977502,-1.93626836334992,
136.39753044607));
#149791=CARTESIAN_POINT('Ctrl Pts',(25.5861340760748,-1.78668785219971,
136.447098931998));
#149792=CARTESIAN_POINT('Ctrl Pts',(25.5787322543995,-1.63528514282548,
136.490639986728));
#149793=CARTESIAN_POINT('Ctrl Pts',(25.5713343400881,-1.4839623577628,136.534158056474));
#149794=CARTESIAN_POINT('Ctrl Pts',(25.5639364257767,-1.33081964804332,
136.571654928886));
#149795=CARTESIAN_POINT('Ctrl Pts',(25.5565385114654,-1.17637756777835,
136.602986866992));
#149796=CARTESIAN_POINT('Ctrl Pts',(25.5491418265532,-1.02196115298549,
136.634313598298));
#149797=CARTESIAN_POINT('Ctrl Pts',(25.541745141641,-0.866246161694955,
136.65947735448));
#149798=CARTESIAN_POINT('Ctrl Pts',(25.5343484567288,-0.70976501781126,
136.678385147817));
#149799=CARTESIAN_POINT('Ctrl Pts',(25.5269520997934,-0.553290812465243,
136.697292102763));
#149800=CARTESIAN_POINT('Ctrl Pts',(25.5195557428579,-0.396050892675834,
136.70994360164));
#149801=CARTESIAN_POINT('Ctrl Pts',(25.5121593859225,-0.238584243338168,
136.716298381221));
#149802=CARTESIAN_POINT('Ctrl Pts',(25.5047618965859,-0.0810934854544955,
136.722654133735));
#149803=CARTESIAN_POINT('Ctrl Pts',(25.4973644072494,0.0766236980771254,
136.722711232359));
#149804=CARTESIAN_POINT('Ctrl Pts',(25.4899669179128,0.234027022798936,
136.716480534745));
#149805=CARTESIAN_POINT('Ctrl Pts',(25.4825668353979,0.391485525011773,
136.710247652969));
#149806=CARTESIAN_POINT('Ctrl Pts',(25.4751667528829,0.548629576587278,
136.69772260121));
#149807=CARTESIAN_POINT('Ctrl Pts',(25.467766670368,0.704922867280941,136.678968205625));
#149808=CARTESIAN_POINT('Ctrl Pts',(25.4603584507015,0.86138801851551,136.660193187654));
#149809=CARTESIAN_POINT('Ctrl Pts',(25.452950231035,1.01700016974872,136.635175190851));
#149810=CARTESIAN_POINT('Ctrl Pts',(25.4455420113686,1.17123134454028,136.604028513236));
#149811=CARTESIAN_POINT('Ctrl Pts',(25.4381292320665,1.32555744604644,136.572862665361));
#149812=CARTESIAN_POINT('Ctrl Pts',(25.4307164527644,1.47850051561693,136.535560708537));
#149813=CARTESIAN_POINT('Ctrl Pts',(25.4233036734624,1.62954713838233,136.492287013564));
#149814=CARTESIAN_POINT('Ctrl Pts',(25.4158803024336,1.78080958364573,136.448951487106));
#149815=CARTESIAN_POINT('Ctrl Pts',(25.4084569314049,1.93016981663079,136.399627297533));
#149816=CARTESIAN_POINT('Ctrl Pts',(25.4010335603761,2.07713303967526,136.344527483103));
#149817=CARTESIAN_POINT('Ctrl Pts',(25.3970975109352,2.1550564668704,136.315312239389));
#149818=CARTESIAN_POINT('Ctrl Pts',(25.3931614614943,2.23230638687109,136.284474045113));
#149819=CARTESIAN_POINT('Ctrl Pts',(25.3892254120534,2.30881190201944,136.252049867477));
#149820=CARTESIAN_POINT('Ctrl Pts',(25.3818021456479,2.45309891592922,136.190898880381));
#149821=CARTESIAN_POINT('Ctrl Pts',(25.3743788792425,2.5951729709797,136.12391910699));
#149822=CARTESIAN_POINT('Ctrl Pts',(25.3669556128371,2.73452846320441,136.051291591614));
#149823=CARTESIAN_POINT('Ctrl Pts',(25.3595411201161,2.87371924880987,135.97874991593));
#149824=CARTESIAN_POINT('Ctrl Pts',(25.352126627395,3.01019753950847,135.900573956051));
#149825=CARTESIAN_POINT('Ctrl Pts',(25.344712134674,3.14347661432864,135.816993193136));
#149826=CARTESIAN_POINT('Ctrl Pts',(25.3373047883202,3.27662722975921,135.733492988507));
#149827=CARTESIAN_POINT('Ctrl Pts',(25.3298974419664,3.40658445386946,135.644598548635));
#149828=CARTESIAN_POINT('Ctrl Pts',(25.3224900956126,3.53288524545814,135.550585686494));
#149829=CARTESIAN_POINT('Ctrl Pts',(25.3150882739371,3.65909183715158,135.456642942693));
#149830=CARTESIAN_POINT('Ctrl Pts',(25.3076864522617,3.78164712819944,135.357589599743));
#149831=CARTESIAN_POINT('Ctrl Pts',(25.3002846305863,3.90011631332493,135.253745216029));
#149832=CARTESIAN_POINT('Ctrl Pts',(25.2928867162749,4.01852295948891,135.149955650957));
#149833=CARTESIAN_POINT('Ctrl Pts',(25.2854888019636,4.13284751553753,135.041380327494));
#149834=CARTESIAN_POINT('Ctrl Pts',(25.2780908876523,4.24268767927291,134.928379509211));
#149835=CARTESIAN_POINT('Ctrl Pts',(25.27069420274,4.3525095895661,134.815397469614));
#149836=CARTESIAN_POINT('Ctrl Pts',(25.2632975178278,4.45784832665976,134.697991662238));
#149837=CARTESIAN_POINT('Ctrl Pts',(25.2559008329156,4.55833786922462,134.57655976826));
#149838=CARTESIAN_POINT('Ctrl Pts',(25.2485044759801,4.65882295597786,134.455133258698));
#149839=CARTESIAN_POINT('Ctrl Pts',(25.2411081190446,4.75445903773717,134.329681305086));
#149840=CARTESIAN_POINT('Ctrl Pts',(25.2337117621092,4.8449200640789,134.200635066898));
#149841=CARTESIAN_POINT('Ctrl Pts',(25.2263142727726,4.93539494023456,134.071569071402));
#149842=CARTESIAN_POINT('Ctrl Pts',(25.218916783436,5.02069296907916,133.938908001315));
#149843=CARTESIAN_POINT('Ctrl Pts',(25.2115192940994,5.10053124851564,133.803112282078));
#149844=CARTESIAN_POINT('Ctrl Pts',(25.2041192115844,5.18039751513722,133.667268959863));
#149845=CARTESIAN_POINT('Ctrl Pts',(25.1967191290695,5.25480003269814,133.528289122304));
#149846=CARTESIAN_POINT('Ctrl Pts',(25.1893190465545,5.32350176983622,133.386657941472));
#149847=CARTESIAN_POINT('Ctrl Pts',(25.181910826888,5.39227905159728,133.244871022595));
#149848=CARTESIAN_POINT('Ctrl Pts',(25.1745026072214,5.45534287111988,133.100427274226));
#149849=CARTESIAN_POINT('Ctrl Pts',(25.1670943875549,5.51250400640318,132.953832678768));
#149850=CARTESIAN_POINT('Ctrl Pts',(25.1596816082528,5.56970032341163,132.807147856783));
#149851=CARTESIAN_POINT('Ctrl Pts',(25.1522688289507,5.6209865956346,132.658309901965));
#149852=CARTESIAN_POINT('Ctrl Pts',(25.1448560496486,5.66622359960249,132.507839611216));
#149853=CARTESIAN_POINT('Ctrl Pts',(25.1374326786198,5.71152524032286,132.357154321461));
#149854=CARTESIAN_POINT('Ctrl Pts',(25.130009307591,5.75076025695564,132.204832398073));
#149855=CARTESIAN_POINT('Ctrl Pts',(25.1225859365622,5.78384043439918,132.051405280723));
#149856=CARTESIAN_POINT('Ctrl Pts',(25.1186498871216,5.80138033822696,131.970054541675));
#149857=CARTESIAN_POINT('Ctrl Pts',(25.114713837681,5.81719076069269,131.888393198882));
#149858=CARTESIAN_POINT('Ctrl Pts',(25.1107777882404,5.83126448143482,131.806500882228));
#149859=CARTESIAN_POINT('Ctrl Pts',(25.1033545218349,5.85780707952975,131.652054528784));
#149860=CARTESIAN_POINT('Ctrl Pts',(25.0959312554294,5.87824959631605,131.496319398934));
#149861=CARTESIAN_POINT('Ctrl Pts',(25.088507989024,5.89247105820696,131.339818730487));
#149862=CARTESIAN_POINT('Ctrl Pts',(25.081093496303,5.90667571151096,131.183503032834));
#149863=CARTESIAN_POINT('Ctrl Pts',(25.073679003582,5.91467391219624,131.026423965734));
#149864=CARTESIAN_POINT('Ctrl Pts',(25.066264510861,5.91639564468866,130.869115061499));
#149865=CARTESIAN_POINT('Ctrl Pts',(25.0588571645073,5.91811571771047,130.711957777509));
#149866=CARTESIAN_POINT('Ctrl Pts',(25.0514498181535,5.91357136183765,130.554571468168));
#149867=CARTESIAN_POINT('Ctrl Pts',(25.0440424717997,5.90274434125828,130.397494786802));
#149868=CARTESIAN_POINT('Ctrl Pts',(25.0366406501243,5.89192539587927,130.24053525915));
#149869=CARTESIAN_POINT('Ctrl Pts',(25.0292388284488,5.87483314150947,130.083885270469));
#149870=CARTESIAN_POINT('Ctrl Pts',(25.0218370067734,5.85150140879616,129.928083363863));
#149871=CARTESIAN_POINT('Ctrl Pts',(25.0144390924621,5.8281819927232,129.772363703874));
#149872=CARTESIAN_POINT('Ctrl Pts',(25.0070411781508,5.79862971315761,129.6174916026));
#149873=CARTESIAN_POINT('Ctrl Pts',(24.9996432638395,5.76293021588128,129.464000259534));
#149874=CARTESIAN_POINT('Ctrl Pts',(24.9922465789273,5.72723665121354,129.310534423945));
#149875=CARTESIAN_POINT('Ctrl Pts',(24.9848498940151,5.68539798080428,129.158449254398));
#149876=CARTESIAN_POINT('Ctrl Pts',(24.9774532091029,5.63755094161994,129.008267651392));
#149877=CARTESIAN_POINT('Ctrl Pts',(24.9700568521675,5.58970602402332,128.858092707595));
#149878=CARTESIAN_POINT('Ctrl Pts',(24.962660495232,5.5358533806978,128.709821518195));
#149879=CARTESIAN_POINT('Ctrl Pts',(24.9552641382965,5.4761795201021,128.563961450874));
#149880=CARTESIAN_POINT('Ctrl Pts',(24.9478666489599,5.41649652328609,128.418079052005));
#149881=CARTESIAN_POINT('Ctrl Pts',(24.9404691596234,5.35099067597582,128.274608855763));
#149882=CARTESIAN_POINT('Ctrl Pts',(24.9330716702868,5.2798964316416,128.134037746893));
#149883=CARTESIAN_POINT('Ctrl Pts',(24.9256715877718,5.20877726533044,127.99341736104));
#149884=CARTESIAN_POINT('Ctrl Pts',(24.9182715052568,5.1320659700031,127.855698418855));
#149885=CARTESIAN_POINT('Ctrl Pts',(24.9108714227418,5.05004261342194,127.721342588893));
#149886=CARTESIAN_POINT('Ctrl Pts',(24.9034632030753,4.96792906372778,127.586839020883));
#149887=CARTESIAN_POINT('Ctrl Pts',(24.8960549834089,4.8804919822371,127.455706269231));
#149888=CARTESIAN_POINT('Ctrl Pts',(24.8886467637424,4.78805478716329,127.328377027613));
#149889=CARTESIAN_POINT('Ctrl Pts',(24.8812339844403,4.69556069853792,127.200969416971));
#149890=CARTESIAN_POINT('Ctrl Pts',(24.8738212051382,4.59806059471343,127.077370273499));
#149891=CARTESIAN_POINT('Ctrl Pts',(24.8664084258361,4.49591738318717,126.957978233292));
#149892=CARTESIAN_POINT('Ctrl Pts',(24.8589850548074,4.39362822465067,126.838415600139));
#149893=CARTESIAN_POINT('Ctrl Pts',(24.8515616837786,4.28668296138282,126.723072349192));
#149894=CARTESIAN_POINT('Ctrl Pts',(24.8441383127499,4.17548102621142,126.612309954436));
#149895=CARTESIAN_POINT('Ctrl Pts',(24.8402022633091,4.11651909192989,126.553581075029));
#149896=CARTESIAN_POINT('Ctrl Pts',(24.8362662138683,4.05636101100038,126.496139368364));
#149897=CARTESIAN_POINT('Ctrl Pts',(24.8323301644275,3.99506987551722,126.44003395103));
#149898=CARTESIAN_POINT('Ctrl Pts',(24.8249068980221,3.87947670682649,126.334220884929));
#149899=CARTESIAN_POINT('Ctrl Pts',(24.8174836316166,3.75950201109489,126.232843374869));
#149900=CARTESIAN_POINT('Ctrl Pts',(24.8100603652112,3.63552061393169,126.13628602217));
#149901=CARTESIAN_POINT('Ctrl Pts',(24.8026458724902,3.51168575248375,126.039842792244));
#149902=CARTESIAN_POINT('Ctrl Pts',(24.7952313797692,3.38385390745977,125.94820860685));
#149903=CARTESIAN_POINT('Ctrl Pts',(24.7878168870482,3.25243610957519,125.861730759319));
#149904=CARTESIAN_POINT('Ctrl Pts',(24.7804095406944,3.12114497711258,125.775336262395));
#149905=CARTESIAN_POINT('Ctrl Pts',(24.7730021943407,2.98627508230078,125.69408841312));
#149906=CARTESIAN_POINT('Ctrl Pts',(24.7655948479869,2.84826975253751,125.618293709081));
#149907=CARTESIAN_POINT('Ctrl Pts',(24.7581930263115,2.71036735235504,125.542555535592));
#149908=CARTESIAN_POINT('Ctrl Pts',(24.7507912046361,2.56933449933088,125.472262588));
#149909=CARTESIAN_POINT('Ctrl Pts',(24.7433893829607,2.42564257132432,125.407677499328));
#149910=CARTESIAN_POINT('Ctrl Pts',(24.7359914686493,2.28202649716826,125.343126504621));
#149911=CARTESIAN_POINT('Ctrl Pts',(24.7285935543379,2.13575448319964,125.284277520683));
#149912=CARTESIAN_POINT('Ctrl Pts',(24.7211956400266,1.98732141889056,125.231346698642));
#149913=CARTESIAN_POINT('Ctrl Pts',(24.7137989551144,1.83891302146392,125.178424672744));
#149914=CARTESIAN_POINT('Ctrl Pts',(24.7064022702022,1.6883446377251,125.131418982065));
#149915=CARTESIAN_POINT('Ctrl Pts',(24.6990055852899,1.53613010834403,125.090497226415));
#149916=CARTESIAN_POINT('Ctrl Pts',(24.6916092283545,1.38392232831514,125.049577285278));
#149917=CARTESIAN_POINT('Ctrl Pts',(24.6842128714191,1.23006890827354,125.014740839698));
#149918=CARTESIAN_POINT('Ctrl Pts',(24.6768165144836,1.07509752339819,124.986105219452));
#149919=CARTESIAN_POINT('Ctrl Pts',(24.6694190251471,0.920102412008413,
124.957465215019));
#149920=CARTESIAN_POINT('Ctrl Pts',(24.6620215358105,0.763989362083347,
124.93502799406));
#149921=CARTESIAN_POINT('Ctrl Pts',(24.654624046474,0.607294731375145,124.918859477328));
#149922=CARTESIAN_POINT('Ctrl Pts',(24.647223963959,0.450545171606831,124.902685292747));
#149923=CARTESIAN_POINT('Ctrl Pts',(24.639823881444,0.293213996241964,124.89278422586));
#149924=CARTESIAN_POINT('Ctrl Pts',(24.632423798929,0.135841003575897,124.889170190856));
#149925=CARTESIAN_POINT('Ctrl Pts',(24.6250155792626,-0.0217050368741682,
124.885552181848));
#149926=CARTESIAN_POINT('Ctrl Pts',(24.6176073595961,-0.179292613026846,
124.888235019489));
#149927=CARTESIAN_POINT('Ctrl Pts',(24.6101991399296,-0.336382871992765,
124.897180484378));
#149928=CARTESIAN_POINT('Ctrl Pts',(24.6027863606276,-0.493569817392334,
124.906131455051));
#149929=CARTESIAN_POINT('Ctrl Pts',(24.5953735813255,-0.650258464994145,
124.921352697622));
#149930=CARTESIAN_POINT('Ctrl Pts',(24.5879608020234,-0.805917270594964,
124.94275436028));
#149931=CARTESIAN_POINT('Ctrl Pts',(24.5805374309947,-0.961798488796456,
124.964186602637));
#149932=CARTESIAN_POINT('Ctrl Pts',(24.5731140599659,-1.11664655958836,
124.991816836919));
#149933=CARTESIAN_POINT('Ctrl Pts',(24.5656906889372,-1.26994146146879,
125.025504394494));
#149934=CARTESIAN_POINT('Ctrl Pts',(24.5617546394963,-1.35122209670789,
125.043366345842));
#149935=CARTESIAN_POINT('Ctrl Pts',(24.5578185900555,-1.43206634354629,
125.062930397549));
#149936=CARTESIAN_POINT('Ctrl Pts',(24.5538825406146,-1.51239877598623,
125.084170017167));
#149937=CARTESIAN_POINT('Ctrl Pts',(24.5464592742092,-1.66390323647658,
125.1242272769));
#149938=CARTESIAN_POINT('Ctrl Pts',(24.5390360078037,-1.81404426043895,
125.170368365808));
#149939=CARTESIAN_POINT('Ctrl Pts',(24.5316127413982,-1.96229566949174,
125.222485818899));
#149940=CARTESIAN_POINT('Ctrl Pts',(24.5241982486772,-2.11037185769075,
125.274541673489));
#149941=CARTESIAN_POINT('Ctrl Pts',(24.5167837559562,-2.25656252778023,
125.332559709599));
#149942=CARTESIAN_POINT('Ctrl Pts',(24.5093692632351,-2.40035331990266,
125.396381835976));
#149943=CARTESIAN_POINT('Ctrl Pts',(24.5019619168813,-2.54400552104704,
125.460142448185));
#149944=CARTESIAN_POINT('Ctrl Pts',(24.4945545705274,-2.68526211022845,
125.529695863283));
#149945=CARTESIAN_POINT('Ctrl Pts',(24.4871472241736,-2.82362559306031,
125.604834766807));
#149946=CARTESIAN_POINT('Ctrl Pts',(24.4797454024982,-2.96188587918515,
125.6799176289));
#149947=CARTESIAN_POINT('Ctrl Pts',(24.4723435808227,-3.09725702877218,
125.760577507234));
#149948=CARTESIAN_POINT('Ctrl Pts',(24.4649417591473,-3.22926328997477,
125.846559777827));
#149949=CARTESIAN_POINT('Ctrl Pts',(24.457543844836,-3.36119986609922,125.932496659048));
#149950=CARTESIAN_POINT('Ctrl Pts',(24.4501459305247,-3.48977477941823,
126.023750133753));
#149951=CARTESIAN_POINT('Ctrl Pts',(24.4427480162133,-3.61453867601762,
126.120020672379));
#149952=CARTESIAN_POINT('Ctrl Pts',(24.4353513313011,-3.73928183912138,
126.216275212588));
#149953=CARTESIAN_POINT('Ctrl Pts',(24.4279546463888,-3.86021494720823,
126.317544934156));
#149954=CARTESIAN_POINT('Ctrl Pts',(24.4205579614766,-3.97691925037793,
126.423488120166));
#149955=CARTESIAN_POINT('Ctrl Pts',(24.4131616045412,-4.0936183787562,126.529426608544));
#149956=CARTESIAN_POINT('Ctrl Pts',(24.4057652476058,-4.20608879865333,
126.640037898417));
#149957=CARTESIAN_POINT('Ctrl Pts',(24.3983688906703,-4.3139465758812,126.754941461324));
#149958=CARTESIAN_POINT('Ctrl Pts',(24.3909714013337,-4.42182086641042,
126.869862616259));
#149959=CARTESIAN_POINT('Ctrl Pts',(24.3835739119972,-4.52508085261635,
126.989077080526));
#149960=CARTESIAN_POINT('Ctrl Pts',(24.3761764226606,-4.62338115903669,
127.112169232932));
#149961=CARTESIAN_POINT('Ctrl Pts',(24.3687763401456,-4.72171592447677,
127.235304535101));
#149962=CARTESIAN_POINT('Ctrl Pts',(24.3613762576305,-4.81508731577404,
127.362319940287));
#149963=CARTESIAN_POINT('Ctrl Pts',(24.3539761751155,-4.90319185236293,
127.492768821855));
#149964=CARTESIAN_POINT('Ctrl Pts',(24.3465679554491,-4.99139326894742,
127.623361145378));
#149965=CARTESIAN_POINT('Ctrl Pts',(24.3391597357826,-5.07431605585901,
127.757394175585));
#149966=CARTESIAN_POINT('Ctrl Pts',(24.3317515161161,-5.15170110501327,
127.894393901759));
#149967=CARTESIAN_POINT('Ctrl Pts',(24.324338736814,-5.22913378337383,128.031477948978));
#149968=CARTESIAN_POINT('Ctrl Pts',(24.316925957512,-5.30102176227275,128.171531999267));
#149969=CARTESIAN_POINT('Ctrl Pts',(24.3095131782099,-5.36715332395629,
128.314060282336));
#149970=CARTESIAN_POINT('Ctrl Pts',(24.3020898071812,-5.4333793775166,128.456792216501));
#149971=CARTESIAN_POINT('Ctrl Pts',(24.2946664361524,-5.4938324435237,128.60200510052));
#149972=CARTESIAN_POINT('Ctrl Pts',(24.2872430651236,-5.54834978615739,
128.749185390743));
#149973=CARTESIAN_POINT('Ctrl Pts',(24.283307015683,-5.57725618934632,128.827223912159));
#149974=CARTESIAN_POINT('Ctrl Pts',(24.2793709662423,-5.60449468870749,
128.905815314474));
#149975=CARTESIAN_POINT('Ctrl Pts',(24.2754349168017,-5.63004683714687,
128.984881798224));
#149976=CARTESIAN_POINT('Ctrl Pts',(24.2665164093745,-5.68794423632163,
129.164034787332));
#149977=CARTESIAN_POINT('Ctrl Pts',(24.2575979019474,-5.73732328000852,
129.34606681738));
#149978=CARTESIAN_POINT('Ctrl Pts',(24.2486793945203,-5.77793595100518,
129.530238681258));
#149979=CARTESIAN_POINT('Ctrl Pts',(24.2398101565805,-5.81832426097514,
129.713393104336));
#149980=CARTESIAN_POINT('Ctrl Pts',(24.2309409186407,-5.85004272511329,
129.898663761957));
#149981=CARTESIAN_POINT('Ctrl Pts',(24.222071680701,-5.87289414555811,130.085302262793));
#149982=CARTESIAN_POINT('Ctrl Pts',(24.2132929185469,-5.89551245688669,
130.270036849773));
#149983=CARTESIAN_POINT('Ctrl Pts',(24.2045141563928,-5.90944364635717,
130.456111473033));
#149984=CARTESIAN_POINT('Ctrl Pts',(24.1957353942387,-5.91454328238171,
130.642779915335));
#149985=CARTESIAN_POINT('Ctrl Pts',(24.1932820128116,-5.91596846648941,
130.69494773596));
#149986=CARTESIAN_POINT('Ctrl Pts',(24.1908286313845,-5.91670417310227,
130.747161813275));
#149987=CARTESIAN_POINT('Ctrl Pts',(24.1883752499575,-5.91674792517552,
130.799405576576));
#149988=CARTESIAN_POINT('',(22.4383751628218,-5.91238909884781,130.807386683679));
#149989=CARTESIAN_POINT('Ctrl Pts',(24.1883751922117,-5.91219990274765,
130.799410614093));
#149990=CARTESIAN_POINT('Ctrl Pts',(24.1245792258041,-5.90151963868852,
132.156885527756));
#149991=CARTESIAN_POINT('Ctrl Pts',(23.9679673847923,-4.76179293726462,
135.505531964573));
#149992=CARTESIAN_POINT('Ctrl Pts',(23.718539669176,0.810670249943998,137.755646417775));
#149993=CARTESIAN_POINT('Ctrl Pts',(23.4400920453631,6.28650068617809,133.879660546521));
#149994=CARTESIAN_POINT('Ctrl Pts',(23.1616444215502,5.98534410444456,127.177624277308));
#149995=CARTESIAN_POINT('Ctrl Pts',(22.8831967977373,0.183948691041906,
123.808381528874));
#149996=CARTESIAN_POINT('Ctrl Pts',(22.6421070546244,-4.98546409398633,
126.457594913206));
#149997=CARTESIAN_POINT('Ctrl Pts',(22.4938331861159,-5.90300137026986,
129.625444179626));
#149998=CARTESIAN_POINT('Ctrl Pts',(22.4383751922117,-5.90844756488801,
130.807384039503));
#149999=CARTESIAN_POINT('',(20.6883751922117,-5.92023233031357,130.808223305572));
#150000=CARTESIAN_POINT('Ctrl Pts',(22.4383751303106,-5.91674922467675,
130.807389608667));
#150001=CARTESIAN_POINT('Ctrl Pts',(22.4302244668188,-5.9166601718607,130.981342968942));
#150002=CARTESIAN_POINT('Ctrl Pts',(22.4220738033269,-5.90889565774037,
131.155031843747));
#150003=CARTESIAN_POINT('Ctrl Pts',(22.413923139835,-5.89355001080322,131.327809595654));
#150004=CARTESIAN_POINT('Ctrl Pts',(22.4057305305205,-5.87812539044425,
131.501476515046));
#150005=CARTESIAN_POINT('Ctrl Pts',(22.3975379212059,-5.85504148845746,
131.674222681994));
#150006=CARTESIAN_POINT('Ctrl Pts',(22.3893453118913,-5.82444442124337,
131.845407084515));
#150007=CARTESIAN_POINT('Ctrl Pts',(22.3811313931613,-5.79376776941935,
132.017036746832));
#150008=CARTESIAN_POINT('Ctrl Pts',(22.3729174744312,-5.75553892972251,
132.187096296581));
#150009=CARTESIAN_POINT('Ctrl Pts',(22.3647035557012,-5.7099541235859,132.354958717992));
#150010=CARTESIAN_POINT('Ctrl Pts',(22.3564598853453,-5.66420420477377,
132.523429153692));
#150011=CARTESIAN_POINT('Ctrl Pts',(22.3482162149894,-5.61104504834546,
132.689686306487));
#150012=CARTESIAN_POINT('Ctrl Pts',(22.3399725446335,-5.55072257989809,
132.85311863244));
#150013=CARTESIAN_POINT('Ctrl Pts',(22.3354155464595,-5.51737707156257,
132.943461984223));
#150014=CARTESIAN_POINT('Ctrl Pts',(22.3308585482854,-5.48184347136795,
133.032942554786));
#150015=CARTESIAN_POINT('Ctrl Pts',(22.3263015501114,-5.44416932289011,
133.121460301697));
#150016=CARTESIAN_POINT('Ctrl Pts',(22.318878283706,-5.3827988263333,133.265654087132));
#150017=CARTESIAN_POINT('Ctrl Pts',(22.3114550173006,-5.31560291797675,
133.40762604585));
#150018=CARTESIAN_POINT('Ctrl Pts',(22.3040317508951,-5.24276341136604,
133.546870849988));
#150019=CARTESIAN_POINT('Ctrl Pts',(22.2966172581741,-5.1700099950031,133.685951078332));
#150020=CARTESIAN_POINT('Ctrl Pts',(22.2892027654531,-5.0916264289242,133.822310240488));
#150021=CARTESIAN_POINT('Ctrl Pts',(22.281788272732,-5.00784293473085,133.95546196528));
#150022=CARTESIAN_POINT('Ctrl Pts',(22.2743809263782,-4.92414019422371,
134.088485353427));
#150023=CARTESIAN_POINT('Ctrl Pts',(22.2669735800244,-4.83504808451739,
134.218307144843));
#150024=CARTESIAN_POINT('Ctrl Pts',(22.2595662336707,-4.74084312293794,
134.344464718605));
#150025=CARTESIAN_POINT('Ctrl Pts',(22.2521644119952,-4.64670842297286,
134.470528199288));
#150026=CARTESIAN_POINT('Ctrl Pts',(22.2447625903198,-4.54746868643463,
134.592932606093));
#150027=CARTESIAN_POINT('Ctrl Pts',(22.2373607686444,-4.44344413303837,
134.711243620558));
#150028=CARTESIAN_POINT('Ctrl Pts',(22.229962854333,-4.33947449339412,134.829492179559));
#150029=CARTESIAN_POINT('Ctrl Pts',(22.2225649400217,-4.23072531314612,
134.943651370063));
#150030=CARTESIAN_POINT('Ctrl Pts',(22.2151670257103,-4.11755746768501,
135.053319438596));
#150031=CARTESIAN_POINT('Ctrl Pts',(22.2077703407981,-4.00440842866689,
135.162969282286));
#150032=CARTESIAN_POINT('Ctrl Pts',(22.2003736558859,-3.88684244961945,
135.268129225746));
#150033=CARTESIAN_POINT('Ctrl Pts',(22.1929769709737,-3.76525776827935,
135.368433853275));
#150034=CARTESIAN_POINT('Ctrl Pts',(22.1855806140382,-3.64367847813143,
135.468734033191));
#150035=CARTESIAN_POINT('Ctrl Pts',(22.1781842571028,-3.51808112795462,
135.564179087687));
#150036=CARTESIAN_POINT('Ctrl Pts',(22.1707879001673,-3.38889737291734,
135.65444362287));
#150037=CARTESIAN_POINT('Ctrl Pts',(22.1633904108308,-3.25969383951737,
135.744721977783));
#150038=CARTESIAN_POINT('Ctrl Pts',(22.1559929214942,-3.12690311396992,
135.829818020288));
#150039=CARTESIAN_POINT('Ctrl Pts',(22.1485954321576,-2.99098605171237,
135.909449549305));
#150040=CARTESIAN_POINT('Ctrl Pts',(22.1411953496426,-2.85502134393895,
135.989108993031));
#150041=CARTESIAN_POINT('Ctrl Pts',(22.1337952671276,-2.71592843934977,
136.063299920781));
#150042=CARTESIAN_POINT('Ctrl Pts',(22.1263951846125,-2.57419287017456,
136.131786039817));
#150043=CARTESIAN_POINT('Ctrl Pts',(22.1189869649461,-2.43230144817048,
136.20034746638));
#150044=CARTESIAN_POINT('Ctrl Pts',(22.1115787452796,-2.28776189466713,
136.26319139408));
#150045=CARTESIAN_POINT('Ctrl Pts',(22.1041705256131,-2.14108047944648,
136.320129371152));
#150046=CARTESIAN_POINT('Ctrl Pts',(22.096757746311,-1.99430878426228,136.377102392599));
#150047=CARTESIAN_POINT('Ctrl Pts',(22.089344967009,-1.84539295282117,136.428162099402));
#150048=CARTESIAN_POINT('Ctrl Pts',(22.0819321877069,-1.69485399329648,
136.473170060818));
#150049=CARTESIAN_POINT('Ctrl Pts',(22.0745088166781,-1.54409993664685,
136.51824233172));
#150050=CARTESIAN_POINT('Ctrl Pts',(22.0670854456493,-1.39171848062952,
136.557245494882));
#150051=CARTESIAN_POINT('Ctrl Pts',(22.0596620746206,-1.23824119854686,
136.590092144065));
#150052=CARTESIAN_POINT('Ctrl Pts',(22.0557260251799,-1.15686386095275,
136.607508225605));
#150053=CARTESIAN_POINT('Ctrl Pts',(22.0517899757393,-1.07517855195031,
136.6231943551));
#150054=CARTESIAN_POINT('Ctrl Pts',(22.0478539262986,-0.993264912318842,
136.63714343338));
#150055=CARTESIAN_POINT('Ctrl Pts',(22.0404306598932,-0.838778344405665,
136.663450959681));
#150056=CARTESIAN_POINT('Ctrl Pts',(22.0330073934877,-0.683012284863759,
136.683656450438));
#150057=CARTESIAN_POINT('Ctrl Pts',(22.0255841270823,-0.526490154997762,
136.697639728485));
#150058=CARTESIAN_POINT('Ctrl Pts',(22.0181696343613,-0.37015302129069,
136.711606479458));
#150059=CARTESIAN_POINT('Ctrl Pts',(22.0107551416403,-0.213061964186039,
136.719365623281));
#150060=CARTESIAN_POINT('Ctrl Pts',(22.0033406489193,-0.0557506219285824,
136.720847956406));
#150061=CARTESIAN_POINT('Ctrl Pts',(21.9959333025655,0.101409097734539,
136.722328860803));
#150062=CARTESIAN_POINT('Ctrl Pts',(21.9885259562117,0.25878830908947,136.717544995021));
#150063=CARTESIAN_POINT('Ctrl Pts',(21.981118609858,0.415848331681116,136.70647894301));
#150064=CARTESIAN_POINT('Ctrl Pts',(21.9737167881825,0.572791212982378,
136.695421144477));
#150065=CARTESIAN_POINT('Ctrl Pts',(21.9663149665071,0.729415008763857,
136.678090515284));
#150066=CARTESIAN_POINT('Ctrl Pts',(21.9589131448317,0.885181228026921,
136.654521705609));
#150067=CARTESIAN_POINT('Ctrl Pts',(21.9515152305203,1.04086521951532,136.630965337725));
#150068=CARTESIAN_POINT('Ctrl Pts',(21.944117316209,1.19569216791252,136.601177403406));
#150069=CARTESIAN_POINT('Ctrl Pts',(21.9367194018976,1.34912900468063,136.565244359773));
#150070=CARTESIAN_POINT('Ctrl Pts',(21.9293227169854,1.50254034302988,136.529317287561));
#150071=CARTESIAN_POINT('Ctrl Pts',(21.9219260320732,1.65456166513102,136.487247217862));
#150072=CARTESIAN_POINT('Ctrl Pts',(21.914529347161,1.80467027918037,136.439171683249));
#150073=CARTESIAN_POINT('Ctrl Pts',(21.9071329902256,1.95477223725647,136.391098280356));
#150074=CARTESIAN_POINT('Ctrl Pts',(21.8997366332901,2.10296130040508,136.337020055881));
#150075=CARTESIAN_POINT('Ctrl Pts',(21.8923402763547,2.24873038536462,136.277124290194));
#150076=CARTESIAN_POINT('Ctrl Pts',(21.8849427870181,2.39452178794319,136.217219354313));
#150077=CARTESIAN_POINT('Ctrl Pts',(21.8775452976815,2.53789212930005,136.151495245641));
#150078=CARTESIAN_POINT('Ctrl Pts',(21.870147808345,2.67835488205304,136.080187158335));
#150079=CARTESIAN_POINT('Ctrl Pts',(21.86274772583,2.81886687380627,136.008854074089));
#150080=CARTESIAN_POINT('Ctrl Pts',(21.8553476433149,2.95646891498172,135.931933282806));
#150081=CARTESIAN_POINT('Ctrl Pts',(21.8479475608,3.09069976377644,135.849705554505));
#150082=CARTESIAN_POINT('Ctrl Pts',(21.8405393411335,3.22507821318868,135.767387408363));
#150083=CARTESIAN_POINT('Ctrl Pts',(21.8331311214671,3.35607774863777,135.679750866398));
#150084=CARTESIAN_POINT('Ctrl Pts',(21.8257229018006,3.4832661691351,135.587120004934));
#150085=CARTESIAN_POINT('Ctrl Pts',(21.8183101224985,3.61053287198317,135.494432130721));
#150086=CARTESIAN_POINT('Ctrl Pts',(21.8108973431965,3.73398349376836,135.396744042944));
#150087=CARTESIAN_POINT('Ctrl Pts',(21.8034845638944,3.85321995114101,135.294419255338));
#150088=CARTESIAN_POINT('Ctrl Pts',(21.7960611928656,3.9726267791556,135.191948261276));
#150089=CARTESIAN_POINT('Ctrl Pts',(21.7886378218369,4.08780714405189,135.084827589056));
#150090=CARTESIAN_POINT('Ctrl Pts',(21.7812144508081,4.1984001801314,134.973457221145));
#150091=CARTESIAN_POINT('Ctrl Pts',(21.7772784013673,4.25703926150438,134.914405979783));
#150092=CARTESIAN_POINT('Ctrl Pts',(21.7733423519265,4.31438935129554,134.854160552016));
#150093=CARTESIAN_POINT('Ctrl Pts',(21.7694063024857,4.37040142898546,134.792784104612));
#150094=CARTESIAN_POINT('Ctrl Pts',(21.7619830360803,4.47603845943128,134.677030040302));
#150095=CARTESIAN_POINT('Ctrl Pts',(21.7545597696748,4.57723327103468,134.556901204187));
#150096=CARTESIAN_POINT('Ctrl Pts',(21.7471365032694,4.67360183334036,134.432773006738));
#150097=CARTESIAN_POINT('Ctrl Pts',(21.7397220105484,4.7698564960083,134.308791518511));
#150098=CARTESIAN_POINT('Ctrl Pts',(21.7323075178274,4.86129603698431,134.180820369883));
#150099=CARTESIAN_POINT('Ctrl Pts',(21.7248930251064,4.9475737888576,134.049271119615));
#150100=CARTESIAN_POINT('Ctrl Pts',(21.7174856787526,5.03376838298534,133.917848661468));
#150101=CARTESIAN_POINT('Ctrl Pts',(21.7100783323988,5.1148108891555,133.782855277437));
#150102=CARTESIAN_POINT('Ctrl Pts',(21.7026709860451,5.19039548480622,133.644734760844));
#150103=CARTESIAN_POINT('Ctrl Pts',(21.6952691643697,5.26592370661386,133.506717259744));
#150104=CARTESIAN_POINT('Ctrl Pts',(21.6878673426943,5.33600194481329,133.365577596133));
#150105=CARTESIAN_POINT('Ctrl Pts',(21.6804655210189,5.40036828404338,133.221787547009));
#150106=CARTESIAN_POINT('Ctrl Pts',(21.6730676067075,5.46470064478401,133.078073403533));
#150107=CARTESIAN_POINT('Ctrl Pts',(21.6656696923962,5.52332695947045,132.93171200081));
#150108=CARTESIAN_POINT('Ctrl Pts',(21.6582717780849,5.57603183036203,132.783198556683));
#150109=CARTESIAN_POINT('Ctrl Pts',(21.6508750931727,5.62872794266023,132.634709792797));
#150110=CARTESIAN_POINT('Ctrl Pts',(21.6434784082604,5.67550443945883,132.484070048754));
#150111=CARTESIAN_POINT('Ctrl Pts',(21.6360817233482,5.71619450311981,132.331793419689));
#150112=CARTESIAN_POINT('Ctrl Pts',(21.6286853664128,5.75688276254074,132.17952354273));
#150113=CARTESIAN_POINT('Ctrl Pts',(21.6212890094774,5.79148502906606,132.025617285708));
#150114=CARTESIAN_POINT('Ctrl Pts',(21.6138926525419,5.81988477608601,131.870602501747));
#150115=CARTESIAN_POINT('Ctrl Pts',(21.6064951632054,5.84828887117973,131.715563984627));
#150116=CARTESIAN_POINT('Ctrl Pts',(21.5990976738687,5.87048848866989,131.559416969847));
#150117=CARTESIAN_POINT('Ctrl Pts',(21.5917001845322,5.88641852412558,131.402697914858));
#150118=CARTESIAN_POINT('Ctrl Pts',(21.5843001020172,5.90235414383049,131.245923922248));
#150119=CARTESIAN_POINT('Ctrl Pts',(21.5769000195022,5.9120157679861,131.088577861331));
#150120=CARTESIAN_POINT('Ctrl Pts',(21.5694999369872,5.91539030390024,130.931199550954));
#150121=CARTESIAN_POINT('Ctrl Pts',(21.5620917173207,5.91876855046352,130.773648186946));
#150122=CARTESIAN_POINT('Ctrl Pts',(21.5546834976543,5.91584589446426,130.616064876099));
#150123=CARTESIAN_POINT('Ctrl Pts',(21.5472752779878,5.90666137530154,130.458988412516));
#150124=CARTESIAN_POINT('Ctrl Pts',(21.5398624986857,5.89747120322051,130.30181527099));
#150125=CARTESIAN_POINT('Ctrl Pts',(21.5324497193837,5.88201152482766,130.145149968972));
#150126=CARTESIAN_POINT('Ctrl Pts',(21.5250369400816,5.86037300074793,129.989523913309));
#150127=CARTESIAN_POINT('Ctrl Pts',(21.5176135690529,5.83870355853024,129.833675491839));
#150128=CARTESIAN_POINT('Ctrl Pts',(21.5101901980241,5.81083770383978,129.678869648872));
#150129=CARTESIAN_POINT('Ctrl Pts',(21.5027668269954,5.77691689652957,129.525626191232));
#150130=CARTESIAN_POINT('Ctrl Pts',(21.4988307775545,5.75893127057486,129.444372832964));
#150131=CARTESIAN_POINT('Ctrl Pts',(21.4948947281136,5.73924421034106,129.363558452899));
#150132=CARTESIAN_POINT('Ctrl Pts',(21.4909586786728,5.71788236303121,129.283258436568));
#150133=CARTESIAN_POINT('Ctrl Pts',(21.4835354122674,5.67759458568581,129.131815111848));
#150134=CARTESIAN_POINT('Ctrl Pts',(21.476112145862,5.63122506112857,128.98174448063));
#150135=CARTESIAN_POINT('Ctrl Pts',(21.4686888794565,5.57888205498102,128.833572557142));
#150136=CARTESIAN_POINT('Ctrl Pts',(21.4612743867355,5.52660091391984,128.685575760562));
#150137=CARTESIAN_POINT('Ctrl Pts',(21.4538598940145,5.46836046768032,128.539473553334));
#150138=CARTESIAN_POINT('Ctrl Pts',(21.4464454012935,5.40431959010051,128.395780054131));
#150139=CARTESIAN_POINT('Ctrl Pts',(21.4390380549397,5.34034043752962,128.252225052133));
#150140=CARTESIAN_POINT('Ctrl Pts',(21.4316307085859,5.27057213449128,128.111074474983));
#150141=CARTESIAN_POINT('Ctrl Pts',(21.4242233622321,5.19522275231093,127.972825500996));
#150142=CARTESIAN_POINT('Ctrl Pts',(21.4168215405567,5.11992956854257,127.834679638309));
#150143=CARTESIAN_POINT('Ctrl Pts',(21.4094197188813,5.03906377176702,127.699431396083));
#150144=CARTESIAN_POINT('Ctrl Pts',(21.4020178972059,4.95288070968222,127.567556138121));
#150145=CARTESIAN_POINT('Ctrl Pts',(21.3946199828945,4.86674314296504,127.43575049608));
#150146=CARTESIAN_POINT('Ctrl Pts',(21.3872220685832,4.77529410479863,127.307314603903));
#150147=CARTESIAN_POINT('Ctrl Pts',(21.3798241542719,4.67883380824042,127.182697359149));
#150148=CARTESIAN_POINT('Ctrl Pts',(21.3724274693596,4.58238954163353,127.058100823521));
#150149=CARTESIAN_POINT('Ctrl Pts',(21.3650307844474,4.48093589773038,126.93732197075));
#150150=CARTESIAN_POINT('Ctrl Pts',(21.3576340995352,4.37481523031845,126.820779030216));
#150151=CARTESIAN_POINT('Ctrl Pts',(21.3502377425997,4.26869926840813,126.704241257319));
#150152=CARTESIAN_POINT('Ctrl Pts',(21.3428413856643,4.15791694578784,126.591939299214));
#150153=CARTESIAN_POINT('Ctrl Pts',(21.3354450287288,4.0428493747614,126.484256510546));
#150154=CARTESIAN_POINT('Ctrl Pts',(21.3280475393922,3.92776418659609,126.376557235368));
#150155=CARTESIAN_POINT('Ctrl Pts',(21.3206500500557,3.80839271625744,126.273478792856));
#150156=CARTESIAN_POINT('Ctrl Pts',(21.3132525607191,3.68515111005727,126.175365925568));
#150157=CARTESIAN_POINT('Ctrl Pts',(21.3058524782041,3.5618663017031,126.077218664966));
#150158=CARTESIAN_POINT('Ctrl Pts',(21.2984523956891,3.43470894823616,125.984040677616));
#150159=CARTESIAN_POINT('Ctrl Pts',(21.2910523131741,3.30412613761959,125.896134764042));
#150160=CARTESIAN_POINT('Ctrl Pts',(21.2836440935076,3.1733997377785,125.808132188879));
#150161=CARTESIAN_POINT('Ctrl Pts',(21.2762358738411,3.03924066841423,125.725413473446));
#150162=CARTESIAN_POINT('Ctrl Pts',(21.2688276541746,2.90212333401301,125.648237004164));
#150163=CARTESIAN_POINT('Ctrl Pts',(21.2614148748726,2.76492160618038,125.571013034053));
#150164=CARTESIAN_POINT('Ctrl Pts',(21.2540020955705,2.62475831680516,125.499338276822));
#150165=CARTESIAN_POINT('Ctrl Pts',(21.2465893162685,2.48212955780155,125.433423695502));
#150166=CARTESIAN_POINT('Ctrl Pts',(21.2391659452397,2.33929700413846,125.367414932337));
#150167=CARTESIAN_POINT('Ctrl Pts',(21.231742574211,2.193992288999,125.307182925623));
#150168=CARTESIAN_POINT('Ctrl Pts',(21.2243192031822,2.04672920309351,125.252889629467));
#150169=CARTESIAN_POINT('Ctrl Pts',(21.2203831537414,1.9686467814178,125.224102021095));
#150170=CARTESIAN_POINT('Ctrl Pts',(21.2164471043007,1.8900140177486,125.196983156011));
#150171=CARTESIAN_POINT('Ctrl Pts',(21.2125110548599,1.81090873953358,125.171551362888));
#150172=CARTESIAN_POINT('Ctrl Pts',(21.2050877884545,1.66171865361026,125.123587794758));
#150173=CARTESIAN_POINT('Ctrl Pts',(21.1976645220491,1.51039612068351,125.081482947169));
#150174=CARTESIAN_POINT('Ctrl Pts',(21.1902412556437,1.35744221163455,125.045430056726));
#150175=CARTESIAN_POINT('Ctrl Pts',(21.1828267629226,1.20466908140384,125.009419777806));
#150176=CARTESIAN_POINT('Ctrl Pts',(21.1754122702017,1.05026877283904,124.979447302931));
#150177=CARTESIAN_POINT('Ctrl Pts',(21.1679977774807,0.894759703731321,
124.955656860743));
#150178=CARTESIAN_POINT('Ctrl Pts',(21.1605904311269,0.739400520119218,
124.931889348678));
#150179=CARTESIAN_POINT('Ctrl Pts',(21.1531830847731,0.582935069993669,
124.914292063222));
#150180=CARTESIAN_POINT('Ctrl Pts',(21.1457757384193,0.425894111184199,
124.902958685096));
#150181=CARTESIAN_POINT('Ctrl Pts',(21.1383739167439,0.268970279446402,
124.891633759832));
#150182=CARTESIAN_POINT('Ctrl Pts',(21.1309720950685,0.111472164418757,
124.886563466352));
#150183=CARTESIAN_POINT('Ctrl Pts',(21.1235702733931,-0.0460622752016699,
124.887789919154));
#150184=CARTESIAN_POINT('Ctrl Pts',(21.1161723590817,-0.203513553617891,
124.889015724522));
#150185=CARTESIAN_POINT('Ctrl Pts',(21.1087744447703,-0.36100074609635,
124.896531653359));
#150186=CARTESIAN_POINT('Ctrl Pts',(21.101376530459,-0.51798390991503,124.910327768016));
#150187=CARTESIAN_POINT('Ctrl Pts',(21.0939798455468,-0.6749409859794,124.92412159001));
#150188=CARTESIAN_POINT('Ctrl Pts',(21.0865831606345,-0.831393828123101,
124.944193493831));
#150189=CARTESIAN_POINT('Ctrl Pts',(21.0791864757223,-0.986805517538934,
124.970481510741));
#150190=CARTESIAN_POINT('Ctrl Pts',(21.0717901187869,-1.1422103158376,124.996768362011));
#150191=CARTESIAN_POINT('Ctrl Pts',(21.0643937618515,-1.2965736851325,125.029270716067));
#150192=CARTESIAN_POINT('Ctrl Pts',(21.0569974049161,-1.4493670977951,125.067875144881));
#150193=CARTESIAN_POINT('Ctrl Pts',(21.0495999155795,-1.60218390351925,
125.106485484131));
#150194=CARTESIAN_POINT('Ctrl Pts',(21.0422024262429,-1.75342991206571,
125.151199666894));
#150195=CARTESIAN_POINT('Ctrl Pts',(21.0348049369063,-1.90259014451064,
125.201853919265));
#150196=CARTESIAN_POINT('Ctrl Pts',(21.0274048543914,-2.05180266484361,
125.252525928405));
#150197=CARTESIAN_POINT('Ctrl Pts',(21.0200047718764,-2.19892760007851,
125.309142032998));
#150198=CARTESIAN_POINT('Ctrl Pts',(21.0126046893614,-2.34346853359358,
125.371489756359));
#150199=CARTESIAN_POINT('Ctrl Pts',(21.005196469695,-2.48816840472444,125.433906037451));
#150200=CARTESIAN_POINT('Ctrl Pts',(20.9977882500285,-2.63027825674252,
125.50206637588));
#150201=CARTESIAN_POINT('Ctrl Pts',(20.990380030362,-2.76932427462137,125.57571130589));
#150202=CARTESIAN_POINT('Ctrl Pts',(20.98296725106,-2.90845587300412,125.649401563125));
#150203=CARTESIAN_POINT('Ctrl Pts',(20.9755544717579,-3.04451955778293,
125.72858295107));
#150204=CARTESIAN_POINT('Ctrl Pts',(20.9681416924559,-3.17706968998805,
125.812952124219));
#150205=CARTESIAN_POINT('Ctrl Pts',(20.9607183214271,-3.30980921603823,
125.897441847999));
#150206=CARTESIAN_POINT('Ctrl Pts',(20.9532949503983,-3.43902485694339,
125.987133949212));
#150207=CARTESIAN_POINT('Ctrl Pts',(20.9458715793696,-3.56430263969862,
126.081683701331));
#150208=CARTESIAN_POINT('Ctrl Pts',(20.9419355299287,-3.63072792611547,
126.131816248596));
#150209=CARTESIAN_POINT('Ctrl Pts',(20.9379994804879,-3.69604672483393,
126.183313810674));
#150210=CARTESIAN_POINT('Ctrl Pts',(20.9340634310471,-3.76020154778401,
126.236120816226));
#150211=CARTESIAN_POINT('Ctrl Pts',(20.9267412047266,-3.87954865971624,
126.334357602062));
#150212=CARTESIAN_POINT('Ctrl Pts',(20.9194189784062,-3.99524768171368,
126.437442896164));
#150213=CARTESIAN_POINT('Ctrl Pts',(20.9120967520858,-4.10687126251552,
126.545072062464));
#150214=CARTESIAN_POINT('Ctrl Pts',(20.9047832287334,-4.21836217103901,
126.65257330412));
#150215=CARTESIAN_POINT('Ctrl Pts',(20.8974697053809,-4.32578700190047,
126.764607409021));
#150216=CARTESIAN_POINT('Ctrl Pts',(20.8901561820285,-4.42874974390157,
126.880828246298));
#150217=CARTESIAN_POINT('Ctrl Pts',(20.8828496514327,-4.5316140390448,126.996937960113));
#150218=CARTESIAN_POINT('Ctrl Pts',(20.8755431208368,-4.63002448194077,
127.117226154788));
#150219=CARTESIAN_POINT('Ctrl Pts',(20.868236590241,-4.723620555289,127.24130863757));
#150220=CARTESIAN_POINT('Ctrl Pts',(20.8607423653231,-4.81962097791119,
127.368578621887));
#150221=CARTESIAN_POINT('Ctrl Pts',(20.8532481404052,-4.91055603775388,
127.499840194328));
#150222=CARTESIAN_POINT('Ctrl Pts',(20.8457539154873,-4.99607891110555,
127.634640428574));
#150223=CARTESIAN_POINT('Ctrl Pts',(20.8384559082725,-5.07936258000908,
127.765911252823));
#150224=CARTESIAN_POINT('Ctrl Pts',(20.8311579010577,-5.15751371329181,
127.900537404431));
#150225=CARTESIAN_POINT('Ctrl Pts',(20.823859893843,-5.23025478183218,128.038069692948));
#150226=CARTESIAN_POINT('Ctrl Pts',(20.816563307892,-5.3029816842792,128.175575197487));
#150227=CARTESIAN_POINT('Ctrl Pts',(20.809266721941,-5.37030043851679,128.315985373361));
#150228=CARTESIAN_POINT('Ctrl Pts',(20.8019701359901,-5.43197903761385,
128.458825647154));
#150229=CARTESIAN_POINT('Ctrl Pts',(20.7946734383954,-5.49365858044433,
128.601668106521));
#150230=CARTESIAN_POINT('Ctrl Pts',(20.7873767408008,-5.54969764470332,
128.746940384638));
#150231=CARTESIAN_POINT('Ctrl Pts',(20.7800800432061,-5.59991214306054,
128.894147395828));
#150232=CARTESIAN_POINT('Ctrl Pts',(20.7724379722899,-5.65250343555768,
129.048322130943));
#150233=CARTESIAN_POINT('Ctrl Pts',(20.7647959013736,-5.69870515924171,
129.204618785034));
#150234=CARTESIAN_POINT('Ctrl Pts',(20.7571538304574,-5.73836449839119,
129.362450965021));
#150235=CARTESIAN_POINT('Ctrl Pts',(20.7498489476912,-5.77627396380313,
129.513319176554));
#150236=CARTESIAN_POINT('Ctrl Pts',(20.742544064925,-5.80820598129173,129.665589919651));
#150237=CARTESIAN_POINT('Ctrl Pts',(20.7352391821588,-5.83407966707298,
129.818741522405));
#150238=CARTESIAN_POINT('Ctrl Pts',(20.7279303509646,-5.85996733807322,
129.971975906512));
#150239=CARTESIAN_POINT('Ctrl Pts',(20.7206215197703,-5.87979010731257,
130.126091718317));
#150240=CARTESIAN_POINT('Ctrl Pts',(20.7133126885761,-5.89351903032862,
130.280562945125));
#150241=CARTESIAN_POINT('Ctrl Pts',(20.7059954531342,-5.9072637399002,130.435211794649));
#150242=CARTESIAN_POINT('Ctrl Pts',(20.6986782176923,-5.91490060277359,
130.590216492637));
#150243=CARTESIAN_POINT('Ctrl Pts',(20.6913609822504,-5.91645273702643,
130.74505148646));
#150244=CARTESIAN_POINT('Ctrl Pts',(20.6903657189042,-5.91666385259631,
130.766111570599));
#150245=CARTESIAN_POINT('Ctrl Pts',(20.6893704555579,-5.9167624764504,130.787168523725));
#150246=CARTESIAN_POINT('Ctrl Pts',(20.6883751922117,-5.91674874062564,
130.808221032684));
#150247=CARTESIAN_POINT('',(18.9383751922117,-5.92064976466596,130.799473661469));
#150248=CARTESIAN_POINT('Ctrl Pts',(20.6883751922117,-5.92329750720146,
130.808225305463));
#150249=CARTESIAN_POINT('Ctrl Pts',(20.6774553972192,-5.92504451074842,
131.039465369392));
#150250=CARTESIAN_POINT('Ctrl Pts',(20.6665356022267,-5.91268190666388,
131.270516923428));
#150251=CARTESIAN_POINT('Ctrl Pts',(20.5627999326298,-5.65527249371549,
133.448917103978));
#150252=CARTESIAN_POINT('Ctrl Pts',(20.3771681834213,-3.06572938391748,
137.09553410706));
#150253=CARTESIAN_POINT('Ctrl Pts',(20.0987205596083,3.63584081539465,136.784178515751));
#150254=CARTESIAN_POINT('Ctrl Pts',(19.8202729357954,6.99625092605647,130.977662406353));
#150255=CARTESIAN_POINT('Ctrl Pts',(19.5418253119827,3.92744822153119,125.011890419323));
#150256=CARTESIAN_POINT('Ctrl Pts',(19.2633776881697,-2.75048753206931,
124.369115566576));
#150257=CARTESIAN_POINT('Ctrl Pts',(19.062227648246,-5.74870851970597,128.176804517244));
#150258=CARTESIAN_POINT('Ctrl Pts',(18.9538934829267,-5.92357746849997,
130.470471986277));
#150259=CARTESIAN_POINT('Ctrl Pts',(18.9383751922117,-5.92064976466596,
130.799473661469));
#150260=CARTESIAN_POINT('',(17.1883751922117,-5.90730668608647,130.802808790882));
#150261=CARTESIAN_POINT('Ctrl Pts',(18.9383751922117,-5.92064976466596,
130.799473661469));
#150262=CARTESIAN_POINT('Ctrl Pts',(18.8610776083224,-5.90606668738842,
132.438251736634));
#150263=CARTESIAN_POINT('Ctrl Pts',(18.6909641498289,-4.34635737984644,
136.069165665711));
#150264=CARTESIAN_POINT('Ctrl Pts',(18.428034816731,1.80946671150537,137.564788913929));
#150265=CARTESIAN_POINT('Ctrl Pts',(18.1495871929181,6.665800747261,132.936181653243));
#150266=CARTESIAN_POINT('Ctrl Pts',(17.8711395691052,5.39658953875396,126.348535006014));
#150267=CARTESIAN_POINT('Ctrl Pts',(17.5926919452923,-0.831823817814186,
123.855574416618));
#150268=CARTESIAN_POINT('Ctrl Pts',(17.3651038196611,-5.29781027684818,
127.037204659635));
#150269=CARTESIAN_POINT('Ctrl Pts',(17.2303315686343,-5.90939828044888,
129.908188672729));
#150270=CARTESIAN_POINT('Ctrl Pts',(17.1883751922117,-5.90730668608647,
130.802808790882));
#150271=CARTESIAN_POINT('',(15.4383751922118,-5.91493869631653,130.809783036639));
#150272=CARTESIAN_POINT('Ctrl Pts',(17.1883751922117,-5.90730668608647,
130.802808790882));
#150273=CARTESIAN_POINT('Ctrl Pts',(17.13751569403,-5.90477125646307,131.887266843558));
#150274=CARTESIAN_POINT('Ctrl Pts',(16.993840321244,-5.09858476319956,134.954310666059));
#150275=CARTESIAN_POINT('Ctrl Pts',(16.7573490738536,-0.162654485168709,
137.8008671779));
#150276=CARTESIAN_POINT('Ctrl Pts',(16.4789014500409,5.79844039827919,134.722989137587));
#150277=CARTESIAN_POINT('Ctrl Pts',(16.2004538262279,6.43105182527334,128.044082923024));
#150278=CARTESIAN_POINT('Ctrl Pts',(15.922006202415,1.1538407991874,123.901737062677));
#150279=CARTESIAN_POINT('Ctrl Pts',(15.6679799910763,-4.62785637852258,
125.90954012655));
#150280=CARTESIAN_POINT('Ctrl Pts',(15.5067696543419,-5.90195263961237,
129.356165732764));
#150281=CARTESIAN_POINT('Ctrl Pts',(15.4383751922118,-5.91493869631653,
130.809783036639));
#150282=CARTESIAN_POINT('',(13.6883751922117,-5.92204994786472,130.803560432901));
#150283=CARTESIAN_POINT('Ctrl Pts',(15.4383751922118,-5.91493869631653,
130.809783036639));
#150284=CARTESIAN_POINT('Ctrl Pts',(15.4139537797376,-5.9195755899671,131.328821956632));
#150285=CARTESIAN_POINT('Ctrl Pts',(15.2967164926591,-5.61893840176707,
133.815232264866));
#150286=CARTESIAN_POINT('Ctrl Pts',(15.0866633309763,-2.12167435304641,
137.473397914658));
#150287=CARTESIAN_POINT('Ctrl Pts',(14.8082157071634,4.46403314239369,136.194162899092));
#150288=CARTESIAN_POINT('Ctrl Pts',(14.5297680833506,6.94751226011757,129.961962893285));
#150289=CARTESIAN_POINT('Ctrl Pts',(14.2513204595376,3.04656701563547,124.503885242677));
#150290=CARTESIAN_POINT('Ctrl Pts',(13.9728728357247,-3.65402448314156,
124.835636666255));
#150291=CARTESIAN_POINT('Ctrl Pts',(13.7852244132827,-5.90671534475003,
128.755576012039));
#150292=CARTESIAN_POINT('Ctrl Pts',(13.6903918654451,-5.92648126663072,
130.760913461161));
#150293=CARTESIAN_POINT('Ctrl Pts',(13.6883751922117,-5.92640055191772,
130.803559845049));
#150294=CARTESIAN_POINT('',(11.9383752134708,-5.91415767949116,130.799325238322));
#150295=CARTESIAN_POINT('Ctrl Pts',(13.6883751922117,-5.91674994598809,
130.803561149034));
#150296=CARTESIAN_POINT('Ctrl Pts',(13.6809794773941,-5.91677104378405,
130.959702858383));
#150297=CARTESIAN_POINT('Ctrl Pts',(13.6735837625766,-5.91060705855891,
131.116089056026));
#150298=CARTESIAN_POINT('Ctrl Pts',(13.666188047759,-5.89822592375295,131.272186990132));
#150299=CARTESIAN_POINT('Ctrl Pts',(13.6588010451561,-5.88585937402858,
131.428101039551));
#150300=CARTESIAN_POINT('Ctrl Pts',(13.6514140425531,-5.86729028044803,
131.583727129818));
#150301=CARTESIAN_POINT('Ctrl Pts',(13.6440270399501,-5.84253853942223,
131.738530825754));
#150302=CARTESIAN_POINT('Ctrl Pts',(13.6366470966912,-5.81781045224694,
131.893186584481));
#150303=CARTESIAN_POINT('Ctrl Pts',(13.6292671534324,-5.7869115376568,132.047021144144));
#150304=CARTESIAN_POINT('Ctrl Pts',(13.6218872101735,-5.74991360270379,
132.199503665408));
#150305=CARTESIAN_POINT('Ctrl Pts',(13.6145126792117,-5.71294280126818,
132.351874359156));
#150306=CARTESIAN_POINT('Ctrl Pts',(13.60713814825,-5.66988197294389,132.502894624388));
#150307=CARTESIAN_POINT('Ctrl Pts',(13.5997636172883,-5.62085423726775,
132.652042464067));
#150308=CARTESIAN_POINT('Ctrl Pts',(13.592105866072,-5.56994358214264,132.806918354699));
#150309=CARTESIAN_POINT('Ctrl Pts',(13.5844481148558,-5.51259864495505,
132.959774724882));
#150310=CARTESIAN_POINT('Ctrl Pts',(13.5767903636396,-5.44901484055608,
133.110042258621));
#150311=CARTESIAN_POINT('Ctrl Pts',(13.5694206793814,-5.38782291238791,
133.254657073942));
#150312=CARTESIAN_POINT('Ctrl Pts',(13.5620509951233,-5.32085313439952,
133.39687391235));
#150313=CARTESIAN_POINT('Ctrl Pts',(13.5546813108651,-5.24832926401106,
133.536204408676));
#150314=CARTESIAN_POINT('Ctrl Pts',(13.5473117254542,-5.17580636636187,
133.675533036206));
#150315=CARTESIAN_POINT('Ctrl Pts',(13.5399421400432,-5.09772969793309,
133.811975064591));
#150316=CARTESIAN_POINT('Ctrl Pts',(13.5325725546323,-5.01436932318016,
133.945066088197));
#150317=CARTESIAN_POINT('Ctrl Pts',(13.5252015847893,-4.93099328855467,
134.078182113951));
#150318=CARTESIAN_POINT('Ctrl Pts',(13.5178306149464,-4.84233177149242,
134.207945562806));
#150319=CARTESIAN_POINT('Ctrl Pts',(13.5104596451035,-4.74869845760246,
134.333920578987));
#150320=CARTESIAN_POINT('Ctrl Pts',(13.5030858069555,-4.65502870767952,
134.4599446165));
#150321=CARTESIAN_POINT('Ctrl Pts',(13.4957119688076,-4.55638353394629,
134.5821769849));
#150322=CARTESIAN_POINT('Ctrl Pts',(13.4883381306597,-4.45311709156444,
134.700214661459));
#150323=CARTESIAN_POINT('Ctrl Pts',(13.480956116768,-4.34973615250395,134.818383212304));
#150324=CARTESIAN_POINT('Ctrl Pts',(13.4735741028763,-4.24172396280241,
134.93234750252));
#150325=CARTESIAN_POINT('Ctrl Pts',(13.4661920889845,-4.12947218201619,
135.041740711498));
#150326=CARTESIAN_POINT('Ctrl Pts',(13.4588052247392,-4.01714664617641,
135.151205797306));
#150327=CARTESIAN_POINT('Ctrl Pts',(13.4514183604939,-3.90057624880907,
135.256093567857));
#150328=CARTESIAN_POINT('Ctrl Pts',(13.4440314962486,-3.78018545722401,
135.356077708016));
#150329=CARTESIAN_POINT('Ctrl Pts',(13.4366345987805,-3.6596311446114,135.456197651828));
#150330=CARTESIAN_POINT('Ctrl Pts',(13.4292377013124,-3.53524637667355,
135.551400441991));
#150331=CARTESIAN_POINT('Ctrl Pts',(13.4218408038443,-3.4074847590033,135.641402914224));
#150332=CARTESIAN_POINT('Ctrl Pts',(13.4198863985959,-3.37372763620945,
135.665183330928));
#150333=CARTESIAN_POINT('Ctrl Pts',(13.4179319933474,-3.33973490196413,
135.688600951994));
#150334=CARTESIAN_POINT('Ctrl Pts',(13.415977588099,-3.3055151971596,135.71165109642));
#150335=CARTESIAN_POINT('Ctrl Pts',(13.4085543216936,-3.17554113713192,
135.799200678518));
#150336=CARTESIAN_POINT('Ctrl Pts',(13.4011310552881,-3.04188989318962,
135.881715356937));
#150337=CARTESIAN_POINT('Ctrl Pts',(13.3937077888826,-2.90498906015586,
135.958870208485));
#150338=CARTESIAN_POINT('Ctrl Pts',(13.3862932961616,-2.76825003253783,
136.035933869406));
#150339=CARTESIAN_POINT('Ctrl Pts',(13.3788788034407,-2.62826938288247,
136.107650131558));
#150340=CARTESIAN_POINT('Ctrl Pts',(13.3714643107197,-2.4855049939392,136.173736325002));
#150341=CARTESIAN_POINT('Ctrl Pts',(13.3640569643659,-2.34287820668858,
136.239758822085));
#150342=CARTESIAN_POINT('Ctrl Pts',(13.3566496180121,-2.19747335810855,
136.300161897735));
#150343=CARTESIAN_POINT('Ctrl Pts',(13.3492422716583,-2.04977423751675,
136.354708006488));
#150344=CARTESIAN_POINT('Ctrl Pts',(13.3418404499829,-1.90218527650209,
136.409213432695));
#150345=CARTESIAN_POINT('Ctrl Pts',(13.3344386283075,-1.75230579928924,
136.457870461206));
#150346=CARTESIAN_POINT('Ctrl Pts',(13.3270368066322,-1.60064084829797,
136.500489077956));
#150347=CARTESIAN_POINT('Ctrl Pts',(13.3196388923208,-1.44905596005355,
136.54308519667));
#150348=CARTESIAN_POINT('Ctrl Pts',(13.3122409780095,-1.2956878336085,136.57964915121));
#150349=CARTESIAN_POINT('Ctrl Pts',(13.3048430636982,-1.14105788839725,
136.610040376029));
#150350=CARTESIAN_POINT('Ctrl Pts',(13.297446378786,-0.98645363987762,136.640426550378));
#150351=CARTESIAN_POINT('Ctrl Pts',(13.2900496938737,-0.830588354698773,
136.664641958985));
#150352=CARTESIAN_POINT('Ctrl Pts',(13.2826530089615,-0.673995012943288,
136.682596856867));
#150353=CARTESIAN_POINT('Ctrl Pts',(13.275256652026,-0.517408614700673,
136.70055095861));
#150354=CARTESIAN_POINT('Ctrl Pts',(13.2678602950906,-0.360094594938191,
136.712245059062));
#150355=CARTESIAN_POINT('Ctrl Pts',(13.2604639381552,-0.202592179745797,
136.717641176715));
#150356=CARTESIAN_POINT('Ctrl Pts',(13.2530664488187,-0.045065650532001,
136.723038120526));
#150357=CARTESIAN_POINT('Ctrl Pts',(13.245668959482,0.112648958440613,136.722135148831));
#150358=CARTESIAN_POINT('Ctrl Pts',(13.2382714701455,0.270011438818095,
136.714946407943));
#150359=CARTESIAN_POINT('Ctrl Pts',(13.2308713876305,0.427429082370029,
136.707755147053));
#150360=CARTESIAN_POINT('Ctrl Pts',(13.2234713051155,0.584493978886043,
136.69427374691));
#150361=CARTESIAN_POINT('Ctrl Pts',(13.2160712226005,0.740670210498876,
136.674568297178));
#150362=CARTESIAN_POINT('Ctrl Pts',(13.2086630029341,0.897018173933227,
136.654841179279));
#150363=CARTESIAN_POINT('Ctrl Pts',(13.2012547832676,1.05247515038622,136.628876390669));
#150364=CARTESIAN_POINT('Ctrl Pts',(13.1938465636011,1.20651386896422,136.596791441192));
#150365=CARTESIAN_POINT('Ctrl Pts',(13.186433784299,1.36064739580324,136.564686743965));
#150366=CARTESIAN_POINT('Ctrl Pts',(13.179021004997,1.51336056409415,136.526454470385));
#150367=CARTESIAN_POINT('Ctrl Pts',(13.1716082256949,1.66414096905166,136.482262113508));
#150368=CARTESIAN_POINT('Ctrl Pts',(13.1641848546662,1.81513681612266,136.43800661252));
#150369=CARTESIAN_POINT('Ctrl Pts',(13.1567614836374,1.96419403146673,136.387774138677));
#150370=CARTESIAN_POINT('Ctrl Pts',(13.1493381126087,2.11081912341345,136.331780738267));
#150371=CARTESIAN_POINT('Ctrl Pts',(13.1454020631678,2.18856326538575,136.302091693826));
#150372=CARTESIAN_POINT('Ctrl Pts',(13.141466013727,2.26562403328145,136.270783828722));
#150373=CARTESIAN_POINT('Ctrl Pts',(13.1375299642861,2.34193075578605,136.237894541046));
#150374=CARTESIAN_POINT('Ctrl Pts',(13.1301066978807,2.48584285297614,136.175866370929));
#150375=CARTESIAN_POINT('Ctrl Pts',(13.1226834314752,2.62750655083135,136.108022993419));
#150376=CARTESIAN_POINT('Ctrl Pts',(13.1152601650698,2.76641735682101,136.034548527228));
#150377=CARTESIAN_POINT('Ctrl Pts',(13.1078456723488,2.90516398177401,135.961160901755));
#150378=CARTESIAN_POINT('Ctrl Pts',(13.1004311796278,3.04116386458929,135.882155608202));
#150379=CARTESIAN_POINT('Ctrl Pts',(13.0930166869068,3.17393169023008,135.797765086288));
#150380=CARTESIAN_POINT('Ctrl Pts',(13.085609340553,3.3065715492417,135.713455903136));
#150381=CARTESIAN_POINT('Ctrl Pts',(13.0782019941992,3.43598523985819,135.623772023763));
#150382=CARTESIAN_POINT('Ctrl Pts',(13.0707946478455,3.56171140840925,135.528992074697));
#150383=CARTESIAN_POINT('Ctrl Pts',(13.0633928261701,3.68734380564007,135.434282816092));
#150384=CARTESIAN_POINT('Ctrl Pts',(13.0559910044947,3.80929386020798,135.33448527953));
#150385=CARTESIAN_POINT('Ctrl Pts',(13.0485891828193,3.92712872013466,135.229921664258));
#150386=CARTESIAN_POINT('Ctrl Pts',(13.0411912685079,4.04490137595686,135.125413247303));
#150387=CARTESIAN_POINT('Ctrl Pts',(13.0337933541966,4.15856288502563,135.016144009467));
#150388=CARTESIAN_POINT('Ctrl Pts',(13.0263954398852,4.26771314562347,134.902476656574));
#150389=CARTESIAN_POINT('Ctrl Pts',(13.018998754973,4.37684526742787,134.788828193133));
#150390=CARTESIAN_POINT('Ctrl Pts',(13.0116020700607,4.48146737036548,134.670783334224));
#150391=CARTESIAN_POINT('Ctrl Pts',(13.0042053851485,4.58121586068676,134.548741981729));
#150392=CARTESIAN_POINT('Ctrl Pts',(12.9968090282131,4.68095992805517,134.426706040676));
#150393=CARTESIAN_POINT('Ctrl Pts',(12.9894126712777,4.77583057625002,134.300674247424));
#150394=CARTESIAN_POINT('Ctrl Pts',(12.9820163143422,4.86550438547872,134.171079738222));
#150395=CARTESIAN_POINT('Ctrl Pts',(12.9746188250056,4.95519192399667,134.041465387768));
#150396=CARTESIAN_POINT('Ctrl Pts',(12.9672213356691,5.03968082687911,133.908287542272));
#150397=CARTESIAN_POINT('Ctrl Pts',(12.9598238463325,5.11869100001087,133.772008340748));
#150398=CARTESIAN_POINT('Ctrl Pts',(12.9524237638176,5.19772887003601,133.635681366762));
#150399=CARTESIAN_POINT('Ctrl Pts',(12.9450236813026,5.27128399937201,133.496251194936));
#150400=CARTESIAN_POINT('Ctrl Pts',(12.9376235987876,5.33912231442844,133.354204431228));
#150401=CARTESIAN_POINT('Ctrl Pts',(12.9302153791212,5.40703522468662,133.2120014725));
#150402=CARTESIAN_POINT('Ctrl Pts',(12.9228071594547,5.46921860568836,133.067176512971));
#150403=CARTESIAN_POINT('Ctrl Pts',(12.9153989397882,5.52548631899722,132.920236677517));
#150404=CARTESIAN_POINT('Ctrl Pts',(12.9079861604861,5.5817886641449,132.773206403046));
#150405=CARTESIAN_POINT('Ctrl Pts',(12.900573381184,5.63216796727591,132.624059011756));
#150406=CARTESIAN_POINT('Ctrl Pts',(12.8931606018819,5.6764881777387,132.473316138391));
#150407=CARTESIAN_POINT('Ctrl Pts',(12.8857372308532,5.72087171499654,132.32235787654));
#150408=CARTESIAN_POINT('Ctrl Pts',(12.8783138598244,5.75917877791385,132.169799940643));
#150409=CARTESIAN_POINT('Ctrl Pts',(12.8708904887957,5.7913243880475,132.016174297513));
#150410=CARTESIAN_POINT('Ctrl Pts',(12.8669544393548,5.80836876186376,131.934718295328));
#150411=CARTESIAN_POINT('Ctrl Pts',(12.863018389914,5.82368179562796,131.852962222998));
#150412=CARTESIAN_POINT('Ctrl Pts',(12.8590823404732,5.837256753842,131.770985752883));
#150413=CARTESIAN_POINT('Ctrl Pts',(12.8516590740678,5.86285870137356,131.616380688644));
#150414=CARTESIAN_POINT('Ctrl Pts',(12.8442358076623,5.88235283546909,131.460524004804));
#150415=CARTESIAN_POINT('Ctrl Pts',(12.8368125412569,5.89562136988027,131.303939665877));
#150416=CARTESIAN_POINT('Ctrl Pts',(12.8293980485359,5.90887422198572,131.147540396634));
#150417=CARTESIAN_POINT('Ctrl Pts',(12.8219835558149,5.91591608961713,130.990415552528));
#150418=CARTESIAN_POINT('Ctrl Pts',(12.8145690630939,5.91668020626019,130.833099082188));
#150419=CARTESIAN_POINT('Ctrl Pts',(12.8071617167401,5.91744358641887,130.675934239386));
#150420=CARTESIAN_POINT('Ctrl Pts',(12.7997543703864,5.91194125960596,130.518578508832));
#150421=CARTESIAN_POINT('Ctrl Pts',(12.7923470240326,5.9001582692831,130.361570644881));
#150422=CARTESIAN_POINT('Ctrl Pts',(12.7849452023572,5.88838406715895,130.204679883318));
#150423=CARTESIAN_POINT('Ctrl Pts',(12.7775433806818,5.8703385565255,130.048136842402));
#150424=CARTESIAN_POINT('Ctrl Pts',(12.7701415590064,5.84605884566799,129.892479849325));
#150425=CARTESIAN_POINT('Ctrl Pts',(12.762743644695,5.82179195188082,129.736905026364));
#150426=CARTESIAN_POINT('Ctrl Pts',(12.7553457303837,5.79129746941189,129.582215687623));
#150427=CARTESIAN_POINT('Ctrl Pts',(12.7479478160723,5.75466428819294,129.428944501368));
#150428=CARTESIAN_POINT('Ctrl Pts',(12.7405511311601,5.71803719474423,129.275698786004));
#150429=CARTESIAN_POINT('Ctrl Pts',(12.7331544462478,5.67527351391464,129.123871118105));
#150430=CARTESIAN_POINT('Ctrl Pts',(12.7257577613356,5.62651316318096,128.973983556124));
#150431=CARTESIAN_POINT('Ctrl Pts',(12.7183614044002,5.57775497453233,128.824102640316));
#150432=CARTESIAN_POINT('Ctrl Pts',(12.7109650474648,5.52300076015743,128.676162014362));
#150433=CARTESIAN_POINT('Ctrl Pts',(12.7035686905293,5.46244011355051,128.530667901218));
#150434=CARTESIAN_POINT('Ctrl Pts',(12.6961712011927,5.40187019495374,128.385151512553));
#150435=CARTESIAN_POINT('Ctrl Pts',(12.6887737118561,5.33549221750866,128.242082727166));
#150436=CARTESIAN_POINT('Ctrl Pts',(12.6813762225195,5.26354359414734,128.101946993598));
#150437=CARTESIAN_POINT('Ctrl Pts',(12.6739761400045,5.19156974930774,127.961762135665));
#150438=CARTESIAN_POINT('Ctrl Pts',(12.6665760574895,5.11402154097226,127.824512708521));
#150439=CARTESIAN_POINT('Ctrl Pts',(12.6591759749745,5.03118184202175,127.690658667313));
#150440=CARTESIAN_POINT('Ctrl Pts',(12.651767755308,4.94825105230635,127.556657439826));
#150441=CARTESIAN_POINT('Ctrl Pts',(12.6443595356415,4.86001734854309,127.426059372093));
#150442=CARTESIAN_POINT('Ctrl Pts',(12.6369513159751,4.76680677688238,127.299295181034));
#150443=CARTESIAN_POINT('Ctrl Pts',(12.629538536673,4.67353883567012,127.172452968731));
#150444=CARTESIAN_POINT('Ctrl Pts',(12.622125757371,4.57528815522929,127.049449626072));
#150445=CARTESIAN_POINT('Ctrl Pts',(12.6147129780689,4.47242006294447,126.930681572643));
#150446=CARTESIAN_POINT('Ctrl Pts',(12.6072896070402,4.3694049879052,126.811743817851));
#150447=CARTESIAN_POINT('Ctrl Pts',(12.5998662360114,4.26175957897851,126.697053710119));
#150448=CARTESIAN_POINT('Ctrl Pts',(12.5924428649826,4.14988546198636,126.586970285276));
#150449=CARTESIAN_POINT('Ctrl Pts',(12.5885068155419,4.0905671207747,126.528601412009));
#150450=CARTESIAN_POINT('Ctrl Pts',(12.5845707661011,4.03006049046271,126.471526968918));
#150451=CARTESIAN_POINT('Ctrl Pts',(12.5806347166603,3.96842896096237,126.415795687626));
#150452=CARTESIAN_POINT('Ctrl Pts',(12.5732114502549,3.85219381977877,126.310688230424));
#150453=CARTESIAN_POINT('Ctrl Pts',(12.5657881838495,3.73160423322244,126.21004291868));
#150454=CARTESIAN_POINT('Ctrl Pts',(12.5583649174441,3.60703736113541,126.11424206492));
#150455=CARTESIAN_POINT('Ctrl Pts',(12.5509504247231,3.48261771674637,126.018554439814));
#150456=CARTESIAN_POINT('Ctrl Pts',(12.543535932002,3.35423043685518,125.927700100912));
#150457=CARTESIAN_POINT('Ctrl Pts',(12.536121439281,3.22228865863494,125.842023833053));
#150458=CARTESIAN_POINT('Ctrl Pts',(12.5287140929273,3.09047405086807,125.756430143206));
#150459=CARTESIAN_POINT('Ctrl Pts',(12.5213067465734,2.95511207616322,125.676004790596));
#150460=CARTESIAN_POINT('Ctrl Pts',(12.5138994002197,2.81664791944207,125.60105156847));
#150461=CARTESIAN_POINT('Ctrl Pts',(12.5064975785442,2.67828703451217,125.526154249285));
#150462=CARTESIAN_POINT('Ctrl Pts',(12.4990957568688,2.53682890137621,125.456721111065));
#150463=CARTESIAN_POINT('Ctrl Pts',(12.4916939351934,2.39274648788165,125.393011912554));
#150464=CARTESIAN_POINT('Ctrl Pts',(12.484296020882,2.24874013437307,125.329336345635));
#150465=CARTESIAN_POINT('Ctrl Pts',(12.4768981065708,2.10211260001836,125.271378851299));
#150466=CARTESIAN_POINT('Ctrl Pts',(12.4695001922595,1.95336008089372,125.219352564137));
#150467=CARTESIAN_POINT('Ctrl Pts',(12.4621035073473,1.80463228173848,125.167334922799));
#150468=CARTESIAN_POINT('Ctrl Pts',(12.4547068224351,1.65378055070234,125.121246655515));
#150469=CARTESIAN_POINT('Ctrl Pts',(12.4473101375229,1.50131973916258,125.081252231094));
#150470=CARTESIAN_POINT('Ctrl Pts',(12.4399137805874,1.34886568789498,125.041259580069));
#150471=CARTESIAN_POINT('Ctrl Pts',(12.432517423652,1.1948030590687,125.007360329364));
#150472=CARTESIAN_POINT('Ctrl Pts',(12.4251210667166,1.0396602323058,124.979668594475));
#150473=CARTESIAN_POINT('Ctrl Pts',(12.41772357738,0.884493652779841,124.951972619911));
#150474=CARTESIAN_POINT('Ctrl Pts',(12.4103260880433,0.728246913534963,
124.930486119106));
#150475=CARTESIAN_POINT('Ctrl Pts',(12.4029285987067,0.571456763664193,
124.915271746632));
#150476=CARTESIAN_POINT('Ctrl Pts',(12.3955285161917,0.414611651249442,
124.900052040782));
#150477=CARTESIAN_POINT('Ctrl Pts',(12.3881284336768,0.257223120262054,
124.891108876859));
#150478=CARTESIAN_POINT('Ctrl Pts',(12.3807283511618,0.0998310436957964,
124.888452882889));
#150479=CARTESIAN_POINT('Ctrl Pts',(12.3733201314954,-0.057734101638944,
124.88579396838));
#150480=CARTESIAN_POINT('Ctrl Pts',(12.3659119118288,-0.215302426864783,
124.889436036619));
#150481=CARTESIAN_POINT('Ctrl Pts',(12.3585036921623,-0.37233532172839,
124.899337588763));
#150482=CARTESIAN_POINT('Ctrl Pts',(12.3510909128603,-0.529464867718775,
124.909245235147));
#150483=CARTESIAN_POINT('Ctrl Pts',(12.3436781335582,-0.686057956218949,
124.925420003975));
#150484=CARTESIAN_POINT('Ctrl Pts',(12.3362653542561,-0.84158359982742,
124.947768809441));
#150485=CARTESIAN_POINT('Ctrl Pts',(12.3288419832274,-0.997331465768686,
124.970149547928));
#150486=CARTESIAN_POINT('Ctrl Pts',(12.3214186121986,-1.15200847450612,
124.998721874444));
#150487=CARTESIAN_POINT('Ctrl Pts',(12.3139952411698,-1.30509547046255,
125.033341957444));
#150488=CARTESIAN_POINT('Ctrl Pts',(12.310059191729,-1.38626586899091,125.051698356148));
#150489=CARTESIAN_POINT('Ctrl Pts',(12.3061231422882,-1.46698952603585,
125.071754167255));
#150490=CARTESIAN_POINT('Ctrl Pts',(12.3021870928474,-1.54719117850762,
125.093482399669));
#150491=CARTESIAN_POINT('Ctrl Pts',(12.294763826442,-1.69844899206153,125.134461167887));
#150492=CARTESIAN_POINT('Ctrl Pts',(12.2873405600365,-1.8483063603538,125.181515352935));
#150493=CARTESIAN_POINT('Ctrl Pts',(12.2799172936311,-1.99623776892161,
125.234534288817));
#150494=CARTESIAN_POINT('Ctrl Pts',(12.2725028009101,-2.14399433484879,
125.287490560718));
#150495=CARTESIAN_POINT('Ctrl Pts',(12.2650883081892,-2.28982912410956,
125.34639742599));
#150496=CARTESIAN_POINT('Ctrl Pts',(12.2576738154682,-2.43322874872264,
125.411093665255));
#150497=CARTESIAN_POINT('Ctrl Pts',(12.2502664691144,-2.57649015937863,
125.475727547848));
#150498=CARTESIAN_POINT('Ctrl Pts',(12.2428591227606,-2.7173207400215,125.546139543234));
#150499=CARTESIAN_POINT('Ctrl Pts',(12.2354517764069,-2.85522426746406,
125.622119312398));
#150500=CARTESIAN_POINT('Ctrl Pts',(12.2280499547315,-2.99302494125285,
125.698042412985));
#150501=CARTESIAN_POINT('Ctrl Pts',(12.2206481330561,-3.1279025831521,125.779524839487));
#150502=CARTESIAN_POINT('Ctrl Pts',(12.2132463113807,-3.25938300009817,
125.866309076607));
#150503=CARTESIAN_POINT('Ctrl Pts',(12.2058483970694,-3.39079400955632,
125.953047501004));
#150504=CARTESIAN_POINT('Ctrl Pts',(12.198450482758,-3.51881105487927,126.045081956985));
#150505=CARTESIAN_POINT('Ctrl Pts',(12.1910525684467,-3.6429866137998,126.142110185192));
#150506=CARTESIAN_POINT('Ctrl Pts',(12.1836558835344,-3.7671415369954,126.239122289067));
#150507=CARTESIAN_POINT('Ctrl Pts',(12.1762591986222,-3.8874559469332,126.341126288495));
#150508=CARTESIAN_POINT('Ctrl Pts',(12.1688625137099,-4.00351318159925,
126.447777923841));
#150509=CARTESIAN_POINT('Ctrl Pts',(12.1614661567745,-4.11956527016589,
126.554424830142));
#150510=CARTESIAN_POINT('Ctrl Pts',(12.154069799839,-4.23136028393053,126.665718710013));
#150511=CARTESIAN_POINT('Ctrl Pts',(12.1466734429035,-4.33851661220324,
126.781276704927));
#150512=CARTESIAN_POINT('Ctrl Pts',(12.1392759535669,-4.44568934638351,
126.896852392065));
#150513=CARTESIAN_POINT('Ctrl Pts',(12.1318784642303,-4.54822172714036,
127.016693220408));
#150514=CARTESIAN_POINT('Ctrl Pts',(12.1244809748937,-4.64577091541466,
127.140381474068));
#150515=CARTESIAN_POINT('Ctrl Pts',(12.1170808923787,-4.74335429940568,
127.264113086454));
#150516=CARTESIAN_POINT('Ctrl Pts',(12.1096808098637,-4.8359507819253,127.3916945165));
#150517=CARTESIAN_POINT('Ctrl Pts',(12.1022807273486,-4.92325960677384,
127.522677298474));
#150518=CARTESIAN_POINT('Ctrl Pts',(12.0948725076822,-5.01066443665062,
127.653804109481));
#150519=CARTESIAN_POINT('Ctrl Pts',(12.0874642880157,-5.09276979009712,
127.788339430907));
#150520=CARTESIAN_POINT('Ctrl Pts',(12.0800560683492,-5.16931944926736,
127.925807683551));
#150521=CARTESIAN_POINT('Ctrl Pts',(12.0726432890471,-5.2459162234752,128.063360545611));
#150522=CARTESIAN_POINT('Ctrl Pts',(12.0652305097451,-5.31695032170018,
128.203849603554));
#150523=CARTESIAN_POINT('Ctrl Pts',(12.057817730443,-5.38221304800567,128.346777807491));
#150524=CARTESIAN_POINT('Ctrl Pts',(12.0503943594142,-5.44756902475539,
128.489910233949));
#150525=CARTESIAN_POINT('Ctrl Pts',(12.0429709883855,-5.50713701866604,
128.63548842248));
#150526=CARTESIAN_POINT('Ctrl Pts',(12.0355476173567,-5.5607574230185,128.782997848332));
#150527=CARTESIAN_POINT('Ctrl Pts',(12.0316115679159,-5.58918824800988,
128.861210885358));
#150528=CARTESIAN_POINT('Ctrl Pts',(12.0276755184751,-5.61594783453282,
128.939966640036));
#150529=CARTESIAN_POINT('Ctrl Pts',(12.0237394690344,-5.64101820942251,
129.01918720205));
#150530=CARTESIAN_POINT('Ctrl Pts',(12.0147583710996,-5.69822264639261,
129.199949064065));
#150531=CARTESIAN_POINT('Ctrl Pts',(12.0057772731648,-5.74676996117718,
129.38357397859));
#150532=CARTESIAN_POINT('Ctrl Pts',(11.99679617523,-5.78641323558252,129.569309027722));
#150533=CARTESIAN_POINT('Ctrl Pts',(11.9878683594006,-5.8258213185738,129.753942167653));
#150534=CARTESIAN_POINT('Ctrl Pts',(11.9789405435712,-5.85643063877623,
129.940660477226));
#150535=CARTESIAN_POINT('Ctrl Pts',(11.9700127277418,-5.87804537080221,
130.128703025815));
#150536=CARTESIAN_POINT('Ctrl Pts',(11.9611813895651,-5.8994265251368,130.314713509222));
#150537=CARTESIAN_POINT('Ctrl Pts',(11.9523500513883,-5.9120063782527,130.502019741965));
#150538=CARTESIAN_POINT('Ctrl Pts',(11.9435187132116,-5.91564207791684,
130.689864467064));
#150539=CARTESIAN_POINT('Ctrl Pts',(11.9418042244861,-5.91634790142387,
130.726332061996));
#150540=CARTESIAN_POINT('Ctrl Pts',(11.9400897357606,-5.91671677188543,
130.762819889619));
#150541=CARTESIAN_POINT('Ctrl Pts',(11.9383752470351,-5.9167478548645,130.799322318615));
#150542=CARTESIAN_POINT('',(10.1883751630607,-5.91241648564898,130.807217379792));
#150543=CARTESIAN_POINT('Ctrl Pts',(11.9383751922117,-5.91251709691396,
130.799327087625));
#150544=CARTESIAN_POINT('Ctrl Pts',(11.8740140765483,-5.90151912380169,
132.168641977221));
#150545=CARTESIAN_POINT('Ctrl Pts',(11.7168370862809,-4.74574414496558,
135.529409927722));
#150546=CARTESIAN_POINT('Ctrl Pts',(11.4668442214086,0.852969679778676,
137.750582846644));
#150547=CARTESIAN_POINT('Ctrl Pts',(11.188396597596,6.3051044354217,133.841335854337));
#150548=CARTESIAN_POINT('Ctrl Pts',(10.9099489737828,5.96315623638791,127.141256983926));
#150549=CARTESIAN_POINT('Ctrl Pts',(10.6315013499702,0.14135877248956,123.807391400271));
#150550=CARTESIAN_POINT('Ctrl Pts',(10.390976756113,-4.99975189704023,126.481739594297));
#150551=CARTESIAN_POINT('Ctrl Pts',(10.2432680368602,-5.90318810762329,
129.637230627951));
#150552=CARTESIAN_POINT('Ctrl Pts',(10.1883751922117,-5.90826796113811,
130.807214753531));
#150553=CARTESIAN_POINT('',(8.43837519221174,-5.91996550474033,130.808373808165));
#150554=CARTESIAN_POINT('Ctrl Pts',(10.1883751326147,-5.91674930901506,
130.807220122726));
#150555=CARTESIAN_POINT('Ctrl Pts',(10.1802557825323,-5.91666555315848,
130.980523676609));
#150556=CARTESIAN_POINT('Ctrl Pts',(10.17213643245,-5.90896352231583,131.153570801375));
#150557=CARTESIAN_POINT('Ctrl Pts',(10.1640170823676,-5.89373526771853,
131.325719569298));
#150558=CARTESIAN_POINT('Ctrl Pts',(10.1558579373264,-5.87843237564924,
131.498712081246));
#150559=CARTESIAN_POINT('Ctrl Pts',(10.1476987922851,-5.8555293843832,131.670797173441));
#150560=CARTESIAN_POINT('Ctrl Pts',(10.1395396472439,-5.82517011905515,
131.841338749721));
#150561=CARTESIAN_POINT('Ctrl Pts',(10.1313603771817,-5.79473597077675,
132.012300977036));
#150562=CARTESIAN_POINT('Ctrl Pts',(10.1231811071196,-5.75680883326587,
132.181711843681));
#150563=CARTESIAN_POINT('Ctrl Pts',(10.1150018370573,-5.71158264529618,
132.348949316363));
#150564=CARTESIAN_POINT('Ctrl Pts',(10.1067934972637,-5.66619572010589,
132.516781163406));
#150565=CARTESIAN_POINT('Ctrl Pts',(10.0985851574701,-5.61345788464016,
132.68242392312));
#150566=CARTESIAN_POINT('Ctrl Pts',(10.0903768176765,-5.55361278413328,
132.84527110223));
#150567=CARTESIAN_POINT('Ctrl Pts',(10.0851199125658,-5.51528590895333,
132.949564076162));
#150568=CARTESIAN_POINT('Ctrl Pts',(10.079863007455,-5.47404489903722,133.052710882648));
#150569=CARTESIAN_POINT('Ctrl Pts',(10.0746061023443,-5.42996361159411,
133.154557575113));
#150570=CARTESIAN_POINT('Ctrl Pts',(10.0671828359389,-5.36771650359163,
133.298375109339));
#150571=CARTESIAN_POINT('Ctrl Pts',(10.0597595695335,-5.29965761661069,
133.439935397079));
#150572=CARTESIAN_POINT('Ctrl Pts',(10.052336303128,-5.2259718369024,133.578734226582));
#150573=CARTESIAN_POINT('Ctrl Pts',(10.044921810407,-5.1523731476664,133.717369007395));
#150574=CARTESIAN_POINT('Ctrl Pts',(10.037507317686,-5.07316097693031,133.853248500117));
#150575=CARTESIAN_POINT('Ctrl Pts',(10.030092824965,-4.98856850270957,133.985887744006));
#150576=CARTESIAN_POINT('Ctrl Pts',(10.0226854786113,-4.90405756190033,
134.118399145198));
#150577=CARTESIAN_POINT('Ctrl Pts',(10.0152781322575,-4.81417684077245,
134.247676202358));
#150578=CARTESIAN_POINT('Ctrl Pts',(10.0078707859037,-4.71920566763366,
134.373257986373));
#150579=CARTESIAN_POINT('Ctrl Pts',(10.0004689642283,-4.62430532757886,
134.498746106754));
#150580=CARTESIAN_POINT('Ctrl Pts',(9.9930671425529,-4.52432231935671,134.620544145244));
#150581=CARTESIAN_POINT('Ctrl Pts',(9.9856653208775,-4.41957950056913,134.738219740698));
#150582=CARTESIAN_POINT('Ctrl Pts',(9.97826740656617,-4.31489197470057,
134.855833216121));
#150583=CARTESIAN_POINT('Ctrl Pts',(9.97086949225485,-4.20544988992888,
134.969328304391));
#150584=CARTESIAN_POINT('Ctrl Pts',(9.96347157794352,-4.09161656054591,
135.078305456233));
#150585=CARTESIAN_POINT('Ctrl Pts',(9.95607489303133,-3.97780214819697,
135.187264498049));
#150586=CARTESIAN_POINT('Ctrl Pts',(9.94867820811911,-3.85959820895147,
135.291706835655));
#150587=CARTESIAN_POINT('Ctrl Pts',(9.94128152320692,-3.73740519755676,
135.391269484306));
#150588=CARTESIAN_POINT('Ctrl Pts',(9.93388516627149,-3.61521760432805,
135.490827718244));
#150589=CARTESIAN_POINT('Ctrl Pts',(9.92648880933602,-3.48904158004227,
135.585506457646));
#150590=CARTESIAN_POINT('Ctrl Pts',(9.91909245240058,-3.35931075263528,
135.674982942252));
#150591=CARTESIAN_POINT('Ctrl Pts',(9.91169496306401,-3.22956006310742,
135.764473125936));
#150592=CARTESIAN_POINT('Ctrl Pts',(9.90429747372752,-3.09625379410099,
135.848759256972));
#150593=CARTESIAN_POINT('Ctrl Pts',(9.89689998439096,-2.95985451035286,
135.927561944866));
#150594=CARTESIAN_POINT('Ctrl Pts',(9.88949990187597,-2.82340741204725,
136.006392256919));
#150595=CARTESIAN_POINT('Ctrl Pts',(9.88209981936093,-2.68386546329304,
136.079735112094));
#150596=CARTESIAN_POINT('Ctrl Pts',(9.87469973684594,-2.54171562570514,
136.147357177601));
#150597=CARTESIAN_POINT('Ctrl Pts',(9.86729151717948,-2.39940947975746,
136.215053600521));
#150598=CARTESIAN_POINT('Ctrl Pts',(9.85988329751304,-2.25449005541267,
136.277016510581));
#150599=CARTESIAN_POINT('Ctrl Pts',(9.85247507784658,-2.1074647602321,136.333060541317));
#150600=CARTESIAN_POINT('Ctrl Pts',(9.84506229854452,-1.9603489734356,136.389139066218));
#150601=CARTESIAN_POINT('Ctrl Pts',(9.8376495192424,-1.81112508613271,136.439291334071));
#150602=CARTESIAN_POINT('Ctrl Pts',(9.83023673994035,-1.66031493951092,
136.483382088219));
#150603=CARTESIAN_POINT('Ctrl Pts',(9.8228133689116,-1.50928930827934,136.527535841304));
#150604=CARTESIAN_POINT('Ctrl Pts',(9.8153899978829,-1.35667325221345,136.565610692654));
#150605=CARTESIAN_POINT('Ctrl Pts',(9.80796662685415,-1.20299886683335,
136.597522473487));
#150606=CARTESIAN_POINT('Ctrl Pts',(9.80403057741325,-1.12151702033605,
136.614442865398));
#150607=CARTESIAN_POINT('Ctrl Pts',(9.80009452797233,-1.03973773884549,
136.629631462605));
#150608=CARTESIAN_POINT('Ctrl Pts',(9.79615847853142,-0.957740704880099,
136.643081650867));
#150609=CARTESIAN_POINT('Ctrl Pts',(9.78873521212603,-0.803096857865298,
136.668448286163));
#150610=CARTESIAN_POINT('Ctrl Pts',(9.78131194572057,-0.647210687750097,
136.687705210344));
#150611=CARTESIAN_POINT('Ctrl Pts',(9.77388867931512,-0.490606337693888,
136.700735434682));
#150612=CARTESIAN_POINT('Ctrl Pts',(9.76647418659409,-0.334187080974039,
136.713750258377));
#150613=CARTESIAN_POINT('Ctrl Pts',(9.75905969387298,-0.177051702291723,
136.720553000588));
#150614=CARTESIAN_POINT('Ctrl Pts',(9.75164520115194,-0.0197342512662653,
136.721077707459));
#150615=CARTESIAN_POINT('Ctrl Pts',(9.74423785479816,0.137431571276773,
136.721601908597));
#150616=CARTESIAN_POINT('Ctrl Pts',(9.73683050844441,0.294778746010715,
136.71586011952));
#150617=CARTESIAN_POINT('Ctrl Pts',(9.72942316209063,0.451768496444515,
136.7038382036));
#150618=CARTESIAN_POINT('Ctrl Pts',(9.72202134041521,0.608641157999782,
136.691825254079));
#150619=CARTESIAN_POINT('Ctrl Pts',(9.71461951873975,0.7651565554465,136.673541532482));
#150620=CARTESIAN_POINT('Ctrl Pts',(9.70721769706432,0.920776418688503,
136.649024966294));
#150621=CARTESIAN_POINT('Ctrl Pts',(9.69981978275297,1.0763141314156,136.62452134221));
#150622=CARTESIAN_POINT('Ctrl Pts',(9.69242186844165,1.2309568836169,136.593791484212));
#150623=CARTESIAN_POINT('Ctrl Pts',(9.68502395413029,1.38417214292008,136.55692509276));
#150624=CARTESIAN_POINT('Ctrl Pts',(9.67762726921806,1.53736194062699,136.520064827833));
#150625=CARTESIAN_POINT('Ctrl Pts',(9.67023058430588,1.68912435367026,136.477070140658));
#150626=CARTESIAN_POINT('Ctrl Pts',(9.66283389939366,1.83893753713031,136.428081743034));
#150627=CARTESIAN_POINT('Ctrl Pts',(9.6554375424582,1.98874407771681,136.379095517607));
#150628=CARTESIAN_POINT('Ctrl Pts',(9.64804118552274,2.13660120576398,136.324116226187));
#150629=CARTESIAN_POINT('Ctrl Pts',(9.64064482858728,2.28200298743408,136.263334232436));
#150630=CARTESIAN_POINT('Ctrl Pts',(9.6332473392507,2.42742703048815,136.202542932805));
#150631=CARTESIAN_POINT('Ctrl Pts',(9.62584984991406,2.57039463422069,136.135947305888));
#150632=CARTESIAN_POINT('Ctrl Pts',(9.61845236057746,2.71042071195736,136.063785503111));
#150633=CARTESIAN_POINT('Ctrl Pts',(9.61105227806245,2.85049587561852,135.991598404126));
#150634=CARTESIAN_POINT('Ctrl Pts',(9.60365219554746,2.98762712865781,135.913841415326));
#150635=CARTESIAN_POINT('Ctrl Pts',(9.59625211303245,3.12135494694482,135.830798109238));
#150636=CARTESIAN_POINT('Ctrl Pts',(9.58884389336597,3.2552298127156,135.747663488497));
#150637=CARTESIAN_POINT('Ctrl Pts',(9.58143567369948,3.38569345254174,135.65923113888));
#150638=CARTESIAN_POINT('Ctrl Pts',(9.574027454033,3.51231564618689,135.565827761635));
#150639=CARTESIAN_POINT('Ctrl Pts',(9.56661467473092,3.6390157736796,135.472366896171));
#150640=CARTESIAN_POINT('Ctrl Pts',(9.5592018954289,3.76186945309335,135.373929139353));
#150641=CARTESIAN_POINT('Ctrl Pts',(9.55178911612683,3.88048082126535,135.270880421428));
#150642=CARTESIAN_POINT('Ctrl Pts',(9.54436574509806,3.9992616669225,135.167684462662));
#150643=CARTESIAN_POINT('Ctrl Pts',(9.53694237406926,4.11378782385723,135.059864639566));
#150644=CARTESIAN_POINT('Ctrl Pts',(9.52951900304049,4.22370086786386,134.947823123889));
#150645=CARTESIAN_POINT('Ctrl Pts',(9.52558295359982,4.28197940112157,134.88841602388));
#150646=CARTESIAN_POINT('Ctrl Pts',(9.52164690415912,4.33896169732797,134.827822606048));
#150647=CARTESIAN_POINT('Ctrl Pts',(9.51771085471844,4.39459912138594,134.766106334395));
#150648=CARTESIAN_POINT('Ctrl Pts',(9.510287588313,4.49952956677796,134.649711372152));
#150649=CARTESIAN_POINT('Ctrl Pts',(9.50286432190755,4.59999124515387,134.528968760205));
#150650=CARTESIAN_POINT('Ctrl Pts',(9.49544105550211,4.69560241840369,134.404256239772));
#150651=CARTESIAN_POINT('Ctrl Pts',(9.4880265627811,4.79110058718675,134.279691119183));
#150652=CARTESIAN_POINT('Ctrl Pts',(9.48061207006012,4.88175943729564,134.151165723124));
#150653=CARTESIAN_POINT('Ctrl Pts',(9.47319757733911,4.96723481301753,134.019093712995));
#150654=CARTESIAN_POINT('Ctrl Pts',(9.46579023098533,5.05262780435421,133.887148998842));
#150655=CARTESIAN_POINT('Ctrl Pts',(9.45838288463151,5.13284706595016,133.751664787188));
#150656=CARTESIAN_POINT('Ctrl Pts',(9.45097553827773,5.2075894824056,133.613086724761));
#150657=CARTESIAN_POINT('Ctrl Pts',(9.44357371660233,5.28227615314697,133.474612019081));
#150658=CARTESIAN_POINT('Ctrl Pts',(9.43617189492692,5.35149393576633,133.333048384335));
#150659=CARTESIAN_POINT('Ctrl Pts',(9.42877007325151,5.4149837915957,133.188869183132));
#150660=CARTESIAN_POINT('Ctrl Pts',(9.42137215894014,5.47844013162446,133.044766093006));
#150661=CARTESIAN_POINT('Ctrl Pts',(9.41397424462879,5.53617441670041,132.898050527002));
#150662=CARTESIAN_POINT('Ctrl Pts',(9.40657633031742,5.58797426760525,132.749219004977));
#150663=CARTESIAN_POINT('Ctrl Pts',(9.39917964540521,5.63976551031455,132.60041221605));
#150664=CARTESIAN_POINT('Ctrl Pts',(9.39178296049298,5.68562415357426,132.449490521201));
#150665=CARTESIAN_POINT('Ctrl Pts',(9.38438627558077,5.72538651228013,132.296969021502));
#150666=CARTESIAN_POINT('Ctrl Pts',(9.37698991864532,5.76514710788134,132.144454284767));
#150667=CARTESIAN_POINT('Ctrl Pts',(9.3695935617099,5.79881186223639,131.990340245453));
#150668=CARTESIAN_POINT('Ctrl Pts',(9.36219720477445,5.82626746408627,131.835155456237));
#150669=CARTESIAN_POINT('Ctrl Pts',(9.35479971543785,5.85372726945892,131.679946907832));
#150670=CARTESIAN_POINT('Ctrl Pts',(9.34740222610125,5.87497596444269,131.523667650722));
#150671=CARTESIAN_POINT('Ctrl Pts',(9.34000473676466,5.88995171138167,131.366854528726));
#150672=CARTESIAN_POINT('Ctrl Pts',(9.33260465424964,5.90493270804553,131.209986436134));
#150673=CARTESIAN_POINT('Ctrl Pts',(9.32520457173462,5.9136363430605,131.052584477426));
#150674=CARTESIAN_POINT('Ctrl Pts',(9.31780448921961,5.91605281000753,130.895188541147));
#150675=CARTESIAN_POINT('Ctrl Pts',(9.31039626955313,5.9184719341084,130.737619531854));
#150676=CARTESIAN_POINT('Ctrl Pts',(9.30298804988662,5.91459007791834,130.580056931698));
#150677=CARTESIAN_POINT('Ctrl Pts',(9.29557983022013,5.90444955990576,130.423039287152));
#150678=CARTESIAN_POINT('Ctrl Pts',(9.28816705091806,5.89430280057356,130.265925000866));
#150679=CARTESIAN_POINT('Ctrl Pts',(9.28075427161598,5.87788974245218,130.109356708943));
#150680=CARTESIAN_POINT('Ctrl Pts',(9.2733414923139,5.85530427931114,129.953865256508));
#150681=CARTESIAN_POINT('Ctrl Pts',(9.26591812128514,5.83268654500121,129.798151630594));
#150682=CARTESIAN_POINT('Ctrl Pts',(9.25849475025642,5.80387885949493,129.643518283187));
#150683=CARTESIAN_POINT('Ctrl Pts',(9.25107137922765,5.76902584423608,129.490484150376));
#150684=CARTESIAN_POINT('Ctrl Pts',(9.24713532978698,5.75054593925979,129.409341781158));
#150685=CARTESIAN_POINT('Ctrl Pts',(9.24319928034628,5.73036730371311,129.328648739123));
#150686=CARTESIAN_POINT('Ctrl Pts',(9.23926323090561,5.7085170431985,129.248480246197));
#150687=CARTESIAN_POINT('Ctrl Pts',(9.23183996450018,5.66730813379008,129.097284970507));
#150688=CARTESIAN_POINT('Ctrl Pts',(9.22441669809475,5.62002594582548,128.947499384207));
#150689=CARTESIAN_POINT('Ctrl Pts',(9.21699343168933,5.56678194491824,128.799648832737));
#150690=CARTESIAN_POINT('Ctrl Pts',(9.20957893896833,5.51360087399835,128.65197302834));
#150691=CARTESIAN_POINT('Ctrl Pts',(9.20216444624736,5.45447214121539,128.506228054175));
#150692=CARTESIAN_POINT('Ctrl Pts',(9.19474995352635,5.38955774705014,128.362927052279));
#150693=CARTESIAN_POINT('Ctrl Pts',(9.18734260717259,5.32470591982197,128.219764169283));
#150694=CARTESIAN_POINT('Ctrl Pts',(9.17993526081881,5.25407968580243,128.07904090679));
#150695=CARTESIAN_POINT('Ctrl Pts',(9.17252791446504,5.17789013892738,127.941253167312));
#150696=CARTESIAN_POINT('Ctrl Pts',(9.16512609278965,5.10175741709096,127.803568195129));
#150697=CARTESIAN_POINT('Ctrl Pts',(9.15772427111429,5.02006982413318,127.668814711798));
#150698=CARTESIAN_POINT('Ctrl Pts',(9.1503224494389,4.93308559669535,127.537466517939));
#150699=CARTESIAN_POINT('Ctrl Pts',(9.14292453512756,4.84614728755411,127.40618766177));
#150700=CARTESIAN_POINT('Ctrl Pts',(9.13552662081615,4.75391811799677,127.278310825464));
#150701=CARTESIAN_POINT('Ctrl Pts',(9.12812870650481,4.65670102808541,127.154283070783));
#150702=CARTESIAN_POINT('Ctrl Pts',(9.12073202159262,4.55950009389069,127.030275927265));
#150703=CARTESIAN_POINT('Ctrl Pts',(9.11333533668043,4.45731311453102,126.910116889373));
#150704=CARTESIAN_POINT('Ctrl Pts',(9.10593865176824,4.35048498333183,126.794222094734));
#150705=CARTESIAN_POINT('Ctrl Pts',(9.09854229483281,4.24366158900391,126.678332438991));
#150706=CARTESIAN_POINT('Ctrl Pts',(9.09114593789743,4.13219770502983,126.566706925023));
#150707=CARTESIAN_POINT('Ctrl Pts',(9.08374958096201,4.01647677024077,126.459726580433));
#150708=CARTESIAN_POINT('Ctrl Pts',(9.07635209162545,3.90073811828117,126.352729856879));
#150709=CARTESIAN_POINT('Ctrl Pts',(9.06895460228889,3.78074139188313,126.250379972193));
#150710=CARTESIAN_POINT('Ctrl Pts',(9.06155711295233,3.65690482819401,126.153019129347));
#150711=CARTESIAN_POINT('Ctrl Pts',(9.05415703043734,3.53302485378928,126.055624156807));
#150712=CARTESIAN_POINT('Ctrl Pts',(9.04675694792233,3.40530265539782,125.963221938731));
#150713=CARTESIAN_POINT('Ctrl Pts',(9.03935686540734,3.27418715593197,125.876112548482));
#150714=CARTESIAN_POINT('Ctrl Pts',(9.03194864574089,3.14292748149564,125.788907372503));
#150715=CARTESIAN_POINT('Ctrl Pts',(9.02454042607443,3.00826736548948,125.707006853991));
#150716=CARTESIAN_POINT('Ctrl Pts',(9.01713220640798,2.87068277648156,125.630666486743));
#150717=CARTESIAN_POINT('Ctrl Pts',(9.00971942710593,2.73301350645463,125.554279133273));
#150718=CARTESIAN_POINT('Ctrl Pts',(9.00230664780383,2.59241650938984,125.483458917735));
#150719=CARTESIAN_POINT('Ctrl Pts',(8.99489386850178,2.4493891522018,125.418413779398));
#150720=CARTESIAN_POINT('Ctrl Pts',(8.98747049747303,2.30615743081849,125.353275701517));
#150721=CARTESIAN_POINT('Ctrl Pts',(8.9800471264443,2.16048875851841,125.293929321806));
#150722=CARTESIAN_POINT('Ctrl Pts',(8.97262375541555,2.01289790235313,125.24053346378));
#150723=CARTESIAN_POINT('Ctrl Pts',(8.96868770597461,1.93464168901706,125.212221698638));
#150724=CARTESIAN_POINT('Ctrl Pts',(8.96475165653366,1.85584530199803,125.185581995953));
#150725=CARTESIAN_POINT('Ctrl Pts',(8.96081560709271,1.77658667887363,125.160632210303));
#150726=CARTESIAN_POINT('Ctrl Pts',(8.95339234068728,1.62710738924394,125.113577693225));
#150727=CARTESIAN_POINT('Ctrl Pts',(8.94596907428184,1.47553135581495,125.072394768949));
#150728=CARTESIAN_POINT('Ctrl Pts',(8.93854580787641,1.32236081647028,125.037273620341));
#150729=CARTESIAN_POINT('Ctrl Pts',(8.93113131515539,1.16937131198288,125.002193982013));
#150730=CARTESIAN_POINT('Ctrl Pts',(8.92371682243439,1.0147914131362,124.973161940961));
#150731=CARTESIAN_POINT('Ctrl Pts',(8.91630232971337,0.859140406076983,
124.950318567397));
#150732=CARTESIAN_POINT('Ctrl Pts',(8.9088949833596,0.703639421318752,124.927497211137));
#150733=CARTESIAN_POINT('Ctrl Pts',(8.90148763700586,0.547069750464317,
124.910852701322));
#150734=CARTESIAN_POINT('Ctrl Pts',(8.89408029065208,0.389962711770638,
124.900475486068));
#150735=CARTESIAN_POINT('Ctrl Pts',(8.88667846897668,0.232972849433727,
124.890106010532));
#150736=CARTESIAN_POINT('Ctrl Pts',(8.87927664730127,0.075446788166063,
124.885994546723));
#150737=CARTESIAN_POINT('Ctrl Pts',(8.87187482562587,-0.082077266939525,
124.888179933649));
#150738=CARTESIAN_POINT('Ctrl Pts',(8.86447691131451,-0.239518166322587,
124.890364166927));
#150739=CARTESIAN_POINT('Ctrl Pts',(8.85707899700321,-0.396956689335564,
124.898838625752));
#150740=CARTESIAN_POINT('Ctrl Pts',(8.84968108269186,-0.553852963753639,
124.913590085875));
#150741=CARTESIAN_POINT('Ctrl Pts',(8.84228439777964,-0.710723164857518,
124.928339094572));
#150742=CARTESIAN_POINT('Ctrl Pts',(8.83488771286733,-0.867050924916991,
124.949362999365));
#150743=CARTESIAN_POINT('Ctrl Pts',(8.82749102795512,-1.02229971229404,
124.976596564282));
#150744=CARTESIAN_POINT('Ctrl Pts',(8.82009467101968,-1.17754161577694,
125.003828921635));
#150745=CARTESIAN_POINT('Ctrl Pts',(8.81269831408429,-1.33170427402173,
125.03727032714));
#150746=CARTESIAN_POINT('Ctrl Pts',(8.80530195714886,-1.48425985966084,
125.076804137574));
#150747=CARTESIAN_POINT('Ctrl Pts',(8.79790446781229,-1.63683880194958,
125.116344000735));
#150748=CARTESIAN_POINT('Ctrl Pts',(8.79050697847572,-1.78780982033592,
125.161978032431));
#150749=CARTESIAN_POINT('Ctrl Pts',(8.78310948913915,-1.93665894237565,
125.213539326967));
#150750=CARTESIAN_POINT('Ctrl Pts',(8.77570940662415,-2.08556024324458,
125.265118696235));
#150751=CARTESIAN_POINT('Ctrl Pts',(8.76830932410908,-2.23233781429737,
125.322629343103));
#150752=CARTESIAN_POINT('Ctrl Pts',(8.76090924159408,-2.37649654151563,
125.385855772993));
#150753=CARTESIAN_POINT('Ctrl Pts',(8.7535010219276,-2.52081378607435,125.449151726842));
#150754=CARTESIAN_POINT('Ctrl Pts',(8.74609280226119,-2.66250609379996,
125.518175865424));
#150755=CARTESIAN_POINT('Ctrl Pts',(8.73868458259471,-2.80110123788644,
125.59266584354));
#150756=CARTESIAN_POINT('Ctrl Pts',(8.73127180329265,-2.93978168497152,
125.667201668995));
#150757=CARTESIAN_POINT('Ctrl Pts',(8.72385902399058,-3.07536084922278,
125.747209848161));
#150758=CARTESIAN_POINT('Ctrl Pts',(8.71644624468851,-3.20739494647732,
125.832384328422));
#150759=CARTESIAN_POINT('Ctrl Pts',(8.70902287365976,-3.3396177002418,125.917680509974));
#150760=CARTESIAN_POINT('Ctrl Pts',(8.70159950263096,-3.46828496580264,
126.008157521682));
#150761=CARTESIAN_POINT('Ctrl Pts',(8.69417613160221,-3.59298487627311,
126.103468123435));
#150762=CARTESIAN_POINT('Ctrl Pts',(8.69024008216141,-3.65910376093801,
126.154004091432));
#150763=CARTESIAN_POINT('Ctrl Pts',(8.68630403272065,-3.7241078691726,126.205898313446));
#150764=CARTESIAN_POINT('Ctrl Pts',(8.68236798327985,-3.78794005225051,
126.259094869223));
#150765=CARTESIAN_POINT('Ctrl Pts',(8.67504798366789,-3.90665084650963,
126.35802624026));
#150766=CARTESIAN_POINT('Ctrl Pts',(8.66772798405598,-4.02168689880861,
126.461781356428));
#150767=CARTESIAN_POINT('Ctrl Pts',(8.66040798444402,-4.13262285489824,
126.570053247798));
#150768=CARTESIAN_POINT('Ctrl Pts',(8.65309668814274,-4.24342691069527,
126.678196406387));
#150769=CARTESIAN_POINT('Ctrl Pts',(8.6457853918414,-4.35014029680781,126.790845389904));
#150770=CARTESIAN_POINT('Ctrl Pts',(8.63847409554012,-4.45236924206574,
126.90765191729));
#150771=CARTESIAN_POINT('Ctrl Pts',(8.63116979082812,-4.55450042862692,
127.024346745843));
#150772=CARTESIAN_POINT('Ctrl Pts',(8.62386548611617,-4.65215545616205,
127.145190919551));
#150773=CARTESIAN_POINT('Ctrl Pts',(8.61656118140417,-4.74497627253956,
127.269798305831));
#150774=CARTESIAN_POINT('Ctrl Pts',(8.60913676518781,-4.83932342829229,
127.396454727743));
#150775=CARTESIAN_POINT('Ctrl Pts',(8.60171234897144,-4.92867568711041,
127.526998947513));
#150776=CARTESIAN_POINT('Ctrl Pts',(8.59428793275509,-5.0126981313822,127.66098854189));
#150777=CARTESIAN_POINT('Ctrl Pts',(8.58699214256618,-5.0952649092545,127.792656802341));
#150778=CARTESIAN_POINT('Ctrl Pts',(8.57969635237722,-5.17268483853595,
127.927651684691));
#150779=CARTESIAN_POINT('Ctrl Pts',(8.57240056218831,-5.24468283714531,
128.065522816554));
#150780=CARTESIAN_POINT('Ctrl Pts',(8.56510620557832,-5.31666668858055,
128.203366857568));
#150781=CARTESIAN_POINT('Ctrl Pts',(8.55781184896839,-5.38323055104187,
128.344085682939));
#150782=CARTESIAN_POINT('Ctrl Pts',(8.55051749235841,-5.44414499442681,
128.487203773035));
#150783=CARTESIAN_POINT('Ctrl Pts',(8.54322303516512,-5.50506027777294,
128.630323836614));
#150784=CARTESIAN_POINT('Ctrl Pts',(8.53592857797181,-5.56032583716038,
128.775842876562));
#150785=CARTESIAN_POINT('Ctrl Pts',(8.52863412077852,-5.60976026776962,
128.923265112108));
#150786=CARTESIAN_POINT('Ctrl Pts',(8.52111254339796,-5.6607338885941,129.075277485736));
#150787=CARTESIAN_POINT('Ctrl Pts',(8.51359096601739,-5.70550721491024,
129.229313086705));
#150788=CARTESIAN_POINT('Ctrl Pts',(8.50606938863683,-5.74393698777221,
129.384811941753));
#150789=CARTESIAN_POINT('Ctrl Pts',(8.4987669129632,-5.7812473107628,129.535781153238));
#150790=CARTESIAN_POINT('Ctrl Pts',(8.49146443728962,-5.81257846859075,
129.688129167305));
#150791=CARTESIAN_POINT('Ctrl Pts',(8.484161961616,-5.83785156299875,129.841334298667));
#150792=CARTESIAN_POINT('Ctrl Pts',(8.47653083338196,-5.86426208908855,
130.001434524369));
#150793=CARTESIAN_POINT('Ctrl Pts',(8.46889970514792,-5.88405653739746,
130.162470332057));
#150794=CARTESIAN_POINT('Ctrl Pts',(8.46126857691388,-5.89720552610408,
130.323842620622));
#150795=CARTESIAN_POINT('Ctrl Pts',(8.45363744867984,-5.91035451481071,
130.485214909186));
#150796=CARTESIAN_POINT('Ctrl Pts',(8.44600632044577,-5.91685808759334,
130.646923203604));
#150797=CARTESIAN_POINT('Ctrl Pts',(8.43837519221174,-5.91674864045279,
130.808371627427));
#150798=CARTESIAN_POINT('',(6.68837519221171,-5.92099708260688,130.799573344013));
#150799=CARTESIAN_POINT('Ctrl Pts',(8.43837519221174,-5.92299826574412,
130.808375864097));
#150800=CARTESIAN_POINT('Ctrl Pts',(8.42689024796347,-5.92488935017588,
131.051615824253));
#150801=CARTESIAN_POINT('Ctrl Pts',(8.32258942911039,-5.80065370683978,
133.258658416759));
#150802=CARTESIAN_POINT('Ctrl Pts',(8.12547273565442,-3.02737642437282,
137.114079511095));
#150803=CARTESIAN_POINT('Ctrl Pts',(7.84702511184098,3.67217430050631,136.761935328562));
#150804=CARTESIAN_POINT('Ctrl Pts',(7.56857748802829,6.99717623890907,130.935071030307));
#150805=CARTESIAN_POINT('Ctrl Pts',(7.29012986421539,3.8921150448166,124.988090248315));
#150806=CARTESIAN_POINT('Ctrl Pts',(7.01168224040252,-2.78960973507063,
124.38597779505));
#150807=CARTESIAN_POINT('Ctrl Pts',(6.81109734973462,-5.75623819392495,
128.201098093543));
#150808=CARTESIAN_POINT('Ctrl Pts',(6.70332833367101,-5.92378219031308,
130.482601527499));
#150809=CARTESIAN_POINT('Ctrl Pts',(6.68837519221171,-5.92099708260688,
130.799573344013));
#150810=CARTESIAN_POINT('',(4.93837519221179,-5.90740647963781,130.802618111737));
#150811=CARTESIAN_POINT('Ctrl Pts',(6.68837519221171,-5.92099708260688,
130.799573344013));
#150812=CARTESIAN_POINT('Ctrl Pts',(6.6105124590667,-5.9064947053841,132.450082170598));
#150813=CARTESIAN_POINT('Ctrl Pts',(6.4398338513174,-4.32747935093831,136.092391492262));
#150814=CARTESIAN_POINT('Ctrl Pts',(6.17633936896388,1.85058583215606,137.553648921391));
#150815=CARTESIAN_POINT('Ctrl Pts',(5.89789174515079,6.67865424514227,132.895565534405));
#150816=CARTESIAN_POINT('Ctrl Pts',(5.61944412133808,5.36936567723543,126.315766989886));
#150817=CARTESIAN_POINT('Ctrl Pts',(5.34099649752515,-0.874107639948943,
123.860766709212));
#150818=CARTESIAN_POINT('Ctrl Pts',(5.1139735211497,-5.30960218217041,127.061555711575));
#150819=CARTESIAN_POINT('Ctrl Pts',(4.97976641937861,-5.90972563308018,
129.920085651997));
#150820=CARTESIAN_POINT('Ctrl Pts',(4.93837519221179,-5.90740647963781,
130.802618111737));
#150821=CARTESIAN_POINT('',(3.18837519221176,-5.9145855427205,130.809751264182));
#150822=CARTESIAN_POINT('Ctrl Pts',(4.93837519221179,-5.90740647963781,
130.802618111737));
#150823=CARTESIAN_POINT('Ctrl Pts',(4.88695054477432,-5.90452515293428,
131.899080422732));
#150824=CARTESIAN_POINT('Ctrl Pts',(4.74271002273249,-5.08506508489207,
134.97853974863));
#150825=CARTESIAN_POINT('Ctrl Pts',(4.50565362608645,-0.120061750281574,
137.801727672856));
#150826=CARTESIAN_POINT('Ctrl Pts',(4.22720600227359,5.82218677065032,134.68761978198));
#150827=CARTESIAN_POINT('Ctrl Pts',(3.9487583784607,6.41413007899093,128.004986426763));
#150828=CARTESIAN_POINT('Ctrl Pts',(3.67031075464771,1.1118011924118,123.894841195861));
#150829=CARTESIAN_POINT('Ctrl Pts',(3.41684969256491,-4.6447312943842,125.933256779022));
#150830=CARTESIAN_POINT('Ctrl Pts',(3.25620450508613,-5.90184342734158,
129.367926591703));
#150831=CARTESIAN_POINT('Ctrl Pts',(3.18837519221176,-5.9145855427205,130.809751264182));
#150832=CARTESIAN_POINT('',(1.43837519221172,-5.9220814725113,130.803783456464));
#150833=CARTESIAN_POINT('Ctrl Pts',(3.18837519221176,-5.9145855427205,130.809751264182));
#150834=CARTESIAN_POINT('Ctrl Pts',(3.16338863048184,-5.91927940793884,
131.340882122744));
#150835=CARTESIAN_POINT('Ctrl Pts',(3.04558619414775,-5.6099754134907,133.839595697384));
#150836=CARTESIAN_POINT('Ctrl Pts',(2.83496788320905,-2.0810387204088,137.486189586833));
#150837=CARTESIAN_POINT('Ctrl Pts',(2.55652025939625,4.49675969049486,136.166889201757));
#150838=CARTESIAN_POINT('Ctrl Pts',(2.27807263558332,6.94225562475717,129.9196870219));
#150839=CARTESIAN_POINT('Ctrl Pts',(1.99962501177045,3.00815778790935,124.485456657748));
#150840=CARTESIAN_POINT('Ctrl Pts',(1.72117738795757,-3.69029009934919,
124.857990337051));
#150841=CARTESIAN_POINT('Ctrl Pts',(1.53409411477124,-5.91236490058832,
128.779722884542));
#150842=CARTESIAN_POINT('Ctrl Pts',(1.43982671618935,-5.9265061143831,130.773088677422));
#150843=CARTESIAN_POINT('Ctrl Pts',(1.43837519221171,-5.92646357529495,
130.803783029388));
#150844=CARTESIAN_POINT('',(-0.311624788304493,-5.91431933878038,130.799248754294));
#150845=CARTESIAN_POINT('Ctrl Pts',(1.43837519221174,-5.9167499719005,130.803783976068));
#150846=CARTESIAN_POINT('Ctrl Pts',(1.43097212084849,-5.91676520388193,
130.960074888071));
#150847=CARTESIAN_POINT('Ctrl Pts',(1.42356904948527,-5.91058352531488,
131.116608525822));
#150848=CARTESIAN_POINT('Ctrl Pts',(1.41616597812202,-5.89817319978246,
131.272851244866));
#150849=CARTESIAN_POINT('Ctrl Pts',(1.40877164548738,-5.88577752363829,
131.428909531983));
#150850=CARTESIAN_POINT('Ctrl Pts',(1.40137731285276,-5.86716786357436,
131.584677213211));
#150851=CARTESIAN_POINT('Ctrl Pts',(1.39398298021811,-5.84236444631937,
131.73961899838));
#150852=CARTESIAN_POINT('Ctrl Pts',(1.38659573990202,-5.817584819411,131.894412170206));
#150853=CARTESIAN_POINT('Ctrl Pts',(1.37920849958587,-5.78662332010163,
132.04838065453));
#150854=CARTESIAN_POINT('Ctrl Pts',(1.37182125926978,-5.74955208297358,
132.200992783769));
#150855=CARTESIAN_POINT('Ctrl Pts',(1.36443947063227,-5.71250820389276,
132.353492287422));
#150856=CARTESIAN_POINT('Ctrl Pts',(1.35705768199478,-5.66936365231962,
132.50463706549));
#150857=CARTESIAN_POINT('Ctrl Pts',(1.34967589335727,-5.62024187187363,
132.653904308355));
#150858=CARTESIAN_POINT('Ctrl Pts',(1.34195115364788,-5.56883793894613,
132.810106369251));
#150859=CARTESIAN_POINT('Ctrl Pts',(1.33422641393849,-5.51088814896009,
132.964251841321));
#150860=CARTESIAN_POINT('Ctrl Pts',(1.32650167422909,-5.44659310119009,
133.115757198114));
#150861=CARTESIAN_POINT('Ctrl Pts',(1.31912484760139,-5.38519382584074,
133.260438933974));
#150862=CARTESIAN_POINT('Ctrl Pts',(1.31174802097365,-5.31800851899369,
133.40271278799));
#150863=CARTESIAN_POINT('Ctrl Pts',(1.30437119434595,-5.24526164482172,
133.542089756809));
#150864=CARTESIAN_POINT('Ctrl Pts',(1.2969945080438,-5.17251615447596,133.681464074332));
#150865=CARTESIAN_POINT('Ctrl Pts',(1.28961782174171,-5.09420948069823,
133.817941283128));
#150866=CARTESIAN_POINT('Ctrl Pts',(1.28224113543956,-5.01061238377904,
133.951056361044));
#150867=CARTESIAN_POINT('Ctrl Pts',(1.27486311199148,-4.92700013350854,
134.084195568261));
#150868=CARTESIAN_POINT('Ctrl Pts',(1.26748508854335,-4.83809575072785,
134.213971113281));
#150869=CARTESIAN_POINT('Ctrl Pts',(1.26010706509527,-4.74421361042342,
134.339946535228));
#150870=CARTESIAN_POINT('Ctrl Pts',(1.25272622647908,-4.65029564832886,
134.46597002452));
#150871=CARTESIAN_POINT('Ctrl Pts',(1.24534538786292,-4.55139637189808,
134.588190203319));
#150872=CARTESIAN_POINT('Ctrl Pts',(1.23796454924673,-4.44787062566144,
134.706203446266));
#150873=CARTESIAN_POINT('Ctrl Pts',(1.23057553704002,-4.34423023431447,
134.824347377875));
#150874=CARTESIAN_POINT('Ctrl Pts',(1.22318652483326,-4.2359533912951,134.93827478933));
#150875=CARTESIAN_POINT('Ctrl Pts',(1.21579751262655,-4.12343246340871,
135.047618243755));
#150876=CARTESIAN_POINT('Ctrl Pts',(1.20840370882591,-4.01083856844906,
135.157032604738));
#150877=CARTESIAN_POINT('Ctrl Pts',(1.20100990502526,-3.89399538428133,
135.261856836618));
#150878=CARTESIAN_POINT('Ctrl Pts',(1.19361610122462,-3.7733281051864,135.361763998123));
#150879=CARTESIAN_POINT('Ctrl Pts',(1.18621214497658,-3.65249513759912,
135.46180834236));
#150880=CARTESIAN_POINT('Ctrl Pts',(1.17880818872853,-3.52782788922118,
135.556921910029));
#150881=CARTESIAN_POINT('Ctrl Pts',(1.17140423248048,-3.3997807577748,135.646820876728));
#150882=CARTESIAN_POINT('Ctrl Pts',(1.16903020176424,-3.35872327269568,
135.675646399348));
#150883=CARTESIAN_POINT('Ctrl Pts',(1.16665617104802,-3.31731848458099,
135.703936150045));
#150884=CARTESIAN_POINT('Ctrl Pts',(1.16428214033178,-3.27558188361879,
135.731681784915));
#150885=CARTESIAN_POINT('Ctrl Pts',(1.15685887392635,-3.14507729255366,
135.818438555928));
#150886=CARTESIAN_POINT('Ctrl Pts',(1.14943560752094,-3.01092623459139,
135.900138132485));
#150887=CARTESIAN_POINT('Ctrl Pts',(1.1420123411155,-2.87355827453246,135.976458200304));
#150888=CARTESIAN_POINT('Ctrl Pts',(1.13459784839449,-2.73635267199463,
136.052688064141));
#150889=CARTESIAN_POINT('Ctrl Pts',(1.12718335567345,-2.59593805861329,
136.123550895612));
#150890=CARTESIAN_POINT('Ctrl Pts',(1.11976886295244,-2.45277402934651,
136.188766817275));
#150891=CARTESIAN_POINT('Ctrl Pts',(1.11236151659866,-2.30974798696096,
136.253919881377));
#150892=CARTESIAN_POINT('Ctrl Pts',(1.10495417024496,-2.16397814173031,
136.313436717314));
#150893=CARTESIAN_POINT('Ctrl Pts',(1.09754682389118,-2.01594972001534,
136.367082728985));
#150894=CARTESIAN_POINT('Ctrl Pts',(1.09014500221579,-1.8680317034825,136.420688729436));
#150895=CARTESIAN_POINT('Ctrl Pts',(1.08274318054034,-1.71785881404619,
136.468432497526));
#150896=CARTESIAN_POINT('Ctrl Pts',(1.07534135886496,-1.56593724143843,
136.510127097048));
#150897=CARTESIAN_POINT('Ctrl Pts',(1.06794344455362,-1.4140958670463,136.551799686314));
#150898=CARTESIAN_POINT('Ctrl Pts',(1.06054553024226,-1.26050800698827,
136.587429368093));
#150899=CARTESIAN_POINT('Ctrl Pts',(1.05314761593092,-1.10569592670047,
136.616878753467));
#150900=CARTESIAN_POINT('Ctrl Pts',(1.04575093101872,-0.95090957337161,
136.646323244888));
#150901=CARTESIAN_POINT('Ctrl Pts',(1.0383542461065,-0.794899769950169,
136.669589408608));
#150902=CARTESIAN_POINT('Ctrl Pts',(1.0309575611943,-0.638200032947009,
136.68659074571));
#150903=CARTESIAN_POINT('Ctrl Pts',(1.02356120425885,-0.481507244174174,
136.703591328955));
#150904=CARTESIAN_POINT('Ctrl Pts',(1.01616484732343,-0.324124953767255,
136.714327597653));
#150905=CARTESIAN_POINT('Ctrl Pts',(1.00876849038798,-0.166592609029845,
136.718764853422));
#150906=CARTESIAN_POINT('Ctrl Pts',(1.00137100105141,-0.00903614568851985,
136.723202788547));
#150907=CARTESIAN_POINT('Ctrl Pts',(0.993973511714845,0.148670044553117,
136.721339779992));
#150908=CARTESIAN_POINT('Ctrl Pts',(0.986576022378273,0.305985849462564,
136.713193262212));
#150909=CARTESIAN_POINT('Ctrl Pts',(0.979175939863302,0.463356801183101,
136.705043888682));
#150910=CARTESIAN_POINT('Ctrl Pts',(0.971775857348313,0.620336722540329,
136.690606639713));
#150911=CARTESIAN_POINT('Ctrl Pts',(0.964375774833343,0.776390107902843,
136.669950866028));
#150912=CARTESIAN_POINT('Ctrl Pts',(0.95696755516688,0.932615090005686,
136.649272379196));
#150913=CARTESIAN_POINT('Ctrl Pts',(0.949559335500442,1.087911131163,136.622361760914));
#150914=CARTESIAN_POINT('Ctrl Pts',(0.94215111583398,1.24175168556608,136.589339728496));
#150915=CARTESIAN_POINT('Ctrl Pts',(0.934738336531926,1.39568692626342,
136.556297371568));
#150916=CARTESIAN_POINT('Ctrl Pts',(0.927325557229862,1.54816453443217,
136.517136197943));
#150917=CARTESIAN_POINT('Ctrl Pts',(0.919912777927806,1.69867313435842,
136.472026816727));
#150918=CARTESIAN_POINT('Ctrl Pts',(0.912489406899048,1.84939678803061,
136.426852981111));
#150919=CARTESIAN_POINT('Ctrl Pts',(0.905066035870255,1.99814546236399,
136.375714084383));
#150920=CARTESIAN_POINT('Ctrl Pts',(0.897642664841499,2.14442698996647,
136.318829172849));
#150921=CARTESIAN_POINT('Ctrl Pts',(0.893706615400625,2.22198896588004,
136.288667427818));
#150922=CARTESIAN_POINT('Ctrl Pts',(0.889770565959759,2.29885772615748,
136.256891052009));
#150923=CARTESIAN_POINT('Ctrl Pts',(0.885834516518884,2.37496282844648,
136.223537873017));
#150924=CARTESIAN_POINT('Ctrl Pts',(0.87841125011346,2.51849467620134,136.160634818356));
#150925=CARTESIAN_POINT('Ctrl Pts',(0.870987983708066,2.659742767461,136.091930350689));
#150926=CARTESIAN_POINT('Ctrl Pts',(0.863564717302637,2.79820373982473,
136.017611656307));
#150927=CARTESIAN_POINT('Ctrl Pts',(0.856150224581625,2.93650106281779,
135.943380800449));
#150928=CARTESIAN_POINT('Ctrl Pts',(0.848735731860612,3.07201749822384,
135.863549100793));
#150929=CARTESIAN_POINT('Ctrl Pts',(0.841321239139603,3.20426915492438,
135.778351947002));
#150930=CARTESIAN_POINT('Ctrl Pts',(0.833913892785829,3.33639334249901,
135.693236909434));
#150931=CARTESIAN_POINT('Ctrl Pts',(0.826506546432057,3.46525870415051,
135.602766913829));
#150932=CARTESIAN_POINT('Ctrl Pts',(0.819099200078284,3.59040559083518,
135.507223389942));
#150933=CARTESIAN_POINT('Ctrl Pts',(0.811697378402865,3.71545913825058,
135.41175112602));
#150934=CARTESIAN_POINT('Ctrl Pts',(0.804295556727454,3.83679943743615,
135.311213093878));
#150935=CARTESIAN_POINT('Ctrl Pts',(0.796893735052038,3.95399560575159,
135.205934121689));
#150936=CARTESIAN_POINT('Ctrl Pts',(0.789495820740721,4.0711299071212,135.10071072545));
#150937=CARTESIAN_POINT('Ctrl Pts',(0.782097906429348,4.18412415743951,
134.990751622254));
#150938=CARTESIAN_POINT('Ctrl Pts',(0.77469999211803,4.29258047029525,134.876421946738));
#150939=CARTESIAN_POINT('Ctrl Pts',(0.767303307205828,4.40101875967986,
134.76211127074));
#150940=CARTESIAN_POINT('Ctrl Pts',(0.759906622293692,4.50492035165083,
134.643431734493));
#150941=CARTESIAN_POINT('Ctrl Pts',(0.75250993738149,4.60392409351145,134.520785445769));
#150942=CARTESIAN_POINT('Ctrl Pts',(0.745113580446058,4.70292344544226,
134.398144595311));
#150943=CARTESIAN_POINT('Ctrl Pts',(0.737717223510577,4.79702514460619,
134.271537632573));
#150944=CARTESIAN_POINT('Ctrl Pts',(0.730320866575141,4.88590841382615,
134.141399654527));
#150945=CARTESIAN_POINT('Ctrl Pts',(0.722923377238545,4.97480529130192,
134.011241752024));
#150946=CARTESIAN_POINT('Ctrl Pts',(0.715525887901973,5.05848193745507,
133.877552066072));
#150947=CARTESIAN_POINT('Ctrl Pts',(0.708128398565378,5.13666107653126,
133.740794432136));
#150948=CARTESIAN_POINT('Ctrl Pts',(0.700728316050354,5.21486762118357,
133.603988858023));
#150949=CARTESIAN_POINT('Ctrl Pts',(0.693328233535386,5.2875726366831,133.464113518565));
#150950=CARTESIAN_POINT('Ctrl Pts',(0.685928151020363,5.35454501588482,
133.321656435574));
#150951=CARTESIAN_POINT('Ctrl Pts',(0.6785199313539,5.42159103810212,133.179042706377));
#150952=CARTESIAN_POINT('Ctrl Pts',(0.671111711687377,5.48289167635482,
133.033841902229));
#150953=CARTESIAN_POINT('Ctrl Pts',(0.663703492020915,5.53826388266825,
132.886562271689));
#150954=CARTESIAN_POINT('Ctrl Pts',(0.65629071271885,5.5936701696508,132.739191992994));
#150955=CARTESIAN_POINT('Ctrl Pts',(0.648877933416802,5.64314063686597,
132.589740691942));
#150956=CARTESIAN_POINT('Ctrl Pts',(0.641465154114741,5.68654241152167,
132.438730821793));
#150957=CARTESIAN_POINT('Ctrl Pts',(0.634041783085998,5.73000620066828,
132.287505181661));
#150958=CARTESIAN_POINT('Ctrl Pts',(0.626618412057289,5.76738389038742,
132.134716886344));
#150959=CARTESIAN_POINT('Ctrl Pts',(0.619195041028547,5.79859374204342,
131.980898410089));
#150960=CARTESIAN_POINT('Ctrl Pts',(0.615258991587718,5.81514195426174,
131.899340163154));
#150961=CARTESIAN_POINT('Ctrl Pts',(0.611322942146822,5.82995703189355,
131.817492390791));
#150962=CARTESIAN_POINT('Ctrl Pts',(0.607386892705989,5.84303272455383,
131.735434804886));
#150963=CARTESIAN_POINT('Ctrl Pts',(0.599963626300545,5.86769307283249,
131.580676758799));
#150964=CARTESIAN_POINT('Ctrl Pts',(0.592540359895133,5.88623810187495,
131.424704296294));
#150965=CARTESIAN_POINT('Ctrl Pts',(0.585117093489686,5.89855321713593,
131.268042089177));
#150966=CARTESIAN_POINT('Ctrl Pts',(0.577702600768656,5.91085377695339,
131.111565043778));
#150967=CARTESIAN_POINT('Ctrl Pts',(0.570288108047624,5.91693905059183,
130.954400244984));
#150968=CARTESIAN_POINT('Ctrl Pts',(0.562873615326595,5.91674552307085,
130.79708203796));
#150969=CARTESIAN_POINT('Ctrl Pts',(0.555466268972801,5.91655218207898,
130.639915460146));
#150970=CARTESIAN_POINT('Ctrl Pts',(0.548058922619009,5.91009208821658,
130.482596139254));
#150971=CARTESIAN_POINT('Ctrl Pts',(0.540651576265219,5.89735356477309,
130.325662910701));
#150972=CARTESIAN_POINT('Ctrl Pts',(0.533249754589813,5.88462454220099,
130.16884672887));
#150973=CARTESIAN_POINT('Ctrl Pts',(0.525847932914469,5.8656264439867,130.012416436479));
#150974=CARTESIAN_POINT('Ctrl Pts',(0.518446111239058,5.84039965467834,
129.856910124858));
#150975=CARTESIAN_POINT('Ctrl Pts',(0.511048196927705,5.81518618239572,
129.701485903808));
#150976=CARTESIAN_POINT('Ctrl Pts',(0.503650282616284,5.78375062700797,
129.546985059673));
#150977=CARTESIAN_POINT('Ctrl Pts',(0.496252368304937,5.7461851193028,129.393939709751));
#150978=CARTESIAN_POINT('Ctrl Pts',(0.488855683392715,5.7086258543034,129.240919793188));
#150979=CARTESIAN_POINT('Ctrl Pts',(0.481458998480501,5.66493874767725,
129.089355252966));
#150980=CARTESIAN_POINT('Ctrl Pts',(0.474062313568282,5.61526689222679,
128.93976728615));
#150981=CARTESIAN_POINT('Ctrl Pts',(0.466665956632824,5.56559723927845,
128.79018595222));
#150982=CARTESIAN_POINT('Ctrl Pts',(0.459269599697343,5.50994348279135,
128.642581371708));
#150983=CARTESIAN_POINT('Ctrl Pts',(0.451873242761877,5.44849829426981,
128.497458604077));
#150984=CARTESIAN_POINT('Ctrl Pts',(0.444475753425283,5.38704369833305,
128.35231361778));
#150985=CARTESIAN_POINT('Ctrl Pts',(0.437078264088703,5.31979605041375,
128.209651544716));
#150986=CARTESIAN_POINT('Ctrl Pts',(0.429680774752114,5.24699571410832,
128.06995637923));
#150987=CARTESIAN_POINT('Ctrl Pts',(0.422280692237107,5.17416985775784,
127.93021224382));
#150988=CARTESIAN_POINT('Ctrl Pts',(0.414880609722111,5.09578760999192,
127.793437417545));
#150989=CARTESIAN_POINT('Ctrl Pts',(0.407480527207099,5.01213463832796,
127.660090125103));
#150990=CARTESIAN_POINT('Ctrl Pts',(0.400072307540625,4.92838968162203,
127.526596203605));
#150991=CARTESIAN_POINT('Ctrl Pts',(0.392664087874122,4.83936262511829,
127.396537659149));
#150992=CARTESIAN_POINT('Ctrl Pts',(0.385255868207651,4.74538213082243,
127.270343215943));
#150993=CARTESIAN_POINT('Ctrl Pts',(0.377843088905566,4.65134379310021,
127.144071102163));
#150994=CARTESIAN_POINT('Ctrl Pts',(0.370430309603479,4.55234617675713,
127.021668118249));
#150995=CARTESIAN_POINT('Ctrl Pts',(0.363017530301391,4.44875701552763,
126.903528452592));
#150996=CARTESIAN_POINT('Ctrl Pts',(0.355594159272623,4.34501984124686,
126.785219983441));
#150997=CARTESIAN_POINT('Ctrl Pts',(0.348170788243878,4.2366782755013,126.671187268809));
#150998=CARTESIAN_POINT('Ctrl Pts',(0.340747417215113,4.12413612222472,
126.561786893061));
#150999=CARTESIAN_POINT('Ctrl Pts',(0.336811367774451,4.06446357214758,
126.503780188815));
#151000=CARTESIAN_POINT('Ctrl Pts',(0.332875318333758,4.00361063455032,
126.447075124216));
#151001=CARTESIAN_POINT('Ctrl Pts',(0.328939268893095,3.94164099481367,
126.391720044111));
#151002=CARTESIAN_POINT('Ctrl Pts',(0.321516002487664,3.82476818827281,
126.287322090601));
#151003=CARTESIAN_POINT('Ctrl Pts',(0.314092736082256,3.7035681793829,126.187412706623));
#151004=CARTESIAN_POINT('Ctrl Pts',(0.30666946967682,3.57842044824294,126.092371901737));
#151005=CARTESIAN_POINT('Ctrl Pts',(0.29925497695581,3.45342063132831,125.997443427191));
#151006=CARTESIAN_POINT('Ctrl Pts',(0.291840484234759,3.32448267400762,
125.907372301423));
#151007=CARTESIAN_POINT('Ctrl Pts',(0.284425991513757,3.19202180460264,
125.822500788));
#151008=CARTESIAN_POINT('Ctrl Pts',(0.27701864515998,3.05968860597046,125.737711076937));
#151009=CARTESIAN_POINT('Ctrl Pts',(0.269611298806304,2.9238395672605,125.658111201183));
#151010=CARTESIAN_POINT('Ctrl Pts',(0.262203952452523,2.7849217144219,125.584002238389));
#151011=CARTESIAN_POINT('Ctrl Pts',(0.254802130777138,2.64610747175942,
125.509948548856));
#151012=CARTESIAN_POINT('Ctrl Pts',(0.247400309101722,2.5042293002962,125.441377792879));
#151013=CARTESIAN_POINT('Ctrl Pts',(0.239998487426334,2.35976174034193,
125.378546845299));
#151014=CARTESIAN_POINT('Ctrl Pts',(0.232600573114961,2.21537044368741,
125.315749065688));
#151015=CARTESIAN_POINT('Ctrl Pts',(0.225202658803554,2.0683928222819,125.258685208589));
#151016=CARTESIAN_POINT('Ctrl Pts',(0.217804744492184,1.91932636041903,
125.207565384158));
#151017=CARTESIAN_POINT('Ctrl Pts',(0.210408059579972,1.770284670698,125.156454054914));
#151018=CARTESIAN_POINT('Ctrl Pts',(0.203011374667773,1.61915518223042,
125.111284918842));
#151019=CARTESIAN_POINT('Ctrl Pts',(0.195614689755558,1.4664537380229,125.072219307659));
#151020=CARTESIAN_POINT('Ctrl Pts',(0.188218332820104,1.31375906475744,
125.033155428686));
#151021=CARTESIAN_POINT('Ctrl Pts',(0.180821975884583,1.15949293599379,
125.000194629006));
#151022=CARTESIAN_POINT('Ctrl Pts',(0.173425618949125,1.00418441621774,
124.973447805602));
#151023=CARTESIAN_POINT('Ctrl Pts',(0.166028129612527,0.848852118310616,
124.946696887191));
#151024=CARTESIAN_POINT('Ctrl Pts',(0.158630640275958,0.692477479526676,
124.926161902732));
#151025=CARTESIAN_POINT('Ctrl Pts',(0.151233150939362,0.535597620410355,
124.911902238289));
#151026=CARTESIAN_POINT('Ctrl Pts',(0.143833068424346,0.378662767302617,
124.897637575143));
#151027=CARTESIAN_POINT('Ctrl Pts',(0.136432985909389,0.221222712782735,
124.889652645576));
#151028=CARTESIAN_POINT('Ctrl Pts',(0.129032903394375,0.0638173845376825,
124.887954791059));
#151029=CARTESIAN_POINT('Ctrl Pts',(0.121624683727909,-0.0937610270469865,
124.886255069575));
#151030=CARTESIAN_POINT('Ctrl Pts',(0.114216464061448,-0.251304262593419,
124.890856233454));
#151031=CARTESIAN_POINT('Ctrl Pts',(0.106808244394983,-0.40827397444272,
124.901713505948));
#151032=CARTESIAN_POINT('Ctrl Pts',(0.0993954650929377,-0.565340298530262,
124.912577460912));
#151033=CARTESIAN_POINT('Ctrl Pts',(0.0919826857909391,-0.72183202531378,
124.929705156634));
#151034=CARTESIAN_POINT('Ctrl Pts',(0.0845699064888947,-0.877218743869465,
124.953000276765));
#151035=CARTESIAN_POINT('Ctrl Pts',(0.0771465354601375,-1.03282748625598,
124.976328682055));
#151036=CARTESIAN_POINT('Ctrl Pts',(0.069723164431318,-1.18732770132546,
125.005842042047));
#151037=CARTESIAN_POINT('Ctrl Pts',(0.0622997934025591,-1.34020111866291,
125.041393367613));
#151038=CARTESIAN_POINT('Ctrl Pts',(0.058363743961779,-1.42125827268231,
125.06024353347));
#151039=CARTESIAN_POINT('Ctrl Pts',(0.0544276945210084,-1.50185834868971,
125.080790360802));
#151040=CARTESIAN_POINT('Ctrl Pts',(0.0504916450802284,-1.58192624929231,
125.103006400865));
#151041=CARTESIAN_POINT('Ctrl Pts',(0.0430683786747836,-1.73293181099582,
125.144905159084));
#151042=CARTESIAN_POINT('Ctrl Pts',(0.0356451122694012,-1.88249997059805,
125.192870696663));
#151043=CARTESIAN_POINT('Ctrl Pts',(0.0282218458639534,-2.03010589702807,
125.246789150697));
#151044=CARTESIAN_POINT('Ctrl Pts',(0.0208073531429645,-2.17753736551032,
125.300643877597));
#151045=CARTESIAN_POINT('Ctrl Pts',(0.0133928604218992,-2.32301086998142,
125.360437389217));
#151046=CARTESIAN_POINT('Ctrl Pts',(0.00597836770091931,-2.46601401336008,
125.426005344026));
#151047=CARTESIAN_POINT('Ctrl Pts',(-0.00142897865282537,-2.60887932492519,
125.491510101973));
#151048=CARTESIAN_POINT('Ctrl Pts',(-0.00883632500662208,-2.74927867850225,
125.562778068504));
#151049=CARTESIAN_POINT('Ctrl Pts',(-0.0162436713603711,-2.88671714049119,
125.639595887852));
#151050=CARTESIAN_POINT('Ctrl Pts',(-0.0236454930357674,-3.02405309569032,
125.716356413574));
#151051=CARTESIAN_POINT('Ctrl Pts',(-0.0310473147111037,-3.15843223196212,
125.798658368884));
#151052=CARTESIAN_POINT('Ctrl Pts',(-0.0384491363865038,-3.28938193259737,
125.88624135671));
#151053=CARTESIAN_POINT('Ctrl Pts',(-0.0458470506978888,-3.42026250590552,
125.973778110159));
#151054=CARTESIAN_POINT('Ctrl Pts',(-0.0532449650092701,-3.54771693951329,
126.066590137045));
#151055=CARTESIAN_POINT('Ctrl Pts',(-0.0606428793206533,-3.67129955938354,
126.164372459416));
#151056=CARTESIAN_POINT('Ctrl Pts',(-0.0680395642328581,-3.79486164206386,
126.262138532139));
#151057=CARTESIAN_POINT('Ctrl Pts',(-0.0754362491450449,-3.91455289555713,
126.364873029631));
#151058=CARTESIAN_POINT('Ctrl Pts',(-0.0828329340572509,-4.02995876117528,
126.472229162298));
#151059=CARTESIAN_POINT('Ctrl Pts',(-0.0902292909927178,-4.14535950957674,
126.579580534681));
#151060=CARTESIAN_POINT('Ctrl Pts',(-0.097625647928219,-4.25647497460286,
126.691552880514));
#151061=CARTESIAN_POINT('Ctrl Pts',(-0.105022004863685,-4.36292588320257,
126.80776102539));
#151062=CARTESIAN_POINT('Ctrl Pts',(-0.112419494200237,-4.46939308970754,
126.923986962029));
#151063=CARTESIAN_POINT('Ctrl Pts',(-0.119816983536782,-4.57119406563906,
127.044449713702));
#151064=CARTESIAN_POINT('Ctrl Pts',(-0.127214472873334,-4.66798852104518,
127.168729485302));
#151065=CARTESIAN_POINT('Ctrl Pts',(-0.134614555388326,-4.76481690759787,
127.293052822982));
#151066=CARTESIAN_POINT('Ctrl Pts',(-0.142014637903356,-4.85663505014213,
127.42119555031));
#151067=CARTESIAN_POINT('Ctrl Pts',(-0.149414720418349,-4.94314492798882,
127.552707379074));
#151068=CARTESIAN_POINT('Ctrl Pts',(-0.156822940084836,-5.02974993233988,
127.684363818613));
#151069=CARTESIAN_POINT('Ctrl Pts',(-0.164231159751286,-5.11103480987731,
127.819396446001));
#151070=CARTESIAN_POINT('Ctrl Pts',(-0.171639379417769,-5.18674624248784,
127.95732813118));
#151071=CARTESIAN_POINT('Ctrl Pts',(-0.179052158719834,-5.26250427422172,
128.095344711009));
#151072=CARTESIAN_POINT('Ctrl Pts',(-0.186464938021906,-5.33268185957847,
128.236263570734));
#151073=CARTESIAN_POINT('Ctrl Pts',(-0.193877717323971,-5.39707333217188,
128.379586399281));
#151074=CARTESIAN_POINT('Ctrl Pts',(-0.201301088352739,-5.46155681032108,
128.523114014207));
#151075=CARTESIAN_POINT('Ctrl Pts',(-0.208724459381482,-5.5202375248212,
128.669052112798));
#151076=CARTESIAN_POINT('Ctrl Pts',(-0.21614783041025,-5.57295900396849,
128.816885208262));
#151077=CARTESIAN_POINT('Ctrl Pts',(-0.220083879851061,-5.60091319724702,
128.895269862684));
#151078=CARTESIAN_POINT('Ctrl Pts',(-0.224019929291911,-5.62719287934486,
128.9741870514));
#151079=CARTESIAN_POINT('Ctrl Pts',(-0.227955978732723,-5.6517805516924,
129.053558756129));
#151080=CARTESIAN_POINT('Ctrl Pts',(-0.237002541632423,-5.7082925258925,
129.235985610793));
#151081=CARTESIAN_POINT('Ctrl Pts',(-0.246049104532169,-5.75600204132922,
129.421259959019));
#151082=CARTESIAN_POINT('Ctrl Pts',(-0.255095667431874,-5.79466319391346,
129.608614393819));
#151083=CARTESIAN_POINT('Ctrl Pts',(-0.264517182244824,-5.83492673110393,
129.803734087598));
#151084=CARTESIAN_POINT('Ctrl Pts',(-0.273938697057761,-5.86537581948693,
130.001110085161));
#151085=CARTESIAN_POINT('Ctrl Pts',(-0.283360211870729,-5.88578779369038,
130.199850394207));
#151086=CARTESIAN_POINT('Ctrl Pts',(-0.292243301940128,-5.90503325569336,
130.387233007377));
#151087=CARTESIAN_POINT('Ctrl Pts',(-0.30112639200945,-5.91535635260079,
130.575828272977));
#151088=CARTESIAN_POINT('Ctrl Pts',(-0.31000948207884,-5.9166181911593,
130.764867041597));
#151089=CARTESIAN_POINT('Ctrl Pts',(-0.310547906822408,-5.91669467412829,
130.776325120905));
#151090=CARTESIAN_POINT('Ctrl Pts',(-0.311086331566016,-5.91673788194359,
130.787784823116));
#151091=CARTESIAN_POINT('Ctrl Pts',(-0.311624756309584,-5.91674778936248,
130.799245974448));
#151092=CARTESIAN_POINT('',(-2.06162483645605,-5.91244912682104,130.807044328504));
#151093=CARTESIAN_POINT('Ctrl Pts',(-0.311624807788274,-5.91284049796445,
130.799250447123));
#151094=CARTESIAN_POINT('Ctrl Pts',(-0.376551072707372,-5.90153303013459,
132.180398272274));
#151095=CARTESIAN_POINT('Ctrl Pts',(-0.53429321223076,-4.72958062977401,
135.55326689347));
#151096=CARTESIAN_POINT('Ctrl Pts',(-0.784851226358526,0.895237502509812,
137.745261880691));
#151097=CARTESIAN_POINT('Ctrl Pts',(-1.06329885017127,6.32347454670116,
133.80289862592));
#151098=CARTESIAN_POINT('Ctrl Pts',(-1.34174647398429,5.94074740138417,
127.105025428197));
#151099=CARTESIAN_POINT('Ctrl Pts',(-1.62019409779717,0.0987636158356631,
123.806660546933));
#151100=CARTESIAN_POINT('Ctrl Pts',(-1.86015354239845,-5.01393093486658,
126.505897385061));
#151101=CARTESIAN_POINT('Ctrl Pts',(-2.00729711239547,-5.90338408802778,
129.649020459756));
#151102=CARTESIAN_POINT('Ctrl Pts',(-2.0616248077882,-5.90809907779839,
130.807041742467));
#151103=CARTESIAN_POINT('',(-3.81162480778819,-5.91969451445794,130.808517656963));
#151104=CARTESIAN_POINT('Ctrl Pts',(-2.06162486479582,-5.916749390203,130.807046884944));
#151105=CARTESIAN_POINT('Ctrl Pts',(-2.06971386832509,-5.91667099475305,
130.979720027814));
#151106=CARTESIAN_POINT('Ctrl Pts',(-2.07780287185427,-5.90902959923856,
131.152144819403));
#151107=CARTESIAN_POINT('Ctrl Pts',(-2.08589187538357,-5.89391499210028,
131.323683858328));
#151108=CARTESIAN_POINT('Ctrl Pts',(-2.09401865753072,-5.87872979419454,
131.496024047578));
#151109=CARTESIAN_POINT('Ctrl Pts',(-2.10214543967794,-5.85600149689041,
131.66746994883));
#151110=CARTESIAN_POINT('Ctrl Pts',(-2.11027222182508,-5.82587165323201,
131.837390163401));
#151111=CARTESIAN_POINT('Ctrl Pts',(-2.11841801499163,-5.79567132668976,
132.007707873122));
#151112=CARTESIAN_POINT('Ctrl Pts',(-2.12656380815816,-5.75803489747663,
132.176492521182));
#151113=CARTESIAN_POINT('Ctrl Pts',(-2.13470960132469,-5.71315404569664,
132.343126815739));
#151114=CARTESIAN_POINT('Ctrl Pts',(-2.14288381330348,-5.66811661487335,
132.510342459299));
#151115=CARTESIAN_POINT('Ctrl Pts',(-2.1510580252823,-5.61578424161571,
132.675392494474));
#151116=CARTESIAN_POINT('Ctrl Pts',(-2.15923223726111,-5.55639832036391,
132.83767521889));
#151117=CARTESIAN_POINT('Ctrl Pts',(-2.16518460664839,-5.51315415926175,
132.955847676786));
#151118=CARTESIAN_POINT('Ctrl Pts',(-2.17113697603566,-5.46617079334389,
133.07255319289));
#151119=CARTESIAN_POINT('Ctrl Pts',(-2.17708934542293,-5.41555669099828,
133.187567761119));
#151120=CARTESIAN_POINT('Ctrl Pts',(-2.18451261182834,-5.352435278139,133.331003714926));
#151121=CARTESIAN_POINT('Ctrl Pts',(-2.19193587823382,-5.28351593448006,
133.47214708612));
#151122=CARTESIAN_POINT('Ctrl Pts',(-2.19935914463929,-5.20898661212708,
133.610494797747));
#151123=CARTESIAN_POINT('Ctrl Pts',(-2.20677363736034,-5.13454537724375,
133.748678993869));
#151124=CARTESIAN_POINT('Ctrl Pts',(-2.21418813008139,-5.05450753708574,
133.884073782093));
#151125=CARTESIAN_POINT('Ctrl Pts',(-2.22160262280244,-4.96910921744193,
134.016195630084));
#151126=CARTESIAN_POINT('Ctrl Pts',(-2.22900996915625,-4.88379320791378,
134.148190134063));
#151127=CARTESIAN_POINT('Ctrl Pts',(-2.23641731551008,-4.79312720592667,
134.276917666559));
#151128=CARTESIAN_POINT('Ctrl Pts',(-2.2438246618639,-4.69739334041939,
134.401919007347));
#151129=CARTESIAN_POINT('Ctrl Pts',(-2.25122648353934,-4.60173087684083,
134.526827117419));
#151130=CARTESIAN_POINT('Ctrl Pts',(-2.25862830521476,-4.50100830184079,
134.648014274325));
#151131=CARTESIAN_POINT('Ctrl Pts',(-2.2660301268902,-4.39555109894441,
134.765050090255));
#151132=CARTESIAN_POINT('Ctrl Pts',(-2.27342804120158,-4.2901495660847,
134.882024123889));
#151133=CARTESIAN_POINT('Ctrl Pts',(-2.28082595551296,-4.18001863220431,
134.994850904326));
#151134=CARTESIAN_POINT('Ctrl Pts',(-2.28822386982435,-4.06552403703358,
135.103133101288));
#151135=CARTESIAN_POINT('Ctrl Pts',(-2.2956205547366,-3.95104846878726,
135.211397303713));
#151136=CARTESIAN_POINT('Ctrl Pts',(-2.30301723964884,-3.83221094943262,
135.315118165317));
#151137=CARTESIAN_POINT('Ctrl Pts',(-2.31041392456109,-3.70941413588868,
135.413935145759));
#151138=CARTESIAN_POINT('Ctrl Pts',(-2.31781028149657,-3.58662276728415,
135.512747744554));
#151139=CARTESIAN_POINT('Ctrl Pts',(-2.32520663843209,-3.45987274438713,
135.606656660505));
#151140=CARTESIAN_POINT('Ctrl Pts',(-2.33260299536758,-3.32959965183265,
135.69534177895));
#151141=CARTESIAN_POINT('Ctrl Pts',(-2.34000048470418,-3.19930661413532,
135.784040475314));
#151142=CARTESIAN_POINT('Ctrl Pts',(-2.34739797404077,-3.06548974138161,
135.867513571626));
#151143=CARTESIAN_POINT('Ctrl Pts',(-2.35479546337737,-2.92861329046739,
135.945484498333));
#151144=CARTESIAN_POINT('Ctrl Pts',(-2.36219554589239,-2.79168885772548,
136.023482757628));
#151145=CARTESIAN_POINT('Ctrl Pts',(-2.36959562840737,-2.65170303558292,
136.09597482248));
#151146=CARTESIAN_POINT('Ctrl Pts',(-2.37699571092239,-2.50914419699526,
136.162730328699));
#151147=CARTESIAN_POINT('Ctrl Pts',(-2.38440393058889,-2.36642860030897,
136.229559239459));
#151148=CARTESIAN_POINT('Ctrl Pts',(-2.39181215025541,-2.2211346751637,
136.29063883582));
#151149=CARTESIAN_POINT('Ctrl Pts',(-2.39922036992192,-2.07377094809798,
136.345786843487));
#151150=CARTESIAN_POINT('Ctrl Pts',(-2.40663314922402,-1.92631652111715,
136.400968793832));
#151151=CARTESIAN_POINT('Ctrl Pts',(-2.41404592852614,-1.77679010749687,
136.450211764322));
#151152=CARTESIAN_POINT('Ctrl Pts',(-2.42145870782824,-1.62571436210178,
136.493383677403));
#151153=CARTESIAN_POINT('Ctrl Pts',(-2.42888207885702,-1.47442275259691,
136.536617276538));
#151154=CARTESIAN_POINT('Ctrl Pts',(-2.43630544988579,-1.32157775172488,
136.573762405197));
#151155=CARTESIAN_POINT('Ctrl Pts',(-2.44372882091457,-1.16771195750656,
136.604738135176));
#151156=CARTESIAN_POINT('Ctrl Pts',(-2.44766487035497,-1.08612862146141,
136.621162210462));
#151157=CARTESIAN_POINT('Ctrl Pts',(-2.45160091979537,-1.00425839785975,
136.635852712559));
#151158=CARTESIAN_POINT('Ctrl Pts',(-2.45553696923577,-0.922181008006428,
136.6488035124));
#151159=CARTESIAN_POINT('Ctrl Pts',(-2.46296023564119,-0.767385612275549,
136.67322831672));
#151160=CARTESIAN_POINT('Ctrl Pts',(-2.47038350204662,-0.611385108007345,
136.691535960751));
#151161=CARTESIAN_POINT('Ctrl Pts',(-2.47780676845204,-0.454704340793631,
136.703612648541));
#151162=CARTESIAN_POINT('Ctrl Pts',(-2.48522126117303,-0.298208757235235,
136.715675062689));
#151163=CARTESIAN_POINT('Ctrl Pts',(-2.49263575389405,-0.141034879685641,
136.721521151211));
#151164=CARTESIAN_POINT('Ctrl Pts',(-2.50005024661505,0.0162828506506795,
136.721088212383));
#151165=CARTESIAN_POINT('Ctrl Pts',(-2.50745759296882,0.173448952235817,
136.720655690839));
#151166=CARTESIAN_POINT('Ctrl Pts',(-2.51486493932254,0.330758259790891,
136.713956191231));
#151167=CARTESIAN_POINT('Ctrl Pts',(-2.52227228567631,0.487671920753468,
136.70097885688));
#151168=CARTESIAN_POINT('Ctrl Pts',(-2.52967410735171,0.644468549587685,
136.688011201514));
#151169=CARTESIAN_POINT('Ctrl Pts',(-2.53707592902713,0.800869748963157,
136.668775065024));
#151170=CARTESIAN_POINT('Ctrl Pts',(-2.54447775070253,0.956337489631983,
136.643311650793));
#151171=CARTESIAN_POINT('Ctrl Pts',(-2.55187566501387,1.11172316009045,
136.617861678501));
#151172=CARTESIAN_POINT('Ctrl Pts',(-2.55927357932525,1.26617598575162,
136.586191035531));
#151173=CARTESIAN_POINT('Ctrl Pts',(-2.56667149363659,1.41916399014193,
136.548392662357));
#151174=CARTESIAN_POINT('Ctrl Pts',(-2.57406817854878,1.57212657070138,
136.510600570586));
#151175=CARTESIAN_POINT('Ctrl Pts',(-2.58146486346097,1.72362445107397,
136.46668285912));
#151176=CARTESIAN_POINT('Ctrl Pts',(-2.58886154837316,1.87313665256134,
136.416783413768));
#151177=CARTESIAN_POINT('Ctrl Pts',(-2.59625790530859,2.02264222452102,
136.36688618101));
#151178=CARTESIAN_POINT('Ctrl Pts',(-2.60365426224399,2.17016193856577,
136.311007859925));
#151179=CARTESIAN_POINT('Ctrl Pts',(-2.61105061917942,2.31519102902924,
136.249341890408));
#151180=CARTESIAN_POINT('Ctrl Pts',(-2.61844810851598,2.4602423238167,136.187666479674));
#151181=CARTESIAN_POINT('Ctrl Pts',(-2.62584559785254,2.60280189220714,
136.120201802237));
#151182=CARTESIAN_POINT('Ctrl Pts',(-2.6332430871891,2.74238610620907,136.047188957973));
#151183=CARTESIAN_POINT('Ctrl Pts',(-2.64064316970409,2.88201925124103,
135.974150519168));
#151184=CARTESIAN_POINT('Ctrl Pts',(-2.64804325221907,3.01867463469476,
135.895560214166));
#151185=CARTESIAN_POINT('Ctrl Pts',(-2.65544333473406,3.15189446714023,
135.811704407492));
#151186=CARTESIAN_POINT('Ctrl Pts',(-2.66285155440052,3.28526078848681,
135.727756392738));
#151187=CARTESIAN_POINT('Ctrl Pts',(-2.67025977406701,3.41518369831154,
135.638531512362));
#151188=CARTESIAN_POINT('Ctrl Pts',(-2.67766799373348,3.54123497307229,
135.544359080434));
#151189=CARTESIAN_POINT('Ctrl Pts',(-2.68508077303554,3.66736383028937,
135.450128686945));
#151190=CARTESIAN_POINT('Ctrl Pts',(-2.69249355233754,3.78961601494304,
135.350944908736));
#151191=CARTESIAN_POINT('Ctrl Pts',(-2.6999063316396,3.90759789872617,135.247176079002));
#151192=CARTESIAN_POINT('Ctrl Pts',(-2.70732970266834,4.02574836055765,
135.143258979497));
#151193=CARTESIAN_POINT('Ctrl Pts',(-2.71475307369716,4.13961606572169,
135.03474400083));
#151194=CARTESIAN_POINT('Ctrl Pts',(-2.7221764447259,4.24884504478696,134.922035489128));
#151195=CARTESIAN_POINT('Ctrl Pts',(-2.72611249416683,4.30676087040284,
134.862274731817));
#151196=CARTESIAN_POINT('Ctrl Pts',(-2.73004854360773,4.36337326153021,
134.801335569227));
#151197=CARTESIAN_POINT('Ctrl Pts',(-2.73398459304866,4.41863397029641,
134.739281760237));
#151198=CARTESIAN_POINT('Ctrl Pts',(-2.7414078594541,4.52285394239833,134.62225021312));
#151199=CARTESIAN_POINT('Ctrl Pts',(-2.74883112585958,4.62257876490229,
134.500898299503));
#151200=CARTESIAN_POINT('Ctrl Pts',(-2.75625439226502,4.71742900618905,
134.375606077355));
#151201=CARTESIAN_POINT('Ctrl Pts',(-2.76366888498604,4.81216714236757,
134.25046194021));
#151202=CARTESIAN_POINT('Ctrl Pts',(-2.77108337770697,4.90204194221244,
134.121387059276));
#151203=CARTESIAN_POINT('Ctrl Pts',(-2.778497870428,4.98671177446159,133.988797183263));
#151204=CARTESIAN_POINT('Ctrl Pts',(-2.78590521678178,5.07129999873854,
133.856335102364));
#151205=CARTESIAN_POINT('Ctrl Pts',(-2.7933125631356,5.15069304320606,133.720365083504));
#151206=CARTESIAN_POINT('Ctrl Pts',(-2.80071990948937,5.22459051085855,
133.581334610305));
#151207=CARTESIAN_POINT('Ctrl Pts',(-2.80812173116479,5.29843286299177,
133.442407831277));
#151208=CARTESIAN_POINT('Ctrl Pts',(-2.81552355284021,5.36678762514084,
133.300425471088));
#151209=CARTESIAN_POINT('Ctrl Pts',(-2.82292537451562,5.42939864492969,
133.155862460418));
#151210=CARTESIAN_POINT('Ctrl Pts',(-2.83032328882698,5.49197661284856,
133.011375763436));
#151211=CARTESIAN_POINT('Ctrl Pts',(-2.83772120313832,5.54881672894887,
132.864311470751));
#151212=CARTESIAN_POINT('Ctrl Pts',(-2.84511911744968,5.59970964040452,
132.715167385835));
#151213=CARTESIAN_POINT('Ctrl Pts',(-2.85251580236189,5.6505940943815,132.566048085959));
#151214=CARTESIAN_POINT('Ctrl Pts',(-2.85991248727416,5.69553318479359,
132.414850032761));
#151215=CARTESIAN_POINT('Ctrl Pts',(-2.86730917218637,5.73436636513568,
132.262089314169));
#151216=CARTESIAN_POINT('Ctrl Pts',(-2.87470552912181,5.77319782357385,
132.109335369148));
#151217=CARTESIAN_POINT('Ctrl Pts',(-2.88210188605724,5.80592381829896,
131.955019258296));
#151218=CARTESIAN_POINT('Ctrl Pts',(-2.88949824299269,5.83243425760153,
131.799670214252));
#151219=CARTESIAN_POINT('Ctrl Pts',(-2.89689573232926,5.85894875572004,
131.644297385874));
#151220=CARTESIAN_POINT('Ctrl Pts',(-2.90429322166587,5.87924574081938,
131.487891677419));
#151221=CARTESIAN_POINT('Ctrl Pts',(-2.91169071100245,5.89326664431007,
131.330990299185));
#151222=CARTESIAN_POINT('Ctrl Pts',(-2.91909079351746,5.90729246280676,
131.174033919417));
#151223=CARTESIAN_POINT('Ctrl Pts',(-2.92649087603246,5.91503778616497,
131.016581895506));
#151224=CARTESIAN_POINT('Ctrl Pts',(-2.93389095854747,5.91649609460213,
130.859174165688));
#151225=CARTESIAN_POINT('Ctrl Pts',(-2.94129917821394,5.91795600659933,
130.70159334989));
#151226=CARTESIAN_POINT('Ctrl Pts',(-2.94870739788036,5.91311509406243,
130.544057298964));
#151227=CARTESIAN_POINT('Ctrl Pts',(-2.95611561754683,5.90201895296102,
130.387104291803));
#151228=CARTESIAN_POINT('Ctrl Pts',(-2.9635283968489,5.8909159823699,130.230054682686));
#151229=CARTESIAN_POINT('Ctrl Pts',(-2.97094117615101,5.87355015271227,
130.073589202554));
#151230=CARTESIAN_POINT('Ctrl Pts',(-2.97835395545309,5.85001858742294,
129.91823811514));
#151231=CARTESIAN_POINT('Ctrl Pts',(-2.98577732648185,5.82645339912962,
129.762665054807));
#151232=CARTESIAN_POINT('Ctrl Pts',(-2.99320069751052,5.79670495028728,
129.608209932956));
#151233=CARTESIAN_POINT('Ctrl Pts',(-3.00062406853928,5.7609210185715,129.455390795709));
#151234=CARTESIAN_POINT('Ctrl Pts',(-3.00456011798005,5.74194751935226,
129.374362422296));
#151235=CARTESIAN_POINT('Ctrl Pts',(-3.00849616742082,5.72127805621818,
129.293793708396));
#151236=CARTESIAN_POINT('Ctrl Pts',(-3.01243221686158,5.69894019216676,
129.213759709542));
#151237=CARTESIAN_POINT('Ctrl Pts',(-3.01985548326705,5.65681167770635,
129.062818085478));
#151238=CARTESIAN_POINT('Ctrl Pts',(-3.0272787496725,5.60861857839295,128.913323094456));
#151239=CARTESIAN_POINT('Ctrl Pts',(-3.03470201607794,5.5544755557017,128.76579939366));
#151240=CARTESIAN_POINT('Ctrl Pts',(-3.04211650879897,5.50039652556691,
128.618450053627));
#151241=CARTESIAN_POINT('Ctrl Pts',(-3.04953100151999,5.44038169727705,
128.473067713157));
#151242=CARTESIAN_POINT('Ctrl Pts',(-3.05694549424101,5.37459619195267,
128.330164518639));
#151243=CARTESIAN_POINT('Ctrl Pts',(-3.06435284059479,5.30887409317512,
128.187399059599));
#151244=CARTESIAN_POINT('Ctrl Pts',(-3.07176018694859,5.23739254525498,
128.047108326315));
#151245=CARTESIAN_POINT('Ctrl Pts',(-3.07916753330238,5.16036565691642,
127.909786927121));
#151246=CARTESIAN_POINT('Ctrl Pts',(-3.0865693549778,5.08339621813723,127.772567947407));
#151247=CARTESIAN_POINT('Ctrl Pts',(-3.09397117665318,5.00088985596024,
127.63831421631));
#151248=CARTESIAN_POINT('Ctrl Pts',(-3.1013729983286,4.91310768640109,127.50749795371));
#151249=CARTESIAN_POINT('Ctrl Pts',(-3.10877091263997,4.82537185636597,
127.376750747997));
#151250=CARTESIAN_POINT('Ctrl Pts',(-3.11616882695138,4.73236597300262,
127.249437706085));
#151251=CARTESIAN_POINT('Ctrl Pts',(-3.12356674126275,4.63439569215218,
127.126004037371));
#151252=CARTESIAN_POINT('Ctrl Pts',(-3.13096342617496,4.5364416921852,127.002590881094));
#151253=CARTESIAN_POINT('Ctrl Pts',(-3.13836011108717,4.43352516394429,
126.883056110618));
#151254=CARTESIAN_POINT('Ctrl Pts',(-3.14575679599938,4.32599352751265,
126.767813756396));
#151255=CARTESIAN_POINT('Ctrl Pts',(-3.15315315293482,4.21846665914646,
126.652576512142));
#151256=CARTESIAN_POINT('Ctrl Pts',(-3.16054950987033,4.10632534415289,
126.541631578635));
#151257=CARTESIAN_POINT('Ctrl Pts',(-3.16794586680578,3.98995533368209,
126.435357642318));
#151258=CARTESIAN_POINT('Ctrl Pts',(-3.17534335614237,3.87356750666544,
126.329067435191));
#151259=CARTESIAN_POINT('Ctrl Pts',(-3.18274084547889,3.75294997072971,
126.227449900944));
#151260=CARTESIAN_POINT('Ctrl Pts',(-3.19013833481549,3.62852303835991,
126.13084469028));
#151261=CARTESIAN_POINT('Ctrl Pts',(-3.1975384173305,3.50405248832185,126.03420561481));
#151262=CARTESIAN_POINT('Ctrl Pts',(-3.20493849984549,3.37577017779809,
125.942582590007));
#151263=CARTESIAN_POINT('Ctrl Pts',(-3.2123385823605,3.24412684801521,125.856272950953));
#151264=CARTESIAN_POINT('Ctrl Pts',(-3.21974680202699,3.11233876285798,
125.769868405579));
#151265=CARTESIAN_POINT('Ctrl Pts',(-3.22715502169347,2.97718259008883,
125.68878911884));
#151266=CARTESIAN_POINT('Ctrl Pts',(-3.23456324135995,2.83913584472054,
125.613287682447));
#151267=CARTESIAN_POINT('Ctrl Pts',(-3.24197602066203,2.70100413388391,
125.53773977618));
#151268=CARTESIAN_POINT('Ctrl Pts',(-3.24938879996411,2.55997863900215,
125.467776726604));
#151269=CARTESIAN_POINT('Ctrl Pts',(-3.25680157926618,2.41655798356017,
125.403603441522));
#151270=CARTESIAN_POINT('Ctrl Pts',(-3.26422495029494,2.27293240195994,
125.339338462641));
#151271=CARTESIAN_POINT('Ctrl Pts',(-3.27164832132375,2.12690517030463,
125.280879909035));
#151272=CARTESIAN_POINT('Ctrl Pts',(-3.27907169235252,1.97899201291219,
125.228383467745));
#151273=CARTESIAN_POINT('Ctrl Pts',(-3.28300774179317,1.90056490773808,
125.200548594938));
#151274=CARTESIAN_POINT('Ctrl Pts',(-3.28694379123385,1.82160781720802,
125.1743890418));
#151275=CARTESIAN_POINT('Ctrl Pts',(-3.29087984067451,1.74219878614146,
125.149922188149));
#151276=CARTESIAN_POINT('Ctrl Pts',(-3.29830310707993,1.59243583181593,
125.103778465746));
#151277=CARTESIAN_POINT('Ctrl Pts',(-3.30572637348536,1.44061191459084,
125.063518990832));
#151278=CARTESIAN_POINT('Ctrl Pts',(-3.31314963989078,1.28723042074159,
125.029330885485));
#151279=CARTESIAN_POINT('Ctrl Pts',(-3.32056413261178,1.13403021108032,
124.99518318764));
#151280=CARTESIAN_POINT('Ctrl Pts',(-3.32797862533272,0.979276449967203,
124.967092656203));
#151281=CARTESIAN_POINT('Ctrl Pts',(-3.33539311805373,0.823489272662264,
124.945197197733));
#151282=CARTESIAN_POINT('Ctrl Pts',(-3.3428004644075,0.667852248904096,
124.92332284293));
#151283=CARTESIAN_POINT('Ctrl Pts',(-3.35020781076128,0.511184159067502,
124.907631725526));
#151284=CARTESIAN_POINT('Ctrl Pts',(-3.35761515711505,0.354016862148698,
124.898211057674));
#151285=CARTESIAN_POINT('Ctrl Pts',(-3.36501697879046,0.196966786529296,
124.888797416111));
#151286=CARTESIAN_POINT('Ctrl Pts',(-3.37241880046591,0.0394186162072712,
124.885644934324));
#151287=CARTESIAN_POINT('Ctrl Pts',(-3.37982062214132,-0.11808921727217,
124.888789174395));
#151288=CARTESIAN_POINT('Ctrl Pts',(-3.38721853645269,-0.275513903592357,
124.891931754645));
#151289=CARTESIAN_POINT('Ctrl Pts',(-3.39461645076402,-0.432897923198201,
124.901364429435));
#151290=CARTESIAN_POINT('Ctrl Pts',(-3.40201436507539,-0.589701494367243,
124.917070688402));
#151291=CARTESIAN_POINT('Ctrl Pts',(-3.40941104998759,-0.746479007627239,
124.932774337273));
#151292=CARTESIAN_POINT('Ctrl Pts',(-3.41680773489981,-0.902675892819454,
124.954749463988));
#151293=CARTESIAN_POINT('Ctrl Pts',(-3.42420441981201,-1.05775602535642,
124.982927567764));
#151294=CARTESIAN_POINT('Ctrl Pts',(-3.43160077674746,-1.2128292814778,
125.011104422094));
#151295=CARTESIAN_POINT('Ctrl Pts',(-3.43899713368289,-1.36678551611854,
125.045483639864));
#151296=CARTESIAN_POINT('Ctrl Pts',(-3.44639349061833,-1.51909762173092,
125.085945366979));
#151297=CARTESIAN_POINT('Ctrl Pts',(-3.4537909799549,-1.67143304671528,
125.126413288887));
#151298=CARTESIAN_POINT('Ctrl Pts',(-3.46118846929145,-1.82212348065478,
125.172965478529));
#151299=CARTESIAN_POINT('Ctrl Pts',(-3.46858595862801,-1.97065597663022,
125.225431904608));
#151300=CARTESIAN_POINT('Ctrl Pts',(-3.475986041143,-2.11924054044208,125.277916722711));
#151301=CARTESIAN_POINT('Ctrl Pts',(-3.48338612365803,-2.26566530841536,
125.336319780775));
#151302=CARTESIAN_POINT('Ctrl Pts',(-3.49078620617303,-2.40943648748165,
125.400422574315));
#151303=CARTESIAN_POINT('Ctrl Pts',(-3.49819442583949,-2.55336575773936,
125.464595855467));
#151304=CARTESIAN_POINT('Ctrl Pts',(-3.50560264550593,-2.69463527071165,
125.534481236485));
#151305=CARTESIAN_POINT('Ctrl Pts',(-3.51301086517239,-2.83277440531145,
125.609813502455));
#151306=CARTESIAN_POINT('Ctrl Pts',(-3.52042364447445,-2.97099856224363,
125.685192134177));
#151307=CARTESIAN_POINT('Ctrl Pts',(-3.52783642377653,-3.1060881820313,
125.766024139831));
#151308=CARTESIAN_POINT('Ctrl Pts',(-3.53524920307859,-3.23760135176302,
125.852000771032));
#151309=CARTESIAN_POINT('Ctrl Pts',(-3.54267257410736,-3.36930243367918,
125.938100249675));
#151310=CARTESIAN_POINT('Ctrl Pts',(-3.55009594513606,-3.49741655608301,
126.029358819219));
#151311=CARTESIAN_POINT('Ctrl Pts',(-3.55751931616481,-3.62153397346784,
126.125426738837));
#151312=CARTESIAN_POINT('Ctrl Pts',(-3.56145536560567,-3.68734400632288,
126.176364254937));
#151313=CARTESIAN_POINT('Ctrl Pts',(-3.56539141504655,-3.75203101532407,
126.22865321393));
#151314=CARTESIAN_POINT('Ctrl Pts',(-3.5693274644874,-3.81553819320636,
126.282237348715));
#151315=CARTESIAN_POINT('Ctrl Pts',(-3.57664552322221,-3.93361324912388,
126.381863090592));
#151316=CARTESIAN_POINT('Ctrl Pts',(-3.58396358195698,-4.04798671406309,
126.486287983218));
#151317=CARTESIAN_POINT('Ctrl Pts',(-3.59128164069176,-4.15823522630859,
126.595202701167));
#151318=CARTESIAN_POINT('Ctrl Pts',(-3.59859099504814,-4.26835260476512,
126.703987871793));
#151319=CARTESIAN_POINT('Ctrl Pts',(-3.6059003494045,-4.37435452104216,
126.817251975381));
#151320=CARTESIAN_POINT('Ctrl Pts',(-3.61320970376087,-4.47584943989803,
126.934644561592));
#151321=CARTESIAN_POINT('Ctrl Pts',(-3.62051206677417,-4.57724727961884,
127.051924862667));
#151322=CARTESIAN_POINT('Ctrl Pts',(-3.62781442978749,-4.67414645020482,
127.173325499512));
#151323=CARTESIAN_POINT('Ctrl Pts',(-3.63511679280077,-4.76619136037824,
127.29845838294));
#151324=CARTESIAN_POINT('Ctrl Pts',(-3.64247129342525,-4.85889345531905,
127.424484693552));
#151325=CARTESIAN_POINT('Ctrl Pts',(-3.64982579404971,-4.94667140748425,
127.554296489972));
#151326=CARTESIAN_POINT('Ctrl Pts',(-3.65718029467419,-5.02920194550765,
127.687461781575));
#151327=CARTESIAN_POINT('Ctrl Pts',(-3.66447414910763,-5.11105192572958,
127.819528974459));
#151328=CARTESIAN_POINT('Ctrl Pts',(-3.67176800354105,-5.18774050561212,
127.954894228281));
#151329=CARTESIAN_POINT('Ctrl Pts',(-3.67906185797449,-5.25899503833872,
128.093105972715));
#151330=CARTESIAN_POINT('Ctrl Pts',(-3.68635426495622,-5.33023543073724,
128.231290289287));
#151331=CARTESIAN_POINT('Ctrl Pts',(-3.69364667193797,-5.39604374529136,
128.372319630748));
#151332=CARTESIAN_POINT('Ctrl Pts',(-3.7009390789197,-5.45619311560956,
128.51571751571));
#151333=CARTESIAN_POINT('Ctrl Pts',(-3.70823157369812,-5.5163432100941,
128.659117127105));
#151334=CARTESIAN_POINT('Ctrl Pts',(-3.71552406847653,-5.57083407676291,
128.804884983558));
#151335=CARTESIAN_POINT('Ctrl Pts',(-3.72281656325495,-5.61948697861811,
128.952524593605));
#151336=CARTESIAN_POINT('Ctrl Pts',(-3.73021725029939,-5.66886170035249,
129.102354601375));
#151337=CARTESIAN_POINT('Ctrl Pts',(-3.73761793734379,-5.71222370981426,
129.254111961045));
#151338=CARTESIAN_POINT('Ctrl Pts',(-3.74501862438822,-5.74943886994097,
129.407262466643));
#151339=CARTESIAN_POINT('Ctrl Pts',(-3.75231896663071,-5.7861494353118,
129.558336427582));
#151340=CARTESIAN_POINT('Ctrl Pts',(-3.75961930887324,-5.81687876911714,
129.710765601758));
#151341=CARTESIAN_POINT('Ctrl Pts',(-3.76691965111573,-5.84154993401416,
129.864028266257));
#151342=CARTESIAN_POINT('Ctrl Pts',(-3.77437051056114,-5.86672976475309,
130.020450874058));
#151343=CARTESIAN_POINT('Ctrl Pts',(-3.7818213700065,-5.88559883849026,
130.177741294122));
#151344=CARTESIAN_POINT('Ctrl Pts',(-3.78927222945191,-5.89813120227993,
130.335341552717));
#151345=CARTESIAN_POINT('Ctrl Pts',(-3.79672308889732,-5.9106635660696,
130.492941811312));
#151346=CARTESIAN_POINT('Ctrl Pts',(-3.80417394834277,-5.91685925896518,
130.650851486073));
#151347=CARTESIAN_POINT('Ctrl Pts',(-3.81162480778818,-5.91674854110931,
130.808515588187));
#151348=CARTESIAN_POINT('',(-5.56162480778817,-5.92133943401158,130.799680554466));
#151349=CARTESIAN_POINT('Ctrl Pts',(-3.81162480778818,-5.92269048599951,
130.808519760851));
#151350=CARTESIAN_POINT('Ctrl Pts',(-3.82367490129221,-5.92472695610432,
131.063763701174));
#151351=CARTESIAN_POINT('Ctrl Pts',(-3.92854086940023,-5.79362457393622,
133.282917976605));
#151352=CARTESIAN_POINT('Ctrl Pts',(-4.1262227121134,-2.98891128428301,
137.132391106201));
#151353=CARTESIAN_POINT('Ctrl Pts',(-4.40467033592598,3.70837171184995,
136.739471381239));
#151354=CARTESIAN_POINT('Ctrl Pts',(-4.68311795973906,6.997842268822,130.892474810749));
#151355=CARTESIAN_POINT('Ctrl Pts',(-4.96156558355173,3.85663764434708,
124.96450560134));
#151356=CARTESIAN_POINT('Ctrl Pts',(-5.24001320736476,-2.82862856805823,
124.403077859063));
#151357=CARTESIAN_POINT('Ctrl Pts',(-5.44003294877681,-5.76368543459087,
128.225386373625));
#151358=CARTESIAN_POINT('Ctrl Pts',(-5.54723681558465,-5.92398027789449,
130.494734343713));
#151359=CARTESIAN_POINT('Ctrl Pts',(-5.56162480778817,-5.92133943401158,
130.799680554466));
#151360=CARTESIAN_POINT('',(-7.31162406064559,-5.91165886957557,130.802412404394));
#151361=CARTESIAN_POINT('Ctrl Pts',(-5.56162480778817,-5.92133943401158,
130.799680554466));
#151362=CARTESIAN_POINT('Ctrl Pts',(-5.64005269018895,-5.90694438913263,
132.4619198174));
#151363=CARTESIAN_POINT('Ctrl Pts',(-5.811296447194,-4.3084791224879,136.1155826924));
#151364=CARTESIAN_POINT('Ctrl Pts',(-6.0753560788034,1.89163637866986,137.542258831492));
#151365=CARTESIAN_POINT('Ctrl Pts',(-6.3538037026163,6.6912602630285,132.854871925206));
#151366=CARTESIAN_POINT('Ctrl Pts',(-6.63225132642916,5.34194285190056,
126.283165300243));
#151367=CARTESIAN_POINT('Ctrl Pts',(-6.91069895024212,-0.916359071709015,
123.86621629923));
#151368=CARTESIAN_POINT('Ctrl Pts',(-7.13715632573601,-5.32128556064457,
127.085904605724));
#151369=CARTESIAN_POINT('Ctrl Pts',(-7.27079782662573,-5.91005140945893,
129.93196890033));
#151370=CARTESIAN_POINT('Ctrl Pts',(-7.31162345291109,-5.90751794173804,
130.80240080057));
#151371=CARTESIAN_POINT('',(-9.06162556537631,-5.91501731293399,130.809728729937));
#151372=CARTESIAN_POINT('Ctrl Pts',(-7.31162480778818,-5.91674968393517,
130.802426670017));
#151373=CARTESIAN_POINT('Ctrl Pts',(-7.31920618702081,-5.91680260022219,
130.964319594534));
#151374=CARTESIAN_POINT('Ctrl Pts',(-7.32678756625346,-5.91020663906297,
131.126157705063));
#151375=CARTESIAN_POINT('Ctrl Pts',(-7.33436894548609,-5.89700160063828,
131.287374783579));
#151376=CARTESIAN_POINT('Ctrl Pts',(-7.34195464930973,-5.88378902975958,
131.448683823981));
#151377=CARTESIAN_POINT('Ctrl Pts',(-7.34954035313338,-5.86395989318124,
131.60937078082));
#151378=CARTESIAN_POINT('Ctrl Pts',(-7.35712605695701,-5.83760574229044,
131.768875915567));
#151379=CARTESIAN_POINT('Ctrl Pts',(-7.36471724504278,-5.81123253804941,
131.928496368285));
#151380=CARTESIAN_POINT('Ctrl Pts',(-7.37230843312853,-5.77832497003735,
132.086932953921));
#151381=CARTESIAN_POINT('Ctrl Pts',(-7.37989962121429,-5.73902546356901,
132.243637273045));
#151382=CARTESIAN_POINT('Ctrl Pts',(-7.3875031414854,-5.6996621134978,132.400596164534));
#151383=CARTESIAN_POINT('Ctrl Pts',(-7.39510666175654,-5.65388615734692,
132.555816829051));
#151384=CARTESIAN_POINT('Ctrl Pts',(-7.40271018202765,-5.60189000088908,
132.708765768903));
#151385=CARTESIAN_POINT('Ctrl Pts',(-7.41032018911973,-5.54984948474697,
132.861845194682));
#151386=CARTESIAN_POINT('Ctrl Pts',(-7.41793019621185,-5.49157830818657,
133.012648707527));
#151387=CARTESIAN_POINT('Ctrl Pts',(-7.42554020330394,-5.42731662350922,
133.160663830372));
#151388=CARTESIAN_POINT('Ctrl Pts',(-7.43316447032582,-5.36293452276646,
133.30895630976));
#151389=CARTESIAN_POINT('Ctrl Pts',(-7.44078873734768,-5.2925396253266,
133.45444964239));
#151390=CARTESIAN_POINT('Ctrl Pts',(-7.44841300436957,-5.21641829709212,
133.596655500322));
#151391=CARTESIAN_POINT('Ctrl Pts',(-7.45480673553567,-5.15258274315095,
133.715909721514));
#151392=CARTESIAN_POINT('Ctrl Pts',(-7.46120046670169,-5.08472090197207,
133.832852405316));
#151393=CARTESIAN_POINT('Ctrl Pts',(-7.46759419786778,-5.01302437116272,
133.947212382545));
#151394=CARTESIAN_POINT('Ctrl Pts',(-7.47501746427324,-4.92978307829047,
134.079986901058));
#151395=CARTESIAN_POINT('Ctrl Pts',(-7.48244073067869,-4.84113729034282,
134.209652823494));
#151396=CARTESIAN_POINT('Ctrl Pts',(-7.48986399708411,-4.7473458793924,
134.33573962072));
#151397=CARTESIAN_POINT('Ctrl Pts',(-7.49727848980512,-4.65366532210083,
134.461677393822));
#151398=CARTESIAN_POINT('Ctrl Pts',(-7.50469298252618,-4.55485146808713,
134.584044165415));
#151399=CARTESIAN_POINT('Ctrl Pts',(-7.51210747524718,-4.45120802225076,
134.702395725816));
#151400=CARTESIAN_POINT('Ctrl Pts',(-7.51951482160097,-4.34766447186931,
134.820633214528));
#151401=CARTESIAN_POINT('Ctrl Pts',(-7.52692216795465,-4.23930084102183,
134.934862917531));
#151402=CARTESIAN_POINT('Ctrl Pts',(-7.53432951430844,-4.12646282892634,
135.044671347217));
#151403=CARTESIAN_POINT('Ctrl Pts',(-7.54173133598383,-4.01370897567789,
135.154397877632));
#151404=CARTESIAN_POINT('Ctrl Pts',(-7.54913315765924,-3.89648765229909,
135.259709441377));
#151405=CARTESIAN_POINT('Ctrl Pts',(-7.55653497933463,-3.77518327665619,
135.360227361683));
#151406=CARTESIAN_POINT('Ctrl Pts',(-7.56393289364595,-3.6539429366493,
135.460692219362));
#151407=CARTESIAN_POINT('Ctrl Pts',(-7.57133080795728,-3.52862412369346,
135.556368235688));
#151408=CARTESIAN_POINT('Ctrl Pts',(-7.57872872226861,-3.39964629634104,
135.646915276243));
#151409=CARTESIAN_POINT('Ctrl Pts',(-7.58612540718083,-3.27068990276289,
135.737447269523));
#151410=CARTESIAN_POINT('Ctrl Pts',(-7.59352209209302,-3.13807600683679,
135.8228517644));
#151411=CARTESIAN_POINT('Ctrl Pts',(-7.60091877700523,-3.00225526314517,
135.902830377937));
#151412=CARTESIAN_POINT('Ctrl Pts',(-7.60831513394069,-2.86644054188765,
135.982805445138));
#151413=CARTESIAN_POINT('Ctrl Pts',(-7.6157114908761,-2.72741957726719,
136.057354919954));
#151414=CARTESIAN_POINT('Ctrl Pts',(-7.62310784781155,-2.58566974565933,
136.126225190146));
#151415=CARTESIAN_POINT('Ctrl Pts',(-7.63050533714813,-2.44389821179039,
136.195106004553));
#151416=CARTESIAN_POINT('Ctrl Pts',(-7.63790282648476,-2.29939731483277,
136.258305719899));
#151417=CARTESIAN_POINT('Ctrl Pts',(-7.64530031582134,-2.15266649036484,
136.315617964466));
#151418=CARTESIAN_POINT('Ctrl Pts',(-7.65270039833633,-2.00588422963427,
136.372950299751));
#151419=CARTESIAN_POINT('Ctrl Pts',(-7.66010048085135,-1.85687083253691,
136.424390919428));
#151420=CARTESIAN_POINT('Ctrl Pts',(-7.66750056336633,-1.70614290023417,
136.469782664199));
#151421=CARTESIAN_POINT('Ctrl Pts',(-7.67490878303281,-1.55524922707422,
136.515224321861));
#151422=CARTESIAN_POINT('Ctrl Pts',(-7.68231700269922,-1.40263761128612,
136.554603713706));
#151423=CARTESIAN_POINT('Ctrl Pts',(-7.68972522236569,-1.24883762586639,
136.587814183276));
#151424=CARTESIAN_POINT('Ctrl Pts',(-7.69713800166776,-1.09494297912192,
136.621045093335));
#151425=CARTESIAN_POINT('Ctrl Pts',(-7.70455078096983,-0.939858872187931,
136.648099451377));
#151426=CARTESIAN_POINT('Ctrl Pts',(-7.7119635602719,-0.784121582926229,
136.668922315228));
#151427=CARTESIAN_POINT('Ctrl Pts',(-7.71938693130066,-0.628161768922276,
136.689774931764));
#151428=CARTESIAN_POINT('Ctrl Pts',(-7.72681030232945,-0.471547279287036,
136.704378236555));
#151429=CARTESIAN_POINT('Ctrl Pts',(-7.7342336733582,-0.314816817708669,
136.712729337762));
#151430=CARTESIAN_POINT('Ctrl Pts',(-7.73816972279904,-0.231714566283128,
136.717157292004));
#151431=CARTESIAN_POINT('Ctrl Pts',(-7.74210577223987,-0.148579678551725,
136.719828398119));
#151432=CARTESIAN_POINT('Ctrl Pts',(-7.74604182168071,-0.0654919224773062,
136.720748144646));
#151433=CARTESIAN_POINT('Ctrl Pts',(-7.75346508808615,0.091208992397516,
136.722482757892));
#151434=CARTESIAN_POINT('Ctrl Pts',(-7.76088835449162,0.2482158189521,136.717990144255));
#151435=CARTESIAN_POINT('Ctrl Pts',(-7.76831162089707,0.40499276102326,
136.707233767653));
#151436=CARTESIAN_POINT('Ctrl Pts',(-7.77572611361809,0.56158440576863,
136.696490104195));
#151437=CARTESIAN_POINT('Ctrl Pts',(-7.78314060633911,0.717946338073995,
136.67949743928));
#151438=CARTESIAN_POINT('Ctrl Pts',(-7.79055509906013,0.873540671836888,
136.656271182257));
#151439=CARTESIAN_POINT('Ctrl Pts',(-7.7979624454139,1.02898503792266,136.633067311576));
#151440=CARTESIAN_POINT('Ctrl Pts',(-7.80536979176764,1.18366291161396,
136.603641864615));
#151441=CARTESIAN_POINT('Ctrl Pts',(-7.81277713812142,1.33703955520385,
136.568062187766));
#151442=CARTESIAN_POINT('Ctrl Pts',(-7.82017895979682,1.49030180470616,
136.532509047581));
#151443=CARTESIAN_POINT('Ctrl Pts',(-7.82758078147224,1.64226439443974,
136.490810900925));
#151444=CARTESIAN_POINT('Ctrl Pts',(-7.83498260314764,1.79240094566833,
136.44308648539));
#151445=CARTESIAN_POINT('Ctrl Pts',(-7.84238051745899,1.94245824098018,
136.395387263203));
#151446=CARTESIAN_POINT('Ctrl Pts',(-7.84977843177032,2.09069106268633,
136.341668220491));
#151447=CARTESIAN_POINT('Ctrl Pts',(-7.85717634608167,2.23658651847378,
136.282098408651));
#151448=CARTESIAN_POINT('Ctrl Pts',(-7.86457303099389,2.38245772908351,
136.222538496234));
#151449=CARTESIAN_POINT('Ctrl Pts',(-7.87196971590612,2.52599199942731,
136.157129885372));
#151450=CARTESIAN_POINT('Ctrl Pts',(-7.87936640081833,2.66669470167901,
136.086090441264));
#151451=CARTESIAN_POINT('Ctrl Pts',(-7.88676275775377,2.80739116502525,
136.015054147119));
#151452=CARTESIAN_POINT('Ctrl Pts',(-7.89415911468924,2.94525597669146,
135.938387684415));
#151453=CARTESIAN_POINT('Ctrl Pts',(-7.90155547162468,3.07981773192763,
135.856355599809));
#151454=CARTESIAN_POINT('Ctrl Pts',(-7.90895296096127,3.21440008891243,
135.77431095588));
#151455=CARTESIAN_POINT('Ctrl Pts',(-7.91635045029784,3.34567806377901,
135.686899248675));
#151456=CARTESIAN_POINT('Ctrl Pts',(-7.92374793963444,3.47320807302478,
135.594429118535));
#151457=CARTESIAN_POINT('Ctrl Pts',(-7.93114802214946,3.60078278771778,
135.501926573134));
#151458=CARTESIAN_POINT('Ctrl Pts',(-7.93854810466452,3.724606618912,135.404362293319));
#151459=CARTESIAN_POINT('Ctrl Pts',(-7.94594818717954,3.84426810849415,
135.302085961839));
#151460=CARTESIAN_POINT('Ctrl Pts',(-7.95335640684601,3.96406117818525,
135.199697167019));
#151461=CARTESIAN_POINT('Ctrl Pts',(-7.96076462651248,4.07968248190624,
135.092586215658));
#151462=CARTESIAN_POINT('Ctrl Pts',(-7.96817284617896,4.19075603941705,
134.981141002095));
#151463=CARTESIAN_POINT('Ctrl Pts',(-7.97558562548104,4.30189796084931,
134.869627195863));
#151464=CARTESIAN_POINT('Ctrl Pts',(-7.982998404783,4.40848630642737,134.753774085851));
#151465=CARTESIAN_POINT('Ctrl Pts',(-7.99041118408508,4.51018498046012,
134.634003160223));
#151466=CARTESIAN_POINT('Ctrl Pts',(-7.99783455511383,4.61202896632739,
134.514061100281));
#151467=CARTESIAN_POINT('Ctrl Pts',(-8.00525792614263,4.70896909740414,
134.390190337543));
#151468=CARTESIAN_POINT('Ctrl Pts',(-8.01268129717138,4.80071175820258,
134.262842535569));
#151469=CARTESIAN_POINT('Ctrl Pts',(-8.01661734661211,4.84935591829206,
134.195319675295));
#151470=CARTESIAN_POINT('Ctrl Pts',(-8.02055339605287,4.89653963301674,
134.126819737847));
#151471=CARTESIAN_POINT('Ctrl Pts',(-8.0244894454936,4.94222440350663,134.05741280096));
#151472=CARTESIAN_POINT('Ctrl Pts',(-8.03191271189902,5.02838445487897,
133.926513484105));
#151473=CARTESIAN_POINT('Ctrl Pts',(-8.03933597830439,5.10947071664635,
133.791990826852));
#151474=CARTESIAN_POINT('Ctrl Pts',(-8.04675924470982,5.18516283905393,
133.654275861042));
#151475=CARTESIAN_POINT('Ctrl Pts',(-8.05417373743083,5.26076549965877,
133.516723662884));
#151476=CARTESIAN_POINT('Ctrl Pts',(-8.06158823015184,5.33098653317177,
133.375986990381));
#151477=CARTESIAN_POINT('Ctrl Pts',(-8.06900272287285,5.39554816333842,
133.232526711472));
#151478=CARTESIAN_POINT('Ctrl Pts',(-8.07641006922662,5.46004756657512,
133.089204704982));
#151479=CARTESIAN_POINT('Ctrl Pts',(-8.08381741558041,5.51889827362221,
132.943164656302));
#151480=CARTESIAN_POINT('Ctrl Pts',(-8.09122476193417,5.57186790611307,
132.794892857779));
#151481=CARTESIAN_POINT('Ctrl Pts',(-8.09862658360956,5.62479803185367,
132.646731645957));
#151482=CARTESIAN_POINT('Ctrl Pts',(-8.10602840528499,5.671855691762,132.496342348608));
#151483=CARTESIAN_POINT('Ctrl Pts',(-8.11343022696039,5.71285626257538,
132.344232003641));
#151484=CARTESIAN_POINT('Ctrl Pts',(-8.12082814127174,5.75383518950658,
132.192201956542));
#151485=CARTESIAN_POINT('Ctrl Pts',(-8.12822605558308,5.78876329839053,
132.038453030722));
#151486=CARTESIAN_POINT('Ctrl Pts',(-8.13562396989443,5.8175055861331,131.883508113421));
#151487=CARTESIAN_POINT('Ctrl Pts',(-8.14302065480663,5.84624309742888,
131.728588945155));
#151488=CARTESIAN_POINT('Ctrl Pts',(-8.15041733971876,5.86879675978339,
131.572474546548));
#151489=CARTESIAN_POINT('Ctrl Pts',(-8.15781402463097,5.88508251093504,
131.415698823461));
#151490=CARTESIAN_POINT('Ctrl Pts',(-8.16521038156641,5.90136753995942,
131.258930051973));
#151491=CARTESIAN_POINT('Ctrl Pts',(-8.17260673850193,5.91138517182087,
131.10150038561));
#151492=CARTESIAN_POINT('Ctrl Pts',(-8.18000309543737,5.91510317133079,
130.943949424468));
#151493=CARTESIAN_POINT('Ctrl Pts',(-8.18740058477395,5.91882174007594,
130.786374341872));
#151494=CARTESIAN_POINT('Ctrl Pts',(-8.19479807411057,5.9162387472346,130.628678300737));
#151495=CARTESIAN_POINT('Ctrl Pts',(-8.20219556344716,5.90737409294855,
130.471401328072));
#151496=CARTESIAN_POINT('Ctrl Pts',(-8.20959564596219,5.89850633117166,
130.314069222208));
#151497=CARTESIAN_POINT('Ctrl Pts',(-8.21699572847713,5.88335254472493,
130.157156849771));
#151498=CARTESIAN_POINT('Ctrl Pts',(-8.22439581099215,5.86198452844846,
130.001199394192));
#151499=CARTESIAN_POINT('Ctrl Pts',(-8.23180403065861,5.8405930158415,129.84507044736));
#151500=CARTESIAN_POINT('Ctrl Pts',(-8.23921225032514,5.81297367779061,
129.689898884433));
#151501=CARTESIAN_POINT('Ctrl Pts',(-8.2466204699916,5.77924963428516,129.536210694602));
#151502=CARTESIAN_POINT('Ctrl Pts',(-8.25403324929363,5.74550483419375,
129.382427912254));
#151503=CARTESIAN_POINT('Ctrl Pts',(-8.26144602859567,5.70564793595996,
129.23013068255));
#151504=CARTESIAN_POINT('Ctrl Pts',(-8.26885880789771,5.65985188158431,
129.079829596962));
#151505=CARTESIAN_POINT('Ctrl Pts',(-8.27628217892648,5.61399039165835,
128.929313754133));
#151506=CARTESIAN_POINT('Ctrl Pts',(-8.2837055499552,5.56217291950594,128.7808001034));
#151507=CARTESIAN_POINT('Ctrl Pts',(-8.29112892098397,5.50462075612902,
128.634779806973));
#151508=CARTESIAN_POINT('Ctrl Pts',(-8.29506497042482,5.47410521816088,
128.557356342097));
#151509=CARTESIAN_POINT('Ctrl Pts',(-8.29900101986567,5.4419782311007,128.48063345719));
#151510=CARTESIAN_POINT('Ctrl Pts',(-8.30293706930652,5.40827794375211,
128.404681421168));
#151511=CARTESIAN_POINT('Ctrl Pts',(-8.31036033571196,5.34472025356365,
128.261438251615));
#151512=CARTESIAN_POINT('Ctrl Pts',(-8.31778360211739,5.27537163726404,
128.120505300964));
#151513=CARTESIAN_POINT('Ctrl Pts',(-8.32520686852283,5.20042157728153,
127.982385071775));
#151514=CARTESIAN_POINT('Ctrl Pts',(-8.33262136124384,5.12556010204561,
127.844428089226));
#151515=CARTESIAN_POINT('Ctrl Pts',(-8.34003585396484,5.04511053745627,
127.709277535795));
#151516=CARTESIAN_POINT('Ctrl Pts',(-8.34745034668586,4.95931047991477,
127.577416222894));
#151517=CARTESIAN_POINT('Ctrl Pts',(-8.35485769303963,4.87359311969916,
127.44568200289));
#151518=CARTESIAN_POINT('Ctrl Pts',(-8.36226503939338,4.78253573534287,
127.317231022774));
#151519=CARTESIAN_POINT('Ctrl Pts',(-8.36967238574715,4.68642185218623,
127.19252164194));
#151520=CARTESIAN_POINT('Ctrl Pts',(-8.37707420742253,4.59037965439009,
127.067905274067));
#151521=CARTESIAN_POINT('Ctrl Pts',(-8.384476029098,4.48928869391211,126.947025243365));
#151522=CARTESIAN_POINT('Ctrl Pts',(-8.39187785077337,4.38347576272227,
126.830310944987));
#151523=CARTESIAN_POINT('Ctrl Pts',(-8.39927576508479,4.27771868935379,
126.713658259177));
#151524=CARTESIAN_POINT('Ctrl Pts',(-8.40667367939615,4.16724485968297,
126.601167202025));
#151525=CARTESIAN_POINT('Ctrl Pts',(-8.41407159370758,4.05242122108274,
126.493233988781));
#151526=CARTESIAN_POINT('Ctrl Pts',(-8.42146827861979,3.93761666408912,
126.38531871208));
#151527=CARTESIAN_POINT('Ctrl Pts',(-8.42886496353199,3.81846400455809,
126.281960031435));
#151528=CARTESIAN_POINT('Ctrl Pts',(-8.4362616484442,3.69536699490435,126.183517259966));
#151529=CARTESIAN_POINT('Ctrl Pts',(-8.44365800537966,3.57227544350102,
126.085078853553));
#151530=CARTESIAN_POINT('Ctrl Pts',(-8.45105436231505,3.44524018126523,
125.991556156052));
#151531=CARTESIAN_POINT('Ctrl Pts',(-8.45845071925049,3.31469776513331,
125.903267954871));
#151532=CARTESIAN_POINT('Ctrl Pts',(-8.46584820858705,3.18413536262459,
125.814966236542));
#151533=CARTESIAN_POINT('Ctrl Pts',(-8.47324569792369,3.0500650463107,125.731900819401));
#151534=CARTESIAN_POINT('Ctrl Pts',(-8.48064318726026,2.9129519127197,125.654346858683));
#151535=CARTESIAN_POINT('Ctrl Pts',(-8.48804326977528,2.77579071433149,
125.576765711544));
#151536=CARTESIAN_POINT('Ctrl Pts',(-8.49544335229031,2.6355848996846,125.504700051159));
#151537=CARTESIAN_POINT('Ctrl Pts',(-8.50284343480533,2.49282354062182,
125.438378754214));
#151538=CARTESIAN_POINT('Ctrl Pts',(-8.51025165447179,2.34990520076914,
125.371984530185));
#151539=CARTESIAN_POINT('Ctrl Pts',(-8.51765987413826,2.20442604333549,
125.31134744147));
#151540=CARTESIAN_POINT('Ctrl Pts',(-8.52506809380472,2.05689514728419,
125.256648213739));
#151541=CARTESIAN_POINT('Ctrl Pts',(-8.53248087310678,1.90927344842785,
125.201915319546));
#151542=CARTESIAN_POINT('Ctrl Pts',(-8.53989365240889,1.75959784874113,
125.153127684114));
#151543=CARTESIAN_POINT('Ctrl Pts',(-8.54730643171095,1.6083914026664,125.110415793604));
#151544=CARTESIAN_POINT('Ctrl Pts',(-8.55472980273972,1.45696890573042,
125.067642874341));
#151545=CARTESIAN_POINT('Ctrl Pts',(-8.56215317376846,1.30401155583226,
125.030963125341));
#151546=CARTESIAN_POINT('Ctrl Pts',(-8.56957654479723,1.15005219484346,
125.000455853389));
#151547=CARTESIAN_POINT('Ctrl Pts',(-8.57351259423796,1.06841924744448,
124.984280165789));
#151548=CARTESIAN_POINT('Ctrl Pts',(-8.57744864367869,0.986504690218252,
124.969838916533));
#151549=CARTESIAN_POINT('Ctrl Pts',(-8.58138469311942,0.904388262755151,
124.957137992021));
#151550=CARTESIAN_POINT('Ctrl Pts',(-8.58880795952485,0.749519243323195,
124.933184444771));
#151551=CARTESIAN_POINT('Ctrl Pts',(-8.59623122593032,0.593463739467604,
124.915351697413));
#151552=CARTESIAN_POINT('Ctrl Pts',(-8.60365449233575,0.436746940704876,
124.903751947921));
#151553=CARTESIAN_POINT('Ctrl Pts',(-8.61106898505675,0.280215368183765,
124.89216590837));
#151554=CARTESIAN_POINT('Ctrl Pts',(-8.61848347777772,0.123024425170152,
124.886798230144));
#151555=CARTESIAN_POINT('Ctrl Pts',(-8.62589797049873,-0.0342912587645142,
124.887709988023));
#151556=CARTESIAN_POINT('Ctrl Pts',(-8.63330531685251,-0.191455315920397,
124.888620867115));
#151557=CARTESIAN_POINT('Ctrl Pts',(-8.6407126632062,-0.348743503857413,
124.895799131111));
#151558=CARTESIAN_POINT('Ctrl Pts',(-8.64812000955999,-0.505616939465063,
124.90925399656));
#151559=CARTESIAN_POINT('Ctrl Pts',(-8.65552183123537,-0.66237337294527,
124.922698826863));
#151560=CARTESIAN_POINT('Ctrl Pts',(-8.66292365291083,-0.818715299698069,
124.942410905705));
#151561=CARTESIAN_POINT('Ctrl Pts',(-8.67032547458621,-0.974104818376584,
124.968347392314));
#151562=CARTESIAN_POINT('Ctrl Pts',(-8.67772338889763,-1.12941230813973,
124.994270187255));
#151563=CARTESIAN_POINT('Ctrl Pts',(-8.68512130320901,-1.28376802384472,
125.0264107848));
#151564=CARTESIAN_POINT('Ctrl Pts',(-8.69251921752044,-1.43664027436086,
125.064674625756));
#151565=CARTESIAN_POINT('Ctrl Pts',(-8.69991590243266,-1.58948712028103,
125.102932107954));
#151566=CARTESIAN_POINT('Ctrl Pts',(-8.70731258734491,-1.74085062851949,
125.147310723432));
#151567=CARTESIAN_POINT('Ctrl Pts',(-8.71470927225712,-1.89021026072991,
125.197665001365));
#151568=CARTESIAN_POINT('Ctrl Pts',(-8.72210562919258,-2.03956327017773,
125.248017046536));
#151569=CARTESIAN_POINT('Ctrl Pts',(-8.72950198612796,-2.18691222653348,
125.304344108062));
#151570=CARTESIAN_POINT('Ctrl Pts',(-8.73689834306342,-2.33175295523339,
125.36645121061));
#151571=CARTESIAN_POINT('Ctrl Pts',(-8.74429583239997,-2.476615859418,125.428567821914));
#151572=CARTESIAN_POINT('Ctrl Pts',(-8.75169332173665,-2.61896942821068,
125.496466089147));
#151573=CARTESIAN_POINT('Ctrl Pts',(-8.75909081107321,-2.75833076968514,
125.569903441554));
#151574=CARTESIAN_POINT('Ctrl Pts',(-8.76649089358819,-2.89774096406203,
125.643366537311));
#151575=CARTESIAN_POINT('Ctrl Pts',(-8.7738909761031,-3.03415651268254,
125.722372410268));
#151576=CARTESIAN_POINT('Ctrl Pts',(-8.78129105861808,-3.16712049983219,
125.806633303872));
#151577=CARTESIAN_POINT('Ctrl Pts',(-8.78869927828456,-3.30023069455512,
125.890986850991));
#151578=CARTESIAN_POINT('Ctrl Pts',(-8.79610749795097,-3.42988143274203,
125.98060675873));
#151579=CARTESIAN_POINT('Ctrl Pts',(-8.80351571761744,-3.55564549515307,
126.075162411179));
#151580=CARTESIAN_POINT('Ctrl Pts',(-8.81092849691953,-3.6814869632464,
126.169776261054));
#151581=CARTESIAN_POINT('Ctrl Pts',(-8.81834127622162,-3.80343670033355,
126.269331673449));
#151582=CARTESIAN_POINT('Ctrl Pts',(-8.8257540555237,-3.92110220101021,
126.373459118804));
#151583=CARTESIAN_POINT('Ctrl Pts',(-8.83317742655246,-4.03893582767187,
126.477735346336));
#151584=CARTESIAN_POINT('Ctrl Pts',(-8.84060079758134,-4.15247272314095,
126.586596396495));
#151585=CARTESIAN_POINT('Ctrl Pts',(-8.8480241686101,-4.26135815032544,
126.699636841579));
#151586=CARTESIAN_POINT('Ctrl Pts',(-8.85196021805085,-4.31909181648815,
126.75957359793));
#151587=CARTESIAN_POINT('Ctrl Pts',(-8.85589626749153,-4.37551846753956,
126.820684786896));
#151588=CARTESIAN_POINT('Ctrl Pts',(-8.85983231693228,-4.43059004989061,
126.882906503043));
#151589=CARTESIAN_POINT('Ctrl Pts',(-8.86718970865023,-4.53353164398957,
126.999213359942));
#151590=CARTESIAN_POINT('Ctrl Pts',(-8.87454710036816,-4.63206126020542,
127.119769697859));
#151591=CARTESIAN_POINT('Ctrl Pts',(-8.88190449208611,-4.7258026946892,
127.244203394441));
#151592=CARTESIAN_POINT('Ctrl Pts',(-8.8893928385737,-4.82121264002974,
127.370851895766));
#151593=CARTESIAN_POINT('Ctrl Pts',(-8.89688118506131,-4.91166201865871,
127.501516857651));
#151594=CARTESIAN_POINT('Ctrl Pts',(-8.90436953154889,-4.9967929033199,
127.635766095726));
#151595=CARTESIAN_POINT('Ctrl Pts',(-8.91170891505276,-5.08023030990724,
127.767344761988));
#151596=CARTESIAN_POINT('Ctrl Pts',(-8.91904829855669,-5.15855859255118,
127.902366116144));
#151597=CARTESIAN_POINT('Ctrl Pts',(-8.92638768206055,-5.23148127387495,
128.04038987901));
#151598=CARTESIAN_POINT('Ctrl Pts',(-8.93372207269983,-5.30435434707122,
128.178319746529));
#151599=CARTESIAN_POINT('Ctrl Pts',(-8.94105646333905,-5.3718289589588,
128.319247623731));
#151600=CARTESIAN_POINT('Ctrl Pts',(-8.94839085397834,-5.43365278803803,
128.462705659732));
#151601=CARTESIAN_POINT('Ctrl Pts',(-8.95572176758381,-5.49544730813234,
128.606095686206));
#151602=CARTESIAN_POINT('Ctrl Pts',(-8.96305268118929,-5.55159622698705,
128.75201313542));
#151603=CARTESIAN_POINT('Ctrl Pts',(-8.97038359479475,-5.60189401281919,
128.899967267535));
#151604=CARTESIAN_POINT('Ctrl Pts',(-8.97798702921087,-5.65406157834139,
129.053421475385));
#151605=CARTESIAN_POINT('Ctrl Pts',(-8.98559046362695,-5.69993441543101,
129.209066325241));
#151606=CARTESIAN_POINT('Ctrl Pts',(-8.99319389804307,-5.73933868459386,
129.366333487772));
#151607=CARTESIAN_POINT('Ctrl Pts',(-9.00052389561581,-5.77732588636504,
129.517944964445));
#151608=CARTESIAN_POINT('Ctrl Pts',(-9.0078538931886,-5.80930162471794,
129.671063696745));
#151609=CARTESIAN_POINT('Ctrl Pts',(-9.01518389076134,-5.83516163910139,
129.82516747622));
#151610=CARTESIAN_POINT('Ctrl Pts',(-9.02251469196999,-5.86102448868856,
129.979288151107));
#151611=CARTESIAN_POINT('Ctrl Pts',(-9.02984549317875,-5.88077022376458,
130.13439371172));
#151612=CARTESIAN_POINT('Ctrl Pts',(-9.03717629438742,-5.89434619599635,
130.289954664798));
#151613=CARTESIAN_POINT('Ctrl Pts',(-9.0445110515798,-5.90792949434753,
130.445599564579));
#151614=CARTESIAN_POINT('Ctrl Pts',(-9.05184580877206,-5.91533636109181,
130.601699967749));
#151615=CARTESIAN_POINT('Ctrl Pts',(-9.05918056596443,-5.91656619986861,
130.757724096767));
#151616=CARTESIAN_POINT('Ctrl Pts',(-9.05999531323902,-5.91670281077001,
130.775055309042));
#151617=CARTESIAN_POINT('Ctrl Pts',(-9.06081006051364,-5.91676325721273,
130.792385582182));
#151618=CARTESIAN_POINT('Ctrl Pts',(-9.06162480778823,-5.91674757799995,
130.80971418943));
#151619=CARTESIAN_POINT('',(-10.8116248077882,-5.92210306258463,130.804007665308));
#151620=CARTESIAN_POINT('Ctrl Pts',(-9.06162590728991,-5.91423641208638,
130.809735292338));
#151621=CARTESIAN_POINT('Ctrl Pts',(-9.087177251775,-5.91897718201145,131.352952955589));
#151622=CARTESIAN_POINT('Ctrl Pts',(-9.20554447086439,-5.6009174926255,
133.863968248938));
#151623=CARTESIAN_POINT('Ctrl Pts',(-9.41672756455816,-2.040325974115,137.498733661377));
#151624=CARTESIAN_POINT('Ctrl Pts',(-9.69517518837099,4.52931960951324,
136.139416793954));
#151625=CARTESIAN_POINT('Ctrl Pts',(-9.9736228121838,6.93674174156142,129.877443932418));
#151626=CARTESIAN_POINT('Ctrl Pts',(-10.2520704359968,2.96963709179157,
124.467262222132));
#151627=CARTESIAN_POINT('Ctrl Pts',(-10.5305180598095,-3.72641897050015,
124.880564352784));
#151628=CARTESIAN_POINT('Ctrl Pts',(-10.7170361837401,-5.91793960293745,
128.803863058467));
#151629=CARTESIAN_POINT('Ctrl Pts',(-10.8107384330663,-5.92652287167294,
130.785264230727));
#151630=CARTESIAN_POINT('Ctrl Pts',(-10.8116248077882,-5.92650673784803,
130.804007402853));
#151631=CARTESIAN_POINT('',(-12.5616247901692,-5.91448392200524,130.799179299216));
#151632=CARTESIAN_POINT('Ctrl Pts',(-10.8116248077882,-5.91674998949168,
130.804007984347));
#151633=CARTESIAN_POINT('Ctrl Pts',(-10.8190355189351,-5.91675931365845,
130.960455989369));
#151634=CARTESIAN_POINT('Ctrl Pts',(-10.826446230082,-5.91055926251472,
131.117144690899));
#151635=CARTESIAN_POINT('Ctrl Pts',(-10.833856941229,-5.89811849125637,
131.273539502001));
#151636=CARTESIAN_POINT('Ctrl Pts',(-10.8412588941427,-5.88569242292915,
131.429749480339));
#151637=CARTESIAN_POINT('Ctrl Pts',(-10.8486608470566,-5.86704034398258,
131.585665889726));
#151638=CARTESIAN_POINT('Ctrl Pts',(-10.8560627999703,-5.84218287332432,
131.740752542529));
#151639=CARTESIAN_POINT('Ctrl Pts',(-10.8634576340751,-5.81734930927392,
131.895690041146));
#151640=CARTESIAN_POINT('Ctrl Pts',(-10.8708524681798,-5.78632229287438,
132.049799004285));
#151641=CARTESIAN_POINT('Ctrl Pts',(-10.8782473022846,-5.74917434773922,
132.202546900504));
#151642=CARTESIAN_POINT('Ctrl Pts',(-10.8856366512894,-5.71205395700066,
132.355181496349));
#151643=CARTESIAN_POINT('Ctrl Pts',(-10.8930260002943,-5.66882176532332,
132.506456672812));
#151644=CARTESIAN_POINT('Ctrl Pts',(-10.9004153492991,-5.61960160090809,
132.655848778363));
#151645=CARTESIAN_POINT('Ctrl Pts',(-10.9078008424935,-5.57040711989483,
132.805162930142));
#151646=CARTESIAN_POINT('Ctrl Pts',(-10.9151863356879,-5.5152310055336,
132.952595612798));
#151647=CARTESIAN_POINT('Ctrl Pts',(-10.9225718288824,-5.45424725585621,
133.097637189305));
#151648=CARTESIAN_POINT('Ctrl Pts',(-10.9299561642655,-5.39327306649797,
133.242656027888));
#151649=CARTESIAN_POINT('Ctrl Pts',(-10.9373404996487,-5.32649319331895,
133.38528415894));
#151650=CARTESIAN_POINT('Ctrl Pts',(-10.9447248350319,-5.25413024738925,
133.525030738321));
#151651=CARTESIAN_POINT('Ctrl Pts',(-10.9521089113768,-5.18176983991028,
133.664772415472));
#151652=CARTESIAN_POINT('Ctrl Pts',(-10.9594929877217,-5.10382692130971,
133.801632409126));
#151653=CARTESIAN_POINT('Ctrl Pts',(-10.9668770640667,-5.0205705190883,
133.93514362272));
#151654=CARTESIAN_POINT('Ctrl Pts',(-10.9742623525782,-4.93730044953324,
134.068676753455));
#151655=CARTESIAN_POINT('Ctrl Pts',(-10.9816476410899,-4.84871535804594,
134.198859691677));
#151656=CARTESIAN_POINT('Ctrl Pts',(-10.9890329296015,-4.75512803777965,
134.325253672861));
#151657=CARTESIAN_POINT('Ctrl Pts',(-10.996420901947,-4.66150670762611,
134.451693585961));
#151658=CARTESIAN_POINT('Ctrl Pts',(-11.0038088742926,-4.5628797525375,
134.574341499877));
#151659=CARTESIAN_POINT('Ctrl Pts',(-11.0111968466382,-4.45960061714789,
134.69279126476));
#151660=CARTESIAN_POINT('Ctrl Pts',(-11.0185929605209,-4.356207668269,134.811371561148));
#151661=CARTESIAN_POINT('Ctrl Pts',(-11.0259890744035,-4.24815254817928,
134.925744187803));
#151662=CARTESIAN_POINT('Ctrl Pts',(-11.0333851882862,-4.13582645113043,
135.035538955645));
#151663=CARTESIAN_POINT('Ctrl Pts',(-11.0407859638256,-4.02342955667067,
135.14540292544));
#151664=CARTESIAN_POINT('Ctrl Pts',(-11.0481867393651,-3.90675659927995,
135.250683037295));
#151665=CARTESIAN_POINT('Ctrl Pts',(-11.0555875149045,-3.78623184874473,
135.351049407229));
#151666=CARTESIAN_POINT('Ctrl Pts',(-11.0629986690587,-3.66553807809285,
135.451556527802));
#151667=CARTESIAN_POINT('Ctrl Pts',(-11.0704098232127,-3.54098202428191,
135.547135919064));
#151668=CARTESIAN_POINT('Ctrl Pts',(-11.0778209773669,-3.41301750281109,
135.637500599814));
#151669=CARTESIAN_POINT('Ctrl Pts',(-11.081018420723,-3.35780892119289,
135.676487232947));
#151670=CARTESIAN_POINT('Ctrl Pts',(-11.0842158640792,-3.30196621716772,
135.714503788482));
#151671=CARTESIAN_POINT('Ctrl Pts',(-11.0874133074354,-3.24552719218759,
135.751529889713));
#151672=CARTESIAN_POINT('Ctrl Pts',(-11.0948365738408,-3.11449690598059,
135.837490634836));
#151673=CARTESIAN_POINT('Ctrl Pts',(-11.1022598402462,-2.97985100501508,
135.918372082122));
#151674=CARTESIAN_POINT('Ctrl Pts',(-11.1096831066517,-2.84202100815124,
135.993854538145));
#151675=CARTESIAN_POINT('Ctrl Pts',(-11.1170975993727,-2.70435391489762,
136.069247780173));
#151676=CARTESIAN_POINT('Ctrl Pts',(-11.1245120920937,-2.5635105409054,
136.139254555114));
#151677=CARTESIAN_POINT('Ctrl Pts',(-11.1319265848147,-2.41995217631083,
136.203597788396));
#151678=CARTESIAN_POINT('Ctrl Pts',(-11.1393339311685,-2.27653217867294,
136.267879005247));
#151679=CARTESIAN_POINT('Ctrl Pts',(-11.1467412775222,-2.13040273834685,
136.326507396052));
#151680=CARTESIAN_POINT('Ctrl Pts',(-11.154148623876,-1.9820505007563,136.379251322768));
#151681=CARTESIAN_POINT('Ctrl Pts',(-11.1615504455514,-1.83380890986177,
136.431955911074));
#151682=CARTESIAN_POINT('Ctrl Pts',(-11.1689522672268,-1.68334817291361,
136.47878464958));
#151683=CARTESIAN_POINT('Ctrl Pts',(-11.1763540889022,-1.53117560819909,
136.519553686864));
#151684=CARTESIAN_POINT('Ctrl Pts',(-11.1837520032136,-1.37908337419568,
136.560301202491));
#151685=CARTESIAN_POINT('Ctrl Pts',(-11.191149917525,-1.22528147177775,
136.594995291237));
#151686=CARTESIAN_POINT('Ctrl Pts',(-11.1985478318364,-1.07029299303037,
136.623501745909));
#151687=CARTESIAN_POINT('Ctrl Pts',(-11.2059445167486,-0.915330270557275,
136.652003463325));
#151688=CARTESIAN_POINT('Ctrl Pts',(-11.2133412016608,-0.759181729893625,
136.674319520023));
#151689=CARTESIAN_POINT('Ctrl Pts',(-11.220737886573,-0.602381404208926,
136.690366666354));
#151690=CARTESIAN_POINT('Ctrl Pts',(-11.2281342435084,-0.445588031215432,
136.706413101137));
#151691=CARTESIAN_POINT('Ctrl Pts',(-11.2355306004439,-0.288143302023389,
136.716191140245));
#151692=CARTESIAN_POINT('Ctrl Pts',(-11.2429269573793,-0.130586865160602,
136.719669369706));
#151693=CARTESIAN_POINT('Ctrl Pts',(-11.2503244467159,0.0269936939955663,
136.723148131694));
#151694=CARTESIAN_POINT('Ctrl Pts',(-11.2577219360525,0.184685621645346,
136.720325155313));
#151695=CARTESIAN_POINT('Ctrl Pts',(-11.2651194253891,0.341948921691745,
136.711221162513));
#151696=CARTESIAN_POINT('Ctrl Pts',(-11.2725195079042,0.499267350144185,
136.702113978323));
#151697=CARTESIAN_POINT('Ctrl Pts',(-11.2799195904191,0.656156479395662,
136.686721415504));
#151698=CARTESIAN_POINT('Ctrl Pts',(-11.2873196729341,0.812081235894015,
136.665116083273));
#151699=CARTESIAN_POINT('Ctrl Pts',(-11.2947278926006,0.968177447691148,
136.643486993757));
#151700=CARTESIAN_POINT('Ctrl Pts',(-11.3021361122671,1.12330679900085,
136.615631542985));
#151701=CARTESIAN_POINT('Ctrl Pts',(-11.3095443319335,1.27694348861063,
136.581673651269));
#151702=CARTESIAN_POINT('Ctrl Pts',(-11.3169571112356,1.43067473903929,
136.547694859037));
#151703=CARTESIAN_POINT('Ctrl Pts',(-11.3243698905376,1.58291113697194,
136.507606236499));
#151704=CARTESIAN_POINT('Ctrl Pts',(-11.3317826698397,1.73314235471533,
136.461581502487));
#151705=CARTESIAN_POINT('Ctrl Pts',(-11.3392060408685,1.883588229868,136.415491006178));
#151706=CARTESIAN_POINT('Ctrl Pts',(-11.3466294118972,2.03202285125357,
136.363447581534));
#151707=CARTESIAN_POINT('Ctrl Pts',(-11.354052782926,2.1779553939957,136.305673266768));
#151708=CARTESIAN_POINT('Ctrl Pts',(-11.3579888323667,2.25533232976046,
136.275039938803));
#151709=CARTESIAN_POINT('Ctrl Pts',(-11.3619248818075,2.33200623401698,
136.242796229776));
#151710=CARTESIAN_POINT('Ctrl Pts',(-11.3658609312483,2.40790689598538,
136.208980395383));
#151711=CARTESIAN_POINT('Ctrl Pts',(-11.3732841976537,2.55105317568001,
136.145204787073));
#151712=CARTESIAN_POINT('Ctrl Pts',(-11.3807074640591,2.69188042634453,
136.075641775118));
#151713=CARTESIAN_POINT('Ctrl Pts',(-11.3881307304646,2.82988643436045,
136.00048160645));
#151714=CARTESIAN_POINT('Ctrl Pts',(-11.3955452231856,2.96772933073578,
135.92541027086));
#151715=CARTESIAN_POINT('Ctrl Pts',(-11.4029597159066,3.10275729712157,
135.844755123294));
#151716=CARTESIAN_POINT('Ctrl Pts',(-11.4103742086276,3.23448788424841,
135.758754494636));
#151717=CARTESIAN_POINT('Ctrl Pts',(-11.4177815549814,3.36609150447582,
135.672836756622));
#151718=CARTESIAN_POINT('Ctrl Pts',(-11.4251889013352,3.49440376200909,
135.581583997183));
#151719=CARTESIAN_POINT('Ctrl Pts',(-11.432596247689,3.61896672946355,135.485280438876));
#151720=CARTESIAN_POINT('Ctrl Pts',(-11.4399980693644,3.74343679315774,
135.389048707396));
#151721=CARTESIAN_POINT('Ctrl Pts',(-11.4473998910398,3.86416284065097,
135.28777390515));
#151722=CARTESIAN_POINT('Ctrl Pts',(-11.4548017127152,3.9807159746075,135.181783477195));
#151723=CARTESIAN_POINT('Ctrl Pts',(-11.4621996270266,4.09720758107121,
135.075849000763));
#151724=CARTESIAN_POINT('Ctrl Pts',(-11.4695975413379,4.20953038559673,
134.965204106781));
#151725=CARTESIAN_POINT('Ctrl Pts',(-11.4769954556492,4.31728873182291,
134.850216345169));
#151726=CARTESIAN_POINT('Ctrl Pts',(-11.4843921405615,4.42502917056719,
134.735247692436));
#151727=CARTESIAN_POINT('Ctrl Pts',(-11.4917888254737,4.52820640145996,
134.615937876565));
#151728=CARTESIAN_POINT('Ctrl Pts',(-11.4991855103859,4.62646172623994,
134.492691196315));
#151729=CARTESIAN_POINT('Ctrl Pts',(-11.5065818673213,4.72471269427572,
134.369449980953));
#151730=CARTESIAN_POINT('Ctrl Pts',(-11.5139782242569,4.81804195743561,
134.242272540197));
#151731=CARTESIAN_POINT('Ctrl Pts',(-11.5213745811923,4.90613139304453,
134.111595915618));
#151732=CARTESIAN_POINT('Ctrl Pts',(-11.5287720705289,4.99423431537117,
133.980899284115));
#151733=CARTESIAN_POINT('Ctrl Pts',(-11.5361695598654,5.07709560412569,
133.846702711627));
#151734=CARTESIAN_POINT('Ctrl Pts',(-11.543567049202,5.15444081218917,133.709471712884));
#151735=CARTESIAN_POINT('Ctrl Pts',(-11.550967131717,5.23181313349533,133.572192608027));
#151736=CARTESIAN_POINT('Ctrl Pts',(-11.558367214232,5.30366534104637,133.431877284069));
#151737=CARTESIAN_POINT('Ctrl Pts',(-11.565767296747,5.36976930270644,133.289015160598));
#151738=CARTESIAN_POINT('Ctrl Pts',(-11.5731755164135,5.43594595246811,
133.145995945536));
#151739=CARTESIAN_POINT('Ctrl Pts',(-11.58058373608,5.49636157645428,133.000424677238));
#151740=CARTESIAN_POINT('Ctrl Pts',(-11.5879919557464,5.55083622393497,
132.852810709111));
#151741=CARTESIAN_POINT('Ctrl Pts',(-11.5954047350485,5.60534439965208,
132.705105887051));
#151742=CARTESIAN_POINT('Ctrl Pts',(-11.6028175143506,5.65390419780506,
132.55535621421));
#151743=CARTESIAN_POINT('Ctrl Pts',(-11.6102302936526,5.69638592838495,
132.404084943004));
#151744=CARTESIAN_POINT('Ctrl Pts',(-11.6176536646814,5.73892835885381,
132.252597528311));
#151745=CARTESIAN_POINT('Ctrl Pts',(-11.6250770357102,5.77537529033085,
132.099584535201));
#151746=CARTESIAN_POINT('Ctrl Pts',(-11.632500406739,5.8056482270167,131.94557892562));
#151747=CARTESIAN_POINT('Ctrl Pts',(-11.6364364561797,5.82169966443649,
131.863921456107));
#151748=CARTESIAN_POINT('Ctrl Pts',(-11.6403725056204,5.83601623695736,
131.781985016613));
#151749=CARTESIAN_POINT('Ctrl Pts',(-11.6443085550612,5.84859217953896,
131.699849355594));
#151750=CARTESIAN_POINT('Ctrl Pts',(-11.6517318214666,5.87231001476642,
131.544944062277));
#151751=CARTESIAN_POINT('Ctrl Pts',(-11.659155087872,5.88990525156296,131.388861600725));
#151752=CARTESIAN_POINT('Ctrl Pts',(-11.6665783542775,5.90126649133266,
131.232127330594));
#151753=CARTESIAN_POINT('Ctrl Pts',(-11.6739928469985,5.91261430306044,
131.075578307353));
#151754=CARTESIAN_POINT('Ctrl Pts',(-11.6814073397195,5.91774275721396,
130.918379377672));
#151755=CARTESIAN_POINT('Ctrl Pts',(-11.6888218324405,5.91659159270028,
130.761065263446));
#151756=CARTESIAN_POINT('Ctrl Pts',(-11.6962291787943,5.9154415377223,130.603902774486));
#151757=CARTESIAN_POINT('Ctrl Pts',(-11.7036365251481,5.90802391619174,
130.446625692782));
#151758=CARTESIAN_POINT('Ctrl Pts',(-11.7110438715019,5.8943303316585,130.289772914846));
#151759=CARTESIAN_POINT('Ctrl Pts',(-11.7184456931773,5.88064696031722,
130.133037123629));
#151760=CARTESIAN_POINT('Ctrl Pts',(-11.7258475148528,5.86069697850371,
129.976725376345));
#151761=CARTESIAN_POINT('Ctrl Pts',(-11.7332493365282,5.8345240455325,129.821375508522));
#151762=CARTESIAN_POINT('Ctrl Pts',(-11.7406472508396,5.80836492904881,
129.666107648684));
#151763=CARTESIAN_POINT('Ctrl Pts',(-11.7480451651509,5.77598946559807,
129.511801024239));
#151764=CARTESIAN_POINT('Ctrl Pts',(-11.7554430794623,5.73749302341003,
129.358987181799));
#151765=CARTESIAN_POINT('Ctrl Pts',(-11.7628397643745,5.69900297863251,
129.206198734248));
#151766=CARTESIAN_POINT('Ctrl Pts',(-11.7702364492867,5.65439406505184,
129.054902937985));
#151767=CARTESIAN_POINT('Ctrl Pts',(-11.7776331341989,5.60381254549375,
128.905620109369));
#151768=CARTESIAN_POINT('Ctrl Pts',(-11.7850294911344,5.55323326877324,
128.756343900111));
#151769=CARTESIAN_POINT('Ctrl Pts',(-11.7924258480699,5.49668203244469,
128.609080834582));
#151770=CARTESIAN_POINT('Ctrl Pts',(-11.7998222050053,5.43435457888297,
128.464334790043));
#151771=CARTESIAN_POINT('Ctrl Pts',(-11.8072196943419,5.37201758282882,
128.319566584515));
#151772=CARTESIAN_POINT('Ctrl Pts',(-11.8146171836785,5.30390275632155,
128.177316510169));
#151773=CARTESIAN_POINT('Ctrl Pts',(-11.8220146730151,5.23025340471511,
128.038067089221));
#151774=CARTESIAN_POINT('Ctrl Pts',(-11.8294147555301,5.15657823544275,
127.898768854604));
#151775=CARTESIAN_POINT('Ctrl Pts',(-11.8368148380451,5.07736485272949,
127.762473697439));
#151776=CARTESIAN_POINT('Ctrl Pts',(-11.8442149205601,4.99290170814379,
127.629638094996));
#151777=CARTESIAN_POINT('Ctrl Pts',(-11.8516231402266,4.90834568764772,
127.496656426152));
#151778=CARTESIAN_POINT('Ctrl Pts',(-11.859031359893,4.81852857733406,127.367142224342));
#151779=CARTESIAN_POINT('Ctrl Pts',(-11.8664395795595,4.72378164288507,
127.24152220517));
#151780=CARTESIAN_POINT('Ctrl Pts',(-11.8738523588615,4.628976393279,127.115824868973));
#151781=CARTESIAN_POINT('Ctrl Pts',(-11.8812651381636,4.52923550942774,
126.994026779493));
#151782=CARTESIAN_POINT('Ctrl Pts',(-11.8886779174657,4.42492911778911,
126.876519879318));
#151783=CARTESIAN_POINT('Ctrl Pts',(-11.8961012884944,4.32047368828646,
126.758845079773));
#151784=CARTESIAN_POINT('Ctrl Pts',(-11.9035246595232,4.21143998035911,
126.645473983765));
#151785=CARTESIAN_POINT('Ctrl Pts',(-11.9109480305519,4.09823396108951,
126.536760710982));
#151786=CARTESIAN_POINT('Ctrl Pts',(-11.9148840799927,4.03820941333243,
126.479118325215));
#151787=CARTESIAN_POINT('Ctrl Pts',(-11.9188201294334,3.977012423375,126.422784740331));
#151788=CARTESIAN_POINT('Ctrl Pts',(-11.9227561788741,3.91470696970683,
126.367807912613));
#151789=CARTESIAN_POINT('Ctrl Pts',(-11.9301794452796,3.79720082857353,
126.264123331302));
#151790=CARTESIAN_POINT('Ctrl Pts',(-11.937602711685,3.67539488846097,126.164953577267));
#151791=CARTESIAN_POINT('Ctrl Pts',(-11.9450259780904,3.54967093566331,
126.070676343028));
#151792=CARTESIAN_POINT('Ctrl Pts',(-11.9524404708114,3.42409557813748,
125.976510536651));
#151793=CARTESIAN_POINT('Ctrl Pts',(-11.9598549635325,3.29461172123091,
125.887225961637));
#151794=CARTESIAN_POINT('Ctrl Pts',(-11.9672694562535,3.16163666902764,
125.803162347595));
#151795=CARTESIAN_POINT('Ctrl Pts',(-11.9746768026073,3.02878978318536,
125.719179757229));
#151796=CARTESIAN_POINT('Ctrl Pts',(-11.982084148961,2.89245871440621,125.640408307933));
#151797=CARTESIAN_POINT('Ctrl Pts',(-11.9894914953148,2.75309231310214,
125.567146350607));
#151798=CARTESIAN_POINT('Ctrl Pts',(-11.9968933169902,2.61382985651876,
125.493939034813));
#151799=CARTESIAN_POINT('Ctrl Pts',(-12.0042951386656,2.47153690407494,
125.426233201992));
#151800=CARTESIAN_POINT('Ctrl Pts',(-12.011696960341,2.3266895509583,125.364282833567));
#151801=CARTESIAN_POINT('Ctrl Pts',(-12.0190948746524,2.18191866163187,
125.302365168259));
#151802=CARTESIAN_POINT('Ctrl Pts',(-12.0264927889637,2.03459639948691,
125.24619706292));
#151803=CARTESIAN_POINT('Ctrl Pts',(-12.0338907032751,1.88522151859995,
125.195985595485));
#151804=CARTESIAN_POINT('Ctrl Pts',(-12.0412873881873,1.73587146110804,
125.145782472284));
#151805=CARTESIAN_POINT('Ctrl Pts',(-12.0486840730995,1.58446981536809,
125.101534141184));
#151806=CARTESIAN_POINT('Ctrl Pts',(-12.0560807580117,1.43153339690129,
125.063398790829));
#151807=CARTESIAN_POINT('Ctrl Pts',(-12.0634771149471,1.27860375979576,
125.025265131435));
#151808=CARTESIAN_POINT('Ctrl Pts',(-12.0708734718826,1.1241398474834,124.993244004154));
#151809=CARTESIAN_POINT('Ctrl Pts',(-12.0782698288181,0.968671389709072,
124.967443083348));
#151810=CARTESIAN_POINT('Ctrl Pts',(-12.0856673181547,0.813179129316302,
124.941638212356));
#151811=CARTESIAN_POINT('Ctrl Pts',(-12.0930648074912,0.656682385513134,
124.922055505173));
#151812=CARTESIAN_POINT('Ctrl Pts',(-12.1004622968278,0.499718630392232,
124.908751077159));
#151813=CARTESIAN_POINT('Ctrl Pts',(-12.1078623793428,0.342699851870522,
124.895441985298));
#151814=CARTESIAN_POINT('Ctrl Pts',(-12.1152624618578,0.185214107817576,
124.888415585973));
#151815=CARTESIAN_POINT('Ctrl Pts',(-12.1226625443728,0.0278013606063731,
124.887675933822));
#151816=CARTESIAN_POINT('Ctrl Pts',(-12.1300707640393,-0.129784478102812,
124.886935468348));
#151817=CARTESIAN_POINT('Ctrl Pts',(-12.1374789837059,-0.287296786147881,
124.892495557369));
#151818=CARTESIAN_POINT('Ctrl Pts',(-12.1448872033723,-0.444197498413058,
124.904308147892));
#151819=CARTESIAN_POINT('Ctrl Pts',(-12.1522999826744,-0.601194780448383,
124.916128008867));
#151820=CARTESIAN_POINT('Ctrl Pts',(-12.1597127619765,-0.757579346657777,
124.934207996812));
#151821=CARTESIAN_POINT('Ctrl Pts',(-12.1671255412786,-0.91282138224968,
124.958448568398));
#151822=CARTESIAN_POINT('Ctrl Pts',(-12.1745489123073,-1.06828523494239,
124.982723776049));
#151823=CARTESIAN_POINT('Ctrl Pts',(-12.1819722833361,-1.22260293128174,
125.013177075888));
#151824=CARTESIAN_POINT('Ctrl Pts',(-12.1893956543649,-1.37525710521962,
125.049658326653));
#151825=CARTESIAN_POINT('Ctrl Pts',(-12.1933317038056,-1.45619801112647,
125.069001561163));
#151826=CARTESIAN_POINT('Ctrl Pts',(-12.1972677532463,-1.53667151942998,
125.090038643349));
#151827=CARTESIAN_POINT('Ctrl Pts',(-12.201203802687,-1.61660270121701,
125.112741667837));
#151828=CARTESIAN_POINT('Ctrl Pts',(-12.2086270690924,-1.76735041550362,
125.155558863484));
#151829=CARTESIAN_POINT('Ctrl Pts',(-12.2160503354979,-1.91662382411278,
125.204433976212));
#151830=CARTESIAN_POINT('Ctrl Pts',(-12.2234736019033,-2.06389879881326,
125.259249950433));
#151831=CARTESIAN_POINT('Ctrl Pts',(-12.2308880946243,-2.21099970672385,
125.314001136724));
#151832=CARTESIAN_POINT('Ctrl Pts',(-12.2383025873453,-2.3561065358316,
125.37467907902));
#151833=CARTESIAN_POINT('Ctrl Pts',(-12.2457170800663,-2.49870789894229,
125.441116319731));
#151834=CARTESIAN_POINT('Ctrl Pts',(-12.2531244264201,-2.64117181749058,
125.507489525727));
#151835=CARTESIAN_POINT('Ctrl Pts',(-12.2605317727739,-2.78113474145283,
125.579610822543));
#151836=CARTESIAN_POINT('Ctrl Pts',(-12.2679391191276,-2.91810304515607,
125.657263845564));
#151837=CARTESIAN_POINT('Ctrl Pts',(-12.275340940803,-3.05496919273051,
125.734858952031));
#151838=CARTESIAN_POINT('Ctrl Pts',(-12.2827427624784,-3.18884484390587,
125.817977386421));
#151839=CARTESIAN_POINT('Ctrl Pts',(-12.2901445841538,-3.31925897584034,
125.906355879532));
#151840=CARTESIAN_POINT('Ctrl Pts',(-12.2975424984651,-3.44960426316988,
125.994687718325));
#151841=CARTESIAN_POINT('Ctrl Pts',(-12.3049404127765,-3.57649136219079,
126.088273876933));
#151842=CARTESIAN_POINT('Ctrl Pts',(-12.3123383270878,-3.6994764636106,
126.186806670107));
#151843=CARTESIAN_POINT('Ctrl Pts',(-12.3197350120001,-3.82244112713774,
126.285323088919));
#151844=CARTESIAN_POINT('Ctrl Pts',(-12.3271316969122,-3.94150478898354,
126.388784277612));
#151845=CARTESIAN_POINT('Ctrl Pts',(-12.3345283818244,-4.05625500914746,
126.496840929478));
#151846=CARTESIAN_POINT('Ctrl Pts',(-12.3419247387599,-4.17100014116654,
126.604892789999));
#151847=CARTESIAN_POINT('Ctrl Pts',(-12.3493210956954,-4.28143194002967,
126.717539452618));
#151848=CARTESIAN_POINT('Ctrl Pts',(-12.3567174526308,-4.3871734843788,
126.834393441321));
#151849=CARTESIAN_POINT('Ctrl Pts',(-12.3641149419674,-4.49293121802787,
126.951265320668));
#151850=CARTESIAN_POINT('Ctrl Pts',(-12.371512431304,-4.59399701686227,
127.07234553188));
#151851=CARTESIAN_POINT('Ctrl Pts',(-12.3789099206405,-4.69003315264681,
127.197212216187));
#151852=CARTESIAN_POINT('Ctrl Pts',(-12.3863100031555,-4.78610295375015,
127.322122672316));
#151853=CARTESIAN_POINT('Ctrl Pts',(-12.3937100856705,-4.87713935396442,
127.450821948551));
#151854=CARTESIAN_POINT('Ctrl Pts',(-12.4011101681855,-4.96284707915426,
127.582857950885));
#151855=CARTESIAN_POINT('Ctrl Pts',(-12.4085183878519,-5.04864904879892,
127.715039140378));
#151856=CARTESIAN_POINT('Ctrl Pts',(-12.4159266075184,-5.12911043838591,
127.850564070045));
#151857=CARTESIAN_POINT('Ctrl Pts',(-12.4233348271848,-5.20398083892142,
127.988954076649));
#151858=CARTESIAN_POINT('Ctrl Pts',(-12.4307476064869,-5.27889732093917,
128.127429259992));
#151859=CARTESIAN_POINT('Ctrl Pts',(-12.438160385789,-5.34821579297108,
128.268772699698));
#151860=CARTESIAN_POINT('Ctrl Pts',(-12.445573165091,-5.41173362580237,
128.412484841975));
#151861=CARTESIAN_POINT('Ctrl Pts',(-12.4529965361198,-5.47534221589199,
128.556402326901));
#151862=CARTESIAN_POINT('Ctrl Pts',(-12.4604199071485,-5.53313347654608,
128.702694927761));
#151863=CARTESIAN_POINT('Ctrl Pts',(-12.4678432781772,-5.58495407687434,
128.850846214828));
#151864=CARTESIAN_POINT('Ctrl Pts',(-12.4717793276181,-5.61243060258706,
128.929399582073));
#151865=CARTESIAN_POINT('Ctrl Pts',(-12.475715377059,-5.63822940645647,
129.008475280521));
#151866=CARTESIAN_POINT('Ctrl Pts',(-12.4796514264999,-5.66233346515659,
129.087995186818));
#151867=CARTESIAN_POINT('Ctrl Pts',(-12.4887665432281,-5.71815372655736,
129.272147657207));
#151868=CARTESIAN_POINT('Ctrl Pts',(-12.4978816599562,-5.76501905627374,
129.459132538451));
#151869=CARTESIAN_POINT('Ctrl Pts',(-12.5069967766844,-5.80268447077341,
129.648167080504));
#151870=CARTESIAN_POINT('Ctrl Pts',(-12.5161014405401,-5.84030669199463,
129.836984844864));
#151871=CARTESIAN_POINT('Ctrl Pts',(-12.5252061043959,-5.86874999000234,
130.027847637754));
#151872=CARTESIAN_POINT('Ctrl Pts',(-12.5343107682516,-5.88781784875314,
130.21995361692));
#151873=CARTESIAN_POINT('Ctrl Pts',(-12.5434154321073,-5.90688570750392,
130.412059596086));
#151874=CARTESIAN_POINT('Ctrl Pts',(-12.5525200959631,-5.9165779597188,
130.605408827073));
#151875=CARTESIAN_POINT('Ctrl Pts',(-12.5616247598188,-5.91674772904762,
130.799176670249));
#151876=CARTESIAN_POINT('',(-14.3116248077882,-5.90794108543601,130.806865238042));
#151877=CARTESIAN_POINT('Ctrl Pts',(-12.5616248077882,-5.91316974211598,
130.799180825377));
#151878=CARTESIAN_POINT('Ctrl Pts',(-12.627116221963,-5.90156166892063,
132.192154654826));
#151879=CARTESIAN_POINT('Ctrl Pts',(-12.7854235107422,-4.71330205150837,
135.577102347049));
#151880=CARTESIAN_POINT('Ctrl Pts',(-13.0365466741257,0.937472151881782,
137.739683717091));
#151881=CARTESIAN_POINT('Ctrl Pts',(-13.3149942979386,6.34161033930907,
133.764350285572));
#151882=CARTESIAN_POINT('Ctrl Pts',(-13.5934419217515,5.91811842979897,
127.068930952691));
#151883=CARTESIAN_POINT('Ctrl Pts',(-13.8718895455643,0.056164799462427,
123.806188995947));
#151884=CARTESIAN_POINT('Ctrl Pts',(-14.11128384091,-5.02800157587884,126.530067858737));
#151885=CARTESIAN_POINT('Ctrl Pts',(-14.2578622616512,-5.90358900820754,
129.660813820107));
#151886=CARTESIAN_POINT('Ctrl Pts',(-14.3116248077882,-5.90794108543601,
130.806865238042));
#151887=CARTESIAN_POINT('',(-16.0616248077882,-5.92237476527066,130.808656821232));
#151888=CARTESIAN_POINT('Ctrl Pts',(-14.3116248077882,-5.90794108543601,
130.806865238042));
#151889=CARTESIAN_POINT('Ctrl Pts',(-14.3506781362555,-5.91110245173523,
131.639361570173));
#151890=CARTESIAN_POINT('Ctrl Pts',(-14.482547339327,-5.35732722362217,
134.446388667616));
#151891=CARTESIAN_POINT('Ctrl Pts',(-14.707232417003,-1.04866502285217,
137.723743697016));
#151892=CARTESIAN_POINT('Ctrl Pts',(-14.9856800408159,5.25464389193611,
135.4267277708));
#151893=CARTESIAN_POINT('Ctrl Pts',(-15.2641276646288,6.72919177365889,
128.881982245949));
#151894=CARTESIAN_POINT('Ctrl Pts',(-15.5425752884417,2.01994115468555,
124.103808531212));
#151895=CARTESIAN_POINT('Ctrl Pts',(-15.8084076694948,-4.24808364837976,
125.420624513406));
#151896=CARTESIAN_POINT('Ctrl Pts',(-15.9814241759437,-5.90849869859571,
129.109618236687));
#151897=CARTESIAN_POINT('Ctrl Pts',(-16.0616248077882,-5.92237476527066,
130.808656821232));
#151898=CARTESIAN_POINT('',(-17.8116248077883,-5.92167625280914,130.799795184471));
#151899=CARTESIAN_POINT('Ctrl Pts',(-16.0616248077882,-5.92237476527066,
130.808656821232));
#151900=CARTESIAN_POINT('Ctrl Pts',(-16.074240050548,-5.92455741577639,
131.075908882834));
#151901=CARTESIAN_POINT('Ctrl Pts',(-16.1796711679109,-5.7865147396121,
133.307183312521));
#151902=CARTESIAN_POINT('Ctrl Pts',(-16.3779181598812,-2.95033538898635,
137.150468213798));
#151903=CARTESIAN_POINT('Ctrl Pts',(-16.6563657836929,3.74443170811431,
136.716787506209));
#151904=CARTESIAN_POINT('Ctrl Pts',(-16.9348134075062,6.99824899111522,
130.849875326086));
#151905=CARTESIAN_POINT('Ctrl Pts',(-17.2132610313189,3.82101733475201,
124.941137352339));
#151906=CARTESIAN_POINT('Ctrl Pts',(-17.4917086551319,-2.86754258517585,
124.420415124962));
#151907=CARTESIAN_POINT('Ctrl Pts',(-17.6911632472883,-5.77105058276818,
128.249669255985));
#151908=CARTESIAN_POINT('Ctrl Pts',(-17.7978019648404,-5.92417162324444,
130.506870325296));
#151909=CARTESIAN_POINT('Ctrl Pts',(-17.8116248077883,-5.92167625280914,
130.799795184471));
#151910=CARTESIAN_POINT('',(-19.5616239976484,-5.91172027463249,130.802225031155));
#151911=CARTESIAN_POINT('Ctrl Pts',(-17.8116248077883,-5.92167625280914,
130.799795184471));
#151912=CARTESIAN_POINT('Ctrl Pts',(-17.8906178394447,-5.90741602598498,
132.473765058911));
#151913=CARTESIAN_POINT('Ctrl Pts',(-18.0624267457055,-4.28935641582584,
136.138738636046));
#151914=CARTESIAN_POINT('Ctrl Pts',(-18.3270515265707,1.93261682990332,
137.530619066297));
#151915=CARTESIAN_POINT('Ctrl Pts',(-18.6054991503834,6.70361833380628,
132.814102333552));
#151916=CARTESIAN_POINT('Ctrl Pts',(-18.8839467741964,5.31432207890837,
126.25073114516));
#151917=CARTESIAN_POINT('Ctrl Pts',(-19.1623943980091,-0.958576547442623,
123.871922984737));
#151918=CARTESIAN_POINT('Ctrl Pts',(-19.3882865867831,-5.33287767884445,
127.110263284248));
#151919=CARTESIAN_POINT('Ctrl Pts',(-19.5213629009526,-5.91038304027362,
129.943875328412));
#151920=CARTESIAN_POINT('Ctrl Pts',(-19.5616233405177,-5.90764080910516,
130.80221248317));
#151921=CARTESIAN_POINT('',(-21.3116256300176,-5.91484479357845,130.809683424605));
#151922=CARTESIAN_POINT('Ctrl Pts',(-19.5616248077881,-5.91674962015507,
130.802240500865));
#151923=CARTESIAN_POINT('Ctrl Pts',(-19.5691919858151,-5.91680751748068,
130.963818389114));
#151924=CARTESIAN_POINT('Ctrl Pts',(-19.5767591638421,-5.91024237122003,
131.125349323677));
#151925=CARTESIAN_POINT('Ctrl Pts',(-19.5843263418691,-5.89709206905609,
131.28626900261));
#151926=CARTESIAN_POINT('Ctrl Pts',(-19.591897422316,-5.88393498523593,
131.447271668378));
#151927=CARTESIAN_POINT('Ctrl Pts',(-19.5994685027628,-5.86418600343569,
131.607662102599));
#151928=CARTESIAN_POINT('Ctrl Pts',(-19.6070395832096,-5.83793478736771,
131.766882295733));
#151929=CARTESIAN_POINT('Ctrl Pts',(-19.6146157566898,-5.81166591221945,
131.926209595608));
#151930=CARTESIAN_POINT('Ctrl Pts',(-19.6221919301698,-5.77888613908945,
132.084364741324));
#151931=CARTESIAN_POINT('Ctrl Pts',(-19.62976810365,-5.73973604494925,132.240800904111));
#151932=CARTESIAN_POINT('Ctrl Pts',(-19.6373562482108,-5.70052408990546,
132.397484251039));
#151933=CARTESIAN_POINT('Ctrl Pts',(-19.6449443927717,-5.65492178265798,
132.552442848179));
#151934=CARTESIAN_POINT('Ctrl Pts',(-19.6525325373325,-5.60311972573027,
132.705144640445));
#151935=CARTESIAN_POINT('Ctrl Pts',(-19.6601268842168,-5.55127532734408,
132.857971246608));
#151936=CARTESIAN_POINT('Ctrl Pts',(-19.667721231101,-5.49322119737034,
133.008537043984));
#151937=CARTESIAN_POINT('Ctrl Pts',(-19.6753155779852,-5.42919574204391,
133.156330888865));
#151938=CARTESIAN_POINT('Ctrl Pts',(-19.6829241974717,-5.36504995907494,
133.304402493347));
#151939=CARTESIAN_POINT('Ctrl Pts',(-19.6905328169581,-5.29491056763434,
133.449691416725));
#151940=CARTESIAN_POINT('Ctrl Pts',(-19.6981414364445,-5.21906227235888,
133.591710534555));
#151941=CARTESIAN_POINT('Ctrl Pts',(-19.705190839508,-5.14878865622799,
133.72329156658));
#151942=CARTESIAN_POINT('Ctrl Pts',(-19.7122402425716,-5.07361507784861,
133.852065885224));
#151943=CARTESIAN_POINT('Ctrl Pts',(-19.7192896456351,-4.99380006069075,
133.977669854994));
#151944=CARTESIAN_POINT('Ctrl Pts',(-19.7267129120405,-4.90975207390692,
134.109935200127));
#151945=CARTESIAN_POINT('Ctrl Pts',(-19.7341361784459,-4.82031861508711,
134.239059108081));
#151946=CARTESIAN_POINT('Ctrl Pts',(-19.7415594448514,-4.72576141575207,
134.364572634271));
#151947=CARTESIAN_POINT('Ctrl Pts',(-19.7489739375724,-4.63131597517402,
134.489937813896));
#151948=CARTESIAN_POINT('Ctrl Pts',(-19.7563884302934,-4.53175907068169,
134.611700810339));
#151949=CARTESIAN_POINT('Ctrl Pts',(-19.7638029230144,-4.42739710557802,
134.729419270888));
#151950=CARTESIAN_POINT('Ctrl Pts',(-19.7712102693681,-4.32313572846548,
134.847024269953));
#151951=CARTESIAN_POINT('Ctrl Pts',(-19.7786176157219,-4.21407875672101,
134.960592216365));
#151952=CARTESIAN_POINT('Ctrl Pts',(-19.7860249620757,-4.10057440017407,
135.069711734548));
#151953=CARTESIAN_POINT('Ctrl Pts',(-19.7934267837511,-3.98715469945836,
135.178749867277));
#151954=CARTESIAN_POINT('Ctrl Pts',(-19.8008286054265,-3.86929448653938,
135.283345920376));
#151955=CARTESIAN_POINT('Ctrl Pts',(-19.8082304271019,-3.74738047727398,
135.383123564154));
#151956=CARTESIAN_POINT('Ctrl Pts',(-19.8156283414133,-3.62553082546509,
135.48284853609));
#151957=CARTESIAN_POINT('Ctrl Pts',(-19.8230262557246,-3.49963192730841,
135.577759928578));
#151958=CARTESIAN_POINT('Ctrl Pts',(-19.830424170036,-3.37010530407945,
135.667520166863));
#151959=CARTESIAN_POINT('Ctrl Pts',(-19.8378208549482,-3.2406002058258,
135.757265488624));
#151960=CARTESIAN_POINT('Ctrl Pts',(-19.8452175398604,-3.1074688855274,
135.841861142729));
#151961=CARTESIAN_POINT('Ctrl Pts',(-19.8526142247726,-2.97116380575872,
135.92101149503));
#151962=CARTESIAN_POINT('Ctrl Pts',(-19.860010581708,-2.83486476989991,
136.000158337721));
#151963=CARTESIAN_POINT('Ctrl Pts',(-19.8674069386435,-2.69539257720325,
136.073860171237));
#151964=CARTESIAN_POINT('Ctrl Pts',(-19.8748032955789,-2.55322613900928,
136.141866293964));
#151965=CARTESIAN_POINT('Ctrl Pts',(-19.8822007849155,-2.41103793477069,
136.209882828602));
#151966=CARTESIAN_POINT('Ctrl Pts',(-19.889598274252,-2.26615500047468,
136.272201755031));
#151967=CARTESIAN_POINT('Ctrl Pts',(-19.8969957635886,-2.11907801868945,
136.328619745558));
#151968=CARTESIAN_POINT('Ctrl Pts',(-19.9043958461036,-1.97194947929667,
136.385057513325));
#151969=CARTESIAN_POINT('Ctrl Pts',(-19.9117959286186,-1.82262570942006,
136.435590093083));
#151970=CARTESIAN_POINT('Ctrl Pts',(-19.9191960111336,-1.67162425732287,
136.480063473145));
#151971=CARTESIAN_POINT('Ctrl Pts',(-19.9266042308,-1.52045676360534,136.524585756261));
#151972=CARTESIAN_POINT('Ctrl Pts',(-19.9340124504665,-1.36760826182186,
136.563035428276));
#151973=CARTESIAN_POINT('Ctrl Pts',(-19.9414206701329,-1.21360896440533,
136.595309058367));
#151974=CARTESIAN_POINT('Ctrl Pts',(-19.948833449435,-1.05951488299108,
136.627602552339));
#151975=CARTESIAN_POINT('Ctrl Pts',(-19.956246228737,-0.904268961850489,
136.65371236815));
#151976=CARTESIAN_POINT('Ctrl Pts',(-19.9636590080391,-0.748407803357998,
136.673586829118));
#151977=CARTESIAN_POINT('Ctrl Pts',(-19.9710823790678,-0.592323943132867,
136.693489687649));
#151978=CARTESIAN_POINT('Ctrl Pts',(-19.9785057500965,-0.43562346074044,
136.707139365023));
#151979=CARTESIAN_POINT('Ctrl Pts',(-19.9859291211253,-0.278845067491367,
136.714536248699));
#151980=CARTESIAN_POINT('Ctrl Pts',(-19.9898651705661,-0.195717401542456,
136.71845825391));
#151981=CARTESIAN_POINT('Ctrl Pts',(-19.9938012200071,-0.112567794325544,
136.720623244878));
#151982=CARTESIAN_POINT('Ctrl Pts',(-19.997737269448,-0.0294759789153038,
136.721037195609));
#151983=CARTESIAN_POINT('Ctrl Pts',(-20.0051605358534,0.127232591737446,
136.72181789377));
#151984=CARTESIAN_POINT('Ctrl Pts',(-20.0125838022589,0.284209161504598,
136.716369618254));
#151985=CARTESIAN_POINT('Ctrl Pts',(-20.0200070686643,0.440917721744524,
136.704659095198));
#151986=CARTESIAN_POINT('Ctrl Pts',(-20.0274215613853,0.597441065480305,
136.692962413008));
#151987=CARTESIAN_POINT('Ctrl Pts',(-20.0348360541062,0.753696661586576,
136.675018243465));
#151988=CARTESIAN_POINT('Ctrl Pts',(-20.0422505468273,0.909146727727743,
136.650845269899));
#151989=CARTESIAN_POINT('Ctrl Pts',(-20.049657893181,1.06444696524235,136.626695595154));
#151990=CARTESIAN_POINT('Ctrl Pts',(-20.0570652395348,1.21894285206313,
136.596329125259));
#151991=CARTESIAN_POINT('Ctrl Pts',(-20.0644725858886,1.37210007034716,
136.559816460456));
#151992=CARTESIAN_POINT('Ctrl Pts',(-20.071874407564,1.52514305819995,136.523331028175));
#151993=CARTESIAN_POINT('Ctrl Pts',(-20.0792762292395,1.67684900396512,
136.480708614672));
#151994=CARTESIAN_POINT('Ctrl Pts',(-20.0866780509149,1.82669226144844,
136.432071159559));
#151995=CARTESIAN_POINT('Ctrl Pts',(-20.0940759652263,1.97645641784294,
136.38345937978));
#151996=CARTESIAN_POINT('Ctrl Pts',(-20.1014738795376,2.12435949007881,
136.328838997098));
#151997=CARTESIAN_POINT('Ctrl Pts',(-20.108871793849,2.26988962440962,136.268382181899));
#151998=CARTESIAN_POINT('Ctrl Pts',(-20.1162684787612,2.41539557427146,
136.207935413527));
#151999=CARTESIAN_POINT('Ctrl Pts',(-20.1236651636734,2.55852902447798,
136.141654280692));
#152000=CARTESIAN_POINT('Ctrl Pts',(-20.1310618485856,2.69879668257461,
136.069759655495));
#152001=CARTESIAN_POINT('Ctrl Pts',(-20.138458205521,2.8390581210563,135.997868218181));
#152002=CARTESIAN_POINT('Ctrl Pts',(-20.1458545624565,2.97645368788785,
135.92036395369));
#152003=CARTESIAN_POINT('Ctrl Pts',(-20.1532509193919,3.11051359742387,
135.837514273351));
#152004=CARTESIAN_POINT('Ctrl Pts',(-20.1606484087285,3.24459403187428,
135.754651908514));
#152005=CARTESIAN_POINT('Ctrl Pts',(-20.168045898065,3.37533747459153,135.666442694552));
#152006=CARTESIAN_POINT('Ctrl Pts',(-20.1754433874016,3.50230222907294,
135.573197966305));
#152007=CARTESIAN_POINT('Ctrl Pts',(-20.1828434699166,3.62931149085276,
135.479920551264));
#152008=CARTESIAN_POINT('Ctrl Pts',(-20.1902435524317,3.75253912641491,
135.381604328283));
#152009=CARTESIAN_POINT('Ctrl Pts',(-20.1976436349467,3.87157581388762,
135.278601478295));
#152010=CARTESIAN_POINT('Ctrl Pts',(-20.2050518546132,3.99074339443513,
135.175485366086));
#152011=CARTESIAN_POINT('Ctrl Pts',(-20.2124600742796,4.10571054119851,
135.06767257955));
#152012=CARTESIAN_POINT('Ctrl Pts',(-20.2198682939461,4.21610364212668,
134.955553294538));
#152013=CARTESIAN_POINT('Ctrl Pts',(-20.2272810732482,4.32656468816663,
134.843365001977));
#152014=CARTESIAN_POINT('Ctrl Pts',(-20.2346938525502,4.43244582814584,
134.726865204941));
#152015=CARTESIAN_POINT('Ctrl Pts',(-20.2421066318523,4.53341353831838,
134.606477429697));
#152016=CARTESIAN_POINT('Ctrl Pts',(-20.249530002881,4.63452551588983,134.485917638755));
#152017=CARTESIAN_POINT('Ctrl Pts',(-20.2569533739098,4.73070981439883,
134.361459068963));
#152018=CARTESIAN_POINT('Ctrl Pts',(-20.2643767449386,4.8216755732019,134.233555162833));
#152019=CARTESIAN_POINT('Ctrl Pts',(-20.2683127943793,4.86990780121213,
134.165737442792));
#152020=CARTESIAN_POINT('Ctrl Pts',(-20.27224884382,4.91667366317013,134.096951553825));
#152021=CARTESIAN_POINT('Ctrl Pts',(-20.2761848932607,4.96193508750228,
134.027267806722));
#152022=CARTESIAN_POINT('Ctrl Pts',(-20.2836081596662,5.04729672123318,
133.89584643444));
#152023=CARTESIAN_POINT('Ctrl Pts',(-20.2910314260716,5.12756260306324,
133.76083267449));
#152024=CARTESIAN_POINT('Ctrl Pts',(-20.298454692477,5.20241501298613,133.622659500786));
#152025=CARTESIAN_POINT('Ctrl Pts',(-20.305869185198,5.2771789535767,133.484649636298));
#152026=CARTESIAN_POINT('Ctrl Pts',(-20.3132836779191,5.34654198198527,
133.343488115957));
#152027=CARTESIAN_POINT('Ctrl Pts',(-20.3206981706401,5.41022913253789,
133.199637490067));
#152028=CARTESIAN_POINT('Ctrl Pts',(-20.3281055169939,5.47385489901702,
133.055925512827));
#152029=CARTESIAN_POINT('Ctrl Pts',(-20.3355128633477,5.53181552846948,
132.909529928972));
#152030=CARTESIAN_POINT('Ctrl Pts',(-20.3429202097014,5.58388160703363,
132.760938436394));
#152031=CARTESIAN_POINT('Ctrl Pts',(-20.3503220313768,5.63590885275183,
132.612457768958));
#152032=CARTESIAN_POINT('Ctrl Pts',(-20.3577238530522,5.68205017845196,
132.461784804643));
#152033=CARTESIAN_POINT('Ctrl Pts',(-20.3651256747276,5.72212405077568,
132.309427695817));
#152034=CARTESIAN_POINT('Ctrl Pts',(-20.3725235890389,5.7621767684143,132.157151015122));
#152035=CARTESIAN_POINT('Ctrl Pts',(-20.3799215033503,5.79616831681066,
132.003192320601));
#152036=CARTESIAN_POINT('Ctrl Pts',(-20.3873194176616,5.82396687833496,
131.848075311607));
#152037=CARTESIAN_POINT('Ctrl Pts',(-20.3947161025738,5.8517608202426,131.692984080246));
#152038=CARTESIAN_POINT('Ctrl Pts',(-20.4021127874861,5.87336375207505,
131.536735283534));
#152039=CARTESIAN_POINT('Ctrl Pts',(-20.4095094723983,5.88869486316469,
131.379863329148));
#152040=CARTESIAN_POINT('Ctrl Pts',(-20.4169058293338,5.9040252944568,131.222998330629));
#152041=CARTESIAN_POINT('Ctrl Pts',(-20.4243021862691,5.91308442165166,
131.065510600904));
#152042=CARTESIAN_POINT('Ctrl Pts',(-20.4316985432046,5.91584329485683,
130.907939926298));
#152043=CARTESIAN_POINT('Ctrl Pts',(-20.4390960325412,5.91860259045253,
130.75034512722));
#152044=CARTESIAN_POINT('Ctrl Pts',(-20.4464935218778,5.91505970490617,
130.592667731239));
#152045=CARTESIAN_POINT('Ctrl Pts',(-20.4538910112144,5.90523782528847,
130.435447634219));
#152046=CARTESIAN_POINT('Ctrl Pts',(-20.4612910937293,5.8954125026261,130.278172423937));
#152047=CARTESIAN_POINT('Ctrl Pts',(-20.4686911762443,5.87930382679594,
130.121355204123));
#152048=CARTESIAN_POINT('Ctrl Pts',(-20.4760912587593,5.85698684912133,
129.965530711256));
#152049=CARTESIAN_POINT('Ctrl Pts',(-20.4834994784258,5.8346453316355,129.80953487334));
#152050=CARTESIAN_POINT('Ctrl Pts',(-20.4909076980923,5.80608193196049,
129.654534312133));
#152051=CARTESIAN_POINT('Ctrl Pts',(-20.4983159177588,5.77142296965002,
129.501054257612));
#152052=CARTESIAN_POINT('Ctrl Pts',(-20.5057286970609,5.73674267532657,
129.347479738679));
#152053=CARTESIAN_POINT('Ctrl Pts',(-20.5131414763629,5.6959594390843,129.195427950941));
#152054=CARTESIAN_POINT('Ctrl Pts',(-20.520554255665,5.64924930783475,129.045408423665));
#152055=CARTESIAN_POINT('Ctrl Pts',(-20.5279776266938,5.60247243495918,
128.895174541453));
#152056=CARTESIAN_POINT('Ctrl Pts',(-20.5354009977225,5.54975187811928,
128.746979069994));
#152057=CARTESIAN_POINT('Ctrl Pts',(-20.5428243687512,5.4913119140608,128.601311815339));
#152058=CARTESIAN_POINT('Ctrl Pts',(-20.546760418192,5.46032564286905,128.524075541682));
#152059=CARTESIAN_POINT('Ctrl Pts',(-20.5506964676328,5.42773221707083,
128.447549644362));
#152060=CARTESIAN_POINT('Ctrl Pts',(-20.5546325170737,5.3935702125098,128.371804158771));
#152061=CARTESIAN_POINT('Ctrl Pts',(-20.5620557834791,5.32914173806776,
128.228950536882));
#152062=CARTESIAN_POINT('Ctrl Pts',(-20.5694790498846,5.25893650776519,
128.088442342102));
#152063=CARTESIAN_POINT('Ctrl Pts',(-20.57690231629,5.18314705939539,127.950780914249));
#152064=CARTESIAN_POINT('Ctrl Pts',(-20.584316809011,5.10744718785952,127.813282190772));
#152065=CARTESIAN_POINT('Ctrl Pts',(-20.591731301732,5.0261764140352,127.678623860702));
#152066=CARTESIAN_POINT('Ctrl Pts',(-20.5991457944531,4.93957526893164,
127.547287280188));
#152067=CARTESIAN_POINT('Ctrl Pts',(-20.6065531408069,4.85305759327196,
127.416077286815));
#152068=CARTESIAN_POINT('Ctrl Pts',(-20.6139604871607,4.76121997842291,
127.288182978741));
#152069=CARTESIAN_POINT('Ctrl Pts',(-20.6213678335145,4.66434873463549,
127.16406098097));
#152070=CARTESIAN_POINT('Ctrl Pts',(-20.6287696551899,4.56754974107713,
127.040031558067));
#152071=CARTESIAN_POINT('Ctrl Pts',(-20.6361714768653,4.46572482252367,
126.919769136361));
#152072=CARTESIAN_POINT('Ctrl Pts',(-20.6435732985407,4.35920337874054,
126.803701113775));
#152073=CARTESIAN_POINT('Ctrl Pts',(-20.650971212852,4.25273816679812,126.687694362593));
#152074=CARTESIAN_POINT('Ctrl Pts',(-20.6583691271634,4.14158161895885,
126.575877875198));
#152075=CARTESIAN_POINT('Ctrl Pts',(-20.6657670414748,4.0261030876717,126.468645625787));
#152076=CARTESIAN_POINT('Ctrl Pts',(-20.673163726387,3.91064374682128,126.36143119643));
#152077=CARTESIAN_POINT('Ctrl Pts',(-20.6805604112992,3.79086412128721,
126.25879974684));
#152078=CARTESIAN_POINT('Ctrl Pts',(-20.6879570962114,3.66717014324457,
126.161108125724));
#152079=CARTESIAN_POINT('Ctrl Pts',(-20.6953534531469,3.54348164992218,
126.063420836357));
#152080=CARTESIAN_POINT('Ctrl Pts',(-20.7027498100824,3.41587944215051,
125.970673171312));
#152081=CARTESIAN_POINT('Ctrl Pts',(-20.7101461670179,3.28480200932697,
125.883181254647));
#152082=CARTESIAN_POINT('Ctrl Pts',(-20.7175436563545,3.15370450821347,
125.795675942745));
#152083=CARTESIAN_POINT('Ctrl Pts',(-20.7249411456912,3.01913103313984,
125.713428188682));
#152084=CARTESIAN_POINT('Ctrl Pts',(-20.7323386350278,2.88154834696496,
125.636710311421));
#152085=CARTESIAN_POINT('Ctrl Pts',(-20.7397387175428,2.74391743139351,
125.559965540827));
#152086=CARTESIAN_POINT('Ctrl Pts',(-20.7471388000578,2.60327553030642,
125.488754688241));
#152087=CARTESIAN_POINT('Ctrl Pts',(-20.7545388825728,2.4601130997225,125.423303648989));
#152088=CARTESIAN_POINT('Ctrl Pts',(-20.7619471022393,2.31679324732848,
125.35778063959));
#152089=CARTESIAN_POINT('Ctrl Pts',(-20.7693553219058,2.17094767011622,
125.298030247263));
#152090=CARTESIAN_POINT('Ctrl Pts',(-20.7767635415723,2.02308653774545,
125.244230095421));
#152091=CARTESIAN_POINT('Ctrl Pts',(-20.7841763208744,1.87513439931468,
125.190396830482));
#152092=CARTESIAN_POINT('Ctrl Pts',(-20.7915891001764,1.72516458858511,
125.142521216831));
#152093=CARTESIAN_POINT('Ctrl Pts',(-20.7990018794785,1.57370094461438,
125.100730554227));
#152094=CARTESIAN_POINT('Ctrl Pts',(-20.8064252505072,1.42202088228663,
125.058880179166));
#152095=CARTESIAN_POINT('Ctrl Pts',(-20.8138486215361,1.26884308629081,
125.02313220456));
#152096=CARTESIAN_POINT('Ctrl Pts',(-20.8212719925648,1.11470087138906,
124.993562692167));
#152097=CARTESIAN_POINT('Ctrl Pts',(-20.8252080420055,1.03297097045967,
124.977884227186));
#152098=CARTESIAN_POINT('Ctrl Pts',(-20.8291440914461,0.950970022939117,
124.963941882654));
#152099=CARTESIAN_POINT('Ctrl Pts',(-20.8330801408867,0.868777802772557,
124.951741059461));
#152100=CARTESIAN_POINT('Ctrl Pts',(-20.8405034072921,0.71376584066374,
124.928730687694));
#152101=CARTESIAN_POINT('Ctrl Pts',(-20.8479266736976,0.557604675160329,
124.911848224881));
#152102=CARTESIAN_POINT('Ctrl Pts',(-20.855349940103,0.400820169029187,
124.901202669942));
#152103=CARTESIAN_POINT('Ctrl Pts',(-20.862764432824,0.244220969164372,
124.890569697164));
#152104=CARTESIAN_POINT('Ctrl Pts',(-20.870178925545,0.0870002639540167,
124.886158984275));
#152105=CARTESIAN_POINT('Ctrl Pts',(-20.877593418266,-0.0703069551563289,
124.888028350481));
#152106=CARTESIAN_POINT('Ctrl Pts',(-20.8850007646198,-0.227462555646608,
124.88989591492));
#152107=CARTESIAN_POINT('Ctrl Pts',(-20.8924081109736,-0.384704133267359,
124.898031503764));
#152108=CARTESIAN_POINT('Ctrl Pts',(-20.8998154573273,-0.541492758788583,
124.912441053054));
#152109=CARTESIAN_POINT('Ctrl Pts',(-20.9072172790027,-0.698164445437596,
124.926839855159));
#152110=CARTESIAN_POINT('Ctrl Pts',(-20.9146191006782,-0.854383482518331,
124.947503266464));
#152111=CARTESIAN_POINT('Ctrl Pts',(-20.9220209223536,-1.00961223943391,
124.974385172636));
#152112=CARTESIAN_POINT('Ctrl Pts',(-20.9294188366649,-1.16475905229657,
125.001252888059));
#152113=CARTESIAN_POINT('Ctrl Pts',(-20.9368167509762,-1.31891625920597,
125.034332497166));
#152114=CARTESIAN_POINT('Ctrl Pts',(-20.9442146652875,-1.47155275449112,
125.07352620596));
#152115=CARTESIAN_POINT('Ctrl Pts',(-20.9516113501998,-1.62416388436031,
125.11271340147));
#152116=CARTESIAN_POINT('Ctrl Pts',(-20.959008035112,-1.77525444295494,
125.158012587351));
#152117=CARTESIAN_POINT('Ctrl Pts',(-20.9664047200242,-1.92430478709526,
125.209275126811));
#152118=CARTESIAN_POINT('Ctrl Pts',(-20.9738010769597,-2.07334852218692,
125.260535393235));
#152119=CARTESIAN_POINT('Ctrl Pts',(-20.9811974338951,-2.22035186969653,
125.317758366071));
#152120=CARTESIAN_POINT('Ctrl Pts',(-20.9885937908305,-2.36481185127169,
125.380746004544));
#152121=CARTESIAN_POINT('Ctrl Pts',(-20.9959912801671,-2.50929395003902,
125.443743286586));
#152122=CARTESIAN_POINT('Ctrl Pts',(-21.0033887695036,-2.6512315653259,
125.512506842399));
#152123=CARTESIAN_POINT('Ctrl Pts',(-21.0107862588402,-2.79014329074996,
125.586791166223));
#152124=CARTESIAN_POINT('Ctrl Pts',(-21.0181863413553,-2.92910371146462,
125.661101530302));
#152125=CARTESIAN_POINT('Ctrl Pts',(-21.0255864238703,-3.06503580144865,
125.740936339628));
#152126=CARTESIAN_POINT('Ctrl Pts',(-21.0329865063853,-3.19748440510901,
125.826005061603));
#152127=CARTESIAN_POINT('Ctrl Pts',(-21.0403947260518,-3.33007864962458,
125.911167325383));
#152128=CARTESIAN_POINT('Ctrl Pts',(-21.0478029457183,-3.459181443868,126.001574793515));
#152129=CARTESIAN_POINT('Ctrl Pts',(-21.0552111653848,-3.58436758906766,
126.096894255611));
#152130=CARTESIAN_POINT('Ctrl Pts',(-21.0626239446869,-3.70963078425137,
126.192272385245));
#152131=CARTESIAN_POINT('Ctrl Pts',(-21.0700367239889,-3.83097223984001,
126.292568295772));
#152132=CARTESIAN_POINT('Ctrl Pts',(-21.077449503291,-3.94800170713282,
126.397410075187));
#152133=CARTESIAN_POINT('Ctrl Pts',(-21.0848728743198,-4.06519839161614,
126.502401657452));
#152134=CARTESIAN_POINT('Ctrl Pts',(-21.0922962453486,-4.17807051539867,
126.611951821977));
#152135=CARTESIAN_POINT('Ctrl Pts',(-21.0997196163774,-4.28626581591441,
126.725652989184));
#152136=CARTESIAN_POINT('Ctrl Pts',(-21.1036556658181,-4.34363356035738,
126.785940076258));
#152137=CARTESIAN_POINT('Ctrl Pts',(-21.1075917152587,-4.39968716480038,
126.847393618015));
#152138=CARTESIAN_POINT('Ctrl Pts',(-21.1115277646994,-4.45437896555516,
126.90994941769));
#152139=CARTESIAN_POINT('Ctrl Pts',(-21.1188905251277,-4.55668525830135,
127.026966079533));
#152140=CARTESIAN_POINT('Ctrl Pts',(-21.1262532855559,-4.65454638571701,
127.148210387153));
#152141=CARTESIAN_POINT('Ctrl Pts',(-21.1336160459842,-4.74758812446407,
127.273307295546));
#152142=CARTESIAN_POINT('Ctrl Pts',(-21.141033077726,-4.84131567900425,
127.399326300157));
#152143=CARTESIAN_POINT('Ctrl Pts',(-21.1484501094678,-4.93015219722535,
127.529254695775));
#152144=CARTESIAN_POINT('Ctrl Pts',(-21.1558671412097,-5.01375270467083,
127.662670884491));
#152145=CARTESIAN_POINT('Ctrl Pts',(-21.1632118482149,-5.09653800936527,
127.794786109286));
#152146=CARTESIAN_POINT('Ctrl Pts',(-21.1705565552201,-5.17418873204522,
127.930321095861));
#152147=CARTESIAN_POINT('Ctrl Pts',(-21.1779012622253,-5.24641037403859,
128.068833474641));
#152148=CARTESIAN_POINT('Ctrl Pts',(-21.1852409137826,-5.31858230502862,
128.207250513726));
#152149=CARTESIAN_POINT('Ctrl Pts',(-21.1925805653399,-5.38533241623092,
128.348640531718));
#152150=CARTESIAN_POINT('Ctrl Pts',(-21.1999202168971,-5.44641050684016,
128.492533817505));
#152151=CARTESIAN_POINT('Ctrl Pts',(-21.2072563252452,-5.50745911206495,
128.636357638959));
#152152=CARTESIAN_POINT('Ctrl Pts',(-21.2145924335934,-5.56284099861111,
128.782681973944));
#152153=CARTESIAN_POINT('Ctrl Pts',(-21.2219285419415,-5.61235286949372,
128.931014458741));
#152154=CARTESIAN_POINT('Ctrl Pts',(-21.229403230762,-5.6628000289697,129.082148972194));
#152155=CARTESIAN_POINT('Ctrl Pts',(-21.2368779195825,-5.70715300054209,
129.235367901247));
#152156=CARTESIAN_POINT('Ctrl Pts',(-21.2443526084031,-5.74524894773119,
129.390131113174));
#152157=CARTESIAN_POINT('Ctrl Pts',(-21.2516875524619,-5.78263266338919,
129.542000913923));
#152158=CARTESIAN_POINT('Ctrl Pts',(-21.2590224965208,-5.81399119400866,
129.695357374521));
#152159=CARTESIAN_POINT('Ctrl Pts',(-21.2663574405796,-5.83922173065768,
129.849677349296));
#152160=CARTESIAN_POINT('Ctrl Pts',(-21.273902001781,-5.86517330252611,
130.008407461612));
#152161=CARTESIAN_POINT('Ctrl Pts',(-21.2814465629825,-5.88464130933544,
130.168156564734));
#152162=CARTESIAN_POINT('Ctrl Pts',(-21.2889911241839,-5.89757087839648,
130.328347700945));
#152163=CARTESIAN_POINT('Ctrl Pts',(-21.2965356853853,-5.91050044745754,
130.488538837157));
#152164=CARTESIAN_POINT('Ctrl Pts',(-21.3040802465867,-5.91689157699635,
130.649171569774));
#152165=CARTESIAN_POINT('Ctrl Pts',(-21.3116248077882,-5.91674761992799,
130.809667648422));
#152166=CARTESIAN_POINT('',(-23.0616248077882,-5.9221143857238,130.804232609979));
#152167=CARTESIAN_POINT('Ctrl Pts',(-21.3116260420174,-5.91389133234292,
130.809691329677));
#152168=CARTESIAN_POINT('Ctrl Pts',(-21.337742490849,-5.91867273821186,
131.365005195582));
#152169=CARTESIAN_POINT('Ctrl Pts',(-21.4566748142849,-5.59177582902208,
133.888337854231));
#152170=CARTESIAN_POINT('Ctrl Pts',(-21.6684230123253,-1.999537622794,137.511029673468));
#152171=CARTESIAN_POINT('Ctrl Pts',(-21.9468706361382,4.56171169292535,
136.111746693683));
#152172=CARTESIAN_POINT('Ctrl Pts',(-22.2253182599512,6.93097081485253,
129.835235190171));
#152173=CARTESIAN_POINT('Ctrl Pts',(-22.5037658837639,2.93100635467636,
124.449302610028));
#152174=CARTESIAN_POINT('Ctrl Pts',(-22.7822135075769,-3.76240975782294,
124.903357876965));
#152175=CARTESIAN_POINT('Ctrl Pts',(-22.9681664822516,-5.92343974002014,
128.827996518787));
#152176=CARTESIAN_POINT('Ctrl Pts',(-23.061303582322,-5.92653152972454,
130.79743998992));
#152177=CARTESIAN_POINT('Ctrl Pts',(-23.0616248077882,-5.92652937499865,
130.804232514548));
#152178=CARTESIAN_POINT('',(-24.8116247921649,-5.91465124248381,130.799116998419));
#152179=CARTESIAN_POINT('Ctrl Pts',(-23.0616248077882,-5.9167499986178,
130.804232725931));
#152180=CARTESIAN_POINT('Ctrl Pts',(-23.06904344305,-5.91675338383835,130.960845812215));
#152181=CARTESIAN_POINT('Ctrl Pts',(-23.0764620783118,-5.91053428214121,
131.11769729394));
#152182=CARTESIAN_POINT('Ctrl Pts',(-23.0838807135736,-5.89806180331044,
131.27425159091));
#152183=CARTESIAN_POINT('Ctrl Pts',(-23.0912905785281,-5.88560406943866,
131.430620809459));
#152184=CARTESIAN_POINT('Ctrl Pts',(-23.0987004434825,-5.86690770278589,
131.586693173578));
#152185=CARTESIAN_POINT('Ctrl Pts',(-23.106110308437,-5.84199377780407,
131.741931554935));
#152186=CARTESIAN_POINT('Ctrl Pts',(-23.1135130349591,-5.81710385411908,
131.897020384486));
#152187=CARTESIAN_POINT('Ctrl Pts',(-23.1209157614812,-5.78600835519952,
132.051276464101));
#152188=CARTESIAN_POINT('Ctrl Pts',(-23.1283184880033,-5.7487802566815,
132.204166362264));
#152189=CARTESIAN_POINT('Ctrl Pts',(-23.1357157023083,-5.71157987894451,
132.356942415574));
#152190=CARTESIAN_POINT('Ctrl Pts',(-23.1431129166133,-5.66825608191381,
132.508353951294));
#152191=CARTESIAN_POINT('Ctrl Pts',(-23.1505101309183,-5.61893314033713,
132.65787644618));
#152192=CARTESIAN_POINT('Ctrl Pts',(-23.1579034548305,-5.56963613901479,
132.807320303185));
#152193=CARTESIAN_POINT('Ctrl Pts',(-23.1652967787427,-5.51434639340068,
132.954876743804));
#152194=CARTESIAN_POINT('Ctrl Pts',(-23.1726901026549,-5.45323834317587,
133.100035275486));
#152195=CARTESIAN_POINT('Ctrl Pts',(-23.180082221126,-5.39214025628437,
133.245170139863));
#152196=CARTESIAN_POINT('Ctrl Pts',(-23.187474339597,-5.32522589225838,
133.387907526963));
#152197=CARTESIAN_POINT('Ctrl Pts',(-23.1948664580682,-5.25271830153739,
133.527755742625));
#152198=CARTESIAN_POINT('Ctrl Pts',(-23.202258272332,-5.18021369471566,
133.667598203123));
#152199=CARTESIAN_POINT('Ctrl Pts',(-23.2096500865959,-5.10211649090185,
133.8045513967));
#152200=CARTESIAN_POINT('Ctrl Pts',(-23.2170419008597,-5.01869616088841,
133.938147369594));
#152201=CARTESIAN_POINT('Ctrl Pts',(-23.2244348753669,-4.93526273694747,
134.071764312148));
#152202=CARTESIAN_POINT('Ctrl Pts',(-23.231827849874,-4.84650472121751,
134.202022667709));
#152203=CARTESIAN_POINT('Ctrl Pts',(-23.2392208243811,-4.75273536194316,
134.328482797888));
#152204=CARTESIAN_POINT('Ctrl Pts',(-23.2466164240032,-4.65893270682275,
134.454987831829));
#152205=CARTESIAN_POINT('Ctrl Pts',(-23.2540120236253,-4.56011538792318,
134.577691655166));
#152206=CARTESIAN_POINT('Ctrl Pts',(-23.2614076232473,-4.45663732663343,
134.696187219736));
#152207=CARTESIAN_POINT('Ctrl Pts',(-23.2688113610781,-4.35304539681253,
134.814813178282));
#152208=CARTESIAN_POINT('Ctrl Pts',(-23.276215098909,-4.24478272858463,
134.929221348638));
#152209=CARTESIAN_POINT('Ctrl Pts',(-23.2836188367398,-4.1322410363748,
135.03904060309));
#152210=CARTESIAN_POINT('Ctrl Pts',(-23.2910271706411,-4.01962948086737,
135.148928030813));
#152211=CARTESIAN_POINT('Ctrl Pts',(-23.2984355045423,-3.90273388561915,
135.254220616916));
#152212=CARTESIAN_POINT('Ctrl Pts',(-23.3058438384435,-3.78197908895288,
135.35458750567));
#152213=CARTESIAN_POINT('Ctrl Pts',(-23.3132626868675,-3.66105290704956,
135.455096843448));
#152214=CARTESIAN_POINT('Ctrl Pts',(-23.3206815352914,-3.53625688098093,
135.550666295677));
#152215=CARTESIAN_POINT('Ctrl Pts',(-23.3281003837154,-3.40804549595954,
135.641007850926));
#152216=CARTESIAN_POINT('Ctrl Pts',(-23.3317698408778,-3.34463050778605,
135.685691937731));
#152217=CARTESIAN_POINT('Ctrl Pts',(-23.3354392980403,-3.28038037848562,
135.729097762255));
#152218=CARTESIAN_POINT('Ctrl Pts',(-23.3391087552027,-3.21535223655167,
135.771194675334));
#152219=CARTESIAN_POINT('Ctrl Pts',(-23.3465320216081,-3.08380111057824,
135.856356209261));
#152220=CARTESIAN_POINT('Ctrl Pts',(-23.3539552880136,-2.9486653559629,
135.936416530185));
#152221=CARTESIAN_POINT('Ctrl Pts',(-23.361378554419,-2.81037842963538,
136.011058577381));
#152222=CARTESIAN_POINT('Ctrl Pts',(-23.36879304714,-2.67225494697077,136.085612403876));
#152223=CARTESIAN_POINT('Ctrl Pts',(-23.376207539861,-2.5309880313707,136.154760528159));
#152224=CARTESIAN_POINT('Ctrl Pts',(-23.383622032582,-2.38704065105636,
136.218228688798));
#152225=CARTESIAN_POINT('Ctrl Pts',(-23.3910293789357,-2.24323201264648,
136.281635676434));
#152226=CARTESIAN_POINT('Ctrl Pts',(-23.3984367252895,-2.0967483921047,
136.339373449612));
#152227=CARTESIAN_POINT('Ctrl Pts',(-23.4058440716433,-1.94807783588486,
136.391213336927));
#152228=CARTESIAN_POINT('Ctrl Pts',(-23.4132458933187,-1.79951816377508,
136.443014560099));
#152229=CARTESIAN_POINT('Ctrl Pts',(-23.4206477149941,-1.64877515469279,
136.488926533766));
#152230=CARTESIAN_POINT('Ctrl Pts',(-23.4280495366695,-1.49635723668165,
136.528768498101));
#152231=CARTESIAN_POINT('Ctrl Pts',(-23.4354474509808,-1.34401977890322,
136.568589430173));
#152232=CARTESIAN_POINT('Ctrl Pts',(-23.4428453652921,-1.19000953331409,
136.602346640283));
#152233=CARTESIAN_POINT('Ctrl Pts',(-23.4502432796035,-1.03485039926491,
136.629909107935));
#152234=CARTESIAN_POINT('Ctrl Pts',(-23.4576399645157,-0.879717049848722,
136.657466995205));
#152235=CARTESIAN_POINT('Ctrl Pts',(-23.4650366494279,-0.723435558084921,
136.678832117951));
#152236=CARTESIAN_POINT('Ctrl Pts',(-23.4724333343401,-0.566540454012888,
136.693924478878));
#152237=CARTESIAN_POINT('Ctrl Pts',(-23.4798296912756,-0.409652306833961,
136.709016170593));
#152238=CARTESIAN_POINT('Ctrl Pts',(-23.487226048211,-0.252150973028266,
136.717835617782));
#152239=CARTESIAN_POINT('Ctrl Pts',(-23.4946224051465,-0.0945762823509183,
136.720354692049));
#152240=CARTESIAN_POINT('Ctrl Pts',(-23.502019894483,0.0630225334133913,
136.722874151993));
#152241=CARTESIAN_POINT('Ctrl Pts',(-23.5094173838196,0.220694355137821,
136.719091312394));
#152242=CARTESIAN_POINT('Ctrl Pts',(-23.5168148731562,0.377899322870641,
136.709030181926));
#152243=CARTESIAN_POINT('Ctrl Pts',(-23.5242149556712,0.535159398561426,
136.698965524544));
#152244=CARTESIAN_POINT('Ctrl Pts',(-23.5316150381861,0.691951922121476,
136.682618218254));
#152245=CARTESIAN_POINT('Ctrl Pts',(-23.5390151207011,0.847742271905184,
136.66006412807));
#152246=CARTESIAN_POINT('Ctrl Pts',(-23.5464233403676,1.00370392919434,
136.637485237345));
#152247=CARTESIAN_POINT('Ctrl Pts',(-23.5538315600341,1.15866084228152,
136.608685986277));
#152248=CARTESIAN_POINT('Ctrl Pts',(-23.5612397797006,1.31208797403423,
136.573793493586));
#152249=CARTESIAN_POINT('Ctrl Pts',(-23.5686525590026,1.46560953762647,
136.538879525147));
#152250=CARTESIAN_POINT('Ctrl Pts',(-23.5760653383046,1.61759908414759,
136.497864939193));
#152251=CARTESIAN_POINT('Ctrl Pts',(-23.5834781176067,1.76754735283541,
136.450926557851));
#152252=CARTESIAN_POINT('Ctrl Pts',(-23.5909014886354,1.91770987464118,
136.403921108748));
#152253=CARTESIAN_POINT('Ctrl Pts',(-23.5983248596642,2.06582494277933,
136.350975084677));
#152254=CARTESIAN_POINT('Ctrl Pts',(-23.605748230693,2.21140309307698,136.292313507527));
#152255=CARTESIAN_POINT('Ctrl Pts',(-23.6096842801338,2.2885921214657,136.261209731756));
#152256=CARTESIAN_POINT('Ctrl Pts',(-23.6136203295746,2.36506832852509,
136.228499884312));
#152257=CARTESIAN_POINT('Ctrl Pts',(-23.6175563790155,2.4407617376494,136.194222647574));
#152258=CARTESIAN_POINT('Ctrl Pts',(-23.6249796454209,2.58351714494553,
136.129576848845));
#152259=CARTESIAN_POINT('Ctrl Pts',(-23.6324029118264,2.72391833660915,
136.059157870285));
#152260=CARTESIAN_POINT('Ctrl Pts',(-23.6398261782318,2.86146426641368,
135.98315901242));
#152261=CARTESIAN_POINT('Ctrl Pts',(-23.6472406709528,2.99884762835166,
135.907249978892));
#152262=CARTESIAN_POINT('Ctrl Pts',(-23.6546551636738,3.13338212220588,
135.825774372123));
#152263=CARTESIAN_POINT('Ctrl Pts',(-23.6620696563948,3.26458675843334,
135.738973455384));
#152264=CARTESIAN_POINT('Ctrl Pts',(-23.6694770027486,3.395664934693,135.652256200637));
#152265=CARTESIAN_POINT('Ctrl Pts',(-23.6768843491024,3.52341933345018,
135.560224058769));
#152266=CARTESIAN_POINT('Ctrl Pts',(-23.6842916954562,3.6473937659479,135.463164034606));
#152267=CARTESIAN_POINT('Ctrl Pts',(-23.6916935171316,3.77127573363693,
135.366176401471));
#152268=CARTESIAN_POINT('Ctrl Pts',(-23.6990953388071,3.89138305588978,
135.264168581894));
#152269=CARTESIAN_POINT('Ctrl Pts',(-23.7064971604825,4.00728883656822,
135.157470625688));
#152270=CARTESIAN_POINT('Ctrl Pts',(-23.7138950747938,4.12313343148609,
135.050828994504));
#152271=CARTESIAN_POINT('Ctrl Pts',(-23.7212929891051,4.23478062805544,
134.939502409724));
#152272=CARTESIAN_POINT('Ctrl Pts',(-23.7286909034164,4.34183701462641,
134.82386082293));
#152273=CARTESIAN_POINT('Ctrl Pts',(-23.7360875883286,4.44887561036875,
134.708238453669));
#152274=CARTESIAN_POINT('Ctrl Pts',(-23.7434842732408,4.55132465691304,
134.588302779243));
#152275=CARTESIAN_POINT('Ctrl Pts',(-23.7508809581531,4.6488279237252,134.464460274419));
#152276=CARTESIAN_POINT('Ctrl Pts',(-23.7582773150885,4.74632686714018,
134.340623260901));
#152277=CARTESIAN_POINT('Ctrl Pts',(-23.765673672024,4.83888023594587,134.212880054734));
#152278=CARTESIAN_POINT('Ctrl Pts',(-23.7730700289595,4.92617257375734,
134.081669625893));
#152279=CARTESIAN_POINT('Ctrl Pts',(-23.7804675182961,5.01347827624883,
133.9504391084));
#152280=CARTESIAN_POINT('Ctrl Pts',(-23.7878650076327,5.09552113714935,
133.815740622081));
#152281=CARTESIAN_POINT('Ctrl Pts',(-23.7952624969693,5.17202954814514,
133.678041343676));
#152282=CARTESIAN_POINT('Ctrl Pts',(-23.8026625794843,5.2485647790457,133.540293795002));
#152283=CARTESIAN_POINT('Ctrl Pts',(-23.8100626619992,5.3195615161386,133.399543685981));
#152284=CARTESIAN_POINT('Ctrl Pts',(-23.8174627445142,5.38479461075073,
133.256281815837));
#152285=CARTESIAN_POINT('Ctrl Pts',(-23.8248709641806,5.4500994358565,133.112862414539));
#152286=CARTESIAN_POINT('Ctrl Pts',(-23.8322791838472,5.50962780685286,
132.966926076288));
#152287=CARTESIAN_POINT('Ctrl Pts',(-23.8396874035136,5.56320287692264,
132.818983240466));
#152288=CARTESIAN_POINT('Ctrl Pts',(-23.8471001828157,5.61681092155418,
132.670949348296));
#152289=CARTESIAN_POINT('Ctrl Pts',(-23.8545129621178,5.66445825124413,
132.520906852696));
#152290=CARTESIAN_POINT('Ctrl Pts',(-23.8619257414199,5.70601836357232,
132.369379785843));
#152291=CARTESIAN_POINT('Ctrl Pts',(-23.8693491124487,5.74763785893798,
132.217636210012));
#152292=CARTESIAN_POINT('Ctrl Pts',(-23.8767724834774,5.78315268161847,
132.064404189062));
#152293=CARTESIAN_POINT('Ctrl Pts',(-23.8841958545062,5.81248758155938,
131.91021715289));
#152294=CARTESIAN_POINT('Ctrl Pts',(-23.8881319039469,5.82804164938912,
131.828463486645));
#152295=CARTESIAN_POINT('Ctrl Pts',(-23.8920679533876,5.84185918629352,
131.746441416203));
#152296=CARTESIAN_POINT('Ctrl Pts',(-23.8960040028284,5.85393491279052,
131.664230723636));
#152297=CARTESIAN_POINT('Ctrl Pts',(-23.9034272692338,5.87670935609358,
131.50918392316));
#152298=CARTESIAN_POINT('Ctrl Pts',(-23.9108505356393,5.89335414864615,
131.352997246254));
#152299=CARTESIAN_POINT('Ctrl Pts',(-23.9182738020448,5.90376109192957,
131.196196720954));
#152300=CARTESIAN_POINT('Ctrl Pts',(-23.9256882947658,5.91415573507031,
131.039581520854));
#152301=CARTESIAN_POINT('Ctrl Pts',(-23.9331027874867,5.91832717970208,
130.882354285348));
#152302=CARTESIAN_POINT('Ctrl Pts',(-23.9405172802078,5.9162184208524,130.725050093253));
#152303=CARTESIAN_POINT('Ctrl Pts',(-23.9479246265615,5.91411169450389,
130.567897516862));
#152304=CARTESIAN_POINT('Ctrl Pts',(-23.9553319729153,5.90573682016777,
130.410668502306));
#152305=CARTESIAN_POINT('Ctrl Pts',(-23.9627393192691,5.89108868196553,
130.253901987224));
#152306=CARTESIAN_POINT('Ctrl Pts',(-23.9701411409445,5.87645146889744,
130.097252394525));
#152307=CARTESIAN_POINT('Ctrl Pts',(-23.9775429626198,5.85555034273875,
129.941064984538));
#152308=CARTESIAN_POINT('Ctrl Pts',(-23.9849447842952,5.82843223595262,
129.785877317061));
#152309=CARTESIAN_POINT('Ctrl Pts',(-23.9923426986066,5.80132844460386,
129.630771571944));
#152310=CARTESIAN_POINT('Ctrl Pts',(-23.9997406129179,5.76801427277528,
129.47666488508));
#152311=CARTESIAN_POINT('Ctrl Pts',(-24.0071385272293,5.72858832260481,
129.324088212697));
#152312=CARTESIAN_POINT('Ctrl Pts',(-24.0145352121415,5.68916892431204,
129.17153689579));
#152313=CARTESIAN_POINT('Ctrl Pts',(-24.0219318970538,5.64363985677666,
129.020515449806));
#152314=CARTESIAN_POINT('Ctrl Pts',(-24.029328581966,5.59215054742784,128.871543291122));
#152315=CARTESIAN_POINT('Ctrl Pts',(-24.0367249389014,5.54066352116895,
128.72257773802));
#152316=CARTESIAN_POINT('Ctrl Pts',(-24.0441212958367,5.48321690052589,
128.575661644361));
#152317=CARTESIAN_POINT('Ctrl Pts',(-24.0515176527722,5.42000949149078,
128.431297686532));
#152318=CARTESIAN_POINT('Ctrl Pts',(-24.0589151421087,5.35679240524017,
128.286911626212));
#152319=CARTESIAN_POINT('Ctrl Pts',(-24.0663126314454,5.28781292416555,
128.145078821713));
#152320=CARTESIAN_POINT('Ctrl Pts',(-24.0737101207819,5.2133172863627,128.006280305243));
#152321=CARTESIAN_POINT('Ctrl Pts',(-24.081110203297,5.13879553422885,127.867433133166));
#152322=CARTESIAN_POINT('Ctrl Pts',(-24.088510285812,5.05875395184917,127.731622695578));
#152323=CARTESIAN_POINT('Ctrl Pts',(-24.095910368327,4.97348376415447,127.599303705405));
#152324=CARTESIAN_POINT('Ctrl Pts',(-24.1033185879935,4.88811981312278,
127.466839216899));
#152325=CARTESIAN_POINT('Ctrl Pts',(-24.1107268076599,4.7975159772053,127.337874156931));
#152326=CARTESIAN_POINT('Ctrl Pts',(-24.1181350273264,4.70200611348575,
127.21283321669));
#152327=CARTESIAN_POINT('Ctrl Pts',(-24.1255478066285,4.60643746503847,
127.087715315836));
#152328=CARTESIAN_POINT('Ctrl Pts',(-24.1329605859306,4.50595700961332,
126.966526634061));
#152329=CARTESIAN_POINT('Ctrl Pts',(-24.1403733652327,4.40093725267633,
126.849656853628));
#152330=CARTESIAN_POINT('Ctrl Pts',(-24.1477967362615,4.29576743858598,
126.732620084172));
#152331=CARTESIAN_POINT('Ctrl Pts',(-24.1552201072901,4.18604562876078,
126.619914807795));
#152332=CARTESIAN_POINT('Ctrl Pts',(-24.1626434783189,4.07217993838861,
126.511892666389));
#152333=CARTESIAN_POINT('Ctrl Pts',(-24.1665795277597,4.01180561718372,
126.454616735059));
#152334=CARTESIAN_POINT('Ctrl Pts',(-24.1705155772005,3.95026684254355,
126.398656717354));
#152335=CARTESIAN_POINT('Ctrl Pts',(-24.1744516266413,3.88762788369584,
126.344060179209));
#152336=CARTESIAN_POINT('Ctrl Pts',(-24.1818748930467,3.7694927622037,126.241092812166));
#152337=CARTESIAN_POINT('Ctrl Pts',(-24.1892981594522,3.64708540443271,
126.142666362847));
#152338=CARTESIAN_POINT('Ctrl Pts',(-24.1967214258576,3.52078988872497,
126.049156192733));
#152339=CARTESIAN_POINT('Ctrl Pts',(-24.2041359185786,3.39464364382862,
125.955756543874));
#152340=CARTESIAN_POINT('Ctrl Pts',(-24.2115504112996,3.26461868540771,
125.867261828084));
#152341=CARTESIAN_POINT('Ctrl Pts',(-24.2189649040206,3.13113437784517,
125.784009228432));
#152342=CARTESIAN_POINT('Ctrl Pts',(-24.2263722503744,2.99777872748367,
125.70083687077));
#152343=CARTESIAN_POINT('Ctrl Pts',(-24.2337795967281,2.86097068043396,
125.622896766838));
#152344=CARTESIAN_POINT('Ctrl Pts',(-24.2411869430819,2.72116089493841,
125.550484529728));
#152345=CARTESIAN_POINT('Ctrl Pts',(-24.2485887647573,2.58145538485581,
125.478126300396));
#152346=CARTESIAN_POINT('Ctrl Pts',(-24.2559905864327,2.4387529241492,125.411287899597));
#152347=CARTESIAN_POINT('Ctrl Pts',(-24.2633924081081,2.29353114524227,
125.350220405919));
#152348=CARTESIAN_POINT('Ctrl Pts',(-24.2707903224195,2.14838602778201,
125.289185149296));
#152349=CARTESIAN_POINT('Ctrl Pts',(-24.2781882367308,2.0007245839777,125.233914877047));
#152350=CARTESIAN_POINT('Ctrl Pts',(-24.2855861510422,1.85104681920726,
125.184613627211));
#152351=CARTESIAN_POINT('Ctrl Pts',(-24.2929828359544,1.70139392816611,
125.135320570349));
#152352=CARTESIAN_POINT('Ctrl Pts',(-24.3003795208666,1.54972573539777,
125.091994683858));
#152353=CARTESIAN_POINT('Ctrl Pts',(-24.3077762057788,1.39656000978726,
125.054791007451));
#152354=CARTESIAN_POINT('Ctrl Pts',(-24.3151725627142,1.24340107570508,
125.017588980693));
#152355=CARTESIAN_POINT('Ctrl Pts',(-24.3225689196496,1.08874510356055,
124.986508712365));
#152356=CARTESIAN_POINT('Ctrl Pts',(-24.3299652765851,0.933122468728264,
124.961654650221));
#152357=CARTESIAN_POINT('Ctrl Pts',(-24.3373627659216,0.777476007673962,
124.936796782856));
#152358=CARTESIAN_POINT('Ctrl Pts',(-24.3447602552583,0.620862957897172,
124.918167078594));
#152359=CARTESIAN_POINT('Ctrl Pts',(-24.3521577445949,0.463821123122597,
124.905818380009));
#152360=CARTESIAN_POINT('Ctrl Pts',(-24.3595578271099,0.306724237574495,
124.893465352607));
#152361=CARTESIAN_POINT('Ctrl Pts',(-24.366957909625,0.149198639679638,
124.887397743888));
#152362=CARTESIAN_POINT('Ctrl Pts',(-24.37435799214,-0.00821569351148752,
124.887616321513));
#152363=CARTESIAN_POINT('Ctrl Pts',(-24.3817662118065,-0.165803119943195,
124.887835139486));
#152364=CARTESIAN_POINT('Ctrl Pts',(-24.3891744314729,-0.32327866380961,
124.894353947618));
#152365=CARTESIAN_POINT('Ctrl Pts',(-24.3965826511394,-0.480104562476285,
124.90712141845));
#152366=CARTESIAN_POINT('Ctrl Pts',(-24.4039954304414,-0.637026984867033,
124.919896747447));
#152367=CARTESIAN_POINT('Ctrl Pts',(-24.4114082097436,-0.793298595614365,
124.938928357654));
#152368=CARTESIAN_POINT('Ctrl Pts',(-24.4188209890456,-0.948390195691438,
124.964113482451));
#152369=CARTESIAN_POINT('Ctrl Pts',(-24.4262443600744,-1.10370339792,124.989334592936));
#152370=CARTESIAN_POINT('Ctrl Pts',(-24.4336677311031,-1.25783285723011,
125.020726704164));
#152371=CARTESIAN_POINT('Ctrl Pts',(-24.4410911021318,-1.41026213111176,
125.058136528301));
#152372=CARTESIAN_POINT('Ctrl Pts',(-24.4450271515726,-1.4910837896137,
125.077972114694));
#152373=CARTESIAN_POINT('Ctrl Pts',(-24.4489632010134,-1.57142774824051,
125.099498672198));
#152374=CARTESIAN_POINT('Ctrl Pts',(-24.4528992504542,-1.65121924933523,
125.122687839842));
#152375=CARTESIAN_POINT('Ctrl Pts',(-24.4603225168596,-1.80170353019258,
125.16642188631));
#152376=CARTESIAN_POINT('Ctrl Pts',(-24.467745783265,-1.95067665642722,
125.216204763103));
#152377=CARTESIAN_POINT('Ctrl Pts',(-24.4751690496705,-2.09761522206942,
125.271916226283));
#152378=CARTESIAN_POINT('Ctrl Pts',(-24.4825835423915,-2.24438011852973,
125.32756184314));
#152379=CARTESIAN_POINT('Ctrl Pts',(-24.4899980351125,-2.38911489528683,
125.38912196767));
#152380=CARTESIAN_POINT('Ctrl Pts',(-24.4974125278335,-2.53130919398322,
125.456426032424));
#152381=CARTESIAN_POINT('Ctrl Pts',(-24.5048198741873,-2.67336644046101,
125.523665226987));
#152382=CARTESIAN_POINT('Ctrl Pts',(-24.512227220541,-2.81288774843008,
125.596637181607));
#152383=CARTESIAN_POINT('Ctrl Pts',(-24.5196345668948,-2.94938081843602,
125.675122530838));
#152384=CARTESIAN_POINT('Ctrl Pts',(-24.5270363885702,-3.08577208676019,
125.753549342734));
#152385=CARTESIAN_POINT('Ctrl Pts',(-24.5344382102455,-3.21913929202749,
125.837481176219));
#152386=CARTESIAN_POINT('Ctrl Pts',(-24.5418400319209,-3.34901302271742,
125.926651899718));
#152387=CARTESIAN_POINT('Ctrl Pts',(-24.5492379462323,-3.47881819407678,
126.015775550687));
#152388=CARTESIAN_POINT('Ctrl Pts',(-24.5566358605436,-3.60513325666363,
126.110132373147));
#152389=CARTESIAN_POINT('Ctrl Pts',(-24.564033774855,-3.72751628237571,
126.209411985957));
#152390=CARTESIAN_POINT('Ctrl Pts',(-24.5714304597672,-3.84987897024865,
126.308675100296));
#152391=CARTESIAN_POINT('Ctrl Pts',(-24.5788271446794,-3.96831062849901,
126.412859146397));
#152392=CARTESIAN_POINT('Ctrl Pts',(-24.5862238295915,-4.08240095109692,
126.521612313383));
#152393=CARTESIAN_POINT('Ctrl Pts',(-24.593620186527,-4.19648621481037,
126.63036065814));
#152394=CARTESIAN_POINT('Ctrl Pts',(-24.6010165434625,-4.30623025541946,
126.74367746338));
#152395=CARTESIAN_POINT('Ctrl Pts',(-24.608412900398,-4.41125851722605,
126.861172965843));
#152396=CARTESIAN_POINT('Ctrl Pts',(-24.6158103897346,-4.5163028591284,
126.978686457168));
#152397=CARTESIAN_POINT('Ctrl Pts',(-24.6232078790711,-4.61662973583615,
127.100379641249));
#152398=CARTESIAN_POINT('Ctrl Pts',(-24.6306053684077,-4.71190399334551,
127.225828611283));
#152399=CARTESIAN_POINT('Ctrl Pts',(-24.6380054509227,-4.80721164909733,
127.351321557257));
#152400=CARTESIAN_POINT('Ctrl Pts',(-24.6454055334377,-4.897462933594,127.480572613399));
#152401=CARTESIAN_POINT('Ctrl Pts',(-24.6528056159527,-4.98236533019543,
127.613127896662));
#152402=CARTESIAN_POINT('Ctrl Pts',(-24.6602138356191,-5.06736108571047,
127.745828938087));
#152403=CARTESIAN_POINT('Ctrl Pts',(-24.6676220552856,-5.14699600582089,
127.881841148107));
#152404=CARTESIAN_POINT('Ctrl Pts',(-24.675030274952,-5.22102259993138,
128.020684348043));
#152405=CARTESIAN_POINT('Ctrl Pts',(-24.6824430542541,-5.29509475617545,
128.159613003652));
#152406=CARTESIAN_POINT('Ctrl Pts',(-24.6898558335562,-5.36355154626121,
128.301375785805));
#152407=CARTESIAN_POINT('Ctrl Pts',(-24.6972686128583,-5.42619338565387,
128.445471916507));
#152408=CARTESIAN_POINT('Ctrl Pts',(-24.704691983887,-5.48892473064418,
128.589773938517));
#152409=CARTESIAN_POINT('Ctrl Pts',(-24.7121153549158,-5.54582439597577,
128.736415620721));
#152410=CARTESIAN_POINT('Ctrl Pts',(-24.7195387259445,-5.59674219725355,
128.88487960959));
#152411=CARTESIAN_POINT('Ctrl Pts',(-24.7234747753854,-5.62374003724726,
128.963598778834));
#152412=CARTESIAN_POINT('Ctrl Pts',(-24.7274108248262,-5.64905700690369,
129.042830056833));
#152413=CARTESIAN_POINT('Ctrl Pts',(-24.731346874267,-5.67267655877129,
129.122495218057));
#152414=CARTESIAN_POINT('Ctrl Pts',(-24.7405338723611,-5.72780614523887,
129.308438940391));
#152415=CARTESIAN_POINT('Ctrl Pts',(-24.7497208704551,-5.77382055480966,
129.49720052025));
#152416=CARTESIAN_POINT('Ctrl Pts',(-24.7589078685492,-5.81047562116316,
129.687980924823));
#152417=CARTESIAN_POINT('Ctrl Pts',(-24.7679691199866,-5.84662897281139,
129.876150030497));
#152418=CARTESIAN_POINT('Ctrl Pts',(-24.777030371424,-5.87367744459647,
130.066283120076));
#152419=CARTESIAN_POINT('Ctrl Pts',(-24.7860916228615,-5.89143236350679,
130.257592596624));
#152420=CARTESIAN_POINT('Ctrl Pts',(-24.7946026697757,-5.90810919328551,
130.4372856491));
#152421=CARTESIAN_POINT('Ctrl Pts',(-24.80311371669,-5.91658710362847,130.618016443981));
#152422=CARTESIAN_POINT('Ctrl Pts',(-24.8116247636042,-5.91674767427923,
130.799114532234));
#152423=CARTESIAN_POINT('',(-26.5616248077882,-5.90779414308507,130.806685475366));
#152424=CARTESIAN_POINT('Ctrl Pts',(-24.8116248077882,-5.91350445555948,
130.799118347467));
#152425=CARTESIAN_POINT('Ctrl Pts',(-24.8776813712188,-5.90160535121287,
132.203911372475));
#152426=CARTESIAN_POINT('Ctrl Pts',(-25.0365538092536,-4.69690807201577,
135.600915768792));
#152427=CARTESIAN_POINT('Ctrl Pts',(-25.2882421218929,0.97967206287985,
137.733848562542));
#152428=CARTESIAN_POINT('Ctrl Pts',(-25.5666897457058,6.3595111412122,133.72569226172));
#152429=CARTESIAN_POINT('Ctrl Pts',(-25.8451373695187,5.89527016016011,
127.032974894907));
#152430=CARTESIAN_POINT('Ctrl Pts',(-26.1235849933315,0.0135639018792721,
123.805976764782));
#152431=CARTESIAN_POINT('Ctrl Pts',(-26.3624141394214,-5.04196418963154,
126.554250593529));
#152432=CARTESIAN_POINT('Ctrl Pts',(-26.5084274109069,-5.90380256593809,
129.672610848885));
#152433=CARTESIAN_POINT('Ctrl Pts',(-26.5616248077882,-5.90779414308507,
130.806685475366));
#152434=CARTESIAN_POINT('',(-28.3116248077882,-5.92205169517661,130.808786883972));
#152435=CARTESIAN_POINT('Ctrl Pts',(-26.5616248077882,-5.90779414308507,
130.806685475366));
#152436=CARTESIAN_POINT('Ctrl Pts',(-26.6012432855112,-5.91076684888552,
131.651281507495));
#152437=CARTESIAN_POINT('Ctrl Pts',(-26.7336776378389,-5.34594544265701,
134.470755369925));
#152438=CARTESIAN_POINT('Ctrl Pts',(-26.9589278647701,-1.00652534475882,
137.729999018512));
#152439=CARTESIAN_POINT('Ctrl Pts',(-27.2373754885831,5.28268419639938,
135.394655620227));
#152440=CARTESIAN_POINT('Ctrl Pts',(-27.515823112396,6.71736503453805,128.841055362868));
#152441=CARTESIAN_POINT('Ctrl Pts',(-27.7942707362089,1.97911556745978,
124.091636721785));
#152442=CARTESIAN_POINT('Ctrl Pts',(-28.0595379680061,-4.26746898338629,
125.443702988462));
#152443=CARTESIAN_POINT('Ctrl Pts',(-28.2319893251994,-5.90797919871711,
129.121481013772));
#152444=CARTESIAN_POINT('Ctrl Pts',(-28.3116248077882,-5.92205169517661,
130.808786883972));
#152445=CARTESIAN_POINT('',(-30.0616248077881,-5.92200696645842,130.799917113144));
#152446=CARTESIAN_POINT('Ctrl Pts',(-28.3116248077882,-5.92205169517661,
130.808786883972));
#152447=CARTESIAN_POINT('Ctrl Pts',(-28.3248051998037,-5.92438082051049,
131.088051253275));
#152448=CARTESIAN_POINT('Ctrl Pts',(-28.4308014664233,-5.77932387060202,
133.33145433914));
#152449=CARTESIAN_POINT('Ctrl Pts',(-28.6296136076478,-2.91165016792604,
137.168310164028));
#152450=CARTESIAN_POINT('Ctrl Pts',(-28.9080612314604,3.7803529530868,136.693884544035));
#152451=CARTESIAN_POINT('Ctrl Pts',(-29.1865088552733,6.99839639071874,
130.807274154852));
#152452=CARTESIAN_POINT('Ctrl Pts',(-29.4649564790863,3.78525543595478,
124.917986367238));
#152453=CARTESIAN_POINT('Ctrl Pts',(-29.743404102899,-2.90635034444604,
124.437988950305));
#152454=CARTESIAN_POINT('Ctrl Pts',(-29.9422935457997,-5.77833397768845,
128.273946643054));
#152455=CARTESIAN_POINT('Ctrl Pts',(-30.0483671140961,-5.92435612236718,
130.519009360987));
#152456=CARTESIAN_POINT('Ctrl Pts',(-30.0616248077881,-5.92200696645842,
130.799917113144));
#152457=CARTESIAN_POINT('',(-31.8116248077882,-5.90777491155152,130.802060587744));
#152458=CARTESIAN_POINT('Ctrl Pts',(-30.0616248077881,-5.92200696645842,
130.799917113144));
#152459=CARTESIAN_POINT('Ctrl Pts',(-30.1411829887004,-5.90790990137895,
132.485618282964));
#152460=CARTESIAN_POINT('Ctrl Pts',(-30.3135570442171,-4.27011095544813,
136.161858688443));
#152461=CARTESIAN_POINT('Ctrl Pts',(-30.5787469743377,1.97352566730395,
137.51873005712));
#152462=CARTESIAN_POINT('Ctrl Pts',(-30.8571945981506,6.71572799954466,
132.773258270183));
#152463=CARTESIAN_POINT('Ctrl Pts',(-31.1356422219637,5.28650438175435,
126.218465726483));
#152464=CARTESIAN_POINT('Ctrl Pts',(-31.4140898457764,-1.00075850276986,
123.877886554275));
#152465=CARTESIAN_POINT('Ctrl Pts',(-31.6394173743847,-5.34438097876868,
127.134633213779));
#152466=CARTESIAN_POINT('Ctrl Pts',(-31.7719290283886,-5.91072106251254,
129.955809741519));
#152467=CARTESIAN_POINT('Ctrl Pts',(-31.8116248077882,-5.90777491155152,
130.802060587744));
#152468=CARTESIAN_POINT('',(-33.5616248231286,-5.91467433100452,130.809612195234));
#152469=CARTESIAN_POINT('Ctrl Pts',(-31.8116248077882,-5.90777491155152,
130.802060587744));
#152470=CARTESIAN_POINT('Ctrl Pts',(-31.8647449029928,-5.90383243147168,
131.934496483914));
#152471=CARTESIAN_POINT('Ctrl Pts',(-32.0106808728018,-5.04386563195127,
135.051161972767));
#152472=CARTESIAN_POINT('Ctrl Pts',(-32.2494327172153,0.00773683405587478,
137.802753338164));
#152473=CARTESIAN_POINT('Ctrl Pts',(-32.5278803410281,5.89212794841245,
134.580653610686));
#152474=CARTESIAN_POINT('Ctrl Pts',(-32.8063279648409,6.36194132462962,
127.888325104698));
#152475=CARTESIAN_POINT('Ctrl Pts',(-33.0847755886539,0.985441421623745,
123.875690778778));
#152476=CARTESIAN_POINT('Ctrl Pts',(-33.3365412029694,-4.69465669647055,
126.004549984482));
#152477=CARTESIAN_POINT('Ctrl Pts',(-33.495490942681,-5.90161251282196,
129.403201726833));
#152478=CARTESIAN_POINT('Ctrl Pts',(-33.5616248077881,-5.91355064207631,
130.809610871177));
#152479=CARTESIAN_POINT('',(-35.3116248077882,-5.92211511787841,130.804457825077));
#152480=CARTESIAN_POINT('Ctrl Pts',(-33.5616248514337,-5.91674766723801,
130.809614638272));
#152481=CARTESIAN_POINT('Ctrl Pts',(-33.5706680044378,-5.91657680444688,
131.002029567238));
#152482=CARTESIAN_POINT('Ctrl Pts',(-33.5797111574419,-5.90701618416332,
131.194029392853));
#152483=CARTESIAN_POINT('Ctrl Pts',(-33.5887543104459,-5.88820921070805,
131.38481117828));
#152484=CARTESIAN_POINT('Ctrl Pts',(-33.5979300201283,-5.86912656018184,
131.5783894883));
#152485=CARTESIAN_POINT('Ctrl Pts',(-33.6071057298108,-5.84052454621328,
131.7707138291));
#152486=CARTESIAN_POINT('Ctrl Pts',(-33.6162814394932,-5.80260190920715,
131.960968436045));
#152487=CARTESIAN_POINT('Ctrl Pts',(-33.6247445717553,-5.7676243103274,
132.136448040104));
#152488=CARTESIAN_POINT('Ctrl Pts',(-33.6332077040174,-5.72471811545822,
132.310167201927));
#152489=CARTESIAN_POINT('Ctrl Pts',(-33.6416708362795,-5.67407496370947,
132.481502194388));
#152490=CARTESIAN_POINT('Ctrl Pts',(-33.6490941026849,-5.62965434077741,
132.631785240217));
#152491=CARTESIAN_POINT('Ctrl Pts',(-33.6565173690903,-5.57919184969903,
132.780529531387));
#152492=CARTESIAN_POINT('Ctrl Pts',(-33.6639406354957,-5.5228101227562,
132.927212216355));
#152493=CARTESIAN_POINT('Ctrl Pts',(-33.6713551282167,-5.46649503433241,
133.07372153457));
#152494=CARTESIAN_POINT('Ctrl Pts',(-33.6787696209375,-5.40427476833725,
133.218173751702));
#152495=CARTESIAN_POINT('Ctrl Pts',(-33.6861841136585,-5.33632222046923,
133.360059293433));
#152496=CARTESIAN_POINT('Ctrl Pts',(-33.6935914600122,-5.26843516782522,
133.501808080536));
#152497=CARTESIAN_POINT('Ctrl Pts',(-33.700998806366,-5.19482699263484,
133.640994782786));
#152498=CARTESIAN_POINT('Ctrl Pts',(-33.7084061527197,-5.11571930563854,
133.777128107367));
#152499=CARTESIAN_POINT('Ctrl Pts',(-33.7158079743951,-5.03667062013976,
133.913159898578));
#152500=CARTESIAN_POINT('Ctrl Pts',(-33.7232097960704,-4.95213077670942,
134.046142525209));
#152501=CARTESIAN_POINT('Ctrl Pts',(-33.7306116177458,-4.86236804723507,
134.175607795648));
#152502=CARTESIAN_POINT('Ctrl Pts',(-33.7380095320571,-4.77265270280689,
134.305004722379));
#152503=CARTESIAN_POINT('Ctrl Pts',(-33.7454074463684,-4.67772017543241,
134.430887684796));
#152504=CARTESIAN_POINT('Ctrl Pts',(-33.7528053606797,-4.57788286062919,
134.552816176441));
#152505=CARTESIAN_POINT('Ctrl Pts',(-33.7602020455918,-4.47806213697645,
134.674724405781));
#152506=CARTESIAN_POINT('Ctrl Pts',(-33.767598730504,-4.37333847986577,
134.792679180076));
#152507=CARTESIAN_POINT('Ctrl Pts',(-33.7749954154162,-4.26406556974834,
134.906271803756));
#152508=CARTESIAN_POINT('Ctrl Pts',(-33.7823917723516,-4.1547975049064,
135.019859390619));
#152509=CARTESIAN_POINT('Ctrl Pts',(-33.7897881292869,-4.04098084693891,
135.129084942428));
#152510=CARTESIAN_POINT('Ctrl Pts',(-33.7971844862223,-3.9230070650703,
135.233575686843));
#152511=CARTESIAN_POINT('Ctrl Pts',(-33.8045819755589,-3.80501522111433,
135.338082429058));
#152512=CARTESIAN_POINT('Ctrl Pts',(-33.8119794648955,-3.68286526543293,
135.437852672959));
#152513=CARTESIAN_POINT('Ctrl Pts',(-33.819376954232,-3.5569826305485,135.532553203373));
#152514=CARTESIAN_POINT('Ctrl Pts',(-33.826777036747,-3.43105586770155,
135.62728693091));
#152515=CARTESIAN_POINT('Ctrl Pts',(-33.8341771192619,-3.30139411859141,
135.71694718233));
#152516=CARTESIAN_POINT('Ctrl Pts',(-33.8415772017769,-3.16845259701143,
135.801243516233));
#152517=CARTESIAN_POINT('Ctrl Pts',(-33.8489854214433,-3.03536489256176,
135.885632542621));
#152518=CARTESIAN_POINT('Ctrl Pts',(-33.8563936411097,-2.89899052878617,
135.964645672416));
#152519=CARTESIAN_POINT('Ctrl Pts',(-33.8638018607762,-2.75981080927196,
136.038037609846));
#152520=CARTESIAN_POINT('Ctrl Pts',(-33.8712146400782,-2.62054542696272,
136.111474718789));
#152521=CARTESIAN_POINT('Ctrl Pts',(-33.8786274193802,-2.47847158446133,
136.179283580962));
#152522=CARTESIAN_POINT('Ctrl Pts',(-33.8860401986822,-2.33409096574279,
136.241266900199));
#152523=CARTESIAN_POINT('Ctrl Pts',(-33.8934635697109,-2.18950404922545,
136.30333878411));
#152524=CARTESIAN_POINT('Ctrl Pts',(-33.9008869407397,-2.04260412128661,
136.359568367478));
#152525=CARTESIAN_POINT('Ctrl Pts',(-33.9083103117684,-1.8939092157265,
136.409807829438));
#152526=CARTESIAN_POINT('Ctrl Pts',(-33.9122463612098,-1.81506760890063,
136.436445997653));
#152527=CARTESIAN_POINT('Ctrl Pts',(-33.9161824106512,-1.73572157262807,
136.461400975028));
#152528=CARTESIAN_POINT('Ctrl Pts',(-33.9201184600926,-1.65594940717217,
136.484656571421));
#152529=CARTESIAN_POINT('Ctrl Pts',(-33.927541726498,-1.50550159274937,
136.52851590043));
#152530=CARTESIAN_POINT('Ctrl Pts',(-33.9349649929035,-1.35308259888669,
136.566460300172));
#152531=CARTESIAN_POINT('Ctrl Pts',(-33.9423882593089,-1.19919860113999,
136.598310330631));
#152532=CARTESIAN_POINT('Ctrl Pts',(-33.9498027520299,-1.04549648149914,
136.630122716998));
#152533=CARTESIAN_POINT('Ctrl Pts',(-33.9572172447509,-0.89033316654087,
136.655854996848));
#152534=CARTESIAN_POINT('Ctrl Pts',(-33.9646317374719,-0.734230829918383,
136.675377194863));
#152535=CARTESIAN_POINT('Ctrl Pts',(-33.9720390838257,-0.578278950605082,
136.694880576649));
#152536=CARTESIAN_POINT('Ctrl Pts',(-33.9794464301795,-0.421390219358522,
136.708185746559));
#152537=CARTESIAN_POINT('Ctrl Pts',(-33.9868537765333,-0.264097760757492,
136.71521359622));
#152538=CARTESIAN_POINT('Ctrl Pts',(-33.9942555982087,-0.106922616806393,
136.722236204245));
#152539=CARTESIAN_POINT('Ctrl Pts',(-34.0016574198841,0.0506552836175792,
136.722990797649));
#152540=CARTESIAN_POINT('Ctrl Pts',(-34.0090592415595,0.208097030143856,
136.717450012167));
#152541=CARTESIAN_POINT('Ctrl Pts',(-34.0164571558708,0.365455664397442,
136.711912151622));
#152542=CARTESIAN_POINT('Ctrl Pts',(-34.0238550701822,0.522677915772416,
136.700085543762));
#152543=CARTESIAN_POINT('Ctrl Pts',(-34.0312529844935,0.679224316300961,
136.68199491128));
#152544=CARTESIAN_POINT('Ctrl Pts',(-34.0386496694057,0.835744701658003,
136.663907285134));
#152545=CARTESIAN_POINT('Ctrl Pts',(-34.0460463543179,0.991589088612023,
136.63955774319));
#152546=CARTESIAN_POINT('Ctrl Pts',(-34.0534430392301,1.14622245708218,
136.60902293689));
#152547=CARTESIAN_POINT('Ctrl Pts',(-34.0608393961656,1.30084896894674,
136.578489484536));
#152548=CARTESIAN_POINT('Ctrl Pts',(-34.0682357531011,1.45426420287109,
136.541771385467));
#152549=CARTESIAN_POINT('Ctrl Pts',(-34.0756321100365,1.60594293625012,
136.498996501273));
#152550=CARTESIAN_POINT('Ctrl Pts',(-34.0830295993731,1.75764489203024,
136.456215068136));
#152551=CARTESIAN_POINT('Ctrl Pts',(-34.0904270887096,1.90760945858968,
136.407375104806));
#152552=CARTESIAN_POINT('Ctrl Pts',(-34.0978245780462,2.05532633589457,
136.352654428773));
#152553=CARTESIAN_POINT('Ctrl Pts',(-34.1052246605612,2.20309499512202,
136.297914570491));
#152554=CARTESIAN_POINT('Ctrl Pts',(-34.1126247430762,2.34861404651103,
136.237290024718));
#152555=CARTESIAN_POINT('Ctrl Pts',(-34.1200248255912,2.49139307931174,
136.171006785039));
#152556=CARTESIAN_POINT('Ctrl Pts',(-34.1274330452576,2.63432911233706,
136.104650660124));
#152557=CARTESIAN_POINT('Ctrl Pts',(-34.1348412649241,2.77451877095215,
136.032623572213));
#152558=CARTESIAN_POINT('Ctrl Pts',(-34.1422494845906,2.91149552453135,
135.955197867289));
#152559=CARTESIAN_POINT('Ctrl Pts',(-34.1496622638926,3.0485565850168,135.877724508135));
#152560=CARTESIAN_POINT('Ctrl Pts',(-34.1570750431947,3.18240048342844,
135.794846107025));
#152561=CARTESIAN_POINT('Ctrl Pts',(-34.1644878224968,3.31259005647194,
135.706878101498));
#152562=CARTESIAN_POINT('Ctrl Pts',(-34.1719111935255,3.44296565048269,
135.61878440316));
#152563=CARTESIAN_POINT('Ctrl Pts',(-34.1793345645543,3.56967619075622,
135.525586796656));
#152564=CARTESIAN_POINT('Ctrl Pts',(-34.186757935583,3.69231730148945,135.427641217705));
#152565=CARTESIAN_POINT('Ctrl Pts',(-34.1906939850238,3.75734456113292,
135.375708121573));
#152566=CARTESIAN_POINT('Ctrl Pts',(-34.1946300344646,3.82122836109007,
135.3224408289));
#152567=CARTESIAN_POINT('Ctrl Pts',(-34.1985660839053,3.88391275693069,
135.267896464745));
#152568=CARTESIAN_POINT('Ctrl Pts',(-34.2059893503108,4.00213357117372,
135.16502749622));
#152569=CARTESIAN_POINT('Ctrl Pts',(-34.2134126167162,4.11644345854232,
135.057302954858));
#152570=CARTESIAN_POINT('Ctrl Pts',(-34.2208358831217,4.22641785081445,
134.945051708775));
#152571=CARTESIAN_POINT('Ctrl Pts',(-34.2282503758427,4.33626226248787,
134.832933134343));
#152572=CARTESIAN_POINT('Ctrl Pts',(-34.2356648685636,4.44178112011132,
134.71629876882));
#152573=CARTESIAN_POINT('Ctrl Pts',(-34.2430793612847,4.54258282415461,
134.595517676855));
#152574=CARTESIAN_POINT('Ctrl Pts',(-34.2504867076384,4.64328737172043,
134.474852998253));
#152575=CARTESIAN_POINT('Ctrl Pts',(-34.2578940539922,4.73928357944742,
134.350049834669));
#152576=CARTESIAN_POINT('Ctrl Pts',(-34.265301400346,4.83021672436177,134.221513958901));
#152577=CARTESIAN_POINT('Ctrl Pts',(-34.2727032220214,4.92108204790593,
134.093073950038));
#152578=CARTESIAN_POINT('Ctrl Pts',(-34.2801050436968,5.00689161294138,
133.96090707574));
#152579=CARTESIAN_POINT('Ctrl Pts',(-34.2875068653722,5.08733110291786,
133.825451945511));
#152580=CARTESIAN_POINT('Ctrl Pts',(-34.2949047796836,5.16772812951372,
133.690068320991));
#152581=CARTESIAN_POINT('Ctrl Pts',(-34.302302693995,5.24276053660876,133.551400217714));
#152582=CARTESIAN_POINT('Ctrl Pts',(-34.3097006083064,5.31215752849287,
133.40991486858));
#152583=CARTESIAN_POINT('Ctrl Pts',(-34.3170972932186,5.38154298785591,
133.268453031744));
#152584=CARTESIAN_POINT('Ctrl Pts',(-34.3244939781307,5.44529472646293,
133.124175213066));
#152585=CARTESIAN_POINT('Ctrl Pts',(-34.3318906630429,5.50318804192056,
132.977572972069));
#152586=CARTESIAN_POINT('Ctrl Pts',(-34.3392870199784,5.56107879032792,
132.830977231568));
#152587=CARTESIAN_POINT('Ctrl Pts',(-34.3466833769139,5.61311149498209,
132.682057620886));
#152588=CARTESIAN_POINT('Ctrl Pts',(-34.3540797338494,5.65910983381282,
132.531325136988));
#152589=CARTESIAN_POINT('Ctrl Pts',(-34.361477223186,5.70511521510666,132.380569575562));
#152590=CARTESIAN_POINT('Ctrl Pts',(-34.3688747125226,5.74508428205129,
132.228000945336));
#152591=CARTESIAN_POINT('Ctrl Pts',(-34.3762722018592,5.77889080790296,
132.074144690877));
#152592=CARTESIAN_POINT('Ctrl Pts',(-34.3836722843742,5.81270918457986,
131.920234502347));
#152593=CARTESIAN_POINT('Ctrl Pts',(-34.3910723668891,5.84036063902073,
131.765036155272));
#152594=CARTESIAN_POINT('Ctrl Pts',(-34.3984724494041,5.86177022704046,
131.60908440116));
#152595=CARTESIAN_POINT('Ctrl Pts',(-34.4058806690706,5.88320335710317,
131.452961162062));
#152596=CARTESIAN_POINT('Ctrl Pts',(-34.4132888887371,5.89838086293466,
131.296083231517));
#152597=CARTESIAN_POINT('Ctrl Pts',(-34.4206971084036,5.90727970572456,
131.138990324608));
#152598=CARTESIAN_POINT('Ctrl Pts',(-34.4281098877057,5.91618402560374,
130.981800729635));
#152599=CARTESIAN_POINT('Ctrl Pts',(-34.4355226670077,5.91880197592184,
130.824396267028));
#152600=CARTESIAN_POINT('Ctrl Pts',(-34.4429354463098,5.91516264577609,
130.667315236341));
#152601=CARTESIAN_POINT('Ctrl Pts',(-34.4503588173386,5.91151811558477,
130.510009760911));
#152602=CARTESIAN_POINT('Ctrl Pts',(-34.4577821883674,5.90159847183417,
130.353029011956));
#152603=CARTESIAN_POINT('Ctrl Pts',(-34.4652055593961,5.88548459832653,
130.196905594242));
#152604=CARTESIAN_POINT('Ctrl Pts',(-34.4691416088369,5.87694063594584,
130.114125212042));
#152605=CARTESIAN_POINT('Ctrl Pts',(-34.4730776582776,5.86665610833664,
130.03158568904));
#152606=CARTESIAN_POINT('Ctrl Pts',(-34.4770137077183,5.85464883710015,
129.94936497036));
#152607=CARTESIAN_POINT('Ctrl Pts',(-34.4844369741237,5.8320034982819,129.794299260948));
#152608=CARTESIAN_POINT('Ctrl Pts',(-34.4918602405292,5.80315907701315,
129.639899369356));
#152609=CARTESIAN_POINT('Ctrl Pts',(-34.4992835069346,5.7681627698604,129.486700258104));
#152610=CARTESIAN_POINT('Ctrl Pts',(-34.5066979996556,5.7332078254364,129.33368221548));
#152611=CARTESIAN_POINT('Ctrl Pts',(-34.5141124923766,5.69211555045192,
129.181862488594));
#152612=CARTESIAN_POINT('Ctrl Pts',(-34.5215269850976,5.64498478033734,
129.031770029681));
#152613=CARTESIAN_POINT('Ctrl Pts',(-34.5289343314514,5.59789943663343,
128.88182223553));
#152614=CARTESIAN_POINT('Ctrl Pts',(-34.5363416778052,5.54478729561533,
128.733598748812));
#152615=CARTESIAN_POINT('Ctrl Pts',(-34.543749024159,5.48579800899795,128.587617338119));
#152616=CARTESIAN_POINT('Ctrl Pts',(-34.5511508458343,5.42685271881607,
128.44174480587));
#152617=CARTESIAN_POINT('Ctrl Pts',(-34.5585526675098,5.36203915022589,
128.298111364639));
#152618=CARTESIAN_POINT('Ctrl Pts',(-34.5659544891851,5.29155642205193,
128.157218536993));
#152619=CARTESIAN_POINT('Ctrl Pts',(-34.5733524034965,5.22111090116154,
128.016400085574));
#152620=CARTESIAN_POINT('Ctrl Pts',(-34.5807503178078,5.14500234739315,
127.878319699479));
#152621=CARTESIAN_POINT('Ctrl Pts',(-34.5881482321192,5.06347748532286,
127.743457757603));
#152622=CARTESIAN_POINT('Ctrl Pts',(-34.5955449170314,4.98196617120563,
127.608618227336));
#152623=CARTESIAN_POINT('Ctrl Pts',(-34.6029416019435,4.89504052813163,
127.476996398926));
#152624=CARTESIAN_POINT('Ctrl Pts',(-34.6103382868558,4.80299266191712,
127.349047020789));
#152625=CARTESIAN_POINT('Ctrl Pts',(-34.6177346437912,4.71094887720146,
127.221103316062));
#152626=CARTESIAN_POINT('Ctrl Pts',(-34.6251310007266,4.61378353894749,
127.096832040857));
#152627=CARTESIAN_POINT('Ctrl Pts',(-34.6325273576621,4.51183125698855,
126.976657746266));
#152628=CARTESIAN_POINT('Ctrl Pts',(-34.6399248469986,4.40986336587497,
126.856465052683));
#152629=CARTESIAN_POINT('Ctrl Pts',(-34.6473223363352,4.30310731328024,
126.740370873347));
#152630=CARTESIAN_POINT('Ctrl Pts',(-34.6547198256718,4.19193694196172,
126.628765422014));
#152631=CARTESIAN_POINT('Ctrl Pts',(-34.6621199081868,4.08072760004171,
126.517120847563));
#152632=CARTESIAN_POINT('Ctrl Pts',(-34.6695199907018,3.9651011217521,126.409968398288));
#152633=CARTESIAN_POINT('Ctrl Pts',(-34.6769200732168,3.84546689951739,
126.307660173105));
#152634=CARTESIAN_POINT('Ctrl Pts',(-34.6843282928833,3.72570112715681,
126.205239449511));
#152635=CARTESIAN_POINT('Ctrl Pts',(-34.6917365125497,3.60191909380826,
126.107673830589));
#152636=CARTESIAN_POINT('Ctrl Pts',(-34.6991447322162,3.47456242401793,
126.01527442873));
#152637=CARTESIAN_POINT('Ctrl Pts',(-34.7065575115182,3.34712736832223,
125.92281815658));
#152638=CARTESIAN_POINT('Ctrl Pts',(-34.7139702908203,3.2161136020986,125.835534643976));
#152639=CARTESIAN_POINT('Ctrl Pts',(-34.7213830701224,3.08198973537656,
125.753690381495));
#152640=CARTESIAN_POINT('Ctrl Pts',(-34.7288064411511,2.94767422618397,
125.671729176094));
#152641=CARTESIAN_POINT('Ctrl Pts',(-34.7362298121799,2.81024006641469,
125.595222924042));
#152642=CARTESIAN_POINT('Ctrl Pts',(-34.7436531832087,2.67017907121341,
125.524391461392));
#152643=CARTESIAN_POINT('Ctrl Pts',(-34.7475892326495,2.59591537083926,
125.486834920316));
#152644=CARTESIAN_POINT('Ctrl Pts',(-34.7515252820903,2.52091349410799,
125.450872956343));
#152645=CARTESIAN_POINT('Ctrl Pts',(-34.7554613315312,2.44524865147138,
125.416532706898));
#152646=CARTESIAN_POINT('Ctrl Pts',(-34.7628845979366,2.30254711967953,
125.351768068167));
#152647=CARTESIAN_POINT('Ctrl Pts',(-34.770307864342,2.15705500379107,125.292578783864));
#152648=CARTESIAN_POINT('Ctrl Pts',(-34.7777311307475,2.00924789382214,
125.239214306491));
#152649=CARTESIAN_POINT('Ctrl Pts',(-34.7851456234685,1.86161547958236,
125.185912901498));
#152650=CARTESIAN_POINT('Ctrl Pts',(-34.7925601161895,1.71167386523139,
125.138422725452));
#152651=CARTESIAN_POINT('Ctrl Pts',(-34.7999746089105,1.55992149622803,
125.096946536907));
#152652=CARTESIAN_POINT('Ctrl Pts',(-34.8073819552643,1.40831539187129,
125.055510324674));
#152653=CARTESIAN_POINT('Ctrl Pts',(-34.814789301618,1.25490236503129,125.020076657996));
#152654=CARTESIAN_POINT('Ctrl Pts',(-34.8221966479718,1.10019891949657,
124.990799497217));
#152655=CARTESIAN_POINT('Ctrl Pts',(-34.8295984696472,0.945610857628153,
124.961544172449));
#152656=CARTESIAN_POINT('Ctrl Pts',(-34.8370002913226,0.789734658627721,
124.938436279892));
#152657=CARTESIAN_POINT('Ctrl Pts',(-34.844402112998,0.633099896222334,
124.921579380438));
#152658=CARTESIAN_POINT('Ctrl Pts',(-34.8518000273094,0.476547820088555,
124.90473137961));
#152659=CARTESIAN_POINT('Ctrl Pts',(-34.8591979416207,0.31923834825994,
124.894127839917));
#152660=CARTESIAN_POINT('Ctrl Pts',(-34.8665958559321,0.16170899776651,
124.889820841511));
#152661=CARTESIAN_POINT('Ctrl Pts',(-34.8739925408443,0.00420582579348278,
124.88551455885));
#152662=CARTESIAN_POINT('Ctrl Pts',(-34.8813892257565,-0.153516779530488,
124.887502750932));
#152663=CARTESIAN_POINT('Ctrl Pts',(-34.8887859106687,-0.310918335154468,
124.89578546349));
#152664=CARTESIAN_POINT('Ctrl Pts',(-34.8961822676042,-0.468312911428527,
124.904067808783));
#152665=CARTESIAN_POINT('Ctrl Pts',(-34.9035786245396,-0.625386093526133,
124.918644099979));
#152666=CARTESIAN_POINT('Ctrl Pts',(-34.9109749814751,-0.781599829800576,
124.939462300583));
#152667=CARTESIAN_POINT('Ctrl Pts',(-34.9183724708116,-0.937837482796614,
124.960283688506));
#152668=CARTESIAN_POINT('Ctrl Pts',(-34.9257699601482,-1.09321505791928,
124.987348839353));
#152669=CARTESIAN_POINT('Ctrl Pts',(-34.9331674494848,-1.24720218614087,
125.020554148692));
#152670=CARTESIAN_POINT('Ctrl Pts',(-34.9405675319998,-1.40124329431176,
125.053771098101));
#152671=CARTESIAN_POINT('Ctrl Pts',(-34.9479676145148,-1.55389262045127,
125.093132412821));
#152672=CARTESIAN_POINT('Ctrl Pts',(-34.9553676970298,-1.70463264716345,
125.138483977475));
#152673=CARTESIAN_POINT('Ctrl Pts',(-34.9627759166963,-1.85553842803146,
125.183885410838));
#152674=CARTESIAN_POINT('Ctrl Pts',(-34.9701841363628,-2.00453035900149,
125.235290140983));
#152675=CARTESIAN_POINT('Ctrl Pts',(-34.9775923560292,-2.15110798355421,
125.29249478052));
#152676=CARTESIAN_POINT('Ctrl Pts',(-34.9850051353313,-2.29777582418927,
125.349734628559));
#152677=CARTESIAN_POINT('Ctrl Pts',(-34.9924179146334,-2.44202605617368,
125.412781350005));
#152678=CARTESIAN_POINT('Ctrl Pts',(-34.9998306939355,-2.58338117826988,
125.481384734635));
#152679=CARTESIAN_POINT('Ctrl Pts',(-35.0072540649642,-2.72493827519343,
125.550086142999));
#152680=CARTESIAN_POINT('Ctrl Pts',(-35.014677435993,-2.86359167218565,
125.624359895948));
#152681=CARTESIAN_POINT('Ctrl Pts',(-35.0221008070218,-2.99889057685087,
125.703911042227));
#152682=CARTESIAN_POINT('Ctrl Pts',(-35.0260368564625,-3.07062930255596,
125.746090968787));
#152683=CARTESIAN_POINT('Ctrl Pts',(-35.0299729059032,-3.14142546773644,
125.789753851896));
#152684=CARTESIAN_POINT('Ctrl Pts',(-35.0339089553439,-3.21121558782093,
125.834851083313));
#152685=CARTESIAN_POINT('Ctrl Pts',(-35.0413287007412,-3.34277514520565,
125.919862712426));
#152686=CARTESIAN_POINT('Ctrl Pts',(-35.0487484461384,-3.47115642993611,
126.01023134199));
#152687=CARTESIAN_POINT('Ctrl Pts',(-35.0561681915356,-3.59589276206859,
126.10569210338));
#152688=CARTESIAN_POINT('Ctrl Pts',(-35.0635791648688,-3.72048162349532,
126.201040005384));
#152689=CARTESIAN_POINT('Ctrl Pts',(-35.070990138202,-3.84143381596459,
126.301467831249));
#152690=CARTESIAN_POINT('Ctrl Pts',(-35.0784011115352,-3.95830956914989,
126.406666231041));
#152691=CARTESIAN_POINT('Ctrl Pts',(-35.0858049436034,-4.0750727000542,
126.511763260929));
#152692=CARTESIAN_POINT('Ctrl Pts',(-35.0932087756717,-4.18776693570188,
126.621621464936));
#152693=CARTESIAN_POINT('Ctrl Pts',(-35.1006126077399,-4.29598378439776,
126.735889911429));
#152694=CARTESIAN_POINT('Ctrl Pts',(-35.1080109236896,-4.40412000768699,
126.850073223861));
#152695=CARTESIAN_POINT('Ctrl Pts',(-35.1154092396391,-4.50778523011824,
126.96865996627));
#152696=CARTESIAN_POINT('Ctrl Pts',(-35.1228075555888,-4.60660628734779,
127.091260958808));
#152697=CARTESIAN_POINT('Ctrl Pts',(-35.1302019761786,-4.70537531333374,
127.213797399496));
#152698=CARTESIAN_POINT('Ctrl Pts',(-35.1375963967684,-4.79930501966338,
127.340343590851));
#152699=CARTESIAN_POINT('Ctrl Pts',(-35.1449908173582,-4.88806125469121,
127.470475836581));
#152700=CARTESIAN_POINT('Ctrl Pts',(-35.1523840254788,-4.9768029362871,
127.60058674442));
#152701=CARTESIAN_POINT('Ctrl Pts',(-35.1597772335994,-5.06037261971129,
127.734282231269));
#152702=CARTESIAN_POINT('Ctrl Pts',(-35.1671704417201,-5.1384783258287,
127.871107976301));
#152703=CARTESIAN_POINT('Ctrl Pts',(-35.1745633391319,-5.21658074945654,
128.00792797106));
#152704=CARTESIAN_POINT('Ctrl Pts',(-35.1819562365439,-5.28921946707104,
128.147877637899));
#152705=CARTESIAN_POINT('Ctrl Pts',(-35.1893491339557,-5.35614763294323,
128.2904765517));
#152706=CARTESIAN_POINT('Ctrl Pts',(-35.1967431841452,-5.42308623495231,
128.433097701009));
#152707=CARTESIAN_POINT('Ctrl Pts',(-35.2041372343345,-5.48431235348562,
128.578368581476));
#152708=CARTESIAN_POINT('Ctrl Pts',(-35.2115312845239,-5.53962668377834,
128.725787364859));
#152709=CARTESIAN_POINT('Ctrl Pts',(-35.2189279513926,-5.59496058925036,
128.87325831825));
#152710=CARTESIAN_POINT('Ctrl Pts',(-35.2263246182613,-5.6443784099813,
129.022878338263));
#152711=CARTESIAN_POINT('Ctrl Pts',(-35.2337212851299,-5.68773028758663,
129.174129119229));
#152712=CARTESIAN_POINT('Ctrl Pts',(-35.2411260889127,-5.7311298556597,
129.325546287925));
#152713=CARTESIAN_POINT('Ctrl Pts',(-35.2485308926954,-5.76845005152466,
129.478597440704));
#152714=CARTESIAN_POINT('Ctrl Pts',(-35.2559356964781,-5.79959169685811,
129.632752017293));
#152715=CARTESIAN_POINT('Ctrl Pts',(-35.2633450869446,-5.83075263195026,
129.787002080313));
#152716=CARTESIAN_POINT('Ctrl Pts',(-35.270754477411,-5.85572733156779,
129.94235656096));
#152717=CARTESIAN_POINT('Ctrl Pts',(-35.2781638678775,-5.8744684193152,
130.098278927555));
#152718=CARTESIAN_POINT('Ctrl Pts',(-35.2855837906031,-5.89323614703997,
130.25442293381));
#152719=CARTESIAN_POINT('Ctrl Pts',(-35.2930037133287,-5.9057525368752,
130.411136066717));
#152720=CARTESIAN_POINT('Ctrl Pts',(-35.3004236360544,-5.91202228871884,
130.567880131708));
#152721=CARTESIAN_POINT('Ctrl Pts',(-35.3041573599656,-5.91517724372873,
130.646754142266));
#152722=CARTESIAN_POINT('Ctrl Pts',(-35.3078910838769,-5.91675129300788,
130.725636030376));
#152723=CARTESIAN_POINT('Ctrl Pts',(-35.3116248077882,-5.91674999920293,
130.804457737012));
#152724=CARTESIAN_POINT('',(-37.0616239770217,-5.91482137216616,130.799044590469));
#152725=CARTESIAN_POINT('Ctrl Pts',(-35.3116248077882,-5.92653083872268,
130.804457897558));
#152726=CARTESIAN_POINT('Ctrl Pts',(-35.3118687315778,-5.92653208400454,
130.809615823741));
#152727=CARTESIAN_POINT('Ctrl Pts',(-35.3121126553674,-5.9265259352798,
130.814773746866));
#152728=CARTESIAN_POINT('Ctrl Pts',(-35.312356579157,-5.9265123836523,130.819931650541));
#152729=CARTESIAN_POINT('Ctrl Pts',(-35.4051724537613,-5.92135582979253,
132.782574742726));
#152730=CARTESIAN_POINT('Ctrl Pts',(-35.5908042029699,-3.76732180451587,
136.702228618086));
#152731=CARTESIAN_POINT('Ctrl Pts',(-35.8692518267827,2.92571392784882,
137.161856865519));
#152732=CARTESIAN_POINT('Ctrl Pts',(-36.1476994505958,6.93016148959074,
131.77925664204));
#152733=CARTESIAN_POINT('Ctrl Pts',(-36.4261470744084,4.5661291996099,125.500774598388));
#152734=CARTESIAN_POINT('Ctrl Pts',(-36.7045946982214,-1.99395275700014,
124.096029011779));
#152735=CARTESIAN_POINT('Ctrl Pts',(-36.9164201919863,-5.59051847633362,
127.717049891396));
#152736=CARTESIAN_POINT('Ctrl Pts',(-37.0354298111468,-5.91863080344013,
130.242067918483));
#152737=CARTESIAN_POINT('Ctrl Pts',(-37.0616235557032,-5.91384448342225,
130.79903650694));
#152738=CARTESIAN_POINT('',(-38.8116256262763,-5.91172911628527,130.806521618407));
#152739=CARTESIAN_POINT('Ctrl Pts',(-37.0616248077882,-5.9167476261515,
130.799060529776));
#152740=CARTESIAN_POINT('Ctrl Pts',(-37.0689647505484,-5.91688749960742,
130.955208120347));
#152741=CARTESIAN_POINT('Ctrl Pts',(-37.0763046933087,-5.91084185943447,
131.111484207038));
#152742=CARTESIAN_POINT('Ctrl Pts',(-37.083644636069,-5.89860708023356,
131.267356379446));
#152743=CARTESIAN_POINT('Ctrl Pts',(-37.0910548573097,-5.88625515547447,
131.424720996657));
#152744=CARTESIAN_POINT('Ctrl Pts',(-37.0984650785504,-5.86759492024982,
131.581673532812));
#152745=CARTESIAN_POINT('Ctrl Pts',(-37.1058752997912,-5.84267655759526,
131.737667215543));
#152746=CARTESIAN_POINT('Ctrl Pts',(-37.113211006174,-5.81800876617095,
131.892092274784));
#152747=CARTESIAN_POINT('Ctrl Pts',(-37.1205467125568,-5.78720820846725,
132.045577296126));
#152748=CARTESIAN_POINT('Ctrl Pts',(-37.1278824189397,-5.75037550520156,
132.197598612913));
#152749=CARTESIAN_POINT('Ctrl Pts',(-37.1352182544506,-5.71354215358158,
132.349622605682));
#152750=CARTESIAN_POINT('Ctrl Pts',(-37.1425540899616,-5.6706765341907,
132.500182473154));
#152751=CARTESIAN_POINT('Ctrl Pts',(-37.1498899254725,-5.62192992566291,
132.648766883397));
#152752=CARTESIAN_POINT('Ctrl Pts',(-37.1572273971942,-5.57317244451913,
132.797384434432));
#152753=CARTESIAN_POINT('Ctrl Pts',(-37.1645648689158,-5.51853148208788,
132.944025290296));
#152754=CARTESIAN_POINT('Ctrl Pts',(-37.1719023406374,-5.45820743073228,
133.088195595317));
#152755=CARTESIAN_POINT('Ctrl Pts',(-37.1793679744049,-5.39682971210151,
133.234884092155));
#152756=CARTESIAN_POINT('Ctrl Pts',(-37.1868336081724,-5.32956868366509,
133.379014551005));
#152757=CARTESIAN_POINT('Ctrl Pts',(-37.1942992419399,-5.25668503500476,
133.520091275282));
#152758=CARTESIAN_POINT('Ctrl Pts',(-37.201648244731,-5.18494000248497,
133.658964045198));
#152759=CARTESIAN_POINT('Ctrl Pts',(-37.2089972475221,-5.10774699201546,
133.794877500466));
#152760=CARTESIAN_POINT('Ctrl Pts',(-37.2163462503132,-5.02539905273462,
133.927387182178));
#152761=CARTESIAN_POINT('Ctrl Pts',(-37.2238701995689,-4.94109078206554,
134.063051319128));
#152762=CARTESIAN_POINT('Ctrl Pts',(-37.2313941488245,-4.85137933113472,
134.195147248156));
#152763=CARTESIAN_POINT('Ctrl Pts',(-37.2389180980802,-4.75662316941709,
134.323233531819));
#152764=CARTESIAN_POINT('Ctrl Pts',(-37.2464420473359,-4.66186700769946,
134.451319815483));
#152765=CARTESIAN_POINT('Ctrl Pts',(-37.2539659965916,-4.56206645123366,
134.575396169357));
#152766=CARTESIAN_POINT('Ctrl Pts',(-37.2614899458473,-4.45762002442124,
134.69506161872));
#152767=CARTESIAN_POINT('Ctrl Pts',(-37.2689132122526,-4.35457126306258,
134.813125747006));
#152768=CARTESIAN_POINT('Ctrl Pts',(-37.2763364786581,-4.24667288625402,
134.927271563592));
#152769=CARTESIAN_POINT('Ctrl Pts',(-37.2837597450635,-4.13425440785265,
135.037075001227));
#152770=CARTESIAN_POINT('Ctrl Pts',(-37.2911742377845,-4.02196879875681,
135.146748660318));
#152771=CARTESIAN_POINT('Ctrl Pts',(-37.2985887305055,-3.90517398655583,
135.252089898103));
#152772=CARTESIAN_POINT('Ctrl Pts',(-37.3060032232265,-3.7842396314193,
135.352707677158));
#152773=CARTESIAN_POINT('Ctrl Pts',(-37.3134105695803,-3.66342183736735,
135.453228477009));
#152774=CARTESIAN_POINT('Ctrl Pts',(-37.3208179159341,-3.53847272841698,
135.549034644404));
#152775=CARTESIAN_POINT('Ctrl Pts',(-37.3282252622878,-3.40979861672405,
135.639772074297));
#152776=CARTESIAN_POINT('Ctrl Pts',(-37.3356270839632,-3.28122047503841,
135.730441828791));
#152777=CARTESIAN_POINT('Ctrl Pts',(-37.3430289056386,-3.14892316623746,
135.816050158977));
#152778=CARTESIAN_POINT('Ctrl Pts',(-37.350430727314,-3.0133457776533,135.896283416156));
#152779=CARTESIAN_POINT('Ctrl Pts',(-37.3578286416254,-2.87783995931628,
135.976474318824));
#152780=CARTESIAN_POINT('Ctrl Pts',(-37.3652265559368,-2.73905783006307,
136.051295609785));
#152781=CARTESIAN_POINT('Ctrl Pts',(-37.3726244702482,-2.59746703435814,
136.120477204693));
#152782=CARTESIAN_POINT('Ctrl Pts',(-37.3800211551604,-2.45589976847555,
136.189647302874));
#152783=CARTESIAN_POINT('Ctrl Pts',(-37.3874178400726,-2.31152509757524,
136.253179401378));
#152784=CARTESIAN_POINT('Ctrl Pts',(-37.3948145249848,-2.16483492256999,
136.310849546141));
#152785=CARTESIAN_POINT('Ctrl Pts',(-37.4022108819203,-2.01815125196061,
136.36851713375));
#152786=CARTESIAN_POINT('Ctrl Pts',(-37.4096072388557,-1.86915262880618,
136.420323147854));
#152787=CARTESIAN_POINT('Ctrl Pts',(-37.4170035957912,-1.71835031781262,
136.466092044239));
#152788=CARTESIAN_POINT('Ctrl Pts',(-37.4244010851277,-1.56752491860069,
136.511867947958));
#152789=CARTESIAN_POINT('Ctrl Pts',(-37.4317985744642,-1.41489563893112,
136.551604785135));
#152790=CARTESIAN_POINT('Ctrl Pts',(-37.4391960638008,-1.26098811485812,
136.585177128811));
#152791=CARTESIAN_POINT('Ctrl Pts',(-37.4465961463158,-1.10702663874159,
136.61876124122));
#152792=CARTESIAN_POINT('Ctrl Pts',(-37.4539962288307,-0.9517863905786,
136.646176478176));
#152793=CARTESIAN_POINT('Ctrl Pts',(-37.4613963113457,-0.795802235308524,
136.667348709382));
#152794=CARTESIAN_POINT('Ctrl Pts',(-37.4688045310121,-0.639646559423499,
136.688544221633));
#152795=CARTESIAN_POINT('Ctrl Pts',(-37.4762127506786,-0.482745712959932,
136.703482968384));
#152796=CARTESIAN_POINT('Ctrl Pts',(-37.4836209703451,-0.325639445438268,
136.712142732207));
#152797=CARTESIAN_POINT('Ctrl Pts',(-37.4910337496472,-0.168436481629955,
136.72080782597));
#152798=CARTESIAN_POINT('Ctrl Pts',(-37.4984465289492,-0.0110282172193689,
136.72318623046));
#152799=CARTESIAN_POINT('Ctrl Pts',(-37.5058593082513,0.146047093129462,
136.71930785394));
#152800=CARTESIAN_POINT('Ctrl Pts',(-37.51328267928,0.303346840047373,136.715423935814));
#152801=CARTESIAN_POINT('Ctrl Pts',(-37.5207060503087,0.460312311211555,
136.705265405573));
#152802=CARTESIAN_POINT('Ctrl Pts',(-37.5281294213375,0.616411025564011,
136.68891395746));
#152803=CARTESIAN_POINT('Ctrl Pts',(-37.5320654707783,0.699178309452366,
136.680244027323));
#152804=CARTESIAN_POINT('Ctrl Pts',(-37.5360015202192,0.78170208557782,
136.66983390052));
#152805=CARTESIAN_POINT('Ctrl Pts',(-37.5399375696601,0.863904436027291,
136.65770151725));
#152806=CARTESIAN_POINT('Ctrl Pts',(-37.5473608360655,1.01893550352477,
136.634820221042));
#152807=CARTESIAN_POINT('Ctrl Pts',(-37.554784102471,1.17329132002504,136.605740862823));
#152808=CARTESIAN_POINT('Ctrl Pts',(-37.5622073688764,1.32643699545262,
136.570511453227));
#152809=CARTESIAN_POINT('Ctrl Pts',(-37.5696218615974,1.47940166541024,
136.535323681868));
#152810=CARTESIAN_POINT('Ctrl Pts',(-37.5770363543184,1.63115868104402,
136.494000410687));
#152811=CARTESIAN_POINT('Ctrl Pts',(-37.5844508470394,1.78117924114398,
136.446641279977));
#152812=CARTESIAN_POINT('Ctrl Pts',(-37.5918581933932,1.93105520577973,
136.39932779578));
#152813=CARTESIAN_POINT('Ctrl Pts',(-37.5992655397469,2.07919769322025,
136.34599014535));
#152814=CARTESIAN_POINT('Ctrl Pts',(-37.6066728861007,2.22508916321667,
136.286778768185));
#152815=CARTESIAN_POINT('Ctrl Pts',(-37.6140747077761,2.3708718218508,136.227611553098));
#152816=CARTESIAN_POINT('Ctrl Pts',(-37.6214765294515,2.51440646153834,
136.162579473914));
#152817=CARTESIAN_POINT('Ctrl Pts',(-37.6288783511269,2.65519186331895,
136.091882412459));
#152818=CARTESIAN_POINT('Ctrl Pts',(-37.6362762654382,2.79590294558063,
136.021222671432));
#152819=CARTESIAN_POINT('Ctrl Pts',(-37.6436741797496,2.93386734751713,
135.944904070954));
#152820=CARTESIAN_POINT('Ctrl Pts',(-37.6510720940609,3.06860506626174,
135.863174066371));
#152821=CARTESIAN_POINT('Ctrl Pts',(-37.658468778973,3.20332039404266,135.781457643832));
#152822=CARTESIAN_POINT('Ctrl Pts',(-37.6658654638852,3.33480978400542,
135.694331795399));
#152823=CARTESIAN_POINT('Ctrl Pts',(-37.6732621487974,3.46261893279522,
135.602089318602));
#152824=CARTESIAN_POINT('Ctrl Pts',(-37.6806585057328,3.59042241439342,
135.509850931933));
#152825=CARTESIAN_POINT('Ctrl Pts',(-37.6880548626682,3.71454567659037,
135.412496586469));
#152826=CARTESIAN_POINT('Ctrl Pts',(-37.6954512196036,3.83456467800391,
135.310361537751));
#152827=CARTESIAN_POINT('Ctrl Pts',(-37.7028487089402,3.95460205463261,
135.208210851896));
#152828=CARTESIAN_POINT('Ctrl Pts',(-37.7102461982768,4.0705336349945,135.101278247345));
#152829=CARTESIAN_POINT('Ctrl Pts',(-37.7176436876134,4.18196977470881,
134.989938160262));
#152830=CARTESIAN_POINT('Ctrl Pts',(-37.7250437701284,4.2934449781901,134.878559043083));
#152831=CARTESIAN_POINT('Ctrl Pts',(-37.7324438526433,4.4004213395681,134.7627696309));
#152832=CARTESIAN_POINT('Ctrl Pts',(-37.7398439351583,4.50254738335946,
134.642979851497));
#152833=CARTESIAN_POINT('Ctrl Pts',(-37.7472521548248,4.60478572523436,
134.523058350917));
#152834=CARTESIAN_POINT('Ctrl Pts',(-37.7546603744913,4.70216285599346,
134.399127982643));
#152835=CARTESIAN_POINT('Ctrl Pts',(-37.7620685941578,4.79436833568445,
134.271630844169));
#152836=CARTESIAN_POINT('Ctrl Pts',(-37.7694813734598,4.88663056630966,
134.144055233334));
#152837=CARTESIAN_POINT('Ctrl Pts',(-37.7768941527619,4.97371459719107,
134.012908788174));
#152838=CARTESIAN_POINT('Ctrl Pts',(-37.7843069320639,5.05535465120457,
133.878660523731));
#152839=CARTESIAN_POINT('Ctrl Pts',(-37.7917303030927,5.13711135635579,
133.744220439071));
#152840=CARTESIAN_POINT('Ctrl Pts',(-37.7991536741214,5.21340836841894,
133.606670008957));
#152841=CARTESIAN_POINT('Ctrl Pts',(-37.8065770451502,5.28402660005538,
133.466501382516));
#152842=CARTESIAN_POINT('Ctrl Pts',(-37.8105130945911,5.3214700809316,133.392180613474));
#152843=CARTESIAN_POINT('Ctrl Pts',(-37.814449144032,5.35731786317353,133.317124095605));
#152844=CARTESIAN_POINT('Ctrl Pts',(-37.8183851934729,5.39154292384411,
133.241407080571));
#152845=CARTESIAN_POINT('Ctrl Pts',(-37.8258084598784,5.45609032013927,
133.09860715327));
#152846=CARTESIAN_POINT('Ctrl Pts',(-37.8332317262838,5.51505812166864,
132.953025129843));
#152847=CARTESIAN_POINT('Ctrl Pts',(-37.8406549926893,5.56819759998688,
132.805136979382));
#152848=CARTESIAN_POINT('Ctrl Pts',(-37.8480694854103,5.62127427185471,
132.657423620433));
#152849=CARTESIAN_POINT('Ctrl Pts',(-37.8554839781313,5.66853620729608,
132.507409907748));
#152850=CARTESIAN_POINT('Ctrl Pts',(-37.8628984708523,5.70978140653925,
132.355594594772));
#152851=CARTESIAN_POINT('Ctrl Pts',(-37.8703058172061,5.75098685210641,
132.203925607112));
#152852=CARTESIAN_POINT('Ctrl Pts',(-37.8777131635599,5.78618700924205,
132.050458833913));
#152853=CARTESIAN_POINT('Ctrl Pts',(-37.8851205099137,5.81522870380972,
131.895711012667));
#152854=CARTESIAN_POINT('Ctrl Pts',(-37.8925223315891,5.84424873798604,
131.741078608184));
#152855=CARTESIAN_POINT('Ctrl Pts',(-37.8999241532645,5.86711938674388,
131.585167423407));
#152856=CARTESIAN_POINT('Ctrl Pts',(-37.90732597494,5.88373789523335,131.42850718905));
#152857=CARTESIAN_POINT('Ctrl Pts',(-37.9147238892513,5.90034763094142,
131.271929654412));
#152858=CARTESIAN_POINT('Ctrl Pts',(-37.9221218035627,5.91071176011901,
131.114604227964));
#152859=CARTESIAN_POINT('Ctrl Pts',(-37.929519717874,5.91477902068223,130.957068505369));
#152860=CARTESIAN_POINT('Ctrl Pts',(-37.9369164027863,5.91884560534056,
130.799558962353));
#152861=CARTESIAN_POINT('Ctrl Pts',(-37.9443130876985,5.91661738860387,
130.641839565358));
#152862=CARTESIAN_POINT('Ctrl Pts',(-37.9517097726107,5.90809514726439,
130.484450796881));
#152863=CARTESIAN_POINT('Ctrl Pts',(-37.9591061295462,5.89957328381004,
130.327069007186));
#152864=CARTESIAN_POINT('Ctrl Pts',(-37.9665024864817,5.88475797084915,
130.17001818961));
#152865=CARTESIAN_POINT('Ctrl Pts',(-37.9738988434171,5.86370206363789,
130.013836315986));
#152866=CARTESIAN_POINT('Ctrl Pts',(-37.9812963327537,5.84264293271358,
129.857630530519));
#152867=CARTESIAN_POINT('Ctrl Pts',(-37.9886938220903,5.81534135498785,
129.702294323873));
#152868=CARTESIAN_POINT('Ctrl Pts',(-37.9960913114268,5.78190174190415,
129.548357906794));
#152869=CARTESIAN_POINT('Ctrl Pts',(-38.0034913939418,5.74845040661577,
129.394367527543));
#152870=CARTESIAN_POINT('Ctrl Pts',(-38.0108914764569,5.70885683118664,
129.241778279389));
#152871=CARTESIAN_POINT('Ctrl Pts',(-38.0182915589719,5.66327591838806,
129.091107444592));
#152872=CARTESIAN_POINT('Ctrl Pts',(-38.0256997786384,5.61764488469003,
128.940270931723));
#152873=CARTESIAN_POINT('Ctrl Pts',(-38.0331079983049,5.56601347371388,
128.791357402531));
#152874=CARTESIAN_POINT('Ctrl Pts',(-38.0405162179713,5.50858583422576,
128.644867003436));
#152875=CARTESIAN_POINT('Ctrl Pts',(-38.0479289972734,5.45112284898393,
128.498286441945));
#152876=CARTESIAN_POINT('Ctrl Pts',(-38.0553417765755,5.38785667624764,
128.354132323378));
#152877=CARTESIAN_POINT('Ctrl Pts',(-38.0627545558775,5.31903825262584,
128.212881767642));
#152878=CARTESIAN_POINT('Ctrl Pts',(-38.0701779269063,5.25012149801281,
128.071429386487));
#152879=CARTESIAN_POINT('Ctrl Pts',(-38.0776012979351,5.17563682420441,
127.932889182062));
#152880=CARTESIAN_POINT('Ctrl Pts',(-38.0850246689639,5.09587986814256,
127.797711497373));
#152881=CARTESIAN_POINT('Ctrl Pts',(-38.0889607184045,5.05359081629822,
127.726037045409));
#152882=CARTESIAN_POINT('Ctrl Pts',(-38.0928967678452,5.00982024403914,
127.655307409686));
#152883=CARTESIAN_POINT('Ctrl Pts',(-38.0968328172858,4.96461685616323,
127.585586000728));
#152884=CARTESIAN_POINT('Ctrl Pts',(-38.1042560836913,4.87936467737595,
127.45409359936));
#152885=CARTESIAN_POINT('Ctrl Pts',(-38.1116793500968,4.78875593506575,
127.325791678178));
#152886=CARTESIAN_POINT('Ctrl Pts',(-38.1191026165022,4.69305663170765,
127.201146772388));
#152887=CARTESIAN_POINT('Ctrl Pts',(-38.1265171092232,4.59747043697866,
127.076649186525));
#152888=CARTESIAN_POINT('Ctrl Pts',(-38.1339316019442,4.49680588243088,
126.955800305716));
#152889=CARTESIAN_POINT('Ctrl Pts',(-38.1413460946652,4.39137339765278,
126.83903966651));
#152890=CARTESIAN_POINT('Ctrl Pts',(-38.1487534410189,4.28604253267327,
126.722391565604));
#152891=CARTESIAN_POINT('Ctrl Pts',(-38.1561607873727,4.17595313471987,
126.609824136937));
#152892=CARTESIAN_POINT('Ctrl Pts',(-38.1635681337265,4.06145715531702,
126.501745559485));
#152893=CARTESIAN_POINT('Ctrl Pts',(-38.1709699554019,3.94704657133514,
126.393747591114));
#152894=CARTESIAN_POINT('Ctrl Pts',(-38.1783717770773,3.82823622024836,
126.290232062869));
#152895=CARTESIAN_POINT('Ctrl Pts',(-38.1857735987527,3.70541623800441,
126.191571757708));
#152896=CARTESIAN_POINT('Ctrl Pts',(-38.1931715130641,3.58266109147218,
126.092963534553));
#152897=CARTESIAN_POINT('Ctrl Pts',(-38.2005694273755,3.45590081949079,
125.999205663265));
#152898=CARTESIAN_POINT('Ctrl Pts',(-38.2079673416869,3.32556000811,125.910631855675));
#152899=CARTESIAN_POINT('Ctrl Pts',(-38.2153640265991,3.19524085700837,
125.822072767446));
#152900=CARTESIAN_POINT('Ctrl Pts',(-38.2227607115113,3.0613426558988,125.738696242707));
#152901=CARTESIAN_POINT('Ctrl Pts',(-38.2301573964235,2.92432054788648,
125.660793771912));
#152902=CARTESIAN_POINT('Ctrl Pts',(-38.237553753359,2.7873045155782,125.582894755395));
#152903=CARTESIAN_POINT('Ctrl Pts',(-38.2449501102944,2.64716517630255,
125.510469494701));
#152904=CARTESIAN_POINT('Ctrl Pts',(-38.2523464672299,2.50438371055579,
125.443764308124));
#152905=CARTESIAN_POINT('Ctrl Pts',(-38.2597439565665,2.36158038460171,
125.377048908812));
#152906=CARTESIAN_POINT('Ctrl Pts',(-38.267141445903,2.21613446496167,125.316055485384));
#152907=CARTESIAN_POINT('Ctrl Pts',(-38.2745389352396,2.06854846988755,
125.260982785393));
#152908=CARTESIAN_POINT('Ctrl Pts',(-38.2819390177546,1.92091073877228,
125.205890779753));
#152909=CARTESIAN_POINT('Ctrl Pts',(-38.2893391002695,1.77113178810304,
125.156723760283));
#152910=CARTESIAN_POINT('Ctrl Pts',(-38.2967391827845,1.6197305508264,125.113631006592));
#152911=CARTESIAN_POINT('Ctrl Pts',(-38.3041474024509,1.46816283232451,
125.070490867988));
#152912=CARTESIAN_POINT('Ctrl Pts',(-38.3115556221174,1.31496962396608,
125.033438436376));
#152913=CARTESIAN_POINT('Ctrl Pts',(-38.3189638417839,1.16068206049287,
125.002572296975));
#152914=CARTESIAN_POINT('Ctrl Pts',(-38.3263766210859,1.00629953559833,
124.971687159979));
#152915=CARTESIAN_POINT('Ctrl Pts',(-38.3337894003881,0.850821681264618,
124.946995960648));
#152916=CARTESIAN_POINT('Ctrl Pts',(-38.3412021796902,0.694785549349044,
124.928545473868));
#152917=CARTESIAN_POINT('Ctrl Pts',(-38.3486255507189,0.538526465691044,
124.910068624167));
#152918=CARTESIAN_POINT('Ctrl Pts',(-38.3560489217477,0.381707882463004,
124.897850325232));
#152919=CARTESIAN_POINT('Ctrl Pts',(-38.3634722927764,0.224868484980453,
124.891885270728));
#152920=CARTESIAN_POINT('Ctrl Pts',(-38.3674083422172,0.1417084731253,124.888722455701));
#152921=CARTESIAN_POINT('Ctrl Pts',(-38.371344391658,0.0585425639595697,
124.887316782014));
#152922=CARTESIAN_POINT('Ctrl Pts',(-38.3752804410988,-0.0245495673137258,
124.887661547878));
#152923=CARTESIAN_POINT('Ctrl Pts',(-38.3827037075042,-0.181258733677899,
124.888311765539));
#152924=CARTESIAN_POINT('Ctrl Pts',(-38.3901269739097,-0.338179012127287,
124.89519314427));
#152925=CARTESIAN_POINT('Ctrl Pts',(-38.3975502403151,-0.494774112546116,
124.908334062329));
#152926=CARTESIAN_POINT('Ctrl Pts',(-38.4049647330361,-0.651184130560886,
124.921459448915));
#152927=CARTESIAN_POINT('Ctrl Pts',(-38.4123792257571,-0.807269367205017,
124.940829617649));
#152928=CARTESIAN_POINT('Ctrl Pts',(-38.4197937184781,-0.962492233156298,
124.966420975568));
#152929=CARTESIAN_POINT('Ctrl Pts',(-38.4272010648318,-1.11756548946534,
124.991987667572));
#152930=CARTESIAN_POINT('Ctrl Pts',(-38.4346084111856,-1.2717776639549,
125.023763551158));
#152931=CARTESIAN_POINT('Ctrl Pts',(-38.4420157575394,-1.42459510569688,
125.061673150245));
#152932=CARTESIAN_POINT('Ctrl Pts',(-38.4494175792147,-1.57729857042446,
125.099554474923));
#152933=CARTESIAN_POINT('Ctrl Pts',(-38.4568194008902,-1.72860901291464,
125.143560316652));
#152934=CARTESIAN_POINT('Ctrl Pts',(-38.4642212225655,-1.87800192229878,
125.193563941305));
#152935=CARTESIAN_POINT('Ctrl Pts',(-38.4716191368769,-2.02731596833021,
125.243541169434));
#152936=CARTESIAN_POINT('Ctrl Pts',(-38.4790170511881,-2.17471414410284,
125.299509756694));
#152937=CARTESIAN_POINT('Ctrl Pts',(-38.4864149654995,-2.31968618927086,
125.361292866214));
#152938=CARTESIAN_POINT('Ctrl Pts',(-38.4938116504117,-2.46463414271443,
125.423065708502));
#152939=CARTESIAN_POINT('Ctrl Pts',(-38.501208335324,-2.60715642266795,
125.490651009083));
#152940=CARTESIAN_POINT('Ctrl Pts',(-38.5086050202362,-2.74676177399196,
125.563823400883));
#152941=CARTESIAN_POINT('Ctrl Pts',(-38.5160013771716,-2.8863609350686,
125.636992548143));
#152942=CARTESIAN_POINT('Ctrl Pts',(-38.5233977341069,-3.02304309405251,
125.715748120738));
#152943=CARTESIAN_POINT('Ctrl Pts',(-38.5307940910424,-3.15634092657646,
125.799818428942));
#152944=CARTESIAN_POINT('Ctrl Pts',(-38.5381915803789,-3.28965916733866,
125.883901608525));
#152945=CARTESIAN_POINT('Ctrl Pts',(-38.5455890697155,-3.41959173417185,
125.97330094475));
#152946=CARTESIAN_POINT('Ctrl Pts',(-38.552986559052,-3.54569979173979,
126.067701082687));
#152947=CARTESIAN_POINT('Ctrl Pts',(-38.560386641567,-3.67185205629075,
126.162134312446));
#152948=CARTESIAN_POINT('Ctrl Pts',(-38.5677867240819,-3.79417684364332,
126.261571610609));
#152949=CARTESIAN_POINT('Ctrl Pts',(-38.5751868065969,-3.9122680647023,
126.365657073465));
#152950=CARTESIAN_POINT('Ctrl Pts',(-38.5825950262633,-4.03048913920025,
126.46985698899));
#152951=CARTESIAN_POINT('Ctrl Pts',(-38.5900032459298,-4.14446707036462,
126.578715029497));
#152952=CARTESIAN_POINT('Ctrl Pts',(-38.5974114655962,-4.25383182435837,
126.691837624004));
#152953=CARTESIAN_POINT('Ctrl Pts',(-38.6048242448983,-4.36326389053382,
126.805029843581));
#152954=CARTESIAN_POINT('Ctrl Pts',(-38.6122370242004,-4.46807687384833,
126.922491569439));
#152955=CARTESIAN_POINT('Ctrl Pts',(-38.6196498035025,-4.56794113161665,
127.04379624761));
#152956=CARTESIAN_POINT('Ctrl Pts',(-38.6270731745312,-4.66794808011922,
127.165274251593));
#152957=CARTESIAN_POINT('Ctrl Pts',(-38.6344965455601,-4.76299195579472,
127.290605877973));
#152958=CARTESIAN_POINT('Ctrl Pts',(-38.6419199165888,-4.8527860504428,
127.419335047334));
#152959=CARTESIAN_POINT('Ctrl Pts',(-38.6458559660298,-4.90039703400673,
127.487590341745));
#152960=CARTESIAN_POINT('Ctrl Pts',(-38.6497920154706,-4.94653287243654,
127.556800375546));
#152961=CARTESIAN_POINT('Ctrl Pts',(-38.6537280649116,-4.99115613774335,
127.626894493251));
#152962=CARTESIAN_POINT('Ctrl Pts',(-38.6613354298912,-5.07740136175988,
127.762368283485));
#152963=CARTESIAN_POINT('Ctrl Pts',(-38.668942794871,-5.15824413217771,
127.901539367087));
#152964=CARTESIAN_POINT('Ctrl Pts',(-38.6765501598506,-5.23336050802567,
128.043949714179));
#152965=CARTESIAN_POINT('Ctrl Pts',(-38.6841471984717,-5.30837491970684,
128.186166751195));
#152966=CARTESIAN_POINT('Ctrl Pts',(-38.6917442370928,-5.37767825823327,
128.331613988293));
#152967=CARTESIAN_POINT('Ctrl Pts',(-38.6993412757139,-5.44098975463447,
128.479804519628));
#152968=CARTESIAN_POINT('Ctrl Pts',(-38.706929205525,-5.5042253408787,128.627817371281));
#152969=CARTESIAN_POINT('Ctrl Pts',(-38.7145171353361,-5.56148326037924,
128.778566646554));
#152970=CARTESIAN_POINT('Ctrl Pts',(-38.7221050651471,-5.61252852435859,
128.931540784864));
#152971=CARTESIAN_POINT('Ctrl Pts',(-38.729682813662,-5.66350529706784,
129.084309666267));
#152972=CARTESIAN_POINT('Ctrl Pts',(-38.7372605621768,-5.70828592504904,
129.239297129655));
#152973=CARTESIAN_POINT('Ctrl Pts',(-38.7448383106917,-5.74668354628789,
129.395971899447));
#152974=CARTESIAN_POINT('Ctrl Pts',(-38.7524101067497,-5.78505100550889,
129.552523598408));
#152975=CARTESIAN_POINT('Ctrl Pts',(-38.7599819028078,-5.81704536229033,
129.710759626737));
#152976=CARTESIAN_POINT('Ctrl Pts',(-38.7675536988658,-5.8425293624966,
129.870133016355));
#152977=CARTESIAN_POINT('Ctrl Pts',(-38.7751197874821,-5.86799415346311,
130.029386274061));
#152978=CARTESIAN_POINT('Ctrl Pts',(-38.7826858760982,-5.88695831494093,
130.189774840909));
#152979=CARTESIAN_POINT('Ctrl Pts',(-38.7902519647145,-5.89933554312272,
130.350741049923));
#152980=CARTESIAN_POINT('Ctrl Pts',(-38.797376245739,-5.91099002621745,
130.502307938262));
#152981=CARTESIAN_POINT('Ctrl Pts',(-38.8045005267636,-5.91680476845105,
130.654386640099));
#152982=CARTESIAN_POINT('Ctrl Pts',(-38.8116248077881,-5.91674961105175,
130.806505989098));
#152983=CARTESIAN_POINT('',(-40.5616248077881,-5.92172186145805,130.808909800869));
#152984=CARTESIAN_POINT('Ctrl Pts',(-38.8116262899063,-5.90765850045092,
130.806534290646));
#152985=CARTESIAN_POINT('Ctrl Pts',(-38.8518094228458,-5.9104285553906,
131.66321689387));
#152986=CARTESIAN_POINT('Ctrl Pts',(-38.9848084303895,-5.33445556096476,
134.495125854073));
#152987=CARTESIAN_POINT('Ctrl Pts',(-39.2106233125373,-0.964348369497292,
137.735997707935));
#152988=CARTESIAN_POINT('Ctrl Pts',(-39.4890709363504,5.31052874905888,
135.362413374583));
#152989=CARTESIAN_POINT('Ctrl Pts',(-39.7675185601631,6.70528938098473,
128.800201230786));
#152990=CARTESIAN_POINT('Ctrl Pts',(-40.0459661839761,1.9382166433815,124.079713654814));
#152991=CARTESIAN_POINT('Ctrl Pts',(-40.3106682665177,-4.28673125538328,
125.466818082008));
#152992=CARTESIAN_POINT('Ctrl Pts',(-40.4825544744551,-5.90748225943271,
129.133335360171));
#152993=CARTESIAN_POINT('Ctrl Pts',(-40.5616248077881,-5.92172186145805,
130.808909800869));
#152994=CARTESIAN_POINT('',(-42.3116248077881,-5.92233099613373,130.800046206929));
#152995=CARTESIAN_POINT('Ctrl Pts',(-40.5616248077881,-5.92172186145805,
130.808909800869));
#152996=CARTESIAN_POINT('Ctrl Pts',(-40.5753703490593,-5.92419726568458,
131.100190697975));
#152997=CARTESIAN_POINT('Ctrl Pts',(-40.6819317649349,-5.77205163170407,
133.35573096718));
#152998=CARTESIAN_POINT('Ctrl Pts',(-40.8813090554146,-2.87285705459878,
137.185916295787));
#152999=CARTESIAN_POINT('Ctrl Pts',(-41.1597566792278,3.8161341156876,136.670763343377));
#153000=CARTESIAN_POINT('Ctrl Pts',(-41.4382043030406,6.99828446217392,
130.764672875656));
#153001=CARTESIAN_POINT('Ctrl Pts',(-41.7166519268534,3.74935327312268,
124.895053503897));
#153002=CARTESIAN_POINT('Ctrl Pts',(-41.9950995506663,-2.94505040783266,
124.455798683895));
#153003=CARTESIAN_POINT('Ctrl Pts',(-42.1934238443113,-5.78553595672184,
128.298218441183));
#153004=CARTESIAN_POINT('Ctrl Pts',(-42.2989322633518,-5.92453367529058,
130.531151337971));
#153005=CARTESIAN_POINT('Ctrl Pts',(-42.3116248077881,-5.92233099613373,
130.800046206929));
#153006=CARTESIAN_POINT('',(-44.0616248077881,-5.9079203307475,130.801880397855));
#153007=CARTESIAN_POINT('Ctrl Pts',(-42.3116248077881,-5.92233099613373,
130.800046206929));
#153008=CARTESIAN_POINT('Ctrl Pts',(-42.3917481379561,-5.90842629875613,
132.497479883376));
#153009=CARTESIAN_POINT('Ctrl Pts',(-42.5646873427284,-4.25074246905246,
136.184942210171));
#153010=CARTESIAN_POINT('Ctrl Pts',(-42.830442422105,2.01436137498844,137.506592244515));
#153011=CARTESIAN_POINT('Ctrl Pts',(-43.1088900459179,6.72758881151127,
132.732341248584));
#153012=CARTESIAN_POINT('Ctrl Pts',(-43.3873376697308,5.25849079123855,
126.186370239837));
#153013=CARTESIAN_POINT('Ctrl Pts',(-43.6657852935438,-1.04290337462631,
123.884106786848));
#153014=CARTESIAN_POINT('Ctrl Pts',(-43.890547672896,-5.35577621547134,
127.158999481025));
#153015=CARTESIAN_POINT('Ctrl Pts',(-44.0224941776442,-5.91105646319498,
129.967728913076));
#153016=CARTESIAN_POINT('Ctrl Pts',(-44.0616248077881,-5.9079203307475,
130.801880397855));
#153017=CARTESIAN_POINT('',(-45.8116248406311,-5.91565936145396,130.80955222336));
#153018=CARTESIAN_POINT('Ctrl Pts',(-44.0616248077881,-5.9079203307475,
130.801880397855));
#153019=CARTESIAN_POINT('Ctrl Pts',(-44.1153100522485,-5.90361771572484,
131.946294025052));
#153020=CARTESIAN_POINT('Ctrl Pts',(-44.2618111713132,-5.02991776548405,
135.075346352124));
#153021=CARTESIAN_POINT('Ctrl Pts',(-44.5011281649824,0.0503378935809273,
137.802576577854));
#153022=CARTESIAN_POINT('Ctrl Pts',(-44.7795757887951,5.91500614821685,
134.544716589515));
#153023=CARTESIAN_POINT('Ctrl Pts',(-45.0580234126083,6.34407271675586,
127.849652189506));
#153024=CARTESIAN_POINT('Ctrl Pts',(-45.3364710364209,0.943246383778656,
123.869820489349));
#153025=CARTESIAN_POINT('Ctrl Pts',(-45.5876715014812,-4.71106648683667,
126.028360352011));
#153026=CARTESIAN_POINT('Ctrl Pts',(-45.7460560919367,-5.90156674869486,
129.414958509883));
#153027=CARTESIAN_POINT('Ctrl Pts',(-45.8116248077881,-5.9132152101497,
130.809549379698));
#153028=CARTESIAN_POINT('',(-47.5616248077881,-5.9209525136144,130.804682771848));
#153029=CARTESIAN_POINT('Ctrl Pts',(-45.8116248552558,-5.9167477212215,
130.809553489618));
#153030=CARTESIAN_POINT('Ctrl Pts',(-45.8206040918004,-5.9165800069701,
131.000646762258));
#153031=CARTESIAN_POINT('Ctrl Pts',(-45.829583328345,-5.9071510035541,131.191332648828));
#153032=CARTESIAN_POINT('Ctrl Pts',(-45.8385625648896,-5.88860123260384,
131.380820577907));
#153033=CARTESIAN_POINT('Ctrl Pts',(-45.8476965180825,-5.8697318400051,
131.573573476911));
#153034=CARTESIAN_POINT('Ctrl Pts',(-45.8568304712754,-5.84142468682038,
131.765086783783));
#153035=CARTESIAN_POINT('Ctrl Pts',(-45.8659644244682,-5.8038773369655,
131.954551219144));
#153036=CARTESIAN_POINT('Ctrl Pts',(-45.8750983776611,-5.76632998711067,
132.144015654505));
#153037=CARTESIAN_POINT('Ctrl Pts',(-45.8842323308539,-5.71954254678255,
132.331431292939));
#153038=CARTESIAN_POINT('Ctrl Pts',(-45.8933662840467,-5.66376059943453,
132.516010825638));
#153039=CARTESIAN_POINT('Ctrl Pts',(-45.9007895504522,-5.61842598395795,
132.666020686132));
#153040=CARTESIAN_POINT('Ctrl Pts',(-45.9082128168576,-5.56705897911314,
132.81445504191));
#153041=CARTESIAN_POINT('Ctrl Pts',(-45.9156360832631,-5.50978539765564,
132.960791797613));
#153042=CARTESIAN_POINT('Ctrl Pts',(-45.9230505759841,-5.45257950881506,
133.106955595424));
#153043=CARTESIAN_POINT('Ctrl Pts',(-45.9304650687051,-5.38948107397045,
133.251026383773));
#153044=CARTESIAN_POINT('Ctrl Pts',(-45.9378795614261,-5.32066608754048,
133.392495650248));
#153045=CARTESIAN_POINT('Ctrl Pts',(-45.9452869077799,-5.25191742758537,
133.533828563318));
#153046=CARTESIAN_POINT('Ctrl Pts',(-45.9526942541338,-5.17746334722068,
133.672564612907));
#153047=CARTESIAN_POINT('Ctrl Pts',(-45.9601016004875,-5.09752844371975,
133.808213864309));
#153048=CARTESIAN_POINT('Ctrl Pts',(-45.967503422163,-5.0176531586855,133.943761943382));
#153049=CARTESIAN_POINT('Ctrl Pts',(-45.9749052438384,-4.93230537858831,
134.076227488131));
#153050=CARTESIAN_POINT('Ctrl Pts',(-45.9823070655138,-4.84175622036051,
134.205143948668));
#153051=CARTESIAN_POINT('Ctrl Pts',(-45.9897049798252,-4.75125486232863,
134.333992355208));
#153052=CARTESIAN_POINT('Ctrl Pts',(-45.9971028941366,-4.65555780851086,
134.459295104067));
#153053=CARTESIAN_POINT('Ctrl Pts',(-46.0045008084479,-4.55498013012467,
134.580613598587));
#153054=CARTESIAN_POINT('Ctrl Pts',(-46.0118974933601,-4.45441916592382,
134.701911932174));
#153055=CARTESIAN_POINT('Ctrl Pts',(-46.0192941782724,-4.34897942490795,
134.819227038416));
#153056=CARTESIAN_POINT('Ctrl Pts',(-46.0266908631846,-4.23901706882133,
134.932152382268));
#153057=CARTESIAN_POINT('Ctrl Pts',(-46.0340872201201,-4.12905958858097,
135.045072718892));
#153058=CARTESIAN_POINT('Ctrl Pts',(-46.0414835770555,-4.01458015243537,
135.153603412703));
#153059=CARTESIAN_POINT('Ctrl Pts',(-46.048879933991,-3.89597249152699,
135.257374081252));
#153060=CARTESIAN_POINT('Ctrl Pts',(-46.0562774233276,-3.77734667148276,
135.361160637355));
#153061=CARTESIAN_POINT('Ctrl Pts',(-46.0636749126641,-3.65459164916284,
135.460185471294));
#153062=CARTESIAN_POINT('Ctrl Pts',(-46.0710724020007,-3.52813487758272,
135.554117963798));
#153063=CARTESIAN_POINT('Ctrl Pts',(-46.0784724845157,-3.40163377677754,
135.648083384191));
#153064=CARTESIAN_POINT('Ctrl Pts',(-46.0858725670307,-3.27142864259895,
135.736952686545));
#153065=CARTESIAN_POINT('Ctrl Pts',(-46.0932726495457,-3.13797644840548,
135.820438205857));
#153066=CARTESIAN_POINT('Ctrl Pts',(-46.1006808692122,-3.00437750980528,
135.90401552608));
#153067=CARTESIAN_POINT('Ctrl Pts',(-46.1080890888787,-2.86752469738175,
135.982197042484));
#153068=CARTESIAN_POINT('Ctrl Pts',(-46.1154973085452,-2.72790079898975,
136.054740393675));
#153069=CARTESIAN_POINT('Ctrl Pts',(-46.1229100878472,-2.58819096441784,
136.127328394087));
#153070=CARTESIAN_POINT('Ctrl Pts',(-46.1303228671493,-2.4457069824236,
136.194271156114));
#153071=CARTESIAN_POINT('Ctrl Pts',(-46.1377356464513,-2.30095172868477,
136.255374441137));
#153072=CARTESIAN_POINT('Ctrl Pts',(-46.1451590174801,-2.15598964185105,
136.316565033399));
#153073=CARTESIAN_POINT('Ctrl Pts',(-46.1525823885089,-2.00875015019221,
136.371899353406));
#153074=CARTESIAN_POINT('Ctrl Pts',(-46.1600057595377,-1.85975217773808,
136.42123273645));
#153075=CARTESIAN_POINT('Ctrl Pts',(-46.1639418089784,-1.78074987758808,
136.447390479878));
#153076=CARTESIAN_POINT('Ctrl Pts',(-46.167877858419,-1.70125340339786,
136.471861993046));
#153077=CARTESIAN_POINT('Ctrl Pts',(-46.1718139078597,-1.62134115253402,
136.49463156275));
#153078=CARTESIAN_POINT('Ctrl Pts',(-46.1792371742651,-1.47062914137653,
136.537574260597));
#153079=CARTESIAN_POINT('Ctrl Pts',(-46.1866604406705,-1.31798199315385,
136.574590139641));
#153080=CARTESIAN_POINT('Ctrl Pts',(-46.1940837070759,-1.16390696634591,
136.60550284442));
#153081=CARTESIAN_POINT('Ctrl Pts',(-46.201498199797,-1.0100140434243,136.63637901295));
#153082=CARTESIAN_POINT('Ctrl Pts',(-46.208912692518,-0.854696963591946,
136.661166292901));
#153083=CARTESIAN_POINT('Ctrl Pts',(-46.216327185239,-0.698478682024039,
136.679737889985));
#153084=CARTESIAN_POINT('Ctrl Pts',(-46.2237345315928,-0.542410969517422,
136.698291587064));
#153085=CARTESIAN_POINT('Ctrl Pts',(-46.2311418779465,-0.385444152710189,
136.710641484224));
#153086=CARTESIAN_POINT('Ctrl Pts',(-46.2385492243003,-0.228111827858697,
136.716711719834));
#153087=CARTESIAN_POINT('Ctrl Pts',(-46.2459510459757,-0.0708968473911126,
136.722777428034));
#153088=CARTESIAN_POINT('Ctrl Pts',(-46.2533528676511,0.0866827269031233,
136.722572786051));
#153089=CARTESIAN_POINT('Ctrl Pts',(-46.2607546893265,0.24408782806416,
136.716073710629));
#153090=CARTESIAN_POINT('Ctrl Pts',(-46.2681526036379,0.401409836297532,
136.709578066018));
#153091=CARTESIAN_POINT('Ctrl Pts',(-46.2755505179492,0.558557182789278,
136.696794620807));
#153092=CARTESIAN_POINT('Ctrl Pts',(-46.2829484322605,0.714990560060742,
136.67775138113));
#153093=CARTESIAN_POINT('Ctrl Pts',(-46.2903451171727,0.871397940942893,
136.658711306094));
#153094=CARTESIAN_POINT('Ctrl Pts',(-46.2977418020848,1.02709121788791,
136.633413546274));
#153095=CARTESIAN_POINT('Ctrl Pts',(-46.305138486997,1.18153584732672,136.60193800851));
#153096=CARTESIAN_POINT('Ctrl Pts',(-46.3125348439324,1.33597362852904,
136.570463866404));
#153097=CARTESIAN_POINT('Ctrl Pts',(-46.3199312008679,1.48916250653336,
136.532812565563));
#153098=CARTESIAN_POINT('Ctrl Pts',(-46.3273275578034,1.64057804679553,
136.489115162388));
#153099=CARTESIAN_POINT('Ctrl Pts',(-46.3347250471399,1.79201676916325,
136.445411069029));
#153100=CARTESIAN_POINT('Ctrl Pts',(-46.3421225364765,1.94168125450721,
136.395659133709));
#153101=CARTESIAN_POINT('Ctrl Pts',(-46.349520025813,2.08906229467371,136.340040276964));
#153102=CARTESIAN_POINT('Ctrl Pts',(-46.356920108328,2.23649499903559,136.284401923115));
#153103=CARTESIAN_POINT('Ctrl Pts',(-46.364320190843,2.38164231547602,136.222892684806));
#153104=CARTESIAN_POINT('Ctrl Pts',(-46.371720273358,2.52401521801844,136.155741536704));
#153105=CARTESIAN_POINT('Ctrl Pts',(-46.3791284930245,2.66654467420348,
136.088516549011));
#153106=CARTESIAN_POINT('Ctrl Pts',(-46.3865367126909,2.80629328610091,
136.015637421353));
#153107=CARTESIAN_POINT('Ctrl Pts',(-46.3939449323574,2.94279618957607,
135.93737933457));
#153108=CARTESIAN_POINT('Ctrl Pts',(-46.4013577116595,3.07938310831084,
135.859073081241));
#153109=CARTESIAN_POINT('Ctrl Pts',(-46.4087704909616,3.21272002255385,
135.775381469877));
#153110=CARTESIAN_POINT('Ctrl Pts',(-46.4161832702636,3.34237169726821,
135.68662259331));
#153111=CARTESIAN_POINT('Ctrl Pts',(-46.4236066412924,3.47220862437528,
135.597736893899));
#153112=CARTESIAN_POINT('Ctrl Pts',(-46.431030012321,3.59834949671244,135.503769691108));
#153113=CARTESIAN_POINT('Ctrl Pts',(-46.4384533833498,3.7203921126505,135.405079375611));
#153114=CARTESIAN_POINT('Ctrl Pts',(-46.4423894327907,3.78510203599523,
135.352751402291));
#153115=CARTESIAN_POINT('Ctrl Pts',(-46.4463254822316,3.84866039920618,
135.299096217713));
#153116=CARTESIAN_POINT('Ctrl Pts',(-46.4502615316725,3.91101160662611,
135.244171286427));
#153117=CARTESIAN_POINT('Ctrl Pts',(-46.457684798078,4.02860403790226,135.140584580175));
#153118=CARTESIAN_POINT('Ctrl Pts',(-46.4651080644834,4.14225605751435,
135.032166197969));
#153119=CARTESIAN_POINT('Ctrl Pts',(-46.4725313308888,4.25154510702018,
134.919247586302));
#153120=CARTESIAN_POINT('Ctrl Pts',(-46.4799458236099,4.36070498594555,
134.806462435056));
#153121=CARTESIAN_POINT('Ctrl Pts',(-46.4873603163309,4.46551190206133,
134.689187907262));
#153122=CARTESIAN_POINT('Ctrl Pts',(-46.4947748090519,4.56557650969404,
134.567795444507));
#153123=CARTESIAN_POINT('Ctrl Pts',(-46.5021821554057,4.66554467129055,
134.446519984378));
#153124=CARTESIAN_POINT('Ctrl Pts',(-46.5095895017595,4.76077938815014,
134.321134776944));
#153125=CARTESIAN_POINT('Ctrl Pts',(-46.5169968481133,4.85092841392537,
134.192047746784));
#153126=CARTESIAN_POINT('Ctrl Pts',(-46.5243986697887,4.94101020315604,
134.063056994602));
#153127=CARTESIAN_POINT('Ctrl Pts',(-46.5318004914641,5.02601364106179,
133.930370221872));
#153128=CARTESIAN_POINT('Ctrl Pts',(-46.5392023131395,5.10562708685644,
133.794427943306));
#153129=CARTESIAN_POINT('Ctrl Pts',(-46.5466002274509,5.18519850533277,
133.658557427611));
#153130=CARTESIAN_POINT('Ctrl Pts',(-46.5539981417623,5.2593854101478,133.519435149973));
#153131=CARTESIAN_POINT('Ctrl Pts',(-46.5613960560736,5.32791985478793,
133.377529983048));
#153132=CARTESIAN_POINT('Ctrl Pts',(-46.5687927409858,5.3964429102466,133.235648398188));
#153133=CARTESIAN_POINT('Ctrl Pts',(-46.576189425898,5.4593152076483,133.090985177716));
#153134=CARTESIAN_POINT('Ctrl Pts',(-46.5835861108102,5.51631504102523,
132.944033239875));
#153135=CARTESIAN_POINT('Ctrl Pts',(-46.5909824677457,5.57331234696981,
132.797087818037));
#153136=CARTESIAN_POINT('Ctrl Pts',(-46.5983788246811,5.62443757163981,
132.647854228649));
#153137=CARTESIAN_POINT('Ctrl Pts',(-46.6057751816165,5.66951750681539,
132.496844532531));
#153138=CARTESIAN_POINT('Ctrl Pts',(-46.6131726709531,5.71460434384419,
132.345811716442));
#153139=CARTESIAN_POINT('Ctrl Pts',(-46.6205701602898,5.7536439416983,132.193002609904));
#153140=CARTESIAN_POINT('Ctrl Pts',(-46.6279676496264,5.78651327450287,
132.038943416127));
#153141=CARTESIAN_POINT('Ctrl Pts',(-46.6353677321414,5.81939412960106,
131.884830217138));
#153142=CARTESIAN_POINT('Ctrl Pts',(-46.6427678146564,5.84610033533533,
131.729466423278));
#153143=CARTESIAN_POINT('Ctrl Pts',(-46.6501678971714,5.86656020409331,
131.573387232352));
#153144=CARTESIAN_POINT('Ctrl Pts',(-46.6575761168379,5.88704257058034,
131.417136416309));
#153145=CARTESIAN_POINT('Ctrl Pts',(-46.6649843365043,5.90126483471731,
131.260169002562));
#153146=CARTESIAN_POINT('Ctrl Pts',(-46.6723925561708,5.90920724351964,
131.103024836439));
#153147=CARTESIAN_POINT('Ctrl Pts',(-46.6798053354729,5.91715454074205,
130.945783950704));
#153148=CARTESIAN_POINT('Ctrl Pts',(-46.6872181147749,5.91881427691498,
130.78836646823));
#153149=CARTESIAN_POINT('Ctrl Pts',(-46.694630894077,5.91421881737888,130.631310501526));
#153150=CARTESIAN_POINT('Ctrl Pts',(-46.7020542651057,5.9096167916347,130.474030125892));
#153151=CARTESIAN_POINT('Ctrl Pts',(-46.7094776361345,5.89874174529678,
130.317112669114));
#153152=CARTESIAN_POINT('Ctrl Pts',(-46.7169010071633,5.88167780278516,
130.161090233727));
#153153=CARTESIAN_POINT('Ctrl Pts',(-46.720837056604,5.87263009102193,130.078363394779));
#153154=CARTESIAN_POINT('Ctrl Pts',(-46.7247731060448,5.86184331245711,
129.995888005881));
#153155=CARTESIAN_POINT('Ctrl Pts',(-46.7287091554855,5.84933576283583,
129.913741902228));
#153156=CARTESIAN_POINT('Ctrl Pts',(-46.736132421891,5.82574691459707,129.75881691443));
#153157=CARTESIAN_POINT('Ctrl Pts',(-46.7435556882964,5.79596315178447,
129.604595467689));
#153158=CARTESIAN_POINT('Ctrl Pts',(-46.7509789547018,5.76003492655879,
129.451612227316));
#153159=CARTESIAN_POINT('Ctrl Pts',(-46.7583934474228,5.72414916551163,
129.298809800429));
#153160=CARTESIAN_POINT('Ctrl Pts',(-46.7658079401439,5.68213348210251,
129.147243026752));
#153161=CARTESIAN_POINT('Ctrl Pts',(-46.7732224328649,5.63408992981298,
128.997440247079));
#153162=CARTESIAN_POINT('Ctrl Pts',(-46.7806297792187,5.58609268370796,
128.847781852965));
#153163=CARTESIAN_POINT('Ctrl Pts',(-46.7880371255726,5.53207924830008,
128.699884421162));
#153164=CARTESIAN_POINT('Ctrl Pts',(-46.7954444719264,5.47220242433592,
128.554264799697));
#153165=CARTESIAN_POINT('Ctrl Pts',(-46.8028462936018,5.41237025876611,
128.408753786839));
#153166=CARTESIAN_POINT('Ctrl Pts',(-46.8102481152771,5.34668355349613,
128.265517545392));
#153167=CARTESIAN_POINT('Ctrl Pts',(-46.8176499369525,5.27534447657152,
128.125056376535));
#153168=CARTESIAN_POINT('Ctrl Pts',(-46.8250478512639,5.20404305899032,
127.984669356036));
#153169=CARTESIAN_POINT('Ctrl Pts',(-46.8324457655753,5.12709538083476,
127.847054822619));
#153170=CARTESIAN_POINT('Ctrl Pts',(-46.8398436798867,5.0447510863124,127.712691644398));
#153171=CARTESIAN_POINT('Ctrl Pts',(-46.8472403647989,4.96242047591803,
127.578350794899));
#153172=CARTESIAN_POINT('Ctrl Pts',(-46.854637049711,4.87469522394634,127.447260546199));
#153173=CARTESIAN_POINT('Ctrl Pts',(-46.8620337346233,4.78187019898427,
127.319873860156));
#153174=CARTESIAN_POINT('Ctrl Pts',(-46.8694300915587,4.68904928998107,
127.192492822572));
#153175=CARTESIAN_POINT('Ctrl Pts',(-46.8768264484943,4.59112927745094,
127.068815322819));
#153176=CARTESIAN_POINT('Ctrl Pts',(-46.8842228054297,4.48844734939068,
126.949263867256));
#153177=CARTESIAN_POINT('Ctrl Pts',(-46.8916202947663,4.38574970046495,
126.829694108061));
#153178=CARTESIAN_POINT('Ctrl Pts',(-46.8990177841029,4.27828892759111,
126.714251934074));
#153179=CARTESIAN_POINT('Ctrl Pts',(-46.9064152734394,4.16644124194198,
126.603325276136));
#153180=CARTESIAN_POINT('Ctrl Pts',(-46.9138153559545,4.05455434826004,
126.49235973303));
#153181=CARTESIAN_POINT('Ctrl Pts',(-46.9212154384694,3.93827774488875,
126.385913120234));
#153182=CARTESIAN_POINT('Ctrl Pts',(-46.9286155209844,3.81802295999359,
126.284335038052));
#153183=CARTESIAN_POINT('Ctrl Pts',(-46.9360237406509,3.69763594259994,
126.182645260326));
#153184=CARTESIAN_POINT('Ctrl Pts',(-46.9434319603175,3.57326229303051,
126.08583494544));
#153185=CARTESIAN_POINT('Ctrl Pts',(-46.950840179984,3.44534552147863,125.994212511725));
#153186=CARTESIAN_POINT('Ctrl Pts',(-46.9582529592861,3.31735001928808,
125.90253368593));
#153187=CARTESIAN_POINT('Ctrl Pts',(-46.9656657385881,3.18580736093037,
125.816049308469));
#153188=CARTESIAN_POINT('Ctrl Pts',(-46.9730785178902,3.05118776995655,
125.735023012418));
#153189=CARTESIAN_POINT('Ctrl Pts',(-46.980501888919,2.91637582819831,125.653880942196));
#153190=CARTESIAN_POINT('Ctrl Pts',(-46.9879252599477,2.77847849949409,
125.578212708367));
#153191=CARTESIAN_POINT('Ctrl Pts',(-46.9953486309765,2.63798892808085,
125.508235149092));
#153192=CARTESIAN_POINT('Ctrl Pts',(-46.9992846804171,2.56349798631965,
125.471131368077));
#153193=CARTESIAN_POINT('Ctrl Pts',(-47.0032207298578,2.48827858852154,
125.435626628109));
#153194=CARTESIAN_POINT('Ctrl Pts',(-47.0071567792984,2.41240610893801,
125.401747608284));
#153195=CARTESIAN_POINT('Ctrl Pts',(-47.0145800457038,2.26931298033693,
125.33785283422));
#153196=CARTESIAN_POINT('Ctrl Pts',(-47.0220033121093,2.12346325810717,
125.279550298363));
#153197=CARTESIAN_POINT('Ctrl Pts',(-47.0294265785147,1.97533404194146,
125.227086553541));
#153198=CARTESIAN_POINT('Ctrl Pts',(-47.0368410712357,1.8273799022079,125.174684816508));
#153199=CARTESIAN_POINT('Ctrl Pts',(-47.0442555639566,1.67715197974729,
125.12810825751));
#153200=CARTESIAN_POINT('Ctrl Pts',(-47.0516700566776,1.52514994503228,
125.087556597165));
#153201=CARTESIAN_POINT('Ctrl Pts',(-47.0590774030314,1.37329441560132,
125.047044022038));
#153202=CARTESIAN_POINT('Ctrl Pts',(-47.0664847493851,1.2196685363637,125.012544880502));
#153203=CARTESIAN_POINT('Ctrl Pts',(-47.0738920957389,1.06478973873867,
124.984209985943));
#153204=CARTESIAN_POINT('Ctrl Pts',(-47.0812939174143,0.910026455563924,
124.955896224619));
#153205=CARTESIAN_POINT('Ctrl Pts',(-47.0886957390897,0.754012480288078,
124.933737622864));
#153206=CARTESIAN_POINT('Ctrl Pts',(-47.0960975607651,0.597278007230945,
124.917834515986));
#153207=CARTESIAN_POINT('Ctrl Pts',(-47.1034954750764,0.440626273082122,
124.901939804235));
#153208=CARTESIAN_POINT('Ctrl Pts',(-47.1108933893877,0.283255169078555,
124.892294048405));
#153209=CARTESIAN_POINT('Ctrl Pts',(-47.118291303699,0.125702519317995,
124.888946055666));
#153210=CARTESIAN_POINT('Ctrl Pts',(-47.1256879886112,-0.0318239480504715,
124.885598619303));
#153211=CARTESIAN_POINT('Ctrl Pts',(-47.1330846735234,-0.189531528449952,
124.888546876815));
#153212=CARTESIAN_POINT('Ctrl Pts',(-47.1404813584356,-0.346879748565037,
124.897787583857));
#153213=CARTESIAN_POINT('Ctrl Pts',(-47.147877715371,-0.504220991695153,
124.907027881157));
#153214=CARTESIAN_POINT('Ctrl Pts',(-47.1552740723065,-0.661202533568382,
124.92256005133));
#153215=CARTESIAN_POINT('Ctrl Pts',(-47.1626704292419,-0.817286649267769,
124.944328783572));
#153216=CARTESIAN_POINT('Ctrl Pts',(-47.1700679185785,-0.973394661843957,
124.966100848662));
#153217=CARTESIAN_POINT('Ctrl Pts',(-47.1774654079151,-1.12860460492493,
124.994111325456));
#153218=CARTESIAN_POINT('Ctrl Pts',(-47.1848628972517,-1.28238674997907,
125.028253382933));
#153219=CARTESIAN_POINT('Ctrl Pts',(-47.1922629797666,-1.43622280312554,
125.062407408856));
#153220=CARTESIAN_POINT('Ctrl Pts',(-47.1996630622816,-1.58862969753152,
125.102697214077));
#153221=CARTESIAN_POINT('Ctrl Pts',(-47.2070631447966,-1.7390908635335,
125.148965535799));
#153222=CARTESIAN_POINT('Ctrl Pts',(-47.214471364463,-1.88971747705528,
125.195284734298));
#153223=CARTESIAN_POINT('Ctrl Pts',(-47.2218795841295,-2.03839373236685,
125.247595468205));
#153224=CARTESIAN_POINT('Ctrl Pts',(-47.229287803796,-2.18462042029797,
125.305691307477));
#153225=CARTESIAN_POINT('Ctrl Pts',(-47.236700583098,-2.33093710831559,
125.363822903768));
#153226=CARTESIAN_POINT('Ctrl Pts',(-47.2441133624,-2.47480088438865,125.427746549209));
#153227=CARTESIAN_POINT('Ctrl Pts',(-47.2515261417021,-2.61573577922724,
125.497209131527));
#153228=CARTESIAN_POINT('Ctrl Pts',(-47.2589495127308,-2.75687204845277,
125.566770965239));
#153229=CARTESIAN_POINT('Ctrl Pts',(-47.2663728837596,-2.89507075110273,
125.641887364649));
#153230=CARTESIAN_POINT('Ctrl Pts',(-47.2737962547883,-3.02988289858559,
125.722260639864));
#153231=CARTESIAN_POINT('Ctrl Pts',(-47.2777323042293,-3.10136353395812,
125.764876478916));
#153232=CARTESIAN_POINT('Ctrl Pts',(-47.2816683536703,-3.17189259909195,
125.808969509407));
#153233=CARTESIAN_POINT('Ctrl Pts',(-47.2856044031113,-3.24140690648408,
125.854490737549));
#153234=CARTESIAN_POINT('Ctrl Pts',(-47.2930162254636,-3.37230660809053,
125.940210000303));
#153235=CARTESIAN_POINT('Ctrl Pts',(-47.3004280478159,-3.50000465181596,
126.031256948241));
#153236=CARTESIAN_POINT('Ctrl Pts',(-47.3078398701682,-3.62403655674368,
126.127364829896));
#153237=CARTESIAN_POINT('Ctrl Pts',(-47.3152429245292,-3.74792173518232,
126.223359018448));
#153238=CARTESIAN_POINT('Ctrl Pts',(-47.3226459788901,-3.86814911387529,
126.324401997154));
#153239=CARTESIAN_POINT('Ctrl Pts',(-47.330049033251,-3.98428134418833,
126.430182668185));
#153240=CARTESIAN_POINT('Ctrl Pts',(-47.3374449580763,-4.10030173297716,
126.535861466795));
#153241=CARTESIAN_POINT('Ctrl Pts',(-47.3448408829016,-4.21223454932345,
126.646268624337));
#153242=CARTESIAN_POINT('Ctrl Pts',(-47.3522368077269,-4.31967394087877,
126.761051625293));
#153243=CARTESIAN_POINT('Ctrl Pts',(-47.3596272357581,-4.42703348140647,
126.87574931731));
#153244=CARTESIAN_POINT('Ctrl Pts',(-47.3670176637894,-4.52990599151765,
126.994816105166));
#153245=CARTESIAN_POINT('Ctrl Pts',(-47.3744080918207,-4.62792115513288,
127.117861418546));
#153246=CARTESIAN_POINT('Ctrl Pts',(-47.3817946513783,-4.72588501331898,
127.240842324621));
#153247=CARTESIAN_POINT('Ctrl Pts',(-47.389181210936,-4.81899635557964,
127.367797316666));
#153248=CARTESIAN_POINT('Ctrl Pts',(-47.3965677704936,-4.90692407484567,
127.498301530647));
#153249=CARTESIAN_POINT('Ctrl Pts',(-47.4039531539833,-4.99483779449974,
127.628784966102));
#153250=CARTESIAN_POINT('Ctrl Pts',(-47.4113385374729,-5.07756931966951,
127.76281619184));
#153251=CARTESIAN_POINT('Ctrl Pts',(-47.4187239209626,-5.1548298966107,
127.899939969742));
#153252=CARTESIAN_POINT('Ctrl Pts',(-47.4261090319252,-5.23208762256904,
128.037058687656));
#153253=CARTESIAN_POINT('Ctrl Pts',(-47.4334941428878,-5.30387461774855,
128.177269404505));
#153254=CARTESIAN_POINT('Ctrl Pts',(-47.4408792538504,-5.36994742205108,
128.320091057533));
#153255=CARTESIAN_POINT('Ctrl Pts',(-47.448265562596,-5.43603094262898,
128.462935874648));
#153256=CARTESIAN_POINT('Ctrl Pts',(-47.4556518713417,-5.49639826988397,
128.608392131039));
#153257=CARTESIAN_POINT('Ctrl Pts',(-47.4630381800873,-5.55085362025247,
128.755957666721));
#153258=CARTESIAN_POINT('Ctrl Pts',(-47.4704271573781,-5.60532864439423,
128.903576515271));
#153259=CARTESIAN_POINT('Ctrl Pts',(-47.4778161346689,-5.65388730982331,
129.053305809042));
#153260=CARTESIAN_POINT('Ctrl Pts',(-47.4852051119597,-5.69638338638967,
129.20462724048));
#153261=CARTESIAN_POINT('Ctrl Pts',(-47.4926022196446,-5.73892622312777,
129.35611517708));
#153262=CARTESIAN_POINT('Ctrl Pts',(-47.4999993273293,-5.77539304871202,
129.509198388863));
#153263=CARTESIAN_POINT('Ctrl Pts',(-47.5073964350142,-5.80568839616147,
129.663346678485));
#153264=CARTESIAN_POINT('Ctrl Pts',(-47.5147981891878,-5.83600277361541,
129.817591796265));
#153265=CARTESIAN_POINT('Ctrl Pts',(-47.5221999433615,-5.86013789172212,
129.972902955716));
#153266=CARTESIAN_POINT('Ctrl Pts',(-47.5296016975352,-5.87805012173235,
130.128744358953));
#153267=CARTESIAN_POINT('Ctrl Pts',(-47.5370138398728,-5.89598749107826,
130.284804481431));
#153268=CARTESIAN_POINT('Ctrl Pts',(-47.5444259822105,-5.90768450440213,
130.441395961452));
#153269=CARTESIAN_POINT('Ctrl Pts',(-47.5518381245481,-5.91314961196789,
130.597981769367));
#153270=CARTESIAN_POINT('Ctrl Pts',(-47.5551003522948,-5.91555491191055,
130.666898223484));
#153271=CARTESIAN_POINT('Ctrl Pts',(-47.5583625800414,-5.91675373834474,
130.735813626156));
#153272=CARTESIAN_POINT('Ctrl Pts',(-47.5616248077881,-5.91674999124214,
130.804682543192));
#153273=CARTESIAN_POINT('',(-49.3116240411325,-5.91499358592128,130.798998257019));
#153274=CARTESIAN_POINT('Ctrl Pts',(-47.5616248077881,-5.92651106080092,
130.804683074284));
#153275=CARTESIAN_POINT('Ctrl Pts',(-47.5624338808334,-5.92652453422277,
130.821791600891));
#153276=CARTESIAN_POINT('Ctrl Pts',(-47.5632429538788,-5.92645688555592,
130.838900017864));
#153277=CARTESIAN_POINT('Ctrl Pts',(-47.5640520269241,-5.92630779380708,
130.856007725069));
#153278=CARTESIAN_POINT('Ctrl Pts',(-47.6568679015285,-5.90920416991987,
132.818583064616));
#153279=CARTESIAN_POINT('Ctrl Pts',(-47.8424996507371,-3.73135000823455,
136.72505210137));
#153280=CARTESIAN_POINT('Ctrl Pts',(-48.1209472745499,2.96435960527904,
137.143929424743));
#153281=CARTESIAN_POINT('Ctrl Pts',(-48.3993948983631,6.93596755856032,
131.737052719471));
#153282=CARTESIAN_POINT('Ctrl Pts',(-48.6778425221754,4.53376016637594,
125.473077537096));
#153283=CARTESIAN_POINT('Ctrl Pts',(-48.9562901459887,-2.03475133220846,
124.108291058007));
#153284=CARTESIAN_POINT('Ctrl Pts',(-49.1675505350751,-5.59967235445915,
127.741419835367));
#153285=CARTESIAN_POINT('Ctrl Pts',(-49.2859950495572,-5.91893576568948,
130.254119462179));
#153286=CARTESIAN_POINT('Ctrl Pts',(-49.3116236894351,-5.9141889528215,
130.798991507132));
#153287=CARTESIAN_POINT('',(-51.0616255637457,-5.91166693131237,130.806334617391));
#153288=CARTESIAN_POINT('Ctrl Pts',(-49.311624807788,-5.91674758335821,
130.799012970911));
#153289=CARTESIAN_POINT('Ctrl Pts',(-49.3189601365017,-5.91688859414086,
130.955030236323));
#153290=CARTESIAN_POINT('Ctrl Pts',(-49.3262954652154,-5.91085441233806,
131.111181924842));
#153291=CARTESIAN_POINT('Ctrl Pts',(-49.333630793929,-5.89864003330865,
131.266936362659));
#153292=CARTESIAN_POINT('Ctrl Pts',(-49.3411122355826,-5.88618235518545,
131.425793284318));
#153293=CARTESIAN_POINT('Ctrl Pts',(-49.3485936772361,-5.8672956371023,
131.584236560695));
#153294=CARTESIAN_POINT('Ctrl Pts',(-49.3560751188896,-5.84203044944819,
131.741703025771));
#153295=CARTESIAN_POINT('Ctrl Pts',(-49.3634057495404,-5.81727455779103,
131.895995279699));
#153296=CARTESIAN_POINT('Ctrl Pts',(-49.3707363801912,-5.78639498403716,
132.049349339782));
#153297=CARTESIAN_POINT('Ctrl Pts',(-49.378067010842,-5.74949152254786,
132.201242070893));
#153298=CARTESIAN_POINT('Ctrl Pts',(-49.3853976119527,-5.7125882097672,
132.353134189928));
#153299=CARTESIAN_POINT('Ctrl Pts',(-49.3927282130636,-5.66966114701411,
132.503564621729));
#153300=CARTESIAN_POINT('Ctrl Pts',(-49.4000588141744,-5.62086080807607,
132.652022474815));
#153301=CARTESIAN_POINT('Ctrl Pts',(-49.4073908965377,-5.57205060833313,
132.80051032593));
#153302=CARTESIAN_POINT('Ctrl Pts',(-49.414722978901,-5.51736488940606,
132.947024443542));
#153303=CARTESIAN_POINT('Ctrl Pts',(-49.4220550612644,-5.4570032682094,
133.091071332381));
#153304=CARTESIAN_POINT('Ctrl Pts',(-49.4296492556269,-5.39448380093025,
133.24026770211));
#153305=CARTESIAN_POINT('Ctrl Pts',(-49.4372434499894,-5.32587525907213,
133.386816757951));
#153306=CARTESIAN_POINT('Ctrl Pts',(-49.4448376443519,-5.25145229250738,
133.530196155895));
#153307=CARTESIAN_POINT('Ctrl Pts',(-49.4521810926983,-5.1794866323373,
133.668841435762));
#153308=CARTESIAN_POINT('Ctrl Pts',(-49.4595245410447,-5.10208465192191,
133.804522744505));
#153309=CARTESIAN_POINT('Ctrl Pts',(-49.4668679893912,-5.01953949060683,
133.936796389412));
#153310=CARTESIAN_POINT('Ctrl Pts',(-49.4745875567617,-4.93276650551575,
134.075844867052));
#153311=CARTESIAN_POINT('Ctrl Pts',(-49.4823071241322,-4.84030990417987,
134.211127013296));
#153312=CARTESIAN_POINT('Ctrl Pts',(-49.4900266915027,-4.7425584360818,
134.342166440792));
#153313=CARTESIAN_POINT('Ctrl Pts',(-49.4977462588732,-4.64480696798372,
134.473205868288));
#153314=CARTESIAN_POINT('Ctrl Pts',(-49.5054658262438,-4.54176099529537,
134.600002253022));
#153315=CARTESIAN_POINT('Ctrl Pts',(-49.5131853936143,-4.43385363374095,
134.722124331353));
#153316=CARTESIAN_POINT('Ctrl Pts',(-49.5206086600197,-4.33008809177773,
134.839558985125));
#153317=CARTESIAN_POINT('Ctrl Pts',(-49.5280319264252,-4.22149687609221,
134.953045878808));
#153318=CARTESIAN_POINT('Ctrl Pts',(-49.5354551928306,-4.10841207585408,
135.062162958854));
#153319=CARTESIAN_POINT('Ctrl Pts',(-49.5428696855516,-3.99546093245856,
135.171151071573));
#153320=CARTESIAN_POINT('Ctrl Pts',(-49.5502841782725,-3.87802704218116,
135.275779394456));
#153321=CARTESIAN_POINT('Ctrl Pts',(-49.5576986709935,-3.75648243869832,
135.375659147552));
#153322=CARTESIAN_POINT('Ctrl Pts',(-49.5651060173473,-3.63505498448056,
135.475442632781));
#153323=CARTESIAN_POINT('Ctrl Pts',(-49.5725133637012,-3.50952499121401,
135.570486424419));
#153324=CARTESIAN_POINT('Ctrl Pts',(-49.5799207100549,-3.38030091906444,
135.660438897317));
#153325=CARTESIAN_POINT('Ctrl Pts',(-49.5873225317303,-3.25117322710323,
135.750324280268));
#153326=CARTESIAN_POINT('Ctrl Pts',(-49.5947243534057,-3.11835724726064,
135.83512569306));
#153327=CARTESIAN_POINT('Ctrl Pts',(-49.6021261750811,-2.98229396800212,
135.914532165657));
#153328=CARTESIAN_POINT('Ctrl Pts',(-49.6095240893924,-2.84630251548943,
135.993896720195));
#153329=CARTESIAN_POINT('Ctrl Pts',(-49.6169220037039,-2.70706749911355,
136.067871818679));
#153330=CARTESIAN_POINT('Ctrl Pts',(-49.6243199180152,-2.5650581987547,
136.13619022845));
#153331=CARTESIAN_POINT('Ctrl Pts',(-49.6317166029274,-2.42307249776545,
136.204497284941));
#153332=CARTESIAN_POINT('Ctrl Pts',(-49.6391132878395,-2.27831376387749,
136.267149356742));
#153333=CARTESIAN_POINT('Ctrl Pts',(-49.6465099727517,-2.13127525216176,
136.32392548828));
#153334=CARTESIAN_POINT('Ctrl Pts',(-49.6539063296872,-1.98424326028772,
136.380699102305));
#153335=CARTESIAN_POINT('Ctrl Pts',(-49.6613026866226,-1.83493203982097,
136.431597159654));
#153336=CARTESIAN_POINT('Ctrl Pts',(-49.668699043558,-1.68385391458236,
136.476447231577));
#153337=CARTESIAN_POINT('Ctrl Pts',(-49.6760965328946,-1.53275265889687,
136.521304170161));
#153338=CARTESIAN_POINT('Ctrl Pts',(-49.6834940222311,-1.37988431768758,
136.56011117336));
#153339=CARTESIAN_POINT('Ctrl Pts',(-49.6908915115677,-1.2257752807794,
136.592746016236));
#153340=CARTESIAN_POINT('Ctrl Pts',(-49.6982915940827,-1.07161222118723,
136.625392299204));
#153341=CARTESIAN_POINT('Ctrl Pts',(-49.7056916765978,-0.916207964937106,
136.651862036767));
#153342=CARTESIAN_POINT('Ctrl Pts',(-49.7130917591128,-0.760097818310723,
136.672084355874));
#153343=CARTESIAN_POINT('Ctrl Pts',(-49.7204999787792,-0.603816012530057,
136.692328911499));
#153344=CARTESIAN_POINT('Ctrl Pts',(-49.7279081984456,-0.446827136684607,
136.706312281484));
#153345=CARTESIAN_POINT('Ctrl Pts',(-49.7353164181121,-0.289671065538309,
136.714015534419));
#153346=CARTESIAN_POINT('Ctrl Pts',(-49.7427291974141,-0.132418267451838,
136.721723528578));
#153347=CARTESIAN_POINT('Ctrl Pts',(-49.7501419767162,0.0250015585711839,
136.723143700219));
#153348=CARTESIAN_POINT('Ctrl Pts',(-49.7575547560182,0.18205034989943,
136.718309233559));
#153349=CARTESIAN_POINT('Ctrl Pts',(-49.764978127047,0.339323539905137,
136.713467859186));
#153350=CARTESIAN_POINT('Ctrl Pts',(-49.7724014980757,0.496224265005591,
136.702354023785));
#153351=CARTESIAN_POINT('Ctrl Pts',(-49.7798248691045,0.652220551304472,
136.685052661446));
#153352=CARTESIAN_POINT('Ctrl Pts',(-49.7837609185454,0.734933525382986,
136.675879063994));
#153353=CARTESIAN_POINT('Ctrl Pts',(-49.7876969679864,0.81739240313919,
136.664966784417));
#153354=CARTESIAN_POINT('Ctrl Pts',(-49.7916330174273,0.899519377310721,
136.652334236893));
#153355=CARTESIAN_POINT('Ctrl Pts',(-49.7990562838328,1.0544082874971,136.628509646511));
#153356=CARTESIAN_POINT('Ctrl Pts',(-49.8064795502382,1.20858422983443,
136.598491219399));
#153357=CARTESIAN_POINT('Ctrl Pts',(-49.8139028166436,1.36151261641186,
136.562330221328));
#153358=CARTESIAN_POINT('Ctrl Pts',(-49.8213173093646,1.51426025433648,
136.526211962554));
#153359=CARTESIAN_POINT('Ctrl Pts',(-49.8287318020855,1.66576291178343,
136.483965668971));
#153360=CARTESIAN_POINT('Ctrl Pts',(-49.8361462948066,1.81549240387893,
136.435694197985));
#153361=CARTESIAN_POINT('Ctrl Pts',(-49.8435536411603,1.96507758105295,
136.387469252861));
#153362=CARTESIAN_POINT('Ctrl Pts',(-49.8509609875141,2.11289264233934,
136.333230805285));
#153363=CARTESIAN_POINT('Ctrl Pts',(-49.8583683338679,2.25842097284595,
136.273132442383));
#153364=CARTESIAN_POINT('Ctrl Pts',(-49.8657701555433,2.403840762833,136.213078903107));
#153365=CARTESIAN_POINT('Ctrl Pts',(-49.8731719772188,2.54697687443162,
136.147174292725));
#153366=CARTESIAN_POINT('Ctrl Pts',(-49.8805737988941,2.68732931470535,
136.075621540422));
#153367=CARTESIAN_POINT('Ctrl Pts',(-49.8879717132055,2.82760766401857,
136.004106560259));
#153368=CARTESIAN_POINT('Ctrl Pts',(-49.8953696275168,2.96510493681251,
135.926949545315));
#153369=CARTESIAN_POINT('Ctrl Pts',(-49.9027675418282,3.09934264544475,
135.844400868261));
#153370=CARTESIAN_POINT('Ctrl Pts',(-49.9101642267403,3.23355804620476,
135.761865909301));
#153371=CARTESIAN_POINT('Ctrl Pts',(-49.9175609116526,3.36451464020499,
135.673941261871));
#153372=CARTESIAN_POINT('Ctrl Pts',(-49.9249575965648,3.49175991484945,
135.580922483548));
#153373=CARTESIAN_POINT('Ctrl Pts',(-49.9323539535002,3.61899954730527,
135.487907829775));
#153374=CARTESIAN_POINT('Ctrl Pts',(-49.9397503104356,3.74252788625252,
135.389799714534));
#153375=CARTESIAN_POINT('Ctrl Pts',(-49.947146667371,3.86192293896113,135.286935968414));
#153376=CARTESIAN_POINT('Ctrl Pts',(-49.9545441567076,3.98133627135712,
135.184056473591));
#153377=CARTESIAN_POINT('Ctrl Pts',(-49.9619416460442,4.09661477466076,
135.076420141819));
#153378=CARTESIAN_POINT('Ctrl Pts',(-49.9693391353808,4.20737109100973,
134.964403774197));
#153379=CARTESIAN_POINT('Ctrl Pts',(-49.9767392178958,4.3181662328137,134.852348139412));
#153380=CARTESIAN_POINT('Ctrl Pts',(-49.9841393004108,4.42443576915005,
134.735909677063));
#153381=CARTESIAN_POINT('Ctrl Pts',(-49.9915393829258,4.52583072639426,
134.615500446872));
#153382=CARTESIAN_POINT('Ctrl Pts',(-49.9989476025923,4.6273371778176,134.494958814354));
#153383=CARTESIAN_POINT('Ctrl Pts',(-50.0063558222587,4.72395810507664,
134.370437979989));
#153384=CARTESIAN_POINT('Ctrl Pts',(-50.0137640419251,4.81538576514369,
134.242381922816));
#153385=CARTESIAN_POINT('Ctrl Pts',(-50.0211768212272,4.9068696974101,134.114247049276));
#153386=CARTESIAN_POINT('Ctrl Pts',(-50.0285896005293,4.99315378919068,
133.982572928743));
#153387=CARTESIAN_POINT('Ctrl Pts',(-50.0360023798314,5.07397512331324,
133.847830185427));
#153388=CARTESIAN_POINT('Ctrl Pts',(-50.0434257508601,5.15491193874802,
133.712894915362));
#153389=CARTESIAN_POINT('Ctrl Pts',(-50.0508491218888,5.23037022869458,
133.57488259217));
#153390=CARTESIAN_POINT('Ctrl Pts',(-50.0582724929176,5.30013390572492,
133.434286689509));
#153391=CARTESIAN_POINT('Ctrl Pts',(-50.0622085423584,5.3371242812435,133.359739368364));
#153392=CARTESIAN_POINT('Ctrl Pts',(-50.0661445917993,5.37251450898053,
133.284466025495));
#153393=CARTESIAN_POINT('Ctrl Pts',(-50.0700806412402,5.40627802457782,
133.208542075665));
#153394=CARTESIAN_POINT('Ctrl Pts',(-50.0775039076456,5.46995496127022,
133.065351875793));
#153395=CARTESIAN_POINT('Ctrl Pts',(-50.0849271740511,5.52803547116503,
132.91941359592));
#153396=CARTESIAN_POINT('Ctrl Pts',(-50.0923504404565,5.58027372778425,
132.771204710396));
#153397=CARTESIAN_POINT('Ctrl Pts',(-50.0997649331775,5.63245024312219,
132.623170995467));
#153398=CARTESIAN_POINT('Ctrl Pts',(-50.1071794258986,5.67879812686119,
132.472872365374));
#153399=CARTESIAN_POINT('Ctrl Pts',(-50.1145939186196,5.71911841902588,
132.32080879395));
#153400=CARTESIAN_POINT('Ctrl Pts',(-50.1220012649734,5.75939984897513,
132.168891787121));
#153401=CARTESIAN_POINT('Ctrl Pts',(-50.1294086113271,5.79366515812602,
132.015213583958));
#153402=CARTESIAN_POINT('Ctrl Pts',(-50.1368159576809,5.82176432070789,
131.860291844793));
#153403=CARTESIAN_POINT('Ctrl Pts',(-50.1442177793563,5.84984252587406,
131.705485652106));
#153404=CARTESIAN_POINT('Ctrl Pts',(-50.1516196010318,5.87176367525707,
131.549438135872));
#153405=CARTESIAN_POINT('Ctrl Pts',(-50.1590214227072,5.88742824053203,
131.392679642489));
#153406=CARTESIAN_POINT('Ctrl Pts',(-50.1664193370186,5.903084536605,131.236003900693));
#153407=CARTESIAN_POINT('Ctrl Pts',(-50.1738172513299,5.91249078923427,
131.078618299723));
#153408=CARTESIAN_POINT('Ctrl Pts',(-50.1812151656413,5.91559900978313,
130.92106073733));
#153409=CARTESIAN_POINT('Ctrl Pts',(-50.1886118505536,5.9187067138021,130.763529358145));
#153410=CARTESIAN_POINT('Ctrl Pts',(-50.1960085354658,5.91551845561344,
130.605826447114));
#153411=CARTESIAN_POINT('Ctrl Pts',(-50.203405220378,5.90603830206536,130.448492471988));
#153412=CARTESIAN_POINT('Ctrl Pts',(-50.2108015773135,5.89655856887723,
130.291165473216));
#153413=CARTESIAN_POINT('Ctrl Pts',(-50.2181979342489,5.88078751750683,
130.134207750443));
#153414=CARTESIAN_POINT('Ctrl Pts',(-50.2255942911844,5.85878127701831,
129.978156943791));
#153415=CARTESIAN_POINT('Ctrl Pts',(-50.232991780521,5.83677166731826,129.822082245362));
#153416=CARTESIAN_POINT('Ctrl Pts',(-50.2403892698575,5.80852501984798,
129.666915109189));
#153417=CARTESIAN_POINT('Ctrl Pts',(-50.2477867591941,5.7741489716597,129.513185100612));
#153418=CARTESIAN_POINT('Ctrl Pts',(-50.2551868417091,5.73976087300087,
129.359401202218));
#153419=CARTESIAN_POINT('Ctrl Pts',(-50.2625869242241,5.69923917708544,
129.207055798521));
#153420=CARTESIAN_POINT('Ctrl Pts',(-50.2699870067391,5.65274193265868,
129.056665219259));
#153421=CARTESIAN_POINT('Ctrl Pts',(-50.2773952264056,5.60619355973164,
128.906109270095));
#153422=CARTESIAN_POINT('Ctrl Pts',(-50.2848034460721,5.55365662644702,
128.75751279498));
#153423=CARTESIAN_POINT('Ctrl Pts',(-50.2922116657386,5.49533832232179,
128.611374688354));
#153424=CARTESIAN_POINT('Ctrl Pts',(-50.2996244450407,5.43698412425355,
128.465146636162));
#153425=CARTESIAN_POINT('Ctrl Pts',(-50.3070372243427,5.37284161665725,
128.321380307587));
#153426=CARTESIAN_POINT('Ctrl Pts',(-50.3144500036448,5.30316463585685,
128.180551286174));
#153427=CARTESIAN_POINT('Ctrl Pts',(-50.3218733746735,5.23338809731875,
128.039521041652));
#153428=CARTESIAN_POINT('Ctrl Pts',(-50.3292967457023,5.15806146999229,
127.901436813406));
#153429=CARTESIAN_POINT('Ctrl Pts',(-50.3367201167311,5.07748312670762,
127.766747136476));
#153430=CARTESIAN_POINT('Ctrl Pts',(-50.3406561661718,5.03475855564861,
127.695331437936));
#153431=CARTESIAN_POINT('Ctrl Pts',(-50.3445922156124,4.99055824298862,
127.624869556566));
#153432=CARTESIAN_POINT('Ctrl Pts',(-50.3485282650531,4.94493127862104,
127.555424605236));
#153433=CARTESIAN_POINT('Ctrl Pts',(-50.3559515314586,4.85888024779004,
127.424453594327));
#153434=CARTESIAN_POINT('Ctrl Pts',(-50.363374797864,4.76749217403929,127.296705611415));
#153435=CARTESIAN_POINT('Ctrl Pts',(-50.3707980642694,4.67103589484764,
127.172645563828));
#153436=CARTESIAN_POINT('Ctrl Pts',(-50.3782125569904,4.57469361896752,
127.048732144915));
#153437=CARTESIAN_POINT('Ctrl Pts',(-50.3856270497114,4.47329528806214,
126.928498276871));
#153438=CARTESIAN_POINT('Ctrl Pts',(-50.3930415424325,4.36715400155214,
126.812381598429));
#153439=CARTESIAN_POINT('Ctrl Pts',(-50.4004488887862,4.26111501801069,
126.696376837614));
#153440=CARTESIAN_POINT('Ctrl Pts',(-50.40785623514,4.15034242987009,126.584481639974));
#153441=CARTESIAN_POINT('Ctrl Pts',(-50.4152635814937,4.03519066683523,
126.477102034492));
#153442=CARTESIAN_POINT('Ctrl Pts',(-50.4226654031691,3.92012478832934,
126.369802516771));
#153443=CARTESIAN_POINT('Ctrl Pts',(-50.4300672248445,3.80068651012137,
126.267012138759));
#153444=CARTESIAN_POINT('Ctrl Pts',(-50.4374690465199,3.67726823016638,
126.169101301637));
#153445=CARTESIAN_POINT('Ctrl Pts',(-50.4448669608312,3.55391510176157,
126.071242150884));
#153446=CARTESIAN_POINT('Ctrl Pts',(-50.4522648751426,3.4265864475819,125.978257642468));
#153447=CARTESIAN_POINT('Ctrl Pts',(-50.4596627894539,3.29570887720916,
125.890478897461));
#153448=CARTESIAN_POINT('Ctrl Pts',(-50.4670594743661,3.16485305631352,
125.802714739688));
#153449=CARTESIAN_POINT('Ctrl Pts',(-50.4744561592783,3.03044979945639,
125.720154836078));
#153450=CARTESIAN_POINT('Ctrl Pts',(-50.4818528441905,2.89295601569535,
125.643087901098));
#153451=CARTESIAN_POINT('Ctrl Pts',(-50.4892492011259,2.75546832855256,
125.566024383347));
#153452=CARTESIAN_POINT('Ctrl Pts',(-50.4966455580614,2.61489071261536,
125.49445353246));
#153453=CARTESIAN_POINT('Ctrl Pts',(-50.5040419149969,2.47170583887421,
125.428618733084));
#153454=CARTESIAN_POINT('Ctrl Pts',(-50.5114394043335,2.32849904316315,
125.362773854232));
#153455=CARTESIAN_POINT('Ctrl Pts',(-50.5188368936701,2.18268453401855,
125.302666931465));
#153456=CARTESIAN_POINT('Ctrl Pts',(-50.5262343830067,2.03476603021457,
125.248493649686));
#153457=CARTESIAN_POINT('Ctrl Pts',(-50.5336344655217,1.88679567380839,
125.194301377546));
#153458=CARTESIAN_POINT('Ctrl Pts',(-50.5410345480367,1.7367202045926,125.146047016012));
#153459=CARTESIAN_POINT('Ctrl Pts',(-50.5484346305517,1.58505945460646,
125.103876683034));
#153460=CARTESIAN_POINT('Ctrl Pts',(-50.5558428502182,1.43323193803482,
125.061659979439));
#153461=CARTESIAN_POINT('Ctrl Pts',(-50.5632510698847,1.27981601932356,
125.025540764864));
#153462=CARTESIAN_POINT('Ctrl Pts',(-50.5706592895511,1.12534342348995,
124.995614389531));
#153463=CARTESIAN_POINT('Ctrl Pts',(-50.5780720688532,0.970775752350672,
124.965669595014));
#153464=CARTESIAN_POINT('Ctrl Pts',(-50.5854848481553,0.815150476322736,
124.941925290982));
#153465=CARTESIAN_POINT('Ctrl Pts',(-50.5928976274574,0.659004922045166,
124.92442498227));
#153466=CARTESIAN_POINT('Ctrl Pts',(-50.6003209984861,0.502636259677368,
124.906899668297));
#153467=CARTESIAN_POINT('Ctrl Pts',(-50.607744369515,0.345746205680676,
124.895636194966));
#153468=CARTESIAN_POINT('Ctrl Pts',(-50.6151677405438,0.188873403088834,
124.890625976909));
#153469=CARTESIAN_POINT('Ctrl Pts',(-50.6191037899845,0.105695679043978,
124.887969439077));
#153470=CARTESIAN_POINT('Ctrl Pts',(-50.6230398394252,0.0225227540158833,
124.887070045928));
#153471=CARTESIAN_POINT('Ctrl Pts',(-50.626975888866,-0.0605657390643266,
124.887920610792));
#153472=CARTESIAN_POINT('Ctrl Pts',(-50.6343991552714,-0.217268043911369,
124.889524749581));
#153473=CARTESIAN_POINT('Ctrl Pts',(-50.6418224216769,-0.37414352608616,
124.89736121909));
#153474=CARTESIAN_POINT('Ctrl Pts',(-50.6492456880823,-0.530655732662615,
124.911455132502));
#153475=CARTESIAN_POINT('Ctrl Pts',(-50.6566601808033,-0.686982954808871,
124.925532388079));
#153476=CARTESIAN_POINT('Ctrl Pts',(-50.6640746735243,-0.842947387840515,
124.945852333067));
#153477=CARTESIAN_POINT('Ctrl Pts',(-50.6714891662454,-0.998011596012674,
124.97238810248));
#153478=CARTESIAN_POINT('Ctrl Pts',(-50.6788965125992,-1.15292634746315,
124.998898295719));
#153479=CARTESIAN_POINT('Ctrl Pts',(-50.686303858953,-1.30694223593648,
125.031612323848));
#153480=CARTESIAN_POINT('Ctrl Pts',(-50.6937112053068,-1.45952607983614,
125.070451463701));
#153481=CARTESIAN_POINT('Ctrl Pts',(-50.7011130269822,-1.61199612094792,
125.109261635858));
#153482=CARTESIAN_POINT('Ctrl Pts',(-50.7085148486576,-1.76303588395808,
125.154187731872));
#153483=CARTESIAN_POINT('Ctrl Pts',(-50.715916670333,-1.91212163918262,
125.205099827116));
#153484=CARTESIAN_POINT('Ctrl Pts',(-50.7233145846443,-2.06112869319554,
125.255985046261));
#153485=CARTESIAN_POINT('Ctrl Pts',(-50.7307124989556,-2.20818344134278,
125.312849851085));
#153486=CARTESIAN_POINT('Ctrl Pts',(-50.7381104132668,-2.3527767091887,
125.375514301893));
#153487=CARTESIAN_POINT('Ctrl Pts',(-50.745507098179,-2.49734594825835,
125.438168339007));
#153488=CARTESIAN_POINT('Ctrl Pts',(-50.7529037830912,-2.63945417669665,
125.50661996096));
#153489=CARTESIAN_POINT('Ctrl Pts',(-50.7603004680034,-2.77861152033932,
125.580640814443));
#153490=CARTESIAN_POINT('Ctrl Pts',(-50.7676968249389,-2.91776269359994,
125.654658385765));
#153491=CARTESIAN_POINT('Ctrl Pts',(-50.7750931818743,-3.05396291265647,
125.734244522298));
#153492=CARTESIAN_POINT('Ctrl Pts',(-50.7824895388098,-3.18674651565259,
125.819124694616));
#153493=CARTESIAN_POINT('Ctrl Pts',(-50.7898870281463,-3.31955044815674,
125.904017862304));
#153494=CARTESIAN_POINT('Ctrl Pts',(-50.797284517483,-3.44893640850621,
125.99420647858));
#153495=CARTESIAN_POINT('Ctrl Pts',(-50.8046820068195,-3.57446748915029,
126.089372523042));
#153496=CARTESIAN_POINT('Ctrl Pts',(-50.8120820893346,-3.70004257452118,
126.184571927813));
#153497=CARTESIAN_POINT('Ctrl Pts',(-50.8194821718496,-3.82175979242311,
126.284752009336));
#153498=CARTESIAN_POINT('Ctrl Pts',(-50.8268822543646,-3.93921522777169,
126.389554398513));
#153499=CARTESIAN_POINT('Ctrl Pts',(-50.8342904740311,-4.05679981744515,
126.49447202869));
#153500=CARTESIAN_POINT('Ctrl Pts',(-50.8416986936975,-4.17011298707178,
126.604021868327));
#153501=CARTESIAN_POINT('Ctrl Pts',(-50.849106913364,-4.27878710544865,
126.717808101233));
#153502=CARTESIAN_POINT('Ctrl Pts',(-50.856519692666,-4.38752811093222,
126.831664367667));
#153503=CARTESIAN_POINT('Ctrl Pts',(-50.8639324719681,-4.49162412943925,
126.94976194361));
#153504=CARTESIAN_POINT('Ctrl Pts',(-50.8713452512702,-4.59074812094708,
127.071672276367));
#153505=CARTESIAN_POINT('Ctrl Pts',(-50.8787686222989,-4.69001374546256,
127.193756800325));
#153506=CARTESIAN_POINT('Ctrl Pts',(-50.8861919933277,-4.78429293101191,
127.319664663649));
#153507=CARTESIAN_POINT('Ctrl Pts',(-50.8936153643564,-4.87330175099166,
127.448938050097));
#153508=CARTESIAN_POINT('Ctrl Pts',(-50.8975514137973,-4.92049636308275,
127.517481901465));
#153509=CARTESIAN_POINT('Ctrl Pts',(-50.9014874632381,-4.96621004560118,
127.586971494906));
#153510=CARTESIAN_POINT('Ctrl Pts',(-50.9054235126789,-5.0104058013515,
127.657335948409));
#153511=CARTESIAN_POINT('Ctrl Pts',(-50.9130462144203,-5.09599696817618,
127.793606401897));
#153512=CARTESIAN_POINT('Ctrl Pts',(-50.9206689161617,-5.17613985804444,
127.933553529582));
#153513=CARTESIAN_POINT('Ctrl Pts',(-50.9282916179031,-5.25051253618389,
128.076715356562));
#153514=CARTESIAN_POINT('Ctrl Pts',(-50.9359038231383,-5.32478280269742,
128.219680048845));
#153515=CARTESIAN_POINT('Ctrl Pts',(-50.9435160283734,-5.39329852644854,
128.365850318301));
#153516=CARTESIAN_POINT('Ctrl Pts',(-50.9511282336086,-5.45578114959963,
128.514735624216));
#153517=CARTESIAN_POINT('Ctrl Pts',(-50.9587311300378,-5.51818736406292,
128.663438861417));
#153518=CARTESIAN_POINT('Ctrl Pts',(-50.966334026467,-5.57457504267055,
128.814850203501));
#153519=CARTESIAN_POINT('Ctrl Pts',(-50.9739369228963,-5.62471157029013,
128.968454761171));
#153520=CARTESIAN_POINT('Ctrl Pts',(-50.9815292619871,-5.67477847861519,
129.121846024434));
#153521=CARTESIAN_POINT('Ctrl Pts',(-50.9891216010781,-5.71861143700816,
129.277424103212));
#153522=CARTESIAN_POINT('Ctrl Pts',(-50.9967139401689,-5.75602608788787,
129.434654722837));
#153523=CARTESIAN_POINT('Ctrl Pts',(-51.0043001049327,-5.79341031200569,
129.591757477616));
#153524=CARTESIAN_POINT('Ctrl Pts',(-51.0118862696965,-5.82438654572741,
129.750509760866));
#153525=CARTESIAN_POINT('Ctrl Pts',(-51.0194724344602,-5.84882012205448,
129.910361880234));
#153526=CARTESIAN_POINT('Ctrl Pts',(-51.0270524158079,-5.87323378278868,
130.070083705549));
#153527=CARTESIAN_POINT('Ctrl Pts',(-51.0346323971556,-5.89111536534244,
130.230903238429));
#153528=CARTESIAN_POINT('Ctrl Pts',(-51.0422123785033,-5.90238121170339,
130.392260394039));
#153529=CARTESIAN_POINT('Ctrl Pts',(-51.0486831882649,-5.91199853729579,
130.530006307879));
#153530=CARTESIAN_POINT('Ctrl Pts',(-51.0551539980265,-5.91679543811377,
130.668143704449));
#153531=CARTESIAN_POINT('Ctrl Pts',(-51.0616248077881,-5.91674967550615,
130.806320183304));
#153532=CARTESIAN_POINT('',(-52.8116248077881,-5.92138584378568,130.809025436609));
#153533=CARTESIAN_POINT('Ctrl Pts',(-51.0616261784267,-5.90753407287618,
130.806346353971));
#153534=CARTESIAN_POINT('Ctrl Pts',(-51.1023744977817,-5.91009664804197,
131.675124094495));
#153535=CARTESIAN_POINT('Ctrl Pts',(-51.2359386917411,-5.32287699652367,
134.519485052779));
#153536=CARTESIAN_POINT('Ctrl Pts',(-51.4623187603045,-0.922135659953538,
137.741739542996));
#153537=CARTESIAN_POINT('Ctrl Pts',(-51.7407663841177,5.33817651812515,
135.330002228618));
#153538=CARTESIAN_POINT('Ctrl Pts',(-52.0192140079303,6.69296526046545,
128.759421363569));
#153539=CARTESIAN_POINT('Ctrl Pts',(-52.2976616317434,1.89724589797152,
124.068039772106));
#153540=CARTESIAN_POINT('Ctrl Pts',(-52.5617985650291,-4.30587073622864,
125.489969153991));
#153541=CARTESIAN_POINT('Ctrl Pts',(-52.7331196237108,-5.90700759757791,
129.145181670511));
#153542=CARTESIAN_POINT('Ctrl Pts',(-52.8116248077881,-5.92138584378568,
130.809025436609));
#153543=CARTESIAN_POINT('',(-54.561624807788,-5.92017284106423,130.80018406539));
#153544=CARTESIAN_POINT('Ctrl Pts',(-52.8116248077881,-5.92138584378568,
130.809025436609));
#153545=CARTESIAN_POINT('Ctrl Pts',(-52.8259354983151,-5.92400685071941,
131.112327103904));
#153546=CARTESIAN_POINT('Ctrl Pts',(-52.9330620634458,-5.76469768580607,
133.380013103561));
#153547=CARTESIAN_POINT('Ctrl Pts',(-53.1330045031822,-2.83395748649668,
137.203285956645));
#153548=CARTESIAN_POINT('Ctrl Pts',(-53.4114521269948,3.85177387003691,
136.647424761012));
#153549=CARTESIAN_POINT('Ctrl Pts',(-53.6898997508079,6.99791320962053,
130.722073067109));
#153550=CARTESIAN_POINT('Ctrl Pts',(-53.9683473746205,3.71331217662896,
124.872339612104));
#153551=CARTESIAN_POINT('Ctrl Pts',(-54.2467949984337,-2.98364134130034,
124.473843665782));
#153552=CARTESIAN_POINT('Ctrl Pts',(-54.4445541428227,-5.79265685533358,
128.322484560607));
#153553=CARTESIAN_POINT('Ctrl Pts',(-54.5494974126075,-5.92470418608257,
130.543296141923));
#153554=CARTESIAN_POINT('Ctrl Pts',(-54.561624807788,-5.92264775691338,
130.800182319391));
#153555=CARTESIAN_POINT('',(-56.3116247825725,-5.9119383046366,130.801701158817));
#153556=CARTESIAN_POINT('Ctrl Pts',(-54.561624807788,-5.91674852761932,
130.800186481168));
#153557=CARTESIAN_POINT('Ctrl Pts',(-54.5689357564989,-5.91685767039822,
130.954894021801));
#153558=CARTESIAN_POINT('Ctrl Pts',(-54.5762467052098,-5.91089487079683,
131.109837684137));
#153559=CARTESIAN_POINT('Ctrl Pts',(-54.5835576539206,-5.89883112223607,
131.264493156993));
#153560=CARTESIAN_POINT('Ctrl Pts',(-54.5908612387532,-5.8867795247627,
131.418992854704));
#153561=CARTESIAN_POINT('Ctrl Pts',(-54.5981648235857,-5.86863923493353,
131.573204559887));
#153562=CARTESIAN_POINT('Ctrl Pts',(-54.6054684084182,-5.84443325961165,
131.726602687982));
#153563=CARTESIAN_POINT('Ctrl Pts',(-54.6127663366966,-5.82024603157801,
131.879882010746));
#153564=CARTESIAN_POINT('Ctrl Pts',(-54.6200642649749,-5.79000252674056,
132.032348632106));
#153565=CARTESIAN_POINT('Ctrl Pts',(-54.6273621932533,-5.75377765361574,
132.18348108919));
#153566=CARTESIAN_POINT('Ctrl Pts',(-54.6347091954536,-5.71730919127959,
132.335629815838));
#153567=CARTESIAN_POINT('Ctrl Pts',(-54.6420561976538,-5.67477864734158,
132.486425974986));
#153568=CARTESIAN_POINT('Ctrl Pts',(-54.649403199854,-5.62631510966825,
132.635346376445));
#153569=CARTESIAN_POINT('Ctrl Pts',(-54.6566959102122,-5.57820970101953,
132.783166306898));
#153570=CARTESIAN_POINT('Ctrl Pts',(-54.6639886205705,-5.52425882523823,
132.929137742254));
#153571=CARTESIAN_POINT('Ctrl Pts',(-54.6712813309288,-5.46463902029307,
133.072763346446));
#153572=CARTESIAN_POINT('Ctrl Pts',(-54.6785738299039,-5.40502094345963,
133.216384787573));
#153573=CARTESIAN_POINT('Ctrl Pts',(-54.6858663288789,-5.33973441171662,
133.35766017723));
#153574=CARTESIAN_POINT('Ctrl Pts',(-54.693158827854,-5.26900418996104,
133.496111982138));
#153575=CARTESIAN_POINT('Ctrl Pts',(-54.7004526507512,-5.19826112743533,
133.63458892238));
#153576=CARTESIAN_POINT('Ctrl Pts',(-54.7077464736486,-5.12207258387678,
133.770240915353));
#153577=CARTESIAN_POINT('Ctrl Pts',(-54.7150402965458,-5.04070922180969,
133.902615142886));
#153578=CARTESIAN_POINT('Ctrl Pts',(-54.7224277923386,-4.95830092873383,
134.036689422279));
#153579=CARTESIAN_POINT('Ctrl Pts',(-54.7298152881314,-4.87058418760669,
134.167400813144));
#153580=CARTESIAN_POINT('Ctrl Pts',(-54.7372027839241,-4.77788483902664,
134.294310048073));
#153581=CARTESIAN_POINT('Ctrl Pts',(-54.7445074650968,-4.68622466008602,
134.419796616869));
#153582=CARTESIAN_POINT('Ctrl Pts',(-54.7518121462695,-4.58969330068087,
134.541565574923));
#153583=CARTESIAN_POINT('Ctrl Pts',(-54.7591168274421,-4.48864520973242,
134.659226989264));
#153584=CARTESIAN_POINT('Ctrl Pts',(-54.766545730545,-4.38587871539249,
134.778889329813));
#153585=CARTESIAN_POINT('Ctrl Pts',(-54.7739746336478,-4.27844077059429,
134.89430285753));
#153586=CARTESIAN_POINT('Ctrl Pts',(-54.7814035367507,-4.16674134915281,
135.005098301802));
#153587=CARTESIAN_POINT('Ctrl Pts',(-54.7888324398536,-4.05504192771117,
135.115893746075));
#153588=CARTESIAN_POINT('Ctrl Pts',(-54.7962613429565,-3.93908137815843,
135.222070878999));
#153589=CARTESIAN_POINT('Ctrl Pts',(-54.8036902460594,-3.81930212530724,
135.323305387988));
#153590=CARTESIAN_POINT('Ctrl Pts',(-54.8111135124648,-3.69961375524164,
135.424463085059));
#153591=CARTESIAN_POINT('Ctrl Pts',(-54.8185367788702,-3.5757227460027,
135.521015376547));
#153592=CARTESIAN_POINT('Ctrl Pts',(-54.8259600452757,-3.44801884360224,
135.612592789234));
#153593=CARTESIAN_POINT('Ctrl Pts',(-54.8333745379967,-3.32046587660907,
135.704061965024));
#153594=CARTESIAN_POINT('Ctrl Pts',(-54.8407890307177,-3.18910928711066,
135.790567750556));
#153595=CARTESIAN_POINT('Ctrl Pts',(-54.8482035234387,-3.05437352208537,
135.871779383573));
#153596=CARTESIAN_POINT('Ctrl Pts',(-54.8556108697925,-2.91976762046351,
135.952912741761));
#153597=CARTESIAN_POINT('Ctrl Pts',(-54.8630182161462,-2.78178934487982,
136.028761914501));
#153598=CARTESIAN_POINT('Ctrl Pts',(-54.8704255625,-2.64089379994834,136.099038180921));
#153599=CARTESIAN_POINT('Ctrl Pts',(-54.8778273841754,-2.50010334022915,
136.16926203265));
#153600=CARTESIAN_POINT('Ctrl Pts',(-54.8852292058509,-2.35640027610511,
136.233921088279));
#153601=CARTESIAN_POINT('Ctrl Pts',(-54.8926310275263,-2.21026600553464,
136.292771566764));
#153602=CARTESIAN_POINT('Ctrl Pts',(-54.9000289418376,-2.06420887810892,
136.35159097854));
#153603=CARTESIAN_POINT('Ctrl Pts',(-54.9074268561489,-1.9157234456159,
136.404607780765));
#153604=CARTESIAN_POINT('Ctrl Pts',(-54.9148247704603,-1.76531276052781,
136.451625567966));
#153605=CARTESIAN_POINT('Ctrl Pts',(-54.9222214553725,-1.61492707096665,
136.498635541664));
#153606=CARTESIAN_POINT('Ctrl Pts',(-54.9296181402848,-1.46261711974746,
136.539648367676));
#153607=CARTESIAN_POINT('Ctrl Pts',(-54.937014825197,-1.30890297514993,
136.574516903503));
#153608=CARTESIAN_POINT('Ctrl Pts',(-54.9444111821324,-1.15519564639844,
136.609383893224));
#153609=CARTESIAN_POINT('Ctrl Pts',(-54.9518075390678,-1.00008461211801,
136.638107051889));
#153610=CARTESIAN_POINT('Ctrl Pts',(-54.9592038960033,-0.844101775724089,
136.660590014944));
#153611=CARTESIAN_POINT('Ctrl Pts',(-54.9666013853398,-0.688095057960154,
136.683076420198));
#153612=CARTESIAN_POINT('Ctrl Pts',(-54.9739988746763,-0.531216641819291,
136.699320674274));
#153613=CARTESIAN_POINT('Ctrl Pts',(-54.9813963640128,-0.374005072893866,
136.70927812486));
#153614=CARTESIAN_POINT('Ctrl Pts',(-54.9887964465278,-0.216738393696886,
136.719239066015));
#153615=CARTESIAN_POINT('Ctrl Pts',(-54.9961965290429,-0.0591387015138569,
136.722908792292));
#153616=CARTESIAN_POINT('Ctrl Pts',(-55.0035966115578,0.0982540774499587,
136.720294753336));
#153617=CARTESIAN_POINT('Ctrl Pts',(-55.0110048312243,0.255819925955066,
136.717677839975));
#153618=CARTESIAN_POINT('Ctrl Pts',(-55.0184130508907,0.413178033388422,
136.708763368567));
#153619=CARTESIAN_POINT('Ctrl Pts',(-55.0258212705572,0.569791480473101,
136.693610844147));
#153620=CARTESIAN_POINT('Ctrl Pts',(-55.0332340498593,0.726501320521672,
136.6784489936));
#153621=CARTESIAN_POINT('Ctrl Pts',(-55.0406468291613,0.882465217976646,
136.657041490165));
#153622=CARTESIAN_POINT('Ctrl Pts',(-55.0480596084634,1.03715559896363,
136.629499141759));
#153623=CARTESIAN_POINT('Ctrl Pts',(-55.0554829794922,1.19206700882078,
136.601917439554));
#153624=CARTESIAN_POINT('Ctrl Pts',(-55.0629063505209,1.34570090429466,
136.568183465048));
#153625=CARTESIAN_POINT('Ctrl Pts',(-55.0703297215497,1.49754323536802,
136.528458347401));
#153626=CARTESIAN_POINT('Ctrl Pts',(-55.0742657709905,1.57805368271103,
136.507395136833));
#153627=CARTESIAN_POINT('Ctrl Pts',(-55.0782018204313,1.65806075277631,
136.484648420463));
#153628=CARTESIAN_POINT('Ctrl Pts',(-55.0821378698722,1.73749012815274,
136.46024769362));
#153629=CARTESIAN_POINT('Ctrl Pts',(-55.0895611362776,1.88729145120475,
136.414228684314));
#153630=CARTESIAN_POINT('Ctrl Pts',(-55.096984402683,2.03548974523695,136.362184541436));
#153631=CARTESIAN_POINT('Ctrl Pts',(-55.1044076690885,2.1815634947261,136.304243460044));
#153632=CARTESIAN_POINT('Ctrl Pts',(-55.1118221618095,2.32746459717403,
136.246370860198));
#153633=CARTESIAN_POINT('Ctrl Pts',(-55.1192366545305,2.4712458096998,136.182615331342));
#153634=CARTESIAN_POINT('Ctrl Pts',(-55.1266511472515,2.61239942869045,
136.113155187662));
#153635=CARTESIAN_POINT('Ctrl Pts',(-55.1340584936053,2.75341699850918,
136.043761992283));
#153636=CARTESIAN_POINT('Ctrl Pts',(-55.1414658399591,2.89181168395572,
135.968675291871));
#153637=CARTESIAN_POINT('Ctrl Pts',(-55.1488731863129,3.02709458082315,
135.888121918144));
#153638=CARTESIAN_POINT('Ctrl Pts',(-55.1562750079882,3.1622765786014,135.807628624162));
#153639=CARTESIAN_POINT('Ctrl Pts',(-55.1636768296637,3.29435108964162,
135.721676965385));
#153640=CARTESIAN_POINT('Ctrl Pts',(-55.171078651339,3.42285280669413,135.630540185942));
#153641=CARTESIAN_POINT('Ctrl Pts',(-55.1784765656504,3.55128668869137,
135.539451516894));
#153642=CARTESIAN_POINT('Ctrl Pts',(-55.1858744799618,3.67615122913889,
135.443183393821));
#153643=CARTESIAN_POINT('Ctrl Pts',(-55.1932723942732,3.79700927440007,
135.342052887059));
#153644=CARTESIAN_POINT('Ctrl Pts',(-55.2006690791854,3.91784723524655,
135.240939186353));
#153645=CARTESIAN_POINT('Ctrl Pts',(-55.2080657640976,4.03467973632571,
135.134964945004));
#153646=CARTESIAN_POINT('Ctrl Pts',(-55.2154624490098,4.14710187287758,
135.024488177069));
#153647=CARTESIAN_POINT('Ctrl Pts',(-55.2228588059452,4.25951902451362,
134.91401630779));
#153648=CARTESIAN_POINT('Ctrl Pts',(-55.2302551628807,4.36752593420728,
134.799042570538));
#153649=CARTESIAN_POINT('Ctrl Pts',(-55.2376515198162,4.47075402093921,
134.679962383325));
#153650=CARTESIAN_POINT('Ctrl Pts',(-55.2450490091528,4.57399791215519,
134.560863964631));
#153651=CARTESIAN_POINT('Ctrl Pts',(-55.2524464984893,4.6724612790629,134.437658126219));
#153652=CARTESIAN_POINT('Ctrl Pts',(-55.2598439878259,4.76581545736149,
134.310773826085));
#153653=CARTESIAN_POINT('Ctrl Pts',(-55.267244070341,4.85920236082283,134.183845046855));
#153654=CARTESIAN_POINT('Ctrl Pts',(-55.274644152856,4.94747628868341,134.053235539056));
#153655=CARTESIAN_POINT('Ctrl Pts',(-55.282044235371,5.03035166523881,133.91940358461));
#153656=CARTESIAN_POINT('Ctrl Pts',(-55.2894524550375,5.11331817179017,
133.785424468172));
#153657=CARTESIAN_POINT('Ctrl Pts',(-55.296860674704,5.19087407527716,133.648216146231));
#153658=CARTESIAN_POINT('Ctrl Pts',(-55.3042688943705,5.26277922098575,
133.508262508105));
#153659=CARTESIAN_POINT('Ctrl Pts',(-55.3116816736725,5.33472862311183,
133.36822273085));
#153660=CARTESIAN_POINT('Ctrl Pts',(-55.3190944529746,5.40102018038405,
133.22543460828));
#153661=CARTESIAN_POINT('Ctrl Pts',(-55.3265072322767,5.46146195207614,
133.080401897623));
#153662=CARTESIAN_POINT('Ctrl Pts',(-55.3339306033054,5.52199008580589,
132.935161957429));
#153663=CARTESIAN_POINT('Ctrl Pts',(-55.3413539743342,5.57665161087823,
132.78767137281));
#153664=CARTESIAN_POINT('Ctrl Pts',(-55.348777345363,5.62530423322799,132.638449722852));
#153665=CARTESIAN_POINT('Ctrl Pts',(-55.3527133948037,5.6511010210011,132.55932882352));
#153666=CARTESIAN_POINT('Ctrl Pts',(-55.3566494442444,5.67520933994965,
132.479721453742));
#153667=CARTESIAN_POINT('Ctrl Pts',(-55.3605854936851,5.69761383495216,
132.399706081803));
#153668=CARTESIAN_POINT('Ctrl Pts',(-55.3680087600905,5.73986801330723,
132.248799587519));
#153669=CARTESIAN_POINT('Ctrl Pts',(-55.375432026496,5.77618659980623,132.095985035081));
#153670=CARTESIAN_POINT('Ctrl Pts',(-55.3828552929015,5.8063955567029,131.94177048283));
#153671=CARTESIAN_POINT('Ctrl Pts',(-55.3902697856225,5.83656880912125,
131.787738199373));
#153672=CARTESIAN_POINT('Ctrl Pts',(-55.3976842783434,5.86064673446612,
131.632309572518));
#153673=CARTESIAN_POINT('Ctrl Pts',(-55.4050987710644,5.87850492730756,
131.476008130865));
#153674=CARTESIAN_POINT('Ctrl Pts',(-55.4125061174182,5.89634590775034,
131.319857338427));
#153675=CARTESIAN_POINT('Ctrl Pts',(-55.419913463772,5.90797904808998,131.162835774353));
#153676=CARTESIAN_POINT('Ctrl Pts',(-55.4273208101258,5.91333092360849,
131.005477375683));
#153677=CARTESIAN_POINT('Ctrl Pts',(-55.4347226318012,5.91867880749633,
130.848236340844));
#153678=CARTESIAN_POINT('Ctrl Pts',(-55.4421244534765,5.91775474200638,
130.690659343106));
#153679=CARTESIAN_POINT('Ctrl Pts',(-55.4495262751519,5.91053710522861,
130.533285553763));
#153680=CARTESIAN_POINT('Ctrl Pts',(-55.4569241894632,5.90332327858513,
130.375994840819));
#153681=CARTESIAN_POINT('Ctrl Pts',(-55.4643221037745,5.88982251428714,
130.218907494594));
#153682=CARTESIAN_POINT('Ctrl Pts',(-55.4717200180858,5.87006528036957,
130.062562689084));
#153683=CARTESIAN_POINT('Ctrl Pts',(-55.479116702998,5.85031132974576,129.906243865245));
#153684=CARTESIAN_POINT('Ctrl Pts',(-55.4865133879103,5.82430301977792,
129.750667707205));
#153685=CARTESIAN_POINT('Ctrl Pts',(-55.4939100728225,5.79212269691946,
129.59636838815));
#153686=CARTESIAN_POINT('Ctrl Pts',(-55.501306429758,5.75994380097016,129.442075910888));
#153687=CARTESIAN_POINT('Ctrl Pts',(-55.5087027866934,5.72159351249984,
129.289060525473));
#153688=CARTESIAN_POINT('Ctrl Pts',(-55.5160991436289,5.67720528083589,
129.137846062649));
#153689=CARTESIAN_POINT('Ctrl Pts',(-55.5234966329654,5.63281025322056,
128.986608448506));
#153690=CARTESIAN_POINT('Ctrl Pts',(-55.530894122302,5.58237554690949,128.837172664168));
#153691=CARTESIAN_POINT('Ctrl Pts',(-55.5382916116386,5.52608440532971,
128.690047086495));
#153692=CARTESIAN_POINT('Ctrl Pts',(-55.5456916941536,5.46977353097736,
128.542869934177));
#153693=CARTESIAN_POINT('Ctrl Pts',(-55.5530917766685,5.40760226723185,
128.398004949341));
#153694=CARTESIAN_POINT('Ctrl Pts',(-55.5604918591835,5.3398018190108,128.255940107487));
#153695=CARTESIAN_POINT('Ctrl Pts',(-55.56790007885,5.27192681722698,128.113719050736));
#153696=CARTESIAN_POINT('Ctrl Pts',(-55.5753082985164,5.19841043027967,
127.974304623126));
#153697=CARTESIAN_POINT('Ctrl Pts',(-55.5827165181829,5.11952995846776,
127.838160427617));
#153698=CARTESIAN_POINT('Ctrl Pts',(-55.590129297485,5.04060093704142,127.701932437627));
#153699=CARTESIAN_POINT('Ctrl Pts',(-55.5975420767871,4.95630145152058,
127.568979004977));
#153700=CARTESIAN_POINT('Ctrl Pts',(-55.6049548560891,4.86695157847769,
127.439733907921));
#153701=CARTESIAN_POINT('Ctrl Pts',(-55.6123782271179,4.77747403814637,
127.310304139411));
#153702=CARTESIAN_POINT('Ctrl Pts',(-55.6198015981466,4.68293192163988,
127.184593586628));
#153703=CARTESIAN_POINT('Ctrl Pts',(-55.6272249691754,4.58368545213959,
127.063002810787));
#153704=CARTESIAN_POINT('Ctrl Pts',(-55.6311610186162,4.53106259262298,
126.998532463904));
#153705=CARTESIAN_POINT('Ctrl Pts',(-55.6350970680571,4.47711779309835,
126.935219724504));
#153706=CARTESIAN_POINT('Ctrl Pts',(-55.639033117498,4.42190877134034,126.873119925311));
#153707=CARTESIAN_POINT('Ctrl Pts',(-55.6464563839034,4.31778627932138,
126.756001642103));
#153708=CARTESIAN_POINT('Ctrl Pts',(-55.6538796503089,4.20885015155603,
126.64284578839));
#153709=CARTESIAN_POINT('Ctrl Pts',(-55.6613029167144,4.09543376026158,
126.534073404999));
#153710=CARTESIAN_POINT('Ctrl Pts',(-55.6687174094354,3.98215141772317,
126.425429581533));
#153711=CARTESIAN_POINT('Ctrl Pts',(-55.6761319021563,3.8643996187672,126.321159171647));
#153712=CARTESIAN_POINT('Ctrl Pts',(-55.6835463948773,3.74255157865935,
126.221649821151));
#153713=CARTESIAN_POINT('Ctrl Pts',(-55.6909537412311,3.6208209802804,126.122236381514));
#153714=CARTESIAN_POINT('Ctrl Pts',(-55.6983610875849,3.49500228785228,
126.027575100232));
#153715=CARTESIAN_POINT('Ctrl Pts',(-55.7057684339386,3.36550502987478,
125.938016357612));
#153716=CARTESIAN_POINT('Ctrl Pts',(-55.713170255614,3.23610435583737,125.848524411281));
#153717=CARTESIAN_POINT('Ctrl Pts',(-55.7205720772894,3.10303088485882,
125.764127637438));
#153718=CARTESIAN_POINT('Ctrl Pts',(-55.7279738989648,2.96672654984779,
125.685135662465));
#153719=CARTESIAN_POINT('Ctrl Pts',(-55.7353718132762,2.83049416883345,
125.60618538674));
#153720=CARTESIAN_POINT('Ctrl Pts',(-55.7427697275877,2.69103464263019,
125.532634414398));
#153721=CARTESIAN_POINT('Ctrl Pts',(-55.7501676418991,2.54881806230884,
125.464748548534));
#153722=CARTESIAN_POINT('Ctrl Pts',(-55.7575643268113,2.40662511580368,
125.39687396407));
#153723=CARTESIAN_POINT('Ctrl Pts',(-55.7649610117235,2.26167636107247,
125.33466277826));
#153724=CARTESIAN_POINT('Ctrl Pts',(-55.7723576966357,2.11446572341416,
125.278334444356));
#153725=CARTESIAN_POINT('Ctrl Pts',(-55.7797540535712,1.96726161323,125.222008608108));
#153726=CARTESIAN_POINT('Ctrl Pts',(-55.7871504105066,1.81779616818379,
125.17156523851));
#153727=CARTESIAN_POINT('Ctrl Pts',(-55.7945467674421,1.66658223453711,
125.127175204174));
#153728=CARTESIAN_POINT('Ctrl Pts',(-55.8019442567786,1.51534514965138,
125.082778373611));
#153729=CARTESIAN_POINT('Ctrl Pts',(-55.8093417461152,1.36235940134909,
125.04443682881));
#153730=CARTESIAN_POINT('Ctrl Pts',(-55.8167392354518,1.20815174902764,
125.012271191994));
#153731=CARTESIAN_POINT('Ctrl Pts',(-55.8241393179668,1.05389003945249,
124.980094279564));
#153732=CARTESIAN_POINT('Ctrl Pts',(-55.8315394004817,0.898405938248125,
124.954097661707));
#153733=CARTESIAN_POINT('Ctrl Pts',(-55.8389394829967,0.742234964929896,
124.934350581856));
#153734=CARTESIAN_POINT('Ctrl Pts',(-55.8463477026632,0.585892265571738,
124.91458178806));
#153735=CARTESIAN_POINT('Ctrl Pts',(-55.8537559223297,0.428861556319229,
124.901076302982));
#153736=CARTESIAN_POINT('Ctrl Pts',(-55.8611641419962,0.271682767056356,
124.893851414749));
#153737=CARTESIAN_POINT('Ctrl Pts',(-55.8685769212983,0.114407236871135,
124.886622079718));
#153738=CARTESIAN_POINT('Ctrl Pts',(-55.8759897006004,-0.0430161825081487,
124.885681046457));
#153739=CARTESIAN_POINT('Ctrl Pts',(-55.8834024799025,-0.200049531943761,
124.890993493222));
#153740=CARTESIAN_POINT('Ctrl Pts',(-55.8908258509313,-0.35730725799318,
124.896313530661));
#153741=CARTESIAN_POINT('Ctrl Pts',(-55.8982492219599,-0.514173429648822,
124.90790486642));
#153742=CARTESIAN_POINT('Ctrl Pts',(-55.9056725929887,-0.670116333988602,
124.925680947655));
#153743=CARTESIAN_POINT('Ctrl Pts',(-55.9096086424294,-0.752801003666507,
124.935106252457));
#153744=CARTESIAN_POINT('Ctrl Pts',(-55.9135446918702,-0.835226286248772,
124.946269457947));
#153745=CARTESIAN_POINT('Ctrl Pts',(-55.9174807413109,-0.917314430879882,
124.959151913217));
#153746=CARTESIAN_POINT('Ctrl Pts',(-55.9249040077163,-1.07213010977379,
124.983447821808));
#153747=CARTESIAN_POINT('Ctrl Pts',(-55.9323272741218,-1.22621397221266,
125.013935368411));
#153748=CARTESIAN_POINT('Ctrl Pts',(-55.9397505405272,-1.37903158879716,
125.05056166039));
#153749=CARTESIAN_POINT('Ctrl Pts',(-55.9471650332482,-1.53166858765001,
125.087144663134));
#153750=CARTESIAN_POINT('Ctrl Pts',(-55.9545795259692,-1.68304196016181,
125.12985188301));
#153751=CARTESIAN_POINT('Ctrl Pts',(-55.9619940186902,-1.83262383696791,
125.178578855475));
#153752=CARTESIAN_POINT('Ctrl Pts',(-55.969401365044,-1.98206154112907,
125.227258863049));
#153753=CARTESIAN_POINT('Ctrl Pts',(-55.9768087113978,-2.12971083456876,
125.281946957596));
#153754=CARTESIAN_POINT('Ctrl Pts',(-55.9842160577516,-2.27505557225412,
125.342487980305));
#153755=CARTESIAN_POINT('Ctrl Pts',(-55.991617879427,-2.42029190635057,
125.402983849236));
#153756=CARTESIAN_POINT('Ctrl Pts',(-55.9990197011024,-2.56322676398866,
125.469323811439));
#153757=CARTESIAN_POINT('Ctrl Pts',(-56.0064215227778,-2.70336077219452,
125.541303416864));
#153758=CARTESIAN_POINT('Ctrl Pts',(-56.0138194370891,-2.84342080474805,
125.613245024815));
#153759=CARTESIAN_POINT('Ctrl Pts',(-56.0212173514004,-2.98068260125099,
125.690820176775));
#153760=CARTESIAN_POINT('Ctrl Pts',(-56.0286152657118,-3.11466843832551,
125.773777044878));
#153761=CARTESIAN_POINT('Ctrl Pts',(-56.036011950624,-3.24863200938505,
125.856720127054));
#153762=CARTESIAN_POINT('Ctrl Pts',(-56.0434086355363,-3.37932038442163,
125.945042954049));
#153763=CARTESIAN_POINT('Ctrl Pts',(-56.0508053204485,-3.50628195251088,
126.038448592361));
#153764=CARTESIAN_POINT('Ctrl Pts',(-56.0582016773839,-3.63323789099132,
126.131850088969));
#153765=CARTESIAN_POINT('Ctrl Pts',(-56.0655980343194,-3.75646705040901,
126.230333727552));
#153766=CARTESIAN_POINT('Ctrl Pts',(-56.0729943912549,-3.8755484682286,
126.333560394685));
#153767=CARTESIAN_POINT('Ctrl Pts',(-56.0803918805915,-3.99464811771743,
126.436802866085));
#153768=CARTESIAN_POINT('Ctrl Pts',(-56.087789369928,-4.10959847909074,
126.544789567404));
#153769=CARTESIAN_POINT('Ctrl Pts',(-56.0951868592646,-4.22001334313334,
126.657142520302));
#153770=CARTESIAN_POINT('Ctrl Pts',(-56.1025869417797,-4.33046691293567,
126.769534858354));
#153771=CARTESIAN_POINT('Ctrl Pts',(-56.1099870242948,-4.43638155841314,
126.886296229282));
#153772=CARTESIAN_POINT('Ctrl Pts',(-56.1173871068098,-4.53740956172568,
127.007013513118));
#153773=CARTESIAN_POINT('Ctrl Pts',(-56.1247953264763,-4.63854865571322,
127.127863538017));
#153774=CARTESIAN_POINT('Ctrl Pts',(-56.1322035461427,-4.7347901368442,
127.252677876477));
#153775=CARTESIAN_POINT('Ctrl Pts',(-56.1396117658091,-4.82582761483588,
127.381011614851));
#153776=CARTESIAN_POINT('Ctrl Pts',(-56.1470245451112,-4.91692112487597,
127.5094243405));
#153777=CARTESIAN_POINT('Ctrl Pts',(-56.1544373244133,-5.00280404626517,
127.641360470222));
#153778=CARTESIAN_POINT('Ctrl Pts',(-56.1618501037154,-5.08321489546729,
127.776348581758));
#153779=CARTESIAN_POINT('Ctrl Pts',(-56.1692734747441,-5.16374063946177,
127.911529570638));
#153780=CARTESIAN_POINT('Ctrl Pts',(-56.1766968457729,-5.23877851785293,
128.049770923644));
#153781=CARTESIAN_POINT('Ctrl Pts',(-56.1841202168016,-5.30811394617773,
128.19057851171));
#153782=CARTESIAN_POINT('Ctrl Pts',(-56.1880562662423,-5.34487725395585,
128.265238073533));
#153783=CARTESIAN_POINT('Ctrl Pts',(-56.1919923156831,-5.38003821160391,
128.340618783419));
#153784=CARTESIAN_POINT('Ctrl Pts',(-56.1959283651238,-5.41357048442335,
128.4166451461));
#153785=CARTESIAN_POINT('Ctrl Pts',(-56.2041038846963,-5.48321995323033,
128.57455856296));
#153786=CARTESIAN_POINT('Ctrl Pts',(-56.2122794042688,-5.54602121981847,
128.735669095438));
#153787=CARTESIAN_POINT('Ctrl Pts',(-56.2204549238413,-5.60169867752389,
128.899392773027));
#153788=CARTESIAN_POINT('Ctrl Pts',(-56.2285995869807,-5.65716599473232,
129.06249851696));
#153789=CARTESIAN_POINT('Ctrl Pts',(-56.2367442501201,-5.70556305390394,
129.228197500401));
#153790=CARTESIAN_POINT('Ctrl Pts',(-56.2448889132596,-5.74666302753057,
129.395888178889));
#153791=CARTESIAN_POINT('Ctrl Pts',(-56.2530141703147,-5.78766507328249,
129.563179305009));
#153792=CARTESIAN_POINT('Ctrl Pts',(-56.2611394273701,-5.82140464485385,
129.732452425879));
#153793=CARTESIAN_POINT('Ctrl Pts',(-56.2692646844253,-5.84770389665012,
129.903089459921));
#153794=CARTESIAN_POINT('Ctrl Pts',(-56.2773578624664,-5.87389931738443,
130.073052808468));
#153795=CARTESIAN_POINT('Ctrl Pts',(-56.2854510405073,-5.89271295735898,
130.244369089194));
#153796=CARTESIAN_POINT('Ctrl Pts',(-56.2935442185484,-5.90401770404672,
130.41641021764));
#153797=CARTESIAN_POINT('Ctrl Pts',(-56.2995710627509,-5.91243614568859,
130.544526153346));
#153798=CARTESIAN_POINT('Ctrl Pts',(-56.3055979069536,-5.91669151175424,
130.673043678158));
#153799=CARTESIAN_POINT('Ctrl Pts',(-56.3116247511561,-5.91674940103896,
130.801698324359));
#153800=CARTESIAN_POINT('',(-58.061624841459,-5.91543455321711,130.809483652149));
#153801=CARTESIAN_POINT('Ctrl Pts',(-56.311624807788,-5.9080768208085,130.80170343381));
#153802=CARTESIAN_POINT('Ctrl Pts',(-56.3658752015043,-5.90341159627506,
131.958087879031));
#153803=CARTESIAN_POINT('Ctrl Pts',(-56.5129414698247,-5.01586192239143,
135.099518527684));
#153804=CARTESIAN_POINT('Ctrl Pts',(-56.7528236127496,0.092937087818058,
137.802140496073));
#153805=CARTESIAN_POINT('Ctrl Pts',(-57.0312712365624,5.9376651652947,134.508640968079));
#153806=CARTESIAN_POINT('Ctrl Pts',(-57.3097188603752,6.3259690269338,127.811088762121));
#153807=CARTESIAN_POINT('Ctrl Pts',(-57.5881664841882,0.901016393590843,
123.864207161853));
#153808=CARTESIAN_POINT('Ctrl Pts',(-57.8388017999925,-4.72736082987953,
126.052192822845));
#153809=CARTESIAN_POINT('Ctrl Pts',(-57.9966212411924,-5.90153607060214,
129.426714923525));
#153810=CARTESIAN_POINT('Ctrl Pts',(-58.061624807788,-5.91288519561185,
130.809480727883));
#153811=CARTESIAN_POINT('',(-59.8116248077881,-5.9209921477642,130.804907070087));
#153812=CARTESIAN_POINT('Ctrl Pts',(-58.0616248588036,-5.91674778079818,
130.8094851585));
#153813=CARTESIAN_POINT('Ctrl Pts',(-58.0705428481065,-5.91658336994005,
130.999312421554));
#153814=CARTESIAN_POINT('Ctrl Pts',(-58.0794608374095,-5.90727989835948,
131.188740026179));
#153815=CARTESIAN_POINT('Ctrl Pts',(-58.0883788267124,-5.88897505791403,
131.376989057103));
#153816=CARTESIAN_POINT('Ctrl Pts',(-58.0978259775627,-5.86958407379152,
131.576408111347));
#153817=CARTESIAN_POINT('Ctrl Pts',(-58.1072731284129,-5.84009146292724,
131.774504383113));
#153818=CARTESIAN_POINT('Ctrl Pts',(-58.1167202792632,-5.80071843205518,
131.970377870661));
#153819=CARTESIAN_POINT('Ctrl Pts',(-58.1261674301134,-5.76134540118317,
132.166251358209));
#153820=CARTESIAN_POINT('Ctrl Pts',(-58.1356145809637,-5.71209208476659,
132.359902120265));
#153821=CARTESIAN_POINT('Ctrl Pts',(-58.1450617318139,-5.65323636242812,
132.550456031059));
#153822=CARTESIAN_POINT('Ctrl Pts',(-58.1524849982193,-5.60698943429867,
132.700187147544));
#153823=CARTESIAN_POINT('Ctrl Pts',(-58.1599082646247,-5.55471981911166,
132.848306067638));
#153824=CARTESIAN_POINT('Ctrl Pts',(-58.1673315310301,-5.49655650543425,
132.994291471513));
#153825=CARTESIAN_POINT('Ctrl Pts',(-58.174746023751,-5.43846193596345,
133.140104332764));
#153826=CARTESIAN_POINT('Ctrl Pts',(-58.182160516472,-5.3744876704066,133.28378835373));
#153827=CARTESIAN_POINT('Ctrl Pts',(-58.1895750091929,-5.30481279538097,
133.424836102752));
#153828=CARTESIAN_POINT('Ctrl Pts',(-58.1969823555467,-5.23520507562311,
133.565747904643));
#153829=CARTESIAN_POINT('Ctrl Pts',(-58.2043897019004,-5.15990784900905,
133.704028160654));
#153830=CARTESIAN_POINT('Ctrl Pts',(-58.2117970482541,-5.07914869102246,
133.839188312343));
#153831=CARTESIAN_POINT('Ctrl Pts',(-58.2191988699295,-4.99844976626266,
133.974247656492));
#153832=CARTESIAN_POINT('Ctrl Pts',(-58.2266006916049,-4.91229721209398,
134.106191210799));
#153833=CARTESIAN_POINT('Ctrl Pts',(-58.2340025132802,-4.82096498044718,
134.234554084384));
#153834=CARTESIAN_POINT('Ctrl Pts',(-58.2414004275915,-4.7296809623748,
134.362849196208));
#153835=CARTESIAN_POINT('Ctrl Pts',(-58.2487983419028,-4.63322292820549,
134.487567088367));
#153836=CARTESIAN_POINT('Ctrl Pts',(-58.2561962562141,-4.53190861318151,
134.60827109026));
#153837=CARTESIAN_POINT('Ctrl Pts',(-58.2635929411263,-4.43061113475851,
134.728955033338));
#153838=CARTESIAN_POINT('Ctrl Pts',(-58.2709896260384,-4.32445921694841,
134.845626124371));
#153839=CARTESIAN_POINT('Ctrl Pts',(-58.2783863109506,-4.21381148959082,
134.957880003905));
#153840=CARTESIAN_POINT('Ctrl Pts',(-58.285782667886,-4.10316866846942,
135.070128905984));
#153841=CARTESIAN_POINT('Ctrl Pts',(-58.2931790248215,-3.98803069622591,
135.177960720152));
#153842=CARTESIAN_POINT('Ctrl Pts',(-58.3005753817569,-3.86879355133091,
135.281007467573));
#153843=CARTESIAN_POINT('Ctrl Pts',(-58.3079728710934,-3.74953815092462,
135.384069991715));
#153844=CARTESIAN_POINT('Ctrl Pts',(-58.3153703604299,-3.62618261070159,
135.482345746291));
#153845=CARTESIAN_POINT('Ctrl Pts',(-58.3227678497665,-3.49915638833094,
135.575506720181));
#153846=CARTESIAN_POINT('Ctrl Pts',(-58.3301679322814,-3.3720856371153,
135.668700351507));
#153847=CARTESIAN_POINT('Ctrl Pts',(-58.3375680147963,-3.24134194267041,
135.75677541171));
#153848=CARTESIAN_POINT('Ctrl Pts',(-58.3449680973113,-3.10738402098666,
135.839447022844));
#153849=CARTESIAN_POINT('Ctrl Pts',(-58.3523763169777,-2.97327879879642,
135.922209539914));
#153850=CARTESIAN_POINT('Ctrl Pts',(-58.3597845366441,-2.83595260885898,
135.999556545884));
#153851=CARTESIAN_POINT('Ctrl Pts',(-58.3671927563105,-2.69588970540682,
136.071248622715));
#153852=CARTESIAN_POINT('Ctrl Pts',(-58.3746055356126,-2.55574059557467,
136.142984824823));
#153853=CARTESIAN_POINT('Ctrl Pts',(-58.3820183149145,-2.4128517538871,
136.209059006115));
#153854=CARTESIAN_POINT('Ctrl Pts',(-58.3894310942165,-2.2677272290903,
136.269279992721));
#153855=CARTESIAN_POINT('Ctrl Pts',(-58.3968544652452,-2.12239534356681,
136.329587025896));
#153856=CARTESIAN_POINT('Ctrl Pts',(-58.4042778362741,-1.97482174420468,
136.384024032109));
#153857=CARTESIAN_POINT('Ctrl Pts',(-58.4117012073028,-1.82552622603439,
136.432449508172));
#153858=CARTESIAN_POINT('Ctrl Pts',(-58.4156372567442,-1.74636615999106,
136.458125857538));
#153859=CARTESIAN_POINT('Ctrl Pts',(-58.4195733061856,-1.66672219362542,
136.482112999708));
#153860=CARTESIAN_POINT('Ctrl Pts',(-58.4235093556269,-1.58667281850235,
136.504395698995));
#153861=CARTESIAN_POINT('Ctrl Pts',(-58.4309326220324,-1.43570219529896,
136.546420174425));
#153862=CARTESIAN_POINT('Ctrl Pts',(-58.4383558884377,-1.28283254911229,
136.582506161133));
#153863=CARTESIAN_POINT('Ctrl Pts',(-58.4457791548431,-1.12857220254967,
136.612480394751));
#153864=CARTESIAN_POINT('Ctrl Pts',(-58.4531936475642,-0.974494178905941,
136.642419201315));
#153865=CARTESIAN_POINT('Ctrl Pts',(-58.4606081402852,-0.819029089530808,
136.666260562867));
#153866=CARTESIAN_POINT('Ctrl Pts',(-58.4680226330062,-0.662700651743137,
136.683880870842));
#153867=CARTESIAN_POINT('Ctrl Pts',(-58.47542997936,-0.506522889189468,
136.7014841957));
#153868=CARTESIAN_POINT('Ctrl Pts',(-58.4828373257138,-0.349483803284461,
136.712878362478));
#153869=CARTESIAN_POINT('Ctrl Pts',(-58.4902446720675,-0.192117442189441,
136.717990759104));
#153870=CARTESIAN_POINT('Ctrl Pts',(-58.4976464937429,-0.0348684508638419,
136.723099342711));
#153871=CARTESIAN_POINT('Ctrl Pts',(-58.5050483154183,0.122706958132031,
136.721935472925));
#153872=CARTESIAN_POINT('Ctrl Pts',(-58.5124501370937,0.280069581224368,
136.714478348388));
#153873=CARTESIAN_POINT('Ctrl Pts',(-58.519848051405,0.437349133812882,
136.707025160408));
#153874=CARTESIAN_POINT('Ctrl Pts',(-58.5272459657164,0.594415752268915,
136.693285351544));
#153875=CARTESIAN_POINT('Ctrl Pts',(-58.5346438800277,0.750730309587199,
136.673290210325));
#153876=CARTESIAN_POINT('Ctrl Pts',(-58.5420405649399,0.907018890261891,
136.653298391937));
#153877=CARTESIAN_POINT('Ctrl Pts',(-58.5494372498521,1.06255528792672,
136.627053351657));
#153878=CARTESIAN_POINT('Ctrl Pts',(-58.5568339347643,1.21680545533208,
136.594638248766));
#153879=CARTESIAN_POINT('Ctrl Pts',(-58.5642302916997,1.3710487831236,136.562224583194));
#153880=CARTESIAN_POINT('Ctrl Pts',(-58.5716266486352,1.5240056287379,136.523641475764));
#153881=CARTESIAN_POINT('Ctrl Pts',(-58.5790230055706,1.6751523651249,136.47902317283));
#153882=CARTESIAN_POINT('Ctrl Pts',(-58.5864204949072,1.82632224246288,
136.43439803872));
#153883=CARTESIAN_POINT('Ctrl Pts',(-58.5938179842437,1.97568110071901,
136.383735974986));
#153884=CARTESIAN_POINT('Ctrl Pts',(-58.6012154735802,2.12272084248869,
136.327220998507));
#153885=CARTESIAN_POINT('Ctrl Pts',(-58.6086155560952,2.26981212881212,
136.27068621079));
#153886=CARTESIAN_POINT('Ctrl Pts',(-58.6160156386103,2.41458233181698,
136.208294559191));
#153887=CARTESIAN_POINT('Ctrl Pts',(-58.6234157211252,2.55654382842102,
136.140277990976));
#153888=CARTESIAN_POINT('Ctrl Pts',(-58.6308239407917,2.69866142628457,
136.072186631553));
#153889=CARTESIAN_POINT('Ctrl Pts',(-58.6382321604582,2.8379638130283,135.99845816471));
#153890=CARTESIAN_POINT('Ctrl Pts',(-58.6456403801246,2.97398780823429,
135.919370595951));
#153891=CARTESIAN_POINT('Ctrl Pts',(-58.6530531594267,3.11009552393966,
135.840234350112));
#153892=CARTESIAN_POINT('Ctrl Pts',(-58.6604659387287,3.24292051316542,
135.755732629717));
#153893=CARTESIAN_POINT('Ctrl Pts',(-58.6678787180307,3.37202948525996,
135.666186171104));
#153894=CARTESIAN_POINT('Ctrl Pts',(-58.6753020890595,3.50132293430843,
135.576511764312));
#153895=CARTESIAN_POINT('Ctrl Pts',(-58.6827254600882,3.62688946451295,
135.481778447222));
#153896=CARTESIAN_POINT('Ctrl Pts',(-58.690148831117,3.74832906332195,135.382347052185));
#153897=CARTESIAN_POINT('Ctrl Pts',(-58.6940848805579,3.81271925251582,
135.329626140711));
#153898=CARTESIAN_POINT('Ctrl Pts',(-58.6980209299988,3.87594982380001,
135.275585052442));
#153899=CARTESIAN_POINT('Ctrl Pts',(-58.7019569794397,3.93796553235037,
135.220281589291));
#153900=CARTESIAN_POINT('Ctrl Pts',(-58.7093802458452,4.05492522322926,
135.115980983754));
#153901=CARTESIAN_POINT('Ctrl Pts',(-58.7168035122506,4.16791516366784,
135.006872778187));
#153902=CARTESIAN_POINT('Ctrl Pts',(-58.7242267786561,4.27651482066179,
134.893290985176));
#153903=CARTESIAN_POINT('Ctrl Pts',(-58.7316412713771,4.38498612187981,
134.779843436411));
#153904=CARTESIAN_POINT('Ctrl Pts',(-58.7390557640981,4.48907721282924,
134.661933091995));
#153905=CARTESIAN_POINT('Ctrl Pts',(-58.7464702568192,4.58840101612065,
134.539933756692));
#153906=CARTESIAN_POINT('Ctrl Pts',(-58.753877603173,4.68762908739097,134.418052008943));
#153907=CARTESIAN_POINT('Ctrl Pts',(-58.7612849495269,4.78209878442577,
134.292089403853));
#153908=CARTESIAN_POINT('Ctrl Pts',(-58.7686922958807,4.87146035055661,
134.16245600267));
#153909=CARTESIAN_POINT('Ctrl Pts',(-58.7760941175561,4.96075526746001,
134.032919286967));
#153910=CARTESIAN_POINT('Ctrl Pts',(-58.7834959392316,5.04494942840241,
133.899717532562));
#153911=CARTESIAN_POINT('Ctrl Pts',(-58.7908977609071,5.1237338799097,133.76329314305));
#153912=CARTESIAN_POINT('Ctrl Pts',(-58.7982956752184,5.2024767417183,133.62694077091));
#153913=CARTESIAN_POINT('Ctrl Pts',(-58.8056935895297,5.27581539523022,
133.48736947414));
#153914=CARTESIAN_POINT('Ctrl Pts',(-58.8130915038411,5.34348475305723,
133.345049747772));
#153915=CARTESIAN_POINT('Ctrl Pts',(-58.8204881887534,5.41114286546462,
133.20275367236));
#153916=CARTESIAN_POINT('Ctrl Pts',(-58.8278848736657,5.47313339190495,
133.057710410642));
#153917=CARTESIAN_POINT('Ctrl Pts',(-58.8352815585779,5.52923763105137,
132.910414221315));
#153918=CARTESIAN_POINT('Ctrl Pts',(-58.8426779155134,5.58533938247696,
132.763124563256));
#153919=CARTESIAN_POINT('Ctrl Pts',(-58.8500742724488,5.63555523269865,
132.613582525067));
#153920=CARTESIAN_POINT('Ctrl Pts',(-58.8574706293843,5.67971509376531,
132.462301212447));
#153921=CARTESIAN_POINT('Ctrl Pts',(-58.8648681187209,5.7238817158195,132.310996738272));
#153922=CARTESIAN_POINT('Ctrl Pts',(-58.8722656080576,5.76199039795617,
132.15795281782));
#153923=CARTESIAN_POINT('Ctrl Pts',(-58.8796630973942,5.79392131972813,
132.003696393444));
#153924=CARTESIAN_POINT('Ctrl Pts',(-58.8870631799092,5.82586343483522,
131.849385894717));
#153925=CARTESIAN_POINT('Ctrl Pts',(-58.8944632624243,5.85162340225436,
131.693862411133));
#153926=CARTESIAN_POINT('Ctrl Pts',(-58.9018633449393,5.87113279360231,
131.537661566964));
#153927=CARTESIAN_POINT('Ctrl Pts',(-58.9092715646058,5.89066363753166,
131.381288963908));
#153928=CARTESIAN_POINT('Ctrl Pts',(-58.9166797842723,5.90393013296248,
131.224237883445));
#153929=CARTESIAN_POINT('Ctrl Pts',(-58.9240880039388,5.91091581346791,
131.067048281142));
#153930=CARTESIAN_POINT('Ctrl Pts',(-58.9315007832409,5.91790579354315,
130.909761931261));
#153931=CARTESIAN_POINT('Ctrl Pts',(-58.938913562543,5.91860725406831,130.752337262083));
#153932=CARTESIAN_POINT('Ctrl Pts',(-58.9463263418451,5.91305583542779,
130.595312179128));
#153933=CARTESIAN_POINT('Ctrl Pts',(-58.9537497128739,5.90749648465999,
130.438062731372));
#153934=CARTESIAN_POINT('Ctrl Pts',(-58.9611730839027,5.89566643871305,
130.281214381404));
#153935=CARTESIAN_POINT('Ctrl Pts',(-58.9685964549315,5.87765305950754,
130.125298709813));
#153936=CARTESIAN_POINT('Ctrl Pts',(-58.972532504372,5.86810193362853,130.042628479597));
#153937=CARTESIAN_POINT('Ctrl Pts',(-58.9764685538124,5.85681330381691,
129.960220280966));
#153938=CARTESIAN_POINT('Ctrl Pts',(-58.9804046032529,5.84380593928373,
129.878151836301));
#153939=CARTESIAN_POINT('Ctrl Pts',(-58.9878278696583,5.81927445571807,
129.723373310919));
#153940=CARTESIAN_POINT('Ctrl Pts',(-58.9952511360636,5.78855245501014,
129.569336023763));
#153941=CARTESIAN_POINT('Ctrl Pts',(-59.002674402469,5.75169364304545,129.416574323121));
#153942=CARTESIAN_POINT('Ctrl Pts',(-59.01008889519,5.71487839513551,129.263993174122));
#153943=CARTESIAN_POINT('Ctrl Pts',(-59.0175033879111,5.67194086020873,
129.112684970017));
#153944=CARTESIAN_POINT('Ctrl Pts',(-59.0249178806321,5.62298630601622,
128.963177420583));
#153945=CARTESIAN_POINT('Ctrl Pts',(-59.0323252269858,5.57407893606622,
128.813813972153));
#153946=CARTESIAN_POINT('Ctrl Pts',(-59.0397325733396,5.51916620775687,
128.666248075659));
#153947=CARTESIAN_POINT('Ctrl Pts',(-59.0471399196933,5.45840406520437,
128.520995639412));
#153948=CARTESIAN_POINT('Ctrl Pts',(-59.0545417413687,5.3976872413502,128.375851537911));
#153949=CARTESIAN_POINT('Ctrl Pts',(-59.0619435630441,5.33112983344623,
128.233017803919));
#153950=CARTESIAN_POINT('Ctrl Pts',(-59.0693453847194,5.25893705126755,
128.092993498693));
#153951=CARTESIAN_POINT('Ctrl Pts',(-59.0767432990308,5.18678237909663,
127.953043111208));
#153952=CARTESIAN_POINT('Ctrl Pts',(-59.0841412133421,5.10899842787934,
127.815899529827));
#153953=CARTESIAN_POINT('Ctrl Pts',(-59.0915391276534,5.02583775220401,
127.682040094138));
#153954=CARTESIAN_POINT('Ctrl Pts',(-59.0989358125656,4.94269089632428,
127.548202903458));
#153955=CARTESIAN_POINT('Ctrl Pts',(-59.1063324974779,4.85416928614718,
127.417649092064));
#153956=CARTESIAN_POINT('Ctrl Pts',(-59.11372918239,4.7605705421038,127.290829818476));
#153957=CARTESIAN_POINT('Ctrl Pts',(-59.1211255393255,4.66697594832682,
127.164016168187));
#153958=CARTESIAN_POINT('Ctrl Pts',(-59.1285218962608,4.56830488998346,
127.040937026801));
#153959=CARTESIAN_POINT('Ctrl Pts',(-59.1359182531963,4.46489712073938,
126.922012840291));
#153960=CARTESIAN_POINT('Ctrl Pts',(-59.1433157425328,4.36147351950169,
126.803070446184));
#153961=CARTESIAN_POINT('Ctrl Pts',(-59.1507132318694,4.25331200834828,
126.688284555299));
#153962=CARTESIAN_POINT('Ctrl Pts',(-59.158110721206,4.14079115292679,126.578040801184));
#153963=CARTESIAN_POINT('Ctrl Pts',(-59.1655108037209,4.02823085349386,
126.467758401292));
#153964=CARTESIAN_POINT('Ctrl Pts',(-59.1729108862359,3.9113084337142,126.362021569393));
#153965=CARTESIAN_POINT('Ctrl Pts',(-59.1803109687509,3.79043754224487,
126.261177394226));
#153966=CARTESIAN_POINT('Ctrl Pts',(-59.1877191884174,3.66943374080454,
126.160222330521));
#153967=CARTESIAN_POINT('Ctrl Pts',(-59.1951274080838,3.54447308372678,
126.064170907012));
#153968=CARTESIAN_POINT('Ctrl Pts',(-59.2025356277503,3.41600095041762,
125.973328836544));
#153969=CARTESIAN_POINT('Ctrl Pts',(-59.2099484070524,3.28744974465408,
125.882430854297));
#153970=CARTESIAN_POINT('Ctrl Pts',(-59.2173611863543,3.15538306852536,
125.796748816688));
#153971=CARTESIAN_POINT('Ctrl Pts',(-59.2247739656563,3.02027274167973,
125.716543489527));
#153972=CARTESIAN_POINT('Ctrl Pts',(-59.232197336685,2.88496936286306,125.636223561233));
#153973=CARTESIAN_POINT('Ctrl Pts',(-59.2396207077139,2.74661397506129,
125.561396149541));
#153974=CARTESIAN_POINT('Ctrl Pts',(-59.2470440787426,2.60570103332997,
125.492275086684));
#153975=CARTESIAN_POINT('Ctrl Pts',(-59.2509801281836,2.53098561046079,
125.455625440619));
#153976=CARTESIAN_POINT('Ctrl Pts',(-59.2549161776246,2.45555147886789,
125.420579240293));
#153977=CARTESIAN_POINT('Ctrl Pts',(-59.2588522270655,2.37947417380949,
125.387162705483));
#153978=CARTESIAN_POINT('Ctrl Pts',(-59.266275493471,2.23599475076708,125.32414016373));
#153979=CARTESIAN_POINT('Ctrl Pts',(-59.2736987598764,2.08979282671053,
125.266726536739));
#153980=CARTESIAN_POINT('Ctrl Pts',(-59.2811220262819,1.94134699333004,
125.215165468532));
#153981=CARTESIAN_POINT('Ctrl Pts',(-59.2885365190029,1.79307661059673,
125.163665341225));
#153982=CARTESIAN_POINT('Ctrl Pts',(-59.2959510117239,1.64256794677638,
125.118004125186));
#153983=CARTESIAN_POINT('Ctrl Pts',(-59.3033655044449,1.49032187883998,
125.078378495698));
#153984=CARTESIAN_POINT('Ctrl Pts',(-59.3107728507987,1.33822255139582,
125.038791058884));
#153985=CARTESIAN_POINT('Ctrl Pts',(-59.3181801971524,1.18438951242256,
125.005227720868));
#153986=CARTESIAN_POINT('Ctrl Pts',(-59.3255875435062,1.02934110179654,
124.977836142491));
#153987=CARTESIAN_POINT('Ctrl Pts',(-59.3329893651816,0.874408332124798,
124.950464993786));
#153988=CARTESIAN_POINT('Ctrl Pts',(-59.3403911868572,0.718262361727727,
124.929256503929));
#153989=CARTESIAN_POINT('Ctrl Pts',(-59.3477930085326,0.561433985871367,
124.914307778923));
#153990=CARTESIAN_POINT('Ctrl Pts',(-59.3551909228439,0.404688398493871,
124.899366945233));
#153991=CARTESIAN_POINT('Ctrl Pts',(-59.3625888371553,0.247261493758251,
124.890679330693));
#153992=CARTESIAN_POINT('Ctrl Pts',(-59.3699867514666,0.0896913829007215,
124.888290467683));
#153993=CARTESIAN_POINT('Ctrl Pts',(-59.3773834363788,-0.0678525426627713,
124.885902001659));
#153994=CARTESIAN_POINT('Ctrl Pts',(-59.384780121291,-0.22553925422612,
124.889810215351));
#153995=CARTESIAN_POINT('Ctrl Pts',(-59.3921768062032,-0.382828308236872,
124.900008574461));
#153996=CARTESIAN_POINT('Ctrl Pts',(-59.3995731631387,-0.540110387886141,
124.910206481366));
#153997=CARTESIAN_POINT('Ctrl Pts',(-59.4069695200742,-0.696994472526925,
124.926693954966));
#153998=CARTESIAN_POINT('Ctrl Pts',(-59.4143658770096,-0.85294318389762,
124.949412412198));
#153999=CARTESIAN_POINT('Ctrl Pts',(-59.4217633663462,-1.00891577141414,
124.972134347684));
#154000=CARTESIAN_POINT('Ctrl Pts',(-59.4291608556827,-1.16395233109188,
125.001089112486));
#154001=CARTESIAN_POINT('Ctrl Pts',(-59.4365583450193,-1.3175237945246,
125.036166652956));
#154002=CARTESIAN_POINT('Ctrl Pts',(-59.4439584275343,-1.47114909219575,
125.071256489804));
#154003=CARTESIAN_POINT('Ctrl Pts',(-59.4513585100493,-1.62330790737527,
125.112473292572));
#154004=CARTESIAN_POINT('Ctrl Pts',(-59.4587585925643,-1.77348463727377,
125.159656656874));
#154005=CARTESIAN_POINT('Ctrl Pts',(-59.4661668122308,-1.92382650192533,
125.206891904135));
#154006=CARTESIAN_POINT('Ctrl Pts',(-59.4735750318972,-2.07218157232565,
125.260106703411));
#154007=CARTESIAN_POINT('Ctrl Pts',(-59.4809832515637,-2.21805190515195,
125.319091589656));
#154008=CARTESIAN_POINT('Ctrl Pts',(-59.4883960308658,-2.36401201873434,
125.378112780113));
#154009=CARTESIAN_POINT('Ctrl Pts',(-59.4958088101678,-2.50748400797178,
125.442910980836));
#154010=CARTESIAN_POINT('Ctrl Pts',(-59.5032215894699,-2.64799345315919,
125.513230186881));
#154011=CARTESIAN_POINT('Ctrl Pts',(-59.5106449604987,-2.78870366483113,
125.583649868304));
#154012=CARTESIAN_POINT('Ctrl Pts',(-59.5180683315274,-2.92644255213581,
125.65960613071));
#154013=CARTESIAN_POINT('Ctrl Pts',(-59.5254917025562,-3.06076294692327,
125.740798556601));
#154014=CARTESIAN_POINT('Ctrl Pts',(-59.5294277519969,-3.13198284321272,
125.783848728994));
#154015=CARTESIAN_POINT('Ctrl Pts',(-59.5333638014378,-3.20224219481042,
125.828370272979));
#154016=CARTESIAN_POINT('Ctrl Pts',(-59.5372998508785,-3.27147811362319,
125.874313811035));
#154017=CARTESIAN_POINT('Ctrl Pts',(-59.5447040751354,-3.40171994041827,
125.960739620477));
#154018=CARTESIAN_POINT('Ctrl Pts',(-59.5521082993922,-3.52873656741033,
126.052464121099));
#154019=CARTESIAN_POINT('Ctrl Pts',(-59.5595125236491,-3.65206569474598,
126.14921865155));
#154020=CARTESIAN_POINT('Ctrl Pts',(-59.5669079843502,-3.77524885112543,
126.245858664437));
#154021=CARTESIAN_POINT('Ctrl Pts',(-59.5743034450512,-3.89475290211312,
126.347516628378));
#154022=CARTESIAN_POINT('Ctrl Pts',(-59.5816989057523,-4.01014290459188,
126.453879673205));
#154023=CARTESIAN_POINT('Ctrl Pts',(-59.5890872484693,-4.12542184648628,
126.560140345714));
#154024=CARTESIAN_POINT('Ctrl Pts',(-59.5964755911865,-4.23659434794291,
126.671096831731));
#154025=CARTESIAN_POINT('Ctrl Pts',(-59.6038639339035,-4.3432571807991,
126.786395009956));
#154026=CARTESIAN_POINT('Ctrl Pts',(-59.6112467984276,-4.4498409269638,
126.901607698688));
#154027=CARTESIAN_POINT('Ctrl Pts',(-59.6186296629518,-4.55192140798027,
127.021155395861));
#154028=CARTESIAN_POINT('Ctrl Pts',(-59.626012527476,-4.64913114114335,
127.144646121195));
#154029=CARTESIAN_POINT('Ctrl Pts',(-59.633746372489,-4.7509622132949,127.274007580714));
#154030=CARTESIAN_POINT('Ctrl Pts',(-59.6414802175019,-4.8474477724383,
127.407695866079));
#154031=CARTESIAN_POINT('Ctrl Pts',(-59.6492140625149,-4.93821123908698,
127.545219577253));
#154032=CARTESIAN_POINT('Ctrl Pts',(-59.6565918955248,-5.02479659206562,
127.67641266093));
#154033=CARTESIAN_POINT('Ctrl Pts',(-59.6639697285347,-5.10617465032543,
127.811095611072));
#154034=CARTESIAN_POINT('Ctrl Pts',(-59.6713475615446,-5.18206199385268,
127.94881092366));
#154035=CARTESIAN_POINT('Ctrl Pts',(-59.6787252287696,-5.25794763213975,
128.086523141691));
#154036=CARTESIAN_POINT('Ctrl Pts',(-59.6861028959945,-5.32834261959897,
128.227267257946));
#154037=CARTESIAN_POINT('Ctrl Pts',(-59.6934805632195,-5.39300911312665,
128.370560447414));
#154038=CARTESIAN_POINT('Ctrl Pts',(-59.7008595412986,-5.45768709651109,
128.513879097025));
#154039=CARTESIAN_POINT('Ctrl Pts',(-59.7082385193777,-5.51663440523919,
128.659747379284));
#154040=CARTESIAN_POINT('Ctrl Pts',(-59.7156174974568,-5.56966110690731,
128.807661913028));
#154041=CARTESIAN_POINT('Ctrl Pts',(-59.7229992635616,-5.62270784384367,
128.955632333849));
#154042=CARTESIAN_POINT('Ctrl Pts',(-59.7303810296664,-5.66982939381967,
129.105650192144));
#154043=CARTESIAN_POINT('Ctrl Pts',(-59.7377627957712,-5.71088555804053,
129.257196532711));
#154044=CARTESIAN_POINT('Ctrl Pts',(-59.7451527055776,-5.7519870161851,
129.40891006202));
#154045=CARTESIAN_POINT('Ctrl Pts',(-59.7525426153839,-5.78700962983586,
129.562155078025));
#154046=CARTESIAN_POINT('Ctrl Pts',(-59.7599325251903,-5.81586409879498,
129.716401359667));
#154047=CARTESIAN_POINT('Ctrl Pts',(-59.7673272013841,-5.84473717847892,
129.870747127982));
#154048=CARTESIAN_POINT('Ctrl Pts',(-59.7747218775778,-5.8674341334322,
130.026095078201));
#154049=CARTESIAN_POINT('Ctrl Pts',(-59.7821165537716,-5.88391755623333,
130.181910013944));
#154050=CARTESIAN_POINT('Ctrl Pts',(-59.7895213737257,-5.90042359042213,
130.337938691211));
#154051=CARTESIAN_POINT('Ctrl Pts',(-59.7969261936799,-5.91069905083801,
130.494435259889));
#154052=CARTESIAN_POINT('Ctrl Pts',(-59.804331013634,-5.91475860492403,
130.650864011815));
#154053=CARTESIAN_POINT('Ctrl Pts',(-59.806762278352,-5.91609150034639,
130.7022251128));
#154054=CARTESIAN_POINT('Ctrl Pts',(-59.8091935430701,-5.91675471187478,
130.753578940631));
#154055=CARTESIAN_POINT('Ctrl Pts',(-59.8116248077881,-5.91674997480182,
130.804906678574));
#154056=CARTESIAN_POINT('',(-61.5616241089946,-5.91516794619516,130.798959479098));
#154057=CARTESIAN_POINT('Ctrl Pts',(-59.8116248077881,-5.92647066646659,
130.804907575703));
#154058=CARTESIAN_POINT('Ctrl Pts',(-59.8129990300892,-5.9265088843322,
130.833967190104));
#154059=CARTESIAN_POINT('Ctrl Pts',(-59.8143732523903,-5.92631371465216,
130.863026276885));
#154060=CARTESIAN_POINT('Ctrl Pts',(-59.9085633492957,-5.89683354231334,
132.854516748754));
#154061=CARTESIAN_POINT('Ctrl Pts',(-60.0941950985041,-3.69523994540662,
136.747656191254));
#154062=CARTESIAN_POINT('Ctrl Pts',(-60.3726427223173,3.00289543727563,
137.125767068913));
#154063=CARTESIAN_POINT('Ctrl Pts',(-60.6510903461299,6.94151661269781,
131.694814235658));
#154064=CARTESIAN_POINT('Ctrl Pts',(-60.929537969943,4.5012231329918,125.445578028453));
#154065=CARTESIAN_POINT('Ctrl Pts',(-61.2079855937559,-2.07547450896312,
124.12080122956));
#154066=CARTESIAN_POINT('Ctrl Pts',(-61.4186808805036,-5.60873709036134,
127.765787223005));
#154067=CARTESIAN_POINT('Ctrl Pts',(-61.5365602926472,-5.9192368584348,
130.266176064463));
#154068=CARTESIAN_POINT('Ctrl Pts',(-61.5616238301864,-5.91453770888721,
130.798954126379));
#154069=CARTESIAN_POINT('',(-63.3116254755953,-5.91161047281451,130.806144527447));
#154070=CARTESIAN_POINT('Ctrl Pts',(-61.561624807788,-5.91674754700121,
130.798972894932));
#154071=CARTESIAN_POINT('Ctrl Pts',(-61.5689558267893,-5.91688950142237,
130.95486593736));
#154072=CARTESIAN_POINT('Ctrl Pts',(-61.5762868457905,-5.91086609325577,
131.11089921841));
#154073=CARTESIAN_POINT('Ctrl Pts',(-61.5836178647918,-5.89867096461179,
131.26654176576));
#154074=CARTESIAN_POINT('Ctrl Pts',(-61.5911704888164,-5.88610719666045,
131.426889139317));
#154075=CARTESIAN_POINT('Ctrl Pts',(-61.598723112841,-5.86699266002491,
131.586821372375));
#154076=CARTESIAN_POINT('Ctrl Pts',(-61.6062757368655,-5.84137829381317,
131.745758615794));
#154077=CARTESIAN_POINT('Ctrl Pts',(-61.6136016021555,-5.8165329690963,
131.899923953704));
#154078=CARTESIAN_POINT('Ctrl Pts',(-61.6209274674455,-5.78557257107751,
132.053152789232));
#154079=CARTESIAN_POINT('Ctrl Pts',(-61.6282533327354,-5.74859609097896,
132.204922485275));
#154080=CARTESIAN_POINT('Ctrl Pts',(-61.6355790136,-5.71162054174657,132.356688360586));
#154081=CARTESIAN_POINT('Ctrl Pts',(-61.6429046944647,-5.66862930161556,
132.506994799048));
#154082=CARTESIAN_POINT('Ctrl Pts',(-61.6502303753293,-5.61977206211482,
132.655331317597));
#154083=CARTESIAN_POINT('Ctrl Pts',(-61.6575573859683,-5.57090595393626,
132.80369476253));
#154084=CARTESIAN_POINT('Ctrl Pts',(-61.6648843966073,-5.51617184659786,
132.950087213911));
#154085=CARTESIAN_POINT('Ctrl Pts',(-61.6722114072463,-5.45576860355499,
133.094015505745));
#154086=CARTESIAN_POINT('Ctrl Pts',(-61.6795412625481,-5.39534190935679,
133.237999676777));
#154087=CARTESIAN_POINT('Ctrl Pts',(-61.6868711178499,-5.32924184664861,
133.379517433259));
#154088=CARTESIAN_POINT('Ctrl Pts',(-61.6942009731517,-5.25771438357038,
133.518097897278));
#154089=CARTESIAN_POINT('Ctrl Pts',(-61.7015389587674,-5.18610758185615,
133.656832075471));
#154090=CARTESIAN_POINT('Ctrl Pts',(-61.7088769443831,-5.10906153733858,
133.792622118929));
#154091=CARTESIAN_POINT('Ctrl Pts',(-61.7162149299988,-5.0268671996667,
133.925023482955));
#154092=CARTESIAN_POINT('Ctrl Pts',(-61.7235578007166,-4.9446181429269,
134.057512990269));
#154093=CARTESIAN_POINT('Ctrl Pts',(-61.7309006714343,-4.8572141803491,
134.186609011208));
#154094=CARTESIAN_POINT('Ctrl Pts',(-61.7382435421521,-4.76498766214409,
134.311898663278));
#154095=CARTESIAN_POINT('Ctrl Pts',(-61.7455963441718,-4.67263640670414,
134.437357770783));
#154096=CARTESIAN_POINT('Ctrl Pts',(-61.7529491461915,-4.57544981514295,
134.558999939309));
#154097=CARTESIAN_POINT('Ctrl Pts',(-61.7603019482111,-4.47379861883439,
134.676447455515));
#154098=CARTESIAN_POINT('Ctrl Pts',(-61.7618282459346,-4.45269782092106,
134.70082726013));
#154099=CARTESIAN_POINT('Ctrl Pts',(-61.763354543658,-4.43140476358562,
134.725026452925));
#154100=CARTESIAN_POINT('Ctrl Pts',(-61.7648808413815,-4.40992294498366,
134.74904186981));
#154101=CARTESIAN_POINT('Ctrl Pts',(-61.772304107787,-4.3054444674859,134.865842697485));
#154102=CARTESIAN_POINT('Ctrl Pts',(-61.7797273741924,-4.19616443681054,
134.978666462967));
#154103=CARTESIAN_POINT('Ctrl Pts',(-61.7871506405979,-4.08241750513419,
135.08709314205));
#154104=CARTESIAN_POINT('Ctrl Pts',(-61.7945651333189,-3.96880501288466,
135.195391669803));
#154105=CARTESIAN_POINT('Ctrl Pts',(-61.80197962604,-3.85073639608633,135.299303200744));
#154106=CARTESIAN_POINT('Ctrl Pts',(-61.809394118761,-3.72858604813662,
135.3984412268));
#154107=CARTESIAN_POINT('Ctrl Pts',(-61.8168014651148,-3.60655343329133,
135.497483699894));
#154108=CARTESIAN_POINT('Ctrl Pts',(-61.8242088114686,-3.48044720726796,
135.591761593892));
#154109=CARTESIAN_POINT('Ctrl Pts',(-61.8316161578223,-3.35067796310653,
135.680925776574));
#154110=CARTESIAN_POINT('Ctrl Pts',(-61.8390179794977,-3.22100550574349,
135.770023457245));
#154111=CARTESIAN_POINT('Ctrl Pts',(-61.8464198011732,-3.08767577640384,
135.854014810297));
#154112=CARTESIAN_POINT('Ctrl Pts',(-61.8538216228486,-2.95113164834545,
135.932591555875));
#154113=CARTESIAN_POINT('Ctrl Pts',(-61.8612195371599,-2.81465960086883,
136.011126821402));
#154114=CARTESIAN_POINT('Ctrl Pts',(-61.8686174514713,-2.67497685677345,
136.084252986235));
#154115=CARTESIAN_POINT('Ctrl Pts',(-61.8760153657827,-2.53255431396588,
136.151705679306));
#154116=CARTESIAN_POINT('Ctrl Pts',(-61.8834120506949,-2.39015543920132,
136.219147162963));
#154117=CARTESIAN_POINT('Ctrl Pts',(-61.8908087356072,-2.24501800641278,
136.280916886466));
#154118=CARTESIAN_POINT('Ctrl Pts',(-61.8982054205194,-2.09763660655163,
136.336796900918));
#154119=CARTESIAN_POINT('Ctrl Pts',(-61.9056017774548,-1.95026174173641,
136.392674437593));
#154120=CARTESIAN_POINT('Ctrl Pts',(-61.9129981343903,-1.80064345673848,
136.44266265214));
#154121=CARTESIAN_POINT('Ctrl Pts',(-61.9203944913257,-1.64929511550924,
136.486592237665));
#154122=CARTESIAN_POINT('Ctrl Pts',(-61.9277919806623,-1.4979236024628,
136.530528548922));
#154123=CARTESIAN_POINT('Ctrl Pts',(-61.9351894699989,-1.34482186430642,
136.568404280136));
#154124=CARTESIAN_POINT('Ctrl Pts',(-61.9425869593355,-1.19051702513014,
136.600100412914));
#154125=CARTESIAN_POINT('Ctrl Pts',(-61.9499870418505,-1.03615809463147,
136.631807656722));
#154126=CARTESIAN_POINT('Ctrl Pts',(-61.9573871243655,-0.880595588856351,
136.657330914044));
#154127=CARTESIAN_POINT('Ctrl Pts',(-61.9647872068805,-0.724365235592859,
136.676602571706));
#154128=CARTESIAN_POINT('Ctrl Pts',(-61.972195426547,-0.567963090995085,
136.695895420537));
#154129=CARTESIAN_POINT('Ctrl Pts',(-61.9796036462135,-0.410892003047028,
136.708922895596));
#154130=CARTESIAN_POINT('Ctrl Pts',(-61.98701186588,-0.253691951750863,
136.715669352196));
#154131=CARTESIAN_POINT('Ctrl Pts',(-61.9944246451821,-0.0963951464457003,
136.722419961128));
#154132=CARTESIAN_POINT('Ctrl Pts',(-62.0018374244841,0.0610304079409894,
136.722881847293));
#154133=CARTESIAN_POINT('Ctrl Pts',(-62.0092502037862,0.218046860748704,
136.717091469636));
#154134=CARTESIAN_POINT('Ctrl Pts',(-62.0166735748149,0.375287666027083,
136.711292818415));
#154135=CARTESIAN_POINT('Ctrl Pts',(-62.0240969458437,0.532117831050493,
136.699224089679));
#154136=CARTESIAN_POINT('Ctrl Pts',(-62.0315203168725,0.688005908796778,
136.680973454223));
#154137=CARTESIAN_POINT('Ctrl Pts',(-62.0354563663132,0.77066150809838,
136.671296529386));
#154138=CARTESIAN_POINT('Ctrl Pts',(-62.0393924157538,0.853052431933938,
136.659882501396));
#154139=CARTESIAN_POINT('Ctrl Pts',(-62.0433284651945,0.93510098657501,
136.646750257722));
#154140=CARTESIAN_POINT('Ctrl Pts',(-62.0507517316,1.08984199998493,136.621983255996));
#154141=CARTESIAN_POINT('Ctrl Pts',(-62.0581749980054,1.24383235511324,
136.591026872334));
#154142=CARTESIAN_POINT('Ctrl Pts',(-62.0655982644109,1.39653778602307,
136.553935625748));
#154143=CARTESIAN_POINT('Ctrl Pts',(-62.0730127571319,1.54906273179517,
136.516888217935));
#154144=CARTESIAN_POINT('Ctrl Pts',(-62.0804272498529,1.70030541706897,
136.473720467399));
#154145=CARTESIAN_POINT('Ctrl Pts',(-62.0878417425739,1.84973829287897,
136.424538444856));
#154146=CARTESIAN_POINT('Ctrl Pts',(-62.0952490889277,1.99902713965721,
136.375403825797));
#154147=CARTESIAN_POINT('Ctrl Pts',(-62.1026564352815,2.14650929744772,
136.320266590901));
#154148=CARTESIAN_POINT('Ctrl Pts',(-62.1100637816352,2.29166909585843,
136.259283469228));
#154149=CARTESIAN_POINT('Ctrl Pts',(-62.1174656033106,2.43672062861471,
136.198345831068));
#154150=CARTESIAN_POINT('Ctrl Pts',(-62.1248674249859,2.5794529081633,136.131571131608));
#154151=CARTESIAN_POINT('Ctrl Pts',(-62.1322692466613,2.71936718611896,
136.059165339871));
#154152=CARTESIAN_POINT('Ctrl Pts',(-62.1396671609727,2.85920760441578,
135.986797770588));
#154153=CARTESIAN_POINT('Ctrl Pts',(-62.147065075284,2.99623265305317,135.908805200259));
#154154=CARTESIAN_POINT('Ctrl Pts',(-62.1544629895953,3.12996537734346,
135.825440909608));
#154155=CARTESIAN_POINT('Ctrl Pts',(-62.1618596745075,3.2636758776817,135.742090472589));
#154156=CARTESIAN_POINT('Ctrl Pts',(-62.1692563594197,3.39409482307481,
135.653370284242));
#154157=CARTESIAN_POINT('Ctrl Pts',(-62.1766530443319,3.52077150845368,
135.559578651238));
#154158=CARTESIAN_POINT('Ctrl Pts',(-62.1840494012674,3.64744257685557,
135.465791177054));
#154159=CARTESIAN_POINT('Ctrl Pts',(-62.1914457582028,3.77037141516492,
135.366932927468));
#154160=CARTESIAN_POINT('Ctrl Pts',(-62.1988421151383,3.88913809494087,
135.263344295601));
#154161=CARTESIAN_POINT('Ctrl Pts',(-62.2062396044749,4.00792295819904,
135.159739804049));
#154162=CARTESIAN_POINT('Ctrl Pts',(-62.2136370938114,4.12254411275699,
135.051403733558));
#154163=CARTESIAN_POINT('Ctrl Pts',(-62.221034583148,4.23261650162447,134.938715236207));
#154164=CARTESIAN_POINT('Ctrl Pts',(-62.228434665663,4.34272747619692,134.825987236077));
#154165=CARTESIAN_POINT('Ctrl Pts',(-62.235834748178,4.44828624963538,134.708904038233));
#154166=CARTESIAN_POINT('Ctrl Pts',(-62.243234830693,4.54894636310545,134.587879819062));
#154167=CARTESIAN_POINT('Ctrl Pts',(-62.2506430503594,4.6497171627184,134.466722521321));
#154168=CARTESIAN_POINT('Ctrl Pts',(-62.258051270026,4.7455783061534,134.341615835029));
#154169=CARTESIAN_POINT('Ctrl Pts',(-62.2654594896924,4.836224758711,134.213005604321));
#154170=CARTESIAN_POINT('Ctrl Pts',(-62.2728722689945,4.92692700264789,
134.084316216162));
#154171=CARTESIAN_POINT('Ctrl Pts',(-62.2802850482965,5.01240795803893,
133.952119299488));
#154172=CARTESIAN_POINT('Ctrl Pts',(-62.2876978275986,5.09240757740633,
133.816887070242));
#154173=CARTESIAN_POINT('Ctrl Pts',(-62.2951211986274,5.17252150398149,
133.681461614846));
#154174=CARTESIAN_POINT('Ctrl Pts',(-62.3025445696562,5.24713827567704,
133.542992512674));
#154175=CARTESIAN_POINT('Ctrl Pts',(-62.3099679406849,5.31604481298278,
133.401974543626));
#154176=CARTESIAN_POINT('Ctrl Pts',(-62.3139039901258,5.3525807124521,133.327203432756));
#154177=CARTESIAN_POINT('Ctrl Pts',(-62.3178400395665,5.38751207428662,
133.251716054167));
#154178=CARTESIAN_POINT('Ctrl Pts',(-62.3217760890074,5.42081279369141,
133.17558798293));
#154179=CARTESIAN_POINT('Ctrl Pts',(-62.3291993554128,5.48361691120855,
133.032012816455));
#154180=CARTESIAN_POINT('Ctrl Pts',(-62.3366226218183,5.54080797727401,
132.885723687931));
#154181=CARTESIAN_POINT('Ctrl Pts',(-62.3440458882237,5.59214307648628,
132.73719955928));
#154182=CARTESIAN_POINT('Ctrl Pts',(-62.3514603809447,5.64341750187446,
132.588850973815));
#154183=CARTESIAN_POINT('Ctrl Pts',(-62.3588748736656,5.6888496164733,132.438272995684));
#154184=CARTESIAN_POINT('Ctrl Pts',(-62.3662893663866,5.72824350747633,
132.285966800583));
#154185=CARTESIAN_POINT('Ctrl Pts',(-62.3736967127404,5.76759942916395,
132.133807403929));
#154186=CARTESIAN_POINT('Ctrl Pts',(-62.3811040590942,5.80092862061613,
131.979923465405));
#154187=CARTESIAN_POINT('Ctrl Pts',(-62.388511405448,5.82808420998719,131.824833549004));
#154188=CARTESIAN_POINT('Ctrl Pts',(-62.3959132271233,5.85521954569522,
131.669859304514));
#154189=CARTESIAN_POINT('Ctrl Pts',(-62.4033150487987,5.87619038340733,
131.51368123922));
#154190=CARTESIAN_POINT('Ctrl Pts',(-62.4107168704741,5.89090042501172,
131.356830295555));
#154191=CARTESIAN_POINT('Ctrl Pts',(-62.4181147847854,5.90560270129963,
131.200062152281));
#154192=CARTESIAN_POINT('Ctrl Pts',(-62.4255126990967,5.91405072882852,
131.042622208774));
#154193=CARTESIAN_POINT('Ctrl Pts',(-62.432910613408,5.91619979418705,130.885048644938));
#154194=CARTESIAN_POINT('Ctrl Pts',(-62.4403072983202,5.91834850240991,
130.727501266969));
#154195=CARTESIAN_POINT('Ctrl Pts',(-62.4477039832325,5.91420032091174,
130.569820685641));
#154196=CARTESIAN_POINT('Ctrl Pts',(-62.4551006681447,5.90376260644601,
130.412547333935));
#154197=CARTESIAN_POINT('Ctrl Pts',(-62.4624970250802,5.89332535479948,
130.255280955894));
#154198=CARTESIAN_POINT('Ctrl Pts',(-62.4698933820155,5.87659914942211,
130.098422144051));
#154199=CARTESIAN_POINT('Ctrl Pts',(-62.477289738951,5.85364339110611,129.942508186891));
#154200=CARTESIAN_POINT('Ctrl Pts',(-62.4846872282875,5.83068411820494,
129.786570358907));
#154201=CARTESIAN_POINT('Ctrl Pts',(-62.4920847176241,5.80149344768047,
129.631578042983));
#154202=CARTESIAN_POINT('Ctrl Pts',(-62.4994822069606,5.76618223820521,
129.478060139429));
#154203=CARTESIAN_POINT('Ctrl Pts',(-62.5068822894756,5.73085865044005,
129.324488420411));
#154204=CARTESIAN_POINT('Ctrl Pts',(-62.5142823719906,5.68941033558519,
129.172392506387));
#154205=CARTESIAN_POINT('Ctrl Pts',(-62.5216824545057,5.64199848250326,
129.022287755439));
#154206=CARTESIAN_POINT('Ctrl Pts',(-62.5290906741721,5.59453449521489,
128.872017948886));
#154207=CARTESIAN_POINT('Ctrl Pts',(-62.5364988938385,5.54109398639783,
128.723744034144));
#154208=CARTESIAN_POINT('Ctrl Pts',(-62.543907113505,5.48188717864237,128.577963635189));
#154209=CARTESIAN_POINT('Ctrl Pts',(-62.551319892807,5.42264393008474,128.432093510831));
#154210=CARTESIAN_POINT('Ctrl Pts',(-62.5587326721091,5.35762746445342,
128.288720299563));
#154211=CARTESIAN_POINT('Ctrl Pts',(-62.5661454514112,5.28709450838142,
128.148318030945));
#154212=CARTESIAN_POINT('Ctrl Pts',(-62.5735688224399,5.21646077151412,
128.007715148981));
#154213=CARTESIAN_POINT('Ctrl Pts',(-62.5809921934686,5.14029498192602,
127.870092013678));
#154214=CARTESIAN_POINT('Ctrl Pts',(-62.5884155644974,5.05889823727925,
127.735895335482));
#154215=CARTESIAN_POINT('Ctrl Pts',(-62.5923516139384,5.01573973017724,
127.664741036694));
#154216=CARTESIAN_POINT('Ctrl Pts',(-62.5962876633793,4.97111131497194,
127.594549520663));
#154217=CARTESIAN_POINT('Ctrl Pts',(-62.6002237128203,4.92506246483318,
127.525383600265));
#154218=CARTESIAN_POINT('Ctrl Pts',(-62.6076469792258,4.83821577061095,
127.394938832994));
#154219=CARTESIAN_POINT('Ctrl Pts',(-62.6150702456312,4.74605175183823,
127.2677495221));
#154220=CARTESIAN_POINT('Ctrl Pts',(-62.6224935120366,4.64884207103577,
127.144278929807));
#154221=CARTESIAN_POINT('Ctrl Pts',(-62.6299080047576,4.55174728400325,
127.020954269501));
#154222=CARTESIAN_POINT('Ctrl Pts',(-62.6373224974786,4.449618934093,126.901339869533));
#154223=CARTESIAN_POINT('Ctrl Pts',(-62.6447369901996,4.34277277895584,
126.785871454602));
#154224=CARTESIAN_POINT('Ctrl Pts',(-62.6521443365534,4.23602960616584,
126.670514332476));
#154225=CARTESIAN_POINT('Ctrl Pts',(-62.6595516829072,4.12457793255688,
126.55929551218));
#154226=CARTESIAN_POINT('Ctrl Pts',(-62.666959029261,4.00877465288077,126.452618857659));
#154227=CARTESIAN_POINT('Ctrl Pts',(-62.6743608509365,3.89305774365899,
126.346021766611));
#154228=CARTESIAN_POINT('Ctrl Pts',(-62.6817626726119,3.7729959641588,126.243960347766));
#154229=CARTESIAN_POINT('Ctrl Pts',(-62.6891644942873,3.64898395980213,
126.146802606805));
#154230=CARTESIAN_POINT('Ctrl Pts',(-62.6965624085986,3.5250374204192,126.04969615466));
#154231=CARTESIAN_POINT('Ctrl Pts',(-62.7039603229099,3.39714510225023,
125.95748845469));
#154232=CARTESIAN_POINT('Ctrl Pts',(-62.7113582372212,3.26573562260086,
125.870508024939));
#154233=CARTESIAN_POINT('Ctrl Pts',(-62.7187549221334,3.13434798082131,
125.783542049755));
#154234=CARTESIAN_POINT('Ctrl Pts',(-62.7261516070456,2.99944464857826,
125.701801826562));
#154235=CARTESIAN_POINT('Ctrl Pts',(-62.7335482919578,2.86148428395073,
125.625573283141));
#154236=CARTESIAN_POINT('Ctrl Pts',(-62.7409446488932,2.72353003663054,
125.549348119774));
#154237=CARTESIAN_POINT('Ctrl Pts',(-62.7483410058287,2.58251935318737,
125.478634330778));
#154238=CARTESIAN_POINT('Ctrl Pts',(-62.7557373627642,2.43893637722032,
125.413672358135));
#154239=CARTESIAN_POINT('Ctrl Pts',(-62.7631348521008,2.2953314183329,125.348700439648));
#154240=CARTESIAN_POINT('Ctrl Pts',(-62.7705323414373,2.14915372289414,
125.289482244828));
#154241=CARTESIAN_POINT('Ctrl Pts',(-62.7779298307739,2.00090819153502,
125.236210388671));
#154242=CARTESIAN_POINT('Ctrl Pts',(-62.7853299132889,1.85261069293574,
125.182919858147));
#154243=CARTESIAN_POINT('Ctrl Pts',(-62.7927299958039,1.70224426627697,
125.135579942633));
#154244=CARTESIAN_POINT('Ctrl Pts',(-62.8001300783188,1.55032962342813,
125.094333593005));
#154245=CARTESIAN_POINT('Ctrl Pts',(-62.8075382979853,1.3982479348112,125.053041888775));
#154246=CARTESIAN_POINT('Ctrl Pts',(-62.8149465176518,1.24461499063038,
125.017857229647));
#154247=CARTESIAN_POINT('Ctrl Pts',(-62.8223547373183,1.08996308647519,
124.988871727316));
#154248=CARTESIAN_POINT('Ctrl Pts',(-62.8297675166204,0.935215996652834,
124.959868384892));
#154249=CARTESIAN_POINT('Ctrl Pts',(-62.8371802959225,0.779449065682284,
124.937071856014));
#154250=CARTESIAN_POINT('Ctrl Pts',(-62.8445930752246,0.623199875073401,
124.920522373851));
#154251=CARTESIAN_POINT('Ctrl Pts',(-62.8520164462534,0.466727428294285,
124.903949245011));
#154252=CARTESIAN_POINT('Ctrl Pts',(-62.8594398172821,0.309771717147762,
124.893641014655));
#154253=CARTESIAN_POINT('Ctrl Pts',(-62.8668631883109,0.152871322426201,
124.889585818702));
#154254=CARTESIAN_POINT('Ctrl Pts',(-62.8707992377517,0.0696789683721043,
124.887435656504));
#154255=CARTESIAN_POINT('Ctrl Pts',(-62.8747352871924,-0.0134978905157239,
124.887042577221));
#154256=CARTESIAN_POINT('Ctrl Pts',(-62.8786713366332,-0.0965796665288729,
124.888398909567));
#154257=CARTESIAN_POINT('Ctrl Pts',(-62.8860946030386,-0.253269303196848,
124.890956910042));
#154258=CARTESIAN_POINT('Ctrl Pts',(-62.8935178694441,-0.410094176017949,
124.899748179946));
#154259=CARTESIAN_POINT('Ctrl Pts',(-62.9009411358495,-0.566517689134258,
124.914794566455));
#154260=CARTESIAN_POINT('Ctrl Pts',(-62.9083556285705,-0.72275632264845,
124.929823169385));
#154261=CARTESIAN_POINT('Ctrl Pts',(-62.9157701212915,-0.878594172747348,
124.951092137663));
#154262=CARTESIAN_POINT('Ctrl Pts',(-62.9231846140125,-1.0334939771783,
124.978571335277));
#154263=CARTESIAN_POINT('Ctrl Pts',(-62.9305919603663,-1.18824448334631,
125.006024047406));
#154264=CARTESIAN_POINT('Ctrl Pts',(-62.93799930672,-1.34205837868717,125.039675007847));
#154265=CARTESIAN_POINT('Ctrl Pts',(-62.9454066530738,-1.49440297069326,
125.079442249267));
#154266=CARTESIAN_POINT('Ctrl Pts',(-62.9528084747492,-1.64663393835414,
125.119179830778));
#154267=CARTESIAN_POINT('Ctrl Pts',(-62.9602102964246,-1.79739742504874,
125.165024516323));
#154268=CARTESIAN_POINT('Ctrl Pts',(-62.9676121181,-1.94617050168461,125.216843195591));
#154269=CARTESIAN_POINT('Ctrl Pts',(-62.9750100324113,-2.09486504217244,
125.268634520182));
#154270=CARTESIAN_POINT('Ctrl Pts',(-62.9824079467227,-2.24157091353098,
125.326393435425));
#154271=CARTESIAN_POINT('Ctrl Pts',(-62.9898058610341,-2.38578004610241,
125.389936905469));
#154272=CARTESIAN_POINT('Ctrl Pts',(-62.9972025459463,-2.5299652137316,
125.453469815741));
#154273=CARTESIAN_POINT('Ctrl Pts',(-63.0045992308585,-2.67165412478181,
125.522785222565));
#154274=CARTESIAN_POINT('Ctrl Pts',(-63.0119959157707,-2.81035830421638,
125.597651794862));
#154275=CARTESIAN_POINT('Ctrl Pts',(-63.0193922727061,-2.94905633336247,
125.672515047497));
#154276=CARTESIAN_POINT('Ctrl Pts',(-63.0267886296416,-3.08476956554182,
125.752928798875));
#154277=CARTESIAN_POINT('Ctrl Pts',(-63.034184986577,-3.21703401866431,
125.838615690039));
#154278=CARTESIAN_POINT('Ctrl Pts',(-63.0415824759136,-3.34931872181129,
125.924315700085));
#154279=CARTESIAN_POINT('Ctrl Pts',(-63.0489799652501,-3.47815328123212,
126.015290254439));
#154280=CARTESIAN_POINT('Ctrl Pts',(-63.0563774545867,-3.60310273335147,
126.111218679012));
#154281=CARTESIAN_POINT('Ctrl Pts',(-63.0637775371017,-3.72809598630953,
126.207180731147));
#154282=CARTESIAN_POINT('Ctrl Pts',(-63.0711776196167,-3.8492011244829,
126.308099883817));
#154283=CARTESIAN_POINT('Ctrl Pts',(-63.0785777021317,-3.96601642176519,
126.413615315822));
#154284=CARTESIAN_POINT('Ctrl Pts',(-63.0859859217982,-4.08296016947491,
126.51924677289));
#154285=CARTESIAN_POINT('Ctrl Pts',(-63.0933941414647,-4.19560437870349,
126.629484352249));
#154286=CARTESIAN_POINT('Ctrl Pts',(-63.1008023611312,-4.30358383450491,
126.743930007164));
#154287=CARTESIAN_POINT('Ctrl Pts',(-63.1082151404333,-4.41162974985904,
126.85844610147));
#154288=CARTESIAN_POINT('Ctrl Pts',(-63.1156279197354,-4.5150049462427,
126.977175151348));
#154289=CARTESIAN_POINT('Ctrl Pts',(-63.1230406990374,-4.6133849984144,
127.09968662126));
#154290=CARTESIAN_POINT('Ctrl Pts',(-63.1304640700662,-4.71190562061876,
127.222373141306));
#154291=CARTESIAN_POINT('Ctrl Pts',(-63.1378874410948,-4.80541662249223,
127.348852576011));
#154292=CARTESIAN_POINT('Ctrl Pts',(-63.1453108121236,-4.89363686954924,
127.478665389273));
#154293=CARTESIAN_POINT('Ctrl Pts',(-63.1492468615643,-4.94041336135445,
127.547495257681));
#154294=CARTESIAN_POINT('Ctrl Pts',(-63.1531829110052,-4.9857031940248,
127.6172618358));
#154295=CARTESIAN_POINT('Ctrl Pts',(-63.157118960446,-5.02946980252924,
127.687894017721));
#154296=CARTESIAN_POINT('Ctrl Pts',(-63.1647574958261,-5.11440592758521,
127.8249670979));
#154297=CARTESIAN_POINT('Ctrl Pts',(-63.1723960312061,-5.19384721590906,
127.965696268982));
#154298=CARTESIAN_POINT('Ctrl Pts',(-63.1800345665862,-5.26747373740206,
128.10961554831));
#154299=CARTESIAN_POINT('Ctrl Pts',(-63.1876624252813,-5.34099734817427,
128.253333665931));
#154300=CARTESIAN_POINT('Ctrl Pts',(-63.1952902839764,-5.40872222743115,
128.400232705789));
#154301=CARTESIAN_POINT('Ctrl Pts',(-63.2029181426715,-5.47037202551696,
128.549818432345));
#154302=CARTESIAN_POINT('Ctrl Pts',(-63.2105364798587,-5.53194486897401,
128.699217437867));
#154303=CARTESIAN_POINT('Ctrl Pts',(-63.2181548170458,-5.58745760920087,
128.851296132596));
#154304=CARTESIAN_POINT('Ctrl Pts',(-63.2257731542331,-5.63667999997509,
129.005536240263));
#154305=CARTESIAN_POINT('Ctrl Pts',(-63.2333805424304,-5.6858316488739,
129.159554675753));
#154306=CARTESIAN_POINT('Ctrl Pts',(-63.2409879306277,-5.7287108711197,
129.315728003917));
#154307=CARTESIAN_POINT('Ctrl Pts',(-63.248595318825,-5.76513580658427,
129.473518893641));
#154308=CARTESIAN_POINT('Ctrl Pts',(-63.2561962949227,-5.80153004027449,
129.631176784905));
#154309=CARTESIAN_POINT('Ctrl Pts',(-63.2637972710204,-5.83148074705281,
129.790449188093));
#154310=CARTESIAN_POINT('Ctrl Pts',(-63.2713982471181,-5.85485583816483,
129.950783628181));
#154311=CARTESIAN_POINT('Ctrl Pts',(-63.2789925608585,-5.87821044069677,
130.110977532987));
#154312=CARTESIAN_POINT('Ctrl Pts',(-63.286586874599,-5.8950008692544,130.272231279304));
#154313=CARTESIAN_POINT('Ctrl Pts',(-63.2941811883394,-5.90514610021885,
130.433982300746));
#154314=CARTESIAN_POINT('Ctrl Pts',(-63.2999957281556,-5.91291373418863,
130.55782597993));
#154315=CARTESIAN_POINT('Ctrl Pts',(-63.3058102679718,-5.91678690610155,
130.681960891403));
#154316=CARTESIAN_POINT('Ctrl Pts',(-63.311624807788,-5.91674973488962,
130.806131827204));
#154317=CARTESIAN_POINT('',(-65.0616248077881,-5.92104421557129,130.809133668594));
#154318=CARTESIAN_POINT('Ctrl Pts',(-63.3116260199717,-5.90742110137121,
130.806154880301));
#154319=CARTESIAN_POINT('Ctrl Pts',(-63.3529395414009,-5.90976699514064,
131.687025087133));
#154320=CARTESIAN_POINT('Ctrl Pts',(-63.4870689374345,-5.31119943819695,
134.543840127222));
#154321=CARTESIAN_POINT('Ctrl Pts',(-63.7140142080715,-0.879888780334608,
137.747224310923));
#154322=CARTESIAN_POINT('Ctrl Pts',(-63.9924618318848,5.36562647909369,
135.297423383343));
#154323=CARTESIAN_POINT('Ctrl Pts',(-64.2709094556975,6.68039312965957,
128.718717272324));
#154324=CARTESIAN_POINT('Ctrl Pts',(-64.5493570795105,1.85620484941623,
124.056615506246));
#154325=CARTESIAN_POINT('Ctrl Pts',(-64.8129288635406,-4.32488770099073,
125.513155569012));
#154326=CARTESIAN_POINT('Ctrl Pts',(-64.9836847729665,-5.9065549279853,
129.157020333449));
#154327=CARTESIAN_POINT('Ctrl Pts',(-65.0616248077881,-5.92104421557129,
130.809133668594));
#154328=CARTESIAN_POINT('',(-66.811624807788,-5.92032734119191,130.800327082424));
#154329=CARTESIAN_POINT('Ctrl Pts',(-65.0616248077881,-5.92104421557129,
130.809133668594));
#154330=CARTESIAN_POINT('Ctrl Pts',(-65.0765006475708,-5.92380967906112,
131.124460359592));
#154331=CARTESIAN_POINT('Ctrl Pts',(-65.1841923619582,-5.75726169392666,
133.404300651249));
#154332=CARTESIAN_POINT('Ctrl Pts',(-65.3846999509489,-2.7949529050576,
137.220418502967));
#154333=CARTESIAN_POINT('Ctrl Pts',(-65.6631475747624,3.88727089549114,
136.623869661759));
#154334=CARTESIAN_POINT('Ctrl Pts',(-65.9415951985748,6.99728264681958,
130.679476307755));
#154335=CARTESIAN_POINT('Ctrl Pts',(-66.2200428223878,3.67713348198754,
124.849845533531));
#154336=CARTESIAN_POINT('Ctrl Pts',(-66.4984904462009,-3.022121714838,124.492123227301));
#154337=CARTESIAN_POINT('Ctrl Pts',(-66.6956844413341,-5.79969700705658,
128.346744915426));
#154338=CARTESIAN_POINT('Ctrl Pts',(-66.8000625618632,-5.92486756286859,
130.555443657081));
#154339=CARTESIAN_POINT('Ctrl Pts',(-66.811624807788,-5.92295665797096,
130.800325291063));
#154340=CARTESIAN_POINT('',(-68.5616247814665,-5.91202197454765,130.801527559385));
#154341=CARTESIAN_POINT('Ctrl Pts',(-66.811624807788,-5.91674862680149,
130.800329520612));
#154342=CARTESIAN_POINT('Ctrl Pts',(-66.8189381851903,-5.91685404465674,
130.955059351555));
#154343=CARTESIAN_POINT('Ctrl Pts',(-66.8262515625927,-5.91088576872365,
131.11002755393));
#154344=CARTESIAN_POINT('Ctrl Pts',(-66.833564939995,-5.89881422802683,
131.264709686999));
#154345=CARTESIAN_POINT('Ctrl Pts',(-66.8408708436195,-5.88675502362949,
131.419233745374));
#154346=CARTESIAN_POINT('Ctrl Pts',(-66.8481767472438,-5.86860499411473,
131.57347193579));
#154347=CARTESIAN_POINT('Ctrl Pts',(-66.8554826508682,-5.84438657742092,
131.726898473788));
#154348=CARTESIAN_POINT('Ctrl Pts',(-66.8627827872296,-5.82018727868801,
131.880203897239));
#154349=CARTESIAN_POINT('Ctrl Pts',(-66.8700829235912,-5.7899291856031,
132.032698565328));
#154350=CARTESIAN_POINT('Ctrl Pts',(-66.8773830599525,-5.75368664151171,
132.183860742173));
#154351=CARTESIAN_POINT('Ctrl Pts',(-66.884799836364,-5.71686502164054,
132.337438156623));
#154352=CARTESIAN_POINT('Ctrl Pts',(-66.8922166127753,-5.67386610235044,
132.489639732482));
#154353=CARTESIAN_POINT('Ctrl Pts',(-66.8996333891867,-5.62482223672649,
132.639927387729));
#154354=CARTESIAN_POINT('Ctrl Pts',(-66.9069280459753,-5.57658589421485,
132.787740508117));
#154355=CARTESIAN_POINT('Ctrl Pts',(-66.914222702764,-5.52250227479232,
132.933701875274));
#154356=CARTESIAN_POINT('Ctrl Pts',(-66.9215173595526,-5.46274784021575,
133.077313893971));
#154357=CARTESIAN_POINT('Ctrl Pts',(-66.928811716405,-5.40299586257673,
133.220920007737));
#154358=CARTESIAN_POINT('Ctrl Pts',(-66.9361060732575,-5.33757368119745,
133.362176609946));
#154359=CARTESIAN_POINT('Ctrl Pts',(-66.9434004301099,-5.26670599742825,
133.500605877025));
#154360=CARTESIAN_POINT('Ctrl Pts',(-66.9506960212525,-5.19582632202199,
133.639058567947));
#154361=CARTESIAN_POINT('Ctrl Pts',(-66.9579916123949,-5.11949948634783,
133.774682629542));
#154362=CARTESIAN_POINT('Ctrl Pts',(-66.9652872035375,-5.03799610746026,
133.90702492163));
#154363=CARTESIAN_POINT('Ctrl Pts',(-66.9727954110615,-4.9541174647778,
134.043224082713));
#154364=CARTESIAN_POINT('Ctrl Pts',(-66.9803036185857,-4.86475618760571,
134.175946905039));
#154365=CARTESIAN_POINT('Ctrl Pts',(-66.9878118261097,-4.77025445314744,
134.304732457061));
#154366=CARTESIAN_POINT('Ctrl Pts',(-66.9951182219343,-4.6782928130569,
134.430056406423));
#154367=CARTESIAN_POINT('Ctrl Pts',(-67.0024246177587,-4.58146379742863,
134.5516517656));
#154368=CARTESIAN_POINT('Ctrl Pts',(-67.0097310135832,-4.48012248870291,
134.669128792854));
#154369=CARTESIAN_POINT('Ctrl Pts',(-67.0173401269571,-4.37458242133302,
134.791473111539));
#154370=CARTESIAN_POINT('Ctrl Pts',(-67.024949240331,-4.26414848190876,
134.909350187863));
#154371=CARTESIAN_POINT('Ctrl Pts',(-67.0325583537049,-4.14926203807001,
135.022364304375));
#154372=CARTESIAN_POINT('Ctrl Pts',(-67.0401674670787,-4.03437559423109,
135.135378420887));
#154373=CARTESIAN_POINT('Ctrl Pts',(-67.0477765804526,-3.91503703897663,
135.243529322294));
#154374=CARTESIAN_POINT('Ctrl Pts',(-67.0553856938265,-3.79172326303862,
135.346470838491));
#154375=CARTESIAN_POINT('Ctrl Pts',(-67.0628089602319,-3.6714213349072,
135.446898084264));
#154376=CARTESIAN_POINT('Ctrl Pts',(-67.0702322266374,-3.54694487987857,
135.542694427125));
#154377=CARTESIAN_POINT('Ctrl Pts',(-67.0776554930429,-3.4186858858318,
135.633492773193));
#154378=CARTESIAN_POINT('Ctrl Pts',(-67.0850699857639,-3.29057848326456,
135.724183803158));
#154379=CARTESIAN_POINT('Ctrl Pts',(-67.0924844784849,-3.15869774222967,
135.809888381094));
#154380=CARTESIAN_POINT('Ctrl Pts',(-67.0998989712059,-3.02347011528522,
135.890278334604));
#154381=CARTESIAN_POINT('Ctrl Pts',(-67.1073063175597,-2.88837282581884,
135.97059080525));
#154382=CARTESIAN_POINT('Ctrl Pts',(-67.1147136639134,-2.74993539120956,
136.045598659754));
#154383=CARTESIAN_POINT('Ctrl Pts',(-67.1221210102672,-2.60861466516525,
136.115015952945));
#154384=CARTESIAN_POINT('Ctrl Pts',(-67.1295228319425,-2.46739934145076,
136.184381472099));
#154385=CARTESIAN_POINT('Ctrl Pts',(-67.136924653618,-2.32330534178862,
136.248164568405));
#154386=CARTESIAN_POINT('Ctrl Pts',(-67.1443264752933,-2.17681553918244,
136.306124395744));
#154387=CARTESIAN_POINT('Ctrl Pts',(-67.1517243896047,-2.03040306740153,
136.364053626542));
#154388=CARTESIAN_POINT('Ctrl Pts',(-67.1591223039162,-1.88159765767546,
136.416165573517));
#154389=CARTESIAN_POINT('Ctrl Pts',(-67.1665202182276,-1.73090354873195,
136.462266897056));
#154390=CARTESIAN_POINT('Ctrl Pts',(-67.1739169031398,-1.58023448241613,
136.508360559391));
#154391=CARTESIAN_POINT('Ctrl Pts',(-67.1813135880519,-1.42767769643456,
136.548445471626));
#154392=CARTESIAN_POINT('Ctrl Pts',(-67.1887102729642,-1.2737541451294,
136.582377659793));
#154393=CARTESIAN_POINT('Ctrl Pts',(-67.1961066298996,-1.11983741895603,
136.616308343371));
#154394=CARTESIAN_POINT('Ctrl Pts',(-67.2035029868351,-0.964554412504578,
136.644086764972));
#154395=CARTESIAN_POINT('Ctrl Pts',(-67.2108993437705,-0.808437605933992,
136.665619799671));
#154396=CARTESIAN_POINT('Ctrl Pts',(-67.2182968331071,-0.652296897481104,
136.687156131133));
#154397=CARTESIAN_POINT('Ctrl Pts',(-67.2256943224437,-0.495322504547796,
136.702445120794));
#154398=CARTESIAN_POINT('Ctrl Pts',(-67.2330918117803,-0.338053234559719,
136.71144539545));
#154399=CARTESIAN_POINT('Ctrl Pts',(-67.2404918942953,-0.180728834072846,
136.720448825138));
#154400=CARTESIAN_POINT('Ctrl Pts',(-67.2478919768104,-0.0231097231805228,
136.723159129364));
#154401=CARTESIAN_POINT('Ctrl Pts',(-67.2552920593254,0.134264227263688,
136.719587044321));
#154402=CARTESIAN_POINT('Ctrl Pts',(-67.2627002789918,0.291811226544174,
136.716011031403));
#154403=CARTESIAN_POINT('Ctrl Pts',(-67.2701084986582,0.449112153578574,
136.706138841696));
#154404=CARTESIAN_POINT('Ctrl Pts',(-67.2775167183247,0.605630461261856,
136.690033247512));
#154405=CARTESIAN_POINT('Ctrl Pts',(-67.2849294976268,0.76224510335187,
136.673917740603));
#154406=CARTESIAN_POINT('Ctrl Pts',(-67.2923422769288,0.918075797607008,
136.651561237288));
#154407=CARTESIAN_POINT('Ctrl Pts',(-67.2997550562309,1.07259565444685,
136.623077754922));
#154408=CARTESIAN_POINT('Ctrl Pts',(-67.3071784272596,1.22733629650462,
136.594553574021));
#154409=CARTESIAN_POINT('Ctrl Pts',(-67.3146017982884,1.38076199722079,
136.559885011399));
#154410=CARTESIAN_POINT('Ctrl Pts',(-67.3220251693172,1.53235969694117,
136.519236322399));
#154411=CARTESIAN_POINT('Ctrl Pts',(-67.3259612187579,1.6127404348687,136.497683412139));
#154412=CARTESIAN_POINT('Ctrl Pts',(-67.3298972681987,1.69260755686729,
136.47445009147));
#154413=CARTESIAN_POINT('Ctrl Pts',(-67.3338333176394,1.77188692644919,
136.449566307563));
#154414=CARTESIAN_POINT('Ctrl Pts',(-67.3412565840448,1.92140534325825,
136.402636267711));
#154415=CARTESIAN_POINT('Ctrl Pts',(-67.3486798504503,2.06928408404975,
136.349690964011));
#154416=CARTESIAN_POINT('Ctrl Pts',(-67.3561031168558,2.21500242332258,
136.290861763759));
#154417=CARTESIAN_POINT('Ctrl Pts',(-67.3635176095768,2.36054853561976,
136.232102094736));
#154418=CARTESIAN_POINT('Ctrl Pts',(-67.3709321022978,2.50393898621277,
136.167472510072));
#154419=CARTESIAN_POINT('Ctrl Pts',(-67.3783465950188,2.64466716634428,
136.097154411184));
#154420=CARTESIAN_POINT('Ctrl Pts',(-67.3857539413726,2.78525970735704,
136.026904087527));
#154421=CARTESIAN_POINT('Ctrl Pts',(-67.3931612877263,2.92319475461249,
135.950976330567));
#154422=CARTESIAN_POINT('Ctrl Pts',(-67.4005686340801,3.05798479375098,
135.869600943917));
#154423=CARTESIAN_POINT('Ctrl Pts',(-67.4079704557555,3.19267430139371,
135.788286250099));
#154424=CARTESIAN_POINT('Ctrl Pts',(-67.4153722774309,3.32422315325712,
135.701532208771));
#154425=CARTESIAN_POINT('Ctrl Pts',(-67.4227740991063,3.45216771402715,
135.609614891455));
#154426=CARTESIAN_POINT('Ctrl Pts',(-67.4301720134176,3.5800447338582,135.517746096577));
#154427=CARTESIAN_POINT('Ctrl Pts',(-67.4375699277289,3.70432094946446,
135.420719671232));
#154428=CARTESIAN_POINT('Ctrl Pts',(-67.4449678420402,3.82456114540592,
135.31885534096));
#154429=CARTESIAN_POINT('Ctrl Pts',(-67.4523645269524,3.94478135960889,
135.217007938691));
#154430=CARTESIAN_POINT('Ctrl Pts',(-67.4597612118647,4.06096660076599,
135.110324468204));
#154431=CARTESIAN_POINT('Ctrl Pts',(-67.4671578967769,4.17271415095235,
134.999165401694));
#154432=CARTESIAN_POINT('Ctrl Pts',(-67.4745542537123,4.28445674613523,
134.888011264093));
#154433=CARTESIAN_POINT('Ctrl Pts',(-67.4819506106478,4.39176177693915,
134.772382188323));
#154434=CARTESIAN_POINT('Ctrl Pts',(-67.4893469675832,4.49426307619539,
134.652675828726));
#154435=CARTESIAN_POINT('Ctrl Pts',(-67.4967444569198,4.59678006866222,
134.53295114178));
#154436=CARTESIAN_POINT('Ctrl Pts',(-67.5041419462564,4.6944916223632,134.409148211626));
#154437=CARTESIAN_POINT('Ctrl Pts',(-67.511539435593,4.78707169027595,134.281697988984));
#154438=CARTESIAN_POINT('Ctrl Pts',(-67.518939518108,4.87968421198824,134.154203088863));
#154439=CARTESIAN_POINT('Ctrl Pts',(-67.5263396006229,4.96716144719189,
134.023058652502));
#154440=CARTESIAN_POINT('Ctrl Pts',(-67.5337396831379,5.04922061516566,
133.888724691713));
#154441=CARTESIAN_POINT('Ctrl Pts',(-67.5411479028044,5.13137001563016,
133.754243016924));
#154442=CARTESIAN_POINT('Ctrl Pts',(-67.5485561224709,5.20808925618579,
133.616565132338));
#154443=CARTESIAN_POINT('Ctrl Pts',(-67.5559643421374,5.27914113213969,
133.476176380198));
#154444=CARTESIAN_POINT('Ctrl Pts',(-67.5633771214394,5.35023673933787,
133.335701221124));
#154445=CARTESIAN_POINT('Ctrl Pts',(-67.5707899007415,5.41565787655098,
133.192512208562));
#154446=CARTESIAN_POINT('Ctrl Pts',(-67.5782026800435,5.47521567312217,
133.047114258806));
#154447=CARTESIAN_POINT('Ctrl Pts',(-67.5856260510723,5.53485856866601,
132.901508557642));
#154448=CARTESIAN_POINT('Ctrl Pts',(-67.593049422101,5.58862126393568,132.753687965464));
#154449=CARTESIAN_POINT('Ctrl Pts',(-67.6004727931298,5.63636463032776,
132.604172917916));
#154450=CARTESIAN_POINT('Ctrl Pts',(-67.6044088425706,5.66167930877564,
132.52489645214));
#154451=CARTESIAN_POINT('Ctrl Pts',(-67.6083448920115,5.68530258839858,
132.445143803118));
#154452=CARTESIAN_POINT('Ctrl Pts',(-67.6122809414524,5.70721959201832,
132.364993531157));
#154453=CARTESIAN_POINT('Ctrl Pts',(-67.6197042078578,5.74855437683823,
132.213832619643));
#154454=CARTESIAN_POINT('Ctrl Pts',(-67.6271274742632,5.78394206488328,
132.060799816961));
#154455=CARTESIAN_POINT('Ctrl Pts',(-67.6345507406687,5.81321171432706,
131.906404231454));
#154456=CARTESIAN_POINT('Ctrl Pts',(-67.6419652333897,5.84244676947592,
131.752191128706));
#154457=CARTESIAN_POINT('Ctrl Pts',(-67.6493797261106,5.865578110545,131.596618812418));
#154458=CARTESIAN_POINT('Ctrl Pts',(-67.6567942188316,5.88248452127648,
131.44021155878));
#154459=CARTESIAN_POINT('Ctrl Pts',(-67.6642015651854,5.89937463697273,
131.283955056342));
#154460=CARTESIAN_POINT('Ctrl Pts',(-67.6716089115392,5.91005172694864,
131.126865587287));
#154461=CARTESIAN_POINT('Ctrl Pts',(-67.679016257893,5.91444561807293,130.969477525719));
#154462=CARTESIAN_POINT('Ctrl Pts',(-67.6864180795684,5.91883623206746,
130.812206850104));
#154463=CARTESIAN_POINT('Ctrl Pts',(-67.6938199012438,5.91695296778733,
130.654638396951));
#154464=CARTESIAN_POINT('Ctrl Pts',(-67.7012217229192,5.90877748581179,
130.497311459183));
#154465=CARTESIAN_POINT('Ctrl Pts',(-67.7086196372306,5.90060631960951,
130.34006757308));
#154466=CARTESIAN_POINT('Ctrl Pts',(-67.716017551542,5.88614957018592,130.183065320302));
#154467=CARTESIAN_POINT('Ctrl Pts',(-67.7234154658534,5.8654409871166,130.026843679389));
#154468=CARTESIAN_POINT('Ctrl Pts',(-67.7308121507656,5.84473584543821,
129.870647999679));
#154469=CARTESIAN_POINT('Ctrl Pts',(-67.7382088356779,5.81778098111208,
129.715233044069));
#154470=CARTESIAN_POINT('Ctrl Pts',(-67.7456055205901,5.78466199072975,
129.561132474582));
#154471=CARTESIAN_POINT('Ctrl Pts',(-67.7530018775255,5.75154446887815,
129.407038738076));
#154472=CARTESIAN_POINT('Ctrl Pts',(-67.7603982344609,5.71226344286773,
129.254259636773));
#154473=CARTESIAN_POINT('Ctrl Pts',(-67.7677945913964,5.66695554825979,
129.103318179369));
#154474=CARTESIAN_POINT('Ctrl Pts',(-67.7751920807329,5.62164071689778,
128.952353612443));
#154475=CARTESIAN_POINT('Ctrl Pts',(-67.7825895700695,5.57029728699078,
128.803227607177));
#154476=CARTESIAN_POINT('Ctrl Pts',(-67.7899870594061,5.51311159320498,
128.656447415556));
#154477=CARTESIAN_POINT('Ctrl Pts',(-67.7973871419211,5.45590585306255,
128.509615770366));
#154478=CARTESIAN_POINT('Ctrl Pts',(-67.8047872244359,5.39285390692614,
128.365131923671));
#154479=CARTESIAN_POINT('Ctrl Pts',(-67.8121873069509,5.32418992587507,
128.223482434522));
#154480=CARTESIAN_POINT('Ctrl Pts',(-67.8195955266174,5.2554504417182,128.081677187199));
#154481=CARTESIAN_POINT('Ctrl Pts',(-67.8270037462839,5.18108676166788,
127.94271285773));
#154482=CARTESIAN_POINT('Ctrl Pts',(-67.8344119659504,5.10137900296805,
127.807051352479));
#154483=CARTESIAN_POINT('Ctrl Pts',(-67.8418247452524,5.02162218547251,
127.671306349835));
#154484=CARTESIAN_POINT('Ctrl Pts',(-67.8492375245545,4.93651493654471,
127.538868535399));
#154485=CARTESIAN_POINT('Ctrl Pts',(-67.8566503038566,4.84637996735821,
127.410169730994));
#154486=CARTESIAN_POINT('Ctrl Pts',(-67.8640736748853,4.75611620910082,
127.281287035702));
#154487=CARTESIAN_POINT('Ctrl Pts',(-67.871497045914,4.66081060842491,127.156154316742));
#154488=CARTESIAN_POINT('Ctrl Pts',(-67.8789204169428,4.56082582016753,
127.035169935126));
#154489=CARTESIAN_POINT('Ctrl Pts',(-67.8828564663836,4.50781148633142,
126.971021113013));
#154490=CARTESIAN_POINT('Ctrl Pts',(-67.8867925158244,4.45348228366514,
126.908037923958));
#154491=CARTESIAN_POINT('Ctrl Pts',(-67.8907285652652,4.39789626569995,
126.846275348317));
#154492=CARTESIAN_POINT('Ctrl Pts',(-67.8981518316706,4.29306277059753,
126.729793058203));
#154493=CARTESIAN_POINT('Ctrl Pts',(-67.905575098076,4.18343984936724,126.617302426135));
#154494=CARTESIAN_POINT('Ctrl Pts',(-67.9129983644815,4.06936343104479,
126.50922245581));
#154495=CARTESIAN_POINT('Ctrl Pts',(-67.9204128572025,3.95542184157551,
126.401270227034));
#154496=CARTESIAN_POINT('Ctrl Pts',(-67.9278273499235,3.83703750070714,
126.29771853766));
#154497=CARTESIAN_POINT('Ctrl Pts',(-67.9352418426445,3.71458597650059,
126.198952754446));
#154498=CARTESIAN_POINT('Ctrl Pts',(-67.9426491889983,3.59225247568294,
126.100282165413));
#154499=CARTESIAN_POINT('Ctrl Pts',(-67.9500565353522,3.46585988429572,
126.006388532077));
#154500=CARTESIAN_POINT('Ctrl Pts',(-67.957463881706,3.33581985611548,125.917619735337));
#154501=CARTESIAN_POINT('Ctrl Pts',(-67.9648657033814,3.20587681669476,
125.828917145716));
#154502=CARTESIAN_POINT('Ctrl Pts',(-67.9722675250568,3.07229206414244,
125.745331991539));
#154503=CARTESIAN_POINT('Ctrl Pts',(-67.9796693467322,2.93550940796286,
125.667171203279));
#154504=CARTESIAN_POINT('Ctrl Pts',(-67.9870672610436,2.79879895828218,
125.589051675491));
#154505=CARTESIAN_POINT('Ctrl Pts',(-67.994465175355,2.65889429029634,125.516350995597));
#154506=CARTESIAN_POINT('Ctrl Pts',(-68.0018630896664,2.51626710438533,
125.449332100192));
#154507=CARTESIAN_POINT('Ctrl Pts',(-68.0092597745786,2.37366362052509,
125.382324342111));
#154508=CARTESIAN_POINT('Ctrl Pts',(-68.0166564594908,2.22833885421258,
125.320996653142));
#154509=CARTESIAN_POINT('Ctrl Pts',(-68.0240531444031,2.08078805746974,
125.265565475805));
#154510=CARTESIAN_POINT('Ctrl Pts',(-68.0314495013385,1.93324380328427,
125.210136756346));
#154511=CARTESIAN_POINT('Ctrl Pts',(-68.0388458582739,1.78347406437819,
125.160604159934));
#154512=CARTESIAN_POINT('Ctrl Pts',(-68.0462422152094,1.63199271763696,
125.117135430176));
#154513=CARTESIAN_POINT('Ctrl Pts',(-68.0536397045459,1.48048817871504,
125.073660045246));
#154514=CARTESIAN_POINT('Ctrl Pts',(-68.0610371938826,1.32727186901836,
125.036250478496));
#154515=CARTESIAN_POINT('Ctrl Pts',(-68.0684346832192,1.17287127244642,
125.005024143385));
#154516=CARTESIAN_POINT('Ctrl Pts',(-68.0758347657342,1.01841655098383,
124.97378686193));
#154517=CARTESIAN_POINT('Ctrl Pts',(-68.0832348482492,0.862777081747325,
124.948737201585));
#154518=CARTESIAN_POINT('Ctrl Pts',(-68.0906349307642,0.70648879583477,
124.929941144643));
#154519=CARTESIAN_POINT('Ctrl Pts',(-68.0980431504307,0.550028654885474,
124.911124419503));
#154520=CARTESIAN_POINT('Ctrl Pts',(-68.1054513700972,0.392918643326962,
124.898575075148));
#154521=CARTESIAN_POINT('Ctrl Pts',(-68.1128595897637,0.235698786277303,
124.892307112679));
#154522=CARTESIAN_POINT('Ctrl Pts',(-68.1202723690658,0.0783821630289842,
124.886035292383));
#154523=CARTESIAN_POINT('Ctrl Pts',(-68.1276851483679,-0.0790440679956438,
124.886052557593));
#154524=CARTESIAN_POINT('Ctrl Pts',(-68.13509792767,-0.236042169595822,
124.892320812501));
#154525=CARTESIAN_POINT('Ctrl Pts',(-68.1425212986987,-0.393264597446046,
124.898598023786));
#154526=CARTESIAN_POINT('Ctrl Pts',(-68.1499446697275,-0.550057302984203,
124.911144033695));
#154527=CARTESIAN_POINT('Ctrl Pts',(-68.1573680407563,-0.705889110011352,
124.929869054301));
#154528=CARTESIAN_POINT('Ctrl Pts',(-68.1613040901969,-0.788514873226247,
124.939797509527));
#154529=CARTESIAN_POINT('Ctrl Pts',(-68.1652401396375,-0.870870675056604,
124.951462254279));
#154530=CARTESIAN_POINT('Ctrl Pts',(-68.1691761890781,-0.952878879620812,
124.964844164702));
#154531=CARTESIAN_POINT('Ctrl Pts',(-68.1765994554835,-1.10754379404624,
124.990082030125));
#154532=CARTESIAN_POINT('Ctrl Pts',(-68.184022721889,-1.26143921531752,
125.021506964069));
#154533=CARTESIAN_POINT('Ctrl Pts',(-68.1914459882944,-1.41403104590956,
125.059062821655));
#154534=CARTESIAN_POINT('Ctrl Pts',(-68.1988604810154,-1.56644252563046,
125.096574291335));
#154535=CARTESIAN_POINT('Ctrl Pts',(-68.2062749737363,-1.71755312257445,
125.140202172629));
#154536=CARTESIAN_POINT('Ctrl Pts',(-68.2136894664573,-1.86683561306241,
125.189838789636));
#154537=CARTESIAN_POINT('Ctrl Pts',(-68.2210968128109,-2.01597421946437,
125.239427565002));
#154538=CARTESIAN_POINT('Ctrl Pts',(-68.2285041591646,-2.16328787534932,
125.295013429462));
#154539=CARTESIAN_POINT('Ctrl Pts',(-68.2359115055183,-2.30826138974307,
125.356438085158));
#154540=CARTESIAN_POINT('Ctrl Pts',(-68.2433133271937,-2.45312677742169,
125.417816928029));
#154541=CARTESIAN_POINT('Ctrl Pts',(-68.2507151488692,-2.5956551566285,
125.485025746154));
#154542=CARTESIAN_POINT('Ctrl Pts',(-68.2581169705446,-2.7353484081873,
125.557857053446));
#154543=CARTESIAN_POINT('Ctrl Pts',(-68.2655148848559,-2.87496791676578,
125.630649913657));
#154544=CARTESIAN_POINT('Ctrl Pts',(-68.2729127991672,-3.01175494815713,
125.709059179844));
#154545=CARTESIAN_POINT('Ctrl Pts',(-68.2803107134786,-3.14523332078233,
125.792830120768));
#154546=CARTESIAN_POINT('Ctrl Pts',(-68.2877073983907,-3.27868951172316,
125.87658714048));
#154547=CARTESIAN_POINT('Ctrl Pts',(-68.2951040833029,-3.4088378192892,
125.965703868289));
#154548=CARTESIAN_POINT('Ctrl Pts',(-68.3025007682151,-3.53522844844189,
126.059880627111));
#154549=CARTESIAN_POINT('Ctrl Pts',(-68.3098971251504,-3.66161347330128,
126.154053210037));
#154550=CARTESIAN_POINT('Ctrl Pts',(-68.3172934820858,-3.78424085170587,
126.253285154815));
#154551=CARTESIAN_POINT('Ctrl Pts',(-68.3246898390212,-3.9026916931995,
126.357234791785));
#154552=CARTESIAN_POINT('Ctrl Pts',(-68.3320873283577,-4.02116066981935,
126.461200343709));
#154553=CARTESIAN_POINT('Ctrl Pts',(-68.3394848176942,-4.13545155572639,
126.56988477976));
#154554=CARTESIAN_POINT('Ctrl Pts',(-68.3468823070307,-4.24518044972245,
126.682907777633));
#154555=CARTESIAN_POINT('Ctrl Pts',(-68.3542823895456,-4.35494780901156,
126.795970395542));
#154556=CARTESIAN_POINT('Ctrl Pts',(-68.3616824720604,-4.46014973252857,
126.913374335658));
#154557=CARTESIAN_POINT('Ctrl Pts',(-68.3690825545753,-4.56044102365434,
127.034704369011));
#154558=CARTESIAN_POINT('Ctrl Pts',(-68.3764907742417,-4.66084259536575,
127.156167817209));
#154559=CARTESIAN_POINT('Ctrl Pts',(-68.3838989939082,-4.75632251306026,
127.28156569236));
#154560=CARTESIAN_POINT('Ctrl Pts',(-68.3913072135746,-4.84657710044748,
127.410451223973));
#154561=CARTESIAN_POINT('Ctrl Pts',(-68.3987199928767,-4.93688723802791,
127.539416082482));
#154562=CARTESIAN_POINT('Ctrl Pts',(-68.4061327721787,-5.02196543553689,
127.671872561452));
#154563=CARTESIAN_POINT('Ctrl Pts',(-68.4135455514808,-5.10155308396407,
127.807347655633));
#154564=CARTESIAN_POINT('Ctrl Pts',(-68.4209689225095,-5.18125445095527,
127.943016322981));
#154565=CARTESIAN_POINT('Ctrl Pts',(-68.4283922935382,-5.25544942471556,
128.081711891558));
#154566=CARTESIAN_POINT('Ctrl Pts',(-68.4358156645669,-5.32392643266154,
128.222938935216));
#154567=CARTESIAN_POINT('Ctrl Pts',(-68.4397517140082,-5.36023458536214,
128.297820902469));
#154568=CARTESIAN_POINT('Ctrl Pts',(-68.4436877634495,-5.39493602778715,
128.373414250463));
#154569=CARTESIAN_POINT('Ctrl Pts',(-68.4476238128907,-5.42800488528706,
128.449643325023));
#154570=CARTESIAN_POINT('Ctrl Pts',(-68.4558328600923,-5.49697348341427,
128.608627118429));
#154571=CARTESIAN_POINT('Ctrl Pts',(-68.464041907294,-5.55901664151482,
128.770788760264));
#154572=CARTESIAN_POINT('Ctrl Pts',(-68.4722509544957,-5.61386054495428,
128.935537366345));
#154573=CARTESIAN_POINT('Ctrl Pts',(-68.4804279058865,-5.66849001917829,
129.099641836758));
#154574=CARTESIAN_POINT('Ctrl Pts',(-68.4886048572773,-5.71597630648745,
129.266312870272));
#154575=CARTESIAN_POINT('Ctrl Pts',(-68.4967818086681,-5.75609457352925,
129.434942557554));
#154576=CARTESIAN_POINT('Ctrl Pts',(-68.5049382975006,-5.79611244589609,
129.603150254459));
#154577=CARTESIAN_POINT('Ctrl Pts',(-68.5130947863331,-5.82879901029771,
129.773306600435));
#154578=CARTESIAN_POINT('Ctrl Pts',(-68.5212512751656,-5.85397853701506,
129.944787554548));
#154579=CARTESIAN_POINT('Ctrl Pts',(-68.5293741259582,-5.87905422126489,
130.115561306908));
#154580=CARTESIAN_POINT('Ctrl Pts',(-68.5374969767507,-5.89668456597095,
130.287648538314));
#154581=CARTESIAN_POINT('Ctrl Pts',(-68.5456198275432,-5.90674465531011,
130.460415651815));
#154582=CARTESIAN_POINT('Ctrl Pts',(-68.550954801205,-5.91335197988504,
130.573886651554));
#154583=CARTESIAN_POINT('Ctrl Pts',(-68.5562897748668,-5.91669473803662,
130.687650583833));
#154584=CARTESIAN_POINT('Ctrl Pts',(-68.5616247485286,-5.91674932031565,
130.801524591425));
#154585=CARTESIAN_POINT('',(-70.3116248421866,-5.91520845600957,130.809408030844));
#154586=CARTESIAN_POINT('Ctrl Pts',(-68.561624807788,-5.90824422428163,
130.801529931163));
#154587=CARTESIAN_POINT('Ctrl Pts',(-68.61644035076,-5.9032143751984,131.969878185027));
#154588=CARTESIAN_POINT('Ctrl Pts',(-68.7640717683365,-5.00169773296238,
135.123678078319));
#154589=CARTESIAN_POINT('Ctrl Pts',(-69.0045190605167,0.135532838237384,
137.801445108984));
#154590=CARTESIAN_POINT('Ctrl Pts',(-69.2829666843298,5.96010416000349,
134.472428083174));
#154591=CARTESIAN_POINT('Ctrl Pts',(-69.5614143081424,6.30763092600427,
127.772636251522));
#154592=CARTESIAN_POINT('Ctrl Pts',(-69.8398619319555,0.858753015907526,
123.858851004297));
#154593=CARTESIAN_POINT('Ctrl Pts',(-70.0899320985043,-4.74354006348326,
126.076046876634));
#154594=CARTESIAN_POINT('Ctrl Pts',(-70.2471863904481,-5.9015201675211,
129.438471216138));
#154595=CARTESIAN_POINT('Ctrl Pts',(-70.311624807788,-5.91256097363447,
130.809405039745));
#154596=CARTESIAN_POINT('',(-72.061624807788,-5.92102598959136,130.805130248854));
#154597=CARTESIAN_POINT('Ctrl Pts',(-70.3116248621877,-5.91674784561244,
130.809409770031));
#154598=CARTESIAN_POINT('Ctrl Pts',(-70.3204841076535,-5.91658688933848,
130.998023145018));
#154599=CARTESIAN_POINT('Ctrl Pts',(-70.3293433531193,-5.90740330510671,
131.186244603552));
#154600=CARTESIAN_POINT('Ctrl Pts',(-70.338202598585,-5.88933200357266,
131.373306233767));
#154601=CARTESIAN_POINT('Ctrl Pts',(-70.3471311539176,-5.87111932210882,
131.561831331354));
#154602=CARTESIAN_POINT('Ctrl Pts',(-70.3560597092502,-5.84387940990915,
131.749178369704));
#154603=CARTESIAN_POINT('Ctrl Pts',(-70.3649882645828,-5.80779893960273,
131.934582737173));
#154604=CARTESIAN_POINT('Ctrl Pts',(-70.3739910897327,-5.77141834348192,
132.121529341657));
#154605=CARTESIAN_POINT('Ctrl Pts',(-70.3829939148826,-5.72604955131969,
132.306500814378));
#154606=CARTESIAN_POINT('Ctrl Pts',(-70.3919967400325,-5.671932023571,132.488735184724));
#154607=CARTESIAN_POINT('Ctrl Pts',(-70.3935835532154,-5.66239341707536,
132.520855313286));
#154608=CARTESIAN_POINT('Ctrl Pts',(-70.3951703663982,-5.65258313575233,
132.552890463939));
#154609=CARTESIAN_POINT('Ctrl Pts',(-70.3967571795811,-5.64250264266975,
132.584836534271));
#154610=CARTESIAN_POINT('Ctrl Pts',(-70.4041804459868,-5.59534511558212,
132.734283358413));
#154611=CARTESIAN_POINT('Ctrl Pts',(-70.4116037123924,-5.54217482691998,
132.882081354229));
#154612=CARTESIAN_POINT('Ctrl Pts',(-70.4190269787981,-5.48312393628243,
133.027709996739));
#154613=CARTESIAN_POINT('Ctrl Pts',(-70.4264414715193,-5.42414283889365,
133.173166518287));
#154614=CARTESIAN_POINT('Ctrl Pts',(-70.4338559642406,-5.35929511321063,
133.316458447614));
#154615=CARTESIAN_POINT('Ctrl Pts',(-70.4412704569618,-5.28876293141317,
133.457079452612));
#154616=CARTESIAN_POINT('Ctrl Pts',(-70.4486778033158,-5.21829873118802,
133.597564921792));
#154617=CARTESIAN_POINT('Ctrl Pts',(-70.4560851496698,-5.14216114848641,
133.735384260204));
#154618=CARTESIAN_POINT('Ctrl Pts',(-70.4634924960238,-5.0605807285695,
133.870050303775));
#154619=CARTESIAN_POINT('Ctrl Pts',(-70.4708943176995,-4.9790611544075,
134.004615908331));
#154620=CARTESIAN_POINT('Ctrl Pts',(-70.4782961393752,-4.89210701857658,
134.136032582983));
#154621=CARTESIAN_POINT('Ctrl Pts',(-70.4856979610508,-4.79999509785458,
134.263837113088));
#154622=CARTESIAN_POINT('Ctrl Pts',(-70.4930958753624,-4.70793180229853,
134.391574176177));
#154623=CARTESIAN_POINT('Ctrl Pts',(-70.500493789674,-4.61071636205924,
134.515702590174));
#154624=CARTESIAN_POINT('Ctrl Pts',(-70.5078917039855,-4.50866916463,134.635787626712));
#154625=CARTESIAN_POINT('Ctrl Pts',(-70.5152883888979,-4.40663892559379,
134.755852707296));
#154626=CARTESIAN_POINT('Ctrl Pts',(-70.5226850738102,-4.29977876448117,
134.871875459832));
#154627=CARTESIAN_POINT('Ctrl Pts',(-70.5300817587226,-4.18844976593796,
134.983453715442));
#154628=CARTESIAN_POINT('Ctrl Pts',(-70.5374781156583,-4.07712570383905,
135.095027023555));
#154629=CARTESIAN_POINT('Ctrl Pts',(-70.544874472594,-3.96133346197043,
135.202155962333));
#154630=CARTESIAN_POINT('Ctrl Pts',(-70.5522708295296,-3.8414712514578,
135.304474970193));
#154631=CARTESIAN_POINT('Ctrl Pts',(-70.5596683188664,-3.72159068973457,
135.406809643356));
#154632=CARTESIAN_POINT('Ctrl Pts',(-70.5670658082032,-3.59763920258552,
135.504332676924));
#154633=CARTESIAN_POINT('Ctrl Pts',(-70.57446329754,-3.47004823641974,135.596718680088));
#154634=CARTESIAN_POINT('Ctrl Pts',(-70.5818633800552,-3.34241254343875,
135.689137069022));
#154635=CARTESIAN_POINT('Ctrl Pts',(-70.5892634625704,-3.21113513347473,
135.776414623421));
#154636=CARTESIAN_POINT('Ctrl Pts',(-70.5966635450856,-3.07667644815211,
135.85826926295));
#154637=CARTESIAN_POINT('Ctrl Pts',(-70.6040717647522,-2.9420699116821,
135.94021391007));
#154638=CARTESIAN_POINT('Ctrl Pts',(-70.611479984419,-2.80427543289505,
136.016723539482));
#154639=CARTESIAN_POINT('Ctrl Pts',(-70.6188882040856,-2.66377871445692,
136.087561685376));
#154640=CARTESIAN_POINT('Ctrl Pts',(-70.6263009833879,-2.52319552263271,
136.158443430966));
#154641=CARTESIAN_POINT('Ctrl Pts',(-70.6337137626902,-2.37990711604169,
136.223646583119));
#154642=CARTESIAN_POINT('Ctrl Pts',(-70.6411265419925,-2.23441869782084,
136.282983039793));
#154643=CARTESIAN_POINT('Ctrl Pts',(-70.6485499130215,-2.08872239892553,
136.342404279179));
#154644=CARTESIAN_POINT('Ctrl Pts',(-70.6559732840504,-1.94082016024555,
136.395941954412));
#154645=CARTESIAN_POINT('Ctrl Pts',(-70.6633966550793,-1.79123262855091,
136.443457729065));
#154646=CARTESIAN_POINT('Ctrl Pts',(-70.6673327045175,-1.71191772999733,
136.468651732894));
#154647=CARTESIAN_POINT('Ctrl Pts',(-70.6712687539558,-1.63212922277147,
136.492153615189));
#154648=CARTESIAN_POINT('Ctrl Pts',(-70.675204803394,-1.55194568972767,
136.513948618345));
#154649=CARTESIAN_POINT('Ctrl Pts',(-70.6826280697994,-1.4007220487503,
136.555053314124));
#154650=CARTESIAN_POINT('Ctrl Pts',(-70.6900513362048,-1.24763556924053,
136.590208071316));
#154651=CARTESIAN_POINT('Ctrl Pts',(-70.6974746026102,-1.09319561909706,
136.619242723068));
#154652=CARTESIAN_POINT('Ctrl Pts',(-70.7048890953312,-0.938938204148988,
136.648243058273));
#154653=CARTESIAN_POINT('Ctrl Pts',(-70.7123035880522,-0.783330866047083,
136.671137617974));
#154654=CARTESIAN_POINT('Ctrl Pts',(-70.7197180807732,-0.626898064847358,
136.687805983913));
#154655=CARTESIAN_POINT('Ctrl Pts',(-70.727125427127,-0.470616039471021,
136.704458284254));
#154656=CARTESIAN_POINT('Ctrl Pts',(-70.7345327734807,-0.313510503609283,
136.714896298435));
#154657=CARTESIAN_POINT('Ctrl Pts',(-70.7419401198345,-0.156115937539085,
136.719050666634));
#154658=CARTESIAN_POINT('Ctrl Pts',(-70.7493419415099,0.00116123772535637,
136.723201936348));
#154659=CARTESIAN_POINT('Ctrl Pts',(-70.7567437631853,0.158726642408166,
136.721078881886));
#154660=CARTESIAN_POINT('Ctrl Pts',(-70.7641455848607,0.316040956301952,
136.712663984561));
#154661=CARTESIAN_POINT('Ctrl Pts',(-70.7715434991721,0.473272225193966,
136.704253529394));
#154662=CARTESIAN_POINT('Ctrl Pts',(-70.7789414134834,0.630252295452986,
136.689557866009));
#154663=CARTESIAN_POINT('Ctrl Pts',(-70.7863393277948,0.786442240524691,
136.668611564176));
#154664=CARTESIAN_POINT('Ctrl Pts',(-70.793736012707,0.942606229661098,
136.647668743239));
#154665=CARTESIAN_POINT('Ctrl Pts',(-70.8011326976192,1.09797998458732,
136.62047739502));
#154666=CARTESIAN_POINT('Ctrl Pts',(-70.8085293825314,1.25202997416255,
136.587123928155));
#154667=CARTESIAN_POINT('Ctrl Pts',(-70.8159257394668,1.40607313300003,
136.553771940218));
#154668=CARTESIAN_POINT('Ctrl Pts',(-70.8233220964023,1.55879227835214,
136.51425845591));
#154669=CARTESIAN_POINT('Ctrl Pts',(-70.8307184533377,1.70966461006603,
136.468720906565));
#154670=CARTESIAN_POINT('Ctrl Pts',(-70.8381159426743,1.86056004071886,
136.423176385305));
#154671=CARTESIAN_POINT('Ctrl Pts',(-70.8455134320108,2.00960773733972,
136.371606070458));
#154672=CARTESIAN_POINT('Ctrl Pts',(-70.8529109213474,2.15630073210085,
136.314197068427));
#154673=CARTESIAN_POINT('Ctrl Pts',(-70.8603110038624,2.3030451498641,136.25676794176));
#154674=CARTESIAN_POINT('Ctrl Pts',(-70.8677110863775,2.44743287492025,
136.193496188818));
#154675=CARTESIAN_POINT('Ctrl Pts',(-70.8751111688925,2.58897770515041,
136.124616720869));
#154676=CARTESIAN_POINT('Ctrl Pts',(-70.882519388559,2.73067817847258,136.055661512865));
#154677=CARTESIAN_POINT('Ctrl Pts',(-70.8899276082255,2.8695291781614,135.981086438873));
#154678=CARTESIAN_POINT('Ctrl Pts',(-70.8973358278919,3.00506922467902,
135.901172318756));
#154679=CARTESIAN_POINT('Ctrl Pts',(-70.904748607194,3.14069269383387,135.821209012832));
#154680=CARTESIAN_POINT('Ctrl Pts',(-70.912161386496,3.27300083616388,135.735900314648));
#154681=CARTESIAN_POINT('Ctrl Pts',(-70.9195741657981,3.40156232145845,
135.645569592165));
#154682=CARTESIAN_POINT('Ctrl Pts',(-70.9269975368269,3.53030750143197,
135.555109800909));
#154683=CARTESIAN_POINT('Ctrl Pts',(-70.9344209078556,3.65529503658982,
135.459613879899));
#154684=CARTESIAN_POINT('Ctrl Pts',(-70.9418442788844,3.7761271182807,135.359445089789));
#154685=CARTESIAN_POINT('Ctrl Pts',(-70.9457803283253,3.84019518732119,
135.306333193754));
#154686=CARTESIAN_POINT('Ctrl Pts',(-70.9497163777662,3.90309562364617,
135.251908204306));
#154687=CARTESIAN_POINT('Ctrl Pts',(-70.9536524272071,3.96477353531171,
135.196228258581));
#154688=CARTESIAN_POINT('Ctrl Pts',(-70.9610756936125,4.08109615180713,
135.091217618658));
#154689=CARTESIAN_POINT('Ctrl Pts',(-70.9684989600179,4.1934198261867,134.981423632777));
#154690=CARTESIAN_POINT('Ctrl Pts',(-70.9759222264233,4.30132606646703,
134.867182867238));
#154691=CARTESIAN_POINT('Ctrl Pts',(-70.9833367191443,4.40910477053255,
134.753077124797));
#154692=CARTESIAN_POINT('Ctrl Pts',(-70.9907512118652,4.51247617918092,
134.634535332972));
#154693=CARTESIAN_POINT('Ctrl Pts',(-70.9981657045862,4.61105549765007,
134.511933645854));
#154694=CARTESIAN_POINT('Ctrl Pts',(-71.0055730509399,4.70953980166063,
134.389450126858));
#154695=CARTESIAN_POINT('Ctrl Pts',(-71.0129803972937,4.80324097826053,
134.262914791706));
#154696=CARTESIAN_POINT('Ctrl Pts',(-71.0203877436475,4.8918117734207,134.132739823114));
#154697=CARTESIAN_POINT('Ctrl Pts',(-71.0277895653228,4.98031650914026,
134.002661943924));
#154698=CARTESIAN_POINT('Ctrl Pts',(-71.0351913869981,5.06369827327327,
133.868950143686));
#154699=CARTESIAN_POINT('Ctrl Pts',(-71.0425932086735,5.14165081110609,
133.732048698484));
#154700=CARTESIAN_POINT('Ctrl Pts',(-71.0499911229848,5.21956219840097,
133.595219522491));
#154701=CARTESIAN_POINT('Ctrl Pts',(-71.0573890372961,5.29204988301889,
133.455204378455));
#154702=CARTESIAN_POINT('Ctrl Pts',(-71.0647869516075,5.35885164651987,
133.312475366355));
#154703=CARTESIAN_POINT('Ctrl Pts',(-71.0721836365196,5.42564230877956,
133.169770073227));
#154704=CARTESIAN_POINT('Ctrl Pts',(-71.0795803214317,5.48674876717679,
133.024352144898));
#154705=CARTESIAN_POINT('Ctrl Pts',(-71.0869770063439,5.5419553331297,132.876717162202));
#154706=CARTESIAN_POINT('Ctrl Pts',(-71.0943733632793,5.5971594511657,132.729088725796));
#154707=CARTESIAN_POINT('Ctrl Pts',(-71.1017697202147,5.64646406617286,
132.579243780142));
#154708=CARTESIAN_POINT('Ctrl Pts',(-71.1091660771501,5.68970221677142,
132.427696456808));
#154709=CARTESIAN_POINT('Ctrl Pts',(-71.1165635664867,5.73294698724122,
132.276125931191));
#154710=CARTESIAN_POINT('Ctrl Pts',(-71.1239610558232,5.77012334153,132.122852867925));
#154711=CARTESIAN_POINT('Ctrl Pts',(-71.1313585451597,5.80111466905825,
131.968404928981));
#154712=CARTESIAN_POINT('Ctrl Pts',(-71.1387586276746,5.83211686054832,
131.813902848551));
#154713=CARTESIAN_POINT('Ctrl Pts',(-71.1461587101896,5.85692963510831,
131.658225438225));
#154714=CARTESIAN_POINT('Ctrl Pts',(-71.1535587927045,5.87548782611979,
131.501908728895));
#154715=CARTESIAN_POINT('Ctrl Pts',(-71.1609670123709,5.8940664237701,131.345420133272));
#154716=CARTESIAN_POINT('Ctrl Pts',(-71.1683752320374,5.90637665890132,
131.18829120568));
#154717=CARTESIAN_POINT('Ctrl Pts',(-71.1757834517039,5.91240535225445,
131.031061991918));
#154718=CARTESIAN_POINT('Ctrl Pts',(-71.1831962310059,5.91843775616775,
130.873736006198));
#154719=CARTESIAN_POINT('Ctrl Pts',(-71.1906090103079,5.91818091505398,
130.716309983746));
#154720=CARTESIAN_POINT('Ctrl Pts',(-71.1980217896099,5.91167374302079,
130.559321603165));
#154721=CARTESIAN_POINT('Ctrl Pts',(-71.2054451606386,5.90515727323503,
130.402108910224));
#154722=CARTESIAN_POINT('Ctrl Pts',(-71.2128685316673,5.89237266604779,
130.245335479142));
#154723=CARTESIAN_POINT('Ctrl Pts',(-71.220291902696,5.87341051764293,130.08953234886));
#154724=CARTESIAN_POINT('Ctrl Pts',(-71.2242279521373,5.8633563315669,130.006921790729));
#154725=CARTESIAN_POINT('Ctrl Pts',(-71.2281640015786,5.85156626881008,
129.924583836008));
#154726=CARTESIAN_POINT('Ctrl Pts',(-71.2321000510199,5.83805957135399,
129.842596091384));
#154727=CARTESIAN_POINT('Ctrl Pts',(-71.2395233174253,5.81258636148441,
129.687969763792));
#154728=CARTESIAN_POINT('Ctrl Pts',(-71.2469465838308,5.78092726129591,
129.534122344127));
#154729=CARTESIAN_POINT('Ctrl Pts',(-71.2543698502362,5.74313922840864,
129.381587843855));
#154730=CARTESIAN_POINT('Ctrl Pts',(-71.2617843429573,5.70539585783808,
129.229233626694));
#154731=CARTESIAN_POINT('Ctrl Pts',(-71.2691988356783,5.66153806245929,
129.078189598941));
#154732=CARTESIAN_POINT('Ctrl Pts',(-71.2766133283993,5.61167432039221,
128.928982819801));
#154733=CARTESIAN_POINT('Ctrl Pts',(-71.2840206747531,5.56185863887714,
128.779919851772));
#154734=CARTESIAN_POINT('Ctrl Pts',(-71.2914280211068,5.50604865247688,
128.632690958695));
#154735=CARTESIAN_POINT('Ctrl Pts',(-71.2988353674606,5.44440344289867,
128.487811090046));
#154736=CARTESIAN_POINT('Ctrl Pts',(-71.306237189136,5.38280421064341,128.343039278269));
#154737=CARTESIAN_POINT('Ctrl Pts',(-71.3136390108115,5.31537856641355,
128.200613344487));
#154738=CARTESIAN_POINT('Ctrl Pts',(-71.321040832487,5.24233475410965,128.061031091542));
#154739=CARTESIAN_POINT('Ctrl Pts',(-71.3284387467984,5.16932950106569,
127.921522522982));
#154740=CARTESIAN_POINT('Ctrl Pts',(-71.3358366611097,5.09071215909823,
127.784854975543));
#154741=CARTESIAN_POINT('Ctrl Pts',(-71.3432345754211,5.00673818381789,
127.651504242594));
#154742=CARTESIAN_POINT('Ctrl Pts',(-71.3506312603333,4.92277816348892,
127.518175670119));
#154743=CARTESIAN_POINT('Ctrl Pts',(-71.3580279452456,4.83346347530592,
127.388163133751));
#154744=CARTESIAN_POINT('Ctrl Pts',(-71.3654246301578,4.73909448051574,
127.261915971951));
#154745=CARTESIAN_POINT('Ctrl Pts',(-71.3728209870933,4.64472967014569,
127.135674408083));
#154746=CARTESIAN_POINT('Ctrl Pts',(-71.3802173440287,4.54531122228001,
127.013198185805));
#154747=CARTESIAN_POINT('Ctrl Pts',(-71.3876137009642,4.4411814436635,126.894905675127));
#154748=CARTESIAN_POINT('Ctrl Pts',(-71.3950111903008,4.33703572251192,
126.776595053563));
#154749=CARTESIAN_POINT('Ctrl Pts',(-71.4024086796374,4.22817748104193,
126.662469699213));
#154750=CARTESIAN_POINT('Ctrl Pts',(-71.4098061689741,4.11498762534811,
126.552912934043));
#154751=CARTESIAN_POINT('Ctrl Pts',(-71.4172062514891,4.00175809112585,
126.443317763919));
#154752=CARTESIAN_POINT('Ctrl Pts',(-71.424606334004,3.88419418753936,126.338294631034));
#154753=CARTESIAN_POINT('Ctrl Pts',(-71.432006416519,3.76271166840945,126.2381880997));
#154754=CARTESIAN_POINT('Ctrl Pts',(-71.4394146361855,3.64109556676105,
126.137971490943));
#154755=CARTESIAN_POINT('Ctrl Pts',(-71.4468228558521,3.51555253263624,
126.042682518032));
#154756=CARTESIAN_POINT('Ctrl Pts',(-71.4542310755186,3.38652979815007,
125.952624176997));
#154757=CARTESIAN_POINT('Ctrl Pts',(-71.4616438548207,3.25742765232351,
125.862510406556));
#154758=CARTESIAN_POINT('Ctrl Pts',(-71.4690566341228,3.12484185220072,
125.77763388378));
#154759=CARTESIAN_POINT('Ctrl Pts',(-71.4764694134249,2.98924579604377,
125.698252497546));
#154760=CARTESIAN_POINT('Ctrl Pts',(-71.4838927844536,2.85345599388315,
125.618757687465));
#154761=CARTESIAN_POINT('Ctrl Pts',(-71.4913161554824,2.71464767379158,
125.544773870667));
#154762=CARTESIAN_POINT('Ctrl Pts',(-71.4987395265112,2.57331658332102,
125.476511865536));
#154763=CARTESIAN_POINT('Ctrl Pts',(-71.5026755759517,2.49837944796581,
125.440317712494));
#154764=CARTESIAN_POINT('Ctrl Pts',(-71.5066116253922,2.42273337783236,
125.405731350467));
#154765=CARTESIAN_POINT('Ctrl Pts',(-71.5105476748328,2.34645406638664,
125.372778538941));
#154766=CARTESIAN_POINT('Ctrl Pts',(-71.5179709412382,2.20259366558696,
125.310630564822));
#154767=CARTESIAN_POINT('Ctrl Pts',(-71.5253942076436,2.05604495727097,
125.254107974183));
#154768=CARTESIAN_POINT('Ctrl Pts',(-71.532817474049,1.90728800739199,125.203451493204));
#154769=CARTESIAN_POINT('Ctrl Pts',(-71.5402319667699,1.75870687587426,
125.15285488398));
#154770=CARTESIAN_POINT('Ctrl Pts',(-71.5476464594908,1.60792304784986,
125.108110702893));
#154771=CARTESIAN_POINT('Ctrl Pts',(-71.5550609522118,1.45543858822795,
125.069412572605));
#154772=CARTESIAN_POINT('Ctrl Pts',(-71.5624682985656,1.30310109886895,
125.030751741032));
#154773=CARTESIAN_POINT('Ctrl Pts',(-71.5698756449194,1.14906660050176,
124.998125450238));
#154774=CARTESIAN_POINT('Ctrl Pts',(-71.5772829912731,0.993854322252511,
124.971678203047));
#154775=CARTESIAN_POINT('Ctrl Pts',(-71.5846848129485,0.838757807176206,
124.94525068121));
#154776=CARTESIAN_POINT('Ctrl Pts',(-71.5920866346238,0.682485627705961,
124.924993089139));
#154777=CARTESIAN_POINT('Ctrl Pts',(-71.5994884562992,0.52556916038521,
124.910999299935));
#154778=CARTESIAN_POINT('Ctrl Pts',(-71.6068863706105,0.368735528046346,
124.897012897943));
#154779=CARTESIAN_POINT('Ctrl Pts',(-71.6142842849218,0.211258656092448,
124.889283746618));
#154780=CARTESIAN_POINT('Ctrl Pts',(-71.6216821992331,0.0536769229582773,
124.887854101856));
#154781=CARTESIAN_POINT('Ctrl Pts',(-71.6290788841453,-0.103878622950895,
124.886424694675));
#154782=CARTESIAN_POINT('Ctrl Pts',(-71.6364755690574,-0.261538622537786,
124.891292719726));
#154783=CARTESIAN_POINT('Ctrl Pts',(-71.6438722539696,-0.418762682039236,
124.902448353));
#154784=CARTESIAN_POINT('Ctrl Pts',(-71.651268610905,-0.575979770061128,
124.913603491622));
#154785=CARTESIAN_POINT('Ctrl Pts',(-71.6586649678404,-0.732760584070799,
124.931045657698));
#154786=CARTESIAN_POINT('Ctrl Pts',(-71.6660613247758,-0.888568112374757,
124.954712998079));
#154787=CARTESIAN_POINT('Ctrl Pts',(-71.6734588141123,-1.04439949520928,
124.97838396199));
#154788=CARTESIAN_POINT('Ctrl Pts',(-71.6808563034489,-1.19925692654631,
125.00828194187));
#154789=CARTESIAN_POINT('Ctrl Pts',(-71.6882537927854,-1.35261201770984,
125.04429366552));
#154790=CARTESIAN_POINT('Ctrl Pts',(-71.6956538753004,-1.5060208672624,
125.080318013025));
#154791=CARTESIAN_POINT('Ctrl Pts',(-71.7030539578153,-1.65792596491327,
125.122460286036));
#154792=CARTESIAN_POINT('Ctrl Pts',(-71.7104540403303,-1.80781269385303,
125.170556944518));
#154793=CARTESIAN_POINT('Ctrl Pts',(-71.7178622599967,-1.95786423866042,
125.218706490221));
#154794=CARTESIAN_POINT('Ctrl Pts',(-71.7252704796631,-2.10589262679697,
125.272823382971));
#154795=CARTESIAN_POINT('Ctrl Pts',(-71.7326786993295,-2.25140119923883,
125.33269513048));
#154796=CARTESIAN_POINT('Ctrl Pts',(-71.7400914786316,-2.39699932977909,
125.392603728051));
#154797=CARTESIAN_POINT('Ctrl Pts',(-71.7475042579336,-2.54007421577242,
125.458274082932));
#154798=CARTESIAN_POINT('Ctrl Pts',(-71.7549170372357,-2.68015300467841,
125.529447306997));
#154799=CARTESIAN_POINT('Ctrl Pts',(-71.7623404082644,-2.82043194472722,
125.600722226703));
#154800=CARTESIAN_POINT('Ctrl Pts',(-71.7697637792931,-2.95770591272066,
125.677515537516));
#154801=CARTESIAN_POINT('Ctrl Pts',(-71.7771871503218,-3.09152957752034,
125.759524105466));
#154802=CARTESIAN_POINT('Ctrl Pts',(-71.781123199763,-3.16248609566007,
125.803007015967));
#154803=CARTESIAN_POINT('Ctrl Pts',(-71.7850592492042,-3.23247313024798,
125.847955423691));
#154804=CARTESIAN_POINT('Ctrl Pts',(-71.7889952986454,-3.30142809493104,
125.894319569214));
#154805=CARTESIAN_POINT('Ctrl Pts',(-71.7963922461212,-3.43101392955234,
125.981450880523));
#154806=CARTESIAN_POINT('Ctrl Pts',(-71.8037891935969,-3.55735086442155,
126.073852199481));
#154807=CARTESIAN_POINT('Ctrl Pts',(-71.8111861410727,-3.67997876379524,
126.171252928281));
#154808=CARTESIAN_POINT('Ctrl Pts',(-71.8185743296968,-3.80246145738337,
126.268538323217));
#154809=CARTESIAN_POINT('Ctrl Pts',(-71.8259625183209,-3.9212435648374,
126.37081111428));
#154810=CARTESIAN_POINT('Ctrl Pts',(-71.8333507069451,-4.03589253330437,
126.477756634981));
#154811=CARTESIAN_POINT('Ctrl Pts',(-71.8407317889035,-4.15043122143831,
126.584599285262));
#154812=CARTESIAN_POINT('Ctrl Pts',(-71.8481128708618,-4.26084441107513,
126.696105463363));
#154813=CARTESIAN_POINT('Ctrl Pts',(-71.8554939528202,-4.36673148392284,
126.811919420777));
#154814=CARTESIAN_POINT('Ctrl Pts',(-71.8628695744455,-4.47254022426022,
126.927647702029));
#154815=CARTESIAN_POINT('Ctrl Pts',(-71.870245196071,-4.5738292611642,127.047677141507));
#154816=CARTESIAN_POINT('Ctrl Pts',(-71.8776208176963,-4.67023393119619,
127.17161432992));
#154817=CARTESIAN_POINT('Ctrl Pts',(-71.8852876506168,-4.77044494193312,
127.300444924067));
#154818=CARTESIAN_POINT('Ctrl Pts',(-71.8929544835373,-4.86537769775476,
127.433497869516));
#154819=CARTESIAN_POINT('Ctrl Pts',(-71.9006213164578,-4.95466745374232,
127.570291820319));
#154820=CARTESIAN_POINT('Ctrl Pts',(-71.9079919684677,-5.04050781654442,
127.701801221775));
#154821=CARTESIAN_POINT('Ctrl Pts',(-71.9153626204778,-5.12113281117333,
127.836767641905));
#154822=CARTESIAN_POINT('Ctrl Pts',(-71.9227332724877,-5.19626186138799,
127.974732862828));
#154823=CARTESIAN_POINT('Ctrl Pts',(-71.9301037804294,-5.27138944311522,
128.112695387055));
#154824=CARTESIAN_POINT('Ctrl Pts',(-71.937474288371,-5.34102111385726,
128.253656265171));
#154825=CARTESIAN_POINT('Ctrl Pts',(-71.9448447963127,-5.40492200940477,
128.397132204068));
#154826=CARTESIAN_POINT('Ctrl Pts',(-71.9522166426895,-5.46883450892819,
128.540634197237));
#154827=CARTESIAN_POINT('Ctrl Pts',(-71.9595884890663,-5.52701400855252,
128.686651816637));
#154828=CARTESIAN_POINT('Ctrl Pts',(-71.966960335443,-5.57927366816981,
128.834681481725));
#154829=CARTESIAN_POINT('Ctrl Pts',(-71.9743350033206,-5.6315533296523,
128.982767803696));
#154830=CARTESIAN_POINT('Ctrl Pts',(-71.9817096711983,-5.67790851565975,
129.132867349833));
#154831=CARTESIAN_POINT('Ctrl Pts',(-71.9890843390759,-5.718202207928,129.284461255191));
#154832=CARTESIAN_POINT('Ctrl Pts',(-71.9964671243711,-5.75854025212212,
129.43622202244));
#154833=CARTESIAN_POINT('Ctrl Pts',(-72.0038499096662,-5.79280338507631,
129.589480069292));
#154834=CARTESIAN_POINT('Ctrl Pts',(-72.0112326949614,-5.82090555401294,
129.743705587049));
#154835=CARTESIAN_POINT('Ctrl Pts',(-72.0186202885717,-5.84902602553843,
129.898031549944));
#154836=CARTESIAN_POINT('Ctrl Pts',(-72.0260078821819,-5.87097748700464,
130.053325867692));
#154837=CARTESIAN_POINT('Ctrl Pts',(-72.0333954757921,-5.88672580388552,
130.209054081092));
#154838=CARTESIAN_POINT('Ctrl Pts',(-72.0407930705532,-5.90249544046816,
130.364993115692));
#154839=CARTESIAN_POINT('Ctrl Pts',(-72.0481906653144,-5.91204514566992,
130.521366844748));
#154840=CARTESIAN_POINT('Ctrl Pts',(-72.0555882600755,-5.91539285414198,
130.677640675702));
#154841=CARTESIAN_POINT('Ctrl Pts',(-72.0576004426463,-5.91630344749795,
130.720147935031));
#154842=CARTESIAN_POINT('Ctrl Pts',(-72.0596126252172,-5.91675547192607,
130.762647832883));
#154843=CARTESIAN_POINT('Ctrl Pts',(-72.061624807788,-5.91674995001673,
130.805129693042));
#154844=CARTESIAN_POINT('',(-73.811624807788,-5.91489018159219,130.798942093786));
#154845=CARTESIAN_POINT('Ctrl Pts',(-72.061624807788,-5.92641032049353,
130.805130948724));
#154846=CARTESIAN_POINT('Ctrl Pts',(-72.0635641793449,-5.92648514252835,
130.846142460203));
#154847=CARTESIAN_POINT('Ctrl Pts',(-72.0655035509017,-5.92609641746022,
130.887152515512));
#154848=CARTESIAN_POINT('Ctrl Pts',(-72.0674429224586,-5.92523982529112,
130.928152795978));
#154849=CARTESIAN_POINT('Ctrl Pts',(-72.1602587970629,-5.88424440537134,
132.890374463603));
#154850=CARTESIAN_POINT('Ctrl Pts',(-72.3458905462715,-3.65899295410281,
136.770040050133));
#154851=CARTESIAN_POINT('Ctrl Pts',(-72.6243381700844,3.04131999587715,
137.107370471042));
#154852=CARTESIAN_POINT('Ctrl Pts',(-72.9027857938972,6.94680844638694,
131.652542755755));
#154853=CARTESIAN_POINT('Ctrl Pts',(-73.1812334177101,4.46851930512866,
125.418277091475));
#154854=CARTESIAN_POINT('Ctrl Pts',(-73.459681041523,-2.11612077824121,
124.133559062861));
#154855=CARTESIAN_POINT('Ctrl Pts',(-73.6698115048829,-5.61771766134115,
127.790156687924));
#154856=CARTESIAN_POINT('Ctrl Pts',(-73.7871260936373,-5.91953532486225,
130.27824939099));
#154857=CARTESIAN_POINT('Ctrl Pts',(-73.811624807788,-5.91489018159219,
130.798942093786));
#154858=CARTESIAN_POINT('',(-75.5616248077879,-5.90731964829396,130.80593864926));
#154859=CARTESIAN_POINT('Ctrl Pts',(-73.811624807788,-5.91489018159219,
130.798942093786));
#154860=CARTESIAN_POINT('Ctrl Pts',(-73.8799419682416,-5.90193672631452,
132.250946746161));
#154861=CARTESIAN_POINT('Ctrl Pts',(-74.0410750033003,-4.63017145259677,
135.695938571682));
#154862=CARTESIAN_POINT('Ctrl Pts',(-74.2950239129616,1.14809306898754,
137.707942502008));
#154863=CARTESIAN_POINT('Ctrl Pts',(-74.5734715367747,6.4287513065015,133.569992040856));
#154864=CARTESIAN_POINT('Ctrl Pts',(-74.8519191605875,5.80170115531016,
126.890561410293));
#154865=CARTESIAN_POINT('Ctrl Pts',(-75.1303667844004,-0.156828928757731,
123.8077210515));
#154866=CARTESIAN_POINT('Ctrl Pts',(-75.366935333467,-5.09674180081162,
126.651095881476));
#154867=CARTESIAN_POINT('Ctrl Pts',(-75.5106880079297,-5.90473716813048,
129.719838266436));
#154868=CARTESIAN_POINT('Ctrl Pts',(-75.5616248077879,-5.90731964829396,
130.80593864926));
#154869=CARTESIAN_POINT('',(-77.311624807788,-5.92069754378162,130.809234386756));
#154870=CARTESIAN_POINT('Ctrl Pts',(-75.5616248077879,-5.90731964829396,
130.80593864926));
#154871=CARTESIAN_POINT('Ctrl Pts',(-75.603503882534,-5.90944290456639,
131.698905605187));
#154872=CARTESIAN_POINT('Ctrl Pts',(-75.738198831884,-5.29942908797976,
134.568186077309));
#154873=CARTESIAN_POINT('Ctrl Pts',(-75.9657096558394,-0.837609296111783,
137.752451808497));
#154874=CARTESIAN_POINT('Ctrl Pts',(-76.2441572796519,5.3928776148045,135.264678045965));
#154875=CARTESIAN_POINT('Ctrl Pts',(-76.522604903465,6.66757345442674,128.678090465366));
#154876=CARTESIAN_POINT('Ctrl Pts',(-76.8010525272776,1.81509501850905,
124.04544128056));
#154877=CARTESIAN_POINT('Ctrl Pts',(-77.0640591620522,-4.34378242790828,
125.536376696356));
#154878=CARTESIAN_POINT('Ctrl Pts',(-77.2342499222222,-5.90612396355947,
129.168851731668));
#154879=CARTESIAN_POINT('Ctrl Pts',(-77.311624807788,-5.92069754378162,
130.809234386756));
#154880=CARTESIAN_POINT('',(-79.0616248077881,-5.92047761364803,130.800476772624));
#154881=CARTESIAN_POINT('Ctrl Pts',(-77.311624807788,-5.92069754378162,
130.809234386756));
#154882=CARTESIAN_POINT('Ctrl Pts',(-77.3270657968265,-5.92360585816317,
131.136590355181));
#154883=CARTESIAN_POINT('Ctrl Pts',(-77.4353226604685,-5.74974331525388,
133.428593509251));
#154884=CARTESIAN_POINT('Ctrl Pts',(-77.636395398717,-2.75584475561056,
137.237313299921));
#154885=CARTESIAN_POINT('Ctrl Pts',(-77.914843022529,3.92262387668917,136.600098918449));
#154886=CARTESIAN_POINT('Ctrl Pts',(-78.1932906463423,6.99639279714031,
130.636884176034));
#154887=CARTESIAN_POINT('Ctrl Pts',(-78.4717382701551,3.64081852980919,
124.827572101703));
#154888=CARTESIAN_POINT('Ctrl Pts',(-78.750185893968,-3.06049010254254,
124.510636691099));
#154889=CARTESIAN_POINT('Ctrl Pts',(-78.9468147398456,-5.80665674345474,
128.370999423577));
#154890=CARTESIAN_POINT('Ctrl Pts',(-79.0506277111191,-5.92502371784771,
130.567593766307));
#154891=CARTESIAN_POINT('Ctrl Pts',(-79.0616248077881,-5.92325710276932,
130.800474949274));
#154892=CARTESIAN_POINT('',(-80.8116247804992,-5.91211101482029,130.801357666489));
#154893=CARTESIAN_POINT('Ctrl Pts',(-79.0616248077881,-5.91674872689752,
130.800479218781));
#154894=CARTESIAN_POINT('Ctrl Pts',(-79.0689408856106,-5.91685024886036,
130.955237845168));
#154895=CARTESIAN_POINT('Ctrl Pts',(-79.0762569634331,-5.91087581439112,
131.110236902362));
#154896=CARTESIAN_POINT('Ctrl Pts',(-79.0835730412556,-5.89879532966383,
131.264951782523));
#154897=CARTESIAN_POINT('Ctrl Pts',(-79.0908815388731,-5.88672736155428,
131.419506362244));
#154898=CARTESIAN_POINT('Ctrl Pts',(-79.0981900364905,-5.86856596065094,
131.573776970751));
#154899=CARTESIAN_POINT('Ctrl Pts',(-79.1054985341081,-5.84433303758537,
131.727237591105));
#154900=CARTESIAN_POINT('Ctrl Pts',(-79.1128011570195,-5.82011959339369,
131.88057485696));
#154901=CARTESIAN_POINT('Ctrl Pts',(-79.1201037799308,-5.78984439899684,
132.033103052641));
#154902=CARTESIAN_POINT('Ctrl Pts',(-79.1274064028422,-5.75358127374173,
132.184300141222));
#154903=CARTESIAN_POINT('Ctrl Pts',(-79.1348928502902,-5.71640531863396,
132.339303223223));
#154904=CARTESIAN_POINT('Ctrl Pts',(-79.1423792977382,-5.67293600697595,
132.492906886673));
#154905=CARTESIAN_POINT('Ctrl Pts',(-79.1498657451862,-5.62330902356941,
132.644557940666));
#154906=CARTESIAN_POINT('Ctrl Pts',(-79.1571626313433,-5.57493862482498,
132.792369100001));
#154907=CARTESIAN_POINT('Ctrl Pts',(-79.1644595175005,-5.5207187620526,
132.938324956991));
#154908=CARTESIAN_POINT('Ctrl Pts',(-79.1717564036576,-5.46082585735375,
133.081927634836));
#154909=CARTESIAN_POINT('Ctrl Pts',(-79.1790529036736,-5.40093612210465,
133.225522713426));
#154910=CARTESIAN_POINT('Ctrl Pts',(-79.1863494036894,-5.33537408989546,
133.366764505674));
#154911=CARTESIAN_POINT('Ctrl Pts',(-79.1936459037054,-5.2643644339058,
133.50517487803));
#154912=CARTESIAN_POINT('Ctrl Pts',(-79.2009435505635,-5.19334361683021,
133.643607005316));
#154913=CARTESIAN_POINT('Ctrl Pts',(-79.2082411974216,-5.11687364797293,
133.77920648526));
#154914=CARTESIAN_POINT('Ctrl Pts',(-79.2155388442796,-5.03522513301774,
133.911519838193));
#154915=CARTESIAN_POINT('Ctrl Pts',(-79.2231673690558,-4.94987464519807,
134.049832325861));
#154916=CARTESIAN_POINT('Ctrl Pts',(-79.230795893832,-4.85886527367793,
134.184553327272));
#154917=CARTESIAN_POINT('Ctrl Pts',(-79.2384244186081,-4.76255600949217,
134.31519966528));
#154918=CARTESIAN_POINT('Ctrl Pts',(-79.2457328170896,-4.67028830364041,
134.44036351102));
#154919=CARTESIAN_POINT('Ctrl Pts',(-79.2530412155711,-4.57315675802231,
134.561787455097));
#154920=CARTESIAN_POINT('Ctrl Pts',(-79.2603496140526,-4.47151711635527,
134.679081928918));
#154921=CARTESIAN_POINT('Ctrl Pts',(-79.2676628513618,-4.36981017995708,
134.796454062398));
#154922=CARTESIAN_POINT('Ctrl Pts',(-79.274976088671,-4.26358946657629,
134.909691002896));
#154923=CARTESIAN_POINT('Ctrl Pts',(-79.2822893259802,-4.15324649538433,
135.018441076109));
#154924=CARTESIAN_POINT('Ctrl Pts',(-79.2896121733775,-4.04275852607044,
135.127334054269));
#154925=CARTESIAN_POINT('Ctrl Pts',(-79.2969350207748,-3.92813777357985,
135.231728144505));
#154926=CARTESIAN_POINT('Ctrl Pts',(-79.3042578681721,-3.80980790028127,
135.331312608194));
#154927=CARTESIAN_POINT('Ctrl Pts',(-79.3051989593126,-3.79460081082798,
135.344110643088));
#154928=CARTESIAN_POINT('Ctrl Pts',(-79.3061400504532,-3.77933249924615,
135.35682930223));
#154929=CARTESIAN_POINT('Ctrl Pts',(-79.3070811415938,-3.76400389706835,
135.369467979431));
#154930=CARTESIAN_POINT('Ctrl Pts',(-79.3145044079992,-3.64309286870323,
135.469161052537));
#154931=CARTESIAN_POINT('Ctrl Pts',(-79.3219276744046,-3.51803558040563,
135.564197897001));
#154932=CARTESIAN_POINT('Ctrl Pts',(-79.32935094081,-3.38922624739663,135.654213811886));
#154933=CARTESIAN_POINT('Ctrl Pts',(-79.336765433531,-3.2605691563223,135.744123335435));
#154934=CARTESIAN_POINT('Ctrl Pts',(-79.3441799262521,-3.12816915064036,
135.829023529961));
#154935=CARTESIAN_POINT('Ctrl Pts',(-79.3515944189731,-2.99245467268624,
135.908588825084));
#154936=CARTESIAN_POINT('Ctrl Pts',(-79.3590017653269,-2.85687100145592,
135.988077432179));
#154937=CARTESIAN_POINT('Ctrl Pts',(-79.3664091116806,-2.71797953767195,
136.062241189004));
#154938=CARTESIAN_POINT('Ctrl Pts',(-79.3738164580344,-2.57623886720719,
136.130796936681));
#154939=CARTESIAN_POINT('Ctrl Pts',(-79.3812182797097,-2.43460391228202,
136.199301552896));
#154940=CARTESIAN_POINT('Ctrl Pts',(-79.3886201013852,-2.29012431653675,
136.262206326375));
#154941=CARTESIAN_POINT('Ctrl Pts',(-79.3960219230606,-2.14328441012716,
136.319273354845));
#154942=CARTESIAN_POINT('Ctrl Pts',(-79.4034198373719,-1.99652201936074,
136.376310258076));
#154943=CARTESIAN_POINT('Ctrl Pts',(-79.4108177516832,-1.84740214644256,
136.427515418772));
#154944=CARTESIAN_POINT('Ctrl Pts',(-79.4182156659946,-1.69643019767104,
136.472698570346));
#154945=CARTESIAN_POINT('Ctrl Pts',(-79.4256123509068,-1.54548333769871,
136.517874213301));
#154946=CARTESIAN_POINT('Ctrl Pts',(-79.433009035819,-1.39268537000304,
136.557029726399));
#154947=CARTESIAN_POINT('Ctrl Pts',(-79.4404057207312,-1.23855811568455,
136.590024309535));
#154948=CARTESIAN_POINT('Ctrl Pts',(-79.4478020776667,-1.08443769553003,
136.623017429657));
#154949=CARTESIAN_POINT('Ctrl Pts',(-79.4551984346021,-0.92898847097632,
136.649850084854));
#154950=CARTESIAN_POINT('Ctrl Pts',(-79.4625947915375,-0.772743479194567,
136.670432393283));
#154951=CARTESIAN_POINT('Ctrl Pts',(-79.4699922808741,-0.616474565906143,
136.691017852916));
#154952=CARTESIAN_POINT('Ctrl Pts',(-79.4773897702108,-0.459410012926293,
136.705351011623));
#154953=CARTESIAN_POINT('Ctrl Pts',(-79.4847872595473,-0.302088869548253,
136.71339377684));
#154954=CARTESIAN_POINT('Ctrl Pts',(-79.4921873420623,-0.144712577487056,
136.721439361435));
#154955=CARTESIAN_POINT('Ctrl Pts',(-79.4995874245773,0.0129201114784148,
136.723190143181));
#154956=CARTESIAN_POINT('Ctrl Pts',(-79.5069875070923,0.170269401851392,
136.718660144416));
#154957=CARTESIAN_POINT('Ctrl Pts',(-79.5143957267587,0.32779171394526,
136.714125164451));
#154958=CARTESIAN_POINT('Ctrl Pts',(-79.5218039464251,0.485029631737011,
136.703295622263));
#154959=CARTESIAN_POINT('Ctrl Pts',(-79.5292121660916,0.641447000175478,
136.686237555115));
#154960=CARTESIAN_POINT('Ctrl Pts',(-79.5366249453937,0.797960640894256,
136.66916898901));
#154961=CARTESIAN_POINT('Ctrl Pts',(-79.5440377246957,0.95365235758637,
136.645864314243));
#154962=CARTESIAN_POINT('Ctrl Pts',(-79.5514505039978,1.10799596448945,
136.616440753384));
#154963=CARTESIAN_POINT('Ctrl Pts',(-79.5588738750265,1.26256010477585,
136.586975150762));
#154964=CARTESIAN_POINT('Ctrl Pts',(-79.5662972460552,1.41577192548795,
136.551373284681));
#154965=CARTESIAN_POINT('Ctrl Pts',(-79.5737206170839,1.56711937634628,
136.50980253058));
#154966=CARTESIAN_POINT('Ctrl Pts',(-79.5776566665248,1.64736742632598,
136.487760719279));
#154967=CARTESIAN_POINT('Ctrl Pts',(-79.5815927159658,1.72709164075768,
136.464041655228));
#154968=CARTESIAN_POINT('Ctrl Pts',(-79.5855287654067,1.80621806682415,
136.438675736334));
#154969=CARTESIAN_POINT('Ctrl Pts',(-79.5929520318121,1.95544803693053,
136.390836404945));
#154970=CARTESIAN_POINT('Ctrl Pts',(-79.6003752982176,2.10300174478034,
136.33699190233));
#154971=CARTESIAN_POINT('Ctrl Pts',(-79.607798564623,2.24835927419038,136.277276763156));
#154972=CARTESIAN_POINT('Ctrl Pts',(-79.615213057344,2.39354500307185,136.217632202318));
#154973=CARTESIAN_POINT('Ctrl Pts',(-79.622627550065,2.53653937834598,136.152130956718));
#154974=CARTESIAN_POINT('Ctrl Pts',(-79.630042042786,2.67683690488364,136.080957508286));
#154975=CARTESIAN_POINT('Ctrl Pts',(-79.6374493891398,2.81699920738231,
136.009852659503));
#154976=CARTESIAN_POINT('Ctrl Pts',(-79.6448567354935,2.95446950521293,
135.933086659525));
#154977=CARTESIAN_POINT('Ctrl Pts',(-79.6522640818472,3.08876169192816,
135.850892275346));
#154978=CARTESIAN_POINT('Ctrl Pts',(-79.6596659035226,3.22295371846438,
135.76875919484));
#154979=CARTESIAN_POINT('Ctrl Pts',(-79.6670677251981,3.35397203655822,
135.681205985664));
#154980=CARTESIAN_POINT('Ctrl Pts',(-79.6744695468735,3.48135470001146,
135.588511536507));
#154981=CARTESIAN_POINT('Ctrl Pts',(-79.6818674611848,3.6086701191482,135.495866020029));
#154982=CARTESIAN_POINT('Ctrl Pts',(-79.6892653754961,3.73235340481413,
135.398084887761));
#154983=CARTESIAN_POINT('Ctrl Pts',(-79.6966632898075,3.85197129589288,
135.295490508598));
#154984=CARTESIAN_POINT('Ctrl Pts',(-79.7040599747197,3.97156930864839,
135.192913178759));
#154985=CARTESIAN_POINT('Ctrl Pts',(-79.7114566596317,4.08710298459685,
135.085524432329));
#154986=CARTESIAN_POINT('Ctrl Pts',(-79.7188533445439,4.19817180757139,
134.973687186283));
#154987=CARTESIAN_POINT('Ctrl Pts',(-79.7262497014793,4.30923570563794,
134.861854899218));
#154988=CARTESIAN_POINT('Ctrl Pts',(-79.7336460584149,4.41583488132454,
134.745574769608));
#154989=CARTESIAN_POINT('Ctrl Pts',(-79.7410424153504,4.51760559488155,
134.625246673391));
#154990=CARTESIAN_POINT('Ctrl Pts',(-79.7484399046869,4.61939188979462,
134.504900154635));
#154991=CARTESIAN_POINT('Ctrl Pts',(-79.7558373940235,4.71634800955154,
134.380504720301));
#154992=CARTESIAN_POINT('Ctrl Pts',(-79.76323488336,4.80815053649018,134.252493297865));
#154993=CARTESIAN_POINT('Ctrl Pts',(-79.770634965875,4.89998524466245,134.124437001224));
#154994=CARTESIAN_POINT('Ctrl Pts',(-79.7780350483901,4.9866625457081,133.992762495906));
#154995=CARTESIAN_POINT('Ctrl Pts',(-79.7854351309051,5.06790246436763,
133.857931506567));
#154996=CARTESIAN_POINT('Ctrl Pts',(-79.7928433505715,5.1492317146695,133.722952256695));
#154997=CARTESIAN_POINT('Ctrl Pts',(-79.800251570238,5.22511144943452,133.584809911168));
#154998=CARTESIAN_POINT('Ctrl Pts',(-79.8076597899044,5.29530742278066,
133.44399124717));
#154999=CARTESIAN_POINT('Ctrl Pts',(-79.8150725692065,5.36554660057672,
133.303085911635));
#155000=CARTESIAN_POINT('Ctrl Pts',(-79.8224853485085,5.43009489352607,
133.159501315004));
#155001=CARTESIAN_POINT('Ctrl Pts',(-79.8298981278106,5.48876650804002,
133.013743513924));
#155002=CARTESIAN_POINT('Ctrl Pts',(-79.8373214988393,5.54752195530829,
132.867777447262));
#155003=CARTESIAN_POINT('Ctrl Pts',(-79.844744869868,5.60038382857864,132.719632325072));
#155004=CARTESIAN_POINT('Ctrl Pts',(-79.8521682408967,5.64721616986486,
132.569829420269));
#155005=CARTESIAN_POINT('Ctrl Pts',(-79.8561042903376,5.67204780094216,
132.490400325668));
#155006=CARTESIAN_POINT('Ctrl Pts',(-79.8600403397786,5.69518516586961,
132.41050535267));
#155007=CARTESIAN_POINT('Ctrl Pts',(-79.8639763892195,5.71661386596347,
132.330223150684));
#155008=CARTESIAN_POINT('Ctrl Pts',(-79.8713996556249,5.75702772557264,
132.178813423265));
#155009=CARTESIAN_POINT('Ctrl Pts',(-79.8788229220304,5.79148320386002,
132.025568041024));
#155010=CARTESIAN_POINT('Ctrl Pts',(-79.8862461884358,5.81981246125332,
131.870997143446));
#155011=CARTESIAN_POINT('Ctrl Pts',(-79.8936606811569,5.84810823581706,
131.716608935831));
#155012=CARTESIAN_POINT('Ctrl Pts',(-79.9010751738779,5.87029213547004,
131.560898694898));
#155013=CARTESIAN_POINT('Ctrl Pts',(-79.9084896665989,5.88624613761831,
131.404391425003));
#155014=CARTESIAN_POINT('Ctrl Pts',(-79.9158970129527,5.90218476269859,
131.248035002708));
#155015=CARTESIAN_POINT('Ctrl Pts',(-79.9233043593065,5.91190540666725,
131.090883449679));
#155016=CARTESIAN_POINT('Ctrl Pts',(-79.9307117056603,5.91534115058,130.933471557284));
#155017=CARTESIAN_POINT('Ctrl Pts',(-79.9381135273357,5.91877433198531,
130.776177068617));
#155018=CARTESIAN_POINT('Ctrl Pts',(-79.9455153490112,5.91593193870001,
130.618622998807));
#155019=CARTESIAN_POINT('Ctrl Pts',(-79.9529171706866,5.90679891447224,
130.461348742422));
#155020=CARTESIAN_POINT('Ctrl Pts',(-79.960315084998,5.89767071149682,130.304157509892));
#155021=CARTESIAN_POINT('Ctrl Pts',(-79.9677129993094,5.88225851264802,
130.147246168339));
#155022=CARTESIAN_POINT('Ctrl Pts',(-79.9751109136208,5.86059934779146,
129.991153480874));
#155023=CARTESIAN_POINT('Ctrl Pts',(-79.982507598533,5.83894378229526,129.835086733183));
#155024=CARTESIAN_POINT('Ctrl Pts',(-79.9899042834451,5.81104336243338,
129.679838738962));
#155025=CARTESIAN_POINT('Ctrl Pts',(-79.9973009683574,5.77698693176365,
129.525942629296));
#155026=CARTESIAN_POINT('Ctrl Pts',(-80.0046973252928,5.74293201119174,
129.372053343545));
#155027=CARTESIAN_POINT('Ctrl Pts',(-80.0120936822283,5.70272170321407,
129.21951618764));
#155028=CARTESIAN_POINT('Ctrl Pts',(-80.0194900391638,5.65649582456277,
129.068853328845));
#155029=CARTESIAN_POINT('Ctrl Pts',(-80.0268875285004,5.61026286861157,
128.918167403182));
#155030=CARTESIAN_POINT('Ctrl Pts',(-80.034285017837,5.55801261765797,128.769356702906));
#155031=CARTESIAN_POINT('Ctrl Pts',(-80.0416825071736,5.49993449070261,
128.622927336331));
#155032=CARTESIAN_POINT('Ctrl Pts',(-80.0490825896886,5.44183600454979,
128.476446639168));
#155033=CARTESIAN_POINT('Ctrl Pts',(-80.0564826722035,5.37790571243548,
128.332349284517));
#155034=CARTESIAN_POINT('Ctrl Pts',(-80.0638827547185,5.30838074292339,
128.191120396947));
#155035=CARTESIAN_POINT('Ctrl Pts',(-80.071290974385,5.23877932355988,128.049736213697));
#155036=CARTESIAN_POINT('Ctrl Pts',(-80.0786991940516,5.16357110597951,
127.911227131742));
#155037=CARTESIAN_POINT('Ctrl Pts',(-80.0861074137181,5.08303901399145,
127.776053343735));
#155038=CARTESIAN_POINT('Ctrl Pts',(-80.0935201930202,5.0024573558443,127.640796358516));
#155039=CARTESIAN_POINT('Ctrl Pts',(-80.1009329723223,4.91654549718926,
127.508879069826));
#155040=CARTESIAN_POINT('Ctrl Pts',(-80.1083457516244,4.82562877184278,
127.380731327052));
#155041=CARTESIAN_POINT('Ctrl Pts',(-80.1157691226531,4.7345821404157,127.252400480774));
#155042=CARTESIAN_POINT('Ctrl Pts',(-80.123192493682,4.63851658715403,127.127850232476));
#155043=CARTESIAN_POINT('Ctrl Pts',(-80.1306158647108,4.53779718511222,
127.007476728205));
#155044=CARTESIAN_POINT('Ctrl Pts',(-80.1345519141514,4.48439334142351,
126.943651807922));
#155045=CARTESIAN_POINT('Ctrl Pts',(-80.1384879635919,4.4296817488055,126.88100050308));
#155046=CARTESIAN_POINT('Ctrl Pts',(-80.1424240130325,4.37372079439489,
126.819577439628));
#155047=CARTESIAN_POINT('Ctrl Pts',(-80.1498472794379,4.26818018085312,
126.703735458901));
#155048=CARTESIAN_POINT('Ctrl Pts',(-80.1572705458433,4.15787452827597,
126.591914216861));
#155049=CARTESIAN_POINT('Ctrl Pts',(-80.1646938122487,4.0431423100696,126.484530664544));
#155050=CARTESIAN_POINT('Ctrl Pts',(-80.1721083049697,3.92854569581723,
126.377274030669));
#155051=CARTESIAN_POINT('Ctrl Pts',(-80.1795227976908,3.80953319981205,
126.274444898952));
#155052=CARTESIAN_POINT('Ctrl Pts',(-80.1869372904118,3.68648272899339,
126.176426342824));
#155053=CARTESIAN_POINT('Ctrl Pts',(-80.1943446367656,3.56355085885057,
126.07850226067));
#155054=CARTESIAN_POINT('Ctrl Pts',(-80.2017519831193,3.4365890520289,125.985379754543));
#155055=CARTESIAN_POINT('Ctrl Pts',(-80.2091593294731,3.30601107232773,
125.897404193045));
#155056=CARTESIAN_POINT('Ctrl Pts',(-80.2165611511485,3.17553048261099,
125.80949424704));
#155057=CARTESIAN_POINT('Ctrl Pts',(-80.2239629728239,3.04143939851723,
125.726723809808));
#155058=CARTESIAN_POINT('Ctrl Pts',(-80.2313647944993,2.90418348970092,
125.649397104538));
#155059=CARTESIAN_POINT('Ctrl Pts',(-80.2387627088107,2.76700003720969,
125.572111219434));
#155060=CARTESIAN_POINT('Ctrl Pts',(-80.246160623122,2.62665541165997,125.50026352594));
#155061=CARTESIAN_POINT('Ctrl Pts',(-80.2535585374334,2.48362290526187,
125.434114084402));
#155062=CARTESIAN_POINT('Ctrl Pts',(-80.2609552223456,2.34061416827208,
125.367975635702));
#155063=CARTESIAN_POINT('Ctrl Pts',(-80.2683519072578,2.194918775442,125.307533716093));
#155064=CARTESIAN_POINT('Ctrl Pts',(-80.27574859217,2.04703328716472,125.253001749348));
#155065=CARTESIAN_POINT('Ctrl Pts',(-80.2831449491054,1.89915435628538,
125.198472200608));
#155066=CARTESIAN_POINT('Ctrl Pts',(-80.2905413060408,1.74908587329303,
125.149852212831));
#155067=CARTESIAN_POINT('Ctrl Pts',(-80.2979376629762,1.59734272665514,
125.107306398401));
#155068=CARTESIAN_POINT('Ctrl Pts',(-80.3053351523128,1.44557634775411,
125.064754070099));
#155069=CARTESIAN_POINT('Ctrl Pts',(-80.3127326416494,1.29213515415045,
125.028277867628));
#155070=CARTESIAN_POINT('Ctrl Pts',(-80.3201301309859,1.1375473346996,124.997991991323));
#155071=CARTESIAN_POINT('Ctrl Pts',(-80.3275302135009,0.982905324727631,
124.967695498351));
#155072=CARTESIAN_POINT('Ctrl Pts',(-80.3349302960158,0.827116254738348,
124.943593723744));
#155073=CARTESIAN_POINT('Ctrl Pts',(-80.3423303785308,0.670716447552981,
124.925749386205));
#155074=CARTESIAN_POINT('Ctrl Pts',(-80.3497385981973,0.514144662701546,
124.907885426983));
#155075=CARTESIAN_POINT('Ctrl Pts',(-80.3571468178638,0.356961170607229,
124.896292688371));
#155076=CARTESIAN_POINT('Ctrl Pts',(-80.3645550375302,0.199706071611347,
124.890981883926));
#155077=CARTESIAN_POINT('Ctrl Pts',(-80.3719678168323,0.0423541847264234,
124.88566781077));
#155078=CARTESIAN_POINT('Ctrl Pts',(-80.3793805961343,-0.11506902445551,
124.886643373811));
#155079=CARTESIAN_POINT('Ctrl Pts',(-80.3867933754363,-0.272026060596711,
124.893867204588));
#155080=CARTESIAN_POINT('Ctrl Pts',(-80.3942167464651,-0.429207364312377,
124.901101357113));
#155081=CARTESIAN_POINT('Ctrl Pts',(-80.4016401174939,-0.585920793721219,
124.914601576276));
#155082=CARTESIAN_POINT('Ctrl Pts',(-80.4090634885226,-0.741635729030356,
124.93427484239));
#155083=CARTESIAN_POINT('Ctrl Pts',(-80.4129995379635,-0.824199524061613,
124.944706080137));
#155084=CARTESIAN_POINT('Ctrl Pts',(-80.4169355874043,-0.906482793422893,
124.95687193191));
#155085=CARTESIAN_POINT('Ctrl Pts',(-80.4208716368452,-0.988408019083317,
124.970752801616));
#155086=CARTESIAN_POINT('Ctrl Pts',(-80.4282949032507,-1.14291643787704,
124.996931688674));
#155087=CARTESIAN_POINT('Ctrl Pts',(-80.4357181696561,-1.29661771533132,
125.029292845497));
#155088=CARTESIAN_POINT('Ctrl Pts',(-80.4431414360616,-1.44897810558652,
125.067776877043));
#155089=CARTESIAN_POINT('Ctrl Pts',(-80.4505559287826,-1.60115841851317,
125.10621542366));
#155090=CARTESIAN_POINT('Ctrl Pts',(-80.4579704215036,-1.75200064043173,
125.150762349724));
#155091=CARTESIAN_POINT('Ctrl Pts',(-80.4653849142246,-1.90097821288504,
125.201306771971));
#155092=CARTESIAN_POINT('Ctrl Pts',(-80.4727922605784,-2.04981219514426,
125.2518024776));
#155093=CARTESIAN_POINT('Ctrl Pts',(-80.4801996069321,-2.19678475471506,
125.308284052219));
#155094=CARTESIAN_POINT('Ctrl Pts',(-80.4876069532858,-2.34138167377254,
125.370590064789));
#155095=CARTESIAN_POINT('Ctrl Pts',(-80.4950087749612,-2.48587074699286,
125.432849607185));
#155096=CARTESIAN_POINT('Ctrl Pts',(-80.5024105966367,-2.62798736632663,
125.500924790785));
#155097=CARTESIAN_POINT('Ctrl Pts',(-80.509812418312,-2.76723468485333,
125.574605101154));
#155098=CARTESIAN_POINT('Ctrl Pts',(-80.5172103326234,-2.90640849580527,
125.64824651626));
#155099=CARTESIAN_POINT('Ctrl Pts',(-80.5246082469348,-3.04271569339197,
125.72748699119));
#155100=CARTESIAN_POINT('Ctrl Pts',(-80.5320061612462,-3.17568165547834,
125.812068900773));
#155101=CARTESIAN_POINT('Ctrl Pts',(-80.5394028461584,-3.30862552103311,
125.896636754376));
#155102=CARTESIAN_POINT('Ctrl Pts',(-80.5467995310706,-3.43822893843607,
125.986544080748));
#155103=CARTESIAN_POINT('Ctrl Pts',(-80.5541962159828,-3.56404394520174,
126.081488470326));
#155104=CARTESIAN_POINT('Ctrl Pts',(-80.5615925729183,-3.68985337319888,
126.176428649972));
#155105=CARTESIAN_POINT('Ctrl Pts',(-80.5689889298536,-3.81187442659001,
126.276405223872));
#155106=CARTESIAN_POINT('Ctrl Pts',(-80.5763852867891,-3.92969030252024,
126.38107397879));
#155107=CARTESIAN_POINT('Ctrl Pts',(-80.5837827761256,-4.04752421636084,
126.48575875876));
#155108=CARTESIAN_POINT('Ctrl Pts',(-80.5911802654623,-4.16115139171191,
126.595136902202));
#155109=CARTESIAN_POINT('Ctrl Pts',(-80.5985777547988,-4.27019024961786,
126.708825756944));
#155110=CARTESIAN_POINT('Ctrl Pts',(-80.6059778373138,-4.37926733092688,
126.822554465138));
#155111=CARTESIAN_POINT('Ctrl Pts',(-80.6133779198288,-4.48375263419014,
126.940596624002));
#155112=CARTESIAN_POINT('Ctrl Pts',(-80.6207780023437,-4.58330349680079,
127.062534910947));
#155113=CARTESIAN_POINT('Ctrl Pts',(-80.6281862220102,-4.68296382581909,
127.184607281575));
#155114=CARTESIAN_POINT('Ctrl Pts',(-80.6355944416767,-4.77767864203371,
127.310584046753));
#155115=CARTESIAN_POINT('Ctrl Pts',(-80.6430026613431,-4.86714699439943,
127.440016595708));
#155116=CARTESIAN_POINT('Ctrl Pts',(-80.6504154406452,-4.95667041304343,
127.569528808238));
#155117=CARTESIAN_POINT('Ctrl Pts',(-80.6578282199473,-5.04094073406692,
127.702500728233));
#155118=CARTESIAN_POINT('Ctrl Pts',(-80.6652409992494,-5.11970223256816,
127.838457784981));
#155119=CARTESIAN_POINT('Ctrl Pts',(-80.6726643702781,-5.1985762691919,
127.974609103547));
#155120=CARTESIAN_POINT('Ctrl Pts',(-80.6800877413068,-5.27192558899847,
128.113753748281));
#155121=CARTESIAN_POINT('Ctrl Pts',(-80.6875111123356,-5.339541639124,128.255395014314));
#155122=CARTESIAN_POINT('Ctrl Pts',(-80.6914471617765,-5.37539329132617,
128.330496612202));
#155123=CARTESIAN_POINT('Ctrl Pts',(-80.6953832112174,-5.40963393264518,
128.406299797149));
#155124=CARTESIAN_POINT('Ctrl Pts',(-80.6993192606582,-5.44223814943938,
128.482728758876));
#155125=CARTESIAN_POINT('Ctrl Pts',(-80.7075629756018,-5.51052486007303,
128.642802605347));
#155126=CARTESIAN_POINT('Ctrl Pts',(-80.7158066905453,-5.57180668670428,
128.806035138289));
#155127=CARTESIAN_POINT('Ctrl Pts',(-80.7240504054889,-5.62581158504579,
128.971828333522));
#155128=CARTESIAN_POINT('Ctrl Pts',(-80.7322607000411,-5.67959754509978,
129.136949395682));
#155129=CARTESIAN_POINT('Ctrl Pts',(-80.7404709945934,-5.7261653457546,
129.304610194852));
#155130=CARTESIAN_POINT('Ctrl Pts',(-80.7486812891456,-5.76529212749997,
129.474196249119));
#155131=CARTESIAN_POINT('Ctrl Pts',(-80.7568699712177,-5.80431591333105,
129.643335891237));
#155132=CARTESIAN_POINT('Ctrl Pts',(-80.7650586532899,-5.83593768790586,
129.814390458695));
#155133=CARTESIAN_POINT('Ctrl Pts',(-80.773247335362,-5.85998381724229,
129.986729756995));
#155134=CARTESIAN_POINT('Ctrl Pts',(-80.7814007344187,-5.88392633772643,
130.15832648768));
#155135=CARTESIAN_POINT('Ctrl Pts',(-80.7895541334754,-5.90035826308932,
130.331196682838));
#155136=CARTESIAN_POINT('Ctrl Pts',(-80.7977075325322,-5.90915685221338,
130.504701046653));
#155137=CARTESIAN_POINT('Ctrl Pts',(-80.8023466037498,-5.91416301973651,
130.603420500307));
#155138=CARTESIAN_POINT('Ctrl Pts',(-80.8069856749674,-5.91669893396806,
130.702344957279));
#155139=CARTESIAN_POINT('Ctrl Pts',(-80.811624746185,-5.91674923638228,
130.801354578692));
#155140=CARTESIAN_POINT('',(-82.5616248426584,-5.91498137599263,130.809325487812));
#155141=CARTESIAN_POINT('Ctrl Pts',(-80.8116248077882,-5.9084223721743,
130.801360122124));
#155142=CARTESIAN_POINT('Ctrl Pts',(-80.8670055000158,-5.90302635562967,
131.981665087397));
#155143=CARTESIAN_POINT('Ctrl Pts',(-81.015202066848,-4.98742482863156,
135.147824577937));
#155144=CARTESIAN_POINT('Ctrl Pts',(-81.2562145082839,0.178123566435826,
137.800490442363));
#155145=CARTESIAN_POINT('Ctrl Pts',(-81.5346621320968,5.98232230086394,
134.436079276676));
#155146=CARTESIAN_POINT('Ctrl Pts',(-81.8131097559099,6.28905909348952,
127.734296082587));
#155147=CARTESIAN_POINT('Ctrl Pts',(-82.0915573797235,0.816457816798208,
123.853752215139));
#155148=CARTESIAN_POINT('Ctrl Pts',(-82.3410623970142,-4.75960452750159,
126.09992199794));
#155149=CARTESIAN_POINT('Ctrl Pts',(-82.497751539704,-5.90151872823958,
129.450227630412));
#155150=CARTESIAN_POINT('Ctrl Pts',(-82.5616248077882,-5.9122429093786,
130.809322447035));
#155151=CARTESIAN_POINT('',(-84.3116248077883,-5.92105424700558,130.805351872892));
#155152=CARTESIAN_POINT('Ctrl Pts',(-82.5616248651526,-5.91674791528943,
130.809327449367));
#155153=CARTESIAN_POINT('Ctrl Pts',(-82.5704277186159,-5.91659056117995,
130.996775834263));
#155154=CARTESIAN_POINT('Ctrl Pts',(-82.5792305720792,-5.90752161874744,
131.183840062295));
#155155=CARTESIAN_POINT('Ctrl Pts',(-82.5880334255424,-5.88967326213172,
131.369762623072));
#155156=CARTESIAN_POINT('Ctrl Pts',(-82.596900390002,-5.87169491631084,
131.557039253943));
#155157=CARTESIAN_POINT('Ctrl Pts',(-82.6057673544616,-5.84480890847867,
131.743157495007));
#155158=CARTESIAN_POINT('Ctrl Pts',(-82.6146343189213,-5.80919903321914,
131.927364248435));
#155159=CARTESIAN_POINT('Ctrl Pts',(-82.6235720648078,-5.77330489858391,
132.113041450618));
#155160=CARTESIAN_POINT('Ctrl Pts',(-82.6325098106944,-5.7285471183117,
132.296776497412));
#155161=CARTESIAN_POINT('Ctrl Pts',(-82.6414475565809,-5.67516207160035,
132.477819916016));
#155162=CARTESIAN_POINT('Ctrl Pts',(-82.6437825801703,-5.66121500430027,
132.525118268252));
#155163=CARTESIAN_POINT('Ctrl Pts',(-82.6461176037597,-5.64667934482961,
132.572233022749));
#155164=CARTESIAN_POINT('Ctrl Pts',(-82.6484526273491,-5.63155983789489,
132.619151061311));
#155165=CARTESIAN_POINT('Ctrl Pts',(-82.6558758937544,-5.58349345929223,
132.768308055291));
#155166=CARTESIAN_POINT('Ctrl Pts',(-82.6632991601597,-5.52942446740412,
132.915779650107));
#155167=CARTESIAN_POINT('Ctrl Pts',(-82.6707224265651,-5.46948818796429,
133.061046134916));
#155168=CARTESIAN_POINT('Ctrl Pts',(-82.678136919286,-5.40962274822936,
133.206140926805));
#155169=CARTESIAN_POINT('Ctrl Pts',(-82.6855514120068,-5.3439039653829,
133.349035454746));
#155170=CARTESIAN_POINT('Ctrl Pts',(-82.6929659047278,-5.2725170904167,
133.489224504947));
#155171=CARTESIAN_POINT('Ctrl Pts',(-82.7003732510815,-5.20119902080825,
133.629278435664));
#155172=CARTESIAN_POINT('Ctrl Pts',(-82.7077805974352,-5.1242239033331,
133.766631749521));
#155173=CARTESIAN_POINT('Ctrl Pts',(-82.7151879437889,-5.04182524448686,
133.900798694866));
#155174=CARTESIAN_POINT('Ctrl Pts',(-82.7225897654642,-4.95948804166888,
134.034865573442));
#155175=CARTESIAN_POINT('Ctrl Pts',(-82.7299915871396,-4.87173554630225,
134.165750498738));
#155176=CARTESIAN_POINT('Ctrl Pts',(-82.7373934088149,-4.77884734975571,
134.292991949512));
#155177=CARTESIAN_POINT('Ctrl Pts',(-82.7447913231262,-4.68600818816535,
134.420166230513));
#155178=CARTESIAN_POINT('Ctrl Pts',(-82.7521892374374,-4.58803894422062,
134.543700566717));
#155179=CARTESIAN_POINT('Ctrl Pts',(-82.7595871517487,-4.48526264579371,
134.663162188099));
#155180=CARTESIAN_POINT('Ctrl Pts',(-82.7669838366608,-4.3825034269229,
134.782603957127));
#155181=CARTESIAN_POINT('Ctrl Pts',(-82.774380521573,-4.27493898226133,
134.897974071897));
#155182=CARTESIAN_POINT('Ctrl Pts',(-82.7817772064852,-4.16293283788085,
135.008872569005));
#155183=CARTESIAN_POINT('Ctrl Pts',(-82.7891735634205,-4.0509316599705,
135.119766148757));
#155184=CARTESIAN_POINT('Ctrl Pts',(-82.7965699203559,-3.93448943921327,
135.22618824244));
#155185=CARTESIAN_POINT('Ctrl Pts',(-82.8039662772913,-3.814006604634,135.327775719268));
#155186=CARTESIAN_POINT('Ctrl Pts',(-82.8113637666278,-3.69350532382517,
135.429378749399));
#155187=CARTESIAN_POINT('Ctrl Pts',(-82.8187612559642,-3.56896248283143,
135.526145448207));
#155188=CARTESIAN_POINT('Ctrl Pts',(-82.8261587453007,-3.44081150081433,
135.617753057246));
#155189=CARTESIAN_POINT('Ctrl Pts',(-82.8335588278157,-3.31261559566933,
135.70939277919));
#155190=CARTESIAN_POINT('Ctrl Pts',(-82.8409589103306,-3.18080933473297,
135.795869593682));
#155191=CARTESIAN_POINT('Ctrl Pts',(-82.8483589928455,-3.04585486820177,
135.876904228453));
#155192=CARTESIAN_POINT('Ctrl Pts',(-82.8557672125119,-2.91075200536077,
135.958027969136));
#155193=CARTESIAN_POINT('Ctrl Pts',(-82.8631754321783,-2.77249434376342,
136.0336973869));
#155194=CARTESIAN_POINT('Ctrl Pts',(-82.8705836518447,-2.63156901651121,
136.103678976925));
#155195=CARTESIAN_POINT('Ctrl Pts',(-82.8779964311467,-2.49055695207155,
136.173703639451));
#155196=CARTESIAN_POINT('Ctrl Pts',(-82.8854092104487,-2.34687429019651,
136.238033346342));
#155197=CARTESIAN_POINT('Ctrl Pts',(-82.8928219897506,-2.20102736969333,
136.296483074355));
#155198=CARTESIAN_POINT('Ctrl Pts',(-82.9002453607793,-2.05497205627038,
136.35501631808));
#155199=CARTESIAN_POINT('Ctrl Pts',(-82.9076687318081,-1.90674665885866,
136.407652678481));
#155200=CARTESIAN_POINT('Ctrl Pts',(-82.9150921028368,-1.75687265667485,
136.454256991016));
#155201=CARTESIAN_POINT('Ctrl Pts',(-82.9190281522783,-1.67740586452409,
136.478967715783));
#155202=CARTESIAN_POINT('Ctrl Pts',(-82.9229642017198,-1.59747577289914,
136.501983467373));
#155203=CARTESIAN_POINT('Ctrl Pts',(-82.9269002511613,-1.51716105303232,
136.523289966812));
#155204=CARTESIAN_POINT('Ctrl Pts',(-82.9343235175668,-1.36568999792873,
136.563473359791));
#155205=CARTESIAN_POINT('Ctrl Pts',(-82.9417467839723,-1.21239235777182,
136.597695584795));
#155206=CARTESIAN_POINT('Ctrl Pts',(-82.9491700503777,-1.05777852687676,
136.62578957879));
#155207=CARTESIAN_POINT('Ctrl Pts',(-82.9565845430987,-0.903347436689951,
136.653850368017));
#155208=CARTESIAN_POINT('Ctrl Pts',(-82.9639990358196,-0.747603615948766,
136.675797277501));
#155209=CARTESIAN_POINT('Ctrl Pts',(-82.9714135285406,-0.59107224801231,
136.691513083753));
#155210=CARTESIAN_POINT('Ctrl Pts',(-82.9788208748944,-0.434691750901128,
136.707213742518));
#155211=CARTESIAN_POINT('Ctrl Pts',(-82.9862282212481,-0.277525586685956,
136.716695217319));
#155212=CARTESIAN_POINT('Ctrl Pts',(-82.9936355676019,-0.120108647953987,
136.71989140315));
#155213=CARTESIAN_POINT('Ctrl Pts',(-83.0010373892773,0.0371908832860754,
136.723085205144));
#155214=CARTESIAN_POINT('Ctrl Pts',(-83.0084392109528,0.194740445012163,
136.720003044677));
#155215=CARTESIAN_POINT('Ctrl Pts',(-83.0158410326282,0.35200062036801,
136.710630686379));
#155216=CARTESIAN_POINT('Ctrl Pts',(-83.0232389469396,0.509177779301398,
136.701263275677));
#155217=CARTESIAN_POINT('Ctrl Pts',(-83.0306368612509,0.66606548440955,
136.685612302325));
#155218=CARTESIAN_POINT('Ctrl Pts',(-83.0380347755622,0.822125029559199,
136.663715616051));
#155219=CARTESIAN_POINT('Ctrl Pts',(-83.0454314604744,0.978158640443431,
136.641822568609));
#155220=CARTESIAN_POINT('Ctrl Pts',(-83.0528281453866,1.13336399519958,
136.613685920037));
#155221=CARTESIAN_POINT('Ctrl Pts',(-83.0602248302988,1.28720809856583,
136.579395325123));
#155222=CARTESIAN_POINT('Ctrl Pts',(-83.0676211872343,1.44104538032332,
136.54510625069));
#155223=CARTESIAN_POINT('Ctrl Pts',(-83.0750175441697,1.59352116634909,
136.504663853691));
#155224=CARTESIAN_POINT('Ctrl Pts',(-83.0824139011051,1.74411350276013,
136.458208745345));
#155225=CARTESIAN_POINT('Ctrl Pts',(-83.0898113904417,1.89472889524231,
136.411746524604));
#155226=CARTESIAN_POINT('Ctrl Pts',(-83.0972088797783,2.04345990721087,
136.359269869601));
#155227=CARTESIAN_POINT('Ctrl Pts',(-83.1046063691148,2.18980071920077,
136.300968969331));
#155228=CARTESIAN_POINT('Ctrl Pts',(-83.1120064516298,2.33619283073524,
136.24264763177));
#155229=CARTESIAN_POINT('Ctrl Pts',(-83.1194065341448,2.48019272750221,
136.178498122042));
#155230=CARTESIAN_POINT('Ctrl Pts',(-83.1268066166598,2.62131564636256,
136.108758306714));
#155231=CARTESIAN_POINT('Ctrl Pts',(-83.1342148363263,2.76259374438019,
136.038941805289));
#155232=CARTESIAN_POINT('Ctrl Pts',(-83.1416230559927,2.90098821183925,
135.963522887555));
#155233=CARTESIAN_POINT('Ctrl Pts',(-83.1490312756591,3.03603928718225,
135.882785177327));
#155234=CARTESIAN_POINT('Ctrl Pts',(-83.1564440549612,3.17117348420867,
135.801997774386));
#155235=CARTESIAN_POINT('Ctrl Pts',(-83.1638568342633,3.30295987691573,
135.71588525956));
#155236=CARTESIAN_POINT('Ctrl Pts',(-83.1712696135653,3.4309691115169,135.624773620444));
#155237=CARTESIAN_POINT('Ctrl Pts',(-83.1786929845941,3.55916125171568,
135.533531796746));
#155238=CARTESIAN_POINT('Ctrl Pts',(-83.1861163556228,3.68356516036802,
135.437276810452));
#155239=CARTESIAN_POINT('Ctrl Pts',(-83.1935397266516,3.80378524746377,
135.336374337059));
#155240=CARTESIAN_POINT('Ctrl Pts',(-83.1974757760924,3.86752882228469,
135.282873424544));
#155241=CARTESIAN_POINT('Ctrl Pts',(-83.2014118255333,3.93009679285136,
135.228066550657));
#155242=CARTESIAN_POINT('Ctrl Pts',(-83.2053478749742,3.9914346221341,135.172012185598));
#155243=CARTESIAN_POINT('Ctrl Pts',(-83.2127711413796,4.10711585387093,
135.066295402495));
#155244=CARTESIAN_POINT('Ctrl Pts',(-83.2201944077851,4.21876909999845,
134.955819704755));
#155245=CARTESIAN_POINT('Ctrl Pts',(-83.2276176741905,4.32597792506152,
134.840924199919));
#155246=CARTESIAN_POINT('Ctrl Pts',(-83.2350321669115,4.43306003819651,
134.726164492029));
#155247=CARTESIAN_POINT('Ctrl Pts',(-83.2424466596325,4.53570793407956,
134.606995645404));
#155248=CARTESIAN_POINT('Ctrl Pts',(-83.2498611523535,4.63353911483465,
134.483796149519));
#155249=CARTESIAN_POINT('Ctrl Pts',(-83.2572684987073,4.73127600221445,
134.360715397946));
#155250=CARTESIAN_POINT('Ctrl Pts',(-83.2646758450611,4.82420518624881,
134.233612021542));
#155251=CARTESIAN_POINT('Ctrl Pts',(-83.2720831914149,4.91198192841564,
134.10290030922));
#155252=CARTESIAN_POINT('Ctrl Pts',(-83.2794850130903,4.99969320337655,
133.972286086625));
#155253=CARTESIAN_POINT('Ctrl Pts',(-83.2868868347657,5.08225948095878,
133.83806919529));
#155254=CARTESIAN_POINT('Ctrl Pts',(-83.2942886564411,5.15937721655751,
133.700695767332));
#155255=CARTESIAN_POINT('Ctrl Pts',(-83.3016865707524,5.23645424230368,
133.563394857737));
#155256=CARTESIAN_POINT('Ctrl Pts',(-83.3090844850638,5.30808827196975,
133.422941054746));
#155257=CARTESIAN_POINT('Ctrl Pts',(-83.3164823993751,5.37401996578059,
133.279808045788));
#155258=CARTESIAN_POINT('Ctrl Pts',(-83.3238790842873,5.43994070294013,
133.13669882294));
#155259=CARTESIAN_POINT('Ctrl Pts',(-83.3312757691996,5.50016082897185,
132.99091161651));
#155260=CARTESIAN_POINT('Ctrl Pts',(-83.3386724541118,5.55446767603133,
132.842943311111));
#155261=CARTESIAN_POINT('Ctrl Pts',(-83.3460688110472,5.6087721150683,132.694981566783));
#155262=CARTESIAN_POINT('Ctrl Pts',(-83.3534651679826,5.65716366785959,
132.544839266222));
#155263=CARTESIAN_POINT('Ctrl Pts',(-83.3608615249181,5.69947850578363,
132.393031547813));
#155264=CARTESIAN_POINT('Ctrl Pts',(-83.3682590142546,5.74179982221738,
132.241200587254));
#155265=CARTESIAN_POINT('Ctrl Pts',(-83.3756565035912,5.77804247107385,
132.087704060762));
#155266=CARTESIAN_POINT('Ctrl Pts',(-83.3830539929277,5.80809305596224,
131.933070330372));
#155267=CARTESIAN_POINT('Ctrl Pts',(-83.3904540754427,5.83815417503662,
131.778382393368));
#155268=CARTESIAN_POINT('Ctrl Pts',(-83.3978541579579,5.86201883728974,
131.622556824982));
#155269=CARTESIAN_POINT('Ctrl Pts',(-83.4052542404729,5.87962514028273,
131.466130042861));
#155270=CARTESIAN_POINT('Ctrl Pts',(-83.4126624601393,5.8972508032158,131.309531253412));
#155271=CARTESIAN_POINT('Ctrl Pts',(-83.4200706798058,5.90860432188552,
131.152330301159));
#155272=CARTESIAN_POINT('Ctrl Pts',(-83.4274788994722,5.91367580468914,
130.995067302122));
#155273=CARTESIAN_POINT('Ctrl Pts',(-83.4348916787743,5.91875040890583,
130.837707510332));
#155274=CARTESIAN_POINT('Ctrl Pts',(-83.4423044580764,5.91753527566853,
130.680285968084));
#155275=CARTESIAN_POINT('Ctrl Pts',(-83.4497172373785,5.91007259136617,
130.523340107136));
#155276=CARTESIAN_POINT('Ctrl Pts',(-83.4571406084072,5.90259924403053,
130.366169994582));
#155277=CARTESIAN_POINT('Ctrl Pts',(-83.4645639794359,5.88886054933901,
130.209477291681));
#155278=CARTESIAN_POINT('Ctrl Pts',(-83.4719873504646,5.86895033438173,
130.053792476049));
#155279=CARTESIAN_POINT('Ctrl Pts',(-83.4759233999054,5.85839346067233,
129.971244651195));
#155280=CARTESIAN_POINT('Ctrl Pts',(-83.4798594493463,5.84610240185867,
129.888979991474));
#155281=CARTESIAN_POINT('Ctrl Pts',(-83.4837954987871,5.83209687197968,
129.807075985004));
#155282=CARTESIAN_POINT('Ctrl Pts',(-83.4912187651925,5.80568287972549,
129.652607584938));
#155283=CARTESIAN_POINT('Ctrl Pts',(-83.4986420315979,5.77308785319627,
129.498955733639));
#155284=CARTESIAN_POINT('Ctrl Pts',(-83.5060652980034,5.73437199963621,
129.346654085959));
#155285=CARTESIAN_POINT('Ctrl Pts',(-83.5134797907244,5.6957019049999,129.19453244618));
#155286=CARTESIAN_POINT('Ctrl Pts',(-83.5208942834454,5.65092547433633,
129.043758191772));
#155287=CARTESIAN_POINT('Ctrl Pts',(-83.5283087761665,5.60015439211455,
128.894857711839));
#155288=CARTESIAN_POINT('Ctrl Pts',(-83.5357161225202,5.54943224497331,
128.746100747794));
#155289=CARTESIAN_POINT('Ctrl Pts',(-83.543123468874,5.4927270685423,128.599214313756));
#155290=CARTESIAN_POINT('Ctrl Pts',(-83.5505308152278,5.43020107622494,
128.454712381283));
#155291=CARTESIAN_POINT('Ctrl Pts',(-83.5579326369032,5.36772171815161,
128.310318223804));
#155292=CARTESIAN_POINT('Ctrl Pts',(-83.5653344585786,5.29943033607883,
128.168305367879));
#155293=CARTESIAN_POINT('Ctrl Pts',(-83.572736280254,5.22553820031607,128.029170339488));
#155294=CARTESIAN_POINT('Ctrl Pts',(-83.5801341945653,5.1516850716366,127.890108759396));
#155295=CARTESIAN_POINT('Ctrl Pts',(-83.5875321088768,5.0722372521146,127.753922310164));
#155296=CARTESIAN_POINT('Ctrl Pts',(-83.5949300231882,4.98745308891698,
127.621085221319));
#155297=CARTESIAN_POINT('Ctrl Pts',(-83.6023267081004,4.90268301530926,
127.488270207588));
#155298=CARTESIAN_POINT('Ctrl Pts',(-83.6097233930125,4.81257855871012,
127.358803763909));
#155299=CARTESIAN_POINT('Ctrl Pts',(-83.6171200779247,4.71744281005215,
127.233133392033));
#155300=CARTESIAN_POINT('Ctrl Pts',(-83.6245164348601,4.62231127981298,
127.107468592513));
#155301=CARTESIAN_POINT('Ctrl Pts',(-83.6319127917957,4.52214912641339,
126.985599827747));
#155302=CARTESIAN_POINT('Ctrl Pts',(-83.6393091487311,4.41730119699303,
126.867943376274));
#155303=CARTESIAN_POINT('Ctrl Pts',(-83.6467066380677,4.31243721508671,
126.750268911296));
#155304=CARTESIAN_POINT('Ctrl Pts',(-83.6541041274043,4.20288627708352,
126.636808322438));
#155305=CARTESIAN_POINT('Ctrl Pts',(-83.6615016167408,4.08903161541035,
126.52794260588));
#155306=CARTESIAN_POINT('Ctrl Pts',(-83.6689016992559,3.9751370421622,126.419038726614));
#155307=CARTESIAN_POINT('Ctrl Pts',(-83.6763017817709,3.85693601114403,
126.314733184414));
#155308=CARTESIAN_POINT('Ctrl Pts',(-83.6837018642859,3.73484636593445,
126.215368006397));
#155309=CARTESIAN_POINT('Ctrl Pts',(-83.6911100839524,3.61262247060866,
126.115893566151));
#155310=CARTESIAN_POINT('Ctrl Pts',(-83.6985183036188,3.48650171148146,
126.021370574806));
#155311=CARTESIAN_POINT('Ctrl Pts',(-83.7059265232853,3.35693315680455,
125.932099300349));
#155312=CARTESIAN_POINT('Ctrl Pts',(-83.7133393025874,3.2272848548442,125.842773080913));
#155313=CARTESIAN_POINT('Ctrl Pts',(-83.7207520818894,3.09418484374474,
125.758705218099));
#155314=CARTESIAN_POINT('Ctrl Pts',(-83.7281648611915,2.95810808284002,
125.680150714299));
#155315=CARTESIAN_POINT('Ctrl Pts',(-83.7355882322202,2.82183688907815,
125.60148396814));
#155316=CARTESIAN_POINT('Ctrl Pts',(-83.7430116032491,2.6825807802918,125.528346487734));
#155317=CARTESIAN_POINT('Ctrl Pts',(-83.7504349742778,2.54083677815922,
125.460946069802));
#155318=CARTESIAN_POINT('Ctrl Pts',(-83.7543710237185,2.46568070712909,
125.425208750965));
#155319=CARTESIAN_POINT('Ctrl Pts',(-83.7583070731592,2.38982550153584,
125.39108350884));
#155320=CARTESIAN_POINT('Ctrl Pts',(-83.7622431226,2.31334701024829,125.358595641672));
#155321=CARTESIAN_POINT('Ctrl Pts',(-83.7696663890055,2.16911096248821,
125.297324538102));
#155322=CARTESIAN_POINT('Ctrl Pts',(-83.777089655411,2.02222090032576,125.241695078277));
#155323=CARTESIAN_POINT('Ctrl Pts',(-83.7845129218165,1.87315834618837,
125.191945061622));
#155324=CARTESIAN_POINT('Ctrl Pts',(-83.7919274145376,1.7242719716111,125.142253845354));
#155325=CARTESIAN_POINT('Ctrl Pts',(-83.7993419072586,1.57321856672915,
125.098428357233));
#155326=CARTESIAN_POINT('Ctrl Pts',(-83.8067563999797,1.4205013657857,125.060659160117));
#155327=CARTESIAN_POINT('Ctrl Pts',(-83.8141637463335,1.26793135943022,
125.022926366376));
#155328=CARTESIAN_POINT('Ctrl Pts',(-83.8215710926874,1.11370110947068,
124.991238331783));
#155329=CARTESIAN_POINT('Ctrl Pts',(-83.8289784390413,0.958330715042835,
124.96573639579));
#155330=CARTESIAN_POINT('Ctrl Pts',(-83.8363802607168,0.803076201716939,
124.940253480104));
#155331=CARTESIAN_POINT('Ctrl Pts',(-83.8437820823923,0.646683603893124,
124.92094753647));
#155332=CARTESIAN_POINT('Ctrl Pts',(-83.8511839040678,0.489684859701897,
124.907909201614));
#155333=CARTESIAN_POINT('Ctrl Pts',(-83.8585818183792,0.332768993925651,
124.894877749594));
#155334=CARTESIAN_POINT('Ctrl Pts',(-83.8659797326906,0.175247990112921,
124.888107347889));
#155335=CARTESIAN_POINT('Ctrl Pts',(-83.873377647002,0.0176604739472239,
124.887636974353));
#155336=CARTESIAN_POINT('Ctrl Pts',(-83.8807743319143,-0.139900854031991,
124.887166678984));
#155337=CARTESIAN_POINT('Ctrl Pts',(-83.8881710168266,-0.297528299496211,
124.89299433501));
#155338=CARTESIAN_POINT('Ctrl Pts',(-83.8955677017389,-0.454681538496048,
124.905106829073));
#155339=CARTESIAN_POINT('Ctrl Pts',(-83.9029640586744,-0.611827809156583,
124.917218786055));
#155340=CARTESIAN_POINT('Ctrl Pts',(-83.9103604156099,-0.768499542967437,
124.935614998284));
#155341=CARTESIAN_POINT('Ctrl Pts',(-83.9177567725454,-0.924160114702367,
124.960230344814));
#155342=CARTESIAN_POINT('Ctrl Pts',(-83.925154261882,-1.07984451846821,
124.984849460016));
#155343=CARTESIAN_POINT('Ctrl Pts',(-83.9325517512187,-1.23451708316797,
125.015689547096));
#155344=CARTESIAN_POINT('Ctrl Pts',(-83.9399492405553,-1.38765011943543,
125.052634119502));
#155345=CARTESIAN_POINT('Ctrl Pts',(-83.9473493230704,-1.54083683625116,
125.08959164277));
#155346=CARTESIAN_POINT('Ctrl Pts',(-83.9547494055855,-1.69248258747714,
125.132657824431));
#155347=CARTESIAN_POINT('Ctrl Pts',(-83.9621494881005,-1.84207376135324,
125.181665994858));
#155348=CARTESIAN_POINT('Ctrl Pts',(-83.9695577077671,-1.99182942610357,
125.230728054806));
#155349=CARTESIAN_POINT('Ctrl Pts',(-83.9769659274336,-2.1395256467322,
125.285745035712));
#155350=CARTESIAN_POINT('Ctrl Pts',(-83.9843741471001,-2.28466706691807,
125.34650142592));
#155351=CARTESIAN_POINT('Ctrl Pts',(-83.9917869264023,-2.42989781922626,
125.407295210671));
#155352=CARTESIAN_POINT('Ctrl Pts',(-83.9991997057044,-2.57257030028518,
125.473835286277));
#155353=CARTESIAN_POINT('Ctrl Pts',(-84.0066124850065,-2.71221324224078,
125.545859891017));
#155354=CARTESIAN_POINT('Ctrl Pts',(-84.0140358560354,-2.85205571258064,
125.617987407891));
#155355=CARTESIAN_POINT('Ctrl Pts',(-84.0214592270643,-2.98885967452723,
125.695614921511));
#155356=CARTESIAN_POINT('Ctrl Pts',(-84.0288825980931,-3.1221816504556,
125.778436592667));
#155357=CARTESIAN_POINT('Ctrl Pts',(-84.0328186475332,-3.19287216109585,
125.822350629984));
#155358=CARTESIAN_POINT('Ctrl Pts',(-84.0367546969732,-3.26258428524958,
125.86772423585));
#155359=CARTESIAN_POINT('Ctrl Pts',(-84.0406907464133,-3.33125574062314,
125.914507270781));
#155360=CARTESIAN_POINT('Ctrl Pts',(-84.0480807349862,-3.46018737073213,
126.002343081487));
#155361=CARTESIAN_POINT('Ctrl Pts',(-84.0554707235591,-3.58584624170242,
126.09542051636));
#155362=CARTESIAN_POINT('Ctrl Pts',(-84.0628607121321,-3.70777436591683,
126.193467015025));
#155363=CARTESIAN_POINT('Ctrl Pts',(-84.0702419467397,-3.82955805762495,
126.291397370663));
#155364=CARTESIAN_POINT('Ctrl Pts',(-84.0776231813473,-3.94761950699797,
126.394284841588));
#155365=CARTESIAN_POINT('Ctrl Pts',(-84.0850044159549,-4.06152853707728,
126.501812941478));
#155366=CARTESIAN_POINT('Ctrl Pts',(-84.0923785549292,-4.17532806559606,
126.609237673842));
#155367=CARTESIAN_POINT('Ctrl Pts',(-84.0997526939036,-4.28498284807336,
126.721293898398));
#155368=CARTESIAN_POINT('Ctrl Pts',(-84.1071268328779,-4.39009486258093,
126.837624218454));
#155369=CARTESIAN_POINT('Ctrl Pts',(-84.1144955286214,-4.49512928851112,
126.953868669125));
#155370=CARTESIAN_POINT('Ctrl Pts',(-84.1218642243649,-4.59562737058503,
127.07438065576));
#155371=CARTESIAN_POINT('Ctrl Pts',(-84.1292329201084,-4.69122725126851,
127.198765321439));
#155372=CARTESIAN_POINT('Ctrl Pts',(-84.1368325820951,-4.78982363853225,
127.3270487312));
#155373=CARTESIAN_POINT('Ctrl Pts',(-84.1444322440818,-4.88320944683711,
127.459451278672));
#155374=CARTESIAN_POINT('Ctrl Pts',(-84.1520319060684,-4.97103155000614,
127.595501647255));
#155375=CARTESIAN_POINT('Ctrl Pts',(-84.1593956889991,-5.05612782210165,
127.727329271121));
#155376=CARTESIAN_POINT('Ctrl Pts',(-84.1667594719297,-5.13600040644814,
127.862581303961));
#155377=CARTESIAN_POINT('Ctrl Pts',(-84.1741232548603,-5.21037154955868,
128.000798797657));
#155378=CARTESIAN_POINT('Ctrl Pts',(-84.1814869129748,-5.28474143207755,
128.139013948566));
#155379=CARTESIAN_POINT('Ctrl Pts',(-84.1888505710893,-5.35360987989874,
128.280194128444));
#155380=CARTESIAN_POINT('Ctrl Pts',(-84.1962142292037,-5.4167449851209,
128.42385556009));
#155381=CARTESIAN_POINT('Ctrl Pts',(-84.2035792504389,-5.47989177757308,
128.567543585565));
#155382=CARTESIAN_POINT('Ctrl Pts',(-84.2109442716741,-5.53730296312743,
128.713713431915));
#155383=CARTESIAN_POINT('Ctrl Pts',(-84.2183092929092,-5.58879476948356,
128.861861302999));
#155384=CARTESIAN_POINT('Ctrl Pts',(-84.2256771657943,-5.6403065128644,
129.010066535204));
#155385=CARTESIAN_POINT('Ctrl Pts',(-84.2330450386795,-5.68589419122215,
129.16025096082));
#155386=CARTESIAN_POINT('Ctrl Pts',(-84.2404129115646,-5.72542394021127,
129.311895788045));
#155387=CARTESIAN_POINT('Ctrl Pts',(-84.247788868667,-5.76499706224492,
129.463707003827));
#155388=CARTESIAN_POINT('Ctrl Pts',(-84.2551648257693,-5.79849888988038,
129.616981455431));
#155389=CARTESIAN_POINT('Ctrl Pts',(-84.2625407828717,-5.8258465888192,
129.771189728485));
#155390=CARTESIAN_POINT('Ctrl Pts',(-84.269921586644,-5.85321225766608,
129.925499330302));
#155391=CARTESIAN_POINT('Ctrl Pts',(-84.2773023904166,-5.87441569162345,
130.080743603662));
#155392=CARTESIAN_POINT('Ctrl Pts',(-84.2846831941889,-5.8894259978173,
130.236388806));
#155393=CARTESIAN_POINT('Ctrl Pts',(-84.2920738499913,-5.90445634003871,
130.392241766362));
#155394=CARTESIAN_POINT('Ctrl Pts',(-84.2994645057937,-5.91327703278537,
130.548496349418));
#155395=CARTESIAN_POINT('Ctrl Pts',(-84.3068551615961,-5.91590924399315,
130.704619054833));
#155396=CARTESIAN_POINT('Ctrl Pts',(-84.3084450436602,-5.91647548675968,
130.738204259687));
#155397=CARTESIAN_POINT('Ctrl Pts',(-84.3100349257242,-5.91675553673264,
130.771783382383));
#155398=CARTESIAN_POINT('Ctrl Pts',(-84.3116248077882,-5.91674991708632,
130.805351152296));
#155399=CARTESIAN_POINT('',(-86.0616248077884,-5.91524629155455,130.798916926214));
#155400=CARTESIAN_POINT('Ctrl Pts',(-84.3116248077882,-5.92633068612177,
130.805352756231));
#155401=CARTESIAN_POINT('Ctrl Pts',(-84.3141293286007,-5.92645332124771,
130.858317280176));
#155402=CARTESIAN_POINT('Ctrl Pts',(-84.3166338494132,-5.92580498622787,
130.911278725251));
#155403=CARTESIAN_POINT('Ctrl Pts',(-84.3191383702257,-5.92437648619433,
130.964219118996));
#155404=CARTESIAN_POINT('Ctrl Pts',(-84.4119542448301,-5.87143722558873,
132.926154880442));
#155405=CARTESIAN_POINT('Ctrl Pts',(-84.5975859940389,-3.62261037746975,
136.79220284857));
#155406=CARTESIAN_POINT('Ctrl Pts',(-84.8760336178514,3.07963185724678,
137.088740312823));
#155407=CARTESIAN_POINT('Ctrl Pts',(-85.1544812416647,6.95184286353423,
131.610239846154));
#155408=CARTESIAN_POINT('Ctrl Pts',(-85.4329288654772,4.43564989463864,
125.391175737797));
#155409=CARTESIAN_POINT('Ctrl Pts',(-85.7113764892903,-2.15668863388649,
124.146564085169));
#155410=CARTESIAN_POINT('Ctrl Pts',(-85.9209418033934,-5.62660433157627,
127.814517552592));
#155411=CARTESIAN_POINT('Ctrl Pts',(-86.0376912428933,-5.9198278487999,
130.290313715552));
#155412=CARTESIAN_POINT('Ctrl Pts',(-86.0616248077884,-5.91524629155455,
130.798916926214));
#155413=CARTESIAN_POINT('',(-87.8116248459704,-5.91288564422817,130.805748365634));
#155414=CARTESIAN_POINT('Ctrl Pts',(-86.0616248077884,-5.91524629155455,
130.798916926214));
#155415=CARTESIAN_POINT('Ctrl Pts',(-86.1305071174976,-5.90206028075724,
132.262709053696));
#155416=CARTESIAN_POINT('Ctrl Pts',(-86.2922053018102,-4.61319546921273,
135.719633866992));
#155417=CARTESIAN_POINT('Ctrl Pts',(-86.546719360729,1.19009585987408,137.70082582626));
#155418=CARTESIAN_POINT('Ctrl Pts',(-86.8251669845419,6.44546738008766,
133.530807166203));
#155419=CARTESIAN_POINT('Ctrl Pts',(-87.1036146083547,5.77776925657911,
126.855317322279));
#155420=CARTESIAN_POINT('Ctrl Pts',(-87.3820622321676,-0.199416554002256,
123.808805345226));
#155421=CARTESIAN_POINT('Ctrl Pts',(-87.6180656319783,-5.11016985858347,
126.675333768416));
#155422=CARTESIAN_POINT('Ctrl Pts',(-87.7612531571857,-5.9049894213493,
129.731655556594));
#155423=CARTESIAN_POINT('Ctrl Pts',(-87.8116248077884,-5.90722993476821,
130.805746223546));
#155424=CARTESIAN_POINT('',(-89.5616248077884,-5.91765122622102,130.809325232297));
#155425=CARTESIAN_POINT('Ctrl Pts',(-87.8116248720577,-5.9167498369114,
130.805749829188));
#155426=CARTESIAN_POINT('Ctrl Pts',(-87.8195256863451,-5.91671021723652,
130.974492806248));
#155427=CARTESIAN_POINT('Ctrl Pts',(-87.8274265006325,-5.90944765888795,
131.143044400043));
#155428=CARTESIAN_POINT('Ctrl Pts',(-87.8353273149198,-5.89503649630339,
131.310794492569));
#155429=CARTESIAN_POINT('Ctrl Pts',(-87.8432437624533,-5.88059681852492,
131.478876510184));
#155430=CARTESIAN_POINT('Ctrl Pts',(-87.8511602099868,-5.85898030346369,
131.646153571259));
#155431=CARTESIAN_POINT('Ctrl Pts',(-87.8590766575203,-5.83031251647461,
131.812024511302));
#155432=CARTESIAN_POINT('Ctrl Pts',(-87.8670169080892,-5.80155853168713,
131.978394189175));
#155433=CARTESIAN_POINT('Ctrl Pts',(-87.874957158658,-5.76571090722074,
132.14334900184));
#155434=CARTESIAN_POINT('Ctrl Pts',(-87.8828974092269,-5.72294601732455,
132.306299179988));
#155435=CARTESIAN_POINT('Ctrl Pts',(-87.8908505397602,-5.68011175804805,
132.469513681343));
#155436=CARTESIAN_POINT('Ctrl Pts',(-87.8988036702936,-5.63033790661179,
132.630716778108));
#155437=CARTESIAN_POINT('Ctrl Pts',(-87.9067568008269,-5.57384969476232,
132.789336723895));
#155438=CARTESIAN_POINT('Ctrl Pts',(-87.9147293056713,-5.51722387418352,
132.948343077545));
#155439=CARTESIAN_POINT('Ctrl Pts',(-87.9227018105157,-5.45385108760204,
133.104753426786));
#155440=CARTESIAN_POINT('Ctrl Pts',(-87.9306743153601,-5.38400431265361,
133.258016690415));
#155441=CARTESIAN_POINT('Ctrl Pts',(-87.9334353701712,-5.35981482920035,
133.311095149403));
#155442=CARTESIAN_POINT('Ctrl Pts',(-87.9361964249824,-5.33484925618582,
133.363796385668));
#155443=CARTESIAN_POINT('Ctrl Pts',(-87.9389574797935,-5.30912016458389,
133.416098284429));
#155444=CARTESIAN_POINT('Ctrl Pts',(-87.9463807461987,-5.23994591257194,
133.55671516984));
#155445=CARTESIAN_POINT('Ctrl Pts',(-87.9538040126041,-5.16507665292041,
133.694794571345));
#155446=CARTESIAN_POINT('Ctrl Pts',(-87.9612272790093,-5.08472159737783,
133.829841875095));
#155447=CARTESIAN_POINT('Ctrl Pts',(-87.9686417717301,-5.00446151483783,
133.964729564147));
#155448=CARTESIAN_POINT('Ctrl Pts',(-87.9760562644508,-4.91872873137602,
134.096591971124));
#155449=CARTESIAN_POINT('Ctrl Pts',(-87.9834707571716,-4.82777975612728,
134.224956061173));
#155450=CARTESIAN_POINT('Ctrl Pts',(-87.9908781035252,-4.73691844092507,
134.35319642908));
#155451=CARTESIAN_POINT('Ctrl Pts',(-87.9982854498788,-4.64085115718459,
134.477944890121));
#155452=CARTESIAN_POINT('Ctrl Pts',(-88.0056927962324,-4.53987933977658,
134.598754659145));
#155453=CARTESIAN_POINT('Ctrl Pts',(-88.0130946179076,-4.43898283095945,
134.719474323686));
#155454=CARTESIAN_POINT('Ctrl Pts',(-88.0204964395829,-4.33318931038353,
134.836260860222));
#155455=CARTESIAN_POINT('Ctrl Pts',(-88.0278982612581,-4.22284229993852,
134.948698136682));
#155456=CARTESIAN_POINT('Ctrl Pts',(-88.0352961755693,-4.11255354082138,
135.061076058378));
#155457=CARTESIAN_POINT('Ctrl Pts',(-88.0426940898805,-3.99771633983363,
135.169109026722));
#155458=CARTESIAN_POINT('Ctrl Pts',(-88.0500920041917,-3.87871303033228,
135.272415652011));
#155459=CARTESIAN_POINT('Ctrl Pts',(-88.0574886891037,-3.7597294970222,
135.375705109613));
#155460=CARTESIAN_POINT('Ctrl Pts',(-88.0648853740157,-3.63658151089322,
135.474269538537));
#155461=CARTESIAN_POINT('Ctrl Pts',(-88.0722820589278,-3.50968672178958,
135.567765878238));
#155462=CARTESIAN_POINT('Ctrl Pts',(-88.0796784158631,-3.38279755933387,
135.661258072212));
#155463=CARTESIAN_POINT('Ctrl Pts',(-88.0870747727984,-3.25216222477146,
135.749682402359));
#155464=CARTESIAN_POINT('Ctrl Pts',(-88.0944711297337,-3.118229543706,135.83273759978));
#155465=CARTESIAN_POINT('Ctrl Pts',(-88.1018686190701,-2.98427635720516,
135.915805513164));
#155466=CARTESIAN_POINT('Ctrl Pts',(-88.1092661084065,-2.84702513628258,
135.993502460308));
#155467=CARTESIAN_POINT('Ctrl Pts',(-88.1166635977429,-2.70695149782632,
136.065571899288));
#155468=CARTESIAN_POINT('Ctrl Pts',(-88.1240636802577,-2.56682875677344,
136.137666602097));
#155469=CARTESIAN_POINT('Ctrl Pts',(-88.1314637627726,-2.42388196004227,
136.204129698402));
#155470=CARTESIAN_POINT('Ctrl Pts',(-88.1388638452875,-2.27860885041737,
136.264751837003));
#155471=CARTESIAN_POINT('Ctrl Pts',(-88.1462720649538,-2.1331759980738,
136.325440635877));
#155472=CARTESIAN_POINT('Ctrl Pts',(-88.1536802846201,-1.98541206901908,
136.380275506577));
#155473=CARTESIAN_POINT('Ctrl Pts',(-88.1610885042865,-1.83583289277636,
136.429096002658));
#155474=CARTESIAN_POINT('Ctrl Pts',(-88.1685012835884,-1.68616165304652,
136.477946546939));
#155475=CARTESIAN_POINT('Ctrl Pts',(-88.1759140628902,-1.53467329824412,
136.520775239082));
#155476=CARTESIAN_POINT('Ctrl Pts',(-88.1833268421921,-1.38189563509513,
136.557472385662));
#155477=CARTESIAN_POINT('Ctrl Pts',(-88.1907502132206,-1.22889967605669,
136.594221966846));
#155478=CARTESIAN_POINT('Ctrl Pts',(-88.1981735842493,-1.07461109453228,
136.624822432275));
#155479=CARTESIAN_POINT('Ctrl Pts',(-88.2055969552779,-0.919565452500392,
136.649215615003));
#155480=CARTESIAN_POINT('Ctrl Pts',(-88.2095330047208,-0.837356532780662,
136.662149465799));
#155481=CARTESIAN_POINT('Ctrl Pts',(-88.2134690541636,-0.754934833286352,
136.67333909607));
#155482=CARTESIAN_POINT('Ctrl Pts',(-88.2174051036064,-0.672380264045972,
136.682781778305));
#155483=CARTESIAN_POINT('Ctrl Pts',(-88.2248283700119,-0.51668492298055,
136.700590382294));
#155484=CARTESIAN_POINT('Ctrl Pts',(-88.2322516364172,-0.360046148254001,
136.712236043032));
#155485=CARTESIAN_POINT('Ctrl Pts',(-88.2396749028227,-0.202993156564742,
136.717627425422));
#155486=CARTESIAN_POINT('Ctrl Pts',(-88.2470893955437,-0.0461257884692195,
136.723012435645));
#155487=CARTESIAN_POINT('Ctrl Pts',(-88.2545038882647,0.111154452662149,
136.722157868729));
#155488=CARTESIAN_POINT('Ctrl Pts',(-88.2619183809857,0.268310939758517,
136.715023846181));
#155489=CARTESIAN_POINT('Ctrl Pts',(-88.2693257273395,0.425315953515783,
136.707896699674));
#155490=CARTESIAN_POINT('Ctrl Pts',(-88.2767330736932,0.582197080288214,
136.694502163438));
#155491=CARTESIAN_POINT('Ctrl Pts',(-88.284140420047,0.738415494164904,
136.674852344881));
#155492=CARTESIAN_POINT('Ctrl Pts',(-88.2915422417224,0.89451739445474,
136.655217181901));
#155493=CARTESIAN_POINT('Ctrl Pts',(-88.2989440633977,1.0499571972343,136.629336072478));
#155494=CARTESIAN_POINT('Ctrl Pts',(-88.3063458850731,1.2041991168331,136.597273101759));
#155495=CARTESIAN_POINT('Ctrl Pts',(-88.3137437993844,1.35835961332359,
136.565227056832));
#155496=CARTESIAN_POINT('Ctrl Pts',(-88.3211417136959,1.51132312143541,
136.527005725522));
#155497=CARTESIAN_POINT('Ctrl Pts',(-88.3285396280072,1.66256210669305,
136.482724625261));
#155498=CARTESIAN_POINT('Ctrl Pts',(-88.3359363129194,1.81377595877445,
136.438450883716));
#155499=CARTESIAN_POINT('Ctrl Pts',(-88.3433329978315,1.96326549888,136.388119476654));
#155500=CARTESIAN_POINT('Ctrl Pts',(-88.3507296827437,2.11051635051412,
136.331896352115));
#155501=CARTESIAN_POINT('Ctrl Pts',(-88.3581260396791,2.25776067289117,
136.275675720567));
#155502=CARTESIAN_POINT('Ctrl Pts',(-88.3655223966145,2.40276615542933,
136.213564024141));
#155503=CARTESIAN_POINT('Ctrl Pts',(-88.3729187535499,2.54503673087071,
136.145776029329));
#155504=CARTESIAN_POINT('Ctrl Pts',(-88.3803162428864,2.6873290883008,136.077977656002));
#155505=CARTESIAN_POINT('Ctrl Pts',(-88.387713732223,2.82688536788368,136.004501414465));
#155506=CARTESIAN_POINT('Ctrl Pts',(-88.3951112215596,2.96323265108595,
135.925608787499));
#155507=CARTESIAN_POINT('Ctrl Pts',(-88.4025113040746,3.0996277306168,135.846688504844));
#155508=CARTESIAN_POINT('Ctrl Pts',(-88.4099113865895,3.2328112511753,135.762348243291));
#155509=CARTESIAN_POINT('Ctrl Pts',(-88.4173114691045,3.36233803753505,
135.672893608503));
#155510=CARTESIAN_POINT('Ctrl Pts',(-88.4247196887709,3.49200725191227,
135.583340609148));
#155511=CARTESIAN_POINT('Ctrl Pts',(-88.4321279084374,3.61801139462666,
135.488662217768));
#155512=CARTESIAN_POINT('Ctrl Pts',(-88.4395361281039,3.73993665908209,
135.389205691127));
#155513=CARTESIAN_POINT('Ctrl Pts',(-88.4469489074059,3.86193696650301,
135.289687950653));
#155514=CARTESIAN_POINT('Ctrl Pts',(-88.4543616867079,3.97985311425477,
135.185386461633));
#155515=CARTESIAN_POINT('Ctrl Pts',(-88.4617744660099,4.09330752172398,
135.076685990837));
#155516=CARTESIAN_POINT('Ctrl Pts',(-88.4691978370386,4.20692403817123,
134.967830203711));
#155517=CARTESIAN_POINT('Ctrl Pts',(-88.4766212080673,4.31606582340914,
134.854563149413));
#155518=CARTESIAN_POINT('Ctrl Pts',(-88.4840445790961,4.42039445560797,
134.737303970747));
#155519=CARTESIAN_POINT('Ctrl Pts',(-88.487980628537,4.47571199973378,134.67513034062));
#155520=CARTESIAN_POINT('Ctrl Pts',(-88.4919166779781,4.52967709439935,
134.611834899044));
#155521=CARTESIAN_POINT('Ctrl Pts',(-88.495852727419,4.58224425155113,134.547483402304));
#155522=CARTESIAN_POINT('Ctrl Pts',(-88.5032759938245,4.68138426937022,
134.4261184878));
#155523=CARTESIAN_POINT('Ctrl Pts',(-88.51069926023,4.77584917742638,134.300628614471));
#155524=CARTESIAN_POINT('Ctrl Pts',(-88.5181225266355,4.8652760783635,134.171409658463));
#155525=CARTESIAN_POINT('Ctrl Pts',(-88.5255370193565,4.95459728413016,
134.04234342853));
#155526=CARTESIAN_POINT('Ctrl Pts',(-88.5329515120776,5.03889212489643,
133.909557192965));
#155527=CARTESIAN_POINT('Ctrl Pts',(-88.5403660047986,5.11783698971795,
133.773480876022));
#155528=CARTESIAN_POINT('Ctrl Pts',(-88.5477733511524,5.19670576450654,
133.637535714556));
#155529=CARTESIAN_POINT('Ctrl Pts',(-88.5551806975061,5.27023464287378,
133.498307105482));
#155530=CARTESIAN_POINT('Ctrl Pts',(-88.5625880438599,5.33814256255764,
133.356254922648));
#155531=CARTESIAN_POINT('Ctrl Pts',(-88.5699898655354,5.40599983395298,
133.214308687691));
#155532=CARTESIAN_POINT('Ctrl Pts',(-88.5773916872109,5.46824433383542,
133.069543407504));
#155533=CARTESIAN_POINT('Ctrl Pts',(-88.5847935088863,5.52464037361033,
132.922444493331));
#155534=CARTESIAN_POINT('Ctrl Pts',(-88.5921914231977,5.58100664235498,
132.775423231529));
#155535=CARTESIAN_POINT('Ctrl Pts',(-88.5995893375091,5.6315304663153,132.626071136821));
#155536=CARTESIAN_POINT('Ctrl Pts',(-88.6069872518206,5.67602388830884,
132.474894478895));
#155537=CARTESIAN_POINT('Ctrl Pts',(-88.6143839367328,5.72050991630278,
132.323742943787));
#155538=CARTESIAN_POINT('Ctrl Pts',(-88.621780621645,5.75896742599438,132.170767805002));
#155539=CARTESIAN_POINT('Ctrl Pts',(-88.6291773065572,5.79125800110753,
132.01649152102));
#155540=CARTESIAN_POINT('Ctrl Pts',(-88.6365736634927,5.82354714442264,
131.862222077811));
#155541=CARTESIAN_POINT('Ctrl Pts',(-88.6439700204282,5.84966982039167,
131.706651969501));
#155542=CARTESIAN_POINT('Ctrl Pts',(-88.6513663773637,5.86953858167827,
131.550314638059));
#155543=CARTESIAN_POINT('Ctrl Pts',(-88.6587638667003,5.88941038492301,
131.393953370973));
#155544=CARTESIAN_POINT('Ctrl Pts',(-88.666161356037,5.90302631992822,131.236825017212));
#155545=CARTESIAN_POINT('Ctrl Pts',(-88.6735588453736,5.910350755544,131.079468794363));
#155546=CARTESIAN_POINT('Ctrl Pts',(-88.6809589278886,5.91767775872933,
130.922057410534));
#155547=CARTESIAN_POINT('Ctrl Pts',(-88.6883590104036,5.9187088540938,130.764418371239));
#155548=CARTESIAN_POINT('Ctrl Pts',(-88.6957590929186,5.9134605282542,130.607091402331));
#155549=CARTESIAN_POINT('Ctrl Pts',(-88.7031673125851,5.90820643134079,
130.449591436246));
#155550=CARTESIAN_POINT('Ctrl Pts',(-88.7105755322517,5.89665913619996,
130.292404599168));
#155551=CARTESIAN_POINT('Ctrl Pts',(-88.7179837519182,5.87888712720884,
130.136066739068));
#155552=CARTESIAN_POINT('Ctrl Pts',(-88.7253965312203,5.86110417984273,
129.979632655623));
#155553=CARTESIAN_POINT('Ctrl Pts',(-88.7328093105224,5.83708894127932,
129.824048958439));
#155554=CARTESIAN_POINT('Ctrl Pts',(-88.7402220898245,5.80696103515571,
129.669841292617));
#155555=CARTESIAN_POINT('Ctrl Pts',(-88.7476454608533,5.77679008086693,
129.51541328765));
#155556=CARTESIAN_POINT('Ctrl Pts',(-88.7550688318821,5.74048910105205,
129.362365603122));
#155557=CARTESIAN_POINT('Ctrl Pts',(-88.7624922029109,5.69822780715882,
129.211209519829));
#155558=CARTESIAN_POINT('Ctrl Pts',(-88.7664282523514,5.67581985509309,
129.131062937534));
#155559=CARTESIAN_POINT('Ctrl Pts',(-88.7703643017918,5.65173705931615,
129.051447842784));
#155560=CARTESIAN_POINT('Ctrl Pts',(-88.7743003512322,5.62601015504827,
128.972438048844));
#155561=CARTESIAN_POINT('Ctrl Pts',(-88.7817236176376,5.57749001650363,
128.82342804327));
#155562=CARTESIAN_POINT('Ctrl Pts',(-88.7891468840431,5.52297242225242,
128.676121698943));
#155563=CARTESIAN_POINT('Ctrl Pts',(-88.7965701504485,5.46259427922258,
128.531038312413));
#155564=CARTESIAN_POINT('Ctrl Pts',(-88.8039846431695,5.40228749814371,
128.386126402398));
#155565=CARTESIAN_POINT('Ctrl Pts',(-88.8113991358904,5.33613409791209,
128.243432561701));
#155566=CARTESIAN_POINT('Ctrl Pts',(-88.8188136286114,5.26432086635844,
128.103461437937));
#155567=CARTESIAN_POINT('Ctrl Pts',(-88.8262209749652,5.19257685110109,
127.963625223611));
#155568=CARTESIAN_POINT('Ctrl Pts',(-88.833628321319,5.11518403392875,127.826506831742));
#155569=CARTESIAN_POINT('Ctrl Pts',(-88.8410356676727,5.03237739871642,
127.692591301021));
#155570=CARTESIAN_POINT('Ctrl Pts',(-88.8484374893481,4.94963252381674,
127.558775649556));
#155571=CARTESIAN_POINT('Ctrl Pts',(-88.8558393110234,4.86148206622286,
127.428158418919));
#155572=CARTESIAN_POINT('Ctrl Pts',(-88.8632411326988,4.76820702072042,
127.301200277237));
#155573=CARTESIAN_POINT('Ctrl Pts',(-88.8706390470101,4.67498121438846,
127.17430915577));
#155574=CARTESIAN_POINT('Ctrl Pts',(-88.8780369613215,4.57663642820413,
127.051073576446));
#155575=CARTESIAN_POINT('Ctrl Pts',(-88.8854348756328,4.47349700574649,
126.931925324101));
#155576=CARTESIAN_POINT('Ctrl Pts',(-88.892831560545,4.37037472318987,126.812796872033));
#155577=CARTESIAN_POINT('Ctrl Pts',(-88.9002282454572,4.26245962981492,
126.697754680818));
#155578=CARTESIAN_POINT('Ctrl Pts',(-88.9076249303694,4.15011646736071,
126.587197605559));
#155579=CARTESIAN_POINT('Ctrl Pts',(-88.9150212873048,4.03777828632004,
126.476645432517));
#155580=CARTESIAN_POINT('Ctrl Pts',(-88.9224176442402,3.92101269266855,
126.370578241839));
#155581=CARTESIAN_POINT('Ctrl Pts',(-88.9298140011756,3.8002212188215,126.26935794386));
#155582=CARTESIAN_POINT('Ctrl Pts',(-88.9372114905122,3.6794112514911,126.168122148795));
#155583=CARTESIAN_POINT('Ctrl Pts',(-88.9446089798487,3.5545744628249,126.071734963771));
#155584=CARTESIAN_POINT('Ctrl Pts',(-88.9520064691853,3.42614525234258,
125.980517826559));
#155585=CARTESIAN_POINT('Ctrl Pts',(-88.9594065517003,3.29767102119944,
125.889268713321));
#155586=CARTESIAN_POINT('Ctrl Pts',(-88.9668066342152,3.16560216510214,
125.803193472302));
#155587=CARTESIAN_POINT('Ctrl Pts',(-88.9742067167302,3.03040168211528,
125.722569967851));
#155588=CARTESIAN_POINT('Ctrl Pts',(-88.9816149363967,2.89505253229862,
125.641857809569));
#155589=CARTESIAN_POINT('Ctrl Pts',(-88.9890231560632,2.75656519942118,
125.566609551064));
#155590=CARTESIAN_POINT('Ctrl Pts',(-88.9964313757297,2.61542752503644,
125.497057213409));
#155591=CARTESIAN_POINT('Ctrl Pts',(-89.0038441550317,2.47420298276853,
125.42746206745));
#155592=CARTESIAN_POINT('Ctrl Pts',(-89.0112569343337,2.33032518892126,
125.363569979129));
#155593=CARTESIAN_POINT('Ctrl Pts',(-89.0186697136357,2.18430104310365,
125.305564429708));
#155594=CARTESIAN_POINT('Ctrl Pts',(-89.0260930846645,2.03806825113843,
125.247475999239));
#155595=CARTESIAN_POINT('Ctrl Pts',(-89.0335164556932,1.88968333332055,
125.195291029769));
#155596=CARTESIAN_POINT('Ctrl Pts',(-89.0409398267219,1.73966817784561,
125.14914309801));
#155597=CARTESIAN_POINT('Ctrl Pts',(-89.0448758761629,1.66012654284449,
125.124674357286));
#155598=CARTESIAN_POINT('Ctrl Pts',(-89.0488119256039,1.58012676943059,
125.10190199201));
#155599=CARTESIAN_POINT('Ctrl Pts',(-89.0527479750449,1.4997475719321,125.080840041646));
#155600=CARTESIAN_POINT('Ctrl Pts',(-89.0601712414504,1.34815491400506,
125.04111786058));
#155601=CARTESIAN_POINT('Ctrl Pts',(-89.0675945078558,1.19475382323004,
125.007362379376));
#155602=CARTESIAN_POINT('Ctrl Pts',(-89.0750177742613,1.04005520004056,
124.979739106827));
#155603=CARTESIAN_POINT('Ctrl Pts',(-89.0824322669823,0.885539417776762,
124.952148482692));
#155604=CARTESIAN_POINT('Ctrl Pts',(-89.0898467597034,0.729729519585911,
124.930675705481));
#155605=CARTESIAN_POINT('Ctrl Pts',(-89.0972612524245,0.573151043182486,
124.915436399663));
#155606=CARTESIAN_POINT('Ctrl Pts',(-89.1046685987783,0.416723483009693,
124.900211782063));
#155607=CARTESIAN_POINT('Ctrl Pts',(-89.1120759451322,0.25952918842875,
124.891208710921));
#155608=CARTESIAN_POINT('Ctrl Pts',(-89.1194832914861,0.102103250750166,
124.888491662908));
#155609=CARTESIAN_POINT('Ctrl Pts',(-89.1268851131615,-0.0552052727252053,
124.885776641372));
#155610=CARTESIAN_POINT('Ctrl Pts',(-89.134286934837,-0.212744723657578,
124.889338314234));
#155611=CARTESIAN_POINT('Ctrl Pts',(-89.1416887565125,-0.369975644361653,
124.899189274999));
#155612=CARTESIAN_POINT('Ctrl Pts',(-89.1490866708239,-0.527123564086124,
124.909035035517));
#155613=CARTESIAN_POINT('Ctrl Pts',(-89.1564845851353,-0.683962906322821,
124.925163448583));
#155614=CARTESIAN_POINT('Ctrl Pts',(-89.1638824994467,-0.839955082635276,
124.947535025007));
#155615=CARTESIAN_POINT('Ctrl Pts',(-89.1712791843589,-0.995921335877792,
124.969902883681));
#155616=CARTESIAN_POINT('Ctrl Pts',(-89.1786758692712,-1.1510403334545,
124.998511793638));
#155617=CARTESIAN_POINT('Ctrl Pts',(-89.1860725541835,-1.3047793554507,
125.033270478252));
#155618=CARTESIAN_POINT('Ctrl Pts',(-89.1934689111189,-1.45851156049757,
125.068027621629));
#155619=CARTESIAN_POINT('Ctrl Pts',(-89.2008652680544,-1.61086354752181,
125.108933915146));
#155620=CARTESIAN_POINT('Ctrl Pts',(-89.2082616249899,-1.76131379303023,
125.155847159586));
#155621=CARTESIAN_POINT('Ctrl Pts',(-89.2156591143265,-1.91178707285532,
125.202767586564));
#155622=CARTESIAN_POINT('Ctrl Pts',(-89.2230566036631,-2.06035767502607,
125.255696684538));
#155623=CARTESIAN_POINT('Ctrl Pts',(-89.2304540929998,-2.20652036129021,
125.314442725857));
#155624=CARTESIAN_POINT('Ctrl Pts',(-89.2378541755148,-2.35273428465765,
125.373209360509));
#155625=CARTESIAN_POINT('Ctrl Pts',(-89.2452542580299,-2.49653826538684,
125.437796859254));
#155626=CARTESIAN_POINT('Ctrl Pts',(-89.252654340545,-2.63744826656805,
125.507965881174));
#155627=CARTESIAN_POINT('Ctrl Pts',(-89.2600625602115,-2.77851321278125,
125.578212061148));
#155628=CARTESIAN_POINT('Ctrl Pts',(-89.267470779878,-2.91667748996452,
125.654051854702));
#155629=CARTESIAN_POINT('Ctrl Pts',(-89.2748789995446,-3.05148220194328,
125.735200239976));
#155630=CARTESIAN_POINT('Ctrl Pts',(-89.2822917788467,-3.18636988397292,
125.816398570729));
#155631=CARTESIAN_POINT('Ctrl Pts',(-89.2897045581488,-3.31789356938112,
125.902911799136));
#155632=CARTESIAN_POINT('Ctrl Pts',(-89.2971173374509,-3.4456248985642,
125.994412632307));
#155633=CARTESIAN_POINT('Ctrl Pts',(-89.3045407084797,-3.57353873626059,
126.08604420616));
#155634=CARTESIAN_POINT('Ctrl Pts',(-89.3119640795085,-3.69764910161482,
126.182677389314));
#155635=CARTESIAN_POINT('Ctrl Pts',(-89.3193874505374,-3.81756151943951,
126.283945303926));
#155636=CARTESIAN_POINT('Ctrl Pts',(-89.3233234999776,-3.88114196062024,
126.337639982135));
#155637=CARTESIAN_POINT('Ctrl Pts',(-89.3272595494179,-3.94354282809521,
126.392637037533));
#155638=CARTESIAN_POINT('Ctrl Pts',(-89.3311955988581,-4.00470976305055,
126.448877834197));
#155639=CARTESIAN_POINT('Ctrl Pts',(-89.3385080480173,-4.11834657297179,
126.553362793676));
#155640=CARTESIAN_POINT('Ctrl Pts',(-89.3458204971765,-4.22808804895773,
126.662479011971));
#155641=CARTESIAN_POINT('Ctrl Pts',(-89.3531329463357,-4.33352468703351,
126.775900074211));
#155642=CARTESIAN_POINT('Ctrl Pts',(-89.3604366596762,-4.43883536521067,
126.889185637958));
#155643=CARTESIAN_POINT('Ctrl Pts',(-89.3677403730167,-4.53985117746494,
127.006765534692));
#155644=CARTESIAN_POINT('Ctrl Pts',(-89.3750440863571,-4.63619615567382,
127.128273598926));
#155645=CARTESIAN_POINT('Ctrl Pts',(-89.3823407809178,-4.73244854752861,
127.249664895386));
#155646=CARTESIAN_POINT('Ctrl Pts',(-89.3896374754785,-4.82403879937958,
127.374976547731));
#155647=CARTESIAN_POINT('Ctrl Pts',(-89.3969341700392,-4.9106284511203,
127.503806303887));
#155648=CARTESIAN_POINT('Ctrl Pts',(-89.4042252189038,-4.99715110555869,
127.632536380162));
#155649=CARTESIAN_POINT('Ctrl Pts',(-89.4115162677685,-5.07868064890465,
127.764778822264));
#155650=CARTESIAN_POINT('Ctrl Pts',(-89.4188073166332,-5.15491973223651,
127.90009941776));
#155651=CARTESIAN_POINT('Ctrl Pts',(-89.4260953266394,-5.23112703964872,
128.035363612573));
#155652=CARTESIAN_POINT('Ctrl Pts',(-89.4333833366456,-5.3020480845713,
128.17370307362));
#155653=CARTESIAN_POINT('Ctrl Pts',(-89.4406713466518,-5.36742963650288,
128.314655884131));
#155654=CARTESIAN_POINT('Ctrl Pts',(-89.4479578575399,-5.43279773967874,
128.455579701142));
#155655=CARTESIAN_POINT('Ctrl Pts',(-89.4552443684281,-5.49262845538774,
128.599115448444));
#155656=CARTESIAN_POINT('Ctrl Pts',(-89.4625308793163,-5.54671533715024,
128.744778249433));
#155657=CARTESIAN_POINT('Ctrl Pts',(-89.4698174294749,-5.60080251041268,
128.890441835469));
#155658=CARTESIAN_POINT('Ctrl Pts',(-89.4771039796335,-5.6491456554883,
129.038232136214));
#155659=CARTESIAN_POINT('Ctrl Pts',(-89.4843905297921,-5.69158725130675,
129.187646318977));
#155660=CARTESIAN_POINT('Ctrl Pts',(-89.4916815851253,-5.73405508818516,
129.337152882492));
#155661=CARTESIAN_POINT('Ctrl Pts',(-89.4989726404585,-5.77061398263426,
129.488284962247));
#155662=CARTESIAN_POINT('Ctrl Pts',(-89.5062636957917,-5.80115681224227,
129.640526350037));
#155663=CARTESIAN_POINT('Ctrl Pts',(-89.5135572427252,-5.8317100793684,
129.792819763859));
#155664=CARTESIAN_POINT('Ctrl Pts',(-89.5208507896587,-5.85624312395901,
129.946222860742));
#155665=CARTESIAN_POINT('Ctrl Pts',(-89.5281443365922,-5.87470046014896,
130.100212148828));
#155666=CARTESIAN_POINT('Ctrl Pts',(-89.5354455288377,-5.89317714386569,
130.25436285305));
#155667=CARTESIAN_POINT('Ctrl Pts',(-89.5427467210833,-5.90556537004156,
130.409100591828));
#155668=CARTESIAN_POINT('Ctrl Pts',(-89.5500479133288,-5.9118617108521,
130.563899239667));
#155669=CARTESIAN_POINT('Ctrl Pts',(-89.5539068781487,-5.9151895725033,
130.645716361596));
#155670=CARTESIAN_POINT('Ctrl Pts',(-89.5577658429685,-5.91681652206415,
130.727550517598));
#155671=CARTESIAN_POINT('Ctrl Pts',(-89.5616248077884,-5.91674791778598,
130.809324474466));
#155672=CARTESIAN_POINT('',(-91.3116248077885,-5.92354848925726,130.800631107972));
#155673=CARTESIAN_POINT('Ctrl Pts',(-89.5616248077884,-5.92034638875527,
130.809327493404));
#155674=CARTESIAN_POINT('Ctrl Pts',(-89.5776309460825,-5.92339549946666,
131.148716982508));
#155675=CARTESIAN_POINT('Ctrl Pts',(-89.5936370843766,-5.89673577148018,
131.487627614299));
#155676=CARTESIAN_POINT('Ctrl Pts',(-89.702459097275,-5.50197556203136,
133.754623470739));
#155677=CARTESIAN_POINT('Ctrl Pts',(-89.8880908464838,-2.71663448732176,
137.253969721429));
#155678=CARTESIAN_POINT('Ctrl Pts',(-90.1665384702964,3.95783150361734,
136.576113411936));
#155679=CARTESIAN_POINT('Ctrl Pts',(-90.4449860941093,6.99524369355141,
130.594298250215));
#155680=CARTESIAN_POINT('Ctrl Pts',(-90.7234337179224,3.60436866576331,
124.805520141973));
#155681=CARTESIAN_POINT('Ctrl Pts',(-91.001881341735,-3.09874508266306,
124.529383371151));
#155682=CARTESIAN_POINT('Ctrl Pts',(-91.1979450383571,-5.81353639408446,
128.395248006798));
#155683=CARTESIAN_POINT('Ctrl Pts',(-91.3011928603751,-5.92517256730769,
130.579746351147));
#155684=CARTESIAN_POINT('Ctrl Pts',(-91.3116248077885,-5.92354848925726,
130.800631107972));
#155685=CARTESIAN_POINT('',(-93.0616248077885,-5.90861108400418,130.801194235313));
#155686=CARTESIAN_POINT('Ctrl Pts',(-91.3116248077885,-5.92354848925726,
130.800631107972));
#155687=CARTESIAN_POINT('Ctrl Pts',(-91.3940087349794,-5.91072270299169,
132.545018133961));
#155688=CARTESIAN_POINT('Ctrl Pts',(-91.569208536774,-4.17203293217058,
136.276898039585));
#155689=CARTESIAN_POINT('Ctrl Pts',(-91.837224213174,2.17694268671267,137.455562093173));
#155690=CARTESIAN_POINT('Ctrl Pts',(-92.1156718369866,6.77253487019274,
132.567973943205));
#155691=CARTESIAN_POINT('Ctrl Pts',(-92.3941194608,5.1444983646849,126.059711304276));
#155692=CARTESIAN_POINT('Ctrl Pts',(-92.6725670846125,-1.21108081525124,
123.911549595256));
#155693=CARTESIAN_POINT('Ctrl Pts',(-92.895068866942,-5.40037890449579,
127.256492211878));
#155694=CARTESIAN_POINT('Ctrl Pts',(-93.0247547746675,-5.91240923823485,
130.015461788493));
#155695=CARTESIAN_POINT('Ctrl Pts',(-93.0616248077885,-5.90861108400418,
130.801194235313));
#155696=CARTESIAN_POINT('',(-94.8116248077886,-5.91193135788434,130.809233089015));
#155697=CARTESIAN_POINT('Ctrl Pts',(-93.0616248077885,-5.90861108400418,
130.801194235313));
#155698=CARTESIAN_POINT('Ctrl Pts',(-93.1175706492718,-5.90284784170329,
131.993448735702));
#155699=CARTESIAN_POINT('Ctrl Pts',(-93.2663323653589,-4.97304284201653,
135.171957595505));
#155700=CARTESIAN_POINT('Ctrl Pts',(-93.5079099560513,0.220707694199726,
137.799276531578));
#155701=CARTESIAN_POINT('Ctrl Pts',(-93.7863575798639,6.00431876457061,
134.399595895508));
#155702=CARTESIAN_POINT('Ctrl Pts',(-94.0648052036771,6.27025421757813,
127.696069676023));
#155703=CARTESIAN_POINT('Ctrl Pts',(-94.3432528274898,0.774132363579867,
123.848910983356));
#155704=CARTESIAN_POINT('Ctrl Pts',(-94.592192695527,-4.77555456394825,
126.123817676288));
#155705=CARTESIAN_POINT('Ctrl Pts',(-94.74831668896,-5.90153144142422,129.461984403364));
#155706=CARTESIAN_POINT('Ctrl Pts',(-94.8116248077886,-5.91193135788434,
130.809233089015));
#155707=CARTESIAN_POINT('',(-96.5616241144883,-5.921965846863,130.805557042125));
#155708=CARTESIAN_POINT('Ctrl Pts',(-94.8116248077886,-5.91193135788434,
130.809233089015));
#155709=CARTESIAN_POINT('Ctrl Pts',(-94.8411325635643,-5.9167787329236,
131.437182330294));
#155710=CARTESIAN_POINT('Ctrl Pts',(-94.963456193944,-5.53504529805508,
134.034588688322));
#155711=CARTESIAN_POINT('Ctrl Pts',(-95.1785956989288,-1.75330463822294,
137.579571564541));
#155712=CARTESIAN_POINT('Ctrl Pts',(-95.4570433227414,4.752472869827,135.94163247643));
#155713=CARTESIAN_POINT('Ctrl Pts',(-95.7354909465543,6.89095998170769,
129.582791519719));
#155714=CARTESIAN_POINT('Ctrl Pts',(-96.0139385703672,2.69699151251502,
124.346512886951));
#155715=CARTESIAN_POINT('Ctrl Pts',(-96.289316103979,-3.90181258504973,
125.036983019214));
#155716=CARTESIAN_POINT('Ctrl Pts',(-96.4718777629867,-5.92093097606058,
128.907556428895));
#155717=CARTESIAN_POINT('Ctrl Pts',(-96.56162354739,-5.9262323504286,130.80554592138));
#155718=CARTESIAN_POINT('',(-98.3116248063916,-5.9157015749469,130.798899360433));
#155719=CARTESIAN_POINT('Ctrl Pts',(-96.5616248077887,-5.91674987627087,
130.80557063768));
#155720=CARTESIAN_POINT('Ctrl Pts',(-96.5646944778568,-5.91673662110768,
130.870385663671));
#155721=CARTESIAN_POINT('Ctrl Pts',(-96.5677641479249,-5.91565837655804,
130.935188584664));
#155722=CARTESIAN_POINT('Ctrl Pts',(-96.570833817993,-5.91351612517523,
130.999956118006));
#155723=CARTESIAN_POINT('Ctrl Pts',(-96.5782570843985,-5.90833560011258,
131.156580981185));
#155724=CARTESIAN_POINT('Ctrl Pts',(-96.5856803508038,-5.89692041521548,
131.313236720677));
#155725=CARTESIAN_POINT('Ctrl Pts',(-96.5931036172093,-5.87925770863647,
131.469386450101));
#155726=CARTESIAN_POINT('Ctrl Pts',(-96.6005181099303,-5.86161587790978,
131.625351623512));
#155727=CARTESIAN_POINT('Ctrl Pts',(-96.6079326026514,-5.83774126504488,
131.78081160999));
#155728=CARTESIAN_POINT('Ctrl Pts',(-96.6153470953724,-5.80767299525278,
131.935229727017));
#155729=CARTESIAN_POINT('Ctrl Pts',(-96.6227544417262,-5.77763370639124,
132.089499010049));
#155730=CARTESIAN_POINT('Ctrl Pts',(-96.63016178808,-5.74141271592911,132.242728058824));
#155731=CARTESIAN_POINT('Ctrl Pts',(-96.6375691344338,-5.69910089664331,
132.394385627552));
#155732=CARTESIAN_POINT('Ctrl Pts',(-96.6449709561092,-5.65682063510867,
132.545930084343));
#155733=CARTESIAN_POINT('Ctrl Pts',(-96.6523727777846,-5.60845868990398,
132.695905036815));
#155734=CARTESIAN_POINT('Ctrl Pts',(-96.65977459946,-5.55415690618363,132.843789857327));
#155735=CARTESIAN_POINT('Ctrl Pts',(-96.6671725137713,-5.49988378795238,
132.991596610593));
#155736=CARTESIAN_POINT('Ctrl Pts',(-96.6745704280827,-5.43967720423761,
133.137315079766));
#155737=CARTESIAN_POINT('Ctrl Pts',(-96.681968342394,-5.37372867000152,
133.280440330278));
#155738=CARTESIAN_POINT('Ctrl Pts',(-96.6893650273062,-5.30779109521531,
133.42354179597));
#155739=CARTESIAN_POINT('Ctrl Pts',(-96.6967617122184,-5.23611361979543,
133.564050559594));
#155740=CARTESIAN_POINT('Ctrl Pts',(-96.7041583971306,-5.15893571916605,
133.701482086889));
#155741=CARTESIAN_POINT('Ctrl Pts',(-96.711554754066,-5.08176124068567,
133.838907520326));
#155742=CARTESIAN_POINT('Ctrl Pts',(-96.7189511110015,-4.99908700472486,
133.973255663251));
#155743=CARTESIAN_POINT('Ctrl Pts',(-96.726347467937,-4.91119809813897,
134.104067241394));
#155744=CARTESIAN_POINT('Ctrl Pts',(-96.7337449572736,-4.82329573553686,
134.234898847124));
#155745=CARTESIAN_POINT('Ctrl Pts',(-96.7411424466101,-4.73017732082761,
134.362192500083));
#155746=CARTESIAN_POINT('Ctrl Pts',(-96.7485399359467,-4.63217076417917,
134.485518665516));
#155747=CARTESIAN_POINT('Ctrl Pts',(-96.7559400184617,-4.53412985148437,
134.608888062744));
#155748=CARTESIAN_POINT('Ctrl Pts',(-96.7633401009766,-4.43119761732927,
134.728286911311));
#155749=CARTESIAN_POINT('Ctrl Pts',(-96.7707401834916,-4.32374155699493,
134.843319581311));
#155750=CARTESIAN_POINT('Ctrl Pts',(-96.7781484031581,-4.21616733767535,
134.958478741557));
#155751=CARTESIAN_POINT('Ctrl Pts',(-96.7855566228246,-4.10405961293047,
135.069261862239));
#155752=CARTESIAN_POINT('Ctrl Pts',(-96.7929648424911,-3.98782248718409,
135.175310442628));
#155753=CARTESIAN_POINT('Ctrl Pts',(-96.8003776217932,-3.87151381942633,
135.281424294148));
#155754=CARTESIAN_POINT('Ctrl Pts',(-96.8077904010953,-3.75107097119409,
135.382797558979));
#155755=CARTESIAN_POINT('Ctrl Pts',(-96.8152031803974,-3.62692984837114,
135.47911306422));
#155756=CARTESIAN_POINT('Ctrl Pts',(-96.8226265514261,-3.50261134689007,
135.575566189572));
#155757=CARTESIAN_POINT('Ctrl Pts',(-96.8300499224549,-3.37458431998493,
135.666946905571));
#155758=CARTESIAN_POINT('Ctrl Pts',(-96.8374732934836,-3.24331294537814,
135.752981809458));
#155759=CARTESIAN_POINT('Ctrl Pts',(-96.8414093429244,-3.17370971274992,
135.798599579877));
#155760=CARTESIAN_POINT('Ctrl Pts',(-96.8453453923651,-3.1031947873653,
135.842715219548));
#155761=CARTESIAN_POINT('Ctrl Pts',(-96.8492814418058,-3.03183987724647,
135.885293358829));
#155762=CARTESIAN_POINT('Ctrl Pts',(-96.8567047082112,-2.89726674366976,
135.965594400697));
#155763=CARTESIAN_POINT('Ctrl Pts',(-96.8641279746166,-2.75929764704575,
136.040666736073));
#155764=CARTESIAN_POINT('Ctrl Pts',(-96.8715512410221,-2.61837733294993,
136.110209343717));
#155765=CARTESIAN_POINT('Ctrl Pts',(-96.8789657337431,-2.47762357496266,
136.179669757773));
#155766=CARTESIAN_POINT('Ctrl Pts',(-96.8863802264642,-2.33392587406002,
136.243613289819));
#155767=CARTESIAN_POINT('Ctrl Pts',(-96.8937947191852,-2.18775690457629,
136.30178276699));
#155768=CARTESIAN_POINT('Ctrl Pts',(-96.9012020655389,-2.04172881824852,
136.359896178229));
#155769=CARTESIAN_POINT('Ctrl Pts',(-96.9086094118927,-1.8932345497504,
136.412246476812));
#155770=CARTESIAN_POINT('Ctrl Pts',(-96.9160167582465,-1.7427701701668,
136.458622965254));
#155771=CARTESIAN_POINT('Ctrl Pts',(-96.9234185799219,-1.59241801259418,
136.50496486436));
#155772=CARTESIAN_POINT('Ctrl Pts',(-96.9308204015973,-1.44009902487803,
136.545341715331));
#155773=CARTESIAN_POINT('Ctrl Pts',(-96.9382222232727,-1.28632789657008,
136.579591444555));
#155774=CARTESIAN_POINT('Ctrl Pts',(-96.9456201375841,-1.13263794284381,
136.613823093614));
#155775=CARTESIAN_POINT('Ctrl Pts',(-96.9530180518955,-0.977497738640905,
136.641933981555));
#155776=CARTESIAN_POINT('Ctrl Pts',(-96.9604159662068,-0.821435618230036,
136.663812305873));
#155777=CARTESIAN_POINT('Ctrl Pts',(-96.967812651119,-0.665399432512547,
136.68568699441));
#155778=CARTESIAN_POINT('Ctrl Pts',(-96.9752093360312,-0.508442003976059,
136.701331123184));
#155779=CARTESIAN_POINT('Ctrl Pts',(-96.9826060209434,-0.351100427334726,
136.710684267048));
#155780=CARTESIAN_POINT('Ctrl Pts',(-96.9900023778789,-0.193765827383783,
136.720036996183));
#155781=CARTESIAN_POINT('Ctrl Pts',(-96.9973987348144,-0.0360474858361569,
136.7230992729));
#155782=CARTESIAN_POINT('Ctrl Pts',(-97.0047950917498,0.121514100447624,
136.719862699883));
#155783=CARTESIAN_POINT('Ctrl Pts',(-97.0121925810864,0.2790998098125,136.716625631338));
#155784=CARTESIAN_POINT('Ctrl Pts',(-97.0195900704229,0.436528342883927,
136.707087800537));
#155785=CARTESIAN_POINT('Ctrl Pts',(-97.0269875597595,0.593261076452136,
136.691292913564));
#155786=CARTESIAN_POINT('Ctrl Pts',(-97.0343876422745,0.750048752436907,
136.675492489718));
#155787=CARTESIAN_POINT('Ctrl Pts',(-97.0417877247895,0.906139772107623,
136.653430680061));
#155788=CARTESIAN_POINT('Ctrl Pts',(-97.0491878073045,1.06100264064333,
136.625202821152));
#155789=CARTESIAN_POINT('Ctrl Pts',(-97.0565960269709,1.21603579682349,
136.59694392281));
#155790=CARTESIAN_POINT('Ctrl Pts',(-97.0640042466373,1.36983773740229,
136.562505501684));
#155791=CARTESIAN_POINT('Ctrl Pts',(-97.0714124663038,1.52188841725016,
136.522033763868));
#155792=CARTESIAN_POINT('Ctrl Pts',(-97.0788252456059,1.67403268175481,
136.481537116372));
#155793=CARTESIAN_POINT('Ctrl Pts',(-97.086238024908,1.82442318194635,136.434999862856));
#155794=CARTESIAN_POINT('Ctrl Pts',(-97.0936508042101,1.97255745350397,
136.382617303586));
#155795=CARTESIAN_POINT('Ctrl Pts',(-97.1010741752388,2.12090338625538,
136.330159897659));
#155796=CARTESIAN_POINT('Ctrl Pts',(-97.1084975462676,2.2669863059375,136.271840643105));
#155797=CARTESIAN_POINT('Ctrl Pts',(-97.1159209172964,2.41032529166931,
136.207902284921));
#155798=CARTESIAN_POINT('Ctrl Pts',(-97.1198569667372,2.48632706127606,
136.174000633232));
#155799=CARTESIAN_POINT('Ctrl Pts',(-97.1237930161779,2.56155783794563,
136.138520010245));
#155800=CARTESIAN_POINT('Ctrl Pts',(-97.1277290656187,2.63594910425982,
136.101501627795));
#155801=CARTESIAN_POINT('Ctrl Pts',(-97.1351523320242,2.77624871085666,
136.031686113799));
#155802=CARTESIAN_POINT('Ctrl Pts',(-97.1425755984296,2.91398485957519,
135.956187236336));
#155803=CARTESIAN_POINT('Ctrl Pts',(-97.1499988648351,3.04866389687383,
135.875216463121));
#155804=CARTESIAN_POINT('Ctrl Pts',(-97.1574133575561,3.18318375473478,
135.794341390635));
#155805=CARTESIAN_POINT('Ctrl Pts',(-97.164827850277,3.31465337656868,135.708007486114));
#155806=CARTESIAN_POINT('Ctrl Pts',(-97.1722423429981,3.44260090353974,
135.616473415646));
#155807=CARTESIAN_POINT('Ctrl Pts',(-97.1796496893518,3.57042510986717,
135.525027569162));
#155808=CARTESIAN_POINT('Ctrl Pts',(-97.1870570357057,3.69473367799984,
135.42839175061));
#155809=CARTESIAN_POINT('Ctrl Pts',(-97.1944643820595,3.81508120363753,
135.326869431505));
#155810=CARTESIAN_POINT('Ctrl Pts',(-97.2018662037349,3.93533896955015,
135.225422831575));
#155811=CARTESIAN_POINT('Ctrl Pts',(-97.2092680254103,4.05164129126286,
135.119097227521));
#155812=CARTESIAN_POINT('Ctrl Pts',(-97.2166698470857,4.16357360938068,
135.008238037493));
#155813=CARTESIAN_POINT('Ctrl Pts',(-97.2240677613971,4.27544683929903,
134.897437369168));
#155814=CARTESIAN_POINT('Ctrl Pts',(-97.2314656757085,4.38295439534775,
134.782108143152));
#155815=CARTESIAN_POINT('Ctrl Pts',(-97.2388635900198,4.48571663733404,
134.662634430043));
#155816=CARTESIAN_POINT('Ctrl Pts',(-97.246260274932,4.58846180209986,134.543180571298));
#155817=CARTESIAN_POINT('Ctrl Pts',(-97.2536569598442,4.68646297472457,
134.419583875136));
#155818=CARTESIAN_POINT('Ctrl Pts',(-97.2610536447564,4.77937900500779,
134.292263553284));
#155819=CARTESIAN_POINT('Ctrl Pts',(-97.2684500016918,4.87229091529686,
134.164948876949));
#155820=CARTESIAN_POINT('Ctrl Pts',(-97.2758463586274,4.96011791151835,
134.033911204755));
#155821=CARTESIAN_POINT('Ctrl Pts',(-97.2832427155628,5.04256077701662,
133.899600733065));
#155822=CARTESIAN_POINT('Ctrl Pts',(-97.2906402048994,5.1250162647283,133.765269698098));
#155823=CARTESIAN_POINT('Ctrl Pts',(-97.298037694236,5.20208578508113,133.627665184095));
#155824=CARTESIAN_POINT('Ctrl Pts',(-97.3054351835726,5.27351497024009,
133.487263974222));
#155825=CARTESIAN_POINT('Ctrl Pts',(-97.3128352660876,5.34496919478907,
133.346813546922));
#155826=CARTESIAN_POINT('Ctrl Pts',(-97.3202353486026,5.41077897836871,
133.203564804336));
#155827=CARTESIAN_POINT('Ctrl Pts',(-97.3276354311176,5.47073724439364,
133.058016439848));
#155828=CARTESIAN_POINT('Ctrl Pts',(-97.3350436507841,5.530761440696,132.91230802997));
#155829=CARTESIAN_POINT('Ctrl Pts',(-97.3424518704505,5.58492112735976,
132.764295293639));
#155830=CARTESIAN_POINT('Ctrl Pts',(-97.349860090117,5.63305821461801,132.614494787517));
#155831=CARTESIAN_POINT('Ctrl Pts',(-97.3572728694191,5.68122492945026,
132.464602081683));
#155832=CARTESIAN_POINT('Ctrl Pts',(-97.3646856487212,5.72336155890942,
132.31291977233));
#155833=CARTESIAN_POINT('Ctrl Pts',(-97.3720984280233,5.75936082040169,
132.159976161488));
#155834=CARTESIAN_POINT('Ctrl Pts',(-97.379521799052,5.79541151932693,132.006814017642));
#155835=CARTESIAN_POINT('Ctrl Pts',(-97.3869451700808,5.82530726514585,
131.852387338417));
#155836=CARTESIAN_POINT('Ctrl Pts',(-97.3943685411096,5.84899233661424,
131.69723194577));
#155837=CARTESIAN_POINT('Ctrl Pts',(-97.3983045905503,5.86155072982207,
131.614964833687));
#155838=CARTESIAN_POINT('Ctrl Pts',(-97.402240639991,5.87236394924333,131.532492907243));
#155839=CARTESIAN_POINT('Ctrl Pts',(-97.4061766894317,5.88142963222386,
131.449896088086));
#155840=CARTESIAN_POINT('Ctrl Pts',(-97.4135999558372,5.89852722739512,
131.294121064911));
#155841=CARTESIAN_POINT('Ctrl Pts',(-97.4210232222426,5.9094576363208,131.137430754673));
#155842=CARTESIAN_POINT('Ctrl Pts',(-97.428446488648,5.91413194098158,130.980354785542));
#155843=CARTESIAN_POINT('Ctrl Pts',(-97.435860981369,5.91880072100244,130.823464467161));
#155844=CARTESIAN_POINT('Ctrl Pts',(-97.44327547409,5.9172281039504,130.666189766683));
#155845=CARTESIAN_POINT('Ctrl Pts',(-97.450689966811,5.90937666170668,130.509067487649));
#155846=CARTESIAN_POINT('Ctrl Pts',(-97.4580973131647,5.90153278697858,
130.352096648982));
#155847=CARTESIAN_POINT('Ctrl Pts',(-97.4655046595185,5.88742215344312,
130.195278309622));
#155848=CARTESIAN_POINT('Ctrl Pts',(-97.4729120058723,5.86705932837742,
130.039151234587));
#155849=CARTESIAN_POINT('Ctrl Pts',(-97.4803138275477,5.84671169067495,
129.883140605015));
#155850=CARTESIAN_POINT('Ctrl Pts',(-97.4877156492232,5.8201211944147,129.727820581767));
#155851=CARTESIAN_POINT('Ctrl Pts',(-97.4951174708985,5.78735437019004,
129.57372665235));
#155852=CARTESIAN_POINT('Ctrl Pts',(-97.5025153852099,5.75460484331674,
129.419714067919));
#155853=CARTESIAN_POINT('Ctrl Pts',(-97.5099132995212,5.71568555923869,
129.266926652509));
#155854=CARTESIAN_POINT('Ctrl Pts',(-97.5173112138326,5.67071444262972,
129.115891407704));
#155855=CARTESIAN_POINT('Ctrl Pts',(-97.5247078987448,5.62575079940453,
128.964881262218));
#155856=CARTESIAN_POINT('Ctrl Pts',(-97.532104583657,5.57473742609889,128.815623066859));
#155857=CARTESIAN_POINT('Ctrl Pts',(-97.5395012685692,5.51784261739424,
128.66863043513));
#155858=CARTESIAN_POINT('Ctrl Pts',(-97.5468976255047,5.46095033146503,
128.521644321209));
#155859=CARTESIAN_POINT('Ctrl Pts',(-97.5542939824401,5.39817726342021,
128.376923919304));
#155860=CARTESIAN_POINT('Ctrl Pts',(-97.5616903393755,5.32974044229802,
128.234964310993));
#155861=CARTESIAN_POINT('Ctrl Pts',(-97.5690878287121,5.2612931433238,128.092982968303));
#155862=CARTESIAN_POINT('Ctrl Pts',(-97.5764853180487,5.18718052680902,
127.953763597112));
#155863=CARTESIAN_POINT('Ctrl Pts',(-97.5838828073852,5.10766623190721,
127.817777917232));
#155864=CARTESIAN_POINT('Ctrl Pts',(-97.5912828899002,5.02812406339271,
127.681744567782));
#155865=CARTESIAN_POINT('Ctrl Pts',(-97.5986829724152,4.94317663475815,
127.548947488614));
#155866=CARTESIAN_POINT('Ctrl Pts',(-97.6060830549301,4.85313158091947,
127.419830455079));
#155867=CARTESIAN_POINT('Ctrl Pts',(-97.6134912745966,4.76298751328711,
127.290571444092));
#155868=CARTESIAN_POINT('Ctrl Pts',(-97.620899494263,4.66773483983959,127.165000866421));
#155869=CARTESIAN_POINT('Ctrl Pts',(-97.6283077139295,4.56772270294536,
127.043530938958));
#155870=CARTESIAN_POINT('Ctrl Pts',(-97.6357204932315,4.46764901024965,
126.921986248781));
#155871=CARTESIAN_POINT('Ctrl Pts',(-97.6431332725336,4.36281026499271,
126.804547515795));
#155872=CARTESIAN_POINT('Ctrl Pts',(-97.6505460518356,4.25359295377042,
126.691590560034));
#155873=CARTESIAN_POINT('Ctrl Pts',(-97.6579694228644,4.14421958773192,
126.578472206077));
#155874=CARTESIAN_POINT('Ctrl Pts',(-97.6653927938932,4.03045542976861,
126.469848676225));
#155875=CARTESIAN_POINT('Ctrl Pts',(-97.672816164922,3.91272116337437,126.366056475196));
#155876=CARTESIAN_POINT('Ctrl Pts',(-97.6767522143629,3.85029563033586,
126.311023359749));
#155877=CARTESIAN_POINT('Ctrl Pts',(-97.6806882638037,3.78675447211467,
126.25734780127));
#155878=CARTESIAN_POINT('Ctrl Pts',(-97.6846243132446,3.72216365198443,
126.205074987129));
#155879=CARTESIAN_POINT('Ctrl Pts',(-97.69204757965,3.60034738103171,126.10649009104));
#155880=CARTESIAN_POINT('Ctrl Pts',(-97.6994708460555,3.47442753834198,
126.012599088388));
#155881=CARTESIAN_POINT('Ctrl Pts',(-97.7068941124609,3.34480165273408,
125.923763065384));
#155882=CARTESIAN_POINT('Ctrl Pts',(-97.7143086051819,3.21532897415821,
125.835032039182));
#155883=CARTESIAN_POINT('Ctrl Pts',(-97.7217230979029,3.08215927646435,
125.751344309189));
#155884=CARTESIAN_POINT('Ctrl Pts',(-97.7291375906239,2.94572395686344,
125.67302152017));
#155885=CARTESIAN_POINT('Ctrl Pts',(-97.7365449369777,2.80942013876025,
125.594774221604));
#155886=CARTESIAN_POINT('Ctrl Pts',(-97.7439522833314,2.66985728643288,
125.521881754306));
#155887=CARTESIAN_POINT('Ctrl Pts',(-97.7513596296852,2.52749655211978,
125.454623078067));
#155888=CARTESIAN_POINT('Ctrl Pts',(-97.7587614513606,2.38524199581328,
125.387414565886));
#155889=CARTESIAN_POINT('Ctrl Pts',(-97.7661632730361,2.24019404862509,
125.325831637004));
#155890=CARTESIAN_POINT('Ctrl Pts',(-97.7735650947115,2.09283919277186,
125.270107761426));
#155891=CARTESIAN_POINT('Ctrl Pts',(-97.7809630090228,1.94556212440044,
125.214413302048));
#155892=CARTESIAN_POINT('Ctrl Pts',(-97.7883609233342,1.79598092095095,
125.164571867925));
#155893=CARTESIAN_POINT('Ctrl Pts',(-97.7957588376455,1.64460270494951,
125.120769102919));
#155894=CARTESIAN_POINT('Ctrl Pts',(-97.8031555225577,1.49324964526107,
125.076973617137));
#155895=CARTESIAN_POINT('Ctrl Pts',(-97.8105522074699,1.34010052395105,
125.039214912448));
#155896=CARTESIAN_POINT('Ctrl Pts',(-97.8179488923821,1.1856784259921,125.007629018411));
#155897=CARTESIAN_POINT('Ctrl Pts',(-97.8253452493176,1.03126317527079,
124.976044524927));
#155898=CARTESIAN_POINT('Ctrl Pts',(-97.832741606253,0.875575425857908,
124.950632372677));
#155899=CARTESIAN_POINT('Ctrl Pts',(-97.8401379631885,0.719149013401902,
124.93147757267));
#155900=CARTESIAN_POINT('Ctrl Pts',(-97.847535452525,0.56269865166281,124.912319840015));
#155901=CARTESIAN_POINT('Ctrl Pts',(-97.8549329418616,0.405509772255039,
124.899421412516));
#155902=CARTESIAN_POINT('Ctrl Pts',(-97.8623304311981,0.248121749818079,
124.892815459169));
#155903=CARTESIAN_POINT('Ctrl Pts',(-97.8697305137131,0.0906785552540618,
124.886207190115));
#155904=CARTESIAN_POINT('Ctrl Pts',(-97.8771305962281,-0.0669635485920499,
124.885895802622));
#155905=CARTESIAN_POINT('Ctrl Pts',(-97.8845306787431,-0.224264916761973,
124.89186234614));
#155906=CARTESIAN_POINT('Ctrl Pts',(-97.8919388984096,-0.381739253957398,
124.897835450487));
#155907=CARTESIAN_POINT('Ctrl Pts',(-97.8993471180761,-0.538871733969701,
124.910100257891));
#155908=CARTESIAN_POINT('Ctrl Pts',(-97.9067553377425,-0.695126827075153,
124.92858583829));
#155909=CARTESIAN_POINT('Ctrl Pts',(-97.9141681170446,-0.8514780925836,
124.947082796254));
#155910=CARTESIAN_POINT('Ctrl Pts',(-97.9215808963467,-1.00695052732344,
124.971808098047));
#155911=CARTESIAN_POINT('Ctrl Pts',(-97.9289936756488,-1.1610190378098,
125.002639721457));
#155912=CARTESIAN_POINT('Ctrl Pts',(-97.9364170466775,-1.31530768860881,
125.033515398537));
#155913=CARTESIAN_POINT('Ctrl Pts',(-97.9438404177062,-1.46818804687434,
125.070514735438));
#155914=CARTESIAN_POINT('Ctrl Pts',(-97.9512637887349,-1.61914961195375,
125.113465688242));
#155915=CARTESIAN_POINT('Ctrl Pts',(-97.9551998381757,-1.69919305603231,
125.136239314012));
#155916=CARTESIAN_POINT('Ctrl Pts',(-97.9591358876166,-1.778697371648,125.160685339546));
#155917=CARTESIAN_POINT('Ctrl Pts',(-97.9630719370574,-1.85758888662536,
125.18677269295));
#155918=CARTESIAN_POINT('Ctrl Pts',(-97.9704952034628,-2.00637582175179,
125.235972627313));
#155919=CARTESIAN_POINT('Ctrl Pts',(-97.9779184698683,-2.15343173215094,
125.291162176854));
#155920=CARTESIAN_POINT('Ctrl Pts',(-97.9853417362737,-2.29823795172998,
125.352202065238));
#155921=CARTESIAN_POINT('Ctrl Pts',(-97.9927562289947,-2.44287302238289,
125.413169809542));
#155922=CARTESIAN_POINT('Ctrl Pts',(-98.0001707217156,-2.58526335423886,
125.479973985526));
#155923=CARTESIAN_POINT('Ctrl Pts',(-98.0075852144366,-2.72490515771916,
125.55242550335));
#155924=CARTESIAN_POINT('Ctrl Pts',(-98.0149925607904,-2.86441236917224,
125.624807189673));
#155925=CARTESIAN_POINT('Ctrl Pts',(-98.0223999071442,-3.00117599702698,
125.70282521089));
#155926=CARTESIAN_POINT('Ctrl Pts',(-98.029807253498,-3.1347120804622,125.786242371141));
#155927=CARTESIAN_POINT('Ctrl Pts',(-98.0372090751734,-3.26814856764799,
125.869597315727));
#155928=CARTESIAN_POINT('Ctrl Pts',(-98.0446108968488,-3.39836198828382,
125.95834318436));
#155929=CARTESIAN_POINT('Ctrl Pts',(-98.0520127185242,-3.5248929619209,
126.052196882013));
#155930=CARTESIAN_POINT('Ctrl Pts',(-98.0594106328356,-3.65135714084228,
126.146001035031));
#155931=CARTESIAN_POINT('Ctrl Pts',(-98.0668085471469,-3.77414244514158,
126.244907425265));
#155932=CARTESIAN_POINT('Ctrl Pts',(-98.0742064614583,-3.89281857526756,
126.348589741213));
#155933=CARTESIAN_POINT('Ctrl Pts',(-98.0816031463705,-4.01147498357355,
126.452254827042));
#155934=CARTESIAN_POINT('Ctrl Pts',(-98.0889998312827,-4.12602329215452,
126.560694018016));
#155935=CARTESIAN_POINT('Ctrl Pts',(-98.0963965161949,-4.23606631528235,
126.673540755235));
#155936=CARTESIAN_POINT('Ctrl Pts',(-98.1037928731303,-4.34610445898721,
126.786382488711));
#155937=CARTESIAN_POINT('Ctrl Pts',(-98.1111892300658,-4.45163745382707,
126.903631112581));
#155938=CARTESIAN_POINT('Ctrl Pts',(-98.1185855870013,-4.55230522642488,
127.024883446321));
#155939=CARTESIAN_POINT('Ctrl Pts',(-98.1259830763379,-4.65298841151566,
127.146154344102));
#155940=CARTESIAN_POINT('Ctrl Pts',(-98.1333805656745,-4.74880465274432,
127.271429885044));
#155941=CARTESIAN_POINT('Ctrl Pts',(-98.140778055011,-4.83943449892919,
127.400274206637));
#155942=CARTESIAN_POINT('Ctrl Pts',(-98.148178137526,-4.93009611526602,
127.529163694407));
#155943=CARTESIAN_POINT('Ctrl Pts',(-98.155578220041,-5.015567502134,127.661624148483));
#155944=CARTESIAN_POINT('Ctrl Pts',(-98.1629783025559,-5.09557291188604,
127.797191307043));
#155945=CARTESIAN_POINT('Ctrl Pts',(-98.1703865222224,-5.17566629581097,
127.93290753563));
#155946=CARTESIAN_POINT('Ctrl Pts',(-98.1777947418888,-5.25028150960514,
128.071736969274));
#155947=CARTESIAN_POINT('Ctrl Pts',(-98.1852029615553,-5.31918876184357,
128.213190712219));
#155948=CARTESIAN_POINT('Ctrl Pts',(-98.1926157408573,-5.38813842534596,
128.354731517582));
#155949=CARTESIAN_POINT('Ctrl Pts',(-98.2000285201593,-5.451372977293,128.498899509704));
#155950=CARTESIAN_POINT('Ctrl Pts',(-98.2074412994613,-5.50871125257117,
128.64518695658));
#155951=CARTESIAN_POINT('Ctrl Pts',(-98.21486467049,-5.56613145546588,128.79168342582));
#155952=CARTESIAN_POINT('Ctrl Pts',(-98.2222880415189,-5.61763843340822,
128.940305046379));
#155953=CARTESIAN_POINT('Ctrl Pts',(-98.2297114125476,-5.66310099374721,
129.090529325659));
#155954=CARTESIAN_POINT('Ctrl Pts',(-98.2336474619885,-5.68720633409882,
129.170181843118));
#155955=CARTESIAN_POINT('Ctrl Pts',(-98.2375835114293,-5.70961322506146,
129.250284749454));
#155956=CARTESIAN_POINT('Ctrl Pts',(-98.2415195608702,-5.730307986688,129.330759267065));
#155957=CARTESIAN_POINT('Ctrl Pts',(-98.2512252464837,-5.78133804949806,
129.529196908549));
#155958=CARTESIAN_POINT('Ctrl Pts',(-98.2609309320973,-5.82208048302636,
129.73038031375));
#155959=CARTESIAN_POINT('Ctrl Pts',(-98.2706366177106,-5.85229309841448,
129.933386420043));
#155960=CARTESIAN_POINT('Ctrl Pts',(-98.2801407901906,-5.88187842799923,
130.132177636403));
#155961=CARTESIAN_POINT('Ctrl Pts',(-98.2896449626705,-5.90136670172385,
130.332716894857));
#155962=CARTESIAN_POINT('Ctrl Pts',(-98.2991491351504,-5.91057510998828,
130.534115484979));
#155963=CARTESIAN_POINT('Ctrl Pts',(-98.303307687164,-5.91460425032748,
130.622237466587));
#155964=CARTESIAN_POINT('Ctrl Pts',(-98.3074662391774,-5.91666588808329,
130.710523658734));
#155965=CARTESIAN_POINT('Ctrl Pts',(-98.311624791191,-5.91674747839506,
130.798898071854));
#155966=CARTESIAN_POINT('',(-100.061624840552,-5.91280015844335,130.805553846743));
#155967=CARTESIAN_POINT('Ctrl Pts',(-98.3116248077888,-5.91560542397323,
130.798899478893));
#155968=CARTESIAN_POINT('Ctrl Pts',(-98.3810722667536,-5.90220073733502,
132.274473302428));
#155969=CARTESIAN_POINT('Ctrl Pts',(-98.5433356003227,-4.59610210103513,
135.743303909333));
#155970=CARTESIAN_POINT('Ctrl Pts',(-98.7984148084961,1.23205455133509,
137.693453599436));
#155971=CARTESIAN_POINT('Ctrl Pts',(-99.076862432309,6.46194461450306,133.491521262083));
#155972=CARTESIAN_POINT('Ctrl Pts',(-99.3553100561219,5.75362326048721,
126.820219567513));
#155973=CARTESIAN_POINT('Ctrl Pts',(-99.6337576799348,-0.241996789793268,
123.81014886183));
#155974=CARTESIAN_POINT('Ctrl Pts',(-99.8691959304905,-5.12349212797977,
126.699581489776));
#155975=CARTESIAN_POINT('Ctrl Pts',(-100.011818306442,-5.9052485242762,
129.743477247566));
#155976=CARTESIAN_POINT('Ctrl Pts',(-100.061624807789,-5.90715198088181,
130.805552007816));
#155977=CARTESIAN_POINT('',(-101.811624807789,-5.91752016895145,130.809410794066));
#155978=CARTESIAN_POINT('Ctrl Pts',(-100.061624863462,-5.91674987942144,
130.805555132688));
#155979=CARTESIAN_POINT('Ctrl Pts',(-100.069501906503,-5.91671591332789,
130.973798193149));
#155980=CARTESIAN_POINT('Ctrl Pts',(-100.077378949543,-5.90950170403371,
131.141858042596));
#155981=CARTESIAN_POINT('Ctrl Pts',(-100.085255992583,-5.89517943177854,
131.309127920029));
#155982=CARTESIAN_POINT('Ctrl Pts',(-100.093147676019,-5.88083053992256,
131.47670868789));
#155983=CARTESIAN_POINT('Ctrl Pts',(-100.101039359456,-5.85934722133416,
131.643496259084));
#155984=CARTESIAN_POINT('Ctrl Pts',(-100.108931042892,-5.83085291951967,
131.808892744195));
#155985=CARTESIAN_POINT('Ctrl Pts',(-100.116845568588,-5.80227614173708,
131.974767964854));
#155986=CARTESIAN_POINT('Ctrl Pts',(-100.124760094284,-5.76664783455927,
132.139243754121));
#155987=CARTESIAN_POINT('Ctrl Pts',(-100.13267461998,-5.72414226850208,
132.30173360131));
#155988=CARTESIAN_POINT('Ctrl Pts',(-100.140601422694,-5.68157076777453,
132.46447550289));
#155989=CARTESIAN_POINT('Ctrl Pts',(-100.148528225409,-5.63210078849964,
132.62522503003));
#155990=CARTESIAN_POINT('Ctrl Pts',(-100.156455028124,-5.57595548860646,
132.783413661721));
#155991=CARTESIAN_POINT('Ctrl Pts',(-100.164400999593,-5.51967441701875,
132.941984828346));
#155992=CARTESIAN_POINT('Ctrl Pts',(-100.172346971061,-5.45668584942095,
133.09798244126));
#155993=CARTESIAN_POINT('Ctrl Pts',(-100.18029294253,-5.38726073115559,
133.250858599795));
#155994=CARTESIAN_POINT('Ctrl Pts',(-100.183746270873,-5.35708849487361,
133.317298754201));
#155995=CARTESIAN_POINT('Ctrl Pts',(-100.187199599217,-5.32570110981252,
133.383149672588));
#155996=CARTESIAN_POINT('Ctrl Pts',(-100.19065292756,-5.293123410409,133.448368016323));
#155997=CARTESIAN_POINT('Ctrl Pts',(-100.198076193966,-5.22309446513999,
133.588561213128));
#155998=CARTESIAN_POINT('Ctrl Pts',(-100.205499460371,-5.14738606413112,
133.726182305912));
#155999=CARTESIAN_POINT('Ctrl Pts',(-100.212922726777,-5.06621042610964,
133.860737963523));
#156000=CARTESIAN_POINT('Ctrl Pts',(-100.220337219498,-4.98513073095086,
133.99513458752));
#156001=CARTESIAN_POINT('Ctrl Pts',(-100.227751712219,-4.89859685201709,
134.12647267161));
#156002=CARTESIAN_POINT('Ctrl Pts',(-100.23516620494,-4.80686817318816,
134.254280751147));
#156003=CARTESIAN_POINT('Ctrl Pts',(-100.242573551294,-4.71522790591366,
134.381965644446));
#156004=CARTESIAN_POINT('Ctrl Pts',(-100.249980897647,-4.61840302278341,
134.506127005366));
#156005=CARTESIAN_POINT('Ctrl Pts',(-100.257388244001,-4.51669767279131,
134.626319891957));
#156006=CARTESIAN_POINT('Ctrl Pts',(-100.264790065677,-4.41506817848608,
134.746423134158));
#156007=CARTESIAN_POINT('Ctrl Pts',(-100.272191887352,-4.30856570521863,
134.862563511726));
#156008=CARTESIAN_POINT('Ctrl Pts',(-100.279593709028,-4.19753630162808,
134.974326991413));
#156009=CARTESIAN_POINT('Ctrl Pts',(-100.286991623339,-4.08656550959543,
135.086031472029));
#156010=CARTESIAN_POINT('Ctrl Pts',(-100.294389537651,-3.97107280892837,
135.193363392137));
#156011=CARTESIAN_POINT('Ctrl Pts',(-100.301787451962,-3.85144284752758,
135.295943696474));
#156012=CARTESIAN_POINT('Ctrl Pts',(-100.309184136874,-3.73183276645624,
135.398506953824));
#156013=CARTESIAN_POINT('Ctrl Pts',(-100.316580821787,-3.60808707231421,
135.496319919834));
#156014=CARTESIAN_POINT('Ctrl Pts',(-100.323977506699,-3.48062549551459,
135.589042082666));
#156015=CARTESIAN_POINT('Ctrl Pts',(-100.331373863634,-3.35316957049486,
135.681760134101));
#156016=CARTESIAN_POINT('Ctrl Pts',(-100.33877022057,-3.22199839230176,
135.76938761159));
#156017=CARTESIAN_POINT('Ctrl Pts',(-100.346166577505,-3.08756261213258,
135.851625983946));
#156018=CARTESIAN_POINT('Ctrl Pts',(-100.353564066842,-2.95310624950226,
135.933876947208));
#156019=CARTESIAN_POINT('Ctrl Pts',(-100.360961556179,-2.81538460815103,
136.010736967669));
#156020=CARTESIAN_POINT('Ctrl Pts',(-100.368359045515,-2.67487485779842,
136.081952403373));
#156021=CARTESIAN_POINT('Ctrl Pts',(-100.37575912803,-2.53431585197084,
136.153192803537));
#156022=CARTESIAN_POINT('Ctrl Pts',(-100.383159210546,-2.39096712397539,
136.218784510709));
#156023=CARTESIAN_POINT('Ctrl Pts',(-100.390559293061,-2.24532768175479,
136.278521207469));
#156024=CARTESIAN_POINT('Ctrl Pts',(-100.397967512727,-2.09952809399517,
136.338323590868));
#156025=CARTESIAN_POINT('Ctrl Pts',(-100.405375732394,-1.95143310723619,
136.392257964627));
#156026=CARTESIAN_POINT('Ctrl Pts',(-100.41278395206,-1.80155951812696,
136.440167025273));
#156027=CARTESIAN_POINT('Ctrl Pts',(-100.420196731362,-1.6515936843244,
136.488105573146));
#156028=CARTESIAN_POINT('Ctrl Pts',(-100.427609510665,-1.49984742583941,
136.530011319157));
#156029=CARTESIAN_POINT('Ctrl Pts',(-100.435022289967,-1.34684920735396,
136.565777784822));
#156030=CARTESIAN_POINT('Ctrl Pts',(-100.442445660996,-1.19363237783882,
136.60159535529));
#156031=CARTESIAN_POINT('Ctrl Pts',(-100.449869032024,-1.03916038119999,
136.631256055372));
#156032=CARTESIAN_POINT('Ctrl Pts',(-100.457292403053,-0.883969123571974,
136.654704979317));
#156033=CARTESIAN_POINT('Ctrl Pts',(-100.461228452493,-0.801682995029756,
136.66713816144));
#156034=CARTESIAN_POINT('Ctrl Pts',(-100.465164501933,-0.719194708221002,
136.677825860104));
#156035=CARTESIAN_POINT('Ctrl Pts',(-100.469100551373,-0.636584188296631,
136.686765834287));
#156036=CARTESIAN_POINT('Ctrl Pts',(-100.476523817779,-0.480783325877515,
136.703626346592));
#156037=CARTESIAN_POINT('Ctrl Pts',(-100.483947084184,-0.324076562861753,
136.714318286882));
#156038=CARTESIAN_POINT('Ctrl Pts',(-100.49137035059,-0.166993662125266,
136.718753543244));
#156039=CARTESIAN_POINT('Ctrl Pts',(-100.498784843311,-0.0100964203325258,
136.723183557501));
#156040=CARTESIAN_POINT('Ctrl Pts',(-100.506199336032,0.147175704769412,
136.721371596949));
#156041=CARTESIAN_POINT('Ctrl Pts',(-100.513613828753,0.30428585330045,
136.713281050435));
#156042=CARTESIAN_POINT('Ctrl Pts',(-100.521021175107,0.461244573155242,
136.705198301895));
#156043=CARTESIAN_POINT('Ctrl Pts',(-100.52842852146,0.618041256940341,
136.690849033882));
#156044=CARTESIAN_POINT('Ctrl Pts',(-100.535835867814,0.774137162429258,
136.670248633565));
#156045=CARTESIAN_POINT('Ctrl Pts',(-100.54323768949,0.930116645703146,
136.649663597805));
#156046=CARTESIAN_POINT('Ctrl Pts',(-100.550639511165,1.08539602288506,
136.6228367617));
#156047=CARTESIAN_POINT('Ctrl Pts',(-100.55804133284,1.23943990833583,136.58983547069));
#156048=CARTESIAN_POINT('Ctrl Pts',(-100.565439247152,1.39340247521811,
136.556851600804));
#156049=CARTESIAN_POINT('Ctrl Pts',(-100.572837161463,1.54613048517815,
136.517699845356));
#156050=CARTESIAN_POINT('Ctrl Pts',(-100.580235075774,1.69709711670182,
136.472498930891));
#156051=CARTESIAN_POINT('Ctrl Pts',(-100.587631760687,1.84803866030994,
136.427305527998));
#156052=CARTESIAN_POINT('Ctrl Pts',(-100.595028445599,1.99721904916031,
136.3760650682));
#156053=CARTESIAN_POINT('Ctrl Pts',(-100.602425130511,2.14412492646037,
136.318946627615));
#156054=CARTESIAN_POINT('Ctrl Pts',(-100.609821487447,2.29102428979989,
136.261830719722));
#156055=CARTESIAN_POINT('Ctrl Pts',(-100.617217844382,2.435648994197,136.198837484552));
#156056=CARTESIAN_POINT('Ctrl Pts',(-100.624614201317,2.5775042889294,136.13018470432));
#156057=CARTESIAN_POINT('Ctrl Pts',(-100.632011690654,2.71938130206996,
136.061521413172));
#156058=CARTESIAN_POINT('Ctrl Pts',(-100.639409179991,2.8584877252611,135.987197014295));
#156059=CARTESIAN_POINT('Ctrl Pts',(-100.646806669327,2.99435224045142,
135.907475864413));
#156060=CARTESIAN_POINT('Ctrl Pts',(-100.654206751842,3.13026438273712,
135.827726768406));
#156061=CARTESIAN_POINT('Ctrl Pts',(-100.661606834357,3.26293203260323,
135.74257734359));
#156062=CARTESIAN_POINT('Ctrl Pts',(-100.669006916872,3.39191188337985,
135.652335899876));
#156063=CARTESIAN_POINT('Ctrl Pts',(-100.676415136539,3.52103356076166,
135.561995226417));
#156064=CARTESIAN_POINT('Ctrl Pts',(-100.683823356205,3.64645903466989,
135.466551566227));
#156065=CARTESIAN_POINT('Ctrl Pts',(-100.691231575872,3.76777662002576,
135.366354688593));
#156066=CARTESIAN_POINT('Ctrl Pts',(-100.698644355174,3.88916887433146,
135.266096141453));
#156067=CARTESIAN_POINT('Ctrl Pts',(-100.706057134476,4.00644792460274,
135.161078795836));
#156068=CARTESIAN_POINT('Ctrl Pts',(-100.713469913778,4.11923853940647,
135.051689709827));
#156069=CARTESIAN_POINT('Ctrl Pts',(-100.720893284807,4.23219031472949,
134.942144323563));
#156070=CARTESIAN_POINT('Ctrl Pts',(-100.728316655835,4.3406405891142,134.828214990815));
#156071=CARTESIAN_POINT('Ctrl Pts',(-100.735740026864,4.44425349844226,
134.710322906693));
#156072=CARTESIAN_POINT('Ctrl Pts',(-100.739676076305,4.49919154912415,
134.647813694912));
#156073=CARTESIAN_POINT('Ctrl Pts',(-100.743612125746,4.55277034661906,
134.584190925211));
#156074=CARTESIAN_POINT('Ctrl Pts',(-100.747548175186,4.60494480399341,
134.519520629554));
#156075=CARTESIAN_POINT('Ctrl Pts',(-100.754971441592,4.70334420229488,
134.397554470233));
#156076=CARTESIAN_POINT('Ctrl Pts',(-100.762394707997,4.79704346765728,
134.271491887234));
#156077=CARTESIAN_POINT('Ctrl Pts',(-100.769817974403,4.88568211925863,
134.141730958427));
#156078=CARTESIAN_POINT('Ctrl Pts',(-100.777232467124,4.97421600733476,
134.012123396261));
#156079=CARTESIAN_POINT('Ctrl Pts',(-100.784646959845,5.05770097880735,
133.878826494297));
#156080=CARTESIAN_POINT('Ctrl Pts',(-100.792061452566,5.13581604579875,
133.742272138735));
#156081=CARTESIAN_POINT('Ctrl Pts',(-100.799468798919,5.21385582254761,
133.605849399401));
#156082=CARTESIAN_POINT('Ctrl Pts',(-100.806876145273,5.28653581453356,
133.466175778759));
#156083=CARTESIAN_POINT('Ctrl Pts',(-100.814283491627,5.35357776408466,
133.323712853042));
#156084=CARTESIAN_POINT('Ctrl Pts',(-100.821685313302,5.42056971122043,
133.18135618155));
#156085=CARTESIAN_POINT('Ctrl Pts',(-100.829087134978,5.48193183050659,
133.036214683591));
#156086=CARTESIAN_POINT('Ctrl Pts',(-100.836488956653,5.53743139255126,
132.88877519612));
#156087=CARTESIAN_POINT('Ctrl Pts',(-100.843886870964,5.5929016568093,132.741413540806));
#156088=CARTESIAN_POINT('Ctrl Pts',(-100.851284785276,5.64251539608859,
132.591756660391));
#156089=CARTESIAN_POINT('Ctrl Pts',(-100.858682699587,5.68608773849637,
132.440311959331));
#156090=CARTESIAN_POINT('Ctrl Pts',(-100.866079384499,5.72965283997126,
132.288892425632));
#156091=CARTESIAN_POINT('Ctrl Pts',(-100.873476069411,5.7671784340452,132.135686019346));
#156092=CARTESIAN_POINT('Ctrl Pts',(-100.880872754324,5.79852928735964,
131.981216031851));
#156093=CARTESIAN_POINT('Ctrl Pts',(-100.888269111259,5.82987875054439,
131.826752893718));
#156094=CARTESIAN_POINT('Ctrl Pts',(-100.895665468195,5.85505394311581,
131.671026651619));
#156095=CARTESIAN_POINT('Ctrl Pts',(-100.90306182513,5.87397066657043,131.514571269957));
#156096=CARTESIAN_POINT('Ctrl Pts',(-100.910459314467,5.89289028622365,
131.358091934578));
#156097=CARTESIAN_POINT('Ctrl Pts',(-100.917856803803,5.90554948406987,
131.200883607982));
#156098=CARTESIAN_POINT('Ctrl Pts',(-100.92525429314,5.91191591198988,131.043485714661));
#156099=CARTESIAN_POINT('Ctrl Pts',(-100.932654375655,5.91828457165133,
130.886032645754));
#156100=CARTESIAN_POINT('Ctrl Pts',(-100.94005445817,5.91835605433714,130.728390250576));
#156101=CARTESIAN_POINT('Ctrl Pts',(-100.947454540685,5.9121501318231,130.571098144622));
#156102=CARTESIAN_POINT('Ctrl Pts',(-100.954862760351,5.90593738525926,
130.413633079827));
#156103=CARTESIAN_POINT('Ctrl Pts',(-100.962270980018,5.89343346317159,
130.25651944672));
#156104=CARTESIAN_POINT('Ctrl Pts',(-100.969679199684,5.87471011052705,
130.100292666462));
#156105=CARTESIAN_POINT('Ctrl Pts',(-100.977091978986,5.85597523397138,
129.943969731228));
#156106=CARTESIAN_POINT('Ctrl Pts',(-100.984504758288,5.83101335823092,
129.788535104223));
#156107=CARTESIAN_POINT('Ctrl Pts',(-100.99191753759,5.79994730447737,129.634513692629));
#156108=CARTESIAN_POINT('Ctrl Pts',(-100.999340908619,5.76883686208931,
129.480272208018));
#156109=CARTESIAN_POINT('Ctrl Pts',(-101.006764279648,5.73160491015267,
129.327448333477));
#156110=CARTESIAN_POINT('Ctrl Pts',(-101.014187650677,5.68842426928217,
129.176552307248));
#156111=CARTESIAN_POINT('Ctrl Pts',(-101.018123700118,5.66552885738664,
129.096543613438));
#156112=CARTESIAN_POINT('Ctrl Pts',(-101.022059749558,5.64096186812597,
129.017076592574));
#156113=CARTESIAN_POINT('Ctrl Pts',(-101.025995798999,5.61475448547331,
128.93822486946));
#156114=CARTESIAN_POINT('Ctrl Pts',(-101.033419065405,5.5653281796963,128.789512980551));
#156115=CARTESIAN_POINT('Ctrl Pts',(-101.04084233181,5.50991490000123,128.64254122954));
#156116=CARTESIAN_POINT('Ctrl Pts',(-101.048265598216,5.44865471188496,
128.497828069963));
#156117=CARTESIAN_POINT('Ctrl Pts',(-101.055680090937,5.38746692822353,
128.353285949322));
#156118=CARTESIAN_POINT('Ctrl Pts',(-101.063094583658,5.3204461357511,128.210997446935));
#156119=CARTESIAN_POINT('Ctrl Pts',(-101.070509076379,5.24778219077092,
128.071466064034));
#156120=CARTESIAN_POINT('Ctrl Pts',(-101.077916422733,5.17518828203687,
127.932069166733));
#156121=CARTESIAN_POINT('Ctrl Pts',(-101.085323769086,5.09696222020373,
127.795424427395));
#156122=CARTESIAN_POINT('Ctrl Pts',(-101.09273111544,5.01334193736096,127.66201544531));
#156123=CARTESIAN_POINT('Ctrl Pts',(-101.100132937116,4.92978402167995,
127.528705964678));
#156124=CARTESIAN_POINT('Ctrl Pts',(-101.107534758791,4.84084009315306,
127.398627750931));
#156125=CARTESIAN_POINT('Ctrl Pts',(-101.114936580466,4.74679394557737,
127.272239753166));
#156126=CARTESIAN_POINT('Ctrl Pts',(-101.122334494778,4.65279744423093,
127.145918474641));
#156127=CARTESIAN_POINT('Ctrl Pts',(-101.129732409089,4.55370431019756,
127.023283831214));
#156128=CARTESIAN_POINT('Ctrl Pts',(-101.137130323401,4.44984150944379,
126.904765625348));
#156129=CARTESIAN_POINT('Ctrl Pts',(-101.144527008313,4.34599596880339,
126.786267115058));
#156130=CARTESIAN_POINT('Ctrl Pts',(-101.151923693225,4.23738258037395,
126.671883965111));
#156131=CARTESIAN_POINT('Ctrl Pts',(-101.159320378137,4.12436850708096,
126.562012802936));
#156132=CARTESIAN_POINT('Ctrl Pts',(-101.166716735073,4.01135944495008,
126.452146512562));
#156133=CARTESIAN_POINT('Ctrl Pts',(-101.174113092008,3.89395035359867,
126.346792072374));
#156134=CARTESIAN_POINT('Ctrl Pts',(-101.181509448944,3.77254496105348,
126.246308941759));
#156135=CARTESIAN_POINT('Ctrl Pts',(-101.18890693828,3.65112098103277,126.14581042692));
#156136=CARTESIAN_POINT('Ctrl Pts',(-101.196304427617,3.52569976914942,
126.050184944692));
#156137=CARTESIAN_POINT('Ctrl Pts',(-101.203701916953,3.39671767355769,
125.959751282579));
#156138=CARTESIAN_POINT('Ctrl Pts',(-101.211101999468,3.26769036349247,
125.869285919086));
#156139=CARTESIAN_POINT('Ctrl Pts',(-101.218502081983,3.1350999899019,125.784016213455));
#156140=CARTESIAN_POINT('Ctrl Pts',(-101.225902164498,2.99941123371145,
125.704217206486));
#156141=CARTESIAN_POINT('Ctrl Pts',(-101.233310384165,2.86357327378423,
125.624330452304));
#156142=CARTESIAN_POINT('Ctrl Pts',(-101.240718603831,2.72463044924826,
125.549926599678));
#156143=CARTESIAN_POINT('Ctrl Pts',(-101.248126823498,2.58307200499659,
125.481234695751));
#156144=CARTESIAN_POINT('Ctrl Pts',(-101.2555396028,2.44142643388451,125.412500513102));
#156145=CARTESIAN_POINT('Ctrl Pts',(-101.262952382102,2.29716237648222,
125.349485433522));
#156146=CARTESIAN_POINT('Ctrl Pts',(-101.270365161404,2.15078783990958,
125.292369849232));
#156147=CARTESIAN_POINT('Ctrl Pts',(-101.277788532433,2.00420415653501,
125.235172655517));
#156148=CARTESIAN_POINT('Ctrl Pts',(-101.285211903462,1.85550432322439,
125.183891914026));
#156149=CARTESIAN_POINT('Ctrl Pts',(-101.29263527449,1.7052110316233,125.138658022112));
#156150=CARTESIAN_POINT('Ctrl Pts',(-101.296571323931,1.62552192218051,
125.114673927248));
#156151=CARTESIAN_POINT('Ctrl Pts',(-101.300507373372,1.54538500913211,
125.092388965221));
#156152=CARTESIAN_POINT('Ctrl Pts',(-101.304443422812,1.46487909081005,
125.071816696076));
#156153=CARTESIAN_POINT('Ctrl Pts',(-101.311866689218,1.3130474413549,125.033018038507));
#156154=CARTESIAN_POINT('Ctrl Pts',(-101.319289955623,1.1594437135535,125.000196978694));
#156155=CARTESIAN_POINT('Ctrl Pts',(-101.326713222029,1.00457980587252,
124.973515912368));
#156156=CARTESIAN_POINT('Ctrl Pts',(-101.334127714749,0.849898934469772,
124.946866380847));
#156157=CARTESIAN_POINT('Ctrl Pts',(-101.34154220747,0.693961212187642,
124.926342460551));
#156158=CARTESIAN_POINT('Ctrl Pts',(-101.348956700191,0.537292870842562,
124.912056574711));
#156159=CARTESIAN_POINT('Ctrl Pts',(-101.356364046545,0.38077553234333,
124.897784458146));
#156160=CARTESIAN_POINT('Ctrl Pts',(-101.363771392899,0.223529345960948,
124.889738440098));
#156161=CARTESIAN_POINT('Ctrl Pts',(-101.371178739253,0.0660897855796993,
124.88797973879));
#156162=CARTESIAN_POINT('Ctrl Pts',(-101.378580560928,-0.0912323504380104,
124.886222349189));
#156163=CARTESIAN_POINT('Ctrl Pts',(-101.385982382603,-0.248747201613833,
124.890742943414));
#156164=CARTESIAN_POINT('Ctrl Pts',(-101.393384204279,-0.405915243597154,
124.901550830904));
#156165=CARTESIAN_POINT('Ctrl Pts',(-101.40078211859,-0.563000317794506,
124.912353012994));
#156166=CARTESIAN_POINT('Ctrl Pts',(-101.408180032902,-0.71973857593204,
124.929435852829));
#156167=CARTESIAN_POINT('Ctrl Pts',(-101.415577947213,-0.875591679933997,
124.952756583412));
#156168=CARTESIAN_POINT('Ctrl Pts',(-101.422974632125,-1.03141888397731,
124.976073438512));
#156169=CARTESIAN_POINT('Ctrl Pts',(-101.430371317037,-1.18636085700193,
125.005626071778));
#156170=CARTESIAN_POINT('Ctrl Pts',(-101.437768001949,-1.33988544459,125.041319965456));
#156171=CARTESIAN_POINT('Ctrl Pts',(-101.445164358885,-1.49340322473696,
125.077012276429));
#156172=CARTESIAN_POINT('Ctrl Pts',(-101.45256071582,-1.64550338081134,
125.118845221833));
#156173=CARTESIAN_POINT('Ctrl Pts',(-101.459957072756,-1.79566526458957,
125.166673430426));
#156174=CARTESIAN_POINT('Ctrl Pts',(-101.467354562092,-1.94585013853554,
125.214508961639));
#156175=CARTESIAN_POINT('Ctrl Pts',(-101.474752051429,-2.09409579359361,
125.268341470383));
#156176=CARTESIAN_POINT('Ctrl Pts',(-101.482149540765,-2.23989816797303,
125.327976157029));
#156177=CARTESIAN_POINT('Ctrl Pts',(-101.48954962328,-2.38575165314857,
125.387631748522));
#156178=CARTESIAN_POINT('Ctrl Pts',(-101.496949705795,-2.52915980708469,
125.453093426255));
#156179=CARTESIAN_POINT('Ctrl Pts',(-101.50434978831,-2.66964005877586,
125.524118907277));
#156180=CARTESIAN_POINT('Ctrl Pts',(-101.511758007977,-2.81027478294568,
125.595222488116));
#156181=CARTESIAN_POINT('Ctrl Pts',(-101.519166227643,-2.94797484191478,
125.671901921703));
#156182=CARTESIAN_POINT('Ctrl Pts',(-101.526574447309,-3.08228308301985,
125.753869398028));
#156183=CARTESIAN_POINT('Ctrl Pts',(-101.533987226611,-3.21667398860627,
125.835887323967));
#156184=CARTESIAN_POINT('Ctrl Pts',(-101.541400005913,-3.34766860660781,
125.923199571487));
#156185=CARTESIAN_POINT('Ctrl Pts',(-101.548812785215,-3.47484057768205,
126.015476246212));
#156186=CARTESIAN_POINT('Ctrl Pts',(-101.556236156244,-3.60219425803251,
126.107884770178));
#156187=CARTESIAN_POINT('Ctrl Pts',(-101.563659527273,-3.72571409029497,
126.205271657962));
#156188=CARTESIAN_POINT('Ctrl Pts',(-101.571082898302,-3.84500783988038,
126.307267637233));
#156189=CARTESIAN_POINT('Ctrl Pts',(-101.575018947743,-3.9082602483304,
126.361348352808));
#156190=CARTESIAN_POINT('Ctrl Pts',(-101.578954997184,-3.9703251769893,
126.416724241041));
#156191=CARTESIAN_POINT('Ctrl Pts',(-101.582891046625,-4.03114862498385,
126.473336336199));
#156192=CARTESIAN_POINT('Ctrl Pts',(-101.590203834316,-4.14415253117462,
126.578515968421));
#156193=CARTESIAN_POINT('Ctrl Pts',(-101.597516622007,-4.25323255256093,
126.68830342459));
#156194=CARTESIAN_POINT('Ctrl Pts',(-101.604829409697,-4.35798115646332,
126.802369762703));
#156195=CARTESIAN_POINT('Ctrl Pts',(-101.612133453102,-4.46260450693228,
126.916299705675));
#156196=CARTESIAN_POINT('Ctrl Pts',(-101.619437496507,-4.56290648635817,
127.034498070333));
#156197=CARTESIAN_POINT('Ctrl Pts',(-101.626741539911,-4.65851334223814,
127.156596370429));
#156198=CARTESIAN_POINT('Ctrl Pts',(-101.634038555917,-4.75402821242929,
127.278577196772));
#156199=CARTESIAN_POINT('Ctrl Pts',(-101.641335571924,-4.84485671208898,
127.404450190631));
#156200=CARTESIAN_POINT('Ctrl Pts',(-101.64863258793,-4.9306628180773,127.533811009789));
#156201=CARTESIAN_POINT('Ctrl Pts',(-101.655923928853,-5.01640219037763,
127.663071221602));
#156202=CARTESIAN_POINT('Ctrl Pts',(-101.663215269776,-5.09712673366964,
127.795813538242));
#156203=CARTESIAN_POINT('Ctrl Pts',(-101.670506610699,-5.17254173400305,
127.931601913376));
#156204=CARTESIAN_POINT('Ctrl Pts',(-101.677794900797,-5.24792517937439,
128.067333472267));
#156205=CARTESIAN_POINT('Ctrl Pts',(-101.685083190895,-5.31800331445087,
128.206108218088));
#156206=CARTESIAN_POINT('Ctrl Pts',(-101.692371480993,-5.3825257125239,
128.347462671676));
#156207=CARTESIAN_POINT('Ctrl Pts',(-101.699658259854,-5.44703473179476,
128.488787815236));
#156208=CARTESIAN_POINT('Ctrl Pts',(-101.706945038716,-5.50599014677343,
128.632691251676));
#156209=CARTESIAN_POINT('Ctrl Pts',(-101.714231817577,-5.55918845395391,
128.778686829434));
#156210=CARTESIAN_POINT('Ctrl Pts',(-101.721518623426,-5.61238695816111,
128.924682947905));
#156211=CARTESIAN_POINT('Ctrl Pts',(-101.728805429276,-5.65982818182036,
129.072770860525));
#156212=CARTESIAN_POINT('Ctrl Pts',(-101.736092235125,-5.70135765486742,
129.222446759676));
#156213=CARTESIAN_POINT('Ctrl Pts',(-101.74338342505,-5.74291211395053,
129.372212710714));
#156214=CARTESIAN_POINT('Ctrl Pts',(-101.750674614976,-5.77854761592046,
129.523568184695));
#156215=CARTESIAN_POINT('Ctrl Pts',(-101.757965804902,-5.80816017317679,
129.675996330103));
#156216=CARTESIAN_POINT('Ctrl Pts',(-101.765259480235,-5.83778282470643,
129.828476434932));
#156217=CARTESIAN_POINT('Ctrl Pts',(-101.772553155568,-5.86137838176501,
129.982029559142));
#156218=CARTESIAN_POINT('Ctrl Pts',(-101.779846830901,-5.87889453206986,
130.136131881803));
#156219=CARTESIAN_POINT('Ctrl Pts',(-101.787147880188,-5.89642839132037,
130.290390002948));
#156220=CARTESIAN_POINT('Ctrl Pts',(-101.794448929476,-5.90787054262023,
130.445198047472));
#156221=CARTESIAN_POINT('Ctrl Pts',(-101.801749978764,-5.91322074119755,
130.600029933695));
#156222=CARTESIAN_POINT('Ctrl Pts',(-101.805041588439,-5.91563282810543,
130.669834439132));
#156223=CARTESIAN_POINT('Ctrl Pts',(-101.808333198114,-5.91680738581963,
130.73964381692));
#156224=CARTESIAN_POINT('Ctrl Pts',(-101.811624807789,-5.91674784530102,
130.809410134943));
#156225=CARTESIAN_POINT('',(-103.561624807789,-5.92383021006907,130.800793567564));
#156226=CARTESIAN_POINT('Ctrl Pts',(-101.811624807789,-5.91999130402177,
130.809412903001));
#156227=CARTESIAN_POINT('Ctrl Pts',(-101.828196095339,-5.92317871838217,
131.16084013514));
#156228=CARTESIAN_POINT('Ctrl Pts',(-101.844767382888,-5.89458903006583,
131.511749486344));
#156229=CARTESIAN_POINT('Ctrl Pts',(-101.954154545042,-5.48391453579545,
133.788060896094));
#156230=CARTESIAN_POINT('Ctrl Pts',(-102.139786294252,-2.67732355314469,
137.270387150308));
#156231=CARTESIAN_POINT('Ctrl Pts',(-102.418233918063,3.99289247164586,
136.551914030995));
#156232=CARTESIAN_POINT('Ctrl Pts',(-102.696681541877,6.99383537863429,
130.551720108334));
#156233=CARTESIAN_POINT('Ctrl Pts',(-102.975129165689,3.56778524051166,
124.783690471483));
#156234=CARTESIAN_POINT('Ctrl Pts',(-103.253576789502,-3.13688523764292,
124.548362572792));
#156235=CARTESIAN_POINT('Ctrl Pts',(-103.449075336869,-5.82033628648036,
128.419490590634));
#156236=CARTESIAN_POINT('Ctrl Pts',(-103.551758009631,-5.9253140316399,
130.591901291897));
#156237=CARTESIAN_POINT('Ctrl Pts',(-103.561624807789,-5.92383021006907,
130.800793567564));
#156238=CARTESIAN_POINT('',(-105.311624807789,-5.90881016785237,130.801032495528));
#156239=CARTESIAN_POINT('Ctrl Pts',(-103.561624807789,-5.92383021006907,
130.800793567564));
#156240=CARTESIAN_POINT('Ctrl Pts',(-103.644573884235,-5.91135588689535,
132.556927732469));
#156241=CARTESIAN_POINT('Ctrl Pts',(-103.820338835288,-4.15204534669574,
136.299789154536));
#156242=CARTESIAN_POINT('Ctrl Pts',(-104.08891966094,2.21739010421207,137.442187193775));
#156243=CARTESIAN_POINT('Ctrl Pts',(-104.367367284755,6.78314500569334,
132.526714925521));
#156244=CARTESIAN_POINT('Ctrl Pts',(-104.645814908566,5.11552102198397,
126.028483189903));
#156245=CARTESIAN_POINT('Ctrl Pts',(-104.924262532381,-1.25301687383302,
123.919049495752));
#156246=CARTESIAN_POINT('Ctrl Pts',(-105.146199165453,-5.41128692724257,
127.280870894205));
#156247=CARTESIAN_POINT('Ctrl Pts',(-105.275319923923,-5.91274898233932,
130.027409099224));
#156248=CARTESIAN_POINT('Ctrl Pts',(-105.311624807789,-5.90881016785237,
130.801032495528));
#156249=CARTESIAN_POINT('',(-107.061624807789,-5.91162666396341,130.809137112237));
#156250=CARTESIAN_POINT('Ctrl Pts',(-105.311624807789,-5.90881016785237,
130.801032495528));
#156251=CARTESIAN_POINT('Ctrl Pts',(-105.368135798528,-5.90267913848951,
132.005229284751));
#156252=CARTESIAN_POINT('Ctrl Pts',(-105.517462663871,-4.95855140697165,
135.196076695011));
#156253=CARTESIAN_POINT('Ctrl Pts',(-105.759605403818,0.263283643556469,
137.797803421612));
#156254=CARTESIAN_POINT('Ctrl Pts',(-106.038053027631,6.02609273603925,
134.362979291574));
#156255=CARTESIAN_POINT('Ctrl Pts',(-106.316500651444,6.25121699508972,
127.657958448323));
#156256=CARTESIAN_POINT('Ctrl Pts',(-106.594948275257,0.731778224585158,
123.844327488307));
#156257=CARTESIAN_POINT('Ctrl Pts',(-106.843322994039,-4.79139051656404,
126.147733406097));
#156258=CARTESIAN_POINT('Ctrl Pts',(-106.998881838216,-5.90155799568876,
129.473741766361));
#156259=CARTESIAN_POINT('Ctrl Pts',(-107.061624807789,-5.91162666396341,
130.809137112237));
#156260=CARTESIAN_POINT('',(-108.811623984105,-5.9219077054752,130.805771569576));
#156261=CARTESIAN_POINT('Ctrl Pts',(-107.061624807789,-5.91162666396341,
130.809137112237));
#156262=CARTESIAN_POINT('Ctrl Pts',(-107.09169771282,-5.91645260871668,
131.449196352165));
#156263=CARTESIAN_POINT('Ctrl Pts',(-107.214586492457,-5.52527017600959,
134.058970572693));
#156264=CARTESIAN_POINT('Ctrl Pts',(-107.430291146694,-1.71202952148277,
137.590118898561));
#156265=CARTESIAN_POINT('Ctrl Pts',(-107.708738770509,4.78365684944718,
135.912607643408));
#156266=CARTESIAN_POINT('Ctrl Pts',(-107.987186394321,6.88339627035972,
129.540866923268));
#156267=CARTESIAN_POINT('Ctrl Pts',(-108.265634018135,2.65763079141432,
124.330215183077));
#156268=CARTESIAN_POINT('Ctrl Pts',(-108.540446324043,-3.9233124235248,
125.059341665262));
#156269=CARTESIAN_POINT('Ctrl Pts',(-108.722442755349,-5.9199882563494,
128.919623569311));
#156270=CARTESIAN_POINT('Ctrl Pts',(-108.811623312048,-5.92611609334515,
130.805758370925));
#156271=CARTESIAN_POINT('',(-110.561624807789,-5.91596713820667,130.798889816873));
#156272=CARTESIAN_POINT('Ctrl Pts',(-108.811624807789,-5.91674982788728,
130.805787746087));
#156273=CARTESIAN_POINT('Ctrl Pts',(-108.815259627113,-5.91673131483953,
130.882541220298));
#156274=CARTESIAN_POINT('Ctrl Pts',(-108.818894446437,-5.9152193692786,
130.959274886021));
#156275=CARTESIAN_POINT('Ctrl Pts',(-108.822529265761,-5.91221591608982,
131.035949745191));
#156276=CARTESIAN_POINT('Ctrl Pts',(-108.829952532166,-5.90608206701258,
131.192540171146));
#156277=CARTESIAN_POINT('Ctrl Pts',(-108.837375798572,-5.89371348566192,
131.349123520698));
#156278=CARTESIAN_POINT('Ctrl Pts',(-108.844799064977,-5.87510057860846,
131.50516283912));
#156279=CARTESIAN_POINT('Ctrl Pts',(-108.852213557698,-5.85650967046538,
131.661017732025));
#156280=CARTESIAN_POINT('Ctrl Pts',(-108.859628050419,-5.83168917087945,
131.816329506644));
#156281=CARTESIAN_POINT('Ctrl Pts',(-108.86704254314,-5.80068147127559,
131.970561728567));
#156282=CARTESIAN_POINT('Ctrl Pts',(-108.874449889494,-5.76970365806003,
132.124645295668));
#156283=CARTESIAN_POINT('Ctrl Pts',(-108.881857235847,-5.73255058997771,
132.277651018013));
#156284=CARTESIAN_POINT('Ctrl Pts',(-108.889264582201,-5.68931637196582,
132.429048212823));
#156285=CARTESIAN_POINT('Ctrl Pts',(-108.896666403877,-5.64611439966498,
132.580332489893));
#156286=CARTESIAN_POINT('Ctrl Pts',(-108.904068225552,-5.59684041039193,
132.730010270789));
#156287=CARTESIAN_POINT('Ctrl Pts',(-108.911470047227,-5.54163941588126,
132.877561800966));
#156288=CARTESIAN_POINT('Ctrl Pts',(-108.918867961539,-5.4864675615459,
133.025035439839));
#156289=CARTESIAN_POINT('Ctrl Pts',(-108.92626587585,-5.42537506363842,
133.170384714623));
#156290=CARTESIAN_POINT('Ctrl Pts',(-108.933663790161,-5.35855650725274,
133.313105865908));
#156291=CARTESIAN_POINT('Ctrl Pts',(-108.941060475073,-5.29174905489902,
133.455803299527));
#156292=CARTESIAN_POINT('Ctrl Pts',(-108.948457159985,-5.21921759077214,
133.595873138712));
#156293=CARTESIAN_POINT('Ctrl Pts',(-108.955853844898,-5.14120453535692,
133.732832315931));
#156294=CARTESIAN_POINT('Ctrl Pts',(-108.963250201833,-5.0631949391221,
133.869785420237));
#156295=CARTESIAN_POINT('Ctrl Pts',(-108.970646558768,-4.97970441964543,
134.003627812462));
#156296=CARTESIAN_POINT('Ctrl Pts',(-108.978042915704,-4.89102085423309,
134.13390196225));
#156297=CARTESIAN_POINT('Ctrl Pts',(-108.98544040504,-4.80232371114049,
134.264196057341));
#156298=CARTESIAN_POINT('Ctrl Pts',(-108.992837894377,-4.70843214910487,
134.390920513623));
#156299=CARTESIAN_POINT('Ctrl Pts',(-109.000235383713,-4.60967668691873,
134.513647800379));
#156300=CARTESIAN_POINT('Ctrl Pts',(-109.007635466228,-4.51088660615854,
134.636418108995));
#156301=CARTESIAN_POINT('Ctrl Pts',(-109.015035548743,-4.40722946441964,
134.755188167652));
#156302=CARTESIAN_POINT('Ctrl Pts',(-109.022435631258,-4.29907515848576,
134.869564590824));
#156303=CARTESIAN_POINT('Ctrl Pts',(-109.029843850925,-4.19080192577381,
134.984066782631));
#156304=CARTESIAN_POINT('Ctrl Pts',(-109.037252070591,-4.07802190982685,
135.094165419218));
#156305=CARTESIAN_POINT('Ctrl Pts',(-109.044660290258,-3.96114138987724,
135.199504466395));
#156306=CARTESIAN_POINT('Ctrl Pts',(-109.05207306956,-3.84418893191785,
135.304908347998));
#156307=CARTESIAN_POINT('Ctrl Pts',(-109.059485848862,-3.72313122737752,
135.405546564814));
#156308=CARTESIAN_POINT('Ctrl Pts',(-109.066898628164,-3.59840610478514,
135.501104603302));
#156309=CARTESIAN_POINT('Ctrl Pts',(-109.074321999192,-3.47350276908874,
135.596799179596));
#156310=CARTESIAN_POINT('Ctrl Pts',(-109.081745370221,-3.34492185387414,
135.687398865671));
#156311=CARTESIAN_POINT('Ctrl Pts',(-109.08916874125,-3.21312919254382,
135.772633089414));
#156312=CARTESIAN_POINT('Ctrl Pts',(-109.093104790691,-3.14324956117784,
135.817826320014));
#156313=CARTESIAN_POINT('Ctrl Pts',(-109.097040840132,-3.07246739784303,
135.861511897964));
#156314=CARTESIAN_POINT('Ctrl Pts',(-109.100976889573,-3.00085462453805,
135.903654890785));
#156315=CARTESIAN_POINT('Ctrl Pts',(-109.108400155979,-2.86579516905582,
135.98313526));
#156316=CARTESIAN_POINT('Ctrl Pts',(-109.115823422384,-2.72737164206612,
136.057366347408));
#156317=CARTESIAN_POINT('Ctrl Pts',(-109.12324668879,-2.58603061330607,
136.126049844639));
#156318=CARTESIAN_POINT('Ctrl Pts',(-109.130661181511,-2.44485663790436,
136.19465216368));
#156319=CARTESIAN_POINT('Ctrl Pts',(-109.138075674232,-2.30077235695841,
136.257719782308));
#156320=CARTESIAN_POINT('Ctrl Pts',(-109.145490166953,-2.15425200152916,
136.314998409728));
#156321=CARTESIAN_POINT('Ctrl Pts',(-109.152897513306,-2.00787286793487,
136.372221829852));
#156322=CARTESIAN_POINT('Ctrl Pts',(-109.16030485966,-1.85906267956538,
136.423667231745));
#156323=CARTESIAN_POINT('Ctrl Pts',(-109.167712206014,-1.70831878088991,
136.469126941551));
#156324=CARTESIAN_POINT('Ctrl Pts',(-109.175114027689,-1.55768731270089,
136.514552745792));
#156325=CARTESIAN_POINT('Ctrl Pts',(-109.182515849365,-1.40512536175021,
136.554001639762));
#156326=CARTESIAN_POINT('Ctrl Pts',(-109.18991767104,-1.25114859464169,
136.587314685914));
#156327=CARTESIAN_POINT('Ctrl Pts',(-109.197315585352,-1.09725311067041,
136.620610146369));
#156328=CARTESIAN_POINT('Ctrl Pts',(-109.204713499663,-0.941944661902468,
136.647776131024));
#156329=CARTESIAN_POINT('Ctrl Pts',(-109.212111413974,-0.785752253391338,
136.668704055564));
#156330=CARTESIAN_POINT('Ctrl Pts',(-109.219508098887,-0.629585801224661,
136.689628502263));
#156331=CARTESIAN_POINT('Ctrl Pts',(-109.226904783799,-0.472536050493206,
136.704316896771));
#156332=CARTESIAN_POINT('Ctrl Pts',(-109.234301468711,-0.315140453785023,
136.712712084506));
#156333=CARTESIAN_POINT('Ctrl Pts',(-109.241697825646,-0.157751836162537,
136.721106899989));
#156334=CARTESIAN_POINT('Ctrl Pts',(-109.249094182582,-1.77758225209934E-5,
136.723209043659));
#156335=CARTESIAN_POINT('Ctrl Pts',(-109.256490539517,0.157521189271796,
136.719013408511));
#156336=CARTESIAN_POINT('Ctrl Pts',(-109.263888028854,0.315084273983848,
136.714817131));
#156337=CARTESIAN_POINT('Ctrl Pts',(-109.271285518191,0.472451830786333,
136.704321164749));
#156338=CARTESIAN_POINT('Ctrl Pts',(-109.278683007527,0.629085512500264,
136.687572493783));
#156339=CARTESIAN_POINT('Ctrl Pts',(-109.286083090042,0.785774101908284,
136.670817951597));
#156340=CARTESIAN_POINT('Ctrl Pts',(-109.293483172557,0.941727933077042,
136.647806380353));
#156341=CARTESIAN_POINT('Ctrl Pts',(-109.300883255072,1.09641610137364,
136.618636350204));
#156342=CARTESIAN_POINT('Ctrl Pts',(-109.308291474739,1.2512743652134,136.589434244609));
#156343=CARTESIAN_POINT('Ctrl Pts',(-109.315699694405,1.4048638197542,136.55406022548));
#156344=CARTESIAN_POINT('Ctrl Pts',(-109.323107914072,1.55666531949973,
136.512663661866));
#156345=CARTESIAN_POINT('Ctrl Pts',(-109.330520693374,1.70856025053627,
136.471241619358));
#156346=CARTESIAN_POINT('Ctrl Pts',(-109.337933472676,1.85866467886952,
136.423789758408));
#156347=CARTESIAN_POINT('Ctrl Pts',(-109.345346251978,2.00647733833629,
136.370506434309));
#156348=CARTESIAN_POINT('Ctrl Pts',(-109.352769623007,2.15450119946242,
136.317146976497));
#156349=CARTESIAN_POINT('Ctrl Pts',(-109.360192994036,2.30022640671125,
136.257939554269));
#156350=CARTESIAN_POINT('Ctrl Pts',(-109.367616365064,2.4431735257698,136.193129835623));
#156351=CARTESIAN_POINT('Ctrl Pts',(-109.371552414505,2.51896751826102,
136.15876616771));
#156352=CARTESIAN_POINT('Ctrl Pts',(-109.375488463946,2.59398092045337,
136.122828251008));
#156353=CARTESIAN_POINT('Ctrl Pts',(-109.379424513386,2.66814546706626,
136.085357713671));
#156354=CARTESIAN_POINT('Ctrl Pts',(-109.386847779792,2.80801748738663,
136.014689449668));
#156355=CARTESIAN_POINT('Ctrl Pts',(-109.394271046197,2.94529150107708,
135.938353531993));
#156356=CARTESIAN_POINT('Ctrl Pts',(-109.401694312603,3.07947515100627,
135.856564429452));
#156357=CARTESIAN_POINT('Ctrl Pts',(-109.409108805324,3.21350020700451,
135.774871994838));
#156358=CARTESIAN_POINT('Ctrl Pts',(-109.416523298045,3.3444418540295,135.68773939698));
#156359=CARTESIAN_POINT('Ctrl Pts',(-109.423937790766,3.47182981656182,
135.595428169514));
#156360=CARTESIAN_POINT('Ctrl Pts',(-109.43134513712,3.59909499777978,135.503205915085));
#156361=CARTESIAN_POINT('Ctrl Pts',(-109.438752483473,3.72281301310655,
135.405815185433));
#156362=CARTESIAN_POINT('Ctrl Pts',(-109.446159829827,3.84254031381146,
135.303562157754));
#156363=CARTESIAN_POINT('Ctrl Pts',(-109.453561651503,3.96217831737845,
135.201385394241));
#156364=CARTESIAN_POINT('Ctrl Pts',(-109.460963473178,4.07783125014783,
135.094353794911));
#156365=CARTESIAN_POINT('Ctrl Pts',(-109.468365294853,4.18908666306373,
134.982815295056));
#156366=CARTESIAN_POINT('Ctrl Pts',(-109.475763209165,4.30028334511317,
134.871335675507));
#156367=CARTESIAN_POINT('Ctrl Pts',(-109.483161123476,4.40708686756276,
134.755354157267));
#156368=CARTESIAN_POINT('Ctrl Pts',(-109.490559037787,4.50911993520033,
134.635257114795));
#156369=CARTESIAN_POINT('Ctrl Pts',(-109.4979557227,4.61113604679298,134.515180030272));
#156370=CARTESIAN_POINT('Ctrl Pts',(-109.505352407612,4.70838303551247,
134.390989063117));
#156371=CARTESIAN_POINT('Ctrl Pts',(-109.512749092524,4.8005223093399,134.263105493967));
#156372=CARTESIAN_POINT('Ctrl Pts',(-109.520145449459,4.89265749761539,
134.135227595308));
#156373=CARTESIAN_POINT('Ctrl Pts',(-109.527541806395,4.97968520310246,
134.003657723085));
#156374=CARTESIAN_POINT('Ctrl Pts',(-109.53493816333,5.06130895516232,133.868847886734));
#156375=CARTESIAN_POINT('Ctrl Pts',(-109.542335652667,5.142945204027,133.734017410654));
#156376=CARTESIAN_POINT('Ctrl Pts',(-109.549733142003,5.21917565872633,
133.595946302098));
#156377=CARTESIAN_POINT('Ctrl Pts',(-109.55713063134,5.28974885845261,133.45511288381));
#156378=CARTESIAN_POINT('Ctrl Pts',(-109.564530713855,5.36034679750456,
133.314230096586));
#156379=CARTESIAN_POINT('Ctrl Pts',(-109.57193079637,5.4252833660262,133.170583405236));
#156380=CARTESIAN_POINT('Ctrl Pts',(-109.579330878885,5.484354526957,133.024672754439));
#156381=CARTESIAN_POINT('Ctrl Pts',(-109.586739098551,5.54349064270199,
132.878601659882));
#156382=CARTESIAN_POINT('Ctrl Pts',(-109.594147318218,5.59674833037502,
132.730261980499));
#156383=CARTESIAN_POINT('Ctrl Pts',(-109.601555537884,5.64397264756525,
132.580171225721));
#156384=CARTESIAN_POINT('Ctrl Pts',(-109.608968317186,5.69122603053486,
132.429988092587));
#156385=CARTESIAN_POINT('Ctrl Pts',(-109.616381096488,5.73243854603033,
132.278052095933));
#156386=CARTESIAN_POINT('Ctrl Pts',(-109.623793875791,5.76750612936996,
132.124892181059));
#156387=CARTESIAN_POINT('Ctrl Pts',(-109.631217246819,5.80262381891711,
131.971513424115));
#156388=CARTESIAN_POINT('Ctrl Pts',(-109.638640617848,5.83157897180921,
131.816907622169));
#156389=CARTESIAN_POINT('Ctrl Pts',(-109.646063988877,5.85431912953475,
131.661610926439));
#156390=CARTESIAN_POINT('Ctrl Pts',(-109.650000038318,5.86637650680343,
131.57926889207));
#156391=CARTESIAN_POINT('Ctrl Pts',(-109.653936087758,5.87668749585636,
131.496732670503));
#156392=CARTESIAN_POINT('Ctrl Pts',(-109.657872137199,5.88525022058892,
131.414082196287));
#156393=CARTESIAN_POINT('Ctrl Pts',(-109.665295403604,5.90139925220106,
131.258205981348));
#156394=CARTESIAN_POINT('Ctrl Pts',(-109.67271867001,5.91137564021911,131.101452037716));
#156395=CARTESIAN_POINT('Ctrl Pts',(-109.680141936415,5.91509369226822,
130.944350525019));
#156396=CARTESIAN_POINT('Ctrl Pts',(-109.687556429136,5.91880734988857,
130.787434693263));
#156397=CARTESIAN_POINT('Ctrl Pts',(-109.694970921857,5.91627738623169,
130.630172479687));
#156398=CARTESIAN_POINT('Ctrl Pts',(-109.702385414578,5.90746964154779,
130.473100905722));
#156399=CARTESIAN_POINT('Ctrl Pts',(-109.709792760932,5.89867038609981,
130.316180723253));
#156400=CARTESIAN_POINT('Ctrl Pts',(-109.717200107286,5.88360541625958,
130.159451184805));
#156401=CARTESIAN_POINT('Ctrl Pts',(-109.72460745364,5.86229257864988,130.003450956739));
#156402=CARTESIAN_POINT('Ctrl Pts',(-109.732009275315,5.84099563695856,
129.847567079528));
#156403=CARTESIAN_POINT('Ctrl Pts',(-109.73941109699,5.81346015629185,129.692411797898));
#156404=CARTESIAN_POINT('Ctrl Pts',(-109.746812918666,5.7797559256749,129.538520184444));
#156405=CARTESIAN_POINT('Ctrl Pts',(-109.754210832977,5.74606948725895,
129.384709809175));
#156406=CARTESIAN_POINT('Ctrl Pts',(-109.761608747288,5.70622086390113,
129.23216213729));
#156407=CARTESIAN_POINT('Ctrl Pts',(-109.7690066616,5.66033118609864,129.081403442771));
#156408=CARTESIAN_POINT('Ctrl Pts',(-109.776403346512,5.61444913432814,
128.930669801611));
#156409=CARTESIAN_POINT('Ctrl Pts',(-109.783800031424,5.56252812918237,
128.781724904543));
#156410=CARTESIAN_POINT('Ctrl Pts',(-109.791196716336,5.50473958873584,
128.635081331097));
#156411=CARTESIAN_POINT('Ctrl Pts',(-109.798593073272,5.44695361069374,
128.48844425998));
#156412=CARTESIAN_POINT('Ctrl Pts',(-109.805989430207,5.38330075152544,
128.344108656892));
#156413=CARTESIAN_POINT('Ctrl Pts',(-109.813385787143,5.31400104995022,
128.202568273118));
#156414=CARTESIAN_POINT('Ctrl Pts',(-109.820783276479,5.24469073841357,
128.06100621915));
#156415=CARTESIAN_POINT('Ctrl Pts',(-109.828180765816,5.16973202720599,
127.922240571904));
#156416=CARTESIAN_POINT('Ctrl Pts',(-109.835578255152,5.0893914220888,127.786741437605));
#156417=CARTESIAN_POINT('Ctrl Pts',(-109.842978337667,5.00902265369714,
127.651194804295));
#156418=CARTESIAN_POINT('Ctrl Pts',(-109.850378420182,4.92326842542812,
127.518917284658));
#156419=CARTESIAN_POINT('Ctrl Pts',(-109.857778502697,4.83243906788443,
127.390350773162));
#156420=CARTESIAN_POINT('Ctrl Pts',(-109.865186722364,4.74150983412451,
127.261642889571));
#156421=CARTESIAN_POINT('Ctrl Pts',(-109.87259494203,4.64549454174053,127.136654468491));
#156422=CARTESIAN_POINT('Ctrl Pts',(-109.880003161697,4.54474483591337,
127.015795593848));
#156423=CARTESIAN_POINT('Ctrl Pts',(-109.887415940999,4.44393312032338,
126.894862332585));
#156424=CARTESIAN_POINT('Ctrl Pts',(-109.894828720301,4.33838143458433,
126.778063958665));
#156425=CARTESIAN_POINT('Ctrl Pts',(-109.902241499603,4.22847854585466,
126.665773932507));
#156426=CARTESIAN_POINT('Ctrl Pts',(-109.909664870632,4.11841862272379,
126.553323461094));
#156427=CARTESIAN_POINT('Ctrl Pts',(-109.91708824166,4.00399535028944,126.445394458505));
#156428=CARTESIAN_POINT('Ctrl Pts',(-109.924511612689,3.88563145265092,
126.342320862401));
#156429=CARTESIAN_POINT('Ctrl Pts',(-109.92844766213,3.82287207402125,126.287668768531));
#156430=CARTESIAN_POINT('Ctrl Pts',(-109.93238371157,3.75900535471351,126.234380997603));
#156431=CARTESIAN_POINT('Ctrl Pts',(-109.936319761011,3.69409753184754,
126.182502334613));
#156432=CARTESIAN_POINT('Ctrl Pts',(-109.943743027417,3.57168340362395,
126.084660795291));
#156433=CARTESIAN_POINT('Ctrl Pts',(-109.951166293822,3.44519435275468,
125.991538042044));
#156434=CARTESIAN_POINT('Ctrl Pts',(-109.958589560228,3.31503009872752,
125.903492734524));
#156435=CARTESIAN_POINT('Ctrl Pts',(-109.966004052949,3.18501968803915,
125.815551489246));
#156436=CARTESIAN_POINT('Ctrl Pts',(-109.97341854567,3.05134302670548,125.732675951541));
#156437=CARTESIAN_POINT('Ctrl Pts',(-109.980833038391,2.91443346188762,
125.655185134177));
#156438=CARTESIAN_POINT('Ctrl Pts',(-109.988240384744,2.77765585566289,
125.577769005381));
#156439=CARTESIAN_POINT('Ctrl Pts',(-109.995647731098,2.63765187197414,
125.505727447306));
#156440=CARTESIAN_POINT('Ctrl Pts',(-110.003055077452,2.49488435262316,
125.439336607411));
#156441=CARTESIAN_POINT('Ctrl Pts',(-110.010456899127,2.35222331467443,
125.372995284309));
#156442=CARTESIAN_POINT('Ctrl Pts',(-110.017858720803,2.20680318212132,
125.31229644444));
#156443=CARTESIAN_POINT('Ctrl Pts',(-110.025260542478,2.05911184936531,
125.257470592128));
#156444=CARTESIAN_POINT('Ctrl Pts',(-110.03265845679,1.91149848171465,125.202673681957));
#156445=CARTESIAN_POINT('Ctrl Pts',(-110.040056371101,1.76161665070222,
125.153743714522));
#156446=CARTESIAN_POINT('Ctrl Pts',(-110.047454285412,1.60997459952522,
125.110863243246));
#156447=CARTESIAN_POINT('Ctrl Pts',(-110.054850970324,1.45835774850584,
125.067989897928));
#156448=CARTESIAN_POINT('Ctrl Pts',(-110.062247655237,1.30498161674168,
125.031164154989));
#156449=CARTESIAN_POINT('Ctrl Pts',(-110.069644340149,1.1503701075644,125.000518857307));
#156450=CARTESIAN_POINT('Ctrl Pts',(-110.077040697084,0.99576545402345,
124.96987491847));
#156451=CARTESIAN_POINT('Ctrl Pts',(-110.08443705402,0.839925898160404,
124.945410952568));
#156452=CARTESIAN_POINT('Ctrl Pts',(-110.091833410955,0.683385783219098,
124.927208719427));
#156453=CARTESIAN_POINT('Ctrl Pts',(-110.099230900292,0.526821701586567,
124.909003699478));
#156454=CARTESIAN_POINT('Ctrl Pts',(-110.106628389628,0.36955721813547,
124.897062364282));
#156455=CARTESIAN_POINT('Ctrl Pts',(-110.114025878965,0.21213189942102,
124.891414598892));
#156456=CARTESIAN_POINT('Ctrl Pts',(-110.12142596148,0.0546513955053594,
124.885764853687));
#156457=CARTESIAN_POINT('Ctrl Pts',(-110.128826043995,-0.102989683101735,
124.886413084194));
#156458=CARTESIAN_POINT('Ctrl Pts',(-110.13622612651,-0.260251816797729,
124.893337055242));
#156459=CARTESIAN_POINT('Ctrl Pts',(-110.143634346176,-0.417686876376887,
124.900268639907));
#156460=CARTESIAN_POINT('Ctrl Pts',(-110.151042565843,-0.574741785724433,
124.913489730079));
#156461=CARTESIAN_POINT('Ctrl Pts',(-110.158450785509,-0.730881456810193,
124.932926137084));
#156462=CARTESIAN_POINT('Ctrl Pts',(-110.165863564811,-0.887117229258178,
124.952374506874));
#156463=CARTESIAN_POINT('Ctrl Pts',(-110.173276344113,-1.04243627352356,
124.978045755402));
#156464=CARTESIAN_POINT('Ctrl Pts',(-110.180689123416,-1.19631424863407,
125.009814666327));
#156465=CARTESIAN_POINT('Ctrl Pts',(-110.188112494444,-1.35041209181179,
125.041628970162));
#156466=CARTESIAN_POINT('Ctrl Pts',(-110.195535865473,-1.503064392093,125.079558247685));
#156467=CARTESIAN_POINT('Ctrl Pts',(-110.202959236502,-1.65376170556361,
125.123427350601));
#156468=CARTESIAN_POINT('Ctrl Pts',(-110.206895285943,-1.73366503709898,
125.146687801592));
#156469=CARTESIAN_POINT('Ctrl Pts',(-110.210831335383,-1.81301906978824,
125.171617339533));
#156470=CARTESIAN_POINT('Ctrl Pts',(-110.214767384824,-1.89175032196432,
125.198184444643));
#156471=CARTESIAN_POINT('Ctrl Pts',(-110.22219065123,-2.04023500644922,
125.24828917575));
#156472=CARTESIAN_POINT('Ctrl Pts',(-110.229613917635,-2.18695223779104,
125.304372873823));
#156473=CARTESIAN_POINT('Ctrl Pts',(-110.237037184041,-2.33138420732124,
125.366293107839));
#156474=CARTESIAN_POINT('Ctrl Pts',(-110.244451676762,-2.47564547025819,
125.42814015728));
#156475=CARTESIAN_POINT('Ctrl Pts',(-110.251866169483,-2.61762650797175,
125.495809865903));
#156476=CARTESIAN_POINT('Ctrl Pts',(-110.259280662204,-2.75682469126078,
125.569110080662));
#156477=CARTESIAN_POINT('Ctrl Pts',(-110.266688008558,-2.89588871009964,
125.642339645914));
#156478=CARTESIAN_POINT('Ctrl Pts',(-110.274095354912,-3.03217488620213,
125.721188740658));
#156479=CARTESIAN_POINT('Ctrl Pts',(-110.281502701265,-3.16520071159223,
125.805417227425));
#156480=CARTESIAN_POINT('Ctrl Pts',(-110.288904522941,-3.29812732130297,
125.889582893409));
#156481=CARTESIAN_POINT('Ctrl Pts',(-110.296306344616,-3.42779810809489,
125.979119763837));
#156482=CARTESIAN_POINT('Ctrl Pts',(-110.303708166292,-3.5537554233102,
126.07374195255));
#156483=CARTESIAN_POINT('Ctrl Pts',(-110.311106080603,-3.67964624663961,
126.168314190947));
#156484=CARTESIAN_POINT('Ctrl Pts',(-110.318503994915,-3.80182720474181,
126.267966177674));
#156485=CARTESIAN_POINT('Ctrl Pts',(-110.325901909226,-3.91986999238874,
126.372368987918));
#156486=CARTESIAN_POINT('Ctrl Pts',(-110.333298594138,-4.0378931634657,
126.476754448309));
#156487=CARTESIAN_POINT('Ctrl Pts',(-110.340695279051,-4.15177924959809,
126.585888918224));
#156488=CARTESIAN_POINT('Ctrl Pts',(-110.348091963963,-4.26113330376478,
126.699403427771));
#156489=CARTESIAN_POINT('Ctrl Pts',(-110.355488320898,-4.37048250905812,
126.812912903966));
#156490=CARTESIAN_POINT('Ctrl Pts',(-110.362884677834,-4.47529982296371,
126.930801764785));
#156491=CARTESIAN_POINT('Ctrl Pts',(-110.370281034769,-4.57522763305013,
127.052664645306));
#156492=CARTESIAN_POINT('Ctrl Pts',(-110.377678524106,-4.67517074233938,
127.174546183344));
#156493=CARTESIAN_POINT('Ctrl Pts',(-110.385076013442,-4.77022262054007,
127.300402663878));
#156494=CARTESIAN_POINT('Ctrl Pts',(-110.392473502779,-4.86006647560802,
127.429796287883));
#156495=CARTESIAN_POINT('Ctrl Pts',(-110.399873585294,-4.94994182529971,
127.559235270621));
#156496=CARTESIAN_POINT('Ctrl Pts',(-110.407273667809,-5.03460530419998,
127.692213559104));
#156497=CARTESIAN_POINT('Ctrl Pts',(-110.414673750324,-5.11378399586417,
127.828265221557));
#156498=CARTESIAN_POINT('Ctrl Pts',(-110.422081969991,-5.19304975263995,
127.9644664868));
#156499=CARTESIAN_POINT('Ctrl Pts',(-110.429490189657,-5.26681848981989,
128.103747552243));
#156500=CARTESIAN_POINT('Ctrl Pts',(-110.436898409324,-5.33486339628371,
128.245618132381));
#156501=CARTESIAN_POINT('Ctrl Pts',(-110.444311188626,-5.40295018325208,
128.387576031494));
#156502=CARTESIAN_POINT('Ctrl Pts',(-110.451723967928,-5.46530597212129,
128.532126279184));
#156503=CARTESIAN_POINT('Ctrl Pts',(-110.45913674723,-5.52175269184324,
128.678760050051));
#156504=CARTESIAN_POINT('Ctrl Pts',(-110.466560118259,-5.57828006528533,
128.825603338125));
#156505=CARTESIAN_POINT('Ctrl Pts',(-110.473983489287,-5.62888138693405,
128.974535742665));
#156506=CARTESIAN_POINT('Ctrl Pts',(-110.481406860316,-5.67342864712985,
129.125033982147));
#156507=CARTESIAN_POINT('Ctrl Pts',(-110.485342909757,-5.69704867338016,
129.204831759869));
#156508=CARTESIAN_POINT('Ctrl Pts',(-110.489278959197,-5.71896754006529,
129.28506957918));
#156509=CARTESIAN_POINT('Ctrl Pts',(-110.493215008638,-5.73917204703325,
129.365668580662));
#156510=CARTESIAN_POINT('Ctrl Pts',(-110.503025581335,-5.78953162392232,
129.56656096664));
#156511=CARTESIAN_POINT('Ctrl Pts',(-110.512836154033,-5.82936219324129,
129.770190592286));
#156512=CARTESIAN_POINT('Ctrl Pts',(-110.522646726731,-5.85842123244092,
129.975607804126));
#156513=CARTESIAN_POINT('Ctrl Pts',(-110.532236678111,-5.88682678853453,
130.176405569441));
#156514=CARTESIAN_POINT('Ctrl Pts',(-110.541826629492,-5.90493989260881,
130.378911712314));
#156515=CARTESIAN_POINT('Ctrl Pts',(-110.551416580872,-5.91257834870321,
130.582216896192));
#156516=CARTESIAN_POINT('Ctrl Pts',(-110.554819315566,-5.91528864811252,
130.65435423821));
#156517=CARTESIAN_POINT('Ctrl Pts',(-110.55822205026,-5.91668060726454,
130.726591950347));
#156518=CARTESIAN_POINT('Ctrl Pts',(-110.561624784954,-5.91674746965208,
130.798888610095));
#156519=CARTESIAN_POINT('',(-112.311624807789,-5.90708586381852,130.805356254123));
#156520=CARTESIAN_POINT('Ctrl Pts',(-110.561624807789,-5.91596713820667,
130.798889816873));
#156521=CARTESIAN_POINT('Ctrl Pts',(-110.63163741601,-5.90235840387917,
132.286239780293));
#156522=CARTESIAN_POINT('Ctrl Pts',(-110.794465898833,-4.57889102550224,
135.766948144642));
#156523=CARTESIAN_POINT('Ctrl Pts',(-111.050110256264,1.27396758855394,
137.685826094749));
#156524=CARTESIAN_POINT('Ctrl Pts',(-111.328557880076,6.47818239918729,
133.452135784232));
#156525=CARTESIAN_POINT('Ctrl Pts',(-111.607005503889,5.72926406176812,
126.785269446559));
#156526=CARTESIAN_POINT('Ctrl Pts',(-111.885453127702,-0.284568058305057,
123.811751551519));
#156527=CARTESIAN_POINT('Ctrl Pts',(-112.120326229002,-5.13670898525614,
126.723838658395));
#156528=CARTESIAN_POINT('Ctrl Pts',(-112.262383455698,-5.90551418374586,
129.755303443924));
#156529=CARTESIAN_POINT('Ctrl Pts',(-112.311624807789,-5.90708586381852,
130.805356254123));
#156530=CARTESIAN_POINT('',(-114.061623931777,-5.91866510547899,130.80947112303));
#156531=CARTESIAN_POINT('Ctrl Pts',(-112.311624807789,-5.90708586381852,
130.805356254123));
#156532=CARTESIAN_POINT('Ctrl Pts',(-112.355199330302,-5.90847667064653,
131.734566112796));
#156533=CARTESIAN_POINT('Ctrl Pts',(-112.491589727419,-5.26349239955701,
134.641212553306));
#156534=CARTESIAN_POINT('Ctrl Pts',(-112.72079599914,-0.710590888339653,
137.766588789623));
#156535=CARTESIAN_POINT('Ctrl Pts',(-112.999243622954,5.47342800940259,
135.165455245776));
#156536=CARTESIAN_POINT('Ctrl Pts',(-113.277691246766,6.62763395832767,
128.556688789929));
#156537=CARTESIAN_POINT('Ctrl Pts',(-113.556138870579,1.69136807746817,
124.013422938799));
#156538=CARTESIAN_POINT('Ctrl Pts',(-113.817449618239,-4.39972576943155,
125.606239437587));
#156539=CARTESIAN_POINT('Ctrl Pts',(-113.985944491294,-5.90495055333275,
129.204287311635));
#156540=CARTESIAN_POINT('Ctrl Pts',(-114.061623489744,-5.91963258048528,
130.809462585875));
#156541=CARTESIAN_POINT('',(-115.811626237887,-5.92090002699625,130.800994224613));
#156542=CARTESIAN_POINT('Ctrl Pts',(-114.061624807789,-5.9167477783002,
130.809488041834));
#156543=CARTESIAN_POINT('Ctrl Pts',(-114.072743188688,-5.91654351548332,
131.045195388206));
#156544=CARTESIAN_POINT('Ctrl Pts',(-114.083861569587,-5.90225126763551,
131.280316005178));
#156545=CARTESIAN_POINT('Ctrl Pts',(-114.094979950486,-5.8740986305719,
131.513512111122));
#156546=CARTESIAN_POINT('Ctrl Pts',(-114.100998006393,-5.8588604276985,
131.639734374552));
#156547=CARTESIAN_POINT('Ctrl Pts',(-114.107016062299,-5.83956221767358,
131.765393514612));
#156548=CARTESIAN_POINT('Ctrl Pts',(-114.113034118206,-5.81624514316456,
131.890280963224));
#156549=CARTESIAN_POINT('Ctrl Pts',(-114.120457384612,-5.78748355328094,
132.044329515808));
#156550=CARTESIAN_POINT('Ctrl Pts',(-114.127880651017,-5.75255407086956,
132.197467552954));
#156551=CARTESIAN_POINT('Ctrl Pts',(-114.135303917423,-5.71152501721092,
132.349162397819));
#156552=CARTESIAN_POINT('Ctrl Pts',(-114.142718410144,-5.67054445648646,
132.500677951976));
#156553=CARTESIAN_POINT('Ctrl Pts',(-114.150132902865,-5.62347877095304,
132.650753352294));
#156554=CARTESIAN_POINT('Ctrl Pts',(-114.157547395586,-5.57044764258701,
132.798863970207));
#156555=CARTESIAN_POINT('Ctrl Pts',(-114.16495474194,-5.51746762761925,
132.94683183353));
#156556=CARTESIAN_POINT('Ctrl Pts',(-114.172362088294,-5.45853374136815,
133.092838335406));
#156557=CARTESIAN_POINT('Ctrl Pts',(-114.179769434648,-5.39381599992676,
133.236372032308));
#156558=CARTESIAN_POINT('Ctrl Pts',(-114.187171256323,-5.3291465274186,
133.379798676363));
#156559=CARTESIAN_POINT('Ctrl Pts',(-114.194573077999,-5.25870194189213,
133.520755848878));
#156560=CARTESIAN_POINT('Ctrl Pts',(-114.201974899674,-5.18270104518394,
133.65875029642));
#156561=CARTESIAN_POINT('Ctrl Pts',(-114.209372813985,-5.10674026875731,
133.796671897768));
#156562=CARTESIAN_POINT('Ctrl Pts',(-114.216770728297,-5.02522920225714,
133.931633562767));
#156563=CARTESIAN_POINT('Ctrl Pts',(-114.224168642608,-4.93843337962503,
134.063165048259));
#156564=CARTESIAN_POINT('Ctrl Pts',(-114.23156532752,-4.85165198088412,
134.194674675605));
#156565=CARTESIAN_POINT('Ctrl Pts',(-114.238962012432,-4.75958777444136,
134.322754943523));
#156566=CARTESIAN_POINT('Ctrl Pts',(-114.246358697344,-4.66255062608722,
134.446963014435));
#156567=CARTESIAN_POINT('Ctrl Pts',(-114.25375505428,-4.56551778046164,
134.57116557783));
#156568=CARTESIAN_POINT('Ctrl Pts',(-114.261151411215,-4.46351266118179,
134.691495991443));
#156569=CARTESIAN_POINT('Ctrl Pts',(-114.268547768151,-4.356886410264,134.807543272724));
#156570=CARTESIAN_POINT('Ctrl Pts',(-114.275945257487,-4.25024383459528,
134.923608321139));
#156571=CARTESIAN_POINT('Ctrl Pts',(-114.283342746824,-4.13897897113188,
135.035388656619));
#156572=CARTESIAN_POINT('Ctrl Pts',(-114.29074023616,-4.02348080581559,
135.142509159022));
#156573=CARTESIAN_POINT('Ctrl Pts',(-114.298140318675,-3.90794215279632,
135.24966721235));
#156574=CARTESIAN_POINT('Ctrl Pts',(-114.30554040119,-3.78816751686652,
135.35216192663));
#156575=CARTESIAN_POINT('Ctrl Pts',(-114.312940483705,-3.6645798980917,
135.449657672976));
#156576=CARTESIAN_POINT('Ctrl Pts',(-114.320348703371,-3.5408563820251,
135.547260625918));
#156577=CARTESIAN_POINT('Ctrl Pts',(-114.327756923038,-3.41331180314285,
135.63985340195));
#156578=CARTESIAN_POINT('Ctrl Pts',(-114.335165142704,-3.2823997470893,
135.727142601649));
#156579=CARTESIAN_POINT('Ctrl Pts',(-114.342577922006,-3.15140711684963,
135.814485526393));
#156580=CARTESIAN_POINT('Ctrl Pts',(-114.349990701308,-3.01704319734404,
135.896518176282));
#156581=CARTESIAN_POINT('Ctrl Pts',(-114.35740348061,-2.87978677346191,
135.972992806249));
#156582=CARTESIAN_POINT('Ctrl Pts',(-114.364826851639,-2.74233423116445,
136.049576706755));
#156583=CARTESIAN_POINT('Ctrl Pts',(-114.372250222667,-2.60198126228096,
136.120586558186));
#156584=CARTESIAN_POINT('Ctrl Pts',(-114.379673593696,-2.45922799312802,
136.185822151417));
#156585=CARTESIAN_POINT('Ctrl Pts',(-114.383609643136,-2.38353678451015,
136.220411628252));
#156586=CARTESIAN_POINT('Ctrl Pts',(-114.387545692577,-2.30717105441215,
136.253378575815));
#156587=CARTESIAN_POINT('Ctrl Pts',(-114.391481742018,-2.23020702790131,
136.28469885304));
#156588=CARTESIAN_POINT('Ctrl Pts',(-114.398905008423,-2.08505527585811,
136.343767918417));
#156589=CARTESIAN_POINT('Ctrl Pts',(-114.406328274828,-1.93733566967042,
136.397155605291));
#156590=CARTESIAN_POINT('Ctrl Pts',(-114.413751541234,-1.78753329477134,
136.444631469448));
#156591=CARTESIAN_POINT('Ctrl Pts',(-114.421166033955,-1.63790797383908,
136.492051221075));
#156592=CARTESIAN_POINT('Ctrl Pts',(-114.428580526676,-1.48620513652192,
136.533572946533));
#156593=CARTESIAN_POINT('Ctrl Pts',(-114.435995019397,-1.33293085872197,
136.569013763104));
#156594=CARTESIAN_POINT('Ctrl Pts',(-114.44340236575,-1.17980431244164,
136.604420420482));
#156595=CARTESIAN_POINT('Ctrl Pts',(-114.450809712104,-1.02510970223607,
136.633757753556));
#156596=CARTESIAN_POINT('Ctrl Pts',(-114.458217058458,-0.869369217879168,
136.65689235396));
#156597=CARTESIAN_POINT('Ctrl Pts',(-114.465618880134,-0.713744890651249,
136.680009699707));
#156598=CARTESIAN_POINT('Ctrl Pts',(-114.473020701809,-0.557076610118659,
136.696933469624));
#156599=CARTESIAN_POINT('Ctrl Pts',(-114.480422523484,-0.39989763209945,
136.707581132365));
#156600=CARTESIAN_POINT('Ctrl Pts',(-114.487820437796,-0.242801627639259,
136.718223174287));
#156601=CARTESIAN_POINT('Ctrl Pts',(-114.495218352107,-0.085195834101807,
136.722595682081));
#156602=CARTESIAN_POINT('Ctrl Pts',(-114.502616266419,0.0723805920462764,
136.720667879059));
#156603=CARTESIAN_POINT('Ctrl Pts',(-114.510012951331,0.229930831850837,
136.718740396403));
#156604=CARTESIAN_POINT('Ctrl Pts',(-114.517409636243,0.387451341047541,
136.710514685474));
#156605=CARTESIAN_POINT('Ctrl Pts',(-114.524806321155,0.544402057809802,
136.696012080607));
#156606=CARTESIAN_POINT('Ctrl Pts',(-114.532202678091,0.701345815212809,
136.681510118801));
#156607=CARTESIAN_POINT('Ctrl Pts',(-114.539599035026,0.857719458703056,
136.660731850808));
#156608=CARTESIAN_POINT('Ctrl Pts',(-114.546995391962,1.01298741618553,
136.633750556243));
#156609=CARTESIAN_POINT('Ctrl Pts',(-114.554392881299,1.16827914558912,
136.606765130773));
#156610=CARTESIAN_POINT('Ctrl Pts',(-114.561790370635,1.32246448410944,
136.573574851671));
#156611=CARTESIAN_POINT('Ctrl Pts',(-114.569187859972,1.47501757614395,
136.534304222224));
#156612=CARTESIAN_POINT('Ctrl Pts',(-114.576587942487,1.62762414542817,
136.49501982652));
#156613=CARTESIAN_POINT('Ctrl Pts',(-114.583988025002,1.77859696773102,
136.44965092976));
#156614=CARTESIAN_POINT('Ctrl Pts',(-114.591388107517,1.92742502709768,
136.398371998267));
#156615=CARTESIAN_POINT('Ctrl Pts',(-114.598796327184,2.07641673821573,
136.347036680318));
#156616=CARTESIAN_POINT('Ctrl Pts',(-114.60620454685,2.2232586233909,136.289778471005));
#156617=CARTESIAN_POINT('Ctrl Pts',(-114.613612766517,2.36745866325774,
136.226820395219));
#156618=CARTESIAN_POINT('Ctrl Pts',(-114.621025545819,2.51174745584301,
136.163823569789));
#156619=CARTESIAN_POINT('Ctrl Pts',(-114.628438325121,2.65339082799382,
136.095120049948));
#156620=CARTESIAN_POINT('Ctrl Pts',(-114.635851104423,2.79192154984266,
136.020978738727));
#156621=CARTESIAN_POINT('Ctrl Pts',(-114.643274475452,2.93065021088314,
135.946731490923));
#156622=CARTESIAN_POINT('Ctrl Pts',(-114.650697846481,3.0662570179886,135.86703112241));
#156623=CARTESIAN_POINT('Ctrl Pts',(-114.658121217509,3.19830319906141,
135.782190185698));
#156624=CARTESIAN_POINT('Ctrl Pts',(-114.66205726695,3.2683172526697,135.737205485325));
#156625=CARTESIAN_POINT('Ctrl Pts',(-114.665993316391,3.33733082178464,
135.690776274222));
#156626=CARTESIAN_POINT('Ctrl Pts',(-114.669929365832,3.405282394333,135.642953633862));
#156627=CARTESIAN_POINT('Ctrl Pts',(-114.677352632237,3.53343693946514,
135.552761626635));
#156628=CARTESIAN_POINT('Ctrl Pts',(-114.684775898643,3.65819956784641,
135.457338287135));
#156629=CARTESIAN_POINT('Ctrl Pts',(-114.692199165048,3.77911419970643,
135.356967170748));
#156630=CARTESIAN_POINT('Ctrl Pts',(-114.699613657769,3.89988592051292,
135.256714684685));
#156631=CARTESIAN_POINT('Ctrl Pts',(-114.70702815049,4.01681841321489,135.151526298038));
#156632=CARTESIAN_POINT('Ctrl Pts',(-114.714442643211,4.12948426701537,
135.041728934219));
#156633=CARTESIAN_POINT('Ctrl Pts',(-114.721849989565,4.24204152922415,
134.932037397233));
#156634=CARTESIAN_POINT('Ctrl Pts',(-114.729257335919,4.350340073857,134.817745985618));
#156635=CARTESIAN_POINT('Ctrl Pts',(-114.736664682272,4.45398540435096,
134.699221921942));
#156636=CARTESIAN_POINT('Ctrl Pts',(-114.744066503948,4.55755343224713,
134.580786257985));
#156637=CARTESIAN_POINT('Ctrl Pts',(-114.751468325623,4.65647491164731,
134.458124507523));
#156638=CARTESIAN_POINT('Ctrl Pts',(-114.758870147299,4.75039216879779,
134.331640703571));
#156639=CARTESIAN_POINT('Ctrl Pts',(-114.76626806161,4.84425984775953,134.205223669434));
#156640=CARTESIAN_POINT('Ctrl Pts',(-114.773665975921,4.93312834354486,
134.07498889897));
#156641=CARTESIAN_POINT('Ctrl Pts',(-114.781063890233,5.01668033561569,
133.941373364232));
#156642=CARTESIAN_POINT('Ctrl Pts',(-114.788460575145,5.10021844286086,
133.807780033974));
#156643=CARTESIAN_POINT('Ctrl Pts',(-114.795857260057,5.17844160216471,
133.670807370693));
#156644=CARTESIAN_POINT('Ctrl Pts',(-114.803253944969,5.25107584609969,
133.530921275429));
#156645=CARTESIAN_POINT('Ctrl Pts',(-114.810650301904,5.32370686935617,
133.391041382862));
#156646=CARTESIAN_POINT('Ctrl Pts',(-114.81804665884,5.39074929796717,133.248248646475));
#156647=CARTESIAN_POINT('Ctrl Pts',(-114.825443015775,5.45197529435011,
133.103033267661));
#156648=CARTESIAN_POINT('Ctrl Pts',(-114.832840505112,5.51321066458958,
132.957795656002));
#156649=CARTESIAN_POINT('Ctrl Pts',(-114.840237994448,5.56862768443936,
132.810135007377));
#156650=CARTESIAN_POINT('Ctrl Pts',(-114.847635483785,5.61804686424543,
132.660561036067));
#156651=CARTESIAN_POINT('Ctrl Pts',(-114.8550355663,5.66748336786831,132.510934631833));
#156652=CARTESIAN_POINT('Ctrl Pts',(-114.862435648815,5.71091772828087,
132.359393923761));
#156653=CARTESIAN_POINT('Ctrl Pts',(-114.86983573133,5.74822051233694,132.206463147358));
#156654=CARTESIAN_POINT('Ctrl Pts',(-114.877243950996,5.78556431463894,
132.053364207844));
#156655=CARTESIAN_POINT('Ctrl Pts',(-114.884652170662,5.81676298725624,
131.898872510325));
#156656=CARTESIAN_POINT('Ctrl Pts',(-114.892060390329,5.84173821886264,
131.743522555029));
#156657=CARTESIAN_POINT('Ctrl Pts',(-114.899473169631,5.86672882230735,
131.588076984428));
#156658=CARTESIAN_POINT('Ctrl Pts',(-114.906885948933,5.88548830776054,
131.431772473239));
#156659=CARTESIAN_POINT('Ctrl Pts',(-114.914298728235,5.89799036179937,
131.275147463837));
#156660=CARTESIAN_POINT('Ctrl Pts',(-114.921722099264,5.91051027935928,
131.118298661276));
#156661=CARTESIAN_POINT('Ctrl Pts',(-114.929145470292,5.91675489371841,
130.961128817903));
#156662=CARTESIAN_POINT('Ctrl Pts',(-114.936568841321,5.91674999712059,
130.804176027378));
#156663=CARTESIAN_POINT('Ctrl Pts',(-114.940504890762,5.91674740082693,
130.720955891807));
#156664=CARTESIAN_POINT('Ctrl Pts',(-114.944440940203,5.91498871043917,
130.637796698842));
#156665=CARTESIAN_POINT('Ctrl Pts',(-114.948376989644,5.91148365346844,
130.554777811116));
#156666=CARTESIAN_POINT('Ctrl Pts',(-114.955800256049,5.90487322541099,
130.398206779802));
#156667=CARTESIAN_POINT('Ctrl Pts',(-114.963223522455,5.89202811549701,
130.241661801239));
#156668=CARTESIAN_POINT('Ctrl Pts',(-114.97064678886,5.87294036464704,130.085679856867));
#156669=CARTESIAN_POINT('Ctrl Pts',(-114.978061281581,5.85387517393344,
129.929882270199));
#156670=CARTESIAN_POINT('Ctrl Pts',(-114.985475774302,5.82858207369721,
129.774646760036));
#156671=CARTESIAN_POINT('Ctrl Pts',(-114.992890267023,5.79710508788874,
129.620509629276));
#156672=CARTESIAN_POINT('Ctrl Pts',(-115.000297613377,5.76565844078429,
129.466521061687));
#156673=CARTESIAN_POINT('Ctrl Pts',(-115.007704959731,5.72803984800505,
129.313629129212));
#156674=CARTESIAN_POINT('Ctrl Pts',(-115.015112306084,5.68434502926818,
129.162364225751));
#156675=CARTESIAN_POINT('Ctrl Pts',(-115.02251412776,5.64068279977563,129.011212141361));
#156676=CARTESIAN_POINT('Ctrl Pts',(-115.029915949435,5.5909534710577,128.861685026835));
#156677=CARTESIAN_POINT('Ctrl Pts',(-115.037317771111,5.53530363613135,
128.714302192945));
#156678=CARTESIAN_POINT('Ctrl Pts',(-115.044715685422,5.47968317831968,
128.566997161305));
#156679=CARTESIAN_POINT('Ctrl Pts',(-115.052113599733,5.41814857019337,
128.421834504317));
#156680=CARTESIAN_POINT('Ctrl Pts',(-115.059511514045,5.35089592921541,
128.279317386806));
#156681=CARTESIAN_POINT('Ctrl Pts',(-115.066908198957,5.28365446440639,
128.136823953055));
#156682=CARTESIAN_POINT('Ctrl Pts',(-115.074304883869,5.21069701183099,
127.996975523491));
#156683=CARTESIAN_POINT('Ctrl Pts',(-115.081701568781,5.13226746114255,
127.860254425562));
#156684=CARTESIAN_POINT('Ctrl Pts',(-115.089097925717,5.05384138810257,
127.72353938999));
#156685=CARTESIAN_POINT('Ctrl Pts',(-115.096494282652,4.96994388514552,
127.589951734135));
#156686=CARTESIAN_POINT('Ctrl Pts',(-115.103890639587,4.88086422080918,
127.459948110036));
#156687=CARTESIAN_POINT('Ctrl Pts',(-115.111288128924,4.79177091814857,
127.32992458205));
#156688=CARTESIAN_POINT('Ctrl Pts',(-115.118685618261,4.69749408535773,
127.203486486365));
#156689=CARTESIAN_POINT('Ctrl Pts',(-115.126083107597,4.59836554095464,
127.081060345729));
#156690=CARTESIAN_POINT('Ctrl Pts',(-115.133483190112,4.49920224719412,
126.9585912888));
#156691=CARTESIAN_POINT('Ctrl Pts',(-115.140883272627,4.39518409038359,
126.84013727696));
#156692=CARTESIAN_POINT('Ctrl Pts',(-115.148283355142,4.28668216292368,
126.726090568075));
#156693=CARTESIAN_POINT('Ctrl Pts',(-115.155691574809,4.17806092644011,
126.61191845311));
#156694=CARTESIAN_POINT('Ctrl Pts',(-115.163099794475,4.06494633050394,
126.502163590066));
#156695=CARTESIAN_POINT('Ctrl Pts',(-115.170508014142,3.94774573611127,
126.39718077491));
#156696=CARTESIAN_POINT('Ctrl Pts',(-115.177920793444,3.83047300670836,
126.292133344582));
#156697=CARTESIAN_POINT('Ctrl Pts',(-115.185333572746,3.709109554784,126.191864051927));
#156698=CARTESIAN_POINT('Ctrl Pts',(-115.192746352048,3.58409416411012,
126.096686076427));
#156699=CARTESIAN_POINT('Ctrl Pts',(-115.200169723077,3.45890014558359,
126.001372106172));
#156700=CARTESIAN_POINT('Ctrl Pts',(-115.207593094105,3.33004407166639,
125.911164195825));
#156701=CARTESIAN_POINT('Ctrl Pts',(-115.215016465134,3.19799259713175,
125.826331498407));
#156702=CARTESIAN_POINT('Ctrl Pts',(-115.218952514575,3.12797573680298,
125.781351166705));
#156703=CARTESIAN_POINT('Ctrl Pts',(-115.222888564016,3.0570609374621,125.737881227666));
#156704=CARTESIAN_POINT('Ctrl Pts',(-115.226824613456,2.98532022709708,
125.695956394701));
#156705=CARTESIAN_POINT('Ctrl Pts',(-115.234247879862,2.85001948629717,
125.616887468158));
#156706=CARTESIAN_POINT('Ctrl Pts',(-115.241671146267,2.71137066658009,
125.543078038184));
#156707=CARTESIAN_POINT('Ctrl Pts',(-115.249094412673,2.56982124356253,
125.474825052563));
#156708=CARTESIAN_POINT('Ctrl Pts',(-115.256508905394,2.42843912020803,
125.406652736303));
#156709=CARTESIAN_POINT('Ctrl Pts',(-115.263923398115,2.28416355051382,
125.344023952788));
#156710=CARTESIAN_POINT('Ctrl Pts',(-115.271337890836,2.13746953731795,
125.287191548239));
#156711=CARTESIAN_POINT('Ctrl Pts',(-115.278745237189,1.99091691333493,
125.230413920901));
#156712=CARTESIAN_POINT('Ctrl Pts',(-115.286152583543,1.84195083213713,
125.179421684325));
#156713=CARTESIAN_POINT('Ctrl Pts',(-115.293559929897,1.69106926797789,
125.134420997658));
#156714=CARTESIAN_POINT('Ctrl Pts',(-115.300961751572,1.54030023698164,
125.089453874201));
#156715=CARTESIAN_POINT('Ctrl Pts',(-115.308363573248,1.3876189238245,125.050469509055));
#156716=CARTESIAN_POINT('Ctrl Pts',(-115.315765394923,1.23354147647298,
125.01762526952));
#156717=CARTESIAN_POINT('Ctrl Pts',(-115.323163309235,1.07954536540657,
124.984798368204));
#156718=CARTESIAN_POINT('Ctrl Pts',(-115.330561223546,0.924154952104155,
124.958105214874));
#156719=CARTESIAN_POINT('Ctrl Pts',(-115.337959137857,0.767899569662173,
124.937652783234));
#156720=CARTESIAN_POINT('Ctrl Pts',(-115.34535582277,0.611670154030214,
124.917203750417));
#156721=CARTESIAN_POINT('Ctrl Pts',(-115.352752507682,0.454576424322626,
124.902993429364));
#156722=CARTESIAN_POINT('Ctrl Pts',(-115.360149192594,0.297156004596891,
124.895077338569));
#156723=CARTESIAN_POINT('Ctrl Pts',(-115.367545549529,0.139742565057531,
124.887161598782));
#156724=CARTESIAN_POINT('Ctrl Pts',(-115.374941906465,-0.0179971628708776,
124.885539553071));
#156725=CARTESIAN_POINT('Ctrl Pts',(-115.3823382634,-0.175522628184875,
124.890214663204));
#156726=CARTESIAN_POINT('Ctrl Pts',(-115.389735752737,-0.333072211050205,
124.894890489108));
#156727=CARTESIAN_POINT('Ctrl Pts',(-115.397133242073,-0.490407092826112,
124.905865379454));
#156728=CARTESIAN_POINT('Ctrl Pts',(-115.40453073141,-0.646989071830415,
124.923090711888));
#156729=CARTESIAN_POINT('Ctrl Pts',(-115.411930813925,-0.803625940404501,
124.940322082636));
#156730=CARTESIAN_POINT('Ctrl Pts',(-115.41933089644,-0.959509009898548,
124.963808217108));
#156731=CARTESIAN_POINT('Ctrl Pts',(-115.426730978955,-1.11410767815242,
124.993448929717));
#156732=CARTESIAN_POINT('Ctrl Pts',(-115.434139198622,-1.26887634353538,
125.023122235336));
#156733=CARTESIAN_POINT('Ctrl Pts',(-115.441547418288,-1.42235742031468,
125.058963564082));
#156734=CARTESIAN_POINT('Ctrl Pts',(-115.448955637955,-1.57403222002663,
125.100821967498));
#156735=CARTESIAN_POINT('Ctrl Pts',(-115.456368417257,-1.72580037304697,
125.142706134063));
#156736=CARTESIAN_POINT('Ctrl Pts',(-115.463781196559,-1.87575967896434,
125.190614641464));
#156737=CARTESIAN_POINT('Ctrl Pts',(-115.471193975861,-2.02340947766266,
125.244347609649));
#156738=CARTESIAN_POINT('Ctrl Pts',(-115.47861734689,-2.17127024531725,
125.298157354019));
#156739=CARTESIAN_POINT('Ctrl Pts',(-115.486040717918,-2.31681457054969,
125.357808039406));
#156740=CARTESIAN_POINT('Ctrl Pts',(-115.493464088947,-2.45956376899659,
125.423052539715));
#156741=CARTESIAN_POINT('Ctrl Pts',(-115.497400138388,-2.53525281923191,
125.4576467393));
#156742=CARTESIAN_POINT('Ctrl Pts',(-115.501336187829,-2.61015649131219,
125.493812804534));
#156743=CARTESIAN_POINT('Ctrl Pts',(-115.505272237269,-2.6842066469748,
125.531508899678));
#156744=CARTESIAN_POINT('Ctrl Pts',(-115.512695503675,-2.8238629295303,
125.602602558666));
#156745=CARTESIAN_POINT('Ctrl Pts',(-115.52011877008,-2.96090396710151,
125.679355937636));
#156746=CARTESIAN_POINT('Ctrl Pts',(-115.527542036486,-3.09483805760692,
125.761553070208));
#156747=CARTESIAN_POINT('Ctrl Pts',(-115.534956529207,-3.22861384913951,
125.843653052596));
#156748=CARTESIAN_POINT('Ctrl Pts',(-115.542371021928,-3.35928968799544,
125.931183788193));
#156749=CARTESIAN_POINT('Ctrl Pts',(-115.549785514649,-3.48639609685202,
126.023882313217));
#156750=CARTESIAN_POINT('Ctrl Pts',(-115.557192861002,-3.61337999576663,
126.116491491912));
#156751=CARTESIAN_POINT('Ctrl Pts',(-115.564600207356,-3.73680101415961,
126.214258325538));
#156752=CARTESIAN_POINT('Ctrl Pts',(-115.57200755371,-3.85621653725284,
126.316875288307));
#156753=CARTESIAN_POINT('Ctrl Pts',(-115.579409375385,-3.97554299574364,
126.419415715473));
#156754=CARTESIAN_POINT('Ctrl Pts',(-115.586811197061,-4.09086962544521,
126.526798826783));
#156755=CARTESIAN_POINT('Ctrl Pts',(-115.594213018736,-4.20178503820745,
126.638675433206));
#156756=CARTESIAN_POINT('Ctrl Pts',(-115.601610933047,-4.31264189958634,
126.750492980839));
#156757=CARTESIAN_POINT('Ctrl Pts',(-115.609008847359,-4.41909191948323,
126.866799035043));
#156758=CARTESIAN_POINT('Ctrl Pts',(-115.61640676167,-4.52075898042449,
126.987206074793));
#156759=CARTESIAN_POINT('Ctrl Pts',(-115.623803446582,-4.6224091461448,
127.107593105078));
#156760=CARTESIAN_POINT('Ctrl Pts',(-115.631200131494,-4.71927768983861,
127.23207948337));
#156761=CARTESIAN_POINT('Ctrl Pts',(-115.638596816407,-4.81102730328872,
127.360242900427));
#156762=CARTESIAN_POINT('Ctrl Pts',(-115.645993173342,-4.90277284846483,
127.488400634584));
#156763=CARTESIAN_POINT('Ctrl Pts',(-115.653389530277,-4.98939969741253,
127.620234779783));
#156764=CARTESIAN_POINT('Ctrl Pts',(-115.660785887213,-5.07061275662749,
127.755292426327));
#156765=CARTESIAN_POINT('Ctrl Pts',(-115.668183376549,-5.15183824976914,
127.890370750541));
#156766=CARTESIAN_POINT('Ctrl Pts',(-115.675580865886,-5.22764811041424,
128.028673238842));
#156767=CARTESIAN_POINT('Ctrl Pts',(-115.682978355222,-5.29779233476972,
128.169720805342));
#156768=CARTESIAN_POINT('Ctrl Pts',(-115.690378437737,-5.36796114807441,
128.310817815848));
#156769=CARTESIAN_POINT('Ctrl Pts',(-115.697778520252,-5.43246020469847,
128.454661486414));
#156770=CARTESIAN_POINT('Ctrl Pts',(-115.705178602767,-5.49108699018608,
128.600751253657));
#156771=CARTESIAN_POINT('Ctrl Pts',(-115.712586822434,-5.5497782418514,
128.747001661617));
#156772=CARTESIAN_POINT('Ctrl Pts',(-115.7199950421,-5.60258418788139,128.895502751981));
#156773=CARTESIAN_POINT('Ctrl Pts',(-115.727403261767,-5.6493514617036,
129.045736546126));
#156774=CARTESIAN_POINT('Ctrl Pts',(-115.734816041069,-5.69614752000235,
129.196062806664));
#156775=CARTESIAN_POINT('Ctrl Pts',(-115.742228820371,-5.73689740369434,
129.348123536281));
#156776=CARTESIAN_POINT('Ctrl Pts',(-115.749641599673,-5.77149865850742,
129.501389475389));
#156777=CARTESIAN_POINT('Ctrl Pts',(-115.757064970702,-5.80614935321605,
129.654874408058));
#156778=CARTESIAN_POINT('Ctrl Pts',(-115.76448834173,-5.83463380511123,
129.809567623405));
#156779=CARTESIAN_POINT('Ctrl Pts',(-115.771911712759,-5.85690118778432,
129.964932813029));
#156780=CARTESIAN_POINT('Ctrl Pts',(-115.7758477622,-5.86870788837696,130.047311164509));
#156781=CARTESIAN_POINT('Ctrl Pts',(-115.779783811641,-5.87876761780374,
130.129878386884));
#156782=CARTESIAN_POINT('Ctrl Pts',(-115.783719861082,-5.88707874326198,
130.212554540263));
#156783=CARTESIAN_POINT('Ctrl Pts',(-115.793021509985,-5.90671954609073,
130.407934339944));
#156784=CARTESIAN_POINT('Ctrl Pts',(-115.802323158887,-5.91663620857664,
130.604307906375));
#156785=CARTESIAN_POINT('Ctrl Pts',(-115.811624807789,-5.91674902639369,
130.800966332757));
#156786=CARTESIAN_POINT('',(-117.561623641159,-5.91240943842373,130.800848266352));
#156787=CARTESIAN_POINT('Ctrl Pts',(-115.811627340781,-5.92410128582936,
130.80101573486));
#156788=CARTESIAN_POINT('Ctrl Pts',(-115.895140722153,-5.91199619999421,
132.568884144565));
#156789=CARTESIAN_POINT('Ctrl Pts',(-116.071469978128,-4.13191312647295,
136.322643274555));
#156790=CARTESIAN_POINT('Ctrl Pts',(-116.340615108709,2.25775535553418,
137.428566327301));
#156791=CARTESIAN_POINT('Ctrl Pts',(-116.619062732521,6.79350378926132,
132.485392085333));
#156792=CARTESIAN_POINT('Ctrl Pts',(-116.897510356334,5.08635412177019,
125.997432047439));
#156793=CARTESIAN_POINT('Ctrl Pts',(-117.175957980147,-1.29490650141688,
123.926804533975));
#156794=CARTESIAN_POINT('Ctrl Pts',(-117.397328771323,-5.42208574202265,
127.305240655926));
#156795=CARTESIAN_POINT('Ctrl Pts',(-117.525883687893,-5.91308356794792,
130.03933258855));
#156796=CARTESIAN_POINT('Ctrl Pts',(-117.561622729858,-5.90901965686141,
130.800830848655));
#156797=CARTESIAN_POINT('',(-119.311626003087,-5.91356406754834,130.809061880768));
#156798=CARTESIAN_POINT('Ctrl Pts',(-117.561624807789,-5.91674897067867,
130.800870564149));
#156799=CARTESIAN_POINT('Ctrl Pts',(-117.569093867034,-5.9168429661827,
130.960222796103));
#156800=CARTESIAN_POINT('Ctrl Pts',(-117.576562926279,-5.91049501553312,
131.119589242322));
#156801=CARTESIAN_POINT('Ctrl Pts',(-117.584031985525,-5.89772831670426,
131.278418910231));
#156802=CARTESIAN_POINT('Ctrl Pts',(-117.591502117278,-5.88495978466076,
131.437271385045));
#156803=CARTESIAN_POINT('Ctrl Pts',(-117.598972249032,-5.8657706965315,
131.595586565996));
#156804=CARTESIAN_POINT('Ctrl Pts',(-117.606442380785,-5.84023618905349,
131.75281821734));
#156805=CARTESIAN_POINT('Ctrl Pts',(-117.613914949671,-5.81469335093576,
131.910101165552));
#156806=CARTESIAN_POINT('Ctrl Pts',(-117.621387518557,-5.78280102702624,
132.066299521576));
#156807=CARTESIAN_POINT('Ctrl Pts',(-117.628860087442,-5.74468556128407,
132.220876895084));
#156808=CARTESIAN_POINT('Ctrl Pts',(-117.636336459297,-5.70655069767341,
132.3755329367));
#156809=CARTESIAN_POINT('Ctrl Pts',(-117.643812831151,-5.66218646917605,
132.528566000158));
#156810=CARTESIAN_POINT('Ctrl Pts',(-117.651289203005,-5.61176918510571,
132.679454528707));
#156811=CARTESIAN_POINT('Ctrl Pts',(-117.658775458655,-5.56128524917017,
132.830542532536));
#156812=CARTESIAN_POINT('Ctrl Pts',(-117.666261714304,-5.50473238764771,
132.979479993584));
#156813=CARTESIAN_POINT('Ctrl Pts',(-117.673747969954,-5.44233557517172,
133.125764083084));
#156814=CARTESIAN_POINT('Ctrl Pts',(-117.681239654599,-5.37989351283663,
133.272154257081));
#156815=CARTESIAN_POINT('Ctrl Pts',(-117.688731339244,-5.3115992067413,
133.415886896698));
#156816=CARTESIAN_POINT('Ctrl Pts',(-117.696223023889,-5.23772362846842,
133.556483753308));
#156817=CARTESIAN_POINT('Ctrl Pts',(-117.703726816965,-5.16372864883794,
133.697307849499));
#156818=CARTESIAN_POINT('Ctrl Pts',(-117.711230610041,-5.08413455551827,
133.834985723117));
#156819=CARTESIAN_POINT('Ctrl Pts',(-117.718734403117,-4.99925627082989,
133.969067128614));
#156820=CARTESIAN_POINT('Ctrl Pts',(-117.723440678002,-4.94602178855046,
134.05316112546));
#156821=CARTESIAN_POINT('Ctrl Pts',(-117.728146952887,-4.89070954258863,
134.135841027791));
#156822=CARTESIAN_POINT('Ctrl Pts',(-117.732853227772,-4.83340515316376,
134.217002583532));
#156823=CARTESIAN_POINT('Ctrl Pts',(-117.740276494178,-4.74301822097579,
134.345019723382));
#156824=CARTESIAN_POINT('Ctrl Pts',(-117.747699760583,-4.64740512449227,
134.469636989212));
#156825=CARTESIAN_POINT('Ctrl Pts',(-117.755123026989,-4.54685011284645,
134.590398733302));
#156826=CARTESIAN_POINT('Ctrl Pts',(-117.76253751971,-4.44641394887382,
134.71101774704));
#156827=CARTESIAN_POINT('Ctrl Pts',(-117.76995201243,-4.34104773268394,
134.827790025518));
#156828=CARTESIAN_POINT('Ctrl Pts',(-117.777366505151,-4.23107903775765,
134.940288655957));
#156829=CARTESIAN_POINT('Ctrl Pts',(-117.784773851505,-4.12121633479946,
135.05267885598));
#156830=CARTESIAN_POINT('Ctrl Pts',(-117.792181197859,-4.00676024358271,
135.160803343133));
#156831=CARTESIAN_POINT('Ctrl Pts',(-117.799588544213,-3.88807858660534,
135.26426818016));
#156832=CARTESIAN_POINT('Ctrl Pts',(-117.806990365888,-3.76948544688534,
135.367655849207));
#156833=CARTESIAN_POINT('Ctrl Pts',(-117.814392187564,-3.64667329681064,
135.466390543755));
#156834=CARTESIAN_POINT('Ctrl Pts',(-117.821794009239,-3.52004671324594,
135.560115205333));
#156835=CARTESIAN_POINT('Ctrl Pts',(-117.829191923551,-3.39348697486942,
135.653790390391));
#156836=CARTESIAN_POINT('Ctrl Pts',(-117.836589837862,-3.2631171124924,
135.742460588118));
#156837=CARTESIAN_POINT('Ctrl Pts',(-117.843987752173,-3.12937458057083,
135.825809143338));
#156838=CARTESIAN_POINT('Ctrl Pts',(-117.851384437086,-2.99565427423154,
135.909143847541));
#156839=CARTESIAN_POINT('Ctrl Pts',(-117.858781121998,-2.85856272722925,
135.987158467187));
#156840=CARTESIAN_POINT('Ctrl Pts',(-117.86617780691,-2.71856625699627,
136.059579744189));
#156841=CARTESIAN_POINT('Ctrl Pts',(-117.873574163846,-2.57857599435348,
136.131997809955));
#156842=CARTESIAN_POINT('Ctrl Pts',(-117.880970520781,-2.43568139615297,
136.198822854695));
#156843=CARTESIAN_POINT('Ctrl Pts',(-117.888366877716,-2.29037300995161,
136.259827787093));
#156844=CARTESIAN_POINT('Ctrl Pts',(-117.895764367053,-2.14504237666494,
136.320842059502));
#156845=CARTESIAN_POINT('Ctrl Pts',(-117.90316185639,-1.99729756375695,
136.376034300808));
#156846=CARTESIAN_POINT('Ctrl Pts',(-117.910559345726,-1.84764855807082,
136.425225797266));
#156847=CARTESIAN_POINT('Ctrl Pts',(-117.917959428241,-1.69794709315796,
136.474434537725));
#156848=CARTESIAN_POINT('Ctrl Pts',(-117.925359510757,-1.54634046086461,
136.517638228681));
#156849=CARTESIAN_POINT('Ctrl Pts',(-117.932759593272,-1.39335309306427,
136.554708234932));
#156850=CARTESIAN_POINT('Ctrl Pts',(-117.940167812938,-1.24019749992534,
136.591819003466));
#156851=CARTESIAN_POINT('Ctrl Pts',(-117.947576032605,-1.08565850223514,
136.622782529891));
#156852=CARTESIAN_POINT('Ctrl Pts',(-117.954984252271,-0.930270718780585,
136.64752131639));
#156853=CARTESIAN_POINT('Ctrl Pts',(-117.962397031573,-0.774787296738102,
136.672275329199));
#156854=CARTESIAN_POINT('Ctrl Pts',(-117.969809810875,-0.618454417802717,
136.69079692407));
#156855=CARTESIAN_POINT('Ctrl Pts',(-117.977222590177,-0.461810563770643,
136.703060607029));
#156856=CARTESIAN_POINT('Ctrl Pts',(-117.984645961206,-0.304942889654284,
136.715341812913));
#156857=CARTESIAN_POINT('Ctrl Pts',(-117.992069332235,-0.147763725040503,
136.721347234294));
#156858=CARTESIAN_POINT('Ctrl Pts',(-117.999492703264,0.00918887628557559,
136.721103482272));
#156859=CARTESIAN_POINT('Ctrl Pts',(-118.003428752704,0.0924089115290399,
136.720974239102));
#156860=CARTESIAN_POINT('Ctrl Pts',(-118.007364802145,0.175565331760546,
136.719088996615));
#156861=CARTESIAN_POINT('Ctrl Pts',(-118.011300851585,0.258578789242901,
136.715457603089));
#156862=CARTESIAN_POINT('Ctrl Pts',(-118.018724117991,0.415139579303627,
136.708608908229));
#156863=CARTESIAN_POINT('Ctrl Pts',(-118.026147384396,0.57166482851955,
136.695525578381));
#156864=CARTESIAN_POINT('Ctrl Pts',(-118.033570650802,0.727617543960155,
136.676200471668));
#156865=CARTESIAN_POINT('Ctrl Pts',(-118.040985143523,0.88338593624262,
136.656898205626));
#156866=CARTESIAN_POINT('Ctrl Pts',(-118.048399636244,1.03858277485292,
136.631368892658));
#156867=CARTESIAN_POINT('Ctrl Pts',(-118.055814128965,1.1926718245104,136.599657372825));
#156868=CARTESIAN_POINT('Ctrl Pts',(-118.063221475319,1.34661235734003,
136.567976417749));
#156869=CARTESIAN_POINT('Ctrl Pts',(-118.070628821672,1.49944686367386,
136.530125193037));
#156870=CARTESIAN_POINT('Ctrl Pts',(-118.078036168026,1.65064509589691,
136.486200225465));
#156871=CARTESIAN_POINT('Ctrl Pts',(-118.085437989702,1.80173055877441,
136.442308018791));
#156872=CARTESIAN_POINT('Ctrl Pts',(-118.092839811377,1.95118182057804,
136.392351192844));
#156873=CARTESIAN_POINT('Ctrl Pts',(-118.100241633053,2.09847979422678,
136.336477130775));
#156874=CARTESIAN_POINT('Ctrl Pts',(-118.107639547364,2.24570001042137,
136.280632564189));
#156875=CARTESIAN_POINT('Ctrl Pts',(-118.115037461675,2.39076885411446,
136.218877114466));
#156876=CARTESIAN_POINT('Ctrl Pts',(-118.122435375987,2.53318345952155,
136.151407664573));
#156877=CARTESIAN_POINT('Ctrl Pts',(-118.129832060899,2.67557439820509,
136.083949426879));
#156878=CARTESIAN_POINT('Ctrl Pts',(-118.137228745811,2.81531163700423,
136.010779233283));
#156879=CARTESIAN_POINT('Ctrl Pts',(-118.144625430723,2.95191322018767,
135.932141707178));
#156880=CARTESIAN_POINT('Ctrl Pts',(-118.152021787659,3.08850874631415,
135.853507667942));
#156881=CARTESIAN_POINT('Ctrl Pts',(-118.159418144594,3.22196856975973,
135.769406964465));
#156882=CARTESIAN_POINT('Ctrl Pts',(-118.16681450153,3.35183647923222,135.680129559896));
#156883=CARTESIAN_POINT('Ctrl Pts',(-118.174211990866,3.48172427181245,
135.590838486728));
#156884=CARTESIAN_POINT('Ctrl Pts',(-118.181609480203,3.60801874779308,
135.496369345851));
#156885=CARTESIAN_POINT('Ctrl Pts',(-118.189006969539,3.73029388989078,
135.397054604492));
#156886=CARTESIAN_POINT('Ctrl Pts',(-118.196407052054,3.85261189534983,
135.297705048504));
#156887=CARTESIAN_POINT('Ctrl Pts',(-118.203807134569,3.97090747209434,
135.193506745304));
#156888=CARTESIAN_POINT('Ctrl Pts',(-118.211207217084,4.08478892745061,
135.084831383811));
#156889=CARTESIAN_POINT('Ctrl Pts',(-118.218615436751,4.19879560717483,
134.976036522585));
#156890=CARTESIAN_POINT('Ctrl Pts',(-118.226023656417,4.30837820196499,
134.862755029416));
#156891=CARTESIAN_POINT('Ctrl Pts',(-118.233431876084,4.41318253619956,
134.745394804767));
#156892=CARTESIAN_POINT('Ctrl Pts',(-118.240844655386,4.51805137575309,
134.627962346857));
#156893=CARTESIAN_POINT('Ctrl Pts',(-118.248257434688,4.61813585778442,
134.506446442675));
#156894=CARTESIAN_POINT('Ctrl Pts',(-118.25567021399,4.71312347092657,134.38128635209));
#156895=CARTESIAN_POINT('Ctrl Pts',(-118.263093585019,4.80824680682499,
134.255947426898));
#156896=CARTESIAN_POINT('Ctrl Pts',(-118.270516956048,4.89825851570351,
134.126954221111));
#156897=CARTESIAN_POINT('Ctrl Pts',(-118.277940327076,4.98289015502144,
133.994773798565));
#156898=CARTESIAN_POINT('Ctrl Pts',(-118.281876376517,5.02776388089454,
133.924688566908));
#156899=CARTESIAN_POINT('Ctrl Pts',(-118.285812425958,5.07112584934273,
133.853707695839));
#156900=CARTESIAN_POINT('Ctrl Pts',(-118.289748475398,5.11294145660963,
133.781903266091));
#156901=CARTESIAN_POINT('Ctrl Pts',(-118.297171741804,5.19180438689723,
133.64648235252));
#156902=CARTESIAN_POINT('Ctrl Pts',(-118.304595008209,5.26540273149978,
133.507721367969));
#156903=CARTESIAN_POINT('Ctrl Pts',(-118.312018274615,5.33344022395911,
133.366068239438));
#156904=CARTESIAN_POINT('Ctrl Pts',(-118.319432767336,5.40139730175232,
133.224582533141));
#156905=CARTESIAN_POINT('Ctrl Pts',(-118.326847260057,5.46380644988677,
133.080211820169));
#156906=CARTESIAN_POINT('Ctrl Pts',(-118.334261752778,5.52041554530835,
132.933431487598));
#156907=CARTESIAN_POINT('Ctrl Pts',(-118.341669099131,5.57697007875264,
132.786792627437));
#156908=CARTESIAN_POINT('Ctrl Pts',(-118.349076445485,5.62773555526403,
132.637749117236));
#156909=CARTESIAN_POINT('Ctrl Pts',(-118.356483791839,5.67250657376463,
132.48679924441));
#156910=CARTESIAN_POINT('Ctrl Pts',(-118.363885613514,5.71724420035027,
132.335961955696));
#156911=CARTESIAN_POINT('Ctrl Pts',(-118.37128743519,5.75599616538529,132.183221491774));
#156912=CARTESIAN_POINT('Ctrl Pts',(-118.378689256865,5.78860588724099,
132.029094239501));
#156913=CARTESIAN_POINT('Ctrl Pts',(-118.386087171176,5.82119839467855,
131.875048349804));
#156914=CARTESIAN_POINT('Ctrl Pts',(-118.393485085488,5.84765503934111,
131.719617494006));
#156915=CARTESIAN_POINT('Ctrl Pts',(-118.400882999799,5.86786965320518,
131.563331167386));
#156916=CARTESIAN_POINT('Ctrl Pts',(-118.408279684711,5.88808090776712,
131.407070812718));
#156917=CARTESIAN_POINT('Ctrl Pts',(-118.415676369624,5.90205214245062,
131.249955639233));
#156918=CARTESIAN_POINT('Ctrl Pts',(-118.423073054536,5.90972865699758,
131.092523354855));
#156919=CARTESIAN_POINT('Ctrl Pts',(-118.430469411471,5.91740483115983,
130.935098051189));
#156920=CARTESIAN_POINT('Ctrl Pts',(-118.437865768407,5.91878682197877,
130.777356037443));
#156921=CARTESIAN_POINT('Ctrl Pts',(-118.445262125342,5.91387199031722,
130.619837869263));
#156922=CARTESIAN_POINT('Ctrl Pts',(-118.452659614679,5.9089564061824,130.462295584649));
#156923=CARTESIAN_POINT('Ctrl Pts',(-118.460057104015,5.89774209163881,
130.304977586979));
#156924=CARTESIAN_POINT('Ctrl Pts',(-118.467454593352,5.88027848803428,
130.148422003318));
#156925=CARTESIAN_POINT('Ctrl Pts',(-118.474854675867,5.8628087625905,129.991811539339));
#156926=CARTESIAN_POINT('Ctrl Pts',(-118.482254758382,5.83908542781921,
129.835964392254));
#156927=CARTESIAN_POINT('Ctrl Pts',(-118.489654840897,5.80920947667834,
129.681411011141));
#156928=CARTESIAN_POINT('Ctrl Pts',(-118.497063060563,5.77930067385799,
129.526687682698));
#156929=CARTESIAN_POINT('Ctrl Pts',(-118.50447128023,5.74322581454411,129.373261328048));
#156930=CARTESIAN_POINT('Ctrl Pts',(-118.511879499896,5.7011366363743,129.221650405338));
#156931=CARTESIAN_POINT('Ctrl Pts',(-118.519292279198,5.65902155301762,
129.069946168635));
#156932=CARTESIAN_POINT('Ctrl Pts',(-118.5267050585,5.61088488855768,128.920059944961));
#156933=CARTESIAN_POINT('Ctrl Pts',(-118.534117837803,5.55692728473598,
128.772492089669));
#156934=CARTESIAN_POINT('Ctrl Pts',(-118.541541208831,5.50289258375951,
128.624713382506));
#156935=CARTESIAN_POINT('Ctrl Pts',(-118.54896457986,5.44302047376027,128.479260004));
#156936=CARTESIAN_POINT('Ctrl Pts',(-118.556387950889,5.37755880902272,
128.336610261877));
#156937=CARTESIAN_POINT('Ctrl Pts',(-118.56032400033,5.34284946364741,128.260973945769));
#156938=CARTESIAN_POINT('Ctrl Pts',(-118.56426004977,5.30656944965414,128.186125399019));
#156939=CARTESIAN_POINT('Ctrl Pts',(-118.568196099211,5.26876070642898,
128.112132696143));
#156940=CARTESIAN_POINT('Ctrl Pts',(-118.575619365617,5.19745459667746,
127.972584767753));
#156941=CARTESIAN_POINT('Ctrl Pts',(-118.583042632022,5.12049275345589,
127.83566069445));
#156942=CARTESIAN_POINT('Ctrl Pts',(-118.590465898428,5.03809189118005,
127.701851849081));
#156943=CARTESIAN_POINT('Ctrl Pts',(-118.597880391149,4.95578841988069,
127.568201154656));
#156944=CARTESIAN_POINT('Ctrl Pts',(-118.60529488387,4.86805891926092,127.437658673999));
#156945=CARTESIAN_POINT('Ctrl Pts',(-118.612709376591,4.77516706726302,
127.310693483704));
#156946=CARTESIAN_POINT('Ctrl Pts',(-118.620116722944,4.68236474792912,
127.18385066724));
#156947=CARTESIAN_POINT('Ctrl Pts',(-118.627524069298,4.58441020173542,
127.060578576244));
#156948=CARTESIAN_POINT('Ctrl Pts',(-118.634931415652,4.48161162769726,
126.94131935698));
#156949=CARTESIAN_POINT('Ctrl Pts',(-118.642333237327,4.37888972471427,
126.822149085742));
#156950=CARTESIAN_POINT('Ctrl Pts',(-118.649735059003,4.27133123025304,
126.706986008402));
#156951=CARTESIAN_POINT('Ctrl Pts',(-118.657136880678,4.15928595900455,
126.596240981229));
#156952=CARTESIAN_POINT('Ctrl Pts',(-118.66453479499,4.04729983558228,126.485554415492));
#156953=CARTESIAN_POINT('Ctrl Pts',(-118.671932709301,3.93083191724816,
126.379281516878));
#156954=CARTESIAN_POINT('Ctrl Pts',(-118.679330623612,3.81027029696671,
126.277797812683));
#156955=CARTESIAN_POINT('Ctrl Pts',(-118.686727308524,3.68972871183952,
126.176330973238));
#156956=CARTESIAN_POINT('Ctrl Pts',(-118.694123993437,3.56509506026617,
126.079651988793));
#156957=CARTESIAN_POINT('Ctrl Pts',(-118.701520678349,3.43679216432674,
125.98809752449));
#156958=CARTESIAN_POINT('Ctrl Pts',(-118.708917035284,3.30849495747179,
125.896547119809));
#156959=CARTESIAN_POINT('Ctrl Pts',(-118.71631339222,3.17652913361562,125.8101210003));
#156960=CARTESIAN_POINT('Ctrl Pts',(-118.723709749155,3.04134805101419,
125.729113569875));
#156961=CARTESIAN_POINT('Ctrl Pts',(-118.731107238492,2.9061462718443,125.648093737007));
#156962=CARTESIAN_POINT('Ctrl Pts',(-118.738504727828,2.76772857399205,
125.572494436992));
#156963=CARTESIAN_POINT('Ctrl Pts',(-118.745902217165,2.6265744232531,125.502564944248));
#156964=CARTESIAN_POINT('Ctrl Pts',(-118.75330229968,2.48537079114643,125.432610937829));
#156965=CARTESIAN_POINT('Ctrl Pts',(-118.760702382195,2.34142913056556,
125.368330861475));
#156966=CARTESIAN_POINT('Ctrl Pts',(-118.76810246471,2.19525031250549,125.309926467634));
#156967=CARTESIAN_POINT('Ctrl Pts',(-118.775510684376,2.04891075580638,
125.251457852157));
#156968=CARTESIAN_POINT('Ctrl Pts',(-118.782918904043,1.90032947574322,
125.198877960655));
#156969=CARTESIAN_POINT('Ctrl Pts',(-118.790327123709,1.75002468373652,
125.15233937125));
#156970=CARTESIAN_POINT('Ctrl Pts',(-118.797739903011,1.59962738163832,
125.105772138118));
#156971=CARTESIAN_POINT('Ctrl Pts',(-118.805152682313,1.44750481371909,
125.065253712159));
#156972=CARTESIAN_POINT('Ctrl Pts',(-118.812565461615,1.29418639487025,
125.030885742083));
#156973=CARTESIAN_POINT('Ctrl Pts',(-118.819988832644,1.14064890747486,
124.996468665439));
#156974=CARTESIAN_POINT('Ctrl Pts',(-118.827412203673,0.985912522772439,
124.968219663269));
#156975=CARTESIAN_POINT('Ctrl Pts',(-118.834835574702,0.83051362589355,
124.946188745753));
#156976=CARTESIAN_POINT('Ctrl Pts',(-118.838771624143,0.748117402020576,
124.93450742466));
#156977=CARTESIAN_POINT('Ctrl Pts',(-118.842707673583,0.665534966065186,
124.92457336014));
#156978=CARTESIAN_POINT('Ctrl Pts',(-118.846643723024,0.582846260308975,
124.916388063338));
#156979=CARTESIAN_POINT('Ctrl Pts',(-118.85406698943,0.426897941883304,
124.900950849024));
#156980=CARTESIAN_POINT('Ctrl Pts',(-118.861490255835,0.270100084963614,
124.891690221222));
#156981=CARTESIAN_POINT('Ctrl Pts',(-118.868913522241,0.112983234878659,
124.888689450983));
#156982=CARTESIAN_POINT('Ctrl Pts',(-118.876328014962,-0.0439479161367905,
124.885692227406));
#156983=CARTESIAN_POINT('Ctrl Pts',(-118.883742507683,-0.201196940265092,
124.888940141434));
#156984=CARTESIAN_POINT('Ctrl Pts',(-118.891157000404,-0.358226665715189,
124.898464900702));
#156985=CARTESIAN_POINT('Ctrl Pts',(-118.898564346757,-0.515105040003833,
124.907980479649));
#156986=CARTESIAN_POINT('Ctrl Pts',(-118.905971693111,-0.671764166295322,
124.923760837307));
#156987=CARTESIAN_POINT('Ctrl Pts',(-118.913379039465,-0.827665465319788,
124.945785667971));
#156988=CARTESIAN_POINT('Ctrl Pts',(-118.92078086114,-0.983450487274067,
124.967794071686));
#156989=CARTESIAN_POINT('Ctrl Pts',(-118.928182682815,-1.13847843934629,
124.996037622975));
#156990=CARTESIAN_POINT('Ctrl Pts',(-118.935584504491,-1.29221457313743,
125.030444090678));
#156991=CARTESIAN_POINT('Ctrl Pts',(-118.942982418802,-1.44586955081935,
125.064832395474));
#156992=CARTESIAN_POINT('Ctrl Pts',(-118.950380333114,-1.59823370497385,
125.10537705615));
#156993=CARTESIAN_POINT('Ctrl Pts',(-118.957778247425,-1.7487813201234,
125.15195454078));
#156994=CARTESIAN_POINT('Ctrl Pts',(-118.965174932337,-1.89930391699073,
125.198524285077));
#156995=CARTESIAN_POINT('Ctrl Pts',(-118.972571617249,-2.04801021771648,
125.251124753345));
#156996=CARTESIAN_POINT('Ctrl Pts',(-118.979968302161,-2.19438843071803,
125.309582189128));
#156997=CARTESIAN_POINT('Ctrl Pts',(-118.987364659097,-2.34076015315663,
125.368037032846));
#156998=CARTESIAN_POINT('Ctrl Pts',(-118.994761016032,-2.48480364645216,
125.432348189252));
#156999=CARTESIAN_POINT('Ctrl Pts',(-119.002157372968,-2.62602616904493,
125.50229336771));
#157000=CARTESIAN_POINT('Ctrl Pts',(-119.009554862304,-2.76727031316644,
125.572249254954));
#157001=CARTESIAN_POINT('Ctrl Pts',(-119.016952351641,-2.90569229208119,
125.647840716076));
#157002=CARTESIAN_POINT('Ctrl Pts',(-119.024349840977,-3.04082322118871,
125.728799101834));
#157003=CARTESIAN_POINT('Ctrl Pts',(-119.031749923492,-3.17600152023414,
125.809785867429));
#157004=CARTESIAN_POINT('Ctrl Pts',(-119.039150006007,-3.30788615249289,
125.896143111718));
#157005=CARTESIAN_POINT('Ctrl Pts',(-119.046550088522,-3.43603664490841,
125.987558489873));
#157006=CARTESIAN_POINT('Ctrl Pts',(-119.053958308189,-3.56432805196397,
126.079074388634));
#157007=CARTESIAN_POINT('Ctrl Pts',(-119.061366527855,-3.68887681499692,
126.175659311899));
#157008=CARTESIAN_POINT('Ctrl Pts',(-119.068774747521,-3.80927445978313,
126.276959745924));
#157009=CARTESIAN_POINT('Ctrl Pts',(-119.076187526823,-3.92974620731146,
126.378322528676));
#157010=CARTESIAN_POINT('Ctrl Pts',(-119.083600306125,-4.04606147037299,
126.484406354453));
#157011=CARTESIAN_POINT('Ctrl Pts',(-119.091013085428,-4.15784856734825,
126.594820755123));
#157012=CARTESIAN_POINT('Ctrl Pts',(-119.098436456456,-4.2697953909698,
126.705392921066));
#157013=CARTESIAN_POINT('Ctrl Pts',(-119.105859827485,-4.37720087212692,
126.820307748184));
#157014=CARTESIAN_POINT('Ctrl Pts',(-119.113283198514,-4.47973300657406,
126.9391409922));
#157015=CARTESIAN_POINT('Ctrl Pts',(-119.117219247955,-4.53409800448784,
127.002149229548));
#157016=CARTESIAN_POINT('Ctrl Pts',(-119.121155297396,-4.58709363814147,
127.066258567251));
#157017=CARTESIAN_POINT('Ctrl Pts',(-119.125091346837,-4.63867542540924,
127.131402564415));
#157018=CARTESIAN_POINT('Ctrl Pts',(-119.132863574377,-4.74053018956919,
127.260037627662));
#157019=CARTESIAN_POINT('Ctrl Pts',(-119.140635801916,-4.83719850919677,
127.393125371721));
#157020=CARTESIAN_POINT('Ctrl Pts',(-119.148408029456,-4.92826918109601,
127.53020523928));
#157021=CARTESIAN_POINT('Ctrl Pts',(-119.155813131687,-5.01503808128868,
127.660810066263));
#157022=CARTESIAN_POINT('Ctrl Pts',(-119.163218233918,-5.09672570044091,
127.795038205085));
#157023=CARTESIAN_POINT('Ctrl Pts',(-119.170623336149,-5.17301572214231,
127.93245551799));
#157024=CARTESIAN_POINT('Ctrl Pts',(-119.17802146723,-5.24923392454755,
128.069743466472));
#157025=CARTESIAN_POINT('Ctrl Pts',(-119.18541959831,-5.32006446199202,
128.210214289691));
#157026=CARTESIAN_POINT('Ctrl Pts',(-119.192817729391,-5.38523393391365,
128.353404469544));
#157027=CARTESIAN_POINT('Ctrl Pts',(-119.200210362271,-5.45035497268593,
128.496488232219));
#157028=CARTESIAN_POINT('Ctrl Pts',(-119.207602995152,-5.50982316662364,
128.642286989992));
#157029=CARTESIAN_POINT('Ctrl Pts',(-119.214995628032,-5.56341082638834,
128.790312321391));
#157030=CARTESIAN_POINT('Ctrl Pts',(-119.222384231907,-5.61696928073043,
128.938256978576));
#157031=CARTESIAN_POINT('Ctrl Pts',(-119.229772835783,-5.66465345539427,
129.088425442635));
#157032=CARTESIAN_POINT('Ctrl Pts',(-119.237161439658,-5.70628368712896,
129.240309133597));
#157033=CARTESIAN_POINT('Ctrl Pts',(-119.244548106085,-5.74790300253594,
129.392152997441));
#157034=CARTESIAN_POINT('Ctrl Pts',(-119.251934772511,-5.78347143426546,
129.545710833374));
#157035=CARTESIAN_POINT('Ctrl Pts',(-119.259321438938,-5.81285912307789,
129.700458729829));
#157036=CARTESIAN_POINT('Ctrl Pts',(-119.266707000318,-5.84224241548663,
129.855183475969));
#157037=CARTESIAN_POINT('Ctrl Pts',(-119.274092561699,-5.86544674003761,
130.011097560354));
#157038=CARTESIAN_POINT('Ctrl Pts',(-119.281478123079,-5.88239337269882,
130.167666993184));
#157039=CARTESIAN_POINT('Ctrl Pts',(-119.288865370254,-5.8993438735216,
130.324272163843));
#157040=CARTESIAN_POINT('Ctrl Pts',(-119.296252617429,-5.91003379119672,
130.48153260989));
#157041=CARTESIAN_POINT('Ctrl Pts',(-119.303639864604,-5.91443626993552,
130.638909200615));
#157042=CARTESIAN_POINT('Ctrl Pts',(-119.306301512332,-5.91602249647667,
130.695612467109));
#157043=CARTESIAN_POINT('Ctrl Pts',(-119.30896316006,-5.91679298923901,
130.75233079368));
#157044=CARTESIAN_POINT('Ctrl Pts',(-119.311624807789,-5.91674815043348,
130.809038955094));
#157045=CARTESIAN_POINT('',(-121.061624807789,-5.92598265696487,130.806004651264));
#157046=CARTESIAN_POINT('Ctrl Pts',(-119.311626841947,-5.91132948029671,
130.809077969991));
#157047=CARTESIAN_POINT('Ctrl Pts',(-119.342264218181,-5.9161197406693,
131.461233790425));
#157048=CARTESIAN_POINT('Ctrl Pts',(-119.465717469021,-5.51539089397821,
134.083364516096));
#157049=CARTESIAN_POINT('Ctrl Pts',(-119.681986594463,-1.67069096485224,
137.600414783785));
#157050=CARTESIAN_POINT('Ctrl Pts',(-119.960434218276,4.8146635689039,135.883393522426));
#157051=CARTESIAN_POINT('Ctrl Pts',(-120.238881842088,6.87557749223074,
129.498989146037));
#157052=CARTESIAN_POINT('Ctrl Pts',(-120.517329465902,2.61817159083127,
124.314157381049));
#157053=CARTESIAN_POINT('Ctrl Pts',(-120.791577121135,-3.9446989483673,
125.081750020864));
#157054=CARTESIAN_POINT('Ctrl Pts',(-120.973008901765,-5.91908509112532,
128.931699198858));
#157055=CARTESIAN_POINT('Ctrl Pts',(-121.061624807789,-5.92598265696487,
130.806004651264));
#157056=CARTESIAN_POINT('',(-122.81162480779,-5.91633098458257,130.798887995784));
#157057=CARTESIAN_POINT('Ctrl Pts',(-121.061624807789,-5.92598265696487,
130.806004651264));
#157058=CARTESIAN_POINT('Ctrl Pts',(-121.065824776369,-5.92630956847657,
130.894837732832));
#157059=CARTESIAN_POINT('Ctrl Pts',(-121.070024744948,-5.92448577112936,
130.983657094296));
#157060=CARTESIAN_POINT('Ctrl Pts',(-121.074224713527,-5.92046945784547,
131.0723772017));
#157061=CARTESIAN_POINT('Ctrl Pts',(-121.167040588132,-5.8317122152397,
133.033019098945));
#157062=CARTESIAN_POINT('Ctrl Pts',(-121.35267233734,-3.51266264211408,
136.857356709837));
#157063=CARTESIAN_POINT('Ctrl Pts',(-121.631119961154,3.19387708256752,
137.031455422673));
#157064=CARTESIAN_POINT('Ctrl Pts',(-121.909567584966,6.96539979793815,
131.48315822011));
#157065=CARTESIAN_POINT('Ctrl Pts',(-122.188015208779,4.3360603777024,125.311079181914));
#157066=CARTESIAN_POINT('Ctrl Pts',(-122.466462832592,-2.27790670131724,
124.187057421366));
#157067=CARTESIAN_POINT('Ctrl Pts',(-122.674332698929,-5.65273738408376,
127.887580674196));
#157068=CARTESIAN_POINT('Ctrl Pts',(-122.789386690661,-5.92067836177203,
130.326534880517));
#157069=CARTESIAN_POINT('Ctrl Pts',(-122.81162480779,-5.91633098458257,
130.798887995784));
#157070=CARTESIAN_POINT('',(-124.56162480779,-5.90703164895106,130.80515921599));
#157071=CARTESIAN_POINT('Ctrl Pts',(-122.81162480779,-5.91633098458257,
130.798887995784));
#157072=CARTESIAN_POINT('Ctrl Pts',(-122.882202565266,-5.9025335874754,
132.298008781056));
#157073=CARTESIAN_POINT('Ctrl Pts',(-123.045596197347,-4.5615619224176,
135.790566014123));
#157074=CARTESIAN_POINT('Ctrl Pts',(-123.30180570403,1.31583341844267,137.677943594819));
#157075=CARTESIAN_POINT('Ctrl Pts',(-123.580253327844,6.49418013243721,
133.412652192102));
#157076=CARTESIAN_POINT('Ctrl Pts',(-123.858700951656,5.70469256306374,
126.750468254505));
#157077=CARTESIAN_POINT('Ctrl Pts',(-124.137148575469,-0.327128782042009,
123.813613354913));
#157078=CARTESIAN_POINT('Ctrl Pts',(-124.371456527514,-5.14982080752232,
126.748104892097));
#157079=CARTESIAN_POINT('Ctrl Pts',(-124.512948604954,-5.90578610812664,
129.767134245352));
#157080=CARTESIAN_POINT('Ctrl Pts',(-124.56162480779,-5.90703164895106,
130.80515921599));
#157081=CARTESIAN_POINT('',(-126.311624008903,-5.91848443048205,130.80954271012));
#157082=CARTESIAN_POINT('Ctrl Pts',(-124.56162480779,-5.90703164895106,
130.80515921599));
#157083=CARTESIAN_POINT('Ctrl Pts',(-124.605764479558,-5.90816110770012,
131.746442200737));
#157084=CARTESIAN_POINT('Ctrl Pts',(-124.742720025934,-5.25131157107666,
134.665544139357));
#157085=CARTESIAN_POINT('Ctrl Pts',(-124.972491446908,-0.668196663714802,
137.770785364084));
#157086=CARTESIAN_POINT('Ctrl Pts',(-125.25093907072,5.49987382026564,135.132056134964));
#157087=CARTESIAN_POINT('Ctrl Pts',(-125.529386694533,6.61382894724947,
128.516386145036));
#157088=CARTESIAN_POINT('Ctrl Pts',(-125.807834318346,1.64999837518252,
124.003252921589));
#157089=CARTESIAN_POINT('Ctrl Pts',(-126.068579969149,-4.41813562501859,
125.629593465656));
#157090=CARTESIAN_POINT('Ctrl Pts',(-126.236509745349,-5.9046045021028,
129.216095594019));
#157091=CARTESIAN_POINT('Ctrl Pts',(-126.311623646944,-5.91927129782895,
130.809535722935));
#157092=CARTESIAN_POINT('',(-128.061626221021,-5.9210303473077,130.801168248253));
#157093=CARTESIAN_POINT('Ctrl Pts',(-126.31162480779,-5.91674771714553,
130.809558131701));
#157094=CARTESIAN_POINT('Ctrl Pts',(-126.322548913763,-5.91654423567127,
131.04119743407));
#157095=CARTESIAN_POINT('Ctrl Pts',(-126.333473019736,-5.90273466878703,
131.272263102242));
#157096=CARTESIAN_POINT('Ctrl Pts',(-126.344397125709,-5.87553903220174,
131.501477281815));
#157097=CARTESIAN_POINT('Ctrl Pts',(-126.351174605797,-5.85866644913645,
131.64368521552));
#157098=CARTESIAN_POINT('Ctrl Pts',(-126.357952085885,-5.83664222687754,
131.785181319252));
#157099=CARTESIAN_POINT('Ctrl Pts',(-126.364729565973,-5.80952707624724,
131.925665978674));
#157100=CARTESIAN_POINT('Ctrl Pts',(-126.372152832378,-5.7798282819857,
132.079536597133));
#157101=CARTESIAN_POINT('Ctrl Pts',(-126.379576098784,-5.74396725203922,
132.232459171309));
#157102=CARTESIAN_POINT('Ctrl Pts',(-126.386999365189,-5.70201554897757,
132.383901450124));
#157103=CARTESIAN_POINT('Ctrl Pts',(-126.39441385791,-5.66011342934495,
132.535164736742));
#157104=CARTESIAN_POINT('Ctrl Pts',(-126.401828350631,-5.6121350642719,
132.684950854323));
#157105=CARTESIAN_POINT('Ctrl Pts',(-126.409242843352,-5.55820332708034,
132.832735912558));
#157106=CARTESIAN_POINT('Ctrl Pts',(-126.416650189706,-5.50432357132758,
132.98037852999));
#157107=CARTESIAN_POINT('Ctrl Pts',(-126.42405753606,-5.44450199396681,
133.126023579409));
#157108=CARTESIAN_POINT('Ctrl Pts',(-126.431464882413,-5.37891172124297,
133.269160661702));
#157109=CARTESIAN_POINT('Ctrl Pts',(-126.438866704089,-5.31337036821911,
133.412190986959));
#157110=CARTESIAN_POINT('Ctrl Pts',(-126.446268525764,-5.24206904155062,
133.552716731677));
#157111=CARTESIAN_POINT('Ctrl Pts',(-126.453670347439,-5.16522954159385,
133.690245983471));
#157112=CARTESIAN_POINT('Ctrl Pts',(-126.461068261751,-5.08843060461076,
133.827702634645));
#157113=CARTESIAN_POINT('Ctrl Pts',(-126.468466176062,-5.00609949836088,
133.962165618118));
#157114=CARTESIAN_POINT('Ctrl Pts',(-126.475864090373,-4.91850461436961,
134.093166315829));
#157115=CARTESIAN_POINT('Ctrl Pts',(-126.483260775286,-4.83092428705931,
134.224145243599));
#157116=CARTESIAN_POINT('Ctrl Pts',(-126.490657460198,-4.73808212540959,
134.351662717531));
#157117=CARTESIAN_POINT('Ctrl Pts',(-126.49805414511,-4.64029068514787,
134.475277794489));
#157118=CARTESIAN_POINT('Ctrl Pts',(-126.505450502045,-4.54250358106108,
134.598887390226));
#157119=CARTESIAN_POINT('Ctrl Pts',(-126.512846858981,-4.43976786631959,
134.71859464028));
#157120=CARTESIAN_POINT('Ctrl Pts',(-126.520243215916,-4.33243717820127,
134.833990707219));
#157121=CARTESIAN_POINT('Ctrl Pts',(-126.527640705253,-4.22509005748029,
134.949404441591));
#157122=CARTESIAN_POINT('Ctrl Pts',(-126.535038194589,-4.11314681686869,
135.060505405236));
#157123=CARTESIAN_POINT('Ctrl Pts',(-126.542435683926,-3.99699871856404,
135.166920852829));
#157124=CARTESIAN_POINT('Ctrl Pts',(-126.549835766441,-3.88080990472375,
135.273373604192));
#157125=CARTESIAN_POINT('Ctrl Pts',(-126.557235848956,-3.76041357352431,
135.375137317277));
#157126=CARTESIAN_POINT('Ctrl Pts',(-126.564635931471,-3.6362347602623,
135.471878944339));
#157127=CARTESIAN_POINT('Ctrl Pts',(-126.572044151137,-3.51191939962938,
135.568726948764));
#157128=CARTESIAN_POINT('Ctrl Pts',(-126.579452370804,-3.38381354534519,
135.660541609214));
#157129=CARTESIAN_POINT('Ctrl Pts',(-126.58686059047,-3.25237256065573,
135.747032292803));
#157130=CARTESIAN_POINT('Ctrl Pts',(-126.594273369772,-3.12085067623341,
135.833576209965));
#157131=CARTESIAN_POINT('Ctrl Pts',(-126.601686149074,-2.98598989015763,
135.914789428664));
#157132=CARTESIAN_POINT('Ctrl Pts',(-126.609098928376,-2.84827048654154,
135.990427122924));
#157133=CARTESIAN_POINT('Ctrl Pts',(-126.616522299405,-2.71035430298296,
136.066172891869));
#157134=CARTESIAN_POINT('Ctrl Pts',(-126.623945670433,-2.56957167739537,
136.136327059293));
#157135=CARTESIAN_POINT('Ctrl Pts',(-126.631369041462,-2.42642394555893,
136.200692464193));
#157136=CARTESIAN_POINT('Ctrl Pts',(-126.635305090903,-2.35052358335188,
136.234820546299));
#157137=CARTESIAN_POINT('Ctrl Pts',(-126.639241140344,-2.27395858895807,
136.267322023191));
#157138=CARTESIAN_POINT('Ctrl Pts',(-126.643177189785,-2.19680533298606,
136.298173218253));
#157139=CARTESIAN_POINT('Ctrl Pts',(-126.650600456191,-2.05129670010231,
136.356357609303));
#157140=CARTESIAN_POINT('Ctrl Pts',(-126.658023722596,-1.90325484481399,
136.408845095856));
#157141=CARTESIAN_POINT('Ctrl Pts',(-126.665446989002,-1.75316624634602,
136.455408190819));
#157142=CARTESIAN_POINT('Ctrl Pts',(-126.672861481723,-1.60325504013736,
136.501916252071));
#157143=CARTESIAN_POINT('Ctrl Pts',(-126.680275974443,-1.45130225899473,
136.542513749999));
#157144=CARTESIAN_POINT('Ctrl Pts',(-126.687690467164,-1.29781508270283,
136.577020885901));
#157145=CARTESIAN_POINT('Ctrl Pts',(-126.695097813518,-1.14447584312969,
136.611494762526));
#157146=CARTESIAN_POINT('Ctrl Pts',(-126.702505159872,-0.989605514383623,
136.639889882046));
#157147=CARTESIAN_POINT('Ctrl Pts',(-126.709912506226,-0.833727088658144,
136.662076017288));
#157148=CARTESIAN_POINT('Ctrl Pts',(-126.717314327901,-0.677964922943527,
136.684245605273));
#157149=CARTESIAN_POINT('Ctrl Pts',(-126.724716149577,-0.521196525320297,
136.70021537734));
#157150=CARTESIAN_POINT('Ctrl Pts',(-126.732117971252,-0.363955644118238,
136.709906049752));
#157151=CARTESIAN_POINT('Ctrl Pts',(-126.739515885563,-0.206797769153853,
136.719591606534));
#157152=CARTESIAN_POINT('Ctrl Pts',(-126.746913799875,-0.0491682789911599,
136.723004642116));
#157153=CARTESIAN_POINT('Ctrl Pts',(-126.754311714186,0.108393492546098,
136.720117662381));
#157154=CARTESIAN_POINT('Ctrl Pts',(-126.761708399098,0.265929080175612,
136.717231162409));
#157155=CARTESIAN_POINT('Ctrl Pts',(-126.769105084011,0.42339659864496,
136.708046731834));
#157156=CARTESIAN_POINT('Ctrl Pts',(-126.776501768923,0.580256126001817,
136.692588992106));
#157157=CARTESIAN_POINT('Ctrl Pts',(-126.783898125858,0.737108698042853,
136.677131937791));
#157158=CARTESIAN_POINT('Ctrl Pts',(-126.791294482794,0.893352961076833,
136.655402164018));
#157159=CARTESIAN_POINT('Ctrl Pts',(-126.798690839729,1.04845379900548,
136.627476209227));
#157160=CARTESIAN_POINT('Ctrl Pts',(-126.806088329066,1.20357838326837,
136.599545978902));
#157161=CARTESIAN_POINT('Ctrl Pts',(-126.813485818402,1.35755882644164,
136.565417744819));
#157162=CARTESIAN_POINT('Ctrl Pts',(-126.820883307739,1.50987004055252,
136.525219208996));
#157163=CARTESIAN_POINT('Ctrl Pts',(-126.828283390254,1.66223464712361,
136.485006581639));
#157164=CARTESIAN_POINT('Ctrl Pts',(-126.835683472769,1.81292849889796,
136.438719511039));
#157165=CARTESIAN_POINT('Ctrl Pts',(-126.843083555284,1.96144165141475,
136.386535570987));
#157166=CARTESIAN_POINT('Ctrl Pts',(-126.85049177495,2.11011810941004,136.334294249328));
#157167=CARTESIAN_POINT('Ctrl Pts',(-126.857899994617,2.25660872697291,
136.276143232643));
#157168=CARTESIAN_POINT('Ctrl Pts',(-126.865308214283,2.40042285146972,
136.212308536753));
#157169=CARTESIAN_POINT('Ctrl Pts',(-126.872720993585,2.54432549116049,
136.148434551674));
#157170=CARTESIAN_POINT('Ctrl Pts',(-126.880133772887,2.68554802116171,
136.078870081342));
#157171=CARTESIAN_POINT('Ctrl Pts',(-126.88754655219,2.82362485715162,136.003886867964));
#157172=CARTESIAN_POINT('Ctrl Pts',(-126.894969923218,2.96189898380015,
135.928796515054));
#157173=CARTESIAN_POINT('Ctrl Pts',(-126.902393294247,3.09701811966087,
135.848272146079));
#157174=CARTESIAN_POINT('Ctrl Pts',(-126.909816665276,3.2285454033614,135.762628978691));
#157175=CARTESIAN_POINT('Ctrl Pts',(-126.913752714717,3.29828432513476,
135.717218916361));
#157176=CARTESIAN_POINT('Ctrl Pts',(-126.917688764158,3.36701398780455,
135.670370460299));
#157177=CARTESIAN_POINT('Ctrl Pts',(-126.921624813598,3.43467319138462,
135.622135065471));
#157178=CARTESIAN_POINT('Ctrl Pts',(-126.929048080004,3.56227633776266,
135.531164616202));
#157179=CARTESIAN_POINT('Ctrl Pts',(-126.936471346409,3.68645578562979,
135.434983579145));
#157180=CARTESIAN_POINT('Ctrl Pts',(-126.943894612815,3.80675718974784,
135.333878280718));
#157181=CARTESIAN_POINT('Ctrl Pts',(-126.951309105536,3.92691640759664,
135.232892480357));
#157182=CARTESIAN_POINT('Ctrl Pts',(-126.958723598257,4.04320642224506,
135.126994241334));
#157183=CARTESIAN_POINT('Ctrl Pts',(-126.966138090978,4.15520182089066,
135.016513082775));
#157184=CARTESIAN_POINT('Ctrl Pts',(-126.973545437332,4.26708927415449,
134.906138410116));
#157185=CARTESIAN_POINT('Ctrl Pts',(-126.980952783685,4.37469008800407,
134.791189872077));
#157186=CARTESIAN_POINT('Ctrl Pts',(-126.988360130039,4.47761200857355,
134.672037085832));
#157187=CARTESIAN_POINT('Ctrl Pts',(-126.995761951715,4.58045716609164,
134.55297316823));
#157188=CARTESIAN_POINT('Ctrl Pts',(-127.00316377339,4.67863013581545,134.429711527284));
#157189=CARTESIAN_POINT('Ctrl Pts',(-127.010565595065,4.77177571008174,
134.302658365782));
#157190=CARTESIAN_POINT('Ctrl Pts',(-127.017963509377,4.86487211352442,
134.175672274655));
#157191=CARTESIAN_POINT('Ctrl Pts',(-127.025361423688,4.95294618676935,
134.044898949382));
#157192=CARTESIAN_POINT('Ctrl Pts',(-127.032759338,5.03568327513056,133.910777285541));
#157193=CARTESIAN_POINT('Ctrl Pts',(-127.040156022912,5.11840661408858,
133.776677910287));
#157194=CARTESIAN_POINT('Ctrl Pts',(-127.047552707824,5.19579453261965,
133.639231618218));
#157195=CARTESIAN_POINT('Ctrl Pts',(-127.054949392736,5.26757590444405,
133.498905969461));
#157196=CARTESIAN_POINT('Ctrl Pts',(-127.062345749671,5.33935409340721,
133.35858654289));
#157197=CARTESIAN_POINT('Ctrl Pts',(-127.069742106607,5.40552605996147,
133.215388345829));
#157198=CARTESIAN_POINT('Ctrl Pts',(-127.077138463542,5.46586695474059,
133.069802957502));
#157199=CARTESIAN_POINT('Ctrl Pts',(-127.084535952879,5.52621708786491,
132.92419527968));
#157200=CARTESIAN_POINT('Ctrl Pts',(-127.091933442216,5.58073422868631,
132.776200027735));
#157201=CARTESIAN_POINT('Ctrl Pts',(-127.099330931552,5.62924199365182,
132.626327999109));
#157202=CARTESIAN_POINT('Ctrl Pts',(-127.106731014067,5.67776676293907,
132.476403433076));
#157203=CARTESIAN_POINT('Ctrl Pts',(-127.114131096582,5.72027784731098,
132.324601135423));
#157204=CARTESIAN_POINT('Ctrl Pts',(-127.121531179097,5.75664900718979,
132.171446119837));
#157205=CARTESIAN_POINT('Ctrl Pts',(-127.128939398764,5.79306016089797,
132.018122694568));
#157206=CARTESIAN_POINT('Ctrl Pts',(-127.13634761843,5.82331782066315,131.863443944246));
#157207=CARTESIAN_POINT('Ctrl Pts',(-127.143755838097,5.84734693026466,
131.707944835901));
#157208=CARTESIAN_POINT('Ctrl Pts',(-127.151168617399,5.87139082938217,
131.55235002045));
#157209=CARTESIAN_POINT('Ctrl Pts',(-127.158581396701,5.88919849734115,
131.395934210909));
#157210=CARTESIAN_POINT('Ctrl Pts',(-127.165994176003,5.90074689885786,
131.239235999853));
#157211=CARTESIAN_POINT('Ctrl Pts',(-127.173417547032,5.91231180127221,
131.082313891045));
#157212=CARTESIAN_POINT('Ctrl Pts',(-127.18084091806,5.91759956248604,130.925108946925));
#157213=CARTESIAN_POINT('Ctrl Pts',(-127.188264289089,5.91663924979412,
130.768159094178));
#157214=CARTESIAN_POINT('Ctrl Pts',(-127.19220033853,5.91613006896249,130.684940516292));
#157215=CARTESIAN_POINT('Ctrl Pts',(-127.196136387971,5.91386519754827,
130.601793569727));
#157216=CARTESIAN_POINT('Ctrl Pts',(-127.200072437411,5.90985484598521,
130.51879755643));
#157217=CARTESIAN_POINT('Ctrl Pts',(-127.207495703817,5.90229144809595,
130.362269665567));
#157218=CARTESIAN_POINT('Ctrl Pts',(-127.214918970222,5.88849364245485,
130.20580577925));
#157219=CARTESIAN_POINT('Ctrl Pts',(-127.222342236628,5.86845673888837,
130.049942917419));
#157220=CARTESIAN_POINT('Ctrl Pts',(-127.229756729349,5.84844351727795,
129.894264272546));
#157221=CARTESIAN_POINT('Ctrl Pts',(-127.23717122207,5.82220592305286,129.739185604818));
#157222=CARTESIAN_POINT('Ctrl Pts',(-127.244585714791,5.78979124397579,
129.58524293921));
#157223=CARTESIAN_POINT('Ctrl Pts',(-127.251993061144,5.75740780738681,
129.431448649338));
#157224=CARTESIAN_POINT('Ctrl Pts',(-127.259400407498,5.71885921500412,
129.278788544648));
#157225=CARTESIAN_POINT('Ctrl Pts',(-127.266807753852,5.67424441342958,
129.127792426539));
#157226=CARTESIAN_POINT('Ctrl Pts',(-127.274209575527,5.62966288725728,
128.976908927031));
#157227=CARTESIAN_POINT('Ctrl Pts',(-127.281611397203,5.57902426592168,
128.827687299435));
#157228=CARTESIAN_POINT('Ctrl Pts',(-127.289013218878,5.52247830091577,
128.680645952548));
#157229=CARTESIAN_POINT('Ctrl Pts',(-127.29641113319,5.46596218608463,128.533682227642));
#157230=CARTESIAN_POINT('Ctrl Pts',(-127.303809047501,5.40354507175694,
128.388896838808));
#157231=CARTESIAN_POINT('Ctrl Pts',(-127.311206961812,5.33542613466919,
128.246791747723));
#157232=CARTESIAN_POINT('Ctrl Pts',(-127.318603646725,5.26731851771308,
128.104710271927));
#157233=CARTESIAN_POINT('Ctrl Pts',(-127.326000331637,5.19351111978584,
127.965308546152));
#157234=CARTESIAN_POINT('Ctrl Pts',(-127.333397016549,5.11425076208616,
127.829067404284));
#157235=CARTESIAN_POINT('Ctrl Pts',(-127.340793373484,5.03499391887379,
127.692832303491));
#157236=CARTESIAN_POINT('Ctrl Pts',(-127.34818973042,4.95028478436528,127.55975783062));
#157237=CARTESIAN_POINT('Ctrl Pts',(-127.355586087355,4.86041540150948,
127.430298868388));
#157238=CARTESIAN_POINT('Ctrl Pts',(-127.362983576692,4.77053225942149,
127.300820085657));
#157239=CARTESIAN_POINT('Ctrl Pts',(-127.370381066029,4.67548750878616,
127.174958222417));
#157240=CARTESIAN_POINT('Ctrl Pts',(-127.377778555365,4.57561555833868,
127.05313777364));
#157241=CARTESIAN_POINT('Ctrl Pts',(-127.38517863788,4.47570859793393,126.931274620894));
#157242=CARTESIAN_POINT('Ctrl Pts',(-127.392578720395,4.3709713051476,126.813455991777));
#157243=CARTESIAN_POINT('Ctrl Pts',(-127.39997880291,4.26177715328981,126.700071877943));
#157244=CARTESIAN_POINT('Ctrl Pts',(-127.407387022576,4.15246293123678,
126.58656308662));
#157245=CARTESIAN_POINT('Ctrl Pts',(-127.414795242243,4.03868232204893,
126.477498817731));
#157246=CARTESIAN_POINT('Ctrl Pts',(-127.422203461909,3.92084483891866,
126.373231380946));
#157247=CARTESIAN_POINT('Ctrl Pts',(-127.429616241211,3.80293482878374,
126.268899769295));
#157248=CARTESIAN_POINT('Ctrl Pts',(-127.437029020513,3.68096325779922,
126.169371108176));
#157249=CARTESIAN_POINT('Ctrl Pts',(-127.444441799816,3.55537080801979,
126.07495590027));
#157250=CARTESIAN_POINT('Ctrl Pts',(-127.451865170844,3.42959890585823,
125.980405787488));
#157251=CARTESIAN_POINT('Ctrl Pts',(-127.459288541873,3.30019609819134,
125.89098393198));
#157252=CARTESIAN_POINT('Ctrl Pts',(-127.466711912902,3.16763066955715,
125.806956641122));
#157253=CARTESIAN_POINT('Ctrl Pts',(-127.470647962343,3.09734129843189,
125.762403355302));
#157254=CARTESIAN_POINT('Ctrl Pts',(-127.474584011783,3.02616319912008,
125.719365900171));
#157255=CARTESIAN_POINT('Ctrl Pts',(-127.478520061224,2.95416860958555,
125.677878550043));
#157256=CARTESIAN_POINT('Ctrl Pts',(-127.485943327629,2.8183890605967,125.599634702476));
#157257=CARTESIAN_POINT('Ctrl Pts',(-127.493366594035,2.67929351077128,
125.526670634738));
#157258=CARTESIAN_POINT('Ctrl Pts',(-127.50078986044,2.53733123504071,125.459280565201));
#157259=CARTESIAN_POINT('Ctrl Pts',(-127.508204353161,2.39553674693082,
125.39197014513));
#157260=CARTESIAN_POINT('Ctrl Pts',(-127.515618845882,2.25088261114735,
125.330220768325));
#157261=CARTESIAN_POINT('Ctrl Pts',(-127.523033338603,2.10384536087433,
125.274282384844));
#157262=CARTESIAN_POINT('Ctrl Pts',(-127.530440684957,1.95694983063899,
125.218397916883));
#157263=CARTESIAN_POINT('Ctrl Pts',(-127.537848031311,1.80767610522029,
125.168313423892));
#157264=CARTESIAN_POINT('Ctrl Pts',(-127.545255377665,1.65652340459452,
125.12423202989));
#157265=CARTESIAN_POINT('Ctrl Pts',(-127.55265719934,1.50548343935553,125.080183513455));
#157266=CARTESIAN_POINT('Ctrl Pts',(-127.560059021015,1.35256764613377,
125.042129285089));
#157267=CARTESIAN_POINT('Ctrl Pts',(-127.567460842691,1.19829312127212,
125.010223567236));
#157268=CARTESIAN_POINT('Ctrl Pts',(-127.574858757002,1.04410003673127,
124.978334692163));
#157269=CARTESIAN_POINT('Ctrl Pts',(-127.582256671313,0.888550013652561,
124.952587938946));
#157270=CARTESIAN_POINT('Ctrl Pts',(-127.589654585625,0.732173026504409,
124.933087057106));
#157271=CARTESIAN_POINT('Ctrl Pts',(-127.597051270537,0.575822026374777,
124.913589415958));
#157272=CARTESIAN_POINT('Ctrl Pts',(-127.604447955449,0.418644704992514,
124.90033563231));
#157273=CARTESIAN_POINT('Ctrl Pts',(-127.611844640361,0.26117901441101,
124.893377950959));
#157274=CARTESIAN_POINT('Ctrl Pts',(-127.619240997297,0.103720306023239,
124.886420578118));
#157275=CARTESIAN_POINT('Ctrl Pts',(-127.626637354232,-0.0540263732060113,
124.885758768956));
#157276=CARTESIAN_POINT('Ctrl Pts',(-127.634033711168,-0.211520461215678,
124.891392694688));
#157277=CARTESIAN_POINT('Ctrl Pts',(-127.641431200504,-0.369038661972731,
124.897027482988));
#157278=CARTESIAN_POINT('Ctrl Pts',(-127.648828689841,-0.526303821425139,
124.908959912077));
#157279=CARTESIAN_POINT('Ctrl Pts',(-127.656226179177,-0.682778043840405,
124.927138084315));
#157280=CARTESIAN_POINT('Ctrl Pts',(-127.663626261692,-0.839307118051996,
124.945322628884));
#157281=CARTESIAN_POINT('Ctrl Pts',(-127.671026344207,-0.995044332627594,
124.969757232701));
#157282=CARTESIAN_POINT('Ctrl Pts',(-127.678426426722,-1.14945970509599,
125.00033848211));
#157283=CARTESIAN_POINT('Ctrl Pts',(-127.685834646389,-1.30404487314005,
125.030953358747));
#157284=CARTESIAN_POINT('Ctrl Pts',(-127.693242866055,-1.45730492992901,
125.067728306313));
#157285=CARTESIAN_POINT('Ctrl Pts',(-127.700651085722,-1.6087221154754,
125.110509221746));
#157286=CARTESIAN_POINT('Ctrl Pts',(-127.708063865024,-1.76023249577339,
125.153316468119));
#157287=CARTESIAN_POINT('Ctrl Pts',(-127.715476644326,-1.90989739060958,
125.202136932745));
#157288=CARTESIAN_POINT('Ctrl Pts',(-127.722889423628,-2.05721736587058,
125.256767691615));
#157289=CARTESIAN_POINT('Ctrl Pts',(-127.730312794657,-2.20474783882064,
125.311476509475));
#157290=CARTESIAN_POINT('Ctrl Pts',(-127.737736165686,-2.34992635680104,
125.372012059291));
#157291=CARTESIAN_POINT('Ctrl Pts',(-127.745159536714,-2.49227574864398,
125.43812430566));
#157292=CARTESIAN_POINT('Ctrl Pts',(-127.749095586155,-2.56775281182466,
125.473178605025));
#157293=CARTESIAN_POINT('Ctrl Pts',(-127.753031635596,-2.64243494300916,
125.509799960098));
#157294=CARTESIAN_POINT('Ctrl Pts',(-127.756967685036,-2.71625425986335,
125.547946121137));
#157295=CARTESIAN_POINT('Ctrl Pts',(-127.764390951442,-2.85547518763159,
125.619888590356));
#157296=CARTESIAN_POINT('Ctrl Pts',(-127.771814217847,-2.99204646654796,
125.697474754956));
#157297=CARTESIAN_POINT('Ctrl Pts',(-127.779237484253,-3.1254777182897,
125.780485659431));
#157298=CARTESIAN_POINT('Ctrl Pts',(-127.786651976974,-3.25875126537266,
125.86339845191));
#157299=CARTESIAN_POINT('Ctrl Pts',(-127.794066469695,-3.38889185867762,
125.951723026688));
#157300=CARTESIAN_POINT('Ctrl Pts',(-127.801480962416,-3.51543163031537,
126.045193567012));
#157301=CARTESIAN_POINT('Ctrl Pts',(-127.80888830877,-3.64184943815671,
126.13857401691));
#157302=CARTESIAN_POINT('Ctrl Pts',(-127.816295655124,-3.76467303537882,
126.237090337914));
#157303=CARTESIAN_POINT('Ctrl Pts',(-127.823703001478,-3.88346168740095,
126.340432315612));
#157304=CARTESIAN_POINT('Ctrl Pts',(-127.831104823153,-4.00216174236476,
126.443697216964));
#157305=CARTESIAN_POINT('Ctrl Pts',(-127.838506644829,-4.11683256385394,
126.551780364644));
#157306=CARTESIAN_POINT('Ctrl Pts',(-127.845908466504,-4.22706489695321,
126.664330071852));
#157307=CARTESIAN_POINT('Ctrl Pts',(-127.853306380816,-4.33723903926251,
126.776820364946));
#157308=CARTESIAN_POINT('Ctrl Pts',(-127.860704295127,-4.44297909892476,
126.893772255756));
#157309=CARTESIAN_POINT('Ctrl Pts',(-127.868102209438,-4.54391132438536,
127.014795940902));
#157310=CARTESIAN_POINT('Ctrl Pts',(-127.875498894351,-4.64482677674047,
127.135799514105));
#157311=CARTESIAN_POINT('Ctrl Pts',(-127.882895579263,-4.74093574176654,
127.260873252274));
#157312=CARTESIAN_POINT('Ctrl Pts',(-127.890292264175,-4.83190348821213,
127.3895928007));
#157313=CARTESIAN_POINT('Ctrl Pts',(-127.897688621111,-4.92286720105278,
127.518306641566));
#157314=CARTESIAN_POINT('Ctrl Pts',(-127.905084978046,-5.00868993314501,
127.650665666403));
#157315=CARTESIAN_POINT('Ctrl Pts',(-127.912481334982,-5.08907935344174,
127.786215177586));
#157316=CARTESIAN_POINT('Ctrl Pts',(-127.919878824318,-5.16948108156372,
127.921785441744));
#157317=CARTESIAN_POINT('Ctrl Pts',(-127.927276313655,-5.24444765112627,
128.060546843761));
#157318=CARTESIAN_POINT('Ctrl Pts',(-127.934673802992,-5.31373197930008,
128.202018784781));
#157319=CARTESIAN_POINT('Ctrl Pts',(-127.942073885507,-5.38304059498783,
128.343540318571));
#157320=CARTESIAN_POINT('Ctrl Pts',(-127.949473968022,-5.44666283934295,
128.487773948112));
#157321=CARTESIAN_POINT('Ctrl Pts',(-127.956874050537,-5.50439924873311,
128.634217886535));
#157322=CARTESIAN_POINT('Ctrl Pts',(-127.964282270203,-5.56219914524093,
128.780822855123));
#157323=CARTESIAN_POINT('Ctrl Pts',(-127.97169048987,-5.6141001446118,128.929642638889));
#157324=CARTESIAN_POINT('Ctrl Pts',(-127.979098709536,-5.65995203619768,
129.080158335222));
#157325=CARTESIAN_POINT('Ctrl Pts',(-127.986511488838,-5.70583214885774,
129.230766671454));
#157326=CARTESIAN_POINT('Ctrl Pts',(-127.99392426814,-5.74565564072694,
129.383072639847));
#157327=CARTESIAN_POINT('Ctrl Pts',(-128.001337047443,-5.77932328118467,
129.536546366953));
#157328=CARTESIAN_POINT('Ctrl Pts',(-128.008760418471,-5.81303902754589,
129.690239384518));
#157329=CARTESIAN_POINT('Ctrl Pts',(-128.0161837895,-5.84058129018013,129.845103126703));
#157330=CARTESIAN_POINT('Ctrl Pts',(-128.023607160529,-5.86190250828191,
130.00060098565));
#157331=CARTESIAN_POINT('Ctrl Pts',(-128.027543209969,-5.87320752971389,
130.083049681574));
#157332=CARTESIAN_POINT('Ctrl Pts',(-128.03147925941,-5.88276446263719,
130.165676610584));
#157333=CARTESIAN_POINT('Ctrl Pts',(-128.03541530885,-5.89057216089617,
130.248401824331));
#157334=CARTESIAN_POINT('Ctrl Pts',(-128.044151808496,-5.90790221584405,
130.432019640013));
#157335=CARTESIAN_POINT('Ctrl Pts',(-128.052888308143,-5.9166486189631,
130.6164602422));
#157336=CARTESIAN_POINT('Ctrl Pts',(-128.06162480779,-5.91674912383553,
130.801140665471));
#157337=CARTESIAN_POINT('',(-129.811623618163,-5.91251901558631,130.800694970794));
#157338=CARTESIAN_POINT('Ctrl Pts',(-128.061627320749,-5.92436185088451,
130.801189712243));
#157339=CARTESIAN_POINT('Ctrl Pts',(-128.145705858053,-5.91267799511827,
132.58081561286));
#157340=CARTESIAN_POINT('Ctrl Pts',(-128.322600269963,-4.11167625071623,
136.345452640801));
#157341=CARTESIAN_POINT('Ctrl Pts',(-128.592310556475,2.29803694488353,
137.414699998437));
#157342=CARTESIAN_POINT('Ctrl Pts',(-128.870758180289,6.80361083705033,
132.444006953921));
#157343=CARTESIAN_POINT('Ctrl Pts',(-129.149205804101,5.05699874483257,
125.966559027475));
#157344=CARTESIAN_POINT('Ctrl Pts',(-129.427653427914,-1.33674814576103,
123.934814422572));
#157345=CARTESIAN_POINT('Ctrl Pts',(-129.648459058428,-5.43280141090012,
127.329622118098));
#157346=CARTESIAN_POINT('Ctrl Pts',(-129.776448814336,-5.91342334095441,
130.051290695285));
#157347=CARTESIAN_POINT('Ctrl Pts',(-129.811622695641,-5.90923887852463,
130.80067733591));
#157348=CARTESIAN_POINT('',(-131.561626024561,-5.91341910262869,130.808953665459));
#157349=CARTESIAN_POINT('Ctrl Pts',(-129.81162480779,-5.91674887854272,
130.800717711655));
#157350=CARTESIAN_POINT('Ctrl Pts',(-129.819083418388,-5.9168468407104,
130.959826280473));
#157351=CARTESIAN_POINT('Ctrl Pts',(-129.826542028985,-5.91052253319917,
131.118956455526));
#157352=CARTESIAN_POINT('Ctrl Pts',(-129.834000639583,-5.89779739881852,
131.277558678624));
#157353=CARTESIAN_POINT('Ctrl Pts',(-129.841460024799,-5.88507094286057,
131.436177373463));
#157354=CARTESIAN_POINT('Ctrl Pts',(-129.848919410016,-5.86594236406024,
131.594267643675));
#157355=CARTESIAN_POINT('Ctrl Pts',(-129.856378795233,-5.84048505975837,
131.751284494781));
#157356=CARTESIAN_POINT('Ctrl Pts',(-129.863840334521,-5.81502040406574,
131.908346688166));
#157357=CARTESIAN_POINT('Ctrl Pts',(-129.871301873809,-5.78322344019467,
132.06433448515));
#157358=CARTESIAN_POINT('Ctrl Pts',(-129.878763413097,-5.74521880623851,
132.218712564906));
#157359=CARTESIAN_POINT('Ctrl Pts',(-129.886228486933,-5.70719616940552,
132.37316377389));
#157360=CARTESIAN_POINT('Ctrl Pts',(-129.893693560768,-5.66296009141423,
132.52600339301));
#157361=CARTESIAN_POINT('Ctrl Pts',(-129.901158634603,-5.61268522274912,
132.676710785893));
#157362=CARTESIAN_POINT('Ctrl Pts',(-129.908633373557,-5.56234526262317,
132.827613301401));
#157363=CARTESIAN_POINT('Ctrl Pts',(-129.916108112511,-5.50595100864783,
132.976377729922));
#157364=CARTESIAN_POINT('Ctrl Pts',(-129.923582851465,-5.44372583382088,
133.12250203014));
#157365=CARTESIAN_POINT('Ctrl Pts',(-129.931062809614,-5.38145721060622,
133.268728360851));
#157366=CARTESIAN_POINT('Ctrl Pts',(-129.938542767764,-5.31334970658557,
133.412310560036));
#157367=CARTESIAN_POINT('Ctrl Pts',(-129.946022725913,-5.23967275794865,
133.55277105855));
#157368=CARTESIAN_POINT('Ctrl Pts',(-129.953514870734,-5.16587577163415,
133.693460401395));
#157369=CARTESIAN_POINT('Ctrl Pts',(-129.961007015556,-5.08649139201798,
133.831017566116));
#157370=CARTESIAN_POINT('Ctrl Pts',(-129.968499160377,-5.00183310721932,
133.964992853373));
#157371=CARTESIAN_POINT('Ctrl Pts',(-129.973848998765,-4.94138204111693,
134.060659201508));
#157372=CARTESIAN_POINT('Ctrl Pts',(-129.979198837152,-4.878242813534,134.154499841785));
#157373=CARTESIAN_POINT('Ctrl Pts',(-129.98454867554,-4.81254188109021,
134.246361664232));
#157374=CARTESIAN_POINT('Ctrl Pts',(-129.991971941945,-4.7213773468976,
134.373826221309));
#157375=CARTESIAN_POINT('Ctrl Pts',(-129.999395208351,-4.62500744123637,
134.497859154213));
#157376=CARTESIAN_POINT('Ctrl Pts',(-130.006818474756,-4.52371918163029,
134.61800655397));
#157377=CARTESIAN_POINT('Ctrl Pts',(-130.014232967477,-4.4225506363356,
134.738011949478));
#157378=CARTESIAN_POINT('Ctrl Pts',(-130.021647460198,-4.31647554633551,
134.854140670372));
#157379=CARTESIAN_POINT('Ctrl Pts',(-130.029061952919,-4.20582407778094,
134.965967805812));
#157380=CARTESIAN_POINT('Ctrl Pts',(-130.036469299273,-4.0952792592774,
135.077687158049));
#157381=CARTESIAN_POINT('Ctrl Pts',(-130.043876645626,-3.98016710422518,
135.185112915191));
#157382=CARTESIAN_POINT('Ctrl Pts',(-130.05128399198,-3.8608578263152,135.287853386321));
#157383=CARTESIAN_POINT('Ctrl Pts',(-130.058685813656,-3.7416375337663,
135.390517229732));
#157384=CARTESIAN_POINT('Ctrl Pts',(-130.066087635331,-3.61822663300769,
135.488502502538));
#157385=CARTESIAN_POINT('Ctrl Pts',(-130.073489457006,-3.49103186692444,
135.581454615659));
#157386=CARTESIAN_POINT('Ctrl Pts',(-130.080887371318,-3.36390424596741,
135.674357660084));
#157387=CARTESIAN_POINT('Ctrl Pts',(-130.088285285629,-3.23299703838111,
135.762232616602));
#157388=CARTESIAN_POINT('Ctrl Pts',(-130.09568319994,-3.09874961808637,
135.844765498814));
#157389=CARTESIAN_POINT('Ctrl Pts',(-130.103079884852,-2.96452450727796,
135.927284665559));
#157390=CARTESIAN_POINT('Ctrl Pts',(-130.110476569765,-2.82696060313257,
136.004463324617));
#157391=CARTESIAN_POINT('Ctrl Pts',(-130.117873254677,-2.68652587784223,
136.07603106157));
#157392=CARTESIAN_POINT('Ctrl Pts',(-130.125269611612,-2.54609737957438,
136.147595625135));
#157393=CARTESIAN_POINT('Ctrl Pts',(-130.132665968548,-2.40279864586589,
136.213549591784));
#157394=CARTESIAN_POINT('Ctrl Pts',(-130.140062325483,-2.25712159755419,
136.273668860512));
#157395=CARTESIAN_POINT('Ctrl Pts',(-130.14745981482,-2.11142224571491,
136.333797333653));
#157396=CARTESIAN_POINT('Ctrl Pts',(-130.154857304156,-1.96334419933927,
136.388089187764));
#157397=CARTESIAN_POINT('Ctrl Pts',(-130.162254793493,-1.8133985237029,
136.436368816844));
#157398=CARTESIAN_POINT('Ctrl Pts',(-130.169654876008,-1.66340028484216,
136.484665370273));
#157399=CARTESIAN_POINT('Ctrl Pts',(-130.177054958522,-1.51153346834006,
136.526945388162));
#157400=CARTESIAN_POINT('Ctrl Pts',(-130.184455041037,-1.35832327939251,
136.563083430062));
#157401=CARTESIAN_POINT('Ctrl Pts',(-130.191863260704,-1.20494462009204,
136.599261209454));
#157402=CARTESIAN_POINT('Ctrl Pts',(-130.19927148037,-1.05022000187908,
136.629283439454));
#157403=CARTESIAN_POINT('Ctrl Pts',(-130.206679700037,-0.894684505386521,
136.653075878059));
#157404=CARTESIAN_POINT('Ctrl Pts',(-130.214092479339,-0.739053279390232,
136.676882960512));
#157405=CARTESIAN_POINT('Ctrl Pts',(-130.221505258641,-0.582610550736434,
136.694452569615));
#157406=CARTESIAN_POINT('Ctrl Pts',(-130.228918037943,-0.425894946433585,
136.705762489757));
#157407=CARTESIAN_POINT('Ctrl Pts',(-130.236341408972,-0.268955419526746,
136.717088570043));
#157408=CARTESIAN_POINT('Ctrl Pts',(-130.24376478,-0.111742610375219,136.722137085971));
#157409=CARTESIAN_POINT('Ctrl Pts',(-130.251188151029,0.0452055991941102,
136.720937923433));
#157410=CARTESIAN_POINT('Ctrl Pts',(-130.25512420047,0.128423305833506,
136.720302098682));
#157411=CARTESIAN_POINT('Ctrl Pts',(-130.259060249911,0.211566709373327,
136.717910694392));
#157412=CARTESIAN_POINT('Ctrl Pts',(-130.262996299352,0.294556523495727,
136.713774041669));
#157413=CARTESIAN_POINT('Ctrl Pts',(-130.270419565758,0.451072722897707,
136.705972443734));
#157414=CARTESIAN_POINT('Ctrl Pts',(-130.277842832163,0.607515430120606,
136.69193654267));
#157415=CARTESIAN_POINT('Ctrl Pts',(-130.285266098569,0.763347618708535,
136.671662465563));
#157416=CARTESIAN_POINT('Ctrl Pts',(-130.29268059129,0.91899562659061,136.651412350732));
#157417=CARTESIAN_POINT('Ctrl Pts',(-130.30009508401,1.07403418558803,136.624938783556));
#157418=CARTESIAN_POINT('Ctrl Pts',(-130.307509576731,1.22792734330951,
136.592289867484));
#157419=CARTESIAN_POINT('Ctrl Pts',(-130.314916923085,1.38167217301248,
136.559672419666));
#157420=CARTESIAN_POINT('Ctrl Pts',(-130.322324269439,1.53427343652915,
136.520891549229));
#157421=CARTESIAN_POINT('Ctrl Pts',(-130.329731615793,1.68520148365469,
136.47604700893));
#157422=CARTESIAN_POINT('Ctrl Pts',(-130.337133437468,1.83601696294807,
136.431235915382));
#157423=CARTESIAN_POINT('Ctrl Pts',(-130.344535259144,1.9851613543867,136.38037026277));
#157424=CARTESIAN_POINT('Ctrl Pts',(-130.351937080819,2.13211647767011,
136.323600591344));
#157425=CARTESIAN_POINT('Ctrl Pts',(-130.35933499513,2.27899402448742,136.266860888186));
#157426=CARTESIAN_POINT('Ctrl Pts',(-130.366732909442,2.42368425743984,
136.204223507422));
#157427=CARTESIAN_POINT('Ctrl Pts',(-130.374130823753,2.5656855185423,136.135888389457));
#157428=CARTESIAN_POINT('Ctrl Pts',(-130.381527508665,2.70766318161153,
136.067564627549));
#157429=CARTESIAN_POINT('Ctrl Pts',(-130.388924193578,2.84695242366649,
135.993545169393));
#157430=CARTESIAN_POINT('Ctrl Pts',(-130.39632087849,2.9830727869974,135.91407756765));
#157431=CARTESIAN_POINT('Ctrl Pts',(-130.403717235425,3.11918711460876,
135.834613489584));
#157432=CARTESIAN_POINT('Ctrl Pts',(-130.411113592361,3.25213252049968,
135.749701936473));
#157433=CARTESIAN_POINT('Ctrl Pts',(-130.418509949296,3.38145456691855,
135.659635643182));
#157434=CARTESIAN_POINT('Ctrl Pts',(-130.425907438633,3.51079641287212,
135.569555560511));
#157435=CARTESIAN_POINT('Ctrl Pts',(-130.433304927969,3.63651348843412,
135.474319379607));
#157436=CARTESIAN_POINT('Ctrl Pts',(-130.440702417306,3.75818180803671,
135.374262154825));
#157437=CARTESIAN_POINT('Ctrl Pts',(-130.448102499821,3.87989277828064,
135.274169855138));
#157438=CARTESIAN_POINT('Ctrl Pts',(-130.455502582336,3.99755187863581,
135.169253383738));
#157439=CARTESIAN_POINT('Ctrl Pts',(-130.462902664851,4.11076968626162,
135.059886807006));
#157440=CARTESIAN_POINT('Ctrl Pts',(-130.470310884517,4.22411198850615,
134.95039997048));
#157441=CARTESIAN_POINT('Ctrl Pts',(-130.477719104184,4.33300297638259,
134.836453515797));
#157442=CARTESIAN_POINT('Ctrl Pts',(-130.48512732385,4.43709096383735,134.718457491831));
#157443=CARTESIAN_POINT('Ctrl Pts',(-130.492540103152,4.54124301571189,
134.600388843281));
#157444=CARTESIAN_POINT('Ctrl Pts',(-130.499952882454,4.64058594161079,
134.478265947858));
#157445=CARTESIAN_POINT('Ctrl Pts',(-130.507365661756,4.73480990985672,
134.352529959638));
#157446=CARTESIAN_POINT('Ctrl Pts',(-130.514789032785,4.82916850972674,
134.226614313943));
#157447=CARTESIAN_POINT('Ctrl Pts',(-130.522212403814,4.91839333264034,
134.097075571281));
#157448=CARTESIAN_POINT('Ctrl Pts',(-130.529635774843,5.00221878418057,
133.964382420923));
#157449=CARTESIAN_POINT('Ctrl Pts',(-130.533571824284,5.04666504995262,
133.894025328673));
#157450=CARTESIAN_POINT('Ctrl Pts',(-130.537507873725,5.08959413429763,
133.822781816101));
#157451=CARTESIAN_POINT('Ctrl Pts',(-130.541443923165,5.13097187287621,
133.750724173248));
#157452=CARTESIAN_POINT('Ctrl Pts',(-130.548867189571,5.20900899647822,
133.614825707674));
#157453=CARTESIAN_POINT('Ctrl Pts',(-130.556290455976,5.28176129997569,
133.475619280029));
#157454=CARTESIAN_POINT('Ctrl Pts',(-130.563713722382,5.34893524905838,
133.333554612474));
#157455=CARTESIAN_POINT('Ctrl Pts',(-130.571128215103,5.4160298041117,133.191657853559));
#157456=CARTESIAN_POINT('Ctrl Pts',(-130.578542707824,5.47755897044204,
133.046909913244));
#157457=CARTESIAN_POINT('Ctrl Pts',(-130.585957200545,5.53327352348262,
132.89978770454));
#157458=CARTESIAN_POINT('Ctrl Pts',(-130.593364546899,5.58893437673969,
132.75280729776));
#157459=CARTESIAN_POINT('Ctrl Pts',(-130.600771893252,5.63879164253432,
132.603457525125));
#157460=CARTESIAN_POINT('Ctrl Pts',(-130.608179239606,5.68264295681117,
132.452237915154));
#157461=CARTESIAN_POINT('Ctrl Pts',(-130.615581061281,5.72646156512317,
132.301131090473));
#157462=CARTESIAN_POINT('Ctrl Pts',(-130.622982882957,5.76428303761727,
132.148157562268));
#157463=CARTESIAN_POINT('Ctrl Pts',(-130.630384704632,5.79595393895926,
131.993834660983));
#157464=CARTESIAN_POINT('Ctrl Pts',(-130.637782618944,5.82760812147905,
131.839593225556));
#157465=CARTESIAN_POINT('Ctrl Pts',(-130.645180533255,5.85311812422539,
131.684004200426));
#157466=CARTESIAN_POINT('Ctrl Pts',(-130.652578447566,5.87238100432991,
131.527597717337));
#157467=CARTESIAN_POINT('Ctrl Pts',(-130.659975132479,5.8916406832932,131.371217226169));
#157468=CARTESIAN_POINT('Ctrl Pts',(-130.667371817391,5.90465525446638,
131.214019916792));
#157469=CARTESIAN_POINT('Ctrl Pts',(-130.674768502303,5.91137329178559,
131.056543820147));
#157470=CARTESIAN_POINT('Ctrl Pts',(-130.682164859238,5.91809103121999,
130.899074706157));
#157471=CARTESIAN_POINT('Ctrl Pts',(-130.689561216174,5.91851277602355,
130.741327202434));
#157472=CARTESIAN_POINT('Ctrl Pts',(-130.696957573109,5.91263917762366,
130.583841870676));
#157473=CARTESIAN_POINT('Ctrl Pts',(-130.704355062446,5.90676467996086,
130.426332427512));
#157474=CARTESIAN_POINT('Ctrl Pts',(-130.711752551782,5.89459293388846,
130.269085609296));
#157475=CARTESIAN_POINT('Ctrl Pts',(-130.719150041119,5.87617665557045,
130.112639232159));
#157476=CARTESIAN_POINT('Ctrl Pts',(-130.726550123634,5.85775392145465,
129.956138012988));
#157477=CARTESIAN_POINT('Ctrl Pts',(-130.733950206149,5.83308234040288,
129.800438164062));
#157478=CARTESIAN_POINT('Ctrl Pts',(-130.741350288664,5.80226613249603,
129.646069509861));
#157479=CARTESIAN_POINT('Ctrl Pts',(-130.74875850833,5.77141603900056,129.491531111454));
#157480=CARTESIAN_POINT('Ctrl Pts',(-130.756166727997,5.73440789830192,
129.338327197348));
#157481=CARTESIAN_POINT('Ctrl Pts',(-130.763574947663,5.69139660122823,
129.186975292411));
#157482=CARTESIAN_POINT('Ctrl Pts',(-130.770987726965,5.64835883141875,
129.035530232901));
#157483=CARTESIAN_POINT('Ctrl Pts',(-130.778400506268,5.59931065883326,
128.885939807811));
#157484=CARTESIAN_POINT('Ctrl Pts',(-130.78581328557,5.54445576730088,128.738703141859));
#157485=CARTESIAN_POINT('Ctrl Pts',(-130.793236656598,5.48952249652728,
128.591256097255));
#157486=CARTESIAN_POINT('Ctrl Pts',(-130.800660027627,5.42876607982015,
128.446169872191));
#157487=CARTESIAN_POINT('Ctrl Pts',(-130.808083398656,5.36243727846669,
128.303921256771));
#157488=CARTESIAN_POINT('Ctrl Pts',(-130.812019448097,5.32726815645068,
128.228497627666));
#157489=CARTESIAN_POINT('Ctrl Pts',(-130.815955497538,5.29053319029321,
128.153871314428));
#157490=CARTESIAN_POINT('Ctrl Pts',(-130.819891546978,5.25227473299223,
128.080110135016));
#157491=CARTESIAN_POINT('Ctrl Pts',(-130.827314813384,5.18012047652921,
127.940998852656));
#157492=CARTESIAN_POINT('Ctrl Pts',(-130.834738079789,5.10232656353443,
127.804545804823));
#157493=CARTESIAN_POINT('Ctrl Pts',(-130.842161346195,5.01911269553447,
127.671241036059));
#157494=CARTESIAN_POINT('Ctrl Pts',(-130.849575838916,4.93599717941601,
127.538093822461));
#157495=CARTESIAN_POINT('Ctrl Pts',(-130.856990331637,4.8474746550883,127.408087794825));
#157496=CARTESIAN_POINT('Ctrl Pts',(-130.864404824358,4.75381165101063,
127.28169041597));
#157497=CARTESIAN_POINT('Ctrl Pts',(-130.871812170712,4.66023892286264,
127.155414863667));
#157498=CARTESIAN_POINT('Ctrl Pts',(-130.879219517065,4.56153579933309,
127.032741333743));
#157499=CARTESIAN_POINT('Ctrl Pts',(-130.886626863419,4.45801316519695,
126.914110088175));
#157500=CARTESIAN_POINT('Ctrl Pts',(-130.894028685094,4.35456774214733,
126.795567322265));
#157501=CARTESIAN_POINT('Ctrl Pts',(-130.90143050677,4.24631021015695,126.681061117715));
#157502=CARTESIAN_POINT('Ctrl Pts',(-130.908832328445,4.13359287843425,
126.571000193759));
#157503=CARTESIAN_POINT('Ctrl Pts',(-130.916230242757,4.02093504931325,
126.460997370107));
#157504=CARTESIAN_POINT('Ctrl Pts',(-130.923628157068,3.90382237556222,
126.35543541376));
#157505=CARTESIAN_POINT('Ctrl Pts',(-130.931026071379,3.78264522889645,
126.254687482625));
#157506=CARTESIAN_POINT('Ctrl Pts',(-130.938422756292,3.6614882196739,126.153956293968));
#157507=CARTESIAN_POINT('Ctrl Pts',(-130.945819441204,3.53626836485406,
126.058037781172));
#157508=CARTESIAN_POINT('Ctrl Pts',(-130.953216126116,3.40741052805931,
125.967266029306));
#157509=CARTESIAN_POINT('Ctrl Pts',(-130.960612483051,3.27855840495609,
125.876498302355));
#157510=CARTESIAN_POINT('Ctrl Pts',(-130.968008839987,3.14606892580091,
125.790877097548));
#157511=CARTESIAN_POINT('Ctrl Pts',(-130.975405196922,3.01039723257024,
125.710694053623));
#157512=CARTESIAN_POINT('Ctrl Pts',(-130.982802686259,2.87470476765698,
125.630498733468));
#157513=CARTESIAN_POINT('Ctrl Pts',(-130.990200175596,2.73582943996688,
125.555743421948));
#157514=CARTESIAN_POINT('Ctrl Pts',(-130.997597664932,2.59425222381635,
125.486674470215));
#157515=CARTESIAN_POINT('Ctrl Pts',(-131.004997747447,2.45262537799198,
125.417581306469));
#157516=CARTESIAN_POINT('Ctrl Pts',(-131.012397829962,2.30829509324542,
125.354178634818));
#157517=CARTESIAN_POINT('Ctrl Pts',(-131.019797912477,2.16176345941615,
125.296665155031));
#157518=CARTESIAN_POINT('Ctrl Pts',(-131.027206132144,2.01507069899187,
125.23908843326));
#157519=CARTESIAN_POINT('Ctrl Pts',(-131.03461435181,1.86617210307173,125.187413972366));
#157520=CARTESIAN_POINT('Ctrl Pts',(-131.042022571477,1.71558680226133,
125.141791193143));
#157521=CARTESIAN_POINT('Ctrl Pts',(-131.049435350779,1.56490881871051,
125.096140333861));
#157522=CARTESIAN_POINT('Ctrl Pts',(-131.056848130081,1.41254242210993,
125.056548671863));
#157523=CARTESIAN_POINT('Ctrl Pts',(-131.064260909383,1.25901763630676,
125.023114631278));
#157524=CARTESIAN_POINT('Ctrl Pts',(-131.071684280412,1.10527348709026,
124.989632818568));
#157525=CARTESIAN_POINT('Ctrl Pts',(-131.079107651441,0.950368009599541,
124.96232626408));
#157526=CARTESIAN_POINT('Ctrl Pts',(-131.086531022469,0.794837883453356,
124.941241711938));
#157527=CARTESIAN_POINT('Ctrl Pts',(-131.09046707191,0.712372078679832,
124.930062176476));
#157528=CARTESIAN_POINT('Ctrl Pts',(-131.094403121351,0.629730701320683,
124.920630998739));
#157529=CARTESIAN_POINT('Ctrl Pts',(-131.098339170791,0.546993701375111,
124.912949203214));
#157530=CARTESIAN_POINT('Ctrl Pts',(-131.105762437197,0.390954301605477,
124.898461576593));
#157531=CARTESIAN_POINT('Ctrl Pts',(-131.113185703602,0.234102977717035,
124.890155593429));
#157532=CARTESIAN_POINT('Ctrl Pts',(-131.120608970008,0.0769707721032721,
124.88811129365));
#157533=CARTESIAN_POINT('Ctrl Pts',(-131.128023462729,-0.0799757162929195,
124.886069410063));
#157534=CARTESIAN_POINT('Ctrl Pts',(-131.13543795545,-0.237202055987336,
124.890274483356));
#157535=CARTESIAN_POINT('Ctrl Pts',(-131.142852448171,-0.394170892128082,
124.900754950662));
#157536=CARTESIAN_POINT('Ctrl Pts',(-131.150259794524,-0.55098843579523,
124.911225316499));
#157537=CARTESIAN_POINT('Ctrl Pts',(-131.157667140878,-0.707548600041204,
124.927959010351));
#157538=CARTESIAN_POINT('Ctrl Pts',(-131.165074487232,-0.863312939181342,
124.950932448404));
#157539=CARTESIAN_POINT('Ctrl Pts',(-131.172476308907,-1.01896110339981,
124.973888752));
#157540=CARTESIAN_POINT('Ctrl Pts',(-131.179878130583,-1.17381425664995,
125.003075479147));
#157541=CARTESIAN_POINT('Ctrl Pts',(-131.187279952258,-1.32733810013195,
125.03841714486));
#157542=CARTESIAN_POINT('Ctrl Pts',(-131.19467786657,-1.48078089957244,
125.073740153983));
#157543=CARTESIAN_POINT('Ctrl Pts',(-131.202075780881,-1.63289542391584,
125.115211547313));
#157544=CARTESIAN_POINT('Ctrl Pts',(-131.209473695192,-1.7831567193988,
125.162704595035));
#157545=CARTESIAN_POINT('Ctrl Pts',(-131.216870380105,-1.93339304418024,
125.210189750273));
#157546=CARTESIAN_POINT('Ctrl Pts',(-131.224267065017,-2.0817763957433,
125.263694461438));
#157547=CARTESIAN_POINT('Ctrl Pts',(-131.231663749929,-2.22779604969253,
125.32304185987));
#157548=CARTESIAN_POINT('Ctrl Pts',(-131.239060106864,-2.37380922897729,
125.382386626776));
#157549=CARTESIAN_POINT('Ctrl Pts',(-131.2464564638,-2.51745857321808,125.447573425274));
#157550=CARTESIAN_POINT('Ctrl Pts',(-131.253852820735,-2.65825270313081,
125.518376969389));
#157551=CARTESIAN_POINT('Ctrl Pts',(-131.261250310072,-2.79906838898466,
125.589191353707));
#157552=CARTESIAN_POINT('Ctrl Pts',(-131.268647799409,-2.93702765658215,
125.66562402817));
#157553=CARTESIAN_POINT('Ctrl Pts',(-131.276045288745,-3.07166326535431,
125.747403494278));
#157554=CARTESIAN_POINT('Ctrl Pts',(-131.28344537126,-3.20634607043021,
125.829211628051));
#157555=CARTESIAN_POINT('Ctrl Pts',(-131.290845453775,-3.3377025781153,
125.916370091531));
#157556=CARTESIAN_POINT('Ctrl Pts',(-131.29824553629,-3.46529422484557,
126.008563864392));
#157557=CARTESIAN_POINT('Ctrl Pts',(-131.305653755957,-3.59302617170761,
126.100859013785));
#157558=CARTESIAN_POINT('Ctrl Pts',(-131.313061975623,-3.71698468729859,
126.198200311227));
#157559=CARTESIAN_POINT('Ctrl Pts',(-131.320470195289,-3.83676345690102,
126.300231763027));
#157560=CARTESIAN_POINT('Ctrl Pts',(-131.327882974592,-3.95661594833819,
126.402326013484));
#157561=CARTESIAN_POINT('Ctrl Pts',(-131.335295753894,-4.0722832939897,
126.509115917794));
#157562=CARTESIAN_POINT('Ctrl Pts',(-131.342708533196,-4.18339619601278,
126.62020875253));
#157563=CARTESIAN_POINT('Ctrl Pts',(-131.350131904224,-4.29466786136111,
126.731460321918));
#157564=CARTESIAN_POINT('Ctrl Pts',(-131.357555275253,-4.40137183337431,
126.847026827581));
#157565=CARTESIAN_POINT('Ctrl Pts',(-131.364978646282,-4.50317869645347,
126.966482012098));
#157566=CARTESIAN_POINT('Ctrl Pts',(-131.368914695723,-4.55715913808003,
127.029820017217));
#157567=CARTESIAN_POINT('Ctrl Pts',(-131.372850745164,-4.60976353810745,
127.094250766581));
#157568=CARTESIAN_POINT('Ctrl Pts',(-131.376786794604,-4.66094781967877,
127.159707549751));
#157569=CARTESIAN_POINT('Ctrl Pts',(-131.384488378487,-4.76109901034053,
127.287785439489));
#157570=CARTESIAN_POINT('Ctrl Pts',(-131.39218996237,-4.85612985087017,
127.420202583377));
#157571=CARTESIAN_POINT('Ctrl Pts',(-131.399891546253,-4.94564361363236,
127.556509049308));
#157572=CARTESIAN_POINT('Ctrl Pts',(-131.4073050145,-5.03180867370954,127.687716301281));
#157573=CARTESIAN_POINT('Ctrl Pts',(-131.414718482747,-5.11286169848056,
127.822526811496));
#157574=CARTESIAN_POINT('Ctrl Pts',(-131.422131950995,-5.18848816115942,
127.960503876447));
#157575=CARTESIAN_POINT('Ctrl Pts',(-131.429538358199,-5.26404259254646,
128.098349523559));
#157576=CARTESIAN_POINT('Ctrl Pts',(-131.436944765404,-5.33418057081548,
128.239355398321));
#157577=CARTESIAN_POINT('Ctrl Pts',(-131.444351172609,-5.39863064300834,
128.383055650638));
#157578=CARTESIAN_POINT('Ctrl Pts',(-131.451751984199,-5.46303202253433,
128.526647335993));
#157579=CARTESIAN_POINT('Ctrl Pts',(-131.45915279579,-5.52175389857244,
128.672929008114));
#157580=CARTESIAN_POINT('Ctrl Pts',(-131.46655360738,-5.57457065688352,
128.821410150733));
#157581=CARTESIAN_POINT('Ctrl Pts',(-131.473950284995,-5.62735791258903,
128.969808354135));
#157582=CARTESIAN_POINT('Ctrl Pts',(-131.481346962609,-5.67424649400309,
129.120403231358));
#157583=CARTESIAN_POINT('Ctrl Pts',(-131.488743640224,-5.71505891104223,
129.272684344388));
#157584=CARTESIAN_POINT('Ctrl Pts',(-131.496138160116,-5.75585942248531,
129.424921034726));
#157585=CARTESIAN_POINT('Ctrl Pts',(-131.503532680008,-5.79058720060037,
129.578842622291));
#157586=CARTESIAN_POINT('Ctrl Pts',(-131.510927199901,-5.81911463531049,
129.733923592975));
#157587=CARTESIAN_POINT('Ctrl Pts',(-131.51832051618,-5.84763742658413,
129.888979320988));
#157588=CARTESIAN_POINT('Ctrl Pts',(-131.52571383246,-5.86996182017713,
130.045193689219));
#157589=CARTESIAN_POINT('Ctrl Pts',(-131.533107148739,-5.88601138189131,
130.202031326608));
#157590=CARTESIAN_POINT('Ctrl Pts',(-131.540501856673,-5.90206396463677,
130.358898485763));
#157591=CARTESIAN_POINT('Ctrl Pts',(-131.547896564607,-5.91183932033364,
130.516388777382));
#157592=CARTESIAN_POINT('Ctrl Pts',(-131.555291272541,-5.91531290361354,
130.673961941027));
#157593=CARTESIAN_POINT('Ctrl Pts',(-131.557402450957,-5.91630460661441,
130.718948851272));
#157594=CARTESIAN_POINT('Ctrl Pts',(-131.559513629373,-5.91678298102441,
130.763942507053));
#157595=CARTESIAN_POINT('Ctrl Pts',(-131.56162480779,-5.9167482353232,130.808930333076));
#157596=CARTESIAN_POINT('',(-133.31162480779,-5.9258324623384,130.806216140417));
#157597=CARTESIAN_POINT('Ctrl Pts',(-131.561626894289,-5.91103949408356,
130.808970343057));
#157598=CARTESIAN_POINT('Ctrl Pts',(-131.592829402331,-5.9157889408592,
131.473237742977));
#157599=CARTESIAN_POINT('Ctrl Pts',(-131.71684778498,-5.50543080433528,
134.107748453049));
#157600=CARTESIAN_POINT('Ctrl Pts',(-131.933682042229,-1.62929050015997,
137.610458838751));
#157601=CARTESIAN_POINT('Ctrl Pts',(-132.212129666044,4.8454918792327,135.853991195998));
#157602=CARTESIAN_POINT('Ctrl Pts',(-132.490577289856,6.86750393704832,
129.457159739833));
#157603=CARTESIAN_POINT('Ctrl Pts',(-132.769024913669,2.57861537293547,
124.298340075881));
#157604=CARTESIAN_POINT('Ctrl Pts',(-133.042707419646,-3.96594661910167,
125.104204454854));
#157605=CARTESIAN_POINT('Ctrl Pts',(-133.223574051021,-5.91819771649719,
128.943738175882));
#157606=CARTESIAN_POINT('Ctrl Pts',(-133.31162480779,-5.9258324623384,130.806216140417));
#157607=CARTESIAN_POINT('',(-135.06162480779,-5.91669650453655,130.79889406161));
#157608=CARTESIAN_POINT('Ctrl Pts',(-133.31162480779,-5.9258324623384,130.806216140417));
#157609=CARTESIAN_POINT('Ctrl Pts',(-133.316389925625,-5.92624563838489,
130.907009447499));
#157610=CARTESIAN_POINT('Ctrl Pts',(-133.32115504346,-5.92389767337334,
131.007783100793));
#157611=CARTESIAN_POINT('Ctrl Pts',(-133.418736035899,-5.8180376903742,
133.068477094558));
#157612=CARTESIAN_POINT('Ctrl Pts',(-133.604367785107,-3.47575125535195,
136.878627136354));
#157613=CARTESIAN_POINT('Ctrl Pts',(-133.882815408921,3.23172400096065,
137.011898012697));
#157614=CARTESIAN_POINT('Ctrl Pts',(-134.161263032733,6.96940277888598,
131.440745277975));
#157615=CARTESIAN_POINT('Ctrl Pts',(-134.439710656546,4.30254087726768,
125.284786129456));
#157616=CARTESIAN_POINT('Ctrl Pts',(-134.718158280359,-2.31814589975123,
124.201046289305));
#157617=CARTESIAN_POINT('Ctrl Pts',(-134.925462997441,-5.6612739620627,
127.911928013576));
#157618=CARTESIAN_POINT('Ctrl Pts',(-135.039951839917,-5.92095229654158,
130.338617738869));
#157619=CARTESIAN_POINT('Ctrl Pts',(-135.06162480779,-5.91669650453655,
130.79889406161));
#157620=CARTESIAN_POINT('',(-136.81162480779,-5.90698938982151,130.80496114814));
#157621=CARTESIAN_POINT('Ctrl Pts',(-135.06162480779,-5.91669650453655,
130.79889406161));
#157622=CARTESIAN_POINT('Ctrl Pts',(-135.132767714522,-5.90272659439496,
132.309780604324));
#157623=CARTESIAN_POINT('Ctrl Pts',(-135.296726495857,-4.54411447408175,
135.814156954017));
#157624=CARTESIAN_POINT('Ctrl Pts',(-135.553501151798,1.35765048963333,
137.669806391752));
#157625=CARTESIAN_POINT('Ctrl Pts',(-135.83194877561,6.50993722145643,133.373071948767));
#157626=CARTESIAN_POINT('Ctrl Pts',(-136.110396399423,5.67990967487751,
126.715817280924));
#157627=CARTESIAN_POINT('Ctrl Pts',(-136.388844023236,-0.369677383902886,
123.815734203013));
#157628=CARTESIAN_POINT('Ctrl Pts',(-136.622586826026,-5.16282797254495,
126.77237981359));
#157629=CARTESIAN_POINT('Ctrl Pts',(-136.76351375421,-5.90606400737249,
129.778969746663));
#157630=CARTESIAN_POINT('Ctrl Pts',(-136.81162480779,-5.90698938982151,
130.80496114814));
#157631=CARTESIAN_POINT('',(-138.561624088733,-5.91830260272839,130.809606478819));
#157632=CARTESIAN_POINT('Ctrl Pts',(-136.81162480779,-5.90698938982151,
130.80496114814));
#157633=CARTESIAN_POINT('Ctrl Pts',(-136.856329628814,-5.90784925577088,
131.758312998952));
#157634=CARTESIAN_POINT('Ctrl Pts',(-136.993850324443,-5.23902913899845,
134.689869888022));
#157635=CARTESIAN_POINT('Ctrl Pts',(-137.224186894675,-0.625777678858699,
137.774723795112));
#157636=CARTESIAN_POINT('Ctrl Pts',(-137.502634518488,5.52611583132312,
135.098496659793));
#157637=CARTESIAN_POINT('Ctrl Pts',(-137.781082142301,6.59977885829072,
128.476168281864));
#157638=CARTESIAN_POINT('Ctrl Pts',(-138.059529766113,1.60856753160757,
123.993334921931));
#157639=CARTESIAN_POINT('Ctrl Pts',(-138.319710321652,-4.43642471316069,
125.652979148224));
#157640=CARTESIAN_POINT('Ctrl Pts',(-138.487075002584,-5.90427870488731,
129.227898504401));
#157641=CARTESIAN_POINT('Ctrl Pts',(-138.561623808914,-5.9189077050571,
130.809601079842));
#157642=CARTESIAN_POINT('',(-140.311626173768,-5.92115491125036,130.801347234396));
#157643=CARTESIAN_POINT('Ctrl Pts',(-138.56162480779,-5.91674766216093,
130.80962035265));
#157644=CARTESIAN_POINT('Ctrl Pts',(-138.572369984272,-5.91654507308181,
131.03751556811));
#157645=CARTESIAN_POINT('Ctrl Pts',(-138.583115160753,-5.90317251244182,
131.264849426288));
#157646=CARTESIAN_POINT('Ctrl Pts',(-138.593860337235,-5.87684304778801,
131.490397317871));
#157647=CARTESIAN_POINT('Ctrl Pts',(-138.60138189607,-5.85841258107345,
131.648279483841));
#157648=CARTESIAN_POINT('Ctrl Pts',(-138.608903454904,-5.83363427395434,
131.805287471932));
#157649=CARTESIAN_POINT('Ctrl Pts',(-138.616425013739,-5.80259373517108,
131.961009443724));
#157650=CARTESIAN_POINT('Ctrl Pts',(-138.623848280145,-5.77195883703105,
132.114696426328));
#157651=CARTESIAN_POINT('Ctrl Pts',(-138.63127154655,-5.73516758839248,
132.267397870938));
#157652=CARTESIAN_POINT('Ctrl Pts',(-138.638694812956,-5.69229479046269,
132.418581971957));
#157653=CARTESIAN_POINT('Ctrl Pts',(-138.646109305677,-5.64947266461969,
132.569587385923));
#157654=CARTESIAN_POINT('Ctrl Pts',(-138.653523798398,-5.6005833978621,
132.719078670389));
#157655=CARTESIAN_POINT('Ctrl Pts',(-138.660938291119,-5.5457530503043,
132.866532692719));
#157656=CARTESIAN_POINT('Ctrl Pts',(-138.668345637473,-5.4909755502998,
133.013844593311));
#157657=CARTESIAN_POINT('Ctrl Pts',(-138.675752983826,-5.43026849853887,
133.159122793345));
#157658=CARTESIAN_POINT('Ctrl Pts',(-138.68316033018,-5.36380812500308,
133.301857957034));
#157659=CARTESIAN_POINT('Ctrl Pts',(-138.690562151856,-5.29739732012109,
133.444486663454));
#157660=CARTESIAN_POINT('Ctrl Pts',(-138.697963973531,-5.22524189440597,
133.584575773143));
#157661=CARTESIAN_POINT('Ctrl Pts',(-138.705365795207,-5.14756663851491,
133.721634732994));
#157662=CARTESIAN_POINT('Ctrl Pts',(-138.712763709518,-5.06993238678681,
133.858621340488));
#157663=CARTESIAN_POINT('Ctrl Pts',(-138.72016162383,-4.98678429159512,
133.992580659863));
#157664=CARTESIAN_POINT('Ctrl Pts',(-138.727559538141,-4.89839359210376,
134.123045715513));
#157665=CARTESIAN_POINT('Ctrl Pts',(-138.734956223053,-4.81001758154322,
134.253489090238));
#157666=CARTESIAN_POINT('Ctrl Pts',(-138.742352907966,-4.71640090498478,
134.380439044978));
#157667=CARTESIAN_POINT('Ctrl Pts',(-138.749749592878,-4.61785879651094,
134.503456547383));
#157668=CARTESIAN_POINT('Ctrl Pts',(-138.757145949813,-4.51932105749745,
134.626468595063));
#157669=CARTESIAN_POINT('Ctrl Pts',(-138.764542306749,-4.41585855420128,
134.745548245764));
#157670=CARTESIAN_POINT('Ctrl Pts',(-138.771938663684,-4.30782740605772,
134.86028882232));
#157671=CARTESIAN_POINT('Ctrl Pts',(-138.779336153021,-4.1997797180699,
134.97504696595));
#157672=CARTESIAN_POINT('Ctrl Pts',(-138.786733642357,-4.08716224840645,
135.085464440872));
#157673=CARTESIAN_POINT('Ctrl Pts',(-138.794131131694,-3.97036852102234,
135.191170890392));
#157674=CARTESIAN_POINT('Ctrl Pts',(-138.801531214209,-3.85353385177799,
135.296914395145));
#157675=CARTESIAN_POINT('Ctrl Pts',(-138.808931296724,-3.73252028663693,
135.397943336143));
#157676=CARTESIAN_POINT('Ctrl Pts',(-138.816331379239,-3.60775488037699,
135.493927259124));
#157677=CARTESIAN_POINT('Ctrl Pts',(-138.823739598905,-3.48285228172649,
135.590016726296));
#157678=CARTESIAN_POINT('Ctrl Pts',(-138.831147818572,-3.35418989904718,
135.681049868937));
#157679=CARTESIAN_POINT('Ctrl Pts',(-138.838556038238,-3.2222248563131,
135.766738831473));
#157680=CARTESIAN_POINT('Ctrl Pts',(-138.845968817541,-3.09017859129717,
135.852480534136));
#157681=CARTESIAN_POINT('Ctrl Pts',(-138.853381596843,-2.95482593596447,
135.932871312259));
#157682=CARTESIAN_POINT('Ctrl Pts',(-138.860794376145,-2.8166486558548,
136.007669268028));
#157683=CARTESIAN_POINT('Ctrl Pts',(-138.868217747174,-2.67827394156724,
136.082574098624));
#157684=CARTESIAN_POINT('Ctrl Pts',(-138.875641118202,-2.53706687602473,
136.151869982453));
#157685=CARTESIAN_POINT('Ctrl Pts',(-138.883064489231,-2.39352998589385,
136.215362813937));
#157686=CARTESIAN_POINT('Ctrl Pts',(-138.887000538672,-2.31742328263425,
136.249028236675));
#157687=CARTESIAN_POINT('Ctrl Pts',(-138.890936588112,-2.24066186110984,
136.281063038531));
#157688=CARTESIAN_POINT('Ctrl Pts',(-138.894872637552,-2.16332223464045,
136.311444008219));
#157689=CARTESIAN_POINT('Ctrl Pts',(-138.902295903958,-2.01746211279161,
136.368741568899));
#157690=CARTESIAN_POINT('Ctrl Pts',(-138.909719170363,-1.86910349414759,
136.420326910188));
#157691=CARTESIAN_POINT('Ctrl Pts',(-138.917142436769,-1.71873423369849,
136.465975510546));
#157692=CARTESIAN_POINT('Ctrl Pts',(-138.92455692949,-1.56854269722742,
136.511570158049));
#157693=CARTESIAN_POINT('Ctrl Pts',(-138.931971422211,-1.4163456029246,
136.551241924091));
#157694=CARTESIAN_POINT('Ctrl Pts',(-138.939385914932,-1.2626512156636,
136.584814100649));
#157695=CARTESIAN_POINT('Ctrl Pts',(-138.946793261285,-1.10910496483953,
136.618353919078));
#157696=CARTESIAN_POINT('Ctrl Pts',(-138.954200607639,-0.954064656329923,
136.645805772855));
#157697=CARTESIAN_POINT('Ctrl Pts',(-138.961607953993,-0.798054065368237,
136.667042620818));
#157698=CARTESIAN_POINT('Ctrl Pts',(-138.969009775668,-0.642159832991233,
136.688263629538));
#157699=CARTESIAN_POINT('Ctrl Pts',(-138.976411597344,-0.485297127387972,
136.70327881199));
#157700=CARTESIAN_POINT('Ctrl Pts',(-138.983813419019,-0.328000169621734,
136.712012134982));
#157701=CARTESIAN_POINT('Ctrl Pts',(-138.99121133333,-0.170786247695105,
136.720740847721));
#157702=CARTESIAN_POINT('Ctrl Pts',(-138.998609247642,-0.0131389019250054,
136.723194284621));
#157703=CARTESIAN_POINT('Ctrl Pts',(-139.006007161953,0.144402376492931,
136.719348235149));
#157704=CARTESIAN_POINT('Ctrl Pts',(-139.013403846865,0.301917474408259,
136.715502824822));
#157705=CARTESIAN_POINT('Ctrl Pts',(-139.020800531778,0.459326167133431,
136.705360014933));
#157706=CARTESIAN_POINT('Ctrl Pts',(-139.02819721669,0.616088692597387,
136.688947713136));
#157707=CARTESIAN_POINT('Ctrl Pts',(-139.035593573625,0.772844267046688,
136.672536139078));
#157708=CARTESIAN_POINT('Ctrl Pts',(-139.042989930561,0.928953359935741,
136.649855664732));
#157709=CARTESIAN_POINT('Ctrl Pts',(-139.050386287496,1.08388133099193,
136.620986084521));
#157710=CARTESIAN_POINT('Ctrl Pts',(-139.057783776833,1.238833021916,136.592112084303));
#157711=CARTESIAN_POINT('Ctrl Pts',(-139.065181266169,1.39260286394066,
136.557047159876));
#157712=CARTESIAN_POINT('Ctrl Pts',(-139.072578755506,1.54466655618022,
136.515922207247));
#157713=CARTESIAN_POINT('Ctrl Pts',(-139.079978838021,1.69678355411159,
136.47478283833));
#157714=CARTESIAN_POINT('Ctrl Pts',(-139.087378920536,1.84719285134129,
136.427579309074));
#157715=CARTESIAN_POINT('Ctrl Pts',(-139.094779003051,1.99538559379863,
136.374492294157));
#157716=CARTESIAN_POINT('Ctrl Pts',(-139.102187222718,2.14374128941111,
136.321346904609));
#157717=CARTESIAN_POINT('Ctrl Pts',(-139.109595442384,2.28987521109871,
136.262305235359));
#157718=CARTESIAN_POINT('Ctrl Pts',(-139.11700366205,2.43329809114091,136.197596284784));
#157719=CARTESIAN_POINT('Ctrl Pts',(-139.124416441352,2.57680924557264,
136.132847506929));
#157720=CARTESIAN_POINT('Ctrl Pts',(-139.131829220655,2.71760570037214,
136.062424663841));
#157721=CARTESIAN_POINT('Ctrl Pts',(-139.139241999957,2.85522353401579,
135.986602326836));
#157722=CARTESIAN_POINT('Ctrl Pts',(-139.146665370985,2.99303800247359,
135.910671651321));
#157723=CARTESIAN_POINT('Ctrl Pts',(-139.154088742014,3.12766446020009,
135.829326265745));
#157724=CARTESIAN_POINT('Ctrl Pts',(-139.161512113043,3.25866797273628,
135.742884041218));
#157725=CARTESIAN_POINT('Ctrl Pts',(-139.165448162484,3.32812917846873,
135.697050299622));
#157726=CARTESIAN_POINT('Ctrl Pts',(-139.169384211925,3.39657238788596,
135.649784334589));
#157727=CARTESIAN_POINT('Ctrl Pts',(-139.173320261365,3.46393671535675,
135.601137972677));
#157728=CARTESIAN_POINT('Ctrl Pts',(-139.180743527771,3.59098373459849,
135.50939245231));
#157729=CARTESIAN_POINT('Ctrl Pts',(-139.188166794176,3.71457540043574,
135.412457281719));
#157730=CARTESIAN_POINT('Ctrl Pts',(-139.195590060582,3.83425911899848,
135.310621547747));
#157731=CARTESIAN_POINT('Ctrl Pts',(-139.203004553303,3.95380138134499,
135.208906175156));
#157732=CARTESIAN_POINT('Ctrl Pts',(-139.210419046024,4.06944460877007,
135.102302007856));
#157733=CARTESIAN_POINT('Ctrl Pts',(-139.217833538745,4.18076540222964,
134.991141148478));
#157734=CARTESIAN_POINT('Ctrl Pts',(-139.225240885098,4.29197890051763,
134.88008743012));
#157735=CARTESIAN_POINT('Ctrl Pts',(-139.232648231452,4.3988779963961,134.764486025116));
#157736=CARTESIAN_POINT('Ctrl Pts',(-139.240055577806,4.50107269323137,
134.644708931554));
#157737=CARTESIAN_POINT('Ctrl Pts',(-139.247457399481,4.60319116940617,
134.525021172266));
#157738=CARTESIAN_POINT('Ctrl Pts',(-139.254859221157,4.70061199161803,
134.401164208341));
#157739=CARTESIAN_POINT('Ctrl Pts',(-139.262261042832,4.7929824314566,134.273546397291));
#157740=CARTESIAN_POINT('Ctrl Pts',(-139.269658957144,4.88530410965899,
134.145995954691));
#157741=CARTESIAN_POINT('Ctrl Pts',(-139.277056871455,4.97258049674658,
134.014688920462));
#157742=CARTESIAN_POINT('Ctrl Pts',(-139.284454785766,5.05449961554519,
133.880066097444));
#157743=CARTESIAN_POINT('Ctrl Pts',(-139.291851470678,5.1364051208723,133.745465646297));
#157744=CARTESIAN_POINT('Ctrl Pts',(-139.299248155591,5.21295493099283,
133.607550818565));
#157745=CARTESIAN_POINT('Ctrl Pts',(-139.306644840503,5.28388077082161,
133.466790816133));
#157746=CARTESIAN_POINT('Ctrl Pts',(-139.314041197438,5.35480346572432,
133.326037055147));
#157747=CARTESIAN_POINT('Ctrl Pts',(-139.321437554374,5.42010251819538,
133.182438703674));
#157748=CARTESIAN_POINT('Ctrl Pts',(-139.328833911309,5.47955607541675,
133.036488700554));
#157749=CARTESIAN_POINT('Ctrl Pts',(-139.336231400646,5.53901873512951,
132.890516352115));
#157750=CARTESIAN_POINT('Ctrl Pts',(-139.343628889982,5.59263397676986,
132.74219198087));
#157751=CARTESIAN_POINT('Ctrl Pts',(-139.351026379319,5.64022852942182,
132.592027448493));
#157752=CARTESIAN_POINT('Ctrl Pts',(-139.358426461834,5.68783976627049,
132.441810276171));
#157753=CARTESIAN_POINT('Ctrl Pts',(-139.365826544349,5.72942599933814,
132.289752014026));
#157754=CARTESIAN_POINT('Ctrl Pts',(-139.373226626864,5.76486418729327,
132.136378434475));
#157755=CARTESIAN_POINT('Ctrl Pts',(-139.38063484653,5.80034134317913,131.982836204907));
#157756=CARTESIAN_POINT('Ctrl Pts',(-139.388043066197,5.82965686888374,
131.827976133461));
#157757=CARTESIAN_POINT('Ctrl Pts',(-139.395451285863,5.85273896607318,
131.672333634145));
#157758=CARTESIAN_POINT('Ctrl Pts',(-139.402864065165,5.87583526990836,
131.516595339467));
#157759=CARTESIAN_POINT('Ctrl Pts',(-139.410276844468,5.89269046050387,
131.360074027619));
#157760=CARTESIAN_POINT('Ctrl Pts',(-139.41768962377,5.90328478156865,131.20330842142));
#157761=CARTESIAN_POINT('Ctrl Pts',(-139.425112994798,5.91389424029617,
131.046318821172));
#157762=CARTESIAN_POINT('Ctrl Pts',(-139.432536365827,5.91822495242524,
130.889084601592));
#157763=CARTESIAN_POINT('Ctrl Pts',(-139.439959736856,5.91630925922449,
130.732143502458));
#157764=CARTESIAN_POINT('Ctrl Pts',(-139.443895786297,5.91529351272302,
130.648929565946));
#157765=CARTESIAN_POINT('Ctrl Pts',(-139.447831835738,5.91252254420794,
130.565797946815));
#157766=CARTESIAN_POINT('Ctrl Pts',(-139.451767885178,5.9080070466573,130.482827883388));
#157767=CARTESIAN_POINT('Ctrl Pts',(-139.459191151584,5.89949095920072,
130.326348933175));
#157768=CARTESIAN_POINT('Ctrl Pts',(-139.466614417989,5.88474096911531,
130.16997193693));
#157769=CARTESIAN_POINT('Ctrl Pts',(-139.474037684395,5.86375565530722,
130.014233933197));
#157770=CARTESIAN_POINT('Ctrl Pts',(-139.481452177116,5.84279514439733,
129.85867999885));
#157771=CARTESIAN_POINT('Ctrl Pts',(-139.488866669837,5.81561402842719,
129.703763920054));
#157772=CARTESIAN_POINT('Ctrl Pts',(-139.496281162558,5.78226285721951,
129.550021423998));
#157773=CARTESIAN_POINT('Ctrl Pts',(-139.503688508911,5.74894383112621,
129.396427110749));
#157774=CARTESIAN_POINT('Ctrl Pts',(-139.511095855265,5.70946666757237,
129.244004490721));
#157775=CARTESIAN_POINT('Ctrl Pts',(-139.518503201619,5.6639335363781,129.09328275318));
#157776=CARTESIAN_POINT('Ctrl Pts',(-139.525905023294,5.61843436551095,
128.942673429598));
#157777=CARTESIAN_POINT('Ctrl Pts',(-139.53330684497,5.56688832799046,128.793762818394));
#157778=CARTESIAN_POINT('Ctrl Pts',(-139.540708666645,5.50944832823656,
128.64706840718));
#157779=CARTESIAN_POINT('Ctrl Pts',(-139.548106580957,5.45203865061142,
128.500451434804));
#157780=CARTESIAN_POINT('Ctrl Pts',(-139.555504495268,5.38874134297153,
128.356048679199));
#157781=CARTESIAN_POINT('Ctrl Pts',(-139.562902409579,5.31975863394631,
128.214360880297));
#157782=CARTESIAN_POINT('Ctrl Pts',(-139.570299094491,5.25078738859596,
128.072696627337));
#157783=CARTESIAN_POINT('Ctrl Pts',(-139.577695779404,5.17613278027719,
127.933746770933));
#157784=CARTESIAN_POINT('Ctrl Pts',(-139.585092464316,5.09604455258802,
127.797990633592));
#157785=CARTESIAN_POINT('Ctrl Pts',(-139.592488821251,5.0159598760948,127.662240515821));
#157786=CARTESIAN_POINT('Ctrl Pts',(-139.599885178187,4.930442248963,127.529684157056));
#157787=CARTESIAN_POINT('Ctrl Pts',(-139.607281535122,4.83978647773083,
127.40077465384));
#157788=CARTESIAN_POINT('Ctrl Pts',(-139.614679024459,4.74911682686866,
127.27184541425));
#157789=CARTESIAN_POINT('Ctrl Pts',(-139.622076513795,4.65330768030736,
127.146564447313));
#157790=CARTESIAN_POINT('Ctrl Pts',(-139.629474003132,4.5526960246077,127.025354204496));
#157791=CARTESIAN_POINT('Ctrl Pts',(-139.636874085647,4.45204909964796,
126.904101471617));
#157792=CARTESIAN_POINT('Ctrl Pts',(-139.644274168162,4.3465965519648,126.786922591035));
#157793=CARTESIAN_POINT('Ctrl Pts',(-139.651674250677,4.23671422193866,
126.674205273741));
#157794=CARTESIAN_POINT('Ctrl Pts',(-139.659082470343,4.12671106499463,
126.56136401217));
#157795=CARTESIAN_POINT('Ctrl Pts',(-139.66649069001,4.01226865873714,126.452994378852));
#157796=CARTESIAN_POINT('Ctrl Pts',(-139.673898909676,3.89379865338024,
126.349446184108));
#157797=CARTESIAN_POINT('Ctrl Pts',(-139.681311688978,3.77525573171182,
126.245834257177));
#157798=CARTESIAN_POINT('Ctrl Pts',(-139.68872446828,3.65268056136824,126.147049915666));
#157799=CARTESIAN_POINT('Ctrl Pts',(-139.696137247583,3.52651570635732,
126.053400973945));
#157800=CARTESIAN_POINT('Ctrl Pts',(-139.703560618611,3.40017058108484,
125.959618222224));
#157801=CARTESIAN_POINT('Ctrl Pts',(-139.71098398964,3.2702258347369,125.870985735115));
#157802=CARTESIAN_POINT('Ctrl Pts',(-139.718407360669,3.13715136426387,
125.787766964479));
#157803=CARTESIAN_POINT('Ctrl Pts',(-139.72234341011,3.06659208694024,125.74364237548));
#157804=CARTESIAN_POINT('Ctrl Pts',(-139.726279459551,2.99515332518775,
125.701038999026));
#157805=CARTESIAN_POINT('Ctrl Pts',(-139.730215508991,2.9229075242693,125.659990669062));
#157806=CARTESIAN_POINT('Ctrl Pts',(-139.737638775397,2.78665419845301,
125.582574799826));
#157807=CARTESIAN_POINT('Ctrl Pts',(-139.745062041802,2.64711707275638,
125.510458798036));
#157808=CARTESIAN_POINT('Ctrl Pts',(-139.752485308208,2.50474720477755,
125.443934141747));
#157809=CARTESIAN_POINT('Ctrl Pts',(-139.759899800929,2.36254560615918,
125.377488112078));
#157810=CARTESIAN_POINT('Ctrl Pts',(-139.76731429365,2.21751826449865,125.316620430127));
#157811=CARTESIAN_POINT('Ctrl Pts',(-139.774728786371,2.07014322566789,
125.261578140531));
#157812=CARTESIAN_POINT('Ctrl Pts',(-139.782136132724,1.92291023244813,
125.206588902767));
#157813=CARTESIAN_POINT('Ctrl Pts',(-139.789543479078,1.77333439420133,
125.157414009261));
#157814=CARTESIAN_POINT('Ctrl Pts',(-139.796950825432,1.62191615812796,
125.114253541376));
#157815=CARTESIAN_POINT('Ctrl Pts',(-139.804352647107,1.47061085548815,
125.071125264197));
#157816=CARTESIAN_POINT('Ctrl Pts',(-139.811754468783,1.31746624855318,
125.034002582723));
#157817=CARTESIAN_POINT('Ctrl Pts',(-139.819156290458,1.16300036288113,
125.00303656883));
#157818=CARTESIAN_POINT('Ctrl Pts',(-139.82655420477,1.00861601854733,124.972086901655));
#157819=CARTESIAN_POINT('Ctrl Pts',(-139.833952119081,0.852912149655667,
124.947287502607));
#157820=CARTESIAN_POINT('Ctrl Pts',(-139.841350033392,0.696419352408148,
124.928738893179));
#157821=CARTESIAN_POINT('Ctrl Pts',(-139.848746718304,0.539952561424241,
124.910193366193));
#157822=CARTESIAN_POINT('Ctrl Pts',(-139.856143403217,0.382697472630334,
124.897896611074));
#157823=CARTESIAN_POINT('Ctrl Pts',(-139.863540088129,0.225192346141724,
124.891897596985));
#157824=CARTESIAN_POINT('Ctrl Pts',(-139.870936445064,0.0676942035959251,
124.885898848898));
#157825=CARTESIAN_POINT('Ctrl Pts',(-139.878332802,-0.0900535815729142,
124.886197300808));
#157826=CARTESIAN_POINT('Ctrl Pts',(-139.885729158935,-0.247510456276855,
124.892789833372));
#157827=CARTESIAN_POINT('Ctrl Pts',(-139.893126648272,-0.404991438030731,
124.89938337527));
#157828=CARTESIAN_POINT('Ctrl Pts',(-139.900524137608,-0.562181047641271,
124.912272900941));
#157829=CARTESIAN_POINT('Ctrl Pts',(-139.907921626945,-0.718541715257594,
124.931403239385));
#157830=CARTESIAN_POINT('Ctrl Pts',(-139.91532170946,-0.874957194863338,
124.950540283938));
#157831=CARTESIAN_POINT('Ctrl Pts',(-139.922721791975,-1.03054278361979,
124.975922451668));
#157832=CARTESIAN_POINT('Ctrl Pts',(-139.93012187449,-1.18476913838338,
125.007443104677));
#157833=CARTESIAN_POINT('Ctrl Pts',(-139.937530094157,-1.33916508087868,
125.038998417885));
#157834=CARTESIAN_POINT('Ctrl Pts',(-139.944938313823,-1.49219843856993,
125.076705621563));
#157835=CARTESIAN_POINT('Ctrl Pts',(-139.952346533489,-1.64335239913165,
125.120407463751));
#157836=CARTESIAN_POINT('Ctrl Pts',(-139.959759312791,-1.79459939243439,
125.164136203693));
#157837=CARTESIAN_POINT('Ctrl Pts',(-139.967172092094,-1.94396433030163,
125.213866816484));
#157838=CARTESIAN_POINT('Ctrl Pts',(-139.974584871396,-2.0909490231294,
125.269393341676));
#157839=CARTESIAN_POINT('Ctrl Pts',(-139.982008242424,-2.23814373457897,
125.324999205771));
#157840=CARTESIAN_POINT('Ctrl Pts',(-139.989431613453,-2.38295106566392,
125.386417376849));
#157841=CARTESIAN_POINT('Ctrl Pts',(-139.996854984482,-2.52489537609378,
125.453394919463));
#157842=CARTESIAN_POINT('Ctrl Pts',(-140.000791033923,-2.60015765539067,
125.48890801966));
#157843=CARTESIAN_POINT('Ctrl Pts',(-140.004727083364,-2.67461547830674,
125.525983307554));
#157844=CARTESIAN_POINT('Ctrl Pts',(-140.008663132804,-2.7482012209517,
125.564578120968));
#157845=CARTESIAN_POINT('Ctrl Pts',(-140.01608639921,-2.88698163504634,
125.637366734561));
#157846=CARTESIAN_POINT('Ctrl Pts',(-140.023509665615,-3.0230780946054,
125.715782809807));
#157847=CARTESIAN_POINT('Ctrl Pts',(-140.03093293202,-3.15600156323604,
125.799604410182));
#157848=CARTESIAN_POINT('Ctrl Pts',(-140.038347424741,-3.28876792736536,
125.883326940386));
#157849=CARTESIAN_POINT('Ctrl Pts',(-140.045761917462,-3.41836845270827,
125.972442081442));
#157850=CARTESIAN_POINT('Ctrl Pts',(-140.053176410183,-3.5443368981461,
126.066681173477));
#157851=CARTESIAN_POINT('Ctrl Pts',(-140.060583756537,-3.67018393045359,
126.160829434328));
#157852=CARTESIAN_POINT('Ctrl Pts',(-140.067991102891,-3.79240555522919,
126.260091592148));
#157853=CARTESIAN_POINT('Ctrl Pts',(-140.075398449244,-3.91056293442113,
126.364154755398));
#157854=CARTESIAN_POINT('Ctrl Pts',(-140.08280027092,-4.02863218738185,
126.468140304414));
#157855=CARTESIAN_POINT('Ctrl Pts',(-140.090202092595,-4.14264295148744,
126.576919483399));
#157856=CARTESIAN_POINT('Ctrl Pts',(-140.09760391427,-4.25218812022256,
126.690138120819));
#157857=CARTESIAN_POINT('Ctrl Pts',(-140.105001828581,-4.3616754609155,
126.803296991001));
#157858=CARTESIAN_POINT('Ctrl Pts',(-140.112399742893,-4.46670164210321,
126.920890384716));
#157859=CARTESIAN_POINT('Ctrl Pts',(-140.119797657204,-4.56689529199973,
127.042526230673));
#157860=CARTESIAN_POINT('Ctrl Pts',(-140.127194342116,-4.66707229152975,
127.16414186296));
#157861=CARTESIAN_POINT('Ctrl Pts',(-140.134591027028,-4.76241811653455,
127.289798326349));
#157862=CARTESIAN_POINT('Ctrl Pts',(-140.14198771194,-4.85260062513205,
127.419069236389));
#157863=CARTESIAN_POINT('Ctrl Pts',(-140.149384068876,-4.94277913494261,
127.548334414422));
#157864=CARTESIAN_POINT('Ctrl Pts',(-140.156780425811,-5.02779456998593,
127.681213414279));
#157865=CARTESIAN_POINT('Ctrl Pts',(-140.164176782746,-5.10735737250467,
127.817249767259));
#157866=CARTESIAN_POINT('Ctrl Pts',(-140.171574272083,-5.1869323562916,
127.953306947751));
#157867=CARTESIAN_POINT('Ctrl Pts',(-140.178971761419,-5.26105285685825,
128.092522121625));
#157868=CARTESIAN_POINT('Ctrl Pts',(-140.186369250756,-5.32947472149487,
128.234413194865));
#157869=CARTESIAN_POINT('Ctrl Pts',(-140.193769333271,-5.39792057130996,
128.376354007801));
#157870=CARTESIAN_POINT('Ctrl Pts',(-140.201169415786,-5.4606636458513,
128.520972251684));
#157871=CARTESIAN_POINT('Ctrl Pts',(-140.208569498301,-5.51750753970128,
128.667764934747));
#157872=CARTESIAN_POINT('Ctrl Pts',(-140.215977717967,-5.57441393925632,
128.814719031457));
#157873=CARTESIAN_POINT('Ctrl Pts',(-140.223385937633,-5.62540806875892,
128.963851994048));
#157874=CARTESIAN_POINT('Ctrl Pts',(-140.2307941573,-5.67034287905158,129.114644015147));
#157875=CARTESIAN_POINT('Ctrl Pts',(-140.238206936602,-5.7153053459702,
129.26552884622));
#157876=CARTESIAN_POINT('Ctrl Pts',(-140.245619715903,-5.75420097034454,
129.418074409631));
#157877=CARTESIAN_POINT('Ctrl Pts',(-140.253032495205,-5.78693374888261,
129.571750237704));
#157878=CARTESIAN_POINT('Ctrl Pts',(-140.260455866234,-5.81971329754973,
129.725645645007));
#157879=CARTESIAN_POINT('Ctrl Pts',(-140.267879237263,-5.84631235033739,
129.880674175493));
#157880=CARTESIAN_POINT('Ctrl Pts',(-140.275302608291,-5.86668661380568,
130.036298941727));
#157881=CARTESIAN_POINT('Ctrl Pts',(-140.279238657733,-5.8774895371729,
130.118814926968));
#157882=CARTESIAN_POINT('Ctrl Pts',(-140.283174707175,-5.88654331946295,
130.201498500882));
#157883=CARTESIAN_POINT('Ctrl Pts',(-140.287110756616,-5.89384730120973,
130.284269709625));
#157884=CARTESIAN_POINT('Ctrl Pts',(-140.295282107008,-5.90901057468745,
130.456105088978));
#157885=CARTESIAN_POINT('Ctrl Pts',(-140.303453457399,-5.91666048185143,
130.628613165077));
#157886=CARTESIAN_POINT('Ctrl Pts',(-140.31162480779,-5.91674921901585,
130.801320588729));
#157887=CARTESIAN_POINT('',(-142.061623600479,-5.91263345657567,130.80054659611));
#157888=CARTESIAN_POINT('Ctrl Pts',(-140.311627245294,-5.92461090629068,
130.801368136286));
#157889=CARTESIAN_POINT('Ctrl Pts',(-140.396270957006,-5.91338488009951,
132.59275803674));
#157890=CARTESIAN_POINT('Ctrl Pts',(-140.573730543324,-4.09131473212171,
136.368220126305));
#157891=CARTESIAN_POINT('Ctrl Pts',(-140.844006004241,2.33823337963563,
137.400588721007));
#157892=CARTESIAN_POINT('Ctrl Pts',(-141.122453628056,6.81346577453316,
132.402561064817));
#157893=CARTESIAN_POINT('Ctrl Pts',(-141.400901251868,5.02745597894928,
125.935865274023));
#157894=CARTESIAN_POINT('Ctrl Pts',(-141.679348875681,-1.3785402564146,
123.94307886473));
#157895=CARTESIAN_POINT('Ctrl Pts',(-141.899589348986,-5.443421615627,127.354004753196));
#157896=CARTESIAN_POINT('Ctrl Pts',(-142.027013947685,-5.91376279909305,
130.06325457639));
#157897=CARTESIAN_POINT('Ctrl Pts',(-142.061622671781,-5.90946782723236,
130.800528840258));
#157898=CARTESIAN_POINT('',(-143.811626040432,-5.91327805224815,130.808839182428));
#157899=CARTESIAN_POINT('Ctrl Pts',(-142.06162480779,-5.91674878554795,
130.800569678778));
#157900=CARTESIAN_POINT('Ctrl Pts',(-142.069073349795,-5.91685057702334,
130.959441826839));
#157901=CARTESIAN_POINT('Ctrl Pts',(-142.0765218918,-5.91054916224425,131.118342907778));
#157902=CARTESIAN_POINT('Ctrl Pts',(-142.083970433805,-5.89786424799386,
131.276724751192));
#157903=CARTESIAN_POINT('Ctrl Pts',(-142.091419462658,-5.8851785046396,
131.435116946666));
#157904=CARTESIAN_POINT('Ctrl Pts',(-142.09886849151,-5.86610845896061,
131.592989472193));
#157905=CARTESIAN_POINT('Ctrl Pts',(-142.106317520362,-5.84072578702984,
131.749798528391));
#157906=CARTESIAN_POINT('Ctrl Pts',(-142.113768429199,-5.81533670902553,
131.906647160026));
#157907=CARTESIAN_POINT('Ctrl Pts',(-142.121219338036,-5.78363188935134,
132.062431426492));
#157908=CARTESIAN_POINT('Ctrl Pts',(-142.128670246872,-5.74573427754804,
132.216617029946));
#157909=CARTESIAN_POINT('Ctrl Pts',(-142.136124429677,-5.70782001333851,
132.370870383351));
#157910=CARTESIAN_POINT('Ctrl Pts',(-142.143578612481,-5.66370762371264,
132.523523319449));
#157911=CARTESIAN_POINT('Ctrl Pts',(-142.151032795286,-5.61357011716365,
132.674056074636));
#157912=CARTESIAN_POINT('Ctrl Pts',(-142.158496430599,-5.56336903218619,
132.824779717576));
#157913=CARTESIAN_POINT('Ctrl Pts',(-142.165960065912,-5.5071276828603,
132.973377461212));
#157914=CARTESIAN_POINT('Ctrl Pts',(-142.173423701226,-5.44506785729073,
133.119348002413));
#157915=CARTESIAN_POINT('Ctrl Pts',(-142.180892350598,-5.38296634002241,
133.265416606406));
#157916=CARTESIAN_POINT('Ctrl Pts',(-142.188360999971,-5.31503871128872,
133.40885415989));
#157917=CARTESIAN_POINT('Ctrl Pts',(-142.195829649343,-5.24155288908102,
133.549183721787));
#157918=CARTESIAN_POINT('Ctrl Pts',(-142.203310567848,-5.16794634795429,
133.689743810233));
#157919=CARTESIAN_POINT('Ctrl Pts',(-142.210791486353,-5.08876355043455,
133.827185388102));
#157920=CARTESIAN_POINT('Ctrl Pts',(-142.218272404858,-5.0043165686423,
133.961059247989));
#157921=CARTESIAN_POINT('Ctrl Pts',(-142.224262977674,-4.93669308187295,
134.068262809332));
#157922=CARTESIAN_POINT('Ctrl Pts',(-142.23025355049,-4.86569481696976,
134.173179102954));
#157923=CARTESIAN_POINT('Ctrl Pts',(-142.236244123306,-4.79150027851089,
134.275593200314));
#157924=CARTESIAN_POINT('Ctrl Pts',(-142.243667389712,-4.69956152044658,
134.402500451375));
#157925=CARTESIAN_POINT('Ctrl Pts',(-142.251090656117,-4.60243837662734,
134.525944455269));
#157926=CARTESIAN_POINT('Ctrl Pts',(-142.258513922523,-4.50042062233194,
134.64547305859));
#157927=CARTESIAN_POINT('Ctrl Pts',(-142.265928415244,-4.39852344454978,
134.764860389029));
#157928=CARTESIAN_POINT('Ctrl Pts',(-142.273342907965,-4.2917434113877,
134.880341249147));
#157929=CARTESIAN_POINT('Ctrl Pts',(-142.280757400686,-4.18041326943229,
134.991492745796));
#157930=CARTESIAN_POINT('Ctrl Pts',(-142.28816474704,-4.06919043165921,
135.102537110447));
#157931=CARTESIAN_POINT('Ctrl Pts',(-142.295572093394,-3.95342647829153,
135.20926015688));
#157932=CARTESIAN_POINT('Ctrl Pts',(-142.302979439748,-3.83349400049477,
135.31127245503));
#157933=CARTESIAN_POINT('Ctrl Pts',(-142.310381261424,-3.71365097286441,
135.413208668559));
#157934=CARTESIAN_POINT('Ctrl Pts',(-142.317783083099,-3.58964589445368,
135.510440888746));
#157935=CARTESIAN_POINT('Ctrl Pts',(-142.325184904775,-3.46188765909607,
135.602617009038));
#157936=CARTESIAN_POINT('Ctrl Pts',(-142.332582819086,-3.33419686631753,
135.694744470272));
#157937=CARTESIAN_POINT('Ctrl Pts',(-142.339980733398,-3.20275716433496,
135.781820929342));
#157938=CARTESIAN_POINT('Ctrl Pts',(-142.347378647709,-3.06800983025294,
135.86353508026));
#157939=CARTESIAN_POINT('Ctrl Pts',(-142.354775332621,-2.93328488873232,
135.945235651769));
#157940=CARTESIAN_POINT('Ctrl Pts',(-142.362172017534,-2.79525372492089,
136.021575490356));
#157941=CARTESIAN_POINT('Ctrl Pts',(-142.369568702446,-2.65438594842956,
136.092287035292));
#157942=CARTESIAN_POINT('Ctrl Pts',(-142.376965059382,-2.51352441816346,
136.162995444803));
#157943=CARTESIAN_POINT('Ctrl Pts',(-142.384361416317,-2.36982685893144,
136.228075889413));
#157944=CARTESIAN_POINT('Ctrl Pts',(-142.391757773253,-2.22378654662323,
136.287307266728));
#157945=CARTESIAN_POINT('Ctrl Pts',(-142.399155262589,-2.07772387517038,
136.346547712518));
#157946=CARTESIAN_POINT('Ctrl Pts',(-142.406552751926,-1.92931808240953,
136.399937167629));
#157947=CARTESIAN_POINT('Ctrl Pts',(-142.413950241263,-1.77908129311106,
136.447303140311));
#157948=CARTESIAN_POINT('Ctrl Pts',(-142.421350323778,-1.62879183853878,
136.494685717061));
#157949=CARTESIAN_POINT('Ctrl Pts',(-142.428750406293,-1.47667046530508,
136.536040495182));
#157950=CARTESIAN_POINT('Ctrl Pts',(-142.436150488808,-1.3232431324667,
136.57124523362));
#157951=CARTESIAN_POINT('Ctrl Pts',(-142.443558708475,-1.16964709050294,
136.606488683287));
#157952=CARTESIAN_POINT('Ctrl Pts',(-142.450966928141,-1.01474258514053,
136.635568504377));
#157953=CARTESIAN_POINT('Ctrl Pts',(-142.458375147808,-0.859065139030692,
136.658413713448));
#157954=CARTESIAN_POINT('Ctrl Pts',(-142.46578792711,-0.703291876050397,
136.681272983363));
#157955=CARTESIAN_POINT('Ctrl Pts',(-142.473200706412,-0.546745094718591,
136.697889955647));
#157956=CARTESIAN_POINT('Ctrl Pts',(-142.480613485715,-0.389963547296973,
136.708245693876));
#157957=CARTESIAN_POINT('Ctrl Pts',(-142.488036856744,-0.232957983047854,
136.71861622887));
#157958=CARTESIAN_POINT('Ctrl Pts',(-142.495460227772,-0.0757173549334295,
136.722707652266));
#157959=CARTESIAN_POINT('Ctrl Pts',(-142.502883598801,0.0812206471090248,
136.720553123645));
#157960=CARTESIAN_POINT('Ctrl Pts',(-142.506819648241,0.164432941444102,
136.719410740873));
#157961=CARTESIAN_POINT('Ctrl Pts',(-142.510755697681,0.247560247345356,
136.716513263394));
#157962=CARTESIAN_POINT('Ctrl Pts',(-142.514691747121,0.330523342852393,
136.711871504761));
#157963=CARTESIAN_POINT('Ctrl Pts',(-142.522115013526,0.486989151831294,
136.703117292841));
#157964=CARTESIAN_POINT('Ctrl Pts',(-142.529538279931,0.643343520020078,
136.688129340668));
#157965=CARTESIAN_POINT('Ctrl Pts',(-142.536961546337,0.799049407337154,
136.66690704443));
#157966=CARTESIAN_POINT('Ctrl Pts',(-142.544376039058,0.954571263226434,
136.645709831184));
#157967=CARTESIAN_POINT('Ctrl Pts',(-142.551790531779,1.10944579760184,
136.618292990788));
#157968=CARTESIAN_POINT('Ctrl Pts',(-142.5592050245,1.2631373608214,136.584707888293));
#157969=CARTESIAN_POINT('Ctrl Pts',(-142.566612370854,1.41668079032637,
136.551155156384));
#157970=CARTESIAN_POINT('Ctrl Pts',(-142.574019717208,1.56904315632977,
136.511446077262));
#157971=CARTESIAN_POINT('Ctrl Pts',(-142.581427063561,1.71969542566331,
136.465683625967));
#157972=CARTESIAN_POINT('Ctrl Pts',(-142.588828885237,1.87023533284973,
136.419955306035));
#157973=CARTESIAN_POINT('Ctrl Pts',(-142.596230706912,2.01906732732325,
136.368182711602));
#157974=CARTESIAN_POINT('Ctrl Pts',(-142.603632528588,2.16567415476532,
136.310519534441));
#157975=CARTESIAN_POINT('Ctrl Pts',(-142.611030442899,2.31220358960521,
136.252886797221));
#157976=CARTESIAN_POINT('Ctrl Pts',(-142.61842835721,2.45650985026844,136.189369806466));
#157977=CARTESIAN_POINT('Ctrl Pts',(-142.625826271522,2.59809250515853,
136.120171552611));
#157978=CARTESIAN_POINT('Ctrl Pts',(-142.633222956434,2.73965163157933,
136.05098479825));
#157979=CARTESIAN_POINT('Ctrl Pts',(-142.640619641346,2.87848771547634,
135.976118818351));
#157980=CARTESIAN_POINT('Ctrl Pts',(-142.648016326259,3.01412181496487,
135.895824085672));
#157981=CARTESIAN_POINT('Ctrl Pts',(-142.655412683194,3.14974990029569,
135.815532913344));
#157982=CARTESIAN_POINT('Ctrl Pts',(-142.662809040129,3.28217596229204,
135.729813657026));
#157983=CARTESIAN_POINT('Ctrl Pts',(-142.670205397065,3.41094735358215,
135.638961812452));
#157984=CARTESIAN_POINT('Ctrl Pts',(-142.677602886402,3.539738460101,135.548096058228));
#157985=CARTESIAN_POINT('Ctrl Pts',(-142.685000375738,3.66487347675334,
135.452096366306));
#157986=CARTESIAN_POINT('Ctrl Pts',(-142.692397865075,3.78593046539778,
135.351300365756));
#157987=CARTESIAN_POINT('Ctrl Pts',(-142.69979794759,3.90702989038176,135.250469031325));
#157988=CARTESIAN_POINT('Ctrl Pts',(-142.707198030105,4.02404815444621,
135.144838279445));
#157989=CARTESIAN_POINT('Ctrl Pts',(-142.71459811262,4.13659811901385,135.034784540091));
#157990=CARTESIAN_POINT('Ctrl Pts',(-142.722006332286,4.24927184383811,
134.924609785337));
#157991=CARTESIAN_POINT('Ctrl Pts',(-142.729414551953,4.35746718980525,
134.810002591467));
#157992=CARTESIAN_POINT('Ctrl Pts',(-142.736822771619,4.46083497346151,
134.69137514057));
#157993=CARTESIAN_POINT('Ctrl Pts',(-142.744235550921,4.56426637826441,
134.572674676456));
#157994=CARTESIAN_POINT('Ctrl Pts',(-142.751648330223,4.66286406684211,
134.449949315099));
#157995=CARTESIAN_POINT('Ctrl Pts',(-142.759061109526,4.7563208986878,134.323642088436));
#157996=CARTESIAN_POINT('Ctrl Pts',(-142.766484480554,4.84991126603712,
134.197154388084));
#157997=CARTESIAN_POINT('Ctrl Pts',(-142.773907851583,4.93834589672733,
134.067074908652));
#157998=CARTESIAN_POINT('Ctrl Pts',(-142.781331222612,5.02136205430695,
133.933873947473));
#157999=CARTESIAN_POINT('Ctrl Pts',(-142.785267272052,5.06537921299629,
133.863247601751));
#158000=CARTESIAN_POINT('Ctrl Pts',(-142.789203321493,5.10787382247675,
133.791744087645));
#158001=CARTESIAN_POINT('Ctrl Pts',(-142.793139370933,5.14881215909193,
133.719435901823));
#158002=CARTESIAN_POINT('Ctrl Pts',(-142.800562637338,5.22602058431397,
133.583064920012));
#158003=CARTESIAN_POINT('Ctrl Pts',(-142.807985903744,5.29792415084296,
133.443418207619));
#158004=CARTESIAN_POINT('Ctrl Pts',(-142.815409170149,5.36423206739362,
133.3009472653));
#158005=CARTESIAN_POINT('Ctrl Pts',(-142.82282366287,5.43046161349344,133.158644711804));
#158006=CARTESIAN_POINT('Ctrl Pts',(-142.830238155591,5.49110851803365,
133.013524907833));
#158007=CARTESIAN_POINT('Ctrl Pts',(-142.837652648312,5.5459264641699,132.866066274666));
#158008=CARTESIAN_POINT('Ctrl Pts',(-142.845059994666,5.60069157470595,
132.718749767682));
#158009=CARTESIAN_POINT('Ctrl Pts',(-142.852467341019,5.64963878230422,
132.569099266825));
#158010=CARTESIAN_POINT('Ctrl Pts',(-142.859874687373,5.69256876743057,
132.417615523207));
#158011=CARTESIAN_POINT('Ctrl Pts',(-142.867276509049,5.73546673375435,
132.26624476188));
#158012=CARTESIAN_POINT('Ctrl Pts',(-142.874678330724,5.77235631221911,
132.113043837882));
#158013=CARTESIAN_POINT('Ctrl Pts',(-142.882080152399,5.80308721947066,
131.958531006077));
#158014=CARTESIAN_POINT('Ctrl Pts',(-142.889478066711,5.83380190411557,
131.804099740393));
#158015=CARTESIAN_POINT('Ctrl Pts',(-142.896875981022,5.85836431966345,
131.64835831134));
#158016=CARTESIAN_POINT('Ctrl Pts',(-142.904273895333,5.87667475221561,
131.491837467483));
#158017=CARTESIAN_POINT('Ctrl Pts',(-142.911670580245,5.89498214190599,
131.335342634551));
#158018=CARTESIAN_POINT('Ctrl Pts',(-142.919067265158,5.90703956730942,
131.178069014288));
#158019=CARTESIAN_POINT('Ctrl Pts',(-142.92646395007,5.91279887846187,131.020554940711));
#158020=CARTESIAN_POINT('Ctrl Pts',(-142.933860307005,5.91855793424043,
130.863047851472));
#158021=CARTESIAN_POINT('Ctrl Pts',(-142.941256663941,5.91801941740107,
130.705300703166));
#158022=CARTESIAN_POINT('Ctrl Pts',(-142.948653020876,5.91118726991158,
130.547854043507));
#158023=CARTESIAN_POINT('Ctrl Pts',(-142.956050510213,5.90435407640287,
130.390383278363));
#158024=CARTESIAN_POINT('Ctrl Pts',(-142.963447999549,5.89122534983063,
130.23321346644));
#158025=CARTESIAN_POINT('Ctrl Pts',(-142.970845488886,5.87185707922157,
130.076882093006));
#158026=CARTESIAN_POINT('Ctrl Pts',(-142.978245571401,5.8524820190953,129.920495917852));
#158027=CARTESIAN_POINT('Ctrl Pts',(-142.985645653916,5.82686310597789,
129.7649491366));
#158028=CARTESIAN_POINT('Ctrl Pts',(-142.993045736431,5.79510778321126,
129.610770929497));
#158029=CARTESIAN_POINT('Ctrl Pts',(-143.000453956097,5.76331754220268,
129.456423187605));
#158030=CARTESIAN_POINT('Ctrl Pts',(-143.007862175763,5.72537749147001,
129.303447391069));
#158031=CARTESIAN_POINT('Ctrl Pts',(-143.01527039543,5.68144566929237,129.152360112306));
#158032=CARTESIAN_POINT('Ctrl Pts',(-143.022683174732,5.63748680781111,
129.001179841843));
#158033=CARTESIAN_POINT('Ctrl Pts',(-143.030095954034,5.58752894459882,
128.851890758466));
#158034=CARTESIAN_POINT('Ctrl Pts',(-143.037508733336,5.53177879802467,
128.704990737763));
#158035=CARTESIAN_POINT('Ctrl Pts',(-143.044932104365,5.47594899302675,
128.557880819422));
#158036=CARTESIAN_POINT('Ctrl Pts',(-143.052355475393,5.41431052096332,
128.413167124023));
#158037=CARTESIAN_POINT('Ctrl Pts',(-143.059778846422,5.34711704083224,
128.27132490638));
#158038=CARTESIAN_POINT('Ctrl Pts',(-143.063714895863,5.31148944537873,
128.196116759124));
#158039=CARTESIAN_POINT('Ctrl Pts',(-143.067650945304,5.27430088828306,
128.1217154447));
#158040=CARTESIAN_POINT('Ctrl Pts',(-143.071586994745,5.23559413458562,
128.048188521997));
#158041=CARTESIAN_POINT('Ctrl Pts',(-143.079010261151,5.16259440511387,
127.909519040486));
#158042=CARTESIAN_POINT('Ctrl Pts',(-143.086433527556,5.08397130502822,
127.773542074441));
#158043=CARTESIAN_POINT('Ctrl Pts',(-143.093856793961,4.99994751482491,
127.640746321939));
#158044=CARTESIAN_POINT('Ctrl Pts',(-143.101271286683,4.91602303376388,
127.508107522989));
#158045=CARTESIAN_POINT('Ctrl Pts',(-143.108685779404,4.82671076596348,
127.378642765794));
#158046=CARTESIAN_POINT('Ctrl Pts',(-143.116100272125,4.73228008052372,
127.252817882081));
#158047=CARTESIAN_POINT('Ctrl Pts',(-143.123507618478,4.63794041093303,
127.127114273126));
#158048=CARTESIAN_POINT('Ctrl Pts',(-143.130914964832,4.53849236754767,
127.005043849986));
#158049=CARTESIAN_POINT('Ctrl Pts',(-143.138322311186,4.43424950938221,
126.887044974036));
#158050=CARTESIAN_POINT('Ctrl Pts',(-143.145724132861,4.33008439947413,
126.769134106101));
#158051=CARTESIAN_POINT('Ctrl Pts',(-143.153125954537,4.22113184147722,
126.65528901741));
#158052=CARTESIAN_POINT('Ctrl Pts',(-143.160527776212,4.10774662606244,
126.545916275019));
#158053=CARTESIAN_POINT('Ctrl Pts',(-143.167925690523,3.99442126582092,
126.436601269647));
#158054=CARTESIAN_POINT('Ctrl Pts',(-143.175323604835,3.87666817630713,
126.331754167205));
#158055=CARTESIAN_POINT('Ctrl Pts',(-143.182721519146,3.7548799935218,126.231745742382));
#158056=CARTESIAN_POINT('Ctrl Pts',(-143.190118204058,3.63311204972211,
126.131753937145));
#158057=CARTESIAN_POINT('Ctrl Pts',(-143.19751488897,3.50731063172423,126.036599450295));
#158058=CARTESIAN_POINT('Ctrl Pts',(-143.204911573883,3.37790262894944,
125.946613774447));
#158059=CARTESIAN_POINT('Ctrl Pts',(-143.212307930818,3.2485003642611,125.856632088657));
#158060=CARTESIAN_POINT('Ctrl Pts',(-143.219704287754,3.11549213925364,
125.771818971278));
#158061=CARTESIAN_POINT('Ctrl Pts',(-143.227100644689,2.97933486275858,
125.692463285063));
#158062=CARTESIAN_POINT('Ctrl Pts',(-143.234498134026,2.84315674023651,
125.61309544929));
#158063=CARTESIAN_POINT('Ctrl Pts',(-143.241895623362,2.70382892878528,
125.539186896349));
#158064=CARTESIAN_POINT('Ctrl Pts',(-143.249293112699,2.56183389341936,
125.470981045003));
#158065=CARTESIAN_POINT('Ctrl Pts',(-143.256693195214,2.4197890819129,125.402751284202));
#158066=CARTESIAN_POINT('Ctrl Pts',(-143.264093277729,2.27507552121324,
125.340228366664));
#158067=CARTESIAN_POINT('Ctrl Pts',(-143.271493360244,2.12819650139914,
125.283607932113));
#158068=CARTESIAN_POINT('Ctrl Pts',(-143.278901579911,1.9811559730047,125.226925237575));
#158069=CARTESIAN_POINT('Ctrl Pts',(-143.286309799577,1.83194557872065,
125.176158122105));
#158070=CARTESIAN_POINT('Ctrl Pts',(-143.293718019244,1.68108534910109,
125.131452843634));
#158071=CARTESIAN_POINT('Ctrl Pts',(-143.301130798546,1.53013226752743,
125.08672004981));
#158072=CARTESIAN_POINT('Ctrl Pts',(-143.308543577848,1.37752768824008,
125.048056618857));
#158073=CARTESIAN_POINT('Ctrl Pts',(-143.31595635715,1.22380222440171,125.015557746674));
#158074=CARTESIAN_POINT('Ctrl Pts',(-143.323379728179,1.06985711041137,
124.983012438578));
#158075=CARTESIAN_POINT('Ctrl Pts',(-143.330803099207,0.914788280213099,
124.956649343626));
#158076=CARTESIAN_POINT('Ctrl Pts',(-143.338226470236,0.759132688026945,
124.936511938155));
#158077=CARTESIAN_POINT('Ctrl Pts',(-143.342162519677,0.676600358145183,
124.925834602583));
#158078=CARTESIAN_POINT('Ctrl Pts',(-143.346098569118,0.593903101680449,
124.916906661104));
#158079=CARTESIAN_POINT('Ctrl Pts',(-143.350034618558,0.511120873387011,
124.909728651507));
#158080=CARTESIAN_POINT('Ctrl Pts',(-143.357457884964,0.354996174372463,
124.896191149424));
#158081=CARTESIAN_POINT('Ctrl Pts',(-143.364881151369,0.198097195700472,
124.888840118679));
#158082=CARTESIAN_POINT('Ctrl Pts',(-143.372304417774,0.0409554571512921,
124.88775236511));
#158083=CARTESIAN_POINT('Ctrl Pts',(-143.379718910495,-0.116000552913623,
124.886665897176));
#158084=CARTESIAN_POINT('Ctrl Pts',(-143.387133403216,-0.273198382092143,
124.891827973915));
#158085=CARTESIAN_POINT('Ctrl Pts',(-143.394547895937,-0.430100512383416,
124.903263760901));
#158086=CARTESIAN_POINT('Ctrl Pts',(-143.401955242291,-0.586851414494252,
124.914688525644));
#158087=CARTESIAN_POINT('Ctrl Pts',(-143.409362588645,-0.743306815297192,
124.932374935615));
#158088=CARTESIAN_POINT('Ctrl Pts',(-143.416769934999,-0.89892842264511,
124.956296129767));
#158089=CARTESIAN_POINT('Ctrl Pts',(-143.424171756674,-1.054433961527,124.980199482589));
#158090=CARTESIAN_POINT('Ctrl Pts',(-143.431573578349,-1.20910657781373,
125.01032830407));
#158091=CARTESIAN_POINT('Ctrl Pts',(-143.438975400025,-1.36241244210333,
125.046603858193));
#158092=CARTESIAN_POINT('Ctrl Pts',(-143.446373314336,-1.5156373774205,
125.082860262734));
#158093=CARTESIAN_POINT('Ctrl Pts',(-143.453771228647,-1.66749663529066,
125.12525685198));
#158094=CARTESIAN_POINT('Ctrl Pts',(-143.461169142958,-1.81746604311702,
125.173663702919));
#158095=CARTESIAN_POINT('Ctrl Pts',(-143.46856582787,-1.96741052874832,
125.222062509518));
#158096=CARTESIAN_POINT('Ctrl Pts',(-143.475962512783,-2.11546543274709,
125.27646948094));
#158097=CARTESIAN_POINT('Ctrl Pts',(-143.483359197695,-2.26112111683015,
125.33670464288));
#158098=CARTESIAN_POINT('Ctrl Pts',(-143.49075555463,-2.40677034238755,
125.396937133929));
#158099=CARTESIAN_POINT('Ctrl Pts',(-143.498151911566,-2.55002021459294,
125.462997158996));
#158100=CARTESIAN_POINT('Ctrl Pts',(-143.505548268501,-2.69038073464604,
125.534656445115));
#158101=CARTESIAN_POINT('Ctrl Pts',(-143.512945757837,-2.83076274425348,
125.606326702454));
#158102=CARTESIAN_POINT('Ctrl Pts',(-143.520343247174,-2.96825418840066,
125.683597758014));
#158103=CARTESIAN_POINT('Ctrl Pts',(-143.52774073651,-3.10238948786392,
125.766195274101));
#158104=CARTESIAN_POINT('Ctrl Pts',(-143.535140819025,-3.23657180824789,
125.848821744619));
#158105=CARTESIAN_POINT('Ctrl Pts',(-143.54254090154,-3.36739532389419,
125.936778197598));
#158106=CARTESIAN_POINT('Ctrl Pts',(-143.549940984055,-3.49442339698252,
126.029746948889));
#158107=CARTESIAN_POINT('Ctrl Pts',(-143.557349203721,-3.62159115049655,
126.122817928879));
#158108=CARTESIAN_POINT('Ctrl Pts',(-143.564757423388,-3.74495482531704,
126.22091199348));
#158109=CARTESIAN_POINT('Ctrl Pts',(-143.572165643054,-3.86411028128924,
126.32367068224));
#158110=CARTESIAN_POINT('Ctrl Pts',(-143.579578422356,-3.98333907545603,
126.426492617258));
#158111=CARTESIAN_POINT('Ctrl Pts',(-143.586991201658,-4.09835421760054,
126.533984642959));
#158112=CARTESIAN_POINT('Ctrl Pts',(-143.59440398096,-4.20878880734122,
126.645751795171));
#158113=CARTESIAN_POINT('Ctrl Pts',(-143.601827351989,-4.31938119120306,
126.757678645532));
#158114=CARTESIAN_POINT('Ctrl Pts',(-143.609250723018,-4.42537970011683,
126.873892547378));
#158115=CARTESIAN_POINT('Ctrl Pts',(-143.616674094046,-4.52645751933683,
126.993965245936));
#158116=CARTESIAN_POINT('Ctrl Pts',(-143.620610143488,-4.58005140442691,
127.057630671829));
#158117=CARTESIAN_POINT('Ctrl Pts',(-143.624546192929,-4.63226262156781,
127.122380445366));
#158118=CARTESIAN_POINT('Ctrl Pts',(-143.628482242371,-4.68304750080456,
127.188147589036));
#158119=CARTESIAN_POINT('Ctrl Pts',(-143.636113182597,-4.78150570962224,
127.315652375148));
#158120=CARTESIAN_POINT('Ctrl Pts',(-143.643744122823,-4.87490999056476,
127.447384705789));
#158121=CARTESIAN_POINT('Ctrl Pts',(-143.651375063048,-4.96287774080348,
127.582905186812));
#158122=CARTESIAN_POINT('Ctrl Pts',(-143.658797252299,-5.04843905709521,
127.714718387778));
#158123=CARTESIAN_POINT('Ctrl Pts',(-143.666219441551,-5.12885712916795,
127.850114878207));
#158124=CARTESIAN_POINT('Ctrl Pts',(-143.673641630802,-5.20381921518821,
127.988655352781));
#158125=CARTESIAN_POINT('Ctrl Pts',(-143.681056664793,-5.27870903503637,
128.127062269308));
#158126=CARTESIAN_POINT('Ctrl Pts',(-143.688471698784,-5.34815316205252,
128.268606812903));
#158127=CARTESIAN_POINT('Ctrl Pts',(-143.695886732775,-5.41188208523512,
128.412820766756));
#158128=CARTESIAN_POINT('Ctrl Pts',(-143.703296068788,-5.47556203682004,
128.556923901418));
#158129=CARTESIAN_POINT('Ctrl Pts',(-143.7107054048,-5.53353537798816,128.703692024345));
#158130=CARTESIAN_POINT('Ctrl Pts',(-143.718114740812,-5.58557856269081,
128.852632490365));
#158131=CARTESIAN_POINT('Ctrl Pts',(-143.725907246394,-5.64031313089013,
129.0092753273));
#158132=CARTESIAN_POINT('Ctrl Pts',(-143.733699751975,-5.68848768069859,
129.168320795676));
#158133=CARTESIAN_POINT('Ctrl Pts',(-143.741492257557,-5.72989940319255,
129.329171344356));
#158134=CARTESIAN_POINT('Ctrl Pts',(-143.748894865279,-5.7692390909901,
129.48197373909));
#158135=CARTESIAN_POINT('Ctrl Pts',(-143.756297473002,-5.80247610360676,
129.636404580094));
#158136=CARTESIAN_POINT('Ctrl Pts',(-143.763700080724,-5.82948772392865,
129.791936082568));
#158137=CARTESIAN_POINT('Ctrl Pts',(-143.771101448252,-5.85649481886142,
129.947441528088));
#158138=CARTESIAN_POINT('Ctrl Pts',(-143.778502815779,-5.87727853829152,
130.104046901191));
#158139=CARTESIAN_POINT('Ctrl Pts',(-143.785904183306,-5.89176743063363,
130.261215051603));
#158140=CARTESIAN_POINT('Ctrl Pts',(-143.793306662413,-5.90625849899951,
130.418406806418));
#158141=CARTESIAN_POINT('Ctrl Pts',(-143.800709141519,-5.91445282034711,
130.576161137043));
#158142=CARTESIAN_POINT('Ctrl Pts',(-143.808111620626,-5.9163308740846,
130.733936538919));
#158143=CARTESIAN_POINT('Ctrl Pts',(-143.809282683014,-5.91662797969786,
130.758896398477));
#158144=CARTESIAN_POINT('Ctrl Pts',(-143.810453745402,-5.91676711521594,
130.783856783679));
#158145=CARTESIAN_POINT('Ctrl Pts',(-143.81162480779,-5.91674832286034,
130.808815550709));
#158146=CARTESIAN_POINT('',(-145.56162480779,-5.92566626415315,130.806424113553));
#158147=CARTESIAN_POINT('Ctrl Pts',(-143.811626935791,-5.91075733511084,
130.808856347913));
#158148=CARTESIAN_POINT('Ctrl Pts',(-143.843394579256,-5.91545624009792,
131.485236077572));
#158149=CARTESIAN_POINT('Ctrl Pts',(-143.87516222272,-5.80834015743627,
132.160170260916));
#158150=CARTESIAN_POINT('Ctrl Pts',(-143.999745740789,-4.92438460180809,
134.641836647651));
#158151=CARTESIAN_POINT('Ctrl Pts',(-144.185377489997,-1.58782966150643,
137.620250691237));
#158152=CARTESIAN_POINT('Ctrl Pts',(-144.46382511381,4.87614063807827,135.824401753654));
#158153=CARTESIAN_POINT('Ctrl Pts',(-144.742272737623,6.85917590398193,
129.415380254652));
#158154=CARTESIAN_POINT('Ctrl Pts',(-145.020720361436,2.53896360349993,
124.282763853699));
#158155=CARTESIAN_POINT('Ctrl Pts',(-145.29383771816,-3.98706758988356,
125.126705578275));
#158156=CARTESIAN_POINT('Ctrl Pts',(-145.474139200277,-5.91733683117123,
128.955762140162));
#158157=CARTESIAN_POINT('Ctrl Pts',(-145.56162480779,-5.92566626415315,
130.806424113553));
#158158=CARTESIAN_POINT('',(-147.31162480779,-5.91706323075389,130.7989080505));
#158159=CARTESIAN_POINT('Ctrl Pts',(-145.56162480779,-5.92566626415315,
130.806424113553));
#158160=CARTESIAN_POINT('Ctrl Pts',(-145.566955074881,-5.92617375451377,
130.919180061563));
#158161=CARTESIAN_POINT('Ctrl Pts',(-145.572285341971,-5.92323536319911,
131.031909033594));
#158162=CARTESIAN_POINT('Ctrl Pts',(-145.577615609062,-5.91676776598012,
131.144435159557));
#158163=CARTESIAN_POINT('Ctrl Pts',(-145.670431483666,-5.80414757598299,
133.1038511925));
#158164=CARTESIAN_POINT('Ctrl Pts',(-145.856063232874,-3.43871107334941,
136.89967247869));
#158165=CARTESIAN_POINT('Ctrl Pts',(-146.134510856688,3.26945116665681,
136.992110580141));
#158166=CARTESIAN_POINT('Ctrl Pts',(-146.412958480499,6.97314750603267,
131.398308754382));
#158167=CARTESIAN_POINT('Ctrl Pts',(-146.691406104313,4.26886194461242,
125.258697606868));
#158168=CARTESIAN_POINT('Ctrl Pts',(-146.969853728126,-2.35829919844555,
124.215279845482));
#158169=CARTESIAN_POINT('Ctrl Pts',(-147.176593295952,-5.66972392369356,
127.936271574623));
#158170=CARTESIAN_POINT('Ctrl Pts',(-147.290516989173,-5.92122118069781,
130.350705029069));
#158171=CARTESIAN_POINT('Ctrl Pts',(-147.31162480779,-5.91706323075389,
130.7989080505));
#158172=CARTESIAN_POINT('',(-149.061624807827,-5.91674998631937,130.804762972876));
#158173=CARTESIAN_POINT('Ctrl Pts',(-147.31162480779,-5.9167474878674,130.798908341457));
#158174=CARTESIAN_POINT('Ctrl Pts',(-147.318933966831,-5.91689049786105,
130.954101146018));
#158175=CARTESIAN_POINT('Ctrl Pts',(-147.326243125871,-5.91092341403555,
131.10947153384));
#158176=CARTESIAN_POINT('Ctrl Pts',(-147.333552284912,-5.89883117521154,
131.264492477854));
#158177=CARTESIAN_POINT('Ctrl Pts',(-147.340856271384,-5.88674749386184,
131.419403716151));
#158178=CARTESIAN_POINT('Ctrl Pts',(-147.348160257856,-5.86854731442905,
131.573965621545));
#158179=CARTESIAN_POINT('Ctrl Pts',(-147.355464244328,-5.84426764698183,
131.727651597128));
#158180=CARTESIAN_POINT('Ctrl Pts',(-147.362765419609,-5.81999732440011,
131.881278421376));
#158181=CARTESIAN_POINT('Ctrl Pts',(-147.37006659489,-5.78965222652408,
132.03402960761));
#158182=CARTESIAN_POINT('Ctrl Pts',(-147.377367770171,-5.75332115896855,
132.185384224991));
#158183=CARTESIAN_POINT('Ctrl Pts',(-147.384667616045,-5.71699670662247,
132.33671128352));
#158184=CARTESIAN_POINT('Ctrl Pts',(-147.391967461918,-5.67468854189339,
132.486641905648));
#158185=CARTESIAN_POINT('Ctrl Pts',(-147.399267307792,-5.62653641745565,
132.634666194661));
#158186=CARTESIAN_POINT('Ctrl Pts',(-147.406567355322,-5.57838296282187,
132.782694572826));
#158187=CARTESIAN_POINT('Ctrl Pts',(-147.413867402853,-5.52438534596461,
132.928816147779));
#158188=CARTESIAN_POINT('Ctrl Pts',(-147.421167450384,-5.46473285050311,
133.072537293915));
#158189=CARTESIAN_POINT('Ctrl Pts',(-147.428469230619,-5.40506619621038,
133.216292553015));
#158190=CARTESIAN_POINT('Ctrl Pts',(-147.435771010854,-5.33974214007272,
133.35764589509));
#158191=CARTESIAN_POINT('Ctrl Pts',(-147.443072791089,-5.26899752875663,
133.49612502116));
#158192=CARTESIAN_POINT('Ctrl Pts',(-147.4503820623,-5.19818033977865,133.634746214464));
#158193=CARTESIAN_POINT('Ctrl Pts',(-147.45769133351,-5.12193166448401,
133.770486960439));
#158194=CARTESIAN_POINT('Ctrl Pts',(-147.465000604721,-5.04053391802298,
133.902900335523));
#158195=CARTESIAN_POINT('Ctrl Pts',(-147.472313795679,-4.95909252033,134.03538472003));
#158196=CARTESIAN_POINT('Ctrl Pts',(-147.479626986638,-4.8724967655997,
134.164537861454));
#158197=CARTESIAN_POINT('Ctrl Pts',(-147.486940177597,-4.78107111505981,
134.289943718747));
#158198=CARTESIAN_POINT('Ctrl Pts',(-147.494264308553,-4.68950869845622,
134.415537174));
#158199=CARTESIAN_POINT('Ctrl Pts',(-147.501588439509,-4.59310219201926,
134.537371847386));
#158200=CARTESIAN_POINT('Ctrl Pts',(-147.508912570465,-4.49221543116387,
134.655065888359));
#158201=CARTESIAN_POINT('Ctrl Pts',(-147.514858038894,-4.41031915497808,
134.750605715421));
#158202=CARTESIAN_POINT('Ctrl Pts',(-147.520803507323,-4.32547134683653,
134.843417653146));
#158203=CARTESIAN_POINT('Ctrl Pts',(-147.526748975753,-4.23788302417541,
134.933316664305));
#158204=CARTESIAN_POINT('Ctrl Pts',(-147.534172242158,-4.12852386082811,
135.045560857908));
#158205=CARTESIAN_POINT('Ctrl Pts',(-147.541595508563,-4.01453691909021,
135.153627061113));
#158206=CARTESIAN_POINT('Ctrl Pts',(-147.549018774969,-3.89627443970795,
135.257109886611));
#158207=CARTESIAN_POINT('Ctrl Pts',(-147.55643326769,-3.77815173675523,
135.360470404002));
#158208=CARTESIAN_POINT('Ctrl Pts',(-147.563847760411,-3.65576383302849,
135.459258083175));
#158209=CARTESIAN_POINT('Ctrl Pts',(-147.571262253132,-3.52950124668865,
135.55310271544));
#158210=CARTESIAN_POINT('Ctrl Pts',(-147.578669599486,-3.40336035698288,
135.646856896716));
#158211=CARTESIAN_POINT('Ctrl Pts',(-147.586076945839,-3.2733525170426,
135.735677294669));
#158212=CARTESIAN_POINT('Ctrl Pts',(-147.593484292193,-3.13990281966218,
135.819232584583));
#158213=CARTESIAN_POINT('Ctrl Pts',(-147.600886113869,-3.00655265410045,
135.902725555811));
#158214=CARTESIAN_POINT('Ctrl Pts',(-147.608287935544,-2.86976605751078,
135.98096104077));
#158215=CARTESIAN_POINT('Ctrl Pts',(-147.61568975722,-2.72999863336022,
136.053649905113));
#158216=CARTESIAN_POINT('Ctrl Pts',(-147.623087671531,-2.59030499134612,
136.126300397569));
#158217=CARTESIAN_POINT('Ctrl Pts',(-147.630485585842,-2.447633985931,136.193409928893));
#158218=CARTESIAN_POINT('Ctrl Pts',(-147.637883500153,-2.30246734934998,
136.254734427469));
#158219=CARTESIAN_POINT('Ctrl Pts',(-147.645280185066,-2.15732483683016,
136.316048735026));
#158220=CARTESIAN_POINT('Ctrl Pts',(-147.652676869978,-2.00968785979474,
136.37157977274));
#158221=CARTESIAN_POINT('Ctrl Pts',(-147.66007355489,-1.86005984450871,
136.421130858313));
#158222=CARTESIAN_POINT('Ctrl Pts',(-147.667469911825,-1.71043846388568,
136.47067974674));
#158223=CARTESIAN_POINT('Ctrl Pts',(-147.674866268761,-1.55882657492322,
136.514249092895));
#158224=CARTESIAN_POINT('Ctrl Pts',(-147.682262625696,-1.40574428777643,
136.551691612026));
#158225=CARTESIAN_POINT('Ctrl Pts',(-147.689660115033,-1.25263856334024,
136.589139863703));
#158226=CARTESIAN_POINT('Ctrl Pts',(-147.697057604369,-1.09806235510469,
136.620459331913));
#158227=CARTESIAN_POINT('Ctrl Pts',(-147.704455093706,-0.942547378665527,
136.645553560918));
#158228=CARTESIAN_POINT('Ctrl Pts',(-147.711855176221,-0.786977886693119,
136.670656586667));
#158229=CARTESIAN_POINT('Ctrl Pts',(-147.719255258736,-0.630469339614789,
136.689529968942));
#158230=CARTESIAN_POINT('Ctrl Pts',(-147.726655341251,-0.473559859136847,
136.702128977066));
#158231=CARTESIAN_POINT('Ctrl Pts',(-147.734063560917,-0.316477840554209,
136.714741839094));
#158232=CARTESIAN_POINT('Ctrl Pts',(-147.741471780584,-0.158994380459275,
136.721066518681));
#158233=CARTESIAN_POINT('Ctrl Pts',(-147.74888000025,-0.00164963514046322,
136.721110387601));
#158234=CARTESIAN_POINT('Ctrl Pts',(-147.756292779552,0.155791953244103,
136.721154283521));
#158235=CARTESIAN_POINT('Ctrl Pts',(-147.763705558854,0.313094284589634,
136.714909680587));
#158236=CARTESIAN_POINT('Ctrl Pts',(-147.771118338156,0.469721549545526,
136.702435916203));
#158237=CARTESIAN_POINT('Ctrl Pts',(-147.778541709185,0.626572610882453,
136.689944328719));
#158238=CARTESIAN_POINT('Ctrl Pts',(-147.785965080214,0.782746309716429,
136.671205847807));
#158239=CARTESIAN_POINT('Ctrl Pts',(-147.793388451242,0.93771543736235,
136.646331202996));
#158240=CARTESIAN_POINT('Ctrl Pts',(-147.797324500683,1.01988378727759,
136.633142069458));
#158241=CARTESIAN_POINT('Ctrl Pts',(-147.801260550124,1.10171370423964,
136.618228684312));
#158242=CARTESIAN_POINT('Ctrl Pts',(-147.805196599565,1.18312836961951,
136.60161322751));
#158243=CARTESIAN_POINT('Ctrl Pts',(-147.812619865971,1.33667388765318,
136.570276994533));
#158244=CARTESIAN_POINT('Ctrl Pts',(-147.820043132376,1.48920577129814,
136.532788974667));
#158245=CARTESIAN_POINT('Ctrl Pts',(-147.827466398781,1.64019256200267,
136.489226396285));
#158246=CARTESIAN_POINT('Ctrl Pts',(-147.834880891502,1.79100089885968,
136.445715305253));
#158247=CARTESIAN_POINT('Ctrl Pts',(-147.842295384223,1.9402674226153,136.396144049259));
#158248=CARTESIAN_POINT('Ctrl Pts',(-147.849709876944,2.08746958160983,
136.34064107545));
#158249=CARTESIAN_POINT('Ctrl Pts',(-147.857117223298,2.23452986162189,
136.285191597498));
#158250=CARTESIAN_POINT('Ctrl Pts',(-147.864524569652,2.37952939105012,
136.223821914395));
#158251=CARTESIAN_POINT('Ctrl Pts',(-147.871931916006,2.52195964398813,
136.156710579648));
#158252=CARTESIAN_POINT('Ctrl Pts',(-147.879333737681,2.66428366706951,
136.089649299065));
#158253=CARTESIAN_POINT('Ctrl Pts',(-147.886735559357,2.80404189296403,
136.016855051986));
#158254=CARTESIAN_POINT('Ctrl Pts',(-147.894137381032,2.94074479995316,
135.938554866331));
#158255=CARTESIAN_POINT('Ctrl Pts',(-147.901535295343,3.07737554254216,
135.860296014734));
#158256=CARTESIAN_POINT('Ctrl Pts',(-147.908933209655,3.21095385524653,
135.776537198147));
#158257=CARTESIAN_POINT('Ctrl Pts',(-147.916331123966,3.3410140056634,135.687551784873));
#158258=CARTESIAN_POINT('Ctrl Pts',(-147.923727808878,3.47105254244226,
135.59858115936));
#158259=CARTESIAN_POINT('Ctrl Pts',(-147.93112449379,3.59757376951305,135.504385871589));
#158260=CARTESIAN_POINT('Ctrl Pts',(-147.938521178703,3.72014009829545,
135.405283156748));
#158261=CARTESIAN_POINT('Ctrl Pts',(-147.945917535638,3.8427009923584,135.306184836226));
#158262=CARTESIAN_POINT('Ctrl Pts',(-147.953313892573,3.96130704653665,
135.202179756007));
#158263=CARTESIAN_POINT('Ctrl Pts',(-147.960710249509,4.07555321375501,
135.09362588849));
#158264=CARTESIAN_POINT('Ctrl Pts',(-147.968107738845,4.18981687235322,
134.985055401098));
#158265=CARTESIAN_POINT('Ctrl Pts',(-147.975505228182,4.2997190442562,134.871934996872));
#158266=CARTESIAN_POINT('Ctrl Pts',(-147.982902717519,4.40489117325363,
134.754659886519));
#158267=CARTESIAN_POINT('Ctrl Pts',(-147.990302800034,4.5101001701777,134.637343665558));
#158268=CARTESIAN_POINT('Ctrl Pts',(-147.997702882548,4.61057557383729,
134.515870116477));
#158269=CARTESIAN_POINT('Ctrl Pts',(-148.005102965063,4.70598888311962,
134.390667798282));
#158270=CARTESIAN_POINT('Ctrl Pts',(-148.01251118473,4.80150710914464,134.265327807267));
#158271=CARTESIAN_POINT('Ctrl Pts',(-148.019919404396,4.89195189813434,
134.136251155931));
#158272=CARTESIAN_POINT('Ctrl Pts',(-148.027327624063,4.97703748450313,
134.003896277682));
#158273=CARTESIAN_POINT('Ctrl Pts',(-148.034740403365,5.0621754396306,133.871459937213));
#158274=CARTESIAN_POINT('Ctrl Pts',(-148.042153182667,5.14194743074158,
133.7357416704));
#158275=CARTESIAN_POINT('Ctrl Pts',(-148.049565961969,5.21611376203199,
133.59722434214));
#158276=CARTESIAN_POINT('Ctrl Pts',(-148.056989332998,5.29038606565472,
133.458509093825));
#158277=CARTESIAN_POINT('Ctrl Pts',(-148.064412704026,5.35903654993662,
133.316987131281));
#158278=CARTESIAN_POINT('Ctrl Pts',(-148.071836075055,5.42187340559484,
133.173161862121));
#158279=CARTESIAN_POINT('Ctrl Pts',(-148.075772124496,5.45519101421609,
133.096902253368));
#158280=CARTESIAN_POINT('Ctrl Pts',(-148.079708173937,5.486875029849,133.019995377734));
#158281=CARTESIAN_POINT('Ctrl Pts',(-148.083644223378,5.51690259076839,
132.94251785371));
#158282=CARTESIAN_POINT('Ctrl Pts',(-148.091067489784,5.57353363353146,
132.796397661398));
#158283=CARTESIAN_POINT('Ctrl Pts',(-148.098490756189,5.62444110961093,
132.647805077326));
#158284=CARTESIAN_POINT('Ctrl Pts',(-148.105914022594,5.66940272709543,
132.497228976448));
#158285=CARTESIAN_POINT('Ctrl Pts',(-148.113328515315,5.71431120368202,
132.346830844015));
#158286=CARTESIAN_POINT('Ctrl Pts',(-148.120743008036,5.75328770421019,
132.194454215421));
#158287=CARTESIAN_POINT('Ctrl Pts',(-148.128157500757,5.78615784296867,
132.040608156998));
#158288=CARTESIAN_POINT('Ctrl Pts',(-148.135564847111,5.81899630024998,
131.886910381198));
#158289=CARTESIAN_POINT('Ctrl Pts',(-148.142972193465,5.84574003524237,
131.731746357735));
#158290=CARTESIAN_POINT('Ctrl Pts',(-148.150379539819,5.86626439939253,
131.575640436386));
#158291=CARTESIAN_POINT('Ctrl Pts',(-148.157781361494,5.88677345569757,
131.419650944724));
#158292=CARTESIAN_POINT('Ctrl Pts',(-148.16518318317,5.90107232886947,131.262721322474));
#158293=CARTESIAN_POINT('Ctrl Pts',(-148.172585004845,5.9090874254831,131.105386132261));
#158294=CARTESIAN_POINT('Ctrl Pts',(-148.179982919156,5.91709829098963,
130.94813399807));
#158295=CARTESIAN_POINT('Ctrl Pts',(-148.187380833468,5.91883196727027,
130.790477094168));
#158296=CARTESIAN_POINT('Ctrl Pts',(-148.194778747779,5.91426670708034,
130.632955016663));
#158297=CARTESIAN_POINT('Ctrl Pts',(-148.202175432691,5.90970220555385,
130.475459116469));
#158298=CARTESIAN_POINT('Ctrl Pts',(-148.209572117603,5.89884085588715,
130.318098370978));
#158299=CARTESIAN_POINT('Ctrl Pts',(-148.216968802516,5.88171302971251,
130.161412409224));
#158300=CARTESIAN_POINT('Ctrl Pts',(-148.224365159451,5.86458596300368,
130.00473339509));
#158301=CARTESIAN_POINT('Ctrl Pts',(-148.231761516386,5.84119301283541,
129.848729476288));
#158302=CARTESIAN_POINT('Ctrl Pts',(-148.239157873322,5.81161641368678,
129.693934923219));
#158303=CARTESIAN_POINT('Ctrl Pts',(-148.246555362658,5.78203528628523,
129.539116670708));
#158304=CARTESIAN_POINT('Ctrl Pts',(-148.253952851995,5.74626869489624,
129.38550851929));
#158305=CARTESIAN_POINT('Ctrl Pts',(-148.261350341332,5.70444992784726,
129.233634166785));
#158306=CARTESIAN_POINT('Ctrl Pts',(-148.268750423847,5.66261650129438,
129.081706574961));
#158307=CARTESIAN_POINT('Ctrl Pts',(-148.276150506362,5.61472677406775,
128.931514351815));
#158308=CARTESIAN_POINT('Ctrl Pts',(-148.283550588876,5.56096374212256,
128.783565521249));
#158309=CARTESIAN_POINT('Ctrl Pts',(-148.290958808543,5.50714159219669,
128.635454005734));
#158310=CARTESIAN_POINT('Ctrl Pts',(-148.298367028209,5.44743336747213,
128.489591160308));
#158311=CARTESIAN_POINT('Ctrl Pts',(-148.305775247876,5.38207029767888,
128.346465202105));
#158312=CARTESIAN_POINT('Ctrl Pts',(-148.313188027178,5.31666699800662,
128.203251152263));
#158313=CARTESIAN_POINT('Ctrl Pts',(-148.32060080648,5.2456020861296,128.062777678566));
#158314=CARTESIAN_POINT('Ctrl Pts',(-148.328013585782,5.16915224852444,
127.925507444152));
#158315=CARTESIAN_POINT('Ctrl Pts',(-148.335436956811,5.09259317580628,
127.788041071591));
#158316=CARTESIAN_POINT('Ctrl Pts',(-148.34286032784,5.01063400424249,127.65378739726));
#158317=CARTESIAN_POINT('Ctrl Pts',(-148.350283698868,4.92359458731299,
127.523179899854));
#158318=CARTESIAN_POINT('Ctrl Pts',(-148.354219748309,4.87744419997718,
127.453928670849));
#158319=CARTESIAN_POINT('Ctrl Pts',(-148.35815579775,4.82986625176899,127.385701966331));
#158320=CARTESIAN_POINT('Ctrl Pts',(-148.36209184719,4.78091284667562,127.318560434682));
#158321=CARTESIAN_POINT('Ctrl Pts',(-148.369515113596,4.68858825244866,
127.191933601403));
#158322=CARTESIAN_POINT('Ctrl Pts',(-148.376938380001,4.59108983741368,
127.068785778736));
#158323=CARTESIAN_POINT('Ctrl Pts',(-148.384361646406,4.48870875170665,
126.949568236016));
#158324=CARTESIAN_POINT('Ctrl Pts',(-148.391776139128,4.38644867194041,
126.830491598532));
#158325=CARTESIAN_POINT('Ctrl Pts',(-148.399190631849,4.27931764936329,
126.715336275004));
#158326=CARTESIAN_POINT('Ctrl Pts',(-148.40660512457,4.16764971616188,126.604524143859));
#158327=CARTESIAN_POINT('Ctrl Pts',(-148.414012470923,4.05608941271872,
126.493818817619));
#158328=CARTESIAN_POINT('Ctrl Pts',(-148.421419817277,3.94000116732137,
126.387448611174));
#158329=CARTESIAN_POINT('Ctrl Pts',(-148.428827163631,3.81975875470066,
126.285801818747));
#158330=CARTESIAN_POINT('Ctrl Pts',(-148.436228985306,3.69960602340812,
126.184230838332));
#158331=CARTESIAN_POINT('Ctrl Pts',(-148.443630806982,3.57530557795129,
126.087376497323));
#158332=CARTESIAN_POINT('Ctrl Pts',(-148.451032628657,3.44726738196088,
125.995589656107));
#158333=CARTESIAN_POINT('Ctrl Pts',(-148.458430542969,3.31929677633676,
125.90385126845));
#158334=CARTESIAN_POINT('Ctrl Pts',(-148.46582845728,3.1875926523864,125.817175269952));
#158335=CARTESIAN_POINT('Ctrl Pts',(-148.473226371591,3.05259723267876,
125.735871622062));
#158336=CARTESIAN_POINT('Ctrl Pts',(-148.480623056503,2.91762424676138,
125.654581485364));
#158337=CARTESIAN_POINT('Ctrl Pts',(-148.488019741416,2.77936137009441,
125.57866211976));
#158338=CARTESIAN_POINT('Ctrl Pts',(-148.495416426328,2.63827902447642,
125.508379655411));
#158339=CARTESIAN_POINT('Ctrl Pts',(-148.502812783263,2.49720293459748,
125.43810030746));
#158340=CARTESIAN_POINT('Ctrl Pts',(-148.510209140199,2.35330795847815,
125.373457530239));
#158341=CARTESIAN_POINT('Ctrl Pts',(-148.517605497134,2.20708804268295,
125.314670923754));
#158342=CARTESIAN_POINT('Ctrl Pts',(-148.525002986471,2.06084574024578,
125.25587531689));
#158343=CARTESIAN_POINT('Ctrl Pts',(-148.532400475807,1.91227813575677,
125.202937805259));
#158344=CARTESIAN_POINT('Ctrl Pts',(-148.539797965144,1.76189787661972,
125.15602932108));
#158345=CARTESIAN_POINT('Ctrl Pts',(-148.547198047659,1.61146490191573,
125.109104393205));
#158346=CARTESIAN_POINT('Ctrl Pts',(-148.554598130174,1.45921836358121,
125.068212811768));
#158347=CARTESIAN_POINT('Ctrl Pts',(-148.561998212689,1.30568459029637,
125.03347521642));
#158348=CARTESIAN_POINT('Ctrl Pts',(-148.569406432355,1.15198199084393,
124.998699423514));
#158349=CARTESIAN_POINT('Ctrl Pts',(-148.576814652022,0.996989694018722,
124.970091213148));
#158350=CARTESIAN_POINT('Ctrl Pts',(-148.584222871688,0.841243436040651,
124.947719938489));
#158351=CARTESIAN_POINT('Ctrl Pts',(-148.59163565099,0.685401318839116,
124.925334894684));
#158352=CARTESIAN_POINT('Ctrl Pts',(-148.599048430293,0.528804686275663,
124.909194473919));
#158353=CARTESIAN_POINT('Ctrl Pts',(-148.606461209595,0.371992345752456,
124.899315972756));
#158354=CARTESIAN_POINT('Ctrl Pts',(-148.613884580623,0.21495594440401,
124.889423356727));
#158355=CARTESIAN_POINT('Ctrl Pts',(-148.621307951652,0.0577035917347928,
124.885810538663));
#158356=CARTESIAN_POINT('Ctrl Pts',(-148.628731322681,-0.0992271257348289,
124.888442722597));
#158357=CARTESIAN_POINT('Ctrl Pts',(-148.632667372122,-0.182435557639672,
124.889838369677));
#158358=CARTESIAN_POINT('Ctrl Pts',(-148.636603421563,-0.265553659599762,
124.892988844659));
#158359=CARTESIAN_POINT('Ctrl Pts',(-148.640539471003,-0.348502242934304,
124.897883092918));
#158360=CARTESIAN_POINT('Ctrl Pts',(-148.647962737409,-0.504940682363872,
124.90711349239));
#158361=CARTESIAN_POINT('Ctrl Pts',(-148.655386003814,-0.661248708158524,
124.922577264053));
#158362=CARTESIAN_POINT('Ctrl Pts',(-148.66280927022,-0.816889280886414,
124.944273377151));
#158363=CARTESIAN_POINT('Ctrl Pts',(-148.670223762941,-0.972345899383371,
124.965943847245));
#158364=CARTESIAN_POINT('Ctrl Pts',(-148.677638255662,-1.12713626895924,
124.993831945456));
#158365=CARTESIAN_POINT('Ctrl Pts',(-148.685052748383,-1.2807248987907,
125.027884676638));
#158366=CARTESIAN_POINT('Ctrl Pts',(-148.692460094737,-1.43416549411733,
125.061904586516));
#158367=CARTESIAN_POINT('Ctrl Pts',(-148.69986744109,-1.58640629360985,
125.102077220338));
#158368=CARTESIAN_POINT('Ctrl Pts',(-148.707274787444,-1.73691857997097,
125.14829799335));
#158369=CARTESIAN_POINT('Ctrl Pts',(-148.714676609119,-1.88731860858998,
125.194484293166));
#158370=CARTESIAN_POINT('Ctrl Pts',(-148.722078430795,-2.03599233571464,
125.246709641185));
#158371=CARTESIAN_POINT('Ctrl Pts',(-148.72948025247,-2.18242297720716,
125.304818772007));
#158372=CARTESIAN_POINT('Ctrl Pts',(-148.736878166782,-2.32877631910385,
125.36289722747));
#158373=CARTESIAN_POINT('Ctrl Pts',(-148.744276081093,-2.47288858747791,
125.426853142636));
#158374=CARTESIAN_POINT('Ctrl Pts',(-148.751673995404,-2.61425997088384,
125.496482004868));
#158375=CARTESIAN_POINT('Ctrl Pts',(-148.759070680316,-2.7556078609312,
125.566099296047));
#158376=CARTESIAN_POINT('Ctrl Pts',(-148.766467365229,-2.89421543545877,
125.641387498452));
#158377=CARTESIAN_POINT('Ctrl Pts',(-148.773864050141,-3.02960451715323,
125.722094682755));
#158378=CARTESIAN_POINT('Ctrl Pts',(-148.781260407076,-3.16498759555432,
125.802798288416));
#158379=CARTESIAN_POINT('Ctrl Pts',(-148.788656764012,-3.29715214423205,
125.888920207067));
#158380=CARTESIAN_POINT('Ctrl Pts',(-148.796053120947,-3.42564641729864,
125.980163566641));
#158381=CARTESIAN_POINT('Ctrl Pts',(-148.803450610284,-3.55416036316647,
126.071420895807));
#158382=CARTESIAN_POINT('Ctrl Pts',(-148.81084809962,-3.67900261016223,
126.16780101101));
#158383=CARTESIAN_POINT('Ctrl Pts',(-148.818245588957,-3.79975224972568,
126.268965000511));
#158384=CARTESIAN_POINT('Ctrl Pts',(-148.825645671472,-3.92054421788826,
126.370164452891));
#158385=CARTESIAN_POINT('Ctrl Pts',(-148.833045753987,-4.03724043625919,
126.47615087884));
#158386=CARTESIAN_POINT('Ctrl Pts',(-148.840445836502,-4.14945491377776,
126.586546671809));
#158387=CARTESIAN_POINT('Ctrl Pts',(-148.847854056168,-4.26179278265012,
126.697063856301));
#158388=CARTESIAN_POINT('Ctrl Pts',(-148.855262275835,-4.36963880258899,
126.811999828733));
#158389=CARTESIAN_POINT('Ctrl Pts',(-148.862670495502,-4.47264504629845,
126.930941346131));
#158390=CARTESIAN_POINT('Ctrl Pts',(-148.870083274804,-4.57571468863245,
127.049956070049));
#158391=CARTESIAN_POINT('Ctrl Pts',(-148.877496054106,-4.67393838672805,
127.172980960398));
#158392=CARTESIAN_POINT('Ctrl Pts',(-148.884908833408,-4.76701034993793,
127.299572052462));
#158393=CARTESIAN_POINT('Ctrl Pts',(-148.892332204437,-4.86021529873281,
127.426344023814));
#158394=CARTESIAN_POINT('Ctrl Pts',(-148.899755575465,-4.94825360260969,
127.556692065321));
#158395=CARTESIAN_POINT('Ctrl Pts',(-148.907178946494,-5.03086395775739,
127.690145082148));
#158396=CARTESIAN_POINT('Ctrl Pts',(-148.911114995935,-5.07466595026532,
127.760905073831));
#158397=CARTESIAN_POINT('Ctrl Pts',(-148.915051045376,-5.11694273081757,
127.83253759572));
#158398=CARTESIAN_POINT('Ctrl Pts',(-148.918987094816,-5.15766079656884,
127.904970048837));
#158399=CARTESIAN_POINT('Ctrl Pts',(-148.926751505812,-5.23798290689435,
128.047853247807));
#158400=CARTESIAN_POINT('Ctrl Pts',(-148.934515916807,-5.31246115629263,
128.194249487309));
#158401=CARTESIAN_POINT('Ctrl Pts',(-148.942280327803,-5.38078957262255,
128.343662721103));
#158402=CARTESIAN_POINT('Ctrl Pts',(-148.950032457311,-5.44900990933353,
128.492839618008));
#158403=CARTESIAN_POINT('Ctrl Pts',(-148.957784586819,-5.51109966585383,
128.645023705493));
#158404=CARTESIAN_POINT('Ctrl Pts',(-148.965536716327,-5.56679783573118,
128.799692959674));
#158405=CARTESIAN_POINT('Ctrl Pts',(-148.973544057282,-5.62432967086496,
128.959454152033));
#158406=CARTESIAN_POINT('Ctrl Pts',(-148.981551398237,-5.67504168273002,
129.121866666269));
#158407=CARTESIAN_POINT('Ctrl Pts',(-148.989558739193,-5.71869808140008,
129.286328069729));
#158408=CARTESIAN_POINT('Ctrl Pts',(-148.997284861167,-5.76082126098831,
129.445013564739));
#158409=CARTESIAN_POINT('Ctrl Pts',(-149.005010983141,-5.79637585996302,
129.60560613198));
#158410=CARTESIAN_POINT('Ctrl Pts',(-149.012737105116,-5.82519898902617,
129.767544674041));
#158411=CARTESIAN_POINT('Ctrl Pts',(-149.020454611823,-5.85398997790732,
129.929302641181));
#158412=CARTESIAN_POINT('Ctrl Pts',(-149.028172118529,-5.87606439770469,
130.092403274386));
#158413=CARTESIAN_POINT('Ctrl Pts',(-149.035889625236,-5.89130968835139,
130.256272377921));
#158414=CARTESIAN_POINT('Ctrl Pts',(-149.043597068162,-5.90653509883906,
130.41992779292));
#158415=CARTESIAN_POINT('Ctrl Pts',(-149.051304511088,-5.91494910876179,
130.584349357764));
#158416=CARTESIAN_POINT('Ctrl Pts',(-149.059011954014,-5.91649057852451,
130.748954871197));
#158417=CARTESIAN_POINT('Ctrl Pts',(-149.059882905273,-5.91666476664925,
130.767555512222));
#158418=CARTESIAN_POINT('Ctrl Pts',(-149.060753856532,-5.91675125147269,
130.78615849435));
#158419=CARTESIAN_POINT('Ctrl Pts',(-149.06162480779,-5.91674998631942,
130.804762972079));
#158420=CARTESIAN_POINT('',(-150.81162480779,-5.91699367364741,130.809674885172));
#158421=CARTESIAN_POINT('Ctrl Pts',(-149.061624807827,-5.91674998631937,
130.804762972876));
#158422=CARTESIAN_POINT('Ctrl Pts',(-149.069413580783,-5.91673867224068,
130.971139738019));
#158423=CARTESIAN_POINT('Ctrl Pts',(-149.077202353739,-5.90970539075821,
131.137365971676));
#158424=CARTESIAN_POINT('Ctrl Pts',(-149.084991126695,-5.89571383838781,
131.302847225553));
#158425=CARTESIAN_POINT('Ctrl Pts',(-149.09279109274,-5.88170217903905,
131.46856628921));
#158426=CARTESIAN_POINT('Ctrl Pts',(-149.100591058784,-5.86071231162993,
131.633537926564));
#158427=CARTESIAN_POINT('Ctrl Pts',(-149.108391024829,-5.83285932808322,
131.797176119708));
#158428=CARTESIAN_POINT('Ctrl Pts',(-149.116210437207,-5.80493690341401,
131.96122228422));
#158429=CARTESIAN_POINT('Ctrl Pts',(-149.124029849585,-5.77011719447778,
132.123928048353));
#158430=CARTESIAN_POINT('Ctrl Pts',(-149.131849261963,-5.72856621314113,
132.284718582437));
#158431=CARTESIAN_POINT('Ctrl Pts',(-149.139678789375,-5.68696148229353,
132.445717111912));
#158432=CARTESIAN_POINT('Ctrl Pts',(-149.147508316787,-5.6386081857672,
132.604795168376));
#158433=CARTESIAN_POINT('Ctrl Pts',(-149.155337844199,-5.58372137006321,
132.761395677037));
#158434=CARTESIAN_POINT('Ctrl Pts',(-149.163185809046,-5.52870530363394,
132.918364957854));
#158435=CARTESIAN_POINT('Ctrl Pts',(-149.171033773893,-5.46712506161874,
133.072844732718));
#158436=CARTESIAN_POINT('Ctrl Pts',(-149.17888173874,-5.39924367833758,
133.224298274703));
#158437=CARTESIAN_POINT('Ctrl Pts',(-149.18506606537,-5.34575202100989,
133.343646180968));
#158438=CARTESIAN_POINT('Ctrl Pts',(-149.191250392,-5.28834849034848,133.461115324402));
#158439=CARTESIAN_POINT('Ctrl Pts',(-149.19743471863,-5.22718104389468,
133.576455294313));
#158440=CARTESIAN_POINT('Ctrl Pts',(-149.204857985035,-5.15375959035101,
133.714901947451));
#158441=CARTESIAN_POINT('Ctrl Pts',(-149.212281251441,-5.07472298733138,
133.850638981989));
#158442=CARTESIAN_POINT('Ctrl Pts',(-149.219704517846,-4.99029540172941,
133.983178379876));
#158443=CARTESIAN_POINT('Ctrl Pts',(-149.227119010567,-4.90596760252235,
134.115561127201));
#158444=CARTESIAN_POINT('Ctrl Pts',(-149.234533503288,-4.81626170222304,
134.244753448903));
#158445=CARTESIAN_POINT('Ctrl Pts',(-149.241947996009,-4.7214484865153,
134.370290335281));
#158446=CARTESIAN_POINT('Ctrl Pts',(-149.249355342363,-4.62672665535452,
134.495706224481));
#158447=CARTESIAN_POINT('Ctrl Pts',(-149.256762688717,-4.5269075322286,
134.617473396564));
#158448=CARTESIAN_POINT('Ctrl Pts',(-149.264170035071,-4.42230600892101,
134.735154446548));
#158449=CARTESIAN_POINT('Ctrl Pts',(-149.271571856746,-4.31778250137589,
134.852747725565));
#158450=CARTESIAN_POINT('Ctrl Pts',(-149.278973678421,-4.20848394275051,
134.966260672825));
#158451=CARTESIAN_POINT('Ctrl Pts',(-149.286375500097,-4.0947663595227,
135.075287803017));
#158452=CARTESIAN_POINT('Ctrl Pts',(-149.293773414408,-3.98110880692223,
135.184257378635));
#158453=CARTESIAN_POINT('Ctrl Pts',(-149.301171328719,-3.863037144318,135.288745595534));
#158454=CARTESIAN_POINT('Ctrl Pts',(-149.308569243031,-3.74094513440269,
135.38838287579));
#158455=CARTESIAN_POINT('Ctrl Pts',(-149.315965927943,-3.61887341396427,
135.488003598137));
#158456=CARTESIAN_POINT('Ctrl Pts',(-149.323362612855,-3.49278296114364,
135.582774747995));
#158457=CARTESIAN_POINT('Ctrl Pts',(-149.330759297767,-3.36310167233426,
135.67236613359));
#158458=CARTESIAN_POINT('Ctrl Pts',(-149.338155654703,-3.23342613372912,
135.761953546609));
#158459=CARTESIAN_POINT('Ctrl Pts',(-149.345552011638,-3.10016038285177,
135.846361439856));
#158460=CARTESIAN_POINT('Ctrl Pts',(-149.352948368573,-2.96376220561619,
135.925302342587));
#158461=CARTESIAN_POINT('Ctrl Pts',(-149.36034585791,-2.82734314547147,
136.004255331372));
#158462=CARTESIAN_POINT('Ctrl Pts',(-149.367743347247,-2.68779102716578,
136.077739476041));
#158463=CARTESIAN_POINT('Ctrl Pts',(-149.375140836583,-2.54558905436183,
136.145512827419));
#158464=CARTESIAN_POINT('Ctrl Pts',(-149.382540919098,-2.40333723287655,
136.213309936639));
#158465=CARTESIAN_POINT('Ctrl Pts',(-149.389941001613,-2.2584340442274,
136.275392106275));
#158466=CARTESIAN_POINT('Ctrl Pts',(-149.397341084128,-2.11138337162196,
136.331565229351));
#158467=CARTESIAN_POINT('Ctrl Pts',(-149.404749303795,-1.96417100168503,
136.387800120551));
#158468=CARTESIAN_POINT('Ctrl Pts',(-149.412157523461,-1.81480678089696,
136.438112855756));
#158469=CARTESIAN_POINT('Ctrl Pts',(-149.419565743127,-1.66381118256195,
136.482358760511));
#158470=CARTESIAN_POINT('Ctrl Pts',(-149.426978522429,-1.51272264895524,
136.526631897881));
#158471=CARTESIAN_POINT('Ctrl Pts',(-149.434391301732,-1.36000109833726,
136.564830673902));
#158472=CARTESIAN_POINT('Ctrl Pts',(-149.441804081034,-1.20617743115649,
136.59686150812));
#158473=CARTESIAN_POINT('Ctrl Pts',(-149.449227452062,-1.05213397350665,
136.628938109496));
#158474=CARTESIAN_POINT('Ctrl Pts',(-149.456650823091,-0.896985621384072,
136.654829106158));
#158475=CARTESIAN_POINT('Ctrl Pts',(-149.46407419412,-0.741269458848689,
136.674492656275));
#158476=CARTESIAN_POINT('Ctrl Pts',(-149.468010243561,-0.6587050131144,
136.684918742367));
#158477=CARTESIAN_POINT('Ctrl Pts',(-149.471946293001,-0.575980966114923,
136.693594940491));
#158478=CARTESIAN_POINT('Ctrl Pts',(-149.475882342442,-0.49317727387102,
136.700520956213));
#158479=CARTESIAN_POINT('Ctrl Pts',(-149.483305608848,-0.337012094513541,
136.713583205712));
#158480=CARTESIAN_POINT('Ctrl Pts',(-149.490728875253,-0.18009146857571,
136.720456655888));
#158481=CARTESIAN_POINT('Ctrl Pts',(-149.498152141658,-0.0229471471463872,
136.72106611902));
#158482=CARTESIAN_POINT('Ctrl Pts',(-149.505566634379,0.13401144274503,
136.721674861818));
#158483=CARTESIAN_POINT('Ctrl Pts',(-149.5129811271,0.291192832209383,136.71603435287));
#158484=CARTESIAN_POINT('Ctrl Pts',(-149.520395619821,0.448059429140211,
136.704121062742));
#158485=CARTESIAN_POINT('Ctrl Pts',(-149.527802966175,0.604774832138994,
136.692219255091));
#158486=CARTESIAN_POINT('Ctrl Pts',(-149.535210312529,0.761175676904451,
136.674056730619));
#158487=CARTESIAN_POINT('Ctrl Pts',(-149.542617658883,0.916723755538576,
136.649661988627));
#158488=CARTESIAN_POINT('Ctrl Pts',(-149.550019480558,1.07215582054716,
136.625285441154));
#158489=CARTESIAN_POINT('Ctrl Pts',(-149.557421302234,1.22673601863348,
136.594685988989));
#158490=CARTESIAN_POINT('Ctrl Pts',(-149.564823123909,1.37993076251357,
136.557943992574));
#158491=CARTESIAN_POINT('Ctrl Pts',(-149.57222103822,1.53304463608083,136.521221391973));
#158492=CARTESIAN_POINT('Ctrl Pts',(-149.579618952532,1.68477414991668,
136.478362791761));
#158493=CARTESIAN_POINT('Ctrl Pts',(-149.587016866843,1.83459552929319,
136.429499709748));
#158494=CARTESIAN_POINT('Ctrl Pts',(-149.594413551755,1.98439201107428,
136.380644747893));
#158495=CARTESIAN_POINT('Ctrl Pts',(-149.601810236668,2.13228063318821,
136.32578740028));
#158496=CARTESIAN_POINT('Ctrl Pts',(-149.60920692158,2.27775230749229,136.265109191545));
#158497=CARTESIAN_POINT('Ctrl Pts',(-149.616603278515,2.4232175314299,136.204433673345));
#158498=CARTESIAN_POINT('Ctrl Pts',(-149.623999635451,2.56626567612014,
136.137937950927));
#158499=CARTESIAN_POINT('Ctrl Pts',(-149.631395992386,2.70640743981672,
136.065851787587));
#158500=CARTESIAN_POINT('Ctrl Pts',(-149.638793481723,2.84657065957509,
135.99375458767));
#158501=CARTESIAN_POINT('Ctrl Pts',(-149.646190971059,2.98382628035887,
135.916065413362));
#158502=CARTESIAN_POINT('Ctrl Pts',(-149.653588460396,3.1177095600905,135.833060018149));
#158503=CARTESIAN_POINT('Ctrl Pts',(-149.660988542911,3.25163977239809,
135.750025525523));
#158504=CARTESIAN_POINT('Ctrl Pts',(-149.668388625426,3.38219497289253,
135.66167129817));
#158505=CARTESIAN_POINT('Ctrl Pts',(-149.675788707941,3.50893949269723,
135.568316347743));
#158506=CARTESIAN_POINT('Ctrl Pts',(-149.683196927608,3.6358233811313,135.474858743951));
#158507=CARTESIAN_POINT('Ctrl Pts',(-149.690605147274,3.75888791995032,
135.376389657123));
#158508=CARTESIAN_POINT('Ctrl Pts',(-149.69801336694,3.87773006190177,135.273268776113));
#158509=CARTESIAN_POINT('Ctrl Pts',(-149.705426146243,3.99664534920893,
135.17008442592));
#158510=CARTESIAN_POINT('Ctrl Pts',(-149.712838925545,4.11133278986144,
135.062242831582));
#158511=CARTESIAN_POINT('Ctrl Pts',(-149.720251704847,4.22142668731228,
134.950140072162));
#158512=CARTESIAN_POINT('Ctrl Pts',(-149.727675075875,4.33167789208653,
134.837877135062));
#158513=CARTESIAN_POINT('Ctrl Pts',(-149.735098446904,4.43732219488111,
134.72134114851));
#158514=CARTESIAN_POINT('Ctrl Pts',(-149.742521817933,4.53803408592429,
134.600961360005));
#158515=CARTESIAN_POINT('Ctrl Pts',(-149.746457867374,4.59143394710403,
134.537133107667));
#158516=CARTESIAN_POINT('Ctrl Pts',(-149.750393916815,4.64344784635833,
134.472224721073));
#158517=CARTESIAN_POINT('Ctrl Pts',(-149.754329966255,4.69403231779098,
134.406303310341));
#158518=CARTESIAN_POINT('Ctrl Pts',(-149.761753232661,4.78943305222581,
134.281977587037));
#158519=CARTESIAN_POINT('Ctrl Pts',(-149.769176499066,4.88003531184366,
134.153671087926));
#158520=CARTESIAN_POINT('Ctrl Pts',(-149.776599765472,4.9654884146336,134.021790549459));
#158521=CARTESIAN_POINT('Ctrl Pts',(-149.784014258193,5.05084051895248,
133.890065882836));
#158522=CARTESIAN_POINT('Ctrl Pts',(-149.791428750914,5.13105537940183,
133.754775895408));
#158523=CARTESIAN_POINT('Ctrl Pts',(-149.798843243635,5.20582261833553,
133.616360160405));
#158524=CARTESIAN_POINT('Ctrl Pts',(-149.806250589989,5.28051779378942,
133.478077835698));
#158525=CARTESIAN_POINT('Ctrl Pts',(-149.813657936342,5.34977562446093,
133.336676087374));
#158526=CARTESIAN_POINT('Ctrl Pts',(-149.821065282696,5.41332917310285,
133.192623129547));
#158527=CARTESIAN_POINT('Ctrl Pts',(-149.828467104372,5.47683532111046,
133.048677611851));
#158528=CARTESIAN_POINT('Ctrl Pts',(-149.835868926047,5.53464550827882,
132.902085161934));
#158529=CARTESIAN_POINT('Ctrl Pts',(-149.843270747722,5.58653892716462,
132.753338138671));
#158530=CARTESIAN_POINT('Ctrl Pts',(-149.850668662034,5.63840495191854,
132.604669637805));
#158531=CARTESIAN_POINT('Ctrl Pts',(-149.858066576345,5.68436030616929,
132.453849180318));
#158532=CARTESIAN_POINT('Ctrl Pts',(-149.865464490657,5.72423252654085,
132.301388521311));
#158533=CARTESIAN_POINT('Ctrl Pts',(-149.872861175569,5.76409812087268,
132.1489531985));
#158534=CARTESIAN_POINT('Ctrl Pts',(-149.880257860481,5.79788249331798,
131.994878575943));
#158535=CARTESIAN_POINT('Ctrl Pts',(-149.887654545393,5.82546319111763,
131.83969108241));
#158536=CARTESIAN_POINT('Ctrl Pts',(-149.895050902328,5.85304266596024,
131.684510470053));
#158537=CARTESIAN_POINT('Ctrl Pts',(-149.902447259264,5.87441894778336,
131.528217452376));
#158538=CARTESIAN_POINT('Ctrl Pts',(-149.9098436162,5.88952086340951,131.371347885469));
#158539=CARTESIAN_POINT('Ctrl Pts',(-149.917241105536,5.90462509117755,
131.21445430143));
#158540=CARTESIAN_POINT('Ctrl Pts',(-149.924638594873,5.91345300424894,
131.056984364006));
#158541=CARTESIAN_POINT('Ctrl Pts',(-149.932036084209,5.91598539739665,
130.899478125364));
#158542=CARTESIAN_POINT('Ctrl Pts',(-149.939436166724,5.91851867827084,
130.741916673154));
#158543=CARTESIAN_POINT('Ctrl Pts',(-149.946836249239,5.91475203933263,
130.584319267406));
#158544=CARTESIAN_POINT('Ctrl Pts',(-149.954236331754,5.90471838445042,
130.427224882275));
#158545=CARTESIAN_POINT('Ctrl Pts',(-149.961644551421,5.89467369653317,
130.269957755718));
#158546=CARTESIAN_POINT('Ctrl Pts',(-149.969052771087,5.87834825424528,
130.113195127169));
#158547=CARTESIAN_POINT('Ctrl Pts',(-149.976460990754,5.85582681712102,
129.957470512307));
#158548=CARTESIAN_POINT('Ctrl Pts',(-149.983873770056,5.83329151842801,
129.801650051542));
#158549=CARTESIAN_POINT('Ctrl Pts',(-149.991286549358,5.80455269394827,
129.646869243687));
#158550=CARTESIAN_POINT('Ctrl Pts',(-149.99869932866,5.76974590829766,129.493649850012));
#158551=CARTESIAN_POINT('Ctrl Pts',(-150.006122699689,5.7348893890795,129.340211529282));
#158552=CARTESIAN_POINT('Ctrl Pts',(-150.013546070717,5.69394768928889,
129.188339438058));
#158553=CARTESIAN_POINT('Ctrl Pts',(-150.020969441746,5.64710600102051,
129.038539455687));
#158554=CARTESIAN_POINT('Ctrl Pts',(-150.024905491187,5.62226941395013,
128.959111910635));
#158555=CARTESIAN_POINT('Ctrl Pts',(-150.028841540628,5.59577493306521,
128.880266575654));
#158556=CARTESIAN_POINT('Ctrl Pts',(-150.032777590068,5.56765552562929,
128.802076294492));
#158557=CARTESIAN_POINT('Ctrl Pts',(-150.040200856474,5.51462320078087,
128.654611864452));
#158558=CARTESIAN_POINT('Ctrl Pts',(-150.047624122879,5.45564804365642,
128.509032820616));
#158559=CARTESIAN_POINT('Ctrl Pts',(-150.055047389285,5.39088270095922,
128.365854052679));
#158560=CARTESIAN_POINT('Ctrl Pts',(-150.062461882006,5.32619390551866,
128.222844510155));
#158561=CARTESIAN_POINT('Ctrl Pts',(-150.069876374727,5.25572869891388,
128.082229933409));
#158562=CARTESIAN_POINT('Ctrl Pts',(-150.077290867448,5.17968913985313,
127.944509052014));
#158563=CARTESIAN_POINT('Ctrl Pts',(-150.084698213801,5.10372287058223,
127.80692091119));
#158564=CARTESIAN_POINT('Ctrl Pts',(-150.092105560155,5.02219312420585,
127.672221237864));
#158565=CARTESIAN_POINT('Ctrl Pts',(-150.099512906509,4.93534953641716,
127.540887695067));
#158566=CARTESIAN_POINT('Ctrl Pts',(-150.106914728184,4.84857071985266,
127.409652105781));
#158567=CARTESIAN_POINT('Ctrl Pts',(-150.11431654986,4.75648615828004,127.281777958146));
#158568=CARTESIAN_POINT('Ctrl Pts',(-150.121718371535,4.65939073535001,
127.157717155719));
#158569=CARTESIAN_POINT('Ctrl Pts',(-150.129116285847,4.56234656833796,
127.033721844023));
#158570=CARTESIAN_POINT('Ctrl Pts',(-150.136514200158,4.46029703749109,
126.913536161702));
#158571=CARTESIAN_POINT('Ctrl Pts',(-150.143912114469,4.35357947620254,
126.797581823212));
#158572=CARTESIAN_POINT('Ctrl Pts',(-150.151308799382,4.24687964943678,
126.681646754229));
#158573=CARTESIAN_POINT('Ctrl Pts',(-150.158705484294,4.13551358439462,
126.569941907893));
#158574=CARTESIAN_POINT('Ctrl Pts',(-150.166102169206,4.019857991804,126.462854854789));
#158575=CARTESIAN_POINT('Ctrl Pts',(-150.173498526141,3.90420752750356,
126.355772550036));
#158576=CARTESIAN_POINT('Ctrl Pts',(-150.180894883077,3.78426818775358,
126.253307885007));
#158577=CARTESIAN_POINT('Ctrl Pts',(-150.188291240012,3.66045233261851,
126.155810383017));
#158578=CARTESIAN_POINT('Ctrl Pts',(-150.195688729349,3.53661752095957,
126.05829795391));
#158579=CARTESIAN_POINT('Ctrl Pts',(-150.203086218686,3.40890530547316,
125.965754433029));
#158580=CARTESIAN_POINT('Ctrl Pts',(-150.210483708022,3.27775966644817,
125.878487889662));
#158581=CARTESIAN_POINT('Ctrl Pts',(-150.217883790537,3.1465680545229,125.791190755145));
#158582=CARTESIAN_POINT('Ctrl Pts',(-150.225283873052,3.01194093332542,
125.709174487823));
#158583=CARTESIAN_POINT('Ctrl Pts',(-150.232683955567,2.87434954242147,
125.632702733436));
#158584=CARTESIAN_POINT('Ctrl Pts',(-150.240092175234,2.73660685563828,
125.556146890494));
#158585=CARTESIAN_POINT('Ctrl Pts',(-150.2475003949,2.5958937161636,125.485147917581));
#158586=CARTESIAN_POINT('Ctrl Pts',(-150.254908614567,2.45270480044723,
125.419922882355));
#158587=CARTESIAN_POINT('Ctrl Pts',(-150.262321393869,2.30942775434246,
125.354657702209));
#158588=CARTESIAN_POINT('Ctrl Pts',(-150.269734173171,2.16367224045783,
125.295173681792));
#158589=CARTESIAN_POINT('Ctrl Pts',(-150.277146952473,2.01595050731278,
125.241638791466));
#158590=CARTESIAN_POINT('Ctrl Pts',(-150.284570323502,1.86801770242816,
125.188027407978));
#158591=CARTESIAN_POINT('Ctrl Pts',(-150.29199369453,1.71811342204681,125.140382244553));
#158592=CARTESIAN_POINT('Ctrl Pts',(-150.299417065559,1.56676337764193,
125.09882093398));
#158593=CARTESIAN_POINT('Ctrl Pts',(-150.303353115,1.48651395250529,125.076784129864));
#158594=CARTESIAN_POINT('Ctrl Pts',(-150.307289164441,1.40585822508792,
125.056456857534));
#158595=CARTESIAN_POINT('Ctrl Pts',(-150.311225213881,1.32487530050843,
125.03785075452));
#158596=CARTESIAN_POINT('Ctrl Pts',(-150.318648480287,1.17214403213982,
125.002760224914));
#158597=CARTESIAN_POINT('Ctrl Pts',(-150.326071746692,1.01778674657429,
124.973688665707));
#158598=CARTESIAN_POINT('Ctrl Pts',(-150.333495013098,0.862319144366244,
124.950785961362));
#158599=CARTESIAN_POINT('Ctrl Pts',(-150.340909505819,0.707035291953226,
124.927910326111));
#158600=CARTESIAN_POINT('Ctrl Pts',(-150.34832399854,0.550644100747854,
124.911189086673));
#158601=CARTESIAN_POINT('Ctrl Pts',(-150.355738491261,0.393674383730942,
124.90072182085));
#158602=CARTESIAN_POINT('Ctrl Pts',(-150.363145837614,0.236855960037095,
124.890264643771));
#158603=CARTESIAN_POINT('Ctrl Pts',(-150.370553183968,0.079460490583632,
124.886049464784));
#158604=CARTESIAN_POINT('Ctrl Pts',(-150.377960530322,-0.077975219002551,
124.888124446847));
#158605=CARTESIAN_POINT('Ctrl Pts',(-150.385362351997,-0.235293507096815,
124.89019788131));
#158606=CARTESIAN_POINT('Ctrl Pts',(-150.392764173673,-0.392651603905657,
124.898552130635));
#158607=CARTESIAN_POINT('Ctrl Pts',(-150.400165995348,-0.549509918353506,
124.913183365766));
#158608=CARTESIAN_POINT('Ctrl Pts',(-150.407563909659,-0.70628542851814,
124.927806877181));
#158609=CARTESIAN_POINT('Ctrl Pts',(-150.414961823971,-0.862561311010674,
124.948700740682));
#158610=CARTESIAN_POINT('Ctrl Pts',(-150.422359738282,-1.01780042857745,
124.975809095096));
#158611=CARTESIAN_POINT('Ctrl Pts',(-150.429756423194,-1.17301374821898,
125.002912944593));
#158612=CARTESIAN_POINT('Ctrl Pts',(-150.437153108107,-1.32719027750919,
125.036229171177));
#158613=CARTESIAN_POINT('Ctrl Pts',(-150.444549793019,-1.47980032098872,
125.07565032881));
#158614=CARTESIAN_POINT('Ctrl Pts',(-150.451946149954,-1.632403597579,125.115069738467));
#158615=CARTESIAN_POINT('Ctrl Pts',(-150.459342506889,-1.78344016503396,
125.16059344757));
#158616=CARTESIAN_POINT('Ctrl Pts',(-150.466738863825,-1.93239306880156,
125.212063451808));
#158617=CARTESIAN_POINT('Ctrl Pts',(-150.474136353161,-2.08136877763899,
125.263541336234));
#158618=CARTESIAN_POINT('Ctrl Pts',(-150.481533842498,-2.22825983473902,
125.320967206583));
#158619=CARTESIAN_POINT('Ctrl Pts',(-150.488931331835,-2.37256707049267,
125.384134048638));
#158620=CARTESIAN_POINT('Ctrl Pts',(-150.496331414349,-2.51692489292431,
125.447323033732));
#158621=CARTESIAN_POINT('Ctrl Pts',(-150.503731496865,-2.65869674890081,
125.516256847787));
#158622=CARTESIAN_POINT('Ctrl Pts',(-150.511131579379,-2.79740610929864,
125.590681530572));
#158623=CARTESIAN_POINT('Ctrl Pts',(-150.518539799046,-2.93626799489769,
125.665188050947));
#158624=CARTESIAN_POINT('Ctrl Pts',(-150.525948018712,-3.07206033060034,
125.745197321283));
#158625=CARTESIAN_POINT('Ctrl Pts',(-150.533356238379,-3.20433310653234,
125.830410486646));
#158626=CARTESIAN_POINT('Ctrl Pts',(-150.540769017681,-3.33668729415122,
125.91567609929));
#158627=CARTESIAN_POINT('Ctrl Pts',(-150.548181796983,-3.46551730073332,
126.006151775118));
#158628=CARTESIAN_POINT('Ctrl Pts',(-150.555594576285,-3.59040492522026,
126.101497337026));
#158629=CARTESIAN_POINT('Ctrl Pts',(-150.563017947314,-3.71547099500153,
126.196979133143));
#158630=CARTESIAN_POINT('Ctrl Pts',(-150.570441318342,-3.8365831455343,
126.297344475108));
#158631=CARTESIAN_POINT('Ctrl Pts',(-150.577864689371,-3.95335824912827,
126.402214650364));
#158632=CARTESIAN_POINT('Ctrl Pts',(-150.581800738812,-4.01527521103776,
126.457819333614));
#158633=CARTESIAN_POINT('Ctrl Pts',(-150.585736788253,-4.07597351174698,
126.514689894168));
#158634=CARTESIAN_POINT('Ctrl Pts',(-150.589672837694,-4.13540060202172,
126.572766069018));
#158635=CARTESIAN_POINT('Ctrl Pts',(-150.596989848785,-4.24587398026017,
126.680728131459));
#158636=CARTESIAN_POINT('Ctrl Pts',(-150.604306859877,-4.35230691777609,
126.793205472225));
#158637=CARTESIAN_POINT('Ctrl Pts',(-150.611623870968,-4.45429975870204,
126.909858823738));
#158638=CARTESIAN_POINT('Ctrl Pts',(-150.618932091929,-4.55617007278003,
127.026372036323));
#158639=CARTESIAN_POINT('Ctrl Pts',(-150.626240312891,-4.65361065207637,
127.147050991511));
#158640=CARTESIAN_POINT('Ctrl Pts',(-150.633548533852,-4.74625659640716,
127.27151772783));
#158641=CARTESIAN_POINT('Ctrl Pts',(-150.6409683786,-4.84031758977789,127.397885535339));
#158642=CARTESIAN_POINT('Ctrl Pts',(-150.648388223347,-4.92943597383426,
127.528157526693));
#158643=CARTESIAN_POINT('Ctrl Pts',(-150.655808068095,-5.01326962268013,
127.661900076396));
#158644=CARTESIAN_POINT('Ctrl Pts',(-150.663103336763,-5.09569573974858,
127.793397144824));
#158645=CARTESIAN_POINT('Ctrl Pts',(-150.670398605431,-5.17301295976667,
127.928248814312));
#158646=CARTESIAN_POINT('Ctrl Pts',(-150.6776938741,-5.24493778813581,128.066011085259));
#158647=CARTESIAN_POINT('Ctrl Pts',(-150.684986052498,-5.31683214920228,
128.203715000213));
#158648=CARTESIAN_POINT('Ctrl Pts',(-150.692278230896,-5.38333848524696,
128.344326723231));
#158649=CARTESIAN_POINT('Ctrl Pts',(-150.699570409294,-5.44421829342693,
128.48737599612));
#158650=CARTESIAN_POINT('Ctrl Pts',(-150.706861034815,-5.50508513719152,
128.630394806526));
#158651=CARTESIAN_POINT('Ctrl Pts',(-150.714151660337,-5.56032768742805,
128.775849779635));
#158652=CARTESIAN_POINT('Ctrl Pts',(-150.721442285858,-5.60975493921973,
128.923249221503));
#158653=CARTESIAN_POINT('Ctrl Pts',(-150.728957496019,-5.66070477662374,
129.075189240912));
#158654=CARTESIAN_POINT('Ctrl Pts',(-150.73647270618,-5.7054751140223,129.229195055014));
#158655=CARTESIAN_POINT('Ctrl Pts',(-150.743987916341,-5.74391178353263,
129.38470996142));
#158656=CARTESIAN_POINT('Ctrl Pts',(-150.751282479144,-5.78121994839688,
129.535658933872));
#158657=CARTESIAN_POINT('Ctrl Pts',(-150.758577041947,-5.81256108288044,
129.688029234886));
#158658=CARTESIAN_POINT('Ctrl Pts',(-150.76587160475,-5.83784605474345,
129.841300908298));
#158659=CARTESIAN_POINT('Ctrl Pts',(-150.77349713859,-5.86427826374589,
130.001526868908));
#158660=CARTESIAN_POINT('Ctrl Pts',(-150.78112267243,-5.88409180770352,
130.162737444565));
#158661=CARTESIAN_POINT('Ctrl Pts',(-150.78874820627,-5.89724546106289,
130.324332978286));
#158662=CARTESIAN_POINT('Ctrl Pts',(-150.79637374011,-5.91039911442222,
130.485928512005));
#158663=CARTESIAN_POINT('Ctrl Pts',(-150.80399927395,-5.91689290169413,
130.647908525579));
#158664=CARTESIAN_POINT('Ctrl Pts',(-150.81162480779,-5.91674761363104,
130.809674664177));
#158665=CARTESIAN_POINT('',(-152.561624807791,-5.92484811461594,130.801501939966));
#158666=CARTESIAN_POINT('Ctrl Pts',(-150.81162480779,-5.91854249043319,
130.809676276221));
#158667=CARTESIAN_POINT('Ctrl Pts',(-150.830456692362,-5.92224981611246,
131.209295934625));
#158668=CARTESIAN_POINT('Ctrl Pts',(-150.942104451545,-5.70288361260892,
133.574456017664));
#158669=CARTESIAN_POINT('Ctrl Pts',(-151.146568085314,-2.5191023459754,
137.333654905673));
#158670=CARTESIAN_POINT('Ctrl Pts',(-151.425015709135,4.13164385332104,
136.452995815532));
#158671=CARTESIAN_POINT('Ctrl Pts',(-151.703463332944,6.98561119344034,
130.381516929611));
#158672=CARTESIAN_POINT('Ctrl Pts',(-151.981910956759,3.42014311286449,
124.69861073587));
#158673=CARTESIAN_POINT('Ctrl Pts',(-152.260358580571,-3.28826940515126,
124.626590400934));
#158674=CARTESIAN_POINT('Ctrl Pts',(-152.453596530916,-5.84674475077773,
128.516399573093));
#158675=CARTESIAN_POINT('Ctrl Pts',(-152.554018606655,-5.92580458990376,
130.640542179685));
#158676=CARTESIAN_POINT('Ctrl Pts',(-152.561624807791,-5.92484811461594,
130.801501939966));
#158677=CARTESIAN_POINT('',(-154.311624807791,-5.90970598804176,130.800431355485));
#158678=CARTESIAN_POINT('Ctrl Pts',(-152.561624807791,-5.92484811461594,
130.801501939966));
#158679=CARTESIAN_POINT('Ctrl Pts',(-152.646834481259,-5.91413304864473,
132.604679159562));
#158680=CARTESIAN_POINT('Ctrl Pts',(-152.824860029333,-4.07084663883969,
136.390942232934));
#158681=CARTESIAN_POINT('Ctrl Pts',(-153.095701452011,2.37834317028329,
137.386233017932));
#158682=CARTESIAN_POINT('Ctrl Pts',(-153.374149075822,6.82306823653916,
132.3610559538));
#158683=CARTESIAN_POINT('Ctrl Pts',(-153.652596699636,4.99772691883392,
125.90535192446));
#158684=CARTESIAN_POINT('Ctrl Pts',(-153.931044323448,-1.4202812847494,
123.951597554207));
#158685=CARTESIAN_POINT('Ctrl Pts',(-154.1507203595,-5.45395989307253,127.378399482155));
#158686=CARTESIAN_POINT('Ctrl Pts',(-154.277580520948,-5.91410690545322,
130.075254683052));
#158687=CARTESIAN_POINT('Ctrl Pts',(-154.311624807791,-5.90970598804176,
130.800431355485));
#158688=CARTESIAN_POINT('',(-156.061624824859,-5.91361334729715,130.808692848313));
#158689=CARTESIAN_POINT('Ctrl Pts',(-154.311624807791,-5.90970598804176,
130.800431355485));
#158690=CARTESIAN_POINT('Ctrl Pts',(-154.370396395552,-5.90210856339691,
132.052323769702));
#158691=CARTESIAN_POINT('Ctrl Pts',(-154.521983857917,-4.89948390548452,
135.292405018535));
#158692=CARTESIAN_POINT('Ctrl Pts',(-154.766387194888,0.433474109379777,
137.789320225665));
#158693=CARTESIAN_POINT('Ctrl Pts',(-155.0448348187,6.11094768694514,134.215207858028));
#158694=CARTESIAN_POINT('Ctrl Pts',(-155.323282442513,6.17275887660265,
127.506693505547));
#158695=CARTESIAN_POINT('Ctrl Pts',(-155.601730066326,0.562106214696297,
123.828574129024));
#158696=CARTESIAN_POINT('Ctrl Pts',(-155.847844188085,-4.85360043142605,
126.243586901841));
#158697=CARTESIAN_POINT('Ctrl Pts',(-156.00114243524,-5.90179639786853,
129.520781549821));
#158698=CARTESIAN_POINT('Ctrl Pts',(-156.061624807791,-5.91048299654473,
130.808690191434));
#158699=CARTESIAN_POINT('',(-157.811624807791,-5.92111944829027,130.806626556176));
#158700=CARTESIAN_POINT('Ctrl Pts',(-156.061624841952,-5.9167484120262,
130.808695509193));
#158701=CARTESIAN_POINT('Ctrl Pts',(-156.070131700184,-5.91661555689736,
130.990031154992));
#158702=CARTESIAN_POINT('Ctrl Pts',(-156.078638558416,-5.90814245645985,
131.171029685701));
#158703=CARTESIAN_POINT('Ctrl Pts',(-156.087145416648,-5.89144563320417,
131.350985638489));
#158704=CARTESIAN_POINT('Ctrl Pts',(-156.095693557071,-5.87466778338968,
131.531814883841));
#158705=CARTESIAN_POINT('Ctrl Pts',(-156.104241697494,-5.84958630670668,
131.711591278413));
#158706=CARTESIAN_POINT('Ctrl Pts',(-156.112789837917,-5.81636890357933,
131.889617886593));
#158707=CARTESIAN_POINT('Ctrl Pts',(-156.121392227815,-5.78294069124846,
132.068774313601));
#158708=CARTESIAN_POINT('Ctrl Pts',(-156.129994617713,-5.74127304004691,
132.246158545632));
#158709=CARTESIAN_POINT('Ctrl Pts',(-156.138597007611,-5.691585441371,132.421081287958));
#158710=CARTESIAN_POINT('Ctrl Pts',(-156.145273109725,-5.65302412451932,
132.556834503472));
#158711=CARTESIAN_POINT('Ctrl Pts',(-156.151949211838,-5.60963343823935,
132.69110558819));
#158712=CARTESIAN_POINT('Ctrl Pts',(-156.158625313952,-5.56153547190469,
132.823581694429));
#158713=CARTESIAN_POINT('Ctrl Pts',(-156.166048580357,-5.50805456170145,
132.970884029261));
#158714=CARTESIAN_POINT('Ctrl Pts',(-156.173471846762,-5.44863658521653,
133.116282898686));
#158715=CARTESIAN_POINT('Ctrl Pts',(-156.180895113167,-5.38343575559325,
133.259263879998));
#158716=CARTESIAN_POINT('Ctrl Pts',(-156.188309605888,-5.31831198793581,
133.402075869664));
#158717=CARTESIAN_POINT('Ctrl Pts',(-156.195724098609,-5.2474191253225,
133.542475323237));
#158718=CARTESIAN_POINT('Ctrl Pts',(-156.20313859133,-5.17096074348685,
133.679964128452));
#158719=CARTESIAN_POINT('Ctrl Pts',(-156.210545937683,-5.09457605511823,
133.817320416779));
#158720=CARTESIAN_POINT('Ctrl Pts',(-156.217953284037,-5.01263670691561,
133.951771317679));
#158721=CARTESIAN_POINT('Ctrl Pts',(-156.22536063039,-4.92539378725776,
134.082839930135));
#158722=CARTESIAN_POINT('Ctrl Pts',(-156.232762452065,-4.83821593666113,
134.213810786675));
#158723=CARTESIAN_POINT('Ctrl Pts',(-156.24016427374,-4.74574259670467,
134.341404068271));
#158724=CARTESIAN_POINT('Ctrl Pts',(-156.247566095415,-4.64827002511213,
134.465168770986));
#158725=CARTESIAN_POINT('Ctrl Pts',(-156.254964009726,-4.55084890853113,
134.588868139278));
#158726=CARTESIAN_POINT('Ctrl Pts',(-156.262361924037,-4.44843404650144,
134.708742661235));
#158727=CARTESIAN_POINT('Ctrl Pts',(-156.269759838349,-4.34136405440738,
134.824371651083));
#158728=CARTESIAN_POINT('Ctrl Pts',(-156.27715652326,-4.23431185540402,
134.93998142549));
#158729=CARTESIAN_POINT('Ctrl Pts',(-156.284553208172,-4.12260631508079,
135.051346794421));
#158730=CARTESIAN_POINT('Ctrl Pts',(-156.291949893084,-4.00662532205224,
135.158081335663));
#158731=CARTESIAN_POINT('Ctrl Pts',(-156.299346250019,-3.89064947174247,
135.264811144185));
#158732=CARTESIAN_POINT('Ctrl Pts',(-156.306742606954,-3.77039882035604,
135.36691028051));
#158733=CARTESIAN_POINT('Ctrl Pts',(-156.314138963889,-3.64628678987608,
135.464030478026));
#158734=CARTESIAN_POINT('Ctrl Pts',(-156.321536453226,-3.52215575752705,
135.561165544891));
#158735=CARTESIAN_POINT('Ctrl Pts',(-156.328933942562,-3.39416246295797,
135.653319925064));
#158736=CARTESIAN_POINT('Ctrl Pts',(-156.336331431898,-3.26275182205814,
135.740186902005));
#158737=CARTESIAN_POINT('Ctrl Pts',(-156.343731514413,-3.13129511536205,
135.827084330029));
#158738=CARTESIAN_POINT('Ctrl Pts',(-156.351131596928,-2.99641898845008,
135.908690458811));
#158739=CARTESIAN_POINT('Ctrl Pts',(-156.358531679442,-2.85859548115215,
135.984743078122));
#158740=CARTESIAN_POINT('Ctrl Pts',(-156.365939899109,-2.72062042273954,
136.060879325106));
#158741=CARTESIAN_POINT('Ctrl Pts',(-156.373348118775,-2.57969183859533,
136.131449686766));
#158742=CARTESIAN_POINT('Ctrl Pts',(-156.380756338441,-2.43630506355726,
136.196238602071));
#158743=CARTESIAN_POINT('Ctrl Pts',(-156.388169117743,-2.29283003635168,
136.261067393872));
#158744=CARTESIAN_POINT('Ctrl Pts',(-156.395581897044,-2.14689414870795,
136.320107509118));
#158745=CARTESIAN_POINT('Ctrl Pts',(-156.402994676346,-1.99901015801677,
136.373192537336));
#158746=CARTESIAN_POINT('Ctrl Pts',(-156.410418047374,-1.8509148637444,
136.426353415931));
#158747=CARTESIAN_POINT('Ctrl Pts',(-156.417841418403,-1.7008662622286,
136.473542101607));
#158748=CARTESIAN_POINT('Ctrl Pts',(-156.425264789431,-1.54939042054123,
136.514642562202));
#158749=CARTESIAN_POINT('Ctrl Pts',(-156.429200838876,-1.46907429459182,
136.536435012622));
#158750=CARTESIAN_POINT('Ctrl Pts',(-156.43313688832,-1.38835707146956,
136.556516702527));
#158751=CARTESIAN_POINT('Ctrl Pts',(-156.437072937764,-1.30731789134756,
136.574876235209));
#158752=CARTESIAN_POINT('Ctrl Pts',(-156.44449620417,-1.1544805269183,136.609501740835));
#158753=CARTESIAN_POINT('Ctrl Pts',(-156.451919470575,-1.00003547249919,
136.638103354904));
#158754=CARTESIAN_POINT('Ctrl Pts',(-156.45934273698,-0.844498882452665,
136.660532763263));
#158755=CARTESIAN_POINT('Ctrl Pts',(-156.466757229701,-0.689146123739063,
136.682935661924));
#158756=CARTESIAN_POINT('Ctrl Pts',(-156.474171722423,-0.532704763226046,
136.69918082292));
#158757=CARTESIAN_POINT('Ctrl Pts',(-156.481586215144,-0.375703914525576,
136.709170278437));
#158758=CARTESIAN_POINT('Ctrl Pts',(-156.488993561497,-0.218854389154062,
136.71915010574));
#158759=CARTESIAN_POINT('Ctrl Pts',(-156.496400907851,-0.0614468191907923,
136.722886207535));
#158760=CARTESIAN_POINT('Ctrl Pts',(-156.503808254205,0.0959818456323094,
136.720332054939));
#158761=CARTESIAN_POINT('Ctrl Pts',(-156.51121007588,0.253293094217742,
136.717779807326));
#158762=CARTESIAN_POINT('Ctrl Pts',(-156.518611897556,0.410625034693445,
136.708946652779));
#158763=CARTESIAN_POINT('Ctrl Pts',(-156.526013719231,0.567438090137523,
136.693838062668));
#158764=CARTESIAN_POINT('Ctrl Pts',(-156.533411633542,0.724168365190709,
136.678737448263));
#158765=CARTESIAN_POINT('Ctrl Pts',(-156.540809547854,0.880379930091205,
136.657368031511));
#158766=CARTESIAN_POINT('Ctrl Pts',(-156.548207462165,1.03553582009553,
136.629787308187));
#158767=CARTESIAN_POINT('Ctrl Pts',(-156.555604147077,1.19066592600552,
136.602211168279));
#158768=CARTESIAN_POINT('Ctrl Pts',(-156.563000831989,1.34474033802766,
136.568425835693));
#158769=CARTESIAN_POINT('Ctrl Pts',(-156.570397516902,1.49722969018486,
136.528540368179));
#158770=CARTESIAN_POINT('Ctrl Pts',(-156.577793873837,1.64971228080395,
136.488656669229));
#158771=CARTESIAN_POINT('Ctrl Pts',(-156.585190230773,1.80060959015691,
136.442673467631));
#158772=CARTESIAN_POINT('Ctrl Pts',(-156.592586587708,1.94940514699695,
136.390750340398));
#158773=CARTESIAN_POINT('Ctrl Pts',(-156.599984077045,2.09822348481703,
136.338819263601));
#158774=CARTESIAN_POINT('Ctrl Pts',(-156.607381566381,2.24493907693255,
136.280946573395));
#158775=CARTESIAN_POINT('Ctrl Pts',(-156.614779055718,2.38905338612669,
136.217340802338));
#158776=CARTESIAN_POINT('Ctrl Pts',(-156.622179138233,2.53321821436831,
136.153712734377));
#158777=CARTESIAN_POINT('Ctrl Pts',(-156.629579220748,2.67477960284958,
136.084347734856));
#158778=CARTESIAN_POINT('Ctrl Pts',(-156.636979303263,2.81326179762183,
136.009501213222));
#158779=CARTESIAN_POINT('Ctrl Pts',(-156.644387522929,2.95189626780375,
135.934572390142));
#158780=CARTESIAN_POINT('Ctrl Pts',(-156.651795742596,3.08744445382917,
135.854150185243));
#158781=CARTESIAN_POINT('Ctrl Pts',(-156.659203962262,3.21945725751989,
135.768534821752));
#158782=CARTESIAN_POINT('Ctrl Pts',(-156.666616741564,3.35155131288852,
135.682866763432));
#158783=CARTESIAN_POINT('Ctrl Pts',(-156.674029520866,3.480105345904,135.591999392457));
#158784=CARTESIAN_POINT('Ctrl Pts',(-156.681442300168,3.6047021928271,135.496274157213));
#158785=CARTESIAN_POINT('Ctrl Pts',(-156.688865671197,3.72947706956828,
135.400412145265));
#158786=CARTESIAN_POINT('Ctrl Pts',(-156.696289042226,3.85028318154151,
135.29967864446));
#158787=CARTESIAN_POINT('Ctrl Pts',(-156.703712413255,3.96673855550187,
135.194453531707));
#158788=CARTESIAN_POINT('Ctrl Pts',(-156.707648462696,4.02848598908599,
135.138660652082));
#158789=CARTESIAN_POINT('Ctrl Pts',(-156.711584512136,4.08901091421956,
135.081605610203));
#158790=CARTESIAN_POINT('Ctrl Pts',(-156.715520561577,4.14826096533169,
135.023348828738));
#158791=CARTESIAN_POINT('Ctrl Pts',(-156.722943827983,4.26000471259557,
134.913478357029));
#158792=CARTESIAN_POINT('Ctrl Pts',(-156.730367094388,4.36754938499623,
134.798999229671));
#158793=CARTESIAN_POINT('Ctrl Pts',(-156.737790360794,4.47049120759569,
134.680265534525));
#158794=CARTESIAN_POINT('Ctrl Pts',(-156.745204853515,4.57331136150992,
134.561672172747));
#158795=CARTESIAN_POINT('Ctrl Pts',(-156.752619346236,4.67153925219407,
134.438834531824));
#158796=CARTESIAN_POINT('Ctrl Pts',(-156.760033838957,4.76480645771854,
134.312144816029));
#158797=CARTESIAN_POINT('Ctrl Pts',(-156.767441185311,4.85798376879888,
134.185577208551));
#158798=CARTESIAN_POINT('Ctrl Pts',(-156.774848531665,4.94620969351042,
134.055165216204));
#158799=CARTESIAN_POINT('Ctrl Pts',(-156.782255878019,5.0291548513403,133.921335440008));
#158800=CARTESIAN_POINT('Ctrl Pts',(-156.789657699694,5.11203814554214,
133.787605479109));
#158801=CARTESIAN_POINT('Ctrl Pts',(-156.79705952137,5.18964831932791,133.650463125918));
#158802=CARTESIAN_POINT('Ctrl Pts',(-156.804461343045,5.26169832140905,
133.510365299192));
#158803=CARTESIAN_POINT('Ctrl Pts',(-156.811859257356,5.33371028885493,
133.370341429017));
#158804=CARTESIAN_POINT('Ctrl Pts',(-156.819257171668,5.40016775983627,
133.227365523592));
#158805=CARTESIAN_POINT('Ctrl Pts',(-156.826655085979,5.46082886461755,
133.081920424434));
#158806=CARTESIAN_POINT('Ctrl Pts',(-156.834051770892,5.52147988862363,
132.936499495612));
#158807=CARTESIAN_POINT('Ctrl Pts',(-156.841448455804,5.57633631464319,
132.788610531647));
#158808=CARTESIAN_POINT('Ctrl Pts',(-156.848845140716,5.62520376080864,
132.638757851505));
#158809=CARTESIAN_POINT('Ctrl Pts',(-156.856241497652,5.67406904014033,
132.488911815988));
#158810=CARTESIAN_POINT('Ctrl Pts',(-156.863637854587,5.71694575190104,
132.337102592328));
#158811=CARTESIAN_POINT('Ctrl Pts',(-156.871034211523,5.75368898742517,
132.183850957685));
#158812=CARTESIAN_POINT('Ctrl Pts',(-156.878431700859,5.79043784843245,
132.030575859826));
#158813=CARTESIAN_POINT('Ctrl Pts',(-156.885829190196,5.82105127638797,
131.875858274301));
#158814=CARTESIAN_POINT('Ctrl Pts',(-156.893226679533,5.8454352440948,131.720230351532));
#158815=CARTESIAN_POINT('Ctrl Pts',(-156.900626762048,5.86982775956375,
131.564547873635));
#158816=CARTESIAN_POINT('Ctrl Pts',(-156.908026844563,5.88798640925056,
131.407954791702));
#158817=CARTESIAN_POINT('Ctrl Pts',(-156.915426927078,5.89986891972477,
131.250989426048));
#158818=CARTESIAN_POINT('Ctrl Pts',(-156.922835146744,5.91176449624079,
131.093851460837));
#158819=CARTESIAN_POINT('Ctrl Pts',(-156.930243366411,5.91737012307851,
130.93634076684));
#158820=CARTESIAN_POINT('Ctrl Pts',(-156.937651586077,5.91669563800539,
130.778997461058));
#158821=CARTESIAN_POINT('Ctrl Pts',(-156.945064365379,5.91602073779795,
130.621557313097));
#158822=CARTESIAN_POINT('Ctrl Pts',(-156.952477144682,5.90905804004873,
130.464285130708));
#158823=CARTESIAN_POINT('Ctrl Pts',(-156.959889923984,5.89586932776679,
130.307716446757));
#158824=CARTESIAN_POINT('Ctrl Pts',(-156.967313295012,5.88266177083427,
130.150924050127));
#158825=CARTESIAN_POINT('Ctrl Pts',(-156.974736666041,5.86321047805915,
129.994837528979));
#158826=CARTESIAN_POINT('Ctrl Pts',(-156.98216003707,5.83762858477514,129.839983580969));
#158827=CARTESIAN_POINT('Ctrl Pts',(-156.98609608651,5.82406445112959,129.757876302081));
#158828=CARTESIAN_POINT('Ctrl Pts',(-156.99003213595,5.80877762895482,129.676115324647));
#158829=CARTESIAN_POINT('Ctrl Pts',(-156.99396818539,5.79179064868332,129.594777365233));
#158830=CARTESIAN_POINT('Ctrl Pts',(-157.001391451796,5.75975373403073,
129.441376512221));
#158831=CARTESIAN_POINT('Ctrl Pts',(-157.008814718201,5.7215697243251,129.289017368863));
#158832=CARTESIAN_POINT('Ctrl Pts',(-157.016237984607,5.67731827349541,
129.13823103559));
#158833=CARTESIAN_POINT('Ctrl Pts',(-157.023652477327,5.63311912420575,
128.987622919241));
#158834=CARTESIAN_POINT('Ctrl Pts',(-157.031066970048,5.58286691222061,
128.838584267457));
#158835=CARTESIAN_POINT('Ctrl Pts',(-157.038481462769,5.52669246904767,
128.691637040031));
#158836=CARTESIAN_POINT('Ctrl Pts',(-157.045888809123,5.47057216891798,
128.544831445875));
#158837=CARTESIAN_POINT('Ctrl Pts',(-157.053296155477,5.40854113364339,
128.400113609376));
#158838=CARTESIAN_POINT('Ctrl Pts',(-157.060703501831,5.34078023653029,
128.257991235959));
#158839=CARTESIAN_POINT('Ctrl Pts',(-157.068105323506,5.27306987805073,
128.115974862769));
#158840=CARTESIAN_POINT('Ctrl Pts',(-157.075507145181,5.19963832690507,
127.976550433743));
#158841=CARTESIAN_POINT('Ctrl Pts',(-157.082908966857,5.12071484354904,
127.840206429006));
#158842=CARTESIAN_POINT('Ctrl Pts',(-157.090306881168,5.04183302328554,
127.703934399208));
#158843=CARTESIAN_POINT('Ctrl Pts',(-157.097704795479,4.9574652311445,127.570739877437));
#158844=CARTESIAN_POINT('Ctrl Pts',(-157.105102709791,4.86788695886932,
127.441087343184));
#158845=CARTESIAN_POINT('Ctrl Pts',(-157.112499394703,4.77832357287775,
127.311456354831));
#158846=CARTESIAN_POINT('Ctrl Pts',(-157.119896079615,4.68355163726892,
127.185366492595));
#158847=CARTESIAN_POINT('Ctrl Pts',(-157.127292764527,4.58389038172495,
127.063253892166));
#158848=CARTESIAN_POINT('Ctrl Pts',(-157.134689121463,4.48423354526548,
126.941146706339));
#158849=CARTESIAN_POINT('Ctrl Pts',(-157.142085478398,4.3796880559703,126.823016720869));
#158850=CARTESIAN_POINT('Ctrl Pts',(-157.149481835334,4.27061373173946,
126.709267344296));
#158851=CARTESIAN_POINT('Ctrl Pts',(-157.15687932467,4.16152270795112,126.595500552404));
#158852=CARTESIAN_POINT('Ctrl Pts',(-157.164276814007,4.04790172700596,
126.486115974285));
#158853=CARTESIAN_POINT('Ctrl Pts',(-157.171674303343,3.93014767812742,
126.381480357983));
#158854=CARTESIAN_POINT('Ctrl Pts',(-157.179074385858,3.81235235074976,
126.276808061828));
#158855=CARTESIAN_POINT('Ctrl Pts',(-157.186474468373,3.69042134968084,
126.176888289784));
#158856=CARTESIAN_POINT('Ctrl Pts',(-157.193874550888,3.56478472922586,
126.082047582963));
#158857=CARTESIAN_POINT('Ctrl Pts',(-157.201282770555,3.43900995839112,
125.987102589036));
#158858=CARTESIAN_POINT('Ctrl Pts',(-157.208690990221,3.30952172882964,
125.897248038899));
#158859=CARTESIAN_POINT('Ctrl Pts',(-157.216099209887,3.17677977382686,
125.812767602195));
#158860=CARTESIAN_POINT('Ctrl Pts',(-157.22351198919,3.04395611836533,125.72823516919));
#158861=CARTESIAN_POINT('Ctrl Pts',(-157.230924768492,2.90787506893844,
125.649083627833));
#158862=CARTESIAN_POINT('Ctrl Pts',(-157.238337547794,2.76902057973649,
125.57555046692));
#158863=CARTESIAN_POINT('Ctrl Pts',(-157.245760918822,2.62996768872893,
125.501912238379));
#158864=CARTESIAN_POINT('Ctrl Pts',(-157.253184289851,2.48813377902014,
125.433908584573));
#158865=CARTESIAN_POINT('Ctrl Pts',(-157.26060766088,2.34402312867773,125.371729014491));
#158866=CARTESIAN_POINT('Ctrl Pts',(-157.264543710321,2.26761220396997,
125.338759914452));
#158867=CARTESIAN_POINT('Ctrl Pts',(-157.268479759762,2.1905614772537,125.307427345457));
#158868=CARTESIAN_POINT('Ctrl Pts',(-157.272415809203,2.11294767059808,
125.277753819194));
#158869=CARTESIAN_POINT('Ctrl Pts',(-157.279839075609,1.96657045350461,
125.221790474746));
#158870=CARTESIAN_POINT('Ctrl Pts',(-157.287262342014,1.81774700121957,
125.171561924975));
#158871=CARTESIAN_POINT('Ctrl Pts',(-157.29468560842,1.66696719846948,125.127288227528));
#158872=CARTESIAN_POINT('Ctrl Pts',(-157.302100101141,1.5163656049239,125.083066857916));
#158873=CARTESIAN_POINT('Ctrl Pts',(-157.309514593862,1.36381261812584,
125.044786435315));
#158874=CARTESIAN_POINT('Ctrl Pts',(-157.316929086583,1.20981809525616,
125.012619019489));
#158875=CARTESIAN_POINT('Ctrl Pts',(-157.324336432937,1.05597199810628,
124.980482607831));
#158876=CARTESIAN_POINT('Ctrl Pts',(-157.331743779291,0.900687493877916,
124.95444754906));
#158877=CARTESIAN_POINT('Ctrl Pts',(-157.339151125644,0.744489495964291,
124.934636096526));
#158878=CARTESIAN_POINT('Ctrl Pts',(-157.34655294732,0.588407996410522,
124.914839420121));
#158879=CARTESIAN_POINT('Ctrl Pts',(-157.353954768995,0.431414728504796,
124.90125715427));
#158880=CARTESIAN_POINT('Ctrl Pts',(-157.361356590671,0.274044585288307,
124.893960451099));
#158881=CARTESIAN_POINT('Ctrl Pts',(-157.368754504982,0.116757516545007,
124.886667599801));
#158882=CARTESIAN_POINT('Ctrl Pts',(-157.376152419294,-0.0409056593381581,
124.885653720275));
#158883=CARTESIAN_POINT('Ctrl Pts',(-157.383550333605,-0.198405252592531,
124.890938096027));
#158884=CARTESIAN_POINT('Ctrl Pts',(-157.390947018517,-0.355878672271614,
124.896221593611));
#158885=CARTESIAN_POINT('Ctrl Pts',(-157.398343703429,-0.513188190552356,
124.907801256666));
#158886=CARTESIAN_POINT('Ctrl Pts',(-157.405740388342,-0.669794322685559,
124.925644250212));
#158887=CARTESIAN_POINT('Ctrl Pts',(-157.413136745277,-0.826393510738753,
124.943486452581));
#158888=CARTESIAN_POINT('Ctrl Pts',(-157.420533102213,-0.982289003760471,
124.967591390976));
#158889=CARTESIAN_POINT('Ctrl Pts',(-157.427929459148,-1.13694691235704,
124.997874392577));
#158890=CARTESIAN_POINT('Ctrl Pts',(-157.435326948485,-1.29162849947469,
125.028162030584));
#158891=CARTESIAN_POINT('Ctrl Pts',(-157.442724437821,-1.44507175852789,
125.064629543427));
#158892=CARTESIAN_POINT('Ctrl Pts',(-157.450121927158,-1.59675360568007,
125.10714125324));
#158893=CARTESIAN_POINT('Ctrl Pts',(-157.457522009673,-1.74848862466842,
125.149667865467));
#158894=CARTESIAN_POINT('Ctrl Pts',(-157.464922092188,-1.89846064317388,
125.198242792467));
#158895=CARTESIAN_POINT('Ctrl Pts',(-157.472322174703,-2.04616247805276,
125.252680720822));
#158896=CARTESIAN_POINT('Ctrl Pts',(-157.47973039437,-2.194026726283,125.307178509276));
#158897=CARTESIAN_POINT('Ctrl Pts',(-157.487138614036,-2.33961545513118,
125.367552044937));
#158898=CARTESIAN_POINT('Ctrl Pts',(-157.494546833703,-2.48244150822397,
125.433567871542));
#158899=CARTESIAN_POINT('Ctrl Pts',(-157.501959613005,-2.62535546836926,
125.499624329787));
#158900=CARTESIAN_POINT('Ctrl Pts',(-157.509372392307,-2.76550303298194,
125.571329829199));
#158901=CARTESIAN_POINT('Ctrl Pts',(-157.516785171609,-2.9024228069489,
125.64840557391));
#158902=CARTESIAN_POINT('Ctrl Pts',(-157.524208542638,-3.03953821831,125.725591448059));
#158903=CARTESIAN_POINT('Ctrl Pts',(-157.531631913667,-3.17341631090493,
125.808162697281));
#158904=CARTESIAN_POINT('Ctrl Pts',(-157.539055284696,-3.30362507084091,
125.895797492393));
#158905=CARTESIAN_POINT('Ctrl Pts',(-157.542991334136,-3.37266487966637,
125.942263563523));
#158906=CARTESIAN_POINT('Ctrl Pts',(-157.546927383576,-3.4406736571893,
125.990152503206));
#158907=CARTESIAN_POINT('Ctrl Pts',(-157.550863433017,-3.50759099353742,
126.03941193111));
#158908=CARTESIAN_POINT('Ctrl Pts',(-157.558218175006,-3.63263000813877,
126.131456095763));
#158909=CARTESIAN_POINT('Ctrl Pts',(-157.565572916995,-3.75424966978868,
126.228577345023));
#158910=CARTESIAN_POINT('Ctrl Pts',(-157.572927658984,-3.87200459353564,
126.330490817255));
#158911=CARTESIAN_POINT('Ctrl Pts',(-157.580273676026,-3.98961982435429,
126.432283389307));
#158912=CARTESIAN_POINT('Ctrl Pts',(-157.587619693069,-4.10337915519362,
126.538856625361));
#158913=CARTESIAN_POINT('Ctrl Pts',(-157.594965710111,-4.21286640760883,
126.649882648658));
#158914=CARTESIAN_POINT('Ctrl Pts',(-157.602304689178,-4.32224876391778,
126.760802301603));
#158915=CARTESIAN_POINT('Ctrl Pts',(-157.609643668245,-4.42736692186733,
126.876165982255));
#158916=CARTESIAN_POINT('Ctrl Pts',(-157.616982647312,-4.52783819494831,
126.99560598608));
#158917=CARTESIAN_POINT('Ctrl Pts',(-157.624316268933,-4.62823612412295,
127.114958798848));
#158918=CARTESIAN_POINT('Ctrl Pts',(-157.631649890554,-4.72399367667982,
127.238381721226));
#158919=CARTESIAN_POINT('Ctrl Pts',(-157.638983512176,-4.8147655874284,
127.365470840237));
#158920=CARTESIAN_POINT('Ctrl Pts',(-157.646313991294,-4.90549860184631,
127.492505500767));
#158921=CARTESIAN_POINT('Ctrl Pts',(-157.653644470413,-4.99125000375958,
127.62320292324));
#158922=CARTESIAN_POINT('Ctrl Pts',(-157.660974949531,-5.07171541329371,
127.757126900068));
#158923=CARTESIAN_POINT('Ctrl Pts',(-157.668303887895,-5.15216391022401,
127.891022728115));
#158924=CARTESIAN_POINT('Ctrl Pts',(-157.675632826258,-5.2273284289208,
128.028143435116));
#158925=CARTESIAN_POINT('Ctrl Pts',(-157.682961764622,-5.29694859574216,
128.16802487708));
#158926=CARTESIAN_POINT('Ctrl Pts',(-157.690290675458,-5.36656850107277,
128.307905793654));
#158927=CARTESIAN_POINT('Ctrl Pts',(-157.697619586294,-5.43064392617252,
128.450547083563));
#158928=CARTESIAN_POINT('Ctrl Pts',(-157.704948497131,-5.48896115645343,
128.595461347467));
#158929=CARTESIAN_POINT('Ctrl Pts',(-157.712278893428,-5.54729020677008,
128.740404983338));
#158930=CARTESIAN_POINT('Ctrl Pts',(-157.719609289726,-5.59985859777098,
128.887622156598));
#158931=CARTESIAN_POINT('Ctrl Pts',(-157.726939686023,-5.64650141551444,
129.036607148585));
#158932=CARTESIAN_POINT('Ctrl Pts',(-157.734277182083,-5.69318940856624,
129.185736438093));
#158933=CARTESIAN_POINT('Ctrl Pts',(-157.741614678143,-5.73394025124491,
129.336636602246));
#158934=CARTESIAN_POINT('Ctrl Pts',(-157.748952174202,-5.76863925827811,
129.488787863838));
#158935=CARTESIAN_POINT('Ctrl Pts',(-157.756293346656,-5.80335565097007,
129.641015359596));
#158936=CARTESIAN_POINT('Ctrl Pts',(-157.763634519109,-5.83201409738659,
129.79449482759));
#158937=CARTESIAN_POINT('Ctrl Pts',(-157.770975691562,-5.8545515050313,
129.948698746594));
#158938=CARTESIAN_POINT('Ctrl Pts',(-157.778327484036,-5.87712151615164,
130.103125742883));
#158939=CARTESIAN_POINT('Ctrl Pts',(-157.78567927651,-5.89355275828968,
130.258278905398));
#158940=CARTESIAN_POINT('Ctrl Pts',(-157.793031068984,-5.90383417195853,
130.413627163003));
#158941=CARTESIAN_POINT('Ctrl Pts',(-157.799228981919,-5.91250189578266,
130.544593179627));
#158942=CARTESIAN_POINT('Ctrl Pts',(-157.805426894855,-5.9167996709415,
130.675697717311));
#158943=CARTESIAN_POINT('Ctrl Pts',(-157.811624807791,-5.91674956674677,
130.806624883877));
#158944=CARTESIAN_POINT('',(-159.561624807791,-5.91743068731423,130.798929988566));
#158945=CARTESIAN_POINT('Ctrl Pts',(-157.811624807791,-5.9254847114659,
130.806628226708));
#158946=CARTESIAN_POINT('Ctrl Pts',(-157.817520224137,-5.92609395467479,
130.931349446311));
#158947=CARTESIAN_POINT('Ctrl Pts',(-157.823415640483,-5.92249881701993,
131.056034883051));
#158948=CARTESIAN_POINT('Ctrl Pts',(-157.829311056829,-5.91458801171559,
131.180445903534));
#158949=CARTESIAN_POINT('Ctrl Pts',(-157.922126931433,-5.7900423867684,
133.139140081975));
#158950=CARTESIAN_POINT('Ctrl Pts',(-158.107758680643,-3.4015434686423,
136.920491957005));
#158951=CARTESIAN_POINT('Ctrl Pts',(-158.386206304455,3.30705718159266,
136.972093858232));
#158952=CARTESIAN_POINT('Ctrl Pts',(-158.664653928267,6.97663384066779,
131.355850221806));
#158953=CARTESIAN_POINT('Ctrl Pts',(-158.943101552081,4.23502482768286,
125.232814580849));
#158954=CARTESIAN_POINT('Ctrl Pts',(-159.221549175893,-2.39836510947921,
124.229757562476));
#158955=CARTESIAN_POINT('Ctrl Pts',(-159.427723594463,-5.67808762901621,
127.960611207063));
#158956=CARTESIAN_POINT('Ctrl Pts',(-159.541082138429,-5.92148486028014,
130.362796665562));
#158957=CARTESIAN_POINT('Ctrl Pts',(-159.561624807791,-5.91743068731423,
130.798929988566));
#158958=CARTESIAN_POINT('',(-161.311624807829,-5.91674999652905,130.804563283626));
#158959=CARTESIAN_POINT('Ctrl Pts',(-159.561624807791,-5.91674750835102,
130.798930615543));
#158960=CARTESIAN_POINT('Ctrl Pts',(-159.568932004374,-5.91688986440021,
130.954047463703));
#158961=CARTESIAN_POINT('Ctrl Pts',(-159.576239200957,-5.91092810715701,
131.109346714272));
#158962=CARTESIAN_POINT('Ctrl Pts',(-159.58354639754,-5.89884604826352,
131.264301767482));
#158963=CARTESIAN_POINT('Ctrl Pts',(-159.590848258521,-5.88677281150266,
131.419143674908));
#158964=CARTESIAN_POINT('Ctrl Pts',(-159.598150119502,-5.86858819695825,
131.573641503703));
#158965=CARTESIAN_POINT('Ctrl Pts',(-159.605451980483,-5.84432808587817,
131.727268948396));
#158966=CARTESIAN_POINT('Ctrl Pts',(-159.612750815579,-5.82007802816727,
131.880832730009));
#158967=CARTESIAN_POINT('Ctrl Pts',(-159.620049650675,-5.78975754077517,
132.033526466032));
#158968=CARTESIAN_POINT('Ctrl Pts',(-159.627348485771,-5.75345431116056,
132.184829397325));
#158969=CARTESIAN_POINT('Ctrl Pts',(-159.634645847149,-5.71715841158406,
132.336101778821));
#158970=CARTESIAN_POINT('Ctrl Pts',(-159.641943208527,-5.67488226185732,
132.485983540557));
#158971=CARTESIAN_POINT('Ctrl Pts',(-159.649240569904,-5.62676452252715,
132.633964829009));
#158972=CARTESIAN_POINT('Ctrl Pts',(-159.656537990201,-5.57864639469371,
132.781947312264));
#158973=CARTESIAN_POINT('Ctrl Pts',(-159.663835410497,-5.52468670211461,
132.928028926103));
#158974=CARTESIAN_POINT('Ctrl Pts',(-159.671132830794,-5.46507367570252,
133.071715967229));
#158975=CARTESIAN_POINT('Ctrl Pts',(-159.678431842531,-5.40544764873038,
133.215434343989));
#158976=CARTESIAN_POINT('Ctrl Pts',(-159.685730854267,-5.34016598231529,
133.356756754134));
#158977=CARTESIAN_POINT('Ctrl Pts',(-159.693029866004,-5.26946452189638,
133.495210709075));
#158978=CARTESIAN_POINT('Ctrl Pts',(-159.700336286835,-5.19869129370716,
133.633805206115));
#158979=CARTESIAN_POINT('Ctrl Pts',(-159.707642707666,-5.1224874584411,
133.769525089707));
#158980=CARTESIAN_POINT('Ctrl Pts',(-159.714949128497,-5.04113449756899,
133.901923133468));
#158981=CARTESIAN_POINT('Ctrl Pts',(-159.722259345137,-4.95973927245551,
134.034389960255));
#158982=CARTESIAN_POINT('Ctrl Pts',(-159.729569561777,-4.87318980763445,
134.163531191305));
#158983=CARTESIAN_POINT('Ctrl Pts',(-159.736879778418,-4.78180970556107,
134.288930390479));
#158984=CARTESIAN_POINT('Ctrl Pts',(-159.744201082717,-4.69029100411616,
134.41451978697));
#158985=CARTESIAN_POINT('Ctrl Pts',(-159.751522387017,-4.59392726697723,
134.53635551228));
#158986=CARTESIAN_POINT('Ctrl Pts',(-159.758843691317,-4.49308159296783,
134.654055197846));
#158987=CARTESIAN_POINT('Ctrl Pts',(-159.765377268717,-4.40308628752762,
134.759091127812));
#158988=CARTESIAN_POINT('Ctrl Pts',(-159.771910846118,-4.30952228015494,
134.860833538824));
#158989=CARTESIAN_POINT('Ctrl Pts',(-159.778444423519,-4.21267037862175,
134.959037361139));
#158990=CARTESIAN_POINT('Ctrl Pts',(-159.785867689924,-4.10262997918174,
135.070613774849));
#158991=CARTESIAN_POINT('Ctrl Pts',(-159.79329095633,-3.98798731970659,
135.177984104969));
#158992=CARTESIAN_POINT('Ctrl Pts',(-159.800714222735,-3.86909710212392,
135.28074511589));
#158993=CARTESIAN_POINT('Ctrl Pts',(-159.808128715456,-3.75034740290522,
135.38338467183));
#158994=CARTESIAN_POINT('Ctrl Pts',(-159.815543208177,-3.62736041810098,
135.481425510788));
#158995=CARTESIAN_POINT('Ctrl Pts',(-159.822957700898,-3.5005289122021,
135.574499808128));
#158996=CARTESIAN_POINT('Ctrl Pts',(-159.830365047252,-3.37381965128336,
135.667484396957));
#158997=CARTESIAN_POINT('Ctrl Pts',(-159.837772393605,-3.24327354511521,
135.755511754651));
#158998=CARTESIAN_POINT('Ctrl Pts',(-159.845179739959,-3.10931769548364,
135.838253150294));
#158999=CARTESIAN_POINT('Ctrl Pts',(-159.852581561635,-2.97546175517859,
135.920932834282));
#159000=CARTESIAN_POINT('Ctrl Pts',(-159.85998338331,-2.83820145132589,
135.99833421088));
#159001=CARTESIAN_POINT('Ctrl Pts',(-159.867385204985,-2.69799413899417,
136.070170924485));
#159002=CARTESIAN_POINT('Ctrl Pts',(-159.874783119297,-2.55786084101086,
136.141969716048));
#159003=CARTESIAN_POINT('Ctrl Pts',(-159.882181033608,-2.41478396419327,
136.208209525083));
#159004=CARTESIAN_POINT('Ctrl Pts',(-159.889578947919,-2.26924671758432,
136.268649216939));
#159005=CARTESIAN_POINT('Ctrl Pts',(-159.896975632832,-2.12373365662606,
136.329078864813));
#159006=CARTESIAN_POINT('Ctrl Pts',(-159.904372317744,-1.97576138177387,
136.383710165482));
#159007=CARTESIAN_POINT('Ctrl Pts',(-159.911769002656,-1.82583450722637,
136.43234950479));
#159008=CARTESIAN_POINT('Ctrl Pts',(-159.919165359592,-1.6759142805936,
136.480986687379));
#159009=CARTESIAN_POINT('Ctrl Pts',(-159.926561716527,-1.52403998167192,
136.523632321694));
#159010=CARTESIAN_POINT('Ctrl Pts',(-159.933958073463,-1.37073260754405,
136.560142291771));
#159011=CARTESIAN_POINT('Ctrl Pts',(-159.941355562799,-1.21740176166583,
136.596657851618));
#159012=CARTESIAN_POINT('Ctrl Pts',(-159.948753052136,-1.06263776687743,
136.627035790296));
#159013=CARTESIAN_POINT('Ctrl Pts',(-159.956150541472,-0.90697291607658,
136.651182890562));
#159014=CARTESIAN_POINT('Ctrl Pts',(-159.963550623987,-0.751253497203818,
136.675338455556));
#159015=CARTESIAN_POINT('Ctrl Pts',(-159.970950706502,-0.594632962231653,
136.693258776203));
#159016=CARTESIAN_POINT('Ctrl Pts',(-159.978350789017,-0.437649695184568,
136.704902398352));
#159017=CARTESIAN_POINT('Ctrl Pts',(-159.985759008684,-0.280493808897315,
136.716558823861));
#159018=CARTESIAN_POINT('Ctrl Pts',(-159.99316722835,-0.122974766486851,
136.721924739746));
#159019=CARTESIAN_POINT('Ctrl Pts',(-160.000575448017,0.0343673306403178,
136.721010805729));
#159020=CARTESIAN_POINT('Ctrl Pts',(-160.007988227319,0.191806269203324,
136.7200963092));
#159021=CARTESIAN_POINT('Ctrl Pts',(-160.015401006621,0.349067673429993,
136.712894278026));
#159022=CARTESIAN_POINT('Ctrl Pts',(-160.022813785923,0.505616105100663,
136.699467310134));
#159023=CARTESIAN_POINT('Ctrl Pts',(-160.030237156952,0.662388220511676,
136.686021157161));
#159024=CARTESIAN_POINT('Ctrl Pts',(-160.03766052798,0.818444959356333,
136.666332349798));
#159025=CARTESIAN_POINT('Ctrl Pts',(-160.045083899009,0.973259796759561,
136.640514824791));
#159026=CARTESIAN_POINT('Ctrl Pts',(-160.04901994845,1.05534633828929,136.626825753548));
#159027=CARTESIAN_POINT('Ctrl Pts',(-160.052955997891,1.13708395712726,
136.611414522782));
#159028=CARTESIAN_POINT('Ctrl Pts',(-160.056892047333,1.21839597108338,
136.594303779649));
#159029=CARTESIAN_POINT('Ctrl Pts',(-160.064315313738,1.37174789172974,
136.56203345211));
#159030=CARTESIAN_POINT('Ctrl Pts',(-160.071738580143,1.52404874909483,
136.52361762194));
#159031=CARTESIAN_POINT('Ctrl Pts',(-160.079161846549,1.67476756458465,
136.479136751222));
#159032=CARTESIAN_POINT('Ctrl Pts',(-160.08657633927,1.82530824295054,136.4347084532));
#159033=CARTESIAN_POINT('Ctrl Pts',(-160.093990831991,1.9742702468371,136.384229487949));
#159034=CARTESIAN_POINT('Ctrl Pts',(-160.101405324712,2.12113181616055,
136.32783148116));
#159035=CARTESIAN_POINT('Ctrl Pts',(-160.108812671065,2.26785183477466,
136.271487832893));
#159036=CARTESIAN_POINT('Ctrl Pts',(-160.116220017419,2.41247510301682,
136.209236633538));
#159037=CARTESIAN_POINT('Ctrl Pts',(-160.123627363773,2.55449419130832,
136.141259528832));
#159038=CARTESIAN_POINT('Ctrl Pts',(-160.131029185448,2.69640735640609,
136.073333124015));
#159039=CARTESIAN_POINT('Ctrl Pts',(-160.138431007124,2.83571987366102,
135.999689477655));
#159040=CARTESIAN_POINT('Ctrl Pts',(-160.145832828799,2.97194361240766,
135.920558593326));
#159041=CARTESIAN_POINT('Ctrl Pts',(-160.15323074311,3.10809543970221,135.841469481575));
#159042=CARTESIAN_POINT('Ctrl Pts',(-160.160628657422,3.24116141381868,
135.756899087742));
#159043=CARTESIAN_POINT('Ctrl Pts',(-160.168026571733,3.3706774750536,135.667123610111));
#159044=CARTESIAN_POINT('Ctrl Pts',(-160.175423256645,3.50017201306936,
135.577363051535));
#159045=CARTESIAN_POINT('Ctrl Pts',(-160.182819941557,3.62611750254257,
135.482399338365));
#159046=CARTESIAN_POINT('Ctrl Pts',(-160.190216626469,3.74807829410105,
135.382552363637));
#159047=CARTESIAN_POINT('Ctrl Pts',(-160.197612983405,3.87003367779022,
135.282709816228));
#159048=CARTESIAN_POINT('Ctrl Pts',(-160.20500934034,3.98800442602976,135.177984674266));
#159049=CARTESIAN_POINT('Ctrl Pts',(-160.212405697276,4.10158767832863,
135.068737369154));
#159050=CARTESIAN_POINT('Ctrl Pts',(-160.219803186612,4.21518832051307,
134.959473338001));
#159051=CARTESIAN_POINT('Ctrl Pts',(-160.227200675949,4.32439986017536,
134.84568602392));
#159052=CARTESIAN_POINT('Ctrl Pts',(-160.234598165285,4.42885615369344,
134.727772873803));
#159053=CARTESIAN_POINT('Ctrl Pts',(-160.2419982478,4.53334906420314,134.609818389415));
#159054=CARTESIAN_POINT('Ctrl Pts',(-160.249398330315,4.63308316231466,
134.487735468656));
#159055=CARTESIAN_POINT('Ctrl Pts',(-160.25679841283,4.72773256176189,134.361954662276));
#159056=CARTESIAN_POINT('Ctrl Pts',(-160.264206632496,4.82248603795442,
134.236035546968));
#159057=CARTESIAN_POINT('Ctrl Pts',(-160.271614852163,4.91214342499873,
134.106410724022));
#159058=CARTESIAN_POINT('Ctrl Pts',(-160.279023071829,4.99642175321808,
133.973540357888));
#159059=CARTESIAN_POINT('Ctrl Pts',(-160.286435851131,5.08075195334219,
133.840588212261));
#159060=CARTESIAN_POINT('Ctrl Pts',(-160.293848630433,5.15969631085155,
133.704386865242));
#159061=CARTESIAN_POINT('Ctrl Pts',(-160.301261409735,5.23301807371878,
133.565420631878));
#159062=CARTESIAN_POINT('Ctrl Pts',(-160.308684780764,5.30644460215935,
133.426255837043));
#159063=CARTESIAN_POINT('Ctrl Pts',(-160.316108151793,5.37423233015227,
133.28431860159));
#159064=CARTESIAN_POINT('Ctrl Pts',(-160.323531522822,5.43619251635348,
133.140113491404));
#159065=CARTESIAN_POINT('Ctrl Pts',(-160.327467572263,5.46904529379542,
133.06365248182));
#159066=CARTESIAN_POINT('Ctrl Pts',(-160.331403621704,5.50026056841827,
132.986554161491));
#159067=CARTESIAN_POINT('Ctrl Pts',(-160.335339671145,5.52981594531894,
132.908895286655));
#159068=CARTESIAN_POINT('Ctrl Pts',(-160.342762937551,5.58555646375567,
132.76243307238));
#159069=CARTESIAN_POINT('Ctrl Pts',(-160.350186203956,5.63555847140281,
132.613533353129));
#159070=CARTESIAN_POINT('Ctrl Pts',(-160.357609470362,5.67960265638814,
132.462686347949));
#159071=CARTESIAN_POINT('Ctrl Pts',(-160.365023963083,5.72359478480446,
132.312017631402));
#159072=CARTESIAN_POINT('Ctrl Pts',(-160.372438455803,5.76164300340042,
132.159406564972));
#159073=CARTESIAN_POINT('Ctrl Pts',(-160.379852948525,5.793576028527,132.005363267096));
#159074=CARTESIAN_POINT('Ctrl Pts',(-160.387260294878,5.82547827540171,
131.851468441949));
#159075=CARTESIAN_POINT('Ctrl Pts',(-160.394667641232,5.85127698744293,
131.696144496611));
#159076=CARTESIAN_POINT('Ctrl Pts',(-160.402074987586,5.87085071027271,
131.539916529914));
#159077=CARTESIAN_POINT('Ctrl Pts',(-160.409476809261,5.89040983428153,
131.383805083929));
#159078=CARTESIAN_POINT('Ctrl Pts',(-160.416878630937,5.90375316737584,
131.226791327923));
#159079=CARTESIAN_POINT('Ctrl Pts',(-160.424280452612,5.91081037152842,
131.069410262599));
#159080=CARTESIAN_POINT('Ctrl Pts',(-160.431678366924,5.91786385023786,
130.912112277514));
#159081=CARTESIAN_POINT('Ctrl Pts',(-160.439076281235,5.91863779207514,
130.754447741251));
#159082=CARTESIAN_POINT('Ctrl Pts',(-160.446474195546,5.91311373487316,
130.5969563723));
#159083=CARTESIAN_POINT('Ctrl Pts',(-160.453870880459,5.90759059566927,
130.439491175557));
#159084=CARTESIAN_POINT('Ctrl Pts',(-160.461267565371,5.89577154771621,
130.282199461714));
#159085=CARTESIAN_POINT('Ctrl Pts',(-160.468664250283,5.87769024695864,
130.125620664928));
#159086=CARTESIAN_POINT('Ctrl Pts',(-160.476060607218,5.85960974794489,
129.969048811009));
#159087=CARTESIAN_POINT('Ctrl Pts',(-160.483456964154,5.83526759106086,
129.813190182125));
#159088=CARTESIAN_POINT('Ctrl Pts',(-160.490853321089,5.80474926151761,
129.658578538194));
#159089=CARTESIAN_POINT('Ctrl Pts',(-160.498250810426,5.7742262595402,129.503943222825));
#159090=CARTESIAN_POINT('Ctrl Pts',(-160.505648299763,5.73752527440648,
129.350555638804));
#159091=CARTESIAN_POINT('Ctrl Pts',(-160.513045789099,5.69478277987167,
129.198938662883));
#159092=CARTESIAN_POINT('Ctrl Pts',(-160.520445871614,5.65202530202185,
129.047268537867));
#159093=CARTESIAN_POINT('Ctrl Pts',(-160.527845954129,5.60322219938922,
128.897370615798));
#159094=CARTESIAN_POINT('Ctrl Pts',(-160.535246036644,5.54855955702418,
128.749751797217));
#159095=CARTESIAN_POINT('Ctrl Pts',(-160.542654256311,5.49383680746418,
128.601970656568));
#159096=CARTESIAN_POINT('Ctrl Pts',(-160.550062475977,5.43324178045389,
128.456473974554));
#159097=CARTESIAN_POINT('Ctrl Pts',(-160.557470695644,5.36700867335544,
128.313748551702));
#159098=CARTESIAN_POINT('Ctrl Pts',(-160.564883474946,5.30073480088472,
128.170935283734));
#159099=CARTESIAN_POINT('Ctrl Pts',(-160.572296254248,5.2288161037707,128.030897004974));
#159100=CARTESIAN_POINT('Ctrl Pts',(-160.57970903355,5.15153207972547,127.894094685721));
#159101=CARTESIAN_POINT('Ctrl Pts',(-160.587132404579,5.07413762864232,
127.757096896898));
#159102=CARTESIAN_POINT('Ctrl Pts',(-160.594555775608,4.99136273537086,
127.623344618718));
#159103=CARTESIAN_POINT('Ctrl Pts',(-160.601979146636,4.90352988617272,
127.493269374802));
#159104=CARTESIAN_POINT('Ctrl Pts',(-160.605915196077,4.85695880200896,
127.424300359367));
#159105=CARTESIAN_POINT('Ctrl Pts',(-160.609851245518,4.80896641999349,
127.356364539404));
#159106=CARTESIAN_POINT('Ctrl Pts',(-160.613787294958,4.75960521233209,
127.289522245003));
#159107=CARTESIAN_POINT('Ctrl Pts',(-160.621210561364,4.66651151519086,
127.163459763835));
#159108=CARTESIAN_POINT('Ctrl Pts',(-160.628633827769,4.56826527082558,
127.040907723338));
#159109=CARTESIAN_POINT('Ctrl Pts',(-160.636057094175,4.46516037098241,
126.922315612172));
#159110=CARTESIAN_POINT('Ctrl Pts',(-160.643471586896,4.36217733256824,
126.803863667031));
#159111=CARTESIAN_POINT('Ctrl Pts',(-160.650886079617,4.25434731174153,
126.689362614007));
#159112=CARTESIAN_POINT('Ctrl Pts',(-160.658300572338,4.14200690259376,
126.579232290359));
#159113=CARTESIAN_POINT('Ctrl Pts',(-160.665707918692,4.02977477136156,
126.469208114463));
#159114=CARTESIAN_POINT('Ctrl Pts',(-160.673115265045,3.91304117117206,
126.363546540911));
#159115=CARTESIAN_POINT('Ctrl Pts',(-160.680522611399,3.79218223348808,
126.262633581458));
#159116=CARTESIAN_POINT('Ctrl Pts',(-160.687924433075,3.67141343695992,
126.161795886697));
#159117=CARTESIAN_POINT('Ctrl Pts',(-160.69532625475,3.54652571463779,126.065699992266));
#159118=CARTESIAN_POINT('Ctrl Pts',(-160.702728076425,3.41793115834349,
125.974694256488));
#159119=CARTESIAN_POINT('Ctrl Pts',(-160.710125990737,3.28940448611521,
125.883736561931));
#159120=CARTESIAN_POINT('Ctrl Pts',(-160.717523905048,3.15717518093391,
125.797863889724));
#159121=CARTESIAN_POINT('Ctrl Pts',(-160.724921819359,3.02168734399846,
125.717383503639));
#159122=CARTESIAN_POINT('Ctrl Pts',(-160.732318504271,2.88622202268293,
125.636916491934));
#159123=CARTESIAN_POINT('Ctrl Pts',(-160.739715189184,2.74749956497993,
125.561840178314));
#159124=CARTESIAN_POINT('Ctrl Pts',(-160.747111874096,2.60599200398201,
125.492417824418));
#159125=CARTESIAN_POINT('Ctrl Pts',(-160.754508231031,2.46449071757763,
125.422998548781));
#159126=CARTESIAN_POINT('Ctrl Pts',(-160.761904587967,2.32020490856619,
125.359232898803));
#159127=CARTESIAN_POINT('Ctrl Pts',(-160.769300944902,2.17362985112807,
125.301337463627));
#159128=CARTESIAN_POINT('Ctrl Pts',(-160.776698434239,2.02703235267489,
125.243433164513));
#159129=CARTESIAN_POINT('Ctrl Pts',(-160.784095923575,1.87814525514074,
125.191401006869));
#159130=CARTESIAN_POINT('Ctrl Pts',(-160.791493412912,1.72748223694418,
125.145408799116));
#159131=CARTESIAN_POINT('Ctrl Pts',(-160.798893495427,1.57676640405821,
125.099400468865));
#159132=CARTESIAN_POINT('Ctrl Pts',(-160.806293577942,1.42427376783506,
125.059436412946));
#159133=CARTESIAN_POINT('Ctrl Pts',(-160.813693660457,1.27053138157105,
125.025634064861));
#159134=CARTESIAN_POINT('Ctrl Pts',(-160.821101880124,1.11661993974935,
124.991794547618));
#159135=CARTESIAN_POINT('Ctrl Pts',(-160.82851009979,0.961456368275483,
124.9641303494));
#159136=CARTESIAN_POINT('Ctrl Pts',(-160.835918319456,0.805576815615801,
124.942707560907));
#159137=CARTESIAN_POINT('Ctrl Pts',(-160.843331098758,0.649601321692446,
124.921271587045));
#159138=CARTESIAN_POINT('Ctrl Pts',(-160.850743878061,0.492909339179487,
124.906084713475));
#159139=CARTESIAN_POINT('Ctrl Pts',(-160.858156657363,0.336039770785305,
124.897160956563));
#159140=CARTESIAN_POINT('Ctrl Pts',(-160.865580028391,0.178946059795572,
124.888224448969));
#159141=CARTESIAN_POINT('Ctrl Pts',(-160.87300339942,0.0216746283987935,
124.885568937547));
#159142=CARTESIAN_POINT('Ctrl Pts',(-160.880426770449,-0.135237158657845,
124.889156354532));
#159143=CARTESIAN_POINT('Ctrl Pts',(-160.88436281989,-0.218435553201027,
124.891058489096));
#159144=CARTESIAN_POINT('Ctrl Pts',(-160.88829886933,-0.301532937337538,
124.894714869186));
#159145=CARTESIAN_POINT('Ctrl Pts',(-160.892234918771,-0.384450191146429,
124.900113958336));
#159146=CARTESIAN_POINT('Ctrl Pts',(-160.899658185177,-0.540829544073461,
124.910296471973));
#159147=CARTESIAN_POINT('Ctrl Pts',(-160.907081451582,-0.69704054147606,
124.926711448447));
#159148=CARTESIAN_POINT('Ctrl Pts',(-160.914504717987,-0.852546160146982,
124.949354587909));
#159149=CARTESIAN_POINT('Ctrl Pts',(-160.921919210708,-1.00786798409102,
124.971970965061));
#159150=CARTESIAN_POINT('Ctrl Pts',(-160.929333703429,-1.1624857229909,
125.000800799484));
#159151=CARTESIAN_POINT('Ctrl Pts',(-160.93674819615,-1.31586421854117,
125.035787837331));
#159152=CARTESIAN_POINT('Ctrl Pts',(-160.944155542504,-1.46909488212195,
125.070741153354));
#159153=CARTESIAN_POINT('Ctrl Pts',(-160.951562888858,-1.62108831872102,
125.111839775829));
#159154=CARTESIAN_POINT('Ctrl Pts',(-160.958970235212,-1.77131645747413,
125.158975903485));
#159155=CARTESIAN_POINT('Ctrl Pts',(-160.966372056887,-1.92143255041314,
125.206076875238));
#159156=CARTESIAN_POINT('Ctrl Pts',(-160.973773878562,-2.06978561244166,
125.259206274819));
#159157=CARTESIAN_POINT('Ctrl Pts',(-160.981175700238,-2.21585981414128,
125.31820569389));
#159158=CARTESIAN_POINT('Ctrl Pts',(-160.988573614549,-2.36185690440853,
125.377173967627));
#159159=CARTESIAN_POINT('Ctrl Pts',(-160.995971528861,-2.50557718490952,
125.442005950122));
#159160=CARTESIAN_POINT('Ctrl Pts',(-161.003369443172,-2.64652209838561,
125.51249409003));
#159161=CARTESIAN_POINT('Ctrl Pts',(-161.010766128084,-2.78744358937308,
125.582970516088));
#159162=CARTESIAN_POINT('Ctrl Pts',(-161.018162812996,-2.92559029516622,
125.659101067226));
#159163=CARTESIAN_POINT('Ctrl Pts',(-161.025559497909,-3.06048558087654,
125.74063090798));
#159164=CARTESIAN_POINT('Ctrl Pts',(-161.032955854844,-3.19537488518891,
125.822157133616));
#159165=CARTESIAN_POINT('Ctrl Pts',(-161.04035221178,-3.32701273660073,
125.909081979748));
#159166=CARTESIAN_POINT('Ctrl Pts',(-161.047748568715,-3.45494920473856,
126.001105829906));
#159167=CARTESIAN_POINT('Ctrl Pts',(-161.055146058052,-3.58290526027554,
126.09314376915));
#159168=CARTESIAN_POINT('Ctrl Pts',(-161.062543547388,-3.70715850111594,
126.190282048845));
#159169=CARTESIAN_POINT('Ctrl Pts',(-161.069941036725,-3.82729008954988,
126.29217920134));
#159170=CARTESIAN_POINT('Ctrl Pts',(-161.07734111924,-3.94746378992712,
126.394112073725));
#159171=CARTESIAN_POINT('Ctrl Pts',(-161.084741201755,-4.06351267673059,
126.500806898996));
#159172=CARTESIAN_POINT('Ctrl Pts',(-161.09214128427,-4.17505306464934,
126.611883727962));
#159173=CARTESIAN_POINT('Ctrl Pts',(-161.099549503937,-4.28671610269077,
126.723082697321));
#159174=CARTESIAN_POINT('Ctrl Pts',(-161.106957723603,-4.39386047660583,
126.83867302959));
#159175=CARTESIAN_POINT('Ctrl Pts',(-161.11436594327,-4.49614078107216,
126.958239371521));
#159176=CARTESIAN_POINT('Ctrl Pts',(-161.121778722572,-4.59848403735984,
127.077879304541));
#159177=CARTESIAN_POINT('Ctrl Pts',(-161.129191501874,-4.69595702817189,
127.201499831054));
#159178=CARTESIAN_POINT('Ctrl Pts',(-161.136604281176,-4.7882566710658,
127.328655133136));
#159179=CARTESIAN_POINT('Ctrl Pts',(-161.144027652205,-4.88068819601723,
127.455992120677));
#159180=CARTESIAN_POINT('Ctrl Pts',(-161.151451023234,-4.9679314032225,
127.586873661283));
#159181=CARTESIAN_POINT('Ctrl Pts',(-161.158874394263,-5.04972786139977,
127.720827078215));
#159182=CARTESIAN_POINT('Ctrl Pts',(-161.162810443703,-5.09309830620011,
127.791852394034));
#159183=CARTESIAN_POINT('Ctrl Pts',(-161.166746493143,-5.13493825596471,
127.863740939493));
#159184=CARTESIAN_POINT('Ctrl Pts',(-161.170682542584,-5.17521465039959,
127.93641991302));
#159185=CARTESIAN_POINT('Ctrl Pts',(-161.178467267524,-5.25487336836381,
128.080164504248));
#159186=CARTESIAN_POINT('Ctrl Pts',(-161.186251992465,-5.32863465868597,
128.22740185616));
#159187=CARTESIAN_POINT('Ctrl Pts',(-161.194036717405,-5.39619452720069,
128.377631298687));
#159188=CARTESIAN_POINT('Ctrl Pts',(-161.201808871549,-5.46364529984529,
128.527618150277));
#159189=CARTESIAN_POINT('Ctrl Pts',(-161.209581025693,-5.52491447891031,
128.680587171784));
#159190=CARTESIAN_POINT('Ctrl Pts',(-161.217353179838,-5.57974322839213,
128.836012053995));
#159191=CARTESIAN_POINT('Ctrl Pts',(-161.225209148834,-5.63516325069629,
128.993113036967));
#159192=CARTESIAN_POINT('Ctrl Pts',(-161.23306511783,-5.68400292496206,
129.152722890867));
#159193=CARTESIAN_POINT('Ctrl Pts',(-161.240921086826,-5.72604313071144,
129.314273161162));
#159194=CARTESIAN_POINT('Ctrl Pts',(-161.248666503456,-5.76749172972071,
129.473550030862));
#159195=CARTESIAN_POINT('Ctrl Pts',(-161.256411920086,-5.8023308548413,
129.634712746245));
#159196=CARTESIAN_POINT('Ctrl Pts',(-161.264157336717,-5.83039894683897,
129.797196935139));
#159197=CARTESIAN_POINT('Ctrl Pts',(-161.272068581896,-5.85906797371045,
129.963159893291));
#159198=CARTESIAN_POINT('Ctrl Pts',(-161.279979827075,-5.88067262040033,
130.130501244622));
#159199=CARTESIAN_POINT('Ctrl Pts',(-161.287891072254,-5.89509459606671,
130.298603496089));
#159200=CARTESIAN_POINT('Ctrl Pts',(-161.295802317433,-5.90951657173305,
130.466705747554));
#159201=CARTESIAN_POINT('Ctrl Pts',(-161.303713562612,-5.916755785072,130.635568548246));
#159202=CARTESIAN_POINT('Ctrl Pts',(-161.311624807791,-5.91674999652907,
130.804563282823));
#159203=CARTESIAN_POINT('',(-163.061624807791,-5.91686277527085,130.809721141343));
#159204=CARTESIAN_POINT('Ctrl Pts',(-161.311624807829,-5.91674999652905,
130.804563283627));
#159205=CARTESIAN_POINT('Ctrl Pts',(-161.31939311633,-5.91674431254827,
130.970504700389));
#159206=CARTESIAN_POINT('Ctrl Pts',(-161.327161424832,-5.90975332908639,
131.13630374045));
#159207=CARTESIAN_POINT('Ctrl Pts',(-161.334929733334,-5.89583865538439,
131.301368778641));
#159208=CARTESIAN_POINT('Ctrl Pts',(-161.342708486022,-5.88190527394895,
131.466655740307));
#159209=CARTESIAN_POINT('Ctrl Pts',(-161.35048723871,-5.86102964709646,
131.631206417196));
#159210=CARTESIAN_POINT('Ctrl Pts',(-161.358265991398,-5.83332481242634,
131.794437480861));
#159211=CARTESIAN_POINT('Ctrl Pts',(-161.366063440059,-5.80555339010722,
131.95806086496));
#159212=CARTESIAN_POINT('Ctrl Pts',(-161.37386088872,-5.77091998786326,
132.120357981835));
#159213=CARTESIAN_POINT('Ctrl Pts',(-161.381658337382,-5.7295885904063,
132.280756617014));
#159214=CARTESIAN_POINT('Ctrl Pts',(-161.389465416141,-5.68820614735775,
132.441353349613));
#159215=CARTESIAN_POINT('Ctrl Pts',(-161.397272494899,-5.64010928699573,
132.600046619344));
#159216=CARTESIAN_POINT('Ctrl Pts',(-161.405079573658,-5.5855110710074,
132.756281885997));
#159217=CARTESIAN_POINT('Ctrl Pts',(-161.412904931998,-5.53078501815113,
132.912882963635));
#159218=CARTESIAN_POINT('Ctrl Pts',(-161.420730290337,-5.46952728045612,
133.067014234323));
#159219=CARTESIAN_POINT('Ctrl Pts',(-161.428555648677,-5.40199896495129,
133.218141416472));
#159220=CARTESIAN_POINT('Ctrl Pts',(-161.43541382125,-5.34281690309353,
133.350589829784));
#159221=CARTESIAN_POINT('Ctrl Pts',(-161.442271993823,-5.27881928973841,
133.480731107596));
#159222=CARTESIAN_POINT('Ctrl Pts',(-161.449130166396,-5.21020966922348,
133.608223268487));
#159223=CARTESIAN_POINT('Ctrl Pts',(-161.456553432802,-5.135946811937,133.7462204193));
#159224=CARTESIAN_POINT('Ctrl Pts',(-161.463976699207,-5.05608540342793,
133.881473820707));
#159225=CARTESIAN_POINT('Ctrl Pts',(-161.471399965612,-4.97085257714099,
134.013496828267));
#159226=CARTESIAN_POINT('Ctrl Pts',(-161.478814458333,-4.88572048897633,
134.145363795596));
#159227=CARTESIAN_POINT('Ctrl Pts',(-161.486228951054,-4.79522982038961,
134.274007658384));
#159228=CARTESIAN_POINT('Ctrl Pts',(-161.493643443775,-4.69965418269364,
134.398965063898));
#159229=CARTESIAN_POINT('Ctrl Pts',(-161.501050790129,-4.60417066439565,
134.52380203076));
#159230=CARTESIAN_POINT('Ctrl Pts',(-161.508458136482,-4.50361215935036,
134.644959319442));
#159231=CARTESIAN_POINT('Ctrl Pts',(-161.515865482836,-4.39829621611526,
134.762001449906));
#159232=CARTESIAN_POINT('Ctrl Pts',(-161.523267304511,-4.29305882148397,
134.878956285933));
#159233=CARTESIAN_POINT('Ctrl Pts',(-161.530669126187,-4.18307130238067,
134.991801798711));
#159234=CARTESIAN_POINT('Ctrl Pts',(-161.538070947862,-4.06869214699103,
135.100134677676));
#159235=CARTESIAN_POINT('Ctrl Pts',(-161.545468862173,-3.95437337146752,
135.208410368557));
#159236=CARTESIAN_POINT('Ctrl Pts',(-161.552866776484,-3.83566784702602,
135.312177913807));
#159237=CARTESIAN_POINT('Ctrl Pts',(-161.560264690796,-3.71297157878944,
135.411070139296));
#159238=CARTESIAN_POINT('Ctrl Pts',(-161.567661375708,-3.59029570044652,
135.509945930692));
#159239=CARTESIAN_POINT('Ctrl Pts',(-161.57505806062,-3.46363068490344,
135.603947776284));
#159240=CARTESIAN_POINT('Ctrl Pts',(-161.582454745532,-3.3334064305968,
135.692748095146));
#159241=CARTESIAN_POINT('Ctrl Pts',(-161.589851102467,-3.20318795057005,
135.781544476507));
#159242=CARTESIAN_POINT('Ctrl Pts',(-161.597247459403,-3.06941085399642,
135.86513957942));
#159243=CARTESIAN_POINT('Ctrl Pts',(-161.604643816338,-2.93253466822418,
135.94324872514));
#159244=CARTESIAN_POINT('Ctrl Pts',(-161.612041305675,-2.79563752635846,
136.021369829569));
#159245=CARTESIAN_POINT('Ctrl Pts',(-161.619438795011,-2.65564067478649,
136.094003119394));
#159246=CARTESIAN_POINT('Ctrl Pts',(-161.626836284348,-2.51302878103162,
136.160909591318));
#159247=CARTESIAN_POINT('Ctrl Pts',(-161.634236366863,-2.37036689489867,
136.227839517203));
#159248=CARTESIAN_POINT('Ctrl Pts',(-161.641636449378,-2.22508847918491,
136.289038469762));
#159249=CARTESIAN_POINT('Ctrl Pts',(-161.649036531892,-2.07769858934638,
136.344315412899));
#159250=CARTESIAN_POINT('Ctrl Pts',(-161.656444751559,-1.93014662917171,
136.399653138717));
#159251=CARTESIAN_POINT('Ctrl Pts',(-161.663852971225,-1.78047890785916,
136.449055719338));
#159252=CARTESIAN_POINT('Ctrl Pts',(-161.671261190892,-1.62921676974423,
136.492381651255));
#159253=CARTESIAN_POINT('Ctrl Pts',(-161.678673970194,-1.47786153230723,
136.535734249559));
#159254=CARTESIAN_POINT('Ctrl Pts',(-161.686086749496,-1.32491028447664,
136.57300265842));
#159255=CARTESIAN_POINT('Ctrl Pts',(-161.693499528798,-1.17089448651533,
136.60409653086));
#159256=CARTESIAN_POINT('Ctrl Pts',(-161.700922899826,-1.01665862355904,
136.635234831682));
#159257=CARTESIAN_POINT('Ctrl Pts',(-161.708346270855,-0.861355540132692,
136.66018091659));
#159258=CARTESIAN_POINT('Ctrl Pts',(-161.715769641884,-0.705522565048401,
136.67889621391));
#159259=CARTESIAN_POINT('Ctrl Pts',(-161.719705691326,-0.622896182474263,
136.688819513619));
#159260=CARTESIAN_POINT('Ctrl Pts',(-161.723641740768,-0.540120853656633,
136.696991986241));
#159261=CARTESIAN_POINT('Ctrl Pts',(-161.727577790209,-0.457276534927223,
136.703413824065));
#159262=CARTESIAN_POINT('Ctrl Pts',(-161.735001056615,-0.301034735329166,
136.715525209779));
#159263=CARTESIAN_POINT('Ctrl Pts',(-161.74242432302,-0.1440751761255,136.721443312216));
#159264=CARTESIAN_POINT('Ctrl Pts',(-161.749847589426,0.0130699437580426,
136.721096181969));
#159265=CARTESIAN_POINT('Ctrl Pts',(-161.757262082147,0.170029331159972,
136.720749462001));
#159266=CARTESIAN_POINT('Ctrl Pts',(-161.764676574868,0.327173473037769,
136.714152249828));
#159267=CARTESIAN_POINT('Ctrl Pts',(-161.772091067589,0.483964644014953,
136.701284288926));
#159268=CARTESIAN_POINT('Ctrl Pts',(-161.779498413943,0.640604693758912,
136.688428730649));
#159269=CARTESIAN_POINT('Ctrl Pts',(-161.786905760296,0.796892080337304,
136.669314486353));
#159270=CARTESIAN_POINT('Ctrl Pts',(-161.79431310665,0.952288779307195,
136.643973331035));
#159271=CARTESIAN_POINT('Ctrl Pts',(-161.801714928326,1.10756957755577,
136.618651076106));
#159272=CARTESIAN_POINT('Ctrl Pts',(-161.809116750001,1.26196064407807,
136.587111217337));
#159273=CARTESIAN_POINT('Ctrl Pts',(-161.816518571676,1.41492889065313,
136.549437361779));
#159274=CARTESIAN_POINT('Ctrl Pts',(-161.823916485988,1.56781638648196,
136.511783393956));
#159275=CARTESIAN_POINT('Ctrl Pts',(-161.831314400299,1.71928219665713,
136.468001967198));
#159276=CARTESIAN_POINT('Ctrl Pts',(-161.83871231461,1.86880335674129,136.418227785244));
#159277=CARTESIAN_POINT('Ctrl Pts',(-161.846108999522,2.01829966912103,
136.368461874856));
#159278=CARTESIAN_POINT('Ctrl Pts',(-161.853505684435,2.16585161895605,
136.312705303604));
#159279=CARTESIAN_POINT('Ctrl Pts',(-161.860902369347,2.31095123252788,
136.251142691725));
#159280=CARTESIAN_POINT('Ctrl Pts',(-161.868298726282,2.45604441223079,
136.189582809596));
#159281=CARTESIAN_POINT('Ctrl Pts',(-161.875695083218,2.59868512823418,
136.122217544531));
#159282=CARTESIAN_POINT('Ctrl Pts',(-161.883091440153,2.73838548649179,
136.049279634088));
#159283=CARTESIAN_POINT('Ctrl Pts',(-161.89048892949,2.87810723323088,135.976330556664));
#159284=CARTESIAN_POINT('Ctrl Pts',(-161.897886418826,3.01488739493115,
135.897807307835));
#159285=CARTESIAN_POINT('Ctrl Pts',(-161.905283908163,3.14826291671537,
135.813988464995));
#159286=CARTESIAN_POINT('Ctrl Pts',(-161.912683990678,3.2816851930818,135.73014023959));
#159287=CARTESIAN_POINT('Ctrl Pts',(-161.920084073193,3.41170013743103,
135.640992922675));
#159288=CARTESIAN_POINT('Ctrl Pts',(-161.927484155708,3.5378740308729,135.546868172033));
#159289=CARTESIAN_POINT('Ctrl Pts',(-161.934892375374,3.66418666548178,
135.452639921551));
#159290=CARTESIAN_POINT('Ctrl Pts',(-161.942300595041,3.78664951491966,
135.35342353035));
#159291=CARTESIAN_POINT('Ctrl Pts',(-161.949708814707,3.90486172892967,
135.24958113408));
#159292=CARTESIAN_POINT('Ctrl Pts',(-161.957121594009,4.02314670058528,
135.145674824549));
#159293=CARTESIAN_POINT('Ctrl Pts',(-161.964534373311,4.13717555395143,
135.037137093263));
#159294=CARTESIAN_POINT('Ctrl Pts',(-161.971947152613,4.24658501030232,
134.924366238045));
#159295=CARTESIAN_POINT('Ctrl Pts',(-161.979370523642,4.35615079601509,
134.81143425054));
#159296=CARTESIAN_POINT('Ctrl Pts',(-161.986793894671,4.46108375383855,
134.694257336274));
#159297=CARTESIAN_POINT('Ctrl Pts',(-161.9942172657,4.5610609929833,134.573266716262));
#159298=CARTESIAN_POINT('Ctrl Pts',(-161.998153315141,4.61407132409991,
134.5091145864));
#159299=CARTESIAN_POINT('Ctrl Pts',(-162.002089364581,4.66568914388588,
134.443890779039));
#159300=CARTESIAN_POINT('Ctrl Pts',(-162.006025414022,4.71587139576867,
134.377662667641));
#159301=CARTESIAN_POINT('Ctrl Pts',(-162.013448680428,4.81051355668355,
134.252758516456));
#159302=CARTESIAN_POINT('Ctrl Pts',(-162.020871946833,4.9003330995738,134.123902872896));
#159303=CARTESIAN_POINT('Ctrl Pts',(-162.028295213239,4.98498182484608,
133.991504600579));
#159304=CARTESIAN_POINT('Ctrl Pts',(-162.03570970596,5.06953050235472,133.859262812024));
#159305=CARTESIAN_POINT('Ctrl Pts',(-162.043124198681,5.1489203280553,133.723487040583));
#159306=CARTESIAN_POINT('Ctrl Pts',(-162.050538691402,5.22284360585934,
133.584618740697));
#159307=CARTESIAN_POINT('Ctrl Pts',(-162.057946037756,5.29669563362507,
133.445884287307));
#159308=CARTESIAN_POINT('Ctrl Pts',(-162.065353384109,5.36509142853283,
133.304063566756));
#159309=CARTESIAN_POINT('Ctrl Pts',(-162.072760730463,5.42776690843336,
133.159626409407));
#159310=CARTESIAN_POINT('Ctrl Pts',(-162.080162552139,5.49039564259637,
133.015296978739));
#159311=CARTESIAN_POINT('Ctrl Pts',(-162.087564373814,5.54731240882532,
132.868355337822));
#159312=CARTESIAN_POINT('Ctrl Pts',(-162.094966195489,5.59829940089622,
132.719295180528));
#159313=CARTESIAN_POINT('Ctrl Pts',(-162.102364109801,5.64925947733088,
132.57031371093));
#159314=CARTESIAN_POINT('Ctrl Pts',(-162.109762024112,5.69429589320263,
132.419216304511));
#159315=CARTESIAN_POINT('Ctrl Pts',(-162.117159938424,5.73323930352933,
132.266515756724));
#159316=CARTESIAN_POINT('Ctrl Pts',(-162.124556623336,5.7721762421678,132.113840584998));
#159317=CARTESIAN_POINT('Ctrl Pts',(-162.131953308248,5.80502209270777,
131.959563162021));
#159318=CARTESIAN_POINT('Ctrl Pts',(-162.13934999316,5.83165760918026,131.804210652216));
#159319=CARTESIAN_POINT('Ctrl Pts',(-162.146746350096,5.85829194460595,
131.648865030905));
#159320=CARTESIAN_POINT('Ctrl Pts',(-162.154142707031,5.878716430416,131.49244478548));
#159321=CARTESIAN_POINT('Ctrl Pts',(-162.161539063967,5.89286315665971,
131.335486195356));
#159322=CARTESIAN_POINT('Ctrl Pts',(-162.168936553303,5.90701204880337,
131.17850357447));
#159323=CARTESIAN_POINT('Ctrl Pts',(-162.17633404264,5.91488123410928,131.020982816586));
#159324=CARTESIAN_POINT('Ctrl Pts',(-162.183731531977,5.91645479515706,
130.863464080773));
#159325=CARTESIAN_POINT('Ctrl Pts',(-162.191131614492,5.91802890781421,
130.705890127012));
#159326=CARTESIAN_POINT('Ctrl Pts',(-162.198531697007,5.91330299852247,
130.548318569779));
#159327=CARTESIAN_POINT('Ctrl Pts',(-162.205931779522,5.90231325142926,
130.391288172948));
#159328=CARTESIAN_POINT('Ctrl Pts',(-162.213339999188,5.89131141997936,
130.234085105053));
#159329=CARTESIAN_POINT('Ctrl Pts',(-162.220748218855,5.87403202154923,
130.077424758553));
#159330=CARTESIAN_POINT('Ctrl Pts',(-162.228156438521,5.85056306176411,
129.921840123288));
#159331=CARTESIAN_POINT('Ctrl Pts',(-162.235569217823,5.82707965722577,
129.766159728274));
#159332=CARTESIAN_POINT('Ctrl Pts',(-162.242981997125,5.79739917049999,
129.611556729531));
#159333=CARTESIAN_POINT('Ctrl Pts',(-162.250394776428,5.76166033979989,
129.458552053439));
#159334=CARTESIAN_POINT('Ctrl Pts',(-162.257818147456,5.72587044378254,
129.305328757091));
#159335=CARTESIAN_POINT('Ctrl Pts',(-162.265241518485,5.68400501402058,
129.153708703452));
#159336=CARTESIAN_POINT('Ctrl Pts',(-162.272664889514,5.63625231860867,
129.00419663518));
#159337=CARTESIAN_POINT('Ctrl Pts',(-162.276600938954,5.61093269369319,
128.924921749096));
#159338=CARTESIAN_POINT('Ctrl Pts',(-162.280536988395,5.58395874975827,
128.846239154367));
#159339=CARTESIAN_POINT('Ctrl Pts',(-162.284473037835,5.5553638968772,128.768221492709));
#159340=CARTESIAN_POINT('Ctrl Pts',(-162.291896304241,5.50143489675405,
128.621082617658));
#159341=CARTESIAN_POINT('Ctrl Pts',(-162.299319570646,5.44157465134277,
128.475865269586));
#159342=CARTESIAN_POINT('Ctrl Pts',(-162.306742837052,5.37593893879817,
128.333083399443));
#159343=CARTESIAN_POINT('Ctrl Pts',(-162.314157329773,5.3103808022151,128.190470285614));
#159344=CARTESIAN_POINT('Ctrl Pts',(-162.321571822494,5.23906094032782,
128.050287255844));
#159345=CARTESIAN_POINT('Ctrl Pts',(-162.328986315215,5.16218444400936,
127.913031800477));
#159346=CARTESIAN_POINT('Ctrl Pts',(-162.336393661568,5.0853820441524,127.775908637086));
#159347=CARTESIAN_POINT('Ctrl Pts',(-162.343801007922,5.00303385318983,
127.641707754139));
#159348=CARTESIAN_POINT('Ctrl Pts',(-162.351208354276,4.9153924098601,127.510905286217));
#159349=CARTESIAN_POINT('Ctrl Pts',(-162.358610175951,4.82781633282532,
127.38020037571));
#159350=CARTESIAN_POINT('Ctrl Pts',(-162.366011997627,4.73495507113505,
127.252889142151));
#159351=CARTESIAN_POINT('Ctrl Pts',(-162.373413819302,4.63710625384166,
127.129421685681));
#159352=CARTESIAN_POINT('Ctrl Pts',(-162.380811733613,4.53930909017728,
127.00601940672));
#159353=CARTESIAN_POINT('Ctrl Pts',(-162.388209647925,4.4365298457112,126.886457155622));
#159354=CARTESIAN_POINT('Ctrl Pts',(-162.395607562236,4.32910841468215,
126.771154585582));
#159355=CARTESIAN_POINT('Ctrl Pts',(-162.403004247148,4.22170483514626,
126.655871176739));
#159356=CARTESIAN_POINT('Ctrl Pts',(-162.41040093206,4.10966085435452,126.544846316883));
#159357=CARTESIAN_POINT('Ctrl Pts',(-162.417797616973,3.99335553530743,
126.438465276272));
#159358=CARTESIAN_POINT('Ctrl Pts',(-162.425193973908,3.87705537336007,
126.332088952709));
#159359=CARTESIAN_POINT('Ctrl Pts',(-162.432590330844,3.75649452430975,
126.230356290917));
#159360=CARTESIAN_POINT('Ctrl Pts',(-162.439986687779,3.63208746822846,
126.133614297583));
#159361=CARTESIAN_POINT('Ctrl Pts',(-162.447384177116,3.5076613651093,126.036857492803));
#159362=CARTESIAN_POINT('Ctrl Pts',(-162.454781666452,3.37938817715672,
125.945093107044));
#159363=CARTESIAN_POINT('Ctrl Pts',(-162.462179155789,3.24771375173889,
125.858626501253));
#159364=CARTESIAN_POINT('Ctrl Pts',(-162.469579238304,3.11599316805516,
125.772129584727));
#159365=CARTESIAN_POINT('Ctrl Pts',(-162.476979320819,2.98086928488876,
125.690934350475));
#159366=CARTESIAN_POINT('Ctrl Pts',(-162.484379403334,2.84281493796091,
125.615301570782));
#159367=CARTESIAN_POINT('Ctrl Pts',(-162.491787623,2.70460878608648,125.539585625074));
#159368=CARTESIAN_POINT('Ctrl Pts',(-162.499195842666,2.56346606280127,
125.469444528426));
#159369=CARTESIAN_POINT('Ctrl Pts',(-162.506604062333,2.41988275674233,
125.405092333241));
#159370=CARTESIAN_POINT('Ctrl Pts',(-162.514016841635,2.27621107755392,
125.340700530353));
#159371=CARTESIAN_POINT('Ctrl Pts',(-162.521429620937,2.13009616806607,
125.282104867221));
#159372=CARTESIAN_POINT('Ctrl Pts',(-162.528842400239,1.98205128979071,
125.22947019289));
#159373=CARTESIAN_POINT('Ctrl Pts',(-162.536265771268,1.83379487805087,
125.176760311669));
#159374=CARTESIAN_POINT('Ctrl Pts',(-162.543689142297,1.6836033454161,125.1300285409));
#159375=CARTESIAN_POINT('Ctrl Pts',(-162.551112513325,1.53200310968357,
125.08938931104));
#159376=CARTESIAN_POINT('Ctrl Pts',(-162.555048562766,1.45162102709549,
125.067841416241));
#159377=CARTESIAN_POINT('Ctrl Pts',(-162.558984612207,1.37084305615965,
125.048005494832));
#159378=CARTESIAN_POINT('Ctrl Pts',(-162.562920661648,1.28974837137003,
125.029892702593));
#159379=CARTESIAN_POINT('Ctrl Pts',(-162.570343928054,1.13680632674361,
124.995732541714));
#159380=CARTESIAN_POINT('Ctrl Pts',(-162.577767194459,0.982274934227822,
124.967601137744));
#159381=CARTESIAN_POINT('Ctrl Pts',(-162.585190460865,0.826670797211579,
124.945645233155));
#159382=CARTESIAN_POINT('Ctrl Pts',(-162.592604953586,0.671250571362725,
124.923715278621));
#159383=CARTESIAN_POINT('Ctrl Pts',(-162.600019446307,0.514760490792069,
124.907946346559));
#159384=CARTESIAN_POINT('Ctrl Pts',(-162.607433939028,0.357729964841097,
124.898434793891));
#159385=CARTESIAN_POINT('Ctrl Pts',(-162.614841285382,0.200850790823578,
124.888932408815));
#159386=CARTESIAN_POINT('Ctrl Pts',(-162.622248631736,0.0434325785518419,
124.885675418823));
#159387=CARTESIAN_POINT('Ctrl Pts',(-162.629655978089,-0.113987583111378,
124.888708718291));
#159388=CARTESIAN_POINT('Ctrl Pts',(-162.637057799765,-0.271290334878907,
124.89173975541));
#159389=CARTESIAN_POINT('Ctrl Pts',(-162.64445962144,-0.428594661520668,
124.90105173335));
#159390=CARTESIAN_POINT('Ctrl Pts',(-162.651861443116,-0.585361005267014,
124.916637538479));
#159391=CARTESIAN_POINT('Ctrl Pts',(-162.659259357427,-0.742044593280763,
124.932215115983));
#159392=CARTESIAN_POINT('Ctrl Pts',(-162.666657271738,-0.898190393466454,
124.954059888023));
#159393=CARTESIAN_POINT('Ctrl Pts',(-162.67405518605,-1.05326161856515,
124.982112724754));
#159394=CARTESIAN_POINT('Ctrl Pts',(-162.681451870962,-1.20830707363929,
125.010160899611));
#159395=CARTESIAN_POINT('Ctrl Pts',(-162.688848555874,-1.3622779410688,
125.044415025217));
#159396=CARTESIAN_POINT('Ctrl Pts',(-162.696245240786,-1.51464518926287,
125.084764433119));
#159397=CARTESIAN_POINT('Ctrl Pts',(-162.703641597722,-1.66700568133349,
125.125112051885));
#159398=CARTESIAN_POINT('Ctrl Pts',(-162.711037954657,-1.81776233469293,
125.171554319996));
#159399=CARTESIAN_POINT('Ctrl Pts',(-162.718434311593,-1.9663991661842,
125.223930089217));
#159400=CARTESIAN_POINT('Ctrl Pts',(-162.725831800929,-2.11505875435425,
125.276313877302));
#159401=CARTESIAN_POINT('Ctrl Pts',(-162.733229290266,-2.26159752233207,
125.334632851241));
#159402=CARTESIAN_POINT('Ctrl Pts',(-162.740626779603,-2.40551756991143,
125.398676962065));
#159403=CARTESIAN_POINT('Ctrl Pts',(-162.748026862118,-2.54948806844015,
125.462743523453));
#159404=CARTESIAN_POINT('Ctrl Pts',(-162.755426944633,-2.6908376780212,
125.532539065852));
#159405=CARTESIAN_POINT('Ctrl Pts',(-162.762827027148,-2.82909142428802,
125.607806732969));
#159406=CARTESIAN_POINT('Ctrl Pts',(-162.770235246814,-2.9674971947615,
125.683157164623));
#159407=CARTESIAN_POINT('Ctrl Pts',(-162.777643466481,-3.1027999754093,
125.763991559064));
#159408=CARTESIAN_POINT('Ctrl Pts',(-162.785051686147,-3.23455158390961,
125.850008327556));
#159409=CARTESIAN_POINT('Ctrl Pts',(-162.792464465449,-3.36638428332694,
125.936078037934));
#159410=CARTESIAN_POINT('Ctrl Pts',(-162.799877244751,-3.49466115186897,
126.027336262275));
#159411=CARTESIAN_POINT('Ctrl Pts',(-162.807290024053,-3.61896606698017,
126.123440284069));
#159412=CARTESIAN_POINT('Ctrl Pts',(-162.814713395082,-3.74344859478323,
126.219681623796));
#159413=CARTESIAN_POINT('Ctrl Pts',(-162.822136766111,-3.863947549065,126.320782350261));
#159414=CARTESIAN_POINT('Ctrl Pts',(-162.82956013714,-3.98008211456447,
126.426361425718));
#159415=CARTESIAN_POINT('Ctrl Pts',(-162.83349618658,-4.04165944779781,
126.482341984856));
#159416=CARTESIAN_POINT('Ctrl Pts',(-162.837432236021,-4.10201043665572,
126.539580979506));
#159417=CARTESIAN_POINT('Ctrl Pts',(-162.841368285461,-4.16108289971568,
126.598017827898));
#159418=CARTESIAN_POINT('Ctrl Pts',(-162.848687074464,-4.27092371841971,
126.706676768753));
#159419=CARTESIAN_POINT('Ctrl Pts',(-162.856005863466,-4.37669434539834,
126.819828129737));
#159420=CARTESIAN_POINT('Ctrl Pts',(-162.863324652469,-4.47799709319613,
126.937130006932));
#159421=CARTESIAN_POINT('Ctrl Pts',(-162.870634636601,-4.57917796869682,
127.054290764072));
#159422=CARTESIAN_POINT('Ctrl Pts',(-162.877944620732,-4.67590141054578,
127.175591814463));
#159423=CARTESIAN_POINT('Ctrl Pts',(-162.885254604864,-4.76780473015378,
127.300652779058));
#159424=CARTESIAN_POINT('Ctrl Pts',(-162.892603363319,-4.86019553222356,
127.426377104097));
#159425=CARTESIAN_POINT('Ctrl Pts',(-162.899952121774,-4.94771462715774,
127.555901093354));
#159426=CARTESIAN_POINT('Ctrl Pts',(-162.90730088023,-5.03003213962764,
127.688801721186));
#159427=CARTESIAN_POINT('Ctrl Pts',(-162.914597894588,-5.1117700378161,
127.820766568774));
#159428=CARTESIAN_POINT('Ctrl Pts',(-162.921894908946,-5.18837915329614,
127.956060330833));
#159429=CARTESIAN_POINT('Ctrl Pts',(-162.929191923305,-5.2595781789961,
128.094237383924));
#159430=CARTESIAN_POINT('Ctrl Pts',(-162.936485811445,-5.33074670130998,
128.23235523862));
#159431=CARTESIAN_POINT('Ctrl Pts',(-162.943779699586,-5.39650956936092,
128.373353585452));
#159432=CARTESIAN_POINT('Ctrl Pts',(-162.951073587727,-5.45663060084042,
128.516760773084));
#159433=CARTESIAN_POINT('Ctrl Pts',(-162.958365886117,-5.51673852854785,
128.660136704182));
#159434=CARTESIAN_POINT('Ctrl Pts',(-162.965658184507,-5.57120691878873,
128.805920076421));
#159435=CARTESIAN_POINT('Ctrl Pts',(-162.972950482897,-5.61984719435055,
128.953618043719));
#159436=CARTESIAN_POINT('Ctrl Pts',(-162.980340009971,-5.66913599384149,
129.103285277534));
#159437=CARTESIAN_POINT('Ctrl Pts',(-162.987729537046,-5.71243999132663,
129.254918155311));
#159438=CARTESIAN_POINT('Ctrl Pts',(-162.99511906412,-5.74961487539809,
129.407986975914));
#159439=CARTESIAN_POINT('Ctrl Pts',(-163.002415090189,-5.78631937902255,
129.559118989394));
#159440=CARTESIAN_POINT('Ctrl Pts',(-163.009711116258,-5.81704892816231,
129.711650428953));
#159441=CARTESIAN_POINT('Ctrl Pts',(-163.017007142327,-5.84171605951823,
129.865060855793));
#159442=CARTESIAN_POINT('Ctrl Pts',(-163.024443419904,-5.86685736713843,
130.021420291257));
#159443=CARTESIAN_POINT('Ctrl Pts',(-163.031879697481,-5.88570073750554,
130.178692438175));
#159444=CARTESIAN_POINT('Ctrl Pts',(-163.039315975059,-5.89820902089197,
130.336321187209));
#159445=CARTESIAN_POINT('Ctrl Pts',(-163.046752252636,-5.91071730427839,
130.493949936243));
#159446=CARTESIAN_POINT('Ctrl Pts',(-163.054188530214,-5.91689052196692,
130.651934866212));
#159447=CARTESIAN_POINT('Ctrl Pts',(-163.061624807791,-5.91674757180022,
130.809721036972));
#159448=CARTESIAN_POINT('',(-164.811624807791,-5.92507222483892,130.801692424892));
#159449=CARTESIAN_POINT('Ctrl Pts',(-163.061624807791,-5.91817580952646,
130.809722330918));
#159450=CARTESIAN_POINT('Ctrl Pts',(-163.081021841618,-5.92200279167935,
131.221400182703));
#159451=CARTESIAN_POINT('Ctrl Pts',(-163.193234750051,-5.69477883690624,
133.5987828848));
#159452=CARTESIAN_POINT('Ctrl Pts',(-163.398263533087,-2.47931000527729,
137.348868423979));
#159453=CARTESIAN_POINT('Ctrl Pts',(-163.676711156899,4.16595214925394,
136.42774067056));
#159454=CARTESIAN_POINT('Ctrl Pts',(-163.955158780713,6.98290779669783,
130.339001365844));
#159455=CARTESIAN_POINT('Ctrl Pts',(-164.233606404525,3.3829123129869,124.677904479389));
#159456=CARTESIAN_POINT('Ctrl Pts',(-164.512054028338,-3.3258143219058,
124.6467214899));
#159457=CARTESIAN_POINT('Ctrl Pts',(-164.704726829427,-5.85315069107131,
128.540611173087));
#159458=CARTESIAN_POINT('Ctrl Pts',(-164.804583755911,-5.92590807902851,
130.652707065092));
#159459=CARTESIAN_POINT('Ctrl Pts',(-164.811624807791,-5.92507222483892,
130.801692424892));
#159460=CARTESIAN_POINT('',(-166.561624807791,-5.90995365707892,130.800293572401));
#159461=CARTESIAN_POINT('Ctrl Pts',(-164.811624807791,-5.92507222483892,
130.801692424892));
#159462=CARTESIAN_POINT('Ctrl Pts',(-164.897399630515,-5.9148897625933,
132.616647497437));
#159463=CARTESIAN_POINT('Ctrl Pts',(-165.075990327845,-4.05023365468494,
136.413624265273));
#159464=CARTESIAN_POINT('Ctrl Pts',(-165.347396899777,2.41836483055078,
137.371633421151));
#159465=CARTESIAN_POINT('Ctrl Pts',(-165.625844523591,6.83241786724281,
132.319493158866));
#159466=CARTESIAN_POINT('Ctrl Pts',(-165.904292147403,4.96781266611051,
125.875020109467));
#159467=CARTESIAN_POINT('Ctrl Pts',(-166.182739771216,-1.46196968404082,
123.960370175338));
#159468=CARTESIAN_POINT('Ctrl Pts',(-166.401850658011,-5.46439026136785,
127.402783795988));
#159469=CARTESIAN_POINT('Ctrl Pts',(-166.528145670204,-5.91444494865032,
130.087230112169));
#159470=CARTESIAN_POINT('Ctrl Pts',(-166.561624807791,-5.90995365707892,
130.800293572401));
#159471=CARTESIAN_POINT('',(-168.311624841251,-5.9133887742954,130.808566527428));
#159472=CARTESIAN_POINT('Ctrl Pts',(-166.561624807791,-5.90995365707892,
130.800293572401));
#159473=CARTESIAN_POINT('Ctrl Pts',(-166.620961544808,-5.90199351813743,
132.0640913302));
#159474=CARTESIAN_POINT('Ctrl Pts',(-166.77311415643,-4.88443978267444,
135.316447813812));
#159475=CARTESIAN_POINT('Ctrl Pts',(-167.018082642654,0.475985509809786,
137.786552130608));
#159476=CARTESIAN_POINT('Ctrl Pts',(-167.296530266468,6.13159726050651,
134.17794558986));
#159477=CARTESIAN_POINT('Ctrl Pts',(-167.57497789028,6.15257067397626,127.469179268363));
#159478=CARTESIAN_POINT('Ctrl Pts',(-167.853425514094,0.51963220783115,
123.825281674103));
#159479=CARTESIAN_POINT('Ctrl Pts',(-168.098974486596,-4.86887118749209,
126.267595478663));
#159480=CARTESIAN_POINT('Ctrl Pts',(-168.251707584496,-5.90188748972451,
129.532545137536));
#159481=CARTESIAN_POINT('Ctrl Pts',(-168.311624807791,-5.91021739760105,
130.808563558795));
#159482=CARTESIAN_POINT('',(-170.061624807791,-5.92111310252186,130.806826412176));
#159483=CARTESIAN_POINT('Ctrl Pts',(-168.311624876699,-5.91674850288211,
130.808569672372));
#159484=CARTESIAN_POINT('Ctrl Pts',(-168.320088487823,-5.91662013988444,
130.989011982903));
#159485=CARTESIAN_POINT('Ctrl Pts',(-168.328552098947,-5.90823344174668,
131.169125107682));
#159486=CARTESIAN_POINT('Ctrl Pts',(-168.337015710071,-5.89170242808678,
131.348210837182));
#159487=CARTESIAN_POINT('Ctrl Pts',(-168.345517826292,-5.875096206779,131.528111315055));
#159488=CARTESIAN_POINT('Ctrl Pts',(-168.354019942514,-5.85027150266959,
131.70697488581));
#159489=CARTESIAN_POINT('Ctrl Pts',(-168.362522058735,-5.81739348635992,
131.884112249821));
#159490=CARTESIAN_POINT('Ctrl Pts',(-168.371076260356,-5.78431405377052,
132.062334787236));
#159491=CARTESIAN_POINT('Ctrl Pts',(-168.379630461977,-5.743082419642,132.238809761398));
#159492=CARTESIAN_POINT('Ctrl Pts',(-168.388184663598,-5.69391546743878,
132.412855943068));
#159493=CARTESIAN_POINT('Ctrl Pts',(-168.395563362972,-5.65150494504025,
132.562985026839));
#159494=CARTESIAN_POINT('Ctrl Pts',(-168.402942062346,-5.60319098766957,
132.711307263188));
#159495=CARTESIAN_POINT('Ctrl Pts',(-168.41032076172,-5.54914085771267,
132.857398927916));
#159496=CARTESIAN_POINT('Ctrl Pts',(-168.417744028125,-5.49476426726326,
133.004372980102));
#159497=CARTESIAN_POINT('Ctrl Pts',(-168.42516729453,-5.43446230746612,
133.14940746154));
#159498=CARTESIAN_POINT('Ctrl Pts',(-168.432590560936,-5.36839232004439,
133.291988897794));
#159499=CARTESIAN_POINT('Ctrl Pts',(-168.440005053656,-5.30240042186101,
133.43440181463));
#159500=CARTESIAN_POINT('Ctrl Pts',(-168.447419546377,-5.23065422140141,
133.574367121954));
#159501=CARTESIAN_POINT('Ctrl Pts',(-168.454834039098,-5.15336032277811,
133.711387955951));
#159502=CARTESIAN_POINT('Ctrl Pts',(-168.462241385452,-5.07614092292436,
133.848276724109));
#159503=CARTESIAN_POINT('Ctrl Pts',(-168.469648731806,-4.99338465206927,
133.982226345878));
#159504=CARTESIAN_POINT('Ctrl Pts',(-168.477056078159,-4.90534549697139,
134.112761457525));
#159505=CARTESIAN_POINT('Ctrl Pts',(-168.484457899835,-4.81737200479691,
134.243199211161));
#159506=CARTESIAN_POINT('Ctrl Pts',(-168.49185972151,-4.72412368163286,
134.370227217285));
#159507=CARTESIAN_POINT('Ctrl Pts',(-168.499261543185,-4.62589952510303,
134.493396283719));
#159508=CARTESIAN_POINT('Ctrl Pts',(-168.506659457496,-4.52772722034086,
134.616500330163));
#159509=CARTESIAN_POINT('Ctrl Pts',(-168.514057371808,-4.4245845455776,
134.735749202791));
#159510=CARTESIAN_POINT('Ctrl Pts',(-168.521455286119,-4.31681267075757,
134.850724284871));
#159511=CARTESIAN_POINT('Ctrl Pts',(-168.528851971031,-4.20905870566811,
134.965680260178));
#159512=CARTESIAN_POINT('Ctrl Pts',(-168.536248655943,-4.09667732237509,
135.076363582438));
#159513=CARTESIAN_POINT('Ctrl Pts',(-168.543645340855,-3.98004875475335,
135.182390136914));
#159514=CARTESIAN_POINT('Ctrl Pts',(-168.551041697791,-3.86342535856451,
135.288411990062));
#159515=CARTESIAN_POINT('Ctrl Pts',(-168.558438054726,-3.74255542871703,
135.389777234882));
#159516=CARTESIAN_POINT('Ctrl Pts',(-168.565834411661,-3.61785449953204,
135.486140127829));
#159517=CARTESIAN_POINT('Ctrl Pts',(-168.573231900998,-3.49313447831644,
135.58251777418));
#159518=CARTESIAN_POINT('Ctrl Pts',(-168.580629390334,-3.36458258529304,
135.673891315433));
#159519=CARTESIAN_POINT('Ctrl Pts',(-168.588026879671,-3.23264559517856,
135.759956749059));
#159520=CARTESIAN_POINT('Ctrl Pts',(-168.595426962186,-3.10066235475653,
135.84605235279));
#159521=CARTESIAN_POINT('Ctrl Pts',(-168.6028270447,-2.96529196711281,135.926835940332));
#159522=CARTESIAN_POINT('Ctrl Pts',(-168.610227127215,-2.82700805947962,
136.002048179755));
#159523=CARTESIAN_POINT('Ctrl Pts',(-168.617635346882,-2.68857209447425,
136.077343122768));
#159524=CARTESIAN_POINT('Ctrl Pts',(-168.625043566548,-2.54721653958297,
136.147054304629));
#159525=CARTESIAN_POINT('Ctrl Pts',(-168.632451786215,-2.4034380326473,
136.210969183546));
#159526=CARTESIAN_POINT('Ctrl Pts',(-168.639864565517,-2.25957103243927,
136.274923401004));
#159527=CARTESIAN_POINT('Ctrl Pts',(-168.647277344819,-2.11327845470429,
136.333074069203));
#159528=CARTESIAN_POINT('Ctrl Pts',(-168.654690124121,-1.96507406032067,
136.385257902049));
#159529=CARTESIAN_POINT('Ctrl Pts',(-168.662113495149,-1.81665790454848,
136.437516297604));
#159530=CARTESIAN_POINT('Ctrl Pts',(-168.669536866178,-1.6663248321565,
136.483790720553));
#159531=CARTESIAN_POINT('Ctrl Pts',(-168.676960237207,-1.51460160679054,
136.523968343207));
#159532=CARTESIAN_POINT('Ctrl Pts',(-168.680896286648,-1.43415431213647,
136.545271482791));
#159533=CARTESIAN_POINT('Ctrl Pts',(-168.68483233609,-1.35331634162635,
136.564861451967));
#159534=CARTESIAN_POINT('Ctrl Pts',(-168.688768385531,-1.27216690334182,
136.582727335986));
#159535=CARTESIAN_POINT('Ctrl Pts',(-168.696191651937,-1.1191215953542,
136.616421835664));
#159536=CARTESIAN_POINT('Ctrl Pts',(-168.703614918342,-0.96450529630121,
136.644082768928));
#159537=CARTESIAN_POINT('Ctrl Pts',(-168.711038184747,-0.808835053812479,
136.665564966352));
#159538=CARTESIAN_POINT('Ctrl Pts',(-168.718452677468,-0.653348800622317,
136.687021773602));
#159539=CARTESIAN_POINT('Ctrl Pts',(-168.72586717019,-0.496811449698955,
136.702314330648));
#159540=CARTESIAN_POINT('Ctrl Pts',(-168.733281662911,-0.339752701209014,
136.711347892355));
#159541=CARTESIAN_POINT('Ctrl Pts',(-168.740689009264,-0.182845331854025,
136.720372747175));
#159542=CARTESIAN_POINT('Ctrl Pts',(-168.748096355618,-0.0254179355759166,
136.723150595193));
#159543=CARTESIAN_POINT('Ctrl Pts',(-168.755503701972,0.131992264607301,
136.719638176953));
#159544=CARTESIAN_POINT('Ctrl Pts',(-168.762905523647,0.289285062324475,
136.716128378407));
#159545=CARTESIAN_POINT('Ctrl Pts',(-168.770307345323,0.446560317885286,
136.70633766334));
#159546=CARTESIAN_POINT('Ctrl Pts',(-168.777709166998,0.603278497670724,
136.690274787578));
#159547=CARTESIAN_POINT('Ctrl Pts',(-168.785107081309,0.759913947148946,
136.674220391283));
#159548=CARTESIAN_POINT('Ctrl Pts',(-168.792504995621,0.915992536105768,
136.651900466323));
#159549=CARTESIAN_POINT('Ctrl Pts',(-168.799902909932,1.07097765973953,
136.623375776065));
#159550=CARTESIAN_POINT('Ctrl Pts',(-168.807299594844,1.22593702765723,
136.594855826093));
#159551=CARTESIAN_POINT('Ctrl Pts',(-168.814696279757,1.37980292412841,
136.560133224793));
#159552=CARTESIAN_POINT('Ctrl Pts',(-168.822092964669,1.5320466568494,136.519320250296));
#159553=CARTESIAN_POINT('Ctrl Pts',(-168.829489321604,1.68428363892374,
136.478509085489));
#159554=CARTESIAN_POINT('Ctrl Pts',(-168.83688567854,1.83489823969964,136.431608181102));
#159555=CARTESIAN_POINT('Ctrl Pts',(-168.844282035475,1.98337496888992,
136.378780255096));
#159556=CARTESIAN_POINT('Ctrl Pts',(-168.851679524812,2.13187443024648,
136.325944241));
#159557=CARTESIAN_POINT('Ctrl Pts',(-168.859077014148,2.27823501657022,
136.267179523589));
#159558=CARTESIAN_POINT('Ctrl Pts',(-168.866474503485,2.42195946927794,
136.202697666295));
#159559=CARTESIAN_POINT('Ctrl Pts',(-168.873874586,2.56573430436995,136.138193204985));
#159560=CARTESIAN_POINT('Ctrl Pts',(-168.881274668515,2.70687082560657,
136.067967766285));
#159561=CARTESIAN_POINT('Ctrl Pts',(-168.88867475103,2.84489484260351,135.992279650958));
#159562=CARTESIAN_POINT('Ctrl Pts',(-168.896082970697,2.98307063119655,
135.916508308766));
#159563=CARTESIAN_POINT('Ctrl Pts',(-168.903491190363,3.11812675304043,
135.835262473623));
#159564=CARTESIAN_POINT('Ctrl Pts',(-168.91089941003,3.24961594582166,135.74884509698));
#159565=CARTESIAN_POINT('Ctrl Pts',(-168.918312189332,3.38118606800704,
135.662374531883));
#159566=CARTESIAN_POINT('Ctrl Pts',(-168.925724968634,3.50918458373577,
135.570726299582));
#159567=CARTESIAN_POINT('Ctrl Pts',(-168.933137747936,3.63319641549096,
135.474244381533));
#159568=CARTESIAN_POINT('Ctrl Pts',(-168.940561118964,3.75738544116676,
135.377624605596));
#159569=CARTESIAN_POINT('Ctrl Pts',(-168.947984489993,3.87757612147127,
135.276157590056));
#159570=CARTESIAN_POINT('Ctrl Pts',(-168.955407861022,3.99338880265521,
135.170225529966));
#159571=CARTESIAN_POINT('Ctrl Pts',(-168.959343910463,4.05479546510575,
135.114057809902));
#159572=CARTESIAN_POINT('Ctrl Pts',(-168.963279959904,4.1149719586162,135.056635392724));
#159573=CARTESIAN_POINT('Ctrl Pts',(-168.967216009344,4.17386628639581,
134.998019018746));
#159574=CARTESIAN_POINT('Ctrl Pts',(-168.97463927575,4.28493915055956,134.887470366778));
#159575=CARTESIAN_POINT('Ctrl Pts',(-168.982062542155,4.3917849634643,134.772338705508));
#159576=CARTESIAN_POINT('Ctrl Pts',(-168.989485808561,4.49400211308639,
134.652980574132));
#159577=CARTESIAN_POINT('Ctrl Pts',(-168.996900301282,4.59609845052623,
134.533763514154));
#159578=CARTESIAN_POINT('Ctrl Pts',(-169.004314794003,4.69357677368831,
134.410330208079));
#159579=CARTESIAN_POINT('Ctrl Pts',(-169.011729286724,4.78607105492777,
134.2830750956));
#159580=CARTESIAN_POINT('Ctrl Pts',(-169.019136633077,4.87847618669688,
134.155942636388));
#159581=CARTESIAN_POINT('Ctrl Pts',(-169.026543979431,4.96590662197317,
134.02499600403));
#159582=CARTESIAN_POINT('Ctrl Pts',(-169.033951325785,5.04803558318792,
133.890663796673));
#159583=CARTESIAN_POINT('Ctrl Pts',(-169.04135314746,5.13010328952486,133.756431779345));
#159584=CARTESIAN_POINT('Ctrl Pts',(-169.048754969136,5.20687720094412,
133.61881953193));
#159585=CARTESIAN_POINT('Ctrl Pts',(-169.056156790811,5.27807305286969,
133.47828571208));
#159586=CARTESIAN_POINT('Ctrl Pts',(-169.063554705123,5.34923132105902,
133.33782607894));
#159587=CARTESIAN_POINT('Ctrl Pts',(-169.070952619434,5.41481722581945,
133.19444827704));
#159588=CARTESIAN_POINT('Ctrl Pts',(-169.078350533745,5.4745918410901,133.048636611282));
#159589=CARTESIAN_POINT('Ctrl Pts',(-169.085747218657,5.5343565229042,132.902849176777));
#159590=CARTESIAN_POINT('Ctrl Pts',(-169.09314390357,5.58831169046194,132.754629026218));
#159591=CARTESIAN_POINT('Ctrl Pts',(-169.100540588482,5.63626603542987,
132.604481652486));
#159592=CARTESIAN_POINT('Ctrl Pts',(-169.107936945417,5.68421825405189,
132.454340936445));
#159593=CARTESIAN_POINT('Ctrl Pts',(-169.115333302353,5.7261700655739,132.302273522745));
#159594=CARTESIAN_POINT('Ctrl Pts',(-169.122729659288,5.76197973413347,
132.148801060998));
#159595=CARTESIAN_POINT('Ctrl Pts',(-169.130127148625,5.79779488524471,
131.995305102225));
#159596=CARTESIAN_POINT('Ctrl Pts',(-169.137524637961,5.82746593614781,
131.840404030635));
#159597=CARTESIAN_POINT('Ctrl Pts',(-169.144922127298,5.8509021007386,131.684630559159));
#159598=CARTESIAN_POINT('Ctrl Pts',(-169.152322209813,5.87434648084059,
131.528802481535));
#159599=CARTESIAN_POINT('Ctrl Pts',(-169.159722292328,5.8915515675544,131.372101764055));
#159600=CARTESIAN_POINT('Ctrl Pts',(-169.167122374843,5.90247836514137,
131.215066974393));
#159601=CARTESIAN_POINT('Ctrl Pts',(-169.174530594509,5.91341717786557,
131.057859508836));
#159602=CARTESIAN_POINT('Ctrl Pts',(-169.181938814176,5.91806388854385,
130.900317610106));
#159603=CARTESIAN_POINT('Ctrl Pts',(-169.189347033842,5.91643162260689,
130.742981325315));
#159604=CARTESIAN_POINT('Ctrl Pts',(-169.196759813144,5.91479835203747,
130.585548202665));
#159605=CARTESIAN_POINT('Ctrl Pts',(-169.204172592446,5.90687842287881,
130.428321318085));
#159606=CARTESIAN_POINT('Ctrl Pts',(-169.211585371748,5.8927368769358,130.271835818424));
#159607=CARTESIAN_POINT('Ctrl Pts',(-169.219008742777,5.8785751248888,130.115126724944));
#159608=CARTESIAN_POINT('Ctrl Pts',(-169.226432113806,5.85817404954565,
129.959161501258));
#159609=CARTESIAN_POINT('Ctrl Pts',(-169.233855484835,5.83164999030207,
129.804466146579));
#159610=CARTESIAN_POINT('Ctrl Pts',(-169.237791534276,5.8175862976549,129.722442957664));
#159611=CARTESIAN_POINT('Ctrl Pts',(-169.241727583717,5.80180205643049,
129.64077655028));
#159612=CARTESIAN_POINT('Ctrl Pts',(-169.245663633157,5.7843202636394,129.559543502424));
#159613=CARTESIAN_POINT('Ctrl Pts',(-169.253086899563,5.75135014802388,
129.406340509366));
#159614=CARTESIAN_POINT('Ctrl Pts',(-169.260510165968,5.71223939242906,
129.254216625775));
#159615=CARTESIAN_POINT('Ctrl Pts',(-169.267933432374,5.66707088226718,
129.103702457365));
#159616=CARTESIAN_POINT('Ctrl Pts',(-169.275347925095,5.62195575753318,
128.953366184201));
#159617=CARTESIAN_POINT('Ctrl Pts',(-169.282762417816,5.57079723602915,
128.804636193235));
#159618=CARTESIAN_POINT('Ctrl Pts',(-169.290176910537,5.51372932415616,
128.65803363818));
#159619=CARTESIAN_POINT('Ctrl Pts',(-169.297584256891,5.4567164164852,128.511572384187));
#159620=CARTESIAN_POINT('Ctrl Pts',(-169.304991603244,5.39380559195493,
128.367234829491));
#159621=CARTESIAN_POINT('Ctrl Pts',(-169.312398949598,5.32518081106764,
128.225527569085));
#159622=CARTESIAN_POINT('Ctrl Pts',(-169.319800771273,5.256607213131,128.0839259993));
#159623=CARTESIAN_POINT('Ctrl Pts',(-169.327202592949,5.18232830642846,
127.944951152179));
#159624=CARTESIAN_POINT('Ctrl Pts',(-169.334604414624,5.10257632068526,
127.809090103225));
#159625=CARTESIAN_POINT('Ctrl Pts',(-169.342002328936,5.02286643539454,
127.67330077426));
#159626=CARTESIAN_POINT('Ctrl Pts',(-169.349400243247,4.93768941353346,
127.540622290972));
#159627=CARTESIAN_POINT('Ctrl Pts',(-169.356798157558,4.84732356915969,
127.411517447249));
#159628=CARTESIAN_POINT('Ctrl Pts',(-169.364194842471,4.75697274194998,
127.282434058409));
#159629=CARTESIAN_POINT('Ctrl Pts',(-169.371591527383,4.66143501746512,
127.156923435997));
#159630=CARTESIAN_POINT('Ctrl Pts',(-169.378988212295,4.56103227435438,
127.035419764382));
#159631=CARTESIAN_POINT('Ctrl Pts',(-169.386384569231,4.46063398320649,
126.913921480367));
#159632=CARTESIAN_POINT('Ctrl Pts',(-169.393780926166,4.35537134014572,
126.796430081639));
#159633=CARTESIAN_POINT('Ctrl Pts',(-169.401177283101,4.24560661206784,
126.68334677895));
#159634=CARTESIAN_POINT('Ctrl Pts',(-169.408574772438,4.13582507872986,
126.570246162918));
#159635=CARTESIAN_POINT('Ctrl Pts',(-169.415972261774,4.02154034794373,
126.461555254602));
#159636=CARTESIAN_POINT('Ctrl Pts',(-169.423369751111,3.90315153407888,
126.357638379274));
#159637=CARTESIAN_POINT('Ctrl Pts',(-169.430769833626,3.78472121919869,
126.253685076047));
#159638=CARTESIAN_POINT('Ctrl Pts',(-169.438169916141,3.66218423721486,
126.154509383896));
#159639=CARTESIAN_POINT('Ctrl Pts',(-169.445569998656,3.5359726222131,126.060435220022));
#159640=CARTESIAN_POINT('Ctrl Pts',(-169.452978218323,3.4096222245656,125.966257611935));
#159641=CARTESIAN_POINT('Ctrl Pts',(-169.460386437989,3.27958942396931,
125.877192958201));
#159642=CARTESIAN_POINT('Ctrl Pts',(-169.467794657656,3.1463356719695,125.79352212468));
#159643=CARTESIAN_POINT('Ctrl Pts',(-169.475207436958,3.01299990450878,
125.709799793156));
#159644=CARTESIAN_POINT('Ctrl Pts',(-169.48262021626,2.87643955844939,125.631478082266));
#159645=CARTESIAN_POINT('Ctrl Pts',(-169.490032995562,2.73714002467679,
125.55879153044));
#159646=CARTESIAN_POINT('Ctrl Pts',(-169.497456366591,2.59764145319803,
125.48600112066));
#159647=CARTESIAN_POINT('Ctrl Pts',(-169.504879737619,2.45539621379955,
125.41886211007));
#159648=CARTESIAN_POINT('Ctrl Pts',(-169.512303108648,2.31090972880087,
125.357560934465));
#159649=CARTESIAN_POINT('Ctrl Pts',(-169.516239158089,2.23429952754937,
125.325057580257));
#159650=CARTESIAN_POINT('Ctrl Pts',(-169.52017520753,2.15705949817252,125.294194621429));
#159651=CARTESIAN_POINT('Ctrl Pts',(-169.52411125697,2.07926649835301,125.264994102221));
#159652=CARTESIAN_POINT('Ctrl Pts',(-169.531534523376,1.93255132852796,
125.209922834311));
#159653=CARTESIAN_POINT('Ctrl Pts',(-169.538957789781,1.78342487815733,
125.160601145754));
#159654=CARTESIAN_POINT('Ctrl Pts',(-169.546381056187,1.63237836244457,
125.117246108052));
#159655=CARTESIAN_POINT('Ctrl Pts',(-169.553795548908,1.48151037116932,
125.073942312405));
#159656=CARTESIAN_POINT('Ctrl Pts',(-169.561210041629,1.32872718702708,
125.036591232382));
#159657=CARTESIAN_POINT('Ctrl Pts',(-169.56862453435,1.17453970512887,125.005361820914));
#159658=CARTESIAN_POINT('Ctrl Pts',(-169.576031880704,1.02050083493077,
124.974162509528));
#159659=CARTESIAN_POINT('Ctrl Pts',(-169.583439227058,0.865060724971309,
124.949073193979));
#159660=CARTESIAN_POINT('Ctrl Pts',(-169.590846573412,0.708745023109134,
124.930212930053));
#159661=CARTESIAN_POINT('Ctrl Pts',(-169.598248395087,0.552545907394415,
124.911366732823));
#159662=CARTESIAN_POINT('Ctrl Pts',(-169.605650216763,0.395472869101588,
124.898740381201));
#159663=CARTESIAN_POINT('Ctrl Pts',(-169.613052038438,0.238061224484711,
124.892401769951));
#159664=CARTESIAN_POINT('Ctrl Pts',(-169.62044995275,0.0807326762501853,
124.886066504803));
#159665=CARTESIAN_POINT('Ctrl Pts',(-169.627847867061,-0.0769337502724467,
124.886012384565));
#159666=CARTESIAN_POINT('Ctrl Pts',(-169.635245781372,-0.234398257929557,
124.892255407137));
#159667=CARTESIAN_POINT('Ctrl Pts',(-169.642642466285,-0.391836597841968,
124.898497392233));
#159668=CARTESIAN_POINT('Ctrl Pts',(-169.650039151197,-0.549072712846464,
124.911034428431));
#159669=CARTESIAN_POINT('Ctrl Pts',(-169.657435836109,-0.705567328065082,
124.929830397364));
#159670=CARTESIAN_POINT('Ctrl Pts',(-169.664832193045,-0.862055004148467,
124.948625532864));
#159671=CARTESIAN_POINT('Ctrl Pts',(-169.67222854998,-1.01780087518644,
124.973679004766));
#159672=CARTESIAN_POINT('Ctrl Pts',(-169.679624906916,-1.17227157710454,
125.004902891881));
#159673=CARTESIAN_POINT('Ctrl Pts',(-169.687022396252,-1.32676592888146,
125.036131559452));
#159674=CARTESIAN_POINT('Ctrl Pts',(-169.694419885589,-1.47998435688509,
125.073532449308));
#159675=CARTESIAN_POINT('Ctrl Pts',(-169.701817374926,-1.63140461288007,
125.116966701934));
#159676=CARTESIAN_POINT('Ctrl Pts',(-169.709217457441,-1.78287794901085,
125.160416180369));
#159677=CARTESIAN_POINT('Ctrl Pts',(-169.716617539956,-1.93255149951431,
125.209903129633));
#159678=CARTESIAN_POINT('Ctrl Pts',(-169.724017622471,-2.07991921869906,
125.265239152371));
#159679=CARTESIAN_POINT('Ctrl Pts',(-169.731425842137,-2.22744898384103,
125.320636022755));
#159680=CARTESIAN_POINT('Ctrl Pts',(-169.738834061804,-2.37266750442005,
125.38189467975));
#159681=CARTESIAN_POINT('Ctrl Pts',(-169.74624228147,-2.51508905420318,
125.448778705959));
#159682=CARTESIAN_POINT('Ctrl Pts',(-169.753655060772,-2.65759826207378,
125.515703898171));
#159683=CARTESIAN_POINT('Ctrl Pts',(-169.761067840075,-2.79730673834968,
125.588261187052));
#159684=CARTESIAN_POINT('Ctrl Pts',(-169.768480619377,-2.93375479357592,
125.666168973255));
#159685=CARTESIAN_POINT('Ctrl Pts',(-169.775903990406,-3.07039781218206,
125.744188077756));
#159686=CARTESIAN_POINT('Ctrl Pts',(-169.783327361434,-3.20377078969541,
125.827572751073));
#159687=CARTESIAN_POINT('Ctrl Pts',(-169.790750732463,-3.33344367929301,
125.915998540195));
#159688=CARTESIAN_POINT('Ctrl Pts',(-169.794686781903,-3.402199356803,125.962884015326));
#159689=CARTESIAN_POINT('Ctrl Pts',(-169.798622831343,-3.46991536070847,
126.011186056468));
#159690=CARTESIAN_POINT('Ctrl Pts',(-169.802558880784,-3.53653160111034,
126.060851916525));
#159691=CARTESIAN_POINT('Ctrl Pts',(-169.809908808481,-3.66092651989311,
126.153594776088));
#159692=CARTESIAN_POINT('Ctrl Pts',(-169.817258736178,-3.78187706383077,
126.251388173978));
#159693=CARTESIAN_POINT('Ctrl Pts',(-169.824608663876,-3.89893990826541,
126.353945114016));
#159694=CARTESIAN_POINT('Ctrl Pts',(-169.831949870823,-4.01586385667119,
126.4563803694));
#159695=CARTESIAN_POINT('Ctrl Pts',(-169.839291077771,-4.12890900020466,
126.563567671924));
#159696=CARTESIAN_POINT('Ctrl Pts',(-169.846632284719,-4.23766145748654,
126.675177171141));
#159697=CARTESIAN_POINT('Ctrl Pts',(-169.853966461502,-4.3463097700869,
126.786679789685));
#159698=CARTESIAN_POINT('Ctrl Pts',(-169.861300638285,-4.45067331315389,
126.902595905783));
#159699=CARTESIAN_POINT('Ctrl Pts',(-169.868634815068,-4.55037192176472,
127.02255603032));
#159700=CARTESIAN_POINT('Ctrl Pts',(-169.875963645743,-4.64999785697112,
127.142428712206));
#159701=CARTESIAN_POINT('Ctrl Pts',(-169.883292476417,-4.74496538355266,
127.266339242789));
#159702=CARTESIAN_POINT('Ctrl Pts',(-169.890621307092,-4.83493196680158,
127.393882141032));
#159703=CARTESIAN_POINT('Ctrl Pts',(-169.897947000245,-4.92486003475322,
127.521370437306));
#159704=CARTESIAN_POINT('Ctrl Pts',(-169.905272693398,-5.00979119925454,
127.652487696564));
#159705=CARTESIAN_POINT('Ctrl Pts',(-169.912598386551,-5.08942400263278,
127.786796387276));
#159706=CARTESIAN_POINT('Ctrl Pts',(-169.919922553488,-5.16904021552028,
127.921077096466));
#159707=CARTESIAN_POINT('Ctrl Pts',(-169.927246720425,-5.24336006876812,
128.058547586537));
#159708=CARTESIAN_POINT('Ctrl Pts',(-169.934570887362,-5.31212627938997,
128.198742657405));
#159709=CARTESIAN_POINT('Ctrl Pts',(-169.941895044416,-5.38089239721408,
128.338937539084));
#159710=CARTESIAN_POINT('Ctrl Pts',(-169.949219201469,-5.44410471934802,
128.481856651774));
#159711=CARTESIAN_POINT('Ctrl Pts',(-169.956543358523,-5.50155276466311,
128.627011830594));
#159712=CARTESIAN_POINT('Ctrl Pts',(-169.963869021802,-5.55901262426792,
128.772196860828));
#159713=CARTESIAN_POINT('Ctrl Pts',(-169.971194685081,-5.61070570805527,
128.919618517567));
#159714=CARTESIAN_POINT('Ctrl Pts',(-169.97852034836,-5.65647044968558,
129.068770627294));
#159715=CARTESIAN_POINT('Ctrl Pts',(-169.985853043202,-5.70227911876219,
129.218065901191));
#159716=CARTESIAN_POINT('Ctrl Pts',(-169.993185738044,-5.74214796873194,
129.369094580373));
#159717=CARTESIAN_POINT('Ctrl Pts',(-170.000518432887,-5.7759657541962,
129.521336779575));
#159718=CARTESIAN_POINT('Ctrl Pts',(-170.007854831032,-5.80980061899016,
129.673655867156));
#159719=CARTESIAN_POINT('Ctrl Pts',(-170.015191229178,-5.83757826355815,
129.827189320821));
#159720=CARTESIAN_POINT('Ctrl Pts',(-170.022527627323,-5.85923908056783,
129.981409854004));
#159721=CARTESIAN_POINT('Ctrl Pts',(-170.029874413467,-5.88093056828681,
130.135848756289));
#159722=CARTESIAN_POINT('Ctrl Pts',(-170.037221199612,-5.8964878893391,
130.290976302403));
#159723=CARTESIAN_POINT('Ctrl Pts',(-170.044567985756,-5.90590348629985,
130.446262065473));
#159724=CARTESIAN_POINT('Ctrl Pts',(-170.050253593101,-5.91319012649709,
130.566436228403));
#159725=CARTESIAN_POINT('Ctrl Pts',(-170.055939200446,-5.91679950964778,
130.686705078958));
#159726=CARTESIAN_POINT('Ctrl Pts',(-170.061624807791,-5.91674948694934,
130.806824594987));
#159727=CARTESIAN_POINT('',(-171.811624807791,-5.91779838983984,130.798959891652));
#159728=CARTESIAN_POINT('Ctrl Pts',(-170.061624807791,-5.92528845016055,
130.806828150962));
#159729=CARTESIAN_POINT('Ctrl Pts',(-170.068085373393,-5.92600628089009,
130.943517473629));
#159730=CARTESIAN_POINT('Ctrl Pts',(-170.074545938994,-5.92168800861787,
131.080160639199));
#159731=CARTESIAN_POINT('Ctrl Pts',(-170.081006504596,-5.91218909021727,
131.216442711532));
#159732=CARTESIAN_POINT('Ctrl Pts',(-170.1738223792,-5.77572264540439,133.174342455337));
#159733=CARTESIAN_POINT('Ctrl Pts',(-170.35945412841,-3.36424981849401,
136.941084799823));
#159734=CARTESIAN_POINT('Ctrl Pts',(-170.637901752222,3.34454065233045,
136.951848588703));
#159735=CARTESIAN_POINT('Ctrl Pts',(-170.916349376035,6.97986165355384,
131.313371253588));
#159736=CARTESIAN_POINT('Ctrl Pts',(-171.194796999848,4.20103078036093,
125.207138010521));
#159737=CARTESIAN_POINT('Ctrl Pts',(-171.47324462366,-2.43834214822045,
124.244478903803));
#159738=CARTESIAN_POINT('Ctrl Pts',(-171.678853892974,-5.68636543667235,
127.98494676486));
#159739=CARTESIAN_POINT('Ctrl Pts',(-171.791647287685,-5.92174318505954,
130.374892560432));
#159740=CARTESIAN_POINT('Ctrl Pts',(-171.811624807791,-5.91779838983984,
130.798959891652));
#159741=CARTESIAN_POINT('',(-173.561624807791,-5.90693470452075,130.804363326736));
#159742=CARTESIAN_POINT('Ctrl Pts',(-171.811624807791,-5.91779838983984,
130.798959891652));
#159743=CARTESIAN_POINT('Ctrl Pts',(-171.88446316229,-5.90341560403291,
132.345116093169));
#159744=CARTESIAN_POINT('Ctrl Pts',(-172.050117391391,-4.49105891822915,
135.884762486509));
#159745=CARTESIAN_POINT('Ctrl Pts',(-172.3085874951,1.48279366496714,137.643869626081));
#159746=CARTESIAN_POINT('Ctrl Pts',(-172.587035118912,6.55575882898706,
133.253765995716));
#159747=CARTESIAN_POINT('Ctrl Pts',(-172.865482742725,5.60430189578342,
126.612778482949));
#159748=CARTESIAN_POINT('Ctrl Pts',(-173.143930366538,-0.49723469427191,
123.823650181717));
#159749=CARTESIAN_POINT('Ctrl Pts',(-173.37597772156,-5.20122531230544,
126.845253006048));
#159750=CARTESIAN_POINT('Ctrl Pts',(-173.515209201978,-5.90693067888632,
129.814505326009));
#159751=CARTESIAN_POINT('Ctrl Pts',(-173.561624807791,-5.90693470452075,
130.804363326736));
#159752=CARTESIAN_POINT('',(-175.311624807791,-5.91780836735944,130.809760420718));
#159753=CARTESIAN_POINT('Ctrl Pts',(-173.561624807791,-5.90693470452075,
130.804363326736));
#159754=CARTESIAN_POINT('Ctrl Pts',(-173.608025076582,-5.90693872882499,
131.793894250518));
#159755=CARTESIAN_POINT('Ctrl Pts',(-173.747241219977,-5.20156840285358,
134.762808706442));
#159756=CARTESIAN_POINT('Ctrl Pts',(-173.979273237976,-0.498387885347994,
137.784988816106));
#159757=CARTESIAN_POINT('Ctrl Pts',(-174.257720861789,5.6036093792587,134.996868513205));
#159758=CARTESIAN_POINT('Ctrl Pts',(-174.536168485602,6.55616337585614,
128.356038269631));
#159759=CARTESIAN_POINT('Ctrl Pts',(-174.814616109415,1.48392351643239,
123.965096656601));
#159760=CARTESIAN_POINT('Ctrl Pts',(-175.073101550145,-4.49057407776603,
125.723321227789));
#159761=CARTESIAN_POINT('Ctrl Pts',(-175.23877111627,-5.90342260648341,
129.263285342462));
#159762=CARTESIAN_POINT('Ctrl Pts',(-175.311624807791,-5.91780836735944,
130.809760420718));
#159763=CARTESIAN_POINT('',(-177.061624807791,-5.92149090377293,130.801889302419));
#159764=CARTESIAN_POINT('Ctrl Pts',(-175.311624807791,-5.91780836735944,
130.809760420718));
#159765=CARTESIAN_POINT('Ctrl Pts',(-175.331586990875,-5.92175011947117,
131.233500357588));
#159766=CARTESIAN_POINT('Ctrl Pts',(-175.351549173958,-5.8801256076613,
131.656471884122));
#159767=CARTESIAN_POINT('Ctrl Pts',(-175.464327231645,-5.37130495022946,
133.986320566974));
#159768=CARTESIAN_POINT('Ctrl Pts',(-175.649958980855,-2.43942579283476,
137.363839433112));
#159769=CARTESIAN_POINT('Ctrl Pts',(-175.928406604667,4.20010607429807,
136.402277149186));
#159770=CARTESIAN_POINT('Ctrl Pts',(-176.206854228481,6.97994564573954,
130.296503046127));
#159771=CARTESIAN_POINT('Ctrl Pts',(-176.485301852292,3.34555615804791,
124.657425240999));
#159772=CARTESIAN_POINT('Ctrl Pts',(-176.763749476106,-3.36323599938494,
124.667080752447));
#159773=CARTESIAN_POINT('Ctrl Pts',(-176.955857127938,-5.85947879357928,
128.56481640463));
#159774=CARTESIAN_POINT('Ctrl Pts',(-177.055148905167,-5.92600379227935,
130.664873565487));
#159775=CARTESIAN_POINT('Ctrl Pts',(-177.061624807791,-5.92528292508171,
130.801887719831));
#159776=CARTESIAN_POINT('',(-178.811624778335,-5.91300466705327,130.800158578124));
#159777=CARTESIAN_POINT('Ctrl Pts',(-177.061624807791,-5.91674948471524,
130.801891281235));
#159778=CARTESIAN_POINT('Ctrl Pts',(-177.068972291863,-5.91681426963166,
130.957121703259));
#159779=CARTESIAN_POINT('Ctrl Pts',(-177.076319775935,-5.91076597571889,
131.112601726254));
#159780=CARTESIAN_POINT('Ctrl Pts',(-177.083667260007,-5.89857192890814,
131.267803992745));
#159781=CARTESIAN_POINT('Ctrl Pts',(-177.091006448241,-5.88639165005279,
131.42283102472));
#159782=CARTESIAN_POINT('Ctrl Pts',(-177.098345636476,-5.86807945544121,
131.577580547625));
#159783=CARTESIAN_POINT('Ctrl Pts',(-177.10568482471,-5.84365464559986,
131.731523464891));
#159784=CARTESIAN_POINT('Ctrl Pts',(-177.113017405978,-5.81925182373462,
131.885327797937));
#159785=CARTESIAN_POINT('Ctrl Pts',(-177.120349987246,-5.78874739755558,
132.038326596132));
#159786=CARTESIAN_POINT('Ctrl Pts',(-177.127682568514,-5.75221258835055,
132.189994371818));
#159787=CARTESIAN_POINT('Ctrl Pts',(-177.135010225576,-5.71570231415444,
132.341560294768));
#159788=CARTESIAN_POINT('Ctrl Pts',(-177.142337882637,-5.67316980720683,
132.491796605054));
#159789=CARTESIAN_POINT('Ctrl Pts',(-177.149665539699,-5.62473759539901,
132.640186738255));
#159790=CARTESIAN_POINT('Ctrl Pts',(-177.156990698151,-5.5763218981673,
132.788526272897));
#159791=CARTESIAN_POINT('Ctrl Pts',(-177.164315856604,-5.52201061408288,
132.935020520132));
#159792=CARTESIAN_POINT('Ctrl Pts',(-177.171641015057,-5.46197646524778,
133.079166907249));
#159793=CARTESIAN_POINT('Ctrl Pts',(-177.178965039566,-5.4019516097736,
133.223290980325));
#159794=CARTESIAN_POINT('Ctrl Pts',(-177.186289064075,-5.33620579825766,
133.365067564186));
#159795=CARTESIAN_POINT('Ctrl Pts',(-177.193613088584,-5.26496024379123,
133.504013223698));
#159796=CARTESIAN_POINT('Ctrl Pts',(-177.200937495439,-5.1937109699983,
133.642966136776));
#159797=CARTESIAN_POINT('Ctrl Pts',(-177.208261902294,-5.11696155583199,
133.779087491855));
#159798=CARTESIAN_POINT('Ctrl Pts',(-177.215586309148,-5.03497947549541,
133.911917896819));
#159799=CARTESIAN_POINT('Ctrl Pts',(-177.222912614691,-4.95297614314753,
134.04478273508));
#159800=CARTESIAN_POINT('Ctrl Pts',(-177.230238920234,-4.86573764564598,
134.174354601081));
#159801=CARTESIAN_POINT('Ctrl Pts',(-177.237565225776,-4.77357498023392,
134.30020278657));
#159802=CARTESIAN_POINT('Ctrl Pts',(-177.24489916596,-4.68131627339521,
134.426182116695));
#159803=CARTESIAN_POINT('Ctrl Pts',(-177.252233106143,-4.58412337606316,
134.548429708487));
#159804=CARTESIAN_POINT('Ctrl Pts',(-177.259567046327,-4.48234821164094,
134.666547183761));
#159805=CARTESIAN_POINT('Ctrl Pts',(-177.266905027796,-4.38051696514717,
134.784729746356));
#159806=CARTESIAN_POINT('Ctrl Pts',(-177.274243009266,-4.27409868182224,
134.898777380797));
#159807=CARTESIAN_POINT('Ctrl Pts',(-177.281580990735,-4.16348187665067,
135.008328888771));
#159808=CARTESIAN_POINT('Ctrl Pts',(-177.288929892491,-4.05270045301331,
135.11804342985));
#159809=CARTESIAN_POINT('Ctrl Pts',(-177.296278794248,-3.93770830787742,
135.223248222139));
#159810=CARTESIAN_POINT('Ctrl Pts',(-177.303627696004,-3.81892739053334,
135.323622078063));
#159811=CARTESIAN_POINT('Ctrl Pts',(-177.30930003858,-3.72724484027508,
135.401096905637));
#159812=CARTESIAN_POINT('Ctrl Pts',(-177.314972381156,-3.63330573039015,
135.475694413771));
#159813=CARTESIAN_POINT('Ctrl Pts',(-177.320644723731,-3.53731516994476,
135.547285026723));
#159814=CARTESIAN_POINT('Ctrl Pts',(-177.328067990137,-3.41169449504985,
135.640974042324));
#159815=CARTESIAN_POINT('Ctrl Pts',(-177.335491256542,-3.28215913785233,
135.729810512298));
#159816=CARTESIAN_POINT('Ctrl Pts',(-177.342914522947,-3.14912059961039,
135.813449358206));
#159817=CARTESIAN_POINT('Ctrl Pts',(-177.350329015668,-3.0162393018725,
135.896989349945));
#159818=CARTESIAN_POINT('Ctrl Pts',(-177.35774350839,-2.87986337766262,
135.975343748868));
#159819=CARTESIAN_POINT('Ctrl Pts',(-177.365158001111,-2.7404366099266,
136.048208226858));
#159820=CARTESIAN_POINT('Ctrl Pts',(-177.372565347464,-2.60114422695826,
136.12100247532));
#159821=CARTESIAN_POINT('Ctrl Pts',(-177.379972693818,-2.45880718307821,
136.188317165231));
#159822=CARTESIAN_POINT('Ctrl Pts',(-177.387380040172,-2.3138973044699,
136.249891797062));
#159823=CARTESIAN_POINT('Ctrl Pts',(-177.394781861847,-2.16909550511661,
136.31142050421));
#159824=CARTESIAN_POINT('Ctrl Pts',(-177.402183683522,-2.02172503394739,
136.367217532269));
#159825=CARTESIAN_POINT('Ctrl Pts',(-177.409585505198,-1.87228122784675,
136.417068837878));
#159826=CARTESIAN_POINT('Ctrl Pts',(-177.416983419509,-1.72291631196724,
136.46689382737));
#159827=CARTESIAN_POINT('Ctrl Pts',(-177.424381333821,-1.57148059411923,
136.510779227457));
#159828=CARTESIAN_POINT('Ctrl Pts',(-177.431779248132,-1.41848814347019,
136.54855959996));
#159829=CARTESIAN_POINT('Ctrl Pts',(-177.439175933044,-1.26552111739154,
136.58633369405));
#159830=CARTESIAN_POINT('Ctrl Pts',(-177.446572617956,-1.11099823401281,
136.61800468472));
#159831=CARTESIAN_POINT('Ctrl Pts',(-177.453969302868,-0.955447549848219,
136.643457340689));
#159832=CARTESIAN_POINT('Ctrl Pts',(-177.461365659804,-0.799903762963973,
136.668908868061));
#159833=CARTESIAN_POINT('Ctrl Pts',(-177.468762016739,-0.643332634308196,
136.688142548689));
#159834=CARTESIAN_POINT('Ctrl Pts',(-177.476158373675,-0.486270944501928,
136.701094555182));
#159835=CARTESIAN_POINT('Ctrl Pts',(-177.483555863011,-0.329185208149992,
136.71404854466));
#159836=CARTESIAN_POINT('Ctrl Pts',(-177.490953352348,-0.171609133160149,
136.720718914368));
#159837=CARTESIAN_POINT('Ctrl Pts',(-177.498350841684,-0.0140829840808063,
136.721093857459));
#159838=CARTESIAN_POINT('Ctrl Pts',(-177.505750924199,0.143498385546124,
136.721468931986));
#159839=CARTESIAN_POINT('Ctrl Pts',(-177.513151006714,0.301029421353311,
136.715544185182));
#159840=CARTESIAN_POINT('Ctrl Pts',(-177.520551089229,0.457971650391806,
136.703359899642));
#159841=CARTESIAN_POINT('Ctrl Pts',(-177.527959308896,0.615086453544958,
136.691162216229));
#159842=CARTESIAN_POINT('Ctrl Pts',(-177.535367528562,0.77161078451577,
136.672691277176));
#159843=CARTESIAN_POINT('Ctrl Pts',(-177.542775748229,0.927012338536299,
136.648039141125));
#159844=CARTESIAN_POINT('Ctrl Pts',(-177.550188527531,1.08250953962031,
136.623371832095));
#159845=CARTESIAN_POINT('Ctrl Pts',(-177.557601306833,1.23688222154091,
136.592515818272));
#159846=CARTESIAN_POINT('Ctrl Pts',(-177.565014086135,1.3896105286662,136.555613797623));
#159847=CARTESIAN_POINT('Ctrl Pts',(-177.572437457163,1.54255706115918,
136.518659049637));
#159848=CARTESIAN_POINT('Ctrl Pts',(-177.579860828192,1.69385416814397,
136.475641142989));
#159849=CARTESIAN_POINT('Ctrl Pts',(-177.587284199221,1.84299855412119,
136.42675218095));
#159850=CARTESIAN_POINT('Ctrl Pts',(-177.591220248662,1.9220784862429,136.4008300802));
#159851=CARTESIAN_POINT('Ctrl Pts',(-177.595156298103,2.00055355631309,
136.373258215113));
#159852=CARTESIAN_POINT('Ctrl Pts',(-177.599092347544,2.07835137893825,
136.344070547532));
#159853=CARTESIAN_POINT('Ctrl Pts',(-177.60651561395,2.22507564441075,136.289023517395));
#159854=CARTESIAN_POINT('Ctrl Pts',(-177.613938880355,2.36983330722165,
136.228060034725));
#159855=CARTESIAN_POINT('Ctrl Pts',(-177.62136214676,2.51211161662649,136.16133978386));
#159856=CARTESIAN_POINT('Ctrl Pts',(-177.628776639481,2.65422176488509,
136.094698390792));
#159857=CARTESIAN_POINT('Ctrl Pts',(-177.636191132203,2.79385805801418,
136.022313929918));
#159858=CARTESIAN_POINT('Ctrl Pts',(-177.643605624924,2.93052458062564,
135.944395271617));
#159859=CARTESIAN_POINT('Ctrl Pts',(-177.651012971277,3.0670593788972,135.866551714253));
#159860=CARTESIAN_POINT('Ctrl Pts',(-177.658420317631,3.20062978296294,
135.783184762192));
#159861=CARTESIAN_POINT('Ctrl Pts',(-177.665827663985,3.33076159361491,
135.694550569807));
#159862=CARTESIAN_POINT('Ctrl Pts',(-177.67322948566,3.46079634705327,135.605982484146));
#159863=CARTESIAN_POINT('Ctrl Pts',(-177.680631307335,3.58739730640505,
135.512155189587));
#159864=CARTESIAN_POINT('Ctrl Pts',(-177.688033129011,3.71011664924135,
135.413369731413));
#159865=CARTESIAN_POINT('Ctrl Pts',(-177.695431043322,3.83277120949215,
135.314636421313));
#159866=CARTESIAN_POINT('Ctrl Pts',(-177.702828957634,3.95154794400457,
135.210950393712));
#159867=CARTESIAN_POINT('Ctrl Pts',(-177.710226871945,4.0660297980114,135.102654726184));
#159868=CARTESIAN_POINT('Ctrl Pts',(-177.717623556857,4.18049262721051,
134.994377055432));
#159869=CARTESIAN_POINT('Ctrl Pts',(-177.725020241769,4.29066172152809,
134.881491521395));
#159870=CARTESIAN_POINT('Ctrl Pts',(-177.732416926681,4.3961547061791,134.764380107649));
#159871=CARTESIAN_POINT('Ctrl Pts',(-177.739813283617,4.50164301316061,
134.647273886747));
#159872=CARTESIAN_POINT('Ctrl Pts',(-177.747209640552,4.60245537290049,
134.525942436072));
#159873=CARTESIAN_POINT('Ctrl Pts',(-177.754605997488,4.69824794256832,
134.4008028641));
#159874=CARTESIAN_POINT('Ctrl Pts',(-177.762003486824,4.79405517832313,
134.275644132939));
#159875=CARTESIAN_POINT('Ctrl Pts',(-177.769400976161,4.88484086681493,
134.146676416024));
#159876=CARTESIAN_POINT('Ctrl Pts',(-177.776798465497,4.97030304842392,
134.01434787133));
#159877=CARTESIAN_POINT('Ctrl Pts',(-177.784198548012,5.05579518866831,
133.88197293907));
#159878=CARTESIAN_POINT('Ctrl Pts',(-177.791598630527,5.13595990414746,
133.746235146767));
#159879=CARTESIAN_POINT('Ctrl Pts',(-177.798998713042,5.21054002796877,
133.60760930069));
#159880=CARTESIAN_POINT('Ctrl Pts',(-177.806406932709,5.28520216030313,
133.468831021244));
#159881=CARTESIAN_POINT('Ctrl Pts',(-177.813815152375,5.35426726036343,
133.327158674864));
#159882=CARTESIAN_POINT('Ctrl Pts',(-177.821223372042,5.41752505596053,
133.183089864567));
#159883=CARTESIAN_POINT('Ctrl Pts',(-177.828636151344,5.4808217856753,133.038932382322));
#159884=CARTESIAN_POINT('Ctrl Pts',(-177.836048930646,5.53830395269912,
132.89237584379));
#159885=CARTESIAN_POINT('Ctrl Pts',(-177.843461709948,5.58981061820532,
132.743934749972));
#159886=CARTESIAN_POINT('Ctrl Pts',(-177.850885080977,5.64139087885053,
132.595281556559));
#159887=CARTESIAN_POINT('Ctrl Pts',(-177.858308452005,5.68697847761942,
132.444738786182));
#159888=CARTESIAN_POINT('Ctrl Pts',(-177.865731823034,5.72646299292331,
132.292833712109));
#159889=CARTESIAN_POINT('Ctrl Pts',(-177.869667872475,5.74739863035717,
132.212289996917));
#159890=CARTESIAN_POINT('Ctrl Pts',(-177.873603921916,5.76661933161712,
132.131363431378));
#159891=CARTESIAN_POINT('Ctrl Pts',(-177.877539971357,5.78411454368991,
132.050133272578));
#159892=CARTESIAN_POINT('Ctrl Pts',(-177.884963237763,5.8171099676497,131.8969357282));
#159893=CARTESIAN_POINT('Ctrl Pts',(-177.892386504168,5.84406471575569,
131.742194755227));
#159894=CARTESIAN_POINT('Ctrl Pts',(-177.899809770574,5.8648359806621,131.586428058668));
#159895=CARTESIAN_POINT('Ctrl Pts',(-177.907224263295,5.88558269565833,
131.430845465408));
#159896=CARTESIAN_POINT('Ctrl Pts',(-177.914638756016,5.90016042593295,
131.274239928101));
#159897=CARTESIAN_POINT('Ctrl Pts',(-177.922053248737,5.90847684567043,
131.11714157395));
#159898=CARTESIAN_POINT('Ctrl Pts',(-177.92946059509,5.91678524972947,130.960194637107));
#159899=CARTESIAN_POINT('Ctrl Pts',(-177.936867941444,5.91884433792153,
130.802756199315));
#159900=CARTESIAN_POINT('Ctrl Pts',(-177.944275287798,5.91461330392035,
130.645363675493));
#159901=CARTESIAN_POINT('Ctrl Pts',(-177.951677109473,5.91038542558397,
130.488088540955));
#159902=CARTESIAN_POINT('Ctrl Pts',(-177.959078931149,5.89987677627389,
130.330859623758));
#159903=CARTESIAN_POINT('Ctrl Pts',(-177.966480752824,5.88309857495163,
130.174216411926));
#159904=CARTESIAN_POINT('Ctrl Pts',(-177.973878667135,5.86632923071125,
130.017655890825));
#159905=CARTESIAN_POINT('Ctrl Pts',(-177.981276581447,5.8432969654369,129.861680829558));
#159906=CARTESIAN_POINT('Ctrl Pts',(-177.988674495758,5.81406499171843,
129.706827549921));
#159907=CARTESIAN_POINT('Ctrl Pts',(-177.99607118067,5.78483787582355,129.552000004089));
#159908=CARTESIAN_POINT('Ctrl Pts',(-178.003467865583,5.74941316546099,
129.398294236358));
#159909=CARTESIAN_POINT('Ctrl Pts',(-178.010864550495,5.70790555132229,
129.246238420919));
#159910=CARTESIAN_POINT('Ctrl Pts',(-178.01826090743,5.66639977767482,129.094189347795));
#159911=CARTESIAN_POINT('Ctrl Pts',(-178.025657264366,5.61881173485485,
128.943790441616));
#159912=CARTESIAN_POINT('Ctrl Pts',(-178.033053621301,5.56530649258613,
128.795556444413));
#159913=CARTESIAN_POINT('Ctrl Pts',(-178.040451110638,5.51179305852807,
128.647299752205));
#159914=CARTESIAN_POINT('Ctrl Pts',(-178.047848599974,5.45236074792454,
128.501208980088));
#159915=CARTESIAN_POINT('Ctrl Pts',(-178.055246089311,5.38722339222336,
128.357780415574));
#159916=CARTESIAN_POINT('Ctrl Pts',(-178.062646171826,5.32206320272322,
128.214301572398));
#159917=CARTESIAN_POINT('Ctrl Pts',(-178.070046254341,5.2511941406124,128.073487134563));
#159918=CARTESIAN_POINT('Ctrl Pts',(-178.077446336856,5.17487666886568,
127.935810108244));
#159919=CARTESIAN_POINT('Ctrl Pts',(-178.084854556523,5.09847527821303,
127.797981691881));
#159920=CARTESIAN_POINT('Ctrl Pts',(-178.092262776189,5.0166136944242,127.663297903417));
#159921=CARTESIAN_POINT('Ctrl Pts',(-178.099670995855,4.92959690775829,
127.532204617385));
#159922=CARTESIAN_POINT('Ctrl Pts',(-178.107083775158,4.84252656371214,
127.401030645623));
#159923=CARTESIAN_POINT('Ctrl Pts',(-178.11449655446,4.75029491250327,127.273451881607));
#159924=CARTESIAN_POINT('Ctrl Pts',(-178.121909333762,4.65324782702965,
127.149881828088));
#159925=CARTESIAN_POINT('Ctrl Pts',(-178.129332704791,4.55606207612909,
127.026135211882));
#159926=CARTESIAN_POINT('Ctrl Pts',(-178.136756075819,4.45404739049054,
126.906409029329));
#159927=CARTESIAN_POINT('Ctrl Pts',(-178.144179446848,4.34758769448162,
126.79108118532));
#159928=CARTESIAN_POINT('Ctrl Pts',(-178.148115496289,4.29114020919341,
126.729931595174));
#159929=CARTESIAN_POINT('Ctrl Pts',(-178.15205154573,4.2334436561737,126.670017889436));
#159930=CARTESIAN_POINT('Ctrl Pts',(-178.15598759517,4.17455901249309,126.611391787046));
#159931=CARTESIAN_POINT('Ctrl Pts',(-178.163410861576,4.06350441223662,
126.500824787596));
#159932=CARTESIAN_POINT('Ctrl Pts',(-178.170834127981,3.94788614894046,
126.394505718966));
#159933=CARTESIAN_POINT('Ctrl Pts',(-178.178257394387,3.82806259163174,
126.292834561224));
#159934=CARTESIAN_POINT('Ctrl Pts',(-178.185671887108,3.70838065581702,
126.191283570348));
#159935=CARTESIAN_POINT('Ctrl Pts',(-178.193086379829,3.58450360127617,
126.094369794788));
#159936=CARTESIAN_POINT('Ctrl Pts',(-178.20050087255,3.45682753468036,126.00245745757));
#159937=CARTESIAN_POINT('Ctrl Pts',(-178.207908218903,3.32927452708373,
125.910633708923));
#159938=CARTESIAN_POINT('Ctrl Pts',(-178.215315565257,3.19793009794471,
125.823802018436));
#159939=CARTESIAN_POINT('Ctrl Pts',(-178.222722911611,3.06322433283905,
125.742287203519));
#159940=CARTESIAN_POINT('Ctrl Pts',(-178.230124733286,2.92861903637594,
125.660833185426));
#159941=CARTESIAN_POINT('Ctrl Pts',(-178.237526554962,2.79065771374413,
125.584688339437));
#159942=CARTESIAN_POINT('Ctrl Pts',(-178.244928376637,2.64980031561801,
125.514134833174));
#159943=CARTESIAN_POINT('Ctrl Pts',(-178.252326290949,2.50901727501513,
125.443618571557));
#159944=CARTESIAN_POINT('Ctrl Pts',(-178.25972420526,2.36534153655218,125.378687938122));
#159945=CARTESIAN_POINT('Ctrl Pts',(-178.267122119571,2.21925849089409,
125.319579645358));
#159946=CARTESIAN_POINT('Ctrl Pts',(-178.274518804484,2.0731997215886,125.26048117532));
#159947=CARTESIAN_POINT('Ctrl Pts',(-178.281915489396,1.92473478477583,
125.207203265498));
#159948=CARTESIAN_POINT('Ctrl Pts',(-178.289312174308,1.77437004148133,
125.159934914415));
#159949=CARTESIAN_POINT('Ctrl Pts',(-178.296708531243,1.62401196551712,
125.11266865926));
#159950=CARTESIAN_POINT('Ctrl Pts',(-178.304104888179,1.47175460668375,
125.071411544961));
#159951=CARTESIAN_POINT('Ctrl Pts',(-178.311501245114,1.31812025624708,
125.036302924324));
#159952=CARTESIAN_POINT('Ctrl Pts',(-178.318898734451,1.16446238399872,
125.001188928467));
#159953=CARTESIAN_POINT('Ctrl Pts',(-178.326296223788,1.00942746431455,
124.972225383793));
#159954=CARTESIAN_POINT('Ctrl Pts',(-178.333693713124,0.853548619055772,
124.949500643373));
#159955=CARTESIAN_POINT('Ctrl Pts',(-178.341093795639,0.697615130709651,
124.92676793683));
#159956=CARTESIAN_POINT('Ctrl Pts',(-178.348493878154,0.540837496942744,
124.910278442666));
#159957=CARTESIAN_POINT('Ctrl Pts',(-178.355893960669,0.383754457847682,
124.900068697396));
#159958=CARTESIAN_POINT('Ctrl Pts',(-178.363302180336,0.22649868980283,
124.889847725462));
#159959=CARTESIAN_POINT('Ctrl Pts',(-178.370710400002,0.068937218506624,
124.885920316844));
#159960=CARTESIAN_POINT('Ctrl Pts',(-178.378118619668,-0.0883899744820926,
124.888270880678));
#159961=CARTESIAN_POINT('Ctrl Pts',(-178.385531398971,-0.245813999732949,
124.890622891245));
#159962=CARTESIAN_POINT('Ctrl Pts',(-178.392944178273,-0.403003087479562,
124.899260553307));
#159963=CARTESIAN_POINT('Ctrl Pts',(-178.400356957575,-0.559422393395732,
124.914116382539));
#159964=CARTESIAN_POINT('Ctrl Pts',(-178.407780328604,-0.7160651985522,
124.928993438476));
#159965=CARTESIAN_POINT('Ctrl Pts',(-178.415203699632,-0.871935656190584,
124.950106356566));
#159966=CARTESIAN_POINT('Ctrl Pts',(-178.422627070661,-1.02650830372507,
124.977336397187));
#159967=CARTESIAN_POINT('Ctrl Pts',(-178.426563120102,-1.10846643036695,
124.9917744181));
#159968=CARTESIAN_POINT('Ctrl Pts',(-178.430499169543,-1.19005992407337,
125.007931340782));
#159969=CARTESIAN_POINT('Ctrl Pts',(-178.434435218983,-1.27121231263882,
125.025783818847));
#159970=CARTESIAN_POINT('Ctrl Pts',(-178.441858485389,-1.42426318479541,
125.05945303532));
#159971=CARTESIAN_POINT('Ctrl Pts',(-178.449281751794,-1.57620692379148,
125.099257901129));
#159972=CARTESIAN_POINT('Ctrl Pts',(-178.4567050182,-1.72651330785561,125.145113109257));
#159973=CARTESIAN_POINT('Ctrl Pts',(-178.464119510921,-1.87664204225593,
125.190914120338));
#159974=CARTESIAN_POINT('Ctrl Pts',(-178.471534003642,-2.02513692022056,
125.242751131763));
#159975=CARTESIAN_POINT('Ctrl Pts',(-178.478948496363,-2.17147740527155,
125.300487759215));
#159976=CARTESIAN_POINT('Ctrl Pts',(-178.486355842717,-2.31767684185384,
125.358168737931));
#159977=CARTESIAN_POINT('Ctrl Pts',(-178.493763189071,-2.46172567447768,
125.421737876344));
#159978=CARTESIAN_POINT('Ctrl Pts',(-178.501170535424,-2.60311815329856,
125.49100890302));
#159979=CARTESIAN_POINT('Ctrl Pts',(-178.5085723571,-2.74440517627349,125.560228264751));
#159980=CARTESIAN_POINT('Ctrl Pts',(-178.515974178775,-2.88303945651406,
125.63514088355));
#159981=CARTESIAN_POINT('Ctrl Pts',(-178.523376000451,-3.01853498383293,
125.715512308383));
#159982=CARTESIAN_POINT('Ctrl Pts',(-178.530773914762,-3.15395898411763,
125.795841305766));
#159983=CARTESIAN_POINT('Ctrl Pts',(-178.538171829073,-3.28624721107121,
125.881623180252));
#159984=CARTESIAN_POINT('Ctrl Pts',(-178.545569743385,-3.41493814626204,
125.972577507812));
#159985=CARTESIAN_POINT('Ctrl Pts',(-178.552966428297,-3.54360769535433,
126.063516720413));
#159986=CARTESIAN_POINT('Ctrl Pts',(-178.560363113209,-3.66868083460214,
126.159626464855));
#159987=CARTESIAN_POINT('Ctrl Pts',(-178.567759798121,-3.78972485369128,
126.260582883586));
#159988=CARTESIAN_POINT('Ctrl Pts',(-178.575156155057,-3.91076350556178,
126.361534825803));
#159989=CARTESIAN_POINT('Ctrl Pts',(-178.582552511992,-4.02777310582645,
126.467332775903));
#159990=CARTESIAN_POINT('Ctrl Pts',(-178.589948868928,-4.14035410183528,
126.577612639047));
#159991=CARTESIAN_POINT('Ctrl Pts',(-178.597346358264,-4.25295233428265,
126.68790938632));
#159992=CARTESIAN_POINT('Ctrl Pts',(-178.604743847601,-4.3611203457351,
126.802689151698));
#159993=CARTESIAN_POINT('Ctrl Pts',(-178.612141336938,-4.46449563686406,
126.921551161654));
#159994=CARTESIAN_POINT('Ctrl Pts',(-178.619541419453,-4.56790716604064,
127.040454838502));
#159995=CARTESIAN_POINT('Ctrl Pts',(-178.626941501968,-4.66652238504518,
127.163443327591));
#159996=CARTESIAN_POINT('Ctrl Pts',(-178.634341584483,-4.7600193524934,
127.290083120499));
#159997=CARTESIAN_POINT('Ctrl Pts',(-178.641749804149,-4.85361912946892,
127.416862166879));
#159998=CARTESIAN_POINT('Ctrl Pts',(-178.649158023815,-4.94208919345739,
127.547300234764));
#159999=CARTESIAN_POINT('Ctrl Pts',(-178.656566243482,-5.02515078827324,
127.680934595132));
#160000=CARTESIAN_POINT('Ctrl Pts',(-178.663979022784,-5.10826350611499,
127.814651205219));
#160001=CARTESIAN_POINT('Ctrl Pts',(-178.671391802086,-5.18596093787455,
127.9515677039));
#160002=CARTESIAN_POINT('Ctrl Pts',(-178.678804581388,-5.25801076360465,
128.091197634567));
#160003=CARTESIAN_POINT('Ctrl Pts',(-178.686227952417,-5.33016353750426,
128.231027075026));
#160004=CARTESIAN_POINT('Ctrl Pts',(-178.693651323446,-5.39665243126757,
128.373577353457));
#160005=CARTESIAN_POINT('Ctrl Pts',(-178.701074694474,-5.45729331853665,
128.518342201639));
#160006=CARTESIAN_POINT('Ctrl Pts',(-178.705010743915,-5.48944657202259,
128.595099997725));
#160007=CARTESIAN_POINT('Ctrl Pts',(-178.708946793355,-5.51995657176065,
128.672480126188));
#160008=CARTESIAN_POINT('Ctrl Pts',(-178.712882842796,-5.54880162463143,
128.750405629503));
#160009=CARTESIAN_POINT('Ctrl Pts',(-178.721434613827,-5.6114726584305,
128.919712715677));
#160010=CARTESIAN_POINT('Ctrl Pts',(-178.729986384858,-5.66643819996979,
129.092017853483));
#160011=CARTESIAN_POINT('Ctrl Pts',(-178.738538155888,-5.71344087978109,
129.266659776783));
#160012=CARTESIAN_POINT('Ctrl Pts',(-178.747059185309,-5.76027459598887,
129.440673903352));
#160013=CARTESIAN_POINT('Ctrl Pts',(-178.75558021473,-5.79920250282132,
129.617007918382));
#160014=CARTESIAN_POINT('Ctrl Pts',(-178.764101244151,-5.8300165114818,
129.79498554439));
#160015=CARTESIAN_POINT('Ctrl Pts',(-178.772561766365,-5.86061171212024,
129.971699364291));
#160016=CARTESIAN_POINT('Ctrl Pts',(-178.781022288579,-5.88320776267889,
130.150033394038));
#160017=CARTESIAN_POINT('Ctrl Pts',(-178.789482810793,-5.89764813416431,
130.329305833264));
#160018=CARTESIAN_POINT('Ctrl Pts',(-178.796863453485,-5.91024537338753,
130.485696394638));
#160019=CARTESIAN_POINT('Ctrl Pts',(-178.804244096178,-5.91663666015527,
130.642800748586));
#160020=CARTESIAN_POINT('Ctrl Pts',(-178.811624738871,-5.91674850538075,
130.800155076613));
#160021=CARTESIAN_POINT('',(-180.561624807791,-5.90996050472777,130.808431327307));
#160022=CARTESIAN_POINT('Ctrl Pts',(-178.811624807791,-5.91021030986751,
130.800161191611));
#160023=CARTESIAN_POINT('Ctrl Pts',(-178.871526694064,-5.90189013011824,
132.075856832088));
#160024=CARTESIAN_POINT('Ctrl Pts',(-179.024244454939,-4.86928404315109,
135.340473970702));
#160025=CARTESIAN_POINT('Ctrl Pts',(-179.269778090423,0.518479272423054,
137.783525307874));
#160026=CARTESIAN_POINT('Ctrl Pts',(-179.548225714233,6.15201962547423,
134.140558312264));
#160027=CARTESIAN_POINT('Ctrl Pts',(-179.826673338048,6.13215448558245,
127.431788617551));
#160028=CARTESIAN_POINT('Ctrl Pts',(-180.10512096186,0.477138945842835,
123.822247831545));
#160029=CARTESIAN_POINT('Ctrl Pts',(-180.350104785108,-4.88402996107005,
126.29162117749));
#160030=CARTESIAN_POINT('Ctrl Pts',(-180.502272733752,-5.90199055707381,
129.544310586215));
#160031=CARTESIAN_POINT('Ctrl Pts',(-180.561624807791,-5.90996050472777,
130.808431327307));
#160032=CARTESIAN_POINT('',(-182.311624807792,-5.92507812272359,130.807023572335));
#160033=CARTESIAN_POINT('Ctrl Pts',(-180.561624807791,-5.90996050472777,
130.808431327307));
#160034=CARTESIAN_POINT('Ctrl Pts',(-180.595088608356,-5.9144541090899,
131.521166055697));
#160035=CARTESIAN_POINT('Ctrl Pts',(-180.721368283525,-5.46467200361853,
134.2052756912));
#160036=CARTESIAN_POINT('Ctrl Pts',(-180.9404638333,-1.46310027610978,137.648109452265));
#160037=CARTESIAN_POINT('Ctrl Pts',(-181.218911457112,4.96699828222215,
135.734521730019));
#160038=CARTESIAN_POINT('Ctrl Pts',(-181.497359080924,6.83266807054414,
129.290356797193));
#160039=CARTESIAN_POINT('Ctrl Pts',(-181.775806704738,2.41944969642949,
124.23748741209));
#160040=CARTESIAN_POINT('Ctrl Pts',(-182.047228613693,-4.04967250708035,
125.19448203293));
#160041=CARTESIAN_POINT('Ctrl Pts',(-182.225834648045,-5.91491065230807,
128.991748760208));
#160042=CARTESIAN_POINT('Ctrl Pts',(-182.311624807792,-5.92507812272359,
130.807023572335));
#160043=CARTESIAN_POINT('',(-184.061624807792,-5.91793140692411,130.798997977614));
#160044=CARTESIAN_POINT('Ctrl Pts',(-182.311624807792,-5.92507812272359,
130.807023572335));
#160045=CARTESIAN_POINT('Ctrl Pts',(-182.318650522649,-5.92591077938457,
130.955684016088));
#160046=CARTESIAN_POINT('Ctrl Pts',(-182.325676237506,-5.920802909146,131.104286291747));
#160047=CARTESIAN_POINT('Ctrl Pts',(-182.425517826968,-5.76118888251318,
133.209457008152));
#160048=CARTESIAN_POINT('Ctrl Pts',(-182.611149576176,-3.32683150482748,
136.961450244072));
#160049=CARTESIAN_POINT('Ctrl Pts',(-182.88959719999,3.38190018988211,136.931375521743));
#160050=CARTESIAN_POINT('Ctrl Pts',(-183.168044823802,6.98283082510118,
131.270873423793));
#160051=CARTESIAN_POINT('Ctrl Pts',(-183.446492447615,4.16688106229984,
125.181668847338));
#160052=CARTESIAN_POINT('Ctrl Pts',(-183.724940071428,-2.47822883329544,
124.259443323958));
#160053=CARTESIAN_POINT('Ctrl Pts',(-183.929984191486,-5.69455770389321,
128.0092781062));
#160054=CARTESIAN_POINT('Ctrl Pts',(-184.042212436941,-5.92199600856727,
130.386992623478));
#160055=CARTESIAN_POINT('Ctrl Pts',(-184.061624807792,-5.9181658456461,
130.798997765173));
#160056=CARTESIAN_POINT('',(-185.811624807754,-5.91674999671234,130.804163375351));
#160057=CARTESIAN_POINT('Ctrl Pts',(-184.061624807792,-5.91674757076024,
130.798999050368));
#160058=CARTESIAN_POINT('Ctrl Pts',(-184.068928931162,-5.91688801138847,
130.953982046063));
#160059=CARTESIAN_POINT('Ctrl Pts',(-184.076233054531,-5.91093487072381,
131.109156665659));
#160060=CARTESIAN_POINT('Ctrl Pts',(-184.083537177901,-5.89886979863471,
131.263997062221));
#160061=CARTESIAN_POINT('Ctrl Pts',(-184.090835650274,-5.88681406095517,
131.41871766309));
#160062=CARTESIAN_POINT('Ctrl Pts',(-184.098134122647,-5.86865583195702,
131.57310417378));
#160063=CARTESIAN_POINT('Ctrl Pts',(-184.10543259502,-5.84442882662681,
131.726630780259));
#160064=CARTESIAN_POINT('Ctrl Pts',(-184.112782708521,-5.8200304005078,
131.881243680798));
#160065=CARTESIAN_POINT('Ctrl Pts',(-184.120132822023,-5.78947697807806,
132.034984065929));
#160066=CARTESIAN_POINT('Ctrl Pts',(-184.127482935524,-5.75285625138199,
132.187319587831));
#160067=CARTESIAN_POINT('Ctrl Pts',(-184.134776202234,-5.71651875443688,
132.338476925796));
#160068=CARTESIAN_POINT('Ctrl Pts',(-184.142069468944,-5.67420758047763,
132.488250678532));
#160069=CARTESIAN_POINT('Ctrl Pts',(-184.149362735654,-5.62605967323285,
132.636131104205));
#160070=CARTESIAN_POINT('Ctrl Pts',(-184.1566557956,-5.57791313097582,132.784007337485));
#160071=CARTESIAN_POINT('Ctrl Pts',(-184.163948855547,-5.52393030354824,
132.929989984487));
#160072=CARTESIAN_POINT('Ctrl Pts',(-184.171241915494,-5.46429776820347,
133.073585256712));
#160073=CARTESIAN_POINT('Ctrl Pts',(-184.178536303616,-5.40465437287707,
133.217206679795));
#160074=CARTESIAN_POINT('Ctrl Pts',(-184.185830691739,-5.33935937028289,
133.358439507777));
#160075=CARTESIAN_POINT('Ctrl Pts',(-184.193125079861,-5.26864703532705,
133.49681098473));
#160076=CARTESIAN_POINT('Ctrl Pts',(-184.200517599794,-5.19698340338551,
133.637043980879));
#160077=CARTESIAN_POINT('Ctrl Pts',(-184.207910119727,-5.11975580564257,
133.774337715552));
#160078=CARTESIAN_POINT('Ctrl Pts',(-184.215302639659,-5.03725512909461,
133.908227774342));
#160079=CARTESIAN_POINT('Ctrl Pts',(-184.222607901079,-4.95572825936504,
134.040537445459));
#160080=CARTESIAN_POINT('Ctrl Pts',(-184.2299131625,-4.86905238698824,134.16952307254));
#160081=CARTESIAN_POINT('Ctrl Pts',(-184.23721842392,-4.7775502821432,134.294768024172));
#160082=CARTESIAN_POINT('Ctrl Pts',(-184.244654573109,-4.68440874160218,
134.422256979315));
#160083=CARTESIAN_POINT('Ctrl Pts',(-184.252090722298,-4.58626664978123,
134.545869616373));
#160084=CARTESIAN_POINT('Ctrl Pts',(-184.259526871487,-4.48350479392226,
134.665204479389));
#160085=CARTESIAN_POINT('Ctrl Pts',(-184.266963020676,-4.38074293806359,
134.784539342404));
#160086=CARTESIAN_POINT('Ctrl Pts',(-184.274399169865,-4.27336164917223,
134.899596175744));
#160087=CARTESIAN_POINT('Ctrl Pts',(-184.281835319054,-4.161777721421,135.010015948187));
#160088=CARTESIAN_POINT('Ctrl Pts',(-184.289258585459,-4.05038710764862,
135.120244423497));
#160089=CARTESIAN_POINT('Ctrl Pts',(-184.296681851865,-3.93444578121529,
135.226211097442));
#160090=CARTESIAN_POINT('Ctrl Pts',(-184.30410511827,-3.81431332688993,
135.327517082559));
#160091=CARTESIAN_POINT('Ctrl Pts',(-184.311519610991,-3.6943228591492,
135.428703332415));
#160092=CARTESIAN_POINT('Ctrl Pts',(-184.318934103712,-3.57015140620211,
135.525239619935));
#160093=CARTESIAN_POINT('Ctrl Pts',(-184.326348596433,-3.44219618145469,
135.616762929393));
#160094=CARTESIAN_POINT('Ctrl Pts',(-184.333755942787,-3.31436428477031,
135.70819802524));
#160095=CARTESIAN_POINT('Ctrl Pts',(-184.341163289141,-3.18275617821301,
135.794629546266));
#160096=CARTESIAN_POINT('Ctrl Pts',(-184.348570635494,-3.04780293399889,
135.8757339856));
#160097=CARTESIAN_POINT('Ctrl Pts',(-184.35597245717,-2.91295034300579,
135.956777934184));
#160098=CARTESIAN_POINT('Ctrl Pts',(-184.363374278845,-2.77475790068248,
136.032502520666));
#160099=CARTESIAN_POINT('Ctrl Pts',(-184.370776100521,-2.63368641439405,
136.102626978663));
#160100=CARTESIAN_POINT('Ctrl Pts',(-184.378174014832,-2.49268939864553,
136.172714418505));
#160101=CARTESIAN_POINT('Ctrl Pts',(-184.385571929143,-2.34881669916657,
136.237207451659));
#160102=CARTESIAN_POINT('Ctrl Pts',(-184.392969843455,-2.20255442484518,
136.295870844097));
#160103=CARTESIAN_POINT('Ctrl Pts',(-184.400366528367,-2.05631645666011,
136.354524487743));
#160104=CARTESIAN_POINT('Ctrl Pts',(-184.407763213279,-1.90769004789607,
136.407350274588));
#160105=CARTESIAN_POINT('Ctrl Pts',(-184.415159898191,-1.75718213247968,
136.454160748172));
#160106=CARTESIAN_POINT('Ctrl Pts',(-184.422556255127,-1.60668089074197,
136.50096914613));
#160107=CARTESIAN_POINT('Ctrl Pts',(-184.429952612062,-1.45429866469017,
136.541762650303));
#160108=CARTESIAN_POINT('Ctrl Pts',(-184.437348968997,-1.30055816731291,
136.576403498205));
#160109=CARTESIAN_POINT('Ctrl Pts',(-184.444746458334,-1.14679413187302,
136.611049649709));
#160110=CARTESIAN_POINT('Ctrl Pts',(-184.45214394767,-0.991671775233469,
136.63954118726));
#160111=CARTESIAN_POINT('Ctrl Pts',(-184.459541437007,-0.835724485702392,
136.661791380836));
#160112=CARTESIAN_POINT('Ctrl Pts',(-184.466941519522,-0.679722529091387,
136.684049374182));
#160113=CARTESIAN_POINT('Ctrl Pts',(-184.474341602037,-0.522895433160513,
136.70006161478));
#160114=CARTESIAN_POINT('Ctrl Pts',(-184.481741684552,-0.365782046711605,
136.709793206022));
#160115=CARTESIAN_POINT('Ctrl Pts',(-184.489149904218,-0.208495897941526,
136.71953549815));
#160116=CARTESIAN_POINT('Ctrl Pts',(-184.496558123885,-0.0509232027779254,
136.722983325656));
#160117=CARTESIAN_POINT('Ctrl Pts',(-184.503966343551,0.106396107174741,
136.720153922853));
#160118=CARTESIAN_POINT('Ctrl Pts',(-184.511379122853,0.263812244537669,
136.717322778599));
#160119=CARTESIAN_POINT('Ctrl Pts',(-184.518791902155,0.420974314123582,
136.708206727033));
#160120=CARTESIAN_POINT('Ctrl Pts',(-184.526204681458,0.577347679482734,
136.692874880052));
#160121=CARTESIAN_POINT('Ctrl Pts',(-184.533628052486,0.733944478439272,
136.677521126208));
#160122=CARTESIAN_POINT('Ctrl Pts',(-184.541051423515,0.889749953635859,
136.655933889856));
#160123=CARTESIAN_POINT('Ctrl Pts',(-184.548474794544,1.04423900632314,
136.628233509394));
#160124=CARTESIAN_POINT('Ctrl Pts',(-184.552410843985,1.1261528089723,136.613546103012));
#160125=CARTESIAN_POINT('Ctrl Pts',(-184.556346893425,1.20769674862925,
136.59714091264));
#160126=CARTESIAN_POINT('Ctrl Pts',(-184.560282942866,1.28879442450105,
136.579041517311));
#160127=CARTESIAN_POINT('Ctrl Pts',(-184.567706209272,1.44174211022288,
136.544906622583));
#160128=CARTESIAN_POINT('Ctrl Pts',(-184.575129475677,1.59356399310633,
136.504639476673));
#160129=CARTESIAN_POINT('Ctrl Pts',(-184.582552742083,1.74373011348117,
136.458327000013));
#160130=CARTESIAN_POINT('Ctrl Pts',(-184.589967234804,1.89371874997225,
136.412069260854));
#160131=CARTESIAN_POINT('Ctrl Pts',(-184.597381727525,2.04205516608679,
136.359780522206));
#160132=CARTESIAN_POINT('Ctrl Pts',(-184.604796220246,2.18821924286488,
136.301598752089));
#160133=CARTESIAN_POINT('Ctrl Pts',(-184.612203566599,2.33424244120238,
136.243473059753));
#160134=CARTESIAN_POINT('Ctrl Pts',(-184.619610912953,2.47809712401023,
136.179465780693));
#160135=CARTESIAN_POINT('Ctrl Pts',(-184.627018259307,2.6192781107327,136.109764724808));
#160136=CARTESIAN_POINT('Ctrl Pts',(-184.634420080982,2.76035379934881,
136.040115654599));
#160137=CARTESIAN_POINT('Ctrl Pts',(-184.641821902658,2.89875942920178,
135.964781427729));
#160138=CARTESIAN_POINT('Ctrl Pts',(-184.649223724333,3.03400970594374,
135.883997973396));
#160139=CARTESIAN_POINT('Ctrl Pts',(-184.656621638644,3.16918858511778,
135.803257164018));
#160140=CARTESIAN_POINT('Ctrl Pts',(-184.664019552956,3.30121510880317,
135.71707304701));
#160141=CARTESIAN_POINT('Ctrl Pts',(-184.671417467267,3.42962861422033,
135.625727449806));
#160142=CARTESIAN_POINT('Ctrl Pts',(-184.678814152179,3.55802077964237,
135.534397032583));
#160143=CARTESIAN_POINT('Ctrl Pts',(-184.686210837092,3.68280081455794,
135.437907053702));
#160144=CARTESIAN_POINT('Ctrl Pts',(-184.693607522004,3.80353699636812,
135.336582686238));
#160145=CARTESIAN_POINT('Ctrl Pts',(-184.701003878939,3.92426782460947,
135.235262811603));
#160146=CARTESIAN_POINT('Ctrl Pts',(-184.708400235875,4.04095487032625,
135.129109214579));
#160147=CARTESIAN_POINT('Ctrl Pts',(-184.71579659281,4.15319969089864,135.018487204419));
#160148=CARTESIAN_POINT('Ctrl Pts',(-184.723194082147,4.2654616964396,134.907848257747));
#160149=CARTESIAN_POINT('Ctrl Pts',(-184.730591571483,4.37327985674116,
134.792739797803));
#160150=CARTESIAN_POINT('Ctrl Pts',(-184.73798906082,4.47629289397063,134.673563699583));
#160151=CARTESIAN_POINT('Ctrl Pts',(-184.745389143335,4.57934204226076,
134.554345824366));
#160152=CARTESIAN_POINT('Ctrl Pts',(-184.75278922585,4.67758246983172,134.431057754148));
#160153=CARTESIAN_POINT('Ctrl Pts',(-184.760189308365,4.77069355624095,
134.304133975219));
#160154=CARTESIAN_POINT('Ctrl Pts',(-184.767597528031,4.86390702786161,
134.177070630548));
#160155=CARTESIAN_POINT('Ctrl Pts',(-184.775005747698,4.95197967345292,
134.046363894402));
#160156=CARTESIAN_POINT('Ctrl Pts',(-184.782413967364,5.03463414650848,
133.912477342097));
#160157=CARTESIAN_POINT('Ctrl Pts',(-184.789826746667,5.11733949201328,
133.778508384854));
#160158=CARTESIAN_POINT('Ctrl Pts',(-184.797239525968,5.194619837159,133.641356036106));
#160159=CARTESIAN_POINT('Ctrl Pts',(-184.804652305271,5.26624434368106,
133.501507457311));
#160160=CARTESIAN_POINT('Ctrl Pts',(-184.812075676299,5.3379711906568,133.361459056308));
#160161=CARTESIAN_POINT('Ctrl Pts',(-184.819499047328,5.4040259024361,133.21870706884));
#160162=CARTESIAN_POINT('Ctrl Pts',(-184.826922418357,5.46422589442022,
133.073758321197));
#160163=CARTESIAN_POINT('Ctrl Pts',(-184.830858467798,5.49614537464935,
132.9969030172));
#160164=CARTESIAN_POINT('Ctrl Pts',(-184.834794517239,5.52641971457611,
132.919430385207));
#160165=CARTESIAN_POINT('Ctrl Pts',(-184.838730566679,5.55502745541382,
132.841417448413));
#160166=CARTESIAN_POINT('Ctrl Pts',(-184.846153833085,5.60898076181651,
132.69428748432));
#160167=CARTESIAN_POINT('Ctrl Pts',(-184.85357709949,5.65716630769147,132.544790058487));
#160168=CARTESIAN_POINT('Ctrl Pts',(-184.861000365896,5.69937076551409,
132.39341802361));
#160169=CARTESIAN_POINT('Ctrl Pts',(-184.868414858617,5.74152534117242,
132.242224897908));
#160170=CARTESIAN_POINT('Ctrl Pts',(-184.875829351338,5.7777128006819,132.089161929462));
#160171=CARTESIAN_POINT('Ctrl Pts',(-184.883243844059,5.80776808344369,
131.93474128417));
#160172=CARTESIAN_POINT('Ctrl Pts',(-184.890651190412,5.83779439779231,
131.78046947531));
#160173=CARTESIAN_POINT('Ctrl Pts',(-184.898058536766,5.86170023104261,
131.624842958691));
#160174=CARTESIAN_POINT('Ctrl Pts',(-184.90546588312,5.87937053055049,131.468388272859));
#160175=CARTESIAN_POINT('Ctrl Pts',(-184.912867704795,5.89702765088234,
131.312050276835));
#160176=CARTESIAN_POINT('Ctrl Pts',(-184.920269526471,5.9084584559214,131.154885710824));
#160177=CARTESIAN_POINT('Ctrl Pts',(-184.927671348146,5.91359912613479,
130.997430392202));
#160178=CARTESIAN_POINT('Ctrl Pts',(-184.935069262458,5.91873708262841,
130.840058193015));
#160179=CARTESIAN_POINT('Ctrl Pts',(-184.942467176769,5.91759150510721,
130.682395919046));
#160180=CARTESIAN_POINT('Ctrl Pts',(-184.94986509108,5.91015050348987,130.52498347355));
#160181=CARTESIAN_POINT('Ctrl Pts',(-184.957261775993,5.90271073843201,
130.367597187147));
#160182=CARTESIAN_POINT('Ctrl Pts',(-184.964658460905,5.88897764325531,
130.210461019335));
#160183=CARTESIAN_POINT('Ctrl Pts',(-184.972055145817,5.86899143866611,
130.054113954552));
#160184=CARTESIAN_POINT('Ctrl Pts',(-184.979451502752,5.84900612028617,
129.897773822362));
#160185=CARTESIAN_POINT('Ctrl Pts',(-184.986847859688,5.82276829113332,
129.742223093914));
#160186=CARTESIAN_POINT('Ctrl Pts',(-184.994244216623,5.79036992825915,
129.587994448844));
#160187=CARTESIAN_POINT('Ctrl Pts',(-185.00164170596,5.75796660511301,129.433742190975));
#160188=CARTESIAN_POINT('Ctrl Pts',(-185.009039195297,5.71940094696954,
129.280812784864));
#160189=CARTESIAN_POINT('Ctrl Pts',(-185.016436684633,5.67481578315034,
129.129727407037));
#160190=CARTESIAN_POINT('Ctrl Pts',(-185.023836767148,5.63021499007076,
128.978589066463));
#160191=CARTESIAN_POINT('Ctrl Pts',(-185.031236849663,5.57959059565481,
128.829296399002));
#160192=CARTESIAN_POINT('Ctrl Pts',(-185.038636932178,5.52313484234269,
128.682354002166));
#160193=CARTESIAN_POINT('Ctrl Pts',(-185.046045151844,5.46661701012626,
128.535250027059));
#160194=CARTESIAN_POINT('Ctrl Pts',(-185.053453371511,5.40425514743527,
128.3905018324));
#160195=CARTESIAN_POINT('Ctrl Pts',(-185.060861591177,5.33628936075163,
128.248593331441));
#160196=CARTESIAN_POINT('Ctrl Pts',(-185.06827437048,5.26828174226036,128.106597488167));
#160197=CARTESIAN_POINT('Ctrl Pts',(-185.075687149781,5.19466350113199,
127.967445150473));
#160198=CARTESIAN_POINT('Ctrl Pts',(-185.083099929084,5.11571972637515,
127.831593851794));
#160199=CARTESIAN_POINT('Ctrl Pts',(-185.090523300112,5.03666315305096,
127.69554844241));
#160200=CARTESIAN_POINT('Ctrl Pts',(-185.097946671141,4.95226604824019,
127.562813806486));
#160201=CARTESIAN_POINT('Ctrl Pts',(-185.10537004217,4.86285612782121,127.433817509607));
#160202=CARTESIAN_POINT('Ctrl Pts',(-185.109306091611,4.81544884265258,
127.365420577777));
#160203=CARTESIAN_POINT('Ctrl Pts',(-185.113242141051,4.76663294343972,
127.298074068215));
#160204=CARTESIAN_POINT('Ctrl Pts',(-185.117178190492,4.71646163297881,
127.231837667725));
#160205=CARTESIAN_POINT('Ctrl Pts',(-185.124601456898,4.62184010724392,
127.10691788357));
#160206=CARTESIAN_POINT('Ctrl Pts',(-185.132024723303,4.52210915344613,
126.9855710088));
#160207=CARTESIAN_POINT('Ctrl Pts',(-185.139447989709,4.41756811377999,
126.868242920823));
#160208=CARTESIAN_POINT('Ctrl Pts',(-185.14686248243,4.31315063294114,126.751053504903));
#160209=CARTESIAN_POINT('Ctrl Pts',(-185.154276975151,4.20393462841209,
126.637873697119));
#160210=CARTESIAN_POINT('Ctrl Pts',(-185.161691467872,4.09026178058174,
126.529119205808));
#160211=CARTESIAN_POINT('Ctrl Pts',(-185.169098814225,3.97669849492183,
126.420469536169));
#160212=CARTESIAN_POINT('Ctrl Pts',(-185.176506160579,3.85868718572215,
126.316236947986));
#160213=CARTESIAN_POINT('Ctrl Pts',(-185.183913506933,3.73660865600951,
126.21680284525));
#160214=CARTESIAN_POINT('Ctrl Pts',(-185.191315328609,3.61462117706974,
126.11744290422));
#160215=CARTESIAN_POINT('Ctrl Pts',(-185.198717150284,3.48857280588916,
126.022874557316));
#160216=CARTESIAN_POINT('Ctrl Pts',(-185.206118971959,3.35887984478284,
125.933441120098));
#160217=CARTESIAN_POINT('Ctrl Pts',(-185.213516886271,3.2292553475808,125.844054894095));
#160218=CARTESIAN_POINT('Ctrl Pts',(-185.220914800582,3.09599039862963,
125.759798390713));
#160219=CARTESIAN_POINT('Ctrl Pts',(-185.228312714894,2.95953280695017,
125.68097344431));
#160220=CARTESIAN_POINT('Ctrl Pts',(-185.235709399806,2.82309789204744,
125.602161597183));
#160221=CARTESIAN_POINT('Ctrl Pts',(-185.243106084718,2.68347171034644,
125.52877970213));
#160222=CARTESIAN_POINT('Ctrl Pts',(-185.25050276963,2.54112946499453,125.461085254585));
#160223=CARTESIAN_POINT('Ctrl Pts',(-185.257899126566,2.39879353124695,
125.393393808683));
#160224=CARTESIAN_POINT('Ctrl Pts',(-185.265295483501,2.25374211042627,
125.33138946918));
#160225=CARTESIAN_POINT('Ctrl Pts',(-185.272691840437,2.10647307683844,
125.275282779531));
#160226=CARTESIAN_POINT('Ctrl Pts',(-185.280089329773,1.95918149598603,
125.219167499804));
#160227=CARTESIAN_POINT('Ctrl Pts',(-185.28748681911,1.80967197519407,125.168951800726));
#160228=CARTESIAN_POINT('Ctrl Pts',(-185.294884308446,1.65846019776952,
125.124797224583));
#160229=CARTESIAN_POINT('Ctrl Pts',(-185.302284390961,1.50719541329015,
125.080627170122));
#160230=CARTESIAN_POINT('Ctrl Pts',(-185.309684473476,1.35422754221607,
125.042522573463));
#160231=CARTESIAN_POINT('Ctrl Pts',(-185.317084555991,1.2000850284593,125.010594442877));
#160232=CARTESIAN_POINT('Ctrl Pts',(-185.324492775658,1.04577301916263,
124.97863120403));
#160233=CARTESIAN_POINT('Ctrl Pts',(-185.331900995324,0.890284153455571,
124.952858070407));
#160234=CARTESIAN_POINT('Ctrl Pts',(-185.339309214991,0.734155344681294,
124.933334600559));
#160235=CARTESIAN_POINT('Ctrl Pts',(-185.346721994293,0.577930441230811,
124.913799114341));
#160236=CARTESIAN_POINT('Ctrl Pts',(-185.354134773595,0.421065180974498,
124.900520988071));
#160237=CARTESIAN_POINT('Ctrl Pts',(-185.361547552897,0.264098597322687,
124.89350767629));
#160238=CARTESIAN_POINT('Ctrl Pts',(-185.368970923926,0.106907732454928,
124.88648434356));
#160239=CARTESIAN_POINT('Ctrl Pts',(-185.376394294955,-0.0503843726528677,
124.885743705147));
#160240=CARTESIAN_POINT('Ctrl Pts',(-185.383817665983,-0.207240856527645,
124.891241154044));
#160241=CARTESIAN_POINT('Ctrl Pts',(-185.387753715424,-0.290409927994593,
124.894156033358));
#160242=CARTESIAN_POINT('Ctrl Pts',(-185.391689764865,-0.373456639755591,
124.898823798456));
#160243=CARTESIAN_POINT('Ctrl Pts',(-185.395625814305,-0.456302018202181,
124.905231950493));
#160244=CARTESIAN_POINT('Ctrl Pts',(-185.403049080711,-0.612545816442367,
124.917317525243));
#160245=CARTESIAN_POINT('Ctrl Pts',(-185.410472347116,-0.768545395500247,
124.935633051325));
#160246=CARTESIAN_POINT('Ctrl Pts',(-185.417895613522,-0.923763824315242,
124.960167691303));
#160247=CARTESIAN_POINT('Ctrl Pts',(-185.425310106243,-1.07879879783747,
124.984673333373));
#160248=CARTESIAN_POINT('Ctrl Pts',(-185.432724598964,-1.23305409374088,
125.015383400464));
#160249=CARTESIAN_POINT('Ctrl Pts',(-185.440139091685,-1.38599527823421,
125.052235127696));
#160250=CARTESIAN_POINT('Ctrl Pts',(-185.447546438038,-1.53878905225622,
125.089051335846));
#160251=CARTESIAN_POINT('Ctrl Pts',(-185.454953784392,-1.69027087592442,
125.131997332593));
#160252=CARTESIAN_POINT('Ctrl Pts',(-185.462361130746,-1.83991402991944,
125.180958895743));
#160253=CARTESIAN_POINT('Ctrl Pts',(-185.469762952421,-1.98944557440407,
125.229883941511));
#160254=CARTESIAN_POINT('Ctrl Pts',(-185.477164774097,-2.1371408264938,
125.284815504598));
#160255=CARTESIAN_POINT('Ctrl Pts',(-185.484566595772,-2.28248592351566,
125.345588908523));
#160256=CARTESIAN_POINT('Ctrl Pts',(-185.491964510084,-2.42775429399301,
125.40633023064));
#160257=CARTESIAN_POINT('Ctrl Pts',(-185.499362424395,-2.57067463664222,
125.472907108294));
#160258=CARTESIAN_POINT('Ctrl Pts',(-185.506760338706,-2.7107509579538,
125.545105935916));
#160259=CARTESIAN_POINT('Ctrl Pts',(-185.514157023618,-2.85080400112102,
125.617292765403));
#160260=CARTESIAN_POINT('Ctrl Pts',(-185.521553708531,-2.98801362948039,
125.695099519758));
#160261=CARTESIAN_POINT('Ctrl Pts',(-185.528950393443,-3.12190634592099,
125.778265579686));
#160262=CARTESIAN_POINT('Ctrl Pts',(-185.536346750378,-3.25579312541823,
125.861427951945));
#160263=CARTESIAN_POINT('Ctrl Pts',(-185.543743107314,-3.38636296832752,
125.949948960309));
#160264=CARTESIAN_POINT('Ctrl Pts',(-185.551139464249,-3.51316962525318,
126.043523532903));
#160265=CARTESIAN_POINT('Ctrl Pts',(-185.558536953586,-3.6399956966021,
126.137112432005));
#160266=CARTESIAN_POINT('Ctrl Pts',(-185.565934442922,-3.7630571343807,
126.235756214237));
#160267=CARTESIAN_POINT('Ctrl Pts',(-185.573331932259,-3.88193928906325,
126.339108338184));
#160268=CARTESIAN_POINT('Ctrl Pts',(-185.580732014774,-4.00086311770033,
126.442496692057));
#160269=CARTESIAN_POINT('Ctrl Pts',(-185.588132097289,-4.1156044648104,
126.550596429015));
#160270=CARTESIAN_POINT('Ctrl Pts',(-185.595532179804,-4.22578429914888,
126.66302295691));
#160271=CARTESIAN_POINT('Ctrl Pts',(-185.60294039947,-4.33608528754245,
126.775573109331));
#160272=CARTESIAN_POINT('Ctrl Pts',(-185.610348619137,-4.44181448473375,
126.892459287456));
#160273=CARTESIAN_POINT('Ctrl Pts',(-185.617756838803,-4.54263156765102,
127.013261963735));
#160274=CARTESIAN_POINT('Ctrl Pts',(-185.625169618105,-4.64351070180004,
127.134138992044));
#160275=CARTESIAN_POINT('Ctrl Pts',(-185.632582397407,-4.73947147030228,
127.258937026566));
#160276=CARTESIAN_POINT('Ctrl Pts',(-185.639995176709,-4.8302162407166,
127.387206592589));
#160277=CARTESIAN_POINT('Ctrl Pts',(-185.647418547738,-4.92109067151479,
127.515659436183));
#160278=CARTESIAN_POINT('Ctrl Pts',(-185.654841918766,-5.00673401647177,
127.6475934058));
#160279=CARTESIAN_POINT('Ctrl Pts',(-185.662265289795,-5.08689361798639,
127.7825327135));
#160280=CARTESIAN_POINT('Ctrl Pts',(-185.666201339236,-5.12939616211485,
127.854080772271));
#160281=CARTESIAN_POINT('Ctrl Pts',(-185.670137388677,-5.17035781537923,
127.926473363939));
#160282=CARTESIAN_POINT('Ctrl Pts',(-185.674073438118,-5.20974640624689,
127.999637289839));
#160283=CARTESIAN_POINT('Ctrl Pts',(-185.681900715772,-5.288075055757,128.145131997376));
#160284=CARTESIAN_POINT('Ctrl Pts',(-185.689727993426,-5.36039597288839,
128.294079034415));
#160285=CARTESIAN_POINT('Ctrl Pts',(-185.69755527108,-5.42640910216598,
128.445968195082));
#160286=CARTESIAN_POINT('Ctrl Pts',(-185.705369342796,-5.49231085616024,
128.597601093116));
#160287=CARTESIAN_POINT('Ctrl Pts',(-185.713183414512,-5.55192591167538,
128.752165934091));
#160288=CARTESIAN_POINT('Ctrl Pts',(-185.720997486229,-5.60499975256745,
128.909127561655));
#160289=CARTESIAN_POINT('Ctrl Pts',(-185.728793533698,-5.6579511712372,
129.065727135315));
#160290=CARTESIAN_POINT('Ctrl Pts',(-185.736589581167,-5.70439137034077,
129.22471217246));
#160291=CARTESIAN_POINT('Ctrl Pts',(-185.744385628636,-5.7441138651048,
129.38552783418));
#160292=CARTESIAN_POINT('Ctrl Pts',(-185.752171064916,-5.78378229363978,
129.54612460994));
#160293=CARTESIAN_POINT('Ctrl Pts',(-185.759956501197,-5.81675116516731,
129.708546741938));
#160294=CARTESIAN_POINT('Ctrl Pts',(-185.767741937477,-5.842863099156,129.872222555356));
#160295=CARTESIAN_POINT('Ctrl Pts',(-185.775512714118,-5.86892586550339,
130.035590174303));
#160296=CARTESIAN_POINT('Ctrl Pts',(-185.783283490759,-5.88815739778654,
130.200206457726));
#160297=CARTESIAN_POINT('Ctrl Pts',(-185.7910542674,-5.90045097199386,130.365488324528));
#160298=CARTESIAN_POINT('Ctrl Pts',(-185.797911114185,-5.9112986849928,
130.511331203479));
#160299=CARTESIAN_POINT('Ctrl Pts',(-185.804767960969,-5.91674511390588,
130.657691966486));
#160300=CARTESIAN_POINT('Ctrl Pts',(-185.811624807754,-5.91674999671234,
130.804163375351));
#160301=CARTESIAN_POINT('',(-187.561624807792,-5.91674750900767,130.809789904034));
#160302=CARTESIAN_POINT('Ctrl Pts',(-185.811624807791,-5.91674999671237,
130.804163376133));
#160303=CARTESIAN_POINT('Ctrl Pts',(-185.819353984328,-5.91675550068887,
130.969268914026));
#160304=CARTESIAN_POINT('Ctrl Pts',(-185.827083160864,-5.90984584058032,
131.134248349692));
#160305=CARTESIAN_POINT('Ctrl Pts',(-185.834812337401,-5.89607849221174,
131.298515427497));
#160306=CARTESIAN_POINT('Ctrl Pts',(-185.84255057446,-5.88229500507678,
131.462975067292));
#160307=CARTESIAN_POINT('Ctrl Pts',(-185.85028881152,-5.86163781335462,
131.626720362507));
#160308=CARTESIAN_POINT('Ctrl Pts',(-185.858027048579,-5.83421588616898,
131.789173064722));
#160309=CARTESIAN_POINT('Ctrl Pts',(-185.865901549692,-5.80631108117604,
131.954486426734));
#160310=CARTESIAN_POINT('Ctrl Pts',(-185.873776050805,-5.77140116501924,
132.118460904788));
#160311=CARTESIAN_POINT('Ctrl Pts',(-185.881650551917,-5.72965398230494,
132.28050282127));
#160312=CARTESIAN_POINT('Ctrl Pts',(-185.889414944337,-5.68849054802612,
132.44027891503));
#160313=CARTESIAN_POINT('Ctrl Pts',(-185.897179336757,-5.64067998075974,
132.59817586172));
#160314=CARTESIAN_POINT('Ctrl Pts',(-185.904943729177,-5.58643216126939,
132.753644144925));
#160315=CARTESIAN_POINT('Ctrl Pts',(-185.912873284636,-5.53103038996559,
132.91241952709));
#160316=CARTESIAN_POINT('Ctrl Pts',(-185.920802840095,-5.46891459747241,
133.068661436369));
#160317=CARTESIAN_POINT('Ctrl Pts',(-185.928732395554,-5.40035816938212,
133.221810142352));
#160318=CARTESIAN_POINT('Ctrl Pts',(-185.936661951013,-5.33180174129202,
133.374958848335));
#160319=CARTESIAN_POINT('Ctrl Pts',(-185.944591506471,-5.25680489255712,
133.525014066598));
#160320=CARTESIAN_POINT('Ctrl Pts',(-185.95252106193,-5.17568835721522,
133.671446349016));
#160321=CARTESIAN_POINT('Ctrl Pts',(-185.959944328336,-5.09975097902817,
133.808529171427));
#160322=CARTESIAN_POINT('Ctrl Pts',(-185.967367594741,-5.01824886787116,
133.942800289093));
#160323=CARTESIAN_POINT('Ctrl Pts',(-185.974790861147,-4.93141506493196,
134.073775858838));
#160324=CARTESIAN_POINT('Ctrl Pts',(-185.982205353868,-4.84468389233649,
134.204596626337));
#160325=CARTESIAN_POINT('Ctrl Pts',(-185.989619846589,-4.75263377562075,
134.332129290969));
#160326=CARTESIAN_POINT('Ctrl Pts',(-185.99703433931,-4.65554394683494,
134.455913865376));
#160327=CARTESIAN_POINT('Ctrl Pts',(-186.004441685664,-4.55854769688175,
134.579579131549));
#160328=CARTESIAN_POINT('Ctrl Pts',(-186.011849032018,-4.45652163394964,
134.699503207619));
#160329=CARTESIAN_POINT('Ctrl Pts',(-186.019256378371,-4.34978858474558,
134.815254511764));
#160330=CARTESIAN_POINT('Ctrl Pts',(-186.026658200047,-4.24313514107611,
134.930919484221));
#160331=CARTESIAN_POINT('Ctrl Pts',(-186.034060021722,-4.13178195327352,
135.042417608329));
#160332=CARTESIAN_POINT('Ctrl Pts',(-186.041461843398,-4.0160923929967,
135.149349967773));
#160333=CARTESIAN_POINT('Ctrl Pts',(-186.048859757709,-3.90046390433854,
135.256225878457));
#160334=CARTESIAN_POINT('Ctrl Pts',(-186.056257672021,-3.78050387557164,
135.358540571827));
#160335=CARTESIAN_POINT('Ctrl Pts',(-186.063655586332,-3.65661275257442,
135.455931722065));
#160336=CARTESIAN_POINT('Ctrl Pts',(-186.071052271244,-3.53274221803405,
135.553306687661));
#160337=CARTESIAN_POINT('Ctrl Pts',(-186.078448956157,-3.4049421790122,
135.645759503541));
#160338=CARTESIAN_POINT('Ctrl Pts',(-186.085845641069,-3.27364649016796,
135.732967846785));
#160339=CARTESIAN_POINT('Ctrl Pts',(-186.093241998004,-3.14235662311216,
135.820172323119));
#160340=CARTESIAN_POINT('Ctrl Pts',(-186.10063835494,-3.00757172538186,
135.902132582656));
#160341=CARTESIAN_POINT('Ctrl Pts',(-186.108034711876,-2.86975475604621,
135.978569562192));
#160342=CARTESIAN_POINT('Ctrl Pts',(-186.115432201212,-2.73191668658033,
136.055018244425));
#160343=CARTESIAN_POINT('Ctrl Pts',(-186.122829690549,-2.59104594766015,
136.125941781829));
#160344=CARTESIAN_POINT('Ctrl Pts',(-186.130227179886,-2.44763008059823,
136.191107089329));
#160345=CARTESIAN_POINT('Ctrl Pts',(-186.137627262401,-2.30416393932624,
136.256295240426));
#160346=CARTESIAN_POINT('Ctrl Pts',(-186.145027344916,-2.15815123321437,
136.315720988395));
#160347=CARTESIAN_POINT('Ctrl Pts',(-186.152427427431,-2.01009930602779,
136.369199460013));
#160348=CARTESIAN_POINT('Ctrl Pts',(-186.159835647097,-1.8618845805278,
136.422736736708));
#160349=CARTESIAN_POINT('Ctrl Pts',(-186.167243866764,-1.71162650717714,
136.47031355006));
#160350=CARTESIAN_POINT('Ctrl Pts',(-186.174652086431,-1.5598481143866,
136.511794754071));
#160351=CARTESIAN_POINT('Ctrl Pts',(-186.182064865733,-1.40797630452743,
136.553301489072));
#160352=CARTESIAN_POINT('Ctrl Pts',(-186.189477645035,-1.25458267355879,
136.588705055152));
#160353=CARTESIAN_POINT('Ctrl Pts',(-186.196890424337,-1.10019974227204,
136.617921582208));
#160354=CARTESIAN_POINT('Ctrl Pts',(-186.204313795366,-0.94559622141344,
136.647179855207));
#160355=CARTESIAN_POINT('Ctrl Pts',(-186.211737166394,-0.790000945331487,
136.67023337849));
#160356=CARTESIAN_POINT('Ctrl Pts',(-186.219160537423,-0.633951672601608,
136.687050124867));
#160357=CARTESIAN_POINT('Ctrl Pts',(-186.223096586864,-0.551210603860005,
136.695966767307));
#160358=CARTESIAN_POINT('Ctrl Pts',(-186.227032636304,-0.468341915081361,
136.703130899092));
#160359=CARTESIAN_POINT('Ctrl Pts',(-186.230968685744,-0.385425554330736,
136.708543685914));
#160360=CARTESIAN_POINT('Ctrl Pts',(-186.23839195215,-0.229047885666553,
136.718752032934));
#160361=CARTESIAN_POINT('Ctrl Pts',(-186.245815218555,-0.0720279097393259,
136.72275881741));
#160362=CARTESIAN_POINT('Ctrl Pts',(-186.253238484961,0.0851013380298015,
136.72049857444));
#160363=CARTESIAN_POINT('Ctrl Pts',(-186.260652977682,0.242044872077285,
136.718241002889));
#160364=CARTESIAN_POINT('Ctrl Pts',(-186.268067470403,0.399097051278048,
136.709731153093));
#160365=CARTESIAN_POINT('Ctrl Pts',(-186.275481963124,0.555719943496593,
136.694955316482));
#160366=CARTESIAN_POINT('Ctrl Pts',(-186.282889309477,0.712191876675316,
136.680193721379));
#160367=CARTESIAN_POINT('Ctrl Pts',(-186.290296655831,0.868234977439624,
136.65917819753));
#160368=CARTESIAN_POINT('Ctrl Pts',(-186.297704002185,1.02331164805928,
136.631947067671));
#160369=CARTESIAN_POINT('Ctrl Pts',(-186.30510582386,1.1782726566464,136.604736247816));
#160370=CARTESIAN_POINT('Ctrl Pts',(-186.312507645536,1.33226830420908,
136.571319116806));
#160371=CARTESIAN_POINT('Ctrl Pts',(-186.319909467211,1.48476655989437,
136.531785765494));
#160372=CARTESIAN_POINT('Ctrl Pts',(-186.327307381523,1.63718431293841,
136.492273283531));
#160373=CARTESIAN_POINT('Ctrl Pts',(-186.334705295834,1.78810588790865,
136.446651104826));
#160374=CARTESIAN_POINT('Ctrl Pts',(-186.342103210145,1.93700999905407,
136.395060289885));
#160375=CARTESIAN_POINT('Ctrl Pts',(-186.349499895057,2.08588936503698,
136.343478048401));
#160376=CARTESIAN_POINT('Ctrl Pts',(-186.35689657997,2.23275158021718,136.285929261356));
#160377=CARTESIAN_POINT('Ctrl Pts',(-186.364293264882,2.37709095615206,
136.22260471955));
#160378=CARTESIAN_POINT('Ctrl Pts',(-186.371689621817,2.52142393192816,
136.15928298562));
#160379=CARTESIAN_POINT('Ctrl Pts',(-186.379085978753,2.66323394903901,
136.090186156123));
#160380=CARTESIAN_POINT('Ctrl Pts',(-186.386482335688,2.80203598302284,
136.015552891158));
#160381=CARTESIAN_POINT('Ctrl Pts',(-186.393879825025,2.94085926795201,
135.94090819965));
#160382=CARTESIAN_POINT('Ctrl Pts',(-186.401277314361,3.07667332397372,
135.860725561701));
#160383=CARTESIAN_POINT('Ctrl Pts',(-186.408674803698,3.20901852202426,
135.775289171449));
#160384=CARTESIAN_POINT('Ctrl Pts',(-186.416074886213,3.34141011347863,
135.689822831602));
#160385=CARTESIAN_POINT('Ctrl Pts',(-186.423474968728,3.47033011248045,
135.599099274988));
#160386=CARTESIAN_POINT('Ctrl Pts',(-186.430875051243,3.59534874825436,
135.503445415793));
#160387=CARTESIAN_POINT('Ctrl Pts',(-186.438283270909,3.72050485487072,
135.407686375345));
#160388=CARTESIAN_POINT('Ctrl Pts',(-186.445691490576,3.84175073429224,
135.306986432451));
#160389=CARTESIAN_POINT('Ctrl Pts',(-186.453099710242,3.95868997473241,
135.201712576012));
#160390=CARTESIAN_POINT('Ctrl Pts',(-186.460512489544,4.07570118932416,
135.096373925272));
#160391=CARTESIAN_POINT('Ctrl Pts',(-186.467925268846,4.18840021653473,
134.986456011451));
#160392=CARTESIAN_POINT('Ctrl Pts',(-186.475338048148,4.29642865357484,
134.872361525536));
#160393=CARTESIAN_POINT('Ctrl Pts',(-186.482761419177,4.40461144671197,
134.758104016068));
#160394=CARTESIAN_POINT('Ctrl Pts',(-186.490184790206,4.50811007610825,
134.639658296061));
#160395=CARTESIAN_POINT('Ctrl Pts',(-186.497608161235,4.60660692473589,
134.517459485557));
#160396=CARTESIAN_POINT('Ctrl Pts',(-186.501544210675,4.65883231727349,
134.452666744113));
#160397=CARTESIAN_POINT('Ctrl Pts',(-186.505480260116,4.7096522547113,134.386819357501));
#160398=CARTESIAN_POINT('Ctrl Pts',(-186.509416309556,4.75902450389532,
134.319985218377));
#160399=CARTESIAN_POINT('Ctrl Pts',(-186.516839575961,4.85213902500785,
134.193938117801));
#160400=CARTESIAN_POINT('Ctrl Pts',(-186.524262842367,4.94038317868034,
134.063998529898));
#160401=CARTESIAN_POINT('Ctrl Pts',(-186.531686108772,5.02341376877007,
133.930579527085));
#160402=CARTESIAN_POINT('Ctrl Pts',(-186.539100601493,5.10634622359734,
133.797318214453));
#160403=CARTESIAN_POINT('Ctrl Pts',(-186.546515094214,5.18407718502282,
133.660585986465));
#160404=CARTESIAN_POINT('Ctrl Pts',(-186.553929586935,5.25630435417878,
133.520828010844));
#160405=CARTESIAN_POINT('Ctrl Pts',(-186.561336933289,5.3284619080698,133.381204739222));
#160406=CARTESIAN_POINT('Ctrl Pts',(-186.568744279642,5.39512606019245,
133.238561855208));
#160407=CARTESIAN_POINT('Ctrl Pts',(-186.576151625996,5.45603846784417,
133.093372369372));
#160408=CARTESIAN_POINT('Ctrl Pts',(-186.583553447672,5.51690544472435,
132.948291171332));
#160409=CARTESIAN_POINT('Ctrl Pts',(-186.590955269347,5.57202907504359,
132.800667496085));
#160410=CARTESIAN_POINT('Ctrl Pts',(-186.598357091022,5.6211975791176,132.650997652563));
#160411=CARTESIAN_POINT('Ctrl Pts',(-186.605755005334,5.67034012752104,
132.501406818586));
#160412=CARTESIAN_POINT('Ctrl Pts',(-186.613152919645,5.71353369422572,
132.349772321271));
#160413=CARTESIAN_POINT('Ctrl Pts',(-186.620550833956,5.75061518974696,
132.196608979731));
#160414=CARTESIAN_POINT('Ctrl Pts',(-186.627947518869,5.78769052299643,
132.043471091159));
#160415=CARTESIAN_POINT('Ctrl Pts',(-186.635344203781,5.81865571320347,
131.88880522507));
#160416=CARTESIAN_POINT('Ctrl Pts',(-186.642740888693,5.84339794111647,
131.733139958559));
#160417=CARTESIAN_POINT('Ctrl Pts',(-186.650137245628,5.86813907193316,
131.577481594409));
#160418=CARTESIAN_POINT('Ctrl Pts',(-186.657533602564,5.88665773050493,
131.42082428662));
#160419=CARTESIAN_POINT('Ctrl Pts',(-186.664929959499,5.89889254076296,
131.26370510162));
#160420=CARTESIAN_POINT('Ctrl Pts',(-186.672327448836,5.91112922420171,
131.106561861272));
#160421=CARTESIAN_POINT('Ctrl Pts',(-186.679724938173,5.91708011472825,
130.948956975106));
#160422=CARTESIAN_POINT('Ctrl Pts',(-186.687122427509,5.91673587218311,
130.791430755944));
#160423=CARTESIAN_POINT('Ctrl Pts',(-186.694522510024,5.91639150896428,
130.633849316211));
#160424=CARTESIAN_POINT('Ctrl Pts',(-186.701922592539,5.90974761986768,
130.47634697145));
#160425=CARTESIAN_POINT('Ctrl Pts',(-186.709322675054,5.89684694545481,
130.319462005091));
#160426=CARTESIAN_POINT('Ctrl Pts',(-186.716730894721,5.88393208542427,
130.162404527584));
#160427=CARTESIAN_POINT('Ctrl Pts',(-186.724139114387,5.86474673092027,
130.005966156498));
#160428=CARTESIAN_POINT('Ctrl Pts',(-186.731547334054,5.83938536984659,
129.850678770763));
#160429=CARTESIAN_POINT('Ctrl Pts',(-186.738960113356,5.81400839927836,
129.695295808233));
#160430=CARTESIAN_POINT('Ctrl Pts',(-186.746372892658,5.78244792237959,
129.541065607525));
#160431=CARTESIAN_POINT('Ctrl Pts',(-186.75378567196,5.7448490090175,129.38850736737));
#160432=CARTESIAN_POINT('Ctrl Pts',(-186.761209042988,5.70719637256474,
129.235731144846));
#160433=CARTESIAN_POINT('Ctrl Pts',(-186.768632414017,5.66348817105071,
129.084632011842));
#160434=CARTESIAN_POINT('Ctrl Pts',(-186.776055785046,5.61391880352735,
128.935712381567));
#160435=CARTESIAN_POINT('Ctrl Pts',(-186.779991834487,5.58763593546334,
128.856751620311));
#160436=CARTESIAN_POINT('Ctrl Pts',(-186.783927883928,5.55970608173856,
128.77840324676));
#160437=CARTESIAN_POINT('Ctrl Pts',(-186.787863933369,5.53016353431541,
128.700739490502));
#160438=CARTESIAN_POINT('Ctrl Pts',(-186.795287199775,5.47444721187183,
128.554268070017));
#160439=CARTESIAN_POINT('Ctrl Pts',(-186.80271046618,5.41282347703181,128.409790243116));
#160440=CARTESIAN_POINT('Ctrl Pts',(-186.810133732586,5.34545435342012,
128.267818026163));
#160441=CARTESIAN_POINT('Ctrl Pts',(-186.817548225307,5.27816485451769,
128.12601360858));
#160442=CARTESIAN_POINT('Ctrl Pts',(-186.824962718028,5.20514364198745,
127.986709240179));
#160443=CARTESIAN_POINT('Ctrl Pts',(-186.832377210749,5.12660184812075,
127.850399877586));
#160444=CARTESIAN_POINT('Ctrl Pts',(-186.839784557103,5.04813575579202,
127.714221895088));
#160445=CARTESIAN_POINT('Ctrl Pts',(-186.847191903456,4.96415986019837,
127.581033492824));
#160446=CARTESIAN_POINT('Ctrl Pts',(-186.85459924981,4.87493247798782,127.451307695592));
#160447=CARTESIAN_POINT('Ctrl Pts',(-186.862001071486,4.78577164492528,
127.321678652754));
#160448=CARTESIAN_POINT('Ctrl Pts',(-186.869402893161,4.69136733467664,
127.195507379004));
#160449=CARTESIAN_POINT('Ctrl Pts',(-186.876804714836,4.59202263391012,
127.073240317689));
#160450=CARTESIAN_POINT('Ctrl Pts',(-186.884202629148,4.4927303764384,126.951037800204));
#160451=CARTESIAN_POINT('Ctrl Pts',(-186.891600543459,4.38850315720013,
126.832735679553));
#160452=CARTESIAN_POINT('Ctrl Pts',(-186.89899845777,4.27968595424607,126.718749439844));
#160453=CARTESIAN_POINT('Ctrl Pts',(-186.906395142683,4.17088683473652,
126.604782142579));
#160454=CARTESIAN_POINT('Ctrl Pts',(-186.913791827595,4.05749950290368,
126.495129572533));
#160455=CARTESIAN_POINT('Ctrl Pts',(-186.921188512507,3.93990768406763,
126.390172356569));
#160456=CARTESIAN_POINT('Ctrl Pts',(-186.928584869443,3.82232107937571,
126.285219794517));
#160457=CARTESIAN_POINT('Ctrl Pts',(-186.935981226378,3.70053063686753,
126.184962421158));
#160458=CARTESIAN_POINT('Ctrl Pts',(-186.943377583313,3.57495503047606,
126.089742171438));
#160459=CARTESIAN_POINT('Ctrl Pts',(-186.95077507265,3.4493601981394,125.994507343255));
#160460=CARTESIAN_POINT('Ctrl Pts',(-186.958172561986,3.31997934549403,
125.904311399832));
#160461=CARTESIAN_POINT('Ctrl Pts',(-186.965570051323,3.18726200443501,
125.819454251586));
#160462=CARTESIAN_POINT('Ctrl Pts',(-186.972970133838,3.05449813951574,
125.734567356798));
#160463=CARTESIAN_POINT('Ctrl Pts',(-186.980370216353,2.91839577182612,
125.655023184307));
#160464=CARTESIAN_POINT('Ctrl Pts',(-186.987770298868,2.77943087677651,
125.581076730611));
#160465=CARTESIAN_POINT('Ctrl Pts',(-186.995178518535,2.64031317554104,
125.507048965188));
#160466=CARTESIAN_POINT('Ctrl Pts',(-187.002586738201,2.49832699064388,
125.438631386499));
#160467=CARTESIAN_POINT('Ctrl Pts',(-187.009994957867,2.35397087991152,
125.376031992747));
#160468=CARTESIAN_POINT('Ctrl Pts',(-187.017407737169,2.20952592040129,
125.313394070112));
#160469=CARTESIAN_POINT('Ctrl Pts',(-187.024820516472,2.06270847584779,
125.256581602402));
#160470=CARTESIAN_POINT('Ctrl Pts',(-187.032233295774,1.91403377665382,
125.205753177825));
#160471=CARTESIAN_POINT('Ctrl Pts',(-187.039656666802,1.76514664407727,
125.15485212721));
#160472=CARTESIAN_POINT('Ctrl Pts',(-187.047080037831,1.61439731357947,
125.109952302834));
#160473=CARTESIAN_POINT('Ctrl Pts',(-187.05450340886,1.46231355706026,125.071161717882));
#160474=CARTESIAN_POINT('Ctrl Pts',(-187.058439458301,1.38167510015412,
125.050594018973));
#160475=CARTESIAN_POINT('Ctrl Pts',(-187.062375507741,1.30066162638929,
125.031742986259));
#160476=CARTESIAN_POINT('Ctrl Pts',(-187.066311557182,1.21935244020638,
125.014618810796));
#160477=CARTESIAN_POINT('Ctrl Pts',(-187.073734823588,1.06600585263888,
124.9823231503));
#160478=CARTESIAN_POINT('Ctrl Pts',(-187.081158089993,0.911143431117751,
124.956075149189));
#160479=CARTESIAN_POINT('Ctrl Pts',(-187.088581356398,0.755283527239422,
124.936015249749));
#160480=CARTESIAN_POINT('Ctrl Pts',(-187.095995849119,0.599607836824118,
124.915979059444));
#160481=CARTESIAN_POINT('Ctrl Pts',(-187.10341034184,0.442937377369268,
124.902116459795));
#160482=CARTESIAN_POINT('Ctrl Pts',(-187.110824834561,0.285802692063943,
124.894517355371));
#160483=CARTESIAN_POINT('Ctrl Pts',(-187.118232180915,0.128819459083885,
124.88692557525));
#160484=CARTESIAN_POINT('Ctrl Pts',(-187.125639527269,-0.0286267386259374,
124.885585289803));
#160485=CARTESIAN_POINT('Ctrl Pts',(-187.133046873623,-0.185998305446971,
124.890534851374));
#160486=CARTESIAN_POINT('Ctrl Pts',(-187.140448695298,-0.343252498615732,
124.895480721376));
#160487=CARTESIAN_POINT('Ctrl Pts',(-187.147850516973,-0.500431800219757,
124.906707085891));
#160488=CARTESIAN_POINT('Ctrl Pts',(-187.155252338649,-0.656996779079823,
124.924200263054));
#160489=CARTESIAN_POINT('Ctrl Pts',(-187.16265025296,-0.813479108507141,
124.941684205705));
#160490=CARTESIAN_POINT('Ctrl Pts',(-187.170048167272,-0.969347390991606,
124.965428331216));
#160491=CARTESIAN_POINT('Ctrl Pts',(-187.177446081583,-1.12406559892257,
124.995366979093));
#160492=CARTESIAN_POINT('Ctrl Pts',(-187.184842766495,-1.27875809549403,
125.02530065171));
#160493=CARTESIAN_POINT('Ctrl Pts',(-187.192239451407,-1.43230053069113,
125.061426732754));
#160494=CARTESIAN_POINT('Ctrl Pts',(-187.199636136319,-1.58416525944525,
125.103628121363));
#160495=CARTESIAN_POINT('Ctrl Pts',(-187.207032493255,-1.73602325435815,
125.145827638718));
#160496=CARTESIAN_POINT('Ctrl Pts',(-187.21442885019,-1.88620333107437,
125.194101828061));
#160497=CARTESIAN_POINT('Ctrl Pts',(-187.221825207126,-2.03419150655014,
125.248283271346));
#160498=CARTESIAN_POINT('Ctrl Pts',(-187.229222696462,-2.18220233939295,
125.302473009948));
#160499=CARTESIAN_POINT('Ctrl Pts',(-187.236620185799,-2.32802025223464,
125.362571674956));
#160500=CARTESIAN_POINT('Ctrl Pts',(-187.244017675135,-2.4711499389764,
125.428363171362));
#160501=CARTESIAN_POINT('Ctrl Pts',(-187.25141775765,-2.61432979960858,
125.494177730874));
#160502=CARTESIAN_POINT('Ctrl Pts',(-187.258817840165,-2.75481921895261,
125.565688939224));
#160503=CARTESIAN_POINT('Ctrl Pts',(-187.26621792268,-2.89214638489867,
125.642634176653));
#160504=CARTESIAN_POINT('Ctrl Pts',(-187.273626142347,-3.02962455618108,
125.719664023281));
#160505=CARTESIAN_POINT('Ctrl Pts',(-187.281034362013,-3.16393320396151,
125.802139649419));
#160506=CARTESIAN_POINT('Ctrl Pts',(-187.28844258168,-3.29462785077745,
125.889754032357));
#160507=CARTESIAN_POINT('Ctrl Pts',(-187.295855360982,-3.42540293796775,
125.977422340486));
#160508=CARTESIAN_POINT('Ctrl Pts',(-187.303268140284,-3.55255929106162,
126.070235488155));
#160509=CARTESIAN_POINT('Ctrl Pts',(-187.310680919586,-3.67568499069044,
126.167845718236));
#160510=CARTESIAN_POINT('Ctrl Pts',(-187.318104290615,-3.79898661809308,
126.26559541839));
#160511=CARTESIAN_POINT('Ctrl Pts',(-187.325527661644,-3.91824580736076,
126.368155647766));
#160512=CARTESIAN_POINT('Ctrl Pts',(-187.332951032672,-4.03308641033856,
126.475140760682));
#160513=CARTESIAN_POINT('Ctrl Pts',(-187.336887082113,-4.09397765360244,
126.531866834624));
#160514=CARTESIAN_POINT('Ctrl Pts',(-187.340823131554,-4.1536273227506,
126.589836320882));
#160515=CARTESIAN_POINT('Ctrl Pts',(-187.344759180995,-4.21198397777087,
126.648988006897));
#160516=CARTESIAN_POINT('Ctrl Pts',(-187.352082400964,-4.32055949944319,
126.759042724129));
#160517=CARTESIAN_POINT('Ctrl Pts',(-187.359405620933,-4.42500455681407,
126.873544452405));
#160518=CARTESIAN_POINT('Ctrl Pts',(-187.366728840903,-4.52492539990628,
126.992145947878));
#160519=CARTESIAN_POINT('Ctrl Pts',(-187.374043222144,-4.62472564397862,
127.1106042978));
#160520=CARTESIAN_POINT('Ctrl Pts',(-187.381357603385,-4.72001229335793,
127.233152278661));
#160521=CARTESIAN_POINT('Ctrl Pts',(-187.388671984626,-4.81042708213411,
127.3594046164));
#160522=CARTESIAN_POINT('Ctrl Pts',(-187.395978017208,-4.90073867116098,
127.485512849288));
#160523=CARTESIAN_POINT('Ctrl Pts',(-187.403284049789,-4.98618925122516,
127.615316708677));
#160524=CARTESIAN_POINT('Ctrl Pts',(-187.410590082371,-5.06645997052641,
127.748396951297));
#160525=CARTESIAN_POINT('Ctrl Pts',(-187.417891395085,-5.14667883307661,
127.881391220987));
#160526=CARTESIAN_POINT('Ctrl Pts',(-187.4251927078,-5.22172429356674,128.017657336095));
#160527=CARTESIAN_POINT('Ctrl Pts',(-187.432494020514,-5.29131999812529,
128.156745985498));
#160528=CARTESIAN_POINT('Ctrl Pts',(-187.439792150053,-5.36088536083589,
128.295773996006));
#160529=CARTESIAN_POINT('Ctrl Pts',(-187.447090279593,-5.42500552334415,
128.437621749531));
#160530=CARTESIAN_POINT('Ctrl Pts',(-187.454388409132,-5.48344955540227,
128.581814434501));
#160531=CARTESIAN_POINT('Ctrl Pts',(-187.461684889562,-5.54188038124945,
128.725974537204));
#160532=CARTESIAN_POINT('Ctrl Pts',(-187.468981369991,-5.59463748570317,
128.87247816067));
#160533=CARTESIAN_POINT('Ctrl Pts',(-187.47627785042,-5.64153778312993,
129.020829848553));
#160534=CARTESIAN_POINT('Ctrl Pts',(-187.483576690867,-5.68845325027215,
129.169229520201));
#160535=CARTESIAN_POINT('Ctrl Pts',(-187.490875531314,-5.7295080036463,
129.319478085701));
#160536=CARTESIAN_POINT('Ctrl Pts',(-187.498174371761,-5.76456856275173,
129.471064008467));
#160537=CARTESIAN_POINT('Ctrl Pts',(-187.505474224208,-5.79963398307961,
129.62267094895));
#160538=CARTESIAN_POINT('Ctrl Pts',(-187.512774076655,-5.82870347565599,
129.775615239507));
#160539=CARTESIAN_POINT('Ctrl Pts',(-187.520073929102,-5.85169470676966,
129.929375119821));
#160540=CARTESIAN_POINT('Ctrl Pts',(-187.527380321913,-5.87470653706738,
130.083272762574));
#160541=CARTESIAN_POINT('Ctrl Pts',(-187.534686714723,-5.89162917731749,
130.237987073307));
#160542=CARTESIAN_POINT('Ctrl Pts',(-187.541993107533,-5.9024321476053,
130.392990582907));
#160543=CARTESIAN_POINT('Ctrl Pts',(-187.54853700762,-5.91210772350591,
130.531817977784));
#160544=CARTESIAN_POINT('Ctrl Pts',(-187.555080907706,-5.91687497723714,
130.670877114353));
#160545=CARTESIAN_POINT('Ctrl Pts',(-187.561624807792,-5.91674750900767,
130.809789904034));
#160546=CARTESIAN_POINT('',(-189.311624807792,-5.92158926949562,130.802089018337));
#160547=CARTESIAN_POINT('Ctrl Pts',(-187.561624807792,-5.91744066498834,
130.809790540083));
#160548=CARTESIAN_POINT('Ctrl Pts',(-187.582152140131,-5.92149194206913,
131.245596366776));
#160549=CARTESIAN_POINT('Ctrl Pts',(-187.695495347076,-5.67831340457064,
133.64744955503));
#160550=CARTESIAN_POINT('Ctrl Pts',(-187.90165442862,-2.39945118657061,
137.378567378342));
#160551=CARTESIAN_POINT('Ctrl Pts',(-188.180102052435,4.23410436286723,
136.376606194958));
#160552=CARTESIAN_POINT('Ctrl Pts',(-188.458549676247,6.97672485032798,
130.254023545258));
#160553=CARTESIAN_POINT('Ctrl Pts',(-188.73699730006,3.3080760322958,124.637173779559));
#160554=CARTESIAN_POINT('Ctrl Pts',(-189.015444923873,-3.40053305091948,
124.687667434156));
#160555=CARTESIAN_POINT('Ctrl Pts',(-189.20698742645,-5.86572937063765,
128.589015218929));
#160556=CARTESIAN_POINT('Ctrl Pts',(-189.305714054423,-5.92609167912231,
130.677041554188));
#160557=CARTESIAN_POINT('Ctrl Pts',(-189.311624807792,-5.92547957657923,
130.802087525964));
#160558=CARTESIAN_POINT('',(-191.061624793292,-5.91313729896144,130.80003214728));
#160559=CARTESIAN_POINT('Ctrl Pts',(-189.311624807792,-5.91674956464851,
130.802090874911));
#160560=CARTESIAN_POINT('Ctrl Pts',(-189.318977448973,-5.91680914766334,
130.957411468767));
#160561=CARTESIAN_POINT('Ctrl Pts',(-189.326330090154,-5.91074854494049,
131.112981837623));
#160562=CARTESIAN_POINT('Ctrl Pts',(-189.333682731335,-5.89853497471983,
131.268274094959));
#160563=CARTESIAN_POINT('Ctrl Pts',(-189.341027006048,-5.88633530215123,
131.42338964739));
#160564=CARTESIAN_POINT('Ctrl Pts',(-189.348371280761,-5.86799662359575,
131.578227341974));
#160565=CARTESIAN_POINT('Ctrl Pts',(-189.355715555474,-5.8435381292413,
131.732257537813));
#160566=CARTESIAN_POINT('Ctrl Pts',(-189.363053149278,-5.81910188418644,
131.886147616115));
#160567=CARTESIAN_POINT('Ctrl Pts',(-189.370390743082,-5.78855696232474,
132.039231283816));
#160568=CARTESIAN_POINT('Ctrl Pts',(-189.377728336886,-5.75197447447406,
132.190982486533));
#160569=CARTESIAN_POINT('Ctrl Pts',(-189.385060929245,-5.71541692194747,
132.342630252726));
#160570=CARTESIAN_POINT('Ctrl Pts',(-189.392393521605,-5.67283008434618,
132.492946992982));
#160571=CARTESIAN_POINT('Ctrl Pts',(-189.399726113965,-5.62433638296606,
132.641415546996));
#160572=CARTESIAN_POINT('Ctrl Pts',(-189.407056104548,-5.57585988828992,
132.789831420881));
#160573=CARTESIAN_POINT('Ctrl Pts',(-189.414386095132,-5.52148081560047,
132.936400051107));
#160574=CARTESIAN_POINT('Ctrl Pts',(-189.421716085716,-5.46137178798303,
133.080618238294));
#160575=CARTESIAN_POINT('Ctrl Pts',(-189.429044866575,-5.40127268062225,
133.224812624041));
#160576=CARTESIAN_POINT('Ctrl Pts',(-189.436373647433,-5.33544564582625,
133.366656986859));
#160577=CARTESIAN_POINT('Ctrl Pts',(-189.443702428292,-5.26411181390032,
133.505667222388));
#160578=CARTESIAN_POINT('Ctrl Pts',(-189.45103151263,-5.19277502809146,
133.644683214231));
#160579=CARTESIAN_POINT('Ctrl Pts',(-189.458360596969,-5.11593116510898,
133.780864506177));
#160580=CARTESIAN_POINT('Ctrl Pts',(-189.465689681307,-5.03384764105057,
133.913750990162));
#160581=CARTESIAN_POINT('Ctrl Pts',(-189.473020582319,-4.95174377079516,
134.046670412968));
#160582=CARTESIAN_POINT('Ctrl Pts',(-189.480351483332,-4.86439785503814,
134.176293078574));
#160583=CARTESIAN_POINT('Ctrl Pts',(-189.487682384344,-4.77212086708803,
134.302187513283));
#160584=CARTESIAN_POINT('Ctrl Pts',(-189.495020896959,-4.6797480688371,
134.428212662962));
#160585=CARTESIAN_POINT('Ctrl Pts',(-189.502359409575,-4.5824341979447,
134.550501542638));
#160586=CARTESIAN_POINT('Ctrl Pts',(-189.509697922191,-4.48053120714239,
134.668654946978));
#160587=CARTESIAN_POINT('Ctrl Pts',(-189.517040396452,-4.37857320471192,
134.78687213562));
#160588=CARTESIAN_POINT('Ctrl Pts',(-189.524382870713,-4.27202140698691,
134.900949123779));
#160589=CARTESIAN_POINT('Ctrl Pts',(-189.531725344974,-4.16126441642406,
135.010523835881));
#160590=CARTESIAN_POINT('Ctrl Pts',(-189.539078893906,-4.05034037083163,
135.120263819778));
#160591=CARTESIAN_POINT('Ctrl Pts',(-189.546432442839,-3.93519874240669,
135.225487704928));
#160592=CARTESIAN_POINT('Ctrl Pts',(-189.553785991771,-3.81626167847011,
135.325873347167));
#160593=CARTESIAN_POINT('Ctrl Pts',(-189.559970718347,-3.71622926868426,
135.410303022565));
#160594=CARTESIAN_POINT('Ctrl Pts',(-189.566155444922,-3.61351273278213,
135.491310933321));
#160595=CARTESIAN_POINT('Ctrl Pts',(-189.572340171498,-3.50837810462016,
135.568729792758));
#160596=CARTESIAN_POINT('Ctrl Pts',(-189.579763437904,-3.38218944555196,
135.661652383818));
#160597=CARTESIAN_POINT('Ctrl Pts',(-189.587186704309,-3.25211571553351,
135.749698689375));
#160598=CARTESIAN_POINT('Ctrl Pts',(-189.594609970715,-3.11857050878932,
135.832526142309));
#160599=CARTESIAN_POINT('Ctrl Pts',(-189.602024463436,-2.98518314138887,
135.915255700071));
#160600=CARTESIAN_POINT('Ctrl Pts',(-189.609438956157,-2.84833277843893,
135.992778488313));
#160601=CARTESIAN_POINT('Ctrl Pts',(-189.616853448878,-2.70846504719477,
136.064792885985));
#160602=CARTESIAN_POINT('Ctrl Pts',(-189.624260795232,-2.5687321257355,
136.13673787347));
#160603=CARTESIAN_POINT('Ctrl Pts',(-189.631668141586,-2.42598795540314,
136.203184870211));
#160604=CARTESIAN_POINT('Ctrl Pts',(-189.63907548794,-2.28070593937386,
136.263876253646));
#160605=CARTESIAN_POINT('Ctrl Pts',(-189.646477309616,-2.13553228015454,
136.324522371158));
#160606=CARTESIAN_POINT('Ctrl Pts',(-189.653879131291,-1.98782488706824,
136.379421279541));
#160607=CARTESIAN_POINT('Ctrl Pts',(-189.661280952967,-1.83808039076475,
136.428361954656));
#160608=CARTESIAN_POINT('Ctrl Pts',(-189.668678867278,-1.68841494341483,
136.477276794369));
#160609=CARTESIAN_POINT('Ctrl Pts',(-189.67607678159,-1.53671488843013,
136.520239549164));
#160610=CARTESIAN_POINT('Ctrl Pts',(-189.683474695901,-1.38349529252278,
136.557087913212));
#160611=CARTESIAN_POINT('Ctrl Pts',(-189.690871380814,-1.23030115893236,
136.59393015373));
#160612=CARTESIAN_POINT('Ctrl Pts',(-189.698268065726,-1.07558834819108,
136.62465993296));
#160613=CARTESIAN_POINT('Ctrl Pts',(-189.705664750638,-0.919885608475016,
136.649165236184));
#160614=CARTESIAN_POINT('Ctrl Pts',(-189.713061107574,-0.7641897727816,
136.673669452817));
#160615=CARTESIAN_POINT('Ctrl Pts',(-189.72045746451,-0.607504464148897,
136.691949684189));
#160616=CARTESIAN_POINT('Ctrl Pts',(-189.727853821445,-0.450366841788114,
136.703945371624));
#160617=CARTESIAN_POINT('Ctrl Pts',(-189.735251310782,-0.293205161256196,
136.71594289563));
#160618=CARTESIAN_POINT('Ctrl Pts',(-189.742648800119,-0.135591401348304,
136.721653931456));
#160619=CARTESIAN_POINT('Ctrl Pts',(-189.750046289455,0.021934111525369,
136.721069961217));
#160620=CARTESIAN_POINT('Ctrl Pts',(-189.75744637197,0.179514844723607,
136.720485786269));
#160621=CARTESIAN_POINT('Ctrl Pts',(-189.764846454486,0.337006896234077,
136.713602213106));
#160622=CARTESIAN_POINT('Ctrl Pts',(-189.772246537001,0.493872048296028,
136.700462801417));
#160623=CARTESIAN_POINT('Ctrl Pts',(-189.779654756667,0.650909689718572,
136.687308941594));
#160624=CARTESIAN_POINT('Ctrl Pts',(-189.787062976334,0.807318682811136,
136.667885536733));
#160625=CARTESIAN_POINT('Ctrl Pts',(-189.794471196001,0.962567293055188,
136.642287884057));
#160626=CARTESIAN_POINT('Ctrl Pts',(-189.801883975303,1.11791145622882,
136.616674476453));
#160627=CARTESIAN_POINT('Ctrl Pts',(-189.809296754605,1.27209344867101,
136.584879323986));
#160628=CARTESIAN_POINT('Ctrl Pts',(-189.816709533907,1.4245942930246,136.547048286487));
#160629=CARTESIAN_POINT('Ctrl Pts',(-189.824132904936,1.57731303773595,
136.509163194228));
#160630=CARTESIAN_POINT('Ctrl Pts',(-189.831556275965,1.72834547933129,
136.465225096164));
#160631=CARTESIAN_POINT('Ctrl Pts',(-189.838979646994,1.87718950102327,
136.41542915571));
#160632=CARTESIAN_POINT('Ctrl Pts',(-189.842915696433,1.95611017275407,
136.389026153255));
#160633=CARTESIAN_POINT('Ctrl Pts',(-189.846851745872,2.03441595105685,
136.360977098998));
#160634=CARTESIAN_POINT('Ctrl Pts',(-189.850787795312,2.11203465861468,
136.331316394783));
#160635=CARTESIAN_POINT('Ctrl Pts',(-189.858211061717,2.25842111873141,
136.275377232289));
#160636=CARTESIAN_POINT('Ctrl Pts',(-189.865634328123,2.40280499749717,
136.213533698149));
#160637=CARTESIAN_POINT('Ctrl Pts',(-189.873057594528,2.54467452571146,
136.145948595003));
#160638=CARTESIAN_POINT('Ctrl Pts',(-189.880472087249,2.68637637592454,
136.078443371836));
#160639=CARTESIAN_POINT('Ctrl Pts',(-189.88788657997,2.82556945715901,136.005210246327));
#160640=CARTESIAN_POINT('Ctrl Pts',(-189.895301072691,2.96175913466819,
135.926461103764));
#160641=CARTESIAN_POINT('Ctrl Pts',(-189.902708419045,3.09781754743913,
135.847787862589));
#160642=CARTESIAN_POINT('Ctrl Pts',(-189.910115765399,3.23087799845622,
135.763609374162));
#160643=CARTESIAN_POINT('Ctrl Pts',(-189.917523111753,3.36046785658173,
135.674184674694));
#160644=CARTESIAN_POINT('Ctrl Pts',(-189.924924933428,3.48996106170153,
135.584826671541));
#160645=CARTESIAN_POINT('Ctrl Pts',(-189.932326755103,3.61598852205761,
135.49023045941));
#160646=CARTESIAN_POINT('Ctrl Pts',(-189.939728576779,3.73810425606627,
135.390699804028));
#160647=CARTESIAN_POINT('Ctrl Pts',(-189.94712649109,3.86015552612914,135.291221690105));
#160648=CARTESIAN_POINT('Ctrl Pts',(-189.954524405402,3.97829889370356,
135.18681455587));
#160649=CARTESIAN_POINT('Ctrl Pts',(-189.961922319713,4.09211940015992,
135.077824011271));
#160650=CARTESIAN_POINT('Ctrl Pts',(-189.969319004625,4.20592099171351,
134.968851578922));
#160651=CARTESIAN_POINT('Ctrl Pts',(-189.976715689538,4.31540087856674,
134.855297505843));
#160652=CARTESIAN_POINT('Ctrl Pts',(-189.98411237445,4.42017901826155,134.73754609616));
#160653=CARTESIAN_POINT('Ctrl Pts',(-189.991508731385,4.52495251198384,
134.619799907697));
#160654=CARTESIAN_POINT('Ctrl Pts',(-189.998905088321,4.62502442492598,
134.497857031564));
#160655=CARTESIAN_POINT('Ctrl Pts',(-190.006301445256,4.72005345968584,
134.372136661575));
#160656=CARTESIAN_POINT('Ctrl Pts',(-190.013698934593,4.81509704363352,
134.246397043477));
#160657=CARTESIAN_POINT('Ctrl Pts',(-190.02109642393,4.90509598697833,134.11687907778));
#160658=CARTESIAN_POINT('Ctrl Pts',(-190.028493913266,4.98975106375987,
133.984032752269));
#160659=CARTESIAN_POINT('Ctrl Pts',(-190.035893995781,5.07443581624746,
133.851139857685));
#160660=CARTESIAN_POINT('Ctrl Pts',(-190.043294078296,5.15377277199098,
133.71491659491));
#160661=CARTESIAN_POINT('Ctrl Pts',(-190.050694160811,5.22750765914304,
133.575839326866));
#160662=CARTESIAN_POINT('Ctrl Pts',(-190.058102380478,5.30132362538356,
133.436609129067));
#160663=CARTESIAN_POINT('Ctrl Pts',(-190.065510600145,5.36952504604308,
133.294518988678));
#160664=CARTESIAN_POINT('Ctrl Pts',(-190.072918819811,5.43190468187914,
133.150067779485));
#160665=CARTESIAN_POINT('Ctrl Pts',(-190.080331599113,5.49432271134037,
133.005527662983));
#160666=CARTESIAN_POINT('Ctrl Pts',(-190.087744378416,5.55091168210434,
132.858623929535));
#160667=CARTESIAN_POINT('Ctrl Pts',(-190.095157157718,5.60151379023981,
132.709872050293));
#160668=CARTESIAN_POINT('Ctrl Pts',(-190.102580528747,5.65218820104032,
132.56090762739));
#160669=CARTESIAN_POINT('Ctrl Pts',(-190.110003899775,5.69685855860319,
132.410090141567));
#160670=CARTESIAN_POINT('Ctrl Pts',(-190.117427270804,5.73541765304766,
132.25794752849));
#160671=CARTESIAN_POINT('Ctrl Pts',(-190.121363320244,5.7558626101311,132.17727786444));
#160672=CARTESIAN_POINT('Ctrl Pts',(-190.125299369684,5.77459033229658,
132.096235796439));
#160673=CARTESIAN_POINT('Ctrl Pts',(-190.129235419124,5.79159074918677,
132.014900644345));
#160674=CARTESIAN_POINT('Ctrl Pts',(-190.13665868553,5.82365300488208,131.861505085854));
#160675=CARTESIAN_POINT('Ctrl Pts',(-190.144081951935,5.84966530135562,
131.706602898674));
#160676=CARTESIAN_POINT('Ctrl Pts',(-190.15150521834,5.86948798532478,131.550712647528));
#160677=CARTESIAN_POINT('Ctrl Pts',(-190.158919711061,5.88928724052766,
131.395006645713));
#160678=CARTESIAN_POINT('Ctrl Pts',(-190.166334203782,5.90291139835537,
131.238315271165));
#160679=CARTESIAN_POINT('Ctrl Pts',(-190.173748696503,5.9102713617377,131.081169203277));
#160680=CARTESIAN_POINT('Ctrl Pts',(-190.181156042857,5.91762423131021,
130.924174598686));
#160681=CARTESIAN_POINT('Ctrl Pts',(-190.18856338921,5.91872490889553,130.766726543612));
#160682=CARTESIAN_POINT('Ctrl Pts',(-190.195970735564,5.91353586032059,
130.609362691417));
#160683=CARTESIAN_POINT('Ctrl Pts',(-190.203372557239,5.90835068193385,
130.45211620712));
#160684=CARTESIAN_POINT('Ctrl Pts',(-190.210774378915,5.8968851302798,130.294954172144));
#160685=CARTESIAN_POINT('Ctrl Pts',(-190.21817620059,5.8791537081288,130.138415996223));
#160686=CARTESIAN_POINT('Ctrl Pts',(-190.225574114901,5.86143164625758,
129.981960455587));
#160687=CARTESIAN_POINT('Ctrl Pts',(-190.232972029212,5.83745034325019,
129.826128488115));
#160688=CARTESIAN_POINT('Ctrl Pts',(-190.240369943524,5.80727627526828,
129.671456020874));
#160689=CARTESIAN_POINT('Ctrl Pts',(-190.247766628436,5.77710722166901,
129.51680925739));
#160690=CARTESIAN_POINT('Ctrl Pts',(-190.255163313348,5.74074751701105,
129.36332197774));
#160691=CARTESIAN_POINT('Ctrl Pts',(-190.26255999826,5.69831506500718,129.211521648174));
#160692=CARTESIAN_POINT('Ctrl Pts',(-190.269956355195,5.6558844945027,129.059728049594));
#160693=CARTESIAN_POINT('Ctrl Pts',(-190.277352712131,5.60738181255083,
128.909621611885));
#160694=CARTESIAN_POINT('Ctrl Pts',(-190.284749069066,5.55297521919776,
128.761716062712));
#160695=CARTESIAN_POINT('Ctrl Pts',(-190.292146558402,5.49856029605635,
128.613787868822));
#160696=CARTESIAN_POINT('Ctrl Pts',(-190.299544047739,5.43823979060307,
128.468061584774));
#160697=CARTESIAN_POINT('Ctrl Pts',(-190.306941537075,5.37223055136691,
128.325032187232));
#160698=CARTESIAN_POINT('Ctrl Pts',(-190.31434161959,5.30619817269379,128.181952650957));
#160699=CARTESIAN_POINT('Ctrl Pts',(-190.321741702105,5.23447324617382,
128.041572222184));
#160700=CARTESIAN_POINT('Ctrl Pts',(-190.32914178462,5.15731910927882,127.904362312813));
#160701=CARTESIAN_POINT('Ctrl Pts',(-190.336550004286,5.08008013347921,
127.767001527043));
#160702=CARTESIAN_POINT('Ctrl Pts',(-190.343958223952,4.99740020795088,
127.632818548654));
#160703=CARTESIAN_POINT('Ctrl Pts',(-190.351366443619,4.90958703146701,
127.502257387358));
#160704=CARTESIAN_POINT('Ctrl Pts',(-190.358779222921,4.82171980743826,
127.371615867845));
#160705=CARTESIAN_POINT('Ctrl Pts',(-190.366192002223,4.72871325692401,
127.244600907808));
#160706=CARTESIAN_POINT('Ctrl Pts',(-190.373604781525,4.63091576352256,
127.121623896911));
#160707=CARTESIAN_POINT('Ctrl Pts',(-190.381028152553,4.53297853247616,
126.998471170694));
#160708=CARTESIAN_POINT('Ctrl Pts',(-190.388451523582,4.43023692968165,
126.879368198737));
#160709=CARTESIAN_POINT('Ctrl Pts',(-190.395874894611,4.32307717280776,
126.764690541873));
#160710=CARTESIAN_POINT('Ctrl Pts',(-190.399810944053,4.26625849842815,
126.703885696528));
#160711=CARTESIAN_POINT('Ctrl Pts',(-190.403746993495,4.20819830263757,
126.644324316123));
#160712=CARTESIAN_POINT('Ctrl Pts',(-190.407683042937,4.14895787620481,
126.586057747456));
#160713=CARTESIAN_POINT('Ctrl Pts',(-190.415106309343,4.03723228082388,
126.476168817428));
#160714=CARTESIAN_POINT('Ctrl Pts',(-190.422529575748,3.92096896531795,
126.370555519829));
#160715=CARTESIAN_POINT('Ctrl Pts',(-190.429952842154,3.80052872686658,
126.269615645822));
#160716=CARTESIAN_POINT('Ctrl Pts',(-190.437367334875,3.68023083877513,
126.168795074362));
#160717=CARTESIAN_POINT('Ctrl Pts',(-190.444781827596,3.55576613772917,
126.072637169181));
#160718=CARTESIAN_POINT('Ctrl Pts',(-190.452196320317,3.42753294018989,
125.981503735342));
#160719=CARTESIAN_POINT('Ctrl Pts',(-190.459603666671,3.29942333863392,
125.890458139337));
#160720=CARTESIAN_POINT('Ctrl Pts',(-190.467011013024,3.16755277385676,
125.804427588461));
#160721=CARTESIAN_POINT('Ctrl Pts',(-190.474418359378,3.03235330072144,
125.72373427605));
#160722=CARTESIAN_POINT('Ctrl Pts',(-190.481820181054,2.89725466445357,
125.643101147756));
#160723=CARTESIAN_POINT('Ctrl Pts',(-190.489222002729,2.75883238263387,
125.567797522283));
#160724=CARTESIAN_POINT('Ctrl Pts',(-190.496623824405,2.61754811504931,
125.498102762175));
#160725=CARTESIAN_POINT('Ctrl Pts',(-190.504021738716,2.47633843033066,
125.428444793389));
#160726=CARTESIAN_POINT('Ctrl Pts',(-190.511419653028,2.33227010265108,
125.364389957968));
#160727=CARTESIAN_POINT('Ctrl Pts',(-190.518817567339,2.18582995461846,
125.306172009307));
#160728=CARTESIAN_POINT('Ctrl Pts',(-190.526214252251,2.03941414228153,
125.247963735412));
#160729=CARTESIAN_POINT('Ctrl Pts',(-190.533610937163,1.89062763842013,
125.195590560915));
#160730=CARTESIAN_POINT('Ctrl Pts',(-190.541007622076,1.73997794516578,
125.149238398477));
#160731=CARTESIAN_POINT('Ctrl Pts',(-190.548403979011,1.58933493187669,
125.102888291342));
#160732=CARTESIAN_POINT('Ctrl Pts',(-190.555800335947,1.43682925025374,
125.0625587752));
#160733=CARTESIAN_POINT('Ctrl Pts',(-190.563196692882,1.28298403016603,
125.028386020943));
#160734=CARTESIAN_POINT('Ctrl Pts',(-190.570594182219,1.12911525598238,
124.994208034749));
#160735=CARTESIAN_POINT('Ctrl Pts',(-190.577991671555,0.97390689941849,
124.966188768263));
#160736=CARTESIAN_POINT('Ctrl Pts',(-190.585389160892,0.817892610288261,
124.944413327655));
#160737=CARTESIAN_POINT('Ctrl Pts',(-190.592789243407,0.661823630589273,
124.9226302537));
#160738=CARTESIAN_POINT('Ctrl Pts',(-190.600189325922,0.50494852531532,
124.907095415004));
#160739=CARTESIAN_POINT('Ctrl Pts',(-190.607589408437,0.347806246985612,
124.897842067942));
#160740=CARTESIAN_POINT('Ctrl Pts',(-190.614997628104,0.190491174567385,
124.888578545873));
#160741=CARTESIAN_POINT('Ctrl Pts',(-190.62240584777,0.0329087152680474,
124.885610331419));
#160742=CARTESIAN_POINT('Ctrl Pts',(-190.629814067437,-0.124401254264218,
124.888918546982));
#160743=CARTESIAN_POINT('Ctrl Pts',(-190.637226846739,-0.281808045457423,
124.892228798696));
#160744=CARTESIAN_POINT('Ctrl Pts',(-190.644639626041,-0.438941640954478,
124.901823155316));
#160745=CARTESIAN_POINT('Ctrl Pts',(-190.652052405343,-0.59526761713485,
124.917630878017));
#160746=CARTESIAN_POINT('Ctrl Pts',(-190.659475776372,-0.75181695920117,
124.933461187533));
#160747=CARTESIAN_POINT('Ctrl Pts',(-190.666899147401,-0.907556008596329,
124.955522542167));
#160748=CARTESIAN_POINT('Ctrl Pts',(-190.67432251843,-1.06196003527188,
124.983693005858));
#160749=CARTESIAN_POINT('Ctrl Pts',(-190.67825856787,-1.14382875507758,
124.998629661646));
#160750=CARTESIAN_POINT('Ctrl Pts',(-190.68219461731,-1.22532238526077,
125.015282967731));
#160751=CARTESIAN_POINT('Ctrl Pts',(-190.68613066675,-1.3063645971489,125.033629112651));
#160752=CARTESIAN_POINT('Ctrl Pts',(-190.693553933156,-1.45920767955153,
125.068229369412));
#160753=CARTESIAN_POINT('Ctrl Pts',(-190.700977199561,-1.61090629986719,
125.108958422396));
#160754=CARTESIAN_POINT('Ctrl Pts',(-190.708400465967,-1.76093076543627,
125.155727738555));
#160755=CARTESIAN_POINT('Ctrl Pts',(-190.715814958688,-1.91077791454581,
125.202441777267));
#160756=CARTESIAN_POINT('Ctrl Pts',(-190.723229451409,-2.05895449464387,
125.255181758744));
#160757=CARTESIAN_POINT('Ctrl Pts',(-190.73064394413,-2.20494080910687,
125.313808132539));
#160758=CARTESIAN_POINT('Ctrl Pts',(-190.738051290484,-2.35078641646454,
125.372378000029));
#160759=CARTESIAN_POINT('Ctrl Pts',(-190.745458636838,-2.49444561681005,
125.436822826783));
#160760=CARTESIAN_POINT('Ctrl Pts',(-190.752865983192,-2.63541380355637,
125.506953266179));
#160761=CARTESIAN_POINT('Ctrl Pts',(-190.760267804868,-2.7762768509102,
125.577031399648));
#160762=CARTESIAN_POINT('Ctrl Pts',(-190.767669626543,-2.91445254820704,
125.652786536705));
#160763=CARTESIAN_POINT('Ctrl Pts',(-190.775071448219,-3.04945632143417,
125.733981272175));
#160764=CARTESIAN_POINT('Ctrl Pts',(-190.78246936253,-3.18438882722145,
125.815133145578));
#160765=CARTESIAN_POINT('Ctrl Pts',(-190.789867276842,-3.31615242456538,
125.901718706713));
#160766=CARTESIAN_POINT('Ctrl Pts',(-190.797265191153,-3.44428731060594,
125.993454727352));
#160767=CARTESIAN_POINT('Ctrl Pts',(-190.804661876065,-3.5724009029514,
126.085175503127));
#160768=CARTESIAN_POINT('Ctrl Pts',(-190.812058560978,-3.69688667759057,
126.182044822578));
#160769=CARTESIAN_POINT('Ctrl Pts',(-190.81945524589,-3.81731390363919,
126.283736200123));
#160770=CARTESIAN_POINT('Ctrl Pts',(-190.826851602826,-3.9377357898191,
126.385423068566));
#160771=CARTESIAN_POINT('Ctrl Pts',(-190.834247959761,-4.05409920001659,
126.491931329125));
#160772=CARTESIAN_POINT('Ctrl Pts',(-190.841644316697,-4.16600680533306,
126.602894461518));
#160773=CARTESIAN_POINT('Ctrl Pts',(-190.849041806034,-4.27793154398928,
126.713874582649));
#160774=CARTESIAN_POINT('Ctrl Pts',(-190.85643929537,-4.38539885432859,
126.829310670813));
#160775=CARTESIAN_POINT('Ctrl Pts',(-190.863836784707,-4.48804868336094,
126.948799753271));
#160776=CARTESIAN_POINT('Ctrl Pts',(-190.871236867222,-4.59073449613216,
127.068330722442));
#160777=CARTESIAN_POINT('Ctrl Pts',(-190.878636949737,-4.68859922218421,
127.19191723167));
#160778=CARTESIAN_POINT('Ctrl Pts',(-190.886037032252,-4.78132356498639,
127.319123820818));
#160779=CARTESIAN_POINT('Ctrl Pts',(-190.893445251919,-4.87414986773537,
127.446470286688));
#160780=CARTESIAN_POINT('Ctrl Pts',(-190.900853471586,-4.9618242790364,
127.57744448025));
#160781=CARTESIAN_POINT('Ctrl Pts',(-190.908261691252,-5.04407086463152,
127.711581984189));
#160782=CARTESIAN_POINT('Ctrl Pts',(-190.915674470554,-5.12636807162771,
127.845802047523));
#160783=CARTESIAN_POINT('Ctrl Pts',(-190.923087249857,-5.20323061424422,
127.98318897578));
#160784=CARTESIAN_POINT('Ctrl Pts',(-190.930500029159,-5.27442913803752,
128.123254907169));
#160785=CARTESIAN_POINT('Ctrl Pts',(-190.937923400188,-5.3457293936204,
128.26352097133));
#160786=CARTESIAN_POINT('Ctrl Pts',(-190.945346771217,-5.41134931149239,
128.406473345405));
#160787=CARTESIAN_POINT('Ctrl Pts',(-190.952770142245,-5.47110785050535,
128.551604649726));
#160788=CARTESIAN_POINT('Ctrl Pts',(-190.956706191685,-5.50279326176559,
128.628556749628));
#160789=CARTESIAN_POINT('Ctrl Pts',(-190.960642241124,-5.53283166141068,
128.706121167425));
#160790=CARTESIAN_POINT('Ctrl Pts',(-190.964578290564,-5.56120182518544,
128.784220814965));
#160791=CARTESIAN_POINT('Ctrl Pts',(-190.973177240122,-5.62318112981626,
128.954842383627));
#160792=CARTESIAN_POINT('Ctrl Pts',(-190.98177618968,-5.67735007641122,
129.128443962409));
#160793=CARTESIAN_POINT('Ctrl Pts',(-190.990375139238,-5.72345280997876,
129.304354452763));
#160794=CARTESIAN_POINT('Ctrl Pts',(-190.998941388787,-5.76938022448008,
129.479595992265));
#160795=CARTESIAN_POINT('Ctrl Pts',(-191.007507638336,-5.80730256775135,
129.657128801406));
#160796=CARTESIAN_POINT('Ctrl Pts',(-191.016073887885,-5.83701346337239,
129.836267444927));
#160797=CARTESIAN_POINT('Ctrl Pts',(-191.024576231815,-5.8665027108652,
130.014069684944));
#160798=CARTESIAN_POINT('Ctrl Pts',(-191.033078575745,-5.88790249831863,
130.19345375926));
#160799=CARTESIAN_POINT('Ctrl Pts',(-191.041580919675,-5.90105816818685,
130.373729617549));
#160800=CARTESIAN_POINT('Ctrl Pts',(-191.048262204323,-5.91139611450565,
130.515393414546));
#160801=CARTESIAN_POINT('Ctrl Pts',(-191.054943488972,-5.9166441504911,
130.657607486087));
#160802=CARTESIAN_POINT('Ctrl Pts',(-191.06162477362,-5.91674841448608,
130.80002908476));
#160803=CARTESIAN_POINT('',(-192.811624807792,-5.9097125884178,130.808293688258));
#160804=CARTESIAN_POINT('Ctrl Pts',(-191.061624807792,-5.91047567621124,
130.800034404554));
#160805=CARTESIAN_POINT('Ctrl Pts',(-191.12209184332,-5.90179870917759,
132.087620467717));
#160806=CARTESIAN_POINT('Ctrl Pts',(-191.275374753451,-4.85401633074215,
135.36448301843));
#160807=CARTESIAN_POINT('Ctrl Pts',(-191.52147353819,0.560953822592365,
137.780239869629));
#160808=CARTESIAN_POINT('Ctrl Pts',(-191.799921162001,6.17221402509524,
134.103047410633));
#160809=CARTESIAN_POINT('Ctrl Pts',(-192.078368785815,6.11151106794695,
127.394522938632));
#160810=CARTESIAN_POINT('Ctrl Pts',(-192.356816409627,0.434628003272854,
123.819472713731));
#160811=CARTESIAN_POINT('Ctrl Pts',(-192.601235083619,-4.89907710821755,
126.315663527414));
#160812=CARTESIAN_POINT('Ctrl Pts',(-192.752837883008,-5.902105290066,129.556078088356));
#160813=CARTESIAN_POINT('Ctrl Pts',(-192.811624807792,-5.9097125884178,
130.808293688258));
#160814=CARTESIAN_POINT('',(-194.561624807792,-5.92485436802142,130.807214191615));
#160815=CARTESIAN_POINT('Ctrl Pts',(-192.811624807792,-5.9097125884178,
130.808293688258));
#160816=CARTESIAN_POINT('Ctrl Pts',(-192.845653757612,-5.91411609097954,
131.533141636508));
#160817=CARTESIAN_POINT('Ctrl Pts',(-192.972498582038,-5.45424420182938,
134.22966001815));
#160818=CARTESIAN_POINT('Ctrl Pts',(-193.192159281066,-1.42141332660588,
137.656888960118));
#160819=CARTESIAN_POINT('Ctrl Pts',(-193.47060690488,4.99691754528912,135.704194857198));
#160820=CARTESIAN_POINT('Ctrl Pts',(-193.749054528692,6.82332530604844,
129.248792458293));
#160821=CARTESIAN_POINT('Ctrl Pts',(-194.027502152505,2.37943044852847,
124.222881204015));
#160822=CARTESIAN_POINT('Ctrl Pts',(-194.298358912204,-4.07028890202498,
125.217162883923));
#160823=CARTESIAN_POINT('Ctrl Pts',(-194.476399797301,-5.91415325007818,
129.003717447568));
#160824=CARTESIAN_POINT('Ctrl Pts',(-194.561624807792,-5.92485436802142,
130.807214191615));
#160825=CARTESIAN_POINT('',(-196.311624807792,-5.91811478187531,130.799043979201));
#160826=CARTESIAN_POINT('Ctrl Pts',(-194.561624807792,-5.92485436802142,
130.807214191615));
#160827=CARTESIAN_POINT('Ctrl Pts',(-194.569215671905,-5.92580750057834,
130.96784894699));
#160828=CARTESIAN_POINT('Ctrl Pts',(-194.576806536018,-5.91984348713247,
131.128411830021));
#160829=CARTESIAN_POINT('Ctrl Pts',(-194.677213274735,-5.74644163664981,
133.244482439234));
#160830=CARTESIAN_POINT('Ctrl Pts',(-194.862845023943,-3.28928991419861,
136.981587535098));
#160831=CARTESIAN_POINT('Ctrl Pts',(-195.141292647756,3.41913440987934,
136.910675415994));
#160832=CARTESIAN_POINT('Ctrl Pts',(-195.419740271569,6.98554124528268,
131.228358307197));
#160833=CARTESIAN_POINT('Ctrl Pts',(-195.698187895382,4.13257693892937,
125.156408035065));
#160834=CARTESIAN_POINT('Ctrl Pts',(-195.976635519195,-2.5180236866903,
124.27465026843));
#160835=CARTESIAN_POINT('Ctrl Pts',(-196.181114489998,-5.70266478639503,
128.033605093401));
#160836=CARTESIAN_POINT('Ctrl Pts',(-196.292777586197,-5.92224318811939,
130.39909676226));
#160837=CARTESIAN_POINT('Ctrl Pts',(-196.311624807792,-5.91853255389597,
130.799043603888));
#160838=CARTESIAN_POINT('',(-198.061624807755,-5.91674998668501,130.803963675558));
#160839=CARTESIAN_POINT('Ctrl Pts',(-196.311624807792,-5.91674761240624,
130.79904520742));
#160840=CARTESIAN_POINT('Ctrl Pts',(-196.318927817343,-5.91688679200283,
130.953970325757));
#160841=CARTESIAN_POINT('Ctrl Pts',(-196.326230826894,-5.91093694148842,
131.109091464218));
#160842=CARTESIAN_POINT('Ctrl Pts',(-196.333533836445,-5.89887867729289,
131.263883101324));
#160843=CARTESIAN_POINT('Ctrl Pts',(-196.340831042499,-5.88682999546239,
131.41855172985));
#160844=CARTESIAN_POINT('Ctrl Pts',(-196.348128248553,-5.86868258965433,
131.572890996276));
#160845=CARTESIAN_POINT('Ctrl Pts',(-196.355425454607,-5.84446913863302,
131.726375286683));
#160846=CARTESIAN_POINT('Ctrl Pts',(-196.362846509282,-5.81984473545903,
131.882464521733));
#160847=CARTESIAN_POINT('Ctrl Pts',(-196.370267563958,-5.78894650617216,
132.037669091922));
#160848=CARTESIAN_POINT('Ctrl Pts',(-196.377688618634,-5.75186394852528,
132.191440889272));
#160849=CARTESIAN_POINT('Ctrl Pts',(-196.3849802672,-5.71542802531407,132.342531260482));
#160850=CARTESIAN_POINT('Ctrl Pts',(-196.392271915766,-5.67302179942338,
132.492238033825));
#160851=CARTESIAN_POINT('Ctrl Pts',(-196.399563564333,-5.62478171151197,
132.640051566593));
#160852=CARTESIAN_POINT('Ctrl Pts',(-196.40685488677,-5.57654378120929,
132.787858488184));
#160853=CARTESIAN_POINT('Ctrl Pts',(-196.414146209206,-5.52247262718137,
132.933771971568));
#160854=CARTESIAN_POINT('Ctrl Pts',(-196.421437531643,-5.46275434354564,
133.077298263999));
#160855=CARTESIAN_POINT('Ctrl Pts',(-196.428730063846,-5.40302615153141,
133.220848370123));
#160856=CARTESIAN_POINT('Ctrl Pts',(-196.43602259605,-5.3376491138028,133.362010141883));
#160857=CARTESIAN_POINT('Ctrl Pts',(-196.443315128253,-5.26685704862626,
133.500310801052));
#160858=CARTESIAN_POINT('Ctrl Pts',(-196.450833098134,-5.19387655310716,
133.642886817326));
#160859=CARTESIAN_POINT('Ctrl Pts',(-196.458351068014,-5.11514103364721,
133.782421580859));
#160860=CARTESIAN_POINT('Ctrl Pts',(-196.465869037895,-5.03095663489101,
133.918426432597));
#160861=CARTESIAN_POINT('Ctrl Pts',(-196.473172341532,-4.9491760165358,
134.050547835598));
#160862=CARTESIAN_POINT('Ctrl Pts',(-196.480475645169,-4.86225370657967,
134.179337872425));
#160863=CARTESIAN_POINT('Ctrl Pts',(-196.487778948806,-4.77051280347123,
134.304380353856));
#160864=CARTESIAN_POINT('Ctrl Pts',(-196.495404251808,-4.67472708529593,
134.434935901931));
#160865=CARTESIAN_POINT('Ctrl Pts',(-196.503029554811,-4.57368851682401,
134.561405546719));
#160866=CARTESIAN_POINT('Ctrl Pts',(-196.510654857813,-4.467808907599,134.683357153744));
#160867=CARTESIAN_POINT('Ctrl Pts',(-196.518280160816,-4.361929298374,134.805308760768));
#160868=CARTESIAN_POINT('Ctrl Pts',(-196.525905463818,-4.25120902523955,
134.922742040811));
#160869=CARTESIAN_POINT('Ctrl Pts',(-196.53353076682,-4.13609959561202,
135.035271949381));
#160870=CARTESIAN_POINT('Ctrl Pts',(-196.540954033226,-4.024040053635,135.144820316129));
#160871=CARTESIAN_POINT('Ctrl Pts',(-196.548377299631,-3.90745582610583,
135.250079258993));
#160872=CARTESIAN_POINT('Ctrl Pts',(-196.555800566037,-3.78670891927233,
135.350652086797));
#160873=CARTESIAN_POINT('Ctrl Pts',(-196.563215058758,-3.66610472525497,
135.451106045871));
#160874=CARTESIAN_POINT('Ctrl Pts',(-196.570629551479,-3.5413479291358,
135.546884677918));
#160875=CARTESIAN_POINT('Ctrl Pts',(-196.578044044199,-3.41283794674118,
135.63762739189));
#160876=CARTESIAN_POINT('Ctrl Pts',(-196.585451390553,-3.28445182710626,
135.728282644617));
#160877=CARTESIAN_POINT('Ctrl Pts',(-196.592858736907,-3.15232002574301,
135.813911428368));
#160878=CARTESIAN_POINT('Ctrl Pts',(-196.60026608326,-3.0168755761589,135.894192866322));
#160879=CARTESIAN_POINT('Ctrl Pts',(-196.607667904936,-2.88153214615492,
135.974414427351));
#160880=CARTESIAN_POINT('Ctrl Pts',(-196.615069726611,-2.74288130716737,
136.049296394212));
#160881=CARTESIAN_POINT('Ctrl Pts',(-196.622471548287,-2.60138556712834,
136.118560810788));
#160882=CARTESIAN_POINT('Ctrl Pts',(-196.629869462598,-2.45996452158867,
136.187788663217));
#160883=CARTESIAN_POINT('Ctrl Pts',(-196.637267376909,-2.31570190033966,
136.251404707507));
#160884=CARTESIAN_POINT('Ctrl Pts',(-196.644665291221,-2.1690852351992,
136.309176673071));
#160885=CARTESIAN_POINT('Ctrl Pts',(-196.652061976133,-2.02249293508921,
136.366939037981));
#160886=CARTESIAN_POINT('Ctrl Pts',(-196.659458661045,-1.87354771447102,
136.418859114951));
#160887=CARTESIAN_POINT('Ctrl Pts',(-196.666855345957,-1.72275763897961,
136.464752536845));
#160888=CARTESIAN_POINT('Ctrl Pts',(-196.674251702893,-1.57197424967773,
136.510643923776));
#160889=CARTESIAN_POINT('Ctrl Pts',(-196.681648059828,-1.41934652527773,
136.550509078279));
#160890=CARTESIAN_POINT('Ctrl Pts',(-196.689044416763,-1.26539800768293,
136.584213422323));
#160891=CARTESIAN_POINT('Ctrl Pts',(-196.6964419061,-1.11142592017751,136.617922926587));
#160892=CARTESIAN_POINT('Ctrl Pts',(-196.703839395436,-0.956133001520995,
136.645469662442));
#160893=CARTESIAN_POINT('Ctrl Pts',(-196.711236884773,-0.800053158089319,
136.666770148359));
#160894=CARTESIAN_POINT('Ctrl Pts',(-196.718636967288,-0.643918601110704,
136.688078101128));
#160895=CARTESIAN_POINT('Ctrl Pts',(-196.726037049803,-0.486996939769862,
136.703135394011));
#160896=CARTESIAN_POINT('Ctrl Pts',(-196.733437132318,-0.329827225310558,
136.711910411173));
#160897=CARTESIAN_POINT('Ctrl Pts',(-196.740845351984,-0.172484686592092,
136.720695077368));
#160898=CARTESIAN_POINT('Ctrl Pts',(-196.748253571651,-0.0148939229818671,
136.723183651275));
#160899=CARTESIAN_POINT('Ctrl Pts',(-196.755661791317,0.142405248829505,
136.719396653602));
#160900=CARTESIAN_POINT('Ctrl Pts',(-196.763074570619,0.299801235656451,
136.715607325096));
#160901=CARTESIAN_POINT('Ctrl Pts',(-196.770487349921,0.456904901399012,
136.705534752304));
#160902=CARTESIAN_POINT('Ctrl Pts',(-196.777900129223,0.613182040216748,
136.689251300328));
#160903=CARTESIAN_POINT('Ctrl Pts',(-196.785323500252,0.769682475138877,
136.672944581791));
#160904=CARTESIAN_POINT('Ctrl Pts',(-196.792746871281,0.925353655985176,
136.650409313252));
#160905=CARTESIAN_POINT('Ctrl Pts',(-196.80017024231,1.07967122626914,136.621769027302));
#160906=CARTESIAN_POINT('Ctrl Pts',(-196.804106291751,1.16149410484353,
136.606583260475));
#160907=CARTESIAN_POINT('Ctrl Pts',(-196.808042341192,1.24293667063961,
136.589681992946));
#160908=CARTESIAN_POINT('Ctrl Pts',(-196.811978390633,1.32392266781222,
136.571089268383));
#160909=CARTESIAN_POINT('Ctrl Pts',(-196.819401657039,1.47665973097384,
136.536023970121));
#160910=CARTESIAN_POINT('Ctrl Pts',(-196.826824923444,1.62823368340216,
136.494833387375));
#160911=CARTESIAN_POINT('Ctrl Pts',(-196.83424818985,1.7781151043552,136.447607664982));
#160912=CARTESIAN_POINT('Ctrl Pts',(-196.841662682571,1.92781937791556,
136.40043775947));
#160913=CARTESIAN_POINT('Ctrl Pts',(-196.849077175292,2.07583474930553,
136.347247023744));
#160914=CARTESIAN_POINT('Ctrl Pts',(-196.856491668013,2.22164194905233,
136.288176589379));
#160915=CARTESIAN_POINT('Ctrl Pts',(-196.863899014366,2.36730861433047,
136.229163089323));
#160916=CARTESIAN_POINT('Ctrl Pts',(-196.87130636072,2.51077100136879,136.164281311885));
#160917=CARTESIAN_POINT('Ctrl Pts',(-196.878713707074,2.65152508222352,
136.093722138661));
#160918=CARTESIAN_POINT('Ctrl Pts',(-196.886115528749,2.79217418337481,
136.02321559113));
#160919=CARTESIAN_POINT('Ctrl Pts',(-196.893517350425,2.93011866807073,
135.947040245676));
#160920=CARTESIAN_POINT('Ctrl Pts',(-196.9009191721,3.06487468712279,135.865434981249));
#160921=CARTESIAN_POINT('Ctrl Pts',(-196.908317086411,3.19955956952096,
135.783872795607));
#160922=CARTESIAN_POINT('Ctrl Pts',(-196.915715000723,3.33105901987783,
135.696886592468));
#160923=CARTESIAN_POINT('Ctrl Pts',(-196.923112915034,3.45891409951243,
135.604760998232));
#160924=CARTESIAN_POINT('Ctrl Pts',(-196.930509599946,3.5867479319525,135.512650713597));
#160925=CARTESIAN_POINT('Ctrl Pts',(-196.937906284858,3.7109382930943,135.415402950964));
#160926=CARTESIAN_POINT('Ctrl Pts',(-196.94530296977,3.83105544775849,135.313345505398));
#160927=CARTESIAN_POINT('Ctrl Pts',(-196.952699326706,3.95116727630217,
135.211292585167));
#160928=CARTESIAN_POINT('Ctrl Pts',(-196.960095683641,4.0672059730031,135.104430647757));
#160929=CARTESIAN_POINT('Ctrl Pts',(-196.967492040577,4.17877532636475,
134.993127421085));
#160930=CARTESIAN_POINT('Ctrl Pts',(-196.974889529913,4.29036176127955,
134.881807153605));
#160931=CARTESIAN_POINT('Ctrl Pts',(-196.98228701925,4.39747722609323,134.766044506611));
#160932=CARTESIAN_POINT('Ctrl Pts',(-196.989684508586,4.49976289599391,
134.646243546852));
#160933=CARTESIAN_POINT('Ctrl Pts',(-196.997084591101,4.60208442197746,
134.526400591052));
#160934=CARTESIAN_POINT('Ctrl Pts',(-197.004484673616,4.69957253990412,
134.40251678771));
#160935=CARTESIAN_POINT('Ctrl Pts',(-197.011884756131,4.79190928011303,
134.275028566775));
#160936=CARTESIAN_POINT('Ctrl Pts',(-197.019292975798,4.88434755406011,
134.147400159435));
#160937=CARTESIAN_POINT('Ctrl Pts',(-197.026701195464,4.97162291886746,
134.01615972179));
#160938=CARTESIAN_POINT('Ctrl Pts',(-197.034109415131,5.05346085508178,
133.881772508856));
#160939=CARTESIAN_POINT('Ctrl Pts',(-197.041522194433,5.13534916118031,
133.747302582836));
#160940=CARTESIAN_POINT('Ctrl Pts',(-197.048934973735,5.2117931892249,133.609682347809));
#160941=CARTESIAN_POINT('Ctrl Pts',(-197.056347753037,5.28256507071789,
133.469400361384));
#160942=CARTESIAN_POINT('Ctrl Pts',(-197.063771124065,5.35343807439412,
133.328917933479));
#160943=CARTESIAN_POINT('Ctrl Pts',(-197.071194495094,5.41862259046731,
133.185766497095));
#160944=CARTESIAN_POINT('Ctrl Pts',(-197.078617866123,5.47793912291705,
133.04045398058));
#160945=CARTESIAN_POINT('Ctrl Pts',(-197.082553915564,5.50939017170535,
132.963405797591));
#160946=CARTESIAN_POINT('Ctrl Pts',(-197.086489965005,5.53919235282093,
132.88575031248));
#160947=CARTESIAN_POINT('Ctrl Pts',(-197.090426014446,5.56732467673674,
132.80756467764));
#160948=CARTESIAN_POINT('Ctrl Pts',(-197.097849280852,5.62038136165785,
132.660109010435));
#160949=CARTESIAN_POINT('Ctrl Pts',(-197.105272547257,5.66765598150285,
132.510321035348));
#160950=CARTESIAN_POINT('Ctrl Pts',(-197.112695813663,5.70893821283385,
132.35869489453));
#160951=CARTESIAN_POINT('Ctrl Pts',(-197.120110306384,5.75017165199582,
132.207247963219));
#160952=CARTESIAN_POINT('Ctrl Pts',(-197.127524799105,5.7854267033022,132.053967547337));
#160953=CARTESIAN_POINT('Ctrl Pts',(-197.134939291826,5.81454142691153,
131.899366808064));
#160954=CARTESIAN_POINT('Ctrl Pts',(-197.14234663818,5.84362808865393,131.744915078805));
#160955=CARTESIAN_POINT('Ctrl Pts',(-197.149753984533,5.86658613620568,
131.589145923993));
#160956=CARTESIAN_POINT('Ctrl Pts',(-197.157161330887,5.88330372424391,
131.432586572775));
#160957=CARTESIAN_POINT('Ctrl Pts',(-197.164563152563,5.90000884367436,
131.276143989427));
#160958=CARTESIAN_POINT('Ctrl Pts',(-197.171964974238,5.91048273160501,
131.118912752756));
#160959=CARTESIAN_POINT('Ctrl Pts',(-197.179366795914,5.91466483135784,
130.961429058695));
#160960=CARTESIAN_POINT('Ctrl Pts',(-197.186764710225,5.91884472341276,
130.804028499051));
#160961=CARTESIAN_POINT('Ctrl Pts',(-197.194162624536,5.91673943210462,
130.646376119654));
#160962=CARTESIAN_POINT('Ctrl Pts',(-197.201560538848,5.90834035411677,
130.489011886135));
#160963=CARTESIAN_POINT('Ctrl Pts',(-197.20895722376,5.8999426719033,130.331673803696));
#160964=CARTESIAN_POINT('Ctrl Pts',(-197.216353908672,5.8852532987146,130.1746241445));
#160965=CARTESIAN_POINT('Ctrl Pts',(-197.223750593585,5.86431573546309,
130.018401638166));
#160966=CARTESIAN_POINT('Ctrl Pts',(-197.23114695052,5.84337910060514,129.862186058901));
#160967=CARTESIAN_POINT('Ctrl Pts',(-197.238543307455,5.81619487614345,
129.706797929561));
#160968=CARTESIAN_POINT('Ctrl Pts',(-197.245939664391,5.7828582799976,129.552769360021));
#160969=CARTESIAN_POINT('Ctrl Pts',(-197.253337153727,5.74951657993387,
129.398717208314));
#160970=CARTESIAN_POINT('Ctrl Pts',(-197.260734643064,5.71002071162072,
129.246025395738));
#160971=CARTESIAN_POINT('Ctrl Pts',(-197.268132132401,5.66451667428286,
129.09521421972));
#160972=CARTESIAN_POINT('Ctrl Pts',(-197.275532214916,5.61899668557493,
128.944350177076));
#160973=CARTESIAN_POINT('Ctrl Pts',(-197.282932297431,5.56746444227009,
128.79536844072));
#160974=CARTESIAN_POINT('Ctrl Pts',(-197.290332379946,5.51011525487502,
128.648772428581));
#160975=CARTESIAN_POINT('Ctrl Pts',(-197.297740599612,5.45270300615285,
128.502015219055));
#160976=CARTESIAN_POINT('Ctrl Pts',(-197.305148819279,5.38946117553666,
128.357649320603));
#160977=CARTESIAN_POINT('Ctrl Pts',(-197.312557038945,5.32063281077705,
128.216157175913));
#160978=CARTESIAN_POINT('Ctrl Pts',(-197.319969818248,5.2517620833074,128.07457794517));
#160979=CARTESIAN_POINT('Ctrl Pts',(-197.32738259755,5.17729814637798,127.935876320775));
#160980=CARTESIAN_POINT('Ctrl Pts',(-197.334795376852,5.09752886885128,
127.80050809227));
#160981=CARTESIAN_POINT('Ctrl Pts',(-197.34221874788,5.01764561323994,127.664946443292));
#160982=CARTESIAN_POINT('Ctrl Pts',(-197.349642118909,4.93244207870739,
127.532728015764));
#160983=CARTESIAN_POINT('Ctrl Pts',(-197.357065489938,4.84224857777326,
127.40427837245));
#160984=CARTESIAN_POINT('Ctrl Pts',(-197.361001539378,4.79442581941926,
127.336171289465));
#160985=CARTESIAN_POINT('Ctrl Pts',(-197.364937588819,4.74520086733818,
127.26912318392));
#160986=CARTESIAN_POINT('Ctrl Pts',(-197.368873638259,4.69462728667099,
127.203193417651));
#160987=CARTESIAN_POINT('Ctrl Pts',(-197.376296904665,4.59924709187124,
127.078851936054));
#160988=CARTESIAN_POINT('Ctrl Pts',(-197.38372017107,4.49877931298799,126.958114400183));
#160989=CARTESIAN_POINT('Ctrl Pts',(-197.391143437476,4.39352600085202,
126.841424857004));
#160990=CARTESIAN_POINT('Ctrl Pts',(-197.398557930197,4.28839708939024,
126.724873231176));
#160991=CARTESIAN_POINT('Ctrl Pts',(-197.405972422918,4.17849415076658,
126.612360349171));
#160992=CARTESIAN_POINT('Ctrl Pts',(-197.413386915639,4.06416138957402,
126.504299831717));
#160993=CARTESIAN_POINT('Ctrl Pts',(-197.420794261992,3.94993882660157,
126.396343467059));
#160994=CARTESIAN_POINT('Ctrl Pts',(-197.428201608346,3.83129521052947,
126.292831178398));
#160995=CARTESIAN_POINT('Ctrl Pts',(-197.4356089547,3.70861365904349,126.194142044607));
#160996=CARTESIAN_POINT('Ctrl Pts',(-197.443010776375,3.58602360808748,
126.095526516895));
#160997=CARTESIAN_POINT('Ctrl Pts',(-197.450412598051,3.45940190792309,
126.001727214337));
#160998=CARTESIAN_POINT('Ctrl Pts',(-197.457814419726,3.32916694301156,
125.91308491198));
#160999=CARTESIAN_POINT('Ctrl Pts',(-197.465212334038,3.19900072812314,
125.824489403203));
#161000=CARTESIAN_POINT('Ctrl Pts',(-197.472610248349,3.06522535501235,
125.741045682467));
#161001=CARTESIAN_POINT('Ctrl Pts',(-197.48000816266,2.92829046175452,125.6630528526));
#161002=CARTESIAN_POINT('Ctrl Pts',(-197.487404847572,2.79137832459229,
125.585072983727));
#161003=CARTESIAN_POINT('Ctrl Pts',(-197.494801532485,2.65130803341802,
125.512542392469));
#161004=CARTESIAN_POINT('Ctrl Pts',(-197.502198217397,2.50855635002252,
125.445715676794));
#161005=CARTESIAN_POINT('Ctrl Pts',(-197.509594574332,2.36581099638625,
125.378891924286));
#161006=CARTESIAN_POINT('Ctrl Pts',(-197.516990931268,2.22038482501944,
125.317771702748));
#161007=CARTESIAN_POINT('Ctrl Pts',(-197.524387288203,2.0727769826413,125.262562521033));
#161008=CARTESIAN_POINT('Ctrl Pts',(-197.53178477754,1.9251465411261,125.207344886652));
#161009=CARTESIAN_POINT('Ctrl Pts',(-197.539182266876,1.77533411318653,
125.158040224843));
#161010=CARTESIAN_POINT('Ctrl Pts',(-197.546579756213,1.62385635592891,
125.11480693579));
#161011=CARTESIAN_POINT('Ctrl Pts',(-197.553979838728,1.47232549837808,
125.071558491375));
#161012=CARTESIAN_POINT('Ctrl Pts',(-197.561379921243,1.31912850795002,
125.034385759555));
#161013=CARTESIAN_POINT('Ctrl Pts',(-197.568780003758,1.16479449450476,
125.003396529755));
#161014=CARTESIAN_POINT('Ctrl Pts',(-197.576188223424,1.01029077494556,
124.972373224112));
#161015=CARTESIAN_POINT('Ctrl Pts',(-197.583596443091,0.854647901707854,
124.947547072864));
#161016=CARTESIAN_POINT('Ctrl Pts',(-197.591004662757,0.698403140736846,
124.928974365113));
#161017=CARTESIAN_POINT('Ctrl Pts',(-197.598417442059,0.542062213722543,
124.910390226172));
#161018=CARTESIAN_POINT('Ctrl Pts',(-197.605830221361,0.38511903209279,
124.898067229277));
#161019=CARTESIAN_POINT('Ctrl Pts',(-197.613243000663,0.228112664648767,
124.892009547583));
#161020=CARTESIAN_POINT('Ctrl Pts',(-197.620666371692,0.0708819591442937,
124.88594321039));
#161021=CARTESIAN_POINT('Ctrl Pts',(-197.628089742721,-0.0864117401809329,
124.886160067387));
#161022=CARTESIAN_POINT('Ctrl Pts',(-197.63551311375,-0.243231853336173,
124.892612244367));
#161023=CARTESIAN_POINT('Ctrl Pts',(-197.639449163191,-0.326381640180508,
124.896033343419));
#161024=CARTESIAN_POINT('Ctrl Pts',(-197.643385212631,-0.409398399272633,
124.901206550941));
#161025=CARTESIAN_POINT('Ctrl Pts',(-197.647321262072,-0.492203234551277,
124.908118887583));
#161026=CARTESIAN_POINT('Ctrl Pts',(-197.654744528478,-0.64837056963286,
124.921155338763));
#161027=CARTESIAN_POINT('Ctrl Pts',(-197.662167794883,-0.804255766574924,
124.940420139216));
#161028=CARTESIAN_POINT('Ctrl Pts',(-197.669591061289,-0.959321970235522,
124.965899183256));
#161029=CARTESIAN_POINT('Ctrl Pts',(-197.67700555401,-1.11420489852084,
124.991348113182));
#161030=CARTESIAN_POINT('Ctrl Pts',(-197.684420046731,-1.26827039553683,
125.022996607056));
#161031=CARTESIAN_POINT('Ctrl Pts',(-197.691834539452,-1.42098441946168,
125.060778647911));
#161032=CARTESIAN_POINT('Ctrl Pts',(-197.699241885806,-1.57355125186026,
125.098524273012));
#161033=CARTESIAN_POINT('Ctrl Pts',(-197.706649232159,-1.72476884444938,
125.142391586927));
#161034=CARTESIAN_POINT('Ctrl Pts',(-197.714056578513,-1.87411118297151,
125.192263163284));
#161035=CARTESIAN_POINT('Ctrl Pts',(-197.721458400189,-2.02334213634406,
125.242097543538));
#161036=CARTESIAN_POINT('Ctrl Pts',(-197.728860221864,-2.17070026796815,
125.297927151792));
#161037=CARTESIAN_POINT('Ctrl Pts',(-197.73626204354,-2.31567272712397,
125.359584186586));
#161038=CARTESIAN_POINT('Ctrl Pts',(-197.743659957851,-2.46056865644708,
125.421208673112));
#161039=CARTESIAN_POINT('Ctrl Pts',(-197.751057872162,-2.60308107876267,
125.488654313942));
#161040=CARTESIAN_POINT('Ctrl Pts',(-197.758455786474,-2.74271531002859,
125.561704488214));
#161041=CARTESIAN_POINT('Ctrl Pts',(-197.765852471386,-2.88232633661789,
125.634742522872));
#161042=CARTESIAN_POINT('Ctrl Pts',(-197.773249156298,-3.01905979100342,
125.713383069601));
#161043=CARTESIAN_POINT('Ctrl Pts',(-197.780645841211,-3.15244377131063,
125.797362631624));
#161044=CARTESIAN_POINT('Ctrl Pts',(-197.788042198146,-3.28582183723238,
125.881338469906));
#161045=CARTESIAN_POINT('Ctrl Pts',(-197.795438555081,-3.41585040848234,
125.970652653875));
#161046=CARTESIAN_POINT('Ctrl Pts',(-197.802834912017,-3.54208510099192,
126.064997400864));
#161047=CARTESIAN_POINT('Ctrl Pts',(-197.810232401353,-3.66833912035446,
126.159356592273));
#161048=CARTESIAN_POINT('Ctrl Pts',(-197.81762989069,-3.79079780538828,
126.258747656766));
#161049=CARTESIAN_POINT('Ctrl Pts',(-197.825027380027,-3.90904862374609,
126.362821535256));
#161050=CARTESIAN_POINT('Ctrl Pts',(-197.832427462542,-4.02734089474615,
126.466931896683));
#161051=CARTESIAN_POINT('Ctrl Pts',(-197.839827545057,-4.14142208218471,
126.575728093952));
#161052=CARTESIAN_POINT('Ctrl Pts',(-197.847227627572,-4.2509155029613,
126.688823234771));
#161053=CARTESIAN_POINT('Ctrl Pts',(-197.854635847238,-4.36052932300976,
126.802042735323));
#161054=CARTESIAN_POINT('Ctrl Pts',(-197.862044066905,-4.46554504194146,
126.919570351452));
#161055=CARTESIAN_POINT('Ctrl Pts',(-197.869452286571,-4.56562489677327,
127.040984491736));
#161056=CARTESIAN_POINT('Ctrl Pts',(-197.876865065873,-4.66576634908582,
127.162473360399));
#161057=CARTESIAN_POINT('Ctrl Pts',(-197.884277845175,-4.76096565859968,
127.287853223139));
#161058=CARTESIAN_POINT('Ctrl Pts',(-197.891690624478,-4.8509279344683,
127.416672801799));
#161059=CARTESIAN_POINT('Ctrl Pts',(-197.899113995506,-4.94101875265536,
127.545676443914));
#161060=CARTESIAN_POINT('Ctrl Pts',(-197.906537366535,-5.02585739131891,
127.678129304451));
#161061=CARTESIAN_POINT('Ctrl Pts',(-197.913960737564,-5.10519409379517,
127.813554066286));
#161062=CARTESIAN_POINT('Ctrl Pts',(-197.917896787004,-5.14726031710364,
127.88535952448));
#161063=CARTESIAN_POINT('Ctrl Pts',(-197.921832836445,-5.18778053718604,
127.958000120082));
#161064=CARTESIAN_POINT('Ctrl Pts',(-197.925768885886,-5.22672302868686,
128.031402459949));
#161065=CARTESIAN_POINT('Ctrl Pts',(-197.933618442971,-5.30438498764153,
128.177786763732));
#161066=CARTESIAN_POINT('Ctrl Pts',(-197.941468000057,-5.37598238513895,
128.327603249052));
#161067=CARTESIAN_POINT('Ctrl Pts',(-197.949317557143,-5.44121712518422,
128.480336788277));
#161068=CARTESIAN_POINT('Ctrl Pts',(-197.957153559567,-5.50633921749837,
128.632806586333));
#161069=CARTESIAN_POINT('Ctrl Pts',(-197.964989561992,-5.56512043354741,
128.788183113502));
#161070=CARTESIAN_POINT('Ctrl Pts',(-197.972825564417,-5.6173084054525,
128.94592664227));
#161071=CARTESIAN_POINT('Ctrl Pts',(-197.98064289557,-5.66937202622657,
129.103294306917));
#161072=CARTESIAN_POINT('Ctrl Pts',(-197.988460226724,-5.71487364188634,
129.263017430468));
#161073=CARTESIAN_POINT('Ctrl Pts',(-197.996277557878,-5.75360906848479,
129.424536987695));
#161074=CARTESIAN_POINT('Ctrl Pts',(-198.004083819218,-5.79228964337747,
129.585827823465));
#161075=CARTESIAN_POINT('Ctrl Pts',(-198.011890080558,-5.82422305311737,
129.748909723495));
#161076=CARTESIAN_POINT('Ctrl Pts',(-198.019696341898,-5.84925431259238,
129.913207123986));
#161077=CARTESIAN_POINT('Ctrl Pts',(-198.027487193755,-5.87423616060821,
130.07718020303));
#161078=CARTESIAN_POINT('Ctrl Pts',(-198.035278045612,-5.89234298762165,
130.242363691703));
#161079=CARTESIAN_POINT('Ctrl Pts',(-198.04306889747,-5.90347053031272,
130.40817094048));
#161080=CARTESIAN_POINT('Ctrl Pts',(-198.049254200898,-5.91230489518304,
130.539808425459));
#161081=CARTESIAN_POINT('Ctrl Pts',(-198.055439504327,-5.91674112270733,
130.671838733572));
#161082=CARTESIAN_POINT('Ctrl Pts',(-198.061624807755,-5.91674998668501,
130.803963675558));
#161083=CARTESIAN_POINT('',(-199.811624807792,-5.91674748832781,130.809812394026));
#161084=CARTESIAN_POINT('Ctrl Pts',(-198.061624807792,-5.91674998668506,
130.803963676344));
#161085=CARTESIAN_POINT('Ctrl Pts',(-198.069335284224,-5.91676103632174,
130.96866800542));
#161086=CARTESIAN_POINT('Ctrl Pts',(-198.077045760657,-5.90989046074581,
131.133254346916));
#161087=CARTESIAN_POINT('Ctrl Pts',(-198.084756237089,-5.89619368993992,
131.297138999004));
#161088=CARTESIAN_POINT('Ctrl Pts',(-198.09247513413,-5.88248196089642,
131.461202629451));
#161089=CARTESIAN_POINT('Ctrl Pts',(-198.10019403117,-5.86192918777857,
131.624562717793));
#161090=CARTESIAN_POINT('Ctrl Pts',(-198.107912928211,-5.83464232566053,
131.786643414988));
#161091=CARTESIAN_POINT('Ctrl Pts',(-198.115938226668,-5.80627231226227,
131.955157901231));
#161092=CARTESIAN_POINT('Ctrl Pts',(-198.123963525126,-5.77062274114287,
132.122288952053));
#161093=CARTESIAN_POINT('Ctrl Pts',(-198.131988823583,-5.72787106095795,
132.287406021976));
#161094=CARTESIAN_POINT('Ctrl Pts',(-198.13973298131,-5.68661704950663,
132.446738742092));
#161095=CARTESIAN_POINT('Ctrl Pts',(-198.147477139037,-5.63875026118319,
132.604195921967));
#161096=CARTESIAN_POINT('Ctrl Pts',(-198.155221296764,-5.58447970808055,
132.759230677835));
#161097=CARTESIAN_POINT('Ctrl Pts',(-198.162974554244,-5.53014538450852,
132.914447606882));
#161098=CARTESIAN_POINT('Ctrl Pts',(-198.170727811723,-5.46939239828204,
133.067236130232));
#161099=CARTESIAN_POINT('Ctrl Pts',(-198.178481069202,-5.40247702272164,
133.217071247017));
#161100=CARTESIAN_POINT('Ctrl Pts',(-198.186248543322,-5.33543894881967,
133.367181106642));
#161101=CARTESIAN_POINT('Ctrl Pts',(-198.194016017441,-5.26221604894185,
133.514326447479));
#161102=CARTESIAN_POINT('Ctrl Pts',(-198.201783491561,-5.18311009938688,
133.658007452781));
#161103=CARTESIAN_POINT('Ctrl Pts',(-198.202594497607,-5.17485060571508,
133.673009261883));
#161104=CARTESIAN_POINT('Ctrl Pts',(-198.203405503652,-5.16652701566992,
133.687973331658));
#161105=CARTESIAN_POINT('Ctrl Pts',(-198.204216509698,-5.15813969907268,
133.702899112627));
#161106=CARTESIAN_POINT('Ctrl Pts',(-198.211639776104,-5.08136926578121,
133.839517142834));
#161107=CARTESIAN_POINT('Ctrl Pts',(-198.219063042509,-4.9990513182663,
133.973289646283));
#161108=CARTESIAN_POINT('Ctrl Pts',(-198.226486308914,-4.91142183868873,
134.103734207348));
#161109=CARTESIAN_POINT('Ctrl Pts',(-198.233900801635,-4.82389592987909,
134.234024593775));
#161110=CARTESIAN_POINT('Ctrl Pts',(-198.241315294356,-4.73107119111244,
134.360994560333));
#161111=CARTESIAN_POINT('Ctrl Pts',(-198.248729787077,-4.63322964933905,
134.484185827951));
#161112=CARTESIAN_POINT('Ctrl Pts',(-198.256137133431,-4.53548241092728,
134.607258359188));
#161113=CARTESIAN_POINT('Ctrl Pts',(-198.263544479785,-4.43272822641348,
134.726559151738));
#161114=CARTESIAN_POINT('Ctrl Pts',(-198.270951826138,-4.32529254368441,
134.841658596914));
#161115=CARTESIAN_POINT('Ctrl Pts',(-198.278353647814,-4.21793699054084,
134.956672196582));
#161116=CARTESIAN_POINT('Ctrl Pts',(-198.285755469489,-4.10590714512817,
135.067490416427));
#161117=CARTESIAN_POINT('Ctrl Pts',(-198.293157291165,-3.98956880068971,
135.173716559471));
#161118=CARTESIAN_POINT('Ctrl Pts',(-198.300555205476,-3.87329187035737,
135.279886626562));
#161119=CARTESIAN_POINT('Ctrl Pts',(-198.307953119787,-3.75271124559411,
135.381469193533));
#161120=CARTESIAN_POINT('Ctrl Pts',(-198.315351034099,-3.62822957043913,
135.478104378909));
#161121=CARTESIAN_POINT('Ctrl Pts',(-198.322747719011,-3.50376858188041,
135.57472350527));
#161122=CARTESIAN_POINT('Ctrl Pts',(-198.330144403923,-3.37540812416725,
135.666396653101));
#161123=CARTESIAN_POINT('Ctrl Pts',(-198.337541088835,-3.24358400599151,
135.752804146452));
#161124=CARTESIAN_POINT('Ctrl Pts',(-198.344937445771,-3.11176573303569,
135.839207808404));
#161125=CARTESIAN_POINT('Ctrl Pts',(-198.352333802706,-2.97648441719638,
135.920346075478));
#161126=CARTESIAN_POINT('Ctrl Pts',(-198.359730159642,-2.83820470770205,
135.995942707804));
#161127=CARTESIAN_POINT('Ctrl Pts',(-198.367127648978,-2.69990382723119,
136.071550914167));
#161128=CARTESIAN_POINT('Ctrl Pts',(-198.374525138315,-2.55860396661923,
136.141615617351));
#161129=CARTESIAN_POINT('Ctrl Pts',(-198.381922627651,-2.41479407700068,
136.205906704399));
#161130=CARTESIAN_POINT('Ctrl Pts',(-198.389322710166,-2.27093377504764,
136.270220328589));
#161131=CARTESIAN_POINT('Ctrl Pts',(-198.396722792681,-2.12456203282009,
136.328756154751));
#161132=CARTESIAN_POINT('Ctrl Pts',(-198.404122875196,-1.97618731005907,
136.381332401434));
#161133=CARTESIAN_POINT('Ctrl Pts',(-198.411531094863,-1.82764943403772,
136.433966461105));
#161134=CARTESIAN_POINT('Ctrl Pts',(-198.418939314529,-1.67710453105635,
136.480627729429));
#161135=CARTESIAN_POINT('Ctrl Pts',(-198.426347534195,-1.52507644250729,
136.521184246734));
#161136=CARTESIAN_POINT('Ctrl Pts',(-198.433760313498,-1.37295478320602,
136.561765725898));
#161137=CARTESIAN_POINT('Ctrl Pts',(-198.441173092799,-1.21934848271258,
136.596234885463));
#161138=CARTESIAN_POINT('Ctrl Pts',(-198.448585872102,-1.06479056249309,
136.624511098484));
#161139=CARTESIAN_POINT('Ctrl Pts',(-198.45600924313,-0.910011802669364,
136.652827713883));
#161140=CARTESIAN_POINT('Ctrl Pts',(-198.463432614159,-0.754279076069821,
136.67493365743));
#161141=CARTESIAN_POINT('Ctrl Pts',(-198.470855985188,-0.598130326265068,
136.690800176017));
#161142=CARTESIAN_POINT('Ctrl Pts',(-198.474792034629,-0.515336512371863,
136.699212984885));
#161143=CARTESIAN_POINT('Ctrl Pts',(-198.47872808407,-0.432425748835829,
136.705872538709));
#161144=CARTESIAN_POINT('Ctrl Pts',(-198.482664133511,-0.349477975144942,
136.710780489823));
#161145=CARTESIAN_POINT('Ctrl Pts',(-198.490087399917,-0.193041062691021,
136.720036732451));
#161146=CARTESIAN_POINT('Ctrl Pts',(-198.497510666322,-0.0359996055459115,
136.72308761753));
#161147=CARTESIAN_POINT('Ctrl Pts',(-198.504933932728,0.1211129722417,136.719870926107));
#161148=CARTESIAN_POINT('Ctrl Pts',(-198.512348425449,0.278039856009755,
136.716658036546));
#161149=CARTESIAN_POINT('Ctrl Pts',(-198.51976291817,0.435037323525875,
136.707192323227));
#161150=CARTESIAN_POINT('Ctrl Pts',(-198.527177410891,0.591567369173254,
136.691463352378));
#161151=CARTESIAN_POINT('Ctrl Pts',(-198.534584757244,0.74794654526894,
136.675749541703));
#161152=CARTESIAN_POINT('Ctrl Pts',(-198.541992103598,0.903858827456171,
136.653784528579));
#161153=CARTESIAN_POINT('Ctrl Pts',(-198.549399449952,1.05876686124651,
136.62560990754));
#161154=CARTESIAN_POINT('Ctrl Pts',(-198.556801271627,1.2135593587809,136.597456300197));
#161155=CARTESIAN_POINT('Ctrl Pts',(-198.564203093303,1.36734873359921,
136.563102373113));
#161156=CARTESIAN_POINT('Ctrl Pts',(-198.571604914978,1.5196035131144,136.522641454096));
#161157=CARTESIAN_POINT('Ctrl Pts',(-198.57900282929,1.67177791851663,136.482201894084));
#161158=CARTESIAN_POINT('Ctrl Pts',(-198.586400743601,1.82241898210764,
136.43566185819));
#161159=CARTESIAN_POINT('Ctrl Pts',(-198.593798657912,1.97100628646992,
136.383165577519));
#161160=CARTESIAN_POINT('Ctrl Pts',(-198.601195342825,2.11956889831808,
136.330678020777));
#161161=CARTESIAN_POINT('Ctrl Pts',(-198.608592027737,2.26607807668035,
136.27223630799));
#161162=CARTESIAN_POINT('Ctrl Pts',(-198.615988712649,2.41002930388112,
136.208034304692));
#161163=CARTESIAN_POINT('Ctrl Pts',(-198.623385069584,2.55397414813362,
136.143835148178));
#161164=CARTESIAN_POINT('Ctrl Pts',(-198.63078142652,2.6953609258196,136.073876361061));
#161165=CARTESIAN_POINT('Ctrl Pts',(-198.638177783455,2.83370607425544,
135.998399551501));
#161166=CARTESIAN_POINT('Ctrl Pts',(-198.645575272792,2.97207240368668,
135.922911186248));
#161167=CARTESIAN_POINT('Ctrl Pts',(-198.652972762128,3.10739584891269,
135.84190329519));
#161168=CARTESIAN_POINT('Ctrl Pts',(-198.660370251465,3.23921851935599,
135.755662865093));
#161169=CARTESIAN_POINT('Ctrl Pts',(-198.66777033398,3.37108740003226,135.669392203545));
#161170=CARTESIAN_POINT('Ctrl Pts',(-198.675170416495,3.49945275040591,
135.577885555203));
#161171=CARTESIAN_POINT('Ctrl Pts',(-198.68257049901,3.62388679768368,135.481472444332));
#161172=CARTESIAN_POINT('Ctrl Pts',(-198.689978718676,3.74845767298839,
135.384953317334));
#161173=CARTESIAN_POINT('Ctrl Pts',(-198.697386938343,3.86908831687014,
135.283517182095));
#161174=CARTESIAN_POINT('Ctrl Pts',(-198.704795158009,3.98538455885265,
135.17753343379));
#161175=CARTESIAN_POINT('Ctrl Pts',(-198.712207937311,4.10175237923126,
135.071484454256));
#161176=CARTESIAN_POINT('Ctrl Pts',(-198.719620716613,4.21378021684949,
134.960882545995));
#161177=CARTESIAN_POINT('Ctrl Pts',(-198.727033495915,4.32111212685275,
134.846132574229));
#161178=CARTESIAN_POINT('Ctrl Pts',(-198.734456866944,4.42859739772255,
134.731218642321));
#161179=CARTESIAN_POINT('Ctrl Pts',(-198.741880237973,4.53137309681198,
134.612145091307));
#161180=CARTESIAN_POINT('Ctrl Pts',(-198.749303609002,4.62912426167716,
134.489348966591));
#161181=CARTESIAN_POINT('Ctrl Pts',(-198.753239658442,4.68095427479721,
134.424239514812));
#161182=CARTESIAN_POINT('Ctrl Pts',(-198.757175707883,4.73137243893255,
134.35808399281));
#161183=CARTESIAN_POINT('Ctrl Pts',(-198.761111757324,4.78033693499349,
134.290950549066));
#161184=CARTESIAN_POINT('Ctrl Pts',(-198.76853502373,4.87268244643274,134.164338969331));
#161185=CARTESIAN_POINT('Ctrl Pts',(-198.775958290135,4.9601339859933,134.033864621697));
#161186=CARTESIAN_POINT('Ctrl Pts',(-198.783381556541,5.04235087838011,
133.899942660058));
#161187=CARTESIAN_POINT('Ctrl Pts',(-198.790796049262,5.12447059722781,
133.766178983056));
#161188=CARTESIAN_POINT('Ctrl Pts',(-198.798210541983,5.20136779059828,
133.628976117973));
#161189=CARTESIAN_POINT('Ctrl Pts',(-198.805625034704,5.27274287508696,
133.488781064463));
#161190=CARTESIAN_POINT('Ctrl Pts',(-198.813032381058,5.34404916558199,
133.348721136224));
#161191=CARTESIAN_POINT('Ctrl Pts',(-198.820439727411,5.40984377485081,
133.205675091435));
#161192=CARTESIAN_POINT('Ctrl Pts',(-198.827847073765,5.46987124432698,
133.060117504508));
#161193=CARTESIAN_POINT('Ctrl Pts',(-198.835248895441,5.52985394305153,
132.914668479921));
#161194=CARTESIAN_POINT('Ctrl Pts',(-198.842650717116,5.58407792484558,
132.766711986614));
#161195=CARTESIAN_POINT('Ctrl Pts',(-198.850052538791,5.63233443512196,
132.616745613487));
#161196=CARTESIAN_POINT('Ctrl Pts',(-198.857450453103,5.68056547116234,
132.46685840644));
#161197=CARTESIAN_POINT('Ctrl Pts',(-198.864848367414,5.7228351953659,132.314963787059));
#161198=CARTESIAN_POINT('Ctrl Pts',(-198.872246281726,5.7589836551197,132.161577557692));
#161199=CARTESIAN_POINT('Ctrl Pts',(-198.879642966638,5.79512610765524,
132.008216818333));
#161200=CARTESIAN_POINT('Ctrl Pts',(-198.88703965155,5.82514922912225,131.853365323941));
#161201=CARTESIAN_POINT('Ctrl Pts',(-198.894436336462,5.84894341995819,
131.697552328582));
#161202=CARTESIAN_POINT('Ctrl Pts',(-198.901832693398,5.87273655573477,
131.541746242135));
#161203=CARTESIAN_POINT('Ctrl Pts',(-198.909229050333,5.89030125370091,
131.384979108511));
#161204=CARTESIAN_POINT('Ctrl Pts',(-198.916625407269,5.90157940820071,
131.227788357802));
#161205=CARTESIAN_POINT('Ctrl Pts',(-198.924022896605,5.9128592894148,131.070573540788));
#161206=CARTESIAN_POINT('Ctrl Pts',(-198.931420385942,5.91785068400867,
130.912935349915));
#161207=CARTESIAN_POINT('Ctrl Pts',(-198.938817875279,5.91654754103343,
130.75541414485));
#161208=CARTESIAN_POINT('Ctrl Pts',(-198.946217957794,5.91524394124343,
130.597837720972));
#161209=CARTESIAN_POINT('Ctrl Pts',(-198.953618040309,5.90764141376477,
130.440378737603));
#161210=CARTESIAN_POINT('Ctrl Pts',(-198.961018122824,5.89378597505109,
130.283575208025));
#161211=CARTESIAN_POINT('Ctrl Pts',(-198.96842634249,5.87991530085824,130.126599256847));
#161212=CARTESIAN_POINT('Ctrl Pts',(-198.975834562157,5.85977801704612,
129.970280570899));
#161213=CARTESIAN_POINT('Ctrl Pts',(-198.983242781823,5.83347184746589,
129.815150444083));
#161214=CARTESIAN_POINT('Ctrl Pts',(-198.990655561125,5.80714948687722,
129.659924837261));
#161215=CARTESIAN_POINT('Ctrl Pts',(-198.998068340427,5.77465075171243,
129.505889611662));
#161216=CARTESIAN_POINT('Ctrl Pts',(-199.005481119729,5.73612386966094,
129.353563073315));
#161217=CARTESIAN_POINT('Ctrl Pts',(-199.012904490758,5.6975419385936,129.201018883665));
#161218=CARTESIAN_POINT('Ctrl Pts',(-199.020327861787,5.65291476358045,
129.050188614405));
#161219=CARTESIAN_POINT('Ctrl Pts',(-199.027751232816,5.60243979840348,
128.901573486076));
#161220=CARTESIAN_POINT('Ctrl Pts',(-199.031687282256,5.57567676073842,
128.82277417907));
#161221=CARTESIAN_POINT('Ctrl Pts',(-199.035623331697,5.54727049570574,
128.744597274093));
#161222=CARTESIAN_POINT('Ctrl Pts',(-199.039559381137,5.51725573431446,
128.667114790649));
#161223=CARTESIAN_POINT('Ctrl Pts',(-199.046982647543,5.46064883105527,
128.520985245009));
#161224=CARTESIAN_POINT('Ctrl Pts',(-199.054405913948,5.39814676042029,
128.376885216112));
#161225=CARTESIAN_POINT('Ctrl Pts',(-199.061829180354,5.32991465982133,
128.235325724552));
#161226=CARTESIAN_POINT('Ctrl Pts',(-199.069243673075,5.26176320389876,
128.093933544556));
#161227=CARTESIAN_POINT('Ctrl Pts',(-199.076658165796,5.18789535905273,
127.955076257988));
#161228=CARTESIAN_POINT('Ctrl Pts',(-199.084072658517,5.10852526660425,
127.819247527084));
#161229=CARTESIAN_POINT('Ctrl Pts',(-199.09148000487,5.02923167403911,127.683549713025));
#161230=CARTESIAN_POINT('Ctrl Pts',(-199.098887351224,4.94444657871635,
127.550874963544));
#161231=CARTESIAN_POINT('Ctrl Pts',(-199.106294697578,4.85443117193422,
127.421694722232));
#161232=CARTESIAN_POINT('Ctrl Pts',(-199.113696519254,4.7644829020383,127.292610828418));
#161233=CARTESIAN_POINT('Ctrl Pts',(-199.121098340929,4.66931230052762,
127.16701655816));
#161234=CARTESIAN_POINT('Ctrl Pts',(-199.128500162604,4.56922516608224,
127.045356501561));
#161235=CARTESIAN_POINT('Ctrl Pts',(-199.135898076916,4.46919086685664,
126.92376066836));
#161236=CARTESIAN_POINT('Ctrl Pts',(-199.143295991227,4.36424544012047,
126.806095200239));
#161237=CARTESIAN_POINT('Ctrl Pts',(-199.150693905538,4.25473638670253,
126.692773473631));
#161238=CARTESIAN_POINT('Ctrl Pts',(-199.158090590451,4.14524553170241,
126.579470579038));
#161239=CARTESIAN_POINT('Ctrl Pts',(-199.165487275363,4.0311928143572,126.470510261472));
#161240=CARTESIAN_POINT('Ctrl Pts',(-199.172883960275,3.91296426986117,
126.3662708049));
#161241=CARTESIAN_POINT('Ctrl Pts',(-199.18028031721,3.79474096774303,126.262035970415));
#161242=CARTESIAN_POINT('Ctrl Pts',(-199.187676674146,3.67234248664227,
126.162521827584));
#161243=CARTESIAN_POINT('Ctrl Pts',(-199.195073031081,3.5461895741899,126.068067756434));
#161244=CARTESIAN_POINT('Ctrl Pts',(-199.202470520418,3.42001734740458,
125.973599224125));
#161245=CARTESIAN_POINT('Ctrl Pts',(-199.209868009754,3.29008984357849,
125.884192529796));
#161246=CARTESIAN_POINT('Ctrl Pts',(-199.217265499091,3.15685841191773,
125.800144841882));
#161247=CARTESIAN_POINT('Ctrl Pts',(-199.224665581606,3.02358027618456,
125.716067691181));
#161248=CARTESIAN_POINT('Ctrl Pts',(-199.232065664121,2.8869962222029,125.637353486203));
#161249=CARTESIAN_POINT('Ctrl Pts',(-199.239465746636,2.74758376880045,
125.564254321323));
#161250=CARTESIAN_POINT('Ctrl Pts',(-199.246873966302,2.60801801707374,
125.491074776397));
#161251=CARTESIAN_POINT('Ctrl Pts',(-199.254282185969,2.4656179856307,125.423522775534));
#161252=CARTESIAN_POINT('Ctrl Pts',(-199.261690405635,2.32088348920477,
125.361803278223));
#161253=CARTESIAN_POINT('Ctrl Pts',(-199.269103184937,2.1760599111109,125.300045793591));
#161254=CARTESIAN_POINT('Ctrl Pts',(-199.276515964239,2.028899353128,125.24412809794));
#161255=CARTESIAN_POINT('Ctrl Pts',(-199.283928743541,1.87991800148424,
125.194205640188));
#161256=CARTESIAN_POINT('Ctrl Pts',(-199.29135211457,1.73072377829936,125.144211850888));
#161257=CARTESIAN_POINT('Ctrl Pts',(-199.298775485599,1.57970392286291,
125.100230512364));
#161258=CARTESIAN_POINT('Ctrl Pts',(-199.306198856628,1.42738685480326,
125.062366423104));
#161259=CARTESIAN_POINT('Ctrl Pts',(-199.310134906068,1.34662469051819,
125.042289974441));
#161260=CARTESIAN_POINT('Ctrl Pts',(-199.314070955509,1.26549796615698,
125.023932443002));
#161261=CARTESIAN_POINT('Ctrl Pts',(-199.31800700495,1.18408604672678,125.007303536905));
#161262=CARTESIAN_POINT('Ctrl Pts',(-199.325430271356,1.03054570746349,
124.975941938976));
#161263=CARTESIAN_POINT('Ctrl Pts',(-199.332853537761,0.875526376150656,
124.950637115694));
#161264=CARTESIAN_POINT('Ctrl Pts',(-199.340276804166,0.719547249692918,
124.931526351391));
#161265=CARTESIAN_POINT('Ctrl Pts',(-199.347691296887,0.563752477609392,
124.912438174424));
#161266=CARTESIAN_POINT('Ctrl Pts',(-199.355105789608,0.407000535315681,
124.899529529172));
#161267=CARTESIAN_POINT('Ctrl Pts',(-199.362520282329,0.24982250344574,
124.892887088972));
#161268=CARTESIAN_POINT('Ctrl Pts',(-199.369927628683,0.0927959656810105,
124.886251051005));
#161269=CARTESIAN_POINT('Ctrl Pts',(-199.377334975037,-0.0646554736133486,
124.885869210084));
#161270=CARTESIAN_POINT('Ctrl Pts',(-199.38474232139,-0.221993995317587,
124.891776645347));
#161271=CARTESIAN_POINT('Ctrl Pts',(-199.392144143066,-0.379215168016295,
124.897679674621));
#161272=CARTESIAN_POINT('Ctrl Pts',(-199.399545964741,-0.536323219385118,
124.909862626159));
#161273=CARTESIAN_POINT('Ctrl Pts',(-199.406947786417,-0.692778811524635,
124.928308534679));
#161274=CARTESIAN_POINT('Ctrl Pts',(-199.414345700728,-0.84915181197491,
124.946744705747));
#161275=CARTESIAN_POINT('Ctrl Pts',(-199.421743615039,-1.00487266934929,
124.971437205811));
#161276=CARTESIAN_POINT('Ctrl Pts',(-199.429141529351,-1.15940576566253,
125.00231711264));
#161277=CARTESIAN_POINT('Ctrl Pts',(-199.436538214263,-1.3139131813789,
125.033191887789));
#161278=CARTESIAN_POINT('Ctrl Pts',(-199.443934899175,-1.46723286208119,
125.070251955885));
#161279=CARTESIAN_POINT('Ctrl Pts',(-199.451331584087,-1.61883788530298,
125.113377006308));
#161280=CARTESIAN_POINT('Ctrl Pts',(-199.458727941023,-1.7704361861996,
125.156500144521));
#161281=CARTESIAN_POINT('Ctrl Pts',(-199.466124297958,-1.92031962173487,
125.205687628209));
#161282=CARTESIAN_POINT('Ctrl Pts',(-199.473520654893,-2.06797523750912,
125.260768913666));
#161283=CARTESIAN_POINT('Ctrl Pts',(-199.48091814423,-2.21565345973426,
125.315858632208));
#161284=CARTESIAN_POINT('Ctrl Pts',(-199.488315633567,-2.36110283327585,
125.376843818751));
#161285=CARTESIAN_POINT('Ctrl Pts',(-199.495713122903,-2.50382937664356,
125.443505367221));
#161286=CARTESIAN_POINT('Ctrl Pts',(-199.503113205418,-2.64660595258121,
125.510190283794));
#161287=CARTESIAN_POINT('Ctrl Pts',(-199.510513287933,-2.78665745995995,
125.582555366178));
#161288=CARTESIAN_POINT('Ctrl Pts',(-199.517913370448,-2.92351369405257,
125.660335127428));
#161289=CARTESIAN_POINT('Ctrl Pts',(-199.525321590115,-3.06052041564315,
125.738200415521));
#161290=CARTESIAN_POINT('Ctrl Pts',(-199.532729809781,-3.1943245224501,
125.821492088438));
#161291=CARTESIAN_POINT('Ctrl Pts',(-199.540138029447,-3.3244834141804,
125.909900423496));
#161292=CARTESIAN_POINT('Ctrl Pts',(-199.54755080875,-3.45472241653674,
125.998363172409));
#161293=CARTESIAN_POINT('Ctrl Pts',(-199.554963588052,-3.58131143374482,
126.091948637279));
#161294=CARTESIAN_POINT('Ctrl Pts',(-199.562376367354,-3.7038406709643,
126.190306559949));
#161295=CARTESIAN_POINT('Ctrl Pts',(-199.569799738382,-3.82654498370379,
126.288805021032));
#161296=CARTESIAN_POINT('Ctrl Pts',(-199.577223109411,-3.94517765014855,
126.39208931474));
#161297=CARTESIAN_POINT('Ctrl Pts',(-199.58464648044,-4.05936487664758,
126.499771512815));
#161298=CARTESIAN_POINT('Ctrl Pts',(-199.588582529881,-4.11990968402192,
126.556867198033));
#161299=CARTESIAN_POINT('Ctrl Pts',(-199.592518579321,-4.17920537128048,
126.615198714714));
#161300=CARTESIAN_POINT('Ctrl Pts',(-199.596454628762,-4.23720087198234,
126.674704538306));
#161301=CARTESIAN_POINT('Ctrl Pts',(-199.603780504856,-4.3451435842251,
126.785458302217));
#161302=CARTESIAN_POINT('Ctrl Pts',(-199.611106380951,-4.44892529945081,
126.900636519193));
#161303=CARTESIAN_POINT('Ctrl Pts',(-199.618432257045,-4.54815423714637,
127.01988924132));
#161304=CARTESIAN_POINT('Ctrl Pts',(-199.625749275158,-4.64726319356173,
127.138997770688));
#161305=CARTESIAN_POINT('Ctrl Pts',(-199.633066293272,-4.74183008260889,
127.262170710391));
#161306=CARTESIAN_POINT('Ctrl Pts',(-199.640383311386,-4.83149884976926,
127.389020308435));
#161307=CARTESIAN_POINT('Ctrl Pts',(-199.647691937754,-4.9210647775684,
127.515724425147));
#161308=CARTESIAN_POINT('Ctrl Pts',(-199.655000564122,-5.00574355056634,
127.646096491343));
#161309=CARTESIAN_POINT('Ctrl Pts',(-199.66230919049,-5.08521874467687,
127.779715038116));
#161310=CARTESIAN_POINT('Ctrl Pts',(-199.669613071836,-5.1646423406467,
127.913246834945));
#161311=CARTESIAN_POINT('Ctrl Pts',(-199.676916953183,-5.23886888252049,
128.050020591129));
#161312=CARTESIAN_POINT('Ctrl Pts',(-199.684220834529,-5.30762463042162,
128.18958503541));
#161313=CARTESIAN_POINT('Ctrl Pts',(-199.691521506071,-5.37635016253885,
128.329088145923));
#161314=CARTESIAN_POINT('Ctrl Pts',(-199.698822177613,-5.43960951509057,
128.471379160608));
#161315=CARTESIAN_POINT('Ctrl Pts',(-199.706122849155,-5.49717452749041,
128.615981588053));
#161316=CARTESIAN_POINT('Ctrl Pts',(-199.713421843476,-5.55472631518357,
128.760550795239));
#161317=CARTESIAN_POINT('Ctrl Pts',(-199.720720837798,-5.60658622516097,
128.907430001561));
#161318=CARTESIAN_POINT('Ctrl Pts',(-199.728019832119,-5.6525740654497,
129.05612236232));
#161319=CARTESIAN_POINT('Ctrl Pts',(-199.735321043721,-5.69857587587576,
129.204859892687));
#161320=CARTESIAN_POINT('Ctrl Pts',(-199.742622255322,-5.73870193341256,
129.355411312575));
#161321=CARTESIAN_POINT('Ctrl Pts',(-199.749923466924,-5.77282175169358,
129.50726401913));
#161322=CARTESIAN_POINT('Ctrl Pts',(-199.757225668922,-5.80694619826219,
129.659137324213));
#161323=CARTESIAN_POINT('Ctrl Pts',(-199.764527870919,-5.83506270707501,
129.81231189086));
#161324=CARTESIAN_POINT('Ctrl Pts',(-199.771830072916,-5.85709199383315,
129.966265194433));
#161325=CARTESIAN_POINT('Ctrl Pts',(-199.779138508574,-5.87914008630182,
130.120349923109));
#161326=CARTESIAN_POINT('Ctrl Pts',(-199.786446944231,-5.8950905299074,
130.275214335113));
#161327=CARTESIAN_POINT('Ctrl Pts',(-199.793755379889,-5.90491592475032,
130.430330559776));
#161328=CARTESIAN_POINT('Ctrl Pts',(-199.799711855857,-5.91292375720509,
130.556752424544));
#161329=CARTESIAN_POINT('Ctrl Pts',(-199.805668331824,-5.9168640205334,
130.683341391447));
#161330=CARTESIAN_POINT('Ctrl Pts',(-199.811624807792,-5.91674748832781,
130.809812394026));
#161331=CARTESIAN_POINT('',(-201.561624807792,-5.9216802870108,130.802292919862));
#161332=CARTESIAN_POINT('Ctrl Pts',(-199.811624807792,-5.91707319532089,
130.809812694137));
#161333=CARTESIAN_POINT('Ctrl Pts',(-199.832717289386,-5.92122840583984,
131.257688120002));
#161334=CARTESIAN_POINT('Ctrl Pts',(-199.946625645587,-5.66995203506684,
133.671789078785));
#161335=CARTESIAN_POINT('Ctrl Pts',(-200.153349876387,-2.35938766776408,
137.393051713948));
#161336=CARTESIAN_POINT('Ctrl Pts',(-200.431797500202,4.26794575514161,
136.350728759107));
#161337=CARTESIAN_POINT('Ctrl Pts',(-200.710245124014,6.97324552981307,
130.211564437336));
#161338=CARTESIAN_POINT('Ctrl Pts',(-200.988692747828,3.27047332456854,
124.617150845494));
#161339=CARTESIAN_POINT('Ctrl Pts',(-201.26714037164,-3.43770409444905,
124.708480772182));
#161340=CARTESIAN_POINT('Ctrl Pts',(-201.458117724962,-5.87190273225,128.613207570693));
#161341=CARTESIAN_POINT('Ctrl Pts',(-201.556279203679,-5.9261716932185,
130.689210903785));
#161342=CARTESIAN_POINT('Ctrl Pts',(-201.561624807792,-5.92566153694035,
130.802291529712));
#161343=CARTESIAN_POINT('',(-203.31162480776,-5.91674832526764,130.799908882784));
#161344=CARTESIAN_POINT('Ctrl Pts',(-201.561624807792,-5.91674963930729,
130.802294641516));
#161345=CARTESIAN_POINT('Ctrl Pts',(-201.568982881734,-5.91680390723813,
130.957712590457));
#161346=CARTESIAN_POINT('Ctrl Pts',(-201.576340955677,-5.91073031198679,
131.113380258586));
#161347=CARTESIAN_POINT('Ctrl Pts',(-201.583699029619,-5.89849601535624,
131.26876918696));
#161348=CARTESIAN_POINT('Ctrl Pts',(-201.591048671187,-5.88627573926641,
131.423980039155));
#161349=CARTESIAN_POINT('Ctrl Pts',(-201.598398312754,-5.86790884059778,
131.578912411785));
#161350=CARTESIAN_POINT('Ctrl Pts',(-201.605747954322,-5.84341445076555,
131.733036082454));
#161351=CARTESIAN_POINT('Ctrl Pts',(-201.61309084544,-5.81894255837628,
131.887018194647));
#161352=CARTESIAN_POINT('Ctrl Pts',(-201.620433736558,-5.78835443516488,
132.040192709969));
#161353=CARTESIAN_POINT('Ctrl Pts',(-201.627776627676,-5.75172113270748,
132.192032975893));
#161354=CARTESIAN_POINT('Ctrl Pts',(-201.635114444198,-5.71511314714554,
132.343768306585));
#161355=CARTESIAN_POINT('Ctrl Pts',(-201.64245226072,-5.67246838760474,
132.494170855111));
#161356=CARTESIAN_POINT('Ctrl Pts',(-201.649790077242,-5.62390921912543,
132.642722839093));
#161357=CARTESIAN_POINT('Ctrl Pts',(-201.65712519342,-5.57536792060671,
132.791220155373));
#161358=CARTESIAN_POINT('Ctrl Pts',(-201.664460309597,-5.52091665958435,
132.937867900585));
#161359=CARTESIAN_POINT('Ctrl Pts',(-201.671795425774,-5.46072800920963,
133.082162226999));
#161360=CARTESIAN_POINT('Ctrl Pts',(-201.679129259572,-5.40054988146438,
133.2264313268));
#161361=CARTESIAN_POINT('Ctrl Pts',(-201.68646309337,-5.33463650595489,
133.368347475309));
#161362=CARTESIAN_POINT('Ctrl Pts',(-201.693796927167,-5.2632089776057,
133.507425881401));
#161363=CARTESIAN_POINT('Ctrl Pts',(-201.701130988438,-5.19177923379931,
133.646508601267));
#161364=CARTESIAN_POINT('Ctrl Pts',(-201.708465049707,-5.11483517035096,
133.782753065024));
#161365=CARTESIAN_POINT('Ctrl Pts',(-201.715799110978,-5.03264419073689,
133.915698434638));
#161366=CARTESIAN_POINT('Ctrl Pts',(-201.723134909502,-4.95043374214518,
134.04867529567));
#161367=CARTESIAN_POINT('Ctrl Pts',(-201.730470708027,-4.86297410395734,
134.178351183875));
#161368=CARTESIAN_POINT('Ctrl Pts',(-201.737806506552,-4.77057626898022,
134.304293848978));
#161369=CARTESIAN_POINT('Ctrl Pts',(-201.745149895269,-4.67808283196083,
134.430366824234));
#161370=CARTESIAN_POINT('Ctrl Pts',(-201.752493283986,-4.58064121767003,
134.55269855382));
#161371=CARTESIAN_POINT('Ctrl Pts',(-201.759836672703,-4.4786034494646,
134.67088899648));
#161372=CARTESIAN_POINT('Ctrl Pts',(-201.767183945264,-4.3765117145283,
134.789141948854));
#161373=CARTESIAN_POINT('Ctrl Pts',(-201.774531217824,-4.26981924252526,
134.903248973441));
#161374=CARTESIAN_POINT('Ctrl Pts',(-201.781878490384,-4.15891476263121,
135.012847110317));
#161375=CARTESIAN_POINT('Ctrl Pts',(-201.789236993135,-4.04784076697534,
135.12261276623));
#161376=CARTESIAN_POINT('Ctrl Pts',(-201.796595495886,-3.93254218153233,
135.227855508902));
#161377=CARTESIAN_POINT('Ctrl Pts',(-201.803953998638,-3.81344138899068,
135.328252231567));
#161378=CARTESIAN_POINT('Ctrl Pts',(-201.81064787218,-3.70509792958346,
135.419580996176));
#161379=CARTESIAN_POINT('Ctrl Pts',(-201.817341745723,-3.5936086492963,
135.506900002018));
#161380=CARTESIAN_POINT('Ctrl Pts',(-201.824035619266,-3.47931103503038,
135.589998013359));
#161381=CARTESIAN_POINT('Ctrl Pts',(-201.831458885672,-3.35255906776189,
135.682150736593));
#161382=CARTESIAN_POINT('Ctrl Pts',(-201.838882152077,-3.22195178485856,
135.769403615139));
#161383=CARTESIAN_POINT('Ctrl Pts',(-201.846305418483,-3.0879048581852,
135.851416605892));
#161384=CARTESIAN_POINT('Ctrl Pts',(-201.853719911204,-2.95401636384689,
135.933332664101));
#161385=CARTESIAN_POINT('Ctrl Pts',(-201.861134403924,-2.8166966332044,
136.010020969021));
#161386=CARTESIAN_POINT('Ctrl Pts',(-201.868548896646,-2.67639312130945,
136.081182617852));
#161387=CARTESIAN_POINT('Ctrl Pts',(-201.875956242999,-2.53622483922201,
136.152275678408));
#161388=CARTESIAN_POINT('Ctrl Pts',(-201.883363589353,-2.39307883188319,
136.217852519758));
#161389=CARTESIAN_POINT('Ctrl Pts',(-201.890770935707,-2.24743006191977,
136.277658405854));
#161390=CARTESIAN_POINT('Ctrl Pts',(-201.898172757382,-2.10188992230359,
136.337419686464));
#161391=CARTESIAN_POINT('Ctrl Pts',(-201.905574579058,-1.95385108065789,
136.391418440872));
#161392=CARTESIAN_POINT('Ctrl Pts',(-201.912976400733,-1.80381144299486,
136.439446671977));
#161393=CARTESIAN_POINT('Ctrl Pts',(-201.920374315044,-1.65385101008865,
136.487449549353));
#161394=CARTESIAN_POINT('Ctrl Pts',(-201.927772229356,-1.50189223927456,
136.529488066856));
#161395=CARTESIAN_POINT('Ctrl Pts',(-201.935170143667,-1.34845117572333,
136.56540305702));
#161396=CARTESIAN_POINT('Ctrl Pts',(-201.942566828579,-1.19503561129339,
136.601312078765));
#161397=CARTESIAN_POINT('Ctrl Pts',(-201.949963513491,-1.04013860613695,
136.631099507851));
#161398=CARTESIAN_POINT('Ctrl Pts',(-201.957360198404,-0.884289580498989,
136.654656550279));
#161399=CARTESIAN_POINT('Ctrl Pts',(-201.964756555339,-0.728447465370143,
136.678212548163));
#161400=CARTESIAN_POINT('Ctrl Pts',(-201.972152912275,-0.571653782799518,
136.695538652899));
#161401=CARTESIAN_POINT('Ctrl Pts',(-201.97954926921,-0.414446050683824,
136.706577576775));
#161402=CARTESIAN_POINT('Ctrl Pts',(-201.986946758547,-0.25721424966346,
136.717618190738));
#161403=CARTESIAN_POINT('Ctrl Pts',(-201.994344247883,-0.0995686452809479,
136.722369681061));
#161404=CARTESIAN_POINT('Ctrl Pts',(-202.00174173722,0.0579503942137365,
136.720826819135));
#161405=CARTESIAN_POINT('Ctrl Pts',(-202.009141819735,0.215524651763755,
136.719283416362));
#161406=CARTESIAN_POINT('Ctrl Pts',(-202.016541902249,0.372971883044187,
136.711441271919));
#161407=CARTESIAN_POINT('Ctrl Pts',(-202.023941984764,0.529754145426437,
136.69734722097));
#161408=CARTESIAN_POINT('Ctrl Pts',(-202.031350204431,0.686708806024008,
136.683237672164));
#161409=CARTESIAN_POINT('Ctrl Pts',(-202.038758424097,0.842996665438895,
136.662862521241));
#161410=CARTESIAN_POINT('Ctrl Pts',(-202.046166643764,0.998086579105648,
136.636320300478));
#161411=CARTESIAN_POINT('Ctrl Pts',(-202.053579423066,1.15327194802645,
136.609761743421));
#161412=CARTESIAN_POINT('Ctrl Pts',(-202.060992202368,1.30725753771265,
136.577028630497));
#161413=CARTESIAN_POINT('Ctrl Pts',(-202.06840498167,1.45952526831276,136.538269977999));
#161414=CARTESIAN_POINT('Ctrl Pts',(-202.075828352699,1.61201056618677,
136.49945594532));
#161415=CARTESIAN_POINT('Ctrl Pts',(-202.083251723727,1.76277274582379,
136.454599283991));
#161416=CARTESIAN_POINT('Ctrl Pts',(-202.090675094756,1.91131088775466,
136.403898210337));
#161417=CARTESIAN_POINT('Ctrl Pts',(-202.094611144197,1.99006937472724,
136.377015284531));
#161418=CARTESIAN_POINT('Ctrl Pts',(-202.098547193638,2.06820295967937,
136.34849008045));
#161419=CARTESIAN_POINT('Ctrl Pts',(-202.102483243078,2.14563967604513,
136.318357438664));
#161420=CARTESIAN_POINT('Ctrl Pts',(-202.109906509484,2.29168290639948,
136.261528216662));
#161421=CARTESIAN_POINT('Ctrl Pts',(-202.117329775889,2.43568765092004,
136.198806922689));
#161422=CARTESIAN_POINT('Ctrl Pts',(-202.124753042294,2.5771431409141,136.130359471653));
#161423=CARTESIAN_POINT('Ctrl Pts',(-202.132167535015,2.71843144226654,
136.06199291982));
#161424=CARTESIAN_POINT('Ctrl Pts',(-202.139582027737,2.85717615375475,
135.987913843359));
#161425=CARTESIAN_POINT('Ctrl Pts',(-202.146996520458,2.99288393960237,
135.908337134613));
#161426=CARTESIAN_POINT('Ctrl Pts',(-202.154403866811,3.12846092517669,
135.828837124895));
#161427=CARTESIAN_POINT('Ctrl Pts',(-202.161811213165,3.26100649253989,
135.743850219369));
#161428=CARTESIAN_POINT('Ctrl Pts',(-202.169218559519,3.39004959613795,
135.653638326486));
#161429=CARTESIAN_POINT('Ctrl Pts',(-202.176620381194,3.51899645452082,
135.563493717036));
#161430=CARTESIAN_POINT('Ctrl Pts',(-202.18402220287,3.64444574588738,135.468132092632));
#161431=CARTESIAN_POINT('Ctrl Pts',(-202.191424024545,3.76595334602514,
135.36785992819));
#161432=CARTESIAN_POINT('Ctrl Pts',(-202.198821938857,3.88739680324591,
135.267640696643));
#161433=CARTESIAN_POINT('Ctrl Pts',(-202.206219853168,4.00490242603697,
135.16251632462));
#161434=CARTESIAN_POINT('Ctrl Pts',(-202.213617767479,4.11805736728282,
135.052834941634));
#161435=CARTESIAN_POINT('Ctrl Pts',(-202.221014452392,4.23119350423076,
134.943171785704));
#161436=CARTESIAN_POINT('Ctrl Pts',(-202.228411137304,4.33998012680202,
134.828953381375));
#161437=CARTESIAN_POINT('Ctrl Pts',(-202.235807822216,4.44403953894811,
134.710566339077));
#161438=CARTESIAN_POINT('Ctrl Pts',(-202.243204179152,4.54809433699053,
134.592184546185));
#161439=CARTESIAN_POINT('Ctrl Pts',(-202.250600536087,4.64742209493324,
134.469634763234));
#161440=CARTESIAN_POINT('Ctrl Pts',(-202.257996893022,4.74168407344933,
134.343338253847));
#161441=CARTESIAN_POINT('Ctrl Pts',(-202.265394382359,4.83596048371523,
134.217022408141));
#161442=CARTESIAN_POINT('Ctrl Pts',(-202.272791871696,4.92516934696955,
134.086958992999));
#161443=CARTESIAN_POINT('Ctrl Pts',(-202.280189361032,5.00901418199923,
133.953599809344));
#161444=CARTESIAN_POINT('Ctrl Pts',(-202.287589443547,5.09288840870597,
133.820193876833));
#161445=CARTESIAN_POINT('Ctrl Pts',(-202.294989526062,5.17139466485451,
133.683490191393));
#161446=CARTESIAN_POINT('Ctrl Pts',(-202.302389608577,5.24428158306487,
133.543966654942));
#161447=CARTESIAN_POINT('Ctrl Pts',(-202.309797828244,5.31724864793465,
133.40428969802));
#161448=CARTESIAN_POINT('Ctrl Pts',(-202.31720604791,5.3845838619657,133.261787028827));
#161449=CARTESIAN_POINT('Ctrl Pts',(-202.324614267577,5.44608302654156,
133.116958773432));
#161450=CARTESIAN_POINT('Ctrl Pts',(-202.332027046879,5.50762004282705,
132.972041378663));
#161451=CARTESIAN_POINT('Ctrl Pts',(-202.339439826181,5.56331372040708,
132.824795893876));
#161452=CARTESIAN_POINT('Ctrl Pts',(-202.346852605483,5.61300939609337,
132.675738741267));
#161453=CARTESIAN_POINT('Ctrl Pts',(-202.354275976512,5.66277607929151,
132.526468608809));
#161454=CARTESIAN_POINT('Ctrl Pts',(-202.361699347541,5.70652754037334,
132.375381996141));
#161455=CARTESIAN_POINT('Ctrl Pts',(-202.36912271857,5.74415978513868,132.223007481763));
#161456=CARTESIAN_POINT('Ctrl Pts',(-202.37305876801,5.76411330428583,132.142214858066));
#161457=CARTESIAN_POINT('Ctrl Pts',(-202.376994817451,5.78234735340238,
132.061060290616));
#161458=CARTESIAN_POINT('Ctrl Pts',(-202.380930866892,5.79885234516005,
131.9796231591));
#161459=CARTESIAN_POINT('Ctrl Pts',(-202.388354133297,5.82998024451299,
131.82603527062));
#161460=CARTESIAN_POINT('Ctrl Pts',(-202.395777399702,5.85504912545923,
131.670977609184));
#161461=CARTESIAN_POINT('Ctrl Pts',(-202.403200666108,5.87392249395432,
131.514969580018));
#161462=CARTESIAN_POINT('Ctrl Pts',(-202.410615158829,5.89277355569518,
131.359145939387));
#161463=CARTESIAN_POINT('Ctrl Pts',(-202.41802965155,5.90544363622744,131.202374533849));
#161464=CARTESIAN_POINT('Ctrl Pts',(-202.425444144271,5.91184687052777,
131.045186575326));
#161465=CARTESIAN_POINT('Ctrl Pts',(-202.432851490625,5.91824393314985,
130.888150120474));
#161466=CARTESIAN_POINT('Ctrl Pts',(-202.440258836978,5.91838615934132,
130.730698282408));
#161467=CARTESIAN_POINT('Ctrl Pts',(-202.447666183332,5.91223928847316,
130.573368933009));
#161468=CARTESIAN_POINT('Ctrl Pts',(-202.455068005008,5.90609700217325,
130.416156925776));
#161469=CARTESIAN_POINT('Ctrl Pts',(-202.462469826683,5.8936749730336,130.259067596714));
#161470=CARTESIAN_POINT('Ctrl Pts',(-202.469871648358,5.87499098709605,
130.10264025728));
#161471=CARTESIAN_POINT('Ctrl Pts',(-202.47726956267,5.85631686428913,129.94629549462));
#161472=CARTESIAN_POINT('Ctrl Pts',(-202.484667476981,5.83138741218186,
129.790612395348));
#161473=CARTESIAN_POINT('Ctrl Pts',(-202.492065391293,5.80027236804441,
129.636126471943));
#161474=CARTESIAN_POINT('Ctrl Pts',(-202.499462076205,5.76916249466294,
129.481666221295));
#161475=CARTESIAN_POINT('Ctrl Pts',(-202.506858761117,5.73186914302823,
129.328403117249));
#161476=CARTESIAN_POINT('Ctrl Pts',(-202.514255446029,5.68851342550535,
129.176863898569));
#161477=CARTESIAN_POINT('Ctrl Pts',(-202.521651802964,5.64515963042055,
129.025331399297));
#161478=CARTESIAN_POINT('Ctrl Pts',(-202.5290481599,5.59574410661747,128.875522992302));
#161479=CARTESIAN_POINT('Ctrl Pts',(-202.536444516835,5.54043817823208,
128.727951371852));
#161480=CARTESIAN_POINT('Ctrl Pts',(-202.543842006172,5.48512378236803,
128.580357157809));
#161481=CARTESIAN_POINT('Ctrl Pts',(-202.551239495508,5.42391731725896,
128.435000761769));
#161482=CARTESIAN_POINT('Ctrl Pts',(-202.558636984845,5.35703864047963,
128.292375831205));
#161483=CARTESIAN_POINT('Ctrl Pts',(-202.56603706736,5.29013651948354,128.149700903693));
#161484=CARTESIAN_POINT('Ctrl Pts',(-202.573437149875,5.21755838634373,
128.009759685829));
#161485=CARTESIAN_POINT('Ctrl Pts',(-202.58083723239,5.13957044327107,127.873021977771));
#161486=CARTESIAN_POINT('Ctrl Pts',(-202.588245452056,5.06149674443775,
127.736133912546));
#161487=CARTESIAN_POINT('Ctrl Pts',(-202.595653671723,4.9780015408993,127.60245671643));
#161488=CARTESIAN_POINT('Ctrl Pts',(-202.603061891389,4.8893952285411,127.472432517859));
#161489=CARTESIAN_POINT('Ctrl Pts',(-202.610474670691,4.80073438047586,
127.342328291562));
#161490=CARTESIAN_POINT('Ctrl Pts',(-202.617887449993,4.70695637704169,
127.215881842089));
#161491=CARTESIAN_POINT('Ctrl Pts',(-202.625300229295,4.60841209962781,
127.093502430771));
#161492=CARTESIAN_POINT('Ctrl Pts',(-202.632723600324,4.50972701752896,
126.970948158011));
#161493=CARTESIAN_POINT('Ctrl Pts',(-202.640146971353,4.40626230469941,
126.852472810054));
#161494=CARTESIAN_POINT('Ctrl Pts',(-202.647570342382,4.29840645779756,
126.738449589756));
#161495=CARTESIAN_POINT('Ctrl Pts',(-202.651506391822,4.24121869980284,
126.677991742403));
#161496=CARTESIAN_POINT('Ctrl Pts',(-202.655442441263,4.18279701272454,
126.618784894444));
#161497=CARTESIAN_POINT('Ctrl Pts',(-202.659378490704,4.12320299875834,
126.560880018632));
#161498=CARTESIAN_POINT('Ctrl Pts',(-202.66680175711,4.01081054828672,126.451673230002));
#161499=CARTESIAN_POINT('Ctrl Pts',(-202.674225023515,3.89390648875168,
126.346769616974));
#161500=CARTESIAN_POINT('Ctrl Pts',(-202.681648289921,3.77285403211578,
126.246564767065));
#161501=CARTESIAN_POINT('Ctrl Pts',(-202.689062782642,3.65194464943049,
126.146478350966));
#161502=CARTESIAN_POINT('Ctrl Pts',(-202.696477275363,3.52689691396513,
126.051079879331));
#161503=CARTESIAN_POINT('Ctrl Pts',(-202.703891768084,3.39811133721108,
125.960728725853));
#161504=CARTESIAN_POINT('Ctrl Pts',(-202.711299114438,3.2694498888457,125.87046465622));
#161505=CARTESIAN_POINT('Ctrl Pts',(-202.718706460791,3.13705807494424,
125.785238432848));
#161506=CARTESIAN_POINT('Ctrl Pts',(-202.726113807145,3.00136990364706,
125.705369613065));
#161507=CARTESIAN_POINT('Ctrl Pts',(-202.733515628821,2.86578293370648,
125.625560362461));
#161508=CARTESIAN_POINT('Ctrl Pts',(-202.740917450496,2.7269048219899,125.551100747908));
#161509=CARTESIAN_POINT('Ctrl Pts',(-202.748319272171,2.5851989202899,125.482267316521));
#161510=CARTESIAN_POINT('Ctrl Pts',(-202.755717186483,2.44356782403319,
125.413470221767));
#161511=CARTESIAN_POINT('Ctrl Pts',(-202.763115100794,2.29911224564274,
125.350293557936));
#161512=CARTESIAN_POINT('Ctrl Pts',(-202.770513015105,2.15232042163001,
125.292968110664));
#161513=CARTESIAN_POINT('Ctrl Pts',(-202.777909700018,2.00555299175515,
125.235652189841));
#161514=CARTESIAN_POINT('Ctrl Pts',(-202.78530638493,1.85645043418548,125.184185691378));
#161515=CARTESIAN_POINT('Ctrl Pts',(-202.792703069842,1.70552137335281,
125.13875143518));
#161516=CARTESIAN_POINT('Ctrl Pts',(-202.800099426778,1.55459900487243,
125.093319193584));
#161517=CARTESIAN_POINT('Ctrl Pts',(-202.807495783713,1.40185065161534,
125.053918770026));
#161518=CARTESIAN_POINT('Ctrl Pts',(-202.814892140649,1.2478002626691,125.020683148431));
#161519=CARTESIAN_POINT('Ctrl Pts',(-202.822289629985,1.09372628821504,
124.987442438377));
#161520=CARTESIAN_POINT('Ctrl Pts',(-202.829687119322,0.938350246075035,
124.960368488343));
#161521=CARTESIAN_POINT('Ctrl Pts',(-202.837084608658,0.782206294241051,
124.939543154443));
#161522=CARTESIAN_POINT('Ctrl Pts',(-202.844484691173,0.626007606387029,
124.918710520255));
#161523=CARTESIAN_POINT('Ctrl Pts',(-202.851884773688,0.469040842675188,
124.904130912675));
#161524=CARTESIAN_POINT('Ctrl Pts',(-202.859284856203,0.311845148080142,
124.895834306707));
#161525=CARTESIAN_POINT('Ctrl Pts',(-202.86669307587,0.154476600659004,
124.887528577766));
#161526=CARTESIAN_POINT('Ctrl Pts',(-202.874101295536,-0.00312100736494086,
124.885519667463));
#161527=CARTESIAN_POINT('Ctrl Pts',(-202.881509515203,-0.160407924259452,
124.889785412166));
#161528=CARTESIAN_POINT('Ctrl Pts',(-202.888922294505,-0.317791648627735,
124.894053782363));
#161529=CARTESIAN_POINT('Ctrl Pts',(-202.896335073807,-0.474863929231365,
124.904604478017));
#161530=CARTESIAN_POINT('Ctrl Pts',(-202.903747853109,-0.631090782958744,
124.921363508425));
#161531=CARTESIAN_POINT('Ctrl Pts',(-202.911171224138,-0.787540860940819,
124.938146484921));
#161532=CARTESIAN_POINT('Ctrl Pts',(-202.918594595167,-0.943142731124381,
124.961155458605));
#161533=CARTESIAN_POINT('Ctrl Pts',(-202.926017966195,-1.09737241544244,
124.990265301498));
#161534=CARTESIAN_POINT('Ctrl Pts',(-202.929954015636,-1.17914869475504,
125.00570003868));
#161535=CARTESIAN_POINT('Ctrl Pts',(-202.933890065077,-1.260539441657,125.022849111077));
#161536=CARTESIAN_POINT('Ctrl Pts',(-202.937826114517,-1.34146847383707,
125.041688243033));
#161537=CARTESIAN_POINT('Ctrl Pts',(-202.945249380923,-1.49409810282559,
125.077218257956));
#161538=CARTESIAN_POINT('Ctrl Pts',(-202.952672647328,-1.64554598320926,
125.118869988883));
#161539=CARTESIAN_POINT('Ctrl Pts',(-202.960095913734,-1.79528297106824,
125.166551680018));
#161540=CARTESIAN_POINT('Ctrl Pts',(-202.967510406455,-1.94484298224202,
125.214177015355));
#161541=CARTESIAN_POINT('Ctrl Pts',(-202.974924899176,-2.0926957737322,
125.267818012581));
#161542=CARTESIAN_POINT('Ctrl Pts',(-202.982339391897,-2.23832250802715,
125.327331960296));
#161543=CARTESIAN_POINT('Ctrl Pts',(-202.98974673825,-2.38380888179367,
125.386788546228));
#161544=CARTESIAN_POINT('Ctrl Pts',(-202.997154084604,-2.52707312651263,
125.452106673295));
#161545=CARTESIAN_POINT('Ctrl Pts',(-203.004561430958,-2.66761179755283,
125.523093926699));
#161546=CARTESIAN_POINT('Ctrl Pts',(-203.011963252633,-2.80804564954954,
125.594028235132));
#161547=CARTESIAN_POINT('Ctrl Pts',(-203.019365074309,-2.94575764374757,
125.670623083307));
#161548=CARTESIAN_POINT('Ctrl Pts',(-203.026766895984,-3.08026466026495,
125.752638120712));
#161549=CARTESIAN_POINT('Ctrl Pts',(-203.034164810295,-3.21470067157453,
125.834609863016));
#161550=CARTESIAN_POINT('Ctrl Pts',(-203.041562724607,-3.34593475675407,
125.921995902334));
#161551=CARTESIAN_POINT('Ctrl Pts',(-203.048960638918,-3.47350884555318,
126.014510216733));
#161552=CARTESIAN_POINT('Ctrl Pts',(-203.05635732383,-3.60106173385371,
126.107009156931));
#161553=CARTESIAN_POINT('Ctrl Pts',(-203.063754008742,-3.72495553101644,
126.20463446186));
#161554=CARTESIAN_POINT('Ctrl Pts',(-203.071150693655,-3.84476150154799,
126.307057030002));
#161555=CARTESIAN_POINT('Ctrl Pts',(-203.07854705059,-3.96456215975726,
126.409475056621));
#161556=CARTESIAN_POINT('Ctrl Pts',(-203.085943407525,-4.08027506799617,
126.516689680931));
#161557=CARTESIAN_POINT('Ctrl Pts',(-203.093339764461,-4.19150513584072,
126.628331970787));
#161558=CARTESIAN_POINT('Ctrl Pts',(-203.100737253797,-4.3027522332923,
126.739991353362));
#161559=CARTESIAN_POINT('Ctrl Pts',(-203.108134743134,-4.40951486027692,
126.85607948678));
#161560=CARTESIAN_POINT('Ctrl Pts',(-203.11553223247,-4.51143542348493,
126.976191214023));
#161561=CARTESIAN_POINT('Ctrl Pts',(-203.122932314985,-4.61339171478823,
127.096345046245));
#161562=CARTESIAN_POINT('Ctrl Pts',(-203.1303323975,-4.71050232147278,127.220524996061));
#161563=CARTESIAN_POINT('Ctrl Pts',(-203.137732480015,-4.80245060369318,
127.348293667753));
#161564=CARTESIAN_POINT('Ctrl Pts',(-203.145140699682,-4.89449999250279,
127.476202834236));
#161565=CARTESIAN_POINT('Ctrl Pts',(-203.152548919348,-4.98137550230915,
127.607708300172));
#161566=CARTESIAN_POINT('Ctrl Pts',(-203.159957139014,-5.06280403100677,
127.74234397716));
#161567=CARTESIAN_POINT('Ctrl Pts',(-203.167369918316,-5.14428267760486,
127.87706252016));
#161568=CARTESIAN_POINT('Ctrl Pts',(-203.174782697619,-5.22030748290961,
128.014914787064));
#161569=CARTESIAN_POINT('Ctrl Pts',(-203.182195476921,-5.29065206648016,
128.155411528975));
#161570=CARTESIAN_POINT('Ctrl Pts',(-203.189618847949,-5.36109716169105,
128.296109019219));
#161571=CARTESIAN_POINT('Ctrl Pts',(-203.197042218978,-5.42584567210385,
128.43945819178));
#161572=CARTESIAN_POINT('Ctrl Pts',(-203.204465590007,-5.48471964848875,
128.584950574338));
#161573=CARTESIAN_POINT('Ctrl Pts',(-203.208401639448,-5.51593604343254,
128.662094126619));
#161574=CARTESIAN_POINT('Ctrl Pts',(-203.212337688889,-5.54550172992229,
128.739839959623));
#161575=CARTESIAN_POINT('Ctrl Pts',(-203.21627373833,-5.5733959533535,128.818110857429));
#161576=CARTESIAN_POINT('Ctrl Pts',(-203.224921721089,-5.63468297906373,
128.990081607504));
#161577=CARTESIAN_POINT('Ctrl Pts',(-203.233569703848,-5.68805083248295,
129.165014549172));
#161578=CARTESIAN_POINT('Ctrl Pts',(-203.242217686606,-5.73324512702968,
129.342228313056));
#161579=CARTESIAN_POINT('Ctrl Pts',(-203.250830811819,-5.77825725629626,
129.518727778925));
#161580=CARTESIAN_POINT('Ctrl Pts',(-203.259443937031,-5.81516149890193,
129.697489615715));
#161581=CARTESIAN_POINT('Ctrl Pts',(-203.268057062243,-5.84375315109936,
129.877818836794));
#161582=CARTESIAN_POINT('Ctrl Pts',(-203.276602616523,-5.87212049858119,
130.056733354925));
#161583=CARTESIAN_POINT('Ctrl Pts',(-203.285148170803,-5.89230509977486,
130.237190643914));
#161584=CARTESIAN_POINT('Ctrl Pts',(-203.293693725083,-5.90415413278233,
130.418492066309));
#161585=CARTESIAN_POINT('Ctrl Pts',(-203.299670752642,-5.91244171653796,
130.545299943557));
#161586=CARTESIAN_POINT('Ctrl Pts',(-203.305647780201,-5.91665247871619,
130.672520358863));
#161587=CARTESIAN_POINT('Ctrl Pts',(-203.31162480776,-5.91674832526764,
130.799908882784));
#161588=CARTESIAN_POINT('',(-205.061626015508,-5.91263662896126,130.80817859488));
#161589=CARTESIAN_POINT('Ctrl Pts',(-203.311624807792,-5.91674832526815,
130.799908883463));
#161590=CARTESIAN_POINT('Ctrl Pts',(-203.31925383089,-5.91687066290775,
130.962506425771));
#161591=CARTESIAN_POINT('Ctrl Pts',(-203.326882853988,-5.91028565918037,
131.125172439786));
#161592=CARTESIAN_POINT('Ctrl Pts',(-203.334511877086,-5.8970065749038,
131.287314050147));
#161593=CARTESIAN_POINT('Ctrl Pts',(-203.341914747701,-5.88412113183752,
131.444649183011));
#161594=CARTESIAN_POINT('Ctrl Pts',(-203.349317618315,-5.86493289222459,
131.601490170919));
#161595=CARTESIAN_POINT('Ctrl Pts',(-203.35672048893,-5.83950678773434,
131.757298725999));
#161596=CARTESIAN_POINT('Ctrl Pts',(-203.364124032299,-5.81407837258119,
131.913121440585));
#161597=CARTESIAN_POINT('Ctrl Pts',(-203.371527575669,-5.78241102307281,
132.067911168375));
#161598=CARTESIAN_POINT('Ctrl Pts',(-203.378931119038,-5.7446210682295,
132.22113842123));
#161599=CARTESIAN_POINT('Ctrl Pts',(-203.386336782644,-5.70682029105092,
132.374409555499));
#161600=CARTESIAN_POINT('Ctrl Pts',(-203.39374244625,-5.66289350593888,
132.526116962837));
#161601=CARTESIAN_POINT('Ctrl Pts',(-203.401148109856,-5.61300728187641,
132.675745082635));
#161602=CARTESIAN_POINT('Ctrl Pts',(-203.40894588088,-5.56047973361094,
132.833295557386));
#161603=CARTESIAN_POINT('Ctrl Pts',(-203.416743651903,-5.5013446649065,
132.988540125356));
#161604=CARTESIAN_POINT('Ctrl Pts',(-203.424541422927,-5.43585428549973,
133.1409005272));
#161605=CARTESIAN_POINT('Ctrl Pts',(-203.431959917198,-5.37354930079099,
133.285850252536));
#161606=CARTESIAN_POINT('Ctrl Pts',(-203.439378411468,-5.305492808283,133.428189425049));
#161607=CARTESIAN_POINT('Ctrl Pts',(-203.446796905739,-5.23194910023918,
133.567445700405));
#161608=CARTESIAN_POINT('Ctrl Pts',(-203.454220864128,-5.15835122331424,
133.706804545468));
#161609=CARTESIAN_POINT('Ctrl Pts',(-203.461644822517,-5.07925826396159,
133.84307564888));
#161610=CARTESIAN_POINT('Ctrl Pts',(-203.469068780906,-4.99497801599823,
133.975815359825));
#161611=CARTESIAN_POINT('Ctrl Pts',(-203.47650313371,-4.91057976578007,
134.108740921968));
#161612=CARTESIAN_POINT('Ctrl Pts',(-203.483937486513,-4.82097993977899,
134.238124918073));
#161613=CARTESIAN_POINT('Ctrl Pts',(-203.491371839317,-4.72652713722884,
134.363556001854));
#161614=CARTESIAN_POINT('Ctrl Pts',(-203.492488346925,-4.71234200565376,
134.382393520477));
#161615=CARTESIAN_POINT('Ctrl Pts',(-203.493604854534,-4.69804748499611,
134.401141949454));
#161616=CARTESIAN_POINT('Ctrl Pts',(-203.494721362142,-4.68364482727004,
134.419799967699));
#161617=CARTESIAN_POINT('Ctrl Pts',(-203.502144628548,-4.58788662156608,
134.543850568851));
#161618=CARTESIAN_POINT('Ctrl Pts',(-203.509567894953,-4.48705182451503,
134.664281756115));
#161619=CARTESIAN_POINT('Ctrl Pts',(-203.516991161359,-4.38144383707481,
134.78065040392));
#161620=CARTESIAN_POINT('Ctrl Pts',(-203.52440565408,-4.27596066950554,
134.896881513646));
#161621=CARTESIAN_POINT('Ctrl Pts',(-203.531820146801,-4.16571578943428,
135.009059367759));
#161622=CARTESIAN_POINT('Ctrl Pts',(-203.539234639522,-4.05105465877887,
135.116771395088));
#161623=CARTESIAN_POINT('Ctrl Pts',(-203.546641985876,-3.93650404283811,
135.22437960551));
#161624=CARTESIAN_POINT('Ctrl Pts',(-203.55404933223,-3.81754592051431,
135.327530304353));
#161625=CARTESIAN_POINT('Ctrl Pts',(-203.561456678584,-3.69456456150438,
135.425845580581));
#161626=CARTESIAN_POINT('Ctrl Pts',(-203.568858500259,-3.57167492663218,
135.524087529567));
#161627=CARTESIAN_POINT('Ctrl Pts',(-203.576260321934,-3.44476832015857,
135.617501004755));
#161628=CARTESIAN_POINT('Ctrl Pts',(-203.58366214361,-3.31426416180886,
135.705746506093));
#161629=CARTESIAN_POINT('Ctrl Pts',(-203.591060057921,-3.18382889558812,
135.793945423318));
#161630=CARTESIAN_POINT('Ctrl Pts',(-203.598457972233,-3.04980016813304,
135.876981591329));
#161631=CARTESIAN_POINT('Ctrl Pts',(-203.605855886544,-2.91262852580243,
135.954557277227));
#161632=CARTESIAN_POINT('Ctrl Pts',(-203.613252571456,-2.77547967891002,
136.032120071453));
#161633=CARTESIAN_POINT('Ctrl Pts',(-203.620649256369,-2.63518927836053,
136.104224000971));
#161634=CARTESIAN_POINT('Ctrl Pts',(-203.628045941281,-2.49223485864503,
136.170615920089));
#161635=CARTESIAN_POINT('Ctrl Pts',(-203.635442298216,-2.3492867776783,
136.23700489532));
#161636=CARTESIAN_POINT('Ctrl Pts',(-203.642838655152,-2.20367525098471,
136.297682206512));
#161637=CARTESIAN_POINT('Ctrl Pts',(-203.650235012087,-2.05590005455707,
136.352441865004));
#161638=CARTESIAN_POINT('Ctrl Pts',(-203.657632501424,-1.90810223337002,
136.40720990734));
#161639=CARTESIAN_POINT('Ctrl Pts',(-203.665029990761,-1.75814043291998,
136.456058363276));
#161640=CARTESIAN_POINT('Ctrl Pts',(-203.672427480097,-1.60653179003577,
136.498830405887));
#161641=CARTESIAN_POINT('Ctrl Pts',(-203.679827562612,-1.45487000097703,
136.541617442172));
#161642=CARTESIAN_POINT('Ctrl Pts',(-203.687227645127,-1.30156057913766,
136.578323722869));
#161643=CARTESIAN_POINT('Ctrl Pts',(-203.694627727642,-1.14713296000083,
136.60884306948));
#161644=CARTESIAN_POINT('Ctrl Pts',(-203.702035947309,-0.992535531820553,
136.63939597525));
#161645=CARTESIAN_POINT('Ctrl Pts',(-203.709444166976,-0.836817817244495,
136.663748288138));
#161646=CARTESIAN_POINT('Ctrl Pts',(-203.716852386642,-0.680517251053971,
136.681845354553));
#161647=CARTESIAN_POINT('Ctrl Pts',(-203.724265165944,-0.524120484472526,
136.699953559411));
#161648=CARTESIAN_POINT('Ctrl Pts',(-203.731677945247,-0.367140522827894,
136.711798818167));
#161649=CARTESIAN_POINT('Ctrl Pts',(-203.739090724549,-0.210116445125973,
136.717378598427));
#161650=CARTESIAN_POINT('Ctrl Pts',(-203.746514095577,-0.0528680040588055,
136.722966351339));
#161651=CARTESIAN_POINT('Ctrl Pts',(-203.753937466606,0.104424306655523,
136.722270747431));
#161652=CARTESIAN_POINT('Ctrl Pts',(-203.761360837635,0.261224055224296,
136.715341293856));
#161653=CARTESIAN_POINT('Ctrl Pts',(-203.765296887076,0.344363044267299,
136.711667131301));
#161654=CARTESIAN_POINT('Ctrl Pts',(-203.769232936516,0.427363673358813,
136.706241273284));
#161655=CARTESIAN_POINT('Ctrl Pts',(-203.773168985957,0.510147086307701,
136.699076939225));
#161656=CARTESIAN_POINT('Ctrl Pts',(-203.780592252362,0.666274019559398,
136.68556522878));
#161657=CARTESIAN_POINT('Ctrl Pts',(-203.788015518767,0.822099859025682,
136.665826056643));
#161658=CARTESIAN_POINT('Ctrl Pts',(-203.795438785173,0.977087794984135,
136.639875162436));
#161659=CARTESIAN_POINT('Ctrl Pts',(-203.802853277894,1.13189254807323,
136.613954940032));
#161660=CARTESIAN_POINT('Ctrl Pts',(-203.810267770615,1.28586100433918,
136.581837670375));
#161661=CARTESIAN_POINT('Ctrl Pts',(-203.817682263336,1.43845932536675,
136.543590995567));
#161662=CARTESIAN_POINT('Ctrl Pts',(-203.82508960969,1.59091056638773,136.505381184343));
#161663=CARTESIAN_POINT('Ctrl Pts',(-203.832496956044,1.74199394153385,
136.461053819284));
#161664=CARTESIAN_POINT('Ctrl Pts',(-203.839904302397,1.8911837963895,136.410727927222));
#161665=CARTESIAN_POINT('Ctrl Pts',(-203.847306124073,2.04026237982279,
136.360439570108));
#161666=CARTESIAN_POINT('Ctrl Pts',(-203.854707945748,2.18744990277064,
136.30416171299));
#161667=CARTESIAN_POINT('Ctrl Pts',(-203.862109767424,2.33223402761866,
136.24206371749));
#161668=CARTESIAN_POINT('Ctrl Pts',(-203.869507681735,2.47694172205335,
136.179998503038));
#161669=CARTESIAN_POINT('Ctrl Pts',(-203.876905596046,2.61924820292951,
136.112119415821));
#161670=CARTESIAN_POINT('Ctrl Pts',(-203.884303510358,2.7586594478157,136.038644581345));
#161671=CARTESIAN_POINT('Ctrl Pts',(-203.89170019527,2.89804752508276,135.965181957054));
#161672=CARTESIAN_POINT('Ctrl Pts',(-203.899096880182,3.03454099135519,
135.886125604982));
#161673=CARTESIAN_POINT('Ctrl Pts',(-203.906493565094,3.16766874893783,
135.801740456992));
#161674=CARTESIAN_POINT('Ctrl Pts',(-203.91388992203,3.30079060349657,135.717359050728));
#161675=CARTESIAN_POINT('Ctrl Pts',(-203.921286278965,3.43054673081018,
135.627649518213));
#161676=CARTESIAN_POINT('Ctrl Pts',(-203.928682635901,3.55649368565297,
135.532920993242));
#161677=CARTESIAN_POINT('Ctrl Pts',(-203.936080125237,3.68245992329573,
135.438177965092));
#161678=CARTESIAN_POINT('Ctrl Pts',(-203.943477614574,3.80461552889866,
135.338414638858));
#161679=CARTESIAN_POINT('Ctrl Pts',(-203.95087510391,3.92254903444112,135.233981327616));
#161680=CARTESIAN_POINT('Ctrl Pts',(-203.958275186425,4.04052388139095,
135.12951140744));
#161681=CARTESIAN_POINT('Ctrl Pts',(-203.96567526894,4.15427340221235,135.020368490215));
#161682=CARTESIAN_POINT('Ctrl Pts',(-203.973075351455,4.26342209311666,
134.906940612938));
#161683=CARTESIAN_POINT('Ctrl Pts',(-203.980483571122,4.37269080422754,
134.793388010048));
#161684=CARTESIAN_POINT('Ctrl Pts',(-203.987891790788,4.47734832309786,
134.675541306575));
#161685=CARTESIAN_POINT('Ctrl Pts',(-203.995300010455,4.57705817148828,
134.55382312002));
#161686=CARTESIAN_POINT('Ctrl Pts',(-204.002712789757,4.6768293896272,134.432030017952));
#161687=CARTESIAN_POINT('Ctrl Pts',(-204.010125569059,4.77164664501153,
134.306360982011));
#161688=CARTESIAN_POINT('Ctrl Pts',(-204.017538348361,4.8612164216961,134.177268185812));
#161689=CARTESIAN_POINT('Ctrl Pts',(-204.02496171939,4.95091417987762,134.047990935772));
#161690=CARTESIAN_POINT('Ctrl Pts',(-204.032385090419,5.03534928462894,
133.915280469116));
#161691=CARTESIAN_POINT('Ctrl Pts',(-204.039808461447,5.11427343323228,
133.779614860926));
#161692=CARTESIAN_POINT('Ctrl Pts',(-204.043744510888,5.15612091057836,
133.707681700217));
#161693=CARTESIAN_POINT('Ctrl Pts',(-204.047680560328,5.19641984998835,
133.634918111469));
#161694=CARTESIAN_POINT('Ctrl Pts',(-204.051616609769,5.23513874963715,
133.561397584048));
#161695=CARTESIAN_POINT('Ctrl Pts',(-204.059039876174,5.30816138600291,
133.422740163822));
#161696=CARTESIAN_POINT('Ctrl Pts',(-204.06646314258,5.3757819339304,133.280969967167));
#161697=CARTESIAN_POINT('Ctrl Pts',(-204.073886408985,5.437723476843,133.136547134955));
#161698=CARTESIAN_POINT('Ctrl Pts',(-204.081300901706,5.49959180999563,
132.992294998537));
#161699=CARTESIAN_POINT('Ctrl Pts',(-204.088715394427,5.5557943529252,132.845396806912));
#161700=CARTESIAN_POINT('Ctrl Pts',(-204.096129887148,5.60609946214324,
132.696338255663));
#161701=CARTESIAN_POINT('Ctrl Pts',(-204.103537233502,5.65635608540307,
132.547423372657));
#161702=CARTESIAN_POINT('Ctrl Pts',(-204.110944579855,5.70072647244532,
132.396352626674));
#161703=CARTESIAN_POINT('Ctrl Pts',(-204.118351926209,5.73902663486398,
132.243632602572));
#161704=CARTESIAN_POINT('Ctrl Pts',(-204.125753747884,5.77729823157674,
132.091026482824));
#161705=CARTESIAN_POINT('Ctrl Pts',(-204.13315556956,5.80950852791993,131.936773894766));
#161706=CARTESIAN_POINT('Ctrl Pts',(-204.140557391235,5.83552308162863,
131.781397426637));
#161707=CARTESIAN_POINT('Ctrl Pts',(-204.147955305546,5.86152390245685,
131.626102980537));
#161708=CARTESIAN_POINT('Ctrl Pts',(-204.155353219858,5.88133543288823,
131.469686203167));
#161709=CARTESIAN_POINT('Ctrl Pts',(-204.162751134169,5.89487415689882,
131.312680631756));
#161710=CARTESIAN_POINT('Ctrl Pts',(-204.170147819081,5.90841063101912,
131.155701151823));
#161711=CARTESIAN_POINT('Ctrl Pts',(-204.177544503993,5.9156763355876,130.998133443599));
#161712=CARTESIAN_POINT('Ctrl Pts',(-204.184941188905,5.91663952547246,
130.840517057061));
#161713=CARTESIAN_POINT('Ctrl Pts',(-204.192337545841,5.91760267264848,
130.682907659399));
#161714=CARTESIAN_POINT('Ctrl Pts',(-204.199733902776,5.91226385852082,
130.525249961006));
#161715=CARTESIAN_POINT('Ctrl Pts',(-204.207130259712,5.90064347312982,
130.368084139275));
#161716=CARTESIAN_POINT('Ctrl Pts',(-204.214527749048,5.8890213086282,130.210894255055));
#161717=CARTESIAN_POINT('Ctrl Pts',(-204.221925238385,5.87111568546889,
130.054196769752));
#161718=CARTESIAN_POINT('Ctrl Pts',(-204.229322727721,5.84699892344906,
129.898527215838));
#161719=CARTESIAN_POINT('Ctrl Pts',(-204.236722810236,5.82287370733566,
129.742803092204));
#161720=CARTESIAN_POINT('Ctrl Pts',(-204.244122892751,5.79253307447818,
129.58810798606));
#161721=CARTESIAN_POINT('Ctrl Pts',(-204.251522975266,5.75610052241988,
129.434967562853));
#161722=CARTESIAN_POINT('Ctrl Pts',(-204.258931194933,5.71962790902519,
129.281658746007));
#161723=CARTESIAN_POINT('Ctrl Pts',(-204.266339414599,5.67705008515344,
129.129908389533));
#161724=CARTESIAN_POINT('Ctrl Pts',(-204.273747634265,5.62854073617138,
128.980228017189));
#161725=CARTESIAN_POINT('Ctrl Pts',(-204.281160413567,5.58000153049444,
128.830455519072));
#161726=CARTESIAN_POINT('Ctrl Pts',(-204.288573192869,5.52552365400217,
128.682755893192));
#161727=CARTESIAN_POINT('Ctrl Pts',(-204.295985972171,5.46532888062469,
128.537620493708));
#161728=CARTESIAN_POINT('Ctrl Pts',(-204.3034093432,5.40504809813207,128.392277717958));
#161729=CARTESIAN_POINT('Ctrl Pts',(-204.310832714229,5.33903426053937,
128.249506824144));
#161730=CARTESIAN_POINT('Ctrl Pts',(-204.318256085258,5.26755537227114,
128.109775127633));
#161731=CARTESIAN_POINT('Ctrl Pts',(-204.322192134699,5.22965555059476,
128.035686029319));
#161732=CARTESIAN_POINT('Ctrl Pts',(-204.32612818414,5.19022004371018,127.962450893188));
#161733=CARTESIAN_POINT('Ctrl Pts',(-204.330064233581,5.14929365279669,
127.890135945416));
#161734=CARTESIAN_POINT('Ctrl Pts',(-204.337487499987,5.07210775681115,
127.753752210805));
#161735=CARTESIAN_POINT('Ctrl Pts',(-204.344910766392,4.98938303310252,
127.620230874498));
#161736=CARTESIAN_POINT('Ctrl Pts',(-204.352334032798,4.90135693104575,
127.490053631635));
#161737=CARTESIAN_POINT('Ctrl Pts',(-204.359748525519,4.81343486853123,
127.360030247463));
#161738=CARTESIAN_POINT('Ctrl Pts',(-204.367163018239,4.72022410681939,
127.233343395595));
#161739=CARTESIAN_POINT('Ctrl Pts',(-204.374577510961,4.62200806639798,
127.110450494586));
#161740=CARTESIAN_POINT('Ctrl Pts',(-204.381984857314,4.52388669029411,
126.987676042383));
#161741=CARTESIAN_POINT('Ctrl Pts',(-204.389392203668,4.42076987115514,
126.868688550817));
#161742=CARTESIAN_POINT('Ctrl Pts',(-204.396799550022,4.31298436294144,
126.753916636035));
#161743=CARTESIAN_POINT('Ctrl Pts',(-204.404201371697,4.20527924522689,
126.639230322478));
#161744=CARTESIAN_POINT('Ctrl Pts',(-204.411603193373,4.09291262618729,
126.528753596247));
#161745=CARTESIAN_POINT('Ctrl Pts',(-204.419005015048,3.97625150478076,
126.422882039137));
#161746=CARTESIAN_POINT('Ctrl Pts',(-204.42640292936,3.85965196787114,126.317066370797));
#161747=CARTESIAN_POINT('Ctrl Pts',(-204.433800843671,3.73876271923734,
126.215851280293));
#161748=CARTESIAN_POINT('Ctrl Pts',(-204.441198757982,3.61398749640891,
126.119595421924));
#161749=CARTESIAN_POINT('Ctrl Pts',(-204.448595442894,3.48923300895941,
126.023355559533));
#161750=CARTESIAN_POINT('Ctrl Pts',(-204.455992127807,3.36059412427482,
125.932073521404));
#161751=CARTESIAN_POINT('Ctrl Pts',(-204.463388812719,3.22850762201203,
125.846067655557));
#161752=CARTESIAN_POINT('Ctrl Pts',(-204.470785169654,3.0964269766028,125.7600656033));
#161753=CARTESIAN_POINT('Ctrl Pts',(-204.47818152659,2.9608993304014,125.679339461843));
#161754=CARTESIAN_POINT('Ctrl Pts',(-204.485577883525,2.82239017126325,
125.604164055545));
#161755=CARTESIAN_POINT('Ctrl Pts',(-204.492975372862,2.68385980601923,
125.5289771397));
#161756=CARTESIAN_POINT('Ctrl Pts',(-204.500372862198,2.54234734704194,
125.459342829222));
#161757=CARTESIAN_POINT('Ctrl Pts',(-204.507770351535,2.39834244358581,
125.395489747801));
#161758=CARTESIAN_POINT('Ctrl Pts',(-204.51517043405,2.25428705943503,125.331614282781));
#161759=CARTESIAN_POINT('Ctrl Pts',(-204.522570516565,2.1077378322723,125.273524232987));
#161760=CARTESIAN_POINT('Ctrl Pts',(-204.52997059908,1.95920377276374,125.221399831452));
#161761=CARTESIAN_POINT('Ctrl Pts',(-204.537378818746,1.81050638478601,
125.169218113778));
#161762=CARTESIAN_POINT('Ctrl Pts',(-204.544787038413,1.65982015826697,
125.123015268486));
#161763=CARTESIAN_POINT('Ctrl Pts',(-204.552195258079,1.5076693338124,125.082921660242));
#161764=CARTESIAN_POINT('Ctrl Pts',(-204.559608037382,1.35542486306415,
125.042803375052));
#161765=CARTESIAN_POINT('Ctrl Pts',(-204.567020816684,1.2017143617988,125.008801899886));
#161766=CARTESIAN_POINT('Ctrl Pts',(-204.574433595986,1.04707109441425,
124.980996238984));
#161767=CARTESIAN_POINT('Ctrl Pts',(-204.581856967014,0.89220686547698,
124.953150848049));
#161768=CARTESIAN_POINT('Ctrl Pts',(-204.589280338043,0.73640757733136,
124.931519003745));
#161769=CARTESIAN_POINT('Ctrl Pts',(-204.596703709072,0.580211258570826,
124.916127821733));
#161770=CARTESIAN_POINT('Ctrl Pts',(-204.600639758513,0.497392222485452,
124.907967047723));
#161771=CARTESIAN_POINT('Ctrl Pts',(-204.604575807954,0.414461573604239,
124.901559876592));
#161772=CARTESIAN_POINT('Ctrl Pts',(-204.608511857394,0.331499246015727,
124.896904412702));
#161773=CARTESIAN_POINT('Ctrl Pts',(-204.6159351238,0.175034885349205,124.888124353097));
#161774=CARTESIAN_POINT('Ctrl Pts',(-204.623358390205,0.017984869765548,
124.885551462325));
#161775=CARTESIAN_POINT('Ctrl Pts',(-204.630781656611,-0.139117189784255,
124.889246335491));
#161776=CARTESIAN_POINT('Ctrl Pts',(-204.638196149331,-0.296033567746183,
124.892936841624));
#161777=CARTESIAN_POINT('Ctrl Pts',(-204.645610642053,-0.453001497684593,
124.902880357385));
#161778=CARTESIAN_POINT('Ctrl Pts',(-204.653025134774,-0.609482944717867,
124.919085678993));
#161779=CARTESIAN_POINT('Ctrl Pts',(-204.660432481127,-0.765813569041512,
124.935275381302));
#161780=CARTESIAN_POINT('Ctrl Pts',(-204.667839827481,-0.92165827510939,
124.957714836041));
#161781=CARTESIAN_POINT('Ctrl Pts',(-204.675247173835,-1.07647983752149,
124.986360813346));
#161782=CARTESIAN_POINT('Ctrl Pts',(-204.68264899551,-1.23118592817213,
125.0149854254));
#161783=CARTESIAN_POINT('Ctrl Pts',(-204.690050817186,-1.38487002911259,
125.049807275314));
#161784=CARTESIAN_POINT('Ctrl Pts',(-204.697452638861,-1.53700095427533,
125.090731418094));
#161785=CARTESIAN_POINT('Ctrl Pts',(-204.704850553172,-1.689051570706,125.131633957337));
#161786=CARTESIAN_POINT('Ctrl Pts',(-204.712248467484,-1.83955028467765,
125.17863227724));
#161787=CARTESIAN_POINT('Ctrl Pts',(-204.719646381795,-1.98797712017319,
125.231580563395));
#161788=CARTESIAN_POINT('Ctrl Pts',(-204.727043066707,-2.1363792898212,
125.284520050505));
#161789=CARTESIAN_POINT('Ctrl Pts',(-204.734439751619,-2.28270991309183,
125.343407416136));
#161790=CARTESIAN_POINT('Ctrl Pts',(-204.741836436532,-2.42646506470635,
125.408047260073));
#161791=CARTESIAN_POINT('Ctrl Pts',(-204.749232793467,-2.57021384206722,
125.472684237812));
#161792=CARTESIAN_POINT('Ctrl Pts',(-204.756629150402,-2.711387034376,125.5430730336));
#161793=CARTESIAN_POINT('Ctrl Pts',(-204.764025507338,-2.84950181656107,
125.6189705686));
#161794=CARTESIAN_POINT('Ctrl Pts',(-204.771422996674,-2.98763774447108,
125.694879723706));
#161795=CARTESIAN_POINT('Ctrl Pts',(-204.778820486011,-3.12271400273242,
125.776299117558));
#161796=CARTESIAN_POINT('Ctrl Pts',(-204.786217975348,-3.25427357637751,
125.862940371059));
#161797=CARTESIAN_POINT('Ctrl Pts',(-204.793618057863,-3.38587926802739,
125.949611996517));
#161798=CARTESIAN_POINT('Ctrl Pts',(-204.801018140377,-3.5139655090601,
126.041508920977));
#161799=CARTESIAN_POINT('Ctrl Pts',(-204.808418222892,-3.63810553162232,
126.138300319705));
#161800=CARTESIAN_POINT('Ctrl Pts',(-204.815826442559,-3.76238205890143,
126.235198150526));
#161801=CARTESIAN_POINT('Ctrl Pts',(-204.823234662225,-3.88270340732681,
126.337000974104));
#161802=CARTESIAN_POINT('Ctrl Pts',(-204.830642881892,-3.99867653255975,
126.443338197255));
#161803=CARTESIAN_POINT('Ctrl Pts',(-204.838055661194,-4.11472103731682,
126.549740869193));
#161804=CARTESIAN_POINT('Ctrl Pts',(-204.845468440496,-4.22641172186707,
126.660683239356));
#161805=CARTESIAN_POINT('Ctrl Pts',(-204.852881219798,-4.33339387527508,
126.775759361022));
#161806=CARTESIAN_POINT('Ctrl Pts',(-204.860304590827,-4.44052888980039,
126.890999908847));
#161807=CARTESIAN_POINT('Ctrl Pts',(-204.867727961855,-4.54294169391004,
127.010385722194));
#161808=CARTESIAN_POINT('Ctrl Pts',(-204.875151332884,-4.64031865683491,
127.133478799047));
#161809=CARTESIAN_POINT('Ctrl Pts',(-204.879087382325,-4.69195025910903,
127.198745701977));
#161810=CARTESIAN_POINT('Ctrl Pts',(-204.883023431766,-4.74216683506,127.265054373102));
#161811=CARTESIAN_POINT('Ctrl Pts',(-204.886959481207,-4.79092677321238,
127.332336536973));
#161812=CARTESIAN_POINT('Ctrl Pts',(-204.894439644792,-4.88359133935193,
127.460201188986));
#161813=CARTESIAN_POINT('Ctrl Pts',(-204.901919808376,-4.97127200205635,
127.591969048914));
#161814=CARTESIAN_POINT('Ctrl Pts',(-204.909399971961,-5.05362495660158,
127.727218215838));
#161815=CARTESIAN_POINT('Ctrl Pts',(-204.916871063548,-5.13587803287105,
127.862303351566));
#161816=CARTESIAN_POINT('Ctrl Pts',(-204.924342155134,-5.21281607482848,
128.000861080831));
#161817=CARTESIAN_POINT('Ctrl Pts',(-204.931813246721,-5.28413634723124,
128.142437698628));
#161818=CARTESIAN_POINT('Ctrl Pts',(-204.939276676359,-5.35538347741398,
128.28386912309));
#161819=CARTESIAN_POINT('Ctrl Pts',(-204.946740105998,-5.42102414483629,
128.428312948119));
#161820=CARTESIAN_POINT('Ctrl Pts',(-204.954203535636,-5.48079969101944,
128.575287871014));
#161821=CARTESIAN_POINT('Ctrl Pts',(-204.961660708341,-5.5405251246347,
128.722139578124));
#161822=CARTESIAN_POINT('Ctrl Pts',(-204.969117881046,-5.59439509099741,
128.871517820658));
#161823=CARTESIAN_POINT('Ctrl Pts',(-204.976575053751,-5.64219757205847,
129.022918190667));
#161824=CARTESIAN_POINT('Ctrl Pts',(-204.984026968987,-5.68996635133299,
129.174211820128));
#161825=CARTESIAN_POINT('Ctrl Pts',(-204.991478884223,-5.73167605837681,
129.327524388969));
#161826=CARTESIAN_POINT('Ctrl Pts',(-204.99893079946,-5.76716343358339,
129.482333199984));
#161827=CARTESIAN_POINT('Ctrl Pts',(-205.006379560772,-5.80263578923023,
129.637076490228));
#161828=CARTESIAN_POINT('Ctrl Pts',(-205.013828322084,-5.83189097662629,
129.793314405558));
#161829=CARTESIAN_POINT('Ctrl Pts',(-205.021277083396,-5.85481604611657,
129.95051073109));
#161830=CARTESIAN_POINT('Ctrl Pts',(-205.028725022292,-5.87773858445527,
130.107689700612));
#161831=CARTESIAN_POINT('Ctrl Pts',(-205.036172961189,-5.89433233816279,
130.265826508781));
#161832=CARTESIAN_POINT('Ctrl Pts',(-205.043620900085,-5.90453575298649,
130.424376270251));
#161833=CARTESIAN_POINT('Ctrl Pts',(-205.049622202654,-5.91275732682686,
130.552130418624));
#161834=CARTESIAN_POINT('Ctrl Pts',(-205.055623505223,-5.91683088167834,
130.680152436099));
#161835=CARTESIAN_POINT('Ctrl Pts',(-205.061624807792,-5.91674878301709,
130.808155504365));
#161836=CARTESIAN_POINT('',(-206.811623442643,-5.92115820836986,130.807369057892));
#161837=CARTESIAN_POINT('Ctrl Pts',(-205.061626944303,-5.90947417380247,
130.808196352657));
#161838=CARTESIAN_POINT('Ctrl Pts',(-205.096220331209,-5.91377200472859,
131.545141902329));
#161839=CARTESIAN_POINT('Ctrl Pts',(-205.223629592719,-5.44370849995411,
134.254054771831));
#161840=CARTESIAN_POINT('Ctrl Pts',(-205.443854728833,-1.37967370610466,
137.665414544981));
#161841=CARTESIAN_POINT('Ctrl Pts',(-205.722302352646,5.0266516457322,135.673686419238));
#161842=CARTESIAN_POINT('Ctrl Pts',(-206.000749976459,6.813729700728,129.207285761534));
#161843=CARTESIAN_POINT('Ctrl Pts',(-206.279197600272,2.3393230299546,124.208518875085));
#161844=CARTESIAN_POINT('Ctrl Pts',(-206.549488398635,-4.09076040919075,
125.239883832662));
#161845=CARTESIAN_POINT('Ctrl Pts',(-206.726963322394,-5.91340440505827,
129.015638925646));
#161846=CARTESIAN_POINT('Ctrl Pts',(-206.811622371547,-5.92461749863669,
130.807348163968));
#161847=CARTESIAN_POINT('',(-208.561625524649,-5.9182976546993,130.799113135042));
#161848=CARTESIAN_POINT('Ctrl Pts',(-206.811624807792,-5.91674922156144,
130.807395687932));
#161849=CARTESIAN_POINT('Ctrl Pts',(-206.819780821161,-5.91666079577132,
130.979778256311));
#161850=CARTESIAN_POINT('Ctrl Pts',(-206.827936834529,-5.90903961803116,
131.151962513016));
#161851=CARTESIAN_POINT('Ctrl Pts',(-206.836092847897,-5.89393313865187,
131.323477867907));
#161852=CARTESIAN_POINT('Ctrl Pts',(-206.843516114303,-5.88018384523864,
131.479584057844));
#161853=CARTESIAN_POINT('Ctrl Pts',(-206.850939380708,-5.86020755555771,
131.635379677207));
#161854=CARTESIAN_POINT('Ctrl Pts',(-206.858362647114,-5.83402082614694,
131.79032794085));
#161855=CARTESIAN_POINT('Ctrl Pts',(-206.865777139835,-5.80786504727567,
131.945093068512));
#161856=CARTESIAN_POINT('Ctrl Pts',(-206.873191632556,-5.77551350102985,
132.099012469469));
#161857=CARTESIAN_POINT('Ctrl Pts',(-206.880606125277,-5.73703464184265,
132.251552408863));
#161858=CARTESIAN_POINT('Ctrl Pts',(-206.888013471631,-5.69859287002863,
132.40394532452));
#161859=CARTESIAN_POINT('Ctrl Pts',(-206.895420817985,-5.6540356331216,
132.554961066011));
#161860=CARTESIAN_POINT('Ctrl Pts',(-206.902828164338,-5.60348275777306,
132.704074160667));
#161861=CARTESIAN_POINT('Ctrl Pts',(-206.910229986014,-5.55296758666621,
132.853076041151));
#161862=CARTESIAN_POINT('Ctrl Pts',(-206.917631807689,-5.49646580036238,
133.00017774834));
#161863=CARTESIAN_POINT('Ctrl Pts',(-206.925033629365,-5.43414753997931,
133.144867202952));
#161864=CARTESIAN_POINT('Ctrl Pts',(-206.932431543676,-5.37186217692081,
133.289480277128));
#161865=CARTESIAN_POINT('Ctrl Pts',(-206.939829457987,-5.30376660206674,
133.431683292801));
#161866=CARTESIAN_POINT('Ctrl Pts',(-206.947227372299,-5.23007969249045,
133.570982560062));
#161867=CARTESIAN_POINT('Ctrl Pts',(-206.954624057211,-5.15640502834161,
133.710258678312));
#161868=CARTESIAN_POINT('Ctrl Pts',(-206.962020742123,-5.07714104799469,
133.846631676217));
#161869=CARTESIAN_POINT('Ctrl Pts',(-206.969417427036,-4.99255339993645,
133.97963085981));
#161870=CARTESIAN_POINT('Ctrl Pts',(-206.976813783971,-4.90796950258341,
134.11262414608));
#161871=CARTESIAN_POINT('Ctrl Pts',(-206.984210140907,-4.81806260721323,
134.242243600501));
#161872=CARTESIAN_POINT('Ctrl Pts',(-206.991606497842,-4.72314252211075,
134.368046248809));
#161873=CARTESIAN_POINT('Ctrl Pts',(-206.999003987179,-4.62820790450037,
134.493868157825));
#161874=CARTESIAN_POINT('Ctrl Pts',(-207.006401476515,-4.52825879375254,
134.615871799175));
#161875=CARTESIAN_POINT('Ctrl Pts',(-207.013798965852,-4.4236461287228,
134.733646238431));
#161876=CARTESIAN_POINT('Ctrl Pts',(-207.021199048367,-4.31899679188596,
134.851461963334));
#161877=CARTESIAN_POINT('Ctrl Pts',(-207.028599130882,-4.20968089363974,
134.965045255495));
#161878=CARTESIAN_POINT('Ctrl Pts',(-207.035999213397,-4.09608704198211,
135.074021202086));
#161879=CARTESIAN_POINT('Ctrl Pts',(-207.043407433063,-3.98236828220669,
135.183116978934));
#161880=CARTESIAN_POINT('Ctrl Pts',(-207.05081565273,-3.86436244426953,
135.287595033992));
#161881=CARTESIAN_POINT('Ctrl Pts',(-207.058223872396,-3.74249265724638,
135.38711953256));
#161882=CARTESIAN_POINT('Ctrl Pts',(-207.065636651698,-3.62054786140282,
135.486705286797));
#161883=CARTESIAN_POINT('Ctrl Pts',(-207.073049431,-3.49473467526279,135.581331185504));
#161884=CARTESIAN_POINT('Ctrl Pts',(-207.080462210303,-3.36550571859837,
135.670704401207));
#161885=CARTESIAN_POINT('Ctrl Pts',(-207.087885581331,-3.23609211354025,
135.760205317552));
#161886=CARTESIAN_POINT('Ctrl Pts',(-207.09530895236,-3.10325330470338,
135.84443836179));
#161887=CARTESIAN_POINT('Ctrl Pts',(-207.102732323389,-2.96746774449341,
135.92315595904));
#161888=CARTESIAN_POINT('Ctrl Pts',(-207.106668372829,-2.89547098234766,
135.9648939179));
#161889=CARTESIAN_POINT('Ctrl Pts',(-207.11060442227,-2.82264614973579,
136.005082076847));
#161890=CARTESIAN_POINT('Ctrl Pts',(-207.11454047171,-2.74906678387943,
136.043689045931));
#161891=CARTESIAN_POINT('Ctrl Pts',(-207.121963738116,-2.61029839619412,
136.116500584748));
#161892=CARTESIAN_POINT('Ctrl Pts',(-207.129387004521,-2.46842545674248,
136.183905304267));
#161893=CARTESIAN_POINT('Ctrl Pts',(-207.136810270927,-2.32390852728499,
136.245626988487));
#161894=CARTESIAN_POINT('Ctrl Pts',(-207.144224763648,-2.17956240483674,
136.307275722802));
#161895=CARTESIAN_POINT('Ctrl Pts',(-207.151639256369,-2.0325788526123,
136.363254646609));
#161896=CARTESIAN_POINT('Ctrl Pts',(-207.15905374909,-1.88344391815646,
136.413332855834));
#161897=CARTESIAN_POINT('Ctrl Pts',(-207.166461095443,-1.73445272556529,
136.463362797795));
#161898=CARTESIAN_POINT('Ctrl Pts',(-207.173868441797,-1.58331463034264,
136.507503229499));
#161899=CARTESIAN_POINT('Ctrl Pts',(-207.181275788151,-1.4305364967586,
136.545570933688));
#161900=CARTESIAN_POINT('Ctrl Pts',(-207.188677609826,-1.27787231087058,
136.583610245546));
#161901=CARTESIAN_POINT('Ctrl Pts',(-207.196079431502,-1.12357088284622,
136.61558575841));
#161902=CARTESIAN_POINT('Ctrl Pts',(-207.203481253177,-0.96815500491798,
136.641363825459));
#161903=CARTESIAN_POINT('Ctrl Pts',(-207.210879167489,-0.812821169821938,
136.667128284467));
#161904=CARTESIAN_POINT('Ctrl Pts',(-207.2182770818,-0.656374423802763,
136.686701752249));
#161905=CARTESIAN_POINT('Ctrl Pts',(-207.225674996111,-0.499348430567841,
136.700001524829));
#161906=CARTESIAN_POINT('Ctrl Pts',(-207.233071681024,-0.342348532204476,
136.713299087228));
#161907=CARTESIAN_POINT('Ctrl Pts',(-207.240468365936,-0.184769949275625,
136.720324992153));
#161908=CARTESIAN_POINT('Ctrl Pts',(-207.247865050848,-0.027152279443601,
136.721048315613));
#161909=CARTESIAN_POINT('Ctrl Pts',(-207.255261407783,0.130458401455771,
136.721771607));
#161910=CARTESIAN_POINT('Ctrl Pts',(-207.262657764719,0.288107792518586,
136.716192870875));
#161911=CARTESIAN_POINT('Ctrl Pts',(-207.270054121654,0.445255748006126,
136.704333319314));
#161912=CARTESIAN_POINT('Ctrl Pts',(-207.277451610991,0.602427763247279,
136.692471952024));
#161913=CARTESIAN_POINT('Ctrl Pts',(-207.284849100328,0.759097817788442,
136.674327882701));
#161914=CARTESIAN_POINT('Ctrl Pts',(-207.292246589664,0.914730489834055,
136.649974246046));
#161915=CARTESIAN_POINT('Ctrl Pts',(-207.299646672179,1.07041771867137,
136.625612072261));
#161916=CARTESIAN_POINT('Ctrl Pts',(-207.307046754694,1.22506647240331,
136.595036054919));
#161917=CARTESIAN_POINT('Ctrl Pts',(-207.314446837209,1.37815127413479,
136.558370491393));
#161918=CARTESIAN_POINT('Ctrl Pts',(-207.321855056876,1.53140440834349,
136.521664610311));
#161919=CARTESIAN_POINT('Ctrl Pts',(-207.329263276542,1.68308979289289,
136.478855897533));
#161920=CARTESIAN_POINT('Ctrl Pts',(-207.336671496209,1.83269616893944,
136.430118816676));
#161921=CARTESIAN_POINT('Ctrl Pts',(-207.344084275511,1.98239462521413,
136.38135173896));
#161922=CARTESIAN_POINT('Ctrl Pts',(-207.351497054813,2.13001117400739,
136.326649151863));
#161923=CARTESIAN_POINT('Ctrl Pts',(-207.358909834115,2.27505479922936,
136.266233576818));
#161924=CARTESIAN_POINT('Ctrl Pts',(-207.366333205144,2.42030566958471,
136.205731677165));
#161925=CARTESIAN_POINT('Ctrl Pts',(-207.373756576173,2.56297593624992,
136.139500643018));
#161926=CARTESIAN_POINT('Ctrl Pts',(-207.381179947201,2.7025986922535,136.067809189665));
#161927=CARTESIAN_POINT('Ctrl Pts',(-207.385115996642,2.77663002768745,
136.029796660885));
#161928=CARTESIAN_POINT('Ctrl Pts',(-207.389052046083,2.84980506487561,
135.99024974826));
#161929=CARTESIAN_POINT('Ctrl Pts',(-207.392988095523,2.92205764589925,
135.949213353704));
#161930=CARTESIAN_POINT('Ctrl Pts',(-207.400411361929,3.05832375878637,
135.87181999427));
#161931=CARTESIAN_POINT('Ctrl Pts',(-207.407834628334,3.19171904753105,
135.788892169611));
#161932=CARTESIAN_POINT('Ctrl Pts',(-207.41525789474,3.32176217890836,135.700668061883));
#161933=CARTESIAN_POINT('Ctrl Pts',(-207.422672387461,3.4516516101038,135.612548227724));
#161934=CARTESIAN_POINT('Ctrl Pts',(-207.430086880182,3.57819646435842,
135.519144778126));
#161935=CARTESIAN_POINT('Ctrl Pts',(-207.437501372903,3.70093975496472,
135.420741829362));
#161936=CARTESIAN_POINT('Ctrl Pts',(-207.444908719256,3.82356474096634,
135.322433725065));
#161937=CARTESIAN_POINT('Ctrl Pts',(-207.45231606561,3.94239516850163,135.219135946626));
#161938=CARTESIAN_POINT('Ctrl Pts',(-207.459723411964,4.05700291918446,
135.11117589991));
#161939=CARTESIAN_POINT('Ctrl Pts',(-207.46712523364,4.17152519108292,135.003296373869));
#161940=CARTESIAN_POINT('Ctrl Pts',(-207.474527055315,4.28183078651756,
134.890761758177));
#161941=CARTESIAN_POINT('Ctrl Pts',(-207.48192887699,4.387524682663,134.773939653374));
#161942=CARTESIAN_POINT('Ctrl Pts',(-207.489326791302,4.49316278382338,
134.65717921805));
#161943=CARTESIAN_POINT('Ctrl Pts',(-207.496724705613,4.59419378426487,
134.536136077267));
#161944=CARTESIAN_POINT('Ctrl Pts',(-207.504122619924,4.69025964452218,
134.411214513895));
#161945=CARTESIAN_POINT('Ctrl Pts',(-207.511519304837,4.7863095403762,134.286313710222));
#161946=CARTESIAN_POINT('Ctrl Pts',(-207.518915989749,4.8773957063178,134.157536058776));
#161947=CARTESIAN_POINT('Ctrl Pts',(-207.526312674661,4.96320045939997,
134.02531882318));
#161948=CARTESIAN_POINT('Ctrl Pts',(-207.533709031597,5.04900140780948,
133.893107450235));
#161949=CARTESIAN_POINT('Ctrl Pts',(-207.541105388532,5.12952120577963,
133.757457109527));
#161950=CARTESIAN_POINT('Ctrl Pts',(-207.548501745467,5.20448573766415,
133.61883370661));
#161951=CARTESIAN_POINT('Ctrl Pts',(-207.555899234804,5.27946174681009,
133.480189080095));
#161952=CARTESIAN_POINT('Ctrl Pts',(-207.563296724141,5.34888061877977,
133.33857081342));
#161953=CARTESIAN_POINT('Ctrl Pts',(-207.570694213477,5.41251447531095,
133.194468903199));
#161954=CARTESIAN_POINT('Ctrl Pts',(-207.578094295992,5.4761706385918,133.050316478276));
#161955=CARTESIAN_POINT('Ctrl Pts',(-207.585494378507,5.53403759814204,
132.903679017647));
#161956=CARTESIAN_POINT('Ctrl Pts',(-207.592894461022,5.58593589576508,
132.755065805672));
#161957=CARTESIAN_POINT('Ctrl Pts',(-207.600302680689,5.6378912609017,132.606289178192));
#161958=CARTESIAN_POINT('Ctrl Pts',(-207.607710900355,5.68386473390605,
132.455532813299));
#161959=CARTESIAN_POINT('Ctrl Pts',(-207.615119120022,5.72372674806762,
132.303321149386));
#161960=CARTESIAN_POINT('Ctrl Pts',(-207.622531899324,5.76361329663376,
132.151015801734));
#161961=CARTESIAN_POINT('Ctrl Pts',(-207.629944678626,5.79738081120918,
131.997253734006));
#161962=CARTESIAN_POINT('Ctrl Pts',(-207.637357457928,5.82495109918533,
131.842568330213));
#161963=CARTESIAN_POINT('Ctrl Pts',(-207.644780828957,5.85256078088182,
131.687661904661));
#161964=CARTESIAN_POINT('Ctrl Pts',(-207.652204199985,5.87395550014103,
131.531829876945));
#161965=CARTESIAN_POINT('Ctrl Pts',(-207.659627571014,5.88910896012277,
131.375610316298));
#161966=CARTESIAN_POINT('Ctrl Pts',(-207.663563620455,5.89714368820723,
131.292778956808));
#161967=CARTESIAN_POINT('Ctrl Pts',(-207.667499669896,5.90342464558926,
131.209838653336));
#161968=CARTESIAN_POINT('Ctrl Pts',(-207.671435719336,5.90795384954832,
131.126869336994));
#161969=CARTESIAN_POINT('Ctrl Pts',(-207.678858985742,5.91649578686362,
130.970391795754));
#161970=CARTESIAN_POINT('Ctrl Pts',(-207.686282252147,5.9188296712671,130.81333804653));
#161971=CARTESIAN_POINT('Ctrl Pts',(-207.693705518553,5.91489571978865,
130.656241791869));
#161972=CARTESIAN_POINT('Ctrl Pts',(-207.701120011274,5.91096641791416,
130.499331211935));
#161973=CARTESIAN_POINT('Ctrl Pts',(-207.708534503995,5.90078403519882,
130.342378596101));
#161974=CARTESIAN_POINT('Ctrl Pts',(-207.715948996716,5.88434059423159,
130.185921992011));
#161975=CARTESIAN_POINT('Ctrl Pts',(-207.723356343069,5.86791300207183,
130.029616186687));
#161976=CARTESIAN_POINT('Ctrl Pts',(-207.730763689423,5.84523640420407,
129.873805810115));
#161977=CARTESIAN_POINT('Ctrl Pts',(-207.738171035777,5.8163548480082,129.719028021284));
#161978=CARTESIAN_POINT('Ctrl Pts',(-207.745572857452,5.78749483276658,
129.564365671568));
#161979=CARTESIAN_POINT('Ctrl Pts',(-207.752974679128,5.75243914213516,
129.41073474152));
#161980=CARTESIAN_POINT('Ctrl Pts',(-207.760376500803,5.71128352937423,
129.258666272102));
#161981=CARTESIAN_POINT('Ctrl Pts',(-207.767774415114,5.67014964234093,
129.106678078445));
#161982=CARTESIAN_POINT('Ctrl Pts',(-207.775172329426,5.622922343438,128.956251062191));
#161983=CARTESIAN_POINT('Ctrl Pts',(-207.782570243737,5.5697482382197,128.80790497685));
#161984=CARTESIAN_POINT('Ctrl Pts',(-207.789966928649,5.51658296957293,
128.659583543936));
#161985=CARTESIAN_POINT('Ctrl Pts',(-207.797363613561,5.45747298183366,
128.513342706659));
#161986=CARTESIAN_POINT('Ctrl Pts',(-207.804760298474,5.39261444187882,
128.369686092349));
#161987=CARTESIAN_POINT('Ctrl Pts',(-207.812156655409,5.32775877781979,
128.226035847924));
#161988=CARTESIAN_POINT('Ctrl Pts',(-207.819553012344,5.25715522197387,
128.084969938857));
#161989=CARTESIAN_POINT('Ctrl Pts',(-207.82694936928,5.18104758767484,127.946970819735));
#161990=CARTESIAN_POINT('Ctrl Pts',(-207.834346858616,5.1049283011025,127.808950572595));
#161991=CARTESIAN_POINT('Ctrl Pts',(-207.841744347953,5.0233034384614,127.673998377207));
#161992=CARTESIAN_POINT('Ctrl Pts',(-207.84914183729,4.93646207401314,127.542570809143));
#161993=CARTESIAN_POINT('Ctrl Pts',(-207.856541919805,4.84959026745932,
127.41109716935));
#161994=CARTESIAN_POINT('Ctrl Pts',(-207.86394200232,4.75749852395979,127.283150928114));
#161995=CARTESIAN_POINT('Ctrl Pts',(-207.871342084835,4.6605183173321,127.159158349336));
#161996=CARTESIAN_POINT('Ctrl Pts',(-207.878750304501,4.56343147099727,
127.03502942797));
#161997=CARTESIAN_POINT('Ctrl Pts',(-207.886158524168,4.4614456566951,126.914863145442));
#161998=CARTESIAN_POINT('Ctrl Pts',(-207.893566743834,4.35493206532541,
126.799051981655));
#161999=CARTESIAN_POINT('Ctrl Pts',(-207.900979523136,4.24835291661749,
126.68316953803));
#162000=CARTESIAN_POINT('Ctrl Pts',(-207.908392302438,4.13724070071562,
126.571647818218));
#162001=CARTESIAN_POINT('Ctrl Pts',(-207.91580508174,4.02200190367991,126.464840914961));
#162002=CARTESIAN_POINT('Ctrl Pts',(-207.923228452769,3.90659844804667,
126.357881400993));
#162003=CARTESIAN_POINT('Ctrl Pts',(-207.930651823798,3.78705691809108,
126.25565040036));
#162004=CARTESIAN_POINT('Ctrl Pts',(-207.938075194826,3.66381579261569,
126.158460876904));
#162005=CARTESIAN_POINT('Ctrl Pts',(-207.942011244267,3.59847039075598,
126.106928659536));
#162006=CARTESIAN_POINT('Ctrl Pts',(-207.945947293708,3.53208537533614,
126.056813052246));
#162007=CARTESIAN_POINT('Ctrl Pts',(-207.949883343149,3.46472908505259,
126.008155562557));
#162008=CARTESIAN_POINT('Ctrl Pts',(-207.957306609555,3.33769722370025,
125.916389055557));
#162009=CARTESIAN_POINT('Ctrl Pts',(-207.96472987596,3.20682497801239,125.829534104802));
#162010=CARTESIAN_POINT('Ctrl Pts',(-207.972153142366,3.0725290529027,125.747929486663));
#162011=CARTESIAN_POINT('Ctrl Pts',(-207.979567635087,2.9383918544239,125.666421318405));
#162012=CARTESIAN_POINT('Ctrl Pts',(-207.986982127808,2.80083934701695,
125.590151322724));
#162013=CARTESIAN_POINT('Ctrl Pts',(-207.994396620529,2.66031989341828,
125.519417039137));
#162014=CARTESIAN_POINT('Ctrl Pts',(-208.001803966883,2.51993587775946,
125.448750931915));
#162015=CARTESIAN_POINT('Ctrl Pts',(-208.009211313236,2.37659094011565,
125.383610081518));
#162016=CARTESIAN_POINT('Ctrl Pts',(-208.01661865959,2.23076081624254,125.324247777193));
#162017=CARTESIAN_POINT('Ctrl Pts',(-208.024020481265,2.08503945797724,
125.264929747515));
#162018=CARTESIAN_POINT('Ctrl Pts',(-208.031422302941,1.93683694840379,
125.211381822536));
#162019=CARTESIAN_POINT('Ctrl Pts',(-208.038824124616,1.78665182429972,
125.16381048294));
#162020=CARTESIAN_POINT('Ctrl Pts',(-208.046222038928,1.63654598175406,
125.116264255884));
#162021=CARTESIAN_POINT('Ctrl Pts',(-208.053619953239,1.48445996401649,
125.074688443328));
#162022=CARTESIAN_POINT('Ctrl Pts',(-208.06101786755,1.33091029831849,125.039240641336));
#162023=CARTESIAN_POINT('Ctrl Pts',(-208.068414552463,1.17738614978904,
125.003798730125));
#162024=CARTESIAN_POINT('Ctrl Pts',(-208.075811237375,1.02239919941734,
124.974482892213));
#162025=CARTESIAN_POINT('Ctrl Pts',(-208.083207922287,0.866479196127633,
124.951400309724));
#162026=CARTESIAN_POINT('Ctrl Pts',(-208.090604279223,0.710566106494265,
124.928318750741));
#162027=CARTESIAN_POINT('Ctrl Pts',(-208.098000636158,0.553720415478458,
124.911469952293));
#162028=CARTESIAN_POINT('Ctrl Pts',(-208.105396993094,0.39647981285127,
124.900909565808));
#162029=CARTESIAN_POINT('Ctrl Pts',(-208.11279448243,0.239215136286403,
124.890347562501));
#162030=CARTESIAN_POINT('Ctrl Pts',(-208.120191971767,0.0815558002050929,
124.886075913179));
#162031=CARTESIAN_POINT('Ctrl Pts',(-208.127589461103,-0.0759578137315606,
124.88809820173));
#162032=CARTESIAN_POINT('Ctrl Pts',(-208.134989543618,-0.233526643821177,
124.890121199191));
#162033=CARTESIAN_POINT('Ctrl Pts',(-208.142389626133,-0.390949277026624,
124.898442522523));
#162034=CARTESIAN_POINT('Ctrl Pts',(-208.149789708648,-0.547687915761142,
124.913013699464));
#162035=CARTESIAN_POINT('Ctrl Pts',(-208.157197928315,-0.704598904742296,
124.927600898913));
#162036=CARTESIAN_POINT('Ctrl Pts',(-208.164606147981,-0.860824025291776,
124.948451641943));
#162037=CARTESIAN_POINT('Ctrl Pts',(-208.172014367648,-1.01583243520272,
124.975465780113));
#162038=CARTESIAN_POINT('Ctrl Pts',(-208.17942714695,-1.17093625020352,
125.002496545034));
#162039=CARTESIAN_POINT('Ctrl Pts',(-208.186839926252,-1.32482149830291,
125.035698185506));
#162040=CARTESIAN_POINT('Ctrl Pts',(-208.194252705554,-1.47697055560345,
125.074920109071));
#162041=CARTESIAN_POINT('Ctrl Pts',(-208.201676076583,-1.62933701061236,
125.11419807476));
#162042=CARTESIAN_POINT('Ctrl Pts',(-208.209099447612,-1.77996196368261,
125.159513396531));
#162043=CARTESIAN_POINT('Ctrl Pts',(-208.21652281864,-1.92834510096755,
125.210666334351));
#162044=CARTESIAN_POINT('Ctrl Pts',(-208.220458868081,-2.00702140075778,
125.23778884938));
#162045=CARTESIAN_POINT('Ctrl Pts',(-208.224394917522,-2.0850678028919,
125.26655173309));
#162046=CARTESIAN_POINT('Ctrl Pts',(-208.228330966962,-2.16241244718007,
125.296919926031));
#162047=CARTESIAN_POINT('Ctrl Pts',(-208.235754233368,-2.30828203246709,
125.35419339016));
#162048=CARTESIAN_POINT('Ctrl Pts',(-208.243177499773,-2.45209520792221,
125.417352694518));
#162049=CARTESIAN_POINT('Ctrl Pts',(-208.250600766178,-2.59334171220647,
125.486230370362));
#162050=CARTESIAN_POINT('Ctrl Pts',(-208.258015258899,-2.73442127485285,
125.555026638513));
#162051=CARTESIAN_POINT('Ctrl Pts',(-208.26542975162,-2.87293987245686,
125.629527663019));
#162052=CARTESIAN_POINT('Ctrl Pts',(-208.272844244341,-3.00840482558562,
125.709517050989));
#162053=CARTESIAN_POINT('Ctrl Pts',(-208.280251590695,-3.14373921249238,
125.789429342175));
#162054=CARTESIAN_POINT('Ctrl Pts',(-208.287658937049,-3.276025495006,125.87481927716));
#162055=CARTESIAN_POINT('Ctrl Pts',(-208.295066283402,-3.40479342691352,
125.965423515004));
#162056=CARTESIAN_POINT('Ctrl Pts',(-208.302468105078,-3.53346531883929,
126.05596017679));
#162057=CARTESIAN_POINT('Ctrl Pts',(-208.309869926753,-3.65862378115038,
126.151703183975));
#162058=CARTESIAN_POINT('Ctrl Pts',(-208.317271748428,-3.77982562449569,
126.252344711299));
#162059=CARTESIAN_POINT('Ctrl Pts',(-208.32466966274,-3.90096348633133,
126.352933110745));
#162060=CARTESIAN_POINT('Ctrl Pts',(-208.332067577051,-4.01814860241678,
126.458414642534));
#162061=CARTESIAN_POINT('Ctrl Pts',(-208.339465491362,-4.13096918713531,
126.568439922199));
#162062=CARTESIAN_POINT('Ctrl Pts',(-208.346862176274,-4.24377102311959,
126.678446917659));
#162063=CARTESIAN_POINT('Ctrl Pts',(-208.354258861187,-4.35220950026474,
126.792995901993));
#162064=CARTESIAN_POINT('Ctrl Pts',(-208.361655546099,-4.45590810098091,
126.911699116984));
#162065=CARTESIAN_POINT('Ctrl Pts',(-208.369051903034,-4.55960210359245,
127.03039706855));
#162066=CARTESIAN_POINT('Ctrl Pts',(-208.37644825997,-4.65855640207167,
127.153248603385));
#162067=CARTESIAN_POINT('Ctrl Pts',(-208.383844616905,-4.75243354084222,
127.279831428812));
#162068=CARTESIAN_POINT('Ctrl Pts',(-208.391242106241,-4.84632505244239,
127.406433634393));
#162069=CARTESIAN_POINT('Ctrl Pts',(-208.398639595578,-4.93513763419133,
127.536767968181));
#162070=CARTESIAN_POINT('Ctrl Pts',(-208.406037084914,-5.01857618137592,
127.67038172896));
#162071=CARTESIAN_POINT('Ctrl Pts',(-208.413437167429,-5.10204397781375,
127.804042327836));
#162072=CARTESIAN_POINT('Ctrl Pts',(-208.420837249944,-5.18013379133206,
127.940984326111));
#162073=CARTESIAN_POINT('Ctrl Pts',(-208.428237332459,-5.25259571028425,
128.080729059002));
#162074=CARTESIAN_POINT('Ctrl Pts',(-208.435645552125,-5.32513730856569,
128.220627455594));
#162075=CARTESIAN_POINT('Ctrl Pts',(-208.443053771792,-5.39203848159874,
128.363334409951));
#162076=CARTESIAN_POINT('Ctrl Pts',(-208.450461991458,-5.45309655392448,
128.508349176811));
#162077=CARTESIAN_POINT('Ctrl Pts',(-208.45787477076,-5.51419220647511,
128.653453197841));
#162078=CARTESIAN_POINT('Ctrl Pts',(-208.465287550062,-5.56943746148115,
128.800867512992));
#162079=CARTESIAN_POINT('Ctrl Pts',(-208.472700329364,-5.61867922828225,
128.950075231718));
#162080=CARTESIAN_POINT('Ctrl Pts',(-208.480123700393,-5.66799135402889,
129.099496145429));
#162081=CARTESIAN_POINT('Ctrl Pts',(-208.487547071422,-5.71128275678052,
129.250715222671));
#162082=CARTESIAN_POINT('Ctrl Pts',(-208.49497044245,-5.74845105162981,
129.403203570866));
#162083=CARTESIAN_POINT('Ctrl Pts',(-208.498906491892,-5.76815857340318,
129.484056552001));
#162084=CARTESIAN_POINT('Ctrl Pts',(-208.502842541333,-5.78614553147746,
129.565266241738));
#162085=CARTESIAN_POINT('Ctrl Pts',(-208.506778590774,-5.80240258017325,
129.646753231576));
#162086=CARTESIAN_POINT('Ctrl Pts',(-208.517519108524,-5.84676409612494,
129.869111327882));
#162087=CARTESIAN_POINT('Ctrl Pts',(-208.528259626274,-5.87835505477374,
130.094094933894));
#162088=CARTESIAN_POINT('Ctrl Pts',(-208.539000144024,-5.89693230953219,
130.320501237895));
#162089=CARTESIAN_POINT('Ctrl Pts',(-208.546541698614,-5.90997650201339,
130.47947453329));
#162090=CARTESIAN_POINT('Ctrl Pts',(-208.554083253203,-5.91660542909776,
130.63914897901));
#162091=CARTESIAN_POINT('Ctrl Pts',(-208.561624807792,-5.91674766075738,
130.799099303841));
#162092=CARTESIAN_POINT('',(-210.311624807793,-5.90698841004286,130.803765473938));
#162093=CARTESIAN_POINT('Ctrl Pts',(-208.561625802215,-5.91889781063289,
130.799118490467));
#162094=CARTESIAN_POINT('Ctrl Pts',(-208.636159273006,-5.90427014288086,
132.380502494848));
#162095=CARTESIAN_POINT('Ctrl Pts',(-208.803508618402,-4.43691936218312,
135.955107010576));
#162096=CARTESIAN_POINT('Ctrl Pts',(-209.063673838401,1.60744234334904,
137.615651952041));
#162097=CARTESIAN_POINT('Ctrl Pts',(-209.342121462214,6.59939415603132,
133.133643190306));
#162098=CARTESIAN_POINT('Ctrl Pts',(-209.620569086027,5.526825137655,126.511137535992));
#162099=CARTESIAN_POINT('Ctrl Pts',(-209.899016709839,-0.624626181811619,
123.833894158043));
#162100=CARTESIAN_POINT('Ctrl Pts',(-210.129368617095,-5.23869439854464,
126.918191279253));
#162101=CARTESIAN_POINT('Ctrl Pts',(-210.266904649746,-5.90784084701446,
129.850086159445));
#162102=CARTESIAN_POINT('Ctrl Pts',(-210.311624807793,-5.90698841004286,
130.803765473938));
#162103=CARTESIAN_POINT('',(-212.061624807793,-5.9167064429625,130.809826898457));
#162104=CARTESIAN_POINT('Ctrl Pts',(-210.311624807793,-5.90698841004286,
130.803765473938));
#162105=CARTESIAN_POINT('Ctrl Pts',(-210.35972052435,-5.90607162958501,
131.829430230063));
#162106=CARTESIAN_POINT('Ctrl Pts',(-210.500632115514,-5.1631795060691,
134.835682530948));
#162107=CARTESIAN_POINT('Ctrl Pts',(-210.734359581277,-0.370831884411458,
137.792925866865));
#162108=CARTESIAN_POINT('Ctrl Pts',(-211.012807205092,5.67923417909519,
134.893842206882));
#162109=CARTESIAN_POINT('Ctrl Pts',(-211.291254828904,6.51036147803477,
128.236724748581));
#162110=CARTESIAN_POINT('Ctrl Pts',(-211.569702452717,1.3587846274958,123.939139217901));
#162111=CARTESIAN_POINT('Ctrl Pts',(-211.826492445681,-4.54363933266225,
125.793924450652));
#162112=CARTESIAN_POINT('Ctrl Pts',(-211.990466564038,-5.90273208346157,
129.298621124659));
#162113=CARTESIAN_POINT('Ctrl Pts',(-212.061624807793,-5.9167064429625,
130.809826898457));
#162114=CARTESIAN_POINT('',(-213.811624807793,-5.92582816037032,130.802499402571));
#162115=CARTESIAN_POINT('Ctrl Pts',(-212.061624807793,-5.9167064429625,
130.809826898457));
#162116=CARTESIAN_POINT('Ctrl Pts',(-212.083282438643,-5.92095966090986,
131.269775529293));
#162117=CARTESIAN_POINT('Ctrl Pts',(-212.104940069493,-5.87187244348729,
131.728826242693));
#162118=CARTESIAN_POINT('Ctrl Pts',(-212.219413574947,-5.31230370266279,
134.083875118018));
#162119=CARTESIAN_POINT('Ctrl Pts',(-212.405045324154,-2.31923672099176,
137.407291903154));
#162120=CARTESIAN_POINT('Ctrl Pts',(-212.683492947968,4.30162899711266,
136.324645800563));
#162121=CARTESIAN_POINT('Ctrl Pts',(-212.961940571781,6.96950781311999,
130.169127295691));
#162122=CARTESIAN_POINT('Ctrl Pts',(-213.240388195594,3.23274942825056,
124.597357180765));
#162123=CARTESIAN_POINT('Ctrl Pts',(-213.518835819407,-3.47474775259045,
124.729519995276));
#162124=CARTESIAN_POINT('Ctrl Pts',(-213.709248023473,-5.87799918612228,
128.637393418206));
#162125=CARTESIAN_POINT('Ctrl Pts',(-213.806844352935,-5.92624379243174,
130.701381486186));
#162126=CARTESIAN_POINT('Ctrl Pts',(-213.811624807793,-5.92582816037032,
130.802499402571));
#162127=CARTESIAN_POINT('',(-215.561623590517,-5.91341522243185,130.799770594371));
#162128=CARTESIAN_POINT('Ctrl Pts',(-213.811624807793,-5.92582816037032,
130.802499402571));
#162129=CARTESIAN_POINT('Ctrl Pts',(-213.899660227539,-5.91817400525774,
132.664656556716));
#162130=CARTESIAN_POINT('Ctrl Pts',(-214.08051152189,-3.96652147180024,
136.503906757722));
#162131=CARTESIAN_POINT('Ctrl Pts',(-214.354178690847,2.57754055760962,
137.310807052006));
#162132=CARTESIAN_POINT('Ctrl Pts',(-214.632626314659,6.86728128874809,
132.15269597331));
#162133=CARTESIAN_POINT('Ctrl Pts',(-214.911073938471,4.84632600086921,
125.755530572531));
#162134=CARTESIAN_POINT('Ctrl Pts',(-215.189521562285,-1.62816612562249,
123.997993334078));
#162135=CARTESIAN_POINT('Ctrl Pts',(-215.406371156135,-5.50515921563603,
127.500311042211));
#162136=CARTESIAN_POINT('Ctrl Pts',(-215.530404875382,-5.91577993612624,
130.13515780681));
#162137=CARTESIAN_POINT('Ctrl Pts',(-215.561622720024,-5.91103173213339,
130.799753902201));
#162138=CARTESIAN_POINT('',(-217.311625997971,-5.91252205760374,130.808030356679));
#162139=CARTESIAN_POINT('Ctrl Pts',(-215.561624807793,-5.91674823766587,
130.799793936299));
#162140=CARTESIAN_POINT('Ctrl Pts',(-215.569324474548,-5.91687487495898,
130.963869538927));
#162141=CARTESIAN_POINT('Ctrl Pts',(-215.577024141303,-5.91017156417642,
131.128022491076));
#162142=CARTESIAN_POINT('Ctrl Pts',(-215.584723808058,-5.89665047465998,
131.291642612095));
#162143=CARTESIAN_POINT('Ctrl Pts',(-215.592118521284,-5.88366490234,131.448782383406));
#162144=CARTESIAN_POINT('Ctrl Pts',(-215.599513234511,-5.86439129366342,
131.605430320925));
#162145=CARTESIAN_POINT('Ctrl Pts',(-215.606907947737,-5.83889352847738,
131.761049138248));
#162146=CARTESIAN_POINT('Ctrl Pts',(-215.614303120355,-5.81339417926048,
131.916677623282));
#162147=CARTESIAN_POINT('Ctrl Pts',(-215.621698292973,-5.78166996330471,
132.071276492695));
#162148=CARTESIAN_POINT('Ctrl Pts',(-215.629093465591,-5.74383617647952,
132.224317145163));
#162149=CARTESIAN_POINT('Ctrl Pts',(-215.636490553458,-5.70599259122162,
132.377397433064));
#162150=CARTESIAN_POINT('Ctrl Pts',(-215.643887641324,-5.66203637385671,
132.528918338521));
#162151=CARTESIAN_POINT('Ctrl Pts',(-215.651284729191,-5.61213308837605,
132.678365089507));
#162152=CARTESIAN_POINT('Ctrl Pts',(-215.658685189034,-5.56220705438438,
132.827879966089));
#162153=CARTESIAN_POINT('Ctrl Pts',(-215.666085648878,-5.5063286721697,
132.975318452261));
#162154=CARTESIAN_POINT('Ctrl Pts',(-215.673486108721,-5.44471209851916,
133.12018460197));
#162155=CARTESIAN_POINT('Ctrl Pts',(-215.680895437876,-5.38302167856777,
133.265224371026));
#162156=CARTESIAN_POINT('Ctrl Pts',(-215.688304767031,-5.3155794815067,
133.40768530491));
#162157=CARTESIAN_POINT('Ctrl Pts',(-215.695714096186,-5.24264651133644,
133.547094312198));
#162158=CARTESIAN_POINT('Ctrl Pts',(-215.703128661892,-5.16966199571579,
133.686601846943));
#162159=CARTESIAN_POINT('Ctrl Pts',(-215.710543227598,-5.09117916043528,
133.823052835578));
#162160=CARTESIAN_POINT('Ctrl Pts',(-215.717957793304,-5.00750270899136,
133.956002599445));
#162161=CARTESIAN_POINT('Ctrl Pts',(-215.725382941123,-4.92370683400875,
134.089142110021));
#162162=CARTESIAN_POINT('Ctrl Pts',(-215.732808088942,-4.83470275432093,
134.218770113668));
#162163=CARTESIAN_POINT('Ctrl Pts',(-215.740233236761,-4.74083625196273,
134.344473920071));
#162164=CARTESIAN_POINT('Ctrl Pts',(-215.742294427811,-4.71477928996594,
134.379368789104));
#162165=CARTESIAN_POINT('Ctrl Pts',(-215.74435561886,-4.68834785493428,
134.41396147569));
#162166=CARTESIAN_POINT('Ctrl Pts',(-215.74641680991,-4.66154984466891,
134.448243657424));
#162167=CARTESIAN_POINT('Ctrl Pts',(-215.753840076316,-4.56503828192443,
134.571709052828));
#162168=CARTESIAN_POINT('Ctrl Pts',(-215.761263342721,-4.46347225429003,
134.69152419875));
#162169=CARTESIAN_POINT('Ctrl Pts',(-215.768686609127,-4.35715785453345,
134.807247824718));
#162170=CARTESIAN_POINT('Ctrl Pts',(-215.776101101848,-4.25096910956851,
134.922834674969));
#162171=CARTESIAN_POINT('Ctrl Pts',(-215.783515594568,-4.1400434136425,
135.034339358809));
#162172=CARTESIAN_POINT('Ctrl Pts',(-215.790930087289,-4.02472873371046,
135.141351415636));
#162173=CARTESIAN_POINT('Ctrl Pts',(-215.798337433643,-3.90952519840813,
135.248260330214));
#162174=CARTESIAN_POINT('Ctrl Pts',(-215.805744779997,-3.78994137252184,
135.350684986059));
#162175=CARTESIAN_POINT('Ctrl Pts',(-215.813152126351,-3.66636381908059,
135.448249818294));
#162176=CARTESIAN_POINT('Ctrl Pts',(-215.820553948026,-3.54287843444136,
135.545741882996));
#162177=CARTESIAN_POINT('Ctrl Pts',(-215.827955769702,-3.41540554491641,
135.638381110914));
#162178=CARTESIAN_POINT('Ctrl Pts',(-215.835357591377,-3.28436662909331,
135.725830561414));
#162179=CARTESIAN_POINT('Ctrl Pts',(-215.842755505688,-3.1533968876935,
135.81323384803));
#162180=CARTESIAN_POINT('Ctrl Pts',(-215.85015342,-3.01886517875771,135.895452606667));
#162181=CARTESIAN_POINT('Ctrl Pts',(-215.857551334311,-2.88122385268178,
135.972191852546));
#162182=CARTESIAN_POINT('Ctrl Pts',(-215.864948019223,-2.74360540009777,
136.048918345755));
#162183=CARTESIAN_POINT('Ctrl Pts',(-215.872344704135,-2.60287868172131,
136.120166951866));
#162184=CARTESIAN_POINT('Ctrl Pts',(-215.879741389048,-2.45952276416553,
136.185687436767));
#162185=CARTESIAN_POINT('Ctrl Pts',(-215.887137745983,-2.31617320316135,
136.251205016421));
#162186=CARTESIAN_POINT('Ctrl Pts',(-215.894534102918,-2.17019501429799,
136.31099482471));
#162187=CARTESIAN_POINT('Ctrl Pts',(-215.901930459854,-2.02208921821998,
136.364853919069));
#162188=CARTESIAN_POINT('Ctrl Pts',(-215.909327949191,-1.87396074676607,
136.418721259392));
#162189=CARTESIAN_POINT('Ctrl Pts',(-215.916725438527,-1.72370437034527,
136.466655950236));
#162190=CARTESIAN_POINT('Ctrl Pts',(-215.924122927864,-1.57183817085506,
136.508504315541));
#162191=CARTESIAN_POINT('Ctrl Pts',(-215.931523010379,-1.41991873490469,
136.550367350724));
#162192=CARTESIAN_POINT('Ctrl Pts',(-215.938923092894,-1.26638871198569,
136.586139713374));
#162193=CARTESIAN_POINT('Ctrl Pts',(-215.946323175409,-1.11177817411067,
136.615718449783));
#162194=CARTESIAN_POINT('Ctrl Pts',(-215.953731395075,-0.956997626054681,
136.645329711054));
#162195=CARTESIAN_POINT('Ctrl Pts',(-215.961139614742,-0.801134557128024,
136.668733674823));
#162196=CARTESIAN_POINT('Ctrl Pts',(-215.968547834408,-0.644726724846512,
136.685878960032));
#162197=CARTESIAN_POINT('Ctrl Pts',(-215.97596061371,-0.488222626153588,
136.703034797879));
#162198=CARTESIAN_POINT('Ctrl Pts',(-215.983373393012,-0.331173467533277,
136.713924255588));
#162199=CARTESIAN_POINT('Ctrl Pts',(-215.990786172314,-0.174118333418985,
136.718548082338));
#162200=CARTESIAN_POINT('Ctrl Pts',(-215.998209543343,-0.0168387915641384,
136.723178515829));
#162201=CARTESIAN_POINT('Ctrl Pts',(-216.005632914372,0.140446370548699,
136.72152544187));
#162202=CARTESIAN_POINT('Ctrl Pts',(-216.0130562854,0.29720103242974,136.713641632108));
#162203=CARTESIAN_POINT('Ctrl Pts',(-216.016992334841,0.380316115439795,
136.709461447002));
#162204=CARTESIAN_POINT('Ctrl Pts',(-216.020928384282,0.463282177994346,
136.703530441126));
#162205=CARTESIAN_POINT('Ctrl Pts',(-216.024864433723,0.546020445833623,
136.695862313673));
#162206=CARTESIAN_POINT('Ctrl Pts',(-216.032287700129,0.702062236798269,
136.681400464612));
#162207=CARTESIAN_POINT('Ctrl Pts',(-216.039710966534,0.857765031229207,
136.660713102083));
#162208=CARTESIAN_POINT('Ctrl Pts',(-216.04713423294,1.01259212516141,136.633819233129));
#162209=CARTESIAN_POINT('Ctrl Pts',(-216.054548725661,1.16723622632573,
136.606957150495));
#162210=CARTESIAN_POINT('Ctrl Pts',(-216.061963218382,1.32100632297602,
136.573903226202));
#162211=CARTESIAN_POINT('Ctrl Pts',(-216.069377711103,1.47336899834449,
136.534728350724));
#162212=CARTESIAN_POINT('Ctrl Pts',(-216.076785057457,1.62558482083053,
136.495591233465));
#162213=CARTESIAN_POINT('Ctrl Pts',(-216.08419240381,1.77639556349853,136.450345002302));
#162214=CARTESIAN_POINT('Ctrl Pts',(-216.091599750164,1.9252763062222,136.399111881671));
#162215=CARTESIAN_POINT('Ctrl Pts',(-216.099001571839,2.07404600807014,
136.347916972633));
#162216=CARTESIAN_POINT('Ctrl Pts',(-216.106403393515,2.22088822468311,
136.290744185985));
#162217=CARTESIAN_POINT('Ctrl Pts',(-216.11380521519,2.36529165889142,136.227765998955));
#162218=CARTESIAN_POINT('Ctrl Pts',(-216.121203129502,2.50961886365209,
136.164821057619));
#162219=CARTESIAN_POINT('Ctrl Pts',(-216.128601043813,2.65150950864942,
136.096076968103));
#162220=CARTESIAN_POINT('Ctrl Pts',(-216.135998958124,2.79047090839696,
136.021754859129));
#162221=CARTESIAN_POINT('Ctrl Pts',(-216.143395643036,2.92940921527988,
135.947445101141));
#162222=CARTESIAN_POINT('Ctrl Pts',(-216.150792327949,3.06541891418995,
135.867559339329));
#162223=CARTESIAN_POINT('Ctrl Pts',(-216.158189012861,3.19803052887582,
135.782365368355));
#162224=CARTESIAN_POINT('Ctrl Pts',(-216.165585369796,3.33063626342411,
135.69717517497));
#162225=CARTESIAN_POINT('Ctrl Pts',(-216.172981726732,3.45984389926964,
135.60667744219));
#162226=CARTESIAN_POINT('Ctrl Pts',(-216.180378083667,3.58521188118791,
135.511183997457));
#162227=CARTESIAN_POINT('Ctrl Pts',(-216.187775573004,3.71059905726426,
135.415675932434));
#162228=CARTESIAN_POINT('Ctrl Pts',(-216.19517306234,3.83214511192364,135.315170858741));
#162229=CARTESIAN_POINT('Ctrl Pts',(-216.202570551677,3.94944071722406,
135.210021587685));
#162230=CARTESIAN_POINT('Ctrl Pts',(-216.209970634192,4.06677744031659,
135.104835456717));
#162231=CARTESIAN_POINT('Ctrl Pts',(-216.217370716707,4.17986046970684,
134.995002136039));
#162232=CARTESIAN_POINT('Ctrl Pts',(-216.224770799222,4.28831667065473,
134.880911941257));
#162233=CARTESIAN_POINT('Ctrl Pts',(-216.232179018888,4.39689213034528,
134.766696292576));
#162234=CARTESIAN_POINT('Ctrl Pts',(-216.239587238555,4.50083034382097,
134.648214692508));
#162235=CARTESIAN_POINT('Ctrl Pts',(-216.246995458221,4.59979741166932,
134.525891798962));
#162236=CARTESIAN_POINT('Ctrl Pts',(-216.254408237523,4.69882539209686,
134.403493617716));
#162237=CARTESIAN_POINT('Ctrl Pts',(-216.261821016825,4.79287590764574,
134.277249730586));
#162238=CARTESIAN_POINT('Ctrl Pts',(-216.269233796127,4.8816582003181,134.147614089525));
#162239=CARTESIAN_POINT('Ctrl Pts',(-216.276657167156,4.97056734929359,
134.017793218981));
#162240=CARTESIAN_POINT('Ctrl Pts',(-216.284080538185,5.05419304337971,
133.884571230695));
#162241=CARTESIAN_POINT('Ctrl Pts',(-216.291503909213,5.13228989463789,
133.748427702382));
#162242=CARTESIAN_POINT('Ctrl Pts',(-216.295439958654,5.17369871908487,
133.676241136949));
#162243=CARTESIAN_POINT('Ctrl Pts',(-216.299376008095,5.21355397923511,
133.603233585252));
#162244=CARTESIAN_POINT('Ctrl Pts',(-216.303312057536,5.25182462119782,
133.529478727058));
#162245=CARTESIAN_POINT('Ctrl Pts',(-216.310735323942,5.32400185755124,
133.390379366318));
#162246=CARTESIAN_POINT('Ctrl Pts',(-216.318158590347,5.39075815720084,
133.248200170866));
#162247=CARTESIAN_POINT('Ctrl Pts',(-216.325581856753,5.4518194097087,133.103402958721));
#162248=CARTESIAN_POINT('Ctrl Pts',(-216.332996349474,5.51280849288693,
132.958776884856));
#162249=CARTESIAN_POINT('Ctrl Pts',(-216.340410842195,5.56811578352684,
132.81153929408));
#162250=CARTESIAN_POINT('Ctrl Pts',(-216.347825334916,5.61751259899866,
132.662177283061));
#162251=CARTESIAN_POINT('Ctrl Pts',(-216.35523268127,5.66686180395983,132.512959232772));
#162252=CARTESIAN_POINT('Ctrl Pts',(-216.362640027623,5.71031175841179,
132.361621190639));
#162253=CARTESIAN_POINT('Ctrl Pts',(-216.370047373977,5.74768156108323,
132.208670852124));
#162254=CARTESIAN_POINT('Ctrl Pts',(-216.377449195653,5.78502349194605,
132.055834589741));
#162255=CARTESIAN_POINT('Ctrl Pts',(-216.384851017328,5.81629421222117,
131.901388786409));
#162256=CARTESIAN_POINT('Ctrl Pts',(-216.392252839003,5.8413624632775,131.745856839073));
#162257=CARTESIAN_POINT('Ctrl Pts',(-216.399650753315,5.86641748099923,
131.590406995842));
#162258=CARTESIAN_POINT('Ctrl Pts',(-216.407048667626,5.88527649104824,
131.433872518103));
#162259=CARTESIAN_POINT('Ctrl Pts',(-216.414446581938,5.89785922674048,
131.276787441584));
#162260=CARTESIAN_POINT('Ctrl Pts',(-216.42184326685,5.91043987141032,131.119728469756));
#162261=CARTESIAN_POINT('Ctrl Pts',(-216.429239951762,5.91674628199853,
130.962119452491));
#162262=CARTESIAN_POINT('Ctrl Pts',(-216.436636636674,5.91674999835537,
130.804500123008));
#162263=CARTESIAN_POINT('Ctrl Pts',(-216.44403299361,5.91675371454741,130.646887782532));
#162264=CARTESIAN_POINT('Ctrl Pts',(-216.451429350545,5.9104552921762,130.489265504047));
#162265=CARTESIAN_POINT('Ctrl Pts',(-216.458825707481,5.89787840911742,
130.332173330818));
#162266=CARTESIAN_POINT('Ctrl Pts',(-216.466223196817,5.8852996005057,130.175057106376));
#162267=CARTESIAN_POINT('Ctrl Pts',(-216.473620686154,5.86644044702607,
130.018471520923));
#162268=CARTESIAN_POINT('Ctrl Pts',(-216.481018175491,5.84137652707394,
129.862951656779));
#162269=CARTESIAN_POINT('Ctrl Pts',(-216.488418258006,5.81630382100349,
129.707377275388));
#162270=CARTESIAN_POINT('Ctrl Pts',(-216.495818340521,5.78502207726764,
129.552869727429));
#162271=CARTESIAN_POINT('Ctrl Pts',(-216.503218423036,5.74765799099632,
129.399953916843));
#162272=CARTESIAN_POINT('Ctrl Pts',(-216.510626642702,5.71025281907119,
129.246869959604));
#162273=CARTESIAN_POINT('Ctrl Pts',(-216.518034862369,5.666752036575,129.095381598012));
#162274=CARTESIAN_POINT('Ctrl Pts',(-216.525443082035,5.61733243944677,
128.945999289073));
#162275=CARTESIAN_POINT('Ctrl Pts',(-216.532855861337,5.56788242538113,
128.796525037816));
#162276=CARTESIAN_POINT('Ctrl Pts',(-216.540268640639,5.51250646869158,
128.649159770763));
#162277=CARTESIAN_POINT('Ctrl Pts',(-216.547681419941,5.45142933021152,
128.504393482973));
#162278=CARTESIAN_POINT('Ctrl Pts',(-216.55510479097,5.39026492185168,128.359420346321));
#162279=CARTESIAN_POINT('Ctrl Pts',(-216.562528161999,5.32338322038728,
128.217053942686));
#162280=CARTESIAN_POINT('Ctrl Pts',(-216.569951533028,5.25105506995864,
128.077759947361));
#162281=CARTESIAN_POINT('Ctrl Pts',(-216.573887582468,5.21270494911401,
128.003902928732));
#162282=CARTESIAN_POINT('Ctrl Pts',(-216.577823631909,5.17282436982461,
127.930909204615));
#162283=CARTESIAN_POINT('Ctrl Pts',(-216.581759681349,5.13145853557716,
127.858844727242));
#162284=CARTESIAN_POINT('Ctrl Pts',(-216.589182947755,5.05344386316463,
127.722933371962));
#162285=CARTESIAN_POINT('Ctrl Pts',(-216.59660621416,4.96990788988157,127.58991807837));
#162286=CARTESIAN_POINT('Ctrl Pts',(-216.604029480566,4.88109099291859,
127.460279087258));
#162287=CARTESIAN_POINT('Ctrl Pts',(-216.611443973287,4.79237907015178,
127.330793318667));
#162288=CARTESIAN_POINT('Ctrl Pts',(-216.618858466008,4.69839885659414,
127.204676214376));
#162289=CARTESIAN_POINT('Ctrl Pts',(-216.626272958729,4.59943655191889,
127.082383459203));
#162290=CARTESIAN_POINT('Ctrl Pts',(-216.633680305082,4.50056963083848,
126.960208574392));
#162291=CARTESIAN_POINT('Ctrl Pts',(-216.641087651436,4.39673041158119,
126.841850988735));
#162292=CARTESIAN_POINT('Ctrl Pts',(-216.64849499779,4.28824825116155,126.727737321392));
#162293=CARTESIAN_POINT('Ctrl Pts',(-216.655896819465,4.17984700083087,
126.613708764328));
#162294=CARTESIAN_POINT('Ctrl Pts',(-216.663298641141,4.06680996049485,
126.503918092479));
#162295=CARTESIAN_POINT('Ctrl Pts',(-216.670700462816,3.94950653033062,
126.398758646283));
#162296=CARTESIAN_POINT('Ctrl Pts',(-216.678098377128,3.83226502373242,
126.293654712937));
#162297=CARTESIAN_POINT('Ctrl Pts',(-216.685496291439,3.71076188991149,
126.193177384882));
#162298=CARTESIAN_POINT('Ctrl Pts',(-216.69289420575,3.58540304214761,126.097682852108));
#162299=CARTESIAN_POINT('Ctrl Pts',(-216.700290890663,3.46006502675123,
126.002204188793));
#162300=CARTESIAN_POINT('Ctrl Pts',(-216.707687575575,3.33087286577215,
125.911706903312));
#162301=CARTESIAN_POINT('Ctrl Pts',(-216.715084260487,3.19826526864947,
125.826506678985));
#162302=CARTESIAN_POINT('Ctrl Pts',(-216.722480617422,3.06566355148662,
125.741310232524));
#162303=CARTESIAN_POINT('Ctrl Pts',(-216.729876974358,2.92964701336309,
125.661410581986));
#162304=CARTESIAN_POINT('Ctrl Pts',(-216.737273331293,2.79068280644374,
125.58707971308));
#162305=CARTESIAN_POINT('Ctrl Pts',(-216.74467082063,2.65169732374956,125.512737463927));
#162306=CARTESIAN_POINT('Ctrl Pts',(-216.752068309967,2.50976360285831,
125.443965870116));
#162307=CARTESIAN_POINT('Ctrl Pts',(-216.759465799303,2.36537267564962,
125.380990570465));
#162308=CARTESIAN_POINT('Ctrl Pts',(-216.766865881818,2.22093113242585,
125.317993194921));
#162309=CARTESIAN_POINT('Ctrl Pts',(-216.774265964333,2.07403100985985,
125.260796308143));
#162310=CARTESIAN_POINT('Ctrl Pts',(-216.781666046848,1.92518240631656,
125.209577041331));
#162311=CARTESIAN_POINT('Ctrl Pts',(-216.789074266515,1.77617012843103,
125.158301453669));
#162312=CARTESIAN_POINT('Ctrl Pts',(-216.796482486181,1.62520544394597,
125.11301673424));
#162313=CARTESIAN_POINT('Ctrl Pts',(-216.803890705847,1.47281337732091,
125.073850054092));
#162314=CARTESIAN_POINT('Ctrl Pts',(-216.811303485149,1.32032751592122,
125.034659267506));
#162315=CARTESIAN_POINT('Ctrl Pts',(-216.818716264452,1.16641288592535,
125.001594101759));
#162316=CARTESIAN_POINT('Ctrl Pts',(-216.826129043754,1.01160322277228,
124.974730313492));
#162317=CARTESIAN_POINT('Ctrl Pts',(-216.833552414782,0.856572360312867,
124.947828140985));
#162318=CARTESIAN_POINT('Ctrl Pts',(-216.840975785811,0.700644279591562,
124.927145091957));
#162319=CARTESIAN_POINT('Ctrl Pts',(-216.84839915684,0.544357164294071,
124.912705006434));
#162320=CARTESIAN_POINT('Ctrl Pts',(-216.852335206281,0.461489985705045,
124.905048526604));
#162321=CARTESIAN_POINT('Ctrl Pts',(-216.856271255721,0.378521871066538,
124.899146296581));
#162322=CARTESIAN_POINT('Ctrl Pts',(-216.860207305162,0.295532741446856,
124.894995934181));
#162323=CARTESIAN_POINT('Ctrl Pts',(-216.867630571568,0.139017832987244,
124.887168480224));
#162324=CARTESIAN_POINT('Ctrl Pts',(-216.875053837973,-0.018044934740192,
124.885551645143));
#162325=CARTESIAN_POINT('Ctrl Pts',(-216.882477104379,-0.175121591811435,
124.890202774679));
#162326=CARTESIAN_POINT('Ctrl Pts',(-216.8898915971,-0.332012597318424,
124.894848406966));
#162327=CARTESIAN_POINT('Ctrl Pts',(-216.897306089821,-0.488917090002346,
124.905747246839));
#162328=CARTESIAN_POINT('Ctrl Pts',(-216.904720582542,-0.645296991405024,
124.922904815183));
#162329=CARTESIAN_POINT('Ctrl Pts',(-216.912127928895,-0.801526167972022,
124.940045846417));
#162330=CARTESIAN_POINT('Ctrl Pts',(-216.919535275249,-0.957231391269231,
124.963433556365));
#162331=CARTESIAN_POINT('Ctrl Pts',(-216.926942621603,-1.11187570900268,
124.99302144572));
#162332=CARTESIAN_POINT('Ctrl Pts',(-216.934344443278,-1.26640468716869,
125.022587267311));
#162333=CARTESIAN_POINT('Ctrl Pts',(-216.941746264954,-1.41987397021381,
125.058343990801));
#162334=CARTESIAN_POINT('Ctrl Pts',(-216.949148086629,-1.57175295986926,
125.100193439472));
#162335=CARTESIAN_POINT('Ctrl Pts',(-216.956546000941,-1.72355177379002,
125.142020796146));
#162336=CARTESIAN_POINT('Ctrl Pts',(-216.963943915252,-1.87376160725783,
125.189934373668));
#162337=CARTESIAN_POINT('Ctrl Pts',(-216.971341829563,-2.02186338150322,
125.243785195091));
#162338=CARTESIAN_POINT('Ctrl Pts',(-216.978738514476,-2.1699405439191,
125.297627067483));
#162339=CARTESIAN_POINT('Ctrl Pts',(-216.986135199388,-2.31590999191378,
125.357404098105));
#162340=CARTESIAN_POINT('Ctrl Pts',(-216.9935318843,-2.45926899900166,125.422917822827));
#162341=CARTESIAN_POINT('Ctrl Pts',(-217.000928241235,-2.60262164940094,
125.488428642601));
#162342=CARTESIAN_POINT('Ctrl Pts',(-217.008324598171,-2.74336374951875,
125.55967549554));
#162343=CARTESIAN_POINT('Ctrl Pts',(-217.015720955106,-2.88101396291893,
125.636412368215));
#162344=CARTESIAN_POINT('Ctrl Pts',(-217.023118444443,-3.01868525091819,
125.713160989502));
#162345=CARTESIAN_POINT('Ctrl Pts',(-217.03051593378,-3.1532633835701,125.795401122365));
#162346=CARTESIAN_POINT('Ctrl Pts',(-217.037913423116,-3.28429310981991,
125.882841611071));
#162347=CARTESIAN_POINT('Ctrl Pts',(-217.045313505631,-3.41536876833806,
125.970312751906));
#162348=CARTESIAN_POINT('Ctrl Pts',(-217.052713588146,-3.54289323356809,
126.062987671034));
#162349=CARTESIAN_POINT('Ctrl Pts',(-217.060113670661,-3.66644175938774,
126.160532951996));
#162350=CARTESIAN_POINT('Ctrl Pts',(-217.067521890328,-3.79012613951173,
126.258185494021));
#162351=CARTESIAN_POINT('Ctrl Pts',(-217.074930109994,-3.90982555597913,
126.360718861628));
#162352=CARTESIAN_POINT('Ctrl Pts',(-217.082338329661,-4.02514922763937,
126.467760075928));
#162353=CARTESIAN_POINT('Ctrl Pts',(-217.089751108963,-4.14054387909489,
126.574867172309));
#162354=CARTESIAN_POINT('Ctrl Pts',(-217.097163888265,-4.25155715657824,
126.686487379865));
#162355=CARTESIAN_POINT('Ctrl Pts',(-217.104576667567,-4.35783682683886,
126.80221260017));
#162356=CARTESIAN_POINT('Ctrl Pts',(-217.112000038595,-4.46426835447682,
126.918103174097));
#162357=CARTESIAN_POINT('Ctrl Pts',(-217.119423409624,-4.56595252578291,
127.03811019131));
#162358=CARTESIAN_POINT('Ctrl Pts',(-217.126846780653,-4.66257838204143,
127.161793748747));
#162359=CARTESIAN_POINT('Ctrl Pts',(-217.130782830094,-4.71381172953475,
127.227373738645));
#162360=CARTESIAN_POINT('Ctrl Pts',(-217.134718879534,-4.76362373538357,
127.293986863771));
#162361=CARTESIAN_POINT('Ctrl Pts',(-217.138654928975,-4.81197320449548,
127.361564596638));
#162362=CARTESIAN_POINT('Ctrl Pts',(-217.146146069748,-4.90399254643782,
127.490179421632));
#162363=CARTESIAN_POINT('Ctrl Pts',(-217.15363721052,-4.99098822520857,
127.622676463298));
#162364=CARTESIAN_POINT('Ctrl Pts',(-217.161128351292,-5.07261844284067,
127.758630377401));
#162365=CARTESIAN_POINT('Ctrl Pts',(-217.168610322293,-5.15414873838094,
127.894417872746));
#162366=CARTESIAN_POINT('Ctrl Pts',(-217.176092293294,-5.23032646158278,
128.033653507964));
#162367=CARTESIAN_POINT('Ctrl Pts',(-217.183574264295,-5.30085110262719,
128.175880419757));
#162368=CARTESIAN_POINT('Ctrl Pts',(-217.191048462408,-5.3713024768669,
128.317959574521));
#162369=CARTESIAN_POINT('Ctrl Pts',(-217.198522660521,-5.43611230127342,
128.463023494699));
#162370=CARTESIAN_POINT('Ctrl Pts',(-217.205996858634,-5.49502432286834,
128.610588010028));
#162371=CARTESIAN_POINT('Ctrl Pts',(-217.213464675629,-5.55388604815469,
128.758026541726));
#162372=CARTESIAN_POINT('Ctrl Pts',(-217.220932492624,-5.60685986334836,
128.907961080522));
#162373=CARTESIAN_POINT('Ctrl Pts',(-217.228400309619,-5.65373629863065,
129.059884642367));
#162374=CARTESIAN_POINT('Ctrl Pts',(-217.235862610705,-5.70057810985261,
129.211695989823));
#162375=CARTESIAN_POINT('Ctrl Pts',(-217.243324911791,-5.74133140817679,
129.365493085869));
#162376=CARTESIAN_POINT('Ctrl Pts',(-217.250787212877,-5.77583559641578,
129.520750970642));
#162377=CARTESIAN_POINT('Ctrl Pts',(-217.258246235064,-5.81032462368122,
129.675940635851));
#162378=CARTESIAN_POINT('Ctrl Pts',(-217.265705257251,-5.83856993091696,
129.832589456409));
#162379=CARTESIAN_POINT('Ctrl Pts',(-217.273164279438,-5.86046130109009,
129.990159229133));
#162380=CARTESIAN_POINT('Ctrl Pts',(-217.280622113517,-5.88234918430061,
130.147703903388));
#162381=CARTESIAN_POINT('Ctrl Pts',(-217.288079947595,-5.89788509194219,
130.306168877629));
#162382=CARTESIAN_POINT('Ctrl Pts',(-217.295537781673,-5.90701024927821,
130.465007589847));
#162383=CARTESIAN_POINT('Ctrl Pts',(-217.300900123713,-5.91357143236328,
130.579216017546));
#162384=CARTESIAN_POINT('Ctrl Pts',(-217.306262465753,-5.91681938424466,
130.693617469333));
#162385=CARTESIAN_POINT('Ctrl Pts',(-217.311624807793,-5.91674887602822,
130.808007605195));
#162386=CARTESIAN_POINT('',(-219.061623395149,-5.9210338050865,130.807548187548));
#162387=CARTESIAN_POINT('Ctrl Pts',(-217.311626920727,-5.90924496437867,
130.808047996124));
#162388=CARTESIAN_POINT('Ctrl Pts',(-217.346785464747,-5.91343255841384,
131.55710594002));
#162389=CARTESIAN_POINT('Ctrl Pts',(-217.474759883373,-5.4330908806276,
134.278437435159));
#162390=CARTESIAN_POINT('Ctrl Pts',(-217.6955501766,-1.337882961292,137.673685890998));
#162391=CARTESIAN_POINT('Ctrl Pts',(-217.973997800414,5.05619948175488,
135.642997546604));
#162392=CARTESIAN_POINT('Ctrl Pts',(-218.252445424226,6.80388161014486,
129.165838244978));
#162393=CARTESIAN_POINT('Ctrl Pts',(-218.530893048039,2.29912892690833,
124.194400957491));
#162394=CARTESIAN_POINT('Ctrl Pts',(-218.800618671839,-4.11112532191061,
125.262650173527));
#162395=CARTESIAN_POINT('Ctrl Pts',(-218.977528421034,-5.91269684251228,
129.027581667749));
#162396=CARTESIAN_POINT('Ctrl Pts',(-219.061622295625,-5.92436876444137,
130.807526727116));
#162397=CARTESIAN_POINT('',(-220.811625604547,-5.91847951006198,130.799176690814));
#162398=CARTESIAN_POINT('Ctrl Pts',(-219.061624807793,-5.91674912645136,
130.807575759414));
#162399=CARTESIAN_POINT('Ctrl Pts',(-219.070345970417,-5.9166489483197,
130.991931194124));
#162400=CARTESIAN_POINT('Ctrl Pts',(-219.079067133041,-5.90793327527812,
131.176047965864));
#162401=CARTESIAN_POINT('Ctrl Pts',(-219.087788295665,-5.8906639236756,
131.359346293784));
#162402=CARTESIAN_POINT('Ctrl Pts',(-219.09521156207,-5.87596462231853,
131.515365895582));
#162403=CARTESIAN_POINT('Ctrl Pts',(-219.102634828476,-5.85504033059687,
131.671037027068));
#162404=CARTESIAN_POINT('Ctrl Pts',(-219.110058094881,-5.82791087230526,
131.825823013823));
#162405=CARTESIAN_POINT('Ctrl Pts',(-219.117472587602,-5.80081347878032,
131.980426056395));
#162406=CARTESIAN_POINT('Ctrl Pts',(-219.124887080323,-5.76752558085258,
132.134145672538));
#162407=CARTESIAN_POINT('Ctrl Pts',(-219.132301573044,-5.72811888068246,
132.286448553982));
#162408=CARTESIAN_POINT('Ctrl Pts',(-219.139708919398,-5.68875016217372,
132.438604640174));
#162409=CARTESIAN_POINT('Ctrl Pts',(-219.147116265752,-5.64327447512745,
132.589346351144));
#162410=CARTESIAN_POINT('Ctrl Pts',(-219.154523612106,-5.59181484267633,
132.738148953379));
#162411=CARTESIAN_POINT('Ctrl Pts',(-219.161925433781,-5.54039359076056,
132.886840573018));
#162412=CARTESIAN_POINT('Ctrl Pts',(-219.169327255457,-5.48299740146014,
133.033595612342));
#162413=CARTESIAN_POINT('Ctrl Pts',(-219.176729077132,-5.41979952991243,
133.177903037255));
#162414=CARTESIAN_POINT('Ctrl Pts',(-219.184126991443,-5.35663502002935,
133.3221342834));
#162415=CARTESIAN_POINT('Ctrl Pts',(-219.191524905755,-5.2876750767107,
133.463920147288));
#162416=CARTESIAN_POINT('Ctrl Pts',(-219.198922820066,-5.21314157820515,
133.602768280522));
#162417=CARTESIAN_POINT('Ctrl Pts',(-219.206319504978,-5.13862046581477,
133.741593339715));
#162418=CARTESIAN_POINT('Ctrl Pts',(-219.21371618989,-5.05852781290098,
133.877481308598));
#162419=CARTESIAN_POINT('Ctrl Pts',(-219.221112874803,-4.97313212827649,
134.009963119001));
#162420=CARTESIAN_POINT('Ctrl Pts',(-219.228509231738,-4.88774023018615,
134.142439055021));
#162421=CARTESIAN_POINT('Ctrl Pts',(-219.235905588674,-4.79704597017358,
134.271508819103));
#162422=CARTESIAN_POINT('Ctrl Pts',(-219.243301945609,-4.70136184729367,
134.39673133108));
#162423=CARTESIAN_POINT('Ctrl Pts',(-219.250699434946,-4.60566307493001,
134.521973014944));
#162424=CARTESIAN_POINT('Ctrl Pts',(-219.258096924282,-4.5049731452149,
134.643365977242));
#162425=CARTESIAN_POINT('Ctrl Pts',(-219.265494413619,-4.39964549197633,
134.760501427425));
#162426=CARTESIAN_POINT('Ctrl Pts',(-219.272894496134,-4.29428091629235,
134.877677939259));
#162427=CARTESIAN_POINT('Ctrl Pts',(-219.280294578649,-4.18427562967898,
134.990593690084));
#162428=CARTESIAN_POINT('Ctrl Pts',(-219.287694661164,-4.07002051513498,
135.098876139587));
#162429=CARTESIAN_POINT('Ctrl Pts',(-219.295102880831,-3.95563976534666,
135.207277656775));
#162430=CARTESIAN_POINT('Ctrl Pts',(-219.302511100497,-3.83700012620945,
135.311035441066));
#162431=CARTESIAN_POINT('Ctrl Pts',(-219.309919320164,-3.7145267632806,
135.409816239692));
#162432=CARTESIAN_POINT('Ctrl Pts',(-219.317332099466,-3.59197802004045,
135.508657836251));
#162433=CARTESIAN_POINT('Ctrl Pts',(-219.324744878768,-3.46559115022453,
135.602516121185));
#162434=CARTESIAN_POINT('Ctrl Pts',(-219.33215765807,-3.33582054774286,
135.691101027671));
#162435=CARTESIAN_POINT('Ctrl Pts',(-219.339581029099,-3.20586452293891,
135.779812508426));
#162436=CARTESIAN_POINT('Ctrl Pts',(-219.347004400128,-3.07251542485004,
135.863235364487));
#162437=CARTESIAN_POINT('Ctrl Pts',(-219.354427771156,-2.93625320407586,
135.941124938036));
#162438=CARTESIAN_POINT('Ctrl Pts',(-219.358363820597,-2.86400370505544,
135.982423858866));
#162439=CARTESIAN_POINT('Ctrl Pts',(-219.362299870038,-2.79093558498296,
136.022167967796));
#162440=CARTESIAN_POINT('Ctrl Pts',(-219.366235919478,-2.71712257079711,
136.060326323101));
#162441=CARTESIAN_POINT('Ctrl Pts',(-219.373659185884,-2.57791352966545,
136.132291790327));
#162442=CARTESIAN_POINT('Ctrl Pts',(-219.381082452289,-2.43563290713131,
136.198831640141));
#162443=CARTESIAN_POINT('Ctrl Pts',(-219.388505718695,-2.29074293782725,
136.259672465233));
#162444=CARTESIAN_POINT('Ctrl Pts',(-219.395920211416,-2.14602421643454,
136.320441381522));
#162445=CARTESIAN_POINT('Ctrl Pts',(-219.403334704137,-1.99870262787695,
136.375524537568));
#162446=CARTESIAN_POINT('Ctrl Pts',(-219.410749196858,-1.84926561627258,
136.424693992284));
#162447=CARTESIAN_POINT('Ctrl Pts',(-219.418156543212,-1.6999726376862,
136.473816055629));
#162448=CARTESIAN_POINT('Ctrl Pts',(-219.425563889566,-1.54856864736606,
136.517035649029));
#162449=CARTESIAN_POINT('Ctrl Pts',(-219.432971235919,-1.39556161548667,
136.554172644048));
#162450=CARTESIAN_POINT('Ctrl Pts',(-219.440373057595,-1.24266870202429,
136.591281940896));
#162451=CARTESIAN_POINT('Ctrl Pts',(-219.44777487927,-1.08817548882546,
136.622317584739));
#162452=CARTESIAN_POINT('Ctrl Pts',(-219.455176700946,-0.932605571982637,
136.647149113619));
#162453=CARTESIAN_POINT('Ctrl Pts',(-219.462574615257,-0.777117779287963,
136.671967534128));
#162454=CARTESIAN_POINT('Ctrl Pts',(-219.469972529568,-0.62055478261063,
136.690588303511));
#162455=CARTESIAN_POINT('Ctrl Pts',(-219.47737044388,-0.463450739213037,
136.702931967887));
#162456=CARTESIAN_POINT('Ctrl Pts',(-219.484767128792,-0.306372803657523,
136.715273580969));
#162457=CARTESIAN_POINT('Ctrl Pts',(-219.492163813704,-0.148754371617358,
136.721340130161));
#162458=CARTESIAN_POINT('Ctrl Pts',(-219.499560498616,0.00886478099952192,
136.721103976725));
#162459=CARTESIAN_POINT('Ctrl Pts',(-219.506956855552,0.166476944618001,
136.720867833762));
#162460=CARTESIAN_POINT('Ctrl Pts',(-219.514353212487,0.324089455452518,
136.714329544408));
#162461=CARTESIAN_POINT('Ctrl Pts',(-219.521749569423,0.481162306895928,
136.701513608368));
#162462=CARTESIAN_POINT('Ctrl Pts',(-219.529147058759,0.638259206593881,
136.688695710175));
#162463=CARTESIAN_POINT('Ctrl Pts',(-219.536544548096,0.79481591030149,
136.669598281929));
#162464=CARTESIAN_POINT('Ctrl Pts',(-219.543942037432,0.950297451335014,
136.644297716241));
#162465=CARTESIAN_POINT('Ctrl Pts',(-219.551342119947,1.1058334961815,136.61898828148));
#162466=CARTESIAN_POINT('Ctrl Pts',(-219.558742202462,1.26029325973372,
136.587471439783));
#162467=CARTESIAN_POINT('Ctrl Pts',(-219.566142284977,1.41315203146586,
136.549874684946));
#162468=CARTESIAN_POINT('Ctrl Pts',(-219.573550504643,1.566178887132,136.512236588613));
#162469=CARTESIAN_POINT('Ctrl Pts',(-219.58095872431,1.71760087251689,136.468505316992));
#162470=CARTESIAN_POINT('Ctrl Pts',(-219.588366943976,1.866907800259,136.418858442646));
#162471=CARTESIAN_POINT('Ctrl Pts',(-219.595779723278,2.01630662392423,
136.369181011478));
#162472=CARTESIAN_POINT('Ctrl Pts',(-219.603192502581,2.16358744755067,
136.313580854063));
#162473=CARTESIAN_POINT('Ctrl Pts',(-219.610605281883,2.30826061869695,
136.252283476663));
#162474=CARTESIAN_POINT('Ctrl Pts',(-219.618028652911,2.45314050565446,
136.190898514696));
#162475=CARTESIAN_POINT('Ctrl Pts',(-219.62545202394,2.59540496186664,136.123800233249));
#162476=CARTESIAN_POINT('Ctrl Pts',(-219.632875394969,2.73458872475895,
136.051260184827));
#162477=CARTESIAN_POINT('Ctrl Pts',(-219.636811444409,2.80838729551299,
136.012797710579));
#162478=CARTESIAN_POINT('Ctrl Pts',(-219.64074749385,2.88132024365648,135.972806093445));
#162479=CARTESIAN_POINT('Ctrl Pts',(-219.644683543291,2.9533216858271,135.931330637229));
#162480=CARTESIAN_POINT('Ctrl Pts',(-219.652106809697,3.08911415867301,
135.853109221209));
#162481=CARTESIAN_POINT('Ctrl Pts',(-219.659530076102,3.22200217070551,
135.769370918026));
#162482=CARTESIAN_POINT('Ctrl Pts',(-219.666953342507,3.35150584750005,
135.680356835435));
#162483=CARTESIAN_POINT('Ctrl Pts',(-219.674367835228,3.48085646170323,
135.591447960098));
#162484=CARTESIAN_POINT('Ctrl Pts',(-219.681782327949,3.60683039806602,
135.497275926604));
#162485=CARTESIAN_POINT('Ctrl Pts',(-219.68919682067,3.72897240784421,135.39812762777));
#162486=CARTESIAN_POINT('Ctrl Pts',(-219.696604167024,3.85099669255481,
135.299074891799));
#162487=CARTESIAN_POINT('Ctrl Pts',(-219.704011513378,3.96919611554074,
135.195055672689));
#162488=CARTESIAN_POINT('Ctrl Pts',(-219.711418859732,4.0831445593603,135.086399976314));
#162489=CARTESIAN_POINT('Ctrl Pts',(-219.718820681407,4.19700801613143,
134.977825319457));
#162490=CARTESIAN_POINT('Ctrl Pts',(-219.726222503082,4.30662653771201,
134.864621327302));
#162491=CARTESIAN_POINT('Ctrl Pts',(-219.733624324758,4.41160734628434,
134.747157998197));
#162492=CARTESIAN_POINT('Ctrl Pts',(-219.741022239069,4.51653273630501,
134.629756677069));
#162493=CARTESIAN_POINT('Ctrl Pts',(-219.74842015338,4.61682504092196,134.508100774558));
#162494=CARTESIAN_POINT('Ctrl Pts',(-219.755818067692,4.71212868828817,
134.382596745536));
#162495=CARTESIAN_POINT('Ctrl Pts',(-219.763214752604,4.80741649791705,
134.257113573007));
#162496=CARTESIAN_POINT('Ctrl Pts',(-219.770611437516,4.89771707012715,
134.127783840167));
#162497=CARTESIAN_POINT('Ctrl Pts',(-219.778008122428,4.98271538960518,
133.995046736364));
#162498=CARTESIAN_POINT('Ctrl Pts',(-219.785404479364,5.06770994016866,
133.862315518264));
#162499=CARTESIAN_POINT('Ctrl Pts',(-219.792800836299,5.14740250416741,
133.726177543978));
#162500=CARTESIAN_POINT('Ctrl Pts',(-219.800197193235,5.22152180713321,
133.587100379048));
#162501=CARTESIAN_POINT('Ctrl Pts',(-219.807594682571,5.29565245795372,
133.448001921048));
#162502=CARTESIAN_POINT('Ctrl Pts',(-219.814992171908,5.36420797316718,
133.305963705855));
#162503=CARTESIAN_POINT('Ctrl Pts',(-219.822389661244,5.42696346148188,
133.161477108162));
#162504=CARTESIAN_POINT('Ctrl Pts',(-219.829789743759,5.48974094863562,
133.016939860917));
#162505=CARTESIAN_POINT('Ctrl Pts',(-219.837189826274,5.54671421220162,
132.869952864533));
#162506=CARTESIAN_POINT('Ctrl Pts',(-219.844589908789,5.59770689746666,
132.721026486348));
#162507=CARTESIAN_POINT('Ctrl Pts',(-219.851998128456,5.64875565443139,
132.5719363483));
#162508=CARTESIAN_POINT('Ctrl Pts',(-219.859406348122,5.69381057887091,
132.420902922995));
#162509=CARTESIAN_POINT('Ctrl Pts',(-219.866814567789,5.73274529888063,
132.268451427817));
#162510=CARTESIAN_POINT('Ctrl Pts',(-219.874227347091,5.77170398256086,
132.115906101288));
#162511=CARTESIAN_POINT('Ctrl Pts',(-219.881640126393,5.80453487815331,
131.961941329969));
#162512=CARTESIAN_POINT('Ctrl Pts',(-219.889052905695,5.83116304135805,
131.80709096397));
#162513=CARTESIAN_POINT('Ctrl Pts',(-219.896476276724,5.85782925213108,
131.652019340507));
#162514=CARTESIAN_POINT('Ctrl Pts',(-219.903899647752,5.87827498121259,
131.496059964268));
#162515=CARTESIAN_POINT('Ctrl Pts',(-219.911323018781,5.89247720762978,
131.339751054596));
#162516=CARTESIAN_POINT('Ctrl Pts',(-219.915259068222,5.90000756885379,
131.256872320109));
#162517=CARTESIAN_POINT('Ctrl Pts',(-219.919195117662,5.90578352869573,
131.173895319359));
#162518=CARTESIAN_POINT('Ctrl Pts',(-219.923131167103,5.90980759096107,
131.090899969696));
#162519=CARTESIAN_POINT('Ctrl Pts',(-219.930554433509,5.91739684680695,
130.934373330425));
#162520=CARTESIAN_POINT('Ctrl Pts',(-219.937977699914,5.91877465722026,
130.777308284025));
#162521=CARTESIAN_POINT('Ctrl Pts',(-219.945400966319,5.91388448913744,
130.620238887073));
#162522=CARTESIAN_POINT('Ctrl Pts',(-219.95281545904,5.90900010082718,130.463355133104));
#162523=CARTESIAN_POINT('Ctrl Pts',(-219.960229951761,5.89786249164671,
130.306467408292));
#162524=CARTESIAN_POINT('Ctrl Pts',(-219.967644444482,5.88046695958147,
130.150113798872));
#162525=CARTESIAN_POINT('Ctrl Pts',(-219.975051790836,5.86308819398497,
129.993910888948));
#162526=CARTESIAN_POINT('Ctrl Pts',(-219.98245913719,5.83946355427546,129.838241438069));
#162527=CARTESIAN_POINT('Ctrl Pts',(-219.989866483544,5.80964035685599,
129.683642327142));
#162528=CARTESIAN_POINT('Ctrl Pts',(-219.997268305219,5.77983940270232,
129.529158522065));
#162529=CARTESIAN_POINT('Ctrl Pts',(-220.004670126895,5.7438491664946,129.375743832381));
#162530=CARTESIAN_POINT('Ctrl Pts',(-220.01207194857,5.70176863231611,129.223928706335));
#162531=CARTESIAN_POINT('Ctrl Pts',(-220.019469862882,5.65971031212406,
129.072193722313));
#162532=CARTESIAN_POINT('Ctrl Pts',(-220.026867777193,5.61156819628912,
128.922056979096));
#162533=CARTESIAN_POINT('Ctrl Pts',(-220.034265691504,5.55749205153644,
128.774037328134));
#162534=CARTESIAN_POINT('Ctrl Pts',(-220.041662376417,5.50342489325805,
128.626042275353));
#162535=CARTESIAN_POINT('Ctrl Pts',(-220.049059061329,5.44342579120522,
128.480163966854));
#162536=CARTESIAN_POINT('Ctrl Pts',(-220.056455746241,5.37769397434287,
128.33690482651));
#162537=CARTESIAN_POINT('Ctrl Pts',(-220.063852103176,5.31196507209816,
128.193652038426));
#162538=CARTESIAN_POINT('Ctrl Pts',(-220.071248460112,5.2405041161445,128.053018526867));
#162539=CARTESIAN_POINT('Ctrl Pts',(-220.078644817047,5.16355785213638,
127.915485253321));
#162540=CARTESIAN_POINT('Ctrl Pts',(-220.086042306384,5.0865998074586,127.777930923079));
#162541=CARTESIAN_POINT('Ctrl Pts',(-220.093439795721,5.00415496481943,
127.643478101749));
#162542=CARTESIAN_POINT('Ctrl Pts',(-220.100837285057,4.91651517242971,
127.512581596768));
#162543=CARTESIAN_POINT('Ctrl Pts',(-220.108237367572,4.82884465804676,
127.38163920622));
#162544=CARTESIAN_POINT('Ctrl Pts',(-220.115637450087,4.73597577570763,
127.254255924113));
#162545=CARTESIAN_POINT('Ctrl Pts',(-220.123037532602,4.63824258787776,
127.130855988673));
#162546=CARTESIAN_POINT('Ctrl Pts',(-220.130445752269,4.54040193236052,
127.007320362319));
#162547=CARTESIAN_POINT('Ctrl Pts',(-220.137853971935,4.4376865213498,126.887777122792));
#162548=CARTESIAN_POINT('Ctrl Pts',(-220.145262191602,4.33046992800464,
126.772616483181));
#162549=CARTESIAN_POINT('Ctrl Pts',(-220.152674970904,4.22318734463529,
126.657384964118));
#162550=CARTESIAN_POINT('Ctrl Pts',(-220.160087750206,4.11139832302276,
126.54654168214));
#162551=CARTESIAN_POINT('Ctrl Pts',(-220.167500529508,3.99551149715896,
126.440438249034));
#162552=CARTESIAN_POINT('Ctrl Pts',(-220.174923900537,3.87945908676399,
126.334183210368));
#162553=CARTESIAN_POINT('Ctrl Pts',(-220.182347271566,3.75929746251838,
126.232681787062));
#162554=CARTESIAN_POINT('Ctrl Pts',(-220.189770642594,3.63546700020045,
126.136244268014));
#162555=CARTESIAN_POINT('Ctrl Pts',(-220.193706692035,3.56980911780938,
126.085110781429));
#162556=CARTESIAN_POINT('Ctrl Pts',(-220.197642741476,3.50312026442755,
126.035400207099));
#162557=CARTESIAN_POINT('Ctrl Pts',(-220.201578790916,3.4354690301533,125.987153635781));
#162558=CARTESIAN_POINT('Ctrl Pts',(-220.209002057322,3.30788091363256,
125.896162107997));
#162559=CARTESIAN_POINT('Ctrl Pts',(-220.216425323727,3.17648238196665,
125.810105422969));
#162560=CARTESIAN_POINT('Ctrl Pts',(-220.223848590133,3.04169219457659,
125.729319814188));
#162561=CARTESIAN_POINT('Ctrl Pts',(-220.231263082854,2.90706131799441,
125.648629687288));
#162562=CARTESIAN_POINT('Ctrl Pts',(-220.238677575575,2.76904708200507,
125.573198425868));
#162563=CARTESIAN_POINT('Ctrl Pts',(-220.246092068296,2.62809965224538,
125.503320834621));
#162564=CARTESIAN_POINT('Ctrl Pts',(-220.25349941465,2.48728807292547,125.433510594027));
#162565=CARTESIAN_POINT('Ctrl Pts',(-220.260906761003,2.34354926028618,
125.369243531862));
#162566=CARTESIAN_POINT('Ctrl Pts',(-220.268314107357,2.1973604831124,125.310770036739));
#162567=CARTESIAN_POINT('Ctrl Pts',(-220.275715929032,2.05128073904362,
125.252340153354));
#162568=CARTESIAN_POINT('Ctrl Pts',(-220.283117750708,1.90275501390172,
125.199695371236));
#162569=CARTESIAN_POINT('Ctrl Pts',(-220.290519572383,1.75228309213406,
125.153039132504));
#162570=CARTESIAN_POINT('Ctrl Pts',(-220.297917486695,1.60189060332305,
125.106407523238));
#162571=CARTESIAN_POINT('Ctrl Pts',(-220.305315401006,1.44955431961587,
125.065758271743));
#162572=CARTESIAN_POINT('Ctrl Pts',(-220.312713315317,1.29579171800591,
125.031245826914));
#162573=CARTESIAN_POINT('Ctrl Pts',(-220.32011000023,1.14205466895057,124.996739117427));
#162574=CARTESIAN_POINT('Ctrl Pts',(-220.327506685142,0.986892136302272,
124.968367272227));
#162575=CARTESIAN_POINT('Ctrl Pts',(-220.334903370054,0.830834511618251,
124.94623424672));
#162576=CARTESIAN_POINT('Ctrl Pts',(-220.34229972699,0.674783806692845,
124.924102202614));
#162577=CARTESIAN_POINT('Ctrl Pts',(-220.349696083925,0.517838458246394,
124.908208480575));
#162578=CARTESIAN_POINT('Ctrl Pts',(-220.35709244086,0.360536484853832,
124.898605457928));
#162579=CARTESIAN_POINT('Ctrl Pts',(-220.364489930197,0.203210428127571,
124.889000965034));
#162580=CARTESIAN_POINT('Ctrl Pts',(-220.371887419533,0.0455280103671136,
124.885689111983));
#162581=CARTESIAN_POINT('Ctrl Pts',(-220.37928490887,-0.111970374962323,
124.888670193141));
#162582=CARTESIAN_POINT('Ctrl Pts',(-220.386684991385,-0.269523971106809,
124.891652319313));
#162583=CARTESIAN_POINT('Ctrl Pts',(-220.3940850739,-0.426893033378565,
124.900931764719));
#162584=CARTESIAN_POINT('Ctrl Pts',(-220.401485156415,-0.583540069219387,
124.916456784272));
#162585=CARTESIAN_POINT('Ctrl Pts',(-220.408893376081,-0.740359354579599,
124.93199887518));
#162586=CARTESIAN_POINT('Ctrl Pts',(-220.416301595748,-0.896454656248115,
124.953800218545));
#162587=CARTESIAN_POINT('Ctrl Pts',(-220.423709815414,-1.05129575148534,
124.981757436393));
#162588=CARTESIAN_POINT('Ctrl Pts',(-220.431122594716,-1.20623214883302,
125.009731861442));
#162589=CARTESIAN_POINT('Ctrl Pts',(-220.438535374018,-1.35991243798555,
125.043869629947));
#162590=CARTESIAN_POINT('Ctrl Pts',(-220.445948153321,-1.51181992133489,
125.084017001318));
#162591=CARTESIAN_POINT('Ctrl Pts',(-220.453371524349,-1.6639444572204,
125.124221737135));
#162592=CARTESIAN_POINT('Ctrl Pts',(-220.460794895378,-1.81429077233319,
125.170453116159));
#162593=CARTESIAN_POINT('Ctrl Pts',(-220.468218266407,-1.96235977797054,
125.222508356506));
#162594=CARTESIAN_POINT('Ctrl Pts',(-220.472154315848,-2.04086951762733,
125.250109293986));
#162595=CARTESIAN_POINT('Ctrl Pts',(-220.476090365289,-2.11873938590875,
125.27934673539));
#162596=CARTESIAN_POINT('Ctrl Pts',(-220.480026414729,-2.19589773737316,
125.310185184482));
#162597=CARTESIAN_POINT('Ctrl Pts',(-220.487449681135,-2.34141598020358,
125.368345537036));
#162598=CARTESIAN_POINT('Ctrl Pts',(-220.49487294754,-2.4848420225225,125.432379102817));
#162599=CARTESIAN_POINT('Ctrl Pts',(-220.502296213946,-2.62566663187468,
125.50211531008));
#162600=CARTESIAN_POINT('Ctrl Pts',(-220.509710706667,-2.76632479823296,
125.571769094937));
#162601=CARTESIAN_POINT('Ctrl Pts',(-220.517125199388,-2.90438732052647,
125.647111941132));
#162602=CARTESIAN_POINT('Ctrl Pts',(-220.524539692109,-3.03936284569548,
125.727924460703));
#162603=CARTESIAN_POINT('Ctrl Pts',(-220.531947038462,-3.17420827637197,
125.808659090125));
#162604=CARTESIAN_POINT('Ctrl Pts',(-220.539354384816,-3.30597231515705,
125.894852707182));
#162605=CARTESIAN_POINT('Ctrl Pts',(-220.54676173117,-3.43418632758138,
125.986239113291));
#162606=CARTESIAN_POINT('Ctrl Pts',(-220.554163552845,-3.56230471315764,
126.077557359971));
#162607=CARTESIAN_POINT('Ctrl Pts',(-220.561565374521,-3.68687804171274,
126.174060468344));
#162608=CARTESIAN_POINT('Ctrl Pts',(-220.568967196196,-3.80746500592656,
126.275437921036));
#162609=CARTESIAN_POINT('Ctrl Pts',(-220.576365110507,-3.92798831322027,
126.37676185736));
#162610=CARTESIAN_POINT('Ctrl Pts',(-220.583763024818,-4.0445291621136,
126.482954773883));
#162611=CARTESIAN_POINT('Ctrl Pts',(-220.59116093913,-4.15667790142167,
126.593664785957));
#162612=CARTESIAN_POINT('Ctrl Pts',(-220.598557624042,-4.26880800364434,
126.704356400035));
#162613=CARTESIAN_POINT('Ctrl Pts',(-220.605954308954,-4.37654717949532,
126.819563357831));
#162614=CARTESIAN_POINT('Ctrl Pts',(-220.613350993866,-4.47952127875511,
126.938895616343));
#162615=CARTESIAN_POINT('Ctrl Pts',(-220.620747350802,-4.58249081203542,
127.058222583538));
#162616=CARTESIAN_POINT('Ctrl Pts',(-220.628143707737,-4.68069544495884,
127.18167420512));
#162617=CARTESIAN_POINT('Ctrl Pts',(-220.635540064673,-4.77380029881667,
127.30882614205));
#162618=CARTESIAN_POINT('Ctrl Pts',(-220.642937554009,-4.86691940726531,
127.435997546267));
#162619=CARTESIAN_POINT('Ctrl Pts',(-220.650335043346,-4.9549369614398,
127.566870092656));
#162620=CARTESIAN_POINT('Ctrl Pts',(-220.657732532682,-5.03756061781539,
127.700989292002));
#162621=CARTESIAN_POINT('Ctrl Pts',(-220.665132615197,-5.12021323778553,
127.835155506625));
#162622=CARTESIAN_POINT('Ctrl Pts',(-220.672532697712,-5.19746799966815,
127.972570322542));
#162623=CARTESIAN_POINT('Ctrl Pts',(-220.679932780227,-5.26907791021533,
128.112753562556));
#162624=CARTESIAN_POINT('Ctrl Pts',(-220.687340999893,-5.34076656322093,
128.253090948454));
#162625=CARTESIAN_POINT('Ctrl Pts',(-220.69474921956,-5.40679779899382,
128.396202505211));
#162626=CARTESIAN_POINT('Ctrl Pts',(-220.702157439226,-5.46697199400874,
128.541586263101));
#162627=CARTESIAN_POINT('Ctrl Pts',(-220.709570218528,-5.52718322523663,
128.687059502268));
#162628=CARTESIAN_POINT('Ctrl Pts',(-220.71698299783,-5.58153010389817,
128.834807379722));
#162629=CARTESIAN_POINT('Ctrl Pts',(-220.724395777132,-5.62986268862889,
128.984312082586));
#162630=CARTESIAN_POINT('Ctrl Pts',(-220.731819148161,-5.67826433322331,
129.13403040478));
#162631=CARTESIAN_POINT('Ctrl Pts',(-220.73924251919,-5.72063442044092,
129.28551020734));
#162632=CARTESIAN_POINT('Ctrl Pts',(-220.746665890219,-5.75687378679056,
129.438221984241));
#162633=CARTESIAN_POINT('Ctrl Pts',(-220.75060193966,-5.77608876838261,
129.51919343263));
#162634=CARTESIAN_POINT('Ctrl Pts',(-220.754537989101,-5.79358104676735,
129.600511109454));
#162635=CARTESIAN_POINT('Ctrl Pts',(-220.758474038542,-5.80934175982063,
129.682095550791));
#162636=CARTESIAN_POINT('Ctrl Pts',(-220.769393094443,-5.85306379874289,
129.90842021691));
#162637=CARTESIAN_POINT('Ctrl Pts',(-220.780312150343,-5.88357025894,130.137373687765));
#162638=CARTESIAN_POINT('Ctrl Pts',(-220.791231206244,-5.90061493995885,
130.36769839933));
#162639=CARTESIAN_POINT('Ctrl Pts',(-220.798029073427,-5.91122643227021,
130.511091455686));
#162640=CARTESIAN_POINT('Ctrl Pts',(-220.80482694061,-5.91662104841901,
130.655015641359));
#162641=CARTESIAN_POINT('Ctrl Pts',(-220.811624807793,-5.91674771557038,
130.799161310626));
#162642=CARTESIAN_POINT('',(-222.561624807793,-5.90703034408285,130.803567381702));
#162643=CARTESIAN_POINT('Ctrl Pts',(-220.811625964301,-5.91926145875612,
130.799183635355));
#162644=CARTESIAN_POINT('Ctrl Pts',(-220.886724530319,-5.90459539466751,
132.39230526411));
#162645=CARTESIAN_POINT('Ctrl Pts',(-221.05463897094,-4.41863354744595,
135.978493543736));
#162646=CARTESIAN_POINT('Ctrl Pts',(-221.315369286169,1.64887482479054,
137.605740796802));
#162647=CARTESIAN_POINT('Ctrl Pts',(-221.593816909981,6.61345088869389,
133.093427648732));
#162648=CARTESIAN_POINT('Ctrl Pts',(-221.872264533795,5.50058867092583,
126.477573726163));
#162649=CARTESIAN_POINT('Ctrl Pts',(-222.150712157606,-0.667045816727497,
123.837825581499));
#162650=CARTESIAN_POINT('Ctrl Pts',(-222.380498915606,-5.25097959326614,
126.942516864827));
#162651=CARTESIAN_POINT('Ctrl Pts',(-222.517469799002,-5.90815259440714,
129.861956814884));
#162652=CARTESIAN_POINT('Ctrl Pts',(-222.561624807793,-5.90703034408285,
130.803567381702));
#162653=CARTESIAN_POINT('',(-224.311624807793,-5.91634088406479,130.809833178867));
#162654=CARTESIAN_POINT('Ctrl Pts',(-222.561624807793,-5.90703034408285,
130.803567381702));
#162655=CARTESIAN_POINT('Ctrl Pts',(-222.610285673606,-5.90579357222084,
131.841265860195));
#162656=CARTESIAN_POINT('Ctrl Pts',(-222.751762414023,-5.15017517596034,
134.85995768299));
#162657=CARTESIAN_POINT('Ctrl Pts',(-222.986055029046,-0.328283633494095,
137.795053743877));
#162658=CARTESIAN_POINT('Ctrl Pts',(-223.264502652858,5.70402279120795,
134.85919532785));
#162659=CARTESIAN_POINT('Ctrl Pts',(-223.542950276671,6.49461092779884,
128.197141902751));
#162660=CARTESIAN_POINT('Ctrl Pts',(-223.821397900484,1.31696890112159,
123.930995106856));
#162661=CARTESIAN_POINT('Ctrl Pts',(-224.077622744192,-4.56108999705214,
125.817514651832));
#162662=CARTESIAN_POINT('Ctrl Pts',(-224.241031713294,-5.90253858859253,
129.310393028754));
#162663=CARTESIAN_POINT('Ctrl Pts',(-224.311624807793,-5.91634088406479,
130.809833178867));
#162664=CARTESIAN_POINT('',(-226.061624807793,-5.92597879789556,130.802710800977));
#162665=CARTESIAN_POINT('Ctrl Pts',(-224.311624807793,-5.91634088406479,
130.809833178867));
#162666=CARTESIAN_POINT('Ctrl Pts',(-224.333847587899,-5.92068586113956,
131.281858509026));
#162667=CARTESIAN_POINT('Ctrl Pts',(-224.356070368004,-5.86896945013117,
131.752943156795));
#162668=CARTESIAN_POINT('Ctrl Pts',(-224.471109022714,-5.29224194237738,
134.11615185666));
#162669=CARTESIAN_POINT('Ctrl Pts',(-224.656740771924,-2.27899983402202,
137.421287418344));
#162670=CARTESIAN_POINT('Ctrl Pts',(-224.935188395735,4.3351528406458,136.298358285803));
#162671=CARTESIAN_POINT('Ctrl Pts',(-225.213636019549,6.9655118387511,130.126713692855));
#162672=CARTESIAN_POINT('Ctrl Pts',(-225.492083643361,3.19490574121353,
124.577793518826));
#162673=CARTESIAN_POINT('Ctrl Pts',(-225.770531267174,-3.51166265267364,
124.750784323824));
#162674=CARTESIAN_POINT('Ctrl Pts',(-225.960378321985,-5.88401903759723,
128.661572723237));
#162675=CARTESIAN_POINT('Ctrl Pts',(-226.057409502191,-5.92630793883599,
130.713553172688));
#162676=CARTESIAN_POINT('Ctrl Pts',(-226.061624807793,-5.92597879789556,
130.802710800977));
#162677=CARTESIAN_POINT('',(-227.811623611839,-5.91356008316327,130.799662206759));
#162678=CARTESIAN_POINT('Ctrl Pts',(-226.061624807793,-5.92597879789556,
130.802710800977));
#162679=CARTESIAN_POINT('Ctrl Pts',(-226.150225376795,-5.91906065782266,
132.676695119892));
#162680=CARTESIAN_POINT('Ctrl Pts',(-226.331641820403,-3.945277242289,136.526362468158));
#162681=CARTESIAN_POINT('Ctrl Pts',(-226.605874138613,2.61709938795056,
137.29499628165));
#162682=CARTESIAN_POINT('Ctrl Pts',(-226.884321762427,6.87536175394465,
132.110867901409));
#162683=CARTESIAN_POINT('Ctrl Pts',(-227.162769386239,4.81550254815928,
125.726123153737));
#162684=CARTESIAN_POINT('Ctrl Pts',(-227.441217010051,-1.66956824900632,
124.008030549637));
#162685=CARTESIAN_POINT('Ctrl Pts',(-227.657501471997,-5.51512181869817,
127.524694996426));
#162686=CARTESIAN_POINT('Ctrl Pts',(-227.780970059337,-5.91611079036253,
130.147161607405));
#162687=CARTESIAN_POINT('Ctrl Pts',(-227.811622772073,-5.91132151002306,
130.799646100255));
#162688=CARTESIAN_POINT('',(-229.561625975116,-5.91241234693134,130.807877191858));
#162689=CARTESIAN_POINT('Ctrl Pts',(-227.811624807793,-5.916748152698,130.799685144877));
#162690=CARTESIAN_POINT('Ctrl Pts',(-227.819395118205,-5.91687897381839,
130.965237522987));
#162691=CARTESIAN_POINT('Ctrl Pts',(-227.827165428617,-5.9100562349648,
131.13087635323));
#162692=CARTESIAN_POINT('Ctrl Pts',(-227.834935739028,-5.89629095285145,
131.295973841373));
#162693=CARTESIAN_POINT('Ctrl Pts',(-227.842322639182,-5.88320489075527,
131.452924927735));
#162694=CARTESIAN_POINT('Ctrl Pts',(-227.849709539335,-5.86384499508312,
131.609386400109));
#162695=CARTESIAN_POINT('Ctrl Pts',(-227.857096439489,-5.83827411370623,
131.764821931585));
#162696=CARTESIAN_POINT('Ctrl Pts',(-227.864483592032,-5.81270235864333,
131.920262773862));
#162697=CARTESIAN_POINT('Ctrl Pts',(-227.871870744576,-5.7809192553894,
132.074677236392));
#162698=CARTESIAN_POINT('Ctrl Pts',(-227.879257897119,-5.74303908593296,
132.227537563679));
#162699=CARTESIAN_POINT('Ctrl Pts',(-227.886646765646,-5.70515011717909,
132.380433399346));
#162700=CARTESIAN_POINT('Ctrl Pts',(-227.894035634173,-5.66116135210173,
132.531774018092));
#162701=CARTESIAN_POINT('Ctrl Pts',(-227.9014245027,-5.61123736849344,132.681045395818));
#162702=CARTESIAN_POINT('Ctrl Pts',(-227.908816551567,-5.56129189644803,
132.830381023397));
#162703=CARTESIAN_POINT('Ctrl Pts',(-227.916208600434,-5.50540623786596,
132.97764528244));
#162704=CARTESIAN_POINT('Ctrl Pts',(-227.923600649301,-5.44379359751809,
133.122342893193));
#162705=CARTESIAN_POINT('Ctrl Pts',(-227.931001429038,-5.38210818547155,
133.267211408664));
#162706=CARTESIAN_POINT('Ctrl Pts',(-227.938402208775,-5.31468243151133,
133.40950687864));
#162707=CARTESIAN_POINT('Ctrl Pts',(-227.945802988512,-5.24177642922586,
133.548756804073));
#162708=CARTESIAN_POINT('Ctrl Pts',(-227.953208848849,-5.16882037732131,
133.688102323908));
#162709=CARTESIAN_POINT('Ctrl Pts',(-227.960614709185,-5.09037676739029,
133.824397810815));
#162710=CARTESIAN_POINT('Ctrl Pts',(-227.968020569522,-5.00674943471655,
133.957199126032));
#162711=CARTESIAN_POINT('Ctrl Pts',(-227.975437096918,-4.92300164908518,
134.090191722146));
#162712=CARTESIAN_POINT('Ctrl Pts',(-227.982853624315,-4.83405544377064,
134.21967979103));
#162713=CARTESIAN_POINT('Ctrl Pts',(-227.990270151711,-4.74025580559906,
134.345251107257));
#162714=CARTESIAN_POINT('Ctrl Pts',(-227.992884187033,-4.70719510828498,
134.389510076247));
#162715=CARTESIAN_POINT('Ctrl Pts',(-227.995498222355,-4.6735318185491,
134.433282798673));
#162716=CARTESIAN_POINT('Ctrl Pts',(-227.998112257678,-4.63928212662991,
134.476552321717));
#162717=CARTESIAN_POINT('Ctrl Pts',(-228.005535524083,-4.54202078311397,
134.599427936319));
#162718=CARTESIAN_POINT('Ctrl Pts',(-228.012958790489,-4.43972728846017,
134.718622601108));
#162719=CARTESIAN_POINT('Ctrl Pts',(-228.020382056894,-4.33271041590368,
134.83369691706));
#162720=CARTESIAN_POINT('Ctrl Pts',(-228.027796549615,-4.22582002840335,
134.948635224726));
#162721=CARTESIAN_POINT('Ctrl Pts',(-228.035211042337,-4.11421762701217,
135.059462606449));
#162722=CARTESIAN_POINT('Ctrl Pts',(-228.042625535058,-3.99825367082837,
135.165770727405));
#162723=CARTESIAN_POINT('Ctrl Pts',(-228.050032881411,-3.88240148507183,
135.271976384592));
#162724=CARTESIAN_POINT('Ctrl Pts',(-228.057440227765,-3.76219638684362,
135.373671202055));
#162725=CARTESIAN_POINT('Ctrl Pts',(-228.064847574119,-3.63802721818065,
135.470481974997));
#162726=CARTESIAN_POINT('Ctrl Pts',(-228.072249395795,-3.51395065956829,
135.567220542813));
#162727=CARTESIAN_POINT('Ctrl Pts',(-228.07965121747,-3.38591621054431,
135.659082090681));
#162728=CARTESIAN_POINT('Ctrl Pts',(-228.087053039145,-3.25434739294053,
135.745732249872));
#162729=CARTESIAN_POINT('Ctrl Pts',(-228.094450953457,-3.12284802949069,
135.832336667119));
#162730=CARTESIAN_POINT('Ctrl Pts',(-228.101848867768,-2.98781832419317,
135.913734969737));
#162731=CARTESIAN_POINT('Ctrl Pts',(-228.10924678208,-2.84971241471892,
135.989634931997));
#162732=CARTESIAN_POINT('Ctrl Pts',(-228.116643466992,-2.71162945594152,
136.06552228106));
#162733=CARTESIAN_POINT('Ctrl Pts',(-228.124040151905,-2.57047163441416,
136.135912923622));
#162734=CARTESIAN_POINT('Ctrl Pts',(-228.131436836817,-2.42671953112006,
136.200559546421));
#162735=CARTESIAN_POINT('Ctrl Pts',(-228.138833193752,-2.28297380194487,
136.265203302722));
#162736=CARTESIAN_POINT('Ctrl Pts',(-228.146229550688,-2.13663436018288,
136.324103392575));
#162737=CARTESIAN_POINT('Ctrl Pts',(-228.153625907623,-1.9882034525649,
136.377059927031));
#162738=CARTESIAN_POINT('Ctrl Pts',(-228.16102339696,-1.83974981979605,
136.430024569267));
#162739=CARTESIAN_POINT('Ctrl Pts',(-228.168420886297,-1.68920443520671,
136.477043718781));
#162740=CARTESIAN_POINT('Ctrl Pts',(-228.175818375633,-1.53708630656534,
136.51796685607));
#162741=CARTESIAN_POINT('Ctrl Pts',(-228.183218458149,-1.38491485315001,
136.558904338901));
#162742=CARTESIAN_POINT('Ctrl Pts',(-228.190618540663,-1.23116991825896,
136.593741457945));
#162743=CARTESIAN_POINT('Ctrl Pts',(-228.198018623179,-1.07638219079224,
136.622378488099));
#162744=CARTESIAN_POINT('Ctrl Pts',(-228.205426842845,-0.921424258306389,
136.651047007613));
#162745=CARTESIAN_POINT('Ctrl Pts',(-228.212835062512,-0.765421610588236,
136.67350175502));
#162746=CARTESIAN_POINT('Ctrl Pts',(-228.220243282178,-0.608912307961287,
136.689694623696));
#162747=CARTESIAN_POINT('Ctrl Pts',(-228.227656061481,-0.452306676469624,
136.705897458814));
#162748=CARTESIAN_POINT('Ctrl Pts',(-228.235068840783,-0.295194140383829,
136.71583071196));
#162749=CARTESIAN_POINT('Ctrl Pts',(-228.242481620085,-0.138113769588865,
136.71949841386));
#162750=CARTESIAN_POINT('Ctrl Pts',(-228.249904991114,0.0191910450060024,
136.723171356346));
#162751=CARTESIAN_POINT('Ctrl Pts',(-228.257328362142,0.176463230261345,
136.720560873587));
#162752=CARTESIAN_POINT('Ctrl Pts',(-228.264751733171,0.33316699685643,
136.711722999772));
#162753=CARTESIAN_POINT('Ctrl Pts',(-228.268687782611,0.416255093935163,
136.707036947015));
#162754=CARTESIAN_POINT('Ctrl Pts',(-228.272623832051,0.499183515576516,
136.700601013057));
#162755=CARTESIAN_POINT('Ctrl Pts',(-228.27655988149,0.581873572371184,
136.692429376359));
#162756=CARTESIAN_POINT('Ctrl Pts',(-228.283983147896,0.737824438863897,
136.677017924571));
#162757=CARTESIAN_POINT('Ctrl Pts',(-228.291406414301,0.893398418636188,
136.655383138227));
#162758=CARTESIAN_POINT('Ctrl Pts',(-228.298829680707,1.04805893336818,
136.627547291088));
#162759=CARTESIAN_POINT('Ctrl Pts',(-228.306244173428,1.20253665221508,
136.599744343609));
#162760=CARTESIAN_POINT('Ctrl Pts',(-228.313658666149,1.35610269124354,
136.565754989506));
#162761=CARTESIAN_POINT('Ctrl Pts',(-228.32107315887,1.5082240750992,136.525653364996));
#162762=CARTESIAN_POINT('Ctrl Pts',(-228.328480505224,1.6601988386374,136.485590391941));
#162763=CARTESIAN_POINT('Ctrl Pts',(-228.335887851577,1.8107313604801,136.43942697129));
#162764=CARTESIAN_POINT('Ctrl Pts',(-228.343295197931,1.95929747424139,
136.387288520551));
#162765=CARTESIAN_POINT('Ctrl Pts',(-228.350697019606,2.10775278179038,
136.335188956636));
#162766=CARTESIAN_POINT('Ctrl Pts',(-228.358098841282,2.25424425077843,
136.277123359014));
#162767=CARTESIAN_POINT('Ctrl Pts',(-228.365500662957,2.39826164342685,
136.213267314133));
#162768=CARTESIAN_POINT('Ctrl Pts',(-228.372898577269,2.54220301041555,
136.14944497836));
#162769=CARTESIAN_POINT('Ctrl Pts',(-228.38029649158,2.68367256172371,136.079838433883));
#162770=CARTESIAN_POINT('Ctrl Pts',(-228.387694405892,2.82217896706645,
136.004671804442));
#162771=CARTESIAN_POINT('Ctrl Pts',(-228.395091090804,2.9606623551568,135.929517666331));
#162772=CARTESIAN_POINT('Ctrl Pts',(-228.402487775716,3.09618324681663,
135.848805454976));
#162773=CARTESIAN_POINT('Ctrl Pts',(-228.409884460629,3.22827380463498,
135.762805817909));
#162774=CARTESIAN_POINT('Ctrl Pts',(-228.417280817564,3.36035850541957,
135.676809994157));
#162775=CARTESIAN_POINT('Ctrl Pts',(-228.424677174499,3.48901286196149,
135.585527414536));
#162776=CARTESIAN_POINT('Ctrl Pts',(-228.432073531435,3.61379722539937,
135.489272588585));
#162777=CARTESIAN_POINT('Ctrl Pts',(-228.439471020772,3.73860069364186,
135.393003025775));
#162778=CARTESIAN_POINT('Ctrl Pts',(-228.446868510108,3.85953269342429,
135.291759928873));
#162779=CARTESIAN_POINT('Ctrl Pts',(-228.454265999445,3.97618605205117,
135.185898594347));
#162780=CARTESIAN_POINT('Ctrl Pts',(-228.46166608196,4.09288030333158,135.080000150295));
#162781=CARTESIAN_POINT('Ctrl Pts',(-228.469066164475,4.20529265095796,
134.969480496077));
#162782=CARTESIAN_POINT('Ctrl Pts',(-228.47646624699,4.31305234306541,134.854732211442));
#162783=CARTESIAN_POINT('Ctrl Pts',(-228.483874466656,4.42093052803276,
134.739857749271));
#162784=CARTESIAN_POINT('Ctrl Pts',(-228.491282686323,4.52414558464567,
134.620745642984));
#162785=CARTESIAN_POINT('Ctrl Pts',(-228.498690905989,4.62236620469127,
134.497822575165));
#162786=CARTESIAN_POINT('Ctrl Pts',(-228.506103685292,4.72064727788989,
134.374823850248));
#162787=CARTESIAN_POINT('Ctrl Pts',(-228.513516464594,4.81392756852741,
134.248009789941));
#162788=CARTESIAN_POINT('Ctrl Pts',(-228.520929243896,4.9019190873274,134.117836107712));
#162789=CARTESIAN_POINT('Ctrl Pts',(-228.528352614925,4.99003633253573,
133.987476427221));
#162790=CARTESIAN_POINT('Ctrl Pts',(-228.535775985954,5.07284951717573,
133.853747853892));
#162791=CARTESIAN_POINT('Ctrl Pts',(-228.543199356982,5.15011617718097,
133.717131450302));
#162792=CARTESIAN_POINT('Ctrl Pts',(-228.547135406423,5.19108481429918,
133.644694155061));
#162793=CARTESIAN_POINT('Ctrl Pts',(-228.551071455863,5.23049491832864,
133.571445345756));
#162794=CARTESIAN_POINT('Ctrl Pts',(-228.555007505303,5.26831588446356,
133.497458889818));
#162795=CARTESIAN_POINT('Ctrl Pts',(-228.562430771709,5.33964504624945,
133.357922742945));
#162796=CARTESIAN_POINT('Ctrl Pts',(-228.569854038114,5.40553462394097,
133.215339817202));
#162797=CARTESIAN_POINT('Ctrl Pts',(-228.577277304519,5.46571332339622,
133.07017359064));
#162798=CARTESIAN_POINT('Ctrl Pts',(-228.58469179724,5.52582089662624,132.925178938502));
#162799=CARTESIAN_POINT('Ctrl Pts',(-228.592106289962,5.58023088554384,
132.777607404523));
#162800=CARTESIAN_POINT('Ctrl Pts',(-228.599520782683,5.62871757685187,
132.627947468401));
#162801=CARTESIAN_POINT('Ctrl Pts',(-228.606928129036,5.67715753486134,
132.47843178016));
#162802=CARTESIAN_POINT('Ctrl Pts',(-228.61433547539,5.71968544666903,132.326832049766));
#162803=CARTESIAN_POINT('Ctrl Pts',(-228.621742821744,5.7561235048417,132.173657064472));
#162804=CARTESIAN_POINT('Ctrl Pts',(-228.629144643419,5.79253438613595,
132.02059632286));
#162805=CARTESIAN_POINT('Ctrl Pts',(-228.636546465095,5.82286437159545,
131.865963027302));
#162806=CARTESIAN_POINT('Ctrl Pts',(-228.64394828677,5.84698539108677,131.710281364054));
#162807=CARTESIAN_POINT('Ctrl Pts',(-228.651346201081,5.87109367727974,
131.554681883944));
#162808=CARTESIAN_POINT('Ctrl Pts',(-228.658744115393,5.88899946811958,
131.39803550628));
#162809=CARTESIAN_POINT('Ctrl Pts',(-228.666142029704,5.90062574923648,
131.240876745501));
#162810=CARTESIAN_POINT('Ctrl Pts',(-228.673538714616,5.91225009827629,
131.083744101658));
#162811=CARTESIAN_POINT('Ctrl Pts',(-228.680935399529,5.91759698119891,
130.926099615613));
#162812=CARTESIAN_POINT('Ctrl Pts',(-228.688332084441,5.91664122389118,
130.76848318383));
#162813=CARTESIAN_POINT('Ctrl Pts',(-228.695728441376,5.91568550896273,
130.610873740925));
#162814=CARTESIAN_POINT('Ctrl Pts',(-228.703124798311,5.90842771173963,
130.453292723101));
#162815=CARTESIAN_POINT('Ctrl Pts',(-228.710521155247,5.89489479705551,
130.296280019483));
#162816=CARTESIAN_POINT('Ctrl Pts',(-228.717918644583,5.88135981044764,
130.139243276821));
#162817=CARTESIAN_POINT('Ctrl Pts',(-228.72531613392,5.86154782548237,129.982775393558));
#162818=CARTESIAN_POINT('Ctrl Pts',(-228.732713623256,5.83553767635279,
129.827410982033));
#162819=CARTESIAN_POINT('Ctrl Pts',(-228.740113705771,5.80951840940571,
129.671992107755));
#162820=CARTESIAN_POINT('Ctrl Pts',(-228.747513788286,5.77729671395034,
129.517677843317));
#162821=CARTESIAN_POINT('Ctrl Pts',(-228.754913870801,5.73900247800852,
129.364992311707));
#162822=CARTESIAN_POINT('Ctrl Pts',(-228.762322090468,5.70066613361748,
129.212138886657));
#162823=CARTESIAN_POINT('Ctrl Pts',(-228.769730310134,5.65624400443657,
129.060918133404));
#162824=CARTESIAN_POINT('Ctrl Pts',(-228.7771385298,5.60591599042587,128.911839423289));
#162825=CARTESIAN_POINT('Ctrl Pts',(-228.784551309102,5.5555570003626,128.762668957716));
#162826=CARTESIAN_POINT('Ctrl Pts',(-228.791964088405,5.49928501545498,
128.615643510168));
#162827=CARTESIAN_POINT('Ctrl Pts',(-228.799376867707,5.4373277751111,128.47125169844));
#162828=CARTESIAN_POINT('Ctrl Pts',(-228.806800238735,5.37528200735645,
128.32665357292));
#162829=CARTESIAN_POINT('Ctrl Pts',(-228.814223609764,5.30753492034926,
128.184696934905));
#162830=CARTESIAN_POINT('Ctrl Pts',(-228.821646980793,5.23436018790941,
128.045845802357));
#162831=CARTESIAN_POINT('Ctrl Pts',(-228.825583030234,5.19556118896182,
127.972223600184));
#162832=CARTESIAN_POINT('Ctrl Pts',(-228.829519079675,5.15523701504349,
127.899473992864));
#162833=CARTESIAN_POINT('Ctrl Pts',(-228.833455129116,5.11343327027361,
127.827662656241));
#162834=CARTESIAN_POINT('Ctrl Pts',(-228.840878395522,5.03459271229616,
127.692228716537));
#162835=CARTESIAN_POINT('Ctrl Pts',(-228.848301661927,4.95024858489456,
127.559724394589));
#162836=CARTESIAN_POINT('Ctrl Pts',(-228.855724928333,4.8606441841678,127.430628459048));
#162837=CARTESIAN_POINT('Ctrl Pts',(-228.863139421054,4.77114568840151,
127.301685104183));
#162838=CARTESIAN_POINT('Ctrl Pts',(-228.870553913775,4.67639950546935,
127.176142420784));
#162839=CARTESIAN_POINT('Ctrl Pts',(-228.877968406496,4.57669460362477,
127.05445434305));
#162840=CARTESIAN_POINT('Ctrl Pts',(-228.885375752849,4.47708580111841,
126.932883552868));
#162841=CARTESIAN_POINT('Ctrl Pts',(-228.892783099203,4.3725280295438,126.815160258903));
#162842=CARTESIAN_POINT('Ctrl Pts',(-228.900190445557,4.26335323676517,
126.701709067524));
#162843=CARTESIAN_POINT('Ctrl Pts',(-228.907592267232,4.15425987066592,
126.588342492323));
#162844=CARTESIAN_POINT('Ctrl Pts',(-228.914994088908,4.04055659766189,
126.479241943189));
#162845=CARTESIAN_POINT('Ctrl Pts',(-228.922395910583,3.92261520546097,
126.374798504627));
#162846=CARTESIAN_POINT('Ctrl Pts',(-228.929793824895,3.80473607360361,
126.270410200943));
#162847=CARTESIAN_POINT('Ctrl Pts',(-228.937191739206,3.68262355694131,
126.170674358564));
#162848=CARTESIAN_POINT('Ctrl Pts',(-228.944589653517,3.55668572946279,
126.075944689971));
#162849=CARTESIAN_POINT('Ctrl Pts',(-228.951986338429,3.43076883056591,
125.981230763729));
#162850=CARTESIAN_POINT('Ctrl Pts',(-228.959383023342,3.30102818055546,
125.891521584306));
#162851=CARTESIAN_POINT('Ctrl Pts',(-228.966779708254,3.16790440239628,
125.807130158624));
#162852=CARTESIAN_POINT('Ctrl Pts',(-228.974176065189,3.03478652708454,
125.722742474945));
#162853=CARTESIAN_POINT('Ctrl Pts',(-228.981572422125,2.89828613718103,
125.643672276036));
#162854=CARTESIAN_POINT('Ctrl Pts',(-228.98896877906,2.75887203184956,125.570188698878));
#162855=CARTESIAN_POINT('Ctrl Pts',(-228.996366268397,2.61943658186264,
125.496693871197));
#162856=CARTESIAN_POINT('Ctrl Pts',(-229.003763757733,2.47708685846287,
125.428787542409));
#162857=CARTESIAN_POINT('Ctrl Pts',(-229.01116124707,2.33231525795974,125.366692358101));
#162858=CARTESIAN_POINT('Ctrl Pts',(-229.018561329585,2.18749290799668,
125.304575406424));
#162859=CARTESIAN_POINT('Ctrl Pts',(-229.0259614121,2.04024733346464,125.248273802112));
#162860=CARTESIAN_POINT('Ctrl Pts',(-229.033361494615,1.89108970152551,
125.197961567972));
#162861=CARTESIAN_POINT('Ctrl Pts',(-229.040769714282,1.74176805543608,
125.147594010359));
#162862=CARTESIAN_POINT('Ctrl Pts',(-229.048177933948,1.59053050703603,
125.103229094834));
#162863=CARTESIAN_POINT('Ctrl Pts',(-229.055586153615,1.43790284518368,
125.064990794117));
#162864=CARTESIAN_POINT('Ctrl Pts',(-229.062998932917,1.28518124355305,
125.026728958365));
#162865=CARTESIAN_POINT('Ctrl Pts',(-229.070411712219,1.13106818819075,
124.994601327278));
#162866=CARTESIAN_POINT('Ctrl Pts',(-229.077824491521,0.976097865799036,
124.968680407095));
#162867=CARTESIAN_POINT('Ctrl Pts',(-229.08524786255,0.820906114542193,
124.942722449886));
#162868=CARTESIAN_POINT('Ctrl Pts',(-229.092671233578,0.664855019216633,
124.922988962552));
#162869=CARTESIAN_POINT('Ctrl Pts',(-229.100094604607,0.508482898657796,
124.909500508601));
#162870=CARTESIAN_POINT('Ctrl Pts',(-229.104030654048,0.425570648240655,
124.902348606664));
#162871=CARTESIAN_POINT('Ctrl Pts',(-229.107966703489,0.342568142260644,
124.896951536459));
#162872=CARTESIAN_POINT('Ctrl Pts',(-229.111902752929,0.259555285804272,
124.893306429343));
#162873=CARTESIAN_POINT('Ctrl Pts',(-229.119326019335,0.102995629270808,
124.886431871082));
#162874=CARTESIAN_POINT('Ctrl Pts',(-229.12674928574,-0.0540740705800281,
124.885771151604));
#162875=CARTESIAN_POINT('Ctrl Pts',(-229.134172552146,-0.211119504637652,
124.891378365161));
#162876=CARTESIAN_POINT('Ctrl Pts',(-229.141587044866,-0.36797932403403,
124.896978951456));
#162877=CARTESIAN_POINT('Ctrl Pts',(-229.149001537587,-0.52481456530801,
124.90883271158));
#162878=CARTESIAN_POINT('Ctrl Pts',(-229.156416030308,-0.681087126363573,
124.92694189088));
#162879=CARTESIAN_POINT('Ctrl Pts',(-229.163823376662,-0.837209066042122,
124.94503361587));
#162880=CARTESIAN_POINT('Ctrl Pts',(-229.171230723016,-0.992769036852196,
124.969368714386));
#162881=CARTESIAN_POINT('Ctrl Pts',(-229.17863806937,-1.14723037950276,
124.999897419402));
#162882=CARTESIAN_POINT('Ctrl Pts',(-229.186039891045,-1.30157651905693,
125.030403354957));
#162883=CARTESIAN_POINT('Ctrl Pts',(-229.19344171272,-1.45482529734682,
125.067093627042));
#162884=CARTESIAN_POINT('Ctrl Pts',(-229.200843534396,-1.60644672356402,
125.109866830858));
#162885=CARTESIAN_POINT('Ctrl Pts',(-229.208241448707,-1.75798811000924,
125.152617455033));
#162886=CARTESIAN_POINT('Ctrl Pts',(-229.215639363018,-1.90790349688792,
125.201444514717));
#162887=CARTESIAN_POINT('Ctrl Pts',(-229.22303727733,-2.05567472191291,
125.256195875943));
#162888=CARTESIAN_POINT('Ctrl Pts',(-229.230433962242,-2.20342139004135,
125.310938138486));
#162889=CARTESIAN_POINT('Ctrl Pts',(-229.237830647154,-2.34902425380694,
125.371602619038));
#162890=CARTESIAN_POINT('Ctrl Pts',(-229.245227332066,-2.49198180414596,
125.437987796907));
#162891=CARTESIAN_POINT('Ctrl Pts',(-229.252623689001,-2.6349330155974,
125.504370031188));
#162892=CARTESIAN_POINT('Ctrl Pts',(-229.260020045937,-2.77523880827291,
125.576472301197));
#162893=CARTESIAN_POINT('Ctrl Pts',(-229.267416402872,-2.91241935220797,
125.654045668033));
#162894=CARTESIAN_POINT('Ctrl Pts',(-229.274813892208,-3.04962089883412,
125.731630911549));
#162895=CARTESIAN_POINT('Ctrl Pts',(-229.282211381545,-3.18369591903235,
125.814688735983));
#162896=CARTESIAN_POINT('Ctrl Pts',(-229.289608870881,-3.31419094253027,
125.902925219751));
#162897=CARTESIAN_POINT('Ctrl Pts',(-229.297008953396,-3.44473171085695,
125.991192634683));
#162898=CARTESIAN_POINT('Ctrl Pts',(-229.304409035911,-3.57168967481552,
126.084642114373));
#162899=CARTESIAN_POINT('Ctrl Pts',(-229.311809118426,-3.69464212575393,
126.182937662988));
#162900=CARTESIAN_POINT('Ctrl Pts',(-229.319217338092,-3.81772977555214,
126.281341297663));
#162901=CARTESIAN_POINT('Ctrl Pts',(-229.326625557759,-3.93680282455531,
126.384601409885));
#162902=CARTESIAN_POINT('Ctrl Pts',(-229.334033777425,-4.05147276928151,
126.49234264888));
#162903=CARTESIAN_POINT('Ctrl Pts',(-229.341446556727,-4.16621329144531,
126.600150200809));
#162904=CARTESIAN_POINT('Ctrl Pts',(-229.348859336029,-4.27654504822498,
126.712444109629));
#162905=CARTESIAN_POINT('Ctrl Pts',(-229.356272115331,-4.38211829710703,
126.82881414033));
#162906=CARTESIAN_POINT('Ctrl Pts',(-229.36369548636,-4.48784239399783,
126.945350445989));
#162907=CARTESIAN_POINT('Ctrl Pts',(-229.371118857388,-4.58879416455572,
127.065974220159));
#162908=CARTESIAN_POINT('Ctrl Pts',(-229.378542228417,-4.68466533364117,
127.190243675036));
#162909=CARTESIAN_POINT('Ctrl Pts',(-229.382478277859,-4.73549852789738,
127.25613432183));
#162910=CARTESIAN_POINT('Ctrl Pts',(-229.3864143273,-4.78490411785535,127.323049432599));
#162911=CARTESIAN_POINT('Ctrl Pts',(-229.390350376742,-4.83284132633213,
127.390920230362));
#162912=CARTESIAN_POINT('Ctrl Pts',(-229.397852896466,-4.92421463286067,
127.520289031871));
#162913=CARTESIAN_POINT('Ctrl Pts',(-229.405355416191,-5.01052398939715,
127.653519099379));
#162914=CARTESIAN_POINT('Ctrl Pts',(-229.412857935915,-5.09142960561877,
127.790181602722));
#162915=CARTESIAN_POINT('Ctrl Pts',(-229.420351182523,-5.17223522247587,
127.926675191171));
#162916=CARTESIAN_POINT('Ctrl Pts',(-229.427844429131,-5.24765021274718,
128.066592460557));
#162917=CARTESIAN_POINT('Ctrl Pts',(-229.435337675739,-5.31737629159523,
128.209473349093));
#162918=CARTESIAN_POINT('Ctrl Pts',(-229.442823031844,-5.38702894782525,
128.352203781889));
#162919=CARTESIAN_POINT('Ctrl Pts',(-229.45030838795,-5.45100446252196,
128.497891296409));
#162920=CARTESIAN_POINT('Ctrl Pts',(-229.457793744055,-5.50904898602782,
128.64604881617));
#162921=CARTESIAN_POINT('Ctrl Pts',(-229.465272587066,-5.5670430043205,
128.794077422354));
#162922=CARTESIAN_POINT('Ctrl Pts',(-229.472751430076,-5.61911617704095,
128.944571417532));
#162923=CARTESIAN_POINT('Ctrl Pts',(-229.480230273087,-5.66506157844929,
129.097021203484));
#162924=CARTESIAN_POINT('Ctrl Pts',(-229.48770333383,-5.71097145716933,
129.24935312288));
#162925=CARTESIAN_POINT('Ctrl Pts',(-229.495176394572,-5.75076290159714,
129.403637473352));
#162926=CARTESIAN_POINT('Ctrl Pts',(-229.502649455315,-5.78427797044171,
129.55934699388));
#162927=CARTESIAN_POINT('Ctrl Pts',(-229.510119103402,-5.81777773425938,
129.714985407934));
#162928=CARTESIAN_POINT('Ctrl Pts',(-229.517588751489,-5.84500675505069,
129.872047341744));
#162929=CARTESIAN_POINT('Ctrl Pts',(-229.525058399576,-5.86585754000281,
130.029992563672));
#162930=CARTESIAN_POINT('Ctrl Pts',(-229.532526496849,-5.88670399601297,
130.187904993755));
#162931=CARTESIAN_POINT('Ctrl Pts',(-229.539994594123,-5.90117480371219,
130.346699987606));
#162932=CARTESIAN_POINT('Ctrl Pts',(-229.547462691397,-5.90921395717982,
130.505829261137));
#162933=CARTESIAN_POINT('Ctrl Pts',(-229.552183396862,-5.91429563653148,
130.606417456997));
#162934=CARTESIAN_POINT('Ctrl Pts',(-229.556904102328,-5.91680844807815,
130.707139070979));
#162935=CARTESIAN_POINT('Ctrl Pts',(-229.561624807793,-5.91674896819402,
130.80785488072));
#162936=CARTESIAN_POINT('',(-231.311623378035,-5.92090363694542,130.807722361332));
#162937=CARTESIAN_POINT('Ctrl Pts',(-229.561626886787,-5.90902547570768,
130.807894616703));
#162938=CARTESIAN_POINT('Ctrl Pts',(-229.597350591376,-5.91309279083499,
131.569064203554));
#162939=CARTESIAN_POINT('Ctrl Pts',(-229.72589017057,-5.42237780748865,
134.302818932609));
#162940=CARTESIAN_POINT('Ctrl Pts',(-229.947245624369,-1.2960426407277,
137.681702691617));
#162941=CARTESIAN_POINT('Ctrl Pts',(-230.22569324818,5.08555995844198,135.61212937651));
#162942=CARTESIAN_POINT('Ctrl Pts',(-230.504140871994,6.79378139922902,
129.124451444466));
#162943=CARTESIAN_POINT('Ctrl Pts',(-230.782588495806,2.25884962879145,
124.180527974388));
#162944=CARTESIAN_POINT('Ctrl Pts',(-231.051748963516,-4.13136558520875,
125.285458413445));
#162945=CARTESIAN_POINT('Ctrl Pts',(-231.228093556619,-5.91201437708188,
129.039513442124));
#162946=CARTESIAN_POINT('Ctrl Pts',(-231.311622275119,-5.92410850363469,
130.807700850245));
#162947=CARTESIAN_POINT('',(-233.061625681752,-5.91866021983708,130.79924806649));
#162948=CARTESIAN_POINT('Ctrl Pts',(-231.311624807793,-5.91674902906247,
130.807750247089));
#162949=CARTESIAN_POINT('Ctrl Pts',(-231.320911119673,-5.9166365522368,
131.004083546839));
#162950=CARTESIAN_POINT('Ctrl Pts',(-231.330197431552,-5.90675262271671,
131.200133270132));
#162951=CARTESIAN_POINT('Ctrl Pts',(-231.339483743431,-5.88717642798294,
131.395194154446));
#162952=CARTESIAN_POINT('Ctrl Pts',(-231.346907009837,-5.87152766337025,
131.551121386745));
#162953=CARTESIAN_POINT('Ctrl Pts',(-231.354330276242,-5.84965614496523,
131.706662261903));
#162954=CARTESIAN_POINT('Ctrl Pts',(-231.361753542648,-5.82158496308475,
131.861280236121));
#162955=CARTESIAN_POINT('Ctrl Pts',(-231.369168035369,-5.79354695901001,
132.015715464733));
#162956=CARTESIAN_POINT('Ctrl Pts',(-231.37658252809,-5.75932394289552,
132.169229599925));
#162957=CARTESIAN_POINT('Ctrl Pts',(-231.383997020811,-5.71899086197203,
132.321289779782));
#162958=CARTESIAN_POINT('Ctrl Pts',(-231.391404367165,-5.67869665559046,
132.473203398312));
#162959=CARTESIAN_POINT('Ctrl Pts',(-231.398811713519,-5.63230420352266,
132.623665492975));
#162960=CARTESIAN_POINT('Ctrl Pts',(-231.406219059873,-5.57993972082383,
132.772152088854));
#162961=CARTESIAN_POINT('Ctrl Pts',(-231.413620881548,-5.52761429353179,
132.920527937828));
#162962=CARTESIAN_POINT('Ctrl Pts',(-231.421022703224,-5.46932582807081,
133.066930871227));
#162963=CARTESIAN_POINT('Ctrl Pts',(-231.428424524899,-5.40525068717784,
133.210850919076));
#162964=CARTESIAN_POINT('Ctrl Pts',(-231.435822439211,-5.34120937105298,
133.354694992653));
#162965=CARTESIAN_POINT('Ctrl Pts',(-231.443220353522,-5.27138761460429,
133.49605845083));
#162966=CARTESIAN_POINT('Ctrl Pts',(-231.450618267833,-5.19601028903398,
133.63445030497));
#162967=CARTESIAN_POINT('Ctrl Pts',(-231.458014952746,-5.1206454898076,
133.772819160895));
#162968=CARTESIAN_POINT('Ctrl Pts',(-231.465411637658,-5.03972713218782,
133.908217065379));
#162969=CARTESIAN_POINT('Ctrl Pts',(-231.47280832257,-4.95352657536361,
134.040176593432));
#162970=CARTESIAN_POINT('Ctrl Pts',(-231.480204679506,-4.86732984076243,
134.17213027026));
#162971=CARTESIAN_POINT('Ctrl Pts',(-231.487601036442,-4.7758515768148,
134.300645561276));
#162972=CARTESIAN_POINT('Ctrl Pts',(-231.494997393377,-4.67940696176591,
134.425283296757));
#162973=CARTESIAN_POINT('Ctrl Pts',(-231.502394882714,-4.58294758080025,
134.549940114593));
#162974=CARTESIAN_POINT('Ctrl Pts',(-231.50979237205,-4.48152056321827,
134.670717899579));
#162975=CARTESIAN_POINT('Ctrl Pts',(-231.517189861387,-4.37548182472375,
134.787210020194));
#162976=CARTESIAN_POINT('Ctrl Pts',(-231.524589943902,-4.26940591451367,
134.90374297694));
#162977=CARTESIAN_POINT('Ctrl Pts',(-231.531990026417,-4.1587153158174,
135.015987002296));
#162978=CARTESIAN_POINT('Ctrl Pts',(-231.539390108932,-4.04380317215016,
135.123571942265));
#162979=CARTESIAN_POINT('Ctrl Pts',(-231.546798328599,-3.92876467076787,
135.231275182935));
#162980=CARTESIAN_POINT('Ctrl Pts',(-231.554206548266,-3.80949562666422,
135.334308851678));
#162981=CARTESIAN_POINT('Ctrl Pts',(-231.561614767932,-3.68642322612335,
135.432342290001));
#162982=CARTESIAN_POINT('Ctrl Pts',(-231.569027547234,-3.56327507657316,
135.530436066271));
#162983=CARTESIAN_POINT('Ctrl Pts',(-231.576440326536,-3.43631920639107,
135.623523259479));
#162984=CARTESIAN_POINT('Ctrl Pts',(-231.583853105839,-3.30601176678733,
135.711316574202));
#162985=CARTESIAN_POINT('Ctrl Pts',(-231.591276476867,-3.17551813780325,
135.799235332129));
#162986=CARTESIAN_POINT('Ctrl Pts',(-231.598699847896,-3.04166369175963,
135.881844908749));
#162987=CARTESIAN_POINT('Ctrl Pts',(-231.606123218925,-2.9049298596653,
135.958903572371));
#162988=CARTESIAN_POINT('Ctrl Pts',(-231.610059268365,-2.83243030101829,
135.999761924813));
#162989=CARTESIAN_POINT('Ctrl Pts',(-231.613995317805,-2.75912160106797,
136.039060510985));
#162990=CARTESIAN_POINT('Ctrl Pts',(-231.617931367245,-2.68507767373807,
136.07676883853));
#162991=CARTESIAN_POINT('Ctrl Pts',(-231.625354633651,-2.5454331376027,
136.147885567456));
#162992=CARTESIAN_POINT('Ctrl Pts',(-231.632777900056,-2.40275010424733,
136.213558081908));
#162993=CARTESIAN_POINT('Ctrl Pts',(-231.640201166462,-2.25749246404825,
136.273515793392));
#162994=CARTESIAN_POINT('Ctrl Pts',(-231.647615659183,-2.11240650631658,
136.333402639841));
#162995=CARTESIAN_POINT('Ctrl Pts',(-231.655030151904,-1.96475234048154,
136.387587986999));
#162996=CARTESIAN_POINT('Ctrl Pts',(-231.662444644625,-1.81501878917212,
136.435846865214));
#162997=CARTESIAN_POINT('Ctrl Pts',(-231.669851990979,-1.66542955669681,
136.484059229706));
#162998=CARTESIAN_POINT('Ctrl Pts',(-231.677259337332,-1.51376528160977,
136.526356383284));
#162999=CARTESIAN_POINT('Ctrl Pts',(-231.684666683686,-1.36053502116693,
136.56256129301));
#163000=CARTESIAN_POINT('Ctrl Pts',(-231.692068505362,-1.20741904563294,
136.598739199747));
#163001=CARTESIAN_POINT('Ctrl Pts',(-231.699470327037,-1.05273977206209,
136.628833824533));
#163002=CARTESIAN_POINT('Ctrl Pts',(-231.706872148713,-0.897021581004777,
136.652717895102));
#163003=CARTESIAN_POINT('Ctrl Pts',(-231.714270063024,-0.741385592368861,
136.676589357457));
#163004=CARTESIAN_POINT('Ctrl Pts',(-231.721667977335,-0.584712146532838,
136.694256738441));
#163005=CARTESIAN_POINT('Ctrl Pts',(-231.729065891647,-0.427535874520726,
136.705643837214));
#163006=CARTESIAN_POINT('Ctrl Pts',(-231.736462576559,-0.270385722353779,
136.717029043657));
#163007=CARTESIAN_POINT('Ctrl Pts',(-231.743859261471,-0.112733281811311,
136.722136012316));
#163008=CARTESIAN_POINT('Ctrl Pts',(-231.751255946383,0.044881512954716,
136.720940390737));
#163009=CARTESIAN_POINT('Ctrl Pts',(-231.758652303319,0.202489318916024,
136.719744822173));
#163010=CARTESIAN_POINT('Ctrl Pts',(-231.766048660254,0.360059109133106,
136.712247221869));
#163011=CARTESIAN_POINT('Ctrl Pts',(-231.773445017189,0.517051036140522,
136.698475376249));
#163012=CARTESIAN_POINT('Ctrl Pts',(-231.780842506526,0.674066999012743,
136.684701422124));
#163013=CARTESIAN_POINT('Ctrl Pts',(-231.788239995863,0.830504550621419,
136.664651342617));
#163014=CARTESIAN_POINT('Ctrl Pts',(-231.795637485199,0.985829199218018,
136.63840478542));
#163015=CARTESIAN_POINT('Ctrl Pts',(-231.803037567714,1.14120829662918,
136.612149027532));
#163016=CARTESIAN_POINT('Ctrl Pts',(-231.810437650229,1.29547334643917,
136.579692529347));
#163017=CARTESIAN_POINT('Ctrl Pts',(-231.817837732744,1.44810042393478,
136.541165976361));
#163018=CARTESIAN_POINT('Ctrl Pts',(-231.825245952411,1.60089533059276,
136.50259705947));
#163019=CARTESIAN_POINT('Ctrl Pts',(-231.832654172077,1.75204830581659,
136.457944849484));
#163020=CARTESIAN_POINT('Ctrl Pts',(-231.840062391744,1.9010502526319,136.407390021332));
#163021=CARTESIAN_POINT('Ctrl Pts',(-231.847475171046,2.05014390765883,
136.356804077527));
#163022=CARTESIAN_POINT('Ctrl Pts',(-231.854887950348,2.19708354857286,
136.300308410078));
#163023=CARTESIAN_POINT('Ctrl Pts',(-231.86230072965,2.34138090472541,136.238131501721));
#163024=CARTESIAN_POINT('Ctrl Pts',(-231.869724100679,2.48588443970751,
136.175865752081));
#163025=CARTESIAN_POINT('Ctrl Pts',(-231.877147471707,2.62773781380484,
136.107902709685));
#163026=CARTESIAN_POINT('Ctrl Pts',(-231.884570842736,2.76647742608029,
136.034516754192));
#163027=CARTESIAN_POINT('Ctrl Pts',(-231.888506892177,2.84004049751884,
135.995605759719));
#163028=CARTESIAN_POINT('Ctrl Pts',(-231.892442941618,2.91272865405808,
135.955170919982));
#163029=CARTESIAN_POINT('Ctrl Pts',(-231.896378991058,2.98447628933346,
135.913257938995));
#163030=CARTESIAN_POINT('Ctrl Pts',(-231.903802257464,3.11979009029819,
135.834211364913));
#163031=CARTESIAN_POINT('Ctrl Pts',(-231.911225523869,3.25216590140438,
135.749665686158));
#163032=CARTESIAN_POINT('Ctrl Pts',(-231.918648790275,3.38112532480981,
135.659864927154));
#163033=CARTESIAN_POINT('Ctrl Pts',(-231.926063282996,3.50993232888618,
135.57017030519));
#163034=CARTESIAN_POINT('Ctrl Pts',(-231.933477775717,3.63533067934663,
135.475233177379));
#163035=CARTESIAN_POINT('Ctrl Pts',(-231.940892268438,3.75686688227963,
135.375343202452));
#163036=CARTESIAN_POINT('Ctrl Pts',(-231.948299614791,3.87828594404449,
135.275549505243));
#163037=CARTESIAN_POINT('Ctrl Pts',(-231.955706961145,3.99584998255798,
135.170812699932));
#163038=CARTESIAN_POINT('Ctrl Pts',(-231.963114307499,4.1091348971128,135.061465380175));
#163039=CARTESIAN_POINT('Ctrl Pts',(-231.970516129175,4.22233531950435,
134.952199615775));
#163040=CARTESIAN_POINT('Ctrl Pts',(-231.97791795085,4.33126270527624,134.838330441974));
#163041=CARTESIAN_POINT('Ctrl Pts',(-231.985319772525,4.43552653617301,
134.720230241213));
#163042=CARTESIAN_POINT('Ctrl Pts',(-231.992717686837,4.53973532700504,
134.602192384629));
#163043=CARTESIAN_POINT('Ctrl Pts',(-232.000115601148,4.63928521942924,
134.479928228397));
#163044=CARTESIAN_POINT('Ctrl Pts',(-232.007513515459,4.73382312239265,
134.353846384322));
#163045=CARTESIAN_POINT('Ctrl Pts',(-232.014910200372,4.82834531487183,
134.227785492762));
#163046=CARTESIAN_POINT('Ctrl Pts',(-232.022306885284,4.91785694722976,
134.097908470888));
#163047=CARTESIAN_POINT('Ctrl Pts',(-232.029703570196,5.00204568345988,
133.9646564175));
#163048=CARTESIAN_POINT('Ctrl Pts',(-232.037099927131,5.08623068667297,
133.831410272648));
#163049=CARTESIAN_POINT('Ctrl Pts',(-232.044496284067,5.16509306366303,
133.694789709427));
#163050=CARTESIAN_POINT('Ctrl Pts',(-232.051892641002,5.23836439119204,
133.55526393604));
#163051=CARTESIAN_POINT('Ctrl Pts',(-232.059290130339,5.31164693674857,
133.4157168009));
#163052=CARTESIAN_POINT('Ctrl Pts',(-232.066687619676,5.37933655485596,
133.273263900467));
#163053=CARTESIAN_POINT('Ctrl Pts',(-232.074085109012,5.44121134952643,
133.128397969306));
#163054=CARTESIAN_POINT('Ctrl Pts',(-232.081485191527,5.50310783431035,
132.983481255619));
#163055=CARTESIAN_POINT('Ctrl Pts',(-232.088885274042,5.55918529072697,
132.836150170137));
#163056=CARTESIAN_POINT('Ctrl Pts',(-232.096285356557,5.60927047408139,
132.686916144263));
#163057=CARTESIAN_POINT('Ctrl Pts',(-232.103693576224,5.65941073124371,
132.537518020237));
#163058=CARTESIAN_POINT('Ctrl Pts',(-232.11110179589,5.70354543759155,132.386213131119));
#163059=CARTESIAN_POINT('Ctrl Pts',(-232.118510015557,5.74155142070898,
132.233527453822));
#163060=CARTESIAN_POINT('Ctrl Pts',(-232.125922794859,5.77958079587487,
132.080747801039));
#163061=CARTESIAN_POINT('Ctrl Pts',(-232.133335574161,5.81147385592338,
131.926586031351));
#163062=CARTESIAN_POINT('Ctrl Pts',(-232.140748353463,5.83715890764027,
131.771576441183));
#163063=CARTESIAN_POINT('Ctrl Pts',(-232.148171724492,5.86288065936353,
131.616345366044));
#163064=CARTESIAN_POINT('Ctrl Pts',(-232.15559509552,5.88237664064327,131.460264420415));
#163065=CARTESIAN_POINT('Ctrl Pts',(-232.163018466549,5.89562710722712,
131.303871953803));
#163066=CARTESIAN_POINT('Ctrl Pts',(-232.16695451599,5.9026528225503,131.220948915421));
#163067=CARTESIAN_POINT('Ctrl Pts',(-232.170890565431,5.90792357082179,
131.137938292135));
#163068=CARTESIAN_POINT('Ctrl Pts',(-232.174826614871,5.91144234228026,
131.054919984575));
#163069=CARTESIAN_POINT('Ctrl Pts',(-232.182249881277,5.91807863543398,
130.898350047427));
#163070=CARTESIAN_POINT('Ctrl Pts',(-232.189673147682,5.91850032080185,
130.741279523956));
#163071=CARTESIAN_POINT('Ctrl Pts',(-232.197096414088,5.9126541173217,130.584242804977));
#163072=CARTESIAN_POINT('Ctrl Pts',(-232.204510906809,5.90681482356856,
130.42739169036));
#163073=CARTESIAN_POINT('Ctrl Pts',(-232.21192539953,5.89472240063129,130.270574670102));
#163074=CARTESIAN_POINT('Ctrl Pts',(-232.219339892251,5.8763754220661,130.114329849094));
#163075=CARTESIAN_POINT('Ctrl Pts',(-232.226747238604,5.85804612700956,
129.958235622727));
#163076=CARTESIAN_POINT('Ctrl Pts',(-232.234154584958,5.8334743208782,129.80271286593));
#163077=CARTESIAN_POINT('Ctrl Pts',(-232.241561931312,5.80271058734489,
129.648298161634));
#163078=CARTESIAN_POINT('Ctrl Pts',(-232.248963752987,5.77196979856478,
129.493998625651));
#163079=CARTESIAN_POINT('Ctrl Pts',(-232.256365574663,5.73504635041257,
129.340805861169));
#163080=CARTESIAN_POINT('Ctrl Pts',(-232.263767396338,5.69204245412661,
129.189249704062));
#163081=CARTESIAN_POINT('Ctrl Pts',(-232.27116531065,5.64906125926263,129.03777355227));
#163082=CARTESIAN_POINT('Ctrl Pts',(-232.278563224961,5.60000611041983,
128.887932645462));
#163083=CARTESIAN_POINT('Ctrl Pts',(-232.285961139272,5.54502992994455,
128.740244913803));
#163084=CARTESIAN_POINT('Ctrl Pts',(-232.293357824184,5.49006288551317,
128.592581725167));
#163085=CARTESIAN_POINT('Ctrl Pts',(-232.300754509097,5.42917689243577,
128.447071351018));
#163086=CARTESIAN_POINT('Ctrl Pts',(-232.308151194009,5.36257423438275,
128.30421499316));
#163087=CARTESIAN_POINT('Ctrl Pts',(-232.315547550944,5.29597452956138,
128.161364969703));
#163088=CARTESIAN_POINT('Ctrl Pts',(-232.32294390788,5.22365882151237,128.021169066879));
#163089=CARTESIAN_POINT('Ctrl Pts',(-232.330340264815,5.1458767790677,127.884106735255));
#163090=CARTESIAN_POINT('Ctrl Pts',(-232.337737754152,5.06808282799377,
127.747023419038));
#163091=CARTESIAN_POINT('Ctrl Pts',(-232.345135243488,4.98482106038119,
127.613074953965));
#163092=CARTESIAN_POINT('Ctrl Pts',(-232.352532732825,4.8963860875755,127.482714362484));
#163093=CARTESIAN_POINT('Ctrl Pts',(-232.35993281534,4.80792011402731,127.352308073301));
#163094=CARTESIAN_POINT('Ctrl Pts',(-232.367332897855,4.71427753413996,
127.225492470557));
#163095=CARTESIAN_POINT('Ctrl Pts',(-232.37473298037,4.615794986648,127.102689751088));
#163096=CARTESIAN_POINT('Ctrl Pts',(-232.382141200036,4.51720414747067,
126.979751997403));
#163097=CARTESIAN_POINT('Ctrl Pts',(-232.389549419703,4.41376294590961,
126.860836230597));
#163098=CARTESIAN_POINT('Ctrl Pts',(-232.396957639369,4.30584732354023,
126.746330382481));
#163099=CARTESIAN_POINT('Ctrl Pts',(-232.404370418671,4.19786528090595,
126.631754057927));
#163100=CARTESIAN_POINT('Ctrl Pts',(-232.411783197973,4.08540359596706,
126.521593321123));
#163101=CARTESIAN_POINT('Ctrl Pts',(-232.419195977275,3.96887303550515,
126.41619728987));
#163102=CARTESIAN_POINT('Ctrl Pts',(-232.426619348304,3.85217597071355,
126.310650663824));
#163103=CARTESIAN_POINT('Ctrl Pts',(-232.434042719333,3.73139870481147,
126.209882579017));
#163104=CARTESIAN_POINT('Ctrl Pts',(-232.441466090361,3.60698349423465,
126.114200637904));
#163105=CARTESIAN_POINT('Ctrl Pts',(-232.445402139802,3.54101556428341,
126.063467776869));
#163106=CARTESIAN_POINT('Ctrl Pts',(-232.449338189243,3.47402534411361,
126.014164077538));
#163107=CARTESIAN_POINT('Ctrl Pts',(-232.453274238684,3.40608167268386,
125.96633021238));
#163108=CARTESIAN_POINT('Ctrl Pts',(-232.460697505089,3.27794202881931,
125.876117035537));
#163109=CARTESIAN_POINT('Ctrl Pts',(-232.468120771495,3.14602208019629,
125.790861805098));
#163110=CARTESIAN_POINT('Ctrl Pts',(-232.4755440379,3.01074262522589,125.710898199216));
#163111=CARTESIAN_POINT('Ctrl Pts',(-232.482958530621,2.875623059337,125.631029103675));
#163112=CARTESIAN_POINT('Ctrl Pts',(-232.490373023342,2.73715220893361,
125.556439371649));
#163113=CARTESIAN_POINT('Ctrl Pts',(-232.497787516063,2.59578202587182,
125.487421062083));
#163114=CARTESIAN_POINT('Ctrl Pts',(-232.505194862417,2.45454810071496,
125.418469274962));
#163115=CARTESIAN_POINT('Ctrl Pts',(-232.512602208771,2.31042073937398,
125.355078382466));
#163116=CARTESIAN_POINT('Ctrl Pts',(-232.520009555125,2.16387872597769,
125.297495863301));
#163117=CARTESIAN_POINT('Ctrl Pts',(-232.5274113768,2.0174460091437,125.239956291352));
#163118=CARTESIAN_POINT('Ctrl Pts',(-232.534813198475,1.86860257210839,
125.188216602865));
#163119=CARTESIAN_POINT('Ctrl Pts',(-232.542215020151,1.71784942846917,
125.142477193863));
#163120=CARTESIAN_POINT('Ctrl Pts',(-232.549612934462,1.56717586624146,
125.096761930338));
#163121=CARTESIAN_POINT('Ctrl Pts',(-232.557010848773,1.41459496144134,
125.057040746177));
#163122=CARTESIAN_POINT('Ctrl Pts',(-232.564408763085,1.26062512164881,
125.023464937382));
#163123=CARTESIAN_POINT('Ctrl Pts',(-232.571805447997,1.1066808688497,124.989894708278));
#163124=CARTESIAN_POINT('Ctrl Pts',(-232.579202132909,0.95134850352873,
124.962467907119));
#163125=CARTESIAN_POINT('Ctrl Pts',(-232.586598817821,0.795159040222278,
124.941285258742));
#163126=CARTESIAN_POINT('Ctrl Pts',(-232.593995174757,0.63897650252075,
124.920103549625));
#163127=CARTESIAN_POINT('Ctrl Pts',(-232.601391531692,0.481937312310916,
124.905165492943));
#163128=CARTESIAN_POINT('Ctrl Pts',(-232.608787888628,0.32457979703512,
124.896520189977));
#163129=CARTESIAN_POINT('Ctrl Pts',(-232.616185377964,0.167198189921571,
124.887873563393));
#163130=CARTESIAN_POINT('Ctrl Pts',(-232.623582867301,0.00949853346116747,
124.885521629336));
#163131=CARTESIAN_POINT('Ctrl Pts',(-232.630980356637,-0.147978787101232,
124.889461392637));
#163132=CARTESIAN_POINT('Ctrl Pts',(-232.638380439152,-0.305511311094459,
124.893402537015));
#163133=CARTESIAN_POINT('Ctrl Pts',(-232.645780521667,-0.462820971064362,
124.903639760644));
#163134=CARTESIAN_POINT('Ctrl Pts',(-232.653180604182,-0.619370599398267,
124.920118047523));
#163135=CARTESIAN_POINT('Ctrl Pts',(-232.660588823849,-0.776092370141994,
124.936614453973));
#163136=CARTESIAN_POINT('Ctrl Pts',(-232.667997043515,-0.932052068761462,
124.959365589816));
#163137=CARTESIAN_POINT('Ctrl Pts',(-232.675405263182,-1.08672011163195,
124.988264851378));
#163138=CARTESIAN_POINT('Ctrl Pts',(-232.682818042484,-1.24148335010205,
125.017181899952));
#163139=CARTESIAN_POINT('Ctrl Pts',(-232.690230821786,-1.39495298562878,
125.052254531504));
#163140=CARTESIAN_POINT('Ctrl Pts',(-232.697643601088,-1.54661326603992,
125.093325863005));
#163141=CARTESIAN_POINT('Ctrl Pts',(-232.705066972117,-1.69849024577166,
125.134455879149));
#163142=CARTESIAN_POINT('Ctrl Pts',(-232.712490343145,-1.8485523517892,
125.181601602307));
#163143=CARTESIAN_POINT('Ctrl Pts',(-232.719913714174,-1.99630173902771,
125.234557216255));
#163144=CARTESIAN_POINT('Ctrl Pts',(-232.723849763615,-2.07464200933777,
125.262635553422));
#163145=CARTESIAN_POINT('Ctrl Pts',(-232.727785813056,-2.15233245826397,
125.292346469113));
#163146=CARTESIAN_POINT('Ctrl Pts',(-232.731721862496,-2.22930165776773,
125.323654031625));
#163147=CARTESIAN_POINT('Ctrl Pts',(-232.739145128901,-2.37446316590539,
125.382699117448));
#163148=CARTESIAN_POINT('Ctrl Pts',(-232.746568395307,-2.51749676037933,
125.447604571862));
#163149=CARTESIAN_POINT('Ctrl Pts',(-232.753991661712,-2.65789425648788,
125.518196726441));
#163150=CARTESIAN_POINT('Ctrl Pts',(-232.761406154433,-2.7981258144153,
125.588705446956));
#163151=CARTESIAN_POINT('Ctrl Pts',(-232.768820647154,-2.93572714543821,
125.664887322981));
#163152=CARTESIAN_POINT('Ctrl Pts',(-232.776235139875,-3.07020824107732,
125.746519979614));
#163153=CARTESIAN_POINT('Ctrl Pts',(-232.783642486228,-3.20455971877371,
125.828073955619));
#163154=CARTESIAN_POINT('Ctrl Pts',(-232.791049832582,-3.33579663126267,
125.915068060809));
#163155=CARTESIAN_POINT('Ctrl Pts',(-232.798457178935,-3.46345197318393,
126.007233248822));
#163156=CARTESIAN_POINT('Ctrl Pts',(-232.805859000611,-3.59101210493502,
126.099329696561));
#163157=CARTESIAN_POINT('Ctrl Pts',(-232.813260822286,-3.71499568362199,
126.196589330162));
#163158=CARTESIAN_POINT('Ctrl Pts',(-232.820662643961,-3.83496330030851,
126.298698951641));
#163159=CARTESIAN_POINT('Ctrl Pts',(-232.828060558272,-3.95486758702402,
126.400754670245));
#163160=CARTESIAN_POINT('Ctrl Pts',(-232.835458472584,-4.07075985026051,
126.507655036483));
#163161=CARTESIAN_POINT('Ctrl Pts',(-232.842856386895,-4.18223258844476,
126.619045678562));
#163162=CARTESIAN_POINT('Ctrl Pts',(-232.850253071807,-4.29368680188208,
126.730417809537));
#163163=CARTESIAN_POINT('Ctrl Pts',(-232.857649756719,-4.40072268412277,
126.846278471755));
#163164=CARTESIAN_POINT('Ctrl Pts',(-232.865046441631,-4.50296846618191,
126.966235351883));
#163165=CARTESIAN_POINT('Ctrl Pts',(-232.872442798566,-4.60520971455621,
127.086186912998));
#163166=CARTESIAN_POINT('Ctrl Pts',(-232.879839155502,-4.70266104291436,
127.21023404678));
#163167=CARTESIAN_POINT('Ctrl Pts',(-232.887235512437,-4.7949901618244,
127.337950383548));
#163168=CARTESIAN_POINT('Ctrl Pts',(-232.894633001773,-4.88733341655824,
127.465686274013));
#163169=CARTESIAN_POINT('Ctrl Pts',(-232.90203049111,-4.97455268163518,
127.597092183468));
#163170=CARTESIAN_POINT('Ctrl Pts',(-232.909427980446,-5.05635838555179,
127.73171185154));
#163171=CARTESIAN_POINT('Ctrl Pts',(-232.916828062961,-5.13819276633097,
127.866378710328));
#163172=CARTESIAN_POINT('Ctrl Pts',(-232.924228145476,-5.2146096138745,
128.004261251926));
#163173=CARTESIAN_POINT('Ctrl Pts',(-232.931628227991,-5.28536486248556,
128.144877804517));
#163174=CARTESIAN_POINT('Ctrl Pts',(-232.939036447657,-5.35619791376658,
128.285648979464));
#163175=CARTESIAN_POINT('Ctrl Pts',(-232.946444667323,-5.42135676546849,
128.429159835566));
#163176=CARTESIAN_POINT('Ctrl Pts',(-232.95385288699,-5.4806448533968,128.574907197233));
#163177=CARTESIAN_POINT('Ctrl Pts',(-232.961265666291,-5.53996943215396,
128.720744263969));
#163178=CARTESIAN_POINT('Ctrl Pts',(-232.968678445593,-5.59341592062896,
128.868820228869));
#163179=CARTESIAN_POINT('Ctrl Pts',(-232.976091224895,-5.64083753230937,
129.018616375915));
#163180=CARTESIAN_POINT('Ctrl Pts',(-232.983514595924,-5.68832690221248,
129.168626558721));
#163181=CARTESIAN_POINT('Ctrl Pts',(-232.990937966952,-5.72977410385884,
129.320361473454));
#163182=CARTESIAN_POINT('Ctrl Pts',(-232.998361337981,-5.76508319884803,
129.473291020265));
#163183=CARTESIAN_POINT('Ctrl Pts',(-233.002297387423,-5.78380492824951,
129.554377935513));
#163184=CARTESIAN_POINT('Ctrl Pts',(-233.006233436866,-5.80080187876953,
129.635800586197));
#163185=CARTESIAN_POINT('Ctrl Pts',(-233.010169486308,-5.81606567216756,
129.717479455923));
#163186=CARTESIAN_POINT('Ctrl Pts',(-233.021282375884,-5.85916087537255,
129.948088413775));
#163187=CARTESIAN_POINT('Ctrl Pts',(-233.03239526546,-5.88855019482882,
130.181332592728));
#163188=CARTESIAN_POINT('Ctrl Pts',(-233.043508155036,-5.90398369189102,
130.415892950463));
#163189=CARTESIAN_POINT('Ctrl Pts',(-233.049547039289,-5.91237044870438,
130.543356005041));
#163190=CARTESIAN_POINT('Ctrl Pts',(-233.055585923541,-5.91663678834088,
130.671207350514));
#163191=CARTESIAN_POINT('Ctrl Pts',(-233.061624807793,-5.91674777656172,
130.799231187579));
#163192=CARTESIAN_POINT('',(-234.811624807793,-5.90708423514873,130.803370312258));
#163193=CARTESIAN_POINT('Ctrl Pts',(-233.061626121642,-5.9196228110901,
130.799256562163));
#163194=CARTESIAN_POINT('Ctrl Pts',(-233.137289784469,-5.9049408922486,
132.404113396264));
#163195=CARTESIAN_POINT('Ctrl Pts',(-233.305769321901,-4.40022697300252,
136.001848438897));
#163196=CARTESIAN_POINT('Ctrl Pts',(-233.567064733934,1.69024620653965,
137.595577613887));
#163197=CARTESIAN_POINT('Ctrl Pts',(-233.84551235775,6.62726255753125,133.053127284941));
#163198=CARTESIAN_POINT('Ctrl Pts',(-234.12395998156,5.47414837784594,126.444170247007));
#163199=CARTESIAN_POINT('Ctrl Pts',(-234.402407605374,-0.709440733999325,
123.84201515248));
#163200=CARTESIAN_POINT('Ctrl Pts',(-234.631629214118,-5.26316317401156,
126.966848296847));
#163201=CARTESIAN_POINT('Ctrl Pts',(-234.768034948258,-5.90846806025998,
129.873832758555));
#163202=CARTESIAN_POINT('Ctrl Pts',(-234.811624807793,-5.90708423514873,
130.803370312258));
#163203=CARTESIAN_POINT('',(-236.561624807793,-5.91597698617805,130.809831571247));
#163204=CARTESIAN_POINT('Ctrl Pts',(-234.811624807793,-5.90708423514873,
130.803370312258));
#163205=CARTESIAN_POINT('Ctrl Pts',(-234.860850822862,-5.90552148187296,
131.853096787939));
#163206=CARTESIAN_POINT('Ctrl Pts',(-235.002892712535,-5.13706619888831,
134.884224157401));
#163207=CARTESIAN_POINT('Ctrl Pts',(-235.237750476812,-0.285723217902968,
137.796922578187));
#163208=CARTESIAN_POINT('Ctrl Pts',(-235.516198100626,5.72860003865988,
134.824398195424));
#163209=CARTESIAN_POINT('Ctrl Pts',(-235.794645724438,6.47861971736538,
128.15765566837));
#163210=CARTESIAN_POINT('Ctrl Pts',(-236.073093348251,1.27510437398114,
123.923105690896));
#163211=CARTESIAN_POINT('Ctrl Pts',(-236.328753042703,-4.57842230759621,
125.841131797943));
#163212=CARTESIAN_POINT('Ctrl Pts',(-236.49159686255,-5.90236292534572,
129.322162102131));
#163213=CARTESIAN_POINT('Ctrl Pts',(-236.561624807793,-5.91597698617805,
130.809831571247));
#163214=CARTESIAN_POINT('',(-238.311625634305,-5.92190600550432,130.802943865459));
#163215=CARTESIAN_POINT('Ctrl Pts',(-236.561624830344,-5.91674746952458,
130.809832762891));
#163216=CARTESIAN_POINT('Ctrl Pts',(-236.571197958137,-5.91655935773222,
131.013228306209));
#163217=CARTESIAN_POINT('Ctrl Pts',(-236.580771085931,-5.9058798916068,
131.216155350628));
#163218=CARTESIAN_POINT('Ctrl Pts',(-236.590344213725,-5.88487424717071,
131.417700374542));
#163219=CARTESIAN_POINT('Ctrl Pts',(-236.600141982541,-5.86337568865675,
131.623974812015));
#163220=CARTESIAN_POINT('Ctrl Pts',(-236.609939751358,-5.83106062150952,
131.828801897574));
#163221=CARTESIAN_POINT('Ctrl Pts',(-236.619737520175,-5.78815400136439,
132.031228099811));
#163222=CARTESIAN_POINT('Ctrl Pts',(-236.623154545409,-5.77319008391645,
132.101825340267));
#163223=CARTESIAN_POINT('Ctrl Pts',(-236.626571570643,-5.75693833299246,
132.17213076509));
#163224=CARTESIAN_POINT('Ctrl Pts',(-236.629988595877,-5.73940963744891,
132.24210453637));
#163225=CARTESIAN_POINT('Ctrl Pts',(-236.637411862283,-5.70132967963608,
132.394118030572));
#163226=CARTESIAN_POINT('Ctrl Pts',(-236.644835128688,-5.6571486452557,
132.544847468187));
#163227=CARTESIAN_POINT('Ctrl Pts',(-236.652258395093,-5.60696713477279,
132.693765315368));
#163228=CARTESIAN_POINT('Ctrl Pts',(-236.659672887815,-5.55684493466795,
132.842507154021));
#163229=CARTESIAN_POINT('Ctrl Pts',(-236.667087380536,-5.50073649329569,
132.989441313911));
#163230=CARTESIAN_POINT('Ctrl Pts',(-236.674501873257,-5.43879318706466,
133.134051419119));
#163231=CARTESIAN_POINT('Ctrl Pts',(-236.681909219611,-5.37690958412411,
133.278522143663));
#163232=CARTESIAN_POINT('Ctrl Pts',(-236.689316565965,-5.30920245832512,
133.420672932107));
#163233=CARTESIAN_POINT('Ctrl Pts',(-236.696723912318,-5.23587262484384,
133.560003631258));
#163234=CARTESIAN_POINT('Ctrl Pts',(-236.704125733994,-5.16259748351916,
133.699230412317));
#163235=CARTESIAN_POINT('Ctrl Pts',(-236.711527555669,-5.08370815770051,
133.835640963176));
#163236=CARTESIAN_POINT('Ctrl Pts',(-236.718929377345,-4.99945305134075,
133.968756254957));
#163237=CARTESIAN_POINT('Ctrl Pts',(-236.726327291656,-4.9152424225958,
134.101801276212));
#163238=CARTESIAN_POINT('Ctrl Pts',(-236.733725205968,-4.82567185361808,
134.231554188142));
#163239=CARTESIAN_POINT('Ctrl Pts',(-236.741123120279,-4.73103499406368,
134.357561772503));
#163240=CARTESIAN_POINT('Ctrl Pts',(-236.748519805192,-4.63641386143831,
134.483548416689));
#163241=CARTESIAN_POINT('Ctrl Pts',(-236.755916490104,-4.53672833316742,
134.605790670398));
#163242=CARTESIAN_POINT('Ctrl Pts',(-236.763313175016,-4.43231464140906,
134.723865367155));
#163243=CARTESIAN_POINT('Ctrl Pts',(-236.770709531952,-4.3279055794632,
134.841934828356));
#163244=CARTESIAN_POINT('Ctrl Pts',(-236.778105888887,-4.21876901817637,
134.955836820395));
#163245=CARTESIAN_POINT('Ctrl Pts',(-236.785502245823,-4.10528045155975,
135.06518248389));
#163246=CARTESIAN_POINT('Ctrl Pts',(-236.79289973516,-3.99177450955385,
135.174544888485));
#163247=CARTESIAN_POINT('Ctrl Pts',(-236.800297224496,-3.87391550435985,
135.279349316525));
#163248=CARTESIAN_POINT('Ctrl Pts',(-236.807694713833,-3.75211452210784,
135.379245006869));
#163249=CARTESIAN_POINT('Ctrl Pts',(-236.815094796348,-3.63027084271049,
135.479175715492));
#163250=CARTESIAN_POINT('Ctrl Pts',(-236.822494878863,-3.50448272345132,
135.574194023839));
#163251=CARTESIAN_POINT('Ctrl Pts',(-236.829894961379,-3.37519279910778,
135.66399065815));
#163252=CARTESIAN_POINT('Ctrl Pts',(-236.837303181045,-3.24576070720091,
135.753886033092));
#163253=CARTESIAN_POINT('Ctrl Pts',(-236.844711400712,-3.11281942710979,
135.838548054235));
#163254=CARTESIAN_POINT('Ctrl Pts',(-236.852119620378,-2.9768395534843,
135.917711459755));
#163255=CARTESIAN_POINT('Ctrl Pts',(-236.859532399681,-2.84077598651554,
135.99692358903));
#163256=CARTESIAN_POINT('Ctrl Pts',(-236.866945178983,-2.70167042848735,
136.070630184656));
#163257=CARTESIAN_POINT('Ctrl Pts',(-236.874357958285,-2.56001584920902,
136.138613087622));
#163258=CARTESIAN_POINT('Ctrl Pts',(-236.881781329314,-2.41815886722468,
136.206693127748));
#163259=CARTESIAN_POINT('Ctrl Pts',(-236.889204700343,-2.27374593159784,
136.269032993795));
#163260=CARTESIAN_POINT('Ctrl Pts',(-236.896628071372,-2.12728842215766,
136.325463272965));
#163261=CARTESIAN_POINT('Ctrl Pts',(-236.900564120811,-2.04963313647679,
136.355383960998));
#163262=CARTESIAN_POINT('Ctrl Pts',(-236.904500170251,-1.97140328625092,
136.383644090074));
#163263=CARTESIAN_POINT('Ctrl Pts',(-236.90843621969,-1.89267642399992,
136.410224201041));
#163264=CARTESIAN_POINT('Ctrl Pts',(-236.915859486096,-1.74420001873219,
136.460353460804));
#163265=CARTESIAN_POINT('Ctrl Pts',(-236.923282752501,-1.59350614572517,
136.504655648109));
#163266=CARTESIAN_POINT('Ctrl Pts',(-236.930706018907,-1.44109301115393,
136.542930256048));
#163267=CARTESIAN_POINT('Ctrl Pts',(-236.938120511628,-1.28886001625062,
136.581159626578));
#163268=CARTESIAN_POINT('Ctrl Pts',(-236.945535004349,-1.13491216305952,
136.613375508264));
#163269=CARTESIAN_POINT('Ctrl Pts',(-236.95294949707,-0.979765715912632,
136.639426144569));
#163270=CARTESIAN_POINT('Ctrl Pts',(-236.960356843424,-0.824768804752221,
136.66545167229));
#163271=CARTESIAN_POINT('Ctrl Pts',(-236.967764189777,-0.668575965184154,
136.685323723171));
#163272=CARTESIAN_POINT('Ctrl Pts',(-236.975171536131,-0.511716535762781,
136.698940903687));
#163273=CARTESIAN_POINT('Ctrl Pts',(-236.982573357807,-0.354974098022284,
136.712547927997));
#163274=CARTESIAN_POINT('Ctrl Pts',(-236.989975179482,-0.197566430655348,
136.719909338676));
#163275=CARTESIAN_POINT('Ctrl Pts',(-236.997377001157,-0.040030822628623,
136.720975198197));
#163276=CARTESIAN_POINT('Ctrl Pts',(-237.004774915469,0.117421623577328,
136.722040495059));
#163277=CARTESIAN_POINT('Ctrl Pts',(-237.01217282978,0.275001503591715,
136.716816856899));
#163278=CARTESIAN_POINT('Ctrl Pts',(-237.019570744091,0.432168787255593,
136.705306363955));
#163279=CARTESIAN_POINT('Ctrl Pts',(-237.026967429004,0.589309952568007,
136.693797783846));
#163280=CARTESIAN_POINT('Ctrl Pts',(-237.034364113916,0.746038285676928,
136.676004449735));
#163281=CARTESIAN_POINT('Ctrl Pts',(-237.041760798828,0.901816022947122,
136.651980511442));
#163282=CARTESIAN_POINT('Ctrl Pts',(-237.049157155763,1.0575868528692,136.627957638396));
#163283=CARTESIAN_POINT('Ctrl Pts',(-237.056553512699,1.21240680182578,
136.597704767387));
#163284=CARTESIAN_POINT('Ctrl Pts',(-237.063949869634,1.36574574772098,
136.561327624166));
#163285=CARTESIAN_POINT('Ctrl Pts',(-237.071347358971,1.51910817020024,
136.524944911512));
#163286=CARTESIAN_POINT('Ctrl Pts',(-237.078744848307,1.67098877489771,
136.48243614585));
#163287=CARTESIAN_POINT('Ctrl Pts',(-237.086142337644,1.82087025443732,
136.433957590619));
#163288=CARTESIAN_POINT('Ctrl Pts',(-237.093542420159,1.97080427469704,
136.385462041306));
#163289=CARTESIAN_POINT('Ctrl Pts',(-237.100942502674,2.11873741957135,
136.330992650683));
#163290=CARTESIAN_POINT('Ctrl Pts',(-237.108342585189,2.26417023337838,
136.270754649904));
#163291=CARTESIAN_POINT('Ctrl Pts',(-237.115750804855,2.40976296551525,
136.210450411251));
#163292=CARTESIAN_POINT('Ctrl Pts',(-237.123159024522,2.55284953081454,
136.144365037632));
#163293=CARTESIAN_POINT('Ctrl Pts',(-237.130567244188,2.69295238908918,
136.07275107316));
#163294=CARTESIAN_POINT('Ctrl Pts',(-237.13798002349,2.83314147833533,136.001093031489));
#163295=CARTESIAN_POINT('Ctrl Pts',(-237.145392802792,2.97034287667068,
135.923899801168));
#163296=CARTESIAN_POINT('Ctrl Pts',(-237.152805582094,3.104106578516,135.841468211385));
#163297=CARTESIAN_POINT('Ctrl Pts',(-237.160228953123,3.23806140821161,
135.758918839482));
#163298=CARTESIAN_POINT('Ctrl Pts',(-237.167652324152,3.36856842226183,
135.671116367089));
#163299=CARTESIAN_POINT('Ctrl Pts',(-237.175075695181,3.49520867559148,
135.578399460786));
#163300=CARTESIAN_POINT('Ctrl Pts',(-237.179011744622,3.56235637659947,
135.529238732351));
#163301=CARTESIAN_POINT('Ctrl Pts',(-237.182947794062,3.62841756849829,
135.478697033813));
#163302=CARTESIAN_POINT('Ctrl Pts',(-237.186883843503,3.69333396072086,
135.426829094158));
#163303=CARTESIAN_POINT('Ctrl Pts',(-237.194307109909,3.81576425047862,
135.329007778713));
#163304=CARTESIAN_POINT('Ctrl Pts',(-237.201730376314,3.93449065462452,
135.22617116986));
#163305=CARTESIAN_POINT('Ctrl Pts',(-237.20915364272,4.0490751884096,135.11863004368));
#163306=CARTESIAN_POINT('Ctrl Pts',(-237.21656813544,4.1635242927914,135.011216022182));
#163307=CARTESIAN_POINT('Ctrl Pts',(-237.223982628162,4.27384100149055,
134.899108804231));
#163308=CARTESIAN_POINT('Ctrl Pts',(-237.231397120883,4.37961858395188,
134.782660709515));
#163309=CARTESIAN_POINT('Ctrl Pts',(-237.238804467236,4.48529421399707,
134.666324851858));
#163310=CARTESIAN_POINT('Ctrl Pts',(-237.24621181359,4.586439178217,134.54565672122));
#163311=CARTESIAN_POINT('Ctrl Pts',(-237.253619159944,4.68268205095096,
134.421046859446));
#163312=CARTESIAN_POINT('Ctrl Pts',(-237.261020981619,4.77885314211912,
134.296529936407));
#163313=CARTESIAN_POINT('Ctrl Pts',(-237.268422803295,4.87012919451791,
134.16807743012));
#163314=CARTESIAN_POINT('Ctrl Pts',(-237.27582462497,4.95617777647921,134.036114384553));
#163315=CARTESIAN_POINT('Ctrl Pts',(-237.283222539281,5.04218093406413,
133.90422100125));
#163316=CARTESIAN_POINT('Ctrl Pts',(-237.290620453593,5.12296191358878,
133.76882108128));
#163317=CARTESIAN_POINT('Ctrl Pts',(-237.298018367904,5.19823056572549,
133.630370091729));
#163318=CARTESIAN_POINT('Ctrl Pts',(-237.305415052816,5.27348670957762,
133.491942110221));
#163319=CARTESIAN_POINT('Ctrl Pts',(-237.312811737728,5.34323216600439,
133.350464393086));
#163320=CARTESIAN_POINT('Ctrl Pts',(-237.320208422641,5.40722181840293,
133.206418645401));
#163321=CARTESIAN_POINT('Ctrl Pts',(-237.327604779576,5.47120863343322,
133.062379284856));
#163322=CARTESIAN_POINT('Ctrl Pts',(-237.335001136512,5.52944000034581,
132.915772461322));
#163323=CARTESIAN_POINT('Ctrl Pts',(-237.342397493447,5.5817183252683,132.767101328884));
#163324=CARTESIAN_POINT('Ctrl Pts',(-237.349794982784,5.63400465413579,
132.618407434516));
#163325=CARTESIAN_POINT('Ctrl Pts',(-237.35719247212,5.68033600240231,132.467648954127));
#163326=CARTESIAN_POINT('Ctrl Pts',(-237.364589961457,5.72056422165255,
132.315345577269));
#163327=CARTESIAN_POINT('Ctrl Pts',(-237.371990043972,5.76080654284263,
132.162988810699));
#163328=CARTESIAN_POINT('Ctrl Pts',(-237.379390126487,5.79494138013114,
132.009086430112));
#163329=CARTESIAN_POINT('Ctrl Pts',(-237.386790209002,5.82287143230362,
131.854169574168));
#163330=CARTESIAN_POINT('Ctrl Pts',(-237.394198428668,5.85083219643978,
131.699082371216));
#163331=CARTESIAN_POINT('Ctrl Pts',(-237.401606648335,5.87257448360726,
131.542978832741));
#163332=CARTESIAN_POINT('Ctrl Pts',(-237.409014868001,5.88805264418454,
131.386397233091));
#163333=CARTESIAN_POINT('Ctrl Pts',(-237.416427647303,5.9035403313114,131.229719260078));
#163334=CARTESIAN_POINT('Ctrl Pts',(-237.423840426605,5.91275618754745,
131.072563011375));
#163335=CARTESIAN_POINT('Ctrl Pts',(-237.431253205907,5.91570670468684,
130.915467532847));
#163336=CARTESIAN_POINT('Ctrl Pts',(-237.438676576936,5.9186614376635,130.758147588931));
#163337=CARTESIAN_POINT('Ctrl Pts',(-237.446099947965,5.91533295984985,
130.600888960837));
#163338=CARTESIAN_POINT('Ctrl Pts',(-237.453523318994,5.90577975098215,
130.444227176479));
#163339=CARTESIAN_POINT('Ctrl Pts',(-237.457459368435,5.90071441041429,
130.361161339363));
#163340=CARTESIAN_POINT('Ctrl Pts',(-237.461395417875,5.89389993587512,
130.278263165059));
#163341=CARTESIAN_POINT('Ctrl Pts',(-237.465331467316,5.88535086493392,
130.195611277425));
#163342=CARTESIAN_POINT('Ctrl Pts',(-237.472754733722,5.86922758394652,
130.039732396829));
#163343=CARTESIAN_POINT('Ctrl Pts',(-237.480178000127,5.8468827539285,129.884258811505));
#163344=CARTESIAN_POINT('Ctrl Pts',(-237.487601266533,5.81834109814454,
129.729726992491));
#163345=CARTESIAN_POINT('Ctrl Pts',(-237.495015759254,5.78983317622748,
129.575377817253));
#163346=CARTESIAN_POINT('Ctrl Pts',(-237.502430251975,5.75514307441088,
129.421968556219));
#163347=CARTESIAN_POINT('Ctrl Pts',(-237.509844744696,5.71434736142671,
129.270031840721));
#163348=CARTESIAN_POINT('Ctrl Pts',(-237.517252091049,5.67359096888664,
129.118241567549));
#163349=CARTESIAN_POINT('Ctrl Pts',(-237.524659437403,5.62674077684647,
128.967921372484));
#163350=CARTESIAN_POINT('Ctrl Pts',(-237.532066783757,5.57392459457616,
128.819594843859));
#163351=CARTESIAN_POINT('Ctrl Pts',(-237.539468605433,5.52114780460723,
128.671378942755));
#163352=CARTESIAN_POINT('Ctrl Pts',(-237.546870427108,5.46241400896619,
128.525154097524));
#163353=CARTESIAN_POINT('Ctrl Pts',(-237.554272248783,5.39790112174626,
128.381429738991));
#163354=CARTESIAN_POINT('Ctrl Pts',(-237.561670163095,5.33342229037732,
128.237781251429));
#163355=CARTESIAN_POINT('Ctrl Pts',(-237.569068077406,5.26317059559922,
128.096630961448));
#163356=CARTESIAN_POINT('Ctrl Pts',(-237.576465991717,5.18737240197308,
127.958469170981));
#163357=CARTESIAN_POINT('Ctrl Pts',(-237.58386267663,5.11158680463171,127.820330340497));
#163358=CARTESIAN_POINT('Ctrl Pts',(-237.591259361542,5.03025671717498,
127.685179350814));
#163359=CARTESIAN_POINT('Ctrl Pts',(-237.598656046454,4.94365492021578,
127.553482798834));
#163360=CARTESIAN_POINT('Ctrl Pts',(-237.606052403389,4.85705696327102,
127.421792086416));
#163361=CARTESIAN_POINT('Ctrl Pts',(-237.613448760325,4.76518796670724,
127.293555819044));
#163362=CARTESIAN_POINT('Ctrl Pts',(-237.62084511726,4.66836444399128,127.16921220511));
#163363=CARTESIAN_POINT('Ctrl Pts',(-237.628242606597,4.57152609734655,
127.044849553852));
#163364=CARTESIAN_POINT('Ctrl Pts',(-237.635640095934,4.46973194353695,
126.924381037252));
#163365=CARTESIAN_POINT('Ctrl Pts',(-237.64303758527,4.36333913426416,126.808212201666));
#163366=CARTESIAN_POINT('Ctrl Pts',(-237.650437667785,4.25690902915715,
126.692002643275));
#163367=CARTESIAN_POINT('Ctrl Pts',(-237.6578377503,4.14587731097074,126.580096041933));
#163368=CARTESIAN_POINT('Ctrl Pts',(-237.665237832815,4.03063824802058,
126.472861353328));
#163369=CARTESIAN_POINT('Ctrl Pts',(-237.672646052481,3.91527246787367,
126.365508749159));
#163370=CARTESIAN_POINT('Ctrl Pts',(-237.680054272148,3.79569037717168,
126.262838571605));
#163371=CARTESIAN_POINT('Ctrl Pts',(-237.687462491814,3.67232016663075,
126.165180177417));
#163372=CARTESIAN_POINT('Ctrl Pts',(-237.694875271117,3.54887402378378,
126.067461676118));
#163373=CARTESIAN_POINT('Ctrl Pts',(-237.702288050419,3.42163541625867,
125.974761324081));
#163374=CARTESIAN_POINT('Ctrl Pts',(-237.709700829721,3.29106136758126,
125.887365027034));
#163375=CARTESIAN_POINT('Ctrl Pts',(-237.717124200749,3.16030074857997,
125.799843854059));
#163376=CARTESIAN_POINT('Ctrl Pts',(-237.724547571778,3.02619548740785,
125.717642066971));
#163377=CARTESIAN_POINT('Ctrl Pts',(-237.731970942807,2.88922774859188,
125.64099993103));
#163378=CARTESIAN_POINT('Ctrl Pts',(-237.735906992248,2.81660416697704,
125.600362431552));
#163379=CARTESIAN_POINT('Ctrl Pts',(-237.739843041688,2.7431761951985,125.561287153868));
#163380=CARTESIAN_POINT('Ctrl Pts',(-237.743779091129,2.66901783964593,
125.523804365224));
#163381=CARTESIAN_POINT('Ctrl Pts',(-237.751202357534,2.52915749547435,
125.453112995638));
#163382=CARTESIAN_POINT('Ctrl Pts',(-237.75862562394,2.38627523847299,125.387875063449));
#163383=CARTESIAN_POINT('Ctrl Pts',(-237.766048890345,2.24083578044774,
125.328359743975));
#163384=CARTESIAN_POINT('Ctrl Pts',(-237.773463383066,2.09556821978388,
125.268914766667));
#163385=CARTESIAN_POINT('Ctrl Pts',(-237.780877875787,1.94774981631503,
125.215179078981));
#163386=CARTESIAN_POINT('Ctrl Pts',(-237.788292368508,1.7978700751362,125.167376161722));
#163387=CARTESIAN_POINT('Ctrl Pts',(-237.795699714862,1.6481347936948,125.119619318714));
#163388=CARTESIAN_POINT('Ctrl Pts',(-237.803107061216,1.4963424831204,125.077783974936));
#163389=CARTESIAN_POINT('Ctrl Pts',(-237.81051440757,1.34300273713837,125.042045613113));
#163390=CARTESIAN_POINT('Ctrl Pts',(-237.817916229245,1.18977735772408,
125.006333906309));
#163391=CARTESIAN_POINT('Ctrl Pts',(-237.82531805092,1.03500720293174,124.976710211422));
#163392=CARTESIAN_POINT('Ctrl Pts',(-237.832719872596,0.879217038255834,
124.95330020409));
#163393=CARTESIAN_POINT('Ctrl Pts',(-237.840117786907,0.723509113995637,
124.92990255472));
#163394=CARTESIAN_POINT('Ctrl Pts',(-237.847515701218,0.566782620430349,
124.912712115646));
#163395=CARTESIAN_POINT('Ctrl Pts',(-237.85491361553,0.40957241803676,124.901803460123));
#163396=CARTESIAN_POINT('Ctrl Pts',(-237.862310300442,0.252388341126501,
124.890896617421));
#163397=CARTESIAN_POINT('Ctrl Pts',(-237.869706985354,0.0947210869634865,
124.886269512216));
#163398=CARTESIAN_POINT('Ctrl Pts',(-237.877103670266,-0.0628893386807736,
124.887944853475));
#163399=CARTESIAN_POINT('Ctrl Pts',(-237.884500027202,-0.220492775713597,
124.889620120448));
#163400=CARTESIAN_POINT('Ctrl Pts',(-237.891896384137,-0.378039015961473,
124.897597274263));
#163401=CARTESIAN_POINT('Ctrl Pts',(-237.899292741072,-0.534988299031808,
124.911846885516));
#163402=CARTESIAN_POINT('Ctrl Pts',(-237.906690230409,-0.691961611438055,
124.926098678421));
#163403=CARTESIAN_POINT('Ctrl Pts',(-237.914087719746,-0.848337412893152,
124.946624807152));
#163404=CARTESIAN_POINT('Ctrl Pts',(-237.921485209082,-1.00358145654447,
124.973343997578));
#163405=CARTESIAN_POINT('Ctrl Pts',(-237.928885291597,-1.15887992075442,
125.000072554375));
#163406=CARTESIAN_POINT('Ctrl Pts',(-237.936285374112,-1.3130454696029,
125.03299843197));
#163407=CARTESIAN_POINT('Ctrl Pts',(-237.943685456627,-1.46555457856517,
125.071989350826));
#163408=CARTESIAN_POINT('Ctrl Pts',(-237.951093676293,-1.61823138697129,
125.111023144205));
#163409=CARTESIAN_POINT('Ctrl Pts',(-237.95850189596,-1.76924775609696,
125.156135205027));
#163410=CARTESIAN_POINT('Ctrl Pts',(-237.965910115626,-1.91809514123826,
125.207143309684));
#163411=CARTESIAN_POINT('Ctrl Pts',(-237.973322894928,-2.0670341394619,
125.258182808978));
#163412=CARTESIAN_POINT('Ctrl Pts',(-237.980735674231,-2.21380114638396,
125.315125448465));
#163413=CARTESIAN_POINT('Ctrl Pts',(-237.988148453533,-2.35790858904034,
125.377741260339));
#163414=CARTESIAN_POINT('Ctrl Pts',(-237.995571824561,-2.50222193916855,
125.440446540621));
#163415=CARTESIAN_POINT('Ctrl Pts',(-238.00299519559,-2.643867800088,125.508841021092));
#163416=CARTESIAN_POINT('Ctrl Pts',(-238.010418566619,-2.78238340812622,
125.582648912322));
#163417=CARTESIAN_POINT('Ctrl Pts',(-238.014354616059,-2.85582770714487,
125.621783627248));
#163418=CARTESIAN_POINT('Ctrl Pts',(-238.0182906655,-2.92839245725591,125.662439517439));
#163419=CARTESIAN_POINT('Ctrl Pts',(-238.022226714941,-3.00001219150598,
125.70457067941));
#163420=CARTESIAN_POINT('Ctrl Pts',(-238.029649981347,-3.13508477512495,
125.784028736018));
#163421=CARTESIAN_POINT('Ctrl Pts',(-238.037073247752,-3.26720264511097,
125.868976929596));
#163422=CARTESIAN_POINT('Ctrl Pts',(-238.044496514157,-3.39588814856414,
125.959169780773));
#163423=CARTESIAN_POINT('Ctrl Pts',(-238.051911006878,-3.52442155643852,
126.04925603149));
#163424=CARTESIAN_POINT('Ctrl Pts',(-238.059325499599,-3.64953037010122,
126.144574389001));
#163425=CARTESIAN_POINT('Ctrl Pts',(-238.06673999232,-3.77076197936284,
126.244833815639));
#163426=CARTESIAN_POINT('Ctrl Pts',(-238.074147338674,-3.89187674103551,
126.344996608467));
#163427=CARTESIAN_POINT('Ctrl Pts',(-238.081554685028,-4.00912145219235,
126.450090753137));
#163428=CARTESIAN_POINT('Ctrl Pts',(-238.088962031382,-4.12207302639116,
126.559782366715));
#163429=CARTESIAN_POINT('Ctrl Pts',(-238.096363853057,-4.23494035704452,
126.669392168149));
#163430=CARTESIAN_POINT('Ctrl Pts',(-238.103765674732,-4.34352065967597,
126.783592352008));
#163431=CARTESIAN_POINT('Ctrl Pts',(-238.111167496408,-4.44742455124296,
126.902009348971));
#163432=CARTESIAN_POINT('Ctrl Pts',(-238.118565410719,-4.55127359275439,
127.020363834524));
#163433=CARTESIAN_POINT('Ctrl Pts',(-238.12596332503,-4.65045089403539,
127.142930420066));
#163434=CARTESIAN_POINT('Ctrl Pts',(-238.133361239342,-4.7446046093423,
127.269299420994));
#163435=CARTESIAN_POINT('Ctrl Pts',(-238.140757924254,-4.83874267800999,
127.395647421687));
#163436=CARTESIAN_POINT('Ctrl Pts',(-238.148154609166,-4.92785859477709,
127.525796284596));
#163437=CARTESIAN_POINT('Ctrl Pts',(-238.155551294078,-5.01164136763678,
127.659303962322));
#163438=CARTESIAN_POINT('Ctrl Pts',(-238.162947651014,-5.09542042548051,
127.792805720178));
#163439=CARTESIAN_POINT('Ctrl Pts',(-238.170344007949,-5.17386661118653,
127.929665680529));
#163440=CARTESIAN_POINT('Ctrl Pts',(-238.177740364884,-5.24671293086851,
128.069413820358));
#163441=CARTESIAN_POINT('Ctrl Pts',(-238.185137854221,-5.31957040350801,
128.209183355984));
#163442=CARTESIAN_POINT('Ctrl Pts',(-238.192535343558,-5.38682613045449,
128.351841620498));
#163443=CARTESIAN_POINT('Ctrl Pts',(-238.199932832894,-5.44825971646252,
128.496895206239));
#163444=CARTESIAN_POINT('Ctrl Pts',(-238.207332915409,-5.50971483791898,
128.641999640289));
#163445=CARTESIAN_POINT('Ctrl Pts',(-238.214732997924,-5.56534360944434,
128.78950072383));
#163446=CARTESIAN_POINT('Ctrl Pts',(-238.222133080439,-5.61497434376742,
128.938886500529));
#163447=CARTESIAN_POINT('Ctrl Pts',(-238.229541300106,-5.66465965218497,
129.088436542247));
#163448=CARTESIAN_POINT('Ctrl Pts',(-238.236949519772,-5.70833363406839,
129.239875061395));
#163449=CARTESIAN_POINT('Ctrl Pts',(-238.244357739438,-5.7458747184651,
129.3926757086));
#163450=CARTESIAN_POINT('Ctrl Pts',(-238.25177051874,-5.78343890877296,
129.545570402053));
#163451=CARTESIAN_POINT('Ctrl Pts',(-238.259183298043,-5.81486260569806,
129.699828529178));
#163452=CARTESIAN_POINT('Ctrl Pts',(-238.266596077345,-5.8400757425728,
129.854915577812));
#163453=CARTESIAN_POINT('Ctrl Pts',(-238.274019448373,-5.86532490515984,
130.010224222095));
#163454=CARTESIAN_POINT('Ctrl Pts',(-238.281442819402,-5.88434573942735,
130.166363783827));
#163455=CARTESIAN_POINT('Ctrl Pts',(-238.288866190431,-5.89712013976513,
130.322795855902));
#163456=CARTESIAN_POINT('Ctrl Pts',(-238.292802239872,-5.90389343334238,
130.40573989406));
#163457=CARTESIAN_POINT('Ctrl Pts',(-238.296738289313,-5.90891150141813,
130.488766175199));
#163458=CARTESIAN_POINT('Ctrl Pts',(-238.300674338754,-5.91217757740723,
130.571794808163));
#163459=CARTESIAN_POINT('Ctrl Pts',(-238.304324495101,-5.91520642350734,
130.648792695533));
#163460=CARTESIAN_POINT('Ctrl Pts',(-238.307974651447,-5.91673115899377,
130.725850138482));
#163461=CARTESIAN_POINT('Ctrl Pts',(-238.311624807793,-5.91674982647209,
130.802927633805));
#163462=CARTESIAN_POINT('',(-240.061624807793,-5.91161849392799,130.79958681816));
#163463=CARTESIAN_POINT('Ctrl Pts',(-238.311626308619,-5.92611269417211,
130.802957108117));
#163464=CARTESIAN_POINT('Ctrl Pts',(-238.400791526601,-5.91996305970325,
132.688770394391));
#163465=CARTESIAN_POINT('Ctrl Pts',(-238.582772619189,-3.92389412409859,
136.548772126044));
#163466=CARTESIAN_POINT('Ctrl Pts',(-238.857569586381,2.65656124071048,
137.27894499841));
#163467=CARTESIAN_POINT('Ctrl Pts',(-239.136017210193,6.8831874500826,132.068991416398));
#163468=CARTESIAN_POINT('Ctrl Pts',(-239.414464834006,4.78450065523404,
125.696903910905));
#163469=CARTESIAN_POINT('Ctrl Pts',(-239.692912457819,-1.71090850592639,
124.018319605701));
#163470=CARTESIAN_POINT('Ctrl Pts',(-239.908632449081,-5.52500361660484,
127.549088971211));
#163471=CARTESIAN_POINT('Ctrl Pts',(-240.031536565739,-5.91644372475995,
130.159198921121));
#163472=CARTESIAN_POINT('Ctrl Pts',(-240.061624807793,-5.91161849392799,
130.79958681816));
#163473=CARTESIAN_POINT('',(-241.811624807794,-5.90881571325937,130.807693068847));
#163474=CARTESIAN_POINT('Ctrl Pts',(-240.061624807793,-5.91161849392799,
130.79958681816));
#163475=CARTESIAN_POINT('Ctrl Pts',(-240.124352440344,-5.90155890633036,
132.13466038688));
#163476=CARTESIAN_POINT('Ctrl Pts',(-240.279895947497,-4.79181868608966,
135.460338528975));
#163477=CARTESIAN_POINT('Ctrl Pts',(-240.528255329258,0.730628432584491,
137.76451454));
#163478=CARTESIAN_POINT('Ctrl Pts',(-240.80670295307,6.25069713114807,133.95179543103));
#163479=CARTESIAN_POINT('Ctrl Pts',(-241.085150576883,6.02668052970619,
127.246737489248));
#163480=CARTESIAN_POINT('Ctrl Pts',(-241.363598200696,0.264438941185339,
123.810961402823));
#163481=CARTESIAN_POINT('Ctrl Pts',(-241.605756277667,-4.95815660938682,
126.411990193879));
#163482=CARTESIAN_POINT('Ctrl Pts',(-241.755098480032,-5.90267469980127,
129.603172291332));
#163483=CARTESIAN_POINT('Ctrl Pts',(-241.811624807794,-5.90881571325937,
130.807693068847));
#163484=CARTESIAN_POINT('',(-243.561624807793,-5.92383771494013,130.807923172733));
#163485=CARTESIAN_POINT('Ctrl Pts',(-241.811624807794,-5.90881571325937,
130.807693068847));
#163486=CARTESIAN_POINT('Ctrl Pts',(-241.847914354636,-5.9127582052693,
131.58098783095));
#163487=CARTESIAN_POINT('Ctrl Pts',(-241.977019776084,-5.41158160550046,
134.327188727802));
#163488=CARTESIAN_POINT('Ctrl Pts',(-242.198941072135,-1.25415429483498,
137.689464649819));
#163489=CARTESIAN_POINT('Ctrl Pts',(-242.477388695948,5.11473198784157,
135.581083052765));
#163490=CARTESIAN_POINT('Ctrl Pts',(-242.755836319761,6.78342944224106,
129.083126893611));
#163491=CARTESIAN_POINT('Ctrl Pts',(-243.034283943573,2.21848662817418,
124.166900439835));
#163492=CARTESIAN_POINT('Ctrl Pts',(-243.302880106251,-4.15150118806808,
125.308311422276));
#163493=CARTESIAN_POINT('Ctrl Pts',(-243.478660394324,-5.91137340593356,
129.0514701503));
#163494=CARTESIAN_POINT('Ctrl Pts',(-243.561624807793,-5.92383771494013,
130.807923172733));
#163495=CARTESIAN_POINT('',(-245.311624807793,-5.91883942950955,130.799307097317));
#163496=CARTESIAN_POINT('Ctrl Pts',(-243.561624807793,-5.92383771494013,
130.807923172733));
#163497=CARTESIAN_POINT('Ctrl Pts',(-243.571476268929,-5.92531776705672,
131.016490050542));
#163498=CARTESIAN_POINT('Ctrl Pts',(-243.581327730064,-5.91526185254255,
131.224912612235));
#163499=CARTESIAN_POINT('Ctrl Pts',(-243.591179191199,-5.89319859537182,
131.432056249349));
#163500=CARTESIAN_POINT('Ctrl Pts',(-243.683995065804,-5.6853288709936,
133.383667039193));
#163501=CARTESIAN_POINT('Ctrl Pts',(-243.869626815012,-3.13791867181878,
137.059840370501));
#163502=CARTESIAN_POINT('Ctrl Pts',(-244.148074438826,3.56679059049603,
136.825620071692));
#163503=CARTESIAN_POINT('Ctrl Pts',(-244.426522062638,6.99379354755183,
131.058156489415));
#163504=CARTESIAN_POINT('Ctrl Pts',(-244.70496968645,3.9938419002167,125.057466899528));
#163505=CARTESIAN_POINT('Ctrl Pts',(-244.983417310265,-2.67625534339352,
124.33789188515));
#163506=CARTESIAN_POINT('Ctrl Pts',(-245.185635684044,-5.7342483307801,
128.130866893151));
#163507=CARTESIAN_POINT('Ctrl Pts',(-245.295038183221,-5.92317274697103,
130.447552151081));
#163508=CARTESIAN_POINT('Ctrl Pts',(-245.311624807793,-5.91998161812495,
130.799306122113));
#163509=CARTESIAN_POINT('',(-247.061624782818,-5.9114750784464,130.803173118476));
#163510=CARTESIAN_POINT('Ctrl Pts',(-245.311624807793,-5.91674784340849,
130.799308883118));
#163511=CARTESIAN_POINT('Ctrl Pts',(-245.31892615016,-5.91687997302728,
130.954063184845));
#163512=CARTESIAN_POINT('Ctrl Pts',(-245.326227492527,-5.91093649428155,
131.109029588657));
#163513=CARTESIAN_POINT('Ctrl Pts',(-245.333528834894,-5.89889422026084,
131.263683533033));
#163514=CARTESIAN_POINT('Ctrl Pts',(-245.340823797219,-5.88686246899084,
131.418202338075));
#163515=CARTESIAN_POINT('Ctrl Pts',(-245.348118759545,-5.86874255656274,
131.572408845108));
#163516=CARTESIAN_POINT('Ctrl Pts',(-245.355413721871,-5.84456334439123,
131.725777936645));
#163517=CARTESIAN_POINT('Ctrl Pts',(-245.362704011208,-5.82039962087947,
131.87904878339));
#163518=CARTESIAN_POINT('Ctrl Pts',(-245.369994300544,-5.79018438262468,
132.031482902934));
#163519=CARTESIAN_POINT('Ctrl Pts',(-245.377284589881,-5.75399834557609,
132.18256002317));
#163520=CARTESIAN_POINT('Ctrl Pts',(-245.384572716181,-5.71782304496787,
132.333592318645));
#163521=CARTESIAN_POINT('Ctrl Pts',(-245.39186084248,-5.67568055576135,
132.483268040689));
#163522=CARTESIAN_POINT('Ctrl Pts',(-245.399148968779,-5.62770273034245,
132.631076945132));
#163523=CARTESIAN_POINT('Ctrl Pts',(-245.406436229452,-5.57973060335499,
132.778868293988));
#163524=CARTESIAN_POINT('Ctrl Pts',(-245.413723490124,-5.52592463746925,
132.924792899662));
#163525=CARTESIAN_POINT('Ctrl Pts',(-245.421010750797,-5.46646650143819,
133.068355880625));
#163526=CARTESIAN_POINT('Ctrl Pts',(-245.428298683994,-5.40700287815248,
133.211932110686));
#163527=CARTESIAN_POINT('Ctrl Pts',(-245.435586617191,-5.34188619451485,
133.35314592632));
#163528=CARTESIAN_POINT('Ctrl Pts',(-245.442874550388,-5.27134606317935,
133.491522920945));
#163529=CARTESIAN_POINT('Ctrl Pts',(-245.450164694634,-5.20078453103629,
133.629941897055));
#163530=CARTESIAN_POINT('Ctrl Pts',(-245.45745483888,-5.12479645279535,
133.765521996797));
#163531=CARTESIAN_POINT('Ctrl Pts',(-245.464744983125,-5.04365697501847,
133.897814169965));
#163532=CARTESIAN_POINT('Ctrl Pts',(-245.472042776834,-4.96243235853778,
134.03024515576));
#163533=CARTESIAN_POINT('Ctrl Pts',(-245.479340570542,-4.87604575298051,
134.159380998799));
#163534=CARTESIAN_POINT('Ctrl Pts',(-245.486638364251,-4.78481544041778,
134.284801934934));
#163535=CARTESIAN_POINT('Ctrl Pts',(-245.49394052254,-4.69353056587861,
134.410297881379));
#163536=CARTESIAN_POINT('Ctrl Pts',(-245.501242680829,-4.59739645440353,
134.532074195589));
#163537=CARTESIAN_POINT('Ctrl Pts',(-245.508544839119,-4.49677055236318,
134.649745534827));
#163538=CARTESIAN_POINT('Ctrl Pts',(-245.515857160924,-4.39600459406856,
134.767580655027));
#163539=CARTESIAN_POINT('Ctrl Pts',(-245.523169482728,-4.29073462575644,
134.881299113301));
#163540=CARTESIAN_POINT('Ctrl Pts',(-245.530481804533,-4.18135408563361,
134.990553228168));
#163541=CARTESIAN_POINT('Ctrl Pts',(-245.533758722319,-4.13233668091564,
135.039513977122));
#163542=CARTESIAN_POINT('Ctrl Pts',(-245.537035640105,-4.08249419958879,
135.087578716439));
#163543=CARTESIAN_POINT('Ctrl Pts',(-245.54031255789,-4.03186404556836,
135.134718903038));
#163544=CARTESIAN_POINT('Ctrl Pts',(-245.547735824296,-3.91717056040364,
135.24150649626));
#163545=CARTESIAN_POINT('Ctrl Pts',(-245.555159090701,-3.79805816502304,
135.343895775135));
#163546=CARTESIAN_POINT('Ctrl Pts',(-245.562582357107,-3.67489841655756,
135.441498979798));
#163547=CARTESIAN_POINT('Ctrl Pts',(-245.569996849828,-3.55188423268733,
135.538986825578));
#163548=CARTESIAN_POINT('Ctrl Pts',(-245.577411342549,-3.42483250729264,
135.631699627332));
#163549=CARTESIAN_POINT('Ctrl Pts',(-245.584825835269,-3.2941513170682,
135.719286625428));
#163550=CARTESIAN_POINT('Ctrl Pts',(-245.592233181623,-3.1635960822946,
135.806789203878));
#163551=CARTESIAN_POINT('Ctrl Pts',(-245.599640527977,-3.02941865495771,
135.889175607681));
#163552=CARTESIAN_POINT('Ctrl Pts',(-245.607047874331,-2.89205975255052,
135.966135598149));
#163553=CARTESIAN_POINT('Ctrl Pts',(-245.614449696006,-2.75480329759579,
136.043038188953));
#163554=CARTESIAN_POINT('Ctrl Pts',(-245.621851517681,-2.61437041652712,
136.114522243312));
#163555=CARTESIAN_POINT('Ctrl Pts',(-245.629253339357,-2.47123024753988,
136.180321148126));
#163556=CARTESIAN_POINT('Ctrl Pts',(-245.636651253668,-2.32816564113242,
136.246085318212));
#163557=CARTESIAN_POINT('Ctrl Pts',(-245.644049167979,-2.18239693135943,
136.306170160162));
#163558=CARTESIAN_POINT('Ctrl Pts',(-245.651447082291,-2.03441716058419,
136.360355342115));
#163559=CARTESIAN_POINT('Ctrl Pts',(-245.658843767203,-1.88646198136328,
136.414531519475));
#163560=CARTESIAN_POINT('Ctrl Pts',(-245.666240452115,-1.73629682059031,
136.462809854446));
#163561=CARTESIAN_POINT('Ctrl Pts',(-245.673637137027,-1.58443408205927,
136.505018404358));
#163562=CARTESIAN_POINT('Ctrl Pts',(-245.681033493962,-1.43257807728075,
136.547225082698));
#163563=CARTESIAN_POINT('Ctrl Pts',(-245.688429850898,-1.27902500407501,
136.583362411157));
#163564=CARTESIAN_POINT('Ctrl Pts',(-245.695826207833,-1.12430152570741,
136.613308598207));
#163565=CARTESIAN_POINT('Ctrl Pts',(-245.70322369717,-0.969554358780719,
136.643259370094));
#163566=CARTESIAN_POINT('Ctrl Pts',(-245.710621186506,-0.813636796417068,
136.66701704228));
#163567=CARTESIAN_POINT('Ctrl Pts',(-245.718018675843,-0.657084619241684,
136.684511156936));
#163568=CARTESIAN_POINT('Ctrl Pts',(-245.725418758358,-0.500477562943501,
136.702011404127));
#163569=CARTESIAN_POINT('Ctrl Pts',(-245.732818840872,-0.343235819668255,
136.713243680774));
#163570=CARTESIAN_POINT('Ctrl Pts',(-245.740218923387,-0.185899050616081,
136.718189504631));
#163571=CARTESIAN_POINT('Ctrl Pts',(-245.747627143054,-0.0283892736110474,
136.723140766929));
#163572=CARTESIAN_POINT('Ctrl Pts',(-245.75503536272,0.129215364502986,
136.721791759783));
#163573=CARTESIAN_POINT('Ctrl Pts',(-245.762443582386,0.286375706668068,
136.714176140671));
#163574=CARTESIAN_POINT('Ctrl Pts',(-245.769856361688,0.443632778401392,
136.706555834272));
#163575=CARTESIAN_POINT('Ctrl Pts',(-245.777269140991,0.600444638309981,
136.692661263232));
#163576=CARTESIAN_POINT('Ctrl Pts',(-245.784681920293,0.756279000772,136.672577777444));
#163577=CARTESIAN_POINT('Ctrl Pts',(-245.792105291321,0.912336026678791,
136.652465595431));
#163578=CARTESIAN_POINT('Ctrl Pts',(-245.79952866235,1.06741239856714,136.626146899487));
#163579=CARTESIAN_POINT('Ctrl Pts',(-245.806952033379,1.22098692301827,
136.593757952032));
#163580=CARTESIAN_POINT('Ctrl Pts',(-245.81088808282,1.30241582086114,136.576584554927));
#163581=CARTESIAN_POINT('Ctrl Pts',(-245.814824132261,1.38342275157227,
136.557705425074));
#163582=CARTESIAN_POINT('Ctrl Pts',(-245.818760181702,1.4639320672993,136.537146455606));
#163583=CARTESIAN_POINT('Ctrl Pts',(-245.826183448107,1.61577012413466,
136.498372880818));
#163584=CARTESIAN_POINT('Ctrl Pts',(-245.833606714513,1.76629628345212,
136.453504155375));
#163585=CARTESIAN_POINT('Ctrl Pts',(-245.841029980918,1.91498347619099,
136.402643287137));
#163586=CARTESIAN_POINT('Ctrl Pts',(-245.848444473639,2.06349493301575,
136.351842532221));
#163587=CARTESIAN_POINT('Ctrl Pts',(-245.85585896636,2.21017139988103,136.295063851339));
#163588=CARTESIAN_POINT('Ctrl Pts',(-245.863273459081,2.35449719735416,
136.232460976822));
#163589=CARTESIAN_POINT('Ctrl Pts',(-245.870680805435,2.49868388819033,
136.169918441312));
#163590=CARTESIAN_POINT('Ctrl Pts',(-245.878088151789,2.64052407995554,
136.101563035246));
#163591=CARTESIAN_POINT('Ctrl Pts',(-245.885495498143,2.77951854148591,
136.027597855145));
#163592=CARTESIAN_POINT('Ctrl Pts',(-245.892897319818,2.91840933570251,
135.953687841067));
#163593=CARTESIAN_POINT('Ctrl Pts',(-245.900299141493,3.05445829764989,
135.874176558433));
#163594=CARTESIAN_POINT('Ctrl Pts',(-245.907700963169,3.18718753752367,
135.789314595604));
#163595=CARTESIAN_POINT('Ctrl Pts',(-245.91509887748,3.31984671066527,135.704497430744));
#163596=CARTESIAN_POINT('Ctrl Pts',(-245.922496791791,3.44918933811908,
135.614335411555));
#163597=CARTESIAN_POINT('Ctrl Pts',(-245.929894706103,3.57476354701164,
135.51912425379));
#163598=CARTESIAN_POINT('Ctrl Pts',(-245.937291391015,3.7003168877483,135.423928918392));
#163599=CARTESIAN_POINT('Ctrl Pts',(-245.944688075927,3.82210275565909,
135.323686335051));
#163600=CARTESIAN_POINT('Ctrl Pts',(-245.952084760839,3.93969952373787,
135.218734664377));
#163601=CARTESIAN_POINT('Ctrl Pts',(-245.959481117775,4.05729107745271,
135.11378764737));
#163602=CARTESIAN_POINT('Ctrl Pts',(-245.96687747471,4.17069362215726,135.004132206769));
#163603=CARTESIAN_POINT('Ctrl Pts',(-245.974273831645,4.27952001683103,
134.890145607998));
#163604=CARTESIAN_POINT('Ctrl Pts',(-245.981671320982,4.38836307310365,
134.776141557589));
#163605=CARTESIAN_POINT('Ctrl Pts',(-245.989068810319,4.49262832652164,
134.657805298687));
#163606=CARTESIAN_POINT('Ctrl Pts',(-245.996466299655,4.59196689640381,
134.535549514531));
#163607=CARTESIAN_POINT('Ctrl Pts',(-246.00386638217,4.6913402892678,134.413250873798));
#163608=CARTESIAN_POINT('Ctrl Pts',(-246.011266464685,4.7857833248092,134.287030261754));
#163609=CARTESIAN_POINT('Ctrl Pts',(-246.0186665472,4.87498875333009,134.157331720544));
#163610=CARTESIAN_POINT('Ctrl Pts',(-246.026074766867,4.9642922723903,134.027490562454));
#163611=CARTESIAN_POINT('Ctrl Pts',(-246.033482986533,5.0483464710805,133.8941641455));
#163612=CARTESIAN_POINT('Ctrl Pts',(-246.0408912062,5.12688823883087,133.757824270472));
#163613=CARTESIAN_POINT('Ctrl Pts',(-246.048303985502,5.2054783477292,133.621400480525));
#163614=CARTESIAN_POINT('Ctrl Pts',(-246.055716764804,5.27854909222213,
133.4819598666));
#163615=CARTESIAN_POINT('Ctrl Pts',(-246.063129544106,5.34588456621218,
133.339996389367));
#163616=CARTESIAN_POINT('Ctrl Pts',(-246.070552915135,5.4133162522849,133.19783006806));
#163617=CARTESIAN_POINT('Ctrl Pts',(-246.077976286163,5.47499615496007,
133.053134026371));
#163618=CARTESIAN_POINT('Ctrl Pts',(-246.085399657192,5.53075719789552,
132.90642041225));
#163619=CARTESIAN_POINT('Ctrl Pts',(-246.089335706633,5.56032304083054,
132.828629333691));
#163620=CARTESIAN_POINT('Ctrl Pts',(-246.093271756074,5.58822571895365,
132.750271277815));
#163621=CARTESIAN_POINT('Ctrl Pts',(-246.097207805515,5.61444612737974,
132.671423885174));
#163622=CARTESIAN_POINT('Ctrl Pts',(-246.104631071921,5.6638969993561,132.522720163409));
#163623=CARTESIAN_POINT('Ctrl Pts',(-246.112054338326,5.70751073580989,
132.37182560037));
#163624=CARTESIAN_POINT('Ctrl Pts',(-246.119477604732,5.74508910646872,
132.219239312449));
#163625=CARTESIAN_POINT('Ctrl Pts',(-246.126892097453,5.78262306261424,
132.066833368848));
#163626=CARTESIAN_POINT('Ctrl Pts',(-246.134306590174,5.81413576344467,
131.912740039266));
#163627=CARTESIAN_POINT('Ctrl Pts',(-246.141721082895,5.83947781099574,
131.757476275494));
#163628=CARTESIAN_POINT('Ctrl Pts',(-246.149128429249,5.86479543292705,
131.602362160785));
#163629=CARTESIAN_POINT('Ctrl Pts',(-246.156535775603,5.88395418216651,
131.446080223678));
#163630=CARTESIAN_POINT('Ctrl Pts',(-246.163943121956,5.89685508293014,
131.28916026012));
#163631=CARTESIAN_POINT('Ctrl Pts',(-246.171344943632,5.90974636171538,
131.132357333391));
#163632=CARTESIAN_POINT('Ctrl Pts',(-246.178746765307,5.91638905487225,
130.974917698161));
#163633=CARTESIAN_POINT('Ctrl Pts',(-246.186148586983,5.91673567837141,
130.817378865788));
#163634=CARTESIAN_POINT('Ctrl Pts',(-246.193546501294,5.91708211889073,
130.659923196939));
#163635=CARTESIAN_POINT('Ctrl Pts',(-246.200944415605,5.91113910813369,
130.502368807587));
#163636=CARTESIAN_POINT('Ctrl Pts',(-246.208342329917,5.89891119181218,
130.345255712764));
#163637=CARTESIAN_POINT('Ctrl Pts',(-246.215739014829,5.88668530754854,
130.188168727288));
#163638=CARTESIAN_POINT('Ctrl Pts',(-246.223135699741,5.86817661955672,
130.031523262602));
#163639=CARTESIAN_POINT('Ctrl Pts',(-246.230532384653,5.84344173223939,
129.875856829516));
#163640=CARTESIAN_POINT('Ctrl Pts',(-246.237928741589,5.81870794169289,
129.720197298843));
#163641=CARTESIAN_POINT('Ctrl Pts',(-246.245325098525,5.78774855933448,
129.565517082127));
#163642=CARTESIAN_POINT('Ctrl Pts',(-246.25272145546,5.75067173007351,129.412345813251));
#163643=CARTESIAN_POINT('Ctrl Pts',(-246.260118944797,5.71358922425522,
129.259151093461));
#163644=CARTESIAN_POINT('Ctrl Pts',(-246.267516434133,5.6703874944759,129.107466144354));
#163645=CARTESIAN_POINT('Ctrl Pts',(-246.27491392347,5.62122516430065,128.957807554496));
#163646=CARTESIAN_POINT('Ctrl Pts',(-246.282314005985,5.57204560034683,
128.808096502052));
#163647=CARTESIAN_POINT('Ctrl Pts',(-246.2897140885,5.51690139228881,128.660413577564));
#163648=CARTESIAN_POINT('Ctrl Pts',(-246.297114171015,5.45600004939328,
128.515257294533));
#163649=CARTESIAN_POINT('Ctrl Pts',(-246.304522390681,5.39503173921034,
128.369941397246));
#163650=CARTESIAN_POINT('Ctrl Pts',(-246.311930610348,5.32829379615479,
128.227158034306));
#163651=CARTESIAN_POINT('Ctrl Pts',(-246.319338830014,5.25604094190495,
128.087383587939));
#163652=CARTESIAN_POINT('Ctrl Pts',(-246.326751609316,5.18374361722872,
127.947523112733));
#163653=CARTESIAN_POINT('Ctrl Pts',(-246.334164388619,5.10592480181901,
127.810675568067));
#163654=CARTESIAN_POINT('Ctrl Pts',(-246.341577167921,5.02288337625871,
127.677289599664));
#163655=CARTESIAN_POINT('Ctrl Pts',(-246.34900053895,4.93972329721543,127.543713043134));
#163656=CARTESIAN_POINT('Ctrl Pts',(-246.356423909978,4.85132591334758,
127.413608249218));
#163657=CARTESIAN_POINT('Ctrl Pts',(-246.363847281007,4.75803180038588,
127.287392612449));
#163658=CARTESIAN_POINT('Ctrl Pts',(-246.367783330447,4.70856502313687,
127.220470053338));
#163659=CARTESIAN_POINT('Ctrl Pts',(-246.371719379888,4.65772225060832,
127.154640296798));
#163660=CARTESIAN_POINT('Ctrl Pts',(-246.375655429328,4.60555847733841,
127.089961382923));
#163661=CARTESIAN_POINT('Ctrl Pts',(-246.383078695734,4.50717922891786,
126.967978969904));
#163662=CARTESIAN_POINT('Ctrl Pts',(-246.390501962139,4.40380164935547,
126.849723301093));
#163663=CARTESIAN_POINT('Ctrl Pts',(-246.397925228545,4.29573851110339,
126.735630937835));
#163664=CARTESIAN_POINT('Ctrl Pts',(-246.405339721266,4.18780309450695,
126.621673422276));
#163665=CARTESIAN_POINT('Ctrl Pts',(-246.412754213987,4.07519339671987,
126.511869686004));
#163666=CARTESIAN_POINT('Ctrl Pts',(-246.420168706708,3.95826359067691,
126.406624846829));
#163667=CARTESIAN_POINT('Ctrl Pts',(-246.427576053061,3.84144648598301,
126.301481446592));
#163668=CARTESIAN_POINT('Ctrl Pts',(-246.434983399415,3.72031783810252,
126.200888443848));
#163669=CARTESIAN_POINT('Ctrl Pts',(-246.442390745769,3.59526988054162,
126.105215477376));
#163670=CARTESIAN_POINT('Ctrl Pts',(-246.449792567444,3.47031518846561,
126.009613867413));
#163671=CARTESIAN_POINT('Ctrl Pts',(-246.45719438912,3.34144730233433,125.918925213011));
#163672=CARTESIAN_POINT('Ctrl Pts',(-246.464596210795,3.20909277939671,
125.833480001848));
#163673=CARTESIAN_POINT('Ctrl Pts',(-246.471994125107,3.07680812538038,
125.748079896545));
#163674=CARTESIAN_POINT('Ctrl Pts',(-246.479392039418,2.94104081296533,
125.667917923884));
#163675=CARTESIAN_POINT('Ctrl Pts',(-246.486789953729,2.80224762916167,
125.593282150746));
#163676=CARTESIAN_POINT('Ctrl Pts',(-246.494186638642,2.66347751026779,
125.518658780719));
#163677=CARTESIAN_POINT('Ctrl Pts',(-246.501583323554,2.52168284643765,
125.449559964178));
#163678=CARTESIAN_POINT('Ctrl Pts',(-246.508980008466,2.37734645680199,
125.38622861596));
#163679=CARTESIAN_POINT('Ctrl Pts',(-246.516376365401,2.23301646719352,
125.32290007592));
#163680=CARTESIAN_POINT('Ctrl Pts',(-246.523772722337,2.08614531770971,
125.265338645704));
#163681=CARTESIAN_POINT('Ctrl Pts',(-246.531169079272,1.93723705930119,
125.213739619987));
#163682=CARTESIAN_POINT('Ctrl Pts',(-246.538566568609,1.78830600265816,
125.162132694328));
#163683=CARTESIAN_POINT('Ctrl Pts',(-246.545964057946,1.63733756882728,
125.116490113025));
#163684=CARTESIAN_POINT('Ctrl Pts',(-246.553361547282,1.48485211831284,
125.076957650318));
#163685=CARTESIAN_POINT('Ctrl Pts',(-246.560761629797,1.33231321425946,
125.037411329568));
#163686=CARTESIAN_POINT('Ctrl Pts',(-246.568161712312,1.17825659586304,
125.00397948553));
#163687=CARTESIAN_POINT('Ctrl Pts',(-246.575561794827,1.0232138404762,124.976756993506));
#163688=CARTESIAN_POINT('Ctrl Pts',(-246.582970014494,0.868000599641695,
124.949504567553));
#163689=CARTESIAN_POINT('Ctrl Pts',(-246.59037823416,0.711799424179775,
124.928475193816));
#163690=CARTESIAN_POINT('Ctrl Pts',(-246.597786453827,0.555148791238356,
124.913712063961));
#163691=CARTESIAN_POINT('Ctrl Pts',(-246.605199233129,0.398401742445324,
124.898939847647));
#163692=CARTESIAN_POINT('Ctrl Pts',(-246.612612012431,0.241205056835051,
124.890441580415));
#163693=CARTESIAN_POINT('Ctrl Pts',(-246.620024791733,0.0840977450162274,
124.888208309538));
#163694=CARTESIAN_POINT('Ctrl Pts',(-246.627448162762,-0.0732340490966529,
124.88597184766));
#163695=CARTESIAN_POINT('Ctrl Pts',(-246.634871533791,-0.230475842183839,
124.890018251153));
#163696=CARTESIAN_POINT('Ctrl Pts',(-246.642294904819,-0.387092378900183,
124.900286595952));
#163697=CARTESIAN_POINT('Ctrl Pts',(-246.64623095426,-0.470134224627617,
124.90573111875));
#163698=CARTESIAN_POINT('Ctrl Pts',(-246.650167003701,-0.553000423662025,
124.912923991829));
#163699=CARTESIAN_POINT('Ctrl Pts',(-246.654103053141,-0.635612419335864,
124.921850318817));
#163700=CARTESIAN_POINT('Ctrl Pts',(-246.661526319547,-0.791416064948631,
124.938685092936));
#163701=CARTESIAN_POINT('Ctrl Pts',(-246.668949585952,-0.946786015185273,
124.961739500879));
#163702=CARTESIAN_POINT('Ctrl Pts',(-246.676372852358,-1.10118591747281,
124.990986370396));
#163703=CARTESIAN_POINT('Ctrl Pts',(-246.683787345079,-1.25540333189839,
125.020198672542));
#163704=CARTESIAN_POINT('Ctrl Pts',(-246.6912018378,-1.4086526173274,125.055588799002));
#163705=CARTESIAN_POINT('Ctrl Pts',(-246.698616330521,-1.56040149755077,
125.097077750129));
#163706=CARTESIAN_POINT('Ctrl Pts',(-246.706023676875,-1.71200411648926,
125.138526712642));
#163707=CARTESIAN_POINT('Ctrl Pts',(-246.713431023229,-1.86210885155117,
125.186062699542));
#163708=CARTESIAN_POINT('Ctrl Pts',(-246.720838369582,-2.01019270337069,
125.23955551246));
#163709=CARTESIAN_POINT('Ctrl Pts',(-246.728240191258,-2.15816610866622,
125.29300842842));
#163710=CARTESIAN_POINT('Ctrl Pts',(-246.735642012933,-2.30412128227739,
125.352409197853));
#163711=CARTESIAN_POINT('Ctrl Pts',(-246.743043834609,-2.44754961095031,
125.417577582726));
#163712=CARTESIAN_POINT('Ctrl Pts',(-246.75044174892,-2.59090222492619,
125.482711565717));
#163713=CARTESIAN_POINT('Ctrl Pts',(-246.757839663231,-2.731730311492,125.553606946494));
#163714=CARTESIAN_POINT('Ctrl Pts',(-246.765237577543,-2.86954460728643,
125.630035124394));
#163715=CARTESIAN_POINT('Ctrl Pts',(-246.772634262455,-3.00733600084452,
125.706450601317));
#163716=CARTESIAN_POINT('Ctrl Pts',(-246.780030947367,-3.14211427150775,
125.788396869658));
#163717=CARTESIAN_POINT('Ctrl Pts',(-246.787427632279,-3.27341407261145,
125.875599021411));
#163718=CARTESIAN_POINT('Ctrl Pts',(-246.794823989215,-3.40470805174401,
125.96279730653));
#163719=CARTESIAN_POINT('Ctrl Pts',(-246.80222034615,-3.5325235570325,126.05525080515));
#163720=CARTESIAN_POINT('Ctrl Pts',(-246.809616703086,-3.65642382968436,
126.152641006474));
#163721=CARTESIAN_POINT('Ctrl Pts',(-246.817014192422,-3.78034307178426,
126.250046118487));
#163722=CARTESIAN_POINT('Ctrl Pts',(-246.824411681759,-3.90034559419467,
126.352389207441));
#163723=CARTESIAN_POINT('Ctrl Pts',(-246.831809171096,-4.01602748535452,
126.459311273844));
#163724=CARTESIAN_POINT('Ctrl Pts',(-246.839209253611,-4.13174992862215,
126.566270821612));
#163725=CARTESIAN_POINT('Ctrl Pts',(-246.846609336125,-4.24314845113487,
126.677812289459));
#163726=CARTESIAN_POINT('Ctrl Pts',(-246.85400941864,-4.34985590107221,
126.79353972872));
#163727=CARTESIAN_POINT('Ctrl Pts',(-246.861417638307,-4.45668068682071,
126.909394422197));
#163728=CARTESIAN_POINT('Ctrl Pts',(-246.868825857974,-4.55880384529215,
127.029444004784));
#163729=CARTESIAN_POINT('Ctrl Pts',(-246.87623407764,-4.65589797806187,
127.153258786559));
#163730=CARTESIAN_POINT('Ctrl Pts',(-246.883646856942,-4.75305187065021,
127.277149774267));
#163731=CARTESIAN_POINT('Ctrl Pts',(-246.891059636244,-4.84517035187053,
127.404810276891));
#163732=CARTESIAN_POINT('Ctrl Pts',(-246.898472415546,-4.93196960550558,
127.535781970376));
#163733=CARTESIAN_POINT('Ctrl Pts',(-246.905895786575,-5.01889288198459,
127.666940802357));
#163734=CARTESIAN_POINT('Ctrl Pts',(-246.913319157604,-5.10048155813349,
127.801419956128));
#163735=CARTESIAN_POINT('Ctrl Pts',(-246.920742528633,-5.17649757250621,
127.938736175261));
#163736=CARTESIAN_POINT('Ctrl Pts',(-246.924678578073,-5.21680308730434,
128.0115445295));
#163737=CARTESIAN_POINT('Ctrl Pts',(-246.928614627514,-5.2555427241668,
128.085150133234));
#163738=CARTESIAN_POINT('Ctrl Pts',(-246.932550676955,-5.29268655403647,
128.159478842662));
#163739=CARTESIAN_POINT('Ctrl Pts',(-246.940496569803,-5.36767059490483,
128.309529793383));
#163740=CARTESIAN_POINT('Ctrl Pts',(-246.948442462651,-5.43635038415996,
128.462932834914));
#163741=CARTESIAN_POINT('Ctrl Pts',(-246.956388355499,-5.4984355816421,
128.619151996626));
#163742=CARTESIAN_POINT('Ctrl Pts',(-246.96431905051,-5.56040203089155,
128.775072363293));
#163743=CARTESIAN_POINT('Ctrl Pts',(-246.972249745521,-5.61579893021929,
128.933797839802));
#163744=CARTESIAN_POINT('Ctrl Pts',(-246.980180440532,-5.66438241210903,
129.094769306202));
#163745=CARTESIAN_POINT('Ctrl Pts',(-246.988089489402,-5.71283328961795,
129.25530141501));
#163746=CARTESIAN_POINT('Ctrl Pts',(-246.995998538272,-5.75450775997896,
129.418067006546));
#163747=CARTESIAN_POINT('Ctrl Pts',(-247.003907587142,-5.78921073565506,
129.582489257448));
#163748=CARTESIAN_POINT('Ctrl Pts',(-247.011803344685,-5.82385539223615,
129.746635193231));
#163749=CARTESIAN_POINT('Ctrl Pts',(-247.019699102229,-5.85155184801984,
129.912431954205));
#163750=CARTESIAN_POINT('Ctrl Pts',(-247.027594859772,-5.87215457678867,
130.079287387609));
#163751=CARTESIAN_POINT('Ctrl Pts',(-247.035471973177,-5.89270865663014,
130.245748827676));
#163752=CARTESIAN_POINT('Ctrl Pts',(-247.043349086582,-5.90620238177112,
130.413263665022));
#163753=CARTESIAN_POINT('Ctrl Pts',(-247.051226199987,-5.91254118359208,
130.58122990514));
#163754=CARTESIAN_POINT('Ctrl Pts',(-247.05469238411,-5.91533046097139,
130.655140471724));
#163755=CARTESIAN_POINT('Ctrl Pts',(-247.058158568234,-5.91673500055715,
130.729138285269));
#163756=CARTESIAN_POINT('Ctrl Pts',(-247.061624752358,-5.91674988049034,
130.803171408753));
#163757=CARTESIAN_POINT('',(-248.811624809121,-5.91570646661543,130.809822233771));
#163758=CARTESIAN_POINT('Ctrl Pts',(-247.061624807794,-5.90715003001972,
130.803174520355));
#163759=CARTESIAN_POINT('Ctrl Pts',(-247.111415972118,-5.90525564854376,
131.864923107975));
#163760=CARTESIAN_POINT('Ctrl Pts',(-247.254023011045,-5.1238521970333,
134.908481577047));
#163761=CARTESIAN_POINT('Ctrl Pts',(-247.489445924582,-0.243152214736913,
137.798532300536));
#163762=CARTESIAN_POINT('Ctrl Pts',(-247.767893548391,5.75296501072868,
134.789452099034));
#163763=CARTESIAN_POINT('Ctrl Pts',(-248.046341172206,6.46238843929711,
128.118267508609));
#163764=CARTESIAN_POINT('Ctrl Pts',(-248.324788796018,1.23319259737722,
123.915471262371));
#163765=CARTESIAN_POINT('Ctrl Pts',(-248.579883341214,-4.59563658194247,
125.864775325139));
#163766=CARTESIAN_POINT('Ctrl Pts',(-248.742162011806,-5.90220478747528,
129.333928644561));
#163767=CARTESIAN_POINT('Ctrl Pts',(-248.811624807794,-5.91561520810599,
130.809822121327));
#163768=CARTESIAN_POINT('',(-250.561625504064,-5.9219643862223,130.803158325684));
#163769=CARTESIAN_POINT('Ctrl Pts',(-248.811624824253,-5.916747478069,130.809823516448));
#163770=CARTESIAN_POINT('Ctrl Pts',(-248.821109605322,-5.9165613768173,
131.011385752081));
#163771=CARTESIAN_POINT('Ctrl Pts',(-248.83059438639,-5.90607209373853,
131.212487319424));
#163772=CARTESIAN_POINT('Ctrl Pts',(-248.840079167459,-5.88544138888699,
131.412234140987));
#163773=CARTESIAN_POINT('Ctrl Pts',(-248.849770269771,-5.864361906919,131.616326029925));
#163774=CARTESIAN_POINT('Ctrl Pts',(-248.859461372084,-5.83269498810474,
131.81900383568));
#163775=CARTESIAN_POINT('Ctrl Pts',(-248.869152474397,-5.79066122698276,
132.019339266275));
#163776=CARTESIAN_POINT('Ctrl Pts',(-248.873329664146,-5.772543267808,132.105690548099));
#163777=CARTESIAN_POINT('Ctrl Pts',(-248.877506853895,-5.75249985213029,
132.191606933873));
#163778=CARTESIAN_POINT('Ctrl Pts',(-248.881684043643,-5.7305513441666,
132.27701531381));
#163779=CARTESIAN_POINT('Ctrl Pts',(-248.889107310048,-5.69154674260298,
132.428794188036));
#163780=CARTESIAN_POINT('Ctrl Pts',(-248.896530576453,-5.646448993928,132.579251890481));
#163781=CARTESIAN_POINT('Ctrl Pts',(-248.903953842859,-5.59536190799099,
132.727861509456));
#163782=CARTESIAN_POINT('Ctrl Pts',(-248.911368335579,-5.5443352027469,
132.876295484204));
#163783=CARTESIAN_POINT('Ctrl Pts',(-248.9187828283,-5.48733337100067,133.022885373731));
#163784=CARTESIAN_POINT('Ctrl Pts',(-248.926197321021,-5.42451092968302,
133.167115733157));
#163785=CARTESIAN_POINT('Ctrl Pts',(-248.933604667374,-5.36174903899972,
133.311207077931));
#163786=CARTESIAN_POINT('Ctrl Pts',(-248.941012013728,-5.29317785546428,
133.452943080153));
#163787=CARTESIAN_POINT('Ctrl Pts',(-248.948419360082,-5.21900123510664,
133.591824818315));
#163788=CARTESIAN_POINT('Ctrl Pts',(-248.955821181757,-5.14487993847098,
133.730602973236));
#163789=CARTESIAN_POINT('Ctrl Pts',(-248.963223003432,-5.06516170455207,
133.866530775002));
#163790=CARTESIAN_POINT('Ctrl Pts',(-248.970624825107,-4.98009784868515,
133.999130715714));
#163791=CARTESIAN_POINT('Ctrl Pts',(-248.978022739419,-4.8950788973656,
134.13166065795));
#163792=CARTESIAN_POINT('Ctrl Pts',(-248.98542065373,-4.8047201451247,134.26086592438));
#163793=CARTESIAN_POINT('Ctrl Pts',(-248.992818568041,-4.70931799504596,
134.386295092684));
#163794=CARTESIAN_POINT('Ctrl Pts',(-249.000215252953,-4.61393169907366,
134.511703416935));
#163795=CARTESIAN_POINT('Ctrl Pts',(-249.007611937866,-4.51350389445523,
134.633336591671));
#163796=CARTESIAN_POINT('Ctrl Pts',(-249.015008622778,-4.40837338305349,
134.750773504998));
#163797=CARTESIAN_POINT('Ctrl Pts',(-249.022404979713,-4.30324753324909,
134.868205211047));
#163798=CARTESIAN_POINT('Ctrl Pts',(-249.029801336648,-4.19341964026121,
134.981440747519));
#163799=CARTESIAN_POINT('Ctrl Pts',(-249.037197693584,-4.0792675582414,
135.090093547974));
#163800=CARTESIAN_POINT('Ctrl Pts',(-249.04459518292,-3.96509799924608,
135.19876298345));
#163801=CARTESIAN_POINT('Ctrl Pts',(-249.051992672257,-3.846603203412,135.302848028488));
#163802=CARTESIAN_POINT('Ctrl Pts',(-249.059390161594,-3.72419638443535,
135.402000430846));
#163803=CARTESIAN_POINT('Ctrl Pts',(-249.066790244108,-3.60174665593858,
135.501187590925));
#163804=CARTESIAN_POINT('Ctrl Pts',(-249.074190326623,-3.47538246383626,
135.595438430817));
#163805=CARTESIAN_POINT('Ctrl Pts',(-249.081590409138,-3.34554831734197,
135.684446376939));
#163806=CARTESIAN_POINT('Ctrl Pts',(-249.088998628805,-3.21557140485613,
135.773552196447));
#163807=CARTESIAN_POINT('Ctrl Pts',(-249.096406848471,-3.08211722611327,
135.857403397694));
#163808=CARTESIAN_POINT('Ctrl Pts',(-249.103815068138,-2.9456579817682,
135.935737588414));
#163809=CARTESIAN_POINT('Ctrl Pts',(-249.11122784744,-2.80911474903517,
136.014119992521));
#163810=CARTESIAN_POINT('Ctrl Pts',(-249.118640626742,-2.66956309534981,
136.086978447522));
#163811=CARTESIAN_POINT('Ctrl Pts',(-249.126053406044,-2.52749730938361,
136.154097799294));
#163812=CARTESIAN_POINT('Ctrl Pts',(-249.133476777072,-2.38522853315999,
136.221313054343));
#163813=CARTESIAN_POINT('Ctrl Pts',(-249.140900148101,-2.24043879271867,
136.282772682851));
#163814=CARTESIAN_POINT('Ctrl Pts',(-249.14832351913,-2.0936404896779,136.338310388072));
#163815=CARTESIAN_POINT('Ctrl Pts',(-249.152259568573,-2.01580450698774,
136.367757812004));
#163816=CARTESIAN_POINT('Ctrl Pts',(-249.156195618015,-1.93740407869069,
136.395541210207));
#163817=CARTESIAN_POINT('Ctrl Pts',(-249.160131667458,-1.8585168743233,
136.421641595971));
#163818=CARTESIAN_POINT('Ctrl Pts',(-249.167554933864,-1.70973806894697,
136.470866108934));
#163819=CARTESIAN_POINT('Ctrl Pts',(-249.174978200269,-1.55877730795987,
136.514250159045));
#163820=CARTESIAN_POINT('Ctrl Pts',(-249.182401466675,-1.4061340088489,
136.551596275833));
#163821=CARTESIAN_POINT('Ctrl Pts',(-249.189815959396,-1.25367112144082,
136.588898252613));
#163822=CARTESIAN_POINT('Ctrl Pts',(-249.197230452117,-1.0995300133307,
136.620176413136));
#163823=CARTESIAN_POINT('Ctrl Pts',(-249.204644944838,-0.944227863070491,
136.645282146323));
#163824=CARTESIAN_POINT('Ctrl Pts',(-249.212052291192,-0.789075398869725,
136.67036368166));
#163825=CARTESIAN_POINT('Ctrl Pts',(-249.219459637545,-0.632764486379176,
136.68928457421));
#163826=CARTESIAN_POINT('Ctrl Pts',(-249.226866983899,-0.475825071556931,
136.701946654563));
#163827=CARTESIAN_POINT('Ctrl Pts',(-249.234268805574,-0.319002708071244,
136.714599291058));
#163828=CARTESIAN_POINT('Ctrl Pts',(-249.24167062725,-0.161553146107153,
136.721002380199));
#163829=CARTESIAN_POINT('Ctrl Pts',(-249.249072448925,-0.00401396866050681,
136.721109256012));
#163830=CARTESIAN_POINT('Ctrl Pts',(-249.256470363237,0.153442045080647,
136.721216075406));
#163831=CARTESIAN_POINT('Ctrl Pts',(-249.263868277548,0.310987207736695,
136.715033300571));
#163832=CARTESIAN_POINT('Ctrl Pts',(-249.271266191859,0.468081511817204,
136.702566299025));
#163833=CARTESIAN_POINT('Ctrl Pts',(-249.278662876771,0.625149709674131,
136.690101369268));
#163834=CARTESIAN_POINT('Ctrl Pts',(-249.286059561684,0.781766825894961,
136.671354314978));
#163835=CARTESIAN_POINT('Ctrl Pts',(-249.293456246596,0.9373954364333,136.646382558491));
#163836=CARTESIAN_POINT('Ctrl Pts',(-249.300852603531,1.09301714623596,
136.621411909279));
#163837=CARTESIAN_POINT('Ctrl Pts',(-249.308248960466,1.24765006892486,
136.590217165813));
#163838=CARTESIAN_POINT('Ctrl Pts',(-249.315645317402,1.40076473580871,
136.55290727889));
#163839=CARTESIAN_POINT('Ctrl Pts',(-249.323042806738,1.55390284493894,
136.515591679728));
#163840=CARTESIAN_POINT('Ctrl Pts',(-249.330440296075,1.7055218727186,136.472159161305));
#163841=CARTESIAN_POINT('Ctrl Pts',(-249.337837785411,1.85510547257604,
136.422769133162));
#163842=CARTESIAN_POINT('Ctrl Pts',(-249.345237867926,2.00474150873273,
136.373361791421));
#163843=CARTESIAN_POINT('Ctrl Pts',(-249.352637950441,2.15234034210798,
136.317992898949));
#163844=CARTESIAN_POINT('Ctrl Pts',(-249.360038032956,2.29740377557393,
136.256870723424));
#163845=CARTESIAN_POINT('Ctrl Pts',(-249.367446252623,2.44262672119807,
136.195681337783));
#163846=CARTESIAN_POINT('Ctrl Pts',(-249.374854472289,2.58530835500866,
136.128726180037));
#163847=CARTESIAN_POINT('Ctrl Pts',(-249.382262691955,2.72497268297404,
136.056260696542));
#163848=CARTESIAN_POINT('Ctrl Pts',(-249.389675471257,2.86472297200286,
135.983750611751));
#163849=CARTESIAN_POINT('Ctrl Pts',(-249.397088250559,3.00145193121146,
135.905723627787));
#163850=CARTESIAN_POINT('Ctrl Pts',(-249.404501029861,3.13471137024171,
135.822479307651));
#163851=CARTESIAN_POINT('Ctrl Pts',(-249.41192440089,3.2681612166075,135.739116044126));
#163852=CARTESIAN_POINT('Ctrl Pts',(-249.419347771919,3.39813133409427,
135.650520765273));
#163853=CARTESIAN_POINT('Ctrl Pts',(-249.426771142948,3.52420484694847,
135.557034681632));
#163854=CARTESIAN_POINT('Ctrl Pts',(-249.430707192388,3.59105204855583,
135.507466116918));
#163855=CARTESIAN_POINT('Ctrl Pts',(-249.434643241829,3.65680435482759,
135.456523221577));
#163856=CARTESIAN_POINT('Ctrl Pts',(-249.43857929127,3.72140380942754,135.404261078411));
#163857=CARTESIAN_POINT('Ctrl Pts',(-249.446002557675,3.84323636472394,
135.305696307444));
#163858=CARTESIAN_POINT('Ctrl Pts',(-249.453425824081,3.96133457351837,
135.202138882594));
#163859=CARTESIAN_POINT('Ctrl Pts',(-249.460849090486,4.07526235095892,
135.093902240322));
#163860=CARTESIAN_POINT('Ctrl Pts',(-249.468263583207,4.18905547522797,
134.985793524773));
#163861=CARTESIAN_POINT('Ctrl Pts',(-249.475678075928,4.29868771155913,
134.87301685479));
#163862=CARTESIAN_POINT('Ctrl Pts',(-249.483092568649,4.40375448160294,
134.75592701942));
#163863=CARTESIAN_POINT('Ctrl Pts',(-249.490499915003,4.50871998433807,
134.638950039641));
#163864=CARTESIAN_POINT('Ctrl Pts',(-249.497907261357,4.60912853341538,
134.517668446599));
#163865=CARTESIAN_POINT('Ctrl Pts',(-249.505314607711,4.70461108739482,
134.392475035873));
#163866=CARTESIAN_POINT('Ctrl Pts',(-249.512716429386,4.80002242688316,
134.267374999115));
#163867=CARTESIAN_POINT('Ctrl Pts',(-249.520118251061,4.8905148612835,134.138369249516));
#163868=CARTESIAN_POINT('Ctrl Pts',(-249.527520072737,4.97575855245018,
134.005884846776));
#163869=CARTESIAN_POINT('Ctrl Pts',(-249.534917987048,5.06095724413607,
133.87347038152));
#163870=CARTESIAN_POINT('Ctrl Pts',(-249.54231590136,5.14091250923251,133.737581233445));
#163871=CARTESIAN_POINT('Ctrl Pts',(-249.549713815671,5.21533697634506,
133.59867462742));
#163872=CARTESIAN_POINT('Ctrl Pts',(-249.557110500583,5.28974907546105,
133.459791105154));
#163873=CARTESIAN_POINT('Ctrl Pts',(-249.564507185496,5.35863202464555,
133.317891448883));
#163874=CARTESIAN_POINT('Ctrl Pts',(-249.571903870408,5.42174364411263,
133.173458846856));
#163875=CARTESIAN_POINT('Ctrl Pts',(-249.579300227344,5.48485246514455,
133.029032649121));
#163876=CARTESIAN_POINT('Ctrl Pts',(-249.586696584279,5.54219031581788,
132.882074071012));
#163877=CARTESIAN_POINT('Ctrl Pts',(-249.594092941215,5.5935626687629,132.733087460103));
#163878=CARTESIAN_POINT('Ctrl Pts',(-249.601490430551,5.64494288694615,
132.584078038963));
#163879=CARTESIAN_POINT('Ctrl Pts',(-249.608887919888,5.69035566713929,
132.433040319712));
#163880=CARTESIAN_POINT('Ctrl Pts',(-249.616285409224,5.72965602716966,
132.280494884094));
#163881=CARTESIAN_POINT('Ctrl Pts',(-249.623685491739,5.76897016388037,
132.12789597391));
#163882=CARTESIAN_POINT('Ctrl Pts',(-249.631085574254,5.80216752125575,
131.973788656333));
#163883=CARTESIAN_POINT('Ctrl Pts',(-249.63848565677,5.82915403307591,131.818704652485));
#163884=CARTESIAN_POINT('Ctrl Pts',(-249.645893876436,5.85617021934014,
131.66345011783));
#163885=CARTESIAN_POINT('Ctrl Pts',(-249.653302096103,5.87696185712679,
131.507217120119));
#163886=CARTESIAN_POINT('Ctrl Pts',(-249.660710315769,5.89148657428888,
131.350544201605));
#163887=CARTESIAN_POINT('Ctrl Pts',(-249.668123095071,5.90602023117203,
131.193774853524));
#163888=CARTESIAN_POINT('Ctrl Pts',(-249.675535874373,5.91427926196693,
131.036565417029));
#163889=CARTESIAN_POINT('Ctrl Pts',(-249.682948653676,5.91627343967264,
130.87945488848));
#163890=CARTESIAN_POINT('Ctrl Pts',(-249.690372024704,5.91827046675297,
130.72211987304));
#163891=CARTESIAN_POINT('Ctrl Pts',(-249.697795395733,5.91398477270314,
130.564884419973));
#163892=CARTESIAN_POINT('Ctrl Pts',(-249.705218766762,5.9034780960863,130.408283691289));
#163893=CARTESIAN_POINT('Ctrl Pts',(-249.709154816202,5.89790720404025,
130.325250227364));
#163894=CARTESIAN_POINT('Ctrl Pts',(-249.713090865643,5.89058823104175,
130.24239507062));
#163895=CARTESIAN_POINT('Ctrl Pts',(-249.717026915084,5.88153619299649,
130.159796754964));
#163896=CARTESIAN_POINT('Ctrl Pts',(-249.724450181489,5.86446433174631,
130.004018909431));
#163897=CARTESIAN_POINT('Ctrl Pts',(-249.731873447894,5.8411735038838,129.848684223995));
#163898=CARTESIAN_POINT('Ctrl Pts',(-249.7392967143,5.81169169786706,129.694329009258));
#163899=CARTESIAN_POINT('Ctrl Pts',(-249.746711207021,5.78224473689672,
129.540156229566));
#163900=CARTESIAN_POINT('Ctrl Pts',(-249.754125699742,5.74662143209289,
129.386960979346));
#163901=CARTESIAN_POINT('Ctrl Pts',(-249.761540192463,5.704901593047,129.235275413968));
#163902=CARTESIAN_POINT('Ctrl Pts',(-249.768947538817,5.66322196515258,
129.083736048848));
#163903=CARTESIAN_POINT('Ctrl Pts',(-249.77635488517,5.61545759944475,128.933703829285));
#163904=CARTESIAN_POINT('Ctrl Pts',(-249.783762231524,5.56173949005624,
128.785701555899));
#163905=CARTESIAN_POINT('Ctrl Pts',(-249.7911640532,5.50806144566054,128.637809668193));
#163906=CARTESIAN_POINT('Ctrl Pts',(-249.798565874875,5.44843862608452,
128.491945061455));
#163907=CARTESIAN_POINT('Ctrl Pts',(-249.80596769655,5.38305204317507,128.348616074058));
#163908=CARTESIAN_POINT('Ctrl Pts',(-249.813365610862,5.31769997733359,
128.205362748917));
#163909=CARTESIAN_POINT('Ctrl Pts',(-249.820763525173,5.24659036227847,
128.06464271613));
#163910=CARTESIAN_POINT('Ctrl Pts',(-249.828161439484,5.16995254298388,
127.926944890599));
#163911=CARTESIAN_POINT('Ctrl Pts',(-249.835558124397,5.09332745950461,
127.78926994795));
#163912=CARTESIAN_POINT('Ctrl Pts',(-249.842954809309,5.01117617647154,
127.654616541628));
#163913=CARTESIAN_POINT('Ctrl Pts',(-249.850351494221,4.92377430975135,
127.523449599399));
#163914=CARTESIAN_POINT('Ctrl Pts',(-249.857747851156,4.83637631852152,
127.392288473248));
#163915=CARTESIAN_POINT('Ctrl Pts',(-249.865144208092,4.74372841352031,
127.264613814455));
#163916=CARTESIAN_POINT('Ctrl Pts',(-249.872540565027,4.64614976984916,
127.140861896585));
#163917=CARTESIAN_POINT('Ctrl Pts',(-249.879938054364,4.54855618663856,
127.017091031981));
#163918=CARTESIAN_POINT('Ctrl Pts',(-249.887335543701,4.4460305927857,126.897244397291));
#163919=CARTESIAN_POINT('Ctrl Pts',(-249.894733033037,4.33893260205083,
126.781725357272));
#163920=CARTESIAN_POINT('Ctrl Pts',(-249.902133115552,4.23179706828147,
126.666165822233));
#163921=CARTESIAN_POINT('Ctrl Pts',(-249.909533198067,4.12008620001085,
126.554937175845));
#163922=CARTESIAN_POINT('Ctrl Pts',(-249.916933280582,4.00419650418772,
126.448405966935));
#163923=CARTESIAN_POINT('Ctrl Pts',(-249.924341500248,3.88817937573012,
126.34175761601));
#163924=CARTESIAN_POINT('Ctrl Pts',(-249.931749719915,3.76797451809576,
126.239817270824));
#163925=CARTESIAN_POINT('Ctrl Pts',(-249.939157939581,3.64401211895541,
126.142911675509));
#163926=CARTESIAN_POINT('Ctrl Pts',(-249.946570718883,3.51997342302683,
126.045946436417));
#163927=CARTESIAN_POINT('Ctrl Pts',(-249.953983498185,3.39217287958458,
125.954022339421));
#163928=CARTESIAN_POINT('Ctrl Pts',(-249.961396277487,3.26106924407624,
125.86742250292));
#163929=CARTESIAN_POINT('Ctrl Pts',(-249.968819648516,3.12977828154515,
125.780698928512));
#163930=CARTESIAN_POINT('Ctrl Pts',(-249.976243019545,2.9951751194234,125.699315001221));
#163931=CARTESIAN_POINT('Ctrl Pts',(-249.983666390574,2.85774337586741,
125.623508046783));
#163932=CARTESIAN_POINT('Ctrl Pts',(-249.987602440014,2.78487376780305,
125.583313380577));
#163933=CARTESIAN_POINT('Ctrl Pts',(-249.991538489455,2.71120929416588,
125.544685803771));
#163934=CARTESIAN_POINT('Ctrl Pts',(-249.995474538896,2.63682414421973,
125.507655132554));
#163935=CARTESIAN_POINT('Ctrl Pts',(-250.002897805302,2.49653607290554,
125.437816442327));
#163936=CARTESIAN_POINT('Ctrl Pts',(-250.010321071707,2.35325934137193,
125.3734494837));
#163937=CARTESIAN_POINT('Ctrl Pts',(-250.017744338112,2.20746029136132,
125.314820598169));
#163938=CARTESIAN_POINT('Ctrl Pts',(-250.025158830833,2.06183356371996,
125.256261007111));
#163939=CARTESIAN_POINT('Ctrl Pts',(-250.032573323555,1.91369079460125,
125.203426127602));
#163940=CARTESIAN_POINT('Ctrl Pts',(-250.039987816276,1.7635228404219,125.156536456545));
#163941=CARTESIAN_POINT('Ctrl Pts',(-250.047395162629,1.61349962377008,
125.109691979519));
#163942=CARTESIAN_POINT('Ctrl Pts',(-250.054802508983,1.46145546194378,
125.068781413732));
#163943=CARTESIAN_POINT('Ctrl Pts',(-250.062209855337,1.30790100743993,
125.033977136615));
#163944=CARTESIAN_POINT('Ctrl Pts',(-250.069611677012,1.15446107964197,
124.999198817841));
#163945=CARTESIAN_POINT('Ctrl Pts',(-250.077013498688,0.999513464543592,
124.970517801673));
#163946=CARTESIAN_POINT('Ctrl Pts',(-250.084415320363,0.843583682939877,
124.948056567025));
#163947=CARTESIAN_POINT('Ctrl Pts',(-250.091813234674,0.687736215453672,
124.925607189489));
#163948=CARTESIAN_POINT('Ctrl Pts',(-250.099211148986,0.530907982584985,
124.909371107564));
#163949=CARTESIAN_POINT('Ctrl Pts',(-250.106609063297,0.373634288849452,
124.899419637277));
#163950=CARTESIAN_POINT('Ctrl Pts',(-250.114005748209,0.216386731148808,
124.889469820744));
#163951=CARTESIAN_POINT('Ctrl Pts',(-250.121402433121,0.0586942316921057,
124.885802566596));
#163952=CARTESIAN_POINT('Ctrl Pts',(-250.128799118034,-0.0989030755182705,
124.888437296211));
#163953=CARTESIAN_POINT('Ctrl Pts',(-250.136195474969,-0.256493394698895,
124.891071909));
#163954=CARTESIAN_POINT('Ctrl Pts',(-250.143591831905,-0.413988156780406,
124.900007943697));
#163955=CARTESIAN_POINT('Ctrl Pts',(-250.15098818884,-0.570847790515854,
124.915212685771));
#163956=CARTESIAN_POINT('Ctrl Pts',(-250.158385678177,-0.72773143986167,
124.93041975573));
#163957=CARTESIAN_POINT('Ctrl Pts',(-250.165783167513,-0.883979395663796,
124.951897408047));
#163958=CARTESIAN_POINT('Ctrl Pts',(-250.17318065685,-1.03905791570666,
124.979561117986));
#163959=CARTESIAN_POINT('Ctrl Pts',(-250.180580739365,-1.1941907982841,
125.007234525395));
#163960=CARTESIAN_POINT('Ctrl Pts',(-250.18798082188,-1.34815306163966,
125.041098242404));
#163961=CARTESIAN_POINT('Ctrl Pts',(-250.195380904395,-1.50042199617141,
125.081016805081));
#163962=CARTESIAN_POINT('Ctrl Pts',(-250.202789124061,-1.65285836605051,
125.120979262323));
#163963=CARTESIAN_POINT('Ctrl Pts',(-250.210197343728,-1.80359732727412,
125.167009766825));
#163964=CARTESIAN_POINT('Ctrl Pts',(-250.217605563394,-1.95213145380731,
125.2189230027));
#163965=CARTESIAN_POINT('Ctrl Pts',(-250.225018342696,-2.10075700061695,
125.270868190306));
#163966=CARTESIAN_POINT('Ctrl Pts',(-250.232431121998,-2.24717466227714,
125.328703187207));
#163967=CARTESIAN_POINT('Ctrl Pts',(-250.2398439013,-2.39089827473667,125.392195061861));
#163968=CARTESIAN_POINT('Ctrl Pts',(-250.247267272329,-2.53482724623345,
125.455777656683));
#163969=CARTESIAN_POINT('Ctrl Pts',(-250.254690643358,-2.67605414616755,
125.525033108521));
#163970=CARTESIAN_POINT('Ctrl Pts',(-250.262114014387,-2.81411789824898,
125.599682816083));
#163971=CARTESIAN_POINT('Ctrl Pts',(-250.266050063827,-2.88732261239898,
125.639263882228));
#163972=CARTESIAN_POINT('Ctrl Pts',(-250.269986113268,-2.95963853411174,
125.680360741391));
#163973=CARTESIAN_POINT('Ctrl Pts',(-250.273922162709,-3.03100047707438,
125.72292709242));
#163974=CARTESIAN_POINT('Ctrl Pts',(-250.281345429115,-3.16558687436931,
125.80320590201));
#163975=CARTESIAN_POINT('Ctrl Pts',(-250.28876869552,-3.2971851927532,125.88895676067));
#163976=CARTESIAN_POINT('Ctrl Pts',(-250.296191961926,-3.42531928247853,
125.979931285968));
#163977=CARTESIAN_POINT('Ctrl Pts',(-250.303606454647,-3.55330192835068,
126.070798286933));
#163978=CARTESIAN_POINT('Ctrl Pts',(-250.311020947368,-3.67782819414175,
126.166876451276));
#163979=CARTESIAN_POINT('Ctrl Pts',(-250.318435440089,-3.79844724967701,
126.267871991556));
#163980=CARTESIAN_POINT('Ctrl Pts',(-250.325842786442,-3.91895004802533,
126.368770188531));
#163981=CARTESIAN_POINT('Ctrl Pts',(-250.333250132796,-4.03555284902245,
126.474576087887));
#163982=CARTESIAN_POINT('Ctrl Pts',(-250.34065747915,-4.14783460650516,
126.584953237426));
#163983=CARTESIAN_POINT('Ctrl Pts',(-250.348059300825,-4.26003262001699,
126.695248063523));
#163984=CARTESIAN_POINT('Ctrl Pts',(-250.355461122501,-4.36791574197479,
126.81010709064));
#163985=CARTESIAN_POINT('Ctrl Pts',(-250.362862944176,-4.47109687057285,
126.929154386092));
#163986=CARTESIAN_POINT('Ctrl Pts',(-250.370260858488,-4.57422353065627,
127.048138837404));
#163987=CARTESIAN_POINT('Ctrl Pts',(-250.377658772799,-4.67265289681752,
127.171306872455));
#163988=CARTESIAN_POINT('Ctrl Pts',(-250.38505668711,-4.76603562369825,
127.29824667245));
#163989=CARTESIAN_POINT('Ctrl Pts',(-250.392453372023,-4.85940283206378,
127.425165377352));
#163990=CARTESIAN_POINT('Ctrl Pts',(-250.399850056935,-4.94772484465036,
127.555854302785));
#163991=CARTESIAN_POINT('Ctrl Pts',(-250.407246741847,-5.03069336608107,
127.689869516444));
#163992=CARTESIAN_POINT('Ctrl Pts',(-250.414643098783,-5.1136582086006,
127.823878787728));
#163993=CARTESIAN_POINT('Ctrl Pts',(-250.422039455718,-5.19126983545631,
127.96121373658));
#163994=CARTESIAN_POINT('Ctrl Pts',(-250.429435812654,-5.26326411887217,
128.101402723426));
#163995=CARTESIAN_POINT('Ctrl Pts',(-250.43683330199,-5.33526942479662,
128.241613173564));
#163996=CARTESIAN_POINT('Ctrl Pts',(-250.444230791327,-5.40165550430265,
128.384678199652));
#163997=CARTESIAN_POINT('Ctrl Pts',(-250.451628280663,-5.46220496974072,
128.530103061562));
#163998=CARTESIAN_POINT('Ctrl Pts',(-250.459028363178,-5.52277566070012,
128.675578901933));
#163999=CARTESIAN_POINT('Ctrl Pts',(-250.466428445694,-5.57750552059136,
128.823415880744));
#164000=CARTESIAN_POINT('Ctrl Pts',(-250.473828528209,-5.62622598174772,
128.97310100604));
#164001=CARTESIAN_POINT('Ctrl Pts',(-250.481236747875,-5.67500001605964,
129.122950725519));
#164002=CARTESIAN_POINT('Ctrl Pts',(-250.488644967542,-5.71775133951511,
129.274652294788));
#164003=CARTESIAN_POINT('Ctrl Pts',(-250.496053187208,-5.75436158745201,
129.427678634188));
#164004=CARTESIAN_POINT('Ctrl Pts',(-250.50346596651,-5.79099436838565,
129.580799158748));
#164005=CARTESIAN_POINT('Ctrl Pts',(-250.510878745812,-5.82147847009779,
129.73524571279));
#164006=CARTESIAN_POINT('Ctrl Pts',(-250.518291525114,-5.84574708094623,
129.890483367544));
#164007=CARTESIAN_POINT('Ctrl Pts',(-250.525714896143,-5.8700503679239,
130.045942833138));
#164008=CARTESIAN_POINT('Ctrl Pts',(-250.533138267172,-5.88812038394804,
130.202195287184));
#164009=CARTESIAN_POINT('Ctrl Pts',(-250.540561638201,-5.89994230118079,
130.358702222338));
#164010=CARTESIAN_POINT('Ctrl Pts',(-250.544497687641,-5.90621056535981,
130.441685954678));
#164011=CARTESIAN_POINT('Ctrl Pts',(-250.548433737081,-5.91072313592196,
130.52474124392));
#164012=CARTESIAN_POINT('Ctrl Pts',(-250.552369786522,-5.91348373254231,
130.60778822007));
#164013=CARTESIAN_POINT('Ctrl Pts',(-250.555454793612,-5.91564744015758,
130.672878995519));
#164014=CARTESIAN_POINT('Ctrl Pts',(-250.558539800703,-5.91673648840975,
130.738005692603));
#164015=CARTESIAN_POINT('Ctrl Pts',(-250.561624807794,-5.91674987505615,
130.803144672231));
#164016=CARTESIAN_POINT('',(-252.311624807794,-5.91192299704699,130.799490663889));
#164017=CARTESIAN_POINT('Ctrl Pts',(-250.561626073556,-5.92622942976624,
130.803169493092));
#164018=CARTESIAN_POINT('Ctrl Pts',(-250.651356519148,-5.92090504172026,
132.700837097956));
#164019=CARTESIAN_POINT('Ctrl Pts',(-250.833902839346,-3.90239773599972,
136.571132087067));
#164020=CARTESIAN_POINT('Ctrl Pts',(-251.109265034147,2.69592465361927,
137.262653797056));
#164021=CARTESIAN_POINT('Ctrl Pts',(-251.387712657961,6.89075808716923,
132.027068070047));
#164022=CARTESIAN_POINT('Ctrl Pts',(-251.666160281773,4.75332147089434,
125.667873926718));
#164023=CARTESIAN_POINT('Ctrl Pts',(-251.944607905586,-1.75218536453816,
124.02886012108));
#164024=CARTESIAN_POINT('Ctrl Pts',(-252.159762747593,-5.53478123322217,
127.573470886404));
#164025=CARTESIAN_POINT('Ctrl Pts',(-252.282101714996,-5.91676991525287,
130.171212797355));
#164026=CARTESIAN_POINT('Ctrl Pts',(-252.311624807794,-5.91192299704699,
130.799490663889));
#164027=CARTESIAN_POINT('',(-254.061624807794,-5.90861635227361,130.807531447417));
#164028=CARTESIAN_POINT('Ctrl Pts',(-252.311624807794,-5.91192299704699,
130.799490663889));
#164029=CARTESIAN_POINT('Ctrl Pts',(-252.3749175896,-5.90153198081667,132.146417769118));
#164030=CARTESIAN_POINT('Ctrl Pts',(-252.53102624601,-4.77598582474867,
135.484254796133));
#164031=CARTESIAN_POINT('Ctrl Pts',(-252.779950777026,0.772983328442457,
137.759938041367));
#164032=CARTESIAN_POINT('Ctrl Pts',(-253.058398400838,6.26974064878271,
133.913687349603));
#164033=CARTESIAN_POINT('Ctrl Pts',(-253.33684602465,6.00491260842544,127.210117287218));
#164034=CARTESIAN_POINT('Ctrl Pts',(-253.615293648464,0.221863234051362,
123.809481262411));
#164035=CARTESIAN_POINT('Ctrl Pts',(-253.856886576178,-4.97265101715999,
126.436108905062));
#164036=CARTESIAN_POINT('Ctrl Pts',(-254.005663629288,-5.90284313340416,
129.614952760039));
#164037=CARTESIAN_POINT('Ctrl Pts',(-254.061624807794,-5.90861635227361,
130.807531447417));
#164038=CARTESIAN_POINT('',(-255.811624807794,-5.92355635148729,130.808085951784));
#164039=CARTESIAN_POINT('Ctrl Pts',(-254.061624807794,-5.90861635227361,
130.807531447417));
#164040=CARTESIAN_POINT('Ctrl Pts',(-254.098479503892,-5.91241845638623,
131.592935298274));
#164041=CARTESIAN_POINT('Ctrl Pts',(-254.228150074594,-5.40067620360337,
134.35156746288));
#164042=CARTESIAN_POINT('Ctrl Pts',(-254.450636519901,-1.21221946432122,
137.696971457865));
#164043=CARTESIAN_POINT('Ctrl Pts',(-254.729084143717,5.1437144673035,135.54985976376));
#164044=CARTESIAN_POINT('Ctrl Pts',(-255.007531767527,6.77282616373886,
129.041866052034));
#164045=CARTESIAN_POINT('Ctrl Pts',(-255.285979391341,2.17804134336251,
124.15351899416));
#164046=CARTESIAN_POINT('Ctrl Pts',(-255.554010404761,-4.17149201360333,
125.331201206967));
#164047=CARTESIAN_POINT('Ctrl Pts',(-255.729225543581,-5.91073967446976,
129.063380221612));
#164048=CARTESIAN_POINT('Ctrl Pts',(-255.811624807794,-5.92355635148729,
130.808085951784));
#164049=CARTESIAN_POINT('',(-257.561624807794,-5.92033794655308,130.799393324114));
#164050=CARTESIAN_POINT('Ctrl Pts',(-255.811624807794,-5.92355635148729,
130.808085951784));
#164051=CARTESIAN_POINT('Ctrl Pts',(-255.822041418185,-5.92517658841868,
131.028645200844));
#164052=CARTESIAN_POINT('Ctrl Pts',(-255.832458028576,-5.91393033387313,
131.249037543385));
#164053=CARTESIAN_POINT('Ctrl Pts',(-255.842874638967,-5.88926851932256,
131.467918319388));
#164054=CARTESIAN_POINT('Ctrl Pts',(-255.935690513571,-5.66952257501434,
133.418227479128));
#164055=CARTESIAN_POINT('Ctrl Pts',(-256.121322262779,-3.09978113180407,
137.078824961414));
#164056=CARTESIAN_POINT('Ctrl Pts',(-256.399769886593,3.60337663794395,
136.803798165417));
#164057=CARTESIAN_POINT('Ctrl Pts',(-256.678217510405,6.99521075334592,
131.015575332266));
#164058=CARTESIAN_POINT('Ctrl Pts',(-256.956665134218,3.95878142380252,
125.033267860759));
#164059=CARTESIAN_POINT('Ctrl Pts',(-257.235112758031,-2.71556236807722,
124.354291237798));
#164060=CARTESIAN_POINT('Ctrl Pts',(-257.436765982556,-5.74194199984043,
128.155182833242));
#164061=CARTESIAN_POINT('Ctrl Pts',(-257.545603332477,-5.92339174586805,
130.459678785459));
#164062=CARTESIAN_POINT('Ctrl Pts',(-257.561624807794,-5.92033794655308,
130.799393324114));
#164063=CARTESIAN_POINT('',(-259.311624331364,-5.91238880389048,130.802664157255));
#164064=CARTESIAN_POINT('Ctrl Pts',(-257.561624807794,-5.92033794655308,
130.799393324114));
#164065=CARTESIAN_POINT('Ctrl Pts',(-257.638419207082,-5.90570042539457,
132.427718644327));
#164066=CARTESIAN_POINT('Ctrl Pts',(-257.808029480972,-4.36304327368764,
136.048423324747));
#164067=CARTESIAN_POINT('Ctrl Pts',(-258.070455629471,1.77275496796904,
137.574574651028));
#164068=CARTESIAN_POINT('Ctrl Pts',(-258.348903253281,6.65423282923866,
132.972130842852));
#164069=CARTESIAN_POINT('Ctrl Pts',(-258.627350877096,5.42050131933435,
126.378127222952));
#164070=CARTESIAN_POINT('Ctrl Pts',(-258.905798500908,-0.79385004661475,
123.850643128868));
#164071=CARTESIAN_POINT('Ctrl Pts',(-259.133889458064,-5.2876300368704,
127.016239948135));
#164072=CARTESIAN_POINT('Ctrl Pts',(-259.269164540617,-5.90905021799741,
129.897487457751));
#164073=CARTESIAN_POINT('Ctrl Pts',(-259.311623748564,-5.90705419484729,
130.802653254356));
#164074=CARTESIAN_POINT('',(-260.000000000001,4.64033908871117,134.475216608242));
#164075=CARTESIAN_POINT('Ctrl Pts',(-259.311624807794,-5.91674975934287,
130.802673070197));
#164076=CARTESIAN_POINT('Ctrl Pts',(-259.319249567293,-5.91679619665931,
130.965488044112));
#164077=CARTESIAN_POINT('Ctrl Pts',(-259.326874326793,-5.91011785639963,
131.128231102469));
#164078=CARTESIAN_POINT('Ctrl Pts',(-259.334499086292,-5.8967587757839,
131.290330269618));
#164079=CARTESIAN_POINT('Ctrl Pts',(-259.342129178135,-5.88339035255241,
131.452542800124));
#164080=CARTESIAN_POINT('Ctrl Pts',(-259.349759269977,-5.86333189910214,
131.614110202848));
#164081=CARTESIAN_POINT('Ctrl Pts',(-259.357389361819,-5.83667914730406,
131.774467361139));
#164082=CARTESIAN_POINT('Ctrl Pts',(-259.3650258447,-5.81000407090589,131.934958836121));
#164083=CARTESIAN_POINT('Ctrl Pts',(-259.37266232758,-5.7767237359774,132.094237710268));
#164084=CARTESIAN_POINT('Ctrl Pts',(-259.38029881046,-5.73698466795682,
132.251750503578));
#164085=CARTESIAN_POINT('Ctrl Pts',(-259.387948278586,-5.69717802673954,
132.40953113515));
#164086=CARTESIAN_POINT('Ctrl Pts',(-259.395597746712,-5.65089078706961,
132.565539354429));
#164087=CARTESIAN_POINT('Ctrl Pts',(-259.403247214838,-5.59831936063122,
132.719236827372));
#164088=CARTESIAN_POINT('Ctrl Pts',(-259.410903777593,-5.54569917593195,
132.873076849643));
#164089=CARTESIAN_POINT('Ctrl Pts',(-259.418560340348,-5.48678329977216,
133.0246015341));
#164090=CARTESIAN_POINT('Ctrl Pts',(-259.426216903103,-5.42181579432039,
133.173293722353));
#164091=CARTESIAN_POINT('Ctrl Pts',(-259.433887329274,-5.35673065493482,
133.322255141307));
#164092=CARTESIAN_POINT('Ctrl Pts',(-259.441557755446,-5.28557213369624,
133.468373507889));
#164093=CARTESIAN_POINT('Ctrl Pts',(-259.449228181618,-5.2086303301978,
133.61115605825));
#164094=CARTESIAN_POINT('Ctrl Pts',(-259.453716703923,-5.16360610422695,
133.694708477349));
#164095=CARTESIAN_POINT('Ctrl Pts',(-259.458205226229,-5.11660235328243,
133.777119156976));
#164096=CARTESIAN_POINT('Ctrl Pts',(-259.462693748535,-5.06768388172451,
133.858294250998));
#164097=CARTESIAN_POINT('Ctrl Pts',(-259.47012929275,-4.98664708755365,
133.992766346643));
#164098=CARTESIAN_POINT('Ctrl Pts',(-259.477564836965,-4.90013544228489,
134.124207857881));
#164099=CARTESIAN_POINT('Ctrl Pts',(-259.48500038118,-4.80840170338421,
134.252143038397));
#164100=CARTESIAN_POINT('Ctrl Pts',(-259.492427278007,-4.71677464898281,
134.379929432863));
#164101=CARTESIAN_POINT('Ctrl Pts',(-259.499854174834,-4.61993780523473,
134.504217314733));
#164102=CARTESIAN_POINT('Ctrl Pts',(-259.50728107166,-4.51818913327925,
134.624556622801));
#164103=CARTESIAN_POINT('Ctrl Pts',(-259.514700934918,-4.41653682138671,
134.744781964731));
#164104=CARTESIAN_POINT('Ctrl Pts',(-259.522120798177,-4.30998218112583,
134.86106589582));
#164105=CARTESIAN_POINT('Ctrl Pts',(-259.529540661435,-4.19886561158322,
134.972988465955));
#164106=CARTESIAN_POINT('Ctrl Pts',(-259.536955099493,-4.08783028742268,
135.084829201383));
#164107=CARTESIAN_POINT('Ctrl Pts',(-259.544369537551,-3.97223993690416,
135.192314663084));
#164108=CARTESIAN_POINT('Ctrl Pts',(-259.551783975609,-3.85247419313978,
135.295059132685));
#164109=CARTESIAN_POINT('Ctrl Pts',(-259.559194592593,-3.73277017134383,
135.39775065233));
#164110=CARTESIAN_POINT('Ctrl Pts',(-259.566605209578,-3.6088953235766,
135.49570580466));
#164111=CARTESIAN_POINT('Ctrl Pts',(-259.574015826562,-3.48126490870701,
135.588576875001));
#164112=CARTESIAN_POINT('Ctrl Pts',(-259.581425300866,-3.35365417381794,
135.681433625081));
#164113=CARTESIAN_POINT('Ctrl Pts',(-259.58883477517,-3.22228932129518,
135.769207630182));
#164114=CARTESIAN_POINT('Ctrl Pts',(-259.596244249474,-3.08761745835792,
135.851592432466));
#164115=CARTESIAN_POINT('Ctrl Pts',(-259.603653447889,-2.95295060988279,
135.93397416718));
#164116=CARTESIAN_POINT('Ctrl Pts',(-259.611062646304,-2.81497731298843,
136.010966903991));
#164117=CARTESIAN_POINT('Ctrl Pts',(-259.618471844718,-2.67417210930629,
136.082308522984));
#164118=CARTESIAN_POINT('Ctrl Pts',(-259.625882215982,-2.53334461666666,
136.153661435099));
#164119=CARTESIAN_POINT('Ctrl Pts',(-259.633292587246,-2.38968465629391,
136.219361280047));
#164120=CARTESIAN_POINT('Ctrl Pts',(-259.640702958511,-2.24368959943131,
136.279192810785));
#164121=CARTESIAN_POINT('Ctrl Pts',(-259.648115951775,-2.09764288535344,
136.339045511624));
#164122=CARTESIAN_POINT('Ctrl Pts',(-259.65552894504,-1.94925977349594,
136.393025622985));
#164123=CARTESIAN_POINT('Ctrl Pts',(-259.662941938305,-1.79905562264375,
136.440966815371));
#164124=CARTESIAN_POINT('Ctrl Pts',(-259.670363046142,-1.64868705204678,
136.488960486191));
#164125=CARTESIAN_POINT('Ctrl Pts',(-259.67778415398,-1.49649381591127,
136.530901923211));
#164126=CARTESIAN_POINT('Ctrl Pts',(-259.685205261817,-1.34300510067358,
136.566675071157));
#164127=CARTESIAN_POINT('Ctrl Pts',(-259.692630935413,-1.18942195310739,
136.602470228159));
#164128=CARTESIAN_POINT('Ctrl Pts',(-259.700056609009,-1.03454210251154,
136.632089463809));
#164129=CARTESIAN_POINT('Ctrl Pts',(-259.707482282606,-0.878902344620537,
136.655468310227));
#164130=CARTESIAN_POINT('Ctrl Pts',(-259.714918445666,-0.723042730901533,
136.67888018147));
#164131=CARTESIAN_POINT('Ctrl Pts',(-259.722354608726,-0.566421434618302,
136.696034017051));
#164132=CARTESIAN_POINT('Ctrl Pts',(-259.729790771786,-0.409578588352051,
136.706917346854));
#164133=CARTESIAN_POINT('Ctrl Pts',(-259.733574305306,-0.329776658048363,
136.71245480519));
#164134=CARTESIAN_POINT('Ctrl Pts',(-259.737357838827,-0.249917354980275,
136.716369795289));
#164135=CARTESIAN_POINT('Ctrl Pts',(-259.741141372347,-0.170071456658404,
136.718665839833));
#164136=CARTESIAN_POINT('Ctrl Pts',(-259.748429931939,-0.0162571492104426,
136.723088916143));
#164137=CARTESIAN_POINT('Ctrl Pts',(-259.755718491532,0.138008324997689,
136.72151530412));
#164138=CARTESIAN_POINT('Ctrl Pts',(-259.763007051124,0.292206850264092,
136.713890693567));
#164139=CARTESIAN_POINT('Ctrl Pts',(-259.770286825596,0.446219515417705,
136.706275273185));
#164140=CARTESIAN_POINT('Ctrl Pts',(-259.777566600069,0.600165009584265,
136.692623380763));
#164141=CARTESIAN_POINT('Ctrl Pts',(-259.784846374541,0.753521181319539,
136.672932538554));
#164142=CARTESIAN_POINT('Ctrl Pts',(-259.792119092978,0.906728710185211,
136.653260782001));
#164143=CARTESIAN_POINT('Ctrl Pts',(-259.799391811415,1.05934767157003,
136.627561769673));
#164144=CARTESIAN_POINT('Ctrl Pts',(-259.806664529853,1.21085730663432,
136.595885040848));
#164145=CARTESIAN_POINT('Ctrl Pts',(-259.813931913241,1.36225579876186,
136.564231549123));
#164146=CARTESIAN_POINT('Ctrl Pts',(-259.821199296629,1.51254620623473,
136.526609145561));
#164147=CARTESIAN_POINT('Ctrl Pts',(-259.828466680018,1.66121458269763,
136.483118991782));
#164148=CARTESIAN_POINT('Ctrl Pts',(-259.835731084076,1.80982201119389,
136.439646667192));
#164149=CARTESIAN_POINT('Ctrl Pts',(-259.842995488133,1.95680835961825,
136.390311483737));
#164150=CARTESIAN_POINT('Ctrl Pts',(-259.850259892191,2.1016717106643,136.335265297914));
#164151=CARTESIAN_POINT('Ctrl Pts',(-259.857522856591,2.24650635271518,
136.280230021135));
#164152=CARTESIAN_POINT('Ctrl Pts',(-259.86478582099,2.3892184718474,136.219486130079));
#164153=CARTESIAN_POINT('Ctrl Pts',(-259.87204878539,2.52932344090061,136.153234657381));
#164154=CARTESIAN_POINT('Ctrl Pts',(-259.879311858217,2.66943050156796,
136.086982195621));
#164155=CARTESIAN_POINT('Ctrl Pts',(-259.886574931045,2.80692998421195,
136.01522215424));
#164156=CARTESIAN_POINT('Ctrl Pts',(-259.893838003872,2.9413596176415,135.938202664436));
#164157=CARTESIAN_POINT('Ctrl Pts',(-259.901102733218,3.07581991098706,
135.861165608482));
#164158=CARTESIAN_POINT('Ctrl Pts',(-259.908367462565,3.2072086261801,135.77886691071));
#164159=CARTESIAN_POINT('Ctrl Pts',(-259.915632191911,3.33509066003826,
135.691599188766));
#164160=CARTESIAN_POINT('Ctrl Pts',(-259.922904436531,3.46310498630635,
135.604241189424));
#164161=CARTESIAN_POINT('Ctrl Pts',(-259.930176681152,3.58760506608904,
135.511904118905));
#164162=CARTESIAN_POINT('Ctrl Pts',(-259.937448925772,3.70818675737722,
135.414922571917));
#164163=CARTESIAN_POINT('Ctrl Pts',(-259.944725048152,3.82883274610836,
135.317889311726));
#164164=CARTESIAN_POINT('Ctrl Pts',(-259.952001170531,3.9455558944256,135.216206898089));
#164165=CARTESIAN_POINT('Ctrl Pts',(-259.95927729291,4.05798808483907,135.110247665063));
#164166=CARTESIAN_POINT('Ctrl Pts',(-259.966564564679,4.17059255798621,
135.004126067982));
#164167=CARTESIAN_POINT('Ctrl Pts',(-259.973851836448,4.27889266917242,
134.893714837875));
#164168=CARTESIAN_POINT('Ctrl Pts',(-259.981139108216,4.38255926705988,
134.779420973486));
#164169=CARTESIAN_POINT('Ctrl Pts',(-259.987426072145,4.47199577802895,
134.680815977621));
#164170=CARTESIAN_POINT('Ctrl Pts',(-259.993713036073,4.55798411034979,
134.57932176143));
#164171=CARTESIAN_POINT('Ctrl Pts',(-260.000000000001,4.64033908871117,
134.475216608242));
#164172=CARTESIAN_POINT('',(-260.,-0.0185920708335255,136.72108140677));
#164173=CARTESIAN_POINT('Origin',(-260.,0.,130.804360617566));
#164174=CARTESIAN_POINT('',(-259.56337387439,-5.91070033503288,130.799418600708));
#164175=CARTESIAN_POINT('Ctrl Pts',(-260.,-0.0185920708348715,136.72108140677));
#164176=CARTESIAN_POINT('Ctrl Pts',(-259.991311830341,-0.203157853229185,
136.720501446988));
#164177=CARTESIAN_POINT('Ctrl Pts',(-259.982623660683,-0.387555641347291,
136.711281624755));
#164178=CARTESIAN_POINT('Ctrl Pts',(-259.973935491024,-0.571044165506732,
136.693489511005));
#164179=CARTESIAN_POINT('Ctrl Pts',(-259.965231695903,-0.754862689346968,
136.675665398568));
#164180=CARTESIAN_POINT('Ctrl Pts',(-259.95652790078,-0.93776857354042,
136.649238166263));
#164181=CARTESIAN_POINT('Ctrl Pts',(-259.947824105659,-1.1190256334236,
136.614327243481));
#164182=CARTESIAN_POINT('Ctrl Pts',(-259.939119990154,-1.30028936528833,
136.579415035644));
#164183=CARTESIAN_POINT('Ctrl Pts',(-259.93041587465,-1.47990405091075,
136.536018539262));
#164184=CARTESIAN_POINT('Ctrl Pts',(-259.921711759146,-1.65714402095923,
136.484308175097));
#164185=CARTESIAN_POINT('Ctrl Pts',(-259.913018683697,-1.83415918481704,
136.432663398902));
#164186=CARTESIAN_POINT('Ctrl Pts',(-259.904325608248,-2.00880554981633,
136.372725847947));
#164187=CARTESIAN_POINT('Ctrl Pts',(-259.895632532799,-2.18037229441418,
136.304715807938));
#164188=CARTESIAN_POINT('Ctrl Pts',(-259.886971363205,-2.35130934427719,
136.236955382527));
#164189=CARTESIAN_POINT('Ctrl Pts',(-259.878310193612,-2.5191892311127,
136.161181632495));
#164190=CARTESIAN_POINT('Ctrl Pts',(-259.869649024019,-2.68332250330789,
136.077662325769));
#164191=CARTESIAN_POINT('Ctrl Pts',(-259.866691412044,-2.73937065317332,
136.049142193578));
#164192=CARTESIAN_POINT('Ctrl Pts',(-259.863733800069,-2.79498204109144,
136.019719294179));
#164193=CARTESIAN_POINT('Ctrl Pts',(-259.860776188094,-2.85012961403489,
135.989405626599));
#164194=CARTESIAN_POINT('Ctrl Pts',(-259.853352615767,-2.98854939318207,
135.913318666693));
#164195=CARTESIAN_POINT('Ctrl Pts',(-259.84592904344,-3.1239691154349,135.831658168558));
#164196=CARTESIAN_POINT('Ctrl Pts',(-259.838505471113,-3.25591924795894,
135.744696680353));
#164197=CARTESIAN_POINT('Ctrl Pts',(-259.831082830257,-3.38785282406021,
135.657746103627));
#164198=CARTESIAN_POINT('Ctrl Pts',(-259.823660189402,-3.51631736824606,
135.565496065799));
#164199=CARTESIAN_POINT('Ctrl Pts',(-259.816237548546,-3.64087156035974,
135.468262936812));
#164200=CARTESIAN_POINT('Ctrl Pts',(-259.808814397566,-3.76543431253152,
135.371023125422));
#164201=CARTESIAN_POINT('Ctrl Pts',(-259.801391246585,-3.88608588625228,
135.268799770186));
#164202=CARTESIAN_POINT('Ctrl Pts',(-259.793968095604,-4.00241743025333,
135.161950005806));
#164203=CARTESIAN_POINT('Ctrl Pts',(-259.78654036091,-4.11882080769124,
135.055034262883));
#164204=CARTESIAN_POINT('Ctrl Pts',(-259.779112626216,-4.23089855479602,
134.943486656561));
#164205=CARTESIAN_POINT('Ctrl Pts',(-259.771684891523,-4.33827781733205,
134.827702032627));
#164206=CARTESIAN_POINT('Ctrl Pts',(-259.764254403954,-4.44569687687905,
134.711874496478));
#164207=CARTESIAN_POINT('Ctrl Pts',(-259.756823916385,-4.54841373821342,
134.59180709261));
#164208=CARTESIAN_POINT('Ctrl Pts',(-259.749393428817,-4.64609561235738,
134.467928021523));
#164209=CARTESIAN_POINT('Ctrl Pts',(-259.74195603147,-4.74386832308964,
134.34393375248));
#164210=CARTESIAN_POINT('Ctrl Pts',(-259.734518634122,-4.83659647863859,
134.216121037179));
#164211=CARTESIAN_POINT('Ctrl Pts',(-259.727081236775,-4.9239901424912,
134.084947705139));
#164212=CARTESIAN_POINT('Ctrl Pts',(-259.725238283246,-4.94564589835924,
134.052443544885));
#164213=CARTESIAN_POINT('Ctrl Pts',(-259.723395329716,-4.96697432049345,
134.019733157467));
#164214=CARTESIAN_POINT('Ctrl Pts',(-259.721552376187,-4.98797143306394,
133.986823743109));
#164215=CARTESIAN_POINT('Ctrl Pts',(-259.713932604088,-5.07478491477979,
133.850758327824));
#164216=CARTESIAN_POINT('Ctrl Pts',(-259.706312831988,-5.15611030533379,
133.711008123288));
#164217=CARTESIAN_POINT('Ctrl Pts',(-259.698693059889,-5.23163338743316,
133.568043425342));
#164218=CARTESIAN_POINT('Ctrl Pts',(-259.691080565604,-5.30708433575536,
133.425215276161));
#164219=CARTESIAN_POINT('Ctrl Pts',(-259.683468071318,-5.37674385685914,
133.279179054989));
#164220=CARTESIAN_POINT('Ctrl Pts',(-259.675855577033,-5.44034190027707,
133.130432536185));
#164221=CARTESIAN_POINT('Ctrl Pts',(-259.668249196025,-5.50388887075926,
132.981805469506));
#164222=CARTESIAN_POINT('Ctrl Pts',(-259.660642815016,-5.56138392811307,
132.83047275924));
#164223=CARTESIAN_POINT('Ctrl Pts',(-259.653036434007,-5.61260362325501,
132.676955376377));
#164224=CARTESIAN_POINT('Ctrl Pts',(-259.645435683464,-5.66378540408173,
132.523551631567));
#164225=CARTESIAN_POINT('Ctrl Pts',(-259.637834932921,-5.70870097555932,
132.367966765819));
#164226=CARTESIAN_POINT('Ctrl Pts',(-259.630234182378,-5.74717554453198,
132.210740304149));
#164227=CARTESIAN_POINT('Ctrl Pts',(-259.622636910555,-5.78563250442226,
132.053585802056));
#164228=CARTESIAN_POINT('Ctrl Pts',(-259.615039638731,-5.81765425465708,
131.894791536687));
#164229=CARTESIAN_POINT('Ctrl Pts',(-259.607442366908,-5.84311614749782,
131.734911126324));
#164230=CARTESIAN_POINT('Ctrl Pts',(-259.599846844175,-5.86857217834461,
131.575067524615));
#164231=CARTESIAN_POINT('Ctrl Pts',(-259.592251321443,-5.88747130420872,
131.414138617028));
#164232=CARTESIAN_POINT('Ctrl Pts',(-259.58465579871,-5.899740131173,131.252687448267));
#164233=CARTESIAN_POINT('Ctrl Pts',(-259.577562263208,-5.91119811276277,
131.101906568833));
#164234=CARTESIAN_POINT('Ctrl Pts',(-259.570468727707,-5.91687368214121,
130.950670495385));
#164235=CARTESIAN_POINT('Ctrl Pts',(-259.563375192205,-5.91674795525148,
130.799441620975));
#164236=CARTESIAN_POINT('',(-257.81337519221,-5.92178402722332,130.799850810543));
#164237=CARTESIAN_POINT('Ctrl Pts',(-259.563373045442,-5.90689618837314,
130.799404120224));
#164238=CARTESIAN_POINT('Ctrl Pts',(-259.52328361442,-5.91028116954653,
129.946147187527));
#164239=CARTESIAN_POINT('Ctrl Pts',(-259.39037830879,-5.33824730543968,
127.12303984211));
#164240=CARTESIAN_POINT('Ctrl Pts',(-259.164657128564,-0.969924417821122,
123.869831148738));
#164241=CARTESIAN_POINT('Ctrl Pts',(-258.886209504748,5.30519432384848,
126.242992475658));
#164242=CARTESIAN_POINT('Ctrl Pts',(-258.607761880936,6.70769697358496,
132.800694938907));
#164243=CARTESIAN_POINT('Ctrl Pts',(-258.329314257122,1.9447785293426,137.527620338931));
#164244=CARTESIAN_POINT('Ctrl Pts',(-258.064518694214,-4.28345898126671,
136.145471011969));
#164245=CARTESIAN_POINT('Ctrl Pts',(-257.89253900591,-5.90755031029441,
132.477311743359));
#164246=CARTESIAN_POINT('Ctrl Pts',(-257.81337519221,-5.92178402722332,
130.799850810543));
#164247=CARTESIAN_POINT('',(-256.06337519221,-5.92227829491472,130.80869798814));
#164248=CARTESIAN_POINT('Ctrl Pts',(-257.81337519221,-5.92178402722332,
130.799850810543));
#164249=CARTESIAN_POINT('Ctrl Pts',(-257.799723131306,-5.92423867867741,
130.510567137243));
#164250=CARTESIAN_POINT('Ctrl Pts',(-257.693255195793,-5.77329314096876,
128.257096185211));
#164251=CARTESIAN_POINT('Ctrl Pts',(-257.493971385687,-2.87925022698376,
124.425616511888));
#164252=CARTESIAN_POINT('Ctrl Pts',(-257.215523761869,3.81020896683791,
124.934163083578));
#164253=CARTESIAN_POINT('Ctrl Pts',(-256.937076138059,6.99832954735633,
130.836978163555));
#164254=CARTESIAN_POINT('Ctrl Pts',(-256.658628514244,3.7552968212212,136.709902062958));
#164255=CARTESIAN_POINT('Ctrl Pts',(-256.380180890433,-2.93865415896156,
137.155878050677));
#164256=CARTESIAN_POINT('Ctrl Pts',(-256.181763116421,-5.78435051408065,
133.314517757552));
#164257=CARTESIAN_POINT('Ctrl Pts',(-256.076161217013,-5.92450519214891,
131.079579575374));
#164258=CARTESIAN_POINT('Ctrl Pts',(-256.06337519221,-5.92227829491472,
130.80869798814));
#164259=CARTESIAN_POINT('',(-254.31337519221,-5.90789551585446,130.806811267338));
#164260=CARTESIAN_POINT('Ctrl Pts',(-256.06337519221,-5.92227829491472,
130.80869798814));
#164261=CARTESIAN_POINT('Ctrl Pts',(-255.983345342409,-5.90833977579574,
129.113205208021));
#164262=CARTESIAN_POINT('Ctrl Pts',(-255.810499618004,-4.25395404596283,
125.427592952043));
#164263=CARTESIAN_POINT('Ctrl Pts',(-255.544838018994,2.00761156116971,
124.100105126704));
#164264=CARTESIAN_POINT('Ctrl Pts',(-255.266390395181,6.72564432193871,
128.869606478615));
#164265=CARTESIAN_POINT('Ctrl Pts',(-254.987942771368,5.26313784737678,
135.417054192137));
#164266=CARTESIAN_POINT('Ctrl Pts',(-254.709495147555,-1.03593483579578,
137.725660886227));
#164267=CARTESIAN_POINT('Ctrl Pts',(-254.484639287835,-5.35389815067843,
134.453752389533));
#164268=CARTESIAN_POINT('Ctrl Pts',(-254.352599302721,-5.91100089308872,
131.642964263266));
#164269=CARTESIAN_POINT('Ctrl Pts',(-254.31337519221,-5.90789551585446,
130.806811267338));
#164270=CARTESIAN_POINT('',(-252.56337517516,-5.91453573035578,130.799159711326));
#164271=CARTESIAN_POINT('Ctrl Pts',(-254.31337519221,-5.90789551585446,
130.806811267338));
#164272=CARTESIAN_POINT('Ctrl Pts',(-254.259783428116,-5.90365264987245,
129.664378372864));
#164273=CARTESIAN_POINT('Ctrl Pts',(-254.113375789419,-5.03223228932717,
126.53737431623));
#164274=CARTESIAN_POINT('Ctrl Pts',(-253.874152276116,0.0432914040588217,
123.806097541657));
#164275=CARTESIAN_POINT('Ctrl Pts',(-253.595704652304,5.91123701504208,
127.058050750705));
#164276=CARTESIAN_POINT('Ctrl Pts',(-253.317257028491,6.34704457441364,
133.75267975028));
#164277=CARTESIAN_POINT('Ctrl Pts',(-253.038809404678,0.950228248086572,
137.737947478949));
#164278=CARTESIAN_POINT('Ctrl Pts',(-252.78751545925,-4.70836014979751,
135.584300855963));
#164279=CARTESIAN_POINT('Ctrl Pts',(-252.629037388428,-5.90157326896774,
132.195707362608));
#164280=CARTESIAN_POINT('Ctrl Pts',(-252.56337519221,-5.91327032966472,
130.799161186809));
#164281=CARTESIAN_POINT('',(-250.81337519221,-5.92210605632582,130.804075584904));
#164282=CARTESIAN_POINT('Ctrl Pts',(-252.563375145356,-5.91674771189706,
130.799157132112));
#164283=CARTESIAN_POINT('Ctrl Pts',(-252.554385525451,-5.91657946607099,
130.607849187631));
#164284=CARTESIAN_POINT('Ctrl Pts',(-252.545395905546,-5.90712912470598,
130.416949906316));
#164285=CARTESIAN_POINT('Ctrl Pts',(-252.536406285641,-5.88853768247511,
130.227251854359));
#164286=CARTESIAN_POINT('Ctrl Pts',(-252.527291320086,-5.86968701277697,
130.034908771158));
#164287=CARTESIAN_POINT('Ctrl Pts',(-252.518176354532,-5.84143860087722,
129.843800628979));
#164288=CARTESIAN_POINT('Ctrl Pts',(-252.509061388977,-5.80398847189683,
129.654730946503));
#164289=CARTESIAN_POINT('Ctrl Pts',(-252.500012311669,-5.76680905412209,
129.467027969111));
#164290=CARTESIAN_POINT('Ctrl Pts',(-252.490963234361,-5.72056062638132,
129.281333985984));
#164291=CARTESIAN_POINT('Ctrl Pts',(-252.481914157052,-5.66548117725332,
129.098414078929));
#164292=CARTESIAN_POINT('Ctrl Pts',(-252.474490890639,-5.62029762860797,
128.948358647194));
#164293=CARTESIAN_POINT('Ctrl Pts',(-252.467067624226,-5.56908010727519,
128.799872645413));
#164294=CARTESIAN_POINT('Ctrl Pts',(-252.459644357813,-5.51195390025377,
128.65347829536));
#164295=CARTESIAN_POINT('Ctrl Pts',(-252.452229865084,-5.4548952116643,
128.507256971271));
#164296=CARTESIAN_POINT('Ctrl Pts',(-252.444815372356,-5.39194187260987,
128.363122722427));
#164297=CARTESIAN_POINT('Ctrl Pts',(-252.437400879627,-5.32326936540353,
128.221584238191));
#164298=CARTESIAN_POINT('Ctrl Pts',(-252.429993533266,-5.25466304734425,
128.080182174074));
#164299=CARTESIAN_POINT('Ctrl Pts',(-252.422586186904,-5.18034869699358,
127.941371227381));
#164300=CARTESIAN_POINT('Ctrl Pts',(-252.415178840543,-5.10055041820027,
127.805641558718));
#164301=CARTESIAN_POINT('Ctrl Pts',(-252.407777018859,-5.02081165597293,
127.670013122361));
#164302=CARTESIAN_POINT('Ctrl Pts',(-252.400375197176,-4.9355972976652,
127.537461708557));
#164303=CARTESIAN_POINT('Ctrl Pts',(-252.392973375493,-4.84517799030723,
127.408454139946));
#164304=CARTESIAN_POINT('Ctrl Pts',(-252.385575461174,-4.75480641459697,
127.279514673425));
#164305=CARTESIAN_POINT('Ctrl Pts',(-252.378177546855,-4.65923557562838,
127.154115631288));
#164306=CARTESIAN_POINT('Ctrl Pts',(-252.370779632536,-4.55878010284036,
127.032695927214));
#164307=CARTESIAN_POINT('Ctrl Pts',(-252.363382947615,-4.45834132392844,
126.911296400891));
#164308=CARTESIAN_POINT('Ctrl Pts',(-252.355986262695,-4.35301975998355,
126.793875187499));
#164309=CARTESIAN_POINT('Ctrl Pts',(-252.348589577775,-4.24317116323312,
126.680839180492));
#164310=CARTESIAN_POINT('Ctrl Pts',(-252.341193220832,-4.13332743728395,
126.56780818562));
#164311=CARTESIAN_POINT('Ctrl Pts',(-252.333796863888,-4.01895733781476,
126.459162278221));
#164312=CARTESIAN_POINT('Ctrl Pts',(-252.326400506945,-3.9004542228339,
126.355272237001));
#164313=CARTESIAN_POINT('Ctrl Pts',(-252.3190030176,-3.78193296472295,126.251366289951));
#164314=CARTESIAN_POINT('Ctrl Pts',(-252.311605528256,-3.65927771187928,
126.152217904996));
#164315=CARTESIAN_POINT('Ctrl Pts',(-252.304208038911,-3.53291558420442,
126.058158131643));
#164316=CARTESIAN_POINT('Ctrl Pts',(-252.296807956388,-3.40650916048073,
125.964065385781));
#164317=CARTESIAN_POINT('Ctrl Pts',(-252.289407873865,-3.27639357401108,
125.875065025821));
#164318=CARTESIAN_POINT('Ctrl Pts',(-252.282007791342,-3.14302550827543,
125.791445176744));
#164319=CARTESIAN_POINT('Ctrl Pts',(-252.274599571667,-3.00951079064127,
125.707733379047));
#164320=CARTESIAN_POINT('Ctrl Pts',(-252.267191351993,-2.87273676783248,
125.629414106142));
#164321=CARTESIAN_POINT('Ctrl Pts',(-252.259783132318,-2.73318598342807,
125.556730205419));
#164322=CARTESIAN_POINT('Ctrl Pts',(-252.252370353008,-2.59354930784409,
125.484001568967));
#164323=CARTESIAN_POINT('Ctrl Pts',(-252.244957573698,-2.45113280209025,
125.416915374782));
#164324=CARTESIAN_POINT('Ctrl Pts',(-252.237544794388,-2.30643914601276,
125.355666367726));
#164325=CARTESIAN_POINT('Ctrl Pts',(-252.230121423351,-2.16153874485486,
125.294329845216));
#164326=CARTESIAN_POINT('Ctrl Pts',(-252.222698052315,-2.01435504338489,
125.238847298903));
#164327=CARTESIAN_POINT('Ctrl Pts',(-252.215274681278,-1.86540681970865,
125.189363915921));
#164328=CARTESIAN_POINT('Ctrl Pts',(-252.211338631931,-1.78643089953227,
125.163126639584));
#164329=CARTESIAN_POINT('Ctrl Pts',(-252.207402582585,-1.70695910773732,
125.138575094991));
#164330=CARTESIAN_POINT('Ctrl Pts',(-252.203466533239,-1.62706982582334,
125.115725074275));
#164331=CARTESIAN_POINT('Ctrl Pts',(-252.196043266835,-1.47640112981881,
125.072630647307));
#164332=CARTESIAN_POINT('Ctrl Pts',(-252.188620000432,-1.32379133005656,
125.035461087659));
#164333=CARTESIAN_POINT('Ctrl Pts',(-252.181196734029,-1.16974750718794,
125.004393261457));
#164334=CARTESIAN_POINT('Ctrl Pts',(-252.17378224131,-1.01588575132546,
124.973362154846));
#164335=CARTESIAN_POINT('Ctrl Pts',(-252.166367748591,-0.860593708413412,
124.948418499748));
#164336=CARTESIAN_POINT('Ctrl Pts',(-252.158953255872,-0.704394205693282,
124.929689616949));
#164337=CARTESIAN_POINT('Ctrl Pts',(-252.15154590952,-0.548345253934723,
124.910978785754));
#164338=CARTESIAN_POINT('Ctrl Pts',(-252.144138563168,-0.391390951766817,
124.898470846027));
#164339=CARTESIAN_POINT('Ctrl Pts',(-252.136731216816,-0.234064818790602,
124.892242196636));
#164340=CARTESIAN_POINT('Ctrl Pts',(-252.129329395143,-0.0768560255804177,
124.886018192806));
#164341=CARTESIAN_POINT('Ctrl Pts',(-252.12192757347,0.0807236748453837,
124.886064168869));
#164342=CARTESIAN_POINT('Ctrl Pts',(-252.114525751796,0.23813524004973,
124.892404750854));
#164343=CARTESIAN_POINT('Ctrl Pts',(-252.107127837487,0.395463708914521,
124.898741985696));
#164344=CARTESIAN_POINT('Ctrl Pts',(-252.099729923178,0.552623847270964,
124.911367193811));
#164345=CARTESIAN_POINT('Ctrl Pts',(-252.092332008868,0.709076319714843,
124.930252912108));
#164346=CARTESIAN_POINT('Ctrl Pts',(-252.084935323958,0.865502792595908,
124.949135491941));
#164347=CARTESIAN_POINT('Ctrl Pts',(-252.077538639048,1.0212214627234,124.97427647241));
#164348=CARTESIAN_POINT('Ctrl Pts',(-252.070141954138,1.17569770634179,
125.005596484942));
#164349=CARTESIAN_POINT('Ctrl Pts',(-252.062745597205,1.33016710032166,
125.036915108713));
#164350=CARTESIAN_POINT('Ctrl Pts',(-252.055349240271,1.48339381147729,
125.074412145596));
#164351=CARTESIAN_POINT('Ctrl Pts',(-252.047952883338,1.63485327357079,
125.117957067307));
#164352=CARTESIAN_POINT('Ctrl Pts',(-252.040555394003,1.78633592449418,
125.161508655857));
#164353=CARTESIAN_POINT('Ctrl Pts',(-252.033157904669,1.9360504288259,125.211109869767));
#164354=CARTESIAN_POINT('Ctrl Pts',(-252.025760415334,2.08348739650297,
125.26658030131));
#164355=CARTESIAN_POINT('Ctrl Pts',(-252.018360332821,2.23097604798114,
125.322070177927));
#164356=CARTESIAN_POINT('Ctrl Pts',(-252.010960250308,2.37618522405199,
125.383433237168));
#164357=CARTESIAN_POINT('Ctrl Pts',(-252.003560167795,2.51862566843399,
125.450440996876));
#164358=CARTESIAN_POINT('Ctrl Pts',(-251.996151948131,2.66122274072767,
125.517522438506));
#164359=CARTESIAN_POINT('Ctrl Pts',(-251.988743728467,2.80104466326066,
125.590260817245));
#164360=CARTESIAN_POINT('Ctrl Pts',(-251.981335508802,2.93762629505646,
125.668381420461));
#164361=CARTESIAN_POINT('Ctrl Pts',(-251.973922729502,3.07429199056805,
125.746550105606));
#164362=CARTESIAN_POINT('Ctrl Pts',(-251.966509950202,3.20771310571814,
125.83010741846));
#164363=CARTESIAN_POINT('Ctrl Pts',(-251.959097170902,3.3374540854052,125.918735704588));
#164364=CARTESIAN_POINT('Ctrl Pts',(-251.951673799875,3.46738044508888,
126.007490626968));
#164365=CARTESIAN_POINT('Ctrl Pts',(-251.944250428849,3.59361586841001,
126.101330771682));
#164366=CARTESIAN_POINT('Ctrl Pts',(-251.936827057822,3.71575779308237,
126.199898153212));
#164367=CARTESIAN_POINT('Ctrl Pts',(-251.932891008357,3.78052037272035,
126.252160944331));
#164368=CARTESIAN_POINT('Ctrl Pts',(-251.928954958891,3.84413272915417,
126.305752105551));
#164369=CARTESIAN_POINT('Ctrl Pts',(-251.925018909426,3.90653920889307,
126.360614228326));
#164370=CARTESIAN_POINT('Ctrl Pts',(-251.917595643021,4.02423588129208,
126.464082479034));
#164371=CARTESIAN_POINT('Ctrl Pts',(-251.910172376617,4.13799700900795,
126.572386370818));
#164372=CARTESIAN_POINT('Ctrl Pts',(-251.902749110212,4.24739970008144,
126.685194882827));
#164373=CARTESIAN_POINT('Ctrl Pts',(-251.895334617492,4.35667308625939,
126.797870064543));
#164374=CARTESIAN_POINT('Ctrl Pts',(-251.887920124772,4.46159803215885,
126.9150390035));
#164375=CARTESIAN_POINT('Ctrl Pts',(-251.880505632052,4.56178481830169,
127.036330650327));
#164376=CARTESIAN_POINT('Ctrl Pts',(-251.8730982857,4.66187504064777,127.157505391698));
#164377=CARTESIAN_POINT('Ctrl Pts',(-251.865690939347,4.7572359587348,127.282794644363));
#164378=CARTESIAN_POINT('Ctrl Pts',(-251.858283592994,4.84751491565739,
127.411790838626));
#164379=CARTESIAN_POINT('Ctrl Pts',(-251.85088177132,4.93772653912762,127.540690822659));
#164380=CARTESIAN_POINT('Ctrl Pts',(-251.843479949645,5.02286353534696,
127.673291938723));
#164381=CARTESIAN_POINT('Ctrl Pts',(-251.836078127971,5.10261382013593,
127.80915398612));
#164382=CARTESIAN_POINT('Ctrl Pts',(-251.828680213661,5.1823220053701,127.944944312999));
#164383=CARTESIAN_POINT('Ctrl Pts',(-251.82128229935,5.25664895385125,128.083991821801));
#164384=CARTESIAN_POINT('Ctrl Pts',(-251.81388438504,5.32532624709685,128.225827909904));
#164385=CARTESIAN_POINT('Ctrl Pts',(-251.806487700129,5.39399212742215,
128.367640427422));
#164386=CARTESIAN_POINT('Ctrl Pts',(-251.799091015218,5.45701005336667,
128.512240268852));
#164387=CARTESIAN_POINT('Ctrl Pts',(-251.791694330306,5.51415782275889,
128.659134739434));
#164388=CARTESIAN_POINT('Ctrl Pts',(-251.784297973372,5.57130305815897,
128.806022696561));
#164389=CARTESIAN_POINT('Ctrl Pts',(-251.776901616437,5.62257851920319,
128.955204732637));
#164390=CARTESIAN_POINT('Ctrl Pts',(-251.769505259503,5.66781048216889,
129.106168961505));
#164391=CARTESIAN_POINT('Ctrl Pts',(-251.762107770167,5.71304937026359,
129.257156303381));
#164392=CARTESIAN_POINT('Ctrl Pts',(-251.754710280832,5.7522428107855,129.40992602373));
#164393=CARTESIAN_POINT('Ctrl Pts',(-251.747312791497,5.78526724809163,
129.563952043483));
#164394=CARTESIAN_POINT('Ctrl Pts',(-251.739912708983,5.81830326206303,
129.718032056819));
#164395=CARTESIAN_POINT('Ctrl Pts',(-251.732512626469,5.84516588901763,
129.873368881604));
#164396=CARTESIAN_POINT('Ctrl Pts',(-251.725112543955,5.8657829024923,130.029427392488));
#164397=CARTESIAN_POINT('Ctrl Pts',(-251.717704324289,5.88642258649274,
130.185657505748));
#164398=CARTESIAN_POINT('Ctrl Pts',(-251.710296104624,5.90080289285541,
130.342610519604));
#164399=CARTESIAN_POINT('Ctrl Pts',(-251.702887884959,5.90890352503909,
130.499746608892));
#164400=CARTESIAN_POINT('Ctrl Pts',(-251.695475105658,5.91700914302668,
130.656979412819));
#164401=CARTESIAN_POINT('Ctrl Pts',(-251.688062326357,5.91882738096768,
130.814395144299));
#164402=CARTESIAN_POINT('Ctrl Pts',(-251.680649547056,5.91439006236425,
130.971455658507));
#164403=CARTESIAN_POINT('Ctrl Pts',(-251.673226176028,5.9099464035119,131.128740588143));
#164404=CARTESIAN_POINT('Ctrl Pts',(-251.665802805,5.89922936182667,131.285668915369));
#164405=CARTESIAN_POINT('Ctrl Pts',(-251.658379433973,5.88232252591546,
131.441708453216));
#164406=CARTESIAN_POINT('Ctrl Pts',(-251.65444338452,5.87335811581224,131.524444360569));
#164407=CARTESIAN_POINT('Ctrl Pts',(-251.650507335067,5.8626543865947,131.606930569052));
#164408=CARTESIAN_POINT('Ctrl Pts',(-251.646571285614,5.85022955562714,
131.689089225087));
#164409=CARTESIAN_POINT('Ctrl Pts',(-251.639148019207,5.82679671225734,
131.844037885828));
#164410=CARTESIAN_POINT('Ctrl Pts',(-251.631724752801,5.79716824906139,
131.998289243483));
#164411=CARTESIAN_POINT('Ctrl Pts',(-251.624301486394,5.76139407982381,
132.151308582215));
#164412=CARTESIAN_POINT('Ctrl Pts',(-251.616886993672,5.72566219268329,
132.304147064796));
#164413=CARTESIAN_POINT('Ctrl Pts',(-251.60947250095,5.68379914211561,132.455756066969));
#164414=CARTESIAN_POINT('Ctrl Pts',(-251.602058008228,5.63590644956803,
132.605607145451));
#164415=CARTESIAN_POINT('Ctrl Pts',(-251.594650661873,5.5880599178005,132.755313791822));
#164416=CARTESIAN_POINT('Ctrl Pts',(-251.587243315518,5.53419542667724,
132.903265534435));
#164417=CARTESIAN_POINT('Ctrl Pts',(-251.579835969163,5.47446525645678,
133.048945371668));
#164418=CARTESIAN_POINT('Ctrl Pts',(-251.572434147486,5.41477963525075,
133.194516555383));
#164419=CARTESIAN_POINT('Ctrl Pts',(-251.56503232581,5.34923718685904,133.337818863736));
#164420=CARTESIAN_POINT('Ctrl Pts',(-251.557630504133,5.27803957547498,
133.478351792237));
#164421=CARTESIAN_POINT('Ctrl Pts',(-251.550232589821,5.20687954875555,
133.6188105345));
#164422=CARTESIAN_POINT('Ctrl Pts',(-251.542834675508,5.13007047272427,
133.756502476267));
#164423=CARTESIAN_POINT('Ctrl Pts',(-251.535436761195,5.04786150929324,
133.8909484983));
#164424=CARTESIAN_POINT('Ctrl Pts',(-251.528040076282,4.96566620750038,
134.025372177845));
#164425=CARTESIAN_POINT('Ctrl Pts',(-251.520643391369,4.87807299385584,
134.156550690065));
#164426=CARTESIAN_POINT('Ctrl Pts',(-251.513246706455,4.78537628071299,
134.28403077643));
#164427=CARTESIAN_POINT('Ctrl Pts',(-251.505850349519,4.69268367783954,
134.411505210195));
#164428=CARTESIAN_POINT('Ctrl Pts',(-251.498453992582,4.59488824495589,
134.535281242258));
#164429=CARTESIAN_POINT('Ctrl Pts',(-251.491057635645,4.49232674446931,
134.654936026959));
#164430=CARTESIAN_POINT('Ctrl Pts',(-251.483660146308,4.38974954155489,
134.774609131115));
#164431=CARTESIAN_POINT('Ctrl Pts',(-251.47626265697,4.2824050610685,134.890159448109));
#164432=CARTESIAN_POINT('Ctrl Pts',(-251.468865167632,4.17066912338748,
135.001198668495));
#164433=CARTESIAN_POINT('Ctrl Pts',(-251.461465085116,4.05889401684656,
135.112276813507));
#164434=CARTESIAN_POINT('Ctrl Pts',(-251.4540650026,3.94272465276058,135.218840450467));
#164435=CARTESIAN_POINT('Ctrl Pts',(-251.446664920083,3.82257220707633,
135.320539564883));
#164436=CARTESIAN_POINT('Ctrl Pts',(-251.439256700416,3.70228764142629,
135.42235050793));
#164437=CARTESIAN_POINT('Ctrl Pts',(-251.431848480748,3.5780115325228,135.519286004722));
#164438=CARTESIAN_POINT('Ctrl Pts',(-251.42444026108,3.45018707979019,135.611037190516));
#164439=CARTESIAN_POINT('Ctrl Pts',(-251.417027481777,3.32228395323944,
135.702844847635));
#164440=CARTESIAN_POINT('Ctrl Pts',(-251.409614702474,3.19082844206446,
135.789461630659));
#164441=CARTESIAN_POINT('Ctrl Pts',(-251.402201923171,3.05629050412772,
135.870623433181));
#164442=CARTESIAN_POINT('Ctrl Pts',(-251.394778552141,2.92156033207666,
135.951901203491));
#164443=CARTESIAN_POINT('Ctrl Pts',(-251.387355181111,2.7837392630747,136.027708246836));
#164444=CARTESIAN_POINT('Ctrl Pts',(-251.379931810081,2.64332022277605,
136.097827228622));
#164445=CARTESIAN_POINT('Ctrl Pts',(-251.375995760654,2.56886667857348,
136.135005995111));
#164446=CARTESIAN_POINT('Ctrl Pts',(-251.372059711227,2.49368306864493,
136.170586454851));
#164447=CARTESIAN_POINT('Ctrl Pts',(-251.3681236618,2.41784474033988,136.204541852868));
#164448=CARTESIAN_POINT('Ctrl Pts',(-251.360700395395,2.27481601949637,
136.268580674038));
#164449=CARTESIAN_POINT('Ctrl Pts',(-251.35327712899,2.12902507563505,136.327030035431));
#164450=CARTESIAN_POINT('Ctrl Pts',(-251.345853862585,1.98094875995439,
136.379642903956));
#164451=CARTESIAN_POINT('Ctrl Pts',(-251.338439369864,1.8330474581819,136.43219358844));
#164452=CARTESIAN_POINT('Ctrl Pts',(-251.331024877143,1.68286650950291,
136.4789213873));
#164453=CARTESIAN_POINT('Ctrl Pts',(-251.323610384423,1.53090538303937,
136.519626076902));
#164454=CARTESIAN_POINT('Ctrl Pts',(-251.316203038069,1.37909072243075,
136.560291533792));
#164455=CARTESIAN_POINT('Ctrl Pts',(-251.308795691716,1.22549965802752,
136.594945342693));
#164456=CARTESIAN_POINT('Ctrl Pts',(-251.301388345363,1.07064946913359,
136.623436169296));
#164457=CARTESIAN_POINT('Ctrl Pts',(-251.293986523688,0.915914773352263,
136.651905746366));
#164458=CARTESIAN_POINT('Ctrl Pts',(-251.286584702013,0.759923188515468,
136.6742214263));
#164459=CARTESIAN_POINT('Ctrl Pts',(-251.279182880338,0.603204807647272,
136.690282339992));
#164460=CARTESIAN_POINT('Ctrl Pts',(-251.271784966027,0.446569157192895,
136.706334775254));
#164461=CARTESIAN_POINT('Ctrl Pts',(-251.264387051716,0.289207845217121,
136.716138982091));
#164462=CARTESIAN_POINT('Ctrl Pts',(-251.256989137405,0.131658646401416,
136.719645611827));
#164463=CARTESIAN_POINT('Ctrl Pts',(-251.249592452493,-0.0258643705954541,
136.723151658825));
#164464=CARTESIAN_POINT('Ctrl Pts',(-251.242195767581,-0.183574839623018,
136.720362197501));
#164465=CARTESIAN_POINT('Ctrl Pts',(-251.23479908267,-0.340932284373179,
136.711279927999));
#164466=CARTESIAN_POINT('Ctrl Pts',(-251.227402725735,-0.498282751729341,
136.702198061215));
#164467=CARTESIAN_POINT('Ctrl Pts',(-251.2200063688,-0.655279853255146,
136.686823962568));
#164468=CARTESIAN_POINT('Ctrl Pts',(-251.212610011865,-0.811385808614204,
136.665212401401));
#164469=CARTESIAN_POINT('Ctrl Pts',(-251.205212522529,-0.967515664193547,
136.643597531448));
#164470=CARTESIAN_POINT('Ctrl Pts',(-251.197815033193,-1.12275373214748,
136.615743348696));
#164471=CARTESIAN_POINT('Ctrl Pts',(-251.190417543856,-1.27657017664553,
136.581756150728));
#164472=CARTESIAN_POINT('Ctrl Pts',(-251.183017461342,-1.43044054125997,
136.547757038601));
#164473=CARTESIAN_POINT('Ctrl Pts',(-251.175617378827,-1.58288792593311,
136.507620711276));
#164474=CARTESIAN_POINT('Ctrl Pts',(-251.168217296313,-1.7333956029165,
136.46150391134));
#164475=CARTESIAN_POINT('Ctrl Pts',(-251.160809076647,-1.88406877856353,
136.415336401241));
#164476=CARTESIAN_POINT('Ctrl Pts',(-251.153400856981,-2.03279762982558,
136.363175394969));
#164477=CARTESIAN_POINT('Ctrl Pts',(-251.145992637315,-2.17908273993251,
136.305226819813));
#164478=CARTESIAN_POINT('Ctrl Pts',(-251.138579858013,-2.32545788608382,
136.247242578277));
#164479=CARTESIAN_POINT('Ctrl Pts',(-251.131167078711,-2.46938595350926,
136.183463820706));
#164480=CARTESIAN_POINT('Ctrl Pts',(-251.12375429941,-2.6103907183032,136.114143179997));
#164481=CARTESIAN_POINT('Ctrl Pts',(-251.116330928381,-2.75159695731775,
136.044723490705));
#164482=CARTESIAN_POINT('Ctrl Pts',(-251.108907557353,-2.88987122410066,
135.969746280717));
#164483=CARTESIAN_POINT('Ctrl Pts',(-251.101484186325,-3.0247642305461,
135.889508787689));
#164484=CARTESIAN_POINT('Ctrl Pts',(-251.097548136879,-3.0962877393667,
135.84696494356));
#164485=CARTESIAN_POINT('Ctrl Pts',(-251.093612087434,-3.16686116580283,
135.802942950607));
#164486=CARTESIAN_POINT('Ctrl Pts',(-251.089676037988,-3.23642127305177,
135.757491738972));
#164487=CARTESIAN_POINT('Ctrl Pts',(-251.082262927628,-3.36742998084501,
135.671889448529));
#164488=CARTESIAN_POINT('Ctrl Pts',(-251.074849817269,-3.49524090964866,
135.580954646384));
#164489=CARTESIAN_POINT('Ctrl Pts',(-251.067436706909,-3.61938921607638,
135.484953770688));
#164490=CARTESIAN_POINT('Ctrl Pts',(-251.060032365242,-3.74339067208673,
135.389066450859));
#164491=CARTESIAN_POINT('Ctrl Pts',(-251.052628023575,-3.86373783562373,
135.288125211725));
#164492=CARTESIAN_POINT('Ctrl Pts',(-251.045223681908,-3.97999295862695,
135.182440860296));
#164493=CARTESIAN_POINT('Ctrl Pts',(-251.037826471706,-4.0961361109251,
135.076858298371));
#164494=CARTESIAN_POINT('Ctrl Pts',(-251.030429261504,-4.20819479333491,
134.966541968504));
#164495=CARTESIAN_POINT('Ctrl Pts',(-251.023032051303,-4.31576271800789,
134.851844122703));
#164496=CARTESIAN_POINT('Ctrl Pts',(-251.015640341042,-4.42325066425436,
134.737231556535));
#164497=CARTESIAN_POINT('Ctrl Pts',(-251.008248630781,-4.5262542457145,
134.618244232668));
#164498=CARTESIAN_POINT('Ctrl Pts',(-251.00085692052,-4.62440267623168,
134.495272490066));
#164499=CARTESIAN_POINT('Ctrl Pts',(-250.993469083091,-4.72249968259949,
134.372365177605));
#164500=CARTESIAN_POINT('Ctrl Pts',(-250.986081245663,-4.81574637096713,
134.245477895747));
#164501=CARTESIAN_POINT('Ctrl Pts',(-250.978693408234,-4.90381113174446,
134.115035314162));
#164502=CARTESIAN_POINT('Ctrl Pts',(-250.971306752627,-4.99186180492488,
133.984613599294));
#164503=CARTESIAN_POINT('Ctrl Pts',(-250.963920097021,-5.07473198604866,
133.850638023283));
#164504=CARTESIAN_POINT('Ctrl Pts',(-250.956533441414,-5.1521323889978,
133.713563671452));
#164505=CARTESIAN_POINT('Ctrl Pts',(-250.949147064478,-5.22952987192629,
133.576494490911));
#164506=CARTESIAN_POINT('Ctrl Pts',(-250.941760687542,-5.30145780279621,
133.436327093028));
#164507=CARTESIAN_POINT('Ctrl Pts',(-250.934374310605,-5.36767216274448,
133.293542434107));
#164508=CARTESIAN_POINT('Ctrl Pts',(-250.926986743122,-5.43389719521569,
133.150734760955));
#164509=CARTESIAN_POINT('Ctrl Pts',(-250.919599175639,-5.49440666570941,
133.005309326591));
#164510=CARTESIAN_POINT('Ctrl Pts',(-250.912211608156,-5.54900420961933,
132.857768235193));
#164511=CARTESIAN_POINT('Ctrl Pts',(-250.904821380464,-5.60362141370727,
132.710174015321));
#164512=CARTESIAN_POINT('Ctrl Pts',(-250.897431152772,-5.65232232312268,
132.560462972647));
#164513=CARTESIAN_POINT('Ctrl Pts',(-250.89004092508,-5.69496010914035,
132.409153413475));
#164514=CARTESIAN_POINT('Ctrl Pts',(-250.882642565357,-5.73764481276505,
132.257677356857));
#164515=CARTESIAN_POINT('Ctrl Pts',(-250.875244205634,-5.7742529686653,
132.104599631833));
#164516=CARTESIAN_POINT('Ctrl Pts',(-250.867845845911,-5.80468849773136,
131.950450494847));
#164517=CARTESIAN_POINT('Ctrl Pts',(-250.860442849322,-5.83514310203205,
131.796204746069));
#164518=CARTESIAN_POINT('Ctrl Pts',(-250.853039852734,-5.85941731376475,
131.64088661638));
#164519=CARTESIAN_POINT('Ctrl Pts',(-250.845636856145,-5.87746688625184,
131.485032023983));
#164520=CARTESIAN_POINT('Ctrl Pts',(-250.838223446978,-5.89554184610583,
131.328958216547));
#164521=CARTESIAN_POINT('Ctrl Pts',(-250.830810037811,-5.9073746551586,
131.172346811769));
#164522=CARTESIAN_POINT('Ctrl Pts',(-250.823396628644,-5.91297314554463,
131.015735030795));
#164523=CARTESIAN_POINT('Ctrl Pts',(-250.820056149833,-5.91549582277577,
130.945165833253));
#164524=CARTESIAN_POINT('Ctrl Pts',(-250.816715671021,-5.91675338732688,
130.874596511954));
#164525=CARTESIAN_POINT('Ctrl Pts',(-250.81337519221,-5.91674999314685,
130.804075842693));
#164526=CARTESIAN_POINT('',(-249.063375969071,-5.91496647234029,130.809715820468));
#164527=CARTESIAN_POINT('Ctrl Pts',(-250.81337519221,-5.92651577310741,
130.804075372663));
#164528=CARTESIAN_POINT('Ctrl Pts',(-250.812659599531,-5.92652634227882,
130.788943599106));
#164529=CARTESIAN_POINT('Ctrl Pts',(-250.811944006853,-5.92647342300579,
130.773811901629));
#164530=CARTESIAN_POINT('Ctrl Pts',(-250.811228414174,-5.92635679277963,
130.758680695231));
#164531=CARTESIAN_POINT('Ctrl Pts',(-250.71841253957,-5.91122928131646,
128.79608912902));
#164532=CARTESIAN_POINT('Ctrl Pts',(-250.532780790362,-3.73730962072342,
124.887429206006));
#164533=CARTESIAN_POINT('Ctrl Pts',(-250.254333166549,2.95797483390075,
124.461810230503));
#164534=CARTESIAN_POINT('Ctrl Pts',(-249.975885542736,6.9350249212652,129.864685209915));
#164535=CARTESIAN_POINT('Ctrl Pts',(-249.697437918923,4.53912590079626,
136.131075983253));
#164536=CARTESIAN_POINT('Ctrl Pts',(-249.41899029511,-2.02800807388145,
137.502475560044));
#164537=CARTESIAN_POINT('Ctrl Pts',(-249.207636433196,-5.59816439000333,
133.871332218785));
#164538=CARTESIAN_POINT('Ctrl Pts',(-249.089098445888,-5.91888558459242,
131.356595549194));
#164539=CARTESIAN_POINT('Ctrl Pts',(-249.063376333184,-5.91413166792106,
130.809722808261));
#164540=CARTESIAN_POINT('',(-247.313374425905,-5.91167834912772,130.802355503486));
#164541=CARTESIAN_POINT('Ctrl Pts',(-249.06337519221,-5.91674758999916,
130.80970091149));
#164542=CARTESIAN_POINT('Ctrl Pts',(-249.056039121377,-5.91688842597513,
130.653662511114));
#164543=CARTESIAN_POINT('Ctrl Pts',(-249.048703050544,-5.91085239615979,
130.497490660387));
#164544=CARTESIAN_POINT('Ctrl Pts',(-249.041366979711,-5.89863472226865,
130.341717152523));
#164545=CARTESIAN_POINT('Ctrl Pts',(-249.033897315869,-5.88619455927311,
130.183106941982));
#164546=CARTESIAN_POINT('Ctrl Pts',(-249.026427652026,-5.86734539502519,
130.02491012295));
#164547=CARTESIAN_POINT('Ctrl Pts',(-249.018957988183,-5.84213773715391,
129.867687129833));
#164548=CARTESIAN_POINT('Ctrl Pts',(-249.01162653947,-5.81739650986932,
129.713373316668));
#164549=CARTESIAN_POINT('Ctrl Pts',(-249.004295090756,-5.7865301308496,
129.559997991909));
#164550=CARTESIAN_POINT('Ctrl Pts',(-248.996963642042,-5.74963852955144,
129.408084376274));
#164551=CARTESIAN_POINT('Ctrl Pts',(-248.989632196889,-5.71274694616648,
129.256170834402));
#164552=CARTESIAN_POINT('Ctrl Pts',(-248.982300751735,-5.66983023572421,
129.10571937014));
#164553=CARTESIAN_POINT('Ctrl Pts',(-248.974969306581,-5.62103900359289,
128.957240945594));
#164554=CARTESIAN_POINT('Ctrl Pts',(-248.967636354787,-5.5722377446736,
128.808732008153));
#164555=CARTESIAN_POINT('Ctrl Pts',(-248.960303402993,-5.51755968027065,
128.662197278831));
#164556=CARTESIAN_POINT('Ctrl Pts',(-248.952970451199,-5.45720455405735,
128.518130310341));
#164557=CARTESIAN_POINT('Ctrl Pts',(-248.945397500889,-5.39487407861425,
128.369348206731));
#164558=CARTESIAN_POINT('Ctrl Pts',(-248.93782455058,-5.32648877245105,
128.223198555189));
#164559=CARTESIAN_POINT('Ctrl Pts',(-248.93025160027,-5.25232094526869,
128.080199232774));
#164560=CARTESIAN_POINT('Ctrl Pts',(-248.922907255254,-5.18039202857906,
127.941516643039));
#164561=CARTESIAN_POINT('Ctrl Pts',(-248.915562910238,-5.10302489309629,
127.805797237635));
#164562=CARTESIAN_POINT('Ctrl Pts',(-248.908218565223,-5.02051266192647,
127.67348483371));
#164563=CARTESIAN_POINT('Ctrl Pts',(-248.900531312266,-4.93414792938501,
127.53499475515));
#164564=CARTESIAN_POINT('Ctrl Pts',(-248.89284405931,-4.84214637605896,
127.400237873611));
#164565=CARTESIAN_POINT('Ctrl Pts',(-248.885156806354,-4.74489163246716,
127.269684683531));
#164566=CARTESIAN_POINT('Ctrl Pts',(-248.877469553398,-4.64763688887508,
127.139131493451));
#164567=CARTESIAN_POINT('Ctrl Pts',(-248.869782300441,-4.54512930921572,
127.012782312023));
#164568=CARTESIAN_POINT('Ctrl Pts',(-248.862095047485,-4.43779615577289,
126.891063306818));
#164569=CARTESIAN_POINT('Ctrl Pts',(-248.85467178108,-4.33414891056291,
126.773524231756));
#164570=CARTESIAN_POINT('Ctrl Pts',(-248.847248514674,-4.22567201910399,
126.659928055844));
#164571=CARTESIAN_POINT('Ctrl Pts',(-248.839825248268,-4.11269714543466,
126.550697166794));
#164572=CARTESIAN_POINT('Ctrl Pts',(-248.832410755547,-3.9998557986837,
126.441595379584));
#164573=CARTESIAN_POINT('Ctrl Pts',(-248.824996262826,-3.88252731748045,
126.336848866352));
#164574=CARTESIAN_POINT('Ctrl Pts',(-248.817581770105,-3.76108334385289,
126.236846781452));
#164575=CARTESIAN_POINT('Ctrl Pts',(-248.810174423751,-3.63975642249939,
126.136941082326));
#164576=CARTESIAN_POINT('Ctrl Pts',(-248.802767077397,-3.51432219181145,
126.041770943571));
#164577=CARTESIAN_POINT('Ctrl Pts',(-248.795359731044,-3.38518875769885,
125.951688401431));
#164578=CARTESIAN_POINT('Ctrl Pts',(-248.787957909368,-3.25615163617297,
125.861673046249));
#164579=CARTESIAN_POINT('Ctrl Pts',(-248.780556087693,-3.12342110962033,
125.776737944937));
#164580=CARTESIAN_POINT('Ctrl Pts',(-248.773154266017,-2.98743785316926,
125.697194511402));
#164581=CARTESIAN_POINT('Ctrl Pts',(-248.765756351706,-2.85152638122117,
125.617693068226));
#164582=CARTESIAN_POINT('Ctrl Pts',(-248.758358437394,-2.71236592044747,
125.543577812451));
#164583=CARTESIAN_POINT('Ctrl Pts',(-248.750960523083,-2.57042548141573,
125.475116449113));
#164584=CARTESIAN_POINT('Ctrl Pts',(-248.74356383817,-2.4285086303101,125.406666462812));
#164585=CARTESIAN_POINT('Ctrl Pts',(-248.736167153258,-2.28381305374583,
125.343868666186));
#164586=CARTESIAN_POINT('Ctrl Pts',(-248.728770468346,-2.13683178406518,
125.286944511352));
#164587=CARTESIAN_POINT('Ctrl Pts',(-248.72137411141,-1.98985703168806,
125.230022880594));
#164588=CARTESIAN_POINT('Ctrl Pts',(-248.713977754475,-1.84059713581557,
125.178974508595));
#164589=CARTESIAN_POINT('Ctrl Pts',(-248.706581397539,-1.68956424639153,
125.133972339871));
#164590=CARTESIAN_POINT('Ctrl Pts',(-248.699183908203,-1.53850823344611,
125.088963281201));
#164591=CARTESIAN_POINT('Ctrl Pts',(-248.691786418866,-1.3856790442339,
125.050002375581));
#164592=CARTESIAN_POINT('Ctrl Pts',(-248.684388929529,-1.23160294524551,
125.017212377909));
#164593=CARTESIAN_POINT('Ctrl Pts',(-248.676988847014,-1.07747283512013,
124.984410885754));
#164594=CARTESIAN_POINT('Ctrl Pts',(-248.669588764499,-0.922095309844468,
124.957784686123));
#164595=CARTESIAN_POINT('Ctrl Pts',(-248.662188681984,-0.766005604067277,
124.937405191023));
#164596=CARTESIAN_POINT('Ctrl Pts',(-248.654780462318,-0.609744261611506,
124.917003286574));
#164597=CARTESIAN_POINT('Ctrl Pts',(-248.647372242651,-0.452769545104186,
124.902861852648));
#164598=CARTESIAN_POINT('Ctrl Pts',(-248.639964022985,-0.295621309973686,
124.89500036424));
#164599=CARTESIAN_POINT('Ctrl Pts',(-248.632551243682,-0.138376352727071,
124.887134037217));
#164600=CARTESIAN_POINT('Ctrl Pts',(-248.62513846438,0.0190419635371055,
124.885555361347));
#164601=CARTESIAN_POINT('Ctrl Pts',(-248.617725685078,0.176095543047275,
124.890231694198));
#164602=CARTESIAN_POINT('Ctrl Pts',(-248.610302314049,0.333373528077153,
124.894914708813));
#164603=CARTESIAN_POINT('Ctrl Pts',(-248.60287894302,0.490285364088859,
124.90587055631));
#164604=CARTESIAN_POINT('Ctrl Pts',(-248.595455571992,0.646298991936183,
124.92301483828));
#164605=CARTESIAN_POINT('Ctrl Pts',(-248.591519522552,0.729021160899325,
124.932105147951));
#164606=CARTESIAN_POINT('Ctrl Pts',(-248.587583473112,0.811490984336267,
124.94293439471));
#164607=CARTESIAN_POINT('Ctrl Pts',(-248.583647423672,0.893630636483042,
124.955484242736));
#164608=CARTESIAN_POINT('Ctrl Pts',(-248.576224157266,1.0485434569725,124.979152864451));
#164609=CARTESIAN_POINT('Ctrl Pts',(-248.568800890861,1.20274954650635,
125.00901603764));
#164610=CARTESIAN_POINT('Ctrl Pts',(-248.561377624455,1.35571426582556,
125.045023034828));
#164611=CARTESIAN_POINT('Ctrl Pts',(-248.553963131734,1.5084981935499,125.080987474736));
#164612=CARTESIAN_POINT('Ctrl Pts',(-248.546548639013,1.66004331170418,
125.12308119991));
#164613=CARTESIAN_POINT('Ctrl Pts',(-248.539134146292,1.80982133211593,
125.17120188482));
#164614=CARTESIAN_POINT('Ctrl Pts',(-248.531726799938,1.95945499083214,
125.219276189201));
#164615=CARTESIAN_POINT('Ctrl Pts',(-248.524319453584,2.10732458951269,
125.273365775303));
#164616=CARTESIAN_POINT('Ctrl Pts',(-248.516912107231,2.25291335888148,
125.333317576255));
#164617=CARTESIAN_POINT('Ctrl Pts',(-248.509510285555,2.39839354265291,
125.393224662892));
#164618=CARTESIAN_POINT('Ctrl Pts',(-248.50210846388,2.54159594059722,125.45898511709));
#164619=CARTESIAN_POINT('Ctrl Pts',(-248.494706642204,2.68202035570336,
125.530396513205));
#164620=CARTESIAN_POINT('Ctrl Pts',(-248.487308727893,2.82237064185423,
125.6017702118));
#164621=CARTESIAN_POINT('Ctrl Pts',(-248.479910813582,2.95994553382201,
125.678788742564));
#164622=CARTESIAN_POINT('Ctrl Pts',(-248.47251289927,3.09426629210827,125.761202214737));
#164623=CARTESIAN_POINT('Ctrl Pts',(-248.465116214358,3.22856472872152,
125.843601991286));
#164624=CARTESIAN_POINT('Ctrl Pts',(-248.457719529446,3.35960978706752,
125.931394734843));
#164625=CARTESIAN_POINT('Ctrl Pts',(-248.450322844533,3.48694865718476,
126.024285343613));
#164626=CARTESIAN_POINT('Ctrl Pts',(-248.442926487598,3.61428188096307,
126.117171833516));
#164627=CARTESIAN_POINT('Ctrl Pts',(-248.435530130662,3.73790894168576,
126.215155519181));
#164628=CARTESIAN_POINT('Ctrl Pts',(-248.428133773727,3.85740750667736,
126.317898995092));
#164629=CARTESIAN_POINT('Ctrl Pts',(-248.42073628439,3.97692436720433,126.420658201292));
#164630=CARTESIAN_POINT('Ctrl Pts',(-248.413338795054,4.09231119036169,
126.528178405362));
#164631=CARTESIAN_POINT('Ctrl Pts',(-248.405941305717,4.20318023908498,
126.64008319642));
#164632=CARTESIAN_POINT('Ctrl Pts',(-248.398541223202,4.31408815278158,
126.752027215529));
#164633=CARTESIAN_POINT('Ctrl Pts',(-248.391141140687,4.42047487634386,
126.868358616781));
#164634=CARTESIAN_POINT('Ctrl Pts',(-248.383741058172,4.52199102142404,
126.988665692043));
#164635=CARTESIAN_POINT('Ctrl Pts',(-248.376332838506,4.62361879394142,
127.109105057302));
#164636=CARTESIAN_POINT('Ctrl Pts',(-248.368924618839,4.72036505140227,
127.233528541592));
#164637=CARTESIAN_POINT('Ctrl Pts',(-248.361516399173,4.81192160389547,
127.361492475963));
#164638=CARTESIAN_POINT('Ctrl Pts',(-248.35410361987,4.90353450791928,127.489535170001));
#164639=CARTESIAN_POINT('Ctrl Pts',(-248.346690840568,4.98995113773683,
127.621122344922));
#164640=CARTESIAN_POINT('Ctrl Pts',(-248.339278061266,5.07090810244087,
127.755783641484));
#164641=CARTESIAN_POINT('Ctrl Pts',(-248.331854690237,5.1519807422527,127.890637348421));
#164642=CARTESIAN_POINT('Ctrl Pts',(-248.324431319209,5.22757795761725,
128.028573623214));
#164643=CARTESIAN_POINT('Ctrl Pts',(-248.31700794818,5.29748316434078,128.169099210034));
#164644=CARTESIAN_POINT('Ctrl Pts',(-248.31307189874,5.33454858229421,128.243609248024));
#164645=CARTESIAN_POINT('Ctrl Pts',(-248.309135849299,5.37001458430393,
128.318846918548));
#164646=CARTESIAN_POINT('Ctrl Pts',(-248.305199799859,5.40385453009061,
128.394736833628));
#164647=CARTESIAN_POINT('Ctrl Pts',(-248.297776533453,5.46767561174162,
128.537862845039));
#164648=CARTESIAN_POINT('Ctrl Pts',(-248.290353267048,5.52590303645513,
128.683742570062));
#164649=CARTESIAN_POINT('Ctrl Pts',(-248.282930000642,5.57829049711204,
128.83189878211));
#164650=CARTESIAN_POINT('Ctrl Pts',(-248.275515507921,5.63061604014097,
128.979879885819));
#164651=CARTESIAN_POINT('Ctrl Pts',(-248.268101015201,5.67711523505334,
129.130131772354));
#164652=CARTESIAN_POINT('Ctrl Pts',(-248.26068652248,5.71758861855437,129.282154668465));
#164653=CARTESIAN_POINT('Ctrl Pts',(-248.253279176126,5.75802299228471,
129.434031039186));
#164654=CARTESIAN_POINT('Ctrl Pts',(-248.245871829772,5.79244302160307,
129.58767466294));
#164655=CARTESIAN_POINT('Ctrl Pts',(-248.238464483418,5.82069815958615,
129.742568030716));
#164656=CARTESIAN_POINT('Ctrl Pts',(-248.231062661743,5.84893222382131,
129.897345873174));
#164657=CARTESIAN_POINT('Ctrl Pts',(-248.223660840068,5.8710104852747,130.053371238049));
#164658=CARTESIAN_POINT('Ctrl Pts',(-248.216259018392,5.88683288166969,
130.210113879424));
#164659=CARTESIAN_POINT('Ctrl Pts',(-248.208861104081,5.90264692554483,
130.366773777579));
#164660=CARTESIAN_POINT('Ctrl Pts',(-248.201463189769,5.91221164389696,
130.524149827675));
#164661=CARTESIAN_POINT('Ctrl Pts',(-248.194065275458,5.9154785065081,130.681704180553));
#164662=CARTESIAN_POINT('Ctrl Pts',(-248.186668590546,5.91874482622592,
130.839232350755));
#164663=CARTESIAN_POINT('Ctrl Pts',(-248.179271905634,5.91571535964195,
130.996938392079));
#164664=CARTESIAN_POINT('Ctrl Pts',(-248.171875220721,5.90639362940904,
131.154281832951));
#164665=CARTESIAN_POINT('Ctrl Pts',(-248.164478863786,5.89707231251142,
131.31161829705));
#164666=CARTESIAN_POINT('Ctrl Pts',(-248.157082506851,5.88145930879928,
131.468591820021));
#164667=CARTESIAN_POINT('Ctrl Pts',(-248.149686149915,5.85961020596212,
131.624664705502));
#164668=CARTESIAN_POINT('Ctrl Pts',(-248.142288660579,5.83775775797154,
131.78076148614));
#164669=CARTESIAN_POINT('Ctrl Pts',(-248.134891171242,5.80966736155416,
131.935956985013));
#164670=CARTESIAN_POINT('Ctrl Pts',(-248.127493681905,5.77544612049189,
132.08972152867));
#164671=CARTESIAN_POINT('Ctrl Pts',(-248.12009359939,5.74121288322676,132.24353997425));
#164672=CARTESIAN_POINT('Ctrl Pts',(-248.112693516876,5.70084460340386,
132.395926101739));
#164673=CARTESIAN_POINT('Ctrl Pts',(-248.105293434361,5.65449880979943,
132.546363422523));
#164674=CARTESIAN_POINT('Ctrl Pts',(-248.097885214694,5.60810205423026,
132.696966164607));
#164675=CARTESIAN_POINT('Ctrl Pts',(-248.090476995028,5.5557147683582,132.845615463476));
#164676=CARTESIAN_POINT('Ctrl Pts',(-248.083068775361,5.49754363926177,
132.991812216325));
#164677=CARTESIAN_POINT('Ctrl Pts',(-248.075655996059,5.43933670680584,
133.138098950836));
#164678=CARTESIAN_POINT('Ctrl Pts',(-248.068243216757,5.3753389890633,133.281929791188));
#164679=CARTESIAN_POINT('Ctrl Pts',(-248.060830437455,5.3058038433676,133.42282889849));
#164680=CARTESIAN_POINT('Ctrl Pts',(-248.053407066426,5.23616934259515,
133.563929329044));
#164681=CARTESIAN_POINT('Ctrl Pts',(-248.045983695398,5.16098178952406,
133.70208933316));
#164682=CARTESIAN_POINT('Ctrl Pts',(-248.038560324369,5.08053910520641,
133.836860075599));
#164683=CARTESIAN_POINT('Ctrl Pts',(-248.034624274928,5.0378864637818,133.908318757025));
#164684=CARTESIAN_POINT('Ctrl Pts',(-248.030688225487,4.99375712111194,
133.978825107679));
#164685=CARTESIAN_POINT('Ctrl Pts',(-248.026752176046,4.94820010351743,
134.048315965294));
#164686=CARTESIAN_POINT('Ctrl Pts',(-248.01932890964,4.86228099012706,134.179373554009));
#164687=CARTESIAN_POINT('Ctrl Pts',(-248.011905643235,4.77102159127743,
134.307213490192));
#164688=CARTESIAN_POINT('Ctrl Pts',(-248.004482376829,4.67469027619907,
134.431370596062));
#164689=CARTESIAN_POINT('Ctrl Pts',(-247.997067884108,4.57847281673531,
134.555380958543));
#164690=CARTESIAN_POINT('Ctrl Pts',(-247.989653391387,4.47719559989458,
134.675716862927));
#164691=CARTESIAN_POINT('Ctrl Pts',(-247.982238898666,4.37117128428337,
134.791940355447));
#164692=CARTESIAN_POINT('Ctrl Pts',(-247.974831552313,4.26524915889839,
134.908051827389));
#164693=CARTESIAN_POINT('Ctrl Pts',(-247.967424205959,4.15458929342252,
135.020058504474));
#164694=CARTESIAN_POINT('Ctrl Pts',(-247.960016859605,4.03954570855317,
135.127554001051));
#164695=CARTESIAN_POINT('Ctrl Pts',(-247.95261503793,3.92458792753074,135.23496932343));
#164696=CARTESIAN_POINT('Ctrl Pts',(-247.945213216254,3.8052532088006,135.337879910926));
#164697=CARTESIAN_POINT('Ctrl Pts',(-247.937811394579,3.68193357716447,
135.435914967441));
#164698=CARTESIAN_POINT('Ctrl Pts',(-247.930413480267,3.5586790450016,135.533898272014));
#164699=CARTESIAN_POINT('Ctrl Pts',(-247.923015565956,3.43144408083488,
135.627010939651));
#164700=CARTESIAN_POINT('Ctrl Pts',(-247.915617651645,3.30065496062629,
135.714921419897));
#164701=CARTESIAN_POINT('Ctrl Pts',(-247.908220966732,3.16988757519691,
135.802817291017));
#164702=CARTESIAN_POINT('Ctrl Pts',(-247.90082428182,3.03556751547619,135.8855124825));
#164703=CARTESIAN_POINT('Ctrl Pts',(-247.893427596908,2.89815139958546,
135.962717819969));
#164704=CARTESIAN_POINT('Ctrl Pts',(-247.886031239973,2.7607413768697,136.039919734071));
#164705=CARTESIAN_POINT('Ctrl Pts',(-247.878634883037,2.620235896397,136.111632095323));
#164706=CARTESIAN_POINT('Ctrl Pts',(-247.871238526102,2.47711738385079,
136.177611033201));
#164707=CARTESIAN_POINT('Ctrl Pts',(-247.863841036765,2.33397695949535,
136.243600072623));
#164708=CARTESIAN_POINT('Ctrl Pts',(-247.856443547429,2.18822304551935,
136.303853784557));
#164709=CARTESIAN_POINT('Ctrl Pts',(-247.849046058092,2.04035916340784,
136.35817597701));
#164710=CARTESIAN_POINT('Ctrl Pts',(-247.841645975577,1.89244344784061,
136.412517212024));
#164711=CARTESIAN_POINT('Ctrl Pts',(-247.834245893062,1.7424166416891,136.460922659066));
#164712=CARTESIAN_POINT('Ctrl Pts',(-247.826845810547,1.59079842960389,
136.503245676845));
#164713=CARTESIAN_POINT('Ctrl Pts',(-247.819437590881,1.43901349770798,
136.545615233133));
#164714=CARTESIAN_POINT('Ctrl Pts',(-247.812029371214,1.28563402495745,
136.581888902843));
#164715=CARTESIAN_POINT('Ctrl Pts',(-247.804621151548,1.1311916400925,136.611970800411));
#164716=CARTESIAN_POINT('Ctrl Pts',(-247.797208372246,0.976654198516669,
136.642071212885));
#164717=CARTESIAN_POINT('Ctrl Pts',(-247.789795592944,0.821052909356628,
136.665972202912));
#164718=CARTESIAN_POINT('Ctrl Pts',(-247.782382813641,0.664925055174279,
136.683629724649));
#164719=CARTESIAN_POINT('Ctrl Pts',(-247.774959442613,0.508574118191981,
136.701312476281));
#164720=CARTESIAN_POINT('Ctrl Pts',(-247.767536071584,0.351695484840332,
136.712733915431));
#164721=CARTESIAN_POINT('Ctrl Pts',(-247.760112700555,0.194827806524608,
136.717902085105));
#164722=CARTESIAN_POINT('Ctrl Pts',(-247.756176651114,0.111652799491557,
136.720642372675));
#164723=CARTESIAN_POINT('Ctrl Pts',(-247.752240601674,0.0284808222158047,
136.72162551162));
#164724=CARTESIAN_POINT('Ctrl Pts',(-247.748304552233,-0.0546084851756728,
136.720858608426));
#164725=CARTESIAN_POINT('Ctrl Pts',(-247.740881285827,-0.211312325782589,
136.719412252935));
#164726=CARTESIAN_POINT('Ctrl Pts',(-247.733458019422,-0.368195618920861,
136.711733744254));
#164727=CARTESIAN_POINT('Ctrl Pts',(-247.726034753017,-0.524721937222637,
136.697797429062));
#164728=CARTESIAN_POINT('Ctrl Pts',(-247.718620260296,-0.681063254415326,
136.683877585438));
#164729=CARTESIAN_POINT('Ctrl Pts',(-247.711205767575,-0.837048068398791,
136.663714690278));
#164730=CARTESIAN_POINT('Ctrl Pts',(-247.703791274854,-0.992138916650457,
136.637335067413));
#164731=CARTESIAN_POINT('Ctrl Pts',(-247.6963839285,-1.14708028250351,136.610980870222));
#164732=CARTESIAN_POINT('Ctrl Pts',(-247.688976582146,-1.30112903243422,
136.578421936227));
#164733=CARTESIAN_POINT('Ctrl Pts',(-247.681569235793,-1.45375190585053,
136.539736451697));
#164734=CARTESIAN_POINT('Ctrl Pts',(-247.674167414117,-1.60626094736971,
136.501079820261));
#164735=CARTESIAN_POINT('Ctrl Pts',(-247.666765592442,-1.75734586959446,
136.456305827931));
#164736=CARTESIAN_POINT('Ctrl Pts',(-247.659363770767,-1.90648281228602,
136.405543871929));
#164737=CARTESIAN_POINT('Ctrl Pts',(-247.651965856455,-2.05554102674641,
136.354808712768));
#164738=CARTESIAN_POINT('Ctrl Pts',(-247.644567942144,-2.20265295713487,
136.298092005196));
#164739=CARTESIAN_POINT('Ctrl Pts',(-247.637170027833,-2.34730924809386,
136.235573176131));
#164740=CARTESIAN_POINT('Ctrl Pts',(-247.62977334292,-2.49194149980182,
136.173064736561));
#164741=CARTESIAN_POINT('Ctrl Pts',(-247.622376658008,-2.63411857967471,
136.104756237117));
#164742=CARTESIAN_POINT('Ctrl Pts',(-247.614979973096,-2.77335038386919,
136.030875537739));
#164743=CARTESIAN_POINT('Ctrl Pts',(-247.607583616161,-2.91257601437956,
135.956998114309));
#164744=CARTESIAN_POINT('Ctrl Pts',(-247.600187259225,-3.04885629913221,
135.877549157195));
#164745=CARTESIAN_POINT('Ctrl Pts',(-247.59279090229,-3.18172530008505,
135.792802726812));
#164746=CARTESIAN_POINT('Ctrl Pts',(-247.585393412953,-3.31461464362113,
135.708043321535));
#164747=CARTESIAN_POINT('Ctrl Pts',(-247.577995923617,-3.44409134868632,
135.617985028821));
#164748=CARTESIAN_POINT('Ctrl Pts',(-247.57059843428,-3.56971818773886,
135.522945428993));
#164749=CARTESIAN_POINT('Ctrl Pts',(-247.563198351765,-3.6953890650849,
135.42787251318));
#164750=CARTESIAN_POINT('Ctrl Pts',(-247.55579826925,-3.81720709192725,
135.327815038682));
#164751=CARTESIAN_POINT('Ctrl Pts',(-247.548398186736,-3.93476799254689,
135.223130967712));
#164752=CARTESIAN_POINT('Ctrl Pts',(-247.540989967069,-4.05245816346248,
135.118331785844));
#164753=CARTESIAN_POINT('Ctrl Pts',(-247.533581747403,-4.16588158063674,
135.008896096001));
#164754=CARTESIAN_POINT('Ctrl Pts',(-247.526173527736,-4.27467021450847,
134.895219344006));
#164755=CARTESIAN_POINT('Ctrl Pts',(-247.518760748434,-4.38352580596943,
134.781472625868));
#164756=CARTESIAN_POINT('Ctrl Pts',(-247.511347969132,-4.4877406833542,
134.663479923365));
#164757=CARTESIAN_POINT('Ctrl Pts',(-247.50393518983,-4.58698737529911,
134.54166945968));
#164758=CARTESIAN_POINT('Ctrl Pts',(-247.496511818802,-4.68637587557155,
134.419684947493));
#164759=CARTESIAN_POINT('Ctrl Pts',(-247.489088447773,-4.78078178910005,
134.293872077067));
#164760=CARTESIAN_POINT('Ctrl Pts',(-247.481665076744,-4.86992072845301,
134.164688378527));
#164761=CARTESIAN_POINT('Ctrl Pts',(-247.477729027303,-4.91718433296531,
134.096192081829));
#164762=CARTESIAN_POINT('Ctrl Pts',(-247.473792977861,-4.96296796091647,
134.0267485524));
#164763=CARTESIAN_POINT('Ctrl Pts',(-247.46985692842,-5.0072345437592,133.956428634961));
#164764=CARTESIAN_POINT('Ctrl Pts',(-247.462236797479,-5.09293396461543,
133.820290360621));
#164765=CARTESIAN_POINT('Ctrl Pts',(-247.454616666537,-5.1731927381962,
133.680472003976));
#164766=CARTESIAN_POINT('Ctrl Pts',(-247.446996535596,-5.24768859798355,
133.537434883131));
#164767=CARTESIAN_POINT('Ctrl Pts',(-247.439386872341,-5.32208212365789,
133.394594250747));
#164768=CARTESIAN_POINT('Ctrl Pts',(-247.431777209087,-5.39072834575388,
133.248543966223));
#164769=CARTESIAN_POINT('Ctrl Pts',(-247.424167545832,-5.45334834088897,
133.099773964966));
#164770=CARTESIAN_POINT('Ctrl Pts',(-247.41656715745,-5.51589201301343,
132.95118528877));
#164771=CARTESIAN_POINT('Ctrl Pts',(-247.408966769067,-5.57242395691912,
132.799883816999));
#164772=CARTESIAN_POINT('Ctrl Pts',(-247.401366380684,-5.62271116517123,
132.6463838844));
#164773=CARTESIAN_POINT('Ctrl Pts',(-247.393776486392,-5.67292894032262,
132.493095893897));
#164774=CARTESIAN_POINT('Ctrl Pts',(-247.3861865921,-5.71691906458911,132.337615822874));
#164775=CARTESIAN_POINT('Ctrl Pts',(-247.378596697808,-5.75449676660908,
132.180477446031));
#164776=CARTESIAN_POINT('Ctrl Pts',(-247.371012940078,-5.79204408640011,
132.023466118313));
#164777=CARTESIAN_POINT('Ctrl Pts',(-247.363429182348,-5.82318923077531,
131.864799491174));
#164778=CARTESIAN_POINT('Ctrl Pts',(-247.355845424619,-5.8477971054084,
131.705026802385));
#164779=CARTESIAN_POINT('Ctrl Pts',(-247.348267771385,-5.87238517209377,
131.545382721577));
#164780=CARTESIAN_POINT('Ctrl Pts',(-247.340690118151,-5.89044640661716,
131.384634695695));
#164781=CARTESIAN_POINT('Ctrl Pts',(-247.333112464918,-5.90189671411097,
131.223342405316));
#164782=CARTESIAN_POINT('Ctrl Pts',(-247.326533374015,-5.9118381315317,
131.083304769971));
#164783=CARTESIAN_POINT('Ctrl Pts',(-247.319954283113,-5.91679692710892,
130.942857179328));
#164784=CARTESIAN_POINT('Ctrl Pts',(-247.31337519221,-5.91674966518615,
130.802370135328));
#164785=CARTESIAN_POINT('',(-245.56337519221,-5.92144182645146,130.799714417675));
#164786=CARTESIAN_POINT('Ctrl Pts',(-247.313373802672,-5.90755386651321,
130.802343603462));
#164787=CARTESIAN_POINT('Ctrl Pts',(-247.272718969984,-5.9101514079421,
129.935566300425));
#164788=CARTESIAN_POINT('Ctrl Pts',(-247.139248262692,-5.32479902775277,
127.093265132076));
#164789=CARTESIAN_POINT('Ctrl Pts',(-246.912961680793,-0.92912039214145,
123.867913700948));
#164790=CARTESIAN_POINT('Ctrl Pts',(-246.634514056983,5.3336169743627,126.273346327016));
#164791=CARTESIAN_POINT('Ctrl Pts',(-246.356066433168,6.6950209031102,132.842559733769));
#164792=CARTESIAN_POINT('Ctrl Pts',(-246.077618809355,1.90402769183364,
137.538767724297));
#164793=CARTESIAN_POINT('Ctrl Pts',(-245.813388395704,-4.30271337160949,
136.122583916631));
#164794=CARTESIAN_POINT('Ctrl Pts',(-245.641973856654,-5.90708458492476,
132.465498504199));
#164795=CARTESIAN_POINT('Ctrl Pts',(-245.56337519221,-5.92144182645146,
130.799714417675));
#164796=CARTESIAN_POINT('',(-243.813375192209,-5.9225958886547,130.808561907707));
#164797=CARTESIAN_POINT('Ctrl Pts',(-245.56337519221,-5.92144182645146,
130.799714417675));
#164798=CARTESIAN_POINT('Ctrl Pts',(-245.54915798205,-5.92403881612739,
130.498401378748));
#164799=CARTESIAN_POINT('Ctrl Pts',(-245.53494077189,-5.90303585155336,
130.197451465269));
#164800=CARTESIAN_POINT('Ctrl Pts',(-245.427907687125,-5.55779885964375,
127.96065567089));
#164801=CARTESIAN_POINT('Ctrl Pts',(-245.242275937917,-2.84039908430047,
124.408292014724));
#164802=CARTESIAN_POINT('Ctrl Pts',(-244.963828314104,3.84588857597675,
124.957421111165));
#164803=CARTESIAN_POINT('Ctrl Pts',(-244.685380690291,6.99799251703414,
130.879601975114));
#164804=CARTESIAN_POINT('Ctrl Pts',(-244.406933066478,3.71928320587602,
136.732639707219));
#164805=CARTESIAN_POINT('Ctrl Pts',(-244.128485442666,-2.97726567439561,
137.137878568468));
#164806=CARTESIAN_POINT('Ctrl Pts',(-243.930632817909,-5.79148458215932,
133.290250095944));
#164807=CARTESIAN_POINT('Ctrl Pts',(-243.825596067757,-5.92467647219331,
131.067434134564));
#164808=CARTESIAN_POINT('Ctrl Pts',(-243.813375192209,-5.9225958886547,
130.808561907707));
#164809=CARTESIAN_POINT('',(-242.06337519221,-5.90805017840298,130.806988762596));
#164810=CARTESIAN_POINT('Ctrl Pts',(-243.813375192209,-5.9225958886547,
130.808561907707));
#164811=CARTESIAN_POINT('Ctrl Pts',(-243.732780193153,-5.90887472541408,
129.101335056553));
#164812=CARTESIAN_POINT('Ctrl Pts',(-243.559369319492,-4.23448331121838,
125.404542141305));
#164813=CARTESIAN_POINT('Ctrl Pts',(-243.293142571227,2.04838543811749,
124.11244925927));
#164814=CARTESIAN_POINT('Ctrl Pts',(-243.014694947414,6.73729691441007,
128.910583751768));
#164815=CARTESIAN_POINT('Ctrl Pts',(-242.736247323601,5.23496166160834,
135.449006667785));
#164816=CARTESIAN_POINT('Ctrl Pts',(-242.457799699788,-1.07804761611268,
137.719226767226));
#164817=CARTESIAN_POINT('Ctrl Pts',(-242.233508989324,-5.3652113839518,
134.429383518755));
#164818=CARTESIAN_POINT('Ctrl Pts',(-242.102034153465,-5.91133744411979,
131.631040389034));
#164819=CARTESIAN_POINT('Ctrl Pts',(-242.06337519221,-5.90805017840298,
130.806988762596));
#164820=CARTESIAN_POINT('',(-240.313375158645,-5.91547317117931,130.799225748986));
#164821=CARTESIAN_POINT('Ctrl Pts',(-242.06337519221,-5.90805017840298,
130.806988762596));
#164822=CARTESIAN_POINT('Ctrl Pts',(-242.00921827886,-5.90344508403932,
129.652583908473));
#164823=CARTESIAN_POINT('Ctrl Pts',(-241.862245490907,-5.01819434382023,
126.513200125347));
#164824=CARTESIAN_POINT('Ctrl Pts',(-241.622456828348,0.0858910237578114,
123.80649070863));
#164825=CARTESIAN_POINT('Ctrl Pts',(-241.344009204537,5.93393234070992,
127.094103550159));
#164826=CARTESIAN_POINT('Ctrl Pts',(-241.065561580723,6.32897972525682,
133.791261380503));
#164827=CARTESIAN_POINT('Ctrl Pts',(-240.787113956911,0.908003930142733,
137.743603327918));
#164828=CARTESIAN_POINT('Ctrl Pts',(-240.536385160739,-4.72467356506664,
135.560472003922));
#164829=CARTESIAN_POINT('Ctrl Pts',(-240.378472239172,-5.9015401168494,
132.183950904784));
#164830=CARTESIAN_POINT('Ctrl Pts',(-240.313375192209,-5.91293939285975,
130.799228662519));
#164831=CARTESIAN_POINT('',(-238.56337519221,-5.92098466177766,130.803851200521));
#164832=CARTESIAN_POINT('Ctrl Pts',(-240.313375141761,-5.91674777057218,
130.799224283353));
#164833=CARTESIAN_POINT('Ctrl Pts',(-240.304447198716,-5.91658280276366,
130.609191300127));
#164834=CARTESIAN_POINT('Ctrl Pts',(-240.29551925567,-5.90725896805116,
130.419559254438));
#164835=CARTESIAN_POINT('Ctrl Pts',(-240.286591312625,-5.88891442289698,
130.231108943084));
#164836=CARTESIAN_POINT('Ctrl Pts',(-240.277195878735,-5.8696093085647,
130.032790872178));
#164837=CARTESIAN_POINT('Ctrl Pts',(-240.267800444845,-5.84031377300887,
129.835781692581));
#164838=CARTESIAN_POINT('Ctrl Pts',(-240.258405010955,-5.8012449903555,
129.640965962096));
#164839=CARTESIAN_POINT('Ctrl Pts',(-240.249009577065,-5.76217620770222,
129.446150231612));
#164840=CARTESIAN_POINT('Ctrl Pts',(-240.239614143174,-5.71333430736417,
129.25352788837));
#164841=CARTESIAN_POINT('Ctrl Pts',(-240.230218709284,-5.65499162829623,
129.063958294424));
#164842=CARTESIAN_POINT('Ctrl Pts',(-240.222795442879,-5.60889548685207,
128.914180688121));
#164843=CARTESIAN_POINT('Ctrl Pts',(-240.215372176473,-5.5567750380937,
128.76600921319));
#164844=CARTESIAN_POINT('Ctrl Pts',(-240.207948910068,-5.4987587456095,
128.619965319072));
#164845=CARTESIAN_POINT('Ctrl Pts',(-240.200534417347,-5.44081102356507,
128.474094036708));
#164846=CARTESIAN_POINT('Ctrl Pts',(-240.193119924626,-5.37698146490024,
128.330345673324));
#164847=CARTESIAN_POINT('Ctrl Pts',(-240.185705431904,-5.30744864521202,
128.189227840643));
#164848=CARTESIAN_POINT('Ctrl Pts',(-240.178298085551,-5.23798284387309,
128.048246022642));
#164849=CARTESIAN_POINT('Ctrl Pts',(-240.170890739197,-5.16282488887633,
127.909890020461));
#164850=CARTESIAN_POINT('Ctrl Pts',(-240.163483392843,-5.08220186366389,
127.77464862144));
#164851=CARTESIAN_POINT('Ctrl Pts',(-240.156081571168,-5.00163897014562,
127.639508090556));
#164852=CARTESIAN_POINT('Ctrl Pts',(-240.148679749492,-4.91561931271538,
127.507477856713));
#164853=CARTESIAN_POINT('Ctrl Pts',(-240.141277927817,-4.8244163750696,
127.379023086393));
#164854=CARTESIAN_POINT('Ctrl Pts',(-240.133880013506,-4.73326158274495,
127.250636126348));
#164855=CARTESIAN_POINT('Ctrl Pts',(-240.126482099194,-4.63692917506799,
127.125821174471));
#164856=CARTESIAN_POINT('Ctrl Pts',(-240.119084184883,-4.53573644743927,
127.005015221071));
#164857=CARTESIAN_POINT('Ctrl Pts',(-240.111687499971,-4.43456053620563,
126.884229343427));
#164858=CARTESIAN_POINT('Ctrl Pts',(-240.104290815059,-4.32852614753222,
126.767451427893));
#164859=CARTESIAN_POINT('Ctrl Pts',(-240.096894130146,-4.21799150393006,
126.655086194818));
#164860=CARTESIAN_POINT('Ctrl Pts',(-240.089497773211,-4.10746176154984,
126.542725944135));
#164861=CARTESIAN_POINT('Ctrl Pts',(-240.082101416275,-3.99243242279038,
126.434778252988));
#164862=CARTESIAN_POINT('Ctrl Pts',(-240.07470505934,-3.87329909540618,
126.331611498733));
#164863=CARTESIAN_POINT('Ctrl Pts',(-240.067307570004,-3.75414752840543,
126.228428949383));
#164864=CARTESIAN_POINT('Ctrl Pts',(-240.059910080667,-3.63089100390062,
126.130029038771));
#164865=CARTESIAN_POINT('Ctrl Pts',(-240.05251259133,-3.50395864907101,
126.036740210266));
#164866=CARTESIAN_POINT('Ctrl Pts',(-240.045112508815,-3.37698179830101,
125.943418679507));
#164867=CARTESIAN_POINT('Ctrl Pts',(-240.0377124263,-3.24632685230914,125.855212019014));
#164868=CARTESIAN_POINT('Ctrl Pts',(-240.030312343786,-3.1124522400116,
125.772405568468));
#164869=CARTESIAN_POINT('Ctrl Pts',(-240.022904124119,-2.97843041881538,
125.689508063716));
#164870=CARTESIAN_POINT('Ctrl Pts',(-240.015495904453,-2.84118217866342,
125.612022824149));
#164871=CARTESIAN_POINT('Ctrl Pts',(-240.008087684786,-2.70119153247436,
125.540189755275));
#164872=CARTESIAN_POINT('Ctrl Pts',(-240.000674905484,-2.56111472437804,
125.468312474347));
#164873=CARTESIAN_POINT('Ctrl Pts',(-239.993262126182,-2.41829248476486,
125.402094452746));
#164874=CARTESIAN_POINT('Ctrl Pts',(-239.98584934688,-2.27322866963384,
125.341727371772));
#164875=CARTESIAN_POINT('Ctrl Pts',(-239.978425975851,-2.12795758052115,
125.281274035481));
#164876=CARTESIAN_POINT('Ctrl Pts',(-239.971002604823,-1.98043886821596,
125.226688466011));
#164877=CARTESIAN_POINT('Ctrl Pts',(-239.963579233794,-1.83119218500668,
125.178112689855));
#164878=CARTESIAN_POINT('Ctrl Pts',(-239.959643184353,-1.75205801244773,
125.152356647779));
#164879=CARTESIAN_POINT('Ctrl Pts',(-239.955707134913,-1.67243823896076,
125.128289324805));
#164880=CARTESIAN_POINT('Ctrl Pts',(-239.951771085472,-1.59241134073006,
125.105926035647));
#164881=CARTESIAN_POINT('Ctrl Pts',(-239.944347819067,-1.44148310821466,
125.063749570226));
#164882=CARTESIAN_POINT('Ctrl Pts',(-239.936924552661,-1.28864987425473,
125.027509678405));
#164883=CARTESIAN_POINT('Ctrl Pts',(-239.929501286256,-1.13441978674124,
124.997380136287));
#164884=CARTESIAN_POINT('Ctrl Pts',(-239.922086793535,-0.980371986382731,
124.967286204787));
#164885=CARTESIAN_POINT('Ctrl Pts',(-239.914672300814,-0.824930981520049,
124.94328831858));
#164886=CARTESIAN_POINT('Ctrl Pts',(-239.907257808093,-0.668620364745964,
124.925510613497));
#164887=CARTESIAN_POINT('Ctrl Pts',(-239.899850461739,-0.512460406029317,
124.907750043235));
#164888=CARTESIAN_POINT('Ctrl Pts',(-239.892443115385,-0.355432872438929,
124.896197760646));
#164889=CARTESIAN_POINT('Ctrl Pts',(-239.885035769031,-0.198071738752809,
124.890926915493));
#164890=CARTESIAN_POINT('Ctrl Pts',(-239.877633947356,-0.0408279709366401,
124.885660001536));
#164891=CARTESIAN_POINT('Ctrl Pts',(-239.870232125681,0.11674853007498,
124.886665209125));
#164892=CARTESIAN_POINT('Ctrl Pts',(-239.862830304005,0.274118581926308,
124.893963882528));
#164893=CARTESIAN_POINT('Ctrl Pts',(-239.855432389694,0.431405559351781,
124.901258703019));
#164894=CARTESIAN_POINT('Ctrl Pts',(-239.848034475382,0.588485932708498,
124.914840355609));
#164895=CARTESIAN_POINT('Ctrl Pts',(-239.840636561071,0.744820543760275,
124.934678094627));
#164896=CARTESIAN_POINT('Ctrl Pts',(-239.833239876159,0.90112917483567,
124.954512536973));
#164897=CARTESIAN_POINT('Ctrl Pts',(-239.825843191246,1.05669191960906,
124.980600955408));
#164898=CARTESIAN_POINT('Ctrl Pts',(-239.818446506334,1.21097464736905,
125.012860728424));
#164899=CARTESIAN_POINT('Ctrl Pts',(-239.811050149399,1.36525053407166,
125.045119071008));
#164900=CARTESIAN_POINT('Ctrl Pts',(-239.803653792463,1.51824615121821,
125.083548147673));
#164901=CARTESIAN_POINT('Ctrl Pts',(-239.796257435528,1.66943773685229,
125.128014239369));
#164902=CARTESIAN_POINT('Ctrl Pts',(-239.788859946191,1.82065247030411,
125.172487138937));
#164903=CARTESIAN_POINT('Ctrl Pts',(-239.781462456855,1.97006226413546,
125.222998788572));
#164904=CARTESIAN_POINT('Ctrl Pts',(-239.774064967518,2.11715883591395,
125.279365683088));
#164905=CARTESIAN_POINT('Ctrl Pts',(-239.766664885003,2.26430697216745,
125.335752336931));
#164906=CARTESIAN_POINT('Ctrl Pts',(-239.759264802488,2.40913992351535,
125.39799818877));
#164907=CARTESIAN_POINT('Ctrl Pts',(-239.751864719973,2.55116983357646,
125.465871782441));
#164908=CARTESIAN_POINT('Ctrl Pts',(-239.744456500306,2.69335592012452,
125.533820010106));
#164909=CARTESIAN_POINT('Ctrl Pts',(-239.73704828064,2.83273247294492,125.60740817695));
#164910=CARTESIAN_POINT('Ctrl Pts',(-239.729640060973,2.96883603193272,
125.686358743983));
#164911=CARTESIAN_POINT('Ctrl Pts',(-239.722227281671,3.10502336039045,
125.765357903773));
#164912=CARTESIAN_POINT('Ctrl Pts',(-239.714814502369,3.23793336649246,
125.849725840755));
#164913=CARTESIAN_POINT('Ctrl Pts',(-239.707401723067,3.36713243685951,
125.939142255031));
#164914=CARTESIAN_POINT('Ctrl Pts',(-239.699978352038,3.49651611291696,
126.028686431672));
#164915=CARTESIAN_POINT('Ctrl Pts',(-239.69255498101,3.62217796580202,126.123293268655));
#164916=CARTESIAN_POINT('Ctrl Pts',(-239.685131609981,3.74371761984629,
126.222602336583));
#164917=CARTESIAN_POINT('Ctrl Pts',(-239.68119556054,3.80816086072349,126.275258387286));
#164918=CARTESIAN_POINT('Ctrl Pts',(-239.677259511099,3.87144581355598,
126.329235781727));
#164919=CARTESIAN_POINT('Ctrl Pts',(-239.673323461659,3.93351717534727,
126.384476773646));
#164920=CARTESIAN_POINT('Ctrl Pts',(-239.665900195253,4.05058182650684,
126.488659560394));
#164921=CARTESIAN_POINT('Ctrl Pts',(-239.658476928847,4.16368156997823,
126.597653941848));
#164922=CARTESIAN_POINT('Ctrl Pts',(-239.651053662442,4.27239553665532,
126.711126329027));
#164923=CARTESIAN_POINT('Ctrl Pts',(-239.643639169721,4.38098101245193,
126.824464601268));
#164924=CARTESIAN_POINT('Ctrl Pts',(-239.636224677,4.48519077375898,126.942270077301));
#164925=CARTESIAN_POINT('Ctrl Pts',(-239.628810184279,4.58463736700177,
127.064169342298));
#164926=CARTESIAN_POINT('Ctrl Pts',(-239.621402837925,4.6839881098739,127.185951116194));
#164927=CARTESIAN_POINT('Ctrl Pts',(-239.613995491571,4.77858458991015,
127.311818536534));
#164928=CARTESIAN_POINT('Ctrl Pts',(-239.606588145218,4.8680766377315,127.441361894451));
#164929=CARTESIAN_POINT('Ctrl Pts',(-239.599186323542,4.95750193900725,
127.570808634044));
#164930=CARTESIAN_POINT('Ctrl Pts',(-239.591784501867,5.04183017721024,
127.703925546399));
#164931=CARTESIAN_POINT('Ctrl Pts',(-239.584382680192,5.1207519535698,127.840270539226));
#164932=CARTESIAN_POINT('Ctrl Pts',(-239.57698476588,5.19963206773796,127.976543556594));
#164933=CARTESIAN_POINT('Ctrl Pts',(-239.569586851569,5.27311121746229,
128.116040938422));
#164934=CARTESIAN_POINT('Ctrl Pts',(-239.562188937258,5.34092384175067,
128.258292456829));
#164935=CARTESIAN_POINT('Ctrl Pts',(-239.554792252345,5.40872519681105,
128.400520335614));
#164936=CARTESIAN_POINT('Ctrl Pts',(-239.547395567433,5.47086173490065,
128.545501105967));
#164937=CARTESIAN_POINT('Ctrl Pts',(-239.539998882521,5.52711425713773,
128.692740729649));
#164938=CARTESIAN_POINT('Ctrl Pts',(-239.532602525585,5.5833642850792,128.839973824573));
#164939=CARTESIAN_POINT('Ctrl Pts',(-239.52520616865,5.63373068270668,128.989465224959));
#164940=CARTESIAN_POINT('Ctrl Pts',(-239.517809811715,5.67804284551261,
129.140701996627));
#164941=CARTESIAN_POINT('Ctrl Pts',(-239.510412322378,5.7223617926238,129.291961923032));
#164942=CARTESIAN_POINT('Ctrl Pts',(-239.503014833041,5.76062455432498,
129.444967394531));
#164943=CARTESIAN_POINT('Ctrl Pts',(-239.495617343705,5.79271077965507,
129.599191589683));
#164944=CARTESIAN_POINT('Ctrl Pts',(-239.48821726119,5.82480825276165,129.753469847888));
#164945=CARTESIAN_POINT('Ctrl Pts',(-239.480817178675,5.85072480266036,
129.908967315098));
#164946=CARTESIAN_POINT('Ctrl Pts',(-239.47341709616,5.87039146168622,130.065148436212));
#164947=CARTESIAN_POINT('Ctrl Pts',(-239.466008876493,5.89007974622549,
130.221501294526));
#164948=CARTESIAN_POINT('Ctrl Pts',(-239.458600656827,5.90350436859606,
130.378538937433));
#164949=CARTESIAN_POINT('Ctrl Pts',(-239.45119243716,5.91064831870181,130.535721426219));
#164950=CARTESIAN_POINT('Ctrl Pts',(-239.443779657858,5.91779666578963,
130.693000658204));
#164951=CARTESIAN_POINT('Ctrl Pts',(-239.436366878556,5.91865663578798,
130.850424541285));
#164952=CARTESIAN_POINT('Ctrl Pts',(-239.428954099254,5.91326332744977,
131.007455134325));
#164953=CARTESIAN_POINT('Ctrl Pts',(-239.421530728226,5.90786231289968,
131.164710100041));
#164954=CARTESIAN_POINT('Ctrl Pts',(-239.414107357197,5.89619020248658,
131.321570282092));
#164955=CARTESIAN_POINT('Ctrl Pts',(-239.406683986168,5.87833382284187,
131.477504012195));
#164956=CARTESIAN_POINT('Ctrl Pts',(-239.402747936727,5.86886594189645,
131.560183817473));
#164957=CARTESIAN_POINT('Ctrl Pts',(-239.398811887287,5.85766029406112,
131.642603340781));
#164958=CARTESIAN_POINT('Ctrl Pts',(-239.394875837846,5.84473557027929,
131.724684840876));
#164959=CARTESIAN_POINT('Ctrl Pts',(-239.38745257144,5.82035994459329,131.879487988383));
#164960=CARTESIAN_POINT('Ctrl Pts',(-239.380029305035,5.7897930585554,132.033556131228));
#164961=CARTESIAN_POINT('Ctrl Pts',(-239.372606038629,5.75308807999222,
132.186354867319));
#164962=CARTESIAN_POINT('Ctrl Pts',(-239.365191545909,5.71642648366544,
132.338973007995));
#164963=CARTESIAN_POINT('Ctrl Pts',(-239.357777053188,5.67364132170575,
132.49032436891));
#164964=CARTESIAN_POINT('Ctrl Pts',(-239.350362560467,5.62483733046353,
132.639881134565));
#164965=CARTESIAN_POINT('Ctrl Pts',(-239.342955214113,5.5760803783455,132.789293751778));
#164966=CARTESIAN_POINT('Ctrl Pts',(-239.335547867759,5.52131626096951,
132.936914864721));
#164967=CARTESIAN_POINT('Ctrl Pts',(-239.328140521405,5.46070040290813,
133.082228408325));
#164968=CARTESIAN_POINT('Ctrl Pts',(-239.32073869973,5.4001297544406,133.227433571607));
#164969=CARTESIAN_POINT('Ctrl Pts',(-239.313336878054,5.33371619859061,
133.370334249396));
#164970=CARTESIAN_POINT('Ctrl Pts',(-239.305935056379,5.26166444252784,
133.510431174063));
#164971=CARTESIAN_POINT('Ctrl Pts',(-239.298537142068,5.18965072202625,
133.650454142654));
#164972=CARTESIAN_POINT('Ctrl Pts',(-239.291139227756,5.11200489917788,
133.787675974645));
#164973=CARTESIAN_POINT('Ctrl Pts',(-239.283741313445,5.02897904781305,
133.921619076398));
#164974=CARTESIAN_POINT('Ctrl Pts',(-239.276344628533,4.94596699383835,
134.055539919237));
#164975=CARTESIAN_POINT('Ctrl Pts',(-239.268947943621,4.85757688227853,
134.186182796258));
#164976=CARTESIAN_POINT('Ctrl Pts',(-239.261551258708,4.76410587914538,
134.313096249498));
#164977=CARTESIAN_POINT('Ctrl Pts',(-239.254154901773,4.67063902061473,
134.440004075263));
#164978=CARTESIAN_POINT('Ctrl Pts',(-239.246758544838,4.57209193983944,
134.563182505476));
#164979=CARTESIAN_POINT('Ctrl Pts',(-239.239362187902,4.46880396696874,
134.68221075228));
#164980=CARTESIAN_POINT('Ctrl Pts',(-239.231964698566,4.36550018044543,
134.801257222613));
#164981=CARTESIAN_POINT('Ctrl Pts',(-239.224567209229,4.25745430125329,
134.916151962402));
#164982=CARTESIAN_POINT('Ctrl Pts',(-239.217169719892,4.14504450655627,
135.026508957116));
#164983=CARTESIAN_POINT('Ctrl Pts',(-239.209769637377,4.03259530678013,
135.136904637304));
#164984=CARTESIAN_POINT('Ctrl Pts',(-239.202369554862,3.91577941196701,
135.242759143993));
#164985=CARTESIAN_POINT('Ctrl Pts',(-239.194969472348,3.79501012108299,
135.343724972118));
#164986=CARTESIAN_POINT('Ctrl Pts',(-239.187561252681,3.67410803194808,
135.444801822551));
#164987=CARTESIAN_POINT('Ctrl Pts',(-239.180153033014,3.54924415173958,
135.540979019406));
#164988=CARTESIAN_POINT('Ctrl Pts',(-239.172744813348,3.42086355181755,
135.631950401542));
#164989=CARTESIAN_POINT('Ctrl Pts',(-239.165332034046,3.29240393577841,
135.722977775045));
#164990=CARTESIAN_POINT('Ctrl Pts',(-239.157919254744,3.16042359925697,
135.808792746258));
#164991=CARTESIAN_POINT('Ctrl Pts',(-239.150506475442,3.02539409909899,
135.889134074431));
#164992=CARTESIAN_POINT('Ctrl Pts',(-239.143083104413,2.89017166245913,
135.969590198061));
#164993=CARTESIAN_POINT('Ctrl Pts',(-239.135659733384,2.75189168800368,
136.04455688092));
#164994=CARTESIAN_POINT('Ctrl Pts',(-239.128236362356,2.61104841523133,
136.11381979302));
#164995=CARTESIAN_POINT('Ctrl Pts',(-239.124300312915,2.53636993251568,
136.150544650959));
#164996=CARTESIAN_POINT('Ctrl Pts',(-239.120364263474,2.46097112694201,
136.185666787633));
#164997=CARTESIAN_POINT('Ctrl Pts',(-239.116428214033,2.38492750732977,
136.219159907224));
#164998=CARTESIAN_POINT('Ctrl Pts',(-239.109004947627,2.24151161398831,
136.282326885485));
#164999=CARTESIAN_POINT('Ctrl Pts',(-239.101581681222,2.09536757343469,
136.339887693094));
#165000=CARTESIAN_POINT('Ctrl Pts',(-239.094158414816,1.94697373179301,
136.391598204264));
#165001=CARTESIAN_POINT('Ctrl Pts',(-239.086743922095,1.7987552793488,136.443247597904));
#165002=CARTESIAN_POINT('Ctrl Pts',(-239.079329429374,1.64829266779216,
136.489060336946));
#165003=CARTESIAN_POINT('Ctrl Pts',(-239.071914936653,1.49608657580917,
136.528839241876));
#165004=CARTESIAN_POINT('Ctrl Pts',(-239.0645075903,1.34402718578767,136.5685798064));
#165005=CARTESIAN_POINT('Ctrl Pts',(-239.057100243946,1.19022801949183,
136.602298020843));
#165006=CARTESIAN_POINT('Ctrl Pts',(-239.049692897592,1.03520726785652,
136.629845702525));
#165007=CARTESIAN_POINT('Ctrl Pts',(-239.042291075917,0.880302136546384,
136.657372838106));
#165008=CARTESIAN_POINT('Ctrl Pts',(-239.034889254241,0.72417759998665,
136.678738539528));
#165009=CARTESIAN_POINT('Ctrl Pts',(-239.027487432566,0.567364355398914,
136.69384516638));
#165010=CARTESIAN_POINT('Ctrl Pts',(-239.020089518254,0.410633891302364,
136.708943818562));
#165011=CARTESIAN_POINT('Ctrl Pts',(-239.012691603943,0.253215813869249,
136.717789940777));
#165012=CARTESIAN_POINT('Ctrl Pts',(-239.005293689632,0.0956481882167628,
136.720337458848));
#165013=CARTESIAN_POINT('Ctrl Pts',(-238.997897004719,-0.0618932525546835,
136.722884553569));
#165014=CARTESIAN_POINT('Ctrl Pts',(-238.990500319807,-0.219583819337571,
136.719135115535));
#165015=CARTESIAN_POINT('Ctrl Pts',(-238.983103634895,-0.376883062274058,
136.709095134873));
#165016=CARTESIAN_POINT('Ctrl Pts',(-238.97570727796,-0.534175330397275,
136.699055599393));
#165017=CARTESIAN_POINT('Ctrl Pts',(-238.968310921024,-0.691075936635662,
136.682726099669));
#165018=CARTESIAN_POINT('Ctrl Pts',(-238.960914564089,-0.847047444013144,
136.66016467765));
#165019=CARTESIAN_POINT('Ctrl Pts',(-238.953517074752,-1.00304283102658,
136.637599801419));
#165020=CARTESIAN_POINT('Ctrl Pts',(-238.946119585416,-1.15810846646915,
136.608801156552));
#165021=CARTESIAN_POINT('Ctrl Pts',(-238.938722096079,-1.31171517139054,
136.573878263925));
#165022=CARTESIAN_POINT('Ctrl Pts',(-238.931322013564,-1.46537572290444,
136.538943129132));
#165023=CARTESIAN_POINT('Ctrl Pts',(-238.923921931049,-1.61757596187038,
136.497879554932));
#165024=CARTESIAN_POINT('Ctrl Pts',(-238.916521848534,-1.76780012425026,
136.450847426477));
#165025=CARTESIAN_POINT('Ctrl Pts',(-238.909113628868,-1.91818947353988,
136.403763581361));
#165026=CARTESIAN_POINT('Ctrl Pts',(-238.901705409201,-2.06659805035564,
136.350698186771));
#165027=CARTESIAN_POINT('Ctrl Pts',(-238.894297189535,-2.21252770071824,
136.291860206273));
#165028=CARTESIAN_POINT('Ctrl Pts',(-238.886884410233,-2.35854716834568,
136.232986011979));
#165029=CARTESIAN_POINT('Ctrl Pts',(-238.879471630931,-2.50208432972178,
136.168332305074));
#165030=CARTESIAN_POINT('Ctrl Pts',(-238.872058851629,-2.64266450761232,
136.09815461268));
#165031=CARTESIAN_POINT('Ctrl Pts',(-238.8646354806,-2.7834455530538,136.027876647108));
#165032=CARTESIAN_POINT('Ctrl Pts',(-238.857212109571,-2.92126085037995,
135.952059111555));
#165033=CARTESIAN_POINT('Ctrl Pts',(-238.849788738542,-3.05566292917917,
135.871001973113));
#165034=CARTESIAN_POINT('Ctrl Pts',(-238.845852689102,-3.12692613629289,
135.828023533371));
#165035=CARTESIAN_POINT('Ctrl Pts',(-238.841916639661,-3.19723028071578,
135.783572755617));
#165036=CARTESIAN_POINT('Ctrl Pts',(-238.83798059022,-3.26651242466866,
135.737698954026));
#165037=CARTESIAN_POINT('Ctrl Pts',(-238.830575131449,-3.39686293686282,
135.651389940007));
#165038=CARTESIAN_POINT('Ctrl Pts',(-238.823169672677,-3.52399215415378,
135.559777460672));
#165039=CARTESIAN_POINT('Ctrl Pts',(-238.815764213906,-3.64743741711899,
135.463129859619));
#165040=CARTESIAN_POINT('Ctrl Pts',(-238.808367519445,-3.77073658344827,
135.36659664035));
#165041=CARTESIAN_POINT('Ctrl Pts',(-238.800970824984,-3.89036018059399,
135.265040388873));
#165042=CARTESIAN_POINT('Ctrl Pts',(-238.793574130524,-4.00587286862359,
135.158773680532));
#165043=CARTESIAN_POINT('Ctrl Pts',(-238.786184555943,-4.12127436692031,
135.052609261966));
#165044=CARTESIAN_POINT('Ctrl Pts',(-238.778794981362,-4.2325725588388,
134.941743664802));
#165045=CARTESIAN_POINT('Ctrl Pts',(-238.771405406781,-4.33936378316464,
134.826530743239));
#165046=CARTESIAN_POINT('Ctrl Pts',(-238.764021313419,-4.44607579506923,
134.711403280895));
#165047=CARTESIAN_POINT('Ctrl Pts',(-238.756637220058,-4.54828724127563,
134.591935188395));
#165048=CARTESIAN_POINT('Ctrl Pts',(-238.749253126696,-4.64563017140943,
134.468518211474));
#165049=CARTESIAN_POINT('Ctrl Pts',(-238.741508212759,-4.74772972233884,
134.339070516573));
#165050=CARTESIAN_POINT('Ctrl Pts',(-238.733763298822,-4.84447267690336,
134.205278594195));
#165051=CARTESIAN_POINT('Ctrl Pts',(-238.726018384885,-4.93548047736706,
134.067635509454));
#165052=CARTESIAN_POINT('Ctrl Pts',(-238.718639333783,-5.02218915041337,
133.936494561414));
#165053=CARTESIAN_POINT('Ctrl Pts',(-238.711260282681,-5.10369184030888,
133.801858290106));
#165054=CARTESIAN_POINT('Ctrl Pts',(-238.703881231578,-5.17970465458188,
133.664184083062));
#165055=CARTESIAN_POINT('Ctrl Pts',(-238.696502350099,-5.25571572154588,
133.52651304074));
#165056=CARTESIAN_POINT('Ctrl Pts',(-238.689123468619,-5.32623698218892,
133.385804530002));
#165057=CARTESIAN_POINT('Ctrl Pts',(-238.681744587139,-5.39103009844791,
133.242541299987));
#165058=CARTESIAN_POINT('Ctrl Pts',(-238.674364399656,-5.45583468256891,
133.099252713528));
#165059=CARTESIAN_POINT('Ctrl Pts',(-238.666984212174,-5.5149089492929,
132.953408849594));
#165060=CARTESIAN_POINT('Ctrl Pts',(-238.659604024691,-5.568062452315,132.805513057941));
#165061=CARTESIAN_POINT('Ctrl Pts',(-238.652221055053,-5.62123599294713,
132.657561513083));
#165062=CARTESIAN_POINT('Ctrl Pts',(-238.644838085415,-5.66848419968955,
132.507556853508));
#165063=CARTESIAN_POINT('Ctrl Pts',(-238.637455115776,-5.70966634504485,
132.35601805101));
#165064=CARTESIAN_POINT('Ctrl Pts',(-238.630063998789,-5.75089393624544,
132.204312020483));
#165065=CARTESIAN_POINT('Ctrl Pts',(-238.622672881802,-5.78604200163665,
132.051068828938));
#165066=CARTESIAN_POINT('Ctrl Pts',(-238.615281764816,-5.81502070102805,
131.896818767389));
#165067=CARTESIAN_POINT('Ctrl Pts',(-238.607885888735,-5.84401805961916,
131.74246938521));
#165068=CARTESIAN_POINT('Ctrl Pts',(-238.600490012655,-5.86683808367786,
131.58711221157));
#165069=CARTESIAN_POINT('Ctrl Pts',(-238.593094136575,-5.88344282135011,
131.431282566778));
#165070=CARTESIAN_POINT('Ctrl Pts',(-238.585688093829,-5.900070384558,131.275238712332));
#165071=CARTESIAN_POINT('Ctrl Pts',(-238.578282051082,-5.91046557869002,
131.118721462958));
#165072=CARTESIAN_POINT('Ctrl Pts',(-238.570876008335,-5.91464252743418,
130.962266713607));
#165073=CARTESIAN_POINT('Ctrl Pts',(-238.568375736293,-5.91605266082417,
130.909447759008));
#165074=CARTESIAN_POINT('Ctrl Pts',(-238.565875464252,-5.91675451944664,
130.856635888774));
#165075=CARTESIAN_POINT('Ctrl Pts',(-238.56337519221,-5.91674997810161,
130.803851564856));
#165076=CARTESIAN_POINT('',(-236.8133759018,-5.91514049166533,130.809755854059));
#165077=CARTESIAN_POINT('Ctrl Pts',(-238.56337519221,-5.92647874297726,
130.803850727833));
#165078=CARTESIAN_POINT('Ctrl Pts',(-238.562094450275,-5.92651203176314,
130.776767969747));
#165079=CARTESIAN_POINT('Ctrl Pts',(-238.560813708341,-5.92634251264235,
130.749685640048));
#165080=CARTESIAN_POINT('Ctrl Pts',(-238.559532966407,-5.92596892446363,
130.722606125681));
#165081=CARTESIAN_POINT('Ctrl Pts',(-238.466717091803,-5.89889484136622,
128.760143007206));
#165082=CARTESIAN_POINT('Ctrl Pts',(-238.281085342595,-3.70122233609977,
124.864788768594));
#165083=CARTESIAN_POINT('Ctrl Pts',(-238.002637718782,2.99652893391074,
124.479933775664));
#165084=CARTESIAN_POINT('Ctrl Pts',(-237.724190094969,6.94061650223621,
129.906918085011));
#165085=CARTESIAN_POINT('Ctrl Pts',(-237.445742471156,4.50661657297107,
136.158608239275));
#165086=CARTESIAN_POINT('Ctrl Pts',(-237.167294847343,-2.06874382639764,
137.490006398721));
#165087=CARTESIAN_POINT('Ctrl Pts',(-236.956506088141,-5.60724384558112,
133.846964395534));
#165088=CARTESIAN_POINT('Ctrl Pts',(-236.838533203544,-5.9191873299868,
131.344539778461));
#165089=CARTESIAN_POINT('Ctrl Pts',(-236.813376193551,-5.91447974316152,
130.80976145495));
#165090=CARTESIAN_POINT('',(-235.063374513861,-5.91162093914216,130.802545185735));
#165091=CARTESIAN_POINT('Ctrl Pts',(-236.813375192209,-5.91674755256041,
130.809742231672));
#165092=CARTESIAN_POINT('Ctrl Pts',(-236.806043481234,-5.91688936434239,
130.653829061879));
#165093=CARTESIAN_POINT('Ctrl Pts',(-236.79871177026,-5.91086422133638,
130.497776607582));
#165094=CARTESIAN_POINT('Ctrl Pts',(-236.791380059285,-5.89866598767684,
130.342115954726));
#165095=CARTESIAN_POINT('Ctrl Pts',(-236.783839206803,-5.88611979199543,
130.182014987229));
#165096=CARTESIAN_POINT('Ctrl Pts',(-236.776298354321,-5.86704303141833,
130.022328917354));
#165097=CARTESIAN_POINT('Ctrl Pts',(-236.768757501839,-5.84148658530926,
129.863634814714));
#165098=CARTESIAN_POINT('Ctrl Pts',(-236.761430869615,-5.816656145774,129.709448888259));
#165099=CARTESIAN_POINT('Ctrl Pts',(-236.754104237391,-5.78570924155664,
129.556199733322));
#165100=CARTESIAN_POINT('Ctrl Pts',(-236.746777605167,-5.74874499510395,
129.404410067094));
#165101=CARTESIAN_POINT('Ctrl Pts',(-236.739451132004,-5.71178155114529,
129.25262369622));
#165102=CARTESIAN_POINT('Ctrl Pts',(-236.732124658841,-5.66880111465606,
129.102297121385));
#165103=CARTESIAN_POINT('Ctrl Pts',(-236.724798185678,-5.61995350497976,
128.953940891027));
#165104=CARTESIAN_POINT('Ctrl Pts',(-236.71747035792,-5.57109686384674,
128.805557231018));
#165105=CARTESIAN_POINT('Ctrl Pts',(-236.710142530162,-5.51637100990835,
128.659145002411));
#165106=CARTESIAN_POINT('Ctrl Pts',(-236.702814702404,-5.45597492971321,
128.515197423549));
#165107=CARTESIAN_POINT('Ctrl Pts',(-236.695113443847,-5.39250102656027,
128.363914183805));
#165108=CARTESIAN_POINT('Ctrl Pts',(-236.68741218529,-5.32276401191484,
128.215353818769));
#165109=CARTESIAN_POINT('Ctrl Pts',(-236.679710926733,-5.24705053215068,
128.07006157109));
#165110=CARTESIAN_POINT('Ctrl Pts',(-236.67237187002,-5.17489797191598,
127.931602637689));
#165111=CARTESIAN_POINT('Ctrl Pts',(-236.665032813306,-5.09731849324256,
127.796111745667));
#165112=CARTESIAN_POINT('Ctrl Pts',(-236.657693756593,-5.01460532544673,
127.664031973538));
#165113=CARTESIAN_POINT('Ctrl Pts',(-236.650349725213,-4.93183609179975,
127.531862673163));
#165114=CARTESIAN_POINT('Ctrl Pts',(-236.643005693833,-4.84392645314405,
127.403109410562));
#165115=CARTESIAN_POINT('Ctrl Pts',(-236.635661662453,-4.75121086146454,
127.278183379763));
#165116=CARTESIAN_POINT('Ctrl Pts',(-236.6283078109,-4.65837129385027,127.153090302395));
#165117=CARTESIAN_POINT('Ctrl Pts',(-236.620953959347,-4.56071318704533,
127.031834963828));
#165118=CARTESIAN_POINT('Ctrl Pts',(-236.613600107794,-4.45860914621786,
126.914793155269));
#165119=CARTESIAN_POINT('Ctrl Pts',(-236.612533271768,-4.44379673556223,
126.897813696687));
#165120=CARTESIAN_POINT('Ctrl Pts',(-236.611466435743,-4.42889081546524,
126.880922847802));
#165121=CARTESIAN_POINT('Ctrl Pts',(-236.610399599717,-4.41389258223086,
126.864121686355));
#165122=CARTESIAN_POINT('Ctrl Pts',(-236.602976333312,-4.30953176365291,
126.74721571922));
#165123=CARTESIAN_POINT('Ctrl Pts',(-236.595553066906,-4.20036538985445,
126.63428197761));
#165124=CARTESIAN_POINT('Ctrl Pts',(-236.588129800501,-4.08672768992291,
126.525740822478));
#165125=CARTESIAN_POINT('Ctrl Pts',(-236.58071530778,-3.97322430031599,
126.417327953978));
#165126=CARTESIAN_POINT('Ctrl Pts',(-236.573300815059,-3.8552603711819,
126.313297593224));
#165127=CARTESIAN_POINT('Ctrl Pts',(-236.565886322338,-3.73320990655597,
126.214036625069));
#165128=CARTESIAN_POINT('Ctrl Pts',(-236.558478975984,-3.61127707876331,
126.114871328372));
#165129=CARTESIAN_POINT('Ctrl Pts',(-236.55107162963,-3.4852658444353,126.020466506665));
#165130=CARTESIAN_POINT('Ctrl Pts',(-236.543664283276,-3.35558644486496,
125.931171705412));
#165131=CARTESIAN_POINT('Ctrl Pts',(-236.536262461601,-3.22600376508298,
125.841943503591));
#165132=CARTESIAN_POINT('Ctrl Pts',(-236.528860639926,-3.09275867365177,
125.757817944319));
#165133=CARTESIAN_POINT('Ctrl Pts',(-236.52145881825,-2.95629373319983,
125.679103753218));
#165134=CARTESIAN_POINT('Ctrl Pts',(-236.514060903939,-2.81990083152731,
125.600431114726));
#165135=CARTESIAN_POINT('Ctrl Pts',(-236.506662989627,-2.68029178847692,
125.527164341358));
#165136=CARTESIAN_POINT('Ctrl Pts',(-236.499265075316,-2.53793723552307,
125.459568278191));
#165137=CARTESIAN_POINT('Ctrl Pts',(-236.491868390404,-2.39560633931356,
125.391983448263));
#165138=CARTESIAN_POINT('Ctrl Pts',(-236.484471705492,-2.25053117561159,
125.330067618179));
#165139=CARTESIAN_POINT('Ctrl Pts',(-236.477075020579,-2.10320611566655,
125.274039234724));
#165140=CARTESIAN_POINT('Ctrl Pts',(-236.469678663644,-1.95588758826947,
125.218013335626));
#165141=CARTESIAN_POINT('Ctrl Pts',(-236.462282306708,-1.80631971190855,
125.167874496786));
#165142=CARTESIAN_POINT('Ctrl Pts',(-236.454885949773,-1.65501567980099,
125.123792541914));
#165143=CARTESIAN_POINT('Ctrl Pts',(-236.447488460436,-1.50368848265942,
125.079703837983));
#165144=CARTESIAN_POINT('Ctrl Pts',(-236.4400909711,-1.35062495892817,125.041673968871));
#165145=CARTESIAN_POINT('Ctrl Pts',(-236.432693481763,-1.19635211259129,
125.009822483668));
#165146=CARTESIAN_POINT('Ctrl Pts',(-236.425293399248,-1.04202518614662,
124.977959832976));
#165147=CARTESIAN_POINT('Ctrl Pts',(-236.417893316733,-0.886488458421695,
124.952279953763));
#165148=CARTESIAN_POINT('Ctrl Pts',(-236.410493234218,-0.730277588853789,
124.932850998591));
#165149=CARTESIAN_POINT('Ctrl Pts',(-236.403085014552,-0.573894949376595,
124.913400679285));
#165150=CARTESIAN_POINT('Ctrl Pts',(-236.395676794885,-0.416837058326022,
124.90021505702));
#165151=CARTESIAN_POINT('Ctrl Pts',(-236.388268575219,-0.259643879677973,
124.893310320178));
#165152=CARTESIAN_POINT('Ctrl Pts',(-236.380855795916,-0.102353951251823,
124.886401333586));
#165153=CARTESIAN_POINT('Ctrl Pts',(-236.373443016614,0.0550710582627565,
124.885780936936));
#165154=CARTESIAN_POINT('Ctrl Pts',(-236.366030237312,0.212093261767607,
124.891413212861));
#165155=CARTESIAN_POINT('Ctrl Pts',(-236.358606866284,0.369339825961107,
124.897053536445));
#165156=CARTESIAN_POINT('Ctrl Pts',(-236.351183495255,0.526182063406159,
124.908964347838));
#165157=CARTESIAN_POINT('Ctrl Pts',(-236.343760124226,0.682088438571443,
124.927058011398));
#165158=CARTESIAN_POINT('Ctrl Pts',(-236.339824074786,0.7647537395973,124.936651705968));
#165159=CARTESIAN_POINT('Ctrl Pts',(-236.335888025345,0.847156114368657,
124.947982769311));
#165160=CARTESIAN_POINT('Ctrl Pts',(-236.331951975905,0.929217850178815,
124.961032392196));
#165161=CARTESIAN_POINT('Ctrl Pts',(-236.324528709499,1.08398372287413,
124.985643573694));
#165162=CARTESIAN_POINT('Ctrl Pts',(-236.317105443094,1.23800516971489,
125.016444889822));
#165163=CARTESIAN_POINT('Ctrl Pts',(-236.309682176688,1.39074787014024,
125.053382359548));
#165164=CARTESIAN_POINT('Ctrl Pts',(-236.302267683967,1.54331004137817,
125.090276172251));
#165165=CARTESIAN_POINT('Ctrl Pts',(-236.294853191246,1.69459611529923,
125.133291615673));
#165166=CARTESIAN_POINT('Ctrl Pts',(-236.287438698525,1.84407843640344,
125.18232315034));
#165167=CARTESIAN_POINT('Ctrl Pts',(-236.280031352172,1.99341668081866,
125.231307426568));
#165168=CARTESIAN_POINT('Ctrl Pts',(-236.272624005818,2.14095428115501,
125.286296134733));
#165169=CARTESIAN_POINT('Ctrl Pts',(-236.265216659464,2.2861754094724,125.347133065079));
#165170=CARTESIAN_POINT('Ctrl Pts',(-236.257814837788,2.431288226393,125.407924620947));
#165171=CARTESIAN_POINT('Ctrl Pts',(-236.250413016113,2.57408766857886,
125.474555570397));
#165172=CARTESIAN_POINT('Ctrl Pts',(-236.243011194438,2.71407478050877,
125.546820446697));
#165173=CARTESIAN_POINT('Ctrl Pts',(-236.235613280126,2.85398799433195,
125.61904717493));
#165174=CARTESIAN_POINT('Ctrl Pts',(-236.228215365815,2.99109150369809,
125.696901736135));
#165175=CARTESIAN_POINT('Ctrl Pts',(-236.220817451504,3.12490809913466,
125.780131329958));
#165176=CARTESIAN_POINT('Ctrl Pts',(-236.213420766591,3.25870245668095,
125.863347092532));
#165177=CARTESIAN_POINT('Ctrl Pts',(-236.206024081679,3.38921066771668,
125.951935917957));
#165178=CARTESIAN_POINT('Ctrl Pts',(-236.198627396767,3.51598172703827,
126.045599953524));
#165179=CARTESIAN_POINT('Ctrl Pts',(-236.191231039831,3.64274716519825,
126.13925983593));
#165180=CARTESIAN_POINT('Ctrl Pts',(-236.183834682896,3.7657754808919,126.237994259192));
#165181=CARTESIAN_POINT('Ctrl Pts',(-236.17643832596,3.88464640315174,126.341463253187));
#165182=CARTESIAN_POINT('Ctrl Pts',(-236.169040836624,4.00353552485323,
126.444948088549));
#165183=CARTESIAN_POINT('Ctrl Pts',(-236.161643347287,4.1182657041598,126.553168692862));
#165184=CARTESIAN_POINT('Ctrl Pts',(-236.154245857951,4.22845150251073,
126.665746301951));
#165185=CARTESIAN_POINT('Ctrl Pts',(-236.146845775435,4.33867592632261,
126.778363374946));
#165186=CARTESIAN_POINT('Ctrl Pts',(-236.139445692921,4.444352536527,126.895340227029));
#165187=CARTESIAN_POINT('Ctrl Pts',(-236.132045610406,4.54513445743372,
127.016263030868));
#165188=CARTESIAN_POINT('Ctrl Pts',(-236.124637390739,4.64602719842297,
127.137318801761));
#165189=CARTESIAN_POINT('Ctrl Pts',(-236.117229171072,4.74201426233549,
127.262328902701));
#165190=CARTESIAN_POINT('Ctrl Pts',(-236.109820951406,4.83279016570902,
127.390847796918));
#165191=CARTESIAN_POINT('Ctrl Pts',(-236.102408172104,4.92362194013614,
127.51944579237));
#165192=CARTESIAN_POINT('Ctrl Pts',(-236.094995392802,5.0092359603708,127.651556571839));
#165193=CARTESIAN_POINT('Ctrl Pts',(-236.0875826135,5.089371703596,127.78670818146));
#165194=CARTESIAN_POINT('Ctrl Pts',(-236.080159242471,5.16962194852946,
127.92205290204));
#165195=CARTESIAN_POINT('Ctrl Pts',(-236.072735871442,5.24437810599711,
128.0604468029));
#165196=CARTESIAN_POINT('Ctrl Pts',(-236.065312500413,5.31342659840628,
128.20139531894));
#165197=CARTESIAN_POINT('Ctrl Pts',(-236.061376450973,5.35003776587558,
128.276129604155));
#165198=CARTESIAN_POINT('Ctrl Pts',(-236.057440401532,5.38504511772872,
128.351581772324));
#165199=CARTESIAN_POINT('Ctrl Pts',(-236.053504352092,5.41842247308797,
128.427676274698));
#165200=CARTESIAN_POINT('Ctrl Pts',(-236.046081085686,5.48137112362688,
128.571188131354));
#165201=CARTESIAN_POINT('Ctrl Pts',(-236.038657819281,5.53870945822938,
128.717419600426));
#165202=CARTESIAN_POINT('Ctrl Pts',(-236.031234552875,5.59019407935361,
128.865891964825));
#165203=CARTESIAN_POINT('Ctrl Pts',(-236.023820060154,5.6416178499312,129.014188847219));
#165204=CARTESIAN_POINT('Ctrl Pts',(-236.016405567433,5.68720155744135,
129.164721003733));
#165205=CARTESIAN_POINT('Ctrl Pts',(-236.008991074712,5.72674878454648,
129.316987456185));
#165206=CARTESIAN_POINT('Ctrl Pts',(-236.001583728359,5.76625789454532,
129.469107148499));
#165207=CARTESIAN_POINT('Ctrl Pts',(-235.994176382005,5.7997420137932,129.62295745008));
#165208=CARTESIAN_POINT('Ctrl Pts',(-235.986769035651,5.82705374838034,
129.778019945086));
#165209=CARTESIAN_POINT('Ctrl Pts',(-235.979367213976,5.85434511284541,
129.932966788633));
#165210=CARTESIAN_POINT('Ctrl Pts',(-235.9719653923,5.8754731945584,130.089123659364));
#165211=CARTESIAN_POINT('Ctrl Pts',(-235.964563570625,5.890341160854,130.245959712079));
#165212=CARTESIAN_POINT('Ctrl Pts',(-235.957165656314,5.90520127846592,
130.402712972262));
#165213=CARTESIAN_POINT('Ctrl Pts',(-235.949767742002,5.91380782692023,
130.5601443297));
#165214=CARTESIAN_POINT('Ctrl Pts',(-235.942369827691,5.91611555093859,
130.717715649781));
#165215=CARTESIAN_POINT('Ctrl Pts',(-235.934973142779,5.91842289145508,
130.875260784366));
#165216=CARTESIAN_POINT('Ctrl Pts',(-235.927576457866,5.91443347956411,
131.032945462539));
#165217=CARTESIAN_POINT('Ctrl Pts',(-235.920179772954,5.90415412785713,
131.190229244183));
#165218=CARTESIAN_POINT('Ctrl Pts',(-235.912783416019,5.89387523194739,
131.3475060517));
#165219=CARTESIAN_POINT('Ctrl Pts',(-235.905387059083,5.87730697511917,
131.504381625531));
#165220=CARTESIAN_POINT('Ctrl Pts',(-235.897990702148,5.85450821714245,
131.660318617652));
#165221=CARTESIAN_POINT('Ctrl Pts',(-235.890593212811,5.83170596861762,
131.816279484125));
#165222=CARTESIAN_POINT('Ctrl Pts',(-235.883195723475,5.80267137359861,
131.971301113369));
#165223=CARTESIAN_POINT('Ctrl Pts',(-235.875798234138,5.76751475815558,
132.124854493719));
#165224=CARTESIAN_POINT('Ctrl Pts',(-235.868398151623,5.73234581861565,
132.278461701968));
#165225=CARTESIAN_POINT('Ctrl Pts',(-235.860998069108,5.69105066911282,
132.430599272918));
#165226=CARTESIAN_POINT('Ctrl Pts',(-235.853597986593,5.64378997951745,
132.580751686447));
#165227=CARTESIAN_POINT('Ctrl Pts',(-235.846189766927,5.59647732193529,
132.73106920799));
#165228=CARTESIAN_POINT('Ctrl Pts',(-235.83878154726,5.54318613620419,132.879396856454));
#165229=CARTESIAN_POINT('Ctrl Pts',(-235.831373327594,5.48412614375368,
133.025236796442));
#165230=CARTESIAN_POINT('Ctrl Pts',(-235.823960548292,5.42502980086329,
133.171166498479));
#165231=CARTESIAN_POINT('Ctrl Pts',(-235.81654776899,5.36015772970096,133.314605101705));
#165232=CARTESIAN_POINT('Ctrl Pts',(-235.809134989688,5.28976617947242,
133.455078318305));
#165233=CARTESIAN_POINT('Ctrl Pts',(-235.801711618659,5.21927405049578,
133.595752249624));
#165234=CARTESIAN_POINT('Ctrl Pts',(-235.794288247631,5.143246871316,133.733452005979));
#165235=CARTESIAN_POINT('Ctrl Pts',(-235.786864876602,5.06198528965285,
133.867730573976));
#165236=CARTESIAN_POINT('Ctrl Pts',(-235.782928827161,5.01889844920773,
133.938928292703));
#165237=CARTESIAN_POINT('Ctrl Pts',(-235.77899277772,4.974340731985,134.009164709201));
#165238=CARTESIAN_POINT('Ctrl Pts',(-235.775056728279,4.92836154788358,
134.078376960812));
#165239=CARTESIAN_POINT('Ctrl Pts',(-235.767633461873,4.84164624163427,
134.208909107304));
#165240=CARTESIAN_POINT('Ctrl Pts',(-235.760210195468,4.74961033563306,
134.336191153046));
#165241=CARTESIAN_POINT('Ctrl Pts',(-235.752786929062,4.65252502580741,
134.459759562515));
#165242=CARTESIAN_POINT('Ctrl Pts',(-235.745372436341,4.55555446275527,
134.583181924386));
#165243=CARTESIAN_POINT('Ctrl Pts',(-235.73795794362,4.45354660354109,134.70289909606));
#165244=CARTESIAN_POINT('Ctrl Pts',(-235.730543450899,4.34681676692741,
134.818475035125));
#165245=CARTESIAN_POINT('Ctrl Pts',(-235.723136104546,4.24018980054857,
134.933939577749));
#165246=CARTESIAN_POINT('Ctrl Pts',(-235.715728758192,4.12885016890964,
135.045270561599));
#165247=CARTESIAN_POINT('Ctrl Pts',(-235.708321411838,4.0131543599336,135.152063763578));
#165248=CARTESIAN_POINT('Ctrl Pts',(-235.700919590163,3.89754484125719,
135.258777315158));
#165249=CARTESIAN_POINT('Ctrl Pts',(-235.693517768487,3.77758588756741,
135.360959571655));
#165250=CARTESIAN_POINT('Ctrl Pts',(-235.686115946812,3.65367177354376,
135.458242130208));
#165251=CARTESIAN_POINT('Ctrl Pts',(-235.6787180325,3.52982307281566,135.555473334056));
#165252=CARTESIAN_POINT('Ctrl Pts',(-235.671320118189,3.40202366278135,
135.647809761191));
#165253=CARTESIAN_POINT('Ctrl Pts',(-235.663922203878,3.27070182974663,
135.734922462163));
#165254=CARTESIAN_POINT('Ctrl Pts',(-235.656525518966,3.13940182001869,
135.822020686584));
#165255=CARTESIAN_POINT('Ctrl Pts',(-235.649128834053,3.00458085983532,
135.903896701589));
#165256=CARTESIAN_POINT('Ctrl Pts',(-235.641732149141,2.86669731914428,
135.98026411772));
#165257=CARTESIAN_POINT('Ctrl Pts',(-235.634335792206,2.72881989235394,
136.056628147641));
#165258=CARTESIAN_POINT('Ctrl Pts',(-235.62693943527,2.58788048162462,136.127483883488));
#165259=CARTESIAN_POINT('Ctrl Pts',(-235.619543078335,2.44436298821062,
136.192590395922));
#165260=CARTESIAN_POINT('Ctrl Pts',(-235.612145588998,2.300823521902,136.25770687633));
#165261=CARTESIAN_POINT('Ctrl Pts',(-235.604748099661,2.15470552696101,
136.317072226458));
#165262=CARTESIAN_POINT('Ctrl Pts',(-235.597350610325,2.00651370981995,
136.370493323027));
#165263=CARTESIAN_POINT('Ctrl Pts',(-235.58995052781,1.85826994426732,136.423933146279));
#165264=CARTESIAN_POINT('Ctrl Pts',(-235.582550445295,1.70795126007021,
136.471424440728));
#165265=CARTESIAN_POINT('Ctrl Pts',(-235.57515036278,1.55607822489781,136.512823731268));
#165266=CARTESIAN_POINT('Ctrl Pts',(-235.567742143113,1.40403818971008,
136.554268544584));
#165267=CARTESIAN_POINT('Ctrl Pts',(-235.560333923447,1.25044075060268,
136.589607877842));
#165268=CARTESIAN_POINT('Ctrl Pts',(-235.552925703781,1.09581811014864,
136.61874908343));
#165269=CARTESIAN_POINT('Ctrl Pts',(-235.545512924479,0.941100302038981,
136.647908224943));
#165270=CARTESIAN_POINT('Ctrl Pts',(-235.538100145176,0.785356403699778,
136.670861582928));
#165271=CARTESIAN_POINT('Ctrl Pts',(-235.530687365874,0.629123955857885,
136.687568382949));
#165272=CARTESIAN_POINT('Ctrl Pts',(-235.523263994846,0.472668275768163,
136.70429905443));
#165273=CARTESIAN_POINT('Ctrl Pts',(-235.515840623817,0.315723023472359,
136.714765317198));
#165274=CARTESIAN_POINT('Ctrl Pts',(-235.508417252788,0.158826791435676,
136.718978493035));
#165275=CARTESIAN_POINT('Ctrl Pts',(-235.504481203347,0.0756366445359733,
136.721212419958));
#165276=CARTESIAN_POINT('Ctrl Pts',(-235.500545153907,-0.00753977640015259,
136.721689249256));
#165277=CARTESIAN_POINT('Ctrl Pts',(-235.496609104466,-0.0906228759804562,
136.720416572072));
#165278=CARTESIAN_POINT('Ctrl Pts',(-235.48918583806,-0.247315008852205,
136.718016342623));
#165279=CARTESIAN_POINT('Ctrl Pts',(-235.481762571655,-0.404148654045105,
136.709382983073));
#165280=CARTESIAN_POINT('Ctrl Pts',(-235.474339305249,-0.560587237971028,
136.694494105962));
#165281=CARTESIAN_POINT('Ctrl Pts',(-235.466924812529,-0.716840924482166,
136.679622826267));
#165282=CARTESIAN_POINT('Ctrl Pts',(-235.459510319808,-0.872700111162586,
136.658510780843));
#165283=CARTESIAN_POINT('Ctrl Pts',(-235.452095827087,-1.02762750568826,
136.631187564718));
#165284=CARTESIAN_POINT('Ctrl Pts',(-235.444688480733,-1.18240557535861,
136.603890683737));
#165285=CARTESIAN_POINT('Ctrl Pts',(-235.437281134379,-1.33625327565069,
136.570394614519));
#165286=CARTESIAN_POINT('Ctrl Pts',(-235.429873788025,-1.48863783179452,
136.530780787991));
#165287=CARTESIAN_POINT('Ctrl Pts',(-235.42247196635,-1.64090873378724,
136.491196506949));
#165288=CARTESIAN_POINT('Ctrl Pts',(-235.415070144675,-1.79171830475907,
136.445503647373));
#165289=CARTESIAN_POINT('Ctrl Pts',(-235.407668322999,-1.9405434818548,
136.393834792972));
#165290=CARTESIAN_POINT('Ctrl Pts',(-235.400270408688,-2.08929009529841,
136.342193214157));
#165291=CARTESIAN_POINT('Ctrl Pts',(-235.392872494377,-2.23605404934729,
136.284582045337));
#165292=CARTESIAN_POINT('Ctrl Pts',(-235.385474580065,-2.38032709030358,
136.221183810699));
#165293=CARTESIAN_POINT('Ctrl Pts',(-235.378077895153,-2.52457615569723,
136.157796111698));
#165294=CARTESIAN_POINT('Ctrl Pts',(-235.370681210241,-2.66633478813374,
136.088623405612));
#165295=CARTESIAN_POINT('Ctrl Pts',(-235.363284525329,-2.80511427989841,
136.013896531562));
#165296=CARTESIAN_POINT('Ctrl Pts',(-235.355888168393,-2.94388761803537,
135.939172970979));
#165297=CARTESIAN_POINT('Ctrl Pts',(-235.348491811458,-3.07968174947808,
135.858895909095));
#165298=CARTESIAN_POINT('Ctrl Pts',(-235.341095454522,-3.21203241310078,
135.773342237545));
#165299=CARTESIAN_POINT('Ctrl Pts',(-235.333697965186,-3.34440333994796,
135.68777546751));
#165300=CARTESIAN_POINT('Ctrl Pts',(-235.326300475849,-3.47332943572068,
135.596930681914));
#165301=CARTESIAN_POINT('Ctrl Pts',(-235.318902986513,-3.59837541417954,
135.501128116722));
#165302=CARTESIAN_POINT('Ctrl Pts',(-235.311502903998,-3.72346522731249,
135.405291968089));
#165303=CARTESIAN_POINT('Ctrl Pts',(-235.304102821483,-3.84467191890259,
135.304494806518));
#165304=CARTESIAN_POINT('Ctrl Pts',(-235.296702738968,-3.96159339973869,
135.199097048531));
#165305=CARTESIAN_POINT('Ctrl Pts',(-235.289294519302,-4.07864344776264,
135.093583394873));
#165306=CARTESIAN_POINT('Ctrl Pts',(-235.281886299635,-4.19139859735822,
134.983459292085));
#165307=CARTESIAN_POINT('Ctrl Pts',(-235.274478079969,-4.29949323297398,
134.869122418965));
#165308=CARTESIAN_POINT('Ctrl Pts',(-235.267065300667,-4.40765439903461,
134.754715173407));
#165309=CARTESIAN_POINT('Ctrl Pts',(-235.259652521364,-4.51114909048871,
134.636090271496));
#165310=CARTESIAN_POINT('Ctrl Pts',(-235.252239742062,-4.60965244875596,
134.513677921893));
#165311=CARTESIAN_POINT('Ctrl Pts',(-235.244816371034,-4.70829655324043,
134.391090663784));
#165312=CARTESIAN_POINT('Ctrl Pts',(-235.237393000005,-4.80193485899353,
134.264705448787));
#165313=CARTESIAN_POINT('Ctrl Pts',(-235.229969628976,-4.89028576896841,
134.134981529697));
#165314=CARTESIAN_POINT('Ctrl Pts',(-235.226033579535,-4.93713154139312,
134.066198795105));
#165315=CARTESIAN_POINT('Ctrl Pts',(-235.222097530094,-4.98249159860291,
133.996477854369));
#165316=CARTESIAN_POINT('Ctrl Pts',(-235.218161480653,-5.0263293039892,
133.925889776546));
#165317=CARTESIAN_POINT('Ctrl Pts',(-235.210525599101,-5.11137384696384,
133.788949880512));
#165318=CARTESIAN_POINT('Ctrl Pts',(-235.202889717548,-5.19093130654541,
133.648350491407));
#165319=CARTESIAN_POINT('Ctrl Pts',(-235.195253835996,-5.2646814211652,
133.504556924529));
#165320=CARTESIAN_POINT('Ctrl Pts',(-235.187628600606,-5.33832871128587,
133.360963838716));
#165321=CARTESIAN_POINT('Ctrl Pts',(-235.180003365216,-5.40618462981095,
133.214185750204));
#165322=CARTESIAN_POINT('Ctrl Pts',(-235.172378129827,-5.46797246205113,
133.064716279127));
#165323=CARTESIAN_POINT('Ctrl Pts',(-235.164762379847,-5.52968343332797,
132.915432740573));
#165324=CARTESIAN_POINT('Ctrl Pts',(-235.157146629867,-5.58534122619445,
132.763464805689));
#165325=CARTESIAN_POINT('Ctrl Pts',(-235.149530879888,-5.63471520293158,
132.609330186382));
#165326=CARTESIAN_POINT('Ctrl Pts',(-235.141926012989,-5.68401862312512,
132.455415828976));
#165327=CARTESIAN_POINT('Ctrl Pts',(-235.134321146091,-5.72705602833567,
132.299341287442));
#165328=CARTESIAN_POINT('Ctrl Pts',(-235.126716279192,-5.76364514583061,
132.141643383268));
#165329=CARTESIAN_POINT('Ctrl Pts',(-235.119117783915,-5.800203607694,131.984077603866));
#165330=CARTESIAN_POINT('Ctrl Pts',(-235.111519288638,-5.83032446630871,
131.824891505164));
#165331=CARTESIAN_POINT('Ctrl Pts',(-235.103920793361,-5.85387520708344,
131.664637097771));
#165332=CARTESIAN_POINT('Ctrl Pts',(-235.096328880991,-5.87740554482536,
131.504521525753));
#165333=CARTESIAN_POINT('Ctrl Pts',(-235.088736968622,-5.8943770629967,
131.343339830038));
#165334=CARTESIAN_POINT('Ctrl Pts',(-235.081145056252,-5.90470830302427,
131.181654162033));
#165335=CARTESIAN_POINT('Ctrl Pts',(-235.075221768238,-5.91276884261537,
131.055505343034));
#165336=CARTESIAN_POINT('Ctrl Pts',(-235.069298480223,-5.91678826105314,
130.929050024163));
#165337=CARTESIAN_POINT('Ctrl Pts',(-235.063375192209,-5.91674972543052,
130.802558086599));
#165338=CARTESIAN_POINT('',(-233.313375192209,-5.92110108695772,130.799604953112));
#165339=CARTESIAN_POINT('Ctrl Pts',(-235.063373960744,-5.9074389915308,
130.802534666533));
#165340=CARTESIAN_POINT('Ctrl Pts',(-235.02215392611,-5.90982138573415,
129.923664387846));
#165341=CARTESIAN_POINT('Ctrl Pts',(-234.88811801687,-5.31313791815044,
127.068909389366));
#165342=CARTESIAN_POINT('Ctrl Pts',(-234.661266233027,-0.886879056514751,
123.862386397694));
#165343=CARTESIAN_POINT('Ctrl Pts',(-234.382818609214,5.36109972483852,
126.305897516605));
#165344=CARTESIAN_POINT('Ctrl Pts',(-234.104370985401,6.68248976334735,
132.88327646317));
#165345=CARTESIAN_POINT('Ctrl Pts',(-233.825923361589,1.86299816711319,
137.550233308306));
#165346=CARTESIAN_POINT('Ctrl Pts',(-233.562258097191,-4.32175058245946,
136.099403303978));
#165347=CARTESIAN_POINT('Ctrl Pts',(-233.391408707398,-5.90662829739712,
132.453658602887));
#165348=CARTESIAN_POINT('Ctrl Pts',(-233.313375192209,-5.92110108695772,
130.799604953112));
#165349=CARTESIAN_POINT('',(-231.563375192209,-5.92030054368718,130.808418273216));
#165350=CARTESIAN_POINT('Ctrl Pts',(-233.313375192209,-5.92110108695772,
130.799604953112));
#165351=CARTESIAN_POINT('Ctrl Pts',(-233.298592832794,-5.92384275477205,
130.486267594354));
#165352=CARTESIAN_POINT('Ctrl Pts',(-233.283810473378,-5.90112681262327,
130.173328526099));
#165353=CARTESIAN_POINT('Ctrl Pts',(-233.176212239358,-5.54038544735297,
127.926876459006));
#165354=CARTESIAN_POINT('Ctrl Pts',(-232.99058049015,-2.80141177327697,
124.391120203632));
#165355=CARTESIAN_POINT('Ctrl Pts',(-232.712132866337,3.88140930090627,
124.980940456769));
#165356=CARTESIAN_POINT('Ctrl Pts',(-232.433685242524,6.99740484494153,
130.922199347785));
#165357=CARTESIAN_POINT('Ctrl Pts',(-232.155237618711,3.68312717870603,
136.755170202472));
#165358=CARTESIAN_POINT('Ctrl Pts',(-231.876789994898,-3.0157644339933,
137.119637761841));
#165359=CARTESIAN_POINT('Ctrl Pts',(-231.679502519397,-5.7985380671585,
133.265988781829));
#165360=CARTESIAN_POINT('Ctrl Pts',(-231.575030918501,-5.92484103517307,
131.055287059807));
#165361=CARTESIAN_POINT('Ctrl Pts',(-231.563375192209,-5.92290613080011,
130.808420059033));
#165362=CARTESIAN_POINT('',(-229.813375218367,-5.91200928751026,130.807165211494));
#165363=CARTESIAN_POINT('Ctrl Pts',(-231.563375192209,-5.91674861031638,
130.808415838792));
#165364=CARTESIAN_POINT('Ctrl Pts',(-231.556062235289,-5.91685465621581,
130.653690142413));
#165365=CARTESIAN_POINT('Ctrl Pts',(-231.548749278369,-5.91088733319179,
130.498726433687));
#165366=CARTESIAN_POINT('Ctrl Pts',(-231.541436321449,-5.89881716077939,
130.344049129338));
#165367=CARTESIAN_POINT('Ctrl Pts',(-231.534130820366,-5.88675929436655,
130.18952952438));
#165368=CARTESIAN_POINT('Ctrl Pts',(-231.526825319284,-5.86861098829339,
130.035296123186));
#165369=CARTESIAN_POINT('Ctrl Pts',(-231.519519818201,-5.84439477175359,
129.881874674909));
#165370=CARTESIAN_POINT('Ctrl Pts',(-231.512220066293,-5.82019761253225,
129.728573963966));
#165371=CARTESIAN_POINT('Ctrl Pts',(-231.504920314386,-5.78994210555702,
129.576084312388));
#165372=CARTESIAN_POINT('Ctrl Pts',(-231.497620562478,-5.75370268483897,
129.42492740897));
#165373=CARTESIAN_POINT('Ctrl Pts',(-231.490215320178,-5.71693955992359,
129.271586102403));
#165374=CARTESIAN_POINT('Ctrl Pts',(-231.482810077877,-5.67401825168733,
129.119616764242));
#165375=CARTESIAN_POINT('Ctrl Pts',(-231.475404835577,-5.62507056860757,
128.969554998247));
#165376=CARTESIAN_POINT('Ctrl Pts',(-231.468110520265,-5.5768560984118,
128.821741085741));
#165377=CARTESIAN_POINT('Ctrl Pts',(-231.460816204953,-5.52279467668824,
128.675778367587));
#165378=CARTESIAN_POINT('Ctrl Pts',(-231.453521889641,-5.46306277529751,
128.5321643946));
#165379=CARTESIAN_POINT('Ctrl Pts',(-231.446227859779,-5.40333321140892,
128.388556041692));
#165380=CARTESIAN_POINT('Ctrl Pts',(-231.438933829917,-5.33793375682769,
128.247296606419));
#165381=CARTESIAN_POINT('Ctrl Pts',(-231.431639800056,-5.26708912099379,
128.108863862975));
#165382=CARTESIAN_POINT('Ctrl Pts',(-231.424344521228,-5.19623235434514,
127.970407415522));
#165383=CARTESIAN_POINT('Ctrl Pts',(-231.4170492424,-5.11992872676776,127.834778965286));
#165384=CARTESIAN_POINT('Ctrl Pts',(-231.409753963573,-5.03844886050293,
127.702431597972));
#165385=CARTESIAN_POINT('Ctrl Pts',(-231.402265695548,-4.95481352707123,
127.566583115378));
#165386=CARTESIAN_POINT('Ctrl Pts',(-231.394777427523,-4.86572451460428,
127.434192088729));
#165387=CARTESIAN_POINT('Ctrl Pts',(-231.387289159498,-4.77152126524011,
127.305715825956));
#165388=CARTESIAN_POINT('Ctrl Pts',(-231.379983067157,-4.67960980635917,
127.180365152569));
#165389=CARTESIAN_POINT('Ctrl Pts',(-231.372676974816,-4.58283036123037,
127.058741230468));
#165390=CARTESIAN_POINT('Ctrl Pts',(-231.365370882475,-4.4815379056025,
126.941233831768));
#165391=CARTESIAN_POINT('Ctrl Pts',(-231.357791526608,-4.37645689484776,
126.819331404287));
#165392=CARTESIAN_POINT('Ctrl Pts',(-231.350212170741,-4.26651906354,126.701859738012));
#165393=CARTESIAN_POINT('Ctrl Pts',(-231.342632814874,-4.15216048765967,
126.589210104569));
#165394=CARTESIAN_POINT('Ctrl Pts',(-231.335053459007,-4.03780191177965,
126.476560471127));
#165395=CARTESIAN_POINT('Ctrl Pts',(-231.32747410314,-3.91902297669403,
126.368733121126));
#165396=CARTESIAN_POINT('Ctrl Pts',(-231.319894747273,-3.79629476082943,
126.266070559472));
#165397=CARTESIAN_POINT('Ctrl Pts',(-231.312471480867,-3.67609401319123,
126.165522233414));
#165398=CARTESIAN_POINT('Ctrl Pts',(-231.305048214462,-3.55171407794731,
126.069600604618));
#165399=CARTESIAN_POINT('Ctrl Pts',(-231.297624948057,-3.4235465731537,
125.978673161467));
#165400=CARTESIAN_POINT('Ctrl Pts',(-231.290210455336,-3.29553055170711,
125.887853187004));
#165401=CARTESIAN_POINT('Ctrl Pts',(-231.282795962614,-3.16373617288102,
125.802015862692));
#165402=CARTESIAN_POINT('Ctrl Pts',(-231.275381469893,-3.02858955858279,
125.721489790155));
#165403=CARTESIAN_POINT('Ctrl Pts',(-231.26797412354,-2.89357320367921,
125.641041331679));
#165404=CARTESIAN_POINT('Ctrl Pts',(-231.260566777186,-2.75521136414399,
125.565894123486));
#165405=CARTESIAN_POINT('Ctrl Pts',(-231.253159430832,-2.61396060553718,
125.496334570607));
#165406=CARTESIAN_POINT('Ctrl Pts',(-231.245757609157,-2.47281519707522,
125.426826897866));
#165407=CARTESIAN_POINT('Ctrl Pts',(-231.238355787481,-2.32878549322126,
125.362898746624));
#165408=CARTESIAN_POINT('Ctrl Pts',(-231.230953965806,-2.1823541242278,
125.30479144908));
#165409=CARTESIAN_POINT('Ctrl Pts',(-231.223556051494,-2.03600005521464,
125.246714825925));
#165410=CARTESIAN_POINT('Ctrl Pts',(-231.216158137183,-1.88724719208587,
125.194453074213));
#165411=CARTESIAN_POINT('Ctrl Pts',(-231.208760222872,-1.73659957864125,
125.148200041171));
#165412=CARTESIAN_POINT('Ctrl Pts',(-231.201363537959,-1.58597700009675,
125.101954694544));
#165413=CARTESIAN_POINT('Ctrl Pts',(-231.193966853047,-1.43346065267384,
125.061716194238));
#165414=CARTESIAN_POINT('Ctrl Pts',(-231.186570168135,-1.27957134548418,
125.027629038696));
#165415=CARTESIAN_POINT('Ctrl Pts',(-231.179173811199,-1.12568886190766,
124.993543394614));
#165416=CARTESIAN_POINT('Ctrl Pts',(-231.171777454264,-0.970433904074944,
124.965608633691));
#165417=CARTESIAN_POINT('Ctrl Pts',(-231.164381097328,-0.814338858108183,
124.943918416957));
#165418=CARTESIAN_POINT('Ctrl Pts',(-231.156983607992,-0.658219913591393,
124.922224879396));
#165419=CARTESIAN_POINT('Ctrl Pts',(-231.149586118655,-0.501260994610848,
124.906777841037));
#165420=CARTESIAN_POINT('Ctrl Pts',(-231.142188629319,-0.344000866660678,
124.897619217586));
#165421=CARTESIAN_POINT('Ctrl Pts',(-231.134788546804,-0.186685611416664,
124.888457383594));
#165422=CARTESIAN_POINT('Ctrl Pts',(-231.127388464289,-0.0290693094113907,
124.885588375131));
#165423=CARTESIAN_POINT('Ctrl Pts',(-231.119988381774,0.128308157965048,
124.889001999604));
#165424=CARTESIAN_POINT('Ctrl Pts',(-231.112580162107,0.285858678045888,
124.892419377708));
#165425=CARTESIAN_POINT('Ctrl Pts',(-231.105171942441,0.44316946558294,
124.902133177177));
#165426=CARTESIAN_POINT('Ctrl Pts',(-231.097763722774,0.599703910538144,
124.918081165978));
#165427=CARTESIAN_POINT('Ctrl Pts',(-231.090350943472,0.7563346998323,124.9340389705));
#165428=CARTESIAN_POINT('Ctrl Pts',(-231.08293816417,0.912187825705787,
124.956238557617));
#165429=CARTESIAN_POINT('Ctrl Pts',(-231.075525384868,1.06673628404196,
124.984566440552));
#165430=CARTESIAN_POINT('Ctrl Pts',(-231.068102013839,1.22150556846323,
125.012934799694));
#165431=CARTESIAN_POINT('Ctrl Pts',(-231.06067864281,1.37496609894559,125.047448861448));
#165432=CARTESIAN_POINT('Ctrl Pts',(-231.053255271781,1.52660465070735,
125.087944887151));
#165433=CARTESIAN_POINT('Ctrl Pts',(-231.049319222341,1.60700704936486,
125.109416851666));
#165434=CARTESIAN_POINT('Ctrl Pts',(-231.0453831729,1.68689752434762,125.132569742896));
#165435=CARTESIAN_POINT('Ctrl Pts',(-231.04144712346,1.76620190905187,125.15737368833));
#165436=CARTESIAN_POINT('Ctrl Pts',(-231.034023857054,1.91576750360562,
125.204153155317));
#165437=CARTESIAN_POINT('Ctrl Pts',(-231.026600590649,2.06369947970118,
125.25694953408));
#165438=CARTESIAN_POINT('Ctrl Pts',(-231.019177324243,2.20947697982862,
125.315631981706));
#165439=CARTESIAN_POINT('Ctrl Pts',(-231.011762831522,2.35508218305738,
125.374245071553));
#165440=CARTESIAN_POINT('Ctrl Pts',(-231.004348338801,2.4985376360528,125.438730244586));
#165441=CARTESIAN_POINT('Ctrl Pts',(-230.99693384608,2.63933654766249,125.508906609582));
#165442=CARTESIAN_POINT('Ctrl Pts',(-230.989526499726,2.77999975198019,
125.579015335955));
#165443=CARTESIAN_POINT('Ctrl Pts',(-230.982119153372,2.91801118045661,
125.654804168566));
#165444=CARTESIAN_POINT('Ctrl Pts',(-230.974711807019,3.05288308759154,
125.736043794794));
#165445=CARTESIAN_POINT('Ctrl Pts',(-230.967309985343,3.18765440217009,
125.817222829443));
#165446=CARTESIAN_POINT('Ctrl Pts',(-230.959908163668,3.31929053940336,
125.903844371151));
#165447=CARTESIAN_POINT('Ctrl Pts',(-230.952506341992,3.44732758623773,
125.995632815365));
#165448=CARTESIAN_POINT('Ctrl Pts',(-230.945108427681,3.57529704331208,
126.087372805174));
#165449=CARTESIAN_POINT('Ctrl Pts',(-230.93771051337,3.69967089116985,126.18427404846));
#165450=CARTESIAN_POINT('Ctrl Pts',(-230.930312599058,3.82001359266216,
126.286017258062));
#165451=CARTESIAN_POINT('Ctrl Pts',(-230.922915914146,3.9403362953802,126.387743559787));
#165452=CARTESIAN_POINT('Ctrl Pts',(-230.915519229233,4.05662889650189,
126.494309990067));
#165453=CARTESIAN_POINT('Ctrl Pts',(-230.908122544321,4.16848831534951,
126.605356482382));
#165454=CARTESIAN_POINT('Ctrl Pts',(-230.900726187386,4.28034277423328,
126.716398050779));
#165455=CARTESIAN_POINT('Ctrl Pts',(-230.89332983045,4.38776417677228,126.83191902323));
#165456=CARTESIAN_POINT('Ctrl Pts',(-230.885933473515,4.49038595558797,
126.951522114286));
#165457=CARTESIAN_POINT('Ctrl Pts',(-230.878535984178,4.59302344605999,
127.07114351688));
#165458=CARTESIAN_POINT('Ctrl Pts',(-230.871138494842,4.69085960655737,
127.194847999179));
#165459=CARTESIAN_POINT('Ctrl Pts',(-230.863741005505,4.78356795630168,
127.322204938975));
#165460=CARTESIAN_POINT('Ctrl Pts',(-230.85634092299,4.87630880481388,127.449606523548));
#165461=CARTESIAN_POINT('Ctrl Pts',(-230.848940840475,4.96391804411382,
127.580662813197));
#165462=CARTESIAN_POINT('Ctrl Pts',(-230.84154075796,5.04611243044084,127.714914081073));
#165463=CARTESIAN_POINT('Ctrl Pts',(-230.834132538294,5.12839719794553,
127.849312972019));
#165464=CARTESIAN_POINT('Ctrl Pts',(-230.826724318627,5.20525502653584,
127.986913538732));
#165465=CARTESIAN_POINT('Ctrl Pts',(-230.819316098961,5.27644822295134,
128.127230678057));
#165466=CARTESIAN_POINT('Ctrl Pts',(-230.811903319658,5.34768523759131,
128.26763418024));
#165467=CARTESIAN_POINT('Ctrl Pts',(-230.804490540357,5.41325051768329,
128.410757248119));
#165468=CARTESIAN_POINT('Ctrl Pts',(-230.797077761054,5.47295468426939,
128.55609515583));
#165469=CARTESIAN_POINT('Ctrl Pts',(-230.789654390026,5.53274415896865,
128.70164072916));
#165470=CARTESIAN_POINT('Ctrl Pts',(-230.782231018997,5.58665566653315,
128.849407113114));
#165471=CARTESIAN_POINT('Ctrl Pts',(-230.774807647968,5.6345495544069,128.9988740124));
#165472=CARTESIAN_POINT('Ctrl Pts',(-230.770871598528,5.65994404295338,
129.078124948804));
#165473=CARTESIAN_POINT('Ctrl Pts',(-230.766935549087,5.68364761299832,
129.15785377127));
#165474=CARTESIAN_POINT('Ctrl Pts',(-230.762999499647,5.7056453082692,129.237981934512));
#165475=CARTESIAN_POINT('Ctrl Pts',(-230.755576233241,5.74713227502902,
129.389101149686));
#165476=CARTESIAN_POINT('Ctrl Pts',(-230.748152966836,5.78267403282317,
129.54209824317));
#165477=CARTESIAN_POINT('Ctrl Pts',(-230.74072970043,5.81209912729416,129.696464279001));
#165478=CARTESIAN_POINT('Ctrl Pts',(-230.733315207709,5.84148944374708,
129.850647866996));
#165479=CARTESIAN_POINT('Ctrl Pts',(-230.725900714988,5.8647774177972,130.006196813632));
#165480=CARTESIAN_POINT('Ctrl Pts',(-230.718486222267,5.88184130535802,
130.162586965034));
#165481=CARTESIAN_POINT('Ctrl Pts',(-230.711078875914,5.89888874610166,
130.318826381721));
#165482=CARTESIAN_POINT('Ctrl Pts',(-230.70367152956,5.9097240029828,130.475905020456));
#165483=CARTESIAN_POINT('Ctrl Pts',(-230.696264183206,5.91427636484807,
130.633288578064));
#165484=CARTESIAN_POINT('Ctrl Pts',(-230.68886236153,5.91882533139009,130.790554753075));
#165485=CARTESIAN_POINT('Ctrl Pts',(-230.681460539855,5.91710072266801,
130.948125022599));
#165486=CARTESIAN_POINT('Ctrl Pts',(-230.67405871818,5.90908365626002,131.105460112452));
#165487=CARTESIAN_POINT('Ctrl Pts',(-230.666660803868,5.90107082199895,
131.262712146337));
#165488=CARTESIAN_POINT('Ctrl Pts',(-230.659262889557,5.88677216440396,
131.419728875929));
#165489=CARTESIAN_POINT('Ctrl Pts',(-230.651864975246,5.86622089033969,
131.575971288981));
#165490=CARTESIAN_POINT('Ctrl Pts',(-230.644468290333,5.84567303152436,
131.732187737379));
#165491=CARTESIAN_POINT('Ctrl Pts',(-230.637071605421,5.81887466712362,
131.887629754875));
#165492=CARTESIAN_POINT('Ctrl Pts',(-230.629674920509,5.78591085634493,
132.041763593532));
#165493=CARTESIAN_POINT('Ctrl Pts',(-230.622278563574,5.75294850721616,
132.195890597733));
#165494=CARTESIAN_POINT('Ctrl Pts',(-230.614882206638,5.71382133335572,
132.348709173387));
#165495=CARTESIAN_POINT('Ctrl Pts',(-230.607485849703,5.66866544364176,
132.499696174487));
#165496=CARTESIAN_POINT('Ctrl Pts',(-230.600088360366,5.62350264044593,
132.650706292083));
#165497=CARTESIAN_POINT('Ctrl Pts',(-230.59269087103,5.57230939052587,132.799883919105));
#165498=CARTESIAN_POINT('Ctrl Pts',(-230.585293381693,5.51527151770472,
132.946721616206));
#165499=CARTESIAN_POINT('Ctrl Pts',(-230.577893299178,5.45821365034543,
133.093610787036));
#165500=CARTESIAN_POINT('Ctrl Pts',(-230.570493216663,5.39530721597336,
133.238158047065));
#165501=CARTESIAN_POINT('Ctrl Pts',(-230.563093134148,5.32678589563614,
133.379876601704));
#165502=CARTESIAN_POINT('Ctrl Pts',(-230.555684914482,5.25818922906313,
133.521750990463));
#165503=CARTESIAN_POINT('Ctrl Pts',(-230.548276694815,5.1839655089468,133.660790125773));
#165504=CARTESIAN_POINT('Ctrl Pts',(-230.540868475149,5.1043943872987,133.796531819455));
#165505=CARTESIAN_POINT('Ctrl Pts',(-230.533455695847,5.02477429095271,
133.932357059885));
#165506=CARTESIAN_POINT('Ctrl Pts',(-230.526042916545,4.93980043590136,
134.064880501096));
#165507=CARTESIAN_POINT('Ctrl Pts',(-230.518630137243,4.84979509835615,
134.193669996549));
#165508=CARTESIAN_POINT('Ctrl Pts',(-230.511206766214,4.7596611569642,134.322643512472));
#165509=CARTESIAN_POINT('Ctrl Pts',(-230.503783395185,4.6644815998839,134.44787213056));
#165510=CARTESIAN_POINT('Ctrl Pts',(-230.496360024156,4.56461868066146,
134.56895712485));
#165511=CARTESIAN_POINT('Ctrl Pts',(-230.492423974715,4.51166896471087,
134.633159294218));
#165512=CARTESIAN_POINT('Ctrl Pts',(-230.488487925274,4.4574032069286,134.696197155051));
#165513=CARTESIAN_POINT('Ctrl Pts',(-230.484551875834,4.40187940545715,
134.758015668568));
#165514=CARTESIAN_POINT('Ctrl Pts',(-230.477128609428,4.29716324872232,
134.874603455768));
#165515=CARTESIAN_POINT('Ctrl Pts',(-230.469705343023,4.18765364911417,
134.987204409386));
#165516=CARTESIAN_POINT('Ctrl Pts',(-230.462282076617,4.07368611360614,
135.095399187692));
#165517=CARTESIAN_POINT('Ctrl Pts',(-230.454867583896,3.95985327826035,
135.203466088757));
#165518=CARTESIAN_POINT('Ctrl Pts',(-230.447453091175,3.8415732628944,135.307136926026));
#165519=CARTESIAN_POINT('Ctrl Pts',(-230.440038598454,3.71922124735563,
135.40602595478));
#165520=CARTESIAN_POINT('Ctrl Pts',(-230.432631252101,3.5969871592959,135.504819670565));
#165521=CARTESIAN_POINT('Ctrl Pts',(-230.425223905747,3.47068917284005,
135.598840520145));
#165522=CARTESIAN_POINT('Ctrl Pts',(-230.417816559393,3.34073859127704,
135.687740208306));
#165523=CARTESIAN_POINT('Ctrl Pts',(-230.410414737718,3.21088493176052,
135.776573591725));
#165524=CARTESIAN_POINT('Ctrl Pts',(-230.403012916042,3.07738440824752,
135.860293209109));
#165525=CARTESIAN_POINT('Ctrl Pts',(-230.395611094367,2.94068052097118,
135.938591683274));
#165526=CARTESIAN_POINT('Ctrl Pts',(-230.388213180055,2.80404879861284,
136.016848824284));
#165527=CARTESIAN_POINT('Ctrl Pts',(-230.380815265744,2.66421740336748,
136.089690336382));
#165528=CARTESIAN_POINT('Ctrl Pts',(-230.373417351433,2.52165777062691,
136.156852808157));
#165529=CARTESIAN_POINT('Ctrl Pts',(-230.36602066652,2.37912182871121,136.224004118748));
#165530=CARTESIAN_POINT('Ctrl Pts',(-230.358623981608,2.2338588864998,136.285478103147));
#165531=CARTESIAN_POINT('Ctrl Pts',(-230.351227296696,2.08636397782904,
136.341057820278));
#165532=CARTESIAN_POINT('Ctrl Pts',(-230.34383093976,1.93887560923709,136.396635072945));
#165533=CARTESIAN_POINT('Ctrl Pts',(-230.336434582825,1.78915582028648,
136.44631844638));
#165534=CARTESIAN_POINT('Ctrl Pts',(-230.32903822589,1.63771831870231,136.489939679639));
#165535=CARTESIAN_POINT('Ctrl Pts',(-230.321640736553,1.48625763165004,
136.533567591421));
#165536=CARTESIAN_POINT('Ctrl Pts',(-230.314243247217,1.3330790670597,136.571131411667));
#165537=CARTESIAN_POINT('Ctrl Pts',(-230.30684575788,1.17870999034055,136.60251319586));
#165538=CARTESIAN_POINT('Ctrl Pts',(-230.299445675365,1.02428679978196,
136.633905980888));
#165539=CARTESIAN_POINT('Ctrl Pts',(-230.29204559285,0.868672631776451,
136.659112340856));
#165540=CARTESIAN_POINT('Ctrl Pts',(-230.284645510335,0.712403350713097,
136.678065753883));
#165541=CARTESIAN_POINT('Ctrl Pts',(-230.277237290669,0.55596223550878,
136.697040008135));
#165542=CARTESIAN_POINT('Ctrl Pts',(-230.269829071002,0.39886493944161,
136.709747539131));
#165543=CARTESIAN_POINT('Ctrl Pts',(-230.262420851336,0.241651473258279,
136.716173802027));
#165544=CARTESIAN_POINT('Ctrl Pts',(-230.255008072034,0.084341244809761,
136.722604020182));
#165545=CARTESIAN_POINT('Ctrl Pts',(-230.247595292731,-0.0730849237969144,
136.722745266382));
#165546=CARTESIAN_POINT('Ctrl Pts',(-230.240182513429,-0.230089257275169,
136.716635094972));
#165547=CARTESIAN_POINT('Ctrl Pts',(-230.232759142401,-0.387317925907647,
136.710516193063));
#165548=CARTESIAN_POINT('Ctrl Pts',(-230.225335771372,-0.544123184456584,
136.698128063022));
#165549=CARTESIAN_POINT('Ctrl Pts',(-230.217912400343,-0.699973766585444,
136.679559957894));
#165550=CARTESIAN_POINT('Ctrl Pts',(-230.213976350902,-0.782609484814435,
136.66971470302));
#165551=CARTESIAN_POINT('Ctrl Pts',(-230.210040301461,-0.864976990053815,
136.658132887677));
#165552=CARTESIAN_POINT('Ctrl Pts',(-230.206104252021,-0.946998627205643,
136.64483355754));
#165553=CARTESIAN_POINT('Ctrl Pts',(-230.198680985615,-1.10168887506227,
136.619751435961));
#165554=CARTESIAN_POINT('Ctrl Pts',(-230.19125771921,-1.25561585987202,
136.588481474199));
#165555=CARTESIAN_POINT('Ctrl Pts',(-230.183834452805,-1.4082454278487,
136.551079279328));
#165556=CARTESIAN_POINT('Ctrl Pts',(-230.176419960084,-1.56069460035156,
136.513721290745));
#165557=CARTESIAN_POINT('Ctrl Pts',(-230.169005467363,-1.71184904931024,
136.470245583799));
#165558=CARTESIAN_POINT('Ctrl Pts',(-230.161590974642,-1.86118144289472,
136.420759303479));
#165559=CARTESIAN_POINT('Ctrl Pts',(-230.154183628288,-2.010369904296,136.371320719899));
#165560=CARTESIAN_POINT('Ctrl Pts',(-230.146776281935,-2.15773945453356,
136.315883212734));
#165561=CARTESIAN_POINT('Ctrl Pts',(-230.139368935581,-2.30277474350538,
136.254604561022));
#165562=CARTESIAN_POINT('Ctrl Pts',(-230.131967113906,-2.44770185968765,
136.193371613239));
#165563=CARTESIAN_POINT('Ctrl Pts',(-230.12456529223,-2.59029783874524,
136.126306340039));
#165564=CARTESIAN_POINT('Ctrl Pts',(-230.117163470555,-2.73006435283812,
136.053615725852));
#165565=CARTESIAN_POINT('Ctrl Pts',(-230.109765556244,-2.86975708527654,
135.980963484474));
#165566=CARTESIAN_POINT('Ctrl Pts',(-230.102367641932,-3.00662299708464,
135.902691987966));
#165567=CARTESIAN_POINT('Ctrl Pts',(-230.094969727621,-3.14018565043765,
135.819055487973));
#165568=CARTESIAN_POINT('Ctrl Pts',(-230.087573042709,-3.27372610809979,
135.73543288685));
#165569=CARTESIAN_POINT('Ctrl Pts',(-230.080176357797,-3.40396408071764,
135.646447249662));
#165570=CARTESIAN_POINT('Ctrl Pts',(-230.072779672885,-3.53044947173783,
135.552397800445));
#165571=CARTESIAN_POINT('Ctrl Pts',(-230.065383315949,-3.65692925426322,
135.45835252148));
#165572=CARTESIAN_POINT('Ctrl Pts',(-230.057986959014,-3.77965648647571,
135.359244099678));
#165573=CARTESIAN_POINT('Ctrl Pts',(-230.050590602079,-3.89821193410659,
135.255413782749));
#165574=CARTESIAN_POINT('Ctrl Pts',(-230.043193112742,-4.01678553287983,
135.151567569133));
#165575=CARTESIAN_POINT('Ctrl Pts',(-230.035795623406,-4.13118579447052,
135.042998266893));
#165576=CARTESIAN_POINT('Ctrl Pts',(-230.028398134069,-4.24102843493114,
134.93008581159));
#165577=CARTESIAN_POINT('Ctrl Pts',(-230.020998051554,-4.35090958055831,
134.817133775002));
#165578=CARTESIAN_POINT('Ctrl Pts',(-230.013597969039,-4.45622966397548,
134.699835821501));
#165579=CARTESIAN_POINT('Ctrl Pts',(-230.006197886524,-4.55664307064725,
134.578606832272));
#165580=CARTESIAN_POINT('Ctrl Pts',(-229.998789666858,-4.65716689218283,
134.457244539306));
#165581=CARTESIAN_POINT('Ctrl Pts',(-229.991381447192,-4.75277302374416,
134.331942865802));
#165582=CARTESIAN_POINT('Ctrl Pts',(-229.983973227525,-4.84315733934463,
134.203148276254));
#165583=CARTESIAN_POINT('Ctrl Pts',(-229.976560448223,-4.93359728498372,
134.074274415785));
#165584=CARTESIAN_POINT('Ctrl Pts',(-229.969147668921,-5.01880880889249,
133.941903668619));
#165585=CARTESIAN_POINT('Ctrl Pts',(-229.961734889619,-5.09853282592591,
133.806508779375));
#165586=CARTESIAN_POINT('Ctrl Pts',(-229.954311518591,-5.1783707563732,
133.670920431566));
#165587=CARTESIAN_POINT('Ctrl Pts',(-229.946888147562,-5.25270534414721,
133.532299639712));
#165588=CARTESIAN_POINT('Ctrl Pts',(-229.939464776533,-5.32132451793056,
133.391141616679));
#165589=CARTESIAN_POINT('Ctrl Pts',(-229.935528727092,-5.35770805037367,
133.316296245809));
#165590=CARTESIAN_POINT('Ctrl Pts',(-229.93159267765,-5.39248558963972,
133.240737876772));
#165591=CARTESIAN_POINT('Ctrl Pts',(-229.927656628208,-5.42563118491665,
133.164542137653));
#165592=CARTESIAN_POINT('Ctrl Pts',(-229.919453204097,-5.49471247556551,
133.005736723049));
#165593=CARTESIAN_POINT('Ctrl Pts',(-229.911249779985,-5.55688125103648,
132.843750280117));
#165594=CARTESIAN_POINT('Ctrl Pts',(-229.903046355874,-5.61186340173011,
132.679172534218));
#165595=CARTESIAN_POINT('Ctrl Pts',(-229.894874816899,-5.66663184734259,
132.515234470473));
#165596=CARTESIAN_POINT('Ctrl Pts',(-229.886703277925,-5.71426930736496,
132.348725421031));
#165597=CARTESIAN_POINT('Ctrl Pts',(-229.87853173895,-5.75455061996164,
132.180252228413));
#165598=CARTESIAN_POINT('Ctrl Pts',(-229.870380481584,-5.79473195508803,
132.012197183132));
#165599=CARTESIAN_POINT('Ctrl Pts',(-229.862229224218,-5.8275934947053,
131.842187947632));
#165600=CARTESIAN_POINT('Ctrl Pts',(-229.854077966851,-5.85295916047295,
131.670847563997));
#165601=CARTESIAN_POINT('Ctrl Pts',(-229.845960083918,-5.87822096929155,
131.500208714856));
#165602=CARTESIAN_POINT('Ctrl Pts',(-229.837842200985,-5.89604806700541,
131.328249822894));
#165603=CARTESIAN_POINT('Ctrl Pts',(-229.829724318052,-5.90631517593186,
131.155603560637));
#165604=CARTESIAN_POINT('Ctrl Pts',(-229.824274629052,-5.91320768116215,
131.039702845633));
#165605=CARTESIAN_POINT('Ctrl Pts',(-229.818824940053,-5.91669413707215,
130.923492707171));
#165606=CARTESIAN_POINT('Ctrl Pts',(-229.813375251053,-5.91674933390121,
130.807168157351));
#165607=CARTESIAN_POINT('',(-228.063375157888,-5.91524724934575,130.799300212791));
#165608=CARTESIAN_POINT('Ctrl Pts',(-229.813375192209,-5.90821578806308,
130.807162853899));
#165609=CARTESIAN_POINT('Ctrl Pts',(-229.758653129604,-5.90324637020015,
129.640793025429));
#165610=CARTESIAN_POINT('Ctrl Pts',(-229.611115192396,-5.00404810123538,
126.489038457145));
#165611=CARTESIAN_POINT('Ctrl Pts',(-229.370761380581,0.128487452770731,
123.807143206003));
#165612=CARTESIAN_POINT('Ctrl Pts',(-229.092313756769,5.95640778655091,
127.130293823035));
#165613=CARTESIAN_POINT('Ctrl Pts',(-228.813866132955,6.31068035119472,
133.829732336119));
#165614=CARTESIAN_POINT('Ctrl Pts',(-228.535418509144,0.865745966962777,
137.749002037465));
#165615=CARTESIAN_POINT('Ctrl Pts',(-228.285254862227,-4.7408718153285,
135.536621484418));
#165616=CARTESIAN_POINT('Ctrl Pts',(-228.127907089916,-5.90152179133772,
132.17219460905));
#165617=CARTESIAN_POINT('Ctrl Pts',(-228.063375192209,-5.91261418727021,
130.799303195672));
#165618=CARTESIAN_POINT('',(-226.313375192209,-5.92101946389561,130.803627806158));
#165619=CARTESIAN_POINT('Ctrl Pts',(-228.063375138329,-5.91674783454524,
130.799298512843));
#165620=CARTESIAN_POINT('Ctrl Pts',(-228.054506342384,-5.91658629655463,
130.610487808902));
#165621=CARTESIAN_POINT('Ctrl Pts',(-228.045637546438,-5.90738325424359,
130.422070303137));
#165622=CARTESIAN_POINT('Ctrl Pts',(-228.036768750493,-5.88927407511812,
130.234815684623));
#165623=CARTESIAN_POINT('Ctrl Pts',(-228.02782973436,-5.87102151351253,
130.046078446082));
#165624=CARTESIAN_POINT('Ctrl Pts',(-228.018890718226,-5.84372132038497,
129.858522591115));
#165625=CARTESIAN_POINT('Ctrl Pts',(-228.009951702093,-5.80756065119015,
129.672914708453));
#165626=CARTESIAN_POINT('Ctrl Pts',(-228.000937814618,-5.77109710774292,
129.485752212729));
#165627=CARTESIAN_POINT('Ctrl Pts',(-227.991923927143,-5.72562408790282,
129.300570461164));
#165628=CARTESIAN_POINT('Ctrl Pts',(-227.982910039668,-5.67138157104477,
129.118133575287));
#165629=CARTESIAN_POINT('Ctrl Pts',(-227.981447780285,-5.6625821901492,
129.088538126159));
#165630=CARTESIAN_POINT('Ctrl Pts',(-227.979985520901,-5.65355212979459,
129.059014865267));
#165631=CARTESIAN_POINT('Ctrl Pts',(-227.978523261518,-5.64429253147647,
129.029567000939));
#165632=CARTESIAN_POINT('Ctrl Pts',(-227.971099995113,-5.59728550528529,
128.880072769964));
#165633=CARTESIAN_POINT('Ctrl Pts',(-227.963676728707,-5.54426406037377,
128.73222131227));
#165634=CARTESIAN_POINT('Ctrl Pts',(-227.956253462302,-5.48535983216093,
128.586533285645));
#165635=CARTESIAN_POINT('Ctrl Pts',(-227.94883896958,-5.42652522385415,
128.441017450169));
#165636=CARTESIAN_POINT('Ctrl Pts',(-227.941424476859,-5.36182181071405,
128.297660298747));
#165637=CARTESIAN_POINT('Ctrl Pts',(-227.934009984138,-5.29143125500573,
128.156968346661));
#165638=CARTESIAN_POINT('Ctrl Pts',(-227.926602637784,-5.22110854436515,
128.016411998775));
#165639=CARTESIAN_POINT('Ctrl Pts',(-227.919195291431,-5.14510976961532,
127.878516067814));
#165640=CARTESIAN_POINT('Ctrl Pts',(-227.911787945077,-5.06366498537831,
127.743767949739));
#165641=CARTESIAN_POINT('Ctrl Pts',(-227.904386123401,-4.98228094573412,
127.609120331895));
#165642=CARTESIAN_POINT('Ctrl Pts',(-227.896984301726,-4.89545917653997,
127.477616170335));
#165643=CARTESIAN_POINT('Ctrl Pts',(-227.88958248005,-4.80347598802572,
127.349718958152));
#165644=CARTESIAN_POINT('Ctrl Pts',(-227.882184565739,-4.71154135672069,
127.221889261912));
#165645=CARTESIAN_POINT('Ctrl Pts',(-227.874786651427,-4.61445094982006,
127.097663025273));
#165646=CARTESIAN_POINT('Ctrl Pts',(-227.867388737116,-4.5125247169297,
126.977475298981));
#165647=CARTESIAN_POINT('Ctrl Pts',(-227.859992052204,-4.41061542232996,
126.857307545709));
#165648=CARTESIAN_POINT('Ctrl Pts',(-227.852595367291,-4.30387213790969,
126.741177255218));
#165649=CARTESIAN_POINT('Ctrl Pts',(-227.845198682379,-4.19265554319056,
126.629486959759));
#165650=CARTESIAN_POINT('Ctrl Pts',(-227.837802325444,-4.08144387993178,
126.517801616765));
#165651=CARTESIAN_POINT('Ctrl Pts',(-227.830405968508,-3.96575956416316,
126.410556141872));
#165652=CARTESIAN_POINT('Ctrl Pts',(-227.823009611573,-3.84600043872704,
126.308116497435));
#165653=CARTESIAN_POINT('Ctrl Pts',(-227.815612122236,-3.72622297786309,
126.205661169227));
#165654=CARTESIAN_POINT('Ctrl Pts',(-227.808214632899,-3.60236974882988,
126.108013379186));
#165655=CARTESIAN_POINT('Ctrl Pts',(-227.800817143563,-3.47487187018399,
126.015498952378));
#165656=CARTESIAN_POINT('Ctrl Pts',(-227.793417061048,-3.3473292973542,
125.922952094782));
#165657=CARTESIAN_POINT('Ctrl Pts',(-227.786016978533,-3.21613983311619,
125.835542402295));
#165658=CARTESIAN_POINT('Ctrl Pts',(-227.778616896018,-3.0817636348362,
125.753552418723));
#165659=CARTESIAN_POINT('Ctrl Pts',(-227.771208676351,-2.94723967611218,
125.671472278736));
#165660=CARTESIAN_POINT('Ctrl Pts',(-227.763800456684,-2.80952230420485,
125.594823943784));
#165661=CARTESIAN_POINT('Ctrl Pts',(-227.756392237018,-2.66909698343816,
125.523844368609));
#165662=CARTESIAN_POINT('Ctrl Pts',(-227.748979457716,-2.52858523322966,
125.452821106689));
#165663=CARTESIAN_POINT('Ctrl Pts',(-227.741566678414,-2.38536255188863,
125.387473711466));
#165664=CARTESIAN_POINT('Ctrl Pts',(-227.734153899112,-2.2399339528973,
125.327990793571));
#165665=CARTESIAN_POINT('Ctrl Pts',(-227.726730528083,-2.09429755870359,
125.268422883694));
#165666=CARTESIAN_POINT('Ctrl Pts',(-227.719307157054,-1.94644930172276,
125.21473631384));
#165667=CARTESIAN_POINT('Ctrl Pts',(-227.711883786025,-1.79690968917086,
125.167069944604));
#165668=CARTESIAN_POINT('Ctrl Pts',(-227.707947736585,-1.71762019845595,
125.141796091901));
#165669=CARTESIAN_POINT('Ctrl Pts',(-227.704011687145,-1.6378553955227,
125.118213883002));
#165670=CARTESIAN_POINT('Ctrl Pts',(-227.700075637705,-1.55769384832639,
125.09633815463));
#165671=CARTESIAN_POINT('Ctrl Pts',(-227.692652371299,-1.40651167204503,
125.055081213631));
#165672=CARTESIAN_POINT('Ctrl Pts',(-227.685229104894,-1.2534606672229,
125.019772332525));
#165673=CARTESIAN_POINT('Ctrl Pts',(-227.677805838488,-1.09905003016062,
124.990582190957));
#165674=CARTESIAN_POINT('Ctrl Pts',(-227.670391345767,-0.944821893647909,
124.961426549712));
#165675=CARTESIAN_POINT('Ctrl Pts',(-227.662976853046,-0.789237686801845,
124.938375321646));
#165676=CARTESIAN_POINT('Ctrl Pts',(-227.655562360325,-0.632821748164266,
124.921549453033));
#165677=CARTESIAN_POINT('Ctrl Pts',(-227.648155013972,-0.476556569097746,
124.904739801826));
#165678=CARTESIAN_POINT('Ctrl Pts',(-227.640747667618,-0.319461622840829,
124.894143604441));
#165679=CARTESIAN_POINT('Ctrl Pts',(-227.633340321264,-0.162071319561586,
124.88983075883));
#165680=CARTESIAN_POINT('Ctrl Pts',(-227.625938499589,-0.00479840390807593,
124.885521129903));
#165681=CARTESIAN_POINT('Ctrl Pts',(-227.618536677913,0.152769058592018,
124.887485531755));
#165682=CARTESIAN_POINT('Ctrl Pts',(-227.611134856238,0.310091765644128,
124.895742026103));
#165683=CARTESIAN_POINT('Ctrl Pts',(-227.603736941926,0.467331423263784,
124.903994161912));
#165684=CARTESIAN_POINT('Ctrl Pts',(-227.596339027615,0.624326210911163,
124.918531755683));
#165685=CARTESIAN_POINT('Ctrl Pts',(-227.588941113304,0.780537167497064,
124.939320780305));
#165686=CARTESIAN_POINT('Ctrl Pts',(-227.581544428391,0.936722164655714,
124.960106350168));
#165687=CARTESIAN_POINT('Ctrl Pts',(-227.574147743479,1.09212321960435,
124.987141239827));
#165688=CARTESIAN_POINT('Ctrl Pts',(-227.566751058567,1.24620671446836,
125.020339577899));
#165689=CARTESIAN_POINT('Ctrl Pts',(-227.559354701631,1.40028337710874,
125.053536443921));
#165690=CARTESIAN_POINT('Ctrl Pts',(-227.551958344696,1.55304223090366,
125.092896136331));
#165691=CARTESIAN_POINT('Ctrl Pts',(-227.54456198776,1.70396033758665,125.138281750269));
#165692=CARTESIAN_POINT('Ctrl Pts',(-227.537164498424,1.85490155021704,
125.18367431286));
#165693=CARTESIAN_POINT('Ctrl Pts',(-227.529767009087,2.00400109708265,
125.235094526453));
#165694=CARTESIAN_POINT('Ctrl Pts',(-227.52236951975,2.15075182221655,125.292355795205));
#165695=CARTESIAN_POINT('Ctrl Pts',(-227.514969437235,2.29755399058986,
125.349637136806));
#165696=CARTESIAN_POINT('Ctrl Pts',(-227.507569354721,2.44200535035133,
125.412763474657));
#165697=CARTESIAN_POINT('Ctrl Pts',(-227.500169272206,2.58361946309799,
125.481500387163));
#165698=CARTESIAN_POINT('Ctrl Pts',(-227.492761052539,2.72538929511969,
125.550312882971));
#165699=CARTESIAN_POINT('Ctrl Pts',(-227.485352832872,2.86431531355729,
125.624748111034));
#165700=CARTESIAN_POINT('Ctrl Pts',(-227.477944613206,2.99993575635128,
125.704525716291));
#165701=CARTESIAN_POINT('Ctrl Pts',(-227.470531833904,3.13563967126485,
125.784352423333));
#165702=CARTESIAN_POINT('Ctrl Pts',(-227.463119054602,3.26803364327327,
125.869527858104));
#165703=CARTESIAN_POINT('Ctrl Pts',(-227.4557062753,3.39668601678758,125.959729087113));
#165704=CARTESIAN_POINT('Ctrl Pts',(-227.448282904271,3.52552221484654,
126.050059199868));
#165705=CARTESIAN_POINT('Ctrl Pts',(-227.440859533242,3.6506058408394,126.145429223372));
#165706=CARTESIAN_POINT('Ctrl Pts',(-227.433436162213,3.77153872055182,
126.245476297705));
#165707=CARTESIAN_POINT('Ctrl Pts',(-227.429500112773,3.83566023511634,
126.298523657109));
#165708=CARTESIAN_POINT('Ctrl Pts',(-227.425564063332,3.89861543970226,
126.352885284942));
#165709=CARTESIAN_POINT('Ctrl Pts',(-227.421628013892,3.96034938385561,
126.408503099368));
#165710=CARTESIAN_POINT('Ctrl Pts',(-227.414204747486,4.07677767588481,
126.513396561609));
#165711=CARTESIAN_POINT('Ctrl Pts',(-227.406781481081,4.18921184414372,
126.623077393891));
#165712=CARTESIAN_POINT('Ctrl Pts',(-227.399358214675,4.29723305797474,
126.737209451461));
#165713=CARTESIAN_POINT('Ctrl Pts',(-227.391943721954,4.40512659970163,
126.851206614417));
#165714=CARTESIAN_POINT('Ctrl Pts',(-227.384529229233,4.50861731487337,
126.969644262183));
#165715=CARTESIAN_POINT('Ctrl Pts',(-227.377114736512,4.60732003017595,
127.092146628308));
#165716=CARTESIAN_POINT('Ctrl Pts',(-227.369707390158,4.70592761208543,
127.214530922041));
#165717=CARTESIAN_POINT('Ctrl Pts',(-227.362300043805,4.79975614875495,
127.340971845974));
#165718=CARTESIAN_POINT('Ctrl Pts',(-227.354892697451,4.88845797130749,
127.471057567248));
#165719=CARTESIAN_POINT('Ctrl Pts',(-227.347490875775,4.97709363669451,
127.601046265684));
#165720=CARTESIAN_POINT('Ctrl Pts',(-227.3400890541,5.06060999206217,127.734674041612));
#165721=CARTESIAN_POINT('Ctrl Pts',(-227.332687232425,5.13870033551353,
127.871496927537));
#165722=CARTESIAN_POINT('Ctrl Pts',(-227.325289318113,5.2167494556802,128.008247585724));
#165723=CARTESIAN_POINT('Ctrl Pts',(-227.317891403802,5.28937808384876,
128.148189671429));
#165724=CARTESIAN_POINT('Ctrl Pts',(-227.31049348949,5.35632352635789,128.290851348937));
#165725=CARTESIAN_POINT('Ctrl Pts',(-227.303096804578,5.42325784374888,
128.433489318662));
#165726=CARTESIAN_POINT('Ctrl Pts',(-227.295700119666,5.4845106914927,128.578845645601));
#165727=CARTESIAN_POINT('Ctrl Pts',(-227.288303434754,5.53986588211983,
128.726424966343));
#165728=CARTESIAN_POINT('Ctrl Pts',(-227.280907077818,5.59521861823997,
128.873997743264));
#165729=CARTESIAN_POINT('Ctrl Pts',(-227.273510720883,5.64467408610982,
129.023792968478));
#165730=CARTESIAN_POINT('Ctrl Pts',(-227.266114363947,5.68806480675869,
129.175296678792));
#165731=CARTESIAN_POINT('Ctrl Pts',(-227.258716874611,5.73146217063765,
129.326823584711));
#165732=CARTESIAN_POINT('Ctrl Pts',(-227.251319385274,5.76879283568528,
129.480059137663));
#165733=CARTESIAN_POINT('Ctrl Pts',(-227.243921895938,5.79993966008191,
129.634475793359));
#165734=CARTESIAN_POINT('Ctrl Pts',(-227.236521813423,5.83109740294951,
129.788946579575));
#165735=CARTESIAN_POINT('Ctrl Pts',(-227.229121730908,5.85606691545617,
129.944598927172));
#165736=CARTESIAN_POINT('Ctrl Pts',(-227.221721648393,5.87478249129061,
130.100896871147));
#165737=CARTESIAN_POINT('Ctrl Pts',(-227.214313428726,5.89351864682472,
130.25736668078));
#165738=CARTESIAN_POINT('Ctrl Pts',(-227.20690520906,5.90598708776309,130.414483133631));
#165739=CARTESIAN_POINT('Ctrl Pts',(-227.199496989393,5.91217409108498,
130.571706197441));
#165740=CARTESIAN_POINT('Ctrl Pts',(-227.192084210091,5.91836490240416,
130.729026029424));
#165741=CARTESIAN_POINT('Ctrl Pts',(-227.184671430789,5.91826657261066,
130.886452230686));
#165742=CARTESIAN_POINT('Ctrl Pts',(-227.177258651487,5.91191747440748,
131.043447083715));
#165743=CARTESIAN_POINT('Ctrl Pts',(-227.169835280458,5.90555930431503,
131.200666258352));
#165744=CARTESIAN_POINT('Ctrl Pts',(-227.16241190943,5.89293255770868,131.357452482698));
#165745=CARTESIAN_POINT('Ctrl Pts',(-227.154988538401,5.87412729602688,
131.513274626859));
#165746=CARTESIAN_POINT('Ctrl Pts',(-227.15105248896,5.86415629505729,131.595895266593));
#165747=CARTESIAN_POINT('Ctrl Pts',(-227.147116439519,5.85244914380482,
131.678245050899));
#165748=CARTESIAN_POINT('Ctrl Pts',(-227.143180390079,5.83902500609958,
131.760246353752));
#165749=CARTESIAN_POINT('Ctrl Pts',(-227.135757123673,5.81370750134011,
131.914898251763));
#165750=CARTESIAN_POINT('Ctrl Pts',(-227.128333857268,5.78220332512043,
132.068777470771));
#165751=CARTESIAN_POINT('Ctrl Pts',(-227.120910590862,5.74456889733928,
132.221349942234));
#165752=CARTESIAN_POINT('Ctrl Pts',(-227.113496098141,5.70697895032642,
132.373742085705));
#165753=CARTESIAN_POINT('Ctrl Pts',(-227.10608160542,5.6632732623841,132.524830197006));
#165754=CARTESIAN_POINT('Ctrl Pts',(-227.098667112699,5.61355978088494,
132.674087107973));
#165755=CARTESIAN_POINT('Ctrl Pts',(-227.091259766346,5.56389421511078,
132.823200159511));
#165756=CARTESIAN_POINT('Ctrl Pts',(-227.083852419992,5.50823250077247,
132.97048517265));
#165757=CARTESIAN_POINT('Ctrl Pts',(-227.076445073638,5.44673320099748,
133.115427037999));
#165758=CARTESIAN_POINT('Ctrl Pts',(-227.069043251963,5.38527976972049,
133.260260800236));
#165759=CARTESIAN_POINT('Ctrl Pts',(-227.061641430287,5.31799756737383,
133.402754552242));
#165760=CARTESIAN_POINT('Ctrl Pts',(-227.054239608612,5.24509433651822,
133.542410281748));
#165761=CARTESIAN_POINT('Ctrl Pts',(-227.0468416943,5.1722295907109,133.68199228808));
#165762=CARTESIAN_POINT('Ctrl Pts',(-227.039443779989,5.09374989822016,
133.818738925507));
#165763=CARTESIAN_POINT('Ctrl Pts',(-227.032045865678,5.00991023545401,
133.952174143681));
#165764=CARTESIAN_POINT('Ctrl Pts',(-227.024649180766,4.92608450531893,
134.085587187343));
#165765=CARTESIAN_POINT('Ctrl Pts',(-227.017252495853,4.83690077115004,
134.215689588156));
#165766=CARTESIAN_POINT('Ctrl Pts',(-227.009855810941,4.74265894160609,
134.342031705458));
#165767=CARTESIAN_POINT('Ctrl Pts',(-227.002459454006,4.64842129084362,
134.468368220617));
#165768=CARTESIAN_POINT('Ctrl Pts',(-226.99506309707,4.54912621385052,134.590944484567));
#165769=CARTESIAN_POINT('Ctrl Pts',(-226.987666740135,4.44511559594414,
134.709341782846));
#165770=CARTESIAN_POINT('Ctrl Pts',(-226.980269250798,4.34108905374633,
134.827757208054));
#165771=CARTESIAN_POINT('Ctrl Pts',(-226.972871761462,4.23234577950193,
134.941992113175));
#165772=CARTESIAN_POINT('Ctrl Pts',(-226.965474272125,4.11926629314812,
135.051662792904));
#165773=CARTESIAN_POINT('Ctrl Pts',(-226.95807418961,4.00614716695582,135.16137191752));
#165774=CARTESIAN_POINT('Ctrl Pts',(-226.950674107095,3.88868907004331,
135.266513371461));
#165775=CARTESIAN_POINT('Ctrl Pts',(-226.94327402458,3.76730740908115,135.366742171972));
#165776=CARTESIAN_POINT('Ctrl Pts',(-226.935865804914,3.64579227650426,
135.467081184352));
#165777=CARTESIAN_POINT('Ctrl Pts',(-226.928457585247,3.5203452518386,135.562496517387));
#165778=CARTESIAN_POINT('Ctrl Pts',(-226.921049365581,3.39141326188787,
135.652684724883));
#165779=CARTESIAN_POINT('Ctrl Pts',(-226.913636586279,3.26240191644866,
135.742928441716));
#165780=CARTESIAN_POINT('Ctrl Pts',(-226.906223806977,3.12990164513015,
135.827938421207));
#165781=CARTESIAN_POINT('Ctrl Pts',(-226.898811027675,2.99438558628782,
135.907456297948));
#165782=CARTESIAN_POINT('Ctrl Pts',(-226.891387656646,2.85867589574575,
135.98708779356));
#165783=CARTESIAN_POINT('Ctrl Pts',(-226.883964285617,2.71994213982124,
136.061211338007));
#165784=CARTESIAN_POINT('Ctrl Pts',(-226.876540914588,2.57867985354334,
136.129615613848));
#165785=CARTESIAN_POINT('Ctrl Pts',(-226.872604865148,2.50377919981375,
136.165885202239));
#165786=CARTESIAN_POINT('Ctrl Pts',(-226.868668815707,2.42816799279131,
136.200547714251));
#165787=CARTESIAN_POINT('Ctrl Pts',(-226.864732766266,2.35192189996657,
136.233577314195));
#165788=CARTESIAN_POINT('Ctrl Pts',(-226.85730949986,2.20812414846543,136.295870108869));
#165789=CARTESIAN_POINT('Ctrl Pts',(-226.849886233455,2.06163242665041,
136.352540229753));
#165790=CARTESIAN_POINT('Ctrl Pts',(-226.84246296705,1.91292655784591,136.403346467413));
#165791=CARTESIAN_POINT('Ctrl Pts',(-226.835048474329,1.76439644702866,
136.45409265632));
#165792=CARTESIAN_POINT('Ctrl Pts',(-226.827633981608,1.61365774805125,
136.498988637935));
#165793=CARTESIAN_POINT('Ctrl Pts',(-226.820219488887,1.46121233061102,
136.537840284171));
#165794=CARTESIAN_POINT('Ctrl Pts',(-226.812812142533,1.3089138458036,136.576654483728));
#165795=CARTESIAN_POINT('Ctrl Pts',(-226.805404796179,1.15491227671018,
136.609435854271));
#165796=CARTESIAN_POINT('Ctrl Pts',(-226.797997449826,0.999726706694797,
136.636039370243));
#165797=CARTESIAN_POINT('Ctrl Pts',(-226.79059562815,0.844656879932347,
136.662623044308));
#165798=CARTESIAN_POINT('Ctrl Pts',(-226.783193806475,0.688405176911631,
136.683037975506));
#165799=CARTESIAN_POINT('Ctrl Pts',(-226.7757919848,0.531502879386526,136.697189755739));
#165800=CARTESIAN_POINT('Ctrl Pts',(-226.768394070489,0.37468340936296,
136.711334065358));
#165801=CARTESIAN_POINT('Ctrl Pts',(-226.760996156177,0.217214399667312,
136.719221775157));
#165802=CARTESIAN_POINT('Ctrl Pts',(-226.753598241866,0.0596341859142466,
136.720810087169));
#165803=CARTESIAN_POINT('Ctrl Pts',(-226.746201556954,-0.0979198408663133,
136.722398135233));
#165804=CARTESIAN_POINT('Ctrl Pts',(-226.738804872042,-0.255584662113312,
136.71768885943));
#165805=CARTESIAN_POINT('Ctrl Pts',(-226.73140818713,-0.412819874445797,
136.706691539648));
#165806=CARTESIAN_POINT('Ctrl Pts',(-226.724011830194,-0.570048114804197,
136.695694707498));
#165807=CARTESIAN_POINT('Ctrl Pts',(-226.716615473259,-0.726846411736703,
136.678410411798));
#165808=CARTESIAN_POINT('Ctrl Pts',(-226.709219116323,-0.882677691542532,
136.654899964956));
#165809=CARTESIAN_POINT('Ctrl Pts',(-226.701821626987,-1.03853282951512,
136.631385918603));
#165810=CARTESIAN_POINT('Ctrl Pts',(-226.69442413765,-1.19342028642395,
136.601643878774));
#165811=CARTESIAN_POINT('Ctrl Pts',(-226.687026648314,-1.34681155980786,
136.565786585577));
#165812=CARTESIAN_POINT('Ctrl Pts',(-226.679626565799,-1.50025660426508,
136.529916722661));
#165813=CARTESIAN_POINT('Ctrl Pts',(-226.672226483284,-1.65220405768046,
136.487927423222));
#165814=CARTESIAN_POINT('Ctrl Pts',(-226.664826400769,-1.80213913883811,
136.439981709049));
#165815=CARTESIAN_POINT('Ctrl Pts',(-226.657418181103,-1.9522390890314,
136.391983273634));
#165816=CARTESIAN_POINT('Ctrl Pts',(-226.650009961436,-2.10032189206058,
136.338015457094));
#165817=CARTESIAN_POINT('Ctrl Pts',(-226.64260174177,-2.24589067519652,
136.278290251528));
#165818=CARTESIAN_POINT('Ctrl Pts',(-226.635188962468,-2.39154905348955,
136.218528286094));
#165819=CARTESIAN_POINT('Ctrl Pts',(-226.627776183166,-2.53468998998896,
136.153002025632));
#165820=CARTESIAN_POINT('Ctrl Pts',(-226.620363403864,-2.67484037172136,
136.081969882026));
#165821=CARTESIAN_POINT('Ctrl Pts',(-226.612940032835,-2.81519100689139,
136.010836244362));
#165822=CARTESIAN_POINT('Ctrl Pts',(-226.605516661807,-2.95254222795981,
135.934181192702));
#165823=CARTESIAN_POINT('Ctrl Pts',(-226.598093290778,-3.08644839879045,
135.852307412462));
#165824=CARTESIAN_POINT('Ctrl Pts',(-226.594157241336,-3.15744866361516,
135.808895969635));
#165825=CARTESIAN_POINT('Ctrl Pts',(-226.590221191895,-3.22748092097847,
135.76401805416));
#165826=CARTESIAN_POINT('Ctrl Pts',(-226.586285142453,-3.29648253445665,
135.71772336242));
#165827=CARTESIAN_POINT('Ctrl Pts',(-226.578887013369,-3.42617674971686,
135.630708676628));
#165828=CARTESIAN_POINT('Ctrl Pts',(-226.571488884284,-3.55262599635902,
135.53841925968));
#165829=CARTESIAN_POINT('Ctrl Pts',(-226.5640907552,-3.67536978180676,135.441125387261));
#165830=CARTESIAN_POINT('Ctrl Pts',(-226.556701385759,-3.79796823430501,
135.343946714201));
#165831=CARTESIAN_POINT('Ctrl Pts',(-226.549312016319,-3.91686966586141,
135.241775610162));
#165832=CARTESIAN_POINT('Ctrl Pts',(-226.541922646879,-4.03164112926855,
135.13492644287));
#165833=CARTESIAN_POINT('Ctrl Pts',(-226.534540385959,-4.14630218336419,
135.028180063698));
#165834=CARTESIAN_POINT('Ctrl Pts',(-226.527158125038,-4.25684090441604,
134.916764833901));
#165835=CARTESIAN_POINT('Ctrl Pts',(-226.519775864118,-4.3628562433914,
134.801036231373));
#165836=CARTESIAN_POINT('Ctrl Pts',(-226.512399066432,-4.46879312581351,
134.68539327369));
#165837=CARTESIAN_POINT('Ctrl Pts',(-226.505022268747,-4.57021303781855,
134.565443574654));
#165838=CARTESIAN_POINT('Ctrl Pts',(-226.497645471062,-4.66675085057975,
134.441580305887));
#165839=CARTESIAN_POINT('Ctrl Pts',(-226.489967542777,-4.76722946404511,
134.312660775302));
#165840=CARTESIAN_POINT('Ctrl Pts',(-226.482289614491,-4.86241866816122,
134.17950169917));
#165841=CARTESIAN_POINT('Ctrl Pts',(-226.474611686205,-4.95195177533823,
134.04258608489));
#165842=CARTESIAN_POINT('Ctrl Pts',(-226.467239868017,-5.03791530136331,
133.91112913737));
#165843=CARTESIAN_POINT('Ctrl Pts',(-226.459868049828,-5.11866481166663,
133.776209754528));
#165844=CARTESIAN_POINT('Ctrl Pts',(-226.452496231639,-5.19391926109291,
133.63828603503));
#165845=CARTESIAN_POINT('Ctrl Pts',(-226.445124560937,-5.2691722049107,
133.500365074958));
#165846=CARTESIAN_POINT('Ctrl Pts',(-226.437752890236,-5.33893012607006,
133.359440227836));
#165847=CARTESIAN_POINT('Ctrl Pts',(-226.430381219534,-5.40295766920539,
133.215994708235));
#165848=CARTESIAN_POINT('Ctrl Pts',(-226.423008214756,-5.46699679962502,
133.072523228805));
#165849=CARTESIAN_POINT('Ctrl Pts',(-226.415635209978,-5.5253033342825,
132.926530512276));
#165850=CARTESIAN_POINT('Ctrl Pts',(-226.4082622052,-5.57768992328781,132.778520105083));
#165851=CARTESIAN_POINT('Ctrl Pts',(-226.400886384224,-5.63009652191107,
132.630453163733));
#165852=CARTESIAN_POINT('Ctrl Pts',(-226.393510563247,-5.67657854823874,
132.480367351838));
#165853=CARTESIAN_POINT('Ctrl Pts',(-226.386134742271,-5.71699845977709,
132.328781548086));
#165854=CARTESIAN_POINT('Ctrl Pts',(-226.37875079904,-5.75746288172915,
132.17702881802));
#165855=CARTESIAN_POINT('Ctrl Pts',(-226.371366855808,-5.79185176377396,
132.023773161657));
#165856=CARTESIAN_POINT('Ctrl Pts',(-226.363982912577,-5.82007851800152,
131.869544454656));
#165857=CARTESIAN_POINT('Ctrl Pts',(-226.356594167713,-5.84832362752866,
131.715215455779));
#165858=CARTESIAN_POINT('Ctrl Pts',(-226.349205422849,-5.87039857370088,
131.559912516861));
#165859=CARTESIAN_POINT('Ctrl Pts',(-226.341816677986,-5.88626868280649,
131.404170217616));
#165860=CARTESIAN_POINT('Ctrl Pts',(-226.334417907912,-5.90216032482148,
131.24821660383));
#165861=CARTESIAN_POINT('Ctrl Pts',(-226.327019137838,-5.91183030008091,
131.091822813332));
#165862=CARTESIAN_POINT('Ctrl Pts',(-226.319620367765,-5.91529600517794,
130.935523621595));
#165863=CARTESIAN_POINT('Ctrl Pts',(-226.31753864258,-5.91627111935416,
130.891547128117));
#165864=CARTESIAN_POINT('Ctrl Pts',(-226.315456917394,-5.91675539410002,
130.847578092369));
#165865=CARTESIAN_POINT('Ctrl Pts',(-226.313375192209,-5.91674995468472,
130.803628334572));
#165866=CARTESIAN_POINT('',(-224.563375192209,-5.91483159952414,130.809774239277));
#165867=CARTESIAN_POINT('Ctrl Pts',(-226.313375192209,-5.92642165134677,
130.80362713756));
#165868=CARTESIAN_POINT('Ctrl Pts',(-226.311529301019,-5.92648962768387,
130.76459263781));
#165869=CARTESIAN_POINT('Ctrl Pts',(-226.30968340983,-5.92613747701628,
130.725559397462));
#165870=CARTESIAN_POINT('Ctrl Pts',(-226.30783751864,-5.92536146718798,
130.686534585569));
#165871=CARTESIAN_POINT('Ctrl Pts',(-226.215021644036,-5.88634181569524,
128.724272634618));
#165872=CARTESIAN_POINT('Ctrl Pts',(-226.029389894828,-3.66499790132608,
124.842368424212));
#165873=CARTESIAN_POINT('Ctrl Pts',(-225.750942271015,3.03497199644419,
124.498291674782));
#165874=CARTESIAN_POINT('Ctrl Pts',(-225.472494647202,6.94595089610799,
129.949184215175));
#165875=CARTESIAN_POINT('Ctrl Pts',(-225.194047023389,4.47394025081266,
136.185942091678));
#165876=CARTESIAN_POINT('Ctrl Pts',(-224.915599399576,-2.10940292084664,
137.477289498338));
#165877=CARTESIAN_POINT('Ctrl Pts',(-224.705375455848,-5.61623921853537,
133.822594326139));
#165878=CARTESIAN_POINT('Ctrl Pts',(-224.587967386727,-5.91948652701702,
131.332466920396));
#165879=CARTESIAN_POINT('Ctrl Pts',(-224.563375192209,-5.91483159952414,
130.809774239277));
#165880=CARTESIAN_POINT('',(-222.813375192209,-5.90733561507725,130.802750946968));
#165881=CARTESIAN_POINT('Ctrl Pts',(-224.563375192209,-5.91483159952414,
130.809774239277));
#165882=CARTESIAN_POINT('Ctrl Pts',(-224.495151512123,-5.90191789701304,
129.359719904591));
#165883=CARTESIAN_POINT('Ctrl Pts',(-224.334111957431,-4.63296812933935,
125.916704457217));
#165884=CARTESIAN_POINT('Ctrl Pts',(-224.080256528137,1.14114131736879,
123.899626225559));
#165885=CARTESIAN_POINT('Ctrl Pts',(-223.801808904323,6.42596335219761,
128.032257530277));
#165886=CARTESIAN_POINT('Ctrl Pts',(-223.523361280512,5.80563899211914,
134.712316147447));
#165887=CARTESIAN_POINT('Ctrl Pts',(-223.244913656698,-0.149783980485487,
137.801154546898));
#165888=CARTESIAN_POINT('Ctrl Pts',(-223.008251627265,-5.09451046644834,
134.961633525739));
#165889=CARTESIAN_POINT('Ctrl Pts',(-222.864405472434,-5.90469612405182,
131.890837229664));
#165890=CARTESIAN_POINT('Ctrl Pts',(-222.813375192209,-5.90733561507725,
130.802750946968));
#165891=CARTESIAN_POINT('',(-221.063375192209,-5.92075521056039,130.799502985017));
#165892=CARTESIAN_POINT('Ctrl Pts',(-222.813375192209,-5.90733561507725,
130.802750946968));
#165893=CARTESIAN_POINT('Ctrl Pts',(-222.77158959783,-5.90949693382502,
129.911783234133));
#165894=CARTESIAN_POINT('Ctrl Pts',(-222.636988128846,-5.30138420352635,
127.044562818406));
#165895=CARTESIAN_POINT('Ctrl Pts',(-222.40957078526,-0.844604857256582,
123.857116331848));
#165896=CARTESIAN_POINT('Ctrl Pts',(-222.131123161446,5.38838381779271,
126.338615398399));
#165897=CARTESIAN_POINT('Ctrl Pts',(-221.852675537634,6.66971100146858,
132.923916157578));
#165898=CARTESIAN_POINT('Ctrl Pts',(-221.574227913821,1.821899608298,137.561448921536));
#165899=CARTESIAN_POINT('Ctrl Pts',(-221.311127798679,-4.3406655091924,
136.076187875004));
#165900=CARTESIAN_POINT('Ctrl Pts',(-221.140843558142,-5.90619376265546,
132.441826029179));
#165901=CARTESIAN_POINT('Ctrl Pts',(-221.063375192209,-5.92075521056039,
130.799502985017));
#165902=CARTESIAN_POINT('',(-219.313375192209,-5.92045153616181,130.808269674344));
#165903=CARTESIAN_POINT('Ctrl Pts',(-221.063375192209,-5.92075521056039,
130.799502985017));
#165904=CARTESIAN_POINT('Ctrl Pts',(-221.048027683538,-5.92364002612731,
130.474137051998));
#165905=CARTESIAN_POINT('Ctrl Pts',(-221.032680174866,-5.89914275629101,
130.149205902182));
#165906=CARTESIAN_POINT('Ctrl Pts',(-220.924516791591,-5.52276673404195,
127.893203873355));
#165907=CARTESIAN_POINT('Ctrl Pts',(-220.738885042383,-2.76232065490982,
124.374186037525));
#165908=CARTESIAN_POINT('Ctrl Pts',(-220.46043741857,3.91678619878236,125.004675591346));
#165909=CARTESIAN_POINT('Ctrl Pts',(-220.181989794757,6.99655788143963,
130.964792353897));
#165910=CARTESIAN_POINT('Ctrl Pts',(-219.903542170944,3.64683467190507,
136.777480188288));
#165911=CARTESIAN_POINT('Ctrl Pts',(-219.625094547131,-3.05415144333025,
137.101162940295));
#165912=CARTESIAN_POINT('Ctrl Pts',(-219.428372220886,-5.80551108210207,
133.241733301106));
#165913=CARTESIAN_POINT('Ctrl Pts',(-219.324465769245,-5.92499839058684,
131.043137371517));
#165914=CARTESIAN_POINT('Ctrl Pts',(-219.313375192209,-5.92320801574442,
130.808271494346));
#165915=CARTESIAN_POINT('',(-217.563375219359,-5.91209744554343,130.80733573345));
#165916=CARTESIAN_POINT('Ctrl Pts',(-219.313375192209,-5.91674871030393,
130.808267229504));
#165917=CARTESIAN_POINT('Ctrl Pts',(-219.306059579814,-5.91685088830008,
130.653513817441));
#165918=CARTESIAN_POINT('Ctrl Pts',(-219.298743967419,-5.91087751960387,
130.498520301917));
#165919=CARTESIAN_POINT('Ctrl Pts',(-219.291428355024,-5.89879859397009,
130.343811260519));
#165920=CARTESIAN_POINT('Ctrl Pts',(-219.284120305473,-5.88673215546926,
130.189262156555));
#165921=CARTESIAN_POINT('Ctrl Pts',(-219.276812255921,-5.86857274844675,
130.034997321644));
#165922=CARTESIAN_POINT('Ctrl Pts',(-219.26950420637,-5.84434236784582,
129.88154273201));
#165923=CARTESIAN_POINT('Ctrl Pts',(-219.26220201398,-5.82013140710079,
129.7282111312));
#165924=CARTESIAN_POINT('Ctrl Pts',(-219.254899821591,-5.78985921545387,
129.575688861118));
#165925=CARTESIAN_POINT('Ctrl Pts',(-219.247597629202,-5.75359969604657,
129.424497906948));
#165926=CARTESIAN_POINT('Ctrl Pts',(-219.240122698798,-5.71648243459886,
129.269730434402));
#165927=CARTESIAN_POINT('Ctrl Pts',(-219.232647768394,-5.67309107105576,
129.116358458185));
#165928=CARTESIAN_POINT('Ctrl Pts',(-219.22517283799,-5.62356073441339,
128.964932655165));
#165929=CARTESIAN_POINT('Ctrl Pts',(-219.217876340133,-5.57521272639103,
128.817121506776));
#165930=CARTESIAN_POINT('Ctrl Pts',(-219.210579842277,-5.52101564217927,
128.67116505339));
#165931=CARTESIAN_POINT('Ctrl Pts',(-219.20328334442,-5.46114590788245,
128.527561123689));
#165932=CARTESIAN_POINT('Ctrl Pts',(-219.195987218609,-5.40127922631816,
128.383964516292));
#165933=CARTESIAN_POINT('Ctrl Pts',(-219.188691092798,-5.33574061779488,
128.242720548933));
#165934=CARTESIAN_POINT('Ctrl Pts',(-219.181394966987,-5.26475475767799,
128.104307302536));
#165935=CARTESIAN_POINT('Ctrl Pts',(-219.174097680021,-5.19375760038916,
127.965872028114));
#165936=CARTESIAN_POINT('Ctrl Pts',(-219.166800393055,-5.11731164224933,
127.830268713036));
#165937=CARTESIAN_POINT('Ctrl Pts',(-219.159503106089,-5.03568748843877,
127.697950779621));
#165938=CARTESIAN_POINT('Ctrl Pts',(-219.15189445554,-4.95058056232268,
127.559987051272));
#165939=CARTESIAN_POINT('Ctrl Pts',(-219.144285804991,-4.85984404607919,
127.425595645752));
#165940=CARTESIAN_POINT('Ctrl Pts',(-219.136677154443,-4.76383411652442,
127.295256020559));
#165941=CARTESIAN_POINT('Ctrl Pts',(-219.129369107119,-4.67161735558365,
127.170065864569));
#165942=CARTESIAN_POINT('Ctrl Pts',(-219.122061059795,-4.57453618848797,
127.048613716132));
#165943=CARTESIAN_POINT('Ctrl Pts',(-219.114753012472,-4.47294624763622,
126.931289171251));
#165944=CARTESIAN_POINT('Ctrl Pts',(-219.10744011649,-4.37128890507438,
126.813886785249));
#165945=CARTESIAN_POINT('Ctrl Pts',(-219.100127220508,-4.26511709451247,
126.700617734469));
#165946=CARTESIAN_POINT('Ctrl Pts',(-219.092814324526,-4.15482222848972,
126.591833726002));
#165947=CARTESIAN_POINT('Ctrl Pts',(-219.085491833986,-4.04438265502116,
126.482906992342));
#165948=CARTESIAN_POINT('Ctrl Pts',(-219.078169343447,-3.92980951568913,
126.378477298318));
#165949=CARTESIAN_POINT('Ctrl Pts',(-219.070846852907,-3.81152636629467,
126.278855416868));
#165950=CARTESIAN_POINT('Ctrl Pts',(-219.069964335106,-3.79727069955119,
126.266848834785));
#165951=CARTESIAN_POINT('Ctrl Pts',(-219.069081817305,-3.78296117632481,
126.254912035624));
#165952=CARTESIAN_POINT('Ctrl Pts',(-219.068199299505,-3.76859856456568,
126.24304551974));
#165953=CARTESIAN_POINT('Ctrl Pts',(-219.060776033099,-3.64778797777036,
126.143230752679));
#165954=CARTESIAN_POINT('Ctrl Pts',(-219.053352766694,-3.52282644481948,
126.048068037059));
#165955=CARTESIAN_POINT('Ctrl Pts',(-219.045929500288,-3.39410781351939,
125.957922470565));
#165956=CARTESIAN_POINT('Ctrl Pts',(-219.038515007567,-3.26554131695244,
125.867883448644));
#165957=CARTESIAN_POINT('Ctrl Pts',(-219.031100514847,-3.13322686381598,
125.782849984492));
#165958=CARTESIAN_POINT('Ctrl Pts',(-219.023686022126,-2.99759256841364,
125.703148079719));
#165959=CARTESIAN_POINT('Ctrl Pts',(-219.016278675772,-2.86208900245175,
125.623522994642));
#165960=CARTESIAN_POINT('Ctrl Pts',(-219.008871329418,-2.7232722840575,
125.549219426543));
#165961=CARTESIAN_POINT('Ctrl Pts',(-219.001463983064,-2.58160071376054,
125.480520995901));
#165962=CARTESIAN_POINT('Ctrl Pts',(-218.994062161389,-2.44003480746567,
125.41187380314));
#165963=CARTESIAN_POINT('Ctrl Pts',(-218.986660339714,-2.29561862334915,
125.348823586028));
#165964=CARTESIAN_POINT('Ctrl Pts',(-218.979258518039,-2.14883625177907,
125.291608734383));
#165965=CARTESIAN_POINT('Ctrl Pts',(-218.971860603727,-2.00213136547997,
125.234424086012));
#165966=CARTESIAN_POINT('Ctrl Pts',(-218.964462689416,-1.85306312628229,
125.183068803489));
#165967=CARTESIAN_POINT('Ctrl Pts',(-218.957064775104,-1.70213674865009,
125.13773366219));
#165968=CARTESIAN_POINT('Ctrl Pts',(-218.949668090192,-1.55123545224399,
125.092406054769));
#165969=CARTESIAN_POINT('Ctrl Pts',(-218.94227140528,-1.39847698742511,
125.053096710286));
#165970=CARTESIAN_POINT('Ctrl Pts',(-218.934874720368,-1.24438303325878,
125.019946954191));
#165971=CARTESIAN_POINT('Ctrl Pts',(-218.927478363433,-1.09029591177985,
124.986798667991));
#165972=CARTESIAN_POINT('Ctrl Pts',(-218.920082006497,-0.934873783645096,
124.95980950563));
#165973=CARTESIAN_POINT('Ctrl Pts',(-218.912685649562,-0.778649595254036,
124.939069885615));
#165974=CARTESIAN_POINT('Ctrl Pts',(-218.905288160225,-0.622401488541358,
124.918327090311));
#165975=CARTESIAN_POINT('Ctrl Pts',(-218.897890670889,-0.465351447141299,
124.90383579164));
#165976=CARTESIAN_POINT('Ctrl Pts',(-218.890493181552,-0.308038481718682,
124.895634624911));
#165977=CARTESIAN_POINT('Ctrl Pts',(-218.883093099037,-0.150670370479677,
124.887430583275));
#165978=CARTESIAN_POINT('Ctrl Pts',(-218.875693016523,0.00696047572782896,
124.885521083135));
#165979=CARTESIAN_POINT('Ctrl Pts',(-218.868292934008,0.164314247561687,
124.889892645673));
#165980=CARTESIAN_POINT('Ctrl Pts',(-218.860884714341,0.321841046044711,
124.894269015194));
#165981=CARTESIAN_POINT('Ctrl Pts',(-218.853476494675,0.479089788321696,
124.904940230102));
#165982=CARTESIAN_POINT('Ctrl Pts',(-218.846068275008,0.635524253120782,
124.921840793018));
#165983=CARTESIAN_POINT('Ctrl Pts',(-218.838655495706,0.792055000722703,
124.93875175795));
#165984=CARTESIAN_POINT('Ctrl Pts',(-218.831242716404,0.947770103810021,
124.961899655972));
#165985=CARTESIAN_POINT('Ctrl Pts',(-218.823829937102,1.1021432588565,124.991167794387));
#165986=CARTESIAN_POINT('Ctrl Pts',(-218.816406566073,1.25673698950607,
125.020477752491));
#165987=CARTESIAN_POINT('Ctrl Pts',(-218.808983195045,1.4099845798288,125.055925332584));
#165988=CARTESIAN_POINT('Ctrl Pts',(-218.801559824016,1.56137381127563,
125.097343674892));
#165989=CARTESIAN_POINT('Ctrl Pts',(-218.797623774575,1.64164401433556,
125.119304673807));
#165990=CARTESIAN_POINT('Ctrl Pts',(-218.793687725133,1.72139207092731,
125.142943452068));
#165991=CARTESIAN_POINT('Ctrl Pts',(-218.789751675692,1.80054399766364,
125.168229686246));
#165992=CARTESIAN_POINT('Ctrl Pts',(-218.782328409287,1.94982206121864,
125.215918734743));
#165993=CARTESIAN_POINT('Ctrl Pts',(-218.774905142881,2.09742990993292,
125.269614639238));
#165994=CARTESIAN_POINT('Ctrl Pts',(-218.767481876476,2.24284749242479,
125.329183388633));
#165995=CARTESIAN_POINT('Ctrl Pts',(-218.760067383755,2.38809320341033,
125.388681732714));
#165996=CARTESIAN_POINT('Ctrl Pts',(-218.752652891034,2.53115345895547,
125.454038965045));
#165997=CARTESIAN_POINT('Ctrl Pts',(-218.745238398313,2.67152257843374,
125.525071112773));
#165998=CARTESIAN_POINT('Ctrl Pts',(-218.737831051959,2.81175640486985,
125.596034797042));
#165999=CARTESIAN_POINT('Ctrl Pts',(-218.730423705605,2.94930392817718,
125.672662340198));
#166000=CARTESIAN_POINT('Ctrl Pts',(-218.723016359252,3.08367880778335,
125.754721464822));
#166001=CARTESIAN_POINT('Ctrl Pts',(-218.715614537576,3.21795346553502,
125.836719386655));
#166002=CARTESIAN_POINT('Ctrl Pts',(-218.708212715901,3.34905987394385,
125.924140629995));
#166003=CARTESIAN_POINT('Ctrl Pts',(-218.700810894226,3.47653580623464,
126.016706771425));
#166004=CARTESIAN_POINT('Ctrl Pts',(-218.693412979915,3.60394444497268,
126.10922404791));
#166005=CARTESIAN_POINT('Ctrl Pts',(-218.686015065603,3.72772612309777,
126.206880594752));
#166006=CARTESIAN_POINT('Ctrl Pts',(-218.678617151292,3.84744725512211,
126.309354479466));
#166007=CARTESIAN_POINT('Ctrl Pts',(-218.67122046638,3.96714849166643,126.411811334881));
#166008=CARTESIAN_POINT('Ctrl Pts',(-218.663823781468,4.08279023804669,
126.5190836968));
#166009=CARTESIAN_POINT('Ctrl Pts',(-218.656427096556,4.1939716128804,126.630809051711));
#166010=CARTESIAN_POINT('Ctrl Pts',(-218.64903073962,4.30514805781513,126.742529452602));
#166011=CARTESIAN_POINT('Ctrl Pts',(-218.641634382685,4.41186426113564,
126.858702189282));
#166012=CARTESIAN_POINT('Ctrl Pts',(-218.63423802575,4.51375608064432,126.978927752262));
#166013=CARTESIAN_POINT('Ctrl Pts',(-218.626840536413,4.61566350005128,
127.099171722084));
#166014=CARTESIAN_POINT('Ctrl Pts',(-218.619443047076,4.71274482357616,
127.223469468902));
#166015=CARTESIAN_POINT('Ctrl Pts',(-218.61204555774,4.80467619780906,127.351388391106));
#166016=CARTESIAN_POINT('Ctrl Pts',(-218.604645475225,4.89663979844203,
127.479352155088));
#166017=CARTESIAN_POINT('Ctrl Pts',(-218.59724539271,4.98344963771258,127.610939318872));
#166018=CARTESIAN_POINT('Ctrl Pts',(-218.589845310195,5.06482527559572,
127.745688439939));
#166019=CARTESIAN_POINT('Ctrl Pts',(-218.582437090529,5.14629039435869,
127.880585731519));
#166020=CARTESIAN_POINT('Ctrl Pts',(-218.575028870862,5.22230918524685,
128.018651604228));
#166021=CARTESIAN_POINT('Ctrl Pts',(-218.567620651196,5.29264691236428,
128.159399516994));
#166022=CARTESIAN_POINT('Ctrl Pts',(-218.560207871894,5.36302793117911,
128.300234057751));
#166023=CARTESIAN_POINT('Ctrl Pts',(-218.552795092592,5.42772076576185,
128.443753588359));
#166024=CARTESIAN_POINT('Ctrl Pts',(-218.54538231329,5.48653911307297,128.589452239501));
#166025=CARTESIAN_POINT('Ctrl Pts',(-218.537958942261,5.54544150279695,
128.735359071709));
#166026=CARTESIAN_POINT('Ctrl Pts',(-218.530535571233,5.59845251558682,
128.883450892541));
#166027=CARTESIAN_POINT('Ctrl Pts',(-218.523112200204,5.64543566865914,
129.033206566239));
#166028=CARTESIAN_POINT('Ctrl Pts',(-218.519176150762,5.67034726376772,
129.112610617786));
#166029=CARTESIAN_POINT('Ctrl Pts',(-218.515240101321,5.69356506267462,
129.19248225344));
#166030=CARTESIAN_POINT('Ctrl Pts',(-218.51130405188,5.71507458751184,129.272742838329));
#166031=CARTESIAN_POINT('Ctrl Pts',(-218.503880785474,5.75564088005899,
129.424111796556));
#166032=CARTESIAN_POINT('Ctrl Pts',(-218.496457519069,5.79025064261305,
129.577322408127));
#166033=CARTESIAN_POINT('Ctrl Pts',(-218.489034252663,5.81873552203086,
129.731864702816));
#166034=CARTESIAN_POINT('Ctrl Pts',(-218.481619759942,5.84718673468681,
129.886224341346));
#166035=CARTESIAN_POINT('Ctrl Pts',(-218.474205267221,5.86952740667652,
130.04191216653));
#166036=CARTESIAN_POINT('Ctrl Pts',(-218.4667907745,5.88563898684256,130.198403293112));
#166037=CARTESIAN_POINT('Ctrl Pts',(-218.459383428146,5.90173503806099,
130.354743587655));
#166038=CARTESIAN_POINT('Ctrl Pts',(-218.451976081792,5.91161391193149,
130.511885273371));
#166039=CARTESIAN_POINT('Ctrl Pts',(-218.444568735438,5.9152081510659,130.669293626545));
#166040=CARTESIAN_POINT('Ctrl Pts',(-218.437166913763,5.91879970948117,
130.82658457863));
#166041=CARTESIAN_POINT('Ctrl Pts',(-218.429765092087,5.91611595775744,
130.984141430561));
#166042=CARTESIAN_POINT('Ctrl Pts',(-218.422363270412,5.90714129653777,
131.141424803201));
#166043=CARTESIAN_POINT('Ctrl Pts',(-218.414965356101,5.8981713729719,131.298625147174));
#166044=CARTESIAN_POINT('Ctrl Pts',(-218.407567441789,5.8829171748978,131.455551927624));
#166045=CARTESIAN_POINT('Ctrl Pts',(-218.400169527478,5.86141518968541,
131.611666344429));
#166046=CARTESIAN_POINT('Ctrl Pts',(-218.392772842565,5.83991677771291,
131.767754817849));
#166047=CARTESIAN_POINT('Ctrl Pts',(-218.385376157653,5.81217269014303,
131.923030826115));
#166048=CARTESIAN_POINT('Ctrl Pts',(-218.377979472741,5.7782712336825,132.076961148957));
#166049=CARTESIAN_POINT('Ctrl Pts',(-218.370583115805,5.74437128044807,
132.230884646367));
#166050=CARTESIAN_POINT('Ctrl Pts',(-218.36318675887,5.70431458147778,132.383462212435));
#166051=CARTESIAN_POINT('Ctrl Pts',(-218.355790401934,5.65824042766622,
132.534171539379));
#166052=CARTESIAN_POINT('Ctrl Pts',(-218.348392912598,5.61215921978409,
132.684903940306));
#166053=CARTESIAN_POINT('Ctrl Pts',(-218.340995423261,5.56005883179809,
132.83376717557));
#166054=CARTESIAN_POINT('Ctrl Pts',(-218.333597933924,5.50212817301582,
132.980254946389));
#166055=CARTESIAN_POINT('Ctrl Pts',(-218.326197851409,5.44417720673067,
133.12679406827));
#166056=CARTESIAN_POINT('Ctrl Pts',(-218.318797768894,5.38039203766882,
133.270955720853));
#166057=CARTESIAN_POINT('Ctrl Pts',(-218.311397686379,5.31100930580515,
133.412254541051));
#166058=CARTESIAN_POINT('Ctrl Pts',(-218.303989466712,5.24155028049538,
133.553708733827));
#166059=CARTESIAN_POINT('Ctrl Pts',(-218.296581247046,5.16648156489098,
133.692293472212));
#166060=CARTESIAN_POINT('Ctrl Pts',(-218.28917302738,5.08608561929285,133.827548278913));
#166061=CARTESIAN_POINT('Ctrl Pts',(-218.281760248077,5.00564019133123,
133.962886332692));
#166062=CARTESIAN_POINT('Ctrl Pts',(-218.274347468775,4.91986120284593,
134.094890058577));
#166063=CARTESIAN_POINT('Ctrl Pts',(-218.266934689473,4.82907355467608,
134.223129279823));
#166064=CARTESIAN_POINT('Ctrl Pts',(-218.259511318444,4.73815618485739,
134.351551735281));
#166065=CARTESIAN_POINT('Ctrl Pts',(-218.252087947416,4.64221608908989,
134.476198648195));
#166066=CARTESIAN_POINT('Ctrl Pts',(-218.244664576387,4.54161794136622,
134.596673505127));
#166067=CARTESIAN_POINT('Ctrl Pts',(-218.240728526946,4.48827838963088,
134.660552165018));
#166068=CARTESIAN_POINT('Ctrl Pts',(-218.236792477506,4.43362990792399,
134.723258526826));
#166069=CARTESIAN_POINT('Ctrl Pts',(-218.232856428066,4.3777308283501,134.784737905841));
#166070=CARTESIAN_POINT('Ctrl Pts',(-218.22543316166,4.27230690881088,134.900686095971));
#166071=CARTESIAN_POINT('Ctrl Pts',(-218.218009895255,4.16211390419733,
135.012618347338));
#166072=CARTESIAN_POINT('Ctrl Pts',(-218.21058662885,4.04748986791888,135.12011736831));
#166073=CARTESIAN_POINT('Ctrl Pts',(-218.203172136129,3.93300130773237,
135.227489334366));
#166074=CARTESIAN_POINT('Ctrl Pts',(-218.195757643408,3.81409241000973,
135.33043824683));
#166075=CARTESIAN_POINT('Ctrl Pts',(-218.188343150687,3.6911406957847,135.428580651953));
#166076=CARTESIAN_POINT('Ctrl Pts',(-218.180935804333,3.56830748704985,
135.526628463731));
#166077=CARTESIAN_POINT('Ctrl Pts',(-218.173528457979,3.44143950900474,
135.619878759632));
#166078=CARTESIAN_POINT('Ctrl Pts',(-218.166121111625,3.31095017748968,
135.707985754613));
#166079=CARTESIAN_POINT('Ctrl Pts',(-218.15871928995,3.18055816984189,135.796027036073));
#166080=CARTESIAN_POINT('Ctrl Pts',(-218.151317468274,3.04655049471087,
135.878932446748));
#166081=CARTESIAN_POINT('Ctrl Pts',(-218.143915646599,2.90937251520491,
135.956397314861));
#166082=CARTESIAN_POINT('Ctrl Pts',(-218.136517732288,2.77226695088732,
136.033821289872));
#166083=CARTESIAN_POINT('Ctrl Pts',(-218.129119817976,2.63199473943562,
136.105810258993));
#166084=CARTESIAN_POINT('Ctrl Pts',(-218.121721903665,2.489028910967,136.172103685455));
#166085=CARTESIAN_POINT('Ctrl Pts',(-218.114325218753,2.34608684082479,
136.238386095153));
#166086=CARTESIAN_POINT('Ctrl Pts',(-218.106928533841,2.2004523804078,136.298974683822));
#166087=CARTESIAN_POINT('Ctrl Pts',(-218.099531848929,2.0526218749625,136.353655527816));
#166088=CARTESIAN_POINT('Ctrl Pts',(-218.092135491993,1.90479792447631,
136.408333947204));
#166089=CARTESIAN_POINT('Ctrl Pts',(-218.084739135058,1.75477847269028,
136.45710501327));
#166090=CARTESIAN_POINT('Ctrl Pts',(-218.077342778122,1.60307824206378,
136.499803595274));
#166091=CARTESIAN_POINT('Ctrl Pts',(-218.069945288786,1.45135478574513,
136.54250871454));
#166092=CARTESIAN_POINT('Ctrl Pts',(-218.062547799449,1.29795039756308,
136.579139397415));
#166093=CARTESIAN_POINT('Ctrl Pts',(-218.055150310113,1.14339315111778,
136.609580911791));
#166094=CARTESIAN_POINT('Ctrl Pts',(-218.047750227598,0.988781724870436,
136.640033097392));
#166095=CARTESIAN_POINT('Ctrl Pts',(-218.040350145083,0.833017001767469,
136.664291722736));
#166096=CARTESIAN_POINT('Ctrl Pts',(-218.032950062568,0.676635241207233,
136.682293529131));
#166097=CARTESIAN_POINT('Ctrl Pts',(-218.025541842902,0.520081522823261,
136.700315130363));
#166098=CARTESIAN_POINT('Ctrl Pts',(-218.018133623235,0.362909783057131,
136.712066130087));
#166099=CARTESIAN_POINT('Ctrl Pts',(-218.010725403569,0.205660111188952,
136.717535270928));
#166100=CARTESIAN_POINT('Ctrl Pts',(-218.003312624267,0.048313654771591,
136.723007777935));
#166101=CARTESIAN_POINT('Ctrl Pts',(-217.995899844964,-0.10911045689851,
136.722190723747));
#166102=CARTESIAN_POINT('Ctrl Pts',(-217.988487065662,-0.266074687102465,
136.715124935603));
#166103=CARTESIAN_POINT('Ctrl Pts',(-217.981063694634,-0.423263195158757,
136.70804905153));
#166104=CARTESIAN_POINT('Ctrl Pts',(-217.973640323605,-0.579990138405261,
136.694706632897));
#166105=CARTESIAN_POINT('Ctrl Pts',(-217.966216952576,-0.735724803657198,
136.675190165065));
#166106=CARTESIAN_POINT('Ctrl Pts',(-217.962280903136,-0.818299059977332,
136.664842065528));
#166107=CARTESIAN_POINT('Ctrl Pts',(-217.958344853695,-0.900594537340759,
136.652759070387));
#166108=CARTESIAN_POINT('Ctrl Pts',(-217.954408804254,-0.982533698024718,
136.63896069767));
#166109=CARTESIAN_POINT('Ctrl Pts',(-217.946985537848,-1.13706839784008,
136.612937397358));
#166110=CARTESIAN_POINT('Ctrl Pts',(-217.939562271443,-1.29080218161052,
136.580731017709));
#166111=CARTESIAN_POINT('Ctrl Pts',(-217.932139005037,-1.44320124394244,
136.542400416311));
#166112=CARTESIAN_POINT('Ctrl Pts',(-217.924724512316,-1.59542018323864,
136.504115118501));
#166113=CARTESIAN_POINT('Ctrl Pts',(-217.917310019595,-1.74630718269074,
136.459720097024));
#166114=CARTESIAN_POINT('Ctrl Pts',(-217.909895526874,-1.89533557246087,
136.409325704903));
#166115=CARTESIAN_POINT('Ctrl Pts',(-217.90248818052,-2.04422032305855,
136.358979884794));
#166116=CARTESIAN_POINT('Ctrl Pts',(-217.895080834166,-2.19124967904206,
136.302646324475));
#166117=CARTESIAN_POINT('Ctrl Pts',(-217.887673487812,-2.3359092603034,
136.240485937141));
#166118=CARTESIAN_POINT('Ctrl Pts',(-217.880271666137,-2.48046094899051,
136.17837191137));
#166119=CARTESIAN_POINT('Ctrl Pts',(-217.872869844462,-2.62264604072322,
136.110439858534));
#166120=CARTESIAN_POINT('Ctrl Pts',(-217.865468022786,-2.76196747686731,
136.036899792692));
#166121=CARTESIAN_POINT('Ctrl Pts',(-217.858070108475,-2.90121536631092,
135.963398548077));
#166122=CARTESIAN_POINT('Ctrl Pts',(-217.850672194163,-3.03760228149763,
135.884295360104));
#166123=CARTESIAN_POINT('Ctrl Pts',(-217.843274279852,-3.17065334113184,
135.799847375918));
#166124=CARTESIAN_POINT('Ctrl Pts',(-217.835877594939,-3.30368229009316,
135.715413425455));
#166125=CARTESIAN_POINT('Ctrl Pts',(-217.828480910027,-3.4333761688747,
135.625636641457));
#166126=CARTESIAN_POINT('Ctrl Pts',(-217.821084225115,-3.55928671072393,
135.530818982279));
#166127=CARTESIAN_POINT('Ctrl Pts',(-217.813687868179,-3.68519166956814,
135.436005527415));
#166128=CARTESIAN_POINT('Ctrl Pts',(-217.806291511244,-3.80731332683775,
135.336151866362));
#166129=CARTESIAN_POINT('Ctrl Pts',(-217.798895154308,-3.92523453330316,
135.231601792504));
#166130=CARTESIAN_POINT('Ctrl Pts',(-217.791497664971,-4.04317379380565,
135.127035711763));
#166131=CARTESIAN_POINT('Ctrl Pts',(-217.784100175635,-4.15691104366667,
135.017772034194));
#166132=CARTESIAN_POINT('Ctrl Pts',(-217.776702686298,-4.2660643188342,
134.904193027564));
#166133=CARTESIAN_POINT('Ctrl Pts',(-217.769302603783,-4.37525585751267,
134.79057420599));
#166134=CARTESIAN_POINT('Ctrl Pts',(-217.761902521268,-4.47985996365709,
134.672637312503));
#166135=CARTESIAN_POINT('Ctrl Pts',(-217.754502438753,-4.579533554635,134.550799324454));
#166136=CARTESIAN_POINT('Ctrl Pts',(-217.747094219086,-4.67931674697361,
134.428827363012));
#166137=CARTESIAN_POINT('Ctrl Pts',(-217.73968599942,-4.77415836032364,
134.302946029394));
#166138=CARTESIAN_POINT('Ctrl Pts',(-217.732277779753,-4.86375699208932,
134.173603631123));
#166139=CARTESIAN_POINT('Ctrl Pts',(-217.724865000451,-4.95341077031833,
134.044181624763));
#166140=CARTESIAN_POINT('Ctrl Pts',(-217.717452221149,-5.03781493714544,
133.911294623383));
#166141=CARTESIAN_POINT('Ctrl Pts',(-217.710039441847,-5.11671328995648,
133.775416939968));
#166142=CARTESIAN_POINT('Ctrl Pts',(-217.702616070818,-5.19572437643342,
133.639345108147));
#166143=CARTESIAN_POINT('Ctrl Pts',(-217.695192699789,-5.26921376285336,
133.500274388875));
#166144=CARTESIAN_POINT('Ctrl Pts',(-217.68776932876,-5.33697239632939,
133.358701276781));
#166145=CARTESIAN_POINT('Ctrl Pts',(-217.68383327932,-5.37289964963588,
133.283635815766));
#166146=CARTESIAN_POINT('Ctrl Pts',(-217.67989722988,-5.40721659929989,
133.207867145932));
#166147=CARTESIAN_POINT('Ctrl Pts',(-217.67596118044,-5.43989775535981,
133.131471051931));
#166148=CARTESIAN_POINT('Ctrl Pts',(-217.66772328069,-5.50829732488929,
132.971578913055));
#166149=CARTESIAN_POINT('Ctrl Pts',(-217.65948538094,-5.56970530852338,
132.808524925761));
#166150=CARTESIAN_POINT('Ctrl Pts',(-217.65124748119,-5.62384937071369,
132.642905916987));
#166151=CARTESIAN_POINT('Ctrl Pts',(-217.643042776513,-5.67777525641049,
132.47795427917));
#166152=CARTESIAN_POINT('Ctrl Pts',(-217.634838071835,-5.72449552927632,
132.310458456378));
#166153=CARTESIAN_POINT('Ctrl Pts',(-217.626633367158,-5.76378700476972,
132.141031828503));
#166154=CARTESIAN_POINT('Ctrl Pts',(-217.6184500779,-5.80297592405403,131.972047427662));
#166155=CARTESIAN_POINT('Ctrl Pts',(-217.610266788641,-5.83477465964333,
131.801142496242));
#166156=CARTESIAN_POINT('Ctrl Pts',(-217.602083499383,-5.85900923233826,
131.628946197039));
#166157=CARTESIAN_POINT('Ctrl Pts',(-217.59393521479,-5.88314013973657,
131.457486481091));
#166158=CARTESIAN_POINT('Ctrl Pts',(-217.585786930197,-5.89977136585755,
131.28474664181));
#166159=CARTESIAN_POINT('Ctrl Pts',(-217.577638645604,-5.90877981142748,
131.111365019109));
#166160=CARTESIAN_POINT('Ctrl Pts',(-217.572884181551,-5.91403617307598,
131.01019811911));
#166161=CARTESIAN_POINT('Ctrl Pts',(-217.568129717498,-5.91669817362437,
130.908813021326));
#166162=CARTESIAN_POINT('Ctrl Pts',(-217.563375253445,-5.91674925046863,
130.807338801387));
#166163=CARTESIAN_POINT('',(-215.813375157388,-5.91502029301215,130.799381620638));
#166164=CARTESIAN_POINT('Ctrl Pts',(-217.563375192209,-5.90839217088997,
130.807333289765));
#166165=CARTESIAN_POINT('Ctrl Pts',(-217.508087980348,-5.90305680765803,
129.629005570252));
#166166=CARTESIAN_POINT('Ctrl Pts',(-217.359984893885,-4.98979320465015,
126.464889769201));
#166167=CARTESIAN_POINT('Ctrl Pts',(-217.119065932814,0.171079120619924,
123.80805498781));
#166168=CARTESIAN_POINT('Ctrl Pts',(-216.840618309002,5.97866251551794,
127.16662023982));
#166169=CARTESIAN_POINT('Ctrl Pts',(-216.562170685189,6.2921471325479,133.868091185466));
#166170=CARTESIAN_POINT('Ctrl Pts',(-216.283723061376,0.823455923246531,
137.754143410778));
#166171=CARTESIAN_POINT('Ctrl Pts',(-216.034124563716,-4.7569552396461,
135.512749812486));
#166172=CARTESIAN_POINT('Ctrl Pts',(-215.87734194066,-5.90151798111243,
132.160438231407));
#166173=CARTESIAN_POINT('Ctrl Pts',(-215.813375192209,-5.91229507969721,
130.799384655716));
#166174=CARTESIAN_POINT('',(-214.063375192209,-5.92104864866457,130.803405895618));
#166175=CARTESIAN_POINT('Ctrl Pts',(-215.813375135314,-5.91674790344546,
130.799379696593));
#166176=CARTESIAN_POINT('Ctrl Pts',(-215.804563110474,-5.91658994349001,
130.611741860083));
#166177=CARTESIAN_POINT('Ctrl Pts',(-215.795751085635,-5.90750238473919,
130.424489465272));
#166178=CARTESIAN_POINT('Ctrl Pts',(-215.786939060796,-5.889617851042,130.238381703482));
#166179=CARTESIAN_POINT('Ctrl Pts',(-215.778062099627,-5.87160152516248,
130.050902502633));
#166180=CARTESIAN_POINT('Ctrl Pts',(-215.769185138457,-5.84465819380242,
129.864584895955));
#166181=CARTESIAN_POINT('Ctrl Pts',(-215.760308177288,-5.80897212291539,
129.680183835342));
#166182=CARTESIAN_POINT('Ctrl Pts',(-215.751359874733,-5.77299925413676,
129.494300800555));
#166183=CARTESIAN_POINT('Ctrl Pts',(-215.742411572178,-5.72814261072141,
129.310365266239));
#166184=CARTESIAN_POINT('Ctrl Pts',(-215.733463269623,-5.67463907513611,
129.129128714384));
#166185=CARTESIAN_POINT('Ctrl Pts',(-215.731251450999,-5.66141420754263,
129.084331125306));
#166186=CARTESIAN_POINT('Ctrl Pts',(-215.729039632374,-5.64766126993599,
129.039698330585));
#166187=CARTESIAN_POINT('Ctrl Pts',(-215.72682781375,-5.63338428331314,
128.995241473059));
#166188=CARTESIAN_POINT('Ctrl Pts',(-215.719404547345,-5.58546811424068,
128.846036156987));
#166189=CARTESIAN_POINT('Ctrl Pts',(-215.71198128094,-5.53154763790908,
128.698510195232));
#166190=CARTESIAN_POINT('Ctrl Pts',(-215.704558014535,-5.47175765669013,
128.553183434634));
#166191=CARTESIAN_POINT('Ctrl Pts',(-215.697143521814,-5.41203834226372,
128.408028438198));
#166192=CARTESIAN_POINT('Ctrl Pts',(-215.689729029094,-5.34646347226255,
128.265067810902));
#166193=CARTESIAN_POINT('Ctrl Pts',(-215.682314536373,-5.2752177888881,
128.124806952812));
#166194=CARTESIAN_POINT('Ctrl Pts',(-215.674907190019,-5.20404077478584,
127.984681283417));
#166195=CARTESIAN_POINT('Ctrl Pts',(-215.667499843666,-5.12720399645217,
127.847250533469));
#166196=CARTESIAN_POINT('Ctrl Pts',(-215.660092497313,-5.04494047116426,
127.713000689491));
#166197=CARTESIAN_POINT('Ctrl Pts',(-215.652690675638,-4.9627383011169,
127.57885097411));
#166198=CARTESIAN_POINT('Ctrl Pts',(-215.645288853963,-4.87511763737922,
127.447877757776));
#166199=CARTESIAN_POINT('Ctrl Pts',(-215.637887032288,-4.78235760647559,
127.320542843014));
#166200=CARTESIAN_POINT('Ctrl Pts',(-215.630489117977,-4.68964654287024,
127.193275147362));
#166201=CARTESIAN_POINT('Ctrl Pts',(-215.623091203666,-4.59180173447565,
127.069642229218));
#166202=CARTESIAN_POINT('Ctrl Pts',(-215.615693289355,-4.48914577324704,
126.95007718364));
#166203=CARTESIAN_POINT('Ctrl Pts',(-215.608296604443,-4.38650687157726,
126.830532007604));
#166204=CARTESIAN_POINT('Ctrl Pts',(-215.600899919531,-4.27905864683187,
126.715053645412));
#166205=CARTESIAN_POINT('Ctrl Pts',(-215.593503234619,-4.16716422217798,
126.604042426298));
#166206=CARTESIAN_POINT('Ctrl Pts',(-215.586106877684,-4.05527475904014,
126.493036129538));
#166207=CARTESIAN_POINT('Ctrl Pts',(-215.578710520749,-3.93893975299797,
126.386496844923));
#166208=CARTESIAN_POINT('Ctrl Pts',(-215.571314163814,-3.81855926723936,
126.284788106246));
#166209=CARTESIAN_POINT('Ctrl Pts',(-215.563916674478,-3.69816035092072,
126.1830637957));
#166210=CARTESIAN_POINT('Ctrl Pts',(-215.556519185141,-3.57371500679695,
126.086171744607));
#166211=CARTESIAN_POINT('Ctrl Pts',(-215.549121695805,-3.44565632882657,
125.994435147653));
#166212=CARTESIAN_POINT('Ctrl Pts',(-215.54172161329,-3.31755276008534,
125.902666392578));
#166213=CARTESIAN_POINT('Ctrl Pts',(-215.534321530776,-3.18583363888663,
125.816056907094));
#166214=CARTESIAN_POINT('Ctrl Pts',(-215.526921448261,-3.05096083399531,
125.734886428666));
#166215=CARTESIAN_POINT('Ctrl Pts',(-215.519513228595,-2.91593972258993,
125.653626694952));
#166216=CARTESIAN_POINT('Ctrl Pts',(-215.512105008929,-2.77775832210689,
125.577818104846));
#166217=CARTESIAN_POINT('Ctrl Pts',(-215.504696789263,-2.6369035302863,
125.507694653541));
#166218=CARTESIAN_POINT('Ctrl Pts',(-215.497284009961,-2.49596204469123,
125.437528042421));
#166219=CARTESIAN_POINT('Ctrl Pts',(-215.48987123066,-2.35234422880253,
125.373053695043));
#166220=CARTESIAN_POINT('Ctrl Pts',(-215.482458451358,-2.20655623487208,
125.314457144385));
#166221=CARTESIAN_POINT('Ctrl Pts',(-215.475035080329,-2.06055993221932,
125.255776868227));
#166222=CARTESIAN_POINT('Ctrl Pts',(-215.467611709301,-1.91238760914617,
125.202991287361));
#166223=CARTESIAN_POINT('Ctrl Pts',(-215.460188338273,-1.7625606085087,
125.156236091333));
#166224=CARTESIAN_POINT('Ctrl Pts',(-215.456252288828,-1.68311873763299,
125.131445364496));
#166225=CARTESIAN_POINT('Ctrl Pts',(-215.452316239383,-1.60321186086013,
125.108349143486));
#166226=CARTESIAN_POINT('Ctrl Pts',(-215.448380189938,-1.52291863500538,
125.086961786484));
#166227=CARTESIAN_POINT('Ctrl Pts',(-215.440956923532,-1.37148811706968,
125.046625898699));
#166228=CARTESIAN_POINT('Ctrl Pts',(-215.433533657127,-1.21822501274709,
125.012249336693));
#166229=CARTESIAN_POINT('Ctrl Pts',(-215.426110390721,-1.06363954787946,
124.983999677325));
#166230=CARTESIAN_POINT('Ctrl Pts',(-215.418695898,-0.90923679019333,124.955783406708));
#166231=CARTESIAN_POINT('Ctrl Pts',(-215.411281405279,-0.753515146594347,
124.933679690956));
#166232=CARTESIAN_POINT('Ctrl Pts',(-215.403866912558,-0.596999682143853,
124.917806282302));
#166233=CARTESIAN_POINT('Ctrl Pts',(-215.396459566204,-0.440635073191145,
124.901948173037));
#166234=CARTESIAN_POINT('Ctrl Pts',(-215.389052219851,-0.283478535478698,
124.892308453501));
#166235=CARTESIAN_POINT('Ctrl Pts',(-215.381644873497,-0.126064894761871,
124.888953767246));
#166236=CARTESIAN_POINT('Ctrl Pts',(-215.374243051821,0.0312313409228329,
124.885601583043));
#166237=CARTESIAN_POINT('Ctrl Pts',(-215.366841230146,0.188783926190721,
124.888525106367));
#166238=CARTESIAN_POINT('Ctrl Pts',(-215.359439408471,0.346053458792463,
124.897739115713));
#166239=CARTESIAN_POINT('Ctrl Pts',(-215.352041494159,0.50323997003168,
124.906948261054));
#166240=CARTESIAN_POINT('Ctrl Pts',(-215.344643579848,0.660143354468876,
124.92244125731));
#166241=CARTESIAN_POINT('Ctrl Pts',(-215.337245665537,0.816224868133231,
124.94418079719));
#166242=CARTESIAN_POINT('Ctrl Pts',(-215.329848980624,0.972280443881844,
124.965916724353));
#166243=CARTESIAN_POINT('Ctrl Pts',(-215.322452295712,1.12751405056174,
124.993897083447));
#166244=CARTESIAN_POINT('Ctrl Pts',(-215.3150556108,1.28139260290848,125.028032756398));
#166245=CARTESIAN_POINT('Ctrl Pts',(-215.307659253865,1.43526433211895,
125.062166915736));
#166246=CARTESIAN_POINT('Ctrl Pts',(-215.300262896929,1.5877807620265,125.102455765403));
#166247=CARTESIAN_POINT('Ctrl Pts',(-215.292866539994,1.73841979743222,
125.148759219802));
#166248=CARTESIAN_POINT('Ctrl Pts',(-215.285469050657,1.88908189605925,
125.195069763377));
#166249=CARTESIAN_POINT('Ctrl Pts',(-215.27807156132,2.03786567102082,125.247396635534));
#166250=CARTESIAN_POINT('Ctrl Pts',(-215.270674071984,2.18426511160827,
125.305550156683));
#166251=CARTESIAN_POINT('Ctrl Pts',(-215.263273989469,2.33071587229246,
125.36372406346));
#166252=CARTESIAN_POINT('Ctrl Pts',(-215.255873906954,2.4747802877687,125.427728548153));
#166253=CARTESIAN_POINT('Ctrl Pts',(-215.248473824439,2.61597335563737,
125.497326232423));
#166254=CARTESIAN_POINT('Ctrl Pts',(-215.241065604772,2.75732167979935,
125.567000446501));
#166255=CARTESIAN_POINT('Ctrl Pts',(-215.233657385106,2.89579201589938,
125.642279977557));
#166256=CARTESIAN_POINT('Ctrl Pts',(-215.226249165439,3.03092431703412,
125.722881664848));
#166257=CARTESIAN_POINT('Ctrl Pts',(-215.218836386137,3.16613978984541,
125.803532961134));
#166258=CARTESIAN_POINT('Ctrl Pts',(-215.211423606835,3.2980128218533,125.889512737487));
#166259=CARTESIAN_POINT('Ctrl Pts',(-215.204010827533,3.42611373125421,
125.98049543879));
#166260=CARTESIAN_POINT('Ctrl Pts',(-215.196587456504,3.55439767724162,
126.071608140442));
#166261=CARTESIAN_POINT('Ctrl Pts',(-215.189164085476,3.67889844132221,
126.167737816495));
#166262=CARTESIAN_POINT('Ctrl Pts',(-215.181740714447,3.79922006549019,
126.26851918995));
#166263=CARTESIAN_POINT('Ctrl Pts',(-215.177804665006,3.86301747770077,
126.321955892371));
#166264=CARTESIAN_POINT('Ctrl Pts',(-215.173868615565,3.92564060121673,
126.37669973921));
#166265=CARTESIAN_POINT('Ctrl Pts',(-215.169932566125,3.9870348401628,126.43269231521));
#166266=CARTESIAN_POINT('Ctrl Pts',(-215.162509299719,4.10282245876953,
126.538292566078));
#166267=CARTESIAN_POINT('Ctrl Pts',(-215.155086033314,4.21458688552747,
126.648655784924));
#166268=CARTESIAN_POINT('Ctrl Pts',(-215.147662766908,4.32191134374749,
126.763443283682));
#166269=CARTESIAN_POINT('Ctrl Pts',(-215.140248274187,4.42910895337063,
126.878095113148));
#166270=CARTESIAN_POINT('Ctrl Pts',(-215.132833781466,4.5318767875213,126.997160543898));
#166271=CARTESIAN_POINT('Ctrl Pts',(-215.125419288745,4.62983196741889,
127.120261471782));
#166272=CARTESIAN_POINT('Ctrl Pts',(-215.118011942391,4.72769273442615,
127.243243750357));
#166273=CARTESIAN_POINT('Ctrl Pts',(-215.110604596037,4.82074985087852,
127.370253492568));
#166274=CARTESIAN_POINT('Ctrl Pts',(-215.103197249683,4.90865816128401,
127.500876756827));
#166275=CARTESIAN_POINT('Ctrl Pts',(-215.095795428008,4.99650090635502,
127.631402597328));
#166276=CARTESIAN_POINT('Ctrl Pts',(-215.088393606332,5.07920228415796,
127.765536285204));
#166277=CARTESIAN_POINT('Ctrl Pts',(-215.080991784657,5.15645830103452,
127.902831994203));
#166278=CARTESIAN_POINT('Ctrl Pts',(-215.073593870346,5.23367353506112,
128.040055225867));
#166279=CARTESIAN_POINT('Ctrl Pts',(-215.066195956034,5.30544895039352,
128.180436829845));
#166280=CARTESIAN_POINT('Ctrl Pts',(-215.058798041723,5.37152473043544,
128.323503380073));
#166281=CARTESIAN_POINT('Ctrl Pts',(-215.05140135681,5.43758952988135,128.466546155237));
#166282=CARTESIAN_POINT('Ctrl Pts',(-215.044004671898,5.49795641753252,
128.612272652531));
#166283=CARTESIAN_POINT('Ctrl Pts',(-215.036607986986,5.55241222534259,
128.760186201728));
#166284=CARTESIAN_POINT('Ctrl Pts',(-215.02921163005,5.60686561852507,128.908093192284));
#166285=CARTESIAN_POINT('Ctrl Pts',(-215.021815273115,5.65540832404635,
129.058186691611));
#166286=CARTESIAN_POINT('Ctrl Pts',(-215.014418916179,5.69787599467857,
129.209951726545));
#166287=CARTESIAN_POINT('Ctrl Pts',(-215.007021426843,5.7403501672197,129.361739997094));
#166288=CARTESIAN_POINT('Ctrl Pts',(-214.999623937506,5.7767473523118,129.515199953302));
#166289=CARTESIAN_POINT('Ctrl Pts',(-214.992226448169,5.80695362161742,
129.669803347577));
#166290=CARTESIAN_POINT('Ctrl Pts',(-214.984826365654,5.83717047968395,
129.824460937833));
#166291=CARTESIAN_POINT('Ctrl Pts',(-214.977426283139,5.86119202954348,
129.980262398064));
#166292=CARTESIAN_POINT('Ctrl Pts',(-214.970026200624,5.87895582867323,
130.136671373225));
#166293=CARTESIAN_POINT('Ctrl Pts',(-214.962617980958,5.89673916092626,
130.293252336133));
#166294=CARTESIAN_POINT('Ctrl Pts',(-214.955209761291,5.90825095840889,
130.450441776919));
#166295=CARTESIAN_POINT('Ctrl Pts',(-214.947801541624,5.91348078568425,
130.607699589797));
#166296=CARTESIAN_POINT('Ctrl Pts',(-214.940388762322,5.91871383183104,
130.765054192235));
#166297=CARTESIAN_POINT('Ctrl Pts',(-214.93297598302,5.91765720588825,130.922476878194));
#166298=CARTESIAN_POINT('Ctrl Pts',(-214.925563203718,5.91035255308703,
131.079430173711));
#166299=CARTESIAN_POINT('Ctrl Pts',(-214.918139832689,5.90303746305534,
131.236607731456));
#166300=CARTESIAN_POINT('Ctrl Pts',(-214.91071646166,5.88945654814317,131.393314188327));
#166301=CARTESIAN_POINT('Ctrl Pts',(-214.903293090632,5.86970310125876,
131.5490189725));
#166302=CARTESIAN_POINT('Ctrl Pts',(-214.899357041192,5.85922934974553,
131.631577385136));
#166303=CARTESIAN_POINT('Ctrl Pts',(-214.895420991752,5.84702112889083,
131.713854378921));
#166304=CARTESIAN_POINT('Ctrl Pts',(-214.891484942312,5.83309807470133,
131.795772445928));
#166305=CARTESIAN_POINT('Ctrl Pts',(-214.884061675906,5.80683962901805,
131.950267363759));
#166306=CARTESIAN_POINT('Ctrl Pts',(-214.876638409501,5.77439933001569,
132.103951956879));
#166307=CARTESIAN_POINT('Ctrl Pts',(-214.869215143095,5.73583684757446,
132.256292510083));
#166308=CARTESIAN_POINT('Ctrl Pts',(-214.861800650374,5.69731994278507,
132.408453009404));
#166309=CARTESIAN_POINT('Ctrl Pts',(-214.854386157653,5.65269534839071,
132.559272272464));
#166310=CARTESIAN_POINT('Ctrl Pts',(-214.846971664932,5.60207421878622,
132.708223797973));
#166311=CARTESIAN_POINT('Ctrl Pts',(-214.839564318579,5.5515018797323,132.857031758395));
#166312=CARTESIAN_POINT('Ctrl Pts',(-214.832156972225,5.49494463099763,
133.003975214029));
#166313=CARTESIAN_POINT('Ctrl Pts',(-214.824749625871,5.43256416838892,
133.148540030247));
#166314=CARTESIAN_POINT('Ctrl Pts',(-214.817347804196,5.37023023148271,
133.292997024571));
#166315=CARTESIAN_POINT('Ctrl Pts',(-214.809945982521,5.30208187580697,
133.435078570634));
#166316=CARTESIAN_POINT('Ctrl Pts',(-214.802544160845,5.22832987161546,
133.574287929983));
#166317=CARTESIAN_POINT('Ctrl Pts',(-214.795146246534,5.15461680053308,
133.713423801795));
#166318=CARTESIAN_POINT('Ctrl Pts',(-214.787748332223,5.07530614649459,
133.849690177459));
#166319=CARTESIAN_POINT('Ctrl Pts',(-214.780350417911,4.99065577903745,
133.982612567563));
#166320=CARTESIAN_POINT('Ctrl Pts',(-214.772953732999,4.90601947893555,
134.115512868378));
#166321=CARTESIAN_POINT('Ctrl Pts',(-214.765557048087,4.81604542689396,
134.245069971992));
#166322=CARTESIAN_POINT('Ctrl Pts',(-214.758160363175,4.72103626310515,
134.370836071701));
#166323=CARTESIAN_POINT('Ctrl Pts',(-214.75076400624,4.62603131212223,134.496596594809));
#166324=CARTESIAN_POINT('Ctrl Pts',(-214.743367649304,4.52599191832748,
134.618566150388));
#166325=CARTESIAN_POINT('Ctrl Pts',(-214.735971292369,4.42126250953769,
134.736328112886));
#166326=CARTESIAN_POINT('Ctrl Pts',(-214.728573803032,4.31651706640775,
134.854108105042));
#166327=CARTESIAN_POINT('Ctrl Pts',(-214.721176313695,4.20708042663369,
134.96767894248));
#166328=CARTESIAN_POINT('Ctrl Pts',(-214.713778824359,4.09333543882564,
135.076659243336));
#166329=CARTESIAN_POINT('Ctrl Pts',(-214.706378741844,3.97955057788893,
135.185677747067));
#166330=CARTESIAN_POINT('Ctrl Pts',(-214.698978659329,3.86145463133097,
135.290102252206));
#166331=CARTESIAN_POINT('Ctrl Pts',(-214.691578576814,3.73946509813376,
135.389590311086));
#166332=CARTESIAN_POINT('Ctrl Pts',(-214.684170357148,3.61734142490346,
135.489187767315));
#166333=CARTESIAN_POINT('Ctrl Pts',(-214.676762137481,3.49131590426694,
135.583837700879));
#166334=CARTESIAN_POINT('Ctrl Pts',(-214.669353917815,3.36183730191046,
135.673239391779));
#166335=CARTESIAN_POINT('Ctrl Pts',(-214.661941138513,3.2322790076347,135.762696107928));
#166336=CARTESIAN_POINT('Ctrl Pts',(-214.654528359211,3.09926371136607,
135.846897945622));
#166337=CARTESIAN_POINT('Ctrl Pts',(-214.647115579909,2.96326611543749,
135.925589424366));
#166338=CARTESIAN_POINT('Ctrl Pts',(-214.63969220888,2.82707419976637,136.004393341186));
#166339=CARTESIAN_POINT('Ctrl Pts',(-214.632268837851,2.68789180320384,
136.077671000546));
#166340=CARTESIAN_POINT('Ctrl Pts',(-214.624845466822,2.54621573794707,
136.145214105383));
#166341=CARTESIAN_POINT('Ctrl Pts',(-214.620909417381,2.47109568866772,
136.181027080247));
#166342=CARTESIAN_POINT('Ctrl Pts',(-214.61697336794,2.39527488199036,136.215228683168));
#166343=CARTESIAN_POINT('Ctrl Pts',(-214.613037318499,2.3188291412728,136.247793539545));
#166344=CARTESIAN_POINT('Ctrl Pts',(-214.605614052093,2.17465486008611,
136.30920984235));
#166345=CARTESIAN_POINT('Ctrl Pts',(-214.598190785688,2.02782088530974,
136.364987176579));
#166346=CARTESIAN_POINT('Ctrl Pts',(-214.590767519282,1.87880849968838,
136.414887258087));
#166347=CARTESIAN_POINT('Ctrl Pts',(-214.583353026561,1.72997223433212,
136.464728361843));
#166348=CARTESIAN_POINT('Ctrl Pts',(-214.57593853384,1.57896303360794,136.508705922394));
#166349=CARTESIAN_POINT('Ctrl Pts',(-214.568524041119,1.42628393962747,
136.546628870274));
#166350=CARTESIAN_POINT('Ctrl Pts',(-214.561116694765,1.27375200350605,
136.584515266589));
#166351=CARTESIAN_POINT('Ctrl Pts',(-214.553709348411,1.11955373819532,
136.616358578508));
#166352=CARTESIAN_POINT('Ctrl Pts',(-214.546302002058,0.964209100253664,
136.642016942966));
#166353=CARTESIAN_POINT('Ctrl Pts',(-214.538900180382,0.808980324203797,
136.667656170448));
#166354=CARTESIAN_POINT('Ctrl Pts',(-214.531498358707,0.652607244681802,
136.687119574938));
#166355=CARTESIAN_POINT('Ctrl Pts',(-214.524096537031,0.495621708287031,
136.700315984152));
#166356=CARTESIAN_POINT('Ctrl Pts',(-214.51669862272,0.33871904333495,136.713505427084));
#166357=CARTESIAN_POINT('Ctrl Pts',(-214.509300708408,0.181204936444183,
136.720434432184));
#166358=CARTESIAN_POINT('Ctrl Pts',(-214.501902794097,0.0236179737786697,
136.72106347928));
#166359=CARTESIAN_POINT('Ctrl Pts',(-214.494506109185,-0.133942800792343,
136.72169242184));
#166360=CARTESIAN_POINT('Ctrl Pts',(-214.487109424272,-0.291576034179248,
136.71602348277));
#166361=CARTESIAN_POINT('Ctrl Pts',(-214.47971273936,-0.448741389502812,
136.704069231375));
#166362=CARTESIAN_POINT('Ctrl Pts',(-214.472316382425,-0.605899775949823,
136.692115510043));
#166363=CARTESIAN_POINT('Ctrl Pts',(-214.464920025489,-0.762589953361557,
136.673877058842));
#166364=CARTESIAN_POINT('Ctrl Pts',(-214.457523668554,-0.918275231213955,
136.649418458361));
#166365=CARTESIAN_POINT('Ctrl Pts',(-214.450126179217,-1.07398434487984,
136.624956113206));
#166366=CARTESIAN_POINT('Ctrl Pts',(-214.44272868988,-1.22868788384681,
136.594271780513));
#166367=CARTESIAN_POINT('Ctrl Pts',(-214.435331200544,-1.38185804172664,
136.557481415447));
#166368=CARTESIAN_POINT('Ctrl Pts',(-214.427931118029,-1.53508189316766,
136.520678153577));
#166369=CARTESIAN_POINT('Ctrl Pts',(-214.420531035514,-1.68677093056666,
136.477764684823));
#166370=CARTESIAN_POINT('Ctrl Pts',(-214.413130952999,-1.83641137460534,
136.428907161575));
#166371=CARTESIAN_POINT('Ctrl Pts',(-214.405722733332,-1.98621636369587,
136.379995914457));
#166372=CARTESIAN_POINT('Ctrl Pts',(-214.398314513666,-2.13396790567806,
136.32512767576));
#166373=CARTESIAN_POINT('Ctrl Pts',(-214.390906293999,-2.27917042748476,
136.26451745826));
#166374=CARTESIAN_POINT('Ctrl Pts',(-214.383493514697,-2.42446231902121,
136.203869936183));
#166375=CARTESIAN_POINT('Ctrl Pts',(-214.376080735395,-2.56720172650639,
136.137473550258));
#166376=CARTESIAN_POINT('Ctrl Pts',(-214.368667956093,-2.70691711875904,
136.065589587557));
#166377=CARTESIAN_POINT('Ctrl Pts',(-214.361244585064,-2.84683214291555,
135.993602913679));
#166378=CARTESIAN_POINT('Ctrl Pts',(-214.353821214035,-2.98371419812839,
135.916113186389));
#166379=CARTESIAN_POINT('Ctrl Pts',(-214.346397843006,-3.11711949905002,
135.833425798208));
#166380=CARTESIAN_POINT('Ctrl Pts',(-214.342461793566,-3.18785419060599,
135.789582960943));
#166381=CARTESIAN_POINT('Ctrl Pts',(-214.338525744126,-3.25761196580092,
135.744279570738));
#166382=CARTESIAN_POINT('Ctrl Pts',(-214.334589694686,-3.32633049188761,
135.697565704341));
#166383=CARTESIAN_POINT('Ctrl Pts',(-214.327198576855,-3.45537021335995,
135.609846356268));
#166384=CARTESIAN_POINT('Ctrl Pts',(-214.319807459024,-3.58114113330062,
135.516880709447));
#166385=CARTESIAN_POINT('Ctrl Pts',(-214.312416341193,-3.70318490983809,
135.418940997844));
#166386=CARTESIAN_POINT('Ctrl Pts',(-214.305033978144,-3.82508412546336,
135.321117295877));
#166387=CARTESIAN_POINT('Ctrl Pts',(-214.297651615096,-3.94326469299833,
135.218331488424));
#166388=CARTESIAN_POINT('Ctrl Pts',(-214.290269252047,-4.0572960434475,
135.110899759188));
#166389=CARTESIAN_POINT('Ctrl Pts',(-214.282893986435,-4.17121776365406,
135.00357131529));
#166390=CARTESIAN_POINT('Ctrl Pts',(-214.275518720823,-4.28099793458178,
134.891606097103));
#166391=CARTESIAN_POINT('Ctrl Pts',(-214.268143455211,-4.38623810574165,
134.775361227266));
#166392=CARTESIAN_POINT('Ctrl Pts',(-214.260773635606,-4.49140056598207,
134.659202194383));
#166393=CARTESIAN_POINT('Ctrl Pts',(-214.253403816001,-4.59202944872852,
134.53877007949));
#166394=CARTESIAN_POINT('Ctrl Pts',(-214.246033996395,-4.68776243321892,
134.414459498788));
#166395=CARTESIAN_POINT('Ctrl Pts',(-214.238423212888,-4.78662550701507,
134.286084454607));
#166396=CARTESIAN_POINT('Ctrl Pts',(-214.23081242938,-4.88026677970626,
134.153573287877));
#166397=CARTESIAN_POINT('Ctrl Pts',(-214.223201645872,-4.96833121822625,
134.017398972223));
#166398=CARTESIAN_POINT('Ctrl Pts',(-214.215836748133,-5.05355051050206,
133.885624115071));
#166399=CARTESIAN_POINT('Ctrl Pts',(-214.208471850393,-5.13354750807239,
133.75041947113));
#166400=CARTESIAN_POINT('Ctrl Pts',(-214.201106952653,-5.20804399196539,
133.612243866608));
#166401=CARTESIAN_POINT('Ctrl Pts',(-214.193742182749,-5.28253918279686,
133.47407066045));
#166402=CARTESIAN_POINT('Ctrl Pts',(-214.186377412844,-5.3515338706958,
133.332926927929));
#166403=CARTESIAN_POINT('Ctrl Pts',(-214.17901264294,-5.41479566029319,
133.18929636508));
#166404=CARTESIAN_POINT('Ctrl Pts',(-214.171646513804,-5.47806912539624,
133.045639293979));
#166405=CARTESIAN_POINT('Ctrl Pts',(-214.164280384668,-5.53560743415387,
132.899494823891));
#166406=CARTESIAN_POINT('Ctrl Pts',(-214.156914255532,-5.58722630848571,
132.751366714183));
#166407=CARTESIAN_POINT('Ctrl Pts',(-214.14954527951,-5.63886513264815,
132.603181355442));
#166408=CARTESIAN_POINT('Ctrl Pts',(-214.142176303489,-5.68457984454065,
132.453011186632));
#166409=CARTESIAN_POINT('Ctrl Pts',(-214.134807327467,-5.72423605993967,
132.301375010478));
#166410=CARTESIAN_POINT('Ctrl Pts',(-214.127430261279,-5.7639358126471,
132.149572357749));
#166411=CARTESIAN_POINT('Ctrl Pts',(-214.120053195091,-5.79756369440894,
131.996300849077));
#166412=CARTESIAN_POINT('Ctrl Pts',(-214.112676128903,-5.82503634052978,
131.842089962823));
#166413=CARTESIAN_POINT('Ctrl Pts',(-214.105294222152,-5.85252701320656,
131.687777888967));
#166414=CARTESIAN_POINT('Ctrl Pts',(-214.0979123154,-5.87385435360959,131.532525581733));
#166415=CARTESIAN_POINT('Ctrl Pts',(-214.090530408648,-5.8889869347913,
131.376866900813));
#166416=CARTESIAN_POINT('Ctrl Pts',(-214.083138624783,-5.90413976361654,
131.220999946007));
#166417=CARTESIAN_POINT('Ctrl Pts',(-214.075746840918,-5.91308126700828,
131.064725906564));
#166418=CARTESIAN_POINT('Ctrl Pts',(-214.068355057054,-5.91583208039486,
130.908578461868));
#166419=CARTESIAN_POINT('Ctrl Pts',(-214.066695102105,-5.9164498238755,
130.873512809487));
#166420=CARTESIAN_POINT('Ctrl Pts',(-214.065035147157,-5.91675557412369,
130.838453519149));
#166421=CARTESIAN_POINT('Ctrl Pts',(-214.063375192209,-5.91674992308523,
130.803406588753));
#166422=CARTESIAN_POINT('',(-212.313375192209,-5.91518716771215,130.809800676931));
#166423=CARTESIAN_POINT('Ctrl Pts',(-214.063375192209,-5.92634516172826,
130.803405041597));
#166424=CARTESIAN_POINT('Ctrl Pts',(-214.060964151763,-5.92645914177806,
130.752417734346));
#166425=CARTESIAN_POINT('Ctrl Pts',(-214.058553111318,-5.92585830881452,
130.701433182352));
#166426=CARTESIAN_POINT('Ctrl Pts',(-214.056142070873,-5.92453444346407,
130.650467411543));
#166427=CARTESIAN_POINT('Ctrl Pts',(-213.963326196269,-5.87357066946307,
128.688479340455));
#166428=CARTESIAN_POINT('Ctrl Pts',(-213.777694447059,-3.62863765870681,
124.820169003641));
#166429=CARTESIAN_POINT('Ctrl Pts',(-213.499246823247,3.07330259697371,
124.516883247605));
#166430=CARTESIAN_POINT('Ctrl Pts',(-213.220799199435,6.9510279052142,129.991482034214));
#166431=CARTESIAN_POINT('Ctrl Pts',(-212.942351575622,4.44109814515497,
136.213076527599));
#166432=CARTESIAN_POINT('Ctrl Pts',(-212.663903951809,-2.14998385059845,
137.464325330124));
#166433=CARTESIAN_POINT('Ctrl Pts',(-212.454245157338,-5.62514049150498,
133.79823295943));
#166434=CARTESIAN_POINT('Ctrl Pts',(-212.337402237471,-5.9197797619191,
131.320403388515));
#166435=CARTESIAN_POINT('Ctrl Pts',(-212.313375192209,-5.91518716771215,
130.809800676931));
#166436=CARTESIAN_POINT('',(-210.563375192209,-5.90724396466958,130.802943052422));
#166437=CARTESIAN_POINT('Ctrl Pts',(-212.313375192209,-5.91518716771215,
130.809800676931));
#166438=CARTESIAN_POINT('Ctrl Pts',(-212.244586362867,-5.90203868542103,
129.3479578908));
#166439=CARTESIAN_POINT('Ctrl Pts',(-212.082981658921,-4.61601153110151,
125.893005037876));
#166440=CARTESIAN_POINT('Ctrl Pts',(-211.828561080369,1.18315125270368,
123.906700605387));
#166441=CARTESIAN_POINT('Ctrl Pts',(-211.550113456557,6.44271887229008,
128.071425553759));
#166442=CARTESIAN_POINT('Ctrl Pts',(-211.271665832744,5.78174259255394,
134.747584314464));
#166443=CARTESIAN_POINT('Ctrl Pts',(-210.993218208931,-0.192372675911253,
137.800113134909));
#166444=CARTESIAN_POINT('Ctrl Pts',(-210.757121328754,-5.10795605870944,
134.937397303148));
#166445=CARTESIAN_POINT('Ctrl Pts',(-210.613840323178,-5.90494721591197,
131.879020657015));
#166446=CARTESIAN_POINT('Ctrl Pts',(-210.563375192209,-5.90724396466958,
130.802943052422));
#166447=CARTESIAN_POINT('',(-208.813375192209,-5.92040475870682,130.799408613133));
#166448=CARTESIAN_POINT('Ctrl Pts',(-210.563375192209,-5.90724396466958,
130.802943052422));
#166449=CARTESIAN_POINT('Ctrl Pts',(-210.521024448574,-5.90917141469214,
129.899890075305));
#166450=CARTESIAN_POINT('Ctrl Pts',(-210.385857830337,-5.28952247014664,
127.020214927324));
#166451=CARTESIAN_POINT('Ctrl Pts',(-210.157875337492,-0.802299360853992,
123.852103698697));
#166452=CARTESIAN_POINT('Ctrl Pts',(-209.87942771368,5.41546824219867,126.371498760019));
#166453=CARTESIAN_POINT('Ctrl Pts',(-209.600980089866,6.65668509099864,
132.964477311082));
#166454=CARTESIAN_POINT('Ctrl Pts',(-209.322532466054,1.78073353831976,
137.572414148371));
#166455=CARTESIAN_POINT('Ctrl Pts',(-209.059997500168,-4.35945843268618,
136.052938256508));
#166456=CARTESIAN_POINT('Ctrl Pts',(-208.890278408886,-5.90578069205309,
132.430000405375));
#166457=CARTESIAN_POINT('Ctrl Pts',(-208.813375192209,-5.92040475870682,
130.799408613133));
#166458=CARTESIAN_POINT('',(-207.063375192208,-5.92350094233479,130.808116397466));
#166459=CARTESIAN_POINT('Ctrl Pts',(-208.813375192209,-5.92040475870682,
130.799408613133));
#166460=CARTESIAN_POINT('Ctrl Pts',(-208.797462534282,-5.92343074097668,
130.462009860137));
#166461=CARTESIAN_POINT('Ctrl Pts',(-208.781549876355,-5.89708361299461,
130.125083613377));
#166462=CARTESIAN_POINT('Ctrl Pts',(-208.672821343824,-5.50494337257859,
127.859639161688));
#166463=CARTESIAN_POINT('Ctrl Pts',(-208.487189594614,-2.72312717773575,
124.3574901439));
#166464=CARTESIAN_POINT('Ctrl Pts',(-208.208741970802,3.95201795870991,
125.028625635385));
#166465=CARTESIAN_POINT('Ctrl Pts',(-207.93029434699,6.99545165791052,131.007379415155));
#166466=CARTESIAN_POINT('Ctrl Pts',(-207.651846723176,3.61040703030553,
136.799568837958));
#166467=CARTESIAN_POINT('Ctrl Pts',(-207.373399099364,-3.0924252799637,
137.082454788425));
#166468=CARTESIAN_POINT('Ctrl Pts',(-207.177241922374,-5.8124039569315,
133.217483732592));
#166469=CARTESIAN_POINT('Ctrl Pts',(-207.073900619989,-5.92514845404535,
131.030985187931));
#166470=CARTESIAN_POINT('Ctrl Pts',(-207.063375192208,-5.92350094233479,
130.808116397466));
#166471=CARTESIAN_POINT('',(-205.313375192208,-5.90857914829821,130.807499840963));
#166472=CARTESIAN_POINT('Ctrl Pts',(-207.063375192208,-5.92350094233479,
130.808116397466));
#166473=CARTESIAN_POINT('Ctrl Pts',(-206.981084745385,-5.91062028060458,
129.06567203012));
#166474=CARTESIAN_POINT('Ctrl Pts',(-206.805978423956,-4.17532705327718,
125.335613429113));
#166475=CARTESIAN_POINT('Ctrl Pts',(-206.538056227925,2.17024453367553,
124.150970564787));
#166476=CARTESIAN_POINT('Ctrl Pts',(-206.259608604111,6.77075566682168,
129.033928966654));
#166477=CARTESIAN_POINT('Ctrl Pts',(-205.981160980299,5.14927311196064,
135.543827565311));
#166478=CARTESIAN_POINT('Ctrl Pts',(-205.702713356486,-1.20413987681471,
137.698387574825));
#166479=CARTESIAN_POINT('Ctrl Pts',(-205.480118093789,-5.39856531937876,
134.356261281287));
#166480=CARTESIAN_POINT('Ctrl Pts',(-205.350338705697,-5.91235307129998,
131.595235086907));
#166481=CARTESIAN_POINT('Ctrl Pts',(-205.313375192208,-5.90857914829821,
130.807499840963));
#166482=CARTESIAN_POINT('',(-203.563375192208,-5.91198242686231,130.79947290462));
#166483=CARTESIAN_POINT('Ctrl Pts',(-205.313375192208,-5.90857914829821,
130.807499840963));
#166484=CARTESIAN_POINT('Ctrl Pts',(-205.257522831092,-5.90287670038602,
129.617221394239));
#166485=CARTESIAN_POINT('Ctrl Pts',(-205.108854595372,-4.97542928644342,
126.440754491598));
#166486=CARTESIAN_POINT('Ctrl Pts',(-204.867370485048,0.213664449080756,
123.809226020325));
#166487=CARTESIAN_POINT('Ctrl Pts',(-204.588922861234,6.00069570294186,
127.203081454398));
#166488=CARTESIAN_POINT('Ctrl Pts',(-204.310475237422,6.27338075607734,
133.906336507158));
#166489=CARTESIAN_POINT('Ctrl Pts',(-204.032027613609,0.781135366069192,
137.759027257328));
#166490=CARTESIAN_POINT('Ctrl Pts',(-203.782994265204,-4.77292417967637,
135.488857499412));
#166491=CARTESIAN_POINT('Ctrl Pts',(-203.626776791404,-5.90152837485451,
132.148681533904));
#166492=CARTESIAN_POINT('Ctrl Pts',(-203.563375192208,-5.91198242686231,
130.79947290462));
#166493=CARTESIAN_POINT('',(-201.813375867204,-5.92197308054016,130.803199987403));
#166494=CARTESIAN_POINT('Ctrl Pts',(-203.563375192208,-5.91198242686231,
130.79947290462));
#166495=CARTESIAN_POINT('Ctrl Pts',(-203.5339609168,-5.91683243646446,130.173526639722));
#166496=CARTESIAN_POINT('Ctrl Pts',(-203.504546641391,-5.82534361100667,
129.54896166662));
#166497=CARTESIAN_POINT('Ctrl Pts',(-203.382316491379,-5.02009495809496,
127.092968345155));
#166498=CARTESIAN_POINT('Ctrl Pts',(-203.196684742167,-1.76012566321133,
124.030918495546));
#166499=CARTESIAN_POINT('Ctrl Pts',(-202.918237118359,4.74729777661893,
125.662306130287));
#166500=CARTESIAN_POINT('Ctrl Pts',(-202.639789494544,6.89218647818192,
132.018990635446));
#166501=CARTESIAN_POINT('Ctrl Pts',(-202.361341870732,2.70349250829908,
137.25948949219));
#166502=CARTESIAN_POINT('Ctrl Pts',(-202.085870845849,-3.89824401710562,
136.575431840637));
#166503=CARTESIAN_POINT('Ctrl Pts',(-201.90321569557,-5.92108948216704,
132.703162475868));
#166504=CARTESIAN_POINT('Ctrl Pts',(-201.813376419895,-5.92624986544025,
130.803210827386));
#166505=CARTESIAN_POINT('',(-200.063375194059,-5.91567330630329,130.809819562943));
#166506=CARTESIAN_POINT('Ctrl Pts',(-201.813375192208,-5.91674988355362,
130.803186748634));
#166507=CARTESIAN_POINT('Ctrl Pts',(-201.810399002507,-5.91673741614191,
130.740346209347));
#166508=CARTESIAN_POINT('Ctrl Pts',(-201.807422812807,-5.9157238558129,
130.677516728804));
#166509=CARTESIAN_POINT('Ctrl Pts',(-201.804446623105,-5.91371007129092,
130.614719495411));
#166510=CARTESIAN_POINT('Ctrl Pts',(-201.7970233567,-5.90868725336307,130.458089495395));
#166511=CARTESIAN_POINT('Ctrl Pts',(-201.789600090295,-5.89742980985056,
130.301422341445));
#166512=CARTESIAN_POINT('Ctrl Pts',(-201.782176823889,-5.87992433832519,
130.145254906719));
#166513=CARTESIAN_POINT('Ctrl Pts',(-201.774762331168,-5.86243955681343,
129.989272048933));
#166514=CARTESIAN_POINT('Ctrl Pts',(-201.767347838447,-5.83872148765387,
129.833788102077));
#166515=CARTESIAN_POINT('Ctrl Pts',(-201.759933345726,-5.80880871565572,
129.679339787793));
#166516=CARTESIAN_POINT('Ctrl Pts',(-201.752525999373,-5.77892477471341,
129.52504033661));
#166517=CARTESIAN_POINT('Ctrl Pts',(-201.745118653019,-5.74285808789947,
129.371774894843));
#166518=CARTESIAN_POINT('Ctrl Pts',(-201.737711306665,-5.70069899303698,
129.220074799512));
#166519=CARTESIAN_POINT('Ctrl Pts',(-201.73030948499,-5.658571342018,129.068487847836));
#166520=CARTESIAN_POINT('Ctrl Pts',(-201.722907663315,-5.6103604300888,
128.918464276076));
#166521=CARTESIAN_POINT('Ctrl Pts',(-201.715505841639,-5.55620757811541,
128.770524854434));
#166522=CARTESIAN_POINT('Ctrl Pts',(-201.708107927328,-5.50208331301106,
128.622663528862));
#166523=CARTESIAN_POINT('Ctrl Pts',(-201.700710013017,-5.44202348275199,
128.476884511958));
#166524=CARTESIAN_POINT('Ctrl Pts',(-201.693312098705,-5.37621909378814,
128.333692930869));
#166525=CARTESIAN_POINT('Ctrl Pts',(-201.685915413793,-5.31042564032021,
128.190525145624));
#166526=CARTESIAN_POINT('Ctrl Pts',(-201.678518728881,-5.23888967855432,
128.049944281665));
#166527=CARTESIAN_POINT('Ctrl Pts',(-201.671122043969,-5.16185019591898,
127.912435114136));
#166528=CARTESIAN_POINT('Ctrl Pts',(-201.663725687034,-5.08481412929481,
127.774932043906));
#166529=CARTESIAN_POINT('Ctrl Pts',(-201.656329330098,-5.00227520947535,
127.640500724959));
#166530=CARTESIAN_POINT('Ctrl Pts',(-201.648932973163,-4.91451806073126,
127.509600718386));
#166531=CARTESIAN_POINT('Ctrl Pts',(-201.641535483827,-4.82674747614365,
127.378680670687));
#166532=CARTESIAN_POINT('Ctrl Pts',(-201.63413799449,-4.73375727975254,
127.251293321958));
#166533=CARTESIAN_POINT('Ctrl Pts',(-201.626740505153,-4.635874949064,127.127868536908));
#166534=CARTESIAN_POINT('Ctrl Pts',(-201.619340422639,-4.53795830587631,
127.004400485491));
#166535=CARTESIAN_POINT('Ctrl Pts',(-201.611940340124,-4.43514634578947,
126.884898055683));
#166536=CARTESIAN_POINT('Ctrl Pts',(-201.604540257609,-4.32780616554116,
126.76975724722));
#166537=CARTESIAN_POINT('Ctrl Pts',(-201.597132037942,-4.22034795372998,
126.654489829602));
#166538=CARTESIAN_POINT('Ctrl Pts',(-201.589723818276,-4.10835183258725,
126.543593884573));
#166539=CARTESIAN_POINT('Ctrl Pts',(-201.58231559861,-3.99222154535993,
126.437428319572));
#166540=CARTESIAN_POINT('Ctrl Pts',(-201.574902819308,-3.87601978187823,
126.331197411437));
#166541=CARTESIAN_POINT('Ctrl Pts',(-201.567490040006,-3.7556790667533,
126.22970292491));
#166542=CARTESIAN_POINT('Ctrl Pts',(-201.560077260704,-3.63163498628868,
126.133262471641));
#166543=CARTESIAN_POINT('Ctrl Pts',(-201.552653889675,-3.50741366582499,
126.03668421973));
#166544=CARTESIAN_POINT('Ctrl Pts',(-201.545230518646,-3.3794787144427,
125.945174640511));
#166545=CARTESIAN_POINT('Ctrl Pts',(-201.537807147618,-3.24829403434159,
125.859007603982));
#166546=CARTESIAN_POINT('Ctrl Pts',(-201.533871098176,-3.17873676920309,
125.813319773655));
#166547=CARTESIAN_POINT('Ctrl Pts',(-201.529935048734,-3.10826629928466,
125.769133155338));
#166548=CARTESIAN_POINT('Ctrl Pts',(-201.525998999293,-3.03695429695874,
125.726483190857));
#166549=CARTESIAN_POINT('Ctrl Pts',(-201.518575732887,-2.90246208617211,
125.646046688922));
#166550=CARTESIAN_POINT('Ctrl Pts',(-201.511152466482,-2.76456864931066,
125.570835471457));
#166551=CARTESIAN_POINT('Ctrl Pts',(-201.503729200076,-2.6237184286282,
125.50115100736));
#166552=CARTESIAN_POINT('Ctrl Pts',(-201.496314707355,-2.4830346812097,
125.431548904513));
#166553=CARTESIAN_POINT('Ctrl Pts',(-201.488900214634,-2.3394014374572,
125.367460716645));
#166554=CARTESIAN_POINT('Ctrl Pts',(-201.481485721913,-2.1932911125198,
125.30914409242));
#166555=CARTESIAN_POINT('Ctrl Pts',(-201.47407837556,-2.04732161421452,
125.250883675953));
#166556=CARTESIAN_POINT('Ctrl Pts',(-201.466671029206,-1.89888013215013,
125.198383886038));
#166557=CARTESIAN_POINT('Ctrl Pts',(-201.459263682852,-1.74846252501016,
125.151855919546));
#166558=CARTESIAN_POINT('Ctrl Pts',(-201.451861861177,-1.5981571049961,
125.105362655367));
#166559=CARTESIAN_POINT('Ctrl Pts',(-201.444460039501,-1.44587884966913,
125.064832455911));
#166560=CARTESIAN_POINT('Ctrl Pts',(-201.437058217826,-1.29214228512928,
125.030427912946));
#166561=CARTESIAN_POINT('Ctrl Pts',(-201.429660303514,-1.13848687692604,
124.996041531872));
#166562=CARTESIAN_POINT('Ctrl Pts',(-201.422262389203,-0.983375056028614,
124.967774448564));
#166563=CARTESIAN_POINT('Ctrl Pts',(-201.414864474892,-0.827335043864665,
124.94573899745));
#166564=CARTESIAN_POINT('Ctrl Pts',(-201.40746778998,-0.67132096271966,
124.923707208227));
#166565=CARTESIAN_POINT('Ctrl Pts',(-201.400071105067,-0.514379365714424,
124.907905048017));
#166566=CARTESIAN_POINT('Ctrl Pts',(-201.392674420155,-0.357047286449173,
124.898393482732));
#166567=CARTESIAN_POINT('Ctrl Pts',(-201.38527806322,-0.199722183453189,
124.8888823392));
#166568=CARTESIAN_POINT('Ctrl Pts',(-201.377881706284,-0.0420070052413085,
124.88566125851));
#166569=CARTESIAN_POINT('Ctrl Pts',(-201.370485349349,0.115557760055124,
124.888739182198));
#166570=CARTESIAN_POINT('Ctrl Pts',(-201.363087860012,0.273146648919818,
124.891817577123));
#166571=CARTESIAN_POINT('Ctrl Pts',(-201.355690370676,0.430584705765377,
124.90119688937));
#166572=CARTESIAN_POINT('Ctrl Pts',(-201.348292881339,0.587333263647712,
124.916833955213));
#166573=CARTESIAN_POINT('Ctrl Pts',(-201.340892798824,0.744136769493798,
124.932476502606));
#166574=CARTESIAN_POINT('Ctrl Pts',(-201.333492716309,0.900249923925743,
124.954381134094));
#166575=CARTESIAN_POINT('Ctrl Pts',(-201.326092633794,1.05514113639827,
124.982453048325));
#166576=CARTESIAN_POINT('Ctrl Pts',(-201.318684414127,1.21020266768233,
125.010555830512));
#166577=CARTESIAN_POINT('Ctrl Pts',(-201.311276194461,1.36403920610859,
125.044839372054));
#166578=CARTESIAN_POINT('Ctrl Pts',(-201.303867974794,1.51613055959717,
125.08515799056));
#166579=CARTESIAN_POINT('Ctrl Pts',(-201.296455195492,1.66831552277604,
125.125501424502));
#166580=CARTESIAN_POINT('Ctrl Pts',(-201.28904241619,1.81875280477592,125.171887227256));
#166581=CARTESIAN_POINT('Ctrl Pts',(-201.281629636888,1.96693974488418,
125.224120604583));
#166582=CARTESIAN_POINT('Ctrl Pts',(-201.274206265859,2.11533842144153,
125.276428615409));
#166583=CARTESIAN_POINT('Ctrl Pts',(-201.266782894831,2.26147998833225,
125.334600750501));
#166584=CARTESIAN_POINT('Ctrl Pts',(-201.259359523802,2.4048832805008,125.398394749225));
#166585=CARTESIAN_POINT('Ctrl Pts',(-201.255423474361,2.48091914692211,
125.432219858064));
#166586=CARTESIAN_POINT('Ctrl Pts',(-201.25148742492,2.55618561065255,125.467624713707));
#166587=CARTESIAN_POINT('Ctrl Pts',(-201.24755137548,2.63061411281273,125.504568173331));
#166588=CARTESIAN_POINT('Ctrl Pts',(-201.240128109074,2.77098394505528,
125.574242385217));
#166589=CARTESIAN_POINT('Ctrl Pts',(-201.232704842669,2.908796043259,125.649602538817));
#166590=CARTESIAN_POINT('Ctrl Pts',(-201.225281576263,3.04355654120713,
125.730437663581));
#166591=CARTESIAN_POINT('Ctrl Pts',(-201.217867083542,3.17815776343784,
125.81117724794));
#166592=CARTESIAN_POINT('Ctrl Pts',(-201.210452590821,3.30971424764855,
125.89737873283));
#166593=CARTESIAN_POINT('Ctrl Pts',(-201.2030380981,3.43775387479355,125.988783927403));
#166594=CARTESIAN_POINT('Ctrl Pts',(-201.195630751746,3.56567009252529,
126.080101022208));
#166595=CARTESIAN_POINT('Ctrl Pts',(-201.188223405393,3.69007589959199,
126.176611626323));
#166596=CARTESIAN_POINT('Ctrl Pts',(-201.180816059039,3.81052558635577,
126.27801271686));
#166597=CARTESIAN_POINT('Ctrl Pts',(-201.173414237363,3.93088543719886,
126.379338178638));
#166598=CARTESIAN_POINT('Ctrl Pts',(-201.166012415688,4.04729475848319,
126.485546624777));
#166599=CARTESIAN_POINT('Ctrl Pts',(-201.158610594013,4.15933864322472,
126.59629305472));
#166600=CARTESIAN_POINT('Ctrl Pts',(-201.151212679701,4.27132338087164,
126.706981022484));
#166601=CARTESIAN_POINT('Ctrl Pts',(-201.14381476539,4.37894700663587,126.822201941411));
#166602=CARTESIAN_POINT('Ctrl Pts',(-201.136416851079,4.48182949379902,
126.941572123354));
#166603=CARTESIAN_POINT('Ctrl Pts',(-201.129020166166,4.58469488375913,
127.060922468139));
#166604=CARTESIAN_POINT('Ctrl Pts',(-201.121623481254,4.68282045537774,
127.184420424934));
#166605=CARTESIAN_POINT('Ctrl Pts',(-201.114226796342,4.77586463652599,
127.311647125726));
#166606=CARTESIAN_POINT('Ctrl Pts',(-201.106830439406,4.86890469199773,
127.438868185153));
#166607=CARTESIAN_POINT('Ctrl Pts',(-201.099434082471,4.95686358463872,
127.569817358517));
#166608=CARTESIAN_POINT('Ctrl Pts',(-201.092037725536,5.03944164464534,
127.704044750962));
#166609=CARTESIAN_POINT('Ctrl Pts',(-201.084640236199,5.12203234756399,
127.838292693965));
#166610=CARTESIAN_POINT('Ctrl Pts',(-201.077242746863,5.19924038189781,
127.975819537438));
#166611=CARTESIAN_POINT('Ctrl Pts',(-201.069845257526,5.27081089987097,
128.11614875458));
#166612=CARTESIAN_POINT('Ctrl Pts',(-201.062445175011,5.34240650677816,
128.25652716391));
#166613=CARTESIAN_POINT('Ctrl Pts',(-201.055045092496,5.40836049318189,
128.399709570458));
#166614=CARTESIAN_POINT('Ctrl Pts',(-201.047645009981,5.46846528047079,
128.545197489595));
#166615=CARTESIAN_POINT('Ctrl Pts',(-201.040236790314,5.52863615915231,
128.690845387655));
#166616=CARTESIAN_POINT('Ctrl Pts',(-201.032828570648,5.58294485137867,
128.838803515936));
#166617=CARTESIAN_POINT('Ctrl Pts',(-201.025420350982,5.63123274734572,
128.988555477216));
#166618=CARTESIAN_POINT('Ctrl Pts',(-201.01800757168,5.67955036370688,129.138399608329));
#166619=CARTESIAN_POINT('Ctrl Pts',(-201.010594792377,5.72183969969134,
129.290039413705));
#166620=CARTESIAN_POINT('Ctrl Pts',(-201.003182013075,5.75799294081597,
129.442946699607));
#166621=CARTESIAN_POINT('Ctrl Pts',(-200.995758642047,5.79419783938699,
129.596072466609));
#166622=CARTESIAN_POINT('Ctrl Pts',(-200.988335271018,5.82424906122381,
129.750468965729));
#166623=CARTESIAN_POINT('Ctrl Pts',(-200.980911899989,5.84809034559499,
129.905600431388));
#166624=CARTESIAN_POINT('Ctrl Pts',(-200.976975850548,5.86073156663221,
129.987854856808));
#166625=CARTESIAN_POINT('Ctrl Pts',(-200.973039801108,5.8716278209937,130.070315853689));
#166626=CARTESIAN_POINT('Ctrl Pts',(-200.969103751667,5.88077666555392,
130.152903502802));
#166627=CARTESIAN_POINT('Ctrl Pts',(-200.961680485262,5.898031100869,130.308661231559));
#166628=CARTESIAN_POINT('Ctrl Pts',(-200.954257218856,5.90911927466106,
130.465340456614));
#166629=CARTESIAN_POINT('Ctrl Pts',(-200.946833952451,5.91395173567687,
130.622411639596));
#166630=CARTESIAN_POINT('Ctrl Pts',(-200.93941945973,5.91877848512508,130.779297177483));
#166631=CARTESIAN_POINT('Ctrl Pts',(-200.932004967009,5.91736422769598,
130.936573381693));
#166632=CARTESIAN_POINT('Ctrl Pts',(-200.924590474288,5.90967099478593,
131.093703486643));
#166633=CARTESIAN_POINT('Ctrl Pts',(-200.917183127934,5.90198517690339,
131.250682143683));
#166634=CARTESIAN_POINT('Ctrl Pts',(-200.90977578158,5.88803244983971,131.40751461145));
#166635=CARTESIAN_POINT('Ctrl Pts',(-200.902368435227,5.86782683838578,
131.563662110531));
#166636=CARTESIAN_POINT('Ctrl Pts',(-200.894966613551,5.84763629703924,
131.719693148917));
#166637=CARTESIAN_POINT('Ctrl Pts',(-200.887564791876,5.82120220493272,
131.87503986722));
#166638=CARTESIAN_POINT('Ctrl Pts',(-200.880162970201,5.78859055344715,
132.029166711216));
#166639=CARTESIAN_POINT('Ctrl Pts',(-200.872765055889,5.75599611739846,
132.183212192852));
#166640=CARTESIAN_POINT('Ctrl Pts',(-200.865367141578,5.71723069365822,
132.336038718374));
#166641=CARTESIAN_POINT('Ctrl Pts',(-200.857969227266,5.67241167620617,
132.487119167727));
#166642=CARTESIAN_POINT('Ctrl Pts',(-200.850572542354,5.62760010686179,
132.63817451025));
#166643=CARTESIAN_POINT('Ctrl Pts',(-200.843175857442,5.57673704647701,
132.787483994966));
#166644=CARTESIAN_POINT('Ctrl Pts',(-200.83577917253,5.51999027249402,132.934533839178));
#166645=CARTESIAN_POINT('Ctrl Pts',(-200.828382815595,5.46324601472245,
133.081577163045));
#166646=CARTESIAN_POINT('Ctrl Pts',(-200.820986458659,5.40061869648633,
133.226360697364));
#166647=CARTESIAN_POINT('Ctrl Pts',(-200.813590101724,5.33232484821961,
133.368389142282));
#166648=CARTESIAN_POINT('Ctrl Pts',(-200.806192612387,5.26402054399037,
133.510439332119));
#166649=CARTESIAN_POINT('Ctrl Pts',(-200.79879512305,5.1900481440821,133.649733256226));
#166650=CARTESIAN_POINT('Ctrl Pts',(-200.791397633714,5.11067081254324,
133.785798929576));
#166651=CARTESIAN_POINT('Ctrl Pts',(-200.783997551199,5.03126565540398,
133.921912300536));
#166652=CARTESIAN_POINT('Ctrl Pts',(-200.776597468684,4.94645198230616,
134.054794845375));
#166653=CARTESIAN_POINT('Ctrl Pts',(-200.769197386169,4.85653698117537,
134.18400247921));
#166654=CARTESIAN_POINT('Ctrl Pts',(-200.761789166503,4.76652310925724,
134.313352190122));
#166655=CARTESIAN_POINT('Ctrl Pts',(-200.754380946836,4.67139692025517,
134.439018613408));
#166656=CARTESIAN_POINT('Ctrl Pts',(-200.74697272717,4.57150714130225,134.560589180836));
#166657=CARTESIAN_POINT('Ctrl Pts',(-200.739559947868,4.47155588185713,
134.682234572919));
#166658=CARTESIAN_POINT('Ctrl Pts',(-200.732147168566,4.36683543800591,
134.799778807794));
#166659=CARTESIAN_POINT('Ctrl Pts',(-200.724734389264,4.25773191773792,
134.912845676462));
#166660=CARTESIAN_POINT('Ctrl Pts',(-200.717311018235,4.14847250524356,
135.026074100376));
#166661=CARTESIAN_POINT('Ctrl Pts',(-200.709887647206,4.03481777724236,
135.134812123521));
#166662=CARTESIAN_POINT('Ctrl Pts',(-200.702464276177,3.91718807819064,
135.238722817768));
#166663=CARTESIAN_POINT('Ctrl Pts',(-200.698528226736,3.85481798926586,
135.293818761162));
#166664=CARTESIAN_POINT('Ctrl Pts',(-200.694592177296,3.79133090880903,
135.347558271593));
#166665=CARTESIAN_POINT('Ctrl Pts',(-200.690656127855,3.72679275456151,
135.399896095293));
#166666=CARTESIAN_POINT('Ctrl Pts',(-200.683232861449,3.60507580982061,
135.498603597382));
#166667=CARTESIAN_POINT('Ctrl Pts',(-200.675809595044,3.4792505691735,135.592621340272));
#166668=CARTESIAN_POINT('Ctrl Pts',(-200.668386328638,3.34971419766227,
135.681587837666));
#166669=CARTESIAN_POINT('Ctrl Pts',(-200.660971835917,3.22033092738485,
135.770449184047));
#166670=CARTESIAN_POINT('Ctrl Pts',(-200.653557343196,3.08724556180289,
135.854270959279));
#166671=CARTESIAN_POINT('Ctrl Pts',(-200.646142850475,2.95088917404671,
135.93273108439));
#166672=CARTESIAN_POINT('Ctrl Pts',(-200.638735504121,2.81466421171077,
136.011115586678));
#166673=CARTESIAN_POINT('Ctrl Pts',(-200.631328157768,2.67517482505955,
136.084148541912));
#166674=CARTESIAN_POINT('Ctrl Pts',(-200.623920811414,2.53288188521501,
136.151550526111));
#166675=CARTESIAN_POINT('Ctrl Pts',(-200.616518989738,2.3906950728134,136.218902239368));
#166676=CARTESIAN_POINT('Ctrl Pts',(-200.609117168063,2.24570920658458,
136.280631184824));
#166677=CARTESIAN_POINT('Ctrl Pts',(-200.601715346387,2.09841053341921,
136.336503402757));
#166678=CARTESIAN_POINT('Ctrl Pts',(-200.594317432076,1.95118961807727,
136.39234612618));
#166679=CARTESIAN_POINT('Ctrl Pts',(-200.586919517765,1.80165867545395,
136.442338147334));
#166680=CARTESIAN_POINT('Ctrl Pts',(-200.579521603453,1.65032464089478,
136.486293311831));
#166681=CARTESIAN_POINT('Ctrl Pts',(-200.572124918541,1.49901575530602,
136.530241171777));
#166682=CARTESIAN_POINT('Ctrl Pts',(-200.564728233629,1.34590473061233,
136.568154062135));
#166683=CARTESIAN_POINT('Ctrl Pts',(-200.557331548716,1.19151451455393,
136.599895426719));
#166684=CARTESIAN_POINT('Ctrl Pts',(-200.549935191781,1.03713114431951,
136.631635383858));
#166685=CARTESIAN_POINT('Ctrl Pts',(-200.542538834845,0.881469061150174,
136.657204284162));
#166686=CARTESIAN_POINT('Ctrl Pts',(-200.53514247791,0.725062014826754,
136.676516579149));
#166687=CARTESIAN_POINT('Ctrl Pts',(-200.527744988573,0.568631022185253,
136.695831830898));
#166688=CARTESIAN_POINT('Ctrl Pts',(-200.520347499237,0.411455209797665,
136.708888524271));
#166689=CARTESIAN_POINT('Ctrl Pts',(-200.5129500099,0.254073918632435,136.715652947198));
#166690=CARTESIAN_POINT('Ctrl Pts',(-200.505549927385,0.0966374576993343,
136.722419741384));
#166691=CARTESIAN_POINT('Ctrl Pts',(-200.49814984487,-0.0610042527022276,
136.72288985748));
#166692=CARTESIAN_POINT('Ctrl Pts',(-200.490749762355,-0.218311548806333,
136.717081702664));
#166693=CARTESIAN_POINT('Ctrl Pts',(-200.483341542688,-0.375791820453863,
136.711267161183));
#166694=CARTESIAN_POINT('Ctrl Pts',(-200.475933323022,-0.532936570164552,
136.699160575621));
#166695=CARTESIAN_POINT('Ctrl Pts',(-200.468525103355,-0.689210197067142,
136.680832336783));
#166696=CARTESIAN_POINT('Ctrl Pts',(-200.461112324053,-0.845580007779526,
136.66249281722));
#166697=CARTESIAN_POINT('Ctrl Pts',(-200.453699544751,-1.00107725944581,
136.637924072098));
#166698=CARTESIAN_POINT('Ctrl Pts',(-200.446286765449,-1.15517673598396,
136.607247594851));
#166699=CARTESIAN_POINT('Ctrl Pts',(-200.43886339442,-1.30949639708053,
136.576527285615));
#166700=CARTESIAN_POINT('Ctrl Pts',(-200.431440023392,-1.4624139322289,
136.539681901662));
#166701=CARTESIAN_POINT('Ctrl Pts',(-200.424016652363,-1.61341866780536,
136.496882972803));
#166702=CARTESIAN_POINT('Ctrl Pts',(-200.420080602922,-1.69348500191474,
136.474189953777));
#166703=CARTESIAN_POINT('Ctrl Pts',(-200.416144553482,-1.77301389176252,
136.449823992991));
#166704=CARTESIAN_POINT('Ctrl Pts',(-200.412208504041,-1.85193163392452,
136.423816088141));
#166705=CARTESIAN_POINT('Ctrl Pts',(-200.404785237635,-2.00076803270955,
136.37476599127));
#166706=CARTESIAN_POINT('Ctrl Pts',(-200.39736197123,-2.14787943854751,
136.3197245393));
#166707=CARTESIAN_POINT('Ctrl Pts',(-200.389938704824,-2.29274704537207,
136.258830486255));
#166708=CARTESIAN_POINT('Ctrl Pts',(-200.382524212103,-2.43744343071588,
136.198008404924));
#166709=CARTESIAN_POINT('Ctrl Pts',(-200.375109719382,-2.57990095506391,
136.131347634659));
#166710=CARTESIAN_POINT('Ctrl Pts',(-200.367695226661,-2.71961563869954,
136.059036757942));
#166711=CARTESIAN_POINT('Ctrl Pts',(-200.360287880307,-2.85919566006293,
135.986795577171));
#166712=CARTESIAN_POINT('Ctrl Pts',(-200.352880533953,-2.99603777440594,
135.908915301869));
#166713=CARTESIAN_POINT('Ctrl Pts',(-200.3454731876,-3.1296577823218,135.825632640475));
#166714=CARTESIAN_POINT('Ctrl Pts',(-200.338071365924,-3.26317813139457,
135.742412094433));
#166715=CARTESIAN_POINT('Ctrl Pts',(-200.330669544249,-3.39348084363586,
135.653797381792));
#166716=CARTESIAN_POINT('Ctrl Pts',(-200.323267722573,-3.52010625378327,
135.560071134889));
#166717=CARTESIAN_POINT('Ctrl Pts',(-200.315869808262,-3.64666481936232,
135.466394365342));
#166718=CARTESIAN_POINT('Ctrl Pts',(-200.30847189395,-3.76954964959203,
135.367611656931));
#166719=CARTESIAN_POINT('Ctrl Pts',(-200.301073979639,-3.88833011657844,
135.264048887727));
#166720=CARTESIAN_POINT('Ctrl Pts',(-200.293677294726,-4.00709084440596,
135.160503328776));
#166721=CARTESIAN_POINT('Ctrl Pts',(-200.286280609814,-4.12174828160482,
135.052179530682));
#166722=CARTESIAN_POINT('Ctrl Pts',(-200.278883924902,-4.23190487356255,
134.939443652236));
#166723=CARTESIAN_POINT('Ctrl Pts',(-200.271487567967,-4.34205658106188,
134.826712772617));
#166724=CARTESIAN_POINT('Ctrl Pts',(-200.264091211031,-4.44770757924775,
134.709570468634));
#166725=CARTESIAN_POINT('Ctrl Pts',(-200.256694854095,-4.5484973889659,
134.588419558052));
#166726=CARTESIAN_POINT('Ctrl Pts',(-200.249297364759,-4.64930262986123,
134.467250098956));
#166727=CARTESIAN_POINT('Ctrl Pts',(-200.241899875422,-4.74524496160936,
134.342071098237));
#166728=CARTESIAN_POINT('Ctrl Pts',(-200.234502386085,-4.83600449432356,
134.21331809653));
#166729=CARTESIAN_POINT('Ctrl Pts',(-200.22710230357,-4.92679584265112,
134.084519960658));
#166730=CARTESIAN_POINT('Ctrl Pts',(-200.219702221055,-5.01240055972236,
133.952145634283));
#166731=CARTESIAN_POINT('Ctrl Pts',(-200.21230213854,-5.09254243056786,
133.816659101343));
#166732=CARTESIAN_POINT('Ctrl Pts',(-200.204893918873,-5.17277242563903,
133.681023587033));
#166733=CARTESIAN_POINT('Ctrl Pts',(-200.197485699207,-5.24752738802124,
133.542269353312));
#166734=CARTESIAN_POINT('Ctrl Pts',(-200.19007747954,-5.31657703414016,
133.400885064313));
#166735=CARTESIAN_POINT('Ctrl Pts',(-200.182664700238,-5.38566917916411,
133.259413755643));
#166736=CARTESIAN_POINT('Ctrl Pts',(-200.175251920936,-5.44904886082607,
133.115309507039));
#166737=CARTESIAN_POINT('Ctrl Pts',(-200.167839141634,-5.50653440287247,
132.969079867834));
#166738=CARTESIAN_POINT('Ctrl Pts',(-200.160415770605,-5.56410208295706,
132.822641288864));
#166739=CARTESIAN_POINT('Ctrl Pts',(-200.152992399576,-5.615758680887,132.674071605666));
#166740=CARTESIAN_POINT('Ctrl Pts',(-200.145569028547,-5.66137247798355,
132.523893178476));
#166741=CARTESIAN_POINT('Ctrl Pts',(-200.141632979107,-5.68555800768561,
132.44426497292));
#166742=CARTESIAN_POINT('Ctrl Pts',(-200.137696929668,-5.70804554235413,
132.364184668557));
#166743=CARTESIAN_POINT('Ctrl Pts',(-200.133760880228,-5.7288213227283,
132.283731029178));
#166744=CARTESIAN_POINT('Ctrl Pts',(-200.124071939592,-5.77996277961027,
132.085687140804));
#166745=CARTESIAN_POINT('Ctrl Pts',(-200.114382998956,-5.82085499360012,
131.88489595805));
#166746=CARTESIAN_POINT('Ctrl Pts',(-200.10469405832,-5.85125580823402,
131.682276347638));
#166747=CARTESIAN_POINT('Ctrl Pts',(-200.095203709521,-5.88103350483466,
131.483809781632));
#166748=CARTESIAN_POINT('Ctrl Pts',(-200.085713360723,-5.90074552551159,
131.283588737847));
#166749=CARTESIAN_POINT('Ctrl Pts',(-200.076223011924,-5.91020894769956,
131.082498635521));
#166750=CARTESIAN_POINT('Ctrl Pts',(-200.071940411166,-5.91447939759482,
130.991755013462));
#166751=CARTESIAN_POINT('Ctrl Pts',(-200.067657810408,-5.91666348839728,
130.900834742462));
#166752=CARTESIAN_POINT('Ctrl Pts',(-200.06337520965,-5.91674748049752,
130.809820885532));
#166753=CARTESIAN_POINT('',(-198.313375158537,-5.91281518750731,130.803135099679));
#166754=CARTESIAN_POINT('Ctrl Pts',(-200.063375192208,-5.91554583036233,
130.809819405987));
#166755=CARTESIAN_POINT('Ctrl Pts',(-199.994021213611,-5.90217632497919,
129.336193982877));
#166756=CARTESIAN_POINT('Ctrl Pts',(-199.831851360409,-4.59893760167832,
125.869330780398));
#166757=CARTESIAN_POINT('Ctrl Pts',(-199.576865632603,1.22511734593415,
123.91403058054));
#166758=CARTESIAN_POINT('Ctrl Pts',(-199.298418008789,6.45923565506566,
128.110694847157));
#166759=CARTESIAN_POINT('Ctrl Pts',(-199.019970384977,5.7576319483906,134.782706363876));
#166760=CARTESIAN_POINT('Ctrl Pts',(-198.741522761164,-0.234954242897439,
137.798812492739));
#166761=CARTESIAN_POINT('Ctrl Pts',(-198.505991030241,-5.12129580041003,
134.913151181637));
#166762=CARTESIAN_POINT('Ctrl Pts',(-198.363275173922,-5.90520520611573,
131.867199701326));
#166763=CARTESIAN_POINT('Ctrl Pts',(-198.313375192208,-5.90716405999748,
130.803136989425));
#166764=CARTESIAN_POINT('',(-196.563375192208,-5.91754067440713,130.799324060973));
#166765=CARTESIAN_POINT('Ctrl Pts',(-198.313375135094,-5.91674987280848,
130.803133783915));
#166766=CARTESIAN_POINT('Ctrl Pts',(-198.305494209198,-5.91671497079014,
130.634808997274));
#166767=CARTESIAN_POINT('Ctrl Pts',(-198.297613283303,-5.90949285436914,
130.466668773567));
#166768=CARTESIAN_POINT('Ctrl Pts',(-198.289732357408,-5.89515605919228,
130.29932042088));
#166769=CARTESIAN_POINT('Ctrl Pts',(-198.281836630896,-5.88079233908077,
130.131657782929));
#166770=CARTESIAN_POINT('Ctrl Pts',(-198.273940904384,-5.85928727531646,
129.964790277688));
#166771=CARTESIAN_POINT('Ctrl Pts',(-198.266045177872,-5.83076466142615,
129.799316327217));
#166772=CARTESIAN_POINT('Ctrl Pts',(-198.258126453544,-5.80215896996073,
129.633360402175));
#166773=CARTESIAN_POINT('Ctrl Pts',(-198.250207729216,-5.76649488777139,
129.468806441626));
#166774=CARTESIAN_POINT('Ctrl Pts',(-198.242289004889,-5.72394703223156,
129.306241485218));
#166775=CARTESIAN_POINT('Ctrl Pts',(-198.234357905677,-5.6813326855795,
129.143422482521));
#166776=CARTESIAN_POINT('Ctrl Pts',(-198.226426806465,-5.63181316657086,
128.982598970972));
#166777=CARTESIAN_POINT('Ctrl Pts',(-198.218495707253,-5.57561197482526,
128.824339994268));
#166778=CARTESIAN_POINT('Ctrl Pts',(-198.210545405859,-5.51927471297368,
128.665697852811));
#166779=CARTESIAN_POINT('Ctrl Pts',(-198.202595104465,-5.45622353317009,
128.509632936207));
#166780=CARTESIAN_POINT('Ctrl Pts',(-198.194644803071,-5.38672971531874,
128.356693659706));
#166781=CARTESIAN_POINT('Ctrl Pts',(-198.19130570656,-5.35754257470302,
128.292459742115));
#166782=CARTESIAN_POINT('Ctrl Pts',(-198.187966610049,-5.32721951801162,
128.228776855833));
#166783=CARTESIAN_POINT('Ctrl Pts',(-198.184627513538,-5.29578296029053,
128.165684169042));
#166784=CARTESIAN_POINT('Ctrl Pts',(-198.177204247133,-5.22589521009871,
128.025420531639));
#166785=CARTESIAN_POINT('Ctrl Pts',(-198.169780980727,-5.15032541721235,
127.887723278348));
#166786=CARTESIAN_POINT('Ctrl Pts',(-198.162357714322,-5.06928530351928,
127.753085953754));
#166787=CARTESIAN_POINT('Ctrl Pts',(-198.154943221601,-4.98834097251064,
127.618607759295));
#166788=CARTESIAN_POINT('Ctrl Pts',(-198.14752872888,-4.90193938086913,
127.487182611414));
#166789=CARTESIAN_POINT('Ctrl Pts',(-198.14011423616,-4.8103394376285,127.359282235686));
#166790=CARTESIAN_POINT('Ctrl Pts',(-198.132706889806,-4.71882778186184,
127.231505135156));
#166791=CARTESIAN_POINT('Ctrl Pts',(-198.125299543452,-4.62212796504708,
127.107246344862));
#166792=CARTESIAN_POINT('Ctrl Pts',(-198.117892197099,-4.52054368801486,
126.986951112778));
#166793=CARTESIAN_POINT('Ctrl Pts',(-198.110490375423,-4.41903517636901,
126.866745601416));
#166794=CARTESIAN_POINT('Ctrl Pts',(-198.103088553748,-4.31264969804995,
126.750498046109));
#166795=CARTESIAN_POINT('Ctrl Pts',(-198.095686732073,-4.20173288463405,
126.638622828328));
#166796=CARTESIAN_POINT('Ctrl Pts',(-198.088288817762,-4.09087462334089,
126.526806668604));
#166797=CARTESIAN_POINT('Ctrl Pts',(-198.080890903451,-3.97549005300435,
126.419358514093));
#166798=CARTESIAN_POINT('Ctrl Pts',(-198.07349298914,-3.85596343966191,
126.316657807164));
#166799=CARTESIAN_POINT('Ctrl Pts',(-198.066096304228,-3.736456689474,126.213974167229));
#166800=CARTESIAN_POINT('Ctrl Pts',(-198.058699619315,-3.61280954527593,
126.116036652106));
#166801=CARTESIAN_POINT('Ctrl Pts',(-198.051302934403,-3.48544139440895,
126.023186196083));
#166802=CARTESIAN_POINT('Ctrl Pts',(-198.043906577468,-3.35807889117926,
125.930339857147));
#166803=CARTESIAN_POINT('Ctrl Pts',(-198.036510220533,-3.22699601099537,
125.842580348711));
#166804=CARTESIAN_POINT('Ctrl Pts',(-198.029113863598,-3.09264310423706,
125.76020665557));
#166805=CARTESIAN_POINT('Ctrl Pts',(-198.021716374261,-2.95826962770573,
125.677820350807));
#166806=CARTESIAN_POINT('Ctrl Pts',(-198.014318884925,-2.82062544600519,
125.600821698323));
#166807=CARTESIAN_POINT('Ctrl Pts',(-198.006921395588,-2.68018747322264,
125.529464820407));
#166808=CARTESIAN_POINT('Ctrl Pts',(-197.999521313073,-2.53970027012625,
125.458082928449));
#166809=CARTESIAN_POINT('Ctrl Pts',(-197.992121230558,-2.39641765864562,
125.392346917666));
#166810=CARTESIAN_POINT('Ctrl Pts',(-197.984721148044,-2.2508384387309,
125.332463607823));
#166811=CARTESIAN_POINT('Ctrl Pts',(-197.977312928377,-2.10509913949819,
125.272514450125));
#166812=CARTESIAN_POINT('Ctrl Pts',(-197.969904708711,-1.95705853397072,
125.21843098787));
#166813=CARTESIAN_POINT('Ctrl Pts',(-197.962496489045,-1.80723326014781,
125.170371044811));
#166814=CARTESIAN_POINT('Ctrl Pts',(-197.955083709743,-1.65731577136839,
125.122281521658));
#166815=CARTESIAN_POINT('Ctrl Pts',(-197.947670930441,-1.50561178442189,
125.080223004612));
#166816=CARTESIAN_POINT('Ctrl Pts',(-197.940258151139,-1.35264965650991,
125.04430250421));
#166817=CARTESIAN_POINT('Ctrl Pts',(-197.93283478011,-1.19946896913657,
125.008330678912));
#166818=CARTESIAN_POINT('Ctrl Pts',(-197.925411409082,-1.04502691596486,
124.97851445706));
#166819=CARTESIAN_POINT('Ctrl Pts',(-197.917988038053,-0.889859347573362,
124.954909283976));
#166820=CARTESIAN_POINT('Ctrl Pts',(-197.91405198861,-0.807585779573266,
124.942393254802));
#166821=CARTESIAN_POINT('Ctrl Pts',(-197.910115939167,-0.725108295893379,
124.931622504652));
#166822=CARTESIAN_POINT('Ctrl Pts',(-197.906179889724,-0.642506819387798,
124.922599355024));
#166823=CARTESIAN_POINT('Ctrl Pts',(-197.898756623319,-0.486723012682509,
124.905581976438));
#166824=CARTESIAN_POINT('Ctrl Pts',(-197.891333356914,-0.330027094746583,
124.894732254595));
#166825=CARTESIAN_POINT('Ctrl Pts',(-197.883910090508,-0.172948739468105,
124.890138834777));
#166826=CARTESIAN_POINT('Ctrl Pts',(-197.876495597787,-0.0160560377610202,
124.885550844));
#166827=CARTESIAN_POINT('Ctrl Pts',(-197.869081105066,0.141217832067213,
124.887204447401));
#166828=CARTESIAN_POINT('Ctrl Pts',(-197.861666612345,0.298336047272165,
124.895136796674));
#166829=CARTESIAN_POINT('Ctrl Pts',(-197.854259265991,0.455302826025905,
124.90306150045));
#166830=CARTESIAN_POINT('Ctrl Pts',(-197.846851919638,0.612113878507934,
124.917252883675));
#166831=CARTESIAN_POINT('Ctrl Pts',(-197.839444573284,0.768230447271629,
124.937696101643));
#166832=CARTESIAN_POINT('Ctrl Pts',(-197.832042751609,0.924230578407954,
124.958124072289));
#166833=CARTESIAN_POINT('Ctrl Pts',(-197.824640929933,1.07953688863353,
124.984794545045));
#166834=CARTESIAN_POINT('Ctrl Pts',(-197.817239108258,1.23361392477094,
125.017640713587));
#166835=CARTESIAN_POINT('Ctrl Pts',(-197.809841193946,1.38760962484074,
125.050469542891));
#166836=CARTESIAN_POINT('Ctrl Pts',(-197.802443279635,1.54037697901615,
125.089467497698));
#166837=CARTESIAN_POINT('Ctrl Pts',(-197.795045365324,1.69138904650517,
125.134516381975));
#166838=CARTESIAN_POINT('Ctrl Pts',(-197.787648680412,1.84237601852799,
125.179557779945));
#166839=CARTESIAN_POINT('Ctrl Pts',(-197.780251995499,1.99160792542631,
125.23064800505));
#166840=CARTESIAN_POINT('Ctrl Pts',(-197.772855310587,2.1385712404262,125.287618498152));
#166841=CARTESIAN_POINT('Ctrl Pts',(-197.765458953652,2.2855280389187,125.344586465122));
#166842=CARTESIAN_POINT('Ctrl Pts',(-197.758062596717,2.43021609746273,
125.407434046729));
#166843=CARTESIAN_POINT('Ctrl Pts',(-197.750666239781,2.57214044630336,
125.475943959028));
#166844=CARTESIAN_POINT('Ctrl Pts',(-197.743268750445,2.71408652412452,
125.544464360369));
#166845=CARTESIAN_POINT('Ctrl Pts',(-197.735871261108,2.8532677135316,125.618648656259));
#166846=CARTESIAN_POINT('Ctrl Pts',(-197.728473771771,2.98921243053313,
125.698232964672));
#166847=CARTESIAN_POINT('Ctrl Pts',(-197.721073689256,3.12520480274389,
125.777845171241));
#166848=CARTESIAN_POINT('Ctrl Pts',(-197.713673606741,3.25795812173416,
125.862860970739));
#166849=CARTESIAN_POINT('Ctrl Pts',(-197.706273524226,3.38702877062359,
125.952972499772));
#166850=CARTESIAN_POINT('Ctrl Pts',(-197.69886530456,3.51624134596045,126.043183115696));
#166851=CARTESIAN_POINT('Ctrl Pts',(-197.691457084894,3.64176285786007,
126.138500437448));
#166852=CARTESIAN_POINT('Ctrl Pts',(-197.684048865227,3.76318126927204,
126.238575110438));
#166853=CARTESIAN_POINT('Ctrl Pts',(-197.676636085925,3.88467441169026,
126.33871137772));
#166854=CARTESIAN_POINT('Ctrl Pts',(-197.669223306623,4.002059143761,126.443610582622));
#166855=CARTESIAN_POINT('Ctrl Pts',(-197.661810527321,4.11495984451519,
126.552886045076));
#166856=CARTESIAN_POINT('Ctrl Pts',(-197.654387156293,4.2280218630853,126.662317645436));
#166857=CARTESIAN_POINT('Ctrl Pts',(-197.646963785264,4.33658679716489,
126.776137722587));
#166858=CARTESIAN_POINT('Ctrl Pts',(-197.639540414235,4.4403183587074,126.893925419813));
#166859=CARTESIAN_POINT('Ctrl Pts',(-197.635604364794,4.49531932164588,
126.956379283164));
#166860=CARTESIAN_POINT('Ctrl Pts',(-197.631668315353,4.54896215332004,
127.019948072493));
#166861=CARTESIAN_POINT('Ctrl Pts',(-197.627732265912,4.60120170033201,
127.084565801267));
#166862=CARTESIAN_POINT('Ctrl Pts',(-197.620308999507,4.69972385564997,
127.206432821078));
#166863=CARTESIAN_POINT('Ctrl Pts',(-197.612885733101,4.79355000507247,
127.332400995022));
#166864=CARTESIAN_POINT('Ctrl Pts',(-197.605462466696,4.88231926713834,
127.462072608398));
#166865=CARTESIAN_POINT('Ctrl Pts',(-197.598047973975,4.97098361130828,
127.591590960695));
#166866=CARTESIAN_POINT('Ctrl Pts',(-197.590633481254,5.05460275620507,
127.72480373464));
#166867=CARTESIAN_POINT('Ctrl Pts',(-197.583218988533,5.13285527925053,
127.861279367452));
#166868=CARTESIAN_POINT('Ctrl Pts',(-197.575811642179,5.21103237956813,
127.997623459912));
#166869=CARTESIAN_POINT('Ctrl Pts',(-197.568404295825,5.28385297112994,
128.137223828763));
#166870=CARTESIAN_POINT('Ctrl Pts',(-197.560996949471,5.35103833164711,
128.279619178182));
#166871=CARTESIAN_POINT('Ctrl Pts',(-197.553595127796,5.41817358278764,
128.421908323777));
#166872=CARTESIAN_POINT('Ctrl Pts',(-197.54619330612,5.47968181295513,128.566987963062));
#166873=CARTESIAN_POINT('Ctrl Pts',(-197.538791484445,5.53532980268285,
128.714371493663));
#166874=CARTESIAN_POINT('Ctrl Pts',(-197.531393570133,5.59094841626997,
128.861677221646));
#166875=CARTESIAN_POINT('Ctrl Pts',(-197.523995655822,5.64071281889356,
129.011284070463));
#166876=CARTESIAN_POINT('Ctrl Pts',(-197.516597741511,5.6844376278525,129.162684822059));
#166877=CARTESIAN_POINT('Ctrl Pts',(-197.509201056598,5.72815517054139,
129.314060413596));
#166878=CARTESIAN_POINT('Ctrl Pts',(-197.501804371686,5.76583500808062,
129.467228957956));
#166879=CARTESIAN_POINT('Ctrl Pts',(-197.494407686774,5.79734138028169,
129.621667300187));
#166880=CARTESIAN_POINT('Ctrl Pts',(-197.487011329838,5.82884635545729,
129.77609879446));
#166881=CARTESIAN_POINT('Ctrl Pts',(-197.479614972903,5.85417833496008,
129.93179960889));
#166882=CARTESIAN_POINT('Ctrl Pts',(-197.472218615968,5.87325258268416,
130.088235864123));
#166883=CARTESIAN_POINT('Ctrl Pts',(-197.464821126631,5.89232975072421,
130.244696070146));
#166884=CARTESIAN_POINT('Ctrl Pts',(-197.457423637294,5.90514723414698,
130.401891570591));
#166885=CARTESIAN_POINT('Ctrl Pts',(-197.450026147958,5.91167214170678,
130.559282973812));
#166886=CARTESIAN_POINT('Ctrl Pts',(-197.442626065443,5.91819933656282,
130.716729550346));
#166887=CARTESIAN_POINT('Ctrl Pts',(-197.435225982928,5.9184295482666,130.874371793638));
#166888=CARTESIAN_POINT('Ctrl Pts',(-197.427825900413,5.91238200524872,
131.03167006856));
#166889=CARTESIAN_POINT('Ctrl Pts',(-197.420417680746,5.9063278123356,131.189141309106));
#166890=CARTESIAN_POINT('Ctrl Pts',(-197.41300946108,5.89398209323351,131.346267452684));
#166891=CARTESIAN_POINT('Ctrl Pts',(-197.405601241413,5.87541605376114,
131.502513006165));
#166892=CARTESIAN_POINT('Ctrl Pts',(-197.398188462111,5.85683858720126,
131.658854726177));
#166893=CARTESIAN_POINT('Ctrl Pts',(-197.390775682809,5.83203323018161,
131.814314408332));
#166894=CARTESIAN_POINT('Ctrl Pts',(-197.383362903507,5.80112227528612,
131.96836702205));
#166895=CARTESIAN_POINT('Ctrl Pts',(-197.375939532478,5.77016715336866,
132.122639753366));
#166896=CARTESIAN_POINT('Ctrl Pts',(-197.368516161449,5.73308909762374,
132.275501039037));
#166897=CARTESIAN_POINT('Ctrl Pts',(-197.361092790421,5.69006041482304,
132.426440467069));
#166898=CARTESIAN_POINT('Ctrl Pts',(-197.35715674098,5.66724557474622,132.506472173542));
#166899=CARTESIAN_POINT('Ctrl Pts',(-197.35322069154,5.64275861274537,132.585963890444));
#166900=CARTESIAN_POINT('Ctrl Pts',(-197.3492846421,5.6166306386455,132.664841961608));
#166901=CARTESIAN_POINT('Ctrl Pts',(-197.341861375694,5.56735409491276,
132.813603542143));
#166902=CARTESIAN_POINT('Ctrl Pts',(-197.334438109289,5.51208882816386,
132.960631013906));
#166903=CARTESIAN_POINT('Ctrl Pts',(-197.327014842883,5.45097438179734,
133.105405782592));
#166904=CARTESIAN_POINT('Ctrl Pts',(-197.319600350162,5.38993216763119,
133.250009439524));
#166905=CARTESIAN_POINT('Ctrl Pts',(-197.312185857442,5.32305467845807,
133.392365352562));
#166906=CARTESIAN_POINT('Ctrl Pts',(-197.304771364721,5.25053126351302,
133.531969829563));
#166907=CARTESIAN_POINT('Ctrl Pts',(-197.297364018367,5.17807774936575,
133.671439750514));
#166908=CARTESIAN_POINT('Ctrl Pts',(-197.289956672013,5.09998931384532,
133.808163185873));
#166909=CARTESIAN_POINT('Ctrl Pts',(-197.282549325659,5.01650340198775,
133.941656297024));
#166910=CARTESIAN_POINT('Ctrl Pts',(-197.275147503984,4.93307975707299,
134.075049843976));
#166911=CARTESIAN_POINT('Ctrl Pts',(-197.267745682308,4.84426684850198,
134.20521754882));
#166912=CARTESIAN_POINT('Ctrl Pts',(-197.260343860633,4.75034800781524,
134.331700176943));
#166913=CARTESIAN_POINT('Ctrl Pts',(-197.252945946322,4.65647874615343,
134.458116035871));
#166914=CARTESIAN_POINT('Ctrl Pts',(-197.24554803201,4.55750914234047,134.580850393335));
#166915=CARTESIAN_POINT('Ctrl Pts',(-197.238150117699,4.453765729412,134.699473117869));
#166916=CARTESIAN_POINT('Ctrl Pts',(-197.230753432787,4.3500395567568,134.818076129458));
#166917=CARTESIAN_POINT('Ctrl Pts',(-197.223356747875,4.24154139500116,
134.932568583504));
#166918=CARTESIAN_POINT('Ctrl Pts',(-197.215960062963,4.12863800752296,
135.042553483085));
#166919=CARTESIAN_POINT('Ctrl Pts',(-197.208563706027,4.01573962629928,
135.152533505821));
#166920=CARTESIAN_POINT('Ctrl Pts',(-197.201167349092,3.89843667513432,
135.258006111018));
#166921=CARTESIAN_POINT('Ctrl Pts',(-197.193770992156,3.77713251991294,
135.35861143296));
#166922=CARTESIAN_POINT('Ctrl Pts',(-197.18637350282,3.65580979271537,135.459232157834));
#166923=CARTESIAN_POINT('Ctrl Pts',(-197.178976013483,3.53048492905807,
135.554983877352));
#166924=CARTESIAN_POINT('Ctrl Pts',(-197.171578524146,3.40159395588911,
135.645547364817));
#166925=CARTESIAN_POINT('Ctrl Pts',(-197.164178441631,3.27265780018913,
135.736142599172));
#166926=CARTESIAN_POINT('Ctrl Pts',(-197.156778359116,3.14015335129741,
135.821545765924));
#166927=CARTESIAN_POINT('Ctrl Pts',(-197.149378276601,3.00454501296717,
135.901481356528));
#166928=CARTESIAN_POINT('Ctrl Pts',(-197.141970056935,2.86878755932826,
135.981504844531));
#166929=CARTESIAN_POINT('Ctrl Pts',(-197.134561837268,2.72991972195824,
136.056048560025));
#166930=CARTESIAN_POINT('Ctrl Pts',(-197.127153617602,2.58843051487615,
136.124882963366));
#166931=CARTESIAN_POINT('Ctrl Pts',(-197.1197408383,2.44685422354838,136.193759733134));
#166932=CARTESIAN_POINT('Ctrl Pts',(-197.112328058998,2.3026536887318,136.256920039268));
#166933=CARTESIAN_POINT('Ctrl Pts',(-197.104915279696,2.15633673565307,
136.31418297813));
#166934=CARTESIAN_POINT('Ctrl Pts',(-197.097491908667,2.00981071804999,
136.371527736965));
#166935=CARTESIAN_POINT('Ctrl Pts',(-197.090068537638,1.86116259434809,
136.422958177311));
#166936=CARTESIAN_POINT('Ctrl Pts',(-197.08264516661,1.71091492463178,136.468343375588));
#166937=CARTESIAN_POINT('Ctrl Pts',(-197.078709117169,1.63125000500077,
136.492407696719));
#166938=CARTESIAN_POINT('Ctrl Pts',(-197.074773067728,1.55113557114578,
136.514773336763));
#166939=CARTESIAN_POINT('Ctrl Pts',(-197.070837018287,1.47065040770534,
136.535426656342));
#166940=CARTESIAN_POINT('Ctrl Pts',(-197.063413751881,1.31885790131885,
136.574378172499));
#166941=CARTESIAN_POINT('Ctrl Pts',(-197.055990485476,1.16528729868185,
136.607353878223));
#166942=CARTESIAN_POINT('Ctrl Pts',(-197.04856721907,1.01045033448641,136.634190862439));
#166943=CARTESIAN_POINT('Ctrl Pts',(-197.041152726349,0.855796374724231,
136.660996127568));
#166944=CARTESIAN_POINT('Ctrl Pts',(-197.033738233628,0.699879396883509,
136.681677050091));
#166945=CARTESIAN_POINT('Ctrl Pts',(-197.026323740907,0.543225519315743,
136.696120676976));
#166946=CARTESIAN_POINT('Ctrl Pts',(-197.018916394553,0.38672263065309,
136.71055038255));
#166947=CARTESIAN_POINT('Ctrl Pts',(-197.011509048199,0.229484625460507,
136.718754726634));
#166948=CARTESIAN_POINT('Ctrl Pts',(-197.004101701846,0.072046915710644,
136.720671951872));
#166949=CARTESIAN_POINT('Ctrl Pts',(-196.99669988017,-0.0852733710555033,
136.722587747171));
#166950=CARTESIAN_POINT('Ctrl Pts',(-196.989298058495,-0.242792694141263,
136.718225755868));
#166951=CARTESIAN_POINT('Ctrl Pts',(-196.981896236819,-0.399971538843124,
136.707576125289));
#166952=CARTESIAN_POINT('Ctrl Pts',(-196.974498322508,-0.557067410055896,
136.696932116566));
#166953=CARTESIAN_POINT('Ctrl Pts',(-196.967100408196,-0.71382278933619,
136.680007104075));
#166954=CARTESIAN_POINT('Ctrl Pts',(-196.959702493885,-0.869699295819346,
136.656843312743));
#166955=CARTESIAN_POINT('Ctrl Pts',(-196.952305808973,-1.02554989845523,
136.633683370814));
#166956=CARTESIAN_POINT('Ctrl Pts',(-196.944909124061,-1.18052154928376,
136.604286762546));
#166957=CARTESIAN_POINT('Ctrl Pts',(-196.937512439148,-1.33408199898751,
136.568747469823));
#166958=CARTESIAN_POINT('Ctrl Pts',(-196.930116082213,-1.48763563966,136.533209752951));
#166959=CARTESIAN_POINT('Ctrl Pts',(-196.922719725277,-1.63977783994152,
136.491529977363));
#166960=CARTESIAN_POINT('Ctrl Pts',(-196.915323368342,-1.7899878054991,
136.443852989993));
#166961=CARTESIAN_POINT('Ctrl Pts',(-196.907925879005,-1.94022076858587,
136.396168703155));
#166962=CARTESIAN_POINT('Ctrl Pts',(-196.900528389669,-2.08852055208359,
136.34248548924));
#166963=CARTESIAN_POINT('Ctrl Pts',(-196.893130900332,-2.23438289831461,
136.28299764024));
#166964=CARTESIAN_POINT('Ctrl Pts',(-196.885730817817,-2.38029637636477,
136.223488937868));
#166965=CARTESIAN_POINT('Ctrl Pts',(-196.878330735302,-2.52377037052379,
136.158171690011));
#166966=CARTESIAN_POINT('Ctrl Pts',(-196.870930652787,-2.66432206607766,
136.087287693602));
#166967=CARTESIAN_POINT('Ctrl Pts',(-196.86352243312,-2.80502831267005,
136.016325752951));
#166968=CARTESIAN_POINT('Ctrl Pts',(-196.856114213454,-2.9428055098375,
135.939785007485));
#166969=CARTESIAN_POINT('Ctrl Pts',(-196.848705993787,-3.07719621535446,
135.857952806763));
#166970=CARTESIAN_POINT('Ctrl Pts',(-196.841293214485,-3.21166963610861,
135.776070239686));
#166971=CARTESIAN_POINT('Ctrl Pts',(-196.833880435183,-3.3427521018158,
135.688889934013));
#166972=CARTESIAN_POINT('Ctrl Pts',(-196.826467655881,-3.47001692118132,
135.596741354654));
#166973=CARTESIAN_POINT('Ctrl Pts',(-196.819044284852,-3.59746358248833,
135.504461109084));
#166974=CARTESIAN_POINT('Ctrl Pts',(-196.811620913823,-3.72108141033138,
135.407198641944));
#166975=CARTESIAN_POINT('Ctrl Pts',(-196.804197542794,-3.84047779850241,
135.305322830439));
#166976=CARTESIAN_POINT('Ctrl Pts',(-196.800261493354,-3.90378462838005,
135.251305830709));
#166977=CARTESIAN_POINT('Ctrl Pts',(-196.796325443914,-3.96590528316954,
135.195992463312));
#166978=CARTESIAN_POINT('Ctrl Pts',(-196.792389394474,-4.02678570265285,
135.139441639578));
#166979=CARTESIAN_POINT('Ctrl Pts',(-196.78507668251,-4.13989428490648,
135.034376931548));
#166980=CARTESIAN_POINT('Ctrl Pts',(-196.777763970547,-4.24908372070728,
134.924700531894));
#166981=CARTESIAN_POINT('Ctrl Pts',(-196.770451258584,-4.35394615139191,
134.810740963125));
#166982=CARTESIAN_POINT('Ctrl Pts',(-196.763147289429,-4.45868321243069,
134.696917640204));
#166983=CARTESIAN_POINT('Ctrl Pts',(-196.755843320274,-4.55910330236656,
134.578821616739));
#166984=CARTESIAN_POINT('Ctrl Pts',(-196.748539351119,-4.65483230230702,
134.456820993792));
#166985=CARTESIAN_POINT('Ctrl Pts',(-196.741242407847,-4.75046921796755,
134.3349377265));
#166986=CARTESIAN_POINT('Ctrl Pts',(-196.733945464575,-4.84142378676094,
134.209157634796));
#166987=CARTESIAN_POINT('Ctrl Pts',(-196.726648521302,-4.92735958258975,
134.079884714006));
#166988=CARTESIAN_POINT('Ctrl Pts',(-196.719357248112,-5.01322860210467,
133.950712244595));
#166989=CARTESIAN_POINT('Ctrl Pts',(-196.712065974921,-5.09408640058275,
133.818052669374));
#166990=CARTESIAN_POINT('Ctrl Pts',(-196.704774701731,-5.16963782844034,
133.682341730301));
#166991=CARTESIAN_POINT('Ctrl Pts',(-196.697486477277,-5.24515766559986,
133.546687536724));
#166992=CARTESIAN_POINT('Ctrl Pts',(-196.690198252823,-5.31537535882009,
133.407984853367));
#166993=CARTESIAN_POINT('Ctrl Pts',(-196.682910028369,-5.38004001794075,
133.266696900013));
#166994=CARTESIAN_POINT('Ctrl Pts',(-196.675623313027,-5.44469128748668,
133.125438201984));
#166995=CARTESIAN_POINT('Ctrl Pts',(-196.668336597685,-5.50379165095616,
132.98159564949));
#166996=CARTESIAN_POINT('Ctrl Pts',(-196.661049882344,-5.5571371184965,
132.835655182303));
#166997=CARTESIAN_POINT('Ctrl Pts',(-196.653763137853,-5.61048279943774,
132.689714131302));
#166998=CARTESIAN_POINT('Ctrl Pts',(-196.646476393361,-5.65807340793315,
132.541675511368));
#166999=CARTESIAN_POINT('Ctrl Pts',(-196.63918964887,-5.69975396984224,
132.392042967965));
#167000=CARTESIAN_POINT('Ctrl Pts',(-196.631898500147,-5.74145972418876,
132.242319984118));
#167001=CARTESIAN_POINT('Ctrl Pts',(-196.624607351424,-5.77724819432482,
132.091001524323));
#167002=CARTESIAN_POINT('Ctrl Pts',(-196.617316202701,-5.80701487487784,
131.938604332756));
#167003=CARTESIAN_POINT('Ctrl Pts',(-196.61002256742,-5.83679170699883,
131.786155167962));
#167004=CARTESIAN_POINT('Ctrl Pts',(-196.602728932139,-5.86054259825711,
131.632626918938));
#167005=CARTESIAN_POINT('Ctrl Pts',(-196.595435296857,-5.87821471232728,
131.478543351162));
#167006=CARTESIAN_POINT('Ctrl Pts',(-196.58813424297,-5.89590480130939,
131.324303059717));
#167007=CARTESIAN_POINT('Ctrl Pts',(-196.580833189082,-5.90750373817299,
131.169506705419));
#167008=CARTESIAN_POINT('Ctrl Pts',(-196.573532135195,-5.91301075271542,
131.014680375962));
#167009=CARTESIAN_POINT('Ctrl Pts',(-196.570146487533,-5.91556446772689,
130.942884247832));
#167010=CARTESIAN_POINT('Ctrl Pts',(-196.56676083987,-5.91680893090054,
130.871081648203));
#167011=CARTESIAN_POINT('Ctrl Pts',(-196.563375192208,-5.91674785692228,
130.799324735758));
#167012=CARTESIAN_POINT('',(-194.813375192208,-5.92378430407072,130.807954965743));
#167013=CARTESIAN_POINT('Ctrl Pts',(-196.563375192208,-5.92005028606524,
130.799321924984));
#167014=CARTESIAN_POINT('Ctrl Pts',(-196.546897385026,-5.92321501407519,
130.449886125491));
#167015=CARTESIAN_POINT('Ctrl Pts',(-196.530419577843,-5.89494931063627,
130.100961680412));
#167016=CARTESIAN_POINT('Ctrl Pts',(-196.421125896056,-5.48691602341415,
127.826183567757));
#167017=CARTESIAN_POINT('Ctrl Pts',(-196.235494146848,-2.68383279408233,
124.341033141431));
#167018=CARTESIAN_POINT('Ctrl Pts',(-195.957046523035,3.98710327515676,
125.052789701408));
#167019=CARTESIAN_POINT('Ctrl Pts',(-195.678598899222,6.99408621534913,
131.049958953475));
#167020=CARTESIAN_POINT('Ctrl Pts',(-195.400151275409,3.57384560374378,
136.821435332985));
#167021=CARTESIAN_POINT('Ctrl Pts',(-195.121703651596,-3.13058452563971,
137.063513999468));
#167022=CARTESIAN_POINT('Ctrl Pts',(-194.926111623863,-5.81921701947016,
133.19324015144));
#167023=CARTESIAN_POINT('Ctrl Pts',(-194.823335470733,-5.92529114525991,
131.018830628555));
#167024=CARTESIAN_POINT('Ctrl Pts',(-194.813375192208,-5.92378430407072,
130.807954965743));
#167025=CARTESIAN_POINT('',(-193.063375192208,-5.90877653025682,130.807662282052));
#167026=CARTESIAN_POINT('Ctrl Pts',(-194.813375192208,-5.92378430407072,
130.807954965743));
#167027=CARTESIAN_POINT('Ctrl Pts',(-194.730519596129,-5.91124949145352,
129.053764187153));
#167028=CARTESIAN_POINT('Ctrl Pts',(-194.554848125446,-4.15536005181142,
125.312715685492));
#167029=CARTESIAN_POINT('Ctrl Pts',(-194.286360780158,2.21070539777845,
124.164304731159));
#167030=CARTESIAN_POINT('Ctrl Pts',(-194.007913156345,6.78140734036955,
129.075177280167));
#167031=CARTESIAN_POINT('Ctrl Pts',(-193.729465532532,5.12032722732323,
135.575084840937));
#167032=CARTESIAN_POINT('Ctrl Pts',(-193.451017908719,-1.24608346573943,
137.690929903266));
#167033=CARTESIAN_POINT('Ctrl Pts',(-193.228987795278,-5.40948930689292,
134.331882897925));
#167034=CARTESIAN_POINT('Ctrl Pts',(-193.099773556441,-5.91269277027163,
131.5832887094));
#167035=CARTESIAN_POINT('Ctrl Pts',(-193.063375192208,-5.90877653025682,
130.807662282052));
#167036=CARTESIAN_POINT('',(-191.313375192208,-5.91167657527647,130.799567797019));
#167037=CARTESIAN_POINT('Ctrl Pts',(-193.063375192208,-5.90877653025682,
130.807662282052));
#167038=CARTESIAN_POINT('Ctrl Pts',(-193.006957681836,-5.90270635330487,
129.605440343458));
#167039=CARTESIAN_POINT('Ctrl Pts',(-192.857724296862,-4.96095598029521,
126.416633059624));
#167040=CARTESIAN_POINT('Ctrl Pts',(-192.61567503728,0.256241860122023,
123.810656260109));
#167041=CARTESIAN_POINT('Ctrl Pts',(-192.337227413466,6.02250653238034,
127.239676115707));
#167042=CARTESIAN_POINT('Ctrl Pts',(-192.058779789655,6.25438191717603,
133.944466883987));
#167043=CARTESIAN_POINT('Ctrl Pts',(-191.780332165841,0.738785863635208,
137.763653396148));
#167044=CARTESIAN_POINT('Ctrl Pts',(-191.531863966693,-4.78877897888325,
135.464945051595));
#167045=CARTESIAN_POINT('Ctrl Pts',(-191.376211642148,-5.90155266118287,
132.136924284238));
#167046=CARTESIAN_POINT('Ctrl Pts',(-191.313375192208,-5.91167657527647,
130.799567797019));
#167047=CARTESIAN_POINT('',(-189.563375998339,-5.92191640313042,130.80298505409));
#167048=CARTESIAN_POINT('Ctrl Pts',(-191.313375192208,-5.91167657527647,
130.799567797019));
#167049=CARTESIAN_POINT('Ctrl Pts',(-191.283395767544,-5.91650671956634,
130.161511730902));
#167050=CARTESIAN_POINT('Ctrl Pts',(-191.160600468276,-5.52689340955663,
127.553783705044));
#167051=CARTESIAN_POINT('Ctrl Pts',(-190.944989294402,-1.71886118746277,
124.020329607269));
#167052=CARTESIAN_POINT('Ctrl Pts',(-190.66654167059,4.77851096535738,125.691299549647));
#167053=CARTESIAN_POINT('Ctrl Pts',(-190.388094046777,6.88466498425298,
132.060922826512));
#167054=CARTESIAN_POINT('Ctrl Pts',(-190.109646422965,2.66414821720038,
137.275826819836));
#167055=CARTESIAN_POINT('Ctrl Pts',(-189.834740626303,-3.91976489026385,
136.553081220811));
#167056=CARTESIAN_POINT('Ctrl Pts',(-189.65265070425,-5.9201422633631,132.691092662961));
#167057=CARTESIAN_POINT('Ctrl Pts',(-189.563376656799,-5.92613653540298,
130.802997987718));
#167058=CARTESIAN_POINT('',(-187.813375192208,-5.91590714834001,130.809830359851));
#167059=CARTESIAN_POINT('Ctrl Pts',(-189.563375192208,-5.91674983639772,
130.802969219882));
#167060=CARTESIAN_POINT('Ctrl Pts',(-189.559833853251,-5.91673225127943,
130.728190637922));
#167061=CARTESIAN_POINT('Ctrl Pts',(-189.556292514295,-5.91529709555501,
130.653430419199));
#167062=CARTESIAN_POINT('Ctrl Pts',(-189.552751175338,-5.91244610460354,
130.578724577319));
#167063=CARTESIAN_POINT('Ctrl Pts',(-189.545327908933,-5.90646992847011,
130.42212805461));
#167064=CARTESIAN_POINT('Ctrl Pts',(-189.537904642528,-5.89425901609847,
130.265532330591));
#167065=CARTESIAN_POINT('Ctrl Pts',(-189.530481376122,-5.87580323340804,
130.109474350058));
#167066=CARTESIAN_POINT('Ctrl Pts',(-189.523066883401,-5.85736926392009,
129.953600817098));
#167067=CARTESIAN_POINT('Ctrl Pts',(-189.51565239068,-5.832705159285,129.798264129616));
#167068=CARTESIAN_POINT('Ctrl Pts',(-189.508237897959,-5.80185277077408,
129.644000764434));
#167069=CARTESIAN_POINT('Ctrl Pts',(-189.500830551605,-5.77103011895677,
129.48988608409));
#167070=CARTESIAN_POINT('Ctrl Pts',(-189.493423205251,-5.73403113012844,
129.336843030134));
#167071=CARTESIAN_POINT('Ctrl Pts',(-189.486015858898,-5.69094937483769,
129.18540237983));
#167072=CARTESIAN_POINT('Ctrl Pts',(-189.478614037222,-5.64789975154543,
129.034074679676));
#167073=CARTESIAN_POINT('Ctrl Pts',(-189.471212215547,-5.59877649678882,
128.884347361008));
#167074=CARTESIAN_POINT('Ctrl Pts',(-189.463810393871,-5.54372409889164,
128.73674032412));
#167075=CARTESIAN_POINT('Ctrl Pts',(-189.45641247956,-5.48870076272677,
128.589211207839));
#167076=CARTESIAN_POINT('Ctrl Pts',(-189.449014565249,-5.42775464698324,
128.443800493114));
#167077=CARTESIAN_POINT('Ctrl Pts',(-189.441616650937,-5.36107982942442,
128.301012135025));
#167078=CARTESIAN_POINT('Ctrl Pts',(-189.434219966025,-5.29441609201077,
128.158247505772));
#167079=CARTESIAN_POINT('Ctrl Pts',(-189.426823281113,-5.22202570001855,
128.018104706153));
#167080=CARTESIAN_POINT('Ctrl Pts',(-189.419426596201,-5.14415058741227,
127.881067047545));
#167081=CARTESIAN_POINT('Ctrl Pts',(-189.412030239265,-5.06627892787009,
127.744035465331));
#167082=CARTESIAN_POINT('Ctrl Pts',(-189.40463388233,-4.98292321570959,
127.610109074916));
#167083=CARTESIAN_POINT('Ctrl Pts',(-189.397237525395,-4.89437086740681,
127.479745696289));
#167084=CARTESIAN_POINT('Ctrl Pts',(-189.389840036058,-4.80580496151345,
127.349362358695));
#167085=CARTESIAN_POINT('Ctrl Pts',(-189.382442546721,-4.71204104506515,
127.222543427878));
#167086=CARTESIAN_POINT('Ctrl Pts',(-189.375045057385,-4.61340920620913,
127.099716767131));
#167087=CARTESIAN_POINT('Ctrl Pts',(-189.36764497487,-4.51474279211475,
126.976847049689));
#167088=CARTESIAN_POINT('Ctrl Pts',(-189.360244892355,-4.41120529168435,
126.857972679567));
#167089=CARTESIAN_POINT('Ctrl Pts',(-189.35284480984,-4.30316620541695,
126.74348741454));
#167090=CARTESIAN_POINT('Ctrl Pts',(-189.345436590173,-4.19500831906767,
126.628876261194));
#167091=CARTESIAN_POINT('Ctrl Pts',(-189.338028370507,-4.08233921785816,
126.518664122988));
#167092=CARTESIAN_POINT('Ctrl Pts',(-189.33062015084,-3.96556482232641,
126.413207443008));
#167093=CARTESIAN_POINT('Ctrl Pts',(-189.323207371538,-3.84871855410236,
126.307685856202));
#167094=CARTESIAN_POINT('Ctrl Pts',(-189.315794592236,-3.72776224286292,
126.206925798223));
#167095=CARTESIAN_POINT('Ctrl Pts',(-189.308381812934,-3.6031334002335,
126.111242223297));
#167096=CARTESIAN_POINT('Ctrl Pts',(-189.300958441905,-3.4783264820694,
126.015421931193));
#167097=CARTESIAN_POINT('Ctrl Pts',(-189.293535070877,-3.349836856241,125.924692823797));
#167098=CARTESIAN_POINT('Ctrl Pts',(-189.286111699848,-3.21813008347746,
125.839325942126));
#167099=CARTESIAN_POINT('Ctrl Pts',(-189.282175650407,-3.14829599229798,
125.794062373115));
#167100=CARTESIAN_POINT('Ctrl Pts',(-189.278239600966,-3.07755785156217,
125.750305547236));
#167101=CARTESIAN_POINT('Ctrl Pts',(-189.274303551526,-3.00598754805893,
125.708090469368));
#167102=CARTESIAN_POINT('Ctrl Pts',(-189.26688028512,-2.8710081892836,125.628474149996));
#167103=CARTESIAN_POINT('Ctrl Pts',(-189.259457018715,-2.73265947523997,
125.55410372251));
#167104=CARTESIAN_POINT('Ctrl Pts',(-189.252033752309,-2.59138767507411,
125.485277944776));
#167105=CARTESIAN_POINT('Ctrl Pts',(-189.244619259588,-2.45028284644415,
125.416533513396));
#167106=CARTESIAN_POINT('Ctrl Pts',(-189.237204766867,-2.30626214089305,
125.353320849256));
#167107=CARTESIAN_POINT('Ctrl Pts',(-189.229790274146,-2.15979953319767,
125.295894720522));
#167108=CARTESIAN_POINT('Ctrl Pts',(-189.222382927793,-2.01347809167781,
125.238523941253));
#167109=CARTESIAN_POINT('Ctrl Pts',(-189.214975581439,-1.86471977876785,
125.186928729472));
#167110=CARTESIAN_POINT('Ctrl Pts',(-189.207568235085,-1.71402172957951,
125.141317259704));
#167111=CARTESIAN_POINT('Ctrl Pts',(-189.20016641341,-1.56343607668177,
125.09573980869));
#167112=CARTESIAN_POINT('Ctrl Pts',(-189.192764591734,-1.4109139238907,
125.056137321127));
#167113=CARTESIAN_POINT('Ctrl Pts',(-189.185362770059,-1.25697077751556,
125.022669253703));
#167114=CARTESIAN_POINT('Ctrl Pts',(-189.177964855747,-1.10310889652911,
124.989218853811));
#167115=CARTESIAN_POINT('Ctrl Pts',(-189.170566941436,-0.94782787973478,
124.961896503906));
#167116=CARTESIAN_POINT('Ctrl Pts',(-189.163169027125,-0.791656622585064,
124.940811320901));
#167117=CARTESIAN_POINT('Ctrl Pts',(-189.155772342213,-0.635511318265274,
124.919729641871));
#167118=CARTESIAN_POINT('Ctrl Pts',(-189.1483756573,-0.478476436789943,
124.904883122484));
#167119=CARTESIAN_POINT('Ctrl Pts',(-189.140978972388,-0.321089372926129,
124.896329458449));
#167120=CARTESIAN_POINT('Ctrl Pts',(-189.133582615453,-0.163709287769656,
124.887776173693));
#167121=CARTESIAN_POINT('Ctrl Pts',(-189.126186258517,-0.00597742402233353,
124.885515209737));
#167122=CARTESIAN_POINT('Ctrl Pts',(-189.118789901582,0.151565685768833,
124.889552217846));
#167123=CARTESIAN_POINT('Ctrl Pts',(-189.111392412245,0.309132915812747,
124.893589844031));
#167124=CARTESIAN_POINT('Ctrl Pts',(-189.103994922909,0.466510961159943,
124.90392735264));
#167125=CARTESIAN_POINT('Ctrl Pts',(-189.096597433572,0.623161427596432,
124.920518301727));
#167126=CARTESIAN_POINT('Ctrl Pts',(-189.089197351057,0.779866807610867,
124.937115066746));
#167127=CARTESIAN_POINT('Ctrl Pts',(-189.081797268542,0.935843729918489,
124.959969597473));
#167128=CARTESIAN_POINT('Ctrl Pts',(-189.074397186027,1.09056119090591,
124.988983858371));
#167129=CARTESIAN_POINT('Ctrl Pts',(-189.06698896636,1.24544877964724,125.018030023431));
#167130=CARTESIAN_POINT('Ctrl Pts',(-189.059580746694,1.39907377419055,
125.053249376451));
#167131=CARTESIAN_POINT('Ctrl Pts',(-189.052172527027,1.55091687890397,
125.094493071184));
#167132=CARTESIAN_POINT('Ctrl Pts',(-189.044759747725,1.7028534405147,125.135762150722));
#167133=CARTESIAN_POINT('Ctrl Pts',(-189.037346968423,1.85300557171295,
125.183062848489));
#167134=CARTESIAN_POINT('Ctrl Pts',(-189.029934189121,2.00087180686703,
125.236197314017));
#167135=CARTESIAN_POINT('Ctrl Pts',(-189.022510818092,2.14894932023193,
125.289407700562));
#167136=CARTESIAN_POINT('Ctrl Pts',(-189.015087447064,2.29473406916035,
125.348468363057));
#167137=CARTESIAN_POINT('Ctrl Pts',(-189.007664076035,2.43774637222091,
125.413134116368));
#167138=CARTESIAN_POINT('Ctrl Pts',(-189.003728026594,2.5135749268355,125.447421450406));
#167139=CARTESIAN_POINT('Ctrl Pts',(-188.999791977153,2.58862447664729,
125.483283818407));
#167140=CARTESIAN_POINT('Ctrl Pts',(-188.995855927713,2.66282671449517,
125.520679660972));
#167141=CARTESIAN_POINT('Ctrl Pts',(-188.988432661307,2.80276981930618,
125.591207052967));
#167142=CARTESIAN_POINT('Ctrl Pts',(-188.981009394902,2.94012062552616,
125.667404711676));
#167143=CARTESIAN_POINT('Ctrl Pts',(-188.973586128496,3.07438656032618,
125.749058664153));
#167144=CARTESIAN_POINT('Ctrl Pts',(-188.966171635775,3.20849380394173,
125.830616108438));
#167145=CARTESIAN_POINT('Ctrl Pts',(-188.958757143054,3.33952311781041,
125.917616817874));
#167146=CARTESIAN_POINT('Ctrl Pts',(-188.951342650333,3.46700396331473,
126.009799732473));
#167147=CARTESIAN_POINT('Ctrl Pts',(-188.943935303979,3.59436193798021,
126.101893797708));
#167148=CARTESIAN_POINT('Ctrl Pts',(-188.936527957626,3.71817795265517,
126.199159907163));
#167149=CARTESIAN_POINT('Ctrl Pts',(-188.929120611272,3.83800815054602,
126.301292330404));
#167150=CARTESIAN_POINT('Ctrl Pts',(-188.921718789596,3.95774897455468,
126.403348579431));
#167151=CARTESIAN_POINT('Ctrl Pts',(-188.914316967921,4.07350961808697,
126.510263674354));
#167152=CARTESIAN_POINT('Ctrl Pts',(-188.906915146246,4.1848772819624,126.62169009535));
#167153=CARTESIAN_POINT('Ctrl Pts',(-188.899517231934,4.29618615571496,
126.733057695206));
#167154=CARTESIAN_POINT('Ctrl Pts',(-188.892119317623,4.40310640502578,
126.848931614914));
#167155=CARTESIAN_POINT('Ctrl Pts',(-188.884721403311,4.50526034583612,
126.968925860105));
#167156=CARTESIAN_POINT('Ctrl Pts',(-188.877324718399,4.60739731051461,
127.08890016443));
#167157=CARTESIAN_POINT('Ctrl Pts',(-188.869928033487,4.70476929697789,
127.2129931513));
#167158=CARTESIAN_POINT('Ctrl Pts',(-188.862531348575,4.79703728919411,
127.340783881217));
#167159=CARTESIAN_POINT('Ctrl Pts',(-188.855134991639,4.88930119015086,
127.468568944758));
#167160=CARTESIAN_POINT('Ctrl Pts',(-188.847738634704,4.97646132833132,
127.600051122683));
#167161=CARTESIAN_POINT('Ctrl Pts',(-188.840342277768,5.05822077812171,
127.734778704295));
#167162=CARTESIAN_POINT('Ctrl Pts',(-188.832944788432,5.13999274549259,
127.869526913045));
#167163=CARTESIAN_POINT('Ctrl Pts',(-188.825547299095,5.21636218440918,
128.007521195684));
#167164=CARTESIAN_POINT('Ctrl Pts',(-188.818149809759,5.28707715257132,
128.148283482907));
#167165=CARTESIAN_POINT('Ctrl Pts',(-188.810749727244,5.35781690975603,
128.289095114132));
#167166=CARTESIAN_POINT('Ctrl Pts',(-188.803349644729,5.42289808223647,
128.432676348477));
#167167=CARTESIAN_POINT('Ctrl Pts',(-188.795949562214,5.48211612966465,
128.57852744696));
#167168=CARTESIAN_POINT('Ctrl Pts',(-188.788541342547,5.54139929342365,
128.724538923719));
#167169=CARTESIAN_POINT('Ctrl Pts',(-188.781133122881,5.59480631631315,
128.872824903103));
#167170=CARTESIAN_POINT('Ctrl Pts',(-188.773724903214,5.64218173492415,
129.022868031955));
#167171=CARTESIAN_POINT('Ctrl Pts',(-188.766312123912,5.68958631231479,
129.173003509849));
#167172=CARTESIAN_POINT('Ctrl Pts',(-188.75889934461,5.73095179023987,129.324897932882));
#167173=CARTESIAN_POINT('Ctrl Pts',(-188.751486565308,5.76617357147899,
129.478022460806));
#167174=CARTESIAN_POINT('Ctrl Pts',(-188.744063194279,5.80144567925094,
129.631365780237));
#167175=CARTESIAN_POINT('Ctrl Pts',(-188.73663982325,5.83055648899496,129.785942349065));
#167176=CARTESIAN_POINT('Ctrl Pts',(-188.729216452221,5.85345300237912,
129.941216069162));
#167177=CARTESIAN_POINT('Ctrl Pts',(-188.725280402781,5.86559328316901,
130.023545921295));
#167178=CARTESIAN_POINT('Ctrl Pts',(-188.72134435334,5.8759873721544,130.106071718954));
#167179=CARTESIAN_POINT('Ctrl Pts',(-188.7174083039,5.88463331274603,130.18871352952));
#167180=CARTESIAN_POINT('Ctrl Pts',(-188.709985037494,5.90093928687214,
130.344573405092));
#167181=CARTESIAN_POINT('Ctrl Pts',(-188.702561771089,5.91107350431225,
130.501317224105));
#167182=CARTESIAN_POINT('Ctrl Pts',(-188.695138504683,5.91494973892084,
130.658414913483));
#167183=CARTESIAN_POINT('Ctrl Pts',(-188.687724011962,5.91882139214203,
130.815326926438));
#167184=CARTESIAN_POINT('Ctrl Pts',(-188.680309519241,5.91644977602051,
130.972591607699));
#167185=CARTESIAN_POINT('Ctrl Pts',(-188.67289502652,5.90780019010058,131.1296719705));
#167186=CARTESIAN_POINT('Ctrl Pts',(-188.665487680167,5.89915894097722,
131.286600933333));
#167187=CARTESIAN_POINT('Ctrl Pts',(-188.658080333813,5.88425178867966,
131.443345561147));
#167188=CARTESIAN_POINT('Ctrl Pts',(-188.650672987459,5.86309603744215,
131.599367169885));
#167189=CARTESIAN_POINT('Ctrl Pts',(-188.643271165784,5.84195606496208,
131.75527241182));
#167190=CARTESIAN_POINT('Ctrl Pts',(-188.635869344108,5.81457682305113,
131.910455340087));
#167191=CARTESIAN_POINT('Ctrl Pts',(-188.628467522433,5.78102756193813,
132.064380812091));
#167192=CARTESIAN_POINT('Ctrl Pts',(-188.621069608122,5.74749601121893,
132.218225028037));
#167193=CARTESIAN_POINT('Ctrl Pts',(-188.61367169381,5.70780100727417,132.3708127459));
#167194=CARTESIAN_POINT('Ctrl Pts',(-188.606273779499,5.66206315063794,
132.521617570001));
#167195=CARTESIAN_POINT('Ctrl Pts',(-188.598877094587,5.61633289480377,
132.672397333077));
#167196=CARTESIAN_POINT('Ctrl Pts',(-188.591480409675,5.56456188758136,
132.821394433549));
#167197=CARTESIAN_POINT('Ctrl Pts',(-188.584083724762,5.50692103084546,
132.968096119547));
#167198=CARTESIAN_POINT('Ctrl Pts',(-188.576687367827,5.44928272996555,
133.114791300639));
#167199=CARTESIAN_POINT('Ctrl Pts',(-188.569291010892,5.38577523360099,
133.259190922191));
#167200=CARTESIAN_POINT('Ctrl Pts',(-188.561894653956,5.3166180832047,133.400801011613));
#167201=CARTESIAN_POINT('Ctrl Pts',(-188.55449716462,5.24745034467193,133.542432781902));
#167202=CARTESIAN_POINT('Ctrl Pts',(-188.547099675283,5.17263139364863,
133.681273834221));
#167203=CARTESIAN_POINT('Ctrl Pts',(-188.539702185946,5.09242726241424,
133.816853794242));
#167204=CARTESIAN_POINT('Ctrl Pts',(-188.532302103431,5.0121950157461,133.952481281607));
#167205=CARTESIAN_POINT('Ctrl Pts',(-188.524902020916,4.92657402028228,
134.084845079539));
#167206=CARTESIAN_POINT('Ctrl Pts',(-188.517501938401,4.83587416152764,
134.213502981324));
#167207=CARTESIAN_POINT('Ctrl Pts',(-188.510093718735,4.74507456895399,
134.342302355698));
#167208=CARTESIAN_POINT('Ctrl Pts',(-188.502685499068,4.64918517523304,
134.467387390564));
#167209=CARTESIAN_POINT('Ctrl Pts',(-188.495277279402,4.54855721245665,
134.588347648134));
#167210=CARTESIAN_POINT('Ctrl Pts',(-188.4878645001,4.44786731484825,134.709382354725));
#167211=CARTESIAN_POINT('Ctrl Pts',(-188.480451720798,4.34243328610366,
134.826286948712));
#167212=CARTESIAN_POINT('Ctrl Pts',(-188.473038941496,4.23264351714947,
134.938687578419));
#167213=CARTESIAN_POINT('Ctrl Pts',(-188.465615570467,4.12269687542492,
135.051248811416));
#167214=CARTESIAN_POINT('Ctrl Pts',(-188.458192199438,4.00838233397257,
135.159292971309));
#167215=CARTESIAN_POINT('Ctrl Pts',(-188.45076882841,3.89012228043788,135.262485694966));
#167216=CARTESIAN_POINT('Ctrl Pts',(-188.446832778969,3.82741796243955,
135.317200953127));
#167217=CARTESIAN_POINT('Ctrl Pts',(-188.442896729528,3.76360493059685,
135.370553004011));
#167218=CARTESIAN_POINT('Ctrl Pts',(-188.438960680087,3.69874937690234,
135.422496995951));
#167219=CARTESIAN_POINT('Ctrl Pts',(-188.431537413681,3.57643382671275,
135.520461743629));
#167220=CARTESIAN_POINT('Ctrl Pts',(-188.424114147276,3.45003860462953,
135.613711810634));
#167221=CARTESIAN_POINT('Ctrl Pts',(-188.41669088087,3.31996306880589,135.701888135025));
#167222=CARTESIAN_POINT('Ctrl Pts',(-188.409276388149,3.1900412714635,135.789960242322));
#167223=CARTESIAN_POINT('Ctrl Pts',(-188.401861895428,3.05644812470781,
135.872970336136));
#167224=CARTESIAN_POINT('Ctrl Pts',(-188.394447402707,2.91961665426848,
135.950598967528));
#167225=CARTESIAN_POINT('Ctrl Pts',(-188.387040056353,2.78291706715196,
136.028152777522));
#167226=CARTESIAN_POINT('Ctrl Pts',(-188.37963271,2.64298569258825,136.100335268136));
#167227=CARTESIAN_POINT('Ctrl Pts',(-188.372225363646,2.50028509409351,
136.16686982602));
#167228=CARTESIAN_POINT('Ctrl Pts',(-188.36482354197,2.35769092708891,136.233354759921));
#167229=CARTESIAN_POINT('Ctrl Pts',(-188.357421720295,2.2123319855006,136.294199991563));
#167230=CARTESIAN_POINT('Ctrl Pts',(-188.35001989862,2.06469593138949,136.349174525481));
#167231=CARTESIAN_POINT('Ctrl Pts',(-188.342621984308,1.91713781320257,
136.40412003877));
#167232=CARTESIAN_POINT('Ctrl Pts',(-188.335224069997,1.76730532541907,
136.453200896397));
#167233=CARTESIAN_POINT('Ctrl Pts',(-188.327826155686,1.61570652716677,
136.496234033285));
#167234=CARTESIAN_POINT('Ctrl Pts',(-188.320429470773,1.46413292188381,
136.539260018847));
#167235=CARTESIAN_POINT('Ctrl Pts',(-188.313032785861,1.31079394745819,
136.576240176501));
#167236=CARTESIAN_POINT('Ctrl Pts',(-188.305636100949,1.15621337319739,
136.607041135925));
#167237=CARTESIAN_POINT('Ctrl Pts',(-188.298239744013,1.00163965320169,
136.637840729602));
#167238=CARTESIAN_POINT('Ctrl Pts',(-188.290843387078,0.845824808937177,
136.662461596891));
#167239=CARTESIAN_POINT('Ctrl Pts',(-188.283447030143,0.689303101053426,
136.680821439981));
#167240=CARTESIAN_POINT('Ctrl Pts',(-188.276049540806,0.53275742929617,
136.69918409401));
#167241=CARTESIAN_POINT('Ctrl Pts',(-188.268652051469,0.375505049213833,
136.711283771691));
#167242=CARTESIAN_POINT('Ctrl Pts',(-188.261254562133,0.21808549699706,
136.7170900447));
#167243=CARTESIAN_POINT('Ctrl Pts',(-188.253854479618,0.060610761600514,
136.722898353089));
#167244=CARTESIAN_POINT('Ctrl Pts',(-188.246454397103,-0.0970308897949569,
136.72240885064));
#167245=CARTESIAN_POINT('Ctrl Pts',(-188.239054314588,-0.254299915471865,
136.715643229275));
#167246=CARTESIAN_POINT('Ctrl Pts',(-188.231646094921,-0.411741874610377,
136.708870168413));
#167247=CARTESIAN_POINT('Ctrl Pts',(-188.224237875255,-0.568810016570274,
136.695807222463));
#167248=CARTESIAN_POINT('Ctrl Pts',(-188.216829655588,-0.724969178892556,
136.676528041282));
#167249=CARTESIAN_POINT('Ctrl Pts',(-188.209416876286,-0.881224454573593,
136.657236994087));
#167250=CARTESIAN_POINT('Ctrl Pts',(-188.202004096984,-1.03656926831098,
136.631722148261));
#167251=CARTESIAN_POINT('Ctrl Pts',(-188.194591317682,-1.19047915331876,
136.600108192126));
#167252=CARTESIAN_POINT('Ctrl Pts',(-188.187167946653,-1.34460895198768,
136.568449064488));
#167253=CARTESIAN_POINT('Ctrl Pts',(-188.179744575625,-1.49729936561825,
136.530673510755));
#167254=CARTESIAN_POINT('Ctrl Pts',(-188.172321204596,-1.648040774199,136.486956166176));
#167255=CARTESIAN_POINT('Ctrl Pts',(-188.168385155155,-1.72796748601767,
136.463776181097));
#167256=CARTESIAN_POINT('Ctrl Pts',(-188.164449105714,-1.80734657986099,
136.438926556829));
#167257=CARTESIAN_POINT('Ctrl Pts',(-188.160513056274,-1.88610454236212,
136.412438739149));
#167258=CARTESIAN_POINT('Ctrl Pts',(-188.153089789868,-2.03463960169,136.36248354166));
#167259=CARTESIAN_POINT('Ctrl Pts',(-188.145666523463,-2.18141322895194,
136.306547600599));
#167260=CARTESIAN_POINT('Ctrl Pts',(-188.138243257057,-2.32590747232902,
136.244772825539));
#167261=CARTESIAN_POINT('Ctrl Pts',(-188.130828764336,-2.47023093550992,
136.183071063134));
#167262=CARTESIAN_POINT('Ctrl Pts',(-188.123414271615,-2.61228003741925,
136.115544348554));
#167263=CARTESIAN_POINT('Ctrl Pts',(-188.115999778894,-2.75155195563308,
136.042384328657));
#167264=CARTESIAN_POINT('Ctrl Pts',(-188.10859243254,-2.89068963832824,
135.969294823142));
#167265=CARTESIAN_POINT('Ctrl Pts',(-188.101185086187,-3.02705513796119,
135.890582993991));
#167266=CARTESIAN_POINT('Ctrl Pts',(-188.093777739833,-3.16016570500775,
135.80648849272));
#167267=CARTESIAN_POINT('Ctrl Pts',(-188.086375918158,-3.29317699317143,
135.722456712301));
#167268=CARTESIAN_POINT('Ctrl Pts',(-188.078974096482,-3.42293786829595,
135.633050451894));
#167269=CARTESIAN_POINT('Ctrl Pts',(-188.071572274807,-3.5489903940987,
135.53855513671));
#167270=CARTESIAN_POINT('Ctrl Pts',(-188.064174360495,-3.67497637775464,
135.444109704868));
#167271=CARTESIAN_POINT('Ctrl Pts',(-188.056776446184,-3.79725761282802,
135.344580791833));
#167272=CARTESIAN_POINT('Ctrl Pts',(-188.049378531873,-3.91540546311575,
135.240296890993));
#167273=CARTESIAN_POINT('Ctrl Pts',(-188.041981846961,-4.03353367937402,
135.136030320245));
#167274=CARTESIAN_POINT('Ctrl Pts',(-188.034585162048,-4.1475295945303,
135.027010576778));
#167275=CARTESIAN_POINT('Ctrl Pts',(-188.027188477136,-4.2569978902504,
134.913606232628));
#167276=CARTESIAN_POINT('Ctrl Pts',(-188.019792120201,-4.36646133203156,
134.800206916945));
#167277=CARTESIAN_POINT('Ctrl Pts',(-188.012395763265,-4.4713972942949,
134.682423655727));
#167278=CARTESIAN_POINT('Ctrl Pts',(-188.00499940633,-4.5714477566311,134.560661453614));
#167279=CARTESIAN_POINT('Ctrl Pts',(-187.997601916993,-4.67151353694821,
134.438880609397));
#167280=CARTESIAN_POINT('Ctrl Pts',(-187.990204427657,-4.76669209099886,
134.313119899753));
#167281=CARTESIAN_POINT('Ctrl Pts',(-187.98280693832,-4.85666618608259,
134.183816804508));
#167282=CARTESIAN_POINT('Ctrl Pts',(-187.975406855805,-4.94667182144627,
134.054468382263));
#167283=CARTESIAN_POINT('Ctrl Pts',(-187.96800677329,-5.03146915236339,
133.92157540827));
#167284=CARTESIAN_POINT('Ctrl Pts',(-187.960606690775,-5.11078479338413,
133.785603539271));
#167285=CARTESIAN_POINT('Ctrl Pts',(-187.953198471109,-5.19018765010589,
133.649482155223));
#167286=CARTESIAN_POINT('Ctrl Pts',(-187.945790251442,-5.26409659104829,
133.510275437626));
#167287=CARTESIAN_POINT('Ctrl Pts',(-187.938382031776,-5.3322843115409,
133.368473443359));
#167288=CARTESIAN_POINT('Ctrl Pts',(-187.930969252474,-5.40051400043771,
133.226584172331));
#167289=CARTESIAN_POINT('Ctrl Pts',(-187.923556473172,-5.46301530435872,
133.082096783536));
#167290=CARTESIAN_POINT('Ctrl Pts',(-187.91614369387,-5.51960964001329,
132.93551992282));
#167291=CARTESIAN_POINT('Ctrl Pts',(-187.908720322841,-5.57628484030872,
132.788733626212));
#167292=CARTESIAN_POINT('Ctrl Pts',(-187.901296951812,-5.62703609533202,
132.639852247296));
#167293=CARTESIAN_POINT('Ctrl Pts',(-187.893873580783,-5.67173486859993,
132.489398938438));
#167294=CARTESIAN_POINT('Ctrl Pts',(-187.889937531343,-5.6954352307193,
132.409624984003));
#167295=CARTESIAN_POINT('Ctrl Pts',(-187.886001481902,-5.71743487721036,
132.329409275315));
#167296=CARTESIAN_POINT('Ctrl Pts',(-187.882065432461,-5.73772052852476,
132.248830658462));
#167297=CARTESIAN_POINT('Ctrl Pts',(-187.872272656446,-5.78819063633813,
132.048353413881));
#167298=CARTESIAN_POINT('Ctrl Pts',(-187.862479880431,-5.82817280781611,
131.845137610024));
#167299=CARTESIAN_POINT('Ctrl Pts',(-187.852687104416,-5.85742459265489,
131.640128350768));
#167300=CARTESIAN_POINT('Ctrl Pts',(-187.843111607346,-5.88602734836112,
131.43966777059));
#167301=CARTESIAN_POINT('Ctrl Pts',(-187.833536110275,-5.90437066060156,
131.237492158579));
#167302=CARTESIAN_POINT('Ctrl Pts',(-187.823960613204,-5.91227224031638,
131.034507350944));
#167303=CARTESIAN_POINT('Ctrl Pts',(-187.820432147727,-5.915183885637,130.959709679258));
#167304=CARTESIAN_POINT('Ctrl Pts',(-187.81690368225,-5.91667814734567,
130.88480237372));
#167305=CARTESIAN_POINT('Ctrl Pts',(-187.813375216773,-5.91674747054566,
130.809831658736));
#167306=CARTESIAN_POINT('',(-186.063375192208,-5.90709598019638,130.803332506185));
#167307=CARTESIAN_POINT('Ctrl Pts',(-187.813375192208,-5.91590714834001,
130.809830359851));
#167308=CARTESIAN_POINT('Ctrl Pts',(-187.743456064355,-5.90233112363404,
129.324427893846));
#167309=CARTESIAN_POINT('Ctrl Pts',(-187.580721061896,-4.58174601807203,
125.845682237925));
#167310=CARTESIAN_POINT('Ctrl Pts',(-187.325170184835,1.26703804199676,
123.92161587942));
#167311=CARTESIAN_POINT('Ctrl Pts',(-187.046722561023,6.47551308848548,
128.150063955324));
#167312=CARTESIAN_POINT('Ctrl Pts',(-186.768274937209,5.73330795305963,
134.817680994228));
#167313=CARTESIAN_POINT('Ctrl Pts',(-186.489827313397,-0.277527103565456,
137.797252668579));
#167314=CARTESIAN_POINT('Ctrl Pts',(-186.254860731729,-5.1345300677341,
134.88889554915));
#167315=CARTESIAN_POINT('Ctrl Pts',(-186.112710024666,-5.90546980125088,
131.855374257204));
#167316=CARTESIAN_POINT('Ctrl Pts',(-186.063375192208,-5.90709598019638,
130.803332506185));
#167317=CARTESIAN_POINT('',(-184.313376079986,-5.91869333543885,130.799262689142));
#167318=CARTESIAN_POINT('Ctrl Pts',(-186.063375192208,-5.90709598019638,
130.803332506185));
#167319=CARTESIAN_POINT('Ctrl Pts',(-186.019894150062,-5.90852920600748,
129.876120039144));
#167320=CARTESIAN_POINT('Ctrl Pts',(-185.883597233311,-5.26549744303905,
126.971533866971));
#167321=CARTESIAN_POINT('Ctrl Pts',(-185.654484441958,-0.717600748298859,
123.842851463917));
#167322=CARTESIAN_POINT('Ctrl Pts',(-185.376036818144,5.46903407832205,
126.437757042646));
#167323=CARTESIAN_POINT('Ctrl Pts',(-185.097589194332,6.62989376413611,
133.045357986287));
#167324=CARTESIAN_POINT('Ctrl Pts',(-184.819141570519,1.69820496902565,
137.593591826879));
#167325=CARTESIAN_POINT('Ctrl Pts',(-184.557737350984,-4.39666896695656,
136.006341653894));
#167326=CARTESIAN_POINT('Ctrl Pts',(-184.389149006053,-5.90500976629783,
132.406387652391));
#167327=CARTESIAN_POINT('Ctrl Pts',(-184.313376535726,-5.91969208008458,
130.799271491783));
#167328=CARTESIAN_POINT('',(-182.56337376072,-5.92087641190242,130.807755266905));
#167329=CARTESIAN_POINT('Ctrl Pts',(-184.313375192208,-5.91674778898835,
130.799245541667));
#167330=CARTESIAN_POINT('Ctrl Pts',(-184.30222306504,-5.91654340696533,
130.56283128179));
#167331=CARTESIAN_POINT('Ctrl Pts',(-184.291070937872,-5.90216644403423,
130.327006005632));
#167332=CARTESIAN_POINT('Ctrl Pts',(-184.279918810703,-5.87384581741895,
130.093118130302));
#167333=CARTESIAN_POINT('Ctrl Pts',(-184.274027981434,-5.85888616230683,
129.969572772447));
#167334=CARTESIAN_POINT('Ctrl Pts',(-184.268137152164,-5.84003663158251,
129.846567305077));
#167335=CARTESIAN_POINT('Ctrl Pts',(-184.262246322894,-5.81733560061832,
129.724297160042));
#167336=CARTESIAN_POINT('Ctrl Pts',(-184.254823056489,-5.78872913575387,
129.570219725698));
#167337=CARTESIAN_POINT('Ctrl Pts',(-184.247399790083,-5.75395386469645,
129.417046595923));
#167338=CARTESIAN_POINT('Ctrl Pts',(-184.239976523677,-5.71307757234325,
129.265310516079));
#167339=CARTESIAN_POINT('Ctrl Pts',(-184.232562030956,-5.67224959237304,
129.11375377568));
#167340=CARTESIAN_POINT('Ctrl Pts',(-184.225147538235,-5.6253350405974,
128.963631061319));
#167341=CARTESIAN_POINT('Ctrl Pts',(-184.217733045514,-5.5724530706871,
128.815467121803));
#167342=CARTESIAN_POINT('Ctrl Pts',(-184.21032569916,-5.51962207041052,
128.66744598827));
#167343=CARTESIAN_POINT('Ctrl Pts',(-184.202918352807,-5.46083522698721,
128.521380220278));
#167344=CARTESIAN_POINT('Ctrl Pts',(-184.195511006453,-5.39626204145504,
128.377781432282));
#167345=CARTESIAN_POINT('Ctrl Pts',(-184.188109184777,-5.33173701704084,
128.23428974568));
#167346=CARTESIAN_POINT('Ctrl Pts',(-184.180707363102,-5.26143439604173,
128.093261714445));
#167347=CARTESIAN_POINT('Ctrl Pts',(-184.173305541426,-5.18557248352986,
127.955190812069));
#167348=CARTESIAN_POINT('Ctrl Pts',(-184.165907627115,-5.1097506179311,
127.817192796247));
#167349=CARTESIAN_POINT('Ctrl Pts',(-184.158509712804,-5.02837548473259,
127.682149126725));
#167350=CARTESIAN_POINT('Ctrl Pts',(-184.151111798492,-4.94171214425669,
127.550530313785));
#167351=CARTESIAN_POINT('Ctrl Pts',(-184.14371511358,-4.85506320565538,
127.418933373503));
#167352=CARTESIAN_POINT('Ctrl Pts',(-184.136318428668,-4.76312800903145,
127.290760471687));
#167353=CARTESIAN_POINT('Ctrl Pts',(-184.128921743756,-4.66621597412815,
127.166454757694));
#167354=CARTESIAN_POINT('Ctrl Pts',(-184.12152538682,-4.56930823640603,
127.042154555547));
#167355=CARTESIAN_POINT('Ctrl Pts',(-184.114129029885,-4.46742432870891,
126.921721494671));
#167356=CARTESIAN_POINT('Ctrl Pts',(-184.106732672949,-4.36091497905957,
126.80556691097));
#167357=CARTESIAN_POINT('Ctrl Pts',(-184.099335183613,-4.25438932255719,
126.689394543706));
#167358=CARTESIAN_POINT('Ctrl Pts',(-184.091937694276,-4.14323706635495,
126.577502233055));
#167359=CARTESIAN_POINT('Ctrl Pts',(-184.084540204939,-4.02784681849153,
126.470265490637));
#167360=CARTESIAN_POINT('Ctrl Pts',(-184.077140122424,-3.91241612075543,
126.362991156545));
#167361=CARTESIAN_POINT('Ctrl Pts',(-184.069740039909,-3.79274474677175,
126.260375893956));
#167362=CARTESIAN_POINT('Ctrl Pts',(-184.062339957394,-3.66925535844911,
126.1627557575));
#167363=CARTESIAN_POINT('Ctrl Pts',(-184.054931737728,-3.54563018084883,
126.065028277668));
#167364=CARTESIAN_POINT('Ctrl Pts',(-184.047523518061,-3.41817889765681,
125.972307124804));
#167365=CARTESIAN_POINT('Ctrl Pts',(-184.040115298395,-3.28735479886558,
125.884886154895));
#167366=CARTESIAN_POINT('Ctrl Pts',(-184.032702519093,-3.15645018002447,
125.797411378838));
#167367=CARTESIAN_POINT('Ctrl Pts',(-184.025289739791,-3.02216892674676,
125.715243480416));
#167368=CARTESIAN_POINT('Ctrl Pts',(-184.017876960489,-2.88498957422633,
125.638630686655));
#167369=CARTESIAN_POINT('Ctrl Pts',(-184.01045358946,-2.74761421341414,
125.561908424942));
#167370=CARTESIAN_POINT('Ctrl Pts',(-184.003030218431,-2.60733281501413,
125.490757289058));
#167371=CARTESIAN_POINT('Ctrl Pts',(-183.995606847402,-2.46464530350015,
125.425377991601));
#167372=CARTESIAN_POINT('Ctrl Pts',(-183.991670797962,-2.38898896116109,
125.390712319337));
#167373=CARTESIAN_POINT('Ctrl Pts',(-183.987734748521,-2.31265646397017,
125.357668496352));
#167374=CARTESIAN_POINT('Ctrl Pts',(-183.983798699081,-2.23572401264854,
125.326270740449));
#167375=CARTESIAN_POINT('Ctrl Pts',(-183.976375432675,-2.09063181042523,
125.267055552704));
#167376=CARTESIAN_POINT('Ctrl Pts',(-183.96895216627,-1.94296603481777,
125.213519155027));
#167377=CARTESIAN_POINT('Ctrl Pts',(-183.961528899864,-1.79321153898064,
125.165892479945));
#167378=CARTESIAN_POINT('Ctrl Pts',(-183.954114407143,-1.64363404052125,
125.118322095638));
#167379=CARTESIAN_POINT('Ctrl Pts',(-183.946699914422,-1.49197308804768,
125.076647642673));
#167380=CARTESIAN_POINT('Ctrl Pts',(-183.939285421701,-1.33873457306213,
125.04105251324));
#167381=CARTESIAN_POINT('Ctrl Pts',(-183.931878075348,-1.18564375512665,
125.005491691733));
#167382=CARTESIAN_POINT('Ctrl Pts',(-183.924470728994,-1.03097876289946,
124.975998612581));
#167383=CARTESIAN_POINT('Ctrl Pts',(-183.91706338264,-0.875261651561804,
124.95270720987));
#167384=CARTESIAN_POINT('Ctrl Pts',(-183.909661560965,-0.71966067992065,
124.929433178765));
#167385=CARTESIAN_POINT('Ctrl Pts',(-183.902259739289,-0.563009519234663,
124.912351669202));
#167386=CARTESIAN_POINT('Ctrl Pts',(-183.894857917614,-0.405841341951333,
124.901545749415));
#167387=CARTESIAN_POINT('Ctrl Pts',(-183.887460003302,-0.248756132525396,
124.890745533989));
#167388=CARTESIAN_POINT('Ctrl Pts',(-183.880062088991,-0.091154821529368,
124.886214336211));
#167389=CARTESIAN_POINT('Ctrl Pts',(-183.87266417468,0.066423465832265,
124.887983475625));
#167390=CARTESIAN_POINT('Ctrl Pts',(-183.865267489768,0.223975566541075,
124.889752321039));
#167391=CARTESIAN_POINT('Ctrl Pts',(-183.857870804855,0.38150427830029,
124.89781942147));
#167392=CARTESIAN_POINT('Ctrl Pts',(-183.850474119943,0.538469518075691,
124.912163986376));
#167393=CARTESIAN_POINT('Ctrl Pts',(-183.843077763008,0.695427797847872,
124.92650791523));
#167394=CARTESIAN_POINT('Ctrl Pts',(-183.835681406072,0.851822283566282,
124.947128721133));
#167395=CARTESIAN_POINT('Ctrl Pts',(-183.828285049137,1.00711732962266,
124.97395366377));
#167396=CARTESIAN_POINT('Ctrl Pts',(-183.8208875598,1.16243615174704,125.000782713374));
#167397=CARTESIAN_POINT('Ctrl Pts',(-183.813490070464,1.31665483117389,
125.033817727484));
#167398=CARTESIAN_POINT('Ctrl Pts',(-183.806092581127,1.46924738720576,
125.072934732353));
#167399=CARTESIAN_POINT('Ctrl Pts',(-183.798692498612,1.6218934343218,125.112065449627));
#167400=CARTESIAN_POINT('Ctrl Pts',(-183.791292416097,1.77291186172737,
125.157282309882));
#167401=CARTESIAN_POINT('Ctrl Pts',(-183.783892333582,1.92179147805772,
125.20841136142));
#167402=CARTESIAN_POINT('Ctrl Pts',(-183.776484113915,2.07083480283121,
125.259596634606));
#167403=CARTESIAN_POINT('Ctrl Pts',(-183.769075894249,2.21773426647063,
125.316706960799));
#167404=CARTESIAN_POINT('Ctrl Pts',(-183.761667674582,2.3619976252977,125.379519810631));
#167405=CARTESIAN_POINT('Ctrl Pts',(-183.75425489528,2.50634977581538,125.442371320724));
#167406=CARTESIAN_POINT('Ctrl Pts',(-183.746842115978,2.64806225327137,
125.510932185989));
#167407=CARTESIAN_POINT('Ctrl Pts',(-183.739429336676,2.7866675572784,125.584933973986));
#167408=CARTESIAN_POINT('Ctrl Pts',(-183.732005965648,2.92547090704354,
125.659041499208));
#167409=CARTESIAN_POINT('Ctrl Pts',(-183.724582594619,3.06115789516633,
125.738605285748));
#167410=CARTESIAN_POINT('Ctrl Pts',(-183.71715922359,3.19328943506455,125.823313223051));
#167411=CARTESIAN_POINT('Ctrl Pts',(-183.713223174149,3.26334874797098,
125.868227403948));
#167412=CARTESIAN_POINT('Ctrl Pts',(-183.709287124708,3.33240903135922,
125.914587102222));
#167413=CARTESIAN_POINT('Ctrl Pts',(-183.705351075268,3.40040872175365,
125.962341298364));
#167414=CARTESIAN_POINT('Ctrl Pts',(-183.697927808862,3.52865401564075,
126.052404221932));
#167415=CARTESIAN_POINT('Ctrl Pts',(-183.690504542457,3.65351266188925,
126.147701890419));
#167416=CARTESIAN_POINT('Ctrl Pts',(-183.683081276051,3.77452829544996,
126.247951207806));
#167417=CARTESIAN_POINT('Ctrl Pts',(-183.67566678333,3.89540089858187,126.348082038826));
#167418=CARTESIAN_POINT('Ctrl Pts',(-183.668252290609,4.01243924548009,
126.453152633621));
#167419=CARTESIAN_POINT('Ctrl Pts',(-183.660837797888,4.12521559638735,
126.562836499301));
#167420=CARTESIAN_POINT('Ctrl Pts',(-183.653430451534,4.23788324920132,
126.672414647542));
#167421=CARTESIAN_POINT('Ctrl Pts',(-183.646023105181,4.34629681818062,
126.786596956152));
#167422=CARTESIAN_POINT('Ctrl Pts',(-183.638615758827,4.45006143720835,
126.905016599969));
#167423=CARTESIAN_POINT('Ctrl Pts',(-183.631213937151,4.55374866466839,
127.023347921947));
#167424=CARTESIAN_POINT('Ctrl Pts',(-183.623812115476,4.65279360120558,
127.145910006866));
#167425=CARTESIAN_POINT('Ctrl Pts',(-183.616410293801,4.74683816642942,
127.272299182054));
#167426=CARTESIAN_POINT('Ctrl Pts',(-183.609012379489,4.84083308625904,
127.398621637381));
#167427=CARTESIAN_POINT('Ctrl Pts',(-183.601614465178,4.92983266949919,
127.528766860743));
#167428=CARTESIAN_POINT('Ctrl Pts',(-183.594216550867,5.01351915578842,
127.662298199815));
#167429=CARTESIAN_POINT('Ctrl Pts',(-183.586819865954,5.09719173490199,
127.795807348402));
#167430=CARTESIAN_POINT('Ctrl Pts',(-183.579423181042,5.17555277139587,
127.932701179883));
#167431=CARTESIAN_POINT('Ctrl Pts',(-183.57202649613,5.24832782886879,128.072514069309));
#167432=CARTESIAN_POINT('Ctrl Pts',(-183.564630139194,5.32109965941941,
128.212320759286));
#167433=CARTESIAN_POINT('Ctrl Pts',(-183.557233782259,5.38828583108009,
128.355045918725));
#167434=CARTESIAN_POINT('Ctrl Pts',(-183.549837425324,5.44965801280331,
128.500199575888));
#167435=CARTESIAN_POINT('Ctrl Pts',(-183.542439935987,5.5110395907644,128.645375456446));
#167436=CARTESIAN_POINT('Ctrl Pts',(-183.53504244665,5.56660526102463,128.7929802312));
#167437=CARTESIAN_POINT('Ctrl Pts',(-183.527644957314,5.61617502079312,
128.942504366853));
#167438=CARTESIAN_POINT('Ctrl Pts',(-183.520244874799,5.665762157164,129.09208091796));
#167439=CARTESIAN_POINT('Ctrl Pts',(-183.512844792284,5.70934908086662,
129.243577815451));
#167440=CARTESIAN_POINT('Ctrl Pts',(-183.505444709769,5.74680583097126,
129.396470954412));
#167441=CARTESIAN_POINT('Ctrl Pts',(-183.498036490102,5.78430376862334,
129.549532215098));
#167442=CARTESIAN_POINT('Ctrl Pts',(-183.490628270436,5.81565798206432,
129.703992420572));
#167443=CARTESIAN_POINT('Ctrl Pts',(-183.483220050769,5.84078962182305,
129.859317149728));
#167444=CARTESIAN_POINT('Ctrl Pts',(-183.475807271467,5.8659367296867,130.014737478662));
#167445=CARTESIAN_POINT('Ctrl Pts',(-183.468394492165,5.88485358757889,
130.17102302182));
#167446=CARTESIAN_POINT('Ctrl Pts',(-183.460981712863,5.89751333993616,
130.327635363594));
#167447=CARTESIAN_POINT('Ctrl Pts',(-183.453558341834,5.91019118114126,
130.484471480425));
#167448=CARTESIAN_POINT('Ctrl Pts',(-183.446134970806,5.91659404558043,
130.641634956467));
#167449=CARTESIAN_POINT('Ctrl Pts',(-183.438711599777,5.91674718368156,
130.798587672361));
#167450=CARTESIAN_POINT('Ctrl Pts',(-183.434775550336,5.91682838117727,
130.881807768356));
#167451=CARTESIAN_POINT('Ctrl Pts',(-183.430839500895,5.9151534241066,130.964968689975));
#167452=CARTESIAN_POINT('Ctrl Pts',(-183.426903451455,5.91173196006602,
131.04799106483));
#167453=CARTESIAN_POINT('Ctrl Pts',(-183.419480185049,5.90527918566564,
131.204568672769));
#167454=CARTESIAN_POINT('Ctrl Pts',(-183.412056918644,5.8925917063369,131.36112650563));
#167455=CARTESIAN_POINT('Ctrl Pts',(-183.404633652238,5.87366102232141,
131.517127590259));
#167456=CARTESIAN_POINT('Ctrl Pts',(-183.397219159517,5.85475271280228,
131.672944294561));
#167457=CARTESIAN_POINT('Ctrl Pts',(-183.389804666796,5.82961593096655,
131.828205193483));
#167458=CARTESIAN_POINT('Ctrl Pts',(-183.382390174075,5.79829416074255,
131.982373940071));
#167459=CARTESIAN_POINT('Ctrl Pts',(-183.374982827722,5.76700257961994,
132.136394093016));
#167460=CARTESIAN_POINT('Ctrl Pts',(-183.367575481368,5.72953795175678,
132.289323825892));
#167461=CARTESIAN_POINT('Ctrl Pts',(-183.360168135014,5.68599546277168,
132.44063264869));
#167462=CARTESIAN_POINT('Ctrl Pts',(-183.352766313339,5.64248544941762,
132.59182861966));
#167463=CARTESIAN_POINT('Ctrl Pts',(-183.345364491663,5.59290670374262,
132.741405730511));
#167464=CARTESIAN_POINT('Ctrl Pts',(-183.337962669988,5.5374052957988,132.888844523131));
#167465=CARTESIAN_POINT('Ctrl Pts',(-183.330564755676,5.48193318661622,
133.03620548396));
#167466=CARTESIAN_POINT('Ctrl Pts',(-183.323166841365,5.42054477297452,
133.181430026141));
#167467=CARTESIAN_POINT('Ctrl Pts',(-183.315768927054,5.35343566560404,
133.324014787634));
#167468=CARTESIAN_POINT('Ctrl Pts',(-183.308372242142,5.28633771054982,
133.466575854126));
#167469=CARTESIAN_POINT('Ctrl Pts',(-183.300975557229,5.21352110739003,
133.606497673161));
#167470=CARTESIAN_POINT('Ctrl Pts',(-183.293578872317,5.13522926000215,
133.743297671965));
#167471=CARTESIAN_POINT('Ctrl Pts',(-183.286182515382,5.05694088415682,
133.880091604913));
#167472=CARTESIAN_POINT('Ctrl Pts',(-183.278786158446,4.97317793223063,
134.013763668875));
#167473=CARTESIAN_POINT('Ctrl Pts',(-183.271389801511,4.88422921281487,
134.143856920781));
#167474=CARTESIAN_POINT('Ctrl Pts',(-183.263992312174,4.7952668751231,134.273970090296));
#167475=CARTESIAN_POINT('Ctrl Pts',(-183.256594822838,4.70111739978136,
134.400503048588));
#167476=CARTESIAN_POINT('Ctrl Pts',(-183.249197333501,4.60211217567657,
134.523028939021));
#167477=CARTESIAN_POINT('Ctrl Pts',(-183.241797250986,4.50307224544381,
134.645597780714));
#167478=CARTESIAN_POINT('Ctrl Pts',(-183.234397168471,4.39917341190046,
134.764156467682));
#167479=CARTESIAN_POINT('Ctrl Pts',(-183.226997085956,4.29078637229727,
134.878312368607));
#167480=CARTESIAN_POINT('Ctrl Pts',(-183.219588866289,4.18228015000174,
134.99259379568));
#167481=CARTESIAN_POINT('Ctrl Pts',(-183.212180646623,4.06927612283048,
135.102462497404));
#167482=CARTESIAN_POINT('Ctrl Pts',(-183.204772426956,3.95218129433147,
135.207563267824));
#167483=CARTESIAN_POINT('Ctrl Pts',(-183.197359647654,3.83501439591901,
135.312728726014));
#167484=CARTESIAN_POINT('Ctrl Pts',(-183.189946868352,3.71375196598444,
135.413120167876));
#167485=CARTESIAN_POINT('Ctrl Pts',(-183.18253408905,3.58883247273898,135.508423972275));
#167486=CARTESIAN_POINT('Ctrl Pts',(-183.175110718021,3.46373448866361,
135.603863951219));
#167487=CARTESIAN_POINT('Ctrl Pts',(-183.167687346993,3.33496930979695,
135.694201560142));
#167488=CARTESIAN_POINT('Ctrl Pts',(-183.160263975964,3.20300331966732,
135.779167176288));
#167489=CARTESIAN_POINT('Ctrl Pts',(-183.156327926523,3.13303178521975,
135.82421798469));
#167490=CARTESIAN_POINT('Ctrl Pts',(-183.152391877082,3.06216079141112,
135.867759305324));
#167491=CARTESIAN_POINT('Ctrl Pts',(-183.148455827642,2.99046233124018,
135.90975635227));
#167492=CARTESIAN_POINT('Ctrl Pts',(-183.141032561236,2.85524127299102,
135.988961472127));
#167493=CARTESIAN_POINT('Ctrl Pts',(-183.133609294831,2.71666684177059,
136.062910469239));
#167494=CARTESIAN_POINT('Ctrl Pts',(-183.126186028425,2.57518621397406,
136.131305945412));
#167495=CARTESIAN_POINT('Ctrl Pts',(-183.118771535704,2.43387280453034,
136.199620583812));
#167496=CARTESIAN_POINT('Ctrl Pts',(-183.111357042983,2.28966036846826,
136.262394605668));
#167497=CARTESIAN_POINT('Ctrl Pts',(-183.103942550262,2.14302365379594,
136.319374686612));
#167498=CARTESIAN_POINT('Ctrl Pts',(-183.096535203909,1.99652827310958,
136.376299848008));
#167499=CARTESIAN_POINT('Ctrl Pts',(-183.089127857555,1.84761361116126,
136.427442051669));
#167500=CARTESIAN_POINT('Ctrl Pts',(-183.081720511201,1.69677743437165,
136.472594637145));
#167501=CARTESIAN_POINT('Ctrl Pts',(-183.074318689525,1.54605375689342,
136.517713546118));
#167502=CARTESIAN_POINT('Ctrl Pts',(-183.06691686785,1.39341177422502,136.556851625278));
#167503=CARTESIAN_POINT('Ctrl Pts',(-183.059515046175,1.23936747561927,
136.589850987697));
#167504=CARTESIAN_POINT('Ctrl Pts',(-183.052117131863,1.08540449579967,
136.622832930009));
#167505=CARTESIAN_POINT('Ctrl Pts',(-183.044719217552,0.930041038421735,
136.649682531358));
#167506=CARTESIAN_POINT('Ctrl Pts',(-183.037321303241,0.773806328602494,
136.670292285112));
#167507=CARTESIAN_POINT('Ctrl Pts',(-183.029924618328,0.617597582157862,
136.690898613898));
#167508=CARTESIAN_POINT('Ctrl Pts',(-183.022527933416,0.460518240359305,
136.705267104356));
#167509=CARTESIAN_POINT('Ctrl Pts',(-183.015131248504,0.303105871090587,
136.713341696687));
#167510=CARTESIAN_POINT('Ctrl Pts',(-183.007734891569,0.145700481651279,
136.721415930983));
#167511=CARTESIAN_POINT('Ctrl Pts',(-183.000338534633,-0.012037533089414,
136.72319680293));
#167512=CARTESIAN_POINT('Ctrl Pts',(-182.992942177698,-0.169567625887687,
136.718680306486));
#167513=CARTESIAN_POINT('Ctrl Pts',(-182.985544688361,-0.327121836945322,
136.714163118556));
#167514=CARTESIAN_POINT('Ctrl Pts',(-182.978147199025,-0.484467689507502,
136.703346653195));
#167515=CARTESIAN_POINT('Ctrl Pts',(-182.970749709688,-0.641066933207348,
136.686278990822));
#167516=CARTESIAN_POINT('Ctrl Pts',(-182.963349627173,-0.797721072529536,
136.669205345406));
#167517=CARTESIAN_POINT('Ctrl Pts',(-182.955949544658,-0.953627711032837,
136.645876180442));
#167518=CARTESIAN_POINT('Ctrl Pts',(-182.948549462143,-1.10825614594989,
136.616391147206));
#167519=CARTESIAN_POINT('Ctrl Pts',(-182.941141242476,-1.26305461072711,
136.586873692145));
#167520=CARTESIAN_POINT('Ctrl Pts',(-182.93373302281,-1.41657169809388,
136.551186920619));
#167521=CARTESIAN_POINT('Ctrl Pts',(-182.926324803144,-1.56828856786049,
136.509481258746));
#167522=CARTESIAN_POINT('Ctrl Pts',(-182.918912023842,-1.7200988168289,
136.467749927734));
#167523=CARTESIAN_POINT('Ctrl Pts',(-182.911499244539,-1.8701062854791,
136.419992437623));
#167524=CARTESIAN_POINT('Ctrl Pts',(-182.904086465237,-2.01781011269092,
136.366408164254));
#167525=CARTESIAN_POINT('Ctrl Pts',(-182.896663094209,-2.1657249860579,
136.312747327163));
#167526=CARTESIAN_POINT('Ctrl Pts',(-182.88923972318,-2.31132929938075,
136.253243219605));
#167527=CARTESIAN_POINT('Ctrl Pts',(-182.881816352151,-2.45414411970913,
136.188142485565));
#167528=CARTESIAN_POINT('Ctrl Pts',(-182.87788030271,-2.52986796424262,
136.153624514306));
#167529=CARTESIAN_POINT('Ctrl Pts',(-182.873944253269,-2.60480801371997,
136.117533887402));
#167530=CARTESIAN_POINT('Ctrl Pts',(-182.870008203829,-2.67889608778898,
136.079912371964));
#167531=CARTESIAN_POINT('Ctrl Pts',(-182.862584937423,-2.81862388327062,
136.008959367975));
#167532=CARTESIAN_POINT('Ctrl Pts',(-182.855161671018,-2.95574213382726,
135.932344013602));
#167533=CARTESIAN_POINT('Ctrl Pts',(-182.847738404613,-3.08975892017157,
135.850281780022));
#167534=CARTESIAN_POINT('Ctrl Pts',(-182.840323911892,-3.22361730980421,
135.768316537187));
#167535=CARTESIAN_POINT('Ctrl Pts',(-182.832909419171,-3.35438121652008,
135.680917422574));
#167536=CARTESIAN_POINT('Ctrl Pts',(-182.82549492645,-3.48158089845803,
135.588346927119));
#167537=CARTESIAN_POINT('Ctrl Pts',(-182.818087580096,-3.60865798055354,
135.495865654593));
#167538=CARTESIAN_POINT('Ctrl Pts',(-182.810680233742,-3.7321773771412,
135.398223142311));
#167539=CARTESIAN_POINT('Ctrl Pts',(-182.803272887389,-3.85169616402163,
135.295726470239));
#167540=CARTESIAN_POINT('Ctrl Pts',(-182.795871065713,-3.97112580928161,
135.193306244053));
#167541=CARTESIAN_POINT('Ctrl Pts',(-182.788469244038,-4.08656050384569,
135.086039308776));
#167542=CARTESIAN_POINT('Ctrl Pts',(-182.781067422363,-4.19758850817627,
134.974274439041));
#167543=CARTESIAN_POINT('Ctrl Pts',(-182.773669508051,-4.30855790168761,
134.86256856911));
#167544=CARTESIAN_POINT('Ctrl Pts',(-182.76627159374,-4.4151249753976,134.746369757665));
#167545=CARTESIAN_POINT('Ctrl Pts',(-182.758873679429,-4.51691322183099,
134.626065146824));
#167546=CARTESIAN_POINT('Ctrl Pts',(-182.751476994517,-4.61868455290431,
134.505780528426));
#167547=CARTESIAN_POINT('Ctrl Pts',(-182.744080309604,-4.71567839198069,
134.381391749517));
#167548=CARTESIAN_POINT('Ctrl Pts',(-182.736683624692,-4.80755700579362,
134.253320779491));
#167549=CARTESIAN_POINT('Ctrl Pts',(-182.729287267757,-4.89943154561279,
134.125255488265));
#167550=CARTESIAN_POINT('Ctrl Pts',(-182.721890910821,-4.98619109355161,
133.993508633881));
#167551=CARTESIAN_POINT('Ctrl Pts',(-182.714494553886,-5.06754010022365,
133.858532828677));
#167552=CARTESIAN_POINT('Ctrl Pts',(-182.70709706455,-5.14890156163604,
133.723536358334));
#167553=CARTESIAN_POINT('Ctrl Pts',(-182.699699575213,-5.22485063968611,
133.585310272575));
#167554=CARTESIAN_POINT('Ctrl Pts',(-182.692302085877,-5.29513684831921,
133.444333405318));
#167555=CARTESIAN_POINT('Ctrl Pts',(-182.684902003362,-5.36544769567369,
133.303307118839));
#167556=CARTESIAN_POINT('Ctrl Pts',(-182.677501920847,-5.43009155481507,
133.159528464853));
#167557=CARTESIAN_POINT('Ctrl Pts',(-182.670101838332,-5.48886540737634,
133.013497802579));
#167558=CARTESIAN_POINT('Ctrl Pts',(-182.662693618666,-5.54770388783085,
132.867306564579));
#167559=CARTESIAN_POINT('Ctrl Pts',(-182.655285398999,-5.6006593318303,
132.718858719442));
#167560=CARTESIAN_POINT('Ctrl Pts',(-182.647877179333,-5.6475778513308,
132.568672091104));
#167561=CARTESIAN_POINT('Ctrl Pts',(-182.640464400031,-5.69452524839718,
132.418393025403));
#167562=CARTESIAN_POINT('Ctrl Pts',(-182.633051620729,-5.73542822034687,
132.26637340365));
#167563=CARTESIAN_POINT('Ctrl Pts',(-182.625638841427,-5.77018378005181,
132.113142382005));
#167564=CARTESIAN_POINT('Ctrl Pts',(-182.618215470398,-5.80498900013038,
131.959692416689));
#167565=CARTESIAN_POINT('Ctrl Pts',(-182.61079209937,-5.83362919713295,
131.80502796056));
#167566=CARTESIAN_POINT('Ctrl Pts',(-182.603368728341,-5.85605300467136,
131.649685270572));
#167567=CARTESIAN_POINT('Ctrl Pts',(-182.5994326789,-5.86794264548235,131.567318848928));
#167568=CARTESIAN_POINT('Ctrl Pts',(-182.595496629458,-5.87808550618547,
131.484761797472));
#167569=CARTESIAN_POINT('Ctrl Pts',(-182.591560580017,-5.88647987348797,
131.40209405441));
#167570=CARTESIAN_POINT('Ctrl Pts',(-182.582165450747,-5.90651675745441,
131.204770788007));
#167571=CARTESIAN_POINT('Ctrl Pts',(-182.572770321477,-5.91663410596626,
131.006423364004));
#167572=CARTESIAN_POINT('Ctrl Pts',(-182.563375192208,-5.91674901010249,
130.807783182575));
#167573=CARTESIAN_POINT('',(-180.813376354123,-5.91239331584027,130.807847145143));
#167574=CARTESIAN_POINT('Ctrl Pts',(-182.56337265757,-5.92405711974599,
130.807733754196));
#167575=CARTESIAN_POINT('Ctrl Pts',(-182.479952757115,-5.91188579994225,
129.041809576944));
#167576=CARTESIAN_POINT('Ctrl Pts',(-182.303716982053,-4.13524844748988,
125.289854803609));
#167577=CARTESIAN_POINT('Ctrl Pts',(-182.034665332392,2.25108434336954,
124.177884947263));
#167578=CARTESIAN_POINT('Ctrl Pts',(-181.756217708577,6.79180772637146,
129.116489669186));
#167579=CARTESIAN_POINT('Ctrl Pts',(-181.477770084765,5.09119160707943,
135.60616533563));
#167580=CARTESIAN_POINT('Ctrl Pts',(-181.199322460952,-1.28798088058456,
137.683217047348));
#167581=CARTESIAN_POINT('Ctrl Pts',(-180.977858187196,-5.42030405385856,
134.307513343875));
#167582=CARTESIAN_POINT('Ctrl Pts',(-180.849209788043,-5.91302735279117,
131.571366059404));
#167583=CARTESIAN_POINT('Ctrl Pts',(-180.813377263496,-5.90898434920711,
130.80786452556));
#167584=CARTESIAN_POINT('',(-179.063374001572,-5.91358993803376,130.79964208133));
#167585=CARTESIAN_POINT('Ctrl Pts',(-180.813375192208,-5.91674898580156,
130.807824938015));
#167586=CARTESIAN_POINT('Ctrl Pts',(-180.80590436759,-5.91684231226662,
130.648431696059));
#167587=CARTESIAN_POINT('Ctrl Pts',(-180.798433542972,-5.91049037800369,
130.489025468643));
#167588=CARTESIAN_POINT('Ctrl Pts',(-180.790962718354,-5.89771667312605,
130.330157490171));
#167589=CARTESIAN_POINT('Ctrl Pts',(-180.783490770938,-5.88494104847493,
130.171265635264));
#167590=CARTESIAN_POINT('Ctrl Pts',(-180.776018823522,-5.86574175873066,
130.012912552212));
#167591=CARTESIAN_POINT('Ctrl Pts',(-180.768546876106,-5.84019423006307,
129.855644686616));
#167592=CARTESIAN_POINT('Ctrl Pts',(-180.761072443837,-5.81463820537227,
129.698324520407));
#167593=CARTESIAN_POINT('Ctrl Pts',(-180.753598011569,-5.78272979363846,
129.542090648727));
#167594=CARTESIAN_POINT('Ctrl Pts',(-180.7461235793,-5.74459562263046,129.3874796434));
#167595=CARTESIAN_POINT('Ctrl Pts',(-180.738645298881,-5.70644181855295,
129.232789037847));
#167596=CARTESIAN_POINT('Ctrl Pts',(-180.731167018461,-5.66205595596423,
129.079723315102));
#167597=CARTESIAN_POINT('Ctrl Pts',(-180.723688738042,-5.61161462016539,
128.928804188864));
#167598=CARTESIAN_POINT('Ctrl Pts',(-180.716200537055,-5.56110636969527,
128.777684855721));
#167599=CARTESIAN_POINT('Ctrl Pts',(-180.708712336068,-5.50452671422177,
128.628718151764));
#167600=CARTESIAN_POINT('Ctrl Pts',(-180.701224135081,-5.4421008949015,
128.482407040896));
#167601=CARTESIAN_POINT('Ctrl Pts',(-180.693730469935,-5.37962952330192,
128.335989166437));
#167602=CARTESIAN_POINT('Ctrl Pts',(-180.686236804789,-5.31130363918635,
128.192231074739));
#167603=CARTESIAN_POINT('Ctrl Pts',(-180.678743139642,-5.23739446975496,
128.051611131928));
#167604=CARTESIAN_POINT('Ctrl Pts',(-180.67123737861,-5.16336599996819,
127.910764207684));
#167605=CARTESIAN_POINT('Ctrl Pts',(-180.663731617577,-5.0837364204128,
127.773065865971));
#167606=CARTESIAN_POINT('Ctrl Pts',(-180.656225856544,-4.99882089239424,
127.638966448073));
#167607=CARTESIAN_POINT('Ctrl Pts',(-180.651626308805,-4.9467844602118,
127.556790014292));
#167608=CARTESIAN_POINT('Ctrl Pts',(-180.647026761065,-4.89276383469503,
127.475964459253));
#167609=CARTESIAN_POINT('Ctrl Pts',(-180.642427213326,-4.83683886899804,
127.396587104281));
#167610=CARTESIAN_POINT('Ctrl Pts',(-180.63500394692,-4.74658088221714,
127.26847901934));
#167611=CARTESIAN_POINT('Ctrl Pts',(-180.627580680515,-4.65109331048002,
127.143765544506));
#167612=CARTESIAN_POINT('Ctrl Pts',(-180.62015741411,-4.55065994398724,
127.022902613477));
#167613=CARTESIAN_POINT('Ctrl Pts',(-180.612742921389,-4.45034528139318,
126.902182532395));
#167614=CARTESIAN_POINT('Ctrl Pts',(-180.605328428668,-4.34509669582955,
126.785304220586));
#167615=CARTESIAN_POINT('Ctrl Pts',(-180.597913935947,-4.23524133075553,
126.672694920446));
#167616=CARTESIAN_POINT('Ctrl Pts',(-180.590506589593,-4.12549184841834,
126.560194157389));
#167617=CARTESIAN_POINT('Ctrl Pts',(-180.583099243239,-4.01114468503391,
126.451954479988));
#167618=CARTESIAN_POINT('Ctrl Pts',(-180.575691896886,-3.89256726626094,
126.348370195658));
#167619=CARTESIAN_POINT('Ctrl Pts',(-180.56829007521,-3.77407828700056,
126.244863168396));
#167620=CARTESIAN_POINT('Ctrl Pts',(-180.560888253535,-3.65136561447588,
126.146004865181));
#167621=CARTESIAN_POINT('Ctrl Pts',(-180.55348643186,-3.52483346582677,
126.05215275167));
#167622=CARTESIAN_POINT('Ctrl Pts',(-180.546088517549,-3.39836811251472,
125.958350181959));
#167623=CARTESIAN_POINT('Ctrl Pts',(-180.538690603237,-3.26808759764599,
125.869548760655));
#167624=CARTESIAN_POINT('Ctrl Pts',(-180.531292688926,-3.13442905661681,
125.78606558324));
#167625=CARTESIAN_POINT('Ctrl Pts',(-180.523896004014,-3.00079272721176,
125.702596279216));
#167626=CARTESIAN_POINT('Ctrl Pts',(-180.516499319102,-2.86377980209576,
125.624443662571));
#167627=CARTESIAN_POINT('Ctrl Pts',(-180.50910263419,-2.72385632332298,
125.551881460787));
#167628=CARTESIAN_POINT('Ctrl Pts',(-180.501706277254,-2.58393904890388,
125.479322476488));
#167629=CARTESIAN_POINT('Ctrl Pts',(-180.494309920319,-2.44111180882452,
125.412353586024));
#167630=CARTESIAN_POINT('Ctrl Pts',(-180.486913563384,-2.29586492173638,
125.351202374526));
#167631=CARTESIAN_POINT('Ctrl Pts',(-180.479516074047,-2.15059579697861,
125.29004180062));
#167632=CARTESIAN_POINT('Ctrl Pts',(-180.472118584711,-2.0029066316598,
125.234700824044));
#167633=CARTESIAN_POINT('Ctrl Pts',(-180.464721095374,-1.85330723241896,
125.185358671956));
#167634=CARTESIAN_POINT('Ctrl Pts',(-180.457321012859,-1.70365539134041,
125.135999223054));
#167635=CARTESIAN_POINT('Ctrl Pts',(-180.449920930344,-1.55209233740366,
125.092642902312));
#167636=CARTESIAN_POINT('Ctrl Pts',(-180.442520847829,-1.39914237269438,
125.055418872912));
#167637=CARTESIAN_POINT('Ctrl Pts',(-180.435112628163,-1.24602422377592,
125.018153911864));
#167638=CARTESIAN_POINT('Ctrl Pts',(-180.427704408496,-1.0915164813912,
124.987034796868));
#167639=CARTESIAN_POINT('Ctrl Pts',(-180.42029618883,-0.936153686024078,
124.962139564007));
#167640=CARTESIAN_POINT('Ctrl Pts',(-180.412883409528,-0.780695267448333,
124.937229008546));
#167641=CARTESIAN_POINT('Ctrl Pts',(-180.405470630226,-0.624381117031028,
124.91855001255));
#167642=CARTESIAN_POINT('Ctrl Pts',(-180.398057850924,-0.467749690625702,
124.906128612175));
#167643=CARTESIAN_POINT('Ctrl Pts',(-180.390634479895,-0.310894461893262,
124.893689463521));
#167644=CARTESIAN_POINT('Ctrl Pts',(-180.383211108867,-0.153721423776527,
124.887525782551));
#167645=CARTESIAN_POINT('Ctrl Pts',(-180.375787737838,0.00323134341759472,
124.887611499941));
#167646=CARTESIAN_POINT('Ctrl Pts',(-180.371851688396,0.0864514666357916,
124.887656949358));
#167647=CARTESIAN_POINT('Ctrl Pts',(-180.367915638954,0.169609742978011,
124.889458461255));
#167648=CARTESIAN_POINT('Ctrl Pts',(-180.363979589513,0.252626814831058,
124.893006267256));
#167649=CARTESIAN_POINT('Ctrl Pts',(-180.356556323107,0.409194421432122,
124.899697318649));
#167650=CARTESIAN_POINT('Ctrl Pts',(-180.349133056702,0.565732764817981,
124.912623037657));
#167651=CARTESIAN_POINT('Ctrl Pts',(-180.341709790296,0.721704859521438,
124.931791106846));
#167652=CARTESIAN_POINT('Ctrl Pts',(-180.334295297575,0.877492608161631,
124.950936520968));
#167653=CARTESIAN_POINT('Ctrl Pts',(-180.326880804854,1.03271507339061,
124.976309554354));
#167654=CARTESIAN_POINT('Ctrl Pts',(-180.319466312133,1.18683597505039,
125.007865906896));
#167655=CARTESIAN_POINT('Ctrl Pts',(-180.31205896578,1.34080832918305,125.039391844237));
#167656=CARTESIAN_POINT('Ctrl Pts',(-180.304651619426,1.49368087018309,
125.077089161737));
#167657=CARTESIAN_POINT('Ctrl Pts',(-180.297244273072,1.6449232535122,125.120861866572));
#167658=CARTESIAN_POINT('Ctrl Pts',(-180.289842451397,1.79605283456535,
125.164601924071));
#167659=CARTESIAN_POINT('Ctrl Pts',(-180.282440629721,1.94555432179695,
125.214408243235));
#167660=CARTESIAN_POINT('Ctrl Pts',(-180.275038808046,2.09290847999003,
125.270133963653));
#167661=CARTESIAN_POINT('Ctrl Pts',(-180.267640893735,2.24018485107,125.325830266896));
#167662=CARTESIAN_POINT('Ctrl Pts',(-180.260242979423,2.38531580236709,
125.387439616482));
#167663=CARTESIAN_POINT('Ctrl Pts',(-180.252845065112,2.52779827011158,
125.454765635876));
#167664=CARTESIAN_POINT('Ctrl Pts',(-180.2454483802,2.67025705985461,125.522080466907));
#167665=CARTESIAN_POINT('Ctrl Pts',(-180.238051695287,2.81006790238803,
125.595109922935));
#167666=CARTESIAN_POINT('Ctrl Pts',(-180.230655010375,2.94674859591522,
125.673609865973));
#167667=CARTESIAN_POINT('Ctrl Pts',(-180.22325865344,3.08342322887723,125.752106328241));
#167668=CARTESIAN_POINT('Ctrl Pts',(-180.215862296504,3.21696766509498,
125.836072609297));
#167669=CARTESIAN_POINT('Ctrl Pts',(-180.208465939569,3.34692540154562,
125.925219205495));
#167670=CARTESIAN_POINT('Ctrl Pts',(-180.201068450232,3.47690303485747,
126.014379450264));
#167671=CARTESIAN_POINT('Ctrl Pts',(-180.193670960896,3.60329256715243,
126.108721378205));
#167672=CARTESIAN_POINT('Ctrl Pts',(-180.186273471559,3.72566764660411,
126.20791295121));
#167673=CARTESIAN_POINT('Ctrl Pts',(-180.178873389044,3.84808562445071,
126.307139295668));
#167674=CARTESIAN_POINT('Ctrl Pts',(-180.171473306529,3.96648605779236,
126.411218435038));
#167675=CARTESIAN_POINT('Ctrl Pts',(-180.164073224014,4.08047687990288,
126.519779074979));
#167676=CARTESIAN_POINT('Ctrl Pts',(-180.156665004348,4.19459304664037,
126.628459088503));
#167677=CARTESIAN_POINT('Ctrl Pts',(-180.149256784681,4.30428964824568,
126.741630186279));
#167678=CARTESIAN_POINT('Ctrl Pts',(-180.141848565015,4.40921209856459,
126.858884824665));
#167679=CARTESIAN_POINT('Ctrl Pts',(-180.134435785713,4.51419912690065,
126.976211631324));
#167680=CARTESIAN_POINT('Ctrl Pts',(-180.127023006411,4.61440591173413,
127.097626699522));
#167681=CARTESIAN_POINT('Ctrl Pts',(-180.119610227109,4.7095194995687,127.222691084278));
#167682=CARTESIAN_POINT('Ctrl Pts',(-180.11218685608,4.80476899015836,127.347934166893));
#167683=CARTESIAN_POINT('Ctrl Pts',(-180.104763485052,4.89491053578961,
127.476836675114));
#167684=CARTESIAN_POINT('Ctrl Pts',(-180.097340114023,4.97967522377445,
127.608931815632));
#167685=CARTESIAN_POINT('Ctrl Pts',(-180.093404064582,5.02461949524755,
127.678971828719));
#167686=CARTESIAN_POINT('Ctrl Pts',(-180.089468015141,5.06805291187504,
127.749909002942));
#167687=CARTESIAN_POINT('Ctrl Pts',(-180.0855319657,5.10994079734045,127.821671292448));
#167688=CARTESIAN_POINT('Ctrl Pts',(-180.078108699294,5.18894004204775,
127.957012730823));
#167689=CARTESIAN_POINT('Ctrl Pts',(-180.070685432889,5.2626780668334,128.095699539363));
#167690=CARTESIAN_POINT('Ctrl Pts',(-180.063262166483,5.33085815437477,
128.2372840896));
#167691=CARTESIAN_POINT('Ctrl Pts',(-180.055847673762,5.39895765871467,
128.378701298656));
#167692=CARTESIAN_POINT('Ctrl Pts',(-180.048433181041,5.46151214110167,
128.523009099099));
#167693=CARTESIAN_POINT('Ctrl Pts',(-180.04101868832,5.51826899994545,128.669732357952));
#167694=CARTESIAN_POINT('Ctrl Pts',(-180.033611341967,5.57497115439181,
128.816314199405));
#167695=CARTESIAN_POINT('Ctrl Pts',(-180.026203995613,5.62588667606558,
128.965306518641));
#167696=CARTESIAN_POINT('Ctrl Pts',(-180.018796649259,5.67080966227076,
129.116211235314));
#167697=CARTESIAN_POINT('Ctrl Pts',(-180.011394827583,5.71569914321786,
129.267003401556));
#167698=CARTESIAN_POINT('Ctrl Pts',(-180.003993005908,5.75460488194266,
129.419704768962));
#167699=CARTESIAN_POINT('Ctrl Pts',(-179.996591184232,5.78736977694945,
129.573799108599));
#167700=CARTESIAN_POINT('Ctrl Pts',(-179.989193269921,5.8201173756232,129.727812103033));
#167701=CARTESIAN_POINT('Ctrl Pts',(-179.98179535561,5.84673050914526,129.883216241026));
#167702=CARTESIAN_POINT('Ctrl Pts',(-179.974397441298,5.86710247640078,
130.039482134464));
#167703=CARTESIAN_POINT('Ctrl Pts',(-179.967000756386,5.88747105820495,
130.195722059347));
#167704=CARTESIAN_POINT('Ctrl Pts',(-179.959604071474,5.90160048400506,
130.352823085647));
#167705=CARTESIAN_POINT('Ctrl Pts',(-179.952207386562,5.9094355121563,130.51024756079));
#167706=CARTESIAN_POINT('Ctrl Pts',(-179.944811029626,5.91727019289419,
130.667665055567));
#167707=CARTESIAN_POINT('Ctrl Pts',(-179.937414672691,5.91881101237257,
130.825405597834));
#167708=CARTESIAN_POINT('Ctrl Pts',(-179.930018315755,5.91405478717383,
130.982928634877));
#167709=CARTESIAN_POINT('Ctrl Pts',(-179.922620826419,5.90929783378486,
131.140475789099));
#167710=CARTESIAN_POINT('Ctrl Pts',(-179.915223337082,5.89824192734704,
131.297804998638));
#167711=CARTESIAN_POINT('Ctrl Pts',(-179.907825847746,5.88093596734664,
131.454378086923));
#167712=CARTESIAN_POINT('Ctrl Pts',(-179.900425765231,5.86362394076881,
131.61100606166));
#167713=CARTESIAN_POINT('Ctrl Pts',(-179.893025682716,5.84005753945498,
131.766877016608));
#167714=CARTESIAN_POINT('Ctrl Pts',(-179.885625600201,5.81033722220633,
131.921460401266));
#167715=CARTESIAN_POINT('Ctrl Pts',(-179.878217380534,5.78058422441342,
132.076213766249));
#167716=CARTESIAN_POINT('Ctrl Pts',(-179.870809160868,5.74466386733851,
132.229676366655));
#167717=CARTESIAN_POINT('Ctrl Pts',(-179.863400941201,5.70272736651028,
132.381329591818));
#167718=CARTESIAN_POINT('Ctrl Pts',(-179.855988161899,5.66076505446567,
132.533076157011));
#167719=CARTESIAN_POINT('Ctrl Pts',(-179.848575382597,5.61277933382527,
132.683010773186));
#167720=CARTESIAN_POINT('Ctrl Pts',(-179.841162603295,5.55897034242447,
132.830632883217));
#167721=CARTESIAN_POINT('Ctrl Pts',(-179.833739232266,5.50508446621329,
132.978465922642));
#167722=CARTESIAN_POINT('Ctrl Pts',(-179.826315861237,5.44535884258079,
133.123979512235));
#167723=CARTESIAN_POINT('Ctrl Pts',(-179.818892490209,5.380040844081,133.266695094951));
#167724=CARTESIAN_POINT('Ctrl Pts',(-179.814956440768,5.34540767399451,
133.342366321317));
#167725=CARTESIAN_POINT('Ctrl Pts',(-179.811020391327,5.30920304288685,
133.417251360219));
#167726=CARTESIAN_POINT('Ctrl Pts',(-179.807084341887,5.27146882157906,
133.491282094949));
#167727=CARTESIAN_POINT('Ctrl Pts',(-179.799661075481,5.20030325783337,
133.630901750236));
#167728=CARTESIAN_POINT('Ctrl Pts',(-179.792237809076,5.12347932154279,
133.767903246486));
#167729=CARTESIAN_POINT('Ctrl Pts',(-179.784814542671,5.04121323225327,
133.901794992893));
#167730=CARTESIAN_POINT('Ctrl Pts',(-179.77740004995,4.95904437464975,134.035528490373));
#167731=CARTESIAN_POINT('Ctrl Pts',(-179.769985557229,4.87144636083707,
134.166159239093));
#167732=CARTESIAN_POINT('Ctrl Pts',(-179.762571064508,4.77868239631381,
134.293217897201));
#167733=CARTESIAN_POINT('Ctrl Pts',(-179.755163718154,4.68600784119206,
134.42015409139));
#167734=CARTESIAN_POINT('Ctrl Pts',(-179.7477563718,4.5881774664831,134.543524749663));
#167735=CARTESIAN_POINT('Ctrl Pts',(-179.740349025446,4.485499025852,134.662887415656));
#167736=CARTESIAN_POINT('Ctrl Pts',(-179.732947203771,4.38289716667605,
134.78216105647));
#167737=CARTESIAN_POINT('Ctrl Pts',(-179.725545382096,4.27545468365737,
134.897432375347));
#167738=CARTESIAN_POINT('Ctrl Pts',(-179.71814356042,4.16352097762122,135.008290164003));
#167739=CARTESIAN_POINT('Ctrl Pts',(-179.710745646109,4.05164636051687,
135.119089431696));
#167740=CARTESIAN_POINT('Ctrl Pts',(-179.703347731798,3.93528550668121,
135.225479547193));
#167741=CARTESIAN_POINT('Ctrl Pts',(-179.695949817487,3.81482613076614,
135.32708459262));
#167742=CARTESIAN_POINT('Ctrl Pts',(-179.688553132574,3.69438677301383,
135.428672753131));
#167743=CARTESIAN_POINT('Ctrl Pts',(-179.681156447662,3.56985053003108,
135.525477181344));
#167744=CARTESIAN_POINT('Ctrl Pts',(-179.67375976275,3.44163988469777,135.617160786548));
#167745=CARTESIAN_POINT('Ctrl Pts',(-179.666363405815,3.31343492435919,
135.708840326406));
#167746=CARTESIAN_POINT('Ctrl Pts',(-179.658967048879,3.18155618927124,
135.795399277593));
#167747=CARTESIAN_POINT('Ctrl Pts',(-179.651570691944,3.04645674102676,
135.876542779866));
#167748=CARTESIAN_POINT('Ctrl Pts',(-179.644173202607,2.91133660871186,
135.957698705416));
#167749=CARTESIAN_POINT('Ctrl Pts',(-179.636775713271,2.77299510144716,
136.033437338946));
#167750=CARTESIAN_POINT('Ctrl Pts',(-179.629378223934,2.63191143379257,
136.103508923395));
#167751=CARTESIAN_POINT('Ctrl Pts',(-179.621978141419,2.49077830947559,
136.17360507133));
#167752=CARTESIAN_POINT('Ctrl Pts',(-179.614578058904,2.3469014450307,136.23803004898));
#167753=CARTESIAN_POINT('Ctrl Pts',(-179.607177976389,2.20078150805586,
136.296581599673));
#167754=CARTESIAN_POINT('Ctrl Pts',(-179.599769756723,2.05450089718987,
136.355197533815));
#167755=CARTESIAN_POINT('Ctrl Pts',(-179.592361537056,1.90597263478008,
136.407927004143));
#167756=CARTESIAN_POINT('Ctrl Pts',(-179.58495331739,1.75571477835447,136.45461691083));
#167757=CARTESIAN_POINT('Ctrl Pts',(-179.577540538088,1.60536444072542,
136.501335554375));
#167758=CARTESIAN_POINT('Ctrl Pts',(-179.570127758786,1.45328274764712,
136.542007130973));
#167759=CARTESIAN_POINT('Ctrl Pts',(-179.562714979484,1.29999901139323,
136.576529458901));
#167760=CARTESIAN_POINT('Ctrl Pts',(-179.555291608455,1.14649625614847,
136.611101113949));
#167761=CARTESIAN_POINT('Ctrl Pts',(-179.547868237426,0.991788393612213,
136.639505904812));
#167762=CARTESIAN_POINT('Ctrl Pts',(-179.540444866397,0.836411758288183,
136.661693281253));
#167763=CARTESIAN_POINT('Ctrl Pts',(-179.536508816957,0.754027338025988,
136.673457560621));
#167764=CARTESIAN_POINT('Ctrl Pts',(-179.532572767516,0.671454946475021,
136.683474771799));
#167765=CARTESIAN_POINT('Ctrl Pts',(-179.528636718075,0.588774524354783,
136.691743323147));
#167766=CARTESIAN_POINT('Ctrl Pts',(-179.521213451669,0.432841828606704,
136.707337552936));
#167767=CARTESIAN_POINT('Ctrl Pts',(-179.513790185264,0.276053375632314,
136.716756054739));
#167768=CARTESIAN_POINT('Ctrl Pts',(-179.506366918858,0.118939626646369,
136.719915023343));
#167769=CARTESIAN_POINT('Ctrl Pts',(-179.498952426137,-0.0379884269357607,
136.723070258309));
#167770=CARTESIAN_POINT('Ctrl Pts',(-179.491537933416,-0.195240641656169,
136.7199806789));
#167771=CARTESIAN_POINT('Ctrl Pts',(-179.484123440695,-0.352279877922297,
136.710614036622));
#167772=CARTESIAN_POINT('Ctrl Pts',(-179.476716094341,-0.509167753859644,
136.701256422266));
#167773=CARTESIAN_POINT('Ctrl Pts',(-179.469308747988,-0.665842689874027,
136.685633811616));
#167774=CARTESIAN_POINT('Ctrl Pts',(-179.461901401634,-0.821766086522907,
136.663765968072));
#167775=CARTESIAN_POINT('Ctrl Pts',(-179.454499579958,-0.977573189619913,
136.641914434392));
#167776=CARTESIAN_POINT('Ctrl Pts',(-179.447097758283,-1.13262950134629,
136.61382699401));
#167777=CARTESIAN_POINT('Ctrl Pts',(-179.439695936607,-1.28640020084502,
136.579575339615));
#167778=CARTESIAN_POINT('Ctrl Pts',(-179.432298022296,-1.44008972598887,
136.545341766401));
#167779=CARTESIAN_POINT('Ctrl Pts',(-179.424900107985,-1.59249462705246,
136.504950540707));
#167780=CARTESIAN_POINT('Ctrl Pts',(-179.417502193673,-1.74308906444127,
136.458524665056));
#167781=CARTESIAN_POINT('Ctrl Pts',(-179.410105508761,-1.89365847576642,
136.412106504543));
#167782=CARTESIAN_POINT('Ctrl Pts',(-179.402708823849,-2.04241766416558,
136.3596557943));
#167783=CARTESIAN_POINT('Ctrl Pts',(-179.395312138936,-2.18885466336137,
136.301345775376));
#167784=CARTESIAN_POINT('Ctrl Pts',(-179.387915782001,-2.33528516938715,
136.243038341979));
#167785=CARTESIAN_POINT('Ctrl Pts',(-179.380519425065,-2.47939334413142,
136.178872254585));
#167786=CARTESIAN_POINT('Ctrl Pts',(-179.37312306813,-2.62068622246135,
136.109069307579));
#167787=CARTESIAN_POINT('Ctrl Pts',(-179.365725578793,-2.76200073309085,
136.039255673564));
#167788=CARTESIAN_POINT('Ctrl Pts',(-179.358328089457,-2.90049875436519,
135.963803626908));
#167789=CARTESIAN_POINT('Ctrl Pts',(-179.35093060012,-3.03571113142043,
135.882981344601));
#167790=CARTESIAN_POINT('Ctrl Pts',(-179.343530517605,-3.17097090696619,
135.802130730167));
#167791=CARTESIAN_POINT('Ctrl Pts',(-179.33613043509,-3.30294242489327,
135.715906323391));
#167792=CARTESIAN_POINT('Ctrl Pts',(-179.328730352575,-3.43118489787047,
135.624620025433));
#167793=CARTESIAN_POINT('Ctrl Pts',(-179.321322132908,-3.55956838662981,
135.533233348805));
#167794=CARTESIAN_POINT('Ctrl Pts',(-179.313913913242,-3.6842143372299,
135.4367738818));
#167795=CARTESIAN_POINT('Ctrl Pts',(-179.306505693575,-3.80471391970313,
135.335594726693));
#167796=CARTESIAN_POINT('Ctrl Pts',(-179.299092914273,-3.92528766765873,
135.234353297504));
#167797=CARTESIAN_POINT('Ctrl Pts',(-179.291680134971,-4.04170968684056,
135.128386642548));
#167798=CARTESIAN_POINT('Ctrl Pts',(-179.284267355669,-4.15360790265782,
135.018084855515));
#167799=CARTESIAN_POINT('Ctrl Pts',(-179.27684398464,-4.26566600389351,
134.907625464115));
#167800=CARTESIAN_POINT('Ctrl Pts',(-179.269420613611,-4.37318713756271,
134.792818841095));
#167801=CARTESIAN_POINT('Ctrl Pts',(-179.261997242582,-4.47583887241952,
134.674088896223));
#167802=CARTESIAN_POINT('Ctrl Pts',(-179.258061193142,-4.53026728532872,
134.611135430574));
#167803=CARTESIAN_POINT('Ctrl Pts',(-179.254125143702,-4.58332744336295,
134.547079486324));
#167804=CARTESIAN_POINT('Ctrl Pts',(-179.250189094261,-4.63497479752016,
134.481987459546));
#167805=CARTESIAN_POINT('Ctrl Pts',(-179.242405181676,-4.73711235857636,
134.35326177809));
#167806=CARTESIAN_POINT('Ctrl Pts',(-179.23462126909,-4.83405257557669,
134.220064488449));
#167807=CARTESIAN_POINT('Ctrl Pts',(-179.226837356504,-4.92538181691207,
134.082857913605));
#167808=CARTESIAN_POINT('Ctrl Pts',(-179.21943360423,-5.01225060826353,
133.952352402468));
#167809=CARTESIAN_POINT('Ctrl Pts',(-179.212029851955,-5.09404316262776,
133.818220254166));
#167810=CARTESIAN_POINT('Ctrl Pts',(-179.20462609968,-5.17044286712766,
133.680895185456));
#167811=CARTESIAN_POINT('Ctrl Pts',(-179.197229304088,-5.24677078525505,
133.543699149556));
#167812=CARTESIAN_POINT('Ctrl Pts',(-179.189832508496,-5.31771575753479,
133.403316488217));
#167813=CARTESIAN_POINT('Ctrl Pts',(-179.182435712904,-5.38300406071346,
133.260210337081));
#167814=CARTESIAN_POINT('Ctrl Pts',(-179.175044399858,-5.44824397184658,
133.117210257003));
#167815=CARTESIAN_POINT('Ctrl Pts',(-179.167653086811,-5.50783540530376,
132.971491044007));
#167816=CARTESIAN_POINT('Ctrl Pts',(-179.160261773764,-5.56155032784516,
132.82354077628));
#167817=CARTESIAN_POINT('Ctrl Pts',(-179.152874472875,-5.61523609281154,
132.67567081903));
#167818=CARTESIAN_POINT('Ctrl Pts',(-179.145487171987,-5.66305157103681,
132.525572568989));
#167819=CARTESIAN_POINT('Ctrl Pts',(-179.138099871098,-5.70481673901178,
132.373754302016));
#167820=CARTESIAN_POINT('Ctrl Pts',(-179.130714471695,-5.74657115666838,
132.221975112935));
#167821=CARTESIAN_POINT('Ctrl Pts',(-179.123329072291,-5.78227826278416,
132.068477147734));
#167822=CARTESIAN_POINT('Ctrl Pts',(-179.115943672887,-5.81180782512948,
131.913784056233));
#167823=CARTESIAN_POINT('Ctrl Pts',(-179.108559362774,-5.84133303208765,
131.759113780793));
#167824=CARTESIAN_POINT('Ctrl Pts',(-179.101175052661,-5.86468244308912,
131.603249097923));
#167825=CARTESIAN_POINT('Ctrl Pts',(-179.093790742548,-5.88177695426642,
131.446723772456));
#167826=CARTESIAN_POINT('Ctrl Pts',(-179.086404697669,-5.89887548138718,
131.290161675136));
#167827=CARTESIAN_POINT('Ctrl Pts',(-179.079018652791,-5.90971613497904,
131.132938997188));
#167828=CARTESIAN_POINT('Ctrl Pts',(-179.071632607912,-5.91427167588424,
130.975594686412));
#167829=CARTESIAN_POINT('Ctrl Pts',(-179.068880136011,-5.91596933661368,
130.916959002315));
#167830=CARTESIAN_POINT('Ctrl Pts',(-179.066127664109,-5.91679467625972,
130.858306445919));
#167831=CARTESIAN_POINT('Ctrl Pts',(-179.063375192208,-5.91674813668029,
130.799664918431));
#167832=CARTESIAN_POINT('',(-177.313376099405,-5.92185101381458,130.802772195749));
#167833=CARTESIAN_POINT('Ctrl Pts',(-179.063373167743,-5.91137817917409,
130.799626087985));
#167834=CARTESIAN_POINT('Ctrl Pts',(-179.032829268644,-5.91617425954304,
130.149473536606));
#167835=CARTESIAN_POINT('Ctrl Pts',(-178.909469494942,-5.51702945710787,
127.529389957826));
#167836=CARTESIAN_POINT('Ctrl Pts',(-178.693293846636,-1.67753301865071,
124.009992103728));
#167837=CARTESIAN_POINT('Ctrl Pts',(-178.414846222822,4.80954708459832,
125.720482435377));
#167838=CARTESIAN_POINT('Ctrl Pts',(-178.13639859901,6.87688837653484,132.102808455183));
#167839=CARTESIAN_POINT('Ctrl Pts',(-177.857950975197,2.62470520511161,
137.291924344931));
#167840=CARTESIAN_POINT('Ctrl Pts',(-177.583610388289,-3.94115904884794,
136.530682336505));
#167841=CARTESIAN_POINT('Ctrl Pts',(-177.402085675986,-5.91922248209783,
132.679038148341));
#167842=CARTESIAN_POINT('Ctrl Pts',(-177.313376838286,-5.92600578683143,
130.802786695663));
#167843=CARTESIAN_POINT('',(-175.563375192208,-5.91627067345725,130.809833481333));
#167844=CARTESIAN_POINT('Ctrl Pts',(-177.313375192207,-5.91674978197843,
130.802754392749));
#167845=CARTESIAN_POINT('Ctrl Pts',(-177.309268703995,-5.91672624024111,
130.716035169074));
#167846=CARTESIAN_POINT('Ctrl Pts',(-177.305162215783,-5.91479628735477,
130.629344163195));
#167847=CARTESIAN_POINT('Ctrl Pts',(-177.301055727571,-5.91096305005085,
130.542738020236));
#167848=CARTESIAN_POINT('Ctrl Pts',(-177.293632461165,-5.9040337371609,
130.386180777579));
#167849=CARTESIAN_POINT('Ctrl Pts',(-177.28620919476,-5.89086980840988,
130.229662286206));
#167850=CARTESIAN_POINT('Ctrl Pts',(-177.278785928355,-5.87146439844034,
130.073719542655));
#167851=CARTESIAN_POINT('Ctrl Pts',(-177.271371435634,-5.85208192405386,
129.917961110475));
#167852=CARTESIAN_POINT('Ctrl Pts',(-177.263956942913,-5.82647269788109,
129.762777438429));
#167853=CARTESIAN_POINT('Ctrl Pts',(-177.256542450192,-5.79468183610456,
129.608704738636));
#167854=CARTESIAN_POINT('Ctrl Pts',(-177.249135103838,-5.76292161555761,
129.454780539912));
#167855=CARTESIAN_POINT('Ctrl Pts',(-177.241727757484,-5.72499169572692,
129.301965544837));
#167856=CARTESIAN_POINT('Ctrl Pts',(-177.234320411131,-5.68098887641932,
129.15078995125));
#167857=CARTESIAN_POINT('Ctrl Pts',(-177.226918589455,-5.63701887607436,
128.999727110124));
#167858=CARTESIAN_POINT('Ctrl Pts',(-177.21951676778,-5.58698509877179,
128.850301592753));
#167859=CARTESIAN_POINT('Ctrl Pts',(-177.212114946105,-5.53103519493896,
128.703032410254));
#167860=CARTESIAN_POINT('Ctrl Pts',(-177.204717031793,-5.47511482662469,
128.555840970009));
#167861=CARTESIAN_POINT('Ctrl Pts',(-177.197319117482,-5.4132846837787,
128.410803945714));
#167862=CARTESIAN_POINT('Ctrl Pts',(-177.189921203171,-5.34574190828615,
128.268424101702));
#167863=CARTESIAN_POINT('Ctrl Pts',(-177.182524518258,-5.27821035717784,
128.126067918638));
#167864=CARTESIAN_POINT('Ctrl Pts',(-177.175127833346,-5.20496821741377,
127.986368376403));
#167865=CARTESIAN_POINT('Ctrl Pts',(-177.167731148434,-5.12626036052953,
127.849807304701));
#167866=CARTESIAN_POINT('Ctrl Pts',(-177.160334791499,-5.04755599363414,
127.713252288259));
#167867=CARTESIAN_POINT('Ctrl Pts',(-177.152938434563,-4.96338657791109,
127.57983578907));
#167868=CARTESIAN_POINT('Ctrl Pts',(-177.145542077628,-4.87404231139147,
127.450013869052));
#167869=CARTESIAN_POINT('Ctrl Pts',(-177.138144588291,-4.78468436603631,
127.320172072967));
#167870=CARTESIAN_POINT('Ctrl Pts',(-177.130747098955,-4.69015020398907,
127.193926259383));
#167871=CARTESIAN_POINT('Ctrl Pts',(-177.123349609618,-4.59077251180646,
127.071702274328));
#167872=CARTESIAN_POINT('Ctrl Pts',(-177.115949527103,-4.49135998292834,
126.949435443845));
#167873=CARTESIAN_POINT('Ctrl Pts',(-177.108549444588,-4.38710077877733,
126.831193538343));
#167874=CARTESIAN_POINT('Ctrl Pts',(-177.101149362073,-4.27836678992182,
126.717368059046));
#167875=CARTESIAN_POINT('Ctrl Pts',(-177.093741142407,-4.16951323686698,
126.603417416933));
#167876=CARTESIAN_POINT('Ctrl Pts',(-177.08633292274,-4.05617533058798,
126.4938931695));
#167877=CARTESIAN_POINT('Ctrl Pts',(-177.078924703074,-3.93876115387232,
126.389149282279));
#167878=CARTESIAN_POINT('Ctrl Pts',(-177.071511923772,-3.82127471069039,
126.284340926943));
#167879=CARTESIAN_POINT('Ctrl Pts',(-177.06409914447,-3.69970728542012,
126.184319031213));
#167880=CARTESIAN_POINT('Ctrl Pts',(-177.056686365168,-3.57449829879662,
126.089395880222));
#167881=CARTESIAN_POINT('Ctrl Pts',(-177.049262994139,-3.44911040770114,
125.994337098581));
#167882=CARTESIAN_POINT('Ctrl Pts',(-177.041839623111,-3.32007086865978,
125.904391825007));
#167883=CARTESIAN_POINT('Ctrl Pts',(-177.034416252082,-3.18784688367952,
125.819828261495));
#167884=CARTESIAN_POINT('Ctrl Pts',(-177.030480202641,-3.11773855416769,
125.774990631044));
#167885=CARTESIAN_POINT('Ctrl Pts',(-177.0265441532,-3.04673536382247,125.731665219015));
#167886=CARTESIAN_POINT('Ctrl Pts',(-177.022608103759,-2.9749094111855,
125.689886592044));
#167887=CARTESIAN_POINT('Ctrl Pts',(-177.015184837353,-2.8394479061316,
125.611093405447));
#167888=CARTESIAN_POINT('Ctrl Pts',(-177.007761570948,-2.70064904146863,
125.537566523763));
#167889=CARTESIAN_POINT('Ctrl Pts',(-177.000338304542,-2.55896089669827,
125.469601982757));
#167890=CARTESIAN_POINT('Ctrl Pts',(-176.992923811821,-2.41744021554856,
125.401717770194));
#167891=CARTESIAN_POINT('Ctrl Pts',(-176.985509319101,-2.27303738493946,
125.339382972151));
#167892=CARTESIAN_POINT('Ctrl Pts',(-176.97809482638,-2.12622792171232,
125.282849466855));
#167893=CARTESIAN_POINT('Ctrl Pts',(-176.970687480026,-1.9795599589727,
125.226370450678));
#167894=CARTESIAN_POINT('Ctrl Pts',(-176.963280133672,-1.83049032751116,
125.175681728911));
#167895=CARTESIAN_POINT('Ctrl Pts',(-176.955872787318,-1.67951742044608,
125.130988446016));
#167896=CARTESIAN_POINT('Ctrl Pts',(-176.948470965643,-1.52865711467097,
125.086328497058));
#167897=CARTESIAN_POINT('Ctrl Pts',(-176.941069143967,-1.3758967161798,
125.047655188872));
#167898=CARTESIAN_POINT('Ctrl Pts',(-176.933667322292,-1.22175269238884,
125.015124837159));
#167899=CARTESIAN_POINT('Ctrl Pts',(-176.926269407981,-1.06769004002861,
124.982611657967));
#167900=CARTESIAN_POINT('Ctrl Pts',(-176.918871493669,-0.912245581333441,
124.956235053905));
#167901=CARTESIAN_POINT('Ctrl Pts',(-176.911473579358,-0.755948866182213,
124.936100920329));
#167902=CARTESIAN_POINT('Ctrl Pts',(-176.904076894446,-0.599678124709309,
124.91597013268));
#167903=CARTESIAN_POINT('Ctrl Pts',(-176.896680209534,-0.44255577774917,
124.90207980426));
#167904=CARTESIAN_POINT('Ctrl Pts',(-176.889283524621,-0.285119561322315,
124.894484358434));
#167905=CARTESIAN_POINT('Ctrl Pts',(-176.881887167686,-0.127690325782278,
124.886889249398));
#167906=CARTESIAN_POINT('Ctrl Pts',(-176.87449081075,0.030052378688286,
124.885588485957));
#167907=CARTESIAN_POINT('Ctrl Pts',(-176.867094453815,0.187567995156329,
124.890584428895));
#167908=CARTESIAN_POINT('Ctrl Pts',(-176.859696964478,0.345107727667371,
124.895581136725));
#167909=CARTESIAN_POINT('Ctrl Pts',(-176.852299475142,0.502419929814423,
124.906876458634));
#167910=CARTESIAN_POINT('Ctrl Pts',(-176.844901985805,0.658966500063999,
124.924420676181));
#167911=CARTESIAN_POINT('Ctrl Pts',(-176.83750190329,0.815567947471321,
124.941971043826));
#167912=CARTESIAN_POINT('Ctrl Pts',(-176.830101820775,0.971402857872432,
124.96577462691));
#167913=CARTESIAN_POINT('Ctrl Pts',(-176.82270173826,1.12594083426236,124.995730159339));
#167914=CARTESIAN_POINT('Ctrl Pts',(-176.815293518594,1.280648741044,125.025718630956));
#167915=CARTESIAN_POINT('Ctrl Pts',(-176.807885298927,1.43405649907329,
125.061872490389));
#167916=CARTESIAN_POINT('Ctrl Pts',(-176.800477079261,1.58564572840909,
125.104039733047));
#167917=CARTESIAN_POINT('Ctrl Pts',(-176.793064299959,1.73732825838658,
125.14623292894));
#167918=CARTESIAN_POINT('Ctrl Pts',(-176.785651520657,1.88718967484081,
125.194446768976));
#167919=CARTESIAN_POINT('Ctrl Pts',(-176.778238741354,2.03472972580306,
125.248480353788));
#167920=CARTESIAN_POINT('Ctrl Pts',(-176.770815370326,2.18248058890885,
125.30259114432));
#167921=CARTESIAN_POINT('Ctrl Pts',(-176.763391999297,2.32790311776757,
125.362538145704));
#167922=CARTESIAN_POINT('Ctrl Pts',(-176.755968628268,2.47051913234672,
125.428073257388));
#167923=CARTESIAN_POINT('Ctrl Pts',(-176.752032578827,2.54613756530169,
125.462821546097));
#167924=CARTESIAN_POINT('Ctrl Pts',(-176.748096529386,2.62096742020819,
125.499140097564));
#167925=CARTESIAN_POINT('Ctrl Pts',(-176.744160479946,2.69494064415454,
125.536986937355));
#167926=CARTESIAN_POINT('Ctrl Pts',(-176.73673721354,2.8344518358904,125.608364896039));
#167927=CARTESIAN_POINT('Ctrl Pts',(-176.729313947135,2.97133626054164,
125.685397236324));
#167928=CARTESIAN_POINT('Ctrl Pts',(-176.721890680729,3.1051026569196,125.767866990796));
#167929=CARTESIAN_POINT('Ctrl Pts',(-176.714476188008,3.23871095252604,
125.850239272868));
#167930=CARTESIAN_POINT('Ctrl Pts',(-176.707061695287,3.36920824071257,
125.938035983006));
#167931=CARTESIAN_POINT('Ctrl Pts',(-176.699647202566,3.49612558072596,
126.030993201758));
#167932=CARTESIAN_POINT('Ctrl Pts',(-176.692239856212,3.6229205930287,126.123860824844));
#167933=CARTESIAN_POINT('Ctrl Pts',(-176.684832509859,3.74614222726404,
126.221878835408));
#167934=CARTESIAN_POINT('Ctrl Pts',(-176.677425163505,3.86534849593,126.324738806798));
#167935=CARTESIAN_POINT('Ctrl Pts',(-176.67002334183,3.98446585606339,126.42752206134));
#167936=CARTESIAN_POINT('Ctrl Pts',(-176.662621520154,4.09957353228987,
126.535139843268));
#167937=CARTESIAN_POINT('Ctrl Pts',(-176.655219698479,4.21026084852899,
126.64724212637));
#167938=CARTESIAN_POINT('Ctrl Pts',(-176.647821784167,4.32088973379546,
126.75928523155));
#167939=CARTESIAN_POINT('Ctrl Pts',(-176.640423869856,4.42710264468329,
126.875807858287));
#167940=CARTESIAN_POINT('Ctrl Pts',(-176.633025955545,4.5285242537886,126.996421720295));
#167941=CARTESIAN_POINT('Ctrl Pts',(-176.625629270632,4.62992900846261,
127.117015538468));
#167942=CARTESIAN_POINT('Ctrl Pts',(-176.61823258572,4.72654380161574,127.241698957101));
#167943=CARTESIAN_POINT('Ctrl Pts',(-176.610835900808,4.81803218587554,
127.370048980809));
#167944=CARTESIAN_POINT('Ctrl Pts',(-176.603439543872,4.90951651344424,
127.498393313341));
#167945=CARTESIAN_POINT('Ctrl Pts',(-176.596043186937,4.99587466741297,
127.630403623705));
#167946=CARTESIAN_POINT('Ctrl Pts',(-176.588646830002,5.0768124773605,127.765626402104));
#167947=CARTESIAN_POINT('Ctrl Pts',(-176.581249340665,5.15776267909337,
127.900869883456));
#167948=CARTESIAN_POINT('Ctrl Pts',(-176.573851851329,5.2332906926952,128.039326491832));
#167949=CARTESIAN_POINT('Ctrl Pts',(-176.566454361992,5.30314749067731,
128.180516633137));
#167950=CARTESIAN_POINT('Ctrl Pts',(-176.559054279477,5.37302877685177,
128.321756268428));
#167951=CARTESIAN_POINT('Ctrl Pts',(-176.551654196962,5.43723472380216,
128.465731010114));
#167952=CARTESIAN_POINT('Ctrl Pts',(-176.544254114447,5.49556383702317,
128.611939883377));
#167953=CARTESIAN_POINT('Ctrl Pts',(-176.53684589478,5.55395708910046,128.758309528326));
#167954=CARTESIAN_POINT('Ctrl Pts',(-176.529437675114,5.60646046363653,
128.90691786402));
#167955=CARTESIAN_POINT('Ctrl Pts',(-176.522029455448,5.65292164937822,
129.057246600539));
#167956=CARTESIAN_POINT('Ctrl Pts',(-176.514616676145,5.69941143120462,
129.207667861888));
#167957=CARTESIAN_POINT('Ctrl Pts',(-176.507203896843,5.73985151825766,
129.359811274075));
#167958=CARTESIAN_POINT('Ctrl Pts',(-176.499791117541,5.77414053445561,
129.513147369935));
#167959=CARTESIAN_POINT('Ctrl Pts',(-176.492367746513,5.80847854440786,
129.6667025596));
#167960=CARTESIAN_POINT('Ctrl Pts',(-176.484944375484,5.83664786334767,
129.821453470244));
#167961=CARTESIAN_POINT('Ctrl Pts',(-176.477521004455,5.85859875730653,
129.976863691054));
#167962=CARTESIAN_POINT('Ctrl Pts',(-176.473584955014,5.87023764798798,
130.059265919145));
#167963=CARTESIAN_POINT('Ctrl Pts',(-176.469648905573,5.8801291864416,130.141853459566));
#167964=CARTESIAN_POINT('Ctrl Pts',(-176.465712856133,5.88827190268693,
130.224546369269));
#167965=CARTESIAN_POINT('Ctrl Pts',(-176.458289589727,5.90362881140016,
130.380502616212));
#167966=CARTESIAN_POINT('Ctrl Pts',(-176.450866323322,5.91280869696112,
130.537305220984));
#167967=CARTESIAN_POINT('Ctrl Pts',(-176.443443056916,5.91572856152709,
130.694423595446));
#167968=CARTESIAN_POINT('Ctrl Pts',(-176.436028564195,5.91864497505563,
130.851356269038));
#167969=CARTESIAN_POINT('Ctrl Pts',(-176.428614071474,5.91531608812268,
131.008603599848));
#167970=CARTESIAN_POINT('Ctrl Pts',(-176.421199578753,5.90571046970631,
131.165628399829));
#167971=CARTESIAN_POINT('Ctrl Pts',(-176.413792232399,5.89611410954661,
131.322501853396));
#167972=CARTESIAN_POINT('Ctrl Pts',(-176.406384886046,5.88025308440494,
131.479152833029));
#167973=CARTESIAN_POINT('Ctrl Pts',(-176.398977539692,5.8581479773177,131.635042769986));
#167974=CARTESIAN_POINT('Ctrl Pts',(-176.391575718016,5.8360593570533,131.790816438346));
#167975=CARTESIAN_POINT('Ctrl Pts',(-176.384173896341,5.80773597988552,
131.945829826216));
#167976=CARTESIAN_POINT('Ctrl Pts',(-176.376772074666,5.77325035232502,
132.099548222463));
#167977=CARTESIAN_POINT('Ctrl Pts',(-176.369374160354,5.73878292945897,
132.253185471965));
#167978=CARTESIAN_POINT('Ctrl Pts',(-176.361976246043,5.69815981622234,
132.405528727975));
#167979=CARTESIAN_POINT('Ctrl Pts',(-176.354578331732,5.65150481523468,
132.556052338697));
#167980=CARTESIAN_POINT('Ctrl Pts',(-176.347181646819,5.60485756746171,
132.706550935126));
#167981=CARTESIAN_POINT('Ctrl Pts',(-176.339784961907,5.55218053179486,
132.855230130211));
#167982=CARTESIAN_POINT('Ctrl Pts',(-176.332388276995,5.49364772820861,
133.001578221912));
#167983=CARTESIAN_POINT('Ctrl Pts',(-176.32499192006,5.43511752002822,133.147919824385));
#167984=CARTESIAN_POINT('Ctrl Pts',(-176.317595563124,5.37073219882822,
133.291930182392));
#167985=CARTESIAN_POINT('Ctrl Pts',(-176.310199206189,5.30071430894531,
133.433116668903));
#167986=CARTESIAN_POINT('Ctrl Pts',(-176.302801716852,5.23068569914471,
133.574324771426));
#167987=CARTESIAN_POINT('Ctrl Pts',(-176.295404227515,5.15502296944984,
133.712707807152));
#167988=CARTESIAN_POINT('Ctrl Pts',(-176.288006738179,5.07399501051325,
133.847797029878));
#167989=CARTESIAN_POINT('Ctrl Pts',(-176.280606655664,4.99293864735137,
133.982933607922));
#167990=CARTESIAN_POINT('Ctrl Pts',(-176.273206573149,4.90651350223879,
134.114773754158));
#167991=CARTESIAN_POINT('Ctrl Pts',(-176.265806490634,4.81503214677668,
134.242877156425));
#167992=CARTESIAN_POINT('Ctrl Pts',(-176.258398270967,4.72345019815959,
134.371121421553));
#167993=CARTESIAN_POINT('Ctrl Pts',(-176.250990051301,4.62680115293626,
134.495620432926));
#167994=CARTESIAN_POINT('Ctrl Pts',(-176.243581831635,4.52543873514238,
134.615965898412));
#167995=CARTESIAN_POINT('Ctrl Pts',(-176.236169052333,4.42401393047166,
134.736385434524));
#167996=CARTESIAN_POINT('Ctrl Pts',(-176.22875627303,4.31787022373021,134.85264605568));
#167997=CARTESIAN_POINT('Ctrl Pts',(-176.221343493728,4.2073982743899,134.964376281378));
#167998=CARTESIAN_POINT('Ctrl Pts',(-176.2139201227,4.09676847754758,135.076266152462));
#167999=CARTESIAN_POINT('Ctrl Pts',(-176.206496751671,3.9817983586106,135.183612445486));
#168000=CARTESIAN_POINT('Ctrl Pts',(-176.199073380642,3.86291233276183,
135.286083374709));
#168001=CARTESIAN_POINT('Ctrl Pts',(-176.195137331201,3.7998761092251,135.34041592014));
#168002=CARTESIAN_POINT('Ctrl Pts',(-176.191201281761,3.73573949061561,
135.393378534495));
#168003=CARTESIAN_POINT('Ctrl Pts',(-176.18726523232,3.67056894072435,135.444926769868));
#168004=CARTESIAN_POINT('Ctrl Pts',(-176.179841965914,3.54765931753379,
135.542145133014));
#168005=CARTESIAN_POINT('Ctrl Pts',(-176.172418699509,3.42069879763591,
135.63462406872));
#168006=CARTESIAN_POINT('Ctrl Pts',(-176.164995433103,3.2900889174967,135.722006952701));
#168007=CARTESIAN_POINT('Ctrl Pts',(-176.157580940382,3.15963340738935,
135.809286557369));
#168008=CARTESIAN_POINT('Ctrl Pts',(-176.150166447661,3.02553742980314,
135.891481893796));
#168009=CARTESIAN_POINT('Ctrl Pts',(-176.14275195494,2.88823594702113,135.968276154911));
#168010=CARTESIAN_POINT('Ctrl Pts',(-176.135344608586,2.75106680057753,
136.044996398826));
#168011=CARTESIAN_POINT('Ctrl Pts',(-176.127937262233,2.6106986233099,136.116325750071));
#168012=CARTESIAN_POINT('Ctrl Pts',(-176.120529915879,2.46759565398815,
136.181990416178));
#168013=CARTESIAN_POINT('Ctrl Pts',(-176.113128094203,2.32459941625988,
136.247606107099));
#168014=CARTESIAN_POINT('Ctrl Pts',(-176.105726272528,2.17887278564117,
136.307565370285));
#168015=CARTESIAN_POINT('Ctrl Pts',(-176.098324450853,2.03090482129261,
136.361640183086));
#168016=CARTESIAN_POINT('Ctrl Pts',(-176.090926536541,1.88301496808065,
136.415686450215));
#168017=CARTESIAN_POINT('Ctrl Pts',(-176.08352862223,1.73288648723452,136.463854325608));
#168018=CARTESIAN_POINT('Ctrl Pts',(-176.076130707919,1.5810285428379,136.505963840277));
#168019=CARTESIAN_POINT('Ctrl Pts',(-176.068734023006,1.42919583447687,
136.54806635711));
#168020=CARTESIAN_POINT('Ctrl Pts',(-176.061337338094,1.27563459235188,
136.584112411747));
#168021=CARTESIAN_POINT('Ctrl Pts',(-176.053940653182,1.12086938792917,
136.61397182467));
#168022=CARTESIAN_POINT('Ctrl Pts',(-176.046544296246,0.966111045957819,
136.643829913595));
#168023=CARTESIAN_POINT('Ctrl Pts',(-176.039147939311,0.810149214374073,
136.667501835533));
#168024=CARTESIAN_POINT('Ctrl Pts',(-176.031751582376,0.653518644899017,
136.684908546396));
#168025=CARTESIAN_POINT('Ctrl Pts',(-176.024354093039,0.496864094883469,
136.702317922271));
#168026=CARTESIAN_POINT('Ctrl Pts',(-176.016956603702,0.339540974151185,
136.713460135902));
#168027=CARTESIAN_POINT('Ctrl Pts',(-176.009559114366,0.182088994122295,
136.718308043839));
#168028=CARTESIAN_POINT('Ctrl Pts',(-176.002159031851,0.0245818195456645,
136.723157651202));
#168029=CARTESIAN_POINT('Ctrl Pts',(-175.994758949336,-0.133053931375224,
136.721708548347));
#168030=CARTESIAN_POINT('Ctrl Pts',(-175.987358866821,-0.290278858964217,
136.713985711135));
#168031=CARTESIAN_POINT('Ctrl Pts',(-175.979950647154,-0.447676671523984,
136.706254381869));
#168032=CARTESIAN_POINT('Ctrl Pts',(-175.972542427488,-0.604662385515286,
136.692235559584));
#168033=CARTESIAN_POINT('Ctrl Pts',(-175.965134207821,-0.760701296722034,
136.672006150458));
#168034=CARTESIAN_POINT('Ctrl Pts',(-175.957721428519,-0.916836247274981,
136.651764290468));
#168035=CARTESIAN_POINT('Ctrl Pts',(-175.950308649217,-1.07202286672424,
136.625304289398));
#168036=CARTESIAN_POINT('Ctrl Pts',(-175.942895869915,-1.22573745701421,
136.592754025842));
#168037=CARTESIAN_POINT('Ctrl Pts',(-175.935472498886,-1.37967168191951,
136.560157252942));
#168038=CARTESIAN_POINT('Ctrl Pts',(-175.928049127857,-1.53212931603322,
136.521452929216));
#168039=CARTESIAN_POINT('Ctrl Pts',(-175.920625756829,-1.6826018118403,
136.476818788879));
#168040=CARTESIAN_POINT('Ctrl Pts',(-175.916689707388,-1.76238593965281,
136.453152696691));
#168041=CARTESIAN_POINT('Ctrl Pts',(-175.912753657947,-1.84161229606844,
136.427820329755));
#168042=CARTESIAN_POINT('Ctrl Pts',(-175.908817608507,-1.92020756050174,
136.400853580761));
#168043=CARTESIAN_POINT('Ctrl Pts',(-175.901394342101,-2.06843577635333,
136.34999513376));
#168044=CARTESIAN_POINT('Ctrl Pts',(-175.893971075696,-2.21486618629056,
136.293166776334));
#168045=CARTESIAN_POINT('Ctrl Pts',(-175.88654780929,-2.35898171193482,
136.230513568346));
#168046=CARTESIAN_POINT('Ctrl Pts',(-175.879133316569,-2.50292690499581,
136.167934411247));
#168047=CARTESIAN_POINT('Ctrl Pts',(-175.871718823848,-2.64456232078667,
136.099544254579));
#168048=CARTESIAN_POINT('Ctrl Pts',(-175.864304331127,-2.7833863128084,
136.025537802471));
#168049=CARTESIAN_POINT('Ctrl Pts',(-175.856896984773,-2.92207650103999,
135.951602680568));
#168050=CARTESIAN_POINT('Ctrl Pts',(-175.849489638419,-3.0579603328917,
135.872062214263));
#168051=CARTESIAN_POINT('Ctrl Pts',(-175.842082292066,-3.19055652661036,
135.787158989265));
#168052=CARTESIAN_POINT('Ctrl Pts',(-175.83468047039,-3.32305382508517,
135.702319088295));
#168053=CARTESIAN_POINT('Ctrl Pts',(-175.827278648715,-3.45226805475828,
135.612124593101));
#168054=CARTESIAN_POINT('Ctrl Pts',(-175.819876827039,-3.57774302529583,
135.516863711193));
#168055=CARTESIAN_POINT('Ctrl Pts',(-175.812478912728,-3.70315175857313,
135.421653116764));
#168056=CARTESIAN_POINT('Ctrl Pts',(-175.805080998417,-3.82482486731538,
135.321381687183));
#168057=CARTESIAN_POINT('Ctrl Pts',(-175.797683084105,-3.94233572289361,
135.216380518983));
#168058=CARTESIAN_POINT('Ctrl Pts',(-175.790286399193,-4.05982705029934,
135.111396800071));
#168059=CARTESIAN_POINT('Ctrl Pts',(-175.782889714281,-4.17315721925357,
135.001685150996));
#168060=CARTESIAN_POINT('Ctrl Pts',(-175.775493029369,-4.28193316234904,
134.887616543378));
#168061=CARTESIAN_POINT('Ctrl Pts',(-175.768096672433,-4.3907042822052,
134.773552993681));
#168062=CARTESIAN_POINT('Ctrl Pts',(-175.760700315498,-4.49492132010646,
134.655133139727));
#168063=CARTESIAN_POINT('Ctrl Pts',(-175.753303958562,-4.59422872765494,
134.532764158023));
#168064=CARTESIAN_POINT('Ctrl Pts',(-175.745906469226,-4.69355133942103,
134.410376441315));
#168065=CARTESIAN_POINT('Ctrl Pts',(-175.738508979889,-4.78796258889911,
134.284038682851));
#168066=CARTESIAN_POINT('Ctrl Pts',(-175.731111490553,-4.87714791233018,
134.154190285438));
#168067=CARTESIAN_POINT('Ctrl Pts',(-175.723711408037,-4.9663644995385,
134.024296369869));
#168068=CARTESIAN_POINT('Ctrl Pts',(-175.716311325522,-5.05035130210546,
133.890889672652));
#168069=CARTESIAN_POINT('Ctrl Pts',(-175.708911243007,-5.12883777423118,
133.754437506076));
#168070=CARTESIAN_POINT('Ctrl Pts',(-175.701503023341,-5.20741055030126,
133.617835296315));
#168071=CARTESIAN_POINT('Ctrl Pts',(-175.694094803674,-5.28047073108043,
133.478181253193));
#168072=CARTESIAN_POINT('Ctrl Pts',(-175.686686584008,-5.347793999225,133.33596680818));
#168073=CARTESIAN_POINT('Ctrl Pts',(-175.679273804706,-5.41515870371796,
133.193664832547));
#168074=CARTESIAN_POINT('Ctrl Pts',(-175.671861025404,-5.47677931388848,
133.048799657591));
#168075=CARTESIAN_POINT('Ctrl Pts',(-175.664448246102,-5.53248034602625,
132.901881006819));
#168076=CARTESIAN_POINT('Ctrl Pts',(-175.657024875073,-5.58826096641077,
132.75475243179));
#168077=CARTESIAN_POINT('Ctrl Pts',(-175.649601504044,-5.63810499791941,
132.605564874005));
#168078=CARTESIAN_POINT('Ctrl Pts',(-175.642178133015,-5.68188709102735,
132.454842258578));
#168079=CARTESIAN_POINT('Ctrl Pts',(-175.638242083575,-5.70510140732827,
132.374925511345));
#168080=CARTESIAN_POINT('Ctrl Pts',(-175.634306034134,-5.72661235042798,
132.294577370783));
#168081=CARTESIAN_POINT('Ctrl Pts',(-175.630369984694,-5.7464071209827,
132.213876762354));
#168082=CARTESIAN_POINT('Ctrl Pts',(-175.620466734164,-5.79621151875603,
132.010830953281));
#168083=CARTESIAN_POINT('Ctrl Pts',(-175.610563483633,-5.83527224067263,
131.805053969676));
#168084=CARTESIAN_POINT('Ctrl Pts',(-175.600660233103,-5.86334628783755,
131.597519410874));
#168085=CARTESIAN_POINT('Ctrl Pts',(-175.590995694119,-5.89074362797718,
131.394987340424));
#168086=CARTESIAN_POINT('Ctrl Pts',(-175.581331155135,-5.90767763415524,
131.1907810782));
#168087=CARTESIAN_POINT('Ctrl Pts',(-175.571666616152,-5.91396652719755,
130.985828184054));
#168088=CARTESIAN_POINT('Ctrl Pts',(-175.568902812819,-5.91576498479371,
130.927217060148));
#168089=CARTESIAN_POINT('Ctrl Pts',(-175.566139009486,-5.91669315462093,
130.868545037559));
#168090=CARTESIAN_POINT('Ctrl Pts',(-175.563375206154,-5.91674746817804,
130.809834218641));
#168091=CARTESIAN_POINT('',(-173.813375192207,-5.90703979259401,130.803529349416));
#168092=CARTESIAN_POINT('Ctrl Pts',(-175.563375192208,-5.91627067345725,
130.809833481333));
#168093=CARTESIAN_POINT('Ctrl Pts',(-175.492890915099,-5.90250338860239,
129.312659330916));
#168094=CARTESIAN_POINT('Ctrl Pts',(-175.329590763386,-4.56443645972603,
125.822059968559));
#168095=CARTESIAN_POINT('Ctrl Pts',(-175.073474737067,1.30891178749135,
123.929456220927));
#168096=CARTESIAN_POINT('Ctrl Pts',(-174.795027113256,6.49155056939029,
128.189531419434));
#168097=CARTESIAN_POINT('Ctrl Pts',(-174.516579489441,5.70877150789232,
134.852506909512));
#168098=CARTESIAN_POINT('Ctrl Pts',(-174.238131865631,-0.320089680364641,
137.795433720237));
#168099=CARTESIAN_POINT('Ctrl Pts',(-174.003730433218,-5.14765923758726,
134.864630788722));
#168100=CARTESIAN_POINT('Ctrl Pts',(-173.86214487541,-5.90574070942643,
131.843544224169));
#168101=CARTESIAN_POINT('Ctrl Pts',(-173.813375192207,-5.90703979259401,
130.803529349416));
#168102=CARTESIAN_POINT('',(-172.06337600335,-5.91851287666386,130.799189814356));
#168103=CARTESIAN_POINT('Ctrl Pts',(-173.813375192207,-5.90703979259401,
130.803529349416));
#168104=CARTESIAN_POINT('Ctrl Pts',(-173.769329000806,-5.90821305561495,
129.864243071036));
#168105=CARTESIAN_POINT('Ctrl Pts',(-173.632466934801,-5.25333338380343,
126.947201347647));
#168106=CARTESIAN_POINT('Ctrl Pts',(-173.40278899419,-0.675210770690227,
123.838612205118));
#168107=CARTESIAN_POINT('Ctrl Pts',(-173.124341370378,5.49551350513835,
126.471129508431));
#168108=CARTESIAN_POINT('Ctrl Pts',(-172.845893746565,6.61612934050591,
133.085674510926));
#168109=CARTESIAN_POINT('Ctrl Pts',(-172.567446122752,1.65684552783385,
137.603803493805));
#168110=CARTESIAN_POINT('Ctrl Pts',(-172.306607000367,-4.4150988260753,
135.982992920257));
#168111=CARTESIAN_POINT('Ctrl Pts',(-172.138583752587,-5.90466033572452,
132.394578448931));
#168112=CARTESIAN_POINT('Ctrl Pts',(-172.063376379411,-5.91933123059252,
130.799197074345));
#168113=CARTESIAN_POINT('',(-170.313373776064,-5.92100765474907,130.807582161906));
#168114=CARTESIAN_POINT('Ctrl Pts',(-172.063375192207,-5.91674772684328,
130.799174154912));
#168115=CARTESIAN_POINT('Ctrl Pts',(-172.052420060435,-5.91654410871785,
130.566885375217));
#168116=CARTESIAN_POINT('Ctrl Pts',(-172.041464928663,-5.90265803068872,
130.335172335765));
#168117=CARTESIAN_POINT('Ctrl Pts',(-172.03050979689,-5.87531071615658,
130.105322313096));
#168118=CARTESIAN_POINT('Ctrl Pts',(-172.023856822969,-5.85870288576437,
129.965736022543));
#168119=CARTESIAN_POINT('Ctrl Pts',(-172.017203849047,-5.83713132794981,
129.826836005019));
#168120=CARTESIAN_POINT('Ctrl Pts',(-172.010550875126,-5.81065316603754,
129.688905398152));
#168121=CARTESIAN_POINT('Ctrl Pts',(-172.003127608721,-5.78110931810908,
129.535004954177));
#168122=CARTESIAN_POINT('Ctrl Pts',(-171.995704342315,-5.74540228303988,
129.382046349289));
#168123=CARTESIAN_POINT('Ctrl Pts',(-171.988281075909,-5.70360308744345,
129.230561906356));
#168124=CARTESIAN_POINT('Ctrl Pts',(-171.980866583188,-5.66185329502501,
129.079256505455));
#168125=CARTESIAN_POINT('Ctrl Pts',(-171.973452090467,-5.61402577289467,
128.929422154712));
#168126=CARTESIAN_POINT('Ctrl Pts',(-171.966037597746,-5.56024286681052,
128.78158286789));
#168127=CARTESIAN_POINT('Ctrl Pts',(-171.958630251392,-5.50651179871599,
128.633886074139));
#168128=CARTESIAN_POINT('Ctrl Pts',(-171.951222905038,-5.44683690068766,
128.488180864608));
#168129=CARTESIAN_POINT('Ctrl Pts',(-171.943815558684,-5.38139078496531,
128.344977812472));
#168130=CARTESIAN_POINT('Ctrl Pts',(-171.936413737009,-5.31599348142539,
128.201881566576));
#168131=CARTESIAN_POINT('Ctrl Pts',(-171.929011915333,-5.24483368531546,
128.061284100271));
#168132=CARTESIAN_POINT('Ctrl Pts',(-171.921610093658,-5.16813270157619,
127.923677549022));
#168133=CARTESIAN_POINT('Ctrl Pts',(-171.914212179347,-5.09147220768898,
127.786143639199));
#168134=CARTESIAN_POINT('Ctrl Pts',(-171.906814265035,-5.00927653303559,
127.651597825255));
#168135=CARTESIAN_POINT('Ctrl Pts',(-171.899416350724,-4.92181359715705,
127.520508995257));
#168136=CARTESIAN_POINT('Ctrl Pts',(-171.892019665812,-4.83436519603208,
127.389441949846));
#168137=CARTESIAN_POINT('Ctrl Pts',(-171.884622980899,-4.74165147792062,
127.261831058413));
#168138=CARTESIAN_POINT('Ctrl Pts',(-171.877226295987,-4.64398455440899,
127.13811757858));
#168139=CARTESIAN_POINT('Ctrl Pts',(-171.869829939052,-4.54632196155081,
127.014409584333));
#168140=CARTESIAN_POINT('Ctrl Pts',(-171.862433582116,-4.44370683130106,
126.894598951067));
#168141=CARTESIAN_POINT('Ctrl Pts',(-171.85503722518,-4.33649238910272,
126.779094872084));
#168142=CARTESIAN_POINT('Ctrl Pts',(-171.847639735844,-4.22926153209957,
126.663573109131));
#168143=CARTESIAN_POINT('Ctrl Pts',(-171.840242246507,-4.11743021503611,
126.552359486918));
#168144=CARTESIAN_POINT('Ctrl Pts',(-171.832844757171,-4.00138932459684,
126.445827144538));
#168145=CARTESIAN_POINT('Ctrl Pts',(-171.825444674656,-3.88530775620348,
126.339257457412));
#168146=CARTESIAN_POINT('Ctrl Pts',(-171.818044592141,-3.76501395122304,
126.237372569665));
#168147=CARTESIAN_POINT('Ctrl Pts',(-171.810644509626,-3.64093260939317,
126.140505956842));
#168148=CARTESIAN_POINT('Ctrl Pts',(-171.803236289959,-3.5167148273719,
126.043532829219));
#168149=CARTESIAN_POINT('Ctrl Pts',(-171.795828070293,-3.38870148558098,
125.951589226399));
#168150=CARTESIAN_POINT('Ctrl Pts',(-171.788419850626,-3.25734765439931,
125.864966239621));
#168151=CARTESIAN_POINT('Ctrl Pts',(-171.781007071324,-3.12591297712631,
125.778289937839));
#168152=CARTESIAN_POINT('Ctrl Pts',(-171.773594292022,-2.99113403244836,
125.696940969901));
#168153=CARTESIAN_POINT('Ctrl Pts',(-171.76618151272,-2.85349085772153,
125.621164645253));
#168154=CARTESIAN_POINT('Ctrl Pts',(-171.758758141691,-2.71565101197164,
125.545280047839));
#168155=CARTESIAN_POINT('Ctrl Pts',(-171.751334770662,-2.57493909550023,
125.47498416291));
#168156=CARTESIAN_POINT('Ctrl Pts',(-171.743911399634,-2.43185624531328,
125.410474656162));
#168157=CARTESIAN_POINT('Ctrl Pts',(-171.739975350194,-2.35599028493666,
125.376270167808));
#168158=CARTESIAN_POINT('Ctrl Pts',(-171.736039300754,-2.27945805489288,
125.34369161463));
#168159=CARTESIAN_POINT('Ctrl Pts',(-171.732103251314,-2.20233590191188,
125.312762750128));
#168160=CARTESIAN_POINT('Ctrl Pts',(-171.724679984909,-2.05688592825637,
125.25443187692));
#168161=CARTESIAN_POINT('Ctrl Pts',(-171.717256718503,-1.90889699730604,
125.201795354637));
#168162=CARTESIAN_POINT('Ctrl Pts',(-171.709833452098,-1.75885535898401,
125.155081160089));
#168163=CARTESIAN_POINT('Ctrl Pts',(-171.702418959377,-1.6089910574183,
125.108422177839));
#168164=CARTESIAN_POINT('Ctrl Pts',(-171.695004466656,-1.45707923064753,
125.06767170027));
#168165=CARTESIAN_POINT('Ctrl Pts',(-171.687589973935,-1.30362687716122,
125.033010036667));
#168166=CARTESIAN_POINT('Ctrl Pts',(-171.680182627581,-1.15032242683059,
124.998381781281));
#168167=CARTESIAN_POINT('Ctrl Pts',(-171.672775281227,-0.995480767443993,
124.969830738274));
#168168=CARTESIAN_POINT('Ctrl Pts',(-171.665367934874,-0.839624759804996,
124.947487661353));
#168169=CARTESIAN_POINT('Ctrl Pts',(-171.657966113198,-0.683884995456607,
124.925161248741));
#168170=CARTESIAN_POINT('Ctrl Pts',(-171.650564291523,-0.527132757157224,
124.909033635737));
#168171=CARTESIAN_POINT('Ctrl Pts',(-171.643162469847,-0.369901713135807,
124.899184643463));
#168172=CARTESIAN_POINT('Ctrl Pts',(-171.635764555536,-0.212753670158198,
124.889340850396));
#168173=CARTESIAN_POINT('Ctrl Pts',(-171.628366641225,-0.0551276964624343,
124.885769100483));
#168174=CARTESIAN_POINT('Ctrl Pts',(-171.620968726913,0.102436902084779,
124.88849743088));
#168175=CARTESIAN_POINT('Ctrl Pts',(-171.613572042001,0.259975316254002,
124.891225307877));
#168176=CARTESIAN_POINT('Ctrl Pts',(-171.606175357089,0.417452002641037,
124.900251180824));
#168177=CARTESIAN_POINT('Ctrl Pts',(-171.598778672177,0.574327014776075,
124.915550971925));
#168178=CARTESIAN_POINT('Ctrl Pts',(-171.591382315241,0.731195070908682,
124.930850084617));
#168179=CARTESIAN_POINT('Ctrl Pts',(-171.583985958306,0.887461134301129,
124.952422526089));
#168180=CARTESIAN_POINT('Ctrl Pts',(-171.57658960137,1.04259001206037,124.980192296745));
#168181=CARTESIAN_POINT('Ctrl Pts',(-171.569192112034,1.19774264044638,
125.007966319024));
#168182=CARTESIAN_POINT('Ctrl Pts',(-171.561794622697,1.35175736905057,
125.041939493946));
#168183=CARTESIAN_POINT('Ctrl Pts',(-171.55439713336,1.50410898158405,125.081984648266));
#168184=CARTESIAN_POINT('Ctrl Pts',(-171.546997050845,1.65651400073979,
125.122043840354));
#168185=CARTESIAN_POINT('Ctrl Pts',(-171.53959696833,1.80725438226129,125.168179154876));
#168186=CARTESIAN_POINT('Ctrl Pts',(-171.532196885815,1.95582000314838,
125.220213531593));
#168187=CARTESIAN_POINT('Ctrl Pts',(-171.524788666149,2.10454898720834,
125.272305125455));
#168188=CARTESIAN_POINT('Ctrl Pts',(-171.517380446482,2.25109808237563,
125.330308612257));
#168189=CARTESIAN_POINT('Ctrl Pts',(-171.509972226816,2.39497640869152,
125.393998470324));
#168190=CARTESIAN_POINT('Ctrl Pts',(-171.502559447514,2.53894328971694,
125.457727528436));
#168191=CARTESIAN_POINT('Ctrl Pts',(-171.495146668212,2.68023579212227,
125.5271497675));
#168192=CARTESIAN_POINT('Ctrl Pts',(-171.487733888909,2.81838805820637,
125.601993914241));
#168193=CARTESIAN_POINT('Ctrl Pts',(-171.480310517881,2.95673772272675,
125.676945001809));
#168194=CARTESIAN_POINT('Ctrl Pts',(-171.472887146852,3.09193786953243,
125.757333279426));
#168195=CARTESIAN_POINT('Ctrl Pts',(-171.465463775823,3.22355132008199,
125.842843969474));
#168196=CARTESIAN_POINT('Ctrl Pts',(-171.461527726382,3.29333592958626,
125.888183789139));
#168197=CARTESIAN_POINT('Ctrl Pts',(-171.457591676941,3.36211272880741,
125.934963018023));
#168198=CARTESIAN_POINT('Ctrl Pts',(-171.4536556275,3.4298204659807,125.983130262808));
#168199=CARTESIAN_POINT('Ctrl Pts',(-171.446232361095,3.55751514520048,
126.073972183222));
#168200=CARTESIAN_POINT('Ctrl Pts',(-171.43880909469,3.68179137415032,126.170028136082));
#168201=CARTESIAN_POINT('Ctrl Pts',(-171.431385828284,3.80219451952221,
126.271012252592));
#168202=CARTESIAN_POINT('Ctrl Pts',(-171.423971335563,3.92245535837514,
126.371877014262));
#168203=CARTESIAN_POINT('Ctrl Pts',(-171.416556842842,4.03885194229015,
126.477658107978));
#168204=CARTESIAN_POINT('Ctrl Pts',(-171.409142350121,4.15095852688988,
126.588026443127));
#168205=CARTESIAN_POINT('Ctrl Pts',(-171.401735003767,4.26295705894264,
126.69828840112));
#168206=CARTESIAN_POINT('Ctrl Pts',(-171.394327657414,4.37067355914808,
126.813128538362));
#168207=CARTESIAN_POINT('Ctrl Pts',(-171.38692031106,4.47371540167417,126.932177632824));
#168208=CARTESIAN_POINT('Ctrl Pts',(-171.379518489384,4.57668039170655,
127.05113793598));
#168209=CARTESIAN_POINT('Ctrl Pts',(-171.372116667709,4.67497742297217,
127.174300664748));
#168210=CARTESIAN_POINT('Ctrl Pts',(-171.364714846034,4.76825087898503,
127.301259974199));
#168211=CARTESIAN_POINT('Ctrl Pts',(-171.357316931722,4.8614750966665,127.428152262819));
#168212=CARTESIAN_POINT('Ctrl Pts',(-171.349919017411,4.94968080003645,
127.558836840615));
#168213=CARTESIAN_POINT('Ctrl Pts',(-171.3425211031,5.03255289264745,127.692875129056));
#168214=CARTESIAN_POINT('Ctrl Pts',(-171.335124418187,5.11541121342024,
127.826891142766));
#168215=CARTESIAN_POINT('Ctrl Pts',(-171.327727733275,5.19293748645846,
127.964259443792));
#168216=CARTESIAN_POINT('Ctrl Pts',(-171.320331048363,5.26486011483673,
128.10451274524));
#168217=CARTESIAN_POINT('Ctrl Pts',(-171.312934691428,5.3367795540903,128.244759827711));
#168218=CARTESIAN_POINT('Ctrl Pts',(-171.305538334492,5.40309567239127,
128.387891324079));
#168219=CARTESIAN_POINT('Ctrl Pts',(-171.298141977557,5.46358312551962,
128.533415881771));
#168220=CARTESIAN_POINT('Ctrl Pts',(-171.29074448822,5.52407983943146,128.678962719643));
#168221=CARTESIAN_POINT('Ctrl Pts',(-171.283346998884,5.57874596802939,
128.826903003628));
#168222=CARTESIAN_POINT('Ctrl Pts',(-171.275949509547,5.62740461353139,
128.976726114142));
#168223=CARTESIAN_POINT('Ctrl Pts',(-171.268549427032,5.67608031624607,
129.126601744915));
#168224=CARTESIAN_POINT('Ctrl Pts',(-171.261149344517,5.71874422776907,
129.278361161495));
#168225=CARTESIAN_POINT('Ctrl Pts',(-171.253749262002,5.75526957995392,
129.43147947757));
#168226=CARTESIAN_POINT('Ctrl Pts',(-171.246341042336,5.79183509551844,
129.584766162974));
#168227=CARTESIAN_POINT('Ctrl Pts',(-171.238932822669,5.82224848492687,
129.739414368654));
#168228=CARTESIAN_POINT('Ctrl Pts',(-171.231524603003,5.84643415334193,
129.894889203426));
#168229=CARTESIAN_POINT('Ctrl Pts',(-171.224111823701,5.87063470763234,
130.050459730365));
#168230=CARTESIAN_POINT('Ctrl Pts',(-171.216699044399,5.88859986057887,
130.206857530197));
#168231=CARTESIAN_POINT('Ctrl Pts',(-171.209286265097,5.90030603460425,
130.363544033812));
#168232=CARTESIAN_POINT('Ctrl Pts',(-171.201862894068,5.91202893496002,
130.520454418451));
#168233=CARTESIAN_POINT('Ctrl Pts',(-171.194439523039,5.91747498208225,
130.67765395867));
#168234=CARTESIAN_POINT('Ctrl Pts',(-171.187016152011,5.91667270161625,
130.834604698789));
#168235=CARTESIAN_POINT('Ctrl Pts',(-171.18308010257,5.91624731326271,130.917823747185));
#168236=CARTESIAN_POINT('Ctrl Pts',(-171.179144053129,5.91406616309129,
131.000972932089));
#168237=CARTESIAN_POINT('Ctrl Pts',(-171.175208003688,5.91013938168198,
131.083972941314));
#168238=CARTESIAN_POINT('Ctrl Pts',(-171.167784737282,5.90273359449494,
131.240508368364));
#168239=CARTESIAN_POINT('Ctrl Pts',(-171.160361470877,5.88909333827066,
131.396986068284));
#168240=CARTESIAN_POINT('Ctrl Pts',(-171.152938204471,5.86921338211624,
131.552869026128));
#168241=CARTESIAN_POINT('Ctrl Pts',(-171.14552371175,5.849356922419,131.708567743261));
#168242=CARTESIAN_POINT('Ctrl Pts',(-171.138109219029,5.8232754891494,131.863672750833));
#168243=CARTESIAN_POINT('Ctrl Pts',(-171.130694726308,5.79101583032626,
132.017647976525));
#168244=CARTESIAN_POINT('Ctrl Pts',(-171.123287379954,5.75878726457693,
132.171474795098));
#168245=CARTESIAN_POINT('Ctrl Pts',(-171.115880033601,5.72039240415578,
132.324173636717));
#168246=CARTESIAN_POINT('Ctrl Pts',(-171.108472687247,5.67592966216109,
132.475214600624));
#168247=CARTESIAN_POINT('Ctrl Pts',(-171.101070865572,5.63150008215673,
132.626142912482));
#168248=CARTESIAN_POINT('Ctrl Pts',(-171.093669043896,5.58101173673197,
132.775415452119));
#168249=CARTESIAN_POINT('Ctrl Pts',(-171.086267222221,5.52461385532159,
132.922513660216));
#168250=CARTESIAN_POINT('Ctrl Pts',(-171.078869307909,5.4682457459138,133.069534216315));
#168251=CARTESIAN_POINT('Ctrl Pts',(-171.071471393598,5.40597444664899,
133.214382379123));
#168252=CARTESIAN_POINT('Ctrl Pts',(-171.064073479287,5.33799862874087,
133.356555986667));
#168253=CARTESIAN_POINT('Ctrl Pts',(-171.056676794374,5.27003410718058,
133.498705967536));
#168254=CARTESIAN_POINT('Ctrl Pts',(-171.049280109462,5.19636710931638,
133.638181938813));
#168255=CARTESIAN_POINT('Ctrl Pts',(-171.04188342455,5.11724397207349,133.774502818333));
#168256=CARTESIAN_POINT('Ctrl Pts',(-171.034487067614,5.03812434323341,
133.910817653242));
#168257=CARTESIAN_POINT('Ctrl Pts',(-171.027090710679,4.95354924344627,
134.043977351708));
#168258=CARTESIAN_POINT('Ctrl Pts',(-171.019694353743,4.86381025749459,
134.173526737185));
#168259=CARTESIAN_POINT('Ctrl Pts',(-171.012296864407,4.77405753227506,
134.303095957005));
#168260=CARTESIAN_POINT('Ctrl Pts',(-171.00489937507,4.67913955927308,134.429053456356));
#168261=CARTESIAN_POINT('Ctrl Pts',(-170.997501885733,4.57939031963322,
134.550974403767));
#168262=CARTESIAN_POINT('Ctrl Pts',(-170.990101803218,4.47960611305218,
134.672938090377));
#168263=CARTESIAN_POINT('Ctrl Pts',(-170.982701720704,4.37498750413481,
134.790862119037));
#168264=CARTESIAN_POINT('Ctrl Pts',(-170.975301638189,4.26590757332199,
134.904356122243));
#168265=CARTESIAN_POINT('Ctrl Pts',(-170.967893418522,4.15670769791139,
135.017974923773));
#168266=CARTESIAN_POINT('Ctrl Pts',(-170.960485198855,4.04303696247064,
135.127153702297));
#168267=CARTESIAN_POINT('Ctrl Pts',(-170.953076979189,3.92530452524635,
135.231539735987));
#168268=CARTESIAN_POINT('Ctrl Pts',(-170.945664199887,3.80749962567142,
135.335990017538));
#168269=CARTESIAN_POINT('Ctrl Pts',(-170.938251420585,3.68562833124752,
135.435641440549));
#168270=CARTESIAN_POINT('Ctrl Pts',(-170.930838641283,3.56013101116293,
135.530183058777));
#168271=CARTESIAN_POINT('Ctrl Pts',(-170.923415270254,3.43445437462199,
135.624859762503));
#168272=CARTESIAN_POINT('Ctrl Pts',(-170.915991899225,3.30514167080891,
135.714411867488));
#168273=CARTESIAN_POINT('Ctrl Pts',(-170.908568528196,3.17266091588127,
135.798572594979));
#168274=CARTESIAN_POINT('Ctrl Pts',(-170.904632478756,3.10241644079015,
135.843196632102));
#168275=CARTESIAN_POINT('Ctrl Pts',(-170.900696429315,3.03128171168346,
135.886305734158));
#168276=CARTESIAN_POINT('Ctrl Pts',(-170.896760379875,2.95932893197784,
135.927865554117));
#168277=CARTESIAN_POINT('Ctrl Pts',(-170.889337113469,2.82362823501603,
136.006246077524));
#168278=CARTESIAN_POINT('Ctrl Pts',(-170.881913847064,2.6846062227242,136.079350162637));
#168279=CARTESIAN_POINT('Ctrl Pts',(-170.874490580658,2.54271187355959,
136.146883138862));
#168280=CARTESIAN_POINT('Ctrl Pts',(-170.867076087937,2.40098523173209,
136.214336296718));
#168281=CARTESIAN_POINT('Ctrl Pts',(-170.859661595216,2.256393344304,136.276231293486));
#168282=CARTESIAN_POINT('Ctrl Pts',(-170.852247102495,2.10941249254478,
136.332317699418));
#168283=CARTESIAN_POINT('Ctrl Pts',(-170.844839756142,1.9625733064638,136.38835004716));
#168284=CARTESIAN_POINT('Ctrl Pts',(-170.837432409788,1.81335008644968,
136.43858481746));
#168285=CARTESIAN_POINT('Ctrl Pts',(-170.830025063434,1.66224184770144,
136.482818383742));
#168286=CARTESIAN_POINT('Ctrl Pts',(-170.822623241758,1.51124631117908,
136.527018958962));
#168287=CARTESIAN_POINT('Ctrl Pts',(-170.815221420083,1.35836891201696,
136.56522713791));
#168288=CARTESIAN_POINT('Ctrl Pts',(-170.807819598408,1.20412659101033,
136.597288177559));
#168289=CARTESIAN_POINT('Ctrl Pts',(-170.800421684096,1.0499656933239,136.629332292434));
#168290=CARTESIAN_POINT('Ctrl Pts',(-170.793023769785,0.89444167332675,
136.655235654859));
#168291=CARTESIAN_POINT('Ctrl Pts',(-170.785625855474,0.738084400753971,
136.674893981739));
#168292=CARTESIAN_POINT('Ctrl Pts',(-170.778229170562,0.581753111923507,
136.694549041761));
#168293=CARTESIAN_POINT('Ctrl Pts',(-170.770832485649,0.424589215361653,
136.707961079465));
#168294=CARTESIAN_POINT('Ctrl Pts',(-170.763435800737,0.267130610244179,
136.715077308423));
#168295=CARTESIAN_POINT('Ctrl Pts',(-170.756039443802,0.10967898700626,
136.722193221839));
#168296=CARTESIAN_POINT('Ctrl Pts',(-170.748643086866,-0.048066945887389,
136.723013864724));
#168297=CARTESIAN_POINT('Ctrl Pts',(-170.741246729931,-0.205566626822125,
136.717538521573));
#168298=CARTESIAN_POINT('Ctrl Pts',(-170.733849240594,-0.36309042136009,
136.712062340133));
#168299=CARTESIAN_POINT('Ctrl Pts',(-170.726451751258,-0.520367515773337,
136.700288266313));
#168300=CARTESIAN_POINT('Ctrl Pts',(-170.719054261921,-0.676859962346667,
136.682267656119));
#168301=CARTESIAN_POINT('Ctrl Pts',(-170.711654179406,-0.833407267104324,
136.664240728829));
#168302=CARTESIAN_POINT('Ctrl Pts',(-170.704254096891,-0.989169005769536,
136.639962948139));
#168303=CARTESIAN_POINT('Ctrl Pts',(-170.696854014376,-1.14361509201325,
136.609537194021));
#168304=CARTESIAN_POINT('Ctrl Pts',(-170.68944579471,-1.29823100760645,
136.579077983658));
#168305=CARTESIAN_POINT('Ctrl Pts',(-170.682037575043,-1.45152801514979,
136.542457371241));
#168306=CARTESIAN_POINT('Ctrl Pts',(-170.674629355377,-1.60298819975292,
136.499828938429));
#168307=CARTESIAN_POINT('Ctrl Pts',(-170.667216576075,-1.75454160557242,
136.457174268527));
#168308=CARTESIAN_POINT('Ctrl Pts',(-170.659803796773,-1.90425558153418,
136.408504525213));
#168309=CARTESIAN_POINT('Ctrl Pts',(-170.652391017471,-2.05163048945519,
136.354022129518));
#168310=CARTESIAN_POINT('Ctrl Pts',(-170.644967646442,-2.19921597355562,
136.29946188682));
#168311=CARTESIAN_POINT('Ctrl Pts',(-170.637544275413,-2.34445537077541,
136.239072546953));
#168312=CARTESIAN_POINT('Ctrl Pts',(-170.630120904384,-2.4868712584297,
136.173103664732));
#168313=CARTESIAN_POINT('Ctrl Pts',(-170.626184854943,-2.56238357928856,
136.138125380476));
#168314=CARTESIAN_POINT('Ctrl Pts',(-170.622248805503,-2.63710254641187,
136.101579240896));
#168315=CARTESIAN_POINT('Ctrl Pts',(-170.618312756062,-2.71096023495891,
136.06350742736));
#168316=CARTESIAN_POINT('Ctrl Pts',(-170.610889489656,-2.85025353053517,
135.991705175216));
#168317=CARTESIAN_POINT('Ctrl Pts',(-170.603466223251,-2.98690286120123,
135.914256562637));
#168318=CARTESIAN_POINT('Ctrl Pts',(-170.596042956845,-3.12041762841813,
135.831380051262));
#168319=CARTESIAN_POINT('Ctrl Pts',(-170.588628464124,-3.25377459226752,
135.748601493041));
#168320=CARTESIAN_POINT('Ctrl Pts',(-170.581213971403,-3.38400405301389,
135.660408000716));
#168321=CARTESIAN_POINT('Ctrl Pts',(-170.573799478682,-3.51063787535615,
135.56706491981));
#168322=CARTESIAN_POINT('Ctrl Pts',(-170.566392132329,-3.63714964325312,
135.47381180648));
#168323=CARTESIAN_POINT('Ctrl Pts',(-170.558984785975,-3.76007237362654,
135.375419205661));
#168324=CARTESIAN_POINT('Ctrl Pts',(-170.551577439621,-3.8789650197663,
135.272196887835));
#168325=CARTESIAN_POINT('Ctrl Pts',(-170.544175617946,-3.99776899128467,
135.169051557108));
#168326=CARTESIAN_POINT('Ctrl Pts',(-170.53677379627,-4.11254858283041,
135.061083925489));
#168327=CARTESIAN_POINT('Ctrl Pts',(-170.529371974595,-4.22289418558466,
134.948645267521));
#168328=CARTESIAN_POINT('Ctrl Pts',(-170.521974060284,-4.33318153775447,
134.836265965046));
#168329=CARTESIAN_POINT('Ctrl Pts',(-170.514576145972,-4.43903930187741,
134.719420602469));
#168330=CARTESIAN_POINT('Ctrl Pts',(-170.507178231661,-4.54009333409802,
134.598498606646));
#168331=CARTESIAN_POINT('Ctrl Pts',(-170.499781546749,-4.64113057297164,
134.477596705865));
#168332=CARTESIAN_POINT('Ctrl Pts',(-170.492384861837,-4.73736542517419,
134.352619802561));
#168333=CARTESIAN_POINT('Ctrl Pts',(-170.484988176925,-4.82846273234404,
134.223991914192));
#168334=CARTESIAN_POINT('Ctrl Pts',(-170.477591819989,-4.91955600016382,
134.095369729318));
#168335=CARTESIAN_POINT('Ctrl Pts',(-170.470195463054,-5.00551196015227,
133.963097185903));
#168336=CARTESIAN_POINT('Ctrl Pts',(-170.462799106118,-5.08603782357858,
133.827628686995));
#168337=CARTESIAN_POINT('Ctrl Pts',(-170.455401616782,-5.16657601572014,
133.692139447514));
#168338=CARTESIAN_POINT('Ctrl Pts',(-170.448004127445,-5.24168226519253,
133.553453599168));
#168339=CARTESIAN_POINT('Ctrl Pts',(-170.440606638109,-5.31110900537997,
133.412051491782));
#168340=CARTESIAN_POINT('Ctrl Pts',(-170.433206555594,-5.38056008300366,
133.270599816107));
#168341=CARTESIAN_POINT('Ctrl Pts',(-170.425806473079,-5.44432752296808,
133.126430320487));
#168342=CARTESIAN_POINT('Ctrl Pts',(-170.418406390564,-5.50221135649625,
132.980044590698));
#168343=CARTESIAN_POINT('Ctrl Pts',(-170.410998170897,-5.56015883925006,
132.833497894751));
#168344=CARTESIAN_POINT('Ctrl Pts',(-170.403589951231,-5.61220965793961,
132.684730445189));
#168345=CARTESIAN_POINT('Ctrl Pts',(-170.396181731564,-5.65821307951348,
132.534260993114));
#168346=CARTESIAN_POINT('Ctrl Pts',(-170.388768952262,-5.70424481542559,
132.383698929604));
#168347=CARTESIAN_POINT('Ctrl Pts',(-170.38135617296,-5.74422164295145,
132.231433136422));
#168348=CARTESIAN_POINT('Ctrl Pts',(-170.373943393658,-5.77804379799479,
132.077993386834));
#168349=CARTESIAN_POINT('Ctrl Pts',(-170.36652002263,-5.81191427971941,
131.924334395337));
#168350=CARTESIAN_POINT('Ctrl Pts',(-170.359096651601,-5.83961245964126,
131.769498463773));
#168351=CARTESIAN_POINT('Ctrl Pts',(-170.351673280572,-5.86109023667217,
131.614022151842));
#168352=CARTESIAN_POINT('Ctrl Pts',(-170.347737231131,-5.87247826940697,
131.531584880648));
#168353=CARTESIAN_POINT('Ctrl Pts',(-170.34380118169,-5.88211839398032,
131.44896761632));
#168354=CARTESIAN_POINT('Ctrl Pts',(-170.339865132249,-5.89000938373772,
131.366250306012));
#168355=CARTESIAN_POINT('Ctrl Pts',(-170.331035152235,-5.90771172281953,
131.180685513758));
#168356=CARTESIAN_POINT('Ctrl Pts',(-170.322205172221,-5.91664660285328,
130.994271132306));
#168357=CARTESIAN_POINT('Ctrl Pts',(-170.313375192207,-5.91674910785689,
130.807609798182));
#168358=CARTESIAN_POINT('',(-168.563376377968,-5.91250207745248,130.808001233738));
#168359=CARTESIAN_POINT('Ctrl Pts',(-170.31337267473,-5.92431952931233,
130.807560669157));
#168360=CARTESIAN_POINT('Ctrl Pts',(-170.229387619299,-5.91256351382009,
129.029879967327));
#168361=CARTESIAN_POINT('Ctrl Pts',(-170.052586689264,-4.11503221513579,
125.267038583023));
#168362=CARTESIAN_POINT('Ctrl Pts',(-169.782969884622,2.29137987422938,
124.191710709827));
#168363=CARTESIAN_POINT('Ctrl Pts',(-169.50452226081,6.80195643944412,129.157864602918));
#168364=CARTESIAN_POINT('Ctrl Pts',(-169.226074636996,5.06186733085566,
135.637067897668));
#168365=CARTESIAN_POINT('Ctrl Pts',(-168.947627013185,-1.32983056882352,
137.675249292881));
#168366=CARTESIAN_POINT('Ctrl Pts',(-168.726727900654,-5.43103555014988,
134.283132100589));
#168367=CARTESIAN_POINT('Ctrl Pts',(-168.598644662728,-5.91336715510493,
131.559408908431));
#168368=CARTESIAN_POINT('Ctrl Pts',(-168.563377299405,-5.90920193984457,
130.80801884743));
#168369=CARTESIAN_POINT('',(-166.813373979163,-5.91344434060639,130.799749243495));
#168370=CARTESIAN_POINT('Ctrl Pts',(-168.563375192207,-5.91674889385541,
130.807978567374));
#168371=CARTESIAN_POINT('Ctrl Pts',(-168.55591487972,-5.91684620926024,
130.648830197611));
#168372=CARTESIAN_POINT('Ctrl Pts',(-168.548454567234,-5.91051804296644,
130.489661439869));
#168373=CARTESIAN_POINT('Ctrl Pts',(-168.540994254747,-5.89778612679078,
130.33102208635));
#168374=CARTESIAN_POINT('Ctrl Pts',(-168.533533119083,-5.88505280576286,
130.172365228406));
#168375=CARTESIAN_POINT('Ctrl Pts',(-168.526071983418,-5.8659143555312,
130.014238254263));
#168376=CARTESIAN_POINT('Ctrl Pts',(-168.518610847753,-5.84044445990559,
129.857186360495));
#168377=CARTESIAN_POINT('Ctrl Pts',(-168.511147511828,-5.81496705330743,
129.700088152738));
#168378=CARTESIAN_POINT('Ctrl Pts',(-168.503684175904,-5.78315453978418,
129.544066016489));
#168379=CARTESIAN_POINT('Ctrl Pts',(-168.496220839979,-5.74513183840758,
129.389655446226));
#168380=CARTESIAN_POINT('Ctrl Pts',(-168.48875392566,-5.70709090654714,
129.235170841786));
#168381=CARTESIAN_POINT('Ctrl Pts',(-168.481287011341,-5.66283394199877,
129.082299695985));
#168382=CARTESIAN_POINT('Ctrl Pts',(-168.473820097022,-5.61253586847653,
128.931562794104));
#168383=CARTESIAN_POINT('Ctrl Pts',(-168.466343481839,-5.56217244871151,
128.780630057879));
#168384=CARTESIAN_POINT('Ctrl Pts',(-168.458866866655,-5.50575235689669,
128.631837450325));
#168385=CARTESIAN_POINT('Ctrl Pts',(-168.451390251472,-5.44349922980364,
128.485687139556));
#168386=CARTESIAN_POINT('Ctrl Pts',(-168.443908382716,-5.38120235948349,
128.339434133765));
#168387=CARTESIAN_POINT('Ctrl Pts',(-168.436426513961,-5.31306443944356,
128.19582745407));
#168388=CARTESIAN_POINT('Ctrl Pts',(-168.428944645206,-5.23935515865615,
128.055344778404));
#168389=CARTESIAN_POINT('Ctrl Pts',(-168.421450603008,-5.16552594851533,
127.914633529127));
#168390=CARTESIAN_POINT('Ctrl Pts',(-168.41395656081,-5.08610744715199,
127.777056754815));
#168391=CARTESIAN_POINT('Ctrl Pts',(-168.406462518613,-5.00141337865723,
127.643064241348));
#168392=CARTESIAN_POINT('Ctrl Pts',(-168.401218934261,-4.94215290473659,
127.549309625577));
#168393=CARTESIAN_POINT('Ctrl Pts',(-168.39597534991,-4.88031051355676,
127.457309165077));
#168394=CARTESIAN_POINT('Ctrl Pts',(-168.390731765558,-4.81600516896356,
127.367207031382));
#168395=CARTESIAN_POINT('Ctrl Pts',(-168.383308499153,-4.72496902417803,
127.239650745969));
#168396=CARTESIAN_POINT('Ctrl Pts',(-168.375885232747,-4.62872405528346,
127.115520841736));
#168397=CARTESIAN_POINT('Ctrl Pts',(-168.368461966342,-4.52755682262028,
126.995271516423));
#168398=CARTESIAN_POINT('Ctrl Pts',(-168.361047473621,-4.42650916122441,
126.875164315826));
#168399=CARTESIAN_POINT('Ctrl Pts',(-168.3536329809,-4.32055105421296,126.758928847513));
#168400=CARTESIAN_POINT('Ctrl Pts',(-168.346218488179,-4.21001223972966,
126.646990354548));
#168401=CARTESIAN_POINT('Ctrl Pts',(-168.338811141825,-4.09957996671779,
126.535159752117));
#168402=CARTESIAN_POINT('Ctrl Pts',(-168.331403795471,-3.98457603628079,
126.427618143785));
#168403=CARTESIAN_POINT('Ctrl Pts',(-168.323996449117,-3.86537026753099,
126.324757593035));
#168404=CARTESIAN_POINT('Ctrl Pts',(-168.316594627442,-3.7462534069409,
126.221973759565));
#168405=CARTESIAN_POINT('Ctrl Pts',(-168.309192805766,-3.62294122944443,
126.123864274832));
#168406=CARTESIAN_POINT('Ctrl Pts',(-168.301790984091,-3.49584012068717,
126.030784137285));
#168407=CARTESIAN_POINT('Ctrl Pts',(-168.29439306978,-3.36880610761551,
125.937753136017));
#168408=CARTESIAN_POINT('Ctrl Pts',(-168.286995155468,-3.237987447083,125.849746414469));
#168409=CARTESIAN_POINT('Ctrl Pts',(-168.279597241157,-3.103823196637,125.767078401279));
#168410=CARTESIAN_POINT('Ctrl Pts',(-168.272200556245,-2.96968124185563,
125.684424126014));
#168411=CARTESIAN_POINT('Ctrl Pts',(-168.264803871332,-2.8321951181089,
125.60710699392));
#168412=CARTESIAN_POINT('Ctrl Pts',(-168.25740718642,-2.69183252507318,
125.535397890477));
#168413=CARTESIAN_POINT('Ctrl Pts',(-168.250010829485,-2.55147615586194,
125.46369196669));
#168414=CARTESIAN_POINT('Ctrl Pts',(-168.242614472549,-2.40824390339317,
125.397593746954));
#168415=CARTESIAN_POINT('Ctrl Pts',(-168.235218115614,-2.26262746260918,
125.337327827473));
#168416=CARTESIAN_POINT('Ctrl Pts',(-168.227820626277,-2.11698872757636,
125.277052681127));
#168417=CARTESIAN_POINT('Ctrl Pts',(-168.220423136941,-1.968965422361,125.22261175576));
#168418=CARTESIAN_POINT('Ctrl Pts',(-168.213025647604,-1.81906843516317,
125.174181171874));
#168419=CARTESIAN_POINT('Ctrl Pts',(-168.205625565089,-1.66911890180864,
125.125733610722));
#168420=CARTESIAN_POINT('Ctrl Pts',(-168.198225482574,-1.51729473375126,
125.083300700601));
#168421=CARTESIAN_POINT('Ctrl Pts',(-168.190825400059,-1.36412100961559,
125.047008410724));
#168422=CARTESIAN_POINT('Ctrl Pts',(-168.183417180392,-1.21077885522382,
125.010676213744));
#168423=CARTESIAN_POINT('Ctrl Pts',(-168.176008960726,-1.05608454462107,
124.980498207797));
#168424=CARTESIAN_POINT('Ctrl Pts',(-168.168600741059,-0.900573083415225,
124.956549173622));
#168425=CARTESIAN_POINT('Ctrl Pts',(-168.161187961757,-0.744965907499412,
124.932585399215));
#168426=CARTESIAN_POINT('Ctrl Pts',(-168.153775182455,-0.588540948868006,
124.9148582779));
#168427=CARTESIAN_POINT('Ctrl Pts',(-168.146362403153,-0.431836811887692,
124.903390567617));
#168428=CARTESIAN_POINT('Ctrl Pts',(-168.138939032124,-0.274908768687989,
124.891906471731));
#168429=CARTESIAN_POINT('Ctrl Pts',(-168.131515661096,-0.117701122545321,
124.886699661856));
#168430=CARTESIAN_POINT('Ctrl Pts',(-168.124092290067,0.0392482148941711,
124.887740793703));
#168431=CARTESIAN_POINT('Ctrl Pts',(-168.120156240626,0.122466519541952,
124.88829282679));
#168432=CARTESIAN_POINT('Ctrl Pts',(-168.116220191186,0.205612288808921,
124.89060051334));
#168433=CARTESIAN_POINT('Ctrl Pts',(-168.112284141746,0.288606226015166,
124.894653602087));
#168434=CARTESIAN_POINT('Ctrl Pts',(-168.10486087534,0.44513020145275,124.902297600971));
#168435=CARTESIAN_POINT('Ctrl Pts',(-168.097437608935,0.601586962025899,
124.916175973822));
#168436=CARTESIAN_POINT('Ctrl Pts',(-168.090014342529,0.757439485450539,
124.936293134282));
#168437=CARTESIAN_POINT('Ctrl Pts',(-168.082599849808,0.913107804135237,
124.956386517928));
#168438=CARTESIAN_POINT('Ctrl Pts',(-168.075185357087,1.06817294059602,
124.982703964414));
#168439=CARTESIAN_POINT('Ctrl Pts',(-168.067770864366,1.22209889427824,
125.015197909963));
#168440=CARTESIAN_POINT('Ctrl Pts',(-168.060363518013,1.3758764883311,125.047660536624));
#168441=CARTESIAN_POINT('Ctrl Pts',(-168.052956171659,1.52851672268564,
125.086287734227));
#168442=CARTESIAN_POINT('Ctrl Pts',(-168.045548825305,1.67948984696516,
125.13098028337));
#168443=CARTESIAN_POINT('Ctrl Pts',(-168.03814700363,1.8303503697927,125.175639499124));
#168444=CARTESIAN_POINT('Ctrl Pts',(-168.030745181954,1.9795459019069,125.226354953478));
#168445=CARTESIAN_POINT('Ctrl Pts',(-168.023343360279,2.12655811169202,
125.282976628013));
#168446=CARTESIAN_POINT('Ctrl Pts',(-168.015945445968,2.27349271487594,
125.339568412406));
#168447=CARTESIAN_POINT('Ctrl Pts',(-168.008547531656,2.41824594363519,
125.402060073807));
#168448=CARTESIAN_POINT('Ctrl Pts',(-168.001149617345,2.56031593892036,
125.470252177029));
#168449=CARTESIAN_POINT('Ctrl Pts',(-167.993752932433,2.70236232474993,
125.53843294796));
#168450=CARTESIAN_POINT('Ctrl Pts',(-167.98635624752,2.84172602588579,125.612312119204));
#168451=CARTESIAN_POINT('Ctrl Pts',(-167.978959562608,2.97792633560266,
125.691642621996));
#168452=CARTESIAN_POINT('Ctrl Pts',(-167.971563205673,3.11412060605507,
125.770969607191));
#168453=CARTESIAN_POINT('Ctrl Pts',(-167.964166848737,3.24715144141897,
125.855747255434));
#168454=CARTESIAN_POINT('Ctrl Pts',(-167.956770491801,3.37656410942032,
125.945683289581));
#168455=CARTESIAN_POINT('Ctrl Pts',(-167.949373002465,3.50599659083153,
126.035633093164));
#168456=CARTESIAN_POINT('Ctrl Pts',(-167.941975513128,3.63180949532877,
126.130742642125));
#168457=CARTESIAN_POINT('Ctrl Pts',(-167.934578023792,3.75357850019519,
126.230677309184));
#168458=CARTESIAN_POINT('Ctrl Pts',(-167.927177941277,3.87539019099803,
126.330647008186));
#168459=CARTESIAN_POINT('Ctrl Pts',(-167.919777858762,3.99315487139164,
126.435444956255));
#168460=CARTESIAN_POINT('Ctrl Pts',(-167.912377776247,4.10648274208797,
126.544697479308));
#168461=CARTESIAN_POINT('Ctrl Pts',(-167.90496955658,4.21993522842804,126.654070136741));
#168462=CARTESIAN_POINT('Ctrl Pts',(-167.897561336914,4.32894089301561,
126.767906892069));
#168463=CARTESIAN_POINT('Ctrl Pts',(-167.890153117247,4.43314763709995,
126.885798050734));
#168464=CARTESIAN_POINT('Ctrl Pts',(-167.882740337945,4.5374185186965,127.003761769441));
#168465=CARTESIAN_POINT('Ctrl Pts',(-167.875327558643,4.63688435894883,
127.125784575242));
#168466=CARTESIAN_POINT('Ctrl Pts',(-167.867914779341,4.73123488214162,
127.251425626252));
#168467=CARTESIAN_POINT('Ctrl Pts',(-167.860491408312,4.82572021778669,
127.377246199087));
#168468=CARTESIAN_POINT('Ctrl Pts',(-167.853068037283,4.91507542714935,
127.506695036217));
#168469=CARTESIAN_POINT('Ctrl Pts',(-167.845644666255,4.99903444402728,
127.639303716035));
#168470=CARTESIAN_POINT('Ctrl Pts',(-167.841708616814,5.04355152934311,
127.709616019973));
#168471=CARTESIAN_POINT('Ctrl Pts',(-167.837772567373,5.08655232653177,
127.780816271422));
#168472=CARTESIAN_POINT('Ctrl Pts',(-167.833836517933,5.12800259848285,
127.85283221478));
#168473=CARTESIAN_POINT('Ctrl Pts',(-167.826413251527,5.20617651776695,
127.988652036417));
#168474=CARTESIAN_POINT('Ctrl Pts',(-167.818989985122,5.27906895038996,
128.127785139697));
#168475=CARTESIAN_POINT('Ctrl Pts',(-167.811566718716,5.34638590936825,
128.269782098244));
#168476=CARTESIAN_POINT('Ctrl Pts',(-167.804152225995,5.41362330529116,
128.411611228178));
#168477=CARTESIAN_POINT('Ctrl Pts',(-167.796737733274,5.47529818614745,
128.55629714182));
#168478=CARTESIAN_POINT('Ctrl Pts',(-167.789323240553,5.5311608472962,128.70336317734));
#168479=CARTESIAN_POINT('Ctrl Pts',(-167.781915894199,5.58696966590894,
128.850287465078));
#168480=CARTESIAN_POINT('Ctrl Pts',(-167.774508547846,5.63697728569962,
128.999586961062));
#168481=CARTESIAN_POINT('Ctrl Pts',(-167.767101201492,5.6809808397436,129.150762340787));
#168482=CARTESIAN_POINT('Ctrl Pts',(-167.759699379817,5.72495157427682,
129.30182496821));
#168483=CARTESIAN_POINT('Ctrl Pts',(-167.752297558141,5.76292705560328,
129.454760336687));
#168484=CARTESIAN_POINT('Ctrl Pts',(-167.744895736466,5.79475332757003,
129.609051270528));
#168485=CARTESIAN_POINT('Ctrl Pts',(-167.737497822154,5.82656279869564,
129.763260755387));
#168486=CARTESIAN_POINT('Ctrl Pts',(-167.730099907843,5.8522294500413,129.918824015798));
#168487=CARTESIAN_POINT('Ctrl Pts',(-167.722701993532,5.87164980500478,
130.075211023938));
#168488=CARTESIAN_POINT('Ctrl Pts',(-167.71530530862,5.8910669326575,130.231572043395));
#168489=CARTESIAN_POINT('Ctrl Pts',(-167.707908623707,5.9042397781346,130.388756168801));
#168490=CARTESIAN_POINT('Ctrl Pts',(-167.700511938795,5.91111637365859,
130.546225421273));
#168491=CARTESIAN_POINT('Ctrl Pts',(-167.69311558186,5.91799266426713,130.703687691393));
#168492=CARTESIAN_POINT('Ctrl Pts',(-167.685719224924,5.91857324374515,
130.861434690498));
#168493=CARTESIAN_POINT('Ctrl Pts',(-167.678322867989,5.9128582192318,131.01892585651));
#168494=CARTESIAN_POINT('Ctrl Pts',(-167.670925378652,5.90714231973359,
131.176441134822));
#168495=CARTESIAN_POINT('Ctrl Pts',(-167.663527889316,5.8951289105827,131.333700128975));
#168496=CARTESIAN_POINT('Ctrl Pts',(-167.656130399979,5.87687016639297,
131.490164970031));
#168497=CARTESIAN_POINT('Ctrl Pts',(-167.648730317464,5.85860502162885,
131.646684659595));
#168498=CARTESIAN_POINT('Ctrl Pts',(-167.641330234949,5.83409022620219,
131.802409271241));
#168499=CARTESIAN_POINT('Ctrl Pts',(-167.633930152434,5.80342946666439,
131.956808875819));
#168500=CARTESIAN_POINT('Ctrl Pts',(-167.626521932768,5.77273499246934,
132.111378258637));
#168501=CARTESIAN_POINT('Ctrl Pts',(-167.619113713101,5.73588113050957,
132.264619358327));
#168502=CARTESIAN_POINT('Ctrl Pts',(-167.611705493435,5.69302225044242,
132.416014494324));
#168503=CARTESIAN_POINT('Ctrl Pts',(-167.604292714133,5.65013699144985,
132.5675028115));
#168504=CARTESIAN_POINT('Ctrl Pts',(-167.596879934831,5.60123946530932,
132.717142547031));
#168505=CARTESIAN_POINT('Ctrl Pts',(-167.589467155529,5.54653285318143,
132.864434371362));
#168506=CARTESIAN_POINT('Ctrl Pts',(-167.5820437845,5.49174807368057,133.011936653159));
#168507=CARTESIAN_POINT('Ctrl Pts',(-167.574620413471,5.43113777410489,
133.157083979899));
#168508=CARTESIAN_POINT('Ctrl Pts',(-167.567197042443,5.36495223553776,
133.29939930923));
#168509=CARTESIAN_POINT('Ctrl Pts',(-167.563260993002,5.32985907488748,
133.374858311654));
#168510=CARTESIAN_POINT('Ctrl Pts',(-167.559324943561,5.29319926807747,
133.449521575252));
#168511=CARTESIAN_POINT('Ctrl Pts',(-167.55538889412,5.25501509979877,133.523321239456));
#168512=CARTESIAN_POINT('Ctrl Pts',(-167.547965627714,5.18300095011559,
133.662505102928));
#168513=CARTESIAN_POINT('Ctrl Pts',(-167.540542361309,5.10534447020123,
133.799036411753));
#168514=CARTESIAN_POINT('Ctrl Pts',(-167.533119094903,5.02226486804838,
133.93242490042));
#168515=CARTESIAN_POINT('Ctrl Pts',(-167.525704602182,4.93928345908594,
134.065655734971));
#168516=CARTESIAN_POINT('Ctrl Pts',(-167.518290109461,4.85089188181637,
134.195750829432));
#168517=CARTESIAN_POINT('Ctrl Pts',(-167.51087561674,4.75735619387874,134.322242452856));
#168518=CARTESIAN_POINT('Ctrl Pts',(-167.503468270387,4.6639106591587,134.448612158891));
#168519=CARTESIAN_POINT('Ctrl Pts',(-167.496060924033,4.56533110480596,
134.571385010133));
#168520=CARTESIAN_POINT('Ctrl Pts',(-167.488653577679,4.46192797214109,
134.690120431801));
#168521=CARTESIAN_POINT('Ctrl Pts',(-167.481251756004,4.35860196143375,
134.808767296112));
#168522=CARTESIAN_POINT('Ctrl Pts',(-167.473849934328,4.25045977983879,
134.92338244639));
#168523=CARTESIAN_POINT('Ctrl Pts',(-167.466448112653,4.13785332484944,
135.033556808869));
#168524=CARTESIAN_POINT('Ctrl Pts',(-167.459050198341,4.02530631393244,
135.143673011159));
#168525=CARTESIAN_POINT('Ctrl Pts',(-167.45165228403,3.90829998916464,135.249352833948));
#168526=CARTESIAN_POINT('Ctrl Pts',(-167.444254369719,3.78722434633334,
135.350222726456));
#168527=CARTESIAN_POINT('Ctrl Pts',(-167.436857684807,3.66616882407613,
135.451075856218));
#168528=CARTESIAN_POINT('Ctrl Pts',(-167.429460999894,3.54104561243058,
135.547120403411));
#168529=CARTESIAN_POINT('Ctrl Pts',(-167.422064314982,3.41227923841575,
135.638021855342));
#168530=CARTESIAN_POINT('Ctrl Pts',(-167.414667958047,3.28351857403687,
135.728919276607));
#168531=CARTESIAN_POINT('Ctrl Pts',(-167.407271601111,3.15111537345175,
135.814673840766));
#168532=CARTESIAN_POINT('Ctrl Pts',(-167.399875244176,3.0155244847571,135.89499345095));
#168533=CARTESIAN_POINT('Ctrl Pts',(-167.392477754839,2.87991283675123,
135.975325358272));
#168534=CARTESIAN_POINT('Ctrl Pts',(-167.385080265503,2.74111285007431,
136.05022046452));
#168535=CARTESIAN_POINT('Ctrl Pts',(-167.377682776166,2.59960525074963,
136.119431934376));
#168536=CARTESIAN_POINT('Ctrl Pts',(-167.370282693651,2.45804804615476,
136.188667666206));
#168537=CARTESIAN_POINT('Ctrl Pts',(-167.362882611136,2.31378167429036,
136.252215630898));
#168538=CARTESIAN_POINT('Ctrl Pts',(-167.355482528621,2.16730802467192,
136.309876623236));
#168539=CARTESIAN_POINT('Ctrl Pts',(-167.348074308955,2.0206733122185,136.367601019763));
#168540=CARTESIAN_POINT('Ctrl Pts',(-167.340666089288,1.87182682244108,
136.419425379445));
#168541=CARTESIAN_POINT('Ctrl Pts',(-167.333257869622,1.72128753523133,
136.465199758856));
#168542=CARTESIAN_POINT('Ctrl Pts',(-167.32584509032,1.57065559360219,136.511002311633));
#168543=CARTESIAN_POINT('Ctrl Pts',(-167.318432311018,1.41832913881467,
136.550747370249));
#168544=CARTESIAN_POINT('Ctrl Pts',(-167.311019531716,1.26483809534467,
136.584335976948));
#168545=CARTESIAN_POINT('Ctrl Pts',(-167.303596160687,1.11112773667353,
136.617972576623));
#168546=CARTESIAN_POINT('Ctrl Pts',(-167.296172789658,0.956249832491398,
136.645435090541));
#168547=CARTESIAN_POINT('Ctrl Pts',(-167.288749418629,0.800741015078611,
136.66667623422));
#168548=CARTESIAN_POINT('Ctrl Pts',(-167.284813369188,0.718286508702174,
136.677938798274));
#168549=CARTESIAN_POINT('Ctrl Pts',(-167.280877319748,0.635654669419594,
136.687453182271));
#168550=CARTESIAN_POINT('Ctrl Pts',(-167.276941270307,0.552925446158012,
136.695218281225));
#168551=CARTESIAN_POINT('Ctrl Pts',(-167.269518003901,0.396900712980493,
136.709863015512));
#168552=CARTESIAN_POINT('Ctrl Pts',(-167.262094737496,0.240057831841021,
136.718326926996));
#168553=CARTESIAN_POINT('Ctrl Pts',(-167.25467147109,0.0829277642722101,
136.720529441088));
#168554=CARTESIAN_POINT('Ctrl Pts',(-167.247256978369,-0.0740165886046808,
136.722729351991));
#168555=CARTESIAN_POINT('Ctrl Pts',(-167.239842485649,-0.231247082656321,
136.71868259096));
#168556=CARTESIAN_POINT('Ctrl Pts',(-167.232427992928,-0.388226391936349,
136.708360179821));
#168557=CARTESIAN_POINT('Ctrl Pts',(-167.225020646574,-0.545054398648819,
136.698047717809));
#168558=CARTESIAN_POINT('Ctrl Pts',(-167.21761330022,-0.701631332572941,
136.681471671805));
#168559=CARTESIAN_POINT('Ctrl Pts',(-167.210205953866,-0.857418724550655,
136.658655083451));
#168560=CARTESIAN_POINT('Ctrl Pts',(-167.202804132191,-1.01308992441347,
136.635855512569));
#168561=CARTESIAN_POINT('Ctrl Pts',(-167.195402310516,-1.16797238708205,
136.606824720804));
#168562=CARTESIAN_POINT('Ctrl Pts',(-167.18800048884,-1.32153173802212,
136.57163765512));
#168563=CARTESIAN_POINT('Ctrl Pts',(-167.180602574529,-1.47501002617788,
136.536469164414));
#168564=CARTESIAN_POINT('Ctrl Pts',(-167.173204660218,-1.62716623067609,
136.495150955186));
#168565=CARTESIAN_POINT('Ctrl Pts',(-167.165806745906,-1.77747527041611,
136.447809228616));
#168566=CARTESIAN_POINT('Ctrl Pts',(-167.158410060994,-1.92775933151911,
136.400475369382));
#168567=CARTESIAN_POINT('Ctrl Pts',(-167.151013376082,-2.07619648139296,
136.347120091528));
#168568=CARTESIAN_POINT('Ctrl Pts',(-167.14361669117,-2.22227581781325,
136.287919749377));
#168569=CARTESIAN_POINT('Ctrl Pts',(-167.136220334234,-2.3683486769231,
136.22872203223));
#168570=CARTESIAN_POINT('Ctrl Pts',(-167.128823977299,-2.51206358448913,
136.163679906325));
#168571=CARTESIAN_POINT('Ctrl Pts',(-167.121427620363,-2.65292893463741,
136.093018162753));
#168572=CARTESIAN_POINT('Ctrl Pts',(-167.114030131027,-2.7938158516292,
136.022345600689));
#168573=CARTESIAN_POINT('Ctrl Pts',(-167.106632641691,-2.93185200883081,
135.94605187522));
#168574=CARTESIAN_POINT('Ctrl Pts',(-167.099235152354,-3.06656989254012,
135.864408014248));
#168575=CARTESIAN_POINT('Ctrl Pts',(-167.091835069839,-3.20133500139531,
135.782735533146));
#168576=CARTESIAN_POINT('Ctrl Pts',(-167.084434987324,-3.33277920175647,
135.695709375824));
#168577=CARTESIAN_POINT('Ctrl Pts',(-167.077034904809,-3.46046361309011,
135.603644120859));
#168578=CARTESIAN_POINT('Ctrl Pts',(-167.069626685143,-3.58828842656047,
135.511477630682));
#168579=CARTESIAN_POINT('Ctrl Pts',(-167.062218465477,-3.71234489160475,
135.41426119557));
#168580=CARTESIAN_POINT('Ctrl Pts',(-167.05481024581,-3.83222633526381,
135.31235039992));
#168581=CARTESIAN_POINT('Ctrl Pts',(-167.047397466508,-3.95218156395179,
135.210376879876));
#168582=CARTESIAN_POINT('Ctrl Pts',(-167.039984687206,-4.06795637699756,
135.103703494364));
#168583=CARTESIAN_POINT('Ctrl Pts',(-167.032571907904,-4.17918108131504,
134.992722594769));
#168584=CARTESIAN_POINT('Ctrl Pts',(-167.025148536875,-4.2905647087055,
134.881583120461));
#168585=CARTESIAN_POINT('Ctrl Pts',(-167.017725165847,-4.39738498975635,
134.766124112885));
#168586=CARTESIAN_POINT('Ctrl Pts',(-167.010301794818,-4.49931207983995,
134.646771497561));
#168587=CARTESIAN_POINT('Ctrl Pts',(-167.006365745377,-4.55335626871649,
134.583487877081));
#168588=CARTESIAN_POINT('Ctrl Pts',(-167.002429695935,-4.60602551696784,
134.519110127383));
#168589=CARTESIAN_POINT('Ctrl Pts',(-166.998493646494,-4.65727568058904,
134.45370491449));
#168590=CARTESIAN_POINT('Ctrl Pts',(-166.990780377565,-4.75770792884831,
134.32553376118));
#168591=CARTESIAN_POINT('Ctrl Pts',(-166.983067108637,-4.85300887122969,
134.193004710594));
#168592=CARTESIAN_POINT('Ctrl Pts',(-166.975353839708,-4.94277941001957,
134.056569446406));
#168593=CARTESIAN_POINT('Ctrl Pts',(-166.96794177963,-5.02904434294246,
133.925462080091));
#168594=CARTESIAN_POINT('Ctrl Pts',(-166.960529719552,-5.11020235861462,
133.790748144403));
#168595=CARTESIAN_POINT('Ctrl Pts',(-166.953117659474,-5.1859386345529,
133.652863915993));
#168596=CARTESIAN_POINT('Ctrl Pts',(-166.945712645278,-5.26160291581968,
133.515110759908));
#168597=CARTESIAN_POINT('Ctrl Pts',(-166.938307631081,-5.33185553661064,
133.374193633447));
#168598=CARTESIAN_POINT('Ctrl Pts',(-166.930902616885,-5.39642472220652,
133.230577998606));
#168599=CARTESIAN_POINT('Ctrl Pts',(-166.923503181855,-5.46094525938241,
133.087070568222));
#168600=CARTESIAN_POINT('Ctrl Pts',(-166.916103746825,-5.51979073326164,
132.940869015276));
#168601=CARTESIAN_POINT('Ctrl Pts',(-166.908704311795,-5.57273518684203,
132.792463507216));
#168602=CARTESIAN_POINT('Ctrl Pts',(-166.901308993002,-5.62565018791908,
132.644140555748));
#168603=CARTESIAN_POINT('Ctrl Pts',(-166.893913674208,-5.67267058019892,
132.493616440793));
#168604=CARTESIAN_POINT('Ctrl Pts',(-166.886518355415,-5.71361851471088,
132.341401290695));
#168605=CARTESIAN_POINT('Ctrl Pts',(-166.879125157563,-5.75455470554994,
132.189229795179));
#168606=CARTESIAN_POINT('Ctrl Pts',(-166.871731959712,-5.78942180747217,
132.035368589346));
#168607=CARTESIAN_POINT('Ctrl Pts',(-166.864338761861,-5.81809183905864,
131.880342919827));
#168608=CARTESIAN_POINT('Ctrl Pts',(-166.856946750918,-5.84675726793967,
131.725342138229));
#168609=CARTESIAN_POINT('Ctrl Pts',(-166.849554739976,-5.86922754325991,
131.569177632432));
#168610=CARTESIAN_POINT('Ctrl Pts',(-166.842162729033,-5.88542585283588,
131.412384542483));
#168611=CARTESIAN_POINT('Ctrl Pts',(-166.83476927801,-5.90162731809879,
131.255560906759));
#168612=CARTESIAN_POINT('Ctrl Pts',(-166.827375826987,-5.91155434066848,
131.098108813454));
#168613=CARTESIAN_POINT('Ctrl Pts',(-166.819982375964,-5.91518199387662,
130.940568333272));
#168614=CARTESIAN_POINT('Ctrl Pts',(-166.817779981378,-5.9162626155997,
130.893639463454));
#168615=CARTESIAN_POINT('Ctrl Pts',(-166.815577586793,-5.9167846129143,
130.846702761056));
#168616=CARTESIAN_POINT('Ctrl Pts',(-166.813375192207,-5.91674822108608,
130.799772505246));
#168617=CARTESIAN_POINT('',(-165.063375192207,-5.92585842785378,130.802539843459));
#168618=CARTESIAN_POINT('Ctrl Pts',(-166.813373113621,-5.91108692821504,
130.799732645576));
#168619=CARTESIAN_POINT('Ctrl Pts',(-166.782264083308,-5.91584379486465,
130.13746865848));
#168620=CARTESIAN_POINT('Ctrl Pts',(-166.658339178391,-5.50708468086315,
127.505006129433));
#168621=CARTESIAN_POINT('Ctrl Pts',(-166.441598398868,-1.63614268822863,
123.999906368037));
#168622=CARTESIAN_POINT('Ctrl Pts',(-166.163150775056,4.84040498430027,
125.749853706071));
#168623=CARTESIAN_POINT('Ctrl Pts',(-165.884703151243,6.86885694319062,
132.144645969399));
#168624=CARTESIAN_POINT('Ctrl Pts',(-165.60625552743,2.58516493360408,137.307781470961));
#168625=CARTESIAN_POINT('Ctrl Pts',(-165.332479541084,-3.96244082963463,
136.508234171304));
#168626=CARTESIAN_POINT('Ctrl Pts',(-165.151519429344,-5.91834266072314,
132.666973356396));
#168627=CARTESIAN_POINT('Ctrl Pts',(-165.063375192207,-5.92585842785378,
130.802539843459));
#168628=CARTESIAN_POINT('',(-163.313375192207,-5.91663594861072,130.809828722829));
#168629=CARTESIAN_POINT('Ctrl Pts',(-165.063375192207,-5.92585842785378,
130.802539843459));
#168630=CARTESIAN_POINT('Ctrl Pts',(-165.058703554739,-5.92625676290626,
130.703725017464));
#168631=CARTESIAN_POINT('Ctrl Pts',(-165.054031917272,-5.92400007146822,
130.604928770715));
#168632=CARTESIAN_POINT('Ctrl Pts',(-165.049360279804,-5.91903141901539,
130.506269102489));
#168633=CARTESIAN_POINT('Ctrl Pts',(-164.9565444052,-5.82031446458566,128.546103430853));
#168634=CARTESIAN_POINT('Ctrl Pts',(-164.77091265599,-3.4818656310583,124.733596888215));
#168635=CARTESIAN_POINT('Ctrl Pts',(-164.492465032178,3.22547203558176,
124.593572368236));
#168636=CARTESIAN_POINT('Ctrl Pts',(-164.214017408366,6.96875847459233,
130.160958835515));
#168637=CARTESIAN_POINT('Ctrl Pts',(-163.935569784553,4.30809631822942,
136.319600108577));
#168638=CARTESIAN_POINT('Ctrl Pts',(-163.65712216074,-2.31149589238026,
137.410005723825));
#168639=CARTESIAN_POINT('Ctrl Pts',(-163.449723963291,-5.65986792970276,
133.700820216349));
#168640=CARTESIAN_POINT('Ctrl Pts',(-163.335141640447,-5.92090732989969,
131.272102409195));
#168641=CARTESIAN_POINT('Ctrl Pts',(-163.313375192207,-5.91663594861072,
130.809828722829));
#168642=CARTESIAN_POINT('',(-161.563375192207,-5.90699555269057,130.803727264571));
#168643=CARTESIAN_POINT('Ctrl Pts',(-163.313375192207,-5.91663594861072,
130.809828722829));
#168644=CARTESIAN_POINT('Ctrl Pts',(-163.242325765842,-5.90269342629282,
129.300887995441));
#168645=CARTESIAN_POINT('Ctrl Pts',(-163.078460464874,-4.54700860849117,
125.798464535153));
#168646=CARTESIAN_POINT('Ctrl Pts',(-162.8217792893,1.35073703078564,123.937551314553));
#168647=CARTESIAN_POINT('Ctrl Pts',(-162.543331665488,6.50734750349729,
128.229095776998));
#168648=CARTESIAN_POINT('Ctrl Pts',(-162.264884041675,5.68402352209907,
134.887182819252));
#168649=CARTESIAN_POINT('Ctrl Pts',(-161.986436417862,-0.36264039612703,
137.793355715106));
#168650=CARTESIAN_POINT('Ctrl Pts',(-161.752600134706,-5.16068368769393,
134.840357278418));
#168651=CARTESIAN_POINT('Ctrl Pts',(-161.611579726154,-5.90601764033103,
131.831709506599));
#168652=CARTESIAN_POINT('Ctrl Pts',(-161.563375192207,-5.90699555269057,
130.803727264571));
#168653=CARTESIAN_POINT('',(-159.813375923929,-5.91833122137932,130.799124748602));
#168654=CARTESIAN_POINT('Ctrl Pts',(-161.563375192207,-5.90699555269057,
130.803727264571));
#168655=CARTESIAN_POINT('Ctrl Pts',(-161.51876385155,-5.90790057090839,
129.852371401689));
#168656=CARTESIAN_POINT('Ctrl Pts',(-161.381336636286,-5.24106778416674,
126.922874610178));
#168657=CARTESIAN_POINT('Ctrl Pts',(-161.151093546426,-0.632795772907546,
123.834631064731));
#168658=CARTESIAN_POINT('Ctrl Pts',(-160.87264592261,5.52178929367618,126.504662543663));
#168659=CARTESIAN_POINT('Ctrl Pts',(-160.594198298798,6.6021197537721,133.125906500654));
#168660=CARTESIAN_POINT('Ctrl Pts',(-160.315750674985,1.61542469162351,
137.613763204867));
#168661=CARTESIAN_POINT('Ctrl Pts',(-160.055476648106,-4.43340787030794,
135.95961243181));
#168662=CARTESIAN_POINT('Ctrl Pts',(-159.888018495832,-5.90433120923933,
132.382774673116));
#168663=CARTESIAN_POINT('Ctrl Pts',(-159.813376218162,-5.91896798354517,
130.799130426129));
#168664=CARTESIAN_POINT('',(-158.06337382183,-5.9211331929274,130.807404054331));
#168665=CARTESIAN_POINT('Ctrl Pts',(-159.813375192207,-5.91674767081739,
130.79911062928));
#168666=CARTESIAN_POINT('Ctrl Pts',(-159.802601402648,-5.91654492606026,
130.570616868126));
#168667=CARTESIAN_POINT('Ctrl Pts',(-159.791827613089,-5.90310296772487,
130.342686443863));
#168668=CARTESIAN_POINT('Ctrl Pts',(-159.78105382353,-5.87663597283087,
130.116552355526));
#168669=CARTESIAN_POINT('Ctrl Pts',(-159.77365435814,-5.85845837509346,
129.961242902792));
#168670=CARTESIAN_POINT('Ctrl Pts',(-159.766254892749,-5.8341378241786,
129.806779859639));
#168671=CARTESIAN_POINT('Ctrl Pts',(-159.758855427359,-5.80375541556725,
129.653554969868));
#168672=CARTESIAN_POINT('Ctrl Pts',(-159.751432160953,-5.77327527933359,
129.499837219102));
#168673=CARTESIAN_POINT('Ctrl Pts',(-159.744008894548,-5.73663780339078,
129.347098807042));
#168674=CARTESIAN_POINT('Ctrl Pts',(-159.736585628143,-5.69391725343677,
129.195871614335));
#168675=CARTESIAN_POINT('Ctrl Pts',(-159.729171135422,-5.65124719562507,
129.044823159611));
#168676=CARTESIAN_POINT('Ctrl Pts',(-159.721756642701,-5.60250847540776,
128.895282724656));
#168677=CARTESIAN_POINT('Ctrl Pts',(-159.71434214998,-5.54782662609658,
128.74777356877));
#168678=CARTESIAN_POINT('Ctrl Pts',(-159.706934803626,-5.4931974812105,
128.600406587763));
#168679=CARTESIAN_POINT('Ctrl Pts',(-159.699527457272,-5.43263673985462,
128.455067335857));
#168680=CARTESIAN_POINT('Ctrl Pts',(-159.692120110918,-5.36632011907443,
128.312265326026));
#168681=CARTESIAN_POINT('Ctrl Pts',(-159.684718289243,-5.300052959732,128.169569823322));
#168682=CARTESIAN_POINT('Ctrl Pts',(-159.677316467568,-5.22803862536594,
128.02940813184));
#168683=CARTESIAN_POINT('Ctrl Pts',(-159.669914645892,-5.15050141258487,
127.892271030781));
#168684=CARTESIAN_POINT('Ctrl Pts',(-159.662516731581,-5.07300513109467,
127.75520632333));
#168685=CARTESIAN_POINT('Ctrl Pts',(-159.65511881727,-4.98999196078019,
127.621163350611));
#168686=CARTESIAN_POINT('Ctrl Pts',(-159.647720902958,-4.9017326704733,
127.490609361102));
#168687=CARTESIAN_POINT('Ctrl Pts',(-159.640324218046,-4.81348804725965,
127.360077067299));
#168688=CARTESIAN_POINT('Ctrl Pts',(-159.632927533134,-4.71999924320396,
127.233032914919));
#168689=CARTESIAN_POINT('Ctrl Pts',(-159.625530848222,-4.62158105017022,
127.109916253496));
#168690=CARTESIAN_POINT('Ctrl Pts',(-159.618134491286,-4.52316722110229,
126.986805051195));
#168691=CARTESIAN_POINT('Ctrl Pts',(-159.610738134351,-4.41982467074444,
126.867621285167));
#168692=CARTESIAN_POINT('Ctrl Pts',(-159.603341777415,-4.31190910887094,
126.752771990949));
#168693=CARTESIAN_POINT('Ctrl Pts',(-159.595944288079,-4.20397702484912,
126.637905113009));
#168694=CARTESIAN_POINT('Ctrl Pts',(-159.588546798742,-4.09147079087838,
126.527374300296));
#168695=CARTESIAN_POINT('Ctrl Pts',(-159.581149309405,-3.97478355780458,
126.421550305551));
#168696=CARTESIAN_POINT('Ctrl Pts',(-159.57374922689,-3.85805542020194,
126.315689214368));
#168697=CARTESIAN_POINT('Ctrl Pts',(-159.566349144375,-3.73714364175878,
126.214538476847));
#168698=CARTESIAN_POINT('Ctrl Pts',(-159.55894906186,-3.61247494430429,
126.118428977084));
#168699=CARTESIAN_POINT('Ctrl Pts',(-159.551540842194,-3.48766916080086,
126.022213795045));
#168700=CARTESIAN_POINT('Ctrl Pts',(-159.544132622527,-3.35909850399577,
125.931051149273));
#168701=CARTESIAN_POINT('Ctrl Pts',(-159.536724402861,-3.2272198077915,
125.84522935547));
#168702=CARTESIAN_POINT('Ctrl Pts',(-159.529311623559,-3.09525994245023,
125.759354739785));
#168703=CARTESIAN_POINT('Ctrl Pts',(-159.521898844257,-2.95998830065875,
125.678827716746));
#168704=CARTESIAN_POINT('Ctrl Pts',(-159.514486064955,-2.82188640414737,
125.60389066913));
#168705=CARTESIAN_POINT('Ctrl Pts',(-159.507062693926,-2.68358718117011,
125.528846547946));
#168706=CARTESIAN_POINT('Ctrl Pts',(-159.499639322897,-2.54244996076335,
125.45940851881));
#168707=CARTESIAN_POINT('Ctrl Pts',(-159.492215951869,-2.39897707389532,
125.395771193194));
#168708=CARTESIAN_POINT('Ctrl Pts',(-159.488279902428,-2.32290430669016,
125.362029156195));
#168709=CARTESIAN_POINT('Ctrl Pts',(-159.484343852987,-2.24617517969082,
125.32991708002));
#168710=CARTESIAN_POINT('Ctrl Pts',(-159.480407803546,-2.16886618280707,
125.299458252984));
#168711=CARTESIAN_POINT('Ctrl Pts',(-159.47298453714,-2.02306382742118,
125.242013855786));
#168712=CARTESIAN_POINT('Ctrl Pts',(-159.465561270735,-1.87475722491181,
125.190279159363));
#168713=CARTESIAN_POINT('Ctrl Pts',(-159.458138004329,-1.72443400395254,
125.14447917636));
#168714=CARTESIAN_POINT('Ctrl Pts',(-159.450723511608,-1.57428845255687,
125.098733325133));
#168715=CARTESIAN_POINT('Ctrl Pts',(-159.443309018888,-1.42213138063707,
125.058908332983));
#168716=CARTESIAN_POINT('Ctrl Pts',(-159.435894526167,-1.26847087488296,
125.025181419611));
#168717=CARTESIAN_POINT('Ctrl Pts',(-159.428487179813,-1.11495847290907,
124.991487013508));
#168718=CARTESIAN_POINT('Ctrl Pts',(-159.421079833459,-0.959945884076821,
124.963879064616));
#168719=CARTESIAN_POINT('Ctrl Pts',(-159.413672487105,-0.803956755437283,
124.942485141416));
#168720=CARTESIAN_POINT('Ctrl Pts',(-159.40627066543,-0.648083969375018,
124.921107174611));
#168721=CARTESIAN_POINT('Ctrl Pts',(-159.398868843755,-0.49123646197319,
124.90593405578));
#168722=CARTESIAN_POINT('Ctrl Pts',(-159.391467022079,-0.33394837746697,
124.897042355978));
#168723=CARTESIAN_POINT('Ctrl Pts',(-159.384069107768,-0.176743324116681,
124.888155350036));
#168724=CARTESIAN_POINT('Ctrl Pts',(-159.376671193457,-0.0190985286100915,
124.88554318034));
#168725=CARTESIAN_POINT('Ctrl Pts',(-159.369273279145,0.138446542508064,
124.889230600621));
#168726=CARTESIAN_POINT('Ctrl Pts',(-159.361876594233,0.295965432493784,
124.892917408119));
#168727=CARTESIAN_POINT('Ctrl Pts',(-159.354479909321,0.453384258152054,
124.902901719124));
#168728=CARTESIAN_POINT('Ctrl Pts',(-159.347083224409,0.610163229585403,
124.919156169481));
#168729=CARTESIAN_POINT('Ctrl Pts',(-159.339686867473,0.766935249274866,
124.935409899098));
#168730=CARTESIAN_POINT('Ctrl Pts',(-159.332290510538,0.923067099844836,
124.957933176764));
#168731=CARTESIAN_POINT('Ctrl Pts',(-159.324894153603,1.07802406094925,
124.986646746421));
#168732=CARTESIAN_POINT('Ctrl Pts',(-159.317496664266,1.23300474636,125.015364712198));
#168733=CARTESIAN_POINT('Ctrl Pts',(-159.31009917493,1.38680981706991,125.050274789043));
#168734=CARTESIAN_POINT('Ctrl Pts',(-159.302701685593,1.53891484066075,
125.091246608928));
#168735=CARTESIAN_POINT('Ctrl Pts',(-159.295301603078,1.69107318443204,
125.132232791421));
#168736=CARTESIAN_POINT('Ctrl Pts',(-159.287901520563,1.8415299343291,125.179284850651));
#168737=CARTESIAN_POINT('Ctrl Pts',(-159.280501438048,1.98977605461909,
125.232222624393));
#168738=CARTESIAN_POINT('Ctrl Pts',(-159.273093218382,2.13818518675821,
125.285218608659));
#168739=CARTESIAN_POINT('Ctrl Pts',(-159.265684998715,2.28437848302263,
125.344113106728));
#168740=CARTESIAN_POINT('Ctrl Pts',(-159.258276779049,2.42786644536294,
125.40867761298));
#168741=CARTESIAN_POINT('Ctrl Pts',(-159.250863999747,2.57144272215026,
125.473281857608));
#168742=CARTESIAN_POINT('Ctrl Pts',(-159.243451220445,2.71231001385916,
125.543562898004));
#168743=CARTESIAN_POINT('Ctrl Pts',(-159.236038441143,2.85000412273718,
125.619246630113));
#168744=CARTESIAN_POINT('Ctrl Pts',(-159.228615070114,2.98789497541499,
125.695038502687));
#168745=CARTESIAN_POINT('Ctrl Pts',(-159.221191699085,3.12260327101227,
125.776248292564));
#168746=CARTESIAN_POINT('Ctrl Pts',(-159.213768328056,3.25369375522823,
125.862558566726));
#168747=CARTESIAN_POINT('Ctrl Pts',(-159.209832278616,3.32320107543327,
125.908322345074));
#168748=CARTESIAN_POINT('Ctrl Pts',(-159.205896229175,3.39169184193513,
125.955519371145));
#168749=CARTESIAN_POINT('Ctrl Pts',(-159.201960179734,3.45910511694965,
126.004097879716));
#168750=CARTESIAN_POINT('Ctrl Pts',(-159.194536913329,3.5862444497292,126.095715430796));
#168751=CARTESIAN_POINT('Ctrl Pts',(-159.187113646923,3.70993365627935,
126.192526108641));
#168752=CARTESIAN_POINT('Ctrl Pts',(-159.179690380518,3.82971985187992,
126.294241282269));
#168753=CARTESIAN_POINT('Ctrl Pts',(-159.172275887797,3.94936447014524,
126.395836237009));
#168754=CARTESIAN_POINT('Ctrl Pts',(-159.164861395076,4.06511497795973,
126.502323909891));
#168755=CARTESIAN_POINT('Ctrl Pts',(-159.157446902355,4.17654764210205,
126.613372624771));
#168756=CARTESIAN_POINT('Ctrl Pts',(-159.150039556001,4.28787290324731,
126.724314306719));
#168757=CARTESIAN_POINT('Ctrl Pts',(-159.142632209647,4.39488834320481,
126.83980801715));
#168758=CARTESIAN_POINT('Ctrl Pts',(-159.135224863293,4.49720359097627,
126.959482150851));
#168759=CARTESIAN_POINT('Ctrl Pts',(-159.127823041618,4.59944252817581,
127.079067027068));
#168760=CARTESIAN_POINT('Ctrl Pts',(-159.120421219942,4.69698801173753,
127.202825835845));
#168761=CARTESIAN_POINT('Ctrl Pts',(-159.113019398267,4.78948690225745,
127.330350575035));
#168762=CARTESIAN_POINT('Ctrl Pts',(-159.105621483956,4.88193696333308,
127.457807994909));
#168763=CARTESIAN_POINT('Ctrl Pts',(-159.098223569644,4.96934551833801,
127.589027084575));
#168764=CARTESIAN_POINT('Ctrl Pts',(-159.090825655333,5.05140014641481,
127.723567355547));
#168765=CARTESIAN_POINT('Ctrl Pts',(-159.083428970421,5.13344113850094,
127.858085268367));
#168766=CARTESIAN_POINT('Ctrl Pts',(-159.076032285508,5.21012977531861,
127.995922948705));
#168767=CARTESIAN_POINT('Ctrl Pts',(-159.068635600596,5.28119730948246,
128.136611465038));
#168768=CARTESIAN_POINT('Ctrl Pts',(-159.061239243661,5.35226169243737,
128.277293743094));
#168769=CARTESIAN_POINT('Ctrl Pts',(-159.053842886725,5.41770530001016,
128.420826272603));
#168770=CARTESIAN_POINT('Ctrl Pts',(-159.04644652979,5.47730578315848,128.566716338357));
#168771=CARTESIAN_POINT('Ctrl Pts',(-159.039049040453,5.53691539129293,
128.712628740252));
#168772=CARTESIAN_POINT('Ctrl Pts',(-159.031651551117,5.59067995255489,
128.860899051487));
#168773=CARTESIAN_POINT('Ctrl Pts',(-159.02425406178,5.63842568072617,129.011015585112));
#168774=CARTESIAN_POINT('Ctrl Pts',(-159.016853979265,5.68618814608851,
129.161184741855));
#168775=CARTESIAN_POINT('Ctrl Pts',(-159.00945389675,5.72792746450482,129.313201054025));
#168776=CARTESIAN_POINT('Ctrl Pts',(-159.002053814235,5.7635200653093,129.466538873358));
#168777=CARTESIAN_POINT('Ctrl Pts',(-158.994645594568,5.79915180383733,
129.620045303386));
#168778=CARTESIAN_POINT('Ctrl Pts',(-158.987237374902,5.82862324223355,
129.774875778727));
#168779=CARTESIAN_POINT('Ctrl Pts',(-158.979829155236,5.85186204309573,
129.930494957939));
#168780=CARTESIAN_POINT('Ctrl Pts',(-158.972416375933,5.87511514705216,
130.086209918159));
#168781=CARTESIAN_POINT('Ctrl Pts',(-158.965003596631,5.8921279293473,130.242714179287));
#168782=CARTESIAN_POINT('Ctrl Pts',(-158.957590817329,5.90288009126378,
130.399469038669));
#168783=CARTESIAN_POINT('Ctrl Pts',(-158.950167446301,5.9136476163734,130.556447876744));
#168784=CARTESIAN_POINT('Ctrl Pts',(-158.942744075272,5.91813664437292,
130.713677656055));
#168785=CARTESIAN_POINT('Ctrl Pts',(-158.935320704243,5.91637897506805,
130.870620604532));
#168786=CARTESIAN_POINT('Ctrl Pts',(-158.931384654802,5.91544701662791,
130.953835521609));
#168787=CARTESIAN_POINT('Ctrl Pts',(-158.927448605361,5.9127597541791,131.036969888669));
#168788=CARTESIAN_POINT('Ctrl Pts',(-158.923512555921,5.90832780090972,
131.11994445666));
#168789=CARTESIAN_POINT('Ctrl Pts',(-158.916089289515,5.89996927536024,
131.276431902343));
#168790=CARTESIAN_POINT('Ctrl Pts',(-158.90866602311,5.88537674768521,131.432823670982));
#168791=CARTESIAN_POINT('Ctrl Pts',(-158.901242756704,5.86454825605106,
131.58858272574));
#168792=CARTESIAN_POINT('Ctrl Pts',(-158.893828263983,5.84374438196431,
131.74415768623));
#168793=CARTESIAN_POINT('Ctrl Pts',(-158.886413771262,5.8167192637182,131.899101054978));
#168794=CARTESIAN_POINT('Ctrl Pts',(-158.878999278541,5.78352291168975,
132.052877054166));
#168795=CARTESIAN_POINT('Ctrl Pts',(-158.871591932187,5.75035855555522,
132.206504838256));
#168796=CARTESIAN_POINT('Ctrl Pts',(-158.864184585834,5.71103488531188,
132.358967130306));
#168797=CARTESIAN_POINT('Ctrl Pts',(-158.85677723948,5.66565353789099,132.509734638443));
#168798=CARTESIAN_POINT('Ctrl Pts',(-158.849375417804,5.62030603759115,
132.660389698485));
#168799=CARTESIAN_POINT('Ctrl Pts',(-158.841973596129,5.5689099632813,132.809352135558));
#168800=CARTESIAN_POINT('Ctrl Pts',(-158.834571774453,5.5116176982491,132.956104308354));
#168801=CARTESIAN_POINT('Ctrl Pts',(-158.827173860142,5.45435567735766,
133.102779011821));
#168802=CARTESIAN_POINT('Ctrl Pts',(-158.819775945831,5.39120379995621,
133.247245427855));
#168803=CARTESIAN_POINT('Ctrl Pts',(-158.81237803152,5.32236379038003,133.389002613153));
#168804=CARTESIAN_POINT('Ctrl Pts',(-158.804981346607,5.25353522076465,
133.530736240978));
#168805=CARTESIAN_POINT('Ctrl Pts',(-158.797584661695,5.17902055795444,
133.669761196163));
#168806=CARTESIAN_POINT('Ctrl Pts',(-158.790187976783,5.09906906279423,
133.805597904978));
#168807=CARTESIAN_POINT('Ctrl Pts',(-158.782791619847,5.0191211127671,133.941428590652));
#168808=CARTESIAN_POINT('Ctrl Pts',(-158.775395262912,4.93373699908124,
134.074070989338));
#168809=CARTESIAN_POINT('Ctrl Pts',(-158.767998905977,4.8432110719056,134.203071707887));
#168810=CARTESIAN_POINT('Ctrl Pts',(-158.76060141664,4.75267128497914,134.332092176776));
#168811=CARTESIAN_POINT('Ctrl Pts',(-158.753203927303,4.65698833153793,
134.457469549783));
#168812=CARTESIAN_POINT('Ctrl Pts',(-158.745806437967,4.55649877260838,
134.578781036348));
#168813=CARTESIAN_POINT('Ctrl Pts',(-158.738406355452,4.45597398721988,
134.700135048466));
#168814=CARTESIAN_POINT('Ctrl Pts',(-158.731006272937,4.35063947960985,
134.817420049101));
#168815=CARTESIAN_POINT('Ctrl Pts',(-158.723606190422,4.24087069958465,
134.930247949026));
#168816=CARTESIAN_POINT('Ctrl Pts',(-158.716197970755,4.13098121750116,
135.043199914827));
#168817=CARTESIAN_POINT('Ctrl Pts',(-158.708789751089,4.01664798590246,
135.151684724491));
#168818=CARTESIAN_POINT('Ctrl Pts',(-158.701381531422,3.89828230257228,
135.255352153387));
#168819=CARTESIAN_POINT('Ctrl Pts',(-158.69396875212,3.77984376713906,135.359083387856));
#168820=CARTESIAN_POINT('Ctrl Pts',(-158.686555972818,3.65736812421176,
135.457991099397));
#168821=CARTESIAN_POINT('Ctrl Pts',(-158.679143193516,3.53129762763767,
135.55176702818));
#168822=CARTESIAN_POINT('Ctrl Pts',(-158.671719822487,3.40504699562614,
135.645676948408));
#168823=CARTESIAN_POINT('Ctrl Pts',(-158.664296451459,3.27519155859747,
135.734440231068));
#168824=CARTESIAN_POINT('Ctrl Pts',(-158.65687308043,3.14220094799595,135.817792951298));
#168825=CARTESIAN_POINT('Ctrl Pts',(-158.652937030989,3.07168613519026,
135.861988563585));
#168826=CARTESIAN_POINT('Ctrl Pts',(-158.649000981548,3.00029030670304,
135.904663849644));
#168827=CARTESIAN_POINT('Ctrl Pts',(-158.645064932108,2.92808587369328,
135.945784902604));
#168828=CARTESIAN_POINT('Ctrl Pts',(-158.637641665702,2.79191056645806,
136.023337925143));
#168829=CARTESIAN_POINT('Ctrl Pts',(-158.630218399297,2.65244612460663,
136.095594389359));
#168830=CARTESIAN_POINT('Ctrl Pts',(-158.622795132891,2.51014331202124,
136.162262363176));
#168831=CARTESIAN_POINT('Ctrl Pts',(-158.61538064017,2.3680086895428,136.228851540985));
#168832=CARTESIAN_POINT('Ctrl Pts',(-158.60796614745,2.22304270865427,136.289865219124));
#168833=CARTESIAN_POINT('Ctrl Pts',(-158.600551654729,2.07572316623768,
136.345055871742));
#168834=CARTESIAN_POINT('Ctrl Pts',(-158.593144308375,1.92854561594214,
136.400193329531));
#168835=CARTESIAN_POINT('Ctrl Pts',(-158.585736962021,1.77901936738352,
136.449518805002));
#168836=CARTESIAN_POINT('Ctrl Pts',(-158.578329615667,1.62764466604802,
136.492831713));
#168837=CARTESIAN_POINT('Ctrl Pts',(-158.570927793992,1.47638286567624,
136.536112316596));
#168838=CARTESIAN_POINT('Ctrl Pts',(-158.563525972316,1.32327571494822,
136.573389179515));
#168839=CARTESIAN_POINT('Ctrl Pts',(-158.556124150641,1.16884108704619,
136.60451070836));
#168840=CARTESIAN_POINT('Ctrl Pts',(-158.54872623633,1.01448798398213,136.635615808392));
#168841=CARTESIAN_POINT('Ctrl Pts',(-158.541328322018,0.858809164365971,
136.660571972034));
#168842=CARTESIAN_POINT('Ctrl Pts',(-158.533930407707,0.702335122916342,
136.679278143593));
#168843=CARTESIAN_POINT('Ctrl Pts',(-158.526533722795,0.545887084613451,
136.697981206525));
#168844=CARTESIAN_POINT('Ctrl Pts',(-158.519137037882,0.388644457054291,
136.710436294489));
#168845=CARTESIAN_POINT('Ctrl Pts',(-158.51174035297,0.231145450774582,
136.716593896378));
#168846=CARTESIAN_POINT('Ctrl Pts',(-158.504343996035,0.0736534281658596,
136.722751225232));
#168847=CARTESIAN_POINT('Ctrl Pts',(-158.496947639099,-0.0840945775471877,
136.722611608645));
#168848=CARTESIAN_POINT('Ctrl Pts',(-158.489551282164,-0.241558010409788,
136.716177621678));
#168849=CARTESIAN_POINT('Ctrl Pts',(-158.482153792827,-0.399045551325945,
136.709742649651));
#168850=CARTESIAN_POINT('Ctrl Pts',(-158.474756303491,-0.556248059629689,
136.697011403663));
#168851=CARTESIAN_POINT('Ctrl Pts',(-158.467358814154,-0.712627910191346,
136.678038513409));
#168852=CARTESIAN_POINT('Ctrl Pts',(-158.459958731639,-0.869062579466975,
136.659058972238));
#168853=CARTESIAN_POINT('Ctrl Pts',(-158.452558649124,-1.02467364648604,
136.633833475447));
#168854=CARTESIAN_POINT('Ctrl Pts',(-158.445158566609,-1.17893166100033,
136.602468127883));
#168855=CARTESIAN_POINT('Ctrl Pts',(-158.437750346943,-1.33335929805991,
136.571068290895));
#168856=CARTESIAN_POINT('Ctrl Pts',(-158.430342127276,-1.48643054530283,
136.533515194578));
#168857=CARTESIAN_POINT('Ctrl Pts',(-158.42293390761,-1.63762843232964,
136.489965570438));
#168858=CARTESIAN_POINT('Ctrl Pts',(-158.415521128308,-1.78891937913304,
136.446389142232));
#168859=CARTESIAN_POINT('Ctrl Pts',(-158.408108349006,-1.93833431469994,
136.39680894919));
#168860=CARTESIAN_POINT('Ctrl Pts',(-158.400695569704,-2.08537484229872,
136.341430450032));
#168861=CARTESIAN_POINT('Ctrl Pts',(-158.393272198675,-2.23262546829905,
136.285972823478));
#168862=CARTESIAN_POINT('Ctrl Pts',(-158.385848827646,-2.37749456751733,
136.22470048905));
#168863=CARTESIAN_POINT('Ctrl Pts',(-158.378425456617,-2.51950624522521,
136.15786590315));
#168864=CARTESIAN_POINT('Ctrl Pts',(-158.374489407176,-2.59480424427137,
136.12242860203));
#168865=CARTESIAN_POINT('Ctrl Pts',(-158.370553357736,-2.66929936030063,
136.085428304004));
#168866=CARTESIAN_POINT('Ctrl Pts',(-158.366617308295,-2.74292392650072,
136.046907603138));
#168867=CARTESIAN_POINT('Ctrl Pts',(-158.359194041889,-2.88177756060691,
135.974258763496));
#168868=CARTESIAN_POINT('Ctrl Pts',(-158.351770775484,-3.01795290779085,
135.895979762598));
#168869=CARTESIAN_POINT('Ctrl Pts',(-158.344347509078,-3.15096070844118,
135.812292044449));
#168870=CARTESIAN_POINT('Ctrl Pts',(-158.336933016357,-3.28381130491713,
135.728703238232));
#168871=CARTESIAN_POINT('Ctrl Pts',(-158.329518523636,-3.41350149399454,
135.639718636236));
#168872=CARTESIAN_POINT('Ctrl Pts',(-158.322104030915,-3.53956476427929,
135.54560642874));
#168873=CARTESIAN_POINT('Ctrl Pts',(-158.314696684561,-3.66550653003723,
135.451584930133));
#168874=CARTESIAN_POINT('Ctrl Pts',(-158.307289338207,-3.78782803924903,
135.352445886752));
#168875=CARTESIAN_POINT('Ctrl Pts',(-158.299881991854,-3.90609013903702,
135.248501748113));
#168876=CARTESIAN_POINT('Ctrl Pts',(-158.292480170178,-4.02426403448955,
135.144635134934));
#168877=CARTESIAN_POINT('Ctrl Pts',(-158.285078348503,-4.13838426981755,
135.035970807751));
#168878=CARTESIAN_POINT('Ctrl Pts',(-158.277676526827,-4.24804338209912,
134.922862528007));
#168879=CARTESIAN_POINT('Ctrl Pts',(-158.270278612516,-4.3576446061889,
134.809813957243));
#168880=CARTESIAN_POINT('Ctrl Pts',(-158.262880698205,-4.46278913812631,
134.692326373282));
#168881=CARTESIAN_POINT('Ctrl Pts',(-158.255482783893,-4.56310521153969,
134.570791473286));
#168882=CARTESIAN_POINT('Ctrl Pts',(-158.248086098981,-4.66340461424173,
134.449276770185));
#168883=CARTESIAN_POINT('Ctrl Pts',(-158.240689414069,-4.75887691355273,
134.323716373552));
#168884=CARTESIAN_POINT('Ctrl Pts',(-158.233292729156,-4.84918953843538,
134.194536333193));
#168885=CARTESIAN_POINT('Ctrl Pts',(-158.225896372221,-4.93949815876135,
134.065362020813));
#168886=CARTESIAN_POINT('Ctrl Pts',(-158.218500015286,-5.02464734566979,
133.932568689775));
#168887=CARTESIAN_POINT('Ctrl Pts',(-158.21110365835,-5.10434708193491,
133.796612516996));
#168888=CARTESIAN_POINT('Ctrl Pts',(-158.203706169013,-5.18405902043334,
133.66063552898));
#168889=CARTESIAN_POINT('Ctrl Pts',(-158.196308679677,-5.25831965823834,
133.521495057102));
#168890=CARTESIAN_POINT('Ctrl Pts',(-158.18891119034,-5.32688435734669,
133.379672949295));
#168891=CARTESIAN_POINT('Ctrl Pts',(-158.181511107825,-5.39547309170373,
133.237801125969));
#168892=CARTESIAN_POINT('Ctrl Pts',(-158.17411102531,-5.45836174956468,
133.093246130967));
#168893=CARTESIAN_POINT('Ctrl Pts',(-158.166710942795,-5.51535341915249,
132.946510758042));
#168894=CARTESIAN_POINT('Ctrl Pts',(-158.159302723129,-5.57240775693998,
132.79961403449));
#168895=CARTESIAN_POINT('Ctrl Pts',(-158.151894503462,-5.6235520215571,
132.650532493136));
#168896=CARTESIAN_POINT('Ctrl Pts',(-158.144486283796,-5.66863864053037,
132.499785793027));
#168897=CARTESIAN_POINT('Ctrl Pts',(-158.137073504493,-5.71375300956531,
132.348946310839));
#168898=CARTESIAN_POINT('Ctrl Pts',(-158.129660725191,-5.75280221131124,
132.196439988492));
#168899=CARTESIAN_POINT('Ctrl Pts',(-158.122247945889,-5.78568970840053,
132.042797196729));
#168900=CARTESIAN_POINT('Ctrl Pts',(-158.11482457486,-5.81862419668799,
131.888934872939));
#168901=CARTESIAN_POINT('Ctrl Pts',(-158.107401203832,-5.84537933316278,
131.733933203442));
#168902=CARTESIAN_POINT('Ctrl Pts',(-158.099977832803,-5.86591028381913,
131.578329030801));
#168903=CARTESIAN_POINT('Ctrl Pts',(-158.096041783362,-5.87679628648974,
131.495823964801));
#168904=CARTESIAN_POINT('Ctrl Pts',(-158.092105733922,-5.88593331771477,
131.413149549017));
#168905=CARTESIAN_POINT('Ctrl Pts',(-158.088169684481,-5.89332063752347,
131.330385736586));
#168906=CARTESIAN_POINT('Ctrl Pts',(-158.079904853723,-5.90883237051814,
131.156600088571));
#168907=CARTESIAN_POINT('Ctrl Pts',(-158.071640022965,-5.9166585591732,
130.982118301593));
#168908=CARTESIAN_POINT('Ctrl Pts',(-158.063375192207,-5.9167492034552,
130.807430782429));
#168909=CARTESIAN_POINT('',(-156.31337639652,-5.91261572195128,130.808150436615));
#168910=CARTESIAN_POINT('Ctrl Pts',(-158.063372747364,-5.92457053254746,
130.807383097723));
#168911=CARTESIAN_POINT('Ctrl Pts',(-157.978822518465,-5.913266273438,129.017939476383));
#168912=CARTESIAN_POINT('Ctrl Pts',(-157.801456414963,-4.0946913805117,
125.244264131813));
#168913=CARTESIAN_POINT('Ctrl Pts',(-157.531274436855,2.33159049714918,
124.205781506578));
#168914=CARTESIAN_POINT('Ctrl Pts',(-157.252826813043,6.81185310351898,
129.19930054815));
#168915=CARTESIAN_POINT('Ctrl Pts',(-156.97437918923,5.032355485277,135.667791381967));
#168916=CARTESIAN_POINT('Ctrl Pts',(-156.695931565417,-1.37163097969959,
137.667026935103));
#168917=CARTESIAN_POINT('Ctrl Pts',(-156.475597610672,-5.44167151906352,
134.25874964179));
#168918=CARTESIAN_POINT('Ctrl Pts',(-156.34807953053,-5.91370668157247,
131.547445981901));
#168919=CARTESIAN_POINT('Ctrl Pts',(-156.313377324993,-5.90942929569692,
130.808168187674));
#168920=CARTESIAN_POINT('',(-154.563373962346,-5.91330263212981,130.799862701196));
#168921=CARTESIAN_POINT('Ctrl Pts',(-156.313375192207,-5.91674880096835,
130.808127411907));
#168922=CARTESIAN_POINT('Ctrl Pts',(-156.30592501074,-5.91684996871559,
130.649216653056));
#168923=CARTESIAN_POINT('Ctrl Pts',(-156.298474829273,-5.91054481878383,
130.490278168592));
#168924=CARTESIAN_POINT('Ctrl Pts',(-156.291024647806,-5.89785334377332,
130.3318603553));
#168925=CARTESIAN_POINT('Ctrl Pts',(-156.283573932567,-5.8851609594741,
130.173431192064));
#168926=CARTESIAN_POINT('Ctrl Pts',(-156.276123217327,-5.86608136692814,
130.015523138905));
#168927=CARTESIAN_POINT('Ctrl Pts',(-156.268672502087,-5.8406865256537,
129.858680189754));
#168928=CARTESIAN_POINT('Ctrl Pts',(-156.261219862126,-5.81528512420402,
129.701796723821));
#168929=CARTESIAN_POINT('Ctrl Pts',(-156.253767222165,-5.78356528241957,
129.545979270953));
#168930=CARTESIAN_POINT('Ctrl Pts',(-156.246314582203,-5.74565022793222,
129.391762295054));
#168931=CARTESIAN_POINT('Ctrl Pts',(-156.238858625697,-5.70771830063484,
129.237476690117));
#168932=CARTESIAN_POINT('Ctrl Pts',(-156.231402669191,-5.66358575588237,
129.084793335707));
#168933=CARTESIAN_POINT('Ctrl Pts',(-156.223946712685,-5.61342587259247,
128.934232136576));
#168934=CARTESIAN_POINT('Ctrl Pts',(-156.216481268912,-5.56320216379481,
128.783479357156));
#168935=CARTESIAN_POINT('Ctrl Pts',(-156.209015825139,-5.50693591093644,
128.634854474635));
#168936=CARTESIAN_POINT('Ctrl Pts',(-156.201550381365,-5.44484916311179,
128.488858910924));
#168937=CARTESIAN_POINT('Ctrl Pts',(-156.194079889917,-5.38272043603389,
128.342764633963));
#168938=CARTESIAN_POINT('Ctrl Pts',(-156.186609398468,-5.3147635256011,
128.199303549248));
#168939=CARTESIAN_POINT('Ctrl Pts',(-156.179138907019,-5.24124659973601,
128.058952698284));
#168940=CARTESIAN_POINT('Ctrl Pts',(-156.171656160374,-5.16760907077987,
127.918371604472));
#168941=CARTESIAN_POINT('Ctrl Pts',(-156.164173413729,-5.08839348286153,
127.780911256275));
#168942=CARTESIAN_POINT('Ctrl Pts',(-156.156690667084,-5.00391214106337,
127.647020938815));
#168943=CARTESIAN_POINT('Ctrl Pts',(-156.150805883987,-4.93747204949496,
127.541723310216));
#168944=CARTESIAN_POINT('Ctrl Pts',(-156.144921100889,-4.86777598405215,
127.438633188503));
#168945=CARTESIAN_POINT('Ctrl Pts',(-156.139036317792,-4.79499301008061,
127.337954323466));
#168946=CARTESIAN_POINT('Ctrl Pts',(-156.131613051386,-4.70318208067051,
127.210954564228));
#168947=CARTESIAN_POINT('Ctrl Pts',(-156.124189784981,-4.60618328101365,
127.08741283028));
#168948=CARTESIAN_POINT('Ctrl Pts',(-156.116766518575,-4.50428593097169,
126.967781566569));
#168949=CARTESIAN_POINT('Ctrl Pts',(-156.109352025854,-4.40250901513543,
126.848291697077));
#168950=CARTESIAN_POINT('Ctrl Pts',(-156.101937533134,-4.2958453129962,
126.732703379411));
#168951=CARTESIAN_POINT('Ctrl Pts',(-156.094523040413,-4.18462714516366,
126.621439841546));
#168952=CARTESIAN_POINT('Ctrl Pts',(-156.087115694059,-4.07351617358825,
126.510283543668));
#168953=CARTESIAN_POINT('Ctrl Pts',(-156.079708347705,-3.95785973761438,
126.403443989399));
#168954=CARTESIAN_POINT('Ctrl Pts',(-156.072301001351,-3.8380300361042,
126.301310983766));
#168955=CARTESIAN_POINT('Ctrl Pts',(-156.064899179676,-3.71828970810598,
126.199254152782));
#168956=CARTESIAN_POINT('Ctrl Pts',(-156.057497358,-3.59438259501838,126.101897122016));
#168957=CARTESIAN_POINT('Ctrl Pts',(-156.050095536325,-3.4667172359339,
126.009592409552));
#168958=CARTESIAN_POINT('Ctrl Pts',(-156.042697622013,-3.33911927039982,
125.917336424029));
#168959=CARTESIAN_POINT('Ctrl Pts',(-156.035299707702,-3.20776731174243,
125.830127663359));
#168960=CARTESIAN_POINT('Ctrl Pts',(-156.027901793391,-3.07310232339073,
125.74827787769));
#168961=CARTESIAN_POINT('Ctrl Pts',(-156.020505108479,-2.93845971391682,
125.666441693971));
#168962=CARTESIAN_POINT('Ctrl Pts',(-156.013108423567,-2.80050548614263,
125.589962911443));
#168963=CARTESIAN_POINT('Ctrl Pts',(-156.005711738654,-2.65970898003594,
125.519109563546));
#168964=CARTESIAN_POINT('Ctrl Pts',(-155.998315381719,-2.51891871699388,
125.448259357362));
#168965=CARTESIAN_POINT('Ctrl Pts',(-155.990919024784,-2.37528675966399,
125.383034257648));
#168966=CARTESIAN_POINT('Ctrl Pts',(-155.983522667848,-2.22930616105943,
125.323655863361));
#168967=CARTESIAN_POINT('Ctrl Pts',(-155.976125178511,-2.08330321245213,
125.264268378091));
#168968=CARTESIAN_POINT('Ctrl Pts',(-155.968727689175,-1.93495125240191,
125.210729521261));
#168969=CARTESIAN_POINT('Ctrl Pts',(-155.961330199838,-1.78476223173872,
125.163212300188));
#168970=CARTESIAN_POINT('Ctrl Pts',(-155.953930117323,-1.63452056254781,
125.115678422027));
#168971=CARTESIAN_POINT('Ctrl Pts',(-155.946530034808,-1.4824409062747,
125.074170494894));
#168972=CARTESIAN_POINT('Ctrl Pts',(-155.939129952293,-1.32904909862578,
125.038811289363));
#168973=CARTESIAN_POINT('Ctrl Pts',(-155.931721732627,-1.17548862091464,
125.003413202751));
#168974=CARTESIAN_POINT('Ctrl Pts',(-155.92431351296,-1.02061347435243,
124.974177424108));
#168975=CARTESIAN_POINT('Ctrl Pts',(-155.916905293294,-0.864959109846162,
124.951175476056));
#168976=CARTESIAN_POINT('Ctrl Pts',(-155.909492513992,-0.709208942675329,
124.928159370688));
#168977=CARTESIAN_POINT('Ctrl Pts',(-155.90207973469,-0.552678972218055,
124.911384780937));
#168978=CARTESIAN_POINT('Ctrl Pts',(-155.894666955388,-0.395907931395946,
124.900871185683));
#168979=CARTESIAN_POINT('Ctrl Pts',(-155.887243584359,-0.238912888759547,
124.890342568111));
#168980=CARTESIAN_POINT('Ctrl Pts',(-155.87982021333,-0.0816764599822073,
124.886092822268));
#168981=CARTESIAN_POINT('Ctrl Pts',(-155.872396842301,0.0752636318832187,
124.888089329988));
#168982=CARTESIAN_POINT('Ctrl Pts',(-155.868460792861,0.158477034319438,
124.889147926287));
#168983=CARTESIAN_POINT('Ctrl Pts',(-155.86452474342,0.241607215557805,
124.891961701979));
#168984=CARTESIAN_POINT('Ctrl Pts',(-155.860588693979,0.324574942789907,
124.896519923284));
#168985=CARTESIAN_POINT('Ctrl Pts',(-155.853165427573,0.481049487009007,
124.905116586408));
#168986=CARTESIAN_POINT('Ctrl Pts',(-155.845742161168,0.63741886720515,
124.919947098834));
#168987=CARTESIAN_POINT('Ctrl Pts',(-155.838318894762,0.793146044176981,
124.941012605116));
#168988=CARTESIAN_POINT('Ctrl Pts',(-155.830904402041,0.948689164557967,
124.962053213718));
#168989=CARTESIAN_POINT('Ctrl Pts',(-155.82348990932,1.10359122625353,124.9893140981));
#168990=CARTESIAN_POINT('Ctrl Pts',(-155.816075416599,1.25731652817408,
125.022744432581));
#168991=CARTESIAN_POINT('Ctrl Pts',(-155.808668070246,1.41089366386142,
125.056142545647));
#168992=CARTESIAN_POINT('Ctrl Pts',(-155.801260723892,1.56329593543008,
125.095698192009));
#168993=CARTESIAN_POINT('Ctrl Pts',(-155.793853377538,1.71399420629504,
125.141308929361));
#168994=CARTESIAN_POINT('Ctrl Pts',(-155.786451555863,1.8645800807045,125.186885648504));
#168995=CARTESIAN_POINT('Ctrl Pts',(-155.779049734187,2.01346412920573,
125.238508358769));
#168996=CARTESIAN_POINT('Ctrl Pts',(-155.771647912512,2.16012894299117,
125.296023889283));
#168997=CARTESIAN_POINT('Ctrl Pts',(-155.7642499982,2.30671633356222,125.353509057796));
#168998=CARTESIAN_POINT('Ctrl Pts',(-155.756852083889,2.45108647589852,
125.41688071536));
#168999=CARTESIAN_POINT('Ctrl Pts',(-155.749454169578,2.59273873426755,
125.485936375525));
#169000=CARTESIAN_POINT('Ctrl Pts',(-155.742057484666,2.73436745260167,
125.554980559892));
#169001=CARTESIAN_POINT('Ctrl Pts',(-155.734660799753,2.87327884816594,
125.629706708731));
#169002=CARTESIAN_POINT('Ctrl Pts',(-155.727264114841,3.00899372711915,
125.709864831656));
#169003=CARTESIAN_POINT('Ctrl Pts',(-155.719867757906,3.14470258833241,
125.790019400285));
#169004=CARTESIAN_POINT('Ctrl Pts',(-155.71247140097,3.27721489333526,125.875605274249));
#169005=CARTESIAN_POINT('Ctrl Pts',(-155.705075044035,3.40607769745273,
125.96632741373));
#169006=CARTESIAN_POINT('Ctrl Pts',(-155.697677554698,3.53496023079448,
126.057063443003));
#169007=CARTESIAN_POINT('Ctrl Pts',(-155.690280065362,3.66019184545004,
126.152937088664));
#169008=CARTESIAN_POINT('Ctrl Pts',(-155.682882576025,3.78135026353552,
126.253611146659));
#169009=CARTESIAN_POINT('Ctrl Pts',(-155.67548249351,3.90255115351646,126.354320495789));
#169010=CARTESIAN_POINT('Ctrl Pts',(-155.668082410995,4.0196757171475,126.459833369229));
#169011=CARTESIAN_POINT('Ctrl Pts',(-155.66068232848,4.13233643702285,126.569773727));
#169012=CARTESIAN_POINT('Ctrl Pts',(-155.653274108814,4.24512103894167,
126.679834975497));
#169013=CARTESIAN_POINT('Ctrl Pts',(-155.645865889147,4.35343172726638,
126.794333170112));
#169014=CARTESIAN_POINT('Ctrl Pts',(-155.638457669481,4.45691890369688,
126.912856480556));
#169015=CARTESIAN_POINT('Ctrl Pts',(-155.631044890179,4.5604697747577,127.031452740119));
#169016=CARTESIAN_POINT('Ctrl Pts',(-155.623632110877,4.65919098468538,
127.154078761921));
#169017=CARTESIAN_POINT('Ctrl Pts',(-155.616219331575,4.75277494704296,
127.280291823507));
#169018=CARTESIAN_POINT('Ctrl Pts',(-155.608795960546,4.84649262655447,
127.406685224234));
#169019=CARTESIAN_POINT('Ctrl Pts',(-155.601372589517,4.93505818855841,
127.536675593498));
#169020=CARTESIAN_POINT('Ctrl Pts',(-155.593949218489,5.01820842319731,
127.669792898749));
#169021=CARTESIAN_POINT('Ctrl Pts',(-155.590013169048,5.06229667276761,
127.740374888102));
#169022=CARTESIAN_POINT('Ctrl Pts',(-155.586077119607,5.10486325711525,
127.81183557844));
#169023=CARTESIAN_POINT('Ctrl Pts',(-155.582141070166,5.14587437960451,
127.884102507085));
#169024=CARTESIAN_POINT('Ctrl Pts',(-155.57471780376,5.22322007670234,128.02039567913));
#169025=CARTESIAN_POINT('Ctrl Pts',(-155.567294537355,5.295264216107,128.159969921523));
#169026=CARTESIAN_POINT('Ctrl Pts',(-155.559871270949,5.36171555206768,
128.302374026632));
#169027=CARTESIAN_POINT('Ctrl Pts',(-155.552456778228,5.42808834806768,
128.444609821914));
#169028=CARTESIAN_POINT('Ctrl Pts',(-155.545042285507,5.48888134200826,
128.589668487366));
#169029=CARTESIAN_POINT('Ctrl Pts',(-155.537627792786,5.54384773545081,
128.737071849968));
#169030=CARTESIAN_POINT('Ctrl Pts',(-155.530220446432,5.59876115021375,
128.884333139659));
#169031=CARTESIAN_POINT('Ctrl Pts',(-155.522813100079,5.64785901507064,
129.033934280045));
#169032=CARTESIAN_POINT('Ctrl Pts',(-155.515405753725,5.69094150638549,
129.185374720963));
#169033=CARTESIAN_POINT('Ctrl Pts',(-155.50800393205,5.73399186515316,129.336702211888));
#169034=CARTESIAN_POINT('Ctrl Pts',(-155.500602110374,5.77103568188583,
129.489865914361));
#169035=CARTESIAN_POINT('Ctrl Pts',(-155.493200288699,5.80192215147819,
129.6443477251));
#169036=CARTESIAN_POINT('Ctrl Pts',(-155.485802374387,5.83279231634359,
129.798747986094));
#169037=CARTESIAN_POINT('Ctrl Pts',(-155.478404460076,5.85751153442523,
129.954464604469));
#169038=CARTESIAN_POINT('Ctrl Pts',(-155.471006545765,5.87597955746785,
130.110966932334));
#169039=CARTESIAN_POINT('Ctrl Pts',(-155.463609860852,5.89444451146012,
130.267443252351));
#169040=CARTESIAN_POINT('Ctrl Pts',(-155.45621317594,5.90666028848924,130.42470465235));
#169041=CARTESIAN_POINT('Ctrl Pts',(-155.448816491028,5.91257819657075,
130.58221284707));
#169042=CARTESIAN_POINT('Ctrl Pts',(-155.441420134092,5.918495842246,130.739714057713));
#169043=CARTESIAN_POINT('Ctrl Pts',(-155.434023777157,5.91811616020948,
130.897461668284));
#169044=CARTESIAN_POINT('Ctrl Pts',(-155.426627420222,5.91144254815312,
131.054915127374));
#169045=CARTESIAN_POINT('Ctrl Pts',(-155.419229930885,5.90476791434974,
131.21239269299));
#169046=CARTESIAN_POINT('Ctrl Pts',(-155.411832441548,5.89179744764637,
131.369575644466));
#169047=CARTESIAN_POINT('Ctrl Pts',(-155.404434952212,5.87258659585107,
131.525926440433));
#169048=CARTESIAN_POINT('Ctrl Pts',(-155.397034869697,5.85336900972132,
131.682332044931));
#169049=CARTESIAN_POINT('Ctrl Pts',(-155.389634787182,5.82790672858541,
131.837904542844));
#169050=CARTESIAN_POINT('Ctrl Pts',(-155.382234704667,5.7963066629028,131.992114646012));
#169051=CARTESIAN_POINT('Ctrl Pts',(-155.374826485,5.76467184969954,132.14649431904));
#169052=CARTESIAN_POINT('Ctrl Pts',(-155.367418265334,5.72688584848713,
132.299508239609));
#169053=CARTESIAN_POINT('Ctrl Pts',(-155.360010045667,5.68310617733135,
132.450639676437));
#169054=CARTESIAN_POINT('Ctrl Pts',(-155.352597266365,5.63929956051847,
132.601864132143));
#169055=CARTESIAN_POINT('Ctrl Pts',(-155.345184487063,5.58949204079213,
132.751203442076));
#169056=CARTESIAN_POINT('Ctrl Pts',(-155.337771707761,5.53388983510917,
132.898159522756));
#169057=CARTESIAN_POINT('Ctrl Pts',(-155.330348336732,5.47820818238717,
133.045325581176));
#169058=CARTESIAN_POINT('Ctrl Pts',(-155.322924965703,5.41671545280354,
133.190101266576));
#169059=CARTESIAN_POINT('Ctrl Pts',(-155.315501594675,5.34966482669673,
133.332011068974));
#169060=CARTESIAN_POINT('Ctrl Pts',(-155.311565545234,5.31411297587865,
133.407255051282));
#169061=CARTESIAN_POINT('Ctrl Pts',(-155.307629495793,5.27699935181552,
133.481693772887));
#169062=CARTESIAN_POINT('Ctrl Pts',(-155.303693446353,5.23836665150149,
133.555259631877));
#169063=CARTESIAN_POINT('Ctrl Pts',(-155.296270179947,5.16550658439187,
133.694002546025));
#169064=CARTESIAN_POINT('Ctrl Pts',(-155.288846913542,5.08702043844345,
133.830058608206));
#169065=CARTESIAN_POINT('Ctrl Pts',(-155.281423647136,5.0031304019728,133.962938896374));
#169066=CARTESIAN_POINT('Ctrl Pts',(-155.274009154415,4.91933951655838,
134.095662131076));
#169067=CARTESIAN_POINT('Ctrl Pts',(-155.266594661694,4.83015765121469,
134.225216750558));
#169068=CARTESIAN_POINT('Ctrl Pts',(-155.259180168973,4.73585370586237,
134.351136652104));
#169069=CARTESIAN_POINT('Ctrl Pts',(-155.25177282262,4.64164065420307,134.476935187307));
#169070=CARTESIAN_POINT('Ctrl Pts',(-155.244365476266,4.54231557310859,
134.599105682126));
#169071=CARTESIAN_POINT('Ctrl Pts',(-155.236958129912,4.43819158005151,
134.717209459683));
#169072=CARTESIAN_POINT('Ctrl Pts',(-155.229556308237,4.33414524659711,
134.835225150988));
#169073=CARTESIAN_POINT('Ctrl Pts',(-155.222154486561,4.22530737367528,
134.949179885558));
#169074=CARTESIAN_POINT('Ctrl Pts',(-155.214752664886,4.1120323424075,135.058666739308));
#169075=CARTESIAN_POINT('Ctrl Pts',(-155.207354750574,3.99881710814603,
135.168095795802));
#169076=CARTESIAN_POINT('Ctrl Pts',(-155.199956836263,3.88116964815559,
135.273061409881));
#169077=CARTESIAN_POINT('Ctrl Pts',(-155.192558921952,3.75948222490738,
135.373192411702));
#169078=CARTESIAN_POINT('Ctrl Pts',(-155.185162237039,3.63781502390215,
135.473306773566));
#169079=CARTESIAN_POINT('Ctrl Pts',(-155.177765552127,3.51210948008041,
135.568587880771));
#169080=CARTESIAN_POINT('Ctrl Pts',(-155.170368867215,3.38279214886937,
135.658703811042));
#169081=CARTESIAN_POINT('Ctrl Pts',(-155.162972510279,3.25348055172469,
135.748815745478));
#169082=CARTESIAN_POINT('Ctrl Pts',(-155.155576153344,3.12055779189248,
135.83376274494));
#169083=CARTESIAN_POINT('Ctrl Pts',(-155.148179796409,2.98448048711869,
135.913255486763));
#169084=CARTESIAN_POINT('Ctrl Pts',(-155.140782307072,2.84838234856177,
135.992760399128));
#169085=CARTESIAN_POINT('Ctrl Pts',(-155.133384817736,2.70912902575761,
136.066809202828));
#169086=CARTESIAN_POINT('Ctrl Pts',(-155.125987328399,2.56720273837941,
136.135157993434));
#169087=CARTESIAN_POINT('Ctrl Pts',(-155.118587245884,2.42522669896138,
136.203530743602));
#169088=CARTESIAN_POINT('Ctrl Pts',(-155.111187163369,2.2805761655214,136.266199340544));
#169089=CARTESIAN_POINT('Ctrl Pts',(-155.103787080854,2.13375423089479,
136.322967637878));
#169090=CARTESIAN_POINT('Ctrl Pts',(-155.096378861188,1.98677085045719,
136.379798357791));
#169091=CARTESIAN_POINT('Ctrl Pts',(-155.088970641521,1.83761164887359,
136.430715686456));
#169092=CARTESIAN_POINT('Ctrl Pts',(-155.081562421855,1.6867965091684,136.475572842404));
#169093=CARTESIAN_POINT('Ctrl Pts',(-155.074149642553,1.53588854526078,
136.520457607184));
#169094=CARTESIAN_POINT('Ctrl Pts',(-155.06673686325,1.38332297327647,136.55927467505));
#169095=CARTESIAN_POINT('Ctrl Pts',(-155.059324083948,1.22963031025704,
136.591928315883));
#169096=CARTESIAN_POINT('Ctrl Pts',(-155.05190071292,1.07571804395343,136.624628613768));
#169097=CARTESIAN_POINT('Ctrl Pts',(-155.044477341891,0.920675837183158,
136.651147833106));
#169098=CARTESIAN_POINT('Ctrl Pts',(-155.037053970862,0.765040600118077,
136.671441956926));
#169099=CARTESIAN_POINT('Ctrl Pts',(-155.033117921421,0.68251906300948,
136.682202388327));
#169100=CARTESIAN_POINT('Ctrl Pts',(-155.02918187198,0.599830837948508,
136.691213592585));
#169101=CARTESIAN_POINT('Ctrl Pts',(-155.02524582254,0.5170558791074,136.698474951406));
#169102=CARTESIAN_POINT('Ctrl Pts',(-155.017822556134,0.360944890052135,
136.712169647524));
#169103=CARTESIAN_POINT('Ctrl Pts',(-155.010399289729,0.204053392616007,
136.719678655057));
#169104=CARTESIAN_POINT('Ctrl Pts',(-155.002976023323,0.0469128289745836,
136.720924633021));
#169105=CARTESIAN_POINT('Ctrl Pts',(-154.995561530602,-0.110042007570774,
136.722169138343));
#169106=CARTESIAN_POINT('Ctrl Pts',(-154.988147037881,-0.267244954724259,
136.717165345645));
#169107=CARTESIAN_POINT('Ctrl Pts',(-154.98073254516,-0.424158520096556,
136.705887548143));
#169108=CARTESIAN_POINT('Ctrl Pts',(-154.973325198807,-0.580920846266409,
136.694620620608));
#169109=CARTESIAN_POINT('Ctrl Pts',(-154.965917852453,-0.73739397608614,
136.67709175348));
#169110=CARTESIAN_POINT('Ctrl Pts',(-154.958510506099,-0.893039590635261,
136.653327265792));
#169111=CARTESIAN_POINT('Ctrl Pts',(-154.951108684424,-1.04856911881288,
136.629580502555));
#169112=CARTESIAN_POINT('Ctrl Pts',(-154.943706862748,-1.20327199319958,
136.599607435151));
#169113=CARTESIAN_POINT('Ctrl Pts',(-154.936305041073,-1.35661430538524,
136.563486262047));
#169114=CARTESIAN_POINT('Ctrl Pts',(-154.928907126762,-1.50987566935792,
136.52738415703));
#169115=CARTESIAN_POINT('Ctrl Pts',(-154.92150921245,-1.66177753908607,
136.485140495328));
#169116=CARTESIAN_POINT('Ctrl Pts',(-154.914111298139,-1.81179561141999,
136.436884672103));
#169117=CARTESIAN_POINT('Ctrl Pts',(-154.906714613227,-1.96178875347212,
136.38863686812));
#169118=CARTESIAN_POINT('Ctrl Pts',(-154.899317928315,-2.10989836442982,
136.334378999752));
#169119=CARTESIAN_POINT('Ctrl Pts',(-154.891921243402,-2.25561462505338,
136.274290528063));
#169120=CARTESIAN_POINT('Ctrl Pts',(-154.884524886467,-2.40132442446565,
136.214204720759));
#169121=CARTESIAN_POINT('Ctrl Pts',(-154.877128529531,-2.5446407394465,
136.148288966499));
#169122=CARTESIAN_POINT('Ctrl Pts',(-154.869732172596,-2.6850733415975,
136.076771044756));
#169123=CARTESIAN_POINT('Ctrl Pts',(-154.862334683259,-2.82552744433759,
136.005242173437));
#169124=CARTESIAN_POINT('Ctrl Pts',(-154.854937193923,-2.96309662248831,
135.928109596246));
#169125=CARTESIAN_POINT('Ctrl Pts',(-154.847539704586,-3.09731502083322,
135.845647181948));
#169126=CARTESIAN_POINT('Ctrl Pts',(-154.840139622071,-3.23158046923057,
135.763155860578));
#169127=CARTESIAN_POINT('Ctrl Pts',(-154.832739539556,-3.36249248131584,
135.675331177492));
#169128=CARTESIAN_POINT('Ctrl Pts',(-154.825339457041,-3.48961409961607,
135.582490377028));
#169129=CARTESIAN_POINT('Ctrl Pts',(-154.817931237375,-3.6168755012035,
135.489547488561));
#169130=CARTESIAN_POINT('Ctrl Pts',(-154.810523017708,-3.74033788373541,
135.391577687729));
#169131=CARTESIAN_POINT('Ctrl Pts',(-154.803114798042,-3.85959674633049,
135.288939027876));
#169132=CARTESIAN_POINT('Ctrl Pts',(-154.79570201874,-3.9789290107659,135.186237195639));
#169133=CARTESIAN_POINT('Ctrl Pts',(-154.788289239438,-4.09405232759739,
135.078861032389));
#169134=CARTESIAN_POINT('Ctrl Pts',(-154.780876460135,-4.2045993989427,
134.967205132668));
#169135=CARTESIAN_POINT('Ctrl Pts',(-154.773453089107,-4.31530442512722,
134.855389693761));
#169136=CARTESIAN_POINT('Ctrl Pts',(-154.766029718078,-4.42141989529531,
134.739282580002));
#169137=CARTESIAN_POINT('Ctrl Pts',(-154.758606347049,-4.52261856366009,
134.619311716877));
#169138=CARTESIAN_POINT('Ctrl Pts',(-154.754670297609,-4.57627652585711,
134.555700286586));
#169139=CARTESIAN_POINT('Ctrl Pts',(-154.750734248168,-4.62855291262859,
134.491003117001));
#169140=CARTESIAN_POINT('Ctrl Pts',(-154.746798198727,-4.6794039866025,
134.42528714163));
#169141=CARTESIAN_POINT('Ctrl Pts',(-154.739155573455,-4.77814149203344,
134.297686464436));
#169142=CARTESIAN_POINT('Ctrl Pts',(-154.731512948183,-4.87181406104119,
134.165839883425));
#169143=CARTESIAN_POINT('Ctrl Pts',(-154.723870322912,-4.96003677850672,
134.030188529647));
#169144=CARTESIAN_POINT('Ctrl Pts',(-154.716449600915,-5.04569795340555,
133.898475806722));
#169145=CARTESIAN_POINT('Ctrl Pts',(-154.709028878919,-5.12622107821451,
133.763176497115));
#169146=CARTESIAN_POINT('Ctrl Pts',(-154.701608156922,-5.20129311617826,
133.624729473247));
#169147=CARTESIAN_POINT('Ctrl Pts',(-154.694194574293,-5.27629292843997,
133.486415647222));
#169148=CARTESIAN_POINT('Ctrl Pts',(-154.686780991664,-5.34585191604673,
133.344960458892));
#169149=CARTESIAN_POINT('Ctrl Pts',(-154.679367409035,-5.40970024717301,
133.200831731149));
#169150=CARTESIAN_POINT('Ctrl Pts',(-154.671959507099,-5.47349965420942,
133.056813442734));
#169151=CARTESIAN_POINT('Ctrl Pts',(-154.664551605163,-5.5315969659786,
132.910126031599));
#169152=CARTESIAN_POINT('Ctrl Pts',(-154.657143703227,-5.58376829481499,
132.761261788376));
#169153=CARTESIAN_POINT('Ctrl Pts',(-154.649740027136,-5.63590986246714,
132.612482464903));
#169154=CARTESIAN_POINT('Ctrl Pts',(-154.642336351045,-5.68213205602446,
132.461529132111));
#169155=CARTESIAN_POINT('Ctrl Pts',(-154.634932674954,-5.72225919274741,
132.3089138049));
#169156=CARTESIAN_POINT('Ctrl Pts',(-154.627531344331,-5.7623736172847,
132.156346825878));
#169157=CARTESIAN_POINT('Ctrl Pts',(-154.620130013707,-5.79639673423116,
132.002119259781));
#169158=CARTESIAN_POINT('Ctrl Pts',(-154.612728683084,-5.82420280300167,
131.846757985179));
#169159=CARTESIAN_POINT('Ctrl Pts',(-154.605328642872,-5.85200402382515,
131.691423797587));
#169160=CARTESIAN_POINT('Ctrl Pts',(-154.597928602659,-5.87359029279718,
131.534956661622));
#169161=CARTESIAN_POINT('Ctrl Pts',(-154.590528562447,-5.88888707822839,
131.377893129613));
#169162=CARTESIAN_POINT('Ctrl Pts',(-154.58312737356,-5.9041862381108,131.220805217338));
#169163=CARTESIAN_POINT('Ctrl Pts',(-154.575726184673,-5.9131939302452,
131.063121094403));
#169164=CARTESIAN_POINT('Ctrl Pts',(-154.568324995785,-5.9158875279668,
130.905381996228));
#169165=CARTESIAN_POINT('Ctrl Pts',(-154.566675061259,-5.91648800715306,
130.870217485747));
#169166=CARTESIAN_POINT('Ctrl Pts',(-154.565025126733,-5.91677489975811,
130.835050248019));
#169167=CARTESIAN_POINT('Ctrl Pts',(-154.563375192207,-5.91674830821855,
130.799886280413));
#169168=CARTESIAN_POINT('',(-152.813375192207,-5.92569483190729,130.802331264594));
#169169=CARTESIAN_POINT('Ctrl Pts',(-154.563373070317,-5.91080345335137,
130.799845598986));
#169170=CARTESIAN_POINT('Ctrl Pts',(-154.531698905183,-5.91551139364249,
130.125469392084));
#169171=CARTESIAN_POINT('Ctrl Pts',(-154.407208865444,-5.49704716835897,
127.480621738463));
#169172=CARTESIAN_POINT('Ctrl Pts',(-154.189902951101,-1.59469172994353,
123.990072773871));
#169173=CARTESIAN_POINT('Ctrl Pts',(-153.911455327288,4.87108352101917,
125.779412273391));
#169174=CARTESIAN_POINT('Ctrl Pts',(-153.633007703476,6.86057098182519,
132.186433818843));
#169175=CARTESIAN_POINT('Ctrl Pts',(-153.354560079662,2.54552886785856,
137.323397610345));
#169176=CARTESIAN_POINT('Ctrl Pts',(-153.081349242573,-3.98358274264103,
136.485740721758));
#169177=CARTESIAN_POINT('Ctrl Pts',(-152.900954280088,-5.91747741062501,
132.654946942402));
#169178=CARTESIAN_POINT('Ctrl Pts',(-152.813375192207,-5.92569483190729,
130.802331264594));
#169179=CARTESIAN_POINT('',(-151.063375192207,-5.91700250792318,130.809816046553));
#169180=CARTESIAN_POINT('Ctrl Pts',(-152.813375192207,-5.92569483190729,
130.802331264594));
#169181=CARTESIAN_POINT('Ctrl Pts',(-152.808138405483,-5.92618619215906,
130.691554212449));
#169182=CARTESIAN_POINT('Ctrl Pts',(-152.80290161876,-5.92335003819969,
130.580802825064));
#169183=CARTESIAN_POINT('Ctrl Pts',(-152.704848957432,-5.80645997517362,
128.51071536498));
#169184=CARTESIAN_POINT('Ctrl Pts',(-152.519217208224,-3.44484665824443,
124.71251426104));
#169185=CARTESIAN_POINT('Ctrl Pts',(-152.240769584411,3.26321910596172,
124.613321803534));
#169186=CARTESIAN_POINT('Ctrl Pts',(-151.962321960598,6.97254592890501,
130.203391567066));
#169187=CARTESIAN_POINT('Ctrl Pts',(-151.683874336785,4.27444367098919,
136.345722529034));
#169188=CARTESIAN_POINT('Ctrl Pts',(-151.405426712973,-2.3516635023825,
137.395812604943));
#169189=CARTESIAN_POINT('Ctrl Pts',(-151.198593664779,-5.66833219350764,
133.676476019849));
#169190=CARTESIAN_POINT('Ctrl Pts',(-151.084576491191,-5.92117706019566,
131.260015846219));
#169191=CARTESIAN_POINT('Ctrl Pts',(-151.063375192207,-5.91700250792318,
130.809816046553));
#169192=CARTESIAN_POINT('',(-149.313375192166,-5.91674998398419,130.803925275142));
#169193=CARTESIAN_POINT('Ctrl Pts',(-151.063375192207,-5.91674748517798,
130.809815811424));
#169194=CARTESIAN_POINT('Ctrl Pts',(-151.056065681028,-5.91689058382068,
130.65460986341));
#169195=CARTESIAN_POINT('Ctrl Pts',(-151.048756169849,-5.91092255348512,
130.499227142345));
#169196=CARTESIAN_POINT('Ctrl Pts',(-151.04144665867,-5.89882852235356,
130.344194749244));
#169197=CARTESIAN_POINT('Ctrl Pts',(-151.034142292742,-5.88674300435314,
130.189271485274));
#169198=CARTESIAN_POINT('Ctrl Pts',(-151.026837926814,-5.8685400977311,
130.03469843971));
#169199=CARTESIAN_POINT('Ctrl Pts',(-151.019533560886,-5.84425700214759,
129.881002260616));
#169200=CARTESIAN_POINT('Ctrl Pts',(-151.012231970289,-5.81998313304877,
129.727364479161));
#169201=CARTESIAN_POINT('Ctrl Pts',(-151.004930379692,-5.78963372854271,
129.574603280231));
#169202=CARTESIAN_POINT('Ctrl Pts',(-150.997628789094,-5.75329778200764,
129.423239625746));
#169203=CARTESIAN_POINT('Ctrl Pts',(-150.990328503748,-5.71696833097914,
129.271903029415));
#169204=CARTESIAN_POINT('Ctrl Pts',(-150.983028218402,-5.67465455591097,
129.121963853903));
#169205=CARTESIAN_POINT('Ctrl Pts',(-150.975727933055,-5.62649639284513,
128.973932005519));
#169206=CARTESIAN_POINT('Ctrl Pts',(-150.968427422173,-5.57833674197355,
128.825895583816));
#169207=CARTESIAN_POINT('Ctrl Pts',(-150.961126911291,-5.52433246254643,
128.67976697175));
#169208=CARTESIAN_POINT('Ctrl Pts',(-150.953826400408,-5.46467301493037,
128.536039784352));
#169209=CARTESIAN_POINT('Ctrl Pts',(-150.946524133204,-5.40499921473299,
128.392278019763));
#169210=CARTESIAN_POINT('Ctrl Pts',(-150.939221866,-5.33966768671681,128.250919183856));
#169211=CARTESIAN_POINT('Ctrl Pts',(-150.931919598796,-5.26891544568148,
128.112435546402));
#169212=CARTESIAN_POINT('Ctrl Pts',(-150.924609826913,-5.19809049121819,
127.973809586672));
#169213=CARTESIAN_POINT('Ctrl Pts',(-150.917300055029,-5.1218338728137,
127.838065068987));
#169214=CARTESIAN_POINT('Ctrl Pts',(-150.909990283146,-5.04042816247926,
127.705648868889));
#169215=CARTESIAN_POINT('Ctrl Pts',(-150.902676570827,-4.95897856924788,
127.573161287971));
#169216=CARTESIAN_POINT('Ctrl Pts',(-150.895362858508,-4.87237456954214,
127.444005916282));
#169217=CARTESIAN_POINT('Ctrl Pts',(-150.888049146189,-4.78094076898396,
127.318598731555));
#169218=CARTESIAN_POINT('Ctrl Pts',(-150.880724518015,-4.68937050173198,
127.19300437421));
#169219=CARTESIAN_POINT('Ctrl Pts',(-150.87339988984,-4.5929562729929,127.071169678463));
#169220=CARTESIAN_POINT('Ctrl Pts',(-150.866075261666,-4.49206204232252,
126.953476411254));
#169221=CARTESIAN_POINT('Ctrl Pts',(-150.860227329559,-4.41150879144472,
126.859510926636));
#169222=CARTESIAN_POINT('Ctrl Pts',(-150.854379397453,-4.32810063904638,
126.768184663981));
#169223=CARTESIAN_POINT('Ctrl Pts',(-150.848531465346,-4.24203829366849,
126.679673759446));
#169224=CARTESIAN_POINT('Ctrl Pts',(-150.84110819894,-4.13279220367148,
126.567319509743));
#169225=CARTESIAN_POINT('Ctrl Pts',(-150.833684932535,-4.01891413083966,
126.459138588643));
#169226=CARTESIAN_POINT('Ctrl Pts',(-150.826261666129,-3.90075590755898,
126.355536737916));
#169227=CARTESIAN_POINT('Ctrl Pts',(-150.818847173408,-3.78273733748545,
126.252057335973));
#169228=CARTESIAN_POINT('Ctrl Pts',(-150.811432680687,-3.66044896444028,
126.153146475329));
#169229=CARTESIAN_POINT('Ctrl Pts',(-150.804018187966,-3.53428093362584,
126.059174757696));
#169230=CARTESIAN_POINT('Ctrl Pts',(-150.796610841613,-3.40823450830928,
125.965293613542));
#169231=CARTESIAN_POINT('Ctrl Pts',(-150.789203495259,-3.27831616692556,
125.876342356604));
#169232=CARTESIAN_POINT('Ctrl Pts',(-150.781796148905,-3.14495066844497,
125.792652739452));
#169233=CARTESIAN_POINT('Ctrl Pts',(-150.774394327229,-3.01168463898511,
125.709025541175));
#169234=CARTESIAN_POINT('Ctrl Pts',(-150.766992505554,-2.87497688651215,
125.630652366382));
#169235=CARTESIAN_POINT('Ctrl Pts',(-150.759590683879,-2.73528272313482,
125.557822808018));
#169236=CARTESIAN_POINT('Ctrl Pts',(-150.752192769567,-2.59566230321896,
125.485031695811));
#169237=CARTESIAN_POINT('Ctrl Pts',(-150.744794855256,-2.45305894225528,
125.417778544041));
#169238=CARTESIAN_POINT('Ctrl Pts',(-150.737396940945,-2.30795412648063,
125.356307909253));
#169239=CARTESIAN_POINT('Ctrl Pts',(-150.730000256032,-2.16287342449411,
125.294847489769));
#169240=CARTESIAN_POINT('Ctrl Pts',(-150.72260357112,-2.01529243612141,
125.239167825537));
#169241=CARTESIAN_POINT('Ctrl Pts',(-150.715206886208,-1.86571438933428,
125.189466105651));
#169242=CARTESIAN_POINT('Ctrl Pts',(-150.707810529273,-1.71614297499406,
125.139766589592));
#169243=CARTESIAN_POINT('Ctrl Pts',(-150.700414172337,-1.56457503256302,
125.096044608544));
#169244=CARTESIAN_POINT('Ctrl Pts',(-150.693017815402,-1.41153052363258,
125.058447970879));
#169245=CARTESIAN_POINT('Ctrl Pts',(-150.685620326065,-1.25846258319711,
125.020845577074));
#169246=CARTESIAN_POINT('Ctrl Pts',(-150.678222836729,-1.10391798867733,
124.989370483008));
#169247=CARTESIAN_POINT('Ctrl Pts',(-150.670825347392,-0.948428358278844,
124.964119679753));
#169248=CARTESIAN_POINT('Ctrl Pts',(-150.663425264877,-0.792884221232128,
124.938860024867));
#169249=CARTESIAN_POINT('Ctrl Pts',(-150.656025182362,-0.636394756969904,
124.919829064768));
#169250=CARTESIAN_POINT('Ctrl Pts',(-150.648625099847,-0.479498041886692,
124.907072071944));
#169251=CARTESIAN_POINT('Ctrl Pts',(-150.641216880181,-0.3224288027352,
124.894301051494));
#169252=CARTESIAN_POINT('Ctrl Pts',(-150.633808660514,-0.16495179074682,
124.88781780609));
#169253=CARTESIAN_POINT('Ctrl Pts',(-150.626400440848,-0.00760716935874803,
124.887615507839));
#169254=CARTESIAN_POINT('Ctrl Pts',(-150.618987661546,0.149834295018352,
124.887413085078));
#169255=CARTESIAN_POINT('Ctrl Pts',(-150.611574882244,0.307142834273683,
124.8934992982));
#169256=CARTESIAN_POINT('Ctrl Pts',(-150.604162102942,0.463782579581826,
124.905815349334));
#169257=CARTESIAN_POINT('Ctrl Pts',(-150.596738731913,0.620646139103517,
124.918148998221));
#169258=CARTESIAN_POINT('Ctrl Pts',(-150.589315360884,0.77683862642008,
124.9367302194));
#169259=CARTESIAN_POINT('Ctrl Pts',(-150.581891989855,0.931832721620842,
124.961448814243));
#169260=CARTESIAN_POINT('Ctrl Pts',(-150.577955940415,1.0140143099217,124.974555206341));
#169261=CARTESIAN_POINT('Ctrl Pts',(-150.574019890974,1.09585920157823,
124.989386189939));
#169262=CARTESIAN_POINT('Ctrl Pts',(-150.570083841534,1.17729055566755,
125.005919662444));
#169263=CARTESIAN_POINT('Ctrl Pts',(-150.562660575129,1.33086754810704,
125.037101275599));
#169264=CARTESIAN_POINT('Ctrl Pts',(-150.555237308723,1.48343710086397,
125.074435693147));
#169265=CARTESIAN_POINT('Ctrl Pts',(-150.547814042318,1.63446767789529,
125.117846221874));
#169266=CARTESIAN_POINT('Ctrl Pts',(-150.540399549597,1.7853197493273,125.161205442961));
#169267=CARTESIAN_POINT('Ctrl Pts',(-150.532985056876,1.93463611037831,
125.210626378381));
#169268=CARTESIAN_POINT('Ctrl Pts',(-150.525570564155,2.08189408032096,
125.265981107202));
#169269=CARTESIAN_POINT('Ctrl Pts',(-150.518163217801,2.22901011748802,
125.321282483051));
#169270=CARTESIAN_POINT('Ctrl Pts',(-150.510755871447,2.37407136613012,
125.382506136005));
#169271=CARTESIAN_POINT('Ctrl Pts',(-150.503348525093,2.51656912081436,
125.449474024681));
#169272=CARTESIAN_POINT('Ctrl Pts',(-150.495946703418,2.65896059529662,
125.516391966178));
#169273=CARTESIAN_POINT('Ctrl Pts',(-150.488544881742,2.79879204637759,
125.589045454751));
#169274=CARTESIAN_POINT('Ctrl Pts',(-150.481143060067,2.93557372399401,
125.667207955488));
#169275=CARTESIAN_POINT('Ctrl Pts',(-150.473745145756,3.07228319562752,
125.745329194849));
#169276=CARTESIAN_POINT('Ctrl Pts',(-150.466347231444,3.20594577680103,
125.828953469883));
#169277=CARTESIAN_POINT('Ctrl Pts',(-150.458949317133,3.33609546009509,
125.917807881369));
#169278=CARTESIAN_POINT('Ctrl Pts',(-150.451552632221,3.46622351487314,
126.006647526864));
#169279=CARTESIAN_POINT('Ctrl Pts',(-150.444155947308,3.59283952240294,
126.100715373524));
#169280=CARTESIAN_POINT('Ctrl Pts',(-150.436759262396,3.71550557490402,
126.199694626926));
#169281=CARTESIAN_POINT('Ctrl Pts',(-150.429362905461,3.83816618826414,
126.298669491484));
#169282=CARTESIAN_POINT('Ctrl Pts',(-150.421966548525,3.95687690432722,
126.402555095354));
#169283=CARTESIAN_POINT('Ctrl Pts',(-150.41457019159,4.0712323157834,126.510993874156));
#169284=CARTESIAN_POINT('Ctrl Pts',(-150.407172702253,4.18560523534468,
126.619449255211));
#169285=CARTESIAN_POINT('Ctrl Pts',(-150.399775212916,4.29562125170189,
126.732458942347));
#169286=CARTESIAN_POINT('Ctrl Pts',(-150.39237772358,4.40091141089656,126.849628096151));
#169287=CARTESIAN_POINT('Ctrl Pts',(-150.384977641065,4.50623847939347,
126.96683832342));
#169288=CARTESIAN_POINT('Ctrl Pts',(-150.37757755855,4.60683614301077,127.088210642926));
#169289=CARTESIAN_POINT('Ctrl Pts',(-150.370177476035,4.70237546928901,
127.213316826643));
#169290=CARTESIAN_POINT('Ctrl Pts',(-150.362769256368,4.79801985087831,
127.33856057747));
#169291=CARTESIAN_POINT('Ctrl Pts',(-150.355361036702,4.88859456042188,
127.467546095133));
#169292=CARTESIAN_POINT('Ctrl Pts',(-150.347952817035,4.97381337088553,
127.599815234193));
#169293=CARTESIAN_POINT('Ctrl Pts',(-150.340540037733,5.05908463210483,
127.732165782699));
#169294=CARTESIAN_POINT('Ctrl Pts',(-150.333127258431,5.138993236577,127.86780365884));
#169295=CARTESIAN_POINT('Ctrl Pts',(-150.325714479129,5.21329900242612,
128.00624623931));
#169296=CARTESIAN_POINT('Ctrl Pts',(-150.3182911081,5.28771093983817,128.144886633031));
#169297=CARTESIAN_POINT('Ctrl Pts',(-150.310867737071,5.35650388682064,
128.286339400131));
#169298=CARTESIAN_POINT('Ctrl Pts',(-150.303444366042,5.41948552731017,
128.430101326382));
#169299=CARTESIAN_POINT('Ctrl Pts',(-150.299508316602,5.45287990431955,
128.506327349195));
#169300=CARTESIAN_POINT('Ctrl Pts',(-150.295572267161,5.48464134089764,
128.583202283417));
#169301=CARTESIAN_POINT('Ctrl Pts',(-150.291636217721,5.51474689818421,
128.660649533612));
#169302=CARTESIAN_POINT('Ctrl Pts',(-150.284212951315,5.57152503966739,
128.806712630441));
#169303=CARTESIAN_POINT('Ctrl Pts',(-150.27678968491,5.62258210680279,128.955253880797));
#169304=CARTESIAN_POINT('Ctrl Pts',(-150.269366418504,5.66769531554686,
129.1057846338));
#169305=CARTESIAN_POINT('Ctrl Pts',(-150.261951925783,5.71275520422461,
129.256137471953));
#169306=CARTESIAN_POINT('Ctrl Pts',(-150.254537433062,5.75188511198533,
129.408474778131));
#169307=CARTESIAN_POINT('Ctrl Pts',(-150.247122940341,5.78491014063071,
129.562287661847));
#169308=CARTESIAN_POINT('Ctrl Pts',(-150.239715593987,5.81790333851021,
129.715952294916));
#169309=CARTESIAN_POINT('Ctrl Pts',(-150.232308247634,5.84480329354514,
129.871089311639));
#169310=CARTESIAN_POINT('Ctrl Pts',(-150.22490090128,5.86548482928115,130.027174488011));
#169311=CARTESIAN_POINT('Ctrl Pts',(-150.217499079605,5.88615093994742,
130.183143250169));
#169312=CARTESIAN_POINT('Ctrl Pts',(-150.210097257929,5.9006078172398,130.340058395429));
#169313=CARTESIAN_POINT('Ctrl Pts',(-150.202695436254,5.90878132952298,
130.497385435539));
#169314=CARTESIAN_POINT('Ctrl Pts',(-150.195297521942,5.91695052707265,
130.654629423929));
#169315=CARTESIAN_POINT('Ctrl Pts',(-150.187899607631,5.91884294613844,
130.812284502283));
#169316=CARTESIAN_POINT('Ctrl Pts',(-150.18050169332,5.91443629617107,130.969811096666));
#169317=CARTESIAN_POINT('Ctrl Pts',(-150.173105008408,5.91003037850896,
131.127311512987));
#169318=CARTESIAN_POINT('Ctrl Pts',(-150.165708323495,5.89932747981234,
131.284683114927));
#169319=CARTESIAN_POINT('Ctrl Pts',(-150.158311638583,5.88235742834927,
131.441386243145));
#169320=CARTESIAN_POINT('Ctrl Pts',(-150.150915281648,5.86538812935606,
131.598082422982));
#169321=CARTESIAN_POINT('Ctrl Pts',(-150.143518924713,5.84215227033082,
131.754109816905));
#169322=CARTESIAN_POINT('Ctrl Pts',(-150.136122567777,5.81273154775772,
131.908934071983));
#169323=CARTESIAN_POINT('Ctrl Pts',(-150.128725078441,5.78330632079681,
132.063782031049));
#169324=CARTESIAN_POINT('Ctrl Pts',(-150.121327589104,5.74769441454144,
132.217426117738));
#169325=CARTESIAN_POINT('Ctrl Pts',(-150.113930099767,5.70602858994373,
132.369342500287));
#169326=CARTESIAN_POINT('Ctrl Pts',(-150.106530017252,5.66434815945597,
132.521312136888));
#169327=CARTESIAN_POINT('Ctrl Pts',(-150.099129934737,5.61660968403365,
132.671552503739));
#169328=CARTESIAN_POINT('Ctrl Pts',(-150.091729852222,5.56299564801337,
132.819555392937));
#169329=CARTESIAN_POINT('Ctrl Pts',(-150.084321632556,5.50932265784876,
132.967721026528));
#169330=CARTESIAN_POINT('Ctrl Pts',(-150.07691341289,5.44976133169865,133.113643917819));
#169331=CARTESIAN_POINT('Ctrl Pts',(-150.069505193223,5.38454240759331,
133.256835617098));
#169332=CARTESIAN_POINT('Ctrl Pts',(-150.062092413921,5.31928334232842,
133.400115448479));
#169333=CARTESIAN_POINT('Ctrl Pts',(-150.054679634619,5.24835990826135,
133.540660405744));
#169334=CARTESIAN_POINT('Ctrl Pts',(-150.047266855317,5.17204832587609,
133.678007547393));
#169335=CARTESIAN_POINT('Ctrl Pts',(-150.039843484288,5.09562770592314,
133.815550937079));
#169336=CARTESIAN_POINT('Ctrl Pts',(-150.03242011326,5.01380375501804,133.949887067486));
#169337=CARTESIAN_POINT('Ctrl Pts',(-150.024996742231,4.92689589001179,
134.080582138081));
#169338=CARTESIAN_POINT('Ctrl Pts',(-150.02106069279,4.88081525465654,134.149879800501));
#169339=CARTESIAN_POINT('Ctrl Pts',(-150.017124643349,4.83330602756548,
134.218154376355));
#169340=CARTESIAN_POINT('Ctrl Pts',(-150.013188593908,4.78442025163299,
134.285345164826));
#169341=CARTESIAN_POINT('Ctrl Pts',(-150.005765327502,4.69222320390343,
134.412064894922));
#169342=CARTESIAN_POINT('Ctrl Pts',(-149.998342061097,4.5948488349964,134.535310825654));
#169343=CARTESIAN_POINT('Ctrl Pts',(-149.990918794691,4.49258784052027,
134.654631394759));
#169344=CARTESIAN_POINT('Ctrl Pts',(-149.98350430197,4.39044771004737,134.773810936861));
#169345=CARTESIAN_POINT('Ctrl Pts',(-149.976089809249,4.28343269088841,
134.889074071511));
#169346=CARTESIAN_POINT('Ctrl Pts',(-149.968675316528,4.17187639027414,
134.999998584166));
#169347=CARTESIAN_POINT('Ctrl Pts',(-149.961267970175,4.06042761182244,
135.110816183599));
#169348=CARTESIAN_POINT('Ctrl Pts',(-149.953860623821,3.9444465287092,135.217303224587));
#169349=CARTESIAN_POINT('Ctrl Pts',(-149.946453277467,3.82430652450501,
135.319071036754));
#169350=CARTESIAN_POINT('Ctrl Pts',(-149.939051455792,3.70425612524892,
135.420762946648));
#169351=CARTESIAN_POINT('Ctrl Pts',(-149.931649634116,3.58005326477897,
135.517742395833));
#169352=CARTESIAN_POINT('Ctrl Pts',(-149.924247812441,3.45210755323912,
135.609658111309));
#169353=CARTESIAN_POINT('Ctrl Pts',(-149.916849898129,3.32422938324483,
135.701525305193));
#169354=CARTESIAN_POINT('Ctrl Pts',(-149.909451983818,3.19261259953175,
135.788333871739));
#169355=CARTESIAN_POINT('Ctrl Pts',(-149.902054069507,3.05769911234658,
135.869773404384));
#169356=CARTESIAN_POINT('Ctrl Pts',(-149.894657384595,2.92280804533483,
135.951199403256));
#169357=CARTESIAN_POINT('Ctrl Pts',(-149.887260699682,2.78462168144833,
136.027257946324));
#169358=CARTESIAN_POINT('Ctrl Pts',(-149.87986401477,2.64361017428252,136.0976824299));
#169359=CARTESIAN_POINT('Ctrl Pts',(-149.872467657835,2.5026049197143,136.168103790781));
#169360=CARTESIAN_POINT('Ctrl Pts',(-149.865071300899,2.35877510490991,
136.232891422106));
#169361=CARTESIAN_POINT('Ctrl Pts',(-149.857674943964,2.21261445506972,
136.291825226629));
#169362=CARTESIAN_POINT('Ctrl Pts',(-149.850277454627,2.06643142766174,
136.350768054068));
#169363=CARTESIAN_POINT('Ctrl Pts',(-149.842879965291,1.91791720090442,
136.403855130574));
#169364=CARTESIAN_POINT('Ctrl Pts',(-149.835482475954,1.76758424983121,
136.450915007833));
#169365=CARTESIAN_POINT('Ctrl Pts',(-149.828082393439,1.6171985997744,136.497991381861));
#169366=CARTESIAN_POINT('Ctrl Pts',(-149.820682310924,1.46499331207091,
136.539036238572));
#169367=CARTESIAN_POINT('Ctrl Pts',(-149.813282228409,1.31149459366289,
136.573928408423));
#169368=CARTESIAN_POINT('Ctrl Pts',(-149.805874008743,1.1578270876337,136.608858945802));
#169369=CARTESIAN_POINT('Ctrl Pts',(-149.798465789076,1.00286367478862,
136.637623202355));
#169370=CARTESIAN_POINT('Ctrl Pts',(-149.79105756941,0.847140021244748,
136.660151285521));
#169371=CARTESIAN_POINT('Ctrl Pts',(-149.783644790108,0.691320522390506,
136.682693234346));
#169372=CARTESIAN_POINT('Ctrl Pts',(-149.776232010806,0.534740220888373,
136.698991323012));
#169373=CARTESIAN_POINT('Ctrl Pts',(-149.768819231503,0.377937906451597,
136.709027712447));
#169374=CARTESIAN_POINT('Ctrl Pts',(-149.761395860475,0.220911545514431,
136.719078442345));
#169375=CARTESIAN_POINT('Ctrl Pts',(-149.753972489446,0.0636629102801282,
136.722849594901));
#169376=CARTESIAN_POINT('Ctrl Pts',(-149.746549118417,-0.0932703779676402,
136.720375424773));
#169377=CARTESIAN_POINT('Ctrl Pts',(-149.742613068976,-0.176480172958929,
136.719063560405));
#169378=CARTESIAN_POINT('Ctrl Pts',(-149.738677019535,-0.259601404975529,
136.71599677807));
#169379=CARTESIAN_POINT('Ctrl Pts',(-149.734740970095,-0.342554874245969,
136.711186052656));
#169380=CARTESIAN_POINT('Ctrl Pts',(-149.727317703689,-0.499002528400226,
136.702113174664));
#169381=CARTESIAN_POINT('Ctrl Pts',(-149.719894437284,-0.655326045325712,
136.686806796327));
#169382=CARTESIAN_POINT('Ctrl Pts',(-149.712471170878,-0.810988384824968,
136.665267407661));
#169383=CARTESIAN_POINT('Ctrl Pts',(-149.705056678157,-0.966466744365004,
136.643753476763));
#169384=CARTESIAN_POINT('Ctrl Pts',(-149.697642185437,-1.12128511580916,
136.61602125006));
#169385=CARTESIAN_POINT('Ctrl Pts',(-149.690227692716,-1.2749079552451,
136.582123183487));
#169386=CARTESIAN_POINT('Ctrl Pts',(-149.682820346362,-1.42838272720545,
136.548257789146));
#169387=CARTESIAN_POINT('Ctrl Pts',(-149.675413000008,-1.58066389907574,
136.508238465913));
#169388=CARTESIAN_POINT('Ctrl Pts',(-149.668005653654,-1.73122264852107,
136.462169266128));
#169389=CARTESIAN_POINT('Ctrl Pts',(-149.660603831979,-1.88166910556994,
136.416134426492));
#169390=CARTESIAN_POINT('Ctrl Pts',(-149.653202010304,-2.03039534267612,
136.36405880351));
#169391=CARTESIAN_POINT('Ctrl Pts',(-149.645800188628,-2.17688441962812,
136.306097142163));
#169392=CARTESIAN_POINT('Ctrl Pts',(-149.638402274317,-2.32329616613749,
136.248166078325));
#169393=CARTESIAN_POINT('Ctrl Pts',(-149.631004360006,-2.46747275823444,
136.184355301241));
#169394=CARTESIAN_POINT('Ctrl Pts',(-149.623606445694,-2.60891417880448,
136.11486882019));
#169395=CARTESIAN_POINT('Ctrl Pts',(-149.616209760782,-2.75033209437662,
136.045393886531));
#169396=CARTESIAN_POINT('Ctrl Pts',(-149.60881307587,-2.88901540582003,
135.970245285314));
#169397=CARTESIAN_POINT('Ctrl Pts',(-149.601416390958,-3.02448568239786,
135.889674464269));
#169398=CARTESIAN_POINT('Ctrl Pts',(-149.594020034022,-3.15994995208127,
135.809107215819));
#169399=CARTESIAN_POINT('Ctrl Pts',(-149.586623677087,-3.29220114933539,
135.72311841641));
#169400=CARTESIAN_POINT('Ctrl Pts',(-149.579227320152,-3.42078722958298,
135.632004483099));
#169401=CARTESIAN_POINT('Ctrl Pts',(-149.571829830815,-3.54939299668735,
135.540876600013));
#169402=CARTESIAN_POINT('Ctrl Pts',(-149.564432341479,-3.6743322248794,
135.444622236477));
#169403=CARTESIAN_POINT('Ctrl Pts',(-149.557034852142,-3.79518366456432,
135.34357988025));
#169404=CARTESIAN_POINT('Ctrl Pts',(-149.549634769627,-3.9160774685339,
135.242502103782));
#169405=CARTESIAN_POINT('Ctrl Pts',(-149.542234687112,-4.03288034475929,
135.13663323219));
#169406=CARTESIAN_POINT('Ctrl Pts',(-149.534834604598,-4.14520592216597,
135.026350483179));
#169407=CARTESIAN_POINT('Ctrl Pts',(-149.527426384931,-4.25765501309316,
134.915946466947));
#169408=CARTESIAN_POINT('Ctrl Pts',(-149.520018165265,-4.3656167066114,
134.801119142203));
#169409=CARTESIAN_POINT('Ctrl Pts',(-149.512609945598,-4.46874265950966,
134.682281401385));
#169410=CARTESIAN_POINT('Ctrl Pts',(-149.505197166296,-4.57193208471119,
134.563370517921));
#169411=CARTESIAN_POINT('Ctrl Pts',(-149.497784386994,-4.6702796059402,
134.440444590711));
#169412=CARTESIAN_POINT('Ctrl Pts',(-149.490371607692,-4.76347898567933,
134.313947276347));
#169413=CARTESIAN_POINT('Ctrl Pts',(-149.482948236663,-4.85681153306298,
134.187269216687));
#169414=CARTESIAN_POINT('Ctrl Pts',(-149.475524865635,-4.94498103886841,
134.057009886425));
#169415=CARTESIAN_POINT('Ctrl Pts',(-149.468101494606,-5.02772572507474,
133.923640117053));
#169416=CARTESIAN_POINT('Ctrl Pts',(-149.464165445165,-5.0715989431393,
133.852924265158));
#169417=CARTESIAN_POINT('Ctrl Pts',(-149.460229395723,-5.11394782856564,
133.781334347775));
#169418=CARTESIAN_POINT('Ctrl Pts',(-149.456293346282,-5.15473880542603,
133.708942930109));
#169419=CARTESIAN_POINT('Ctrl Pts',(-149.448532235494,-5.23517054168529,
133.566201376429));
#169420=CARTESIAN_POINT('Ctrl Pts',(-149.440771124706,-5.30976717986972,
133.419943423783));
#169421=CARTESIAN_POINT('Ctrl Pts',(-149.433010013918,-5.37822242016894,
133.270664362382));
#169422=CARTESIAN_POINT('Ctrl Pts',(-149.425261138445,-5.44656974145093,
133.121620637962));
#169423=CARTESIAN_POINT('Ctrl Pts',(-149.417512262972,-5.50879482582847,
132.969565589936));
#169424=CARTESIAN_POINT('Ctrl Pts',(-149.409763387499,-5.56463630721829,
132.815020541792));
#169425=CARTESIAN_POINT('Ctrl Pts',(-149.401731037891,-5.62252061607184,
132.654821831516));
#169426=CARTESIAN_POINT('Ctrl Pts',(-149.393698688284,-5.67354521648552,
132.491947762961));
#169427=CARTESIAN_POINT('Ctrl Pts',(-149.385666338676,-5.71747147437235,
132.327006506221));
#169428=CARTESIAN_POINT('Ctrl Pts',(-149.377943353434,-5.75970592107237,
132.168417929558));
#169429=CARTESIAN_POINT('Ctrl Pts',(-149.370220368192,-5.7953784543159,
132.00791877723));
#169430=CARTESIAN_POINT('Ctrl Pts',(-149.362497382951,-5.82432596352126,
131.846069613952));
#169431=CARTESIAN_POINT('Ctrl Pts',(-149.354782943143,-5.85324144249298,
131.684399535738));
#169432=CARTESIAN_POINT('Ctrl Pts',(-149.347068503335,-5.87544666835424,
131.52138274165));
#169433=CARTESIAN_POINT('Ctrl Pts',(-149.339354063527,-5.89082885337101,
131.357592922111));
#169434=CARTESIAN_POINT('Ctrl Pts',(-149.331649592881,-5.90619116040465,
131.194014763741));
#169435=CARTESIAN_POINT('Ctrl Pts',(-149.323945122236,-5.91474797918278,
131.029665894648));
#169436=CARTESIAN_POINT('Ctrl Pts',(-149.316240651591,-5.91643793876513,
130.865128036802));
#169437=CARTESIAN_POINT('Ctrl Pts',(-149.315285498462,-5.91664744961356,
130.844729639967));
#169438=CARTESIAN_POINT('Ctrl Pts',(-149.314330345334,-5.9167514851978,
130.824328347825));
#169439=CARTESIAN_POINT('Ctrl Pts',(-149.313375192206,-5.91674998398426,
130.803925276003));
#169440=CARTESIAN_POINT('',(-147.563375192206,-5.91701416015386,130.799054768139));
#169441=CARTESIAN_POINT('Ctrl Pts',(-149.313375192165,-5.9167499839842,
130.803925275142));
#169442=CARTESIAN_POINT('Ctrl Pts',(-149.305582974739,-5.91673773693701,
130.637475344648));
#169443=CARTESIAN_POINT('Ctrl Pts',(-149.297790757313,-5.90969735063202,
130.471177295381));
#169444=CARTESIAN_POINT('Ctrl Pts',(-149.289998539887,-5.8956928681459,
130.305626051896));
#169445=CARTESIAN_POINT('Ctrl Pts',(-149.282195001545,-5.88166803925994,
130.139834287436));
#169446=CARTESIAN_POINT('Ctrl Pts',(-149.274391463202,-5.86065894060254,
129.974791803421));
#169447=CARTESIAN_POINT('Ctrl Pts',(-149.26658792486,-5.8327810051871,129.8110850727));
#169448=CARTESIAN_POINT('Ctrl Pts',(-149.258764812563,-5.80483314233355,
129.646967709265));
#169449=CARTESIAN_POINT('Ctrl Pts',(-149.250941700266,-5.76998203666509,
129.484193106869));
#169450=CARTESIAN_POINT('Ctrl Pts',(-149.243118587969,-5.72839403677041,
129.323336538763));
#169451=CARTESIAN_POINT('Ctrl Pts',(-149.23528527844,-5.68675182795818,
129.162270298145));
#169452=CARTESIAN_POINT('Ctrl Pts',(-149.227451968912,-5.63835528362459,
129.003127379344));
#169453=CARTESIAN_POINT('Ctrl Pts',(-149.219618659384,-5.58341978017229,
128.846465288167));
#169454=CARTESIAN_POINT('Ctrl Pts',(-149.211766885304,-5.52835478363359,
128.689433915625));
#169455=CARTESIAN_POINT('Ctrl Pts',(-149.203915111225,-5.46672011538763,
128.534895355183));
#169456=CARTESIAN_POINT('Ctrl Pts',(-149.196063337145,-5.39877913040065,
128.383386750782));
#169457=CARTESIAN_POINT('Ctrl Pts',(-149.189990798919,-5.34623377896548,
128.266210456308));
#169458=CARTESIAN_POINT('Ctrl Pts',(-149.183918260694,-5.28991730978643,
128.150846052432));
#169459=CARTESIAN_POINT('Ctrl Pts',(-149.177845722469,-5.22996959741401,
128.037530559065));
#169460=CARTESIAN_POINT('Ctrl Pts',(-149.170422456063,-5.15668758208057,
127.899010048543));
#169461=CARTESIAN_POINT('Ctrl Pts',(-149.162999189657,-5.0777876918209,
127.763193501392));
#169462=CARTESIAN_POINT('Ctrl Pts',(-149.155575923252,-4.99349360203296,
127.630569161128));
#169463=CARTESIAN_POINT('Ctrl Pts',(-149.148161430531,-4.90929914085919,
127.498101571821));
#169464=CARTESIAN_POINT('Ctrl Pts',(-149.14074693781,-4.81972336890147,
127.368818991347));
#169465=CARTESIAN_POINT('Ctrl Pts',(-149.133332445089,-4.72503660349127,
127.243186701823));
#169466=CARTESIAN_POINT('Ctrl Pts',(-149.125925098735,-4.63044110075019,
127.117675501429));
#169467=CARTESIAN_POINT('Ctrl Pts',(-149.118517752381,-4.53074463475934,
126.995807883875));
#169468=CARTESIAN_POINT('Ctrl Pts',(-149.111110406027,-4.42626165672246,
126.878021570982));
#169469=CARTESIAN_POINT('Ctrl Pts',(-149.103708584351,-4.32185660603251,
126.760323107565));
#169470=CARTESIAN_POINT('Ctrl Pts',(-149.096306762676,-4.21267239822448,
126.646700165871));
#169471=CARTESIAN_POINT('Ctrl Pts',(-149.088904941,-4.09906465131535,126.537558589485));
#169472=CARTESIAN_POINT('Ctrl Pts',(-149.081507026689,-3.98551687705182,
126.428474628088));
#169473=CARTESIAN_POINT('Ctrl Pts',(-149.074109112378,-3.86755048277244,
126.323867578601));
#169474=CARTESIAN_POINT('Ctrl Pts',(-149.066711198066,-3.74555885884481,
126.224107415239));
#169475=CARTESIAN_POINT('Ctrl Pts',(-149.059314513154,-3.62358750771175,
126.124363830205));
#169476=CARTESIAN_POINT('Ctrl Pts',(-149.051917828242,-3.49759254323203,
126.029465768769));
#169477=CARTESIAN_POINT('Ctrl Pts',(-149.044521143329,-3.3680015291144,
125.939743853382));
#169478=CARTESIAN_POINT('Ctrl Pts',(-149.037124786394,-3.23841626119776,
125.850025916358));
#169479=CARTESIAN_POINT('Ctrl Pts',(-149.029728429458,-3.10523556760557,
125.765483881521));
#169480=CARTESIAN_POINT('Ctrl Pts',(-149.022332072523,-2.96891694456745,
125.68640568041));
#169481=CARTESIAN_POINT('Ctrl Pts',(-149.014934583186,-2.83257745080014,
125.607315372224));
#169482=CARTESIAN_POINT('Ctrl Pts',(-149.00753709385,-2.6930993939181,125.533690750727));
#169483=CARTESIAN_POINT('Ctrl Pts',(-149.000139604513,-2.55096573372212,
125.465774251507));
#169484=CARTESIAN_POINT('Ctrl Pts',(-148.992739521998,-2.4087822487921,
125.397833944263));
#169485=CARTESIAN_POINT('Ctrl Pts',(-148.985339439483,-2.26394164370845,
125.335605904064));
#169486=CARTESIAN_POINT('Ctrl Pts',(-148.977939356968,-2.11694760597834,
125.279284745142));
#169487=CARTESIAN_POINT('Ctrl Pts',(-148.970531137301,-1.96979193319219,
125.222901655316));
#169488=CARTESIAN_POINT('Ctrl Pts',(-148.963122917635,-1.82047844766713,
125.172438551798));
#169489=CARTESIAN_POINT('Ctrl Pts',(-148.955714697968,-1.66952747677182,
125.128040633033));
#169490=CARTESIAN_POINT('Ctrl Pts',(-148.948301918666,-1.51848359807267,
125.083615388091));
#169491=CARTESIAN_POINT('Ctrl Pts',(-148.940889139364,-1.365800586957,125.045262857144));
#169492=CARTESIAN_POINT('Ctrl Pts',(-148.933476360062,-1.2120092493786,
125.013077155161));
#169493=CARTESIAN_POINT('Ctrl Pts',(-148.926052989033,-1.05799816752519,
124.980845464738));
#169494=CARTESIAN_POINT('Ctrl Pts',(-148.918629618004,-0.902875963515867,
124.954798263382));
#169495=CARTESIAN_POINT('Ctrl Pts',(-148.911206246975,-0.747179679008069,
124.934977933691));
#169496=CARTESIAN_POINT('Ctrl Pts',(-148.907270197536,-0.664625773109596,
124.924468719309));
#169497=CARTESIAN_POINT('Ctrl Pts',(-148.903334148097,-0.581910504076674,
124.915709231308));
#169498=CARTESIAN_POINT('Ctrl Pts',(-148.899398098657,-0.499113827592994,
124.908699844624));
#169499=CARTESIAN_POINT('Ctrl Pts',(-148.891974832252,-0.342961879688421,
124.89548036009));
#169500=CARTESIAN_POINT('Ctrl Pts',(-148.884551565846,-0.186048254126534,
124.888448911088));
#169501=CARTESIAN_POINT('Ctrl Pts',(-148.877128299441,-0.0289046260206381,
124.887681220717));
#169502=CARTESIAN_POINT('Ctrl Pts',(-148.86971380672,0.12805327136725,124.886914437692));
#169503=CARTESIAN_POINT('Ctrl Pts',(-148.862299313999,0.285240260544175,
124.892396678909));
#169504=CARTESIAN_POINT('Ctrl Pts',(-148.854884821278,0.442118773367819,
124.90415201509));
#169505=CARTESIAN_POINT('Ctrl Pts',(-148.847477474924,0.598846080773985,
124.915896021035));
#169506=CARTESIAN_POINT('Ctrl Pts',(-148.84007012857,0.755265133979427,
124.933901057353));
#169507=CARTESIAN_POINT('Ctrl Pts',(-148.832662782216,0.910837696663221,
124.958139166677));
#169508=CARTESIAN_POINT('Ctrl Pts',(-148.825260960541,1.06629422746079,
124.982359198304));
#169509=CARTESIAN_POINT('Ctrl Pts',(-148.817859138866,1.22090515756829,
125.012802989209));
#169510=CARTESIAN_POINT('Ctrl Pts',(-148.81045731719,1.37413681905786,125.049390716254));
#169511=CARTESIAN_POINT('Ctrl Pts',(-148.803059402879,1.52728759074608,
125.085959128922));
#169512=CARTESIAN_POINT('Ctrl Pts',(-148.795661488567,1.67906018170088,
125.128664931993));
#169513=CARTESIAN_POINT('Ctrl Pts',(-148.788263574256,1.82893068503546,
125.17737713511));
#169514=CARTESIAN_POINT('Ctrl Pts',(-148.780866889344,1.97877628261109,
125.226081243142));
#169515=CARTESIAN_POINT('Ctrl Pts',(-148.773470204431,2.12672006524806,
125.2807896549));
#169516=CARTESIAN_POINT('Ctrl Pts',(-148.766073519519,2.2722527622858,125.341321358437));
#169517=CARTESIAN_POINT('Ctrl Pts',(-148.758677162584,2.41777900625125,
125.401850377935));
#169518=CARTESIAN_POINT('Ctrl Pts',(-148.751280805648,2.56089403251859,
125.468202032442));
#169519=CARTESIAN_POINT('Ctrl Pts',(-148.743884448712,2.70110830824247,
125.540147051453));
#169520=CARTESIAN_POINT('Ctrl Pts',(-148.736486959376,2.84134405112992,
125.612103085431));
#169521=CARTESIAN_POINT('Ctrl Pts',(-148.729089470039,2.97867782703762,
125.689654018606));
#169522=CARTESIAN_POINT('Ctrl Pts',(-148.721691980703,3.1126446164693,125.77252456558));
#169523=CARTESIAN_POINT('Ctrl Pts',(-148.714291898188,3.24665836775153,
125.855424162696));
#169524=CARTESIAN_POINT('Ctrl Pts',(-148.706891815673,3.3773024653361,125.943646890118));
#169525=CARTESIAN_POINT('Ctrl Pts',(-148.699491733158,3.50414091935663,
126.036874175027));
#169526=CARTESIAN_POINT('Ctrl Pts',(-148.692083513491,3.63111884529648,
126.130203972921));
#169527=CARTESIAN_POINT('Ctrl Pts',(-148.684675293824,3.75428246958552,
126.228549096987));
#169528=CARTESIAN_POINT('Ctrl Pts',(-148.677267074158,3.87322838300728,
126.33155026438));
#169529=CARTESIAN_POINT('Ctrl Pts',(-148.669854294856,3.99224750565403,
126.434614827273));
#169530=CARTESIAN_POINT('Ctrl Pts',(-148.662441515554,4.10704347313671,
126.542340888941));
#169531=CARTESIAN_POINT('Ctrl Pts',(-148.655028736252,4.21725019028441,
126.654332738738));
#169532=CARTESIAN_POINT('Ctrl Pts',(-148.647605365223,4.3276143759579,126.766484607743));
#169533=CARTESIAN_POINT('Ctrl Pts',(-148.640181994194,4.43337596449143,
126.882914162692));
#169534=CARTESIAN_POINT('Ctrl Pts',(-148.632758623165,4.53420901407189,
127.003192484056));
#169535=CARTESIAN_POINT('Ctrl Pts',(-148.628822573725,4.58767311641224,
127.066966936079));
#169536=CARTESIAN_POINT('Ctrl Pts',(-148.624886524284,4.63975234510969,
127.131822917325));
#169537=CARTESIAN_POINT('Ctrl Pts',(-148.620950474843,4.69040316671737,
127.197693361477));
#169538=CARTESIAN_POINT('Ctrl Pts',(-148.613527208438,4.78592903551642,
127.321922963407));
#169539=CARTESIAN_POINT('Ctrl Pts',(-148.606103942032,4.87666044014705,
127.450138170678));
#169540=CARTESIAN_POINT('Ctrl Pts',(-148.598680675627,4.96224628923592,
127.581932600144));
#169541=CARTESIAN_POINT('Ctrl Pts',(-148.591266182906,5.04773098295863,
127.71357125954));
#169542=CARTESIAN_POINT('Ctrl Pts',(-148.583851690185,5.12808202531325,
127.848780410589));
#169543=CARTESIAN_POINT('Ctrl Pts',(-148.576437197464,5.20298859620775,
127.987120792803));
#169544=CARTESIAN_POINT('Ctrl Pts',(-148.56902985111,5.27782296932904,128.125327837348));
#169545=CARTESIAN_POINT('Ctrl Pts',(-148.561622504757,5.34722314135069,
128.266659778754));
#169546=CARTESIAN_POINT('Ctrl Pts',(-148.554215158403,5.4109217037192,128.410648671922));
#169547=CARTESIAN_POINT('Ctrl Pts',(-148.546813336727,5.47457275729669,
128.55453017274));
#169548=CARTESIAN_POINT('Ctrl Pts',(-148.539411515052,5.5325305181004,128.701064339663));
#169549=CARTESIAN_POINT('Ctrl Pts',(-148.532009693377,5.58457368304614,
128.849759036392));
#169550=CARTESIAN_POINT('Ctrl Pts',(-148.524611779065,5.63658937481022,
128.998375238348));
#169551=CARTESIAN_POINT('Ctrl Pts',(-148.517213864754,5.68269656585787,
129.149149347248));
#169552=CARTESIAN_POINT('Ctrl Pts',(-148.509815950443,5.72272227761775,
129.301569781901));
#169553=CARTESIAN_POINT('Ctrl Pts',(-148.502419265531,5.76274133783043,
129.453964887044));
#169554=CARTESIAN_POINT('Ctrl Pts',(-148.495022580618,5.79668082983904,
129.608005414244));
#169555=CARTESIAN_POINT('Ctrl Pts',(-148.487625895706,5.82441777088901,
129.763165058292));
#169556=CARTESIAN_POINT('Ctrl Pts',(-148.480229538771,5.85215348205395,
129.918317822399));
#169557=CARTESIAN_POINT('Ctrl Pts',(-148.472833181835,5.87368712341728,
130.074589237215));
#169558=CARTESIAN_POINT('Ctrl Pts',(-148.4654368249,5.88894698228776,130.231443518586));
#169559=CARTESIAN_POINT('Ctrl Pts',(-148.458039335563,5.90420917748159,
130.388321814747));
#169560=CARTESIAN_POINT('Ctrl Pts',(-148.450641846227,5.91319564148672,
130.545782783581));
#169561=CARTESIAN_POINT('Ctrl Pts',(-148.44324435689,5.91588662531099,130.70328639253));
#169562=CARTESIAN_POINT('Ctrl Pts',(-148.435844274375,5.91857855245547,
130.860845214126));
#169563=CARTESIAN_POINT('Ctrl Pts',(-148.42844419186,5.91497059918249,131.018446332588));
#169564=CARTESIAN_POINT('Ctrl Pts',(-148.421044109345,5.90509512665435,
131.175550740903));
#169565=CARTESIAN_POINT('Ctrl Pts',(-148.413635889679,5.89520879502896,
131.332827901666));
#169566=CARTESIAN_POINT('Ctrl Pts',(-148.406227670013,5.87904120424122,
131.489606888725));
#169567=CARTESIAN_POINT('Ctrl Pts',(-148.398819450346,5.8566765765891,131.645354101329));
#169568=CARTESIAN_POINT('Ctrl Pts',(-148.391406671044,5.83429818388178,
131.801197173744));
#169569=CARTESIAN_POINT('Ctrl Pts',(-148.383993891742,5.80571522171299,
131.956006840065));
#169570=CARTESIAN_POINT('Ctrl Pts',(-148.37658111244,5.771062729272,132.109261202786));
#169571=CARTESIAN_POINT('Ctrl Pts',(-148.369157741411,5.73636072372482,
132.262734542528));
#169572=CARTESIAN_POINT('Ctrl Pts',(-148.361734370383,5.69557196366407,
132.414647780684));
#169573=CARTESIAN_POINT('Ctrl Pts',(-148.354310999354,5.64888113172408,
132.564494851695));
#169574=CARTESIAN_POINT('Ctrl Pts',(-148.350374949913,5.62412453229683,
132.643947364281));
#169575=CARTESIAN_POINT('Ctrl Pts',(-148.346438900472,5.59770945367184,
132.722819336412));
#169576=CARTESIAN_POINT('Ctrl Pts',(-148.342502851031,5.56966878975008,
132.801037891184));
#169577=CARTESIAN_POINT('Ctrl Pts',(-148.335079584625,5.51678497271598,
132.948555644358));
#169578=CARTESIAN_POINT('Ctrl Pts',(-148.32765631822,5.45795642803586,133.094193996082));
#169579=CARTESIAN_POINT('Ctrl Pts',(-148.320233051815,5.39333528389671,
133.237437903222));
#169580=CARTESIAN_POINT('Ctrl Pts',(-148.312818559094,5.32879051658329,
133.38051250796));
#169581=CARTESIAN_POINT('Ctrl Pts',(-148.305404066372,5.25846692955907,
133.521197964362));
#169582=CARTESIAN_POINT('Ctrl Pts',(-148.297989573651,5.18256607926244,
133.658995339659));
#169583=CARTESIAN_POINT('Ctrl Pts',(-148.290582227298,5.10673838506294,
133.796659900657));
#169584=CARTESIAN_POINT('Ctrl Pts',(-148.283174880944,5.02534430819991,
133.931441597449));
#169585=CARTESIAN_POINT('Ctrl Pts',(-148.27576753459,4.93863300328432,134.062862515888));
#169586=CARTESIAN_POINT('Ctrl Pts',(-148.268365712915,4.85198637093111,
134.194185415649));
#169587=CARTESIAN_POINT('Ctrl Pts',(-148.260963891239,4.76003061164661,
134.322152217781));
#169588=CARTESIAN_POINT('Ctrl Pts',(-148.253562069564,4.66306015391342,
134.446310722041));
#169589=CARTESIAN_POINT('Ctrl Pts',(-148.246164155252,4.56614088613032,
134.570403683993));
#169590=CARTESIAN_POINT('Ctrl Pts',(-148.238766240941,4.46421242115982,
134.690692058368));
#169591=CARTESIAN_POINT('Ctrl Pts',(-148.23136832663,4.35761166760262,134.806753791265));
#169592=CARTESIAN_POINT('Ctrl Pts',(-148.223971641717,4.25102862915689,
134.922796236808));
#169593=CARTESIAN_POINT('Ctrl Pts',(-148.216574956805,4.13977509541776,
135.034613160252));
#169594=CARTESIAN_POINT('Ctrl Pts',(-148.209178271893,4.02422738668002,
135.141816611901));
#169595=CARTESIAN_POINT('Ctrl Pts',(-148.201781914958,3.90868480144878,
135.249015310037));
#169596=CARTESIAN_POINT('Ctrl Pts',(-148.194385558022,3.78884869347208,
135.351600689231));
#169597=CARTESIAN_POINT('Ctrl Pts',(-148.186989201087,3.66513107067269,
135.44922281114));
#169598=CARTESIAN_POINT('Ctrl Pts',(-148.17959171175,3.54139450638942,135.546859879245));
#169599=CARTESIAN_POINT('Ctrl Pts',(-148.172194222414,3.41377553708434,
135.639531945775));
#169600=CARTESIAN_POINT('Ctrl Pts',(-148.164796733077,3.2827178326284,135.726930494555));
#169601=CARTESIAN_POINT('Ctrl Pts',(-148.157396650562,3.15161418609714,
135.814359680762));
#169602=CARTESIAN_POINT('Ctrl Pts',(-148.149996568047,3.01706971476592,
135.896511461641));
#169603=CARTESIAN_POINT('Ctrl Pts',(-148.142596485532,2.87955539249854,
135.973121717098));
#169604=CARTESIAN_POINT('Ctrl Pts',(-148.135188265865,2.7418898590968,136.049816213406));
#169605=CARTESIAN_POINT('Ctrl Pts',(-148.127780046199,2.60124827933473,
136.120956833432));
#169606=CARTESIAN_POINT('Ctrl Pts',(-148.120371826532,2.45812511084739,
136.186326011539));
#169607=CARTESIAN_POINT('Ctrl Pts',(-148.11295904723,2.314913852438,136.251735423284));
#169608=CARTESIAN_POINT('Ctrl Pts',(-148.105546267928,2.16921830649471,
136.311366173782));
#169609=CARTESIAN_POINT('Ctrl Pts',(-148.098133488626,2.0215505521491,136.365049776978));
#169610=CARTESIAN_POINT('Ctrl Pts',(-148.090710117598,1.87367180319136,
136.418810085824));
#169611=CARTESIAN_POINT('Ctrl Pts',(-148.083286746569,1.72381557238988,
136.466606162698));
#169612=CARTESIAN_POINT('Ctrl Pts',(-148.07586337554,1.57250745250771,136.508319845533));
#169613=CARTESIAN_POINT('Ctrl Pts',(-148.071927326099,1.49228025675812,
136.530437441078));
#169614=CARTESIAN_POINT('Ctrl Pts',(-148.067991276658,1.41164503761781,
136.550845914807));
#169615=CARTESIAN_POINT('Ctrl Pts',(-148.064055227218,1.33068088844758,
136.569533549545));
#169616=CARTESIAN_POINT('Ctrl Pts',(-148.056631960812,1.17798502991737,
136.604777845438));
#169617=CARTESIAN_POINT('Ctrl Pts',(-148.049208694407,1.02365709455418,
136.634004811209));
#169618=CARTESIAN_POINT('Ctrl Pts',(-148.041785428002,0.868212631733326,
136.657064043215));
#169619=CARTESIAN_POINT('Ctrl Pts',(-148.034370935281,0.712951891358672,
136.680096021123));
#169620=CARTESIAN_POINT('Ctrl Pts',(-148.02695644256,0.556577615933735,
136.696974721311));
#169621=CARTESIAN_POINT('Ctrl Pts',(-148.019541949839,0.399618517907053,
136.707600033569));
#169622=CARTESIAN_POINT('Ctrl Pts',(-148.012134603485,0.242810702968456,
136.71821510475));
#169623=CARTESIAN_POINT('Ctrl Pts',(-148.004727257131,0.0854195575373565,
136.722588762027));
#169624=CARTESIAN_POINT('Ctrl Pts',(-147.997319910777,-0.0720181615264252,
136.720672301961));
#169625=CARTESIAN_POINT('Ctrl Pts',(-147.989918089102,-0.229338457599992,
136.718757271263));
#169626=CARTESIAN_POINT('Ctrl Pts',(-147.982516267427,-0.386704886477705,
136.71056146897));
#169627=CARTESIAN_POINT('Ctrl Pts',(-147.975114445751,-0.543577853502071,
136.696088180826));
#169628=CARTESIAN_POINT('Ctrl Pts',(-147.96771653144,-0.700368008508242,
136.681622533019));
#169629=CARTESIAN_POINT('Ctrl Pts',(-147.960318617129,-0.856664849670433,
136.660886033232));
#169630=CARTESIAN_POINT('Ctrl Pts',(-147.952920702817,-1.01193118376104,
136.633934001771));
#169631=CARTESIAN_POINT('Ctrl Pts',(-147.945524017905,-1.16717171540351,
136.606986449249));
#169632=CARTESIAN_POINT('Ctrl Pts',(-147.938127332993,-1.32138171242044,
136.573825478853));
#169633=CARTESIAN_POINT('Ctrl Pts',(-147.930730648081,-1.47403137143431,
136.534558003218));
#169634=CARTESIAN_POINT('Ctrl Pts',(-147.923334291145,-1.62667426180234,
136.495292268743));
#169635=CARTESIAN_POINT('Ctrl Pts',(-147.91593793421,-1.77775659020682,
136.44992066041));
#169636=CARTESIAN_POINT('Ctrl Pts',(-147.908541577275,-1.92676124326431,
136.398600661929));
#169637=CARTESIAN_POINT('Ctrl Pts',(-147.901144087938,-2.07578870931458,
136.347272806226));
#169638=CARTESIAN_POINT('Ctrl Pts',(-147.893746598602,-2.22273751367075,
136.289994868594));
#169639=CARTESIAN_POINT('Ctrl Pts',(-147.886349109265,-2.36710827853568,
136.226973360533));
#169640=CARTESIAN_POINT('Ctrl Pts',(-147.87894902675,-2.51152965234864,
136.16392976038));
#169641=CARTESIAN_POINT('Ctrl Pts',(-147.871548944235,-2.65337084544653,
136.095138730387));
#169642=CARTESIAN_POINT('Ctrl Pts',(-147.86414886172,-2.79215507323656,
136.02085375084));
#169643=CARTESIAN_POINT('Ctrl Pts',(-147.856740642054,-2.93109190855221,
135.946487087322));
#169644=CARTESIAN_POINT('Ctrl Pts',(-147.849332422388,-3.06696473620898,
135.866614585924));
#169645=CARTESIAN_POINT('Ctrl Pts',(-147.841924202721,-3.19932324564573,
135.781534648316));
#169646=CARTESIAN_POINT('Ctrl Pts',(-147.834511423419,-3.3317632195369,
135.696402345426));
#169647=CARTESIAN_POINT('Ctrl Pts',(-147.827098644117,-3.46068426015495,
135.606056433519));
#169648=CARTESIAN_POINT('Ctrl Pts',(-147.819685864815,-3.58566782413148,
135.510836668444));
#169649=CARTESIAN_POINT('Ctrl Pts',(-147.812262493786,-3.71082997048519,
135.415480848903));
#169650=CARTESIAN_POINT('Ctrl Pts',(-147.804839122758,-3.83204311680381,
135.315237504817));
#169651=CARTESIAN_POINT('Ctrl Pts',(-147.797415751729,-3.94892375426819,
135.210484962779));
#169652=CARTESIAN_POINT('Ctrl Pts',(-147.793479702288,-4.01089667277319,
135.154942651479));
#169653=CARTESIAN_POINT('Ctrl Pts',(-147.789543652846,-4.07165220529871,
135.098133236456));
#169654=CARTESIAN_POINT('Ctrl Pts',(-147.785607603405,-4.13113774195879,
135.040116927774));
#169655=CARTESIAN_POINT('Ctrl Pts',(-147.778290858419,-4.24171574881784,
134.932270077268));
#169656=CARTESIAN_POINT('Ctrl Pts',(-147.770974113432,-4.34825821180401,
134.819904157256));
#169657=CARTESIAN_POINT('Ctrl Pts',(-147.763657368446,-4.45036514945744,
134.703358001381));
#169658=CARTESIAN_POINT('Ctrl Pts',(-147.756349411285,-4.55234945089338,
134.586951824042));
#169659=CARTESIAN_POINT('Ctrl Pts',(-147.749041454124,-4.64990857515767,
134.466375686573));
#169660=CARTESIAN_POINT('Ctrl Pts',(-147.741733496963,-4.74267725621687,
134.342007152462));
#169661=CARTESIAN_POINT('Ctrl Pts',(-147.734301900931,-4.83701543401553,
134.215534502969));
#169662=CARTESIAN_POINT('Ctrl Pts',(-147.7268703049,-4.92639929930953,134.085140227386));
#169663=CARTESIAN_POINT('Ctrl Pts',(-147.719438708868,-5.01048467166432,
133.951259713107));
#169664=CARTESIAN_POINT('Ctrl Pts',(-147.712143701413,-5.09302460192625,
133.819839847766));
#169665=CARTESIAN_POINT('Ctrl Pts',(-147.704848693958,-5.17045889754112,
133.685061122964));
#169666=CARTESIAN_POINT('Ctrl Pts',(-147.697553686503,-5.24250370133411,
133.547367271586));
#169667=CARTESIAN_POINT('Ctrl Pts',(-147.690261763559,-5.31451804279654,
133.409731640585));
#169668=CARTESIAN_POINT('Ctrl Pts',(-147.682969840614,-5.38114724798181,
133.269183675585));
#169669=CARTESIAN_POINT('Ctrl Pts',(-147.675677917669,-5.44215242935071,
133.126193406165));
#169670=CARTESIAN_POINT('Ctrl Pts',(-147.668387541704,-5.50314466848771,
132.98323347209));
#169671=CARTESIAN_POINT('Ctrl Pts',(-147.661097165738,-5.55851510777398,
132.83783261877));
#169672=CARTESIAN_POINT('Ctrl Pts',(-147.653806789773,-5.60807233973095,
132.690482351401));
#169673=CARTESIAN_POINT('Ctrl Pts',(-147.646270823309,-5.65929900346469,
132.538168303591));
#169674=CARTESIAN_POINT('Ctrl Pts',(-147.638734856845,-5.70431376762358,
132.383771600791));
#169675=CARTESIAN_POINT('Ctrl Pts',(-147.631198890381,-5.74296078845821,
132.227853485385));
#169676=CARTESIAN_POINT('Ctrl Pts',(-147.623904542744,-5.78036870507304,
132.076934430465));
#169677=CARTESIAN_POINT('Ctrl Pts',(-147.616610195108,-5.81181086636718,
131.924590415814));
#169678=CARTESIAN_POINT('Ctrl Pts',(-147.609315847471,-5.83719786223342,
131.771341320392));
#169679=CARTESIAN_POINT('Ctrl Pts',(-147.601659071593,-5.86384624084512,
131.610477863438));
#169680=CARTESIAN_POINT('Ctrl Pts',(-147.594002295716,-5.88382227129655,
131.448617561023));
#169681=CARTESIAN_POINT('Ctrl Pts',(-147.586345519838,-5.8970840217172,
131.286367467422));
#169682=CARTESIAN_POINT('Ctrl Pts',(-147.578688743961,-5.91034577213782,
131.124117373821));
#169683=CARTESIAN_POINT('Ctrl Pts',(-147.571031968084,-5.91689326760382,
130.961477977213));
#169684=CARTESIAN_POINT('Ctrl Pts',(-147.563375192206,-5.91674762120188,
130.799055007147));
#169685=CARTESIAN_POINT('',(-145.813375192206,-5.92480979664972,130.807250319294));
#169686=CARTESIAN_POINT('Ctrl Pts',(-147.563375192206,-5.9186030338184,
130.799053343379));
#169687=CARTESIAN_POINT('Ctrl Pts',(-147.544636788001,-5.92229012192935,
130.401427829348));
#169688=CARTESIAN_POINT('Ctrl Pts',(-147.525898383797,-5.88565898036021,
130.00447795396));
#169689=CARTESIAN_POINT('Ctrl Pts',(-147.414344104987,-5.41278022280702,
127.693477101972));
#169690=CARTESIAN_POINT('Ctrl Pts',(-147.228712355779,-2.52567537098746,
124.277606106268));
#169691=CARTESIAN_POINT('Ctrl Pts',(-146.950264731965,4.12595418657829,
125.151568158913));
#169692=CARTESIAN_POINT('Ctrl Pts',(-146.671817108153,6.98603341074523,
131.220170326794));
#169693=CARTESIAN_POINT('Ctrl Pts',(-146.39336948434,3.42628921714421,136.906663685328));
#169694=CARTESIAN_POINT('Ctrl Pts',(-146.114921860528,-3.2820473834807,
136.985438638666));
#169695=CARTESIAN_POINT('Ctrl Pts',(-145.921590429816,-5.84567763105308,
133.09632707134));
#169696=CARTESIAN_POINT('Ctrl Pts',(-145.821074873709,-5.92578672622296,
130.970191063743));
#169697=CARTESIAN_POINT('Ctrl Pts',(-145.813375192206,-5.92480979664972,
130.807250319294));
#169698=CARTESIAN_POINT('',(-144.063375192206,-5.90966590561723,130.808266582045));
#169699=CARTESIAN_POINT('Ctrl Pts',(-145.813375192206,-5.92480979664972,
130.807250319294));
#169700=CARTESIAN_POINT('Ctrl Pts',(-145.728258999105,-5.9140103205709,
129.00602050689));
#169701=CARTESIAN_POINT('Ctrl Pts',(-145.550326931398,-4.07424408851649,
125.221534978211));
#169702=CARTESIAN_POINT('Ctrl Pts',(-145.279578989089,2.37171472213127,
124.220096816113));
#169703=CARTESIAN_POINT('Ctrl Pts',(-145.001131365275,6.82149735186778,
129.240795969467));
#169704=CARTESIAN_POINT('Ctrl Pts',(-144.722683741463,5.00265716391772,
135.698334650054));
#169705=CARTESIAN_POINT('Ctrl Pts',(-144.44423611765,-1.41338056428836,
137.658550278703));
#169706=CARTESIAN_POINT('Ctrl Pts',(-144.22446660123,-5.45222549990329,
134.234355068096));
#169707=CARTESIAN_POINT('Ctrl Pts',(-144.097512959417,-5.91405090638656,
131.535446847972));
#169708=CARTESIAN_POINT('Ctrl Pts',(-144.063375192206,-5.90966590561723,
130.808266582045));
#169709=CARTESIAN_POINT('',(-142.313375175084,-5.91365185916051,130.800007985964));
#169710=CARTESIAN_POINT('Ctrl Pts',(-144.063375192206,-5.90966590561723,
130.808266582045));
#169711=CARTESIAN_POINT('Ctrl Pts',(-144.004697084812,-5.90212869486523,
129.558344128823));
#169712=CARTESIAN_POINT('Ctrl Pts',(-143.853203102813,-4.90196159472372,
126.320294665178));
#169713=CARTESIAN_POINT('Ctrl Pts',(-143.608893246212,0.426440781348736,
123.818968088136));
#169714=CARTESIAN_POINT('Ctrl Pts',(-143.330445622398,6.10751023032449,
127.387362034476));
#169715=CARTESIAN_POINT('Ctrl Pts',(-143.051997998586,6.17607614610116,
134.095810749031));
#169716=CARTESIAN_POINT('Ctrl Pts',(-142.773550374773,0.569129801701234,
137.77957758904));
#169717=CARTESIAN_POINT('Ctrl Pts',(-142.527342772645,-4.85106370396208,
135.369103867334));
#169718=CARTESIAN_POINT('Ctrl Pts',(-142.373951045124,-5.90178250636266,
132.089885314399));
#169719=CARTESIAN_POINT('Ctrl Pts',(-142.313375192206,-5.9105277485179,
130.80001065018));
#169720=CARTESIAN_POINT('',(-140.563375192206,-5.92111884170449,130.80212814766));
#169721=CARTESIAN_POINT('Ctrl Pts',(-142.313375158114,-5.91674839705925,
130.800005345262));
#169722=CARTESIAN_POINT('Ctrl Pts',(-142.304860995865,-5.91661480626093,
130.618518841854));
#169723=CARTESIAN_POINT('Ctrl Pts',(-142.296346833615,-5.90812709802129,
130.437370762715));
#169724=CARTESIAN_POINT('Ctrl Pts',(-142.287832671366,-5.89140221138,130.257267804374));
#169725=CARTESIAN_POINT('Ctrl Pts',(-142.279276745037,-5.8745952850168,
130.0762813963));
#169726=CARTESIAN_POINT('Ctrl Pts',(-142.270720818708,-5.84947027717438,
129.896350514552));
#169727=CARTESIAN_POINT('Ctrl Pts',(-142.262164892379,-5.81619531024774,
129.718173398182));
#169728=CARTESIAN_POINT('Ctrl Pts',(-142.253554344712,-5.782707914749,129.538858792766));
#169729=CARTESIAN_POINT('Ctrl Pts',(-142.244943797045,-5.74096625036584,
129.361320542769));
#169730=CARTESIAN_POINT('Ctrl Pts',(-142.236333249378,-5.69119024460289,
129.186249322804));
#169731=CARTESIAN_POINT('Ctrl Pts',(-142.229773875301,-5.65327169929296,
129.052882937033));
#169732=CARTESIAN_POINT('Ctrl Pts',(-142.223214501224,-5.6106917110202,
128.920947786416));
#169733=CARTESIAN_POINT('Ctrl Pts',(-142.216655127147,-5.56356579263376,
128.790740436515));
#169734=CARTESIAN_POINT('Ctrl Pts',(-142.209231860741,-5.51023322725657,
128.643384326779));
#169735=CARTESIAN_POINT('Ctrl Pts',(-142.201808594336,-5.45096168202031,
128.497925703494));
#169736=CARTESIAN_POINT('Ctrl Pts',(-142.19438532793,-5.38590485202148,
128.354879144382));
#169737=CARTESIAN_POINT('Ctrl Pts',(-142.186970835209,-5.32092491379289,
128.212001654423));
#169738=CARTESIAN_POINT('Ctrl Pts',(-142.179556342488,-5.25017345436617,
128.071530890473));
#169739=CARTESIAN_POINT('Ctrl Pts',(-142.172141849767,-5.17385354782587,
127.933965169522));
#169740=CARTESIAN_POINT('Ctrl Pts',(-142.164734503413,-5.09760720128489,
127.796532039593));
#169741=CARTESIAN_POINT('Ctrl Pts',(-142.157327157059,-5.01580327231036,
127.661998702671));
#169742=CARTESIAN_POINT('Ctrl Pts',(-142.149919810705,-4.92869236896547,
127.530842312347));
#169743=CARTESIAN_POINT('Ctrl Pts',(-142.14251798903,-4.84164643621855,
127.399783743408));
#169744=CARTESIAN_POINT('Ctrl Pts',(-142.135116167354,-4.74930161593849,
127.272097415708));
#169745=CARTESIAN_POINT('Ctrl Pts',(-142.127714345679,-4.65195371158615,
127.148234631258));
#169746=CARTESIAN_POINT('Ctrl Pts',(-142.120316431368,-4.55465719643503,
127.024437233007));
#169747=CARTESIAN_POINT('Ctrl Pts',(-142.112918517056,-4.45236308715456,
126.904459650984));
#169748=CARTESIAN_POINT('Ctrl Pts',(-142.105520602745,-4.34540957537183,
126.788722911701));
#169749=CARTESIAN_POINT('Ctrl Pts',(-142.098123917832,-4.23847383732228,
126.673005405764));
#169750=CARTESIAN_POINT('Ctrl Pts',(-142.09072723292,-4.12688048664842,
126.561527617734));
#169751=CARTESIAN_POINT('Ctrl Pts',(-142.083330548008,-4.0110070226874,
126.454676350122));
#169752=CARTESIAN_POINT('Ctrl Pts',(-142.075934191072,-3.8951386966772,
126.347829820406));
#169753=CARTESIAN_POINT('Ctrl Pts',(-142.068537834137,-3.77499090916475,
126.245609656272));
#169754=CARTESIAN_POINT('Ctrl Pts',(-142.061141477201,-3.65097673125637,
126.148364540428));
#169755=CARTESIAN_POINT('Ctrl Pts',(-142.053743987864,-3.52694356646076,
126.051104536109));
#169756=CARTESIAN_POINT('Ctrl Pts',(-142.046346498528,-3.39904312638324,
125.958821327073));
#169757=CARTESIAN_POINT('Ctrl Pts',(-142.038949009191,-3.26772001785685,
125.871822077686));
#169758=CARTESIAN_POINT('Ctrl Pts',(-142.031548926676,-3.13635087421852,
125.784792330848));
#169759=CARTESIAN_POINT('Ctrl Pts',(-142.024148844161,-3.00155698432438,
125.70305043758));
#169760=CARTESIAN_POINT('Ctrl Pts',(-142.016748761646,-2.86381012374739,
125.626859083271));
#169761=CARTESIAN_POINT('Ctrl Pts',(-142.009340541979,-2.72591179633629,
125.550583948736));
#169762=CARTESIAN_POINT('Ctrl Pts',(-142.001932322313,-2.58505434043865,
125.479871722819));
#169763=CARTESIAN_POINT('Ctrl Pts',(-141.994524102646,-2.44173287359424,
125.414938465191));
#169764=CARTESIAN_POINT('Ctrl Pts',(-141.987111323344,-2.29832319477843,
125.349965242227));
#169765=CARTESIAN_POINT('Ctrl Pts',(-141.979698544042,-2.15244682819286,
125.29077821506));
#169766=CARTESIAN_POINT('Ctrl Pts',(-141.97228576474,-2.00461636341079,
125.237544310372));
#169767=CARTESIAN_POINT('Ctrl Pts',(-141.964862393711,-1.85657467152787,
125.184234342584));
#169768=CARTESIAN_POINT('Ctrl Pts',(-141.957439022682,-1.7065736600313,
125.136894597918));
#169769=CARTESIAN_POINT('Ctrl Pts',(-141.950015651653,-1.55513927889432,
125.095641638168));
#169770=CARTESIAN_POINT('Ctrl Pts',(-141.946079602214,-1.4748451364164,
125.073768329062));
#169771=CARTESIAN_POINT('Ctrl Pts',(-141.942143552774,-1.3941481744168,
125.053605375738));
#169772=CARTESIAN_POINT('Ctrl Pts',(-141.938207503334,-1.31312752155294,
125.035164254584));
#169773=CARTESIAN_POINT('Ctrl Pts',(-141.930784236928,-1.16032509878548,
125.000384875608));
#169774=CARTESIAN_POINT('Ctrl Pts',(-141.923360970523,-1.00590892142774,
124.971627766364));
#169775=CARTESIAN_POINT('Ctrl Pts',(-141.915937704117,-0.850394994243977,
124.949041760641));
#169776=CARTESIAN_POINT('Ctrl Pts',(-141.908523211396,-0.695064871607517,
124.926482449701));
#169777=CARTESIAN_POINT('Ctrl Pts',(-141.901108718676,-0.538639947539334,
124.910079777198));
#169778=CARTESIAN_POINT('Ctrl Pts',(-141.893694225955,-0.381649236740049,
124.899932243659));
#169779=CARTESIAN_POINT('Ctrl Pts',(-141.886286879601,-0.224809839497981,
124.889794490695));
#169780=CARTESIAN_POINT('Ctrl Pts',(-141.878879533247,-0.067406111182322,
124.885899898183));
#169781=CARTESIAN_POINT('Ctrl Pts',(-141.871472186893,0.0900250455968013,
124.888295535633));
#169782=CARTESIAN_POINT('Ctrl Pts',(-141.864070365218,0.247338784279661,
124.890689386326));
#169783=CARTESIAN_POINT('Ctrl Pts',(-141.856668543542,0.404679539044736,
124.899364119935));
#169784=CARTESIAN_POINT('Ctrl Pts',(-141.849266721867,0.561507727734568,
124.91431480839));
#169785=CARTESIAN_POINT('Ctrl Pts',(-141.841868807556,0.718253128043891,
124.929257604492));
#169786=CARTESIAN_POINT('Ctrl Pts',(-141.834470893244,0.874486130477881,
124.95046972205));
#169787=CARTESIAN_POINT('Ctrl Pts',(-141.827072978933,1.02966971267315,
124.977894205983));
#169788=CARTESIAN_POINT('Ctrl Pts',(-141.819676294021,1.18482750617259,
125.005314132464));
#169789=CARTESIAN_POINT('Ctrl Pts',(-141.812279609108,1.33893585831316,
125.038944311447));
#169790=CARTESIAN_POINT('Ctrl Pts',(-141.804882924196,1.49146529357663,
125.078676218251));
#169791=CARTESIAN_POINT('Ctrl Pts',(-141.797486567261,1.6439879655251,125.118406363301));
#169792=CARTESIAN_POINT('Ctrl Pts',(-141.790090210325,1.79493149855872,
125.164237604115));
#169793=CARTESIAN_POINT('Ctrl Pts',(-141.78269385339,1.94377926101553,125.216010883794));
#169794=CARTESIAN_POINT('Ctrl Pts',(-141.775296364053,2.09264981244476,
125.267792090095));
#169795=CARTESIAN_POINT('Ctrl Pts',(-141.767898874717,2.23942360180544,
125.325517024033));
#169796=CARTESIAN_POINT('Ctrl Pts',(-141.76050138538,2.38360188216347,125.38897765513));
#169797=CARTESIAN_POINT('Ctrl Pts',(-141.753101302865,2.52783070399438,
125.452460532253));
#169798=CARTESIAN_POINT('Ctrl Pts',(-141.74570122035,2.669461863862,125.521682959412));
#169799=CARTESIAN_POINT('Ctrl Pts',(-141.738301137835,2.80801935088878,
125.596390006327));
#169800=CARTESIAN_POINT('Ctrl Pts',(-141.730892918169,2.9467291961164,125.671179201319));
#169801=CARTESIAN_POINT('Ctrl Pts',(-141.723484698502,3.08235829000079,
125.751464882904));
#169802=CARTESIAN_POINT('Ctrl Pts',(-141.716076478836,3.21445723229865,
125.836947280202));
#169803=CARTESIAN_POINT('Ctrl Pts',(-141.708663699534,3.34663747929169,
125.922482290489));
#169804=CARTESIAN_POINT('Ctrl Pts',(-141.701250920232,3.47528294087858,
126.013220175222));
#169805=CARTESIAN_POINT('Ctrl Pts',(-141.693838140929,3.5999761097295,126.108819906223));
#169806=CARTESIAN_POINT('Ctrl Pts',(-141.686414769901,3.72484744602743,
126.204556234603));
#169807=CARTESIAN_POINT('Ctrl Pts',(-141.678991398872,3.84575492463823,
126.305168045493));
#169808=CARTESIAN_POINT('Ctrl Pts',(-141.671568027843,3.96231619001513,
126.410275846781));
#169809=CARTESIAN_POINT('Ctrl Pts',(-141.667631978402,4.02411976976779,
126.466006525052));
#169810=CARTESIAN_POINT('Ctrl Pts',(-141.663695928961,4.08470211255227,
126.523000595873));
#169811=CARTESIAN_POINT('Ctrl Pts',(-141.659759879521,4.14401079198502,
126.581197689332));
#169812=CARTESIAN_POINT('Ctrl Pts',(-141.652336613115,4.25586511043332,
126.690955591325));
#169813=CARTESIAN_POINT('Ctrl Pts',(-141.64491334671,4.3635249965711,126.805326374652));
#169814=CARTESIAN_POINT('Ctrl Pts',(-141.637490080304,4.46658631913643,
126.923956358187));
#169815=CARTESIAN_POINT('Ctrl Pts',(-141.630075587583,4.56952583177748,
127.042446130935));
#169816=CARTESIAN_POINT('Ctrl Pts',(-141.622661094862,4.66787735705226,
127.165184804592));
#169817=CARTESIAN_POINT('Ctrl Pts',(-141.615246602141,4.76127207831011,
127.291780546051));
#169818=CARTESIAN_POINT('Ctrl Pts',(-141.607839255787,4.85457678221937,
127.418254269768));
#169819=CARTESIAN_POINT('Ctrl Pts',(-141.600431909434,4.94293397315485,
127.548577361921));
#169820=CARTESIAN_POINT('Ctrl Pts',(-141.59302456308,5.02601384122901,127.68232355336));
#169821=CARTESIAN_POINT('Ctrl Pts',(-141.585622741405,5.1090317452029,127.815969991843));
#169822=CARTESIAN_POINT('Ctrl Pts',(-141.578220919729,5.18677996734848,
127.953034130356));
#169823=CARTESIAN_POINT('Ctrl Pts',(-141.570819098054,5.25897099645432,
128.093059339406));
#169824=CARTESIAN_POINT('Ctrl Pts',(-141.563421183742,5.33112391647804,
128.233010630238));
#169825=CARTESIAN_POINT('Ctrl Pts',(-141.556023269431,5.39772531523721,
128.37591954761));
#169826=CARTESIAN_POINT('Ctrl Pts',(-141.54862535512,5.45853283694908,128.521303493785));
#169827=CARTESIAN_POINT('Ctrl Pts',(-141.541228670207,5.51933025355391,
128.666663279785));
#169828=CARTESIAN_POINT('Ctrl Pts',(-141.533831985295,5.57433556015751,
128.814496934219));
#169829=CARTESIAN_POINT('Ctrl Pts',(-141.526435300383,5.62335386719548,
128.964300334098));
#169830=CARTESIAN_POINT('Ctrl Pts',(-141.519038943448,5.67237000071036,
129.114097091537));
#169831=CARTESIAN_POINT('Ctrl Pts',(-141.511642586512,5.71539954641086,
129.265863065971));
#169832=CARTESIAN_POINT('Ctrl Pts',(-141.504246229577,5.75229707133786,
129.419077626413));
#169833=CARTESIAN_POINT('Ctrl Pts',(-141.49684874024,5.78920024537022,129.572315644396));
#169834=CARTESIAN_POINT('Ctrl Pts',(-141.489451250904,5.81996944189205,
129.727002327038));
#169835=CARTESIAN_POINT('Ctrl Pts',(-141.482053761567,5.84451009793547,
129.882605618865));
#169836=CARTESIAN_POINT('Ctrl Pts',(-141.474653679052,5.86905935666778,
130.038263457184));
#169837=CARTESIAN_POINT('Ctrl Pts',(-141.467253596537,5.88737566965912,
130.194838175915));
#169838=CARTESIAN_POINT('Ctrl Pts',(-141.459853514022,5.8994162214694,130.351791497581));
#169839=CARTESIAN_POINT('Ctrl Pts',(-141.452445294356,5.91147001310417,
130.508917405559));
#169840=CARTESIAN_POINT('Ctrl Pts',(-141.445037074689,5.9172342335473,130.666422375443));
#169841=CARTESIAN_POINT('Ctrl Pts',(-141.437628855023,5.91671817672114,
130.823766280598));
#169842=CARTESIAN_POINT('Ctrl Pts',(-141.430216075721,5.9162018022706,130.981207028302));
#169843=CARTESIAN_POINT('Ctrl Pts',(-141.422803296419,5.90939746434237,
131.138486141658));
#169844=CARTESIAN_POINT('Ctrl Pts',(-141.415390517117,5.8963664066898,131.295068025866));
#169845=CARTESIAN_POINT('Ctrl Pts',(-141.407967146088,5.88331672965098,
131.451873641612));
#169846=CARTESIAN_POINT('Ctrl Pts',(-141.400543775059,5.86402260919348,
131.607979669011));
#169847=CARTESIAN_POINT('Ctrl Pts',(-141.39312040403,5.83859665026538,131.762859296756));
#169848=CARTESIAN_POINT('Ctrl Pts',(-141.389184354589,5.82511519675411,
131.844980191673));
#169849=CARTESIAN_POINT('Ctrl Pts',(-141.385248305149,5.80991070689763,
131.926756519875));
#169850=CARTESIAN_POINT('Ctrl Pts',(-141.381312255708,5.79300563387162,
132.008111542148));
#169851=CARTESIAN_POINT('Ctrl Pts',(-141.373888989303,5.76112319373395,
132.161544575151));
#169852=CARTESIAN_POINT('Ctrl Pts',(-141.366465722897,5.72309261276887,
132.313942088495));
#169853=CARTESIAN_POINT('Ctrl Pts',(-141.359042456492,5.67899301010359,
132.464772901818));
#169854=CARTESIAN_POINT('Ctrl Pts',(-141.351627963771,5.63494552950641,
132.615425445645));
#169855=CARTESIAN_POINT('Ctrl Pts',(-141.34421347105,5.5848434089989,132.764514620489));
#169856=CARTESIAN_POINT('Ctrl Pts',(-141.336798978329,5.52881695446466,
132.911518335091));
#169857=CARTESIAN_POINT('Ctrl Pts',(-141.329391631975,5.47284450033665,
133.058380361978));
#169858=CARTESIAN_POINT('Ctrl Pts',(-141.321984285621,5.41095921191094,
133.203160583745));
#169859=CARTESIAN_POINT('Ctrl Pts',(-141.314576939267,5.34334145119713,
133.345351113105));
#169860=CARTESIAN_POINT('Ctrl Pts',(-141.307175117592,5.27577412236033,
133.487435591403));
#169861=CARTESIAN_POINT('Ctrl Pts',(-141.299773295917,5.20248299394662,
133.626933887483));
#169862=CARTESIAN_POINT('Ctrl Pts',(-141.292371474241,5.12369683444817,
133.763357290624));
#169863=CARTESIAN_POINT('Ctrl Pts',(-141.28497355993,5.04495226555005,133.899708676912));
#169864=CARTESIAN_POINT('Ctrl Pts',(-141.277575645619,4.9607186288334,134.032988080521));
#169865=CARTESIAN_POINT('Ctrl Pts',(-141.270177731307,4.87127094822071,
134.162730744803));
#169866=CARTESIAN_POINT('Ctrl Pts',(-141.262781046395,4.78183813218993,
134.292451848209));
#169867=CARTESIAN_POINT('Ctrl Pts',(-141.255384361483,4.68719320364637,
134.418637071745));
#169868=CARTESIAN_POINT('Ctrl Pts',(-141.247987676571,4.58765495296829,
134.540849958512));
#169869=CARTESIAN_POINT('Ctrl Pts',(-141.240591319635,4.48812111592056,
134.663057426232));
#169870=CARTESIAN_POINT('Ctrl Pts',(-141.2331949627,4.38369462389926,134.781292617962));
#169871=CARTESIAN_POINT('Ctrl Pts',(-141.225798605765,4.27473488843274,
134.895151763068));
#169872=CARTESIAN_POINT('Ctrl Pts',(-141.218401116428,4.16575847095225,
135.0090283403));
#169873=CARTESIAN_POINT('Ctrl Pts',(-141.211003627091,4.05224768618999,
135.118527267163));
#169874=CARTESIAN_POINT('Ctrl Pts',(-141.203606137755,3.93459905389209,
135.223281396174));
#169875=CARTESIAN_POINT('Ctrl Pts',(-141.19620605524,3.81690918004836,135.328072246582));
#169876=CARTESIAN_POINT('Ctrl Pts',(-141.188805972725,3.69507884932558,
135.428114739471));
#169877=CARTESIAN_POINT('Ctrl Pts',(-141.18140589021,3.56953778701891,135.523081900874));
#169878=CARTESIAN_POINT('Ctrl Pts',(-141.173997670543,3.44385867940884,
135.618153488433));
#169879=CARTESIAN_POINT('Ctrl Pts',(-141.166589450877,3.31446098942122,
135.708138373838));
#169880=CARTESIAN_POINT('Ctrl Pts',(-141.15918123121,3.1818041644834,135.792752424689));
#169881=CARTESIAN_POINT('Ctrl Pts',(-141.151768451908,3.04906569148296,
135.877418554077));
#169882=CARTESIAN_POINT('Ctrl Pts',(-141.144355672606,2.91306440818519,
135.956707074394));
#169883=CARTESIAN_POINT('Ctrl Pts',(-141.136942893304,2.7742840294092,136.030380009672));
#169884=CARTESIAN_POINT('Ctrl Pts',(-141.129519522275,2.63530535472006,
136.104158212294));
#169885=CARTESIAN_POINT('Ctrl Pts',(-141.122096151247,2.49353998932446,
136.172304643226));
#169886=CARTESIAN_POINT('Ctrl Pts',(-141.114672780218,2.34949202021907,
136.234629285821));
#169887=CARTESIAN_POINT('Ctrl Pts',(-141.110736730777,2.27311433061705,
136.267675306783));
#169888=CARTESIAN_POINT('Ctrl Pts',(-141.106800681336,2.19609519151904,
136.299085441743));
#169889=CARTESIAN_POINT('Ctrl Pts',(-141.102864631896,2.11851130228841,
136.328837101775));
#169890=CARTESIAN_POINT('Ctrl Pts',(-141.09544136549,1.97219050850881,136.384947804077));
#169891=CARTESIAN_POINT('Ctrl Pts',(-141.088018099085,1.823417706452,136.435326177708));
#169892=CARTESIAN_POINT('Ctrl Pts',(-141.08059483268,1.67268255902159,136.479751671867));
#169893=CARTESIAN_POINT('Ctrl Pts',(-141.073180339959,1.52212556801767,
136.524124658783));
#169894=CARTESIAN_POINT('Ctrl Pts',(-141.065765847238,1.3696112028514,136.562558666543));
#169895=CARTESIAN_POINT('Ctrl Pts',(-141.058351354517,1.21564914719937,
136.594881122099));
#169896=CARTESIAN_POINT('Ctrl Pts',(-141.050944008163,1.06183548597314,
136.627172424055));
#169897=CARTESIAN_POINT('Ctrl Pts',(-141.043536661809,0.906577274986908,
136.653363824539));
#169898=CARTESIAN_POINT('Ctrl Pts',(-141.036129315456,0.750399304271718,
136.673332541732));
#169899=CARTESIAN_POINT('Ctrl Pts',(-141.02872749378,0.594337816979347,
136.693286365502));
#169900=CARTESIAN_POINT('Ctrl Pts',(-141.021325672105,0.437358304549525,
136.707026699922));
#169901=CARTESIAN_POINT('Ctrl Pts',(-141.01392385043,0.279995588109698,
136.714481854321));
#169902=CARTESIAN_POINT('Ctrl Pts',(-141.006525936119,0.122715942222971,
136.721933073202));
#169903=CARTESIAN_POINT('Ctrl Pts',(-140.999128021807,-0.0349461328669095,
136.723105702193));
#169904=CARTESIAN_POINT('Ctrl Pts',(-140.991730107496,-0.192450967081312,
136.71797991439));
#169905=CARTESIAN_POINT('Ctrl Pts',(-140.984333422584,-0.349929626849472,
136.7128549784));
#169906=CARTESIAN_POINT('Ctrl Pts',(-140.976936737672,-0.507250724868555,
136.7014337151));
#169907=CARTESIAN_POINT('Ctrl Pts',(-140.96954005276,-0.663874743601535,
136.683748416249));
#169908=CARTESIAN_POINT('Ctrl Pts',(-140.962143695824,-0.820491817461393,
136.666063901584));
#169909=CARTESIAN_POINT('Ctrl Pts',(-140.954747338889,-0.976411502552809,
136.64211594552));
#169910=CARTESIAN_POINT('Ctrl Pts',(-140.947350981954,-1.13109982449628,
136.611988683268));
#169911=CARTESIAN_POINT('Ctrl Pts',(-140.939953492617,-1.28581182961674,
136.581856808454));
#169912=CARTESIAN_POINT('Ctrl Pts',(-140.932556003281,-1.43929172977447,
136.545543815072));
#169913=CARTESIAN_POINT('Ctrl Pts',(-140.925158513944,-1.59101630478494,
136.503184854232));
#169914=CARTESIAN_POINT('Ctrl Pts',(-140.917758431429,-1.74279406661019,
136.460811044523));
#169915=CARTESIAN_POINT('Ctrl Pts',(-140.910358348914,-1.89281491885331,
136.412387147954));
#169916=CARTESIAN_POINT('Ctrl Pts',(-140.902958266399,-2.04057149203691,
136.35809796717));
#169917=CARTESIAN_POINT('Ctrl Pts',(-140.895550046733,-2.18849053876267,
136.303749089851));
#169918=CARTESIAN_POINT('Ctrl Pts',(-140.888141827067,-2.33413998350985,
136.243522177097));
#169919=CARTESIAN_POINT('Ctrl Pts',(-140.8807336074,-2.47703243508653,136.177650194541));
#169920=CARTESIAN_POINT('Ctrl Pts',(-140.873320828098,-2.62001283458287,
136.111737668879));
#169921=CARTESIAN_POINT('Ctrl Pts',(-140.865908048796,-2.76023252793015,
136.040173319447));
#169922=CARTESIAN_POINT('Ctrl Pts',(-140.858495269494,-2.89722983953149,
135.9632354774));
#169923=CARTESIAN_POINT('Ctrl Pts',(-140.851071898466,-3.03442289931639,
135.886187702956));
#169924=CARTESIAN_POINT('Ctrl Pts',(-140.843648527437,-3.16838406447379,
135.803751296535));
#169925=CARTESIAN_POINT('Ctrl Pts',(-140.836225156408,-3.29868099728236,
135.716247652166));
#169926=CARTESIAN_POINT('Ctrl Pts',(-140.832289106967,-3.3677675575067,
135.669851120288));
#169927=CARTESIAN_POINT('Ctrl Pts',(-140.828353057525,-3.4358245196271,
135.622030682439));
#169928=CARTESIAN_POINT('Ctrl Pts',(-140.824417008083,-3.50279142106041,
135.572838658099));
#169929=CARTESIAN_POINT('Ctrl Pts',(-140.817061441009,-3.62793708869477,
135.48091012928));
#169930=CARTESIAN_POINT('Ctrl Pts',(-140.809705873935,-3.74966752560646,
135.383900102303));
#169931=CARTESIAN_POINT('Ctrl Pts',(-140.802350306861,-3.86753700508942,
135.282093087998));
#169932=CARTESIAN_POINT('Ctrl Pts',(-140.795003465457,-3.98526665985458,
135.180406844033));
#169933=CARTESIAN_POINT('Ctrl Pts',(-140.787656624052,-4.09914418577709,
135.073935182324));
#169934=CARTESIAN_POINT('Ctrl Pts',(-140.780309782647,-4.20875302359296,
134.963005655183));
#169935=CARTESIAN_POINT('Ctrl Pts',(-140.772969980566,-4.31825684047936,
134.852182414381));
#169936=CARTESIAN_POINT('Ctrl Pts',(-140.765630178486,-4.4234998433306,
134.736910077744));
#169937=CARTESIAN_POINT('Ctrl Pts',(-140.758290376405,-4.52409892771506,
134.6175560564));
#169938=CARTESIAN_POINT('Ctrl Pts',(-140.75095593373,-4.62462455626116,
134.49828918545));
#169939=CARTESIAN_POINT('Ctrl Pts',(-140.743621491055,-4.72051277178754,
134.374946852361));
#169940=CARTESIAN_POINT('Ctrl Pts',(-140.73628704838,-4.81141785660132,
134.247932712307));
#169941=CARTESIAN_POINT('Ctrl Pts',(-140.728955749256,-4.90228397938208,
134.120973010672));
#169942=CARTESIAN_POINT('Ctrl Pts',(-140.721624450132,-4.98817099931069,
133.990344941953));
#169943=CARTESIAN_POINT('Ctrl Pts',(-140.714293151009,-5.0687740522275,
133.856484496108));
#169944=CARTESIAN_POINT('Ctrl Pts',(-140.706963395188,-5.14936013749517,
133.72265222906));
#169945=CARTESIAN_POINT('Ctrl Pts',(-140.699633639367,-5.22466427218869,
133.585589264541));
#169946=CARTESIAN_POINT('Ctrl Pts',(-140.692303883546,-5.29442557038256,
133.445759573078));
#169947=CARTESIAN_POINT('Ctrl Pts',(-140.684974158339,-5.36418657720871,
133.305930465633));
#169948=CARTESIAN_POINT('Ctrl Pts',(-140.677644433132,-5.4284046235115,
133.163334994985));
#169949=CARTESIAN_POINT('Ctrl Pts',(-140.670314707924,-5.48686545862238,
133.018460434981));
#169950=CARTESIAN_POINT('Ctrl Pts',(-140.662983500884,-5.54533811261946,
132.873556586036));
#169951=CARTESIAN_POINT('Ctrl Pts',(-140.655652293844,-5.59805109692929,
132.726373083998));
#169952=CARTESIAN_POINT('Ctrl Pts',(-140.648321086804,-5.64483894244176,
132.577415573396));
#169953=CARTESIAN_POINT('Ctrl Pts',(-140.640982769134,-5.69167216807135,
132.428313587039));
#169954=CARTESIAN_POINT('Ctrl Pts',(-140.633644451465,-5.73256866190942,
132.27743451913));
#169955=CARTESIAN_POINT('Ctrl Pts',(-140.626306133795,-5.76741316800669,
132.125298130094));
#169956=CARTESIAN_POINT('Ctrl Pts',(-140.618964144388,-5.80227510859987,
131.973085619409));
#169957=CARTESIAN_POINT('Ctrl Pts',(-140.611622154982,-5.831078958612,131.819614908167));
#169958=CARTESIAN_POINT('Ctrl Pts',(-140.604280165575,-5.85376104713312,
131.665413557615));
#169959=CARTESIAN_POINT('Ctrl Pts',(-140.596927518036,-5.87647606251779,
131.510988357887));
#169960=CARTESIAN_POINT('Ctrl Pts',(-140.589574870498,-5.8930515219413,
131.355830778268));
#169961=CARTESIAN_POINT('Ctrl Pts',(-140.58222222296,-5.90347578439235,
131.200471997853));
#169962=CARTESIAN_POINT('Ctrl Pts',(-140.575939879375,-5.91238261665805,
131.067728352472));
#169963=CARTESIAN_POINT('Ctrl Pts',(-140.569657535791,-5.91679961509745,
130.934837971546));
#169964=CARTESIAN_POINT('Ctrl Pts',(-140.563375192206,-5.91674957945076,
130.802129795026));
#169965=CARTESIAN_POINT('',(-138.813375192206,-5.91736987688761,130.80979542472));
#169966=CARTESIAN_POINT('Ctrl Pts',(-140.563375192206,-5.92551577431234,
130.802126489862));
#169967=CARTESIAN_POINT('Ctrl Pts',(-140.557573256227,-5.92610769889885,
130.679384615503));
#169968=CARTESIAN_POINT('Ctrl Pts',(-140.551771320248,-5.92262577300941,
130.556676961143));
#169969=CARTESIAN_POINT('Ctrl Pts',(-140.545969384269,-5.91496369122512,
130.434230880662));
#169970=CARTESIAN_POINT('Ctrl Pts',(-140.453153509665,-5.79239032525184,
128.475412290975));
#169971=CARTESIAN_POINT('Ctrl Pts',(-140.267521760457,-3.40770003536918,
124.691657369469));
#169972=CARTESIAN_POINT('Ctrl Pts',(-139.989074136643,3.30084525658034,
124.633300650055));
#169973=CARTESIAN_POINT('Ctrl Pts',(-139.710626512832,6.97607501294665,
130.245846567736));
#169974=CARTESIAN_POINT('Ctrl Pts',(-139.432178889018,4.2406326326787,136.371639612287));
#169975=CARTESIAN_POINT('Ctrl Pts',(-139.153731265205,-2.39174397063631,
137.381375237385));
#169976=CARTESIAN_POINT('Ctrl Pts',(-138.947463366267,-5.67671014154374,
133.65213572739));
#169977=CARTESIAN_POINT('Ctrl Pts',(-138.834011341935,-5.92144161112725,
131.247924922634));
#169978=CARTESIAN_POINT('Ctrl Pts',(-138.813375192206,-5.91736987688761,
130.80979542472));
#169979=CARTESIAN_POINT('',(-137.063375192162,-5.91674999530446,130.804124896006));
#169980=CARTESIAN_POINT('Ctrl Pts',(-138.813375192206,-5.91674750446427,
130.809794853102));
#169981=CARTESIAN_POINT('Ctrl Pts',(-138.806067690693,-5.91688998265966,
130.65466585632));
#169982=CARTESIAN_POINT('Ctrl Pts',(-138.79876018918,-5.91092739121872,
130.499355244819));
#169983=CARTESIAN_POINT('Ctrl Pts',(-138.791452687668,-5.89884372612642,
130.344389686703));
#169984=CARTESIAN_POINT('Ctrl Pts',(-138.784150495039,-5.88676883979125,
130.189536710737));
#169985=CARTESIAN_POINT('Ctrl Pts',(-138.776848302411,-5.86858175993033,
130.035028670686));
#169986=CARTESIAN_POINT('Ctrl Pts',(-138.769546109782,-5.84431855243523,
129.881391918118));
#169987=CARTESIAN_POINT('Ctrl Pts',(-138.762246907774,-5.82006528196007,
129.727818087629));
#169988=CARTESIAN_POINT('Ctrl Pts',(-138.754947705765,-5.78974089254672,
129.575115213749));
#169989=CARTESIAN_POINT('Ctrl Pts',(-138.747648503757,-5.75343325457911,
129.423804082105));
#169990=CARTESIAN_POINT('Ctrl Pts',(-138.740350751801,-5.71713282945005,
129.272523009778));
#169991=CARTESIAN_POINT('Ctrl Pts',(-138.733052999844,-5.67485160934117,
129.122633503306));
#169992=CARTESIAN_POINT('Ctrl Pts',(-138.725755247888,-5.62672843348385,
128.974645421607));
#169993=CARTESIAN_POINT('Ctrl Pts',(-138.718457413593,-5.57860471467061,
128.826655670213));
#169994=CARTESIAN_POINT('Ctrl Pts',(-138.711159579299,-5.52463902766561,
128.680567751835));
#169995=CARTESIAN_POINT('Ctrl Pts',(-138.703861745005,-5.46501977561738,
128.536875355296));
#169996=CARTESIAN_POINT('Ctrl Pts',(-138.696562296083,-5.40538733295829,
128.393151167173));
#169997=CARTESIAN_POINT('Ctrl Pts',(-138.689262847161,-5.34009898392624,
128.251823910245));
#169998=CARTESIAN_POINT('Ctrl Pts',(-138.681963398239,-5.26939073775277,
128.113366040205));
#169999=CARTESIAN_POINT('Ctrl Pts',(-138.674656526794,-5.19861059113215,
127.974767377779));
#170000=CARTESIAN_POINT('Ctrl Pts',(-138.667349655348,-5.12239971494985,
127.839044272446));
#170001=CARTESIAN_POINT('Ctrl Pts',(-138.660042783902,-5.04103974336814,
127.706643899032));
#170002=CARTESIAN_POINT('Ctrl Pts',(-138.65273209628,-4.95963727972471,
127.574174376568));
#170003=CARTESIAN_POINT('Ctrl Pts',(-138.645421408657,-4.87308057835454,
127.445031361011));
#170004=CARTESIAN_POINT('Ctrl Pts',(-138.638110721035,-4.7816933820704,
127.319631221707));
#170005=CARTESIAN_POINT('Ctrl Pts',(-138.63078897038,-4.69016789243111,
127.194041318336));
#170006=CARTESIAN_POINT('Ctrl Pts',(-138.623467219725,-4.59379754355125,
127.072205906881));
#170007=CARTESIAN_POINT('Ctrl Pts',(-138.61614546907,-4.49294555443513,
126.954507268751));
#170008=CARTESIAN_POINT('Ctrl Pts',(-138.60970898524,-4.40428749602942,
126.85103947575));
#170009=CARTESIAN_POINT('Ctrl Pts',(-138.60327250141,-4.31216671313621,
126.7507681547));
#170010=CARTESIAN_POINT('Ctrl Pts',(-138.596836017579,-4.21685155889043,
126.65392768921));
#170011=CARTESIAN_POINT('Ctrl Pts',(-138.589412751174,-4.10692356076298,
126.54224053313));
#170012=CARTESIAN_POINT('Ctrl Pts',(-138.581989484768,-3.99238906985639,
126.434754824523));
#170013=CARTESIAN_POINT('Ctrl Pts',(-138.574566218363,-3.8736023819033,
126.331874155942));
#170014=CARTESIAN_POINT('Ctrl Pts',(-138.567151725642,-3.75495608995075,
126.229115083767));
#170015=CARTESIAN_POINT('Ctrl Pts',(-138.559737232921,-3.63206788414376,
126.130950459749));
#170016=CARTESIAN_POINT('Ctrl Pts',(-138.5523227402,-3.505330158414,126.037748503809));
#170017=CARTESIAN_POINT('Ctrl Pts',(-138.544915393846,-3.37871458727518,
125.944636379423));
#170018=CARTESIAN_POINT('Ctrl Pts',(-138.537508047492,-3.24825718142959,
125.856477620365));
#170019=CARTESIAN_POINT('Ctrl Pts',(-138.530100701139,-3.11438471144978,
125.773601387431));
#170020=CARTESIAN_POINT('Ctrl Pts',(-138.522698879463,-2.98061208860919,
125.690786966719));
#170021=CARTESIAN_POINT('Ctrl Pts',(-138.515297057788,-2.84342978925489,
125.613247422891));
#170022=CARTESIAN_POINT('Ctrl Pts',(-138.507895236112,-2.70329487989415,
125.541269571912));
#170023=CARTESIAN_POINT('Ctrl Pts',(-138.500497321801,-2.56323394666166,
125.469329717482));
#170024=CARTESIAN_POINT('Ctrl Pts',(-138.49309940749,-2.42022383878538,
125.402945878891));
#170025=CARTESIAN_POINT('Ctrl Pts',(-138.485701493178,-2.27474752226647,
125.342359677211));
#170026=CARTESIAN_POINT('Ctrl Pts',(-138.478304808266,-2.12929538127153,
125.281783543858));
#170027=CARTESIAN_POINT('Ctrl Pts',(-138.470908123354,-1.98137818931292,
125.227003278606));
#170028=CARTESIAN_POINT('Ctrl Pts',(-138.463511438442,-1.8315003653847,
125.178213003604));
#170029=CARTESIAN_POINT('Ctrl Pts',(-138.456115081506,-1.68162918719668,
125.129424892014));
#170030=CARTESIAN_POINT('Ctrl Pts',(-138.448718724571,-1.52979790486113,
125.086626358119));
#170031=CARTESIAN_POINT('Ctrl Pts',(-138.441322367636,-1.37652737008728,
125.049962042398));
#170032=CARTESIAN_POINT('Ctrl Pts',(-138.433924878299,-1.22323336920327,
125.013292113276));
#170033=CARTESIAN_POINT('Ctrl Pts',(-138.426527388962,-1.06850004020659,
124.982758359183));
#170034=CARTESIAN_POINT('Ctrl Pts',(-138.419129899626,-0.91285958186534,
124.95845453328));
#170035=CARTESIAN_POINT('Ctrl Pts',(-138.411729817111,-0.757164564002912,
124.934142187707));
#170036=CARTESIAN_POINT('Ctrl Pts',(-138.404329734596,-0.600562152272778,
124.916064175994));
#170037=CARTESIAN_POINT('Ctrl Pts',(-138.396929652081,-0.443590688686608,
124.904262494364));
#170038=CARTESIAN_POINT('Ctrl Pts',(-138.389521432415,-0.286446618838942,
124.892447835572));
#170039=CARTESIAN_POINT('Ctrl Pts',(-138.382113212748,-0.12893305918083,
124.886923317556));
#170040=CARTESIAN_POINT('Ctrl Pts',(-138.374704993082,0.0284098784218015,
124.887678824423));
#170041=CARTESIAN_POINT('Ctrl Pts',(-138.36729221378,0.185849657977568,
124.888434796293));
#170042=CARTESIAN_POINT('Ctrl Pts',(-138.359879434478,0.343118234162838,
124.895478478378));
#170043=CARTESIAN_POINT('Ctrl Pts',(-138.352466655175,0.499680105999917,
124.908747811914));
#170044=CARTESIAN_POINT('Ctrl Pts',(-138.345043284147,0.656465680781722,
124.922036105296));
#170045=CARTESIAN_POINT('Ctrl Pts',(-138.337619913118,0.812542165046005,
124.941567770211));
#170046=CARTESIAN_POINT('Ctrl Pts',(-138.330196542089,0.967382919462458,
124.967229400124));
#170047=CARTESIAN_POINT('Ctrl Pts',(-138.326260492648,1.04948320280673,
124.980835812047));
#170048=CARTESIAN_POINT('Ctrl Pts',(-138.322324443208,1.13123629766687,
124.996164733947));
#170049=CARTESIAN_POINT('Ctrl Pts',(-138.318388393767,1.21256549908842,
125.013193595892));
#170050=CARTESIAN_POINT('Ctrl Pts',(-138.310965127361,1.36594983477179,
125.045309498068));
#170051=CARTESIAN_POINT('Ctrl Pts',(-138.303541860956,1.51828929557144,
125.083571958067));
#170052=CARTESIAN_POINT('Ctrl Pts',(-138.296118594551,1.66905282214581,
125.127901048487));
#170053=CARTESIAN_POINT('Ctrl Pts',(-138.28870410183,1.8196381587519,125.172177745604));
#170054=CARTESIAN_POINT('Ctrl Pts',(-138.281289609109,1.96865091405452,
125.222506696438));
#170055=CARTESIAN_POINT('Ctrl Pts',(-138.273875116388,2.11556919570139,
125.278756800724));
#170056=CARTESIAN_POINT('Ctrl Pts',(-138.266467770034,2.26234587197746,
125.334952689041));
#170057=CARTESIAN_POINT('Ctrl Pts',(-138.25906042368,2.4070317472174,125.397058236656));
#170058=CARTESIAN_POINT('Ctrl Pts',(-138.251653077326,2.54911920920186,
125.46489230885));
#170059=CARTESIAN_POINT('Ctrl Pts',(-138.244251255651,2.69110069699652,
125.532675787834));
#170060=CARTESIAN_POINT('Ctrl Pts',(-138.236849433975,2.83048729491822,
125.606179124038));
#170061=CARTESIAN_POINT('Ctrl Pts',(-138.2294476123,2.96679064095992,125.685172805499));
#170062=CARTESIAN_POINT('Ctrl Pts',(-138.222049697989,3.10302203352585,
125.764124786811));
#170063=CARTESIAN_POINT('Ctrl Pts',(-138.214651783677,3.23617309354354,
125.84856115455));
#170064=CARTESIAN_POINT('Ctrl Pts',(-138.207253869366,3.3657794834426,125.938206177833));
#170065=CARTESIAN_POINT('Ctrl Pts',(-138.199857184454,3.49536433511115,
126.027836303739));
#170066=CARTESIAN_POINT('Ctrl Pts',(-138.192460499542,3.62140537905713,
126.122673155114));
#170067=CARTESIAN_POINT('Ctrl Pts',(-138.185063814629,3.74346664403109,
126.222397277738));
#170068=CARTESIAN_POINT('Ctrl Pts',(-138.177667457694,3.86552249668065,
126.32211697849));
#170069=CARTESIAN_POINT('Ctrl Pts',(-138.170271100758,3.98359863215166,
126.426723283421));
#170070=CARTESIAN_POINT('Ctrl Pts',(-138.162874743823,4.09729182724135,
126.535856166951));
#170071=CARTESIAN_POINT('Ctrl Pts',(-138.155477254486,4.21100242904946,
126.645005759003));
#170072=CARTESIAN_POINT('Ctrl Pts',(-138.14807976515,4.32032848502308,126.758683051048));
#170073=CARTESIAN_POINT('Ctrl Pts',(-138.140682275813,4.42490345153916,
126.876490965063));
#170074=CARTESIAN_POINT('Ctrl Pts',(-138.133282193298,4.5295150766481,126.994340176459));
#170075=CARTESIAN_POINT('Ctrl Pts',(-138.125882110783,4.62937204866553,
127.116322613748));
#170076=CARTESIAN_POINT('Ctrl Pts',(-138.118482028268,4.72414804797195,
127.242008054534));
#170077=CARTESIAN_POINT('Ctrl Pts',(-138.111073808602,4.81902826323241,
127.367831699382));
#170078=CARTESIAN_POINT('Ctrl Pts',(-138.103665588935,4.90881612317972,
127.497366181206));
#170079=CARTESIAN_POINT('Ctrl Pts',(-138.096257369269,4.99322819494413,
127.630151620711));
#170080=CARTESIAN_POINT('Ctrl Pts',(-138.088844589967,5.07769222093021,
127.763018787438));
#170081=CARTESIAN_POINT('Ctrl Pts',(-138.081431810664,5.15677367863044,
127.899140576879));
#170082=CARTESIAN_POINT('Ctrl Pts',(-138.074019031362,5.23023532848394,
128.038032912615));
#170083=CARTESIAN_POINT('Ctrl Pts',(-138.066595660334,5.30380194378787,
128.177123704234));
#170084=CARTESIAN_POINT('Ctrl Pts',(-138.059172289305,5.37173255305411,
128.318992612735));
#170085=CARTESIAN_POINT('Ctrl Pts',(-138.051748918276,5.43383790699033,
128.463135262532));
#170086=CARTESIAN_POINT('Ctrl Pts',(-138.047812868835,5.46676765584518,
128.53956315411));
#170087=CARTESIAN_POINT('Ctrl Pts',(-138.043876819394,5.4980605444152,128.616630004902));
#170088=CARTESIAN_POINT('Ctrl Pts',(-138.039940769954,5.52769410052333,
128.694259081256));
#170089=CARTESIAN_POINT('Ctrl Pts',(-138.032517503548,5.58358206251097,
128.840665096537));
#170090=CARTESIAN_POINT('Ctrl Pts',(-138.025094237143,5.63373397092519,
128.989514393627));
#170091=CARTESIAN_POINT('Ctrl Pts',(-138.017670970737,5.6779300204067,129.140316974549));
#170092=CARTESIAN_POINT('Ctrl Pts',(-138.010256478016,5.72207383382811,
129.290941319345));
#170093=CARTESIAN_POINT('Ctrl Pts',(-138.002841985295,5.76027569618112,
129.443513997921));
#170094=CARTESIAN_POINT('Ctrl Pts',(-137.995427492574,5.79236381026875,
129.597525064564));
#170095=CARTESIAN_POINT('Ctrl Pts',(-137.988020146221,5.82442099662392,
129.751387689543));
#170096=CARTESIAN_POINT('Ctrl Pts',(-137.980612799867,5.85037609021098,
129.906685579598));
#170097=CARTESIAN_POINT('Ctrl Pts',(-137.973205453513,5.87010710799512,
130.062893758452));
#170098=CARTESIAN_POINT('Ctrl Pts',(-137.965803631837,5.88982340964174,
130.218985431352));
#170099=CARTESIAN_POINT('Ctrl Pts',(-137.958401810162,5.90332483205459,
130.375985672453));
#170100=CARTESIAN_POINT('Ctrl Pts',(-137.950999988487,5.91054049855355,
130.533359552147));
#170101=CARTESIAN_POINT('Ctrl Pts',(-137.943602074175,5.91775235595837,
130.690650355395));
#170102=CARTESIAN_POINT('Ctrl Pts',(-137.936204159864,5.91868504875209,
130.848314032459));
#170103=CARTESIAN_POINT('Ctrl Pts',(-137.928806245553,5.91331957133809,
131.005810883711));
#170104=CARTESIAN_POINT('Ctrl Pts',(-137.92140956064,5.90795498556912,131.163281561843));
#170105=CARTESIAN_POINT('Ctrl Pts',(-137.914012875728,5.89629431956377,
131.32058509647));
#170106=CARTESIAN_POINT('Ctrl Pts',(-137.906616190816,5.87837068609705,
131.477182019823));
#170107=CARTESIAN_POINT('Ctrl Pts',(-137.899219833881,5.86044784738302,
131.633771999504));
#170108=CARTESIAN_POINT('Ctrl Pts',(-137.891823476945,5.83626263583146,
131.789655059332));
#170109=CARTESIAN_POINT('Ctrl Pts',(-137.88442712001,5.80589999917085,131.944297353586));
#170110=CARTESIAN_POINT('Ctrl Pts',(-137.877029630673,5.77553271391306,
132.09896332397));
#170111=CARTESIAN_POINT('Ctrl Pts',(-137.869632141336,5.73898619229852,
132.252387784208));
#170112=CARTESIAN_POINT('Ctrl Pts',(-137.862234652,5.69639638153221,132.404047720398));
#170113=CARTESIAN_POINT('Ctrl Pts',(-137.854834569485,5.65379164097407,
132.555760820742));
#170114=CARTESIAN_POINT('Ctrl Pts',(-137.84743448697,5.60513949427872,132.705707806337));
#170115=CARTESIAN_POINT('Ctrl Pts',(-137.840034404455,5.55062551600754,
132.853381589529));
#170116=CARTESIAN_POINT('Ctrl Pts',(-137.832626184789,5.49605159401254,
133.00121775523));
#170117=CARTESIAN_POINT('Ctrl Pts',(-137.825217965122,5.43560309733815,
133.14677537621));
#170118=CARTESIAN_POINT('Ctrl Pts',(-137.817809745456,5.36951373307164,
133.289567416377));
#170119=CARTESIAN_POINT('Ctrl Pts',(-137.810396966154,5.30338369190437,
133.432447342661));
#170120=CARTESIAN_POINT('Ctrl Pts',(-137.802984186852,5.23160603483752,
133.57255796488));
#170121=CARTESIAN_POINT('Ctrl Pts',(-137.79557140755,5.15445979529367,133.709438031543));
#170122=CARTESIAN_POINT('Ctrl Pts',(-137.788148036521,5.07720332558484,
133.846513678865));
#170123=CARTESIAN_POINT('Ctrl Pts',(-137.780724665492,4.99456314853259,
133.980349234721));
#170124=CARTESIAN_POINT('Ctrl Pts',(-137.773301294463,4.90686131573687,
134.110512850998));
#170125=CARTESIAN_POINT('Ctrl Pts',(-137.769365245022,4.86035969961123,
134.179528723582));
#170126=CARTESIAN_POINT('Ctrl Pts',(-137.765429195582,4.81243574603676,
134.247512832312));
#170127=CARTESIAN_POINT('Ctrl Pts',(-137.761493146141,4.76314186644666,
134.314404794297));
#170128=CARTESIAN_POINT('Ctrl Pts',(-137.754069879735,4.67017514795067,
134.440560946972));
#170129=CARTESIAN_POINT('Ctrl Pts',(-137.74664661333,4.57205235020373,134.56321184882));
#170130=CARTESIAN_POINT('Ctrl Pts',(-137.739223346924,4.46906691221595,
134.681907715492));
#170131=CARTESIAN_POINT('Ctrl Pts',(-137.731808854203,4.36620319446316,
134.800463293508));
#170132=CARTESIAN_POINT('Ctrl Pts',(-137.724394361482,4.25848851862847,
134.915072861803));
#170133=CARTESIAN_POINT('Ctrl Pts',(-137.716979868761,4.14625905590145,
135.025316244418));
#170134=CARTESIAN_POINT('Ctrl Pts',(-137.709572522408,4.03413776415629,
135.13545337031));
#170135=CARTESIAN_POINT('Ctrl Pts',(-137.702165176054,3.91751061306116,
135.241232428567));
#170136=CARTESIAN_POINT('Ctrl Pts',(-137.6947578297,3.79675334521557,135.342267028908));
#170137=CARTESIAN_POINT('Ctrl Pts',(-137.687356008025,3.67608614269556,
135.443226273832));
#170138=CARTESIAN_POINT('Ctrl Pts',(-137.679954186349,3.55129524198303,
135.539447868148));
#170139=CARTESIAN_POINT('Ctrl Pts',(-137.672552364674,3.42279238393125,
135.630583038777));
#170140=CARTESIAN_POINT('Ctrl Pts',(-137.665154450362,3.29435736153908,
135.721670099859));
#170141=CARTESIAN_POINT('Ctrl Pts',(-137.657756536051,3.1622145879964,135.807675869323));
#170142=CARTESIAN_POINT('Ctrl Pts',(-137.65035862174,3.02680785489518,135.888292636392));
#170143=CARTESIAN_POINT('Ctrl Pts',(-137.642961936828,2.89142362393589,
135.968896006417));
#170144=CARTESIAN_POINT('Ctrl Pts',(-137.635565251915,2.75277683038301,
136.044111960678));
#170145=CARTESIAN_POINT('Ctrl Pts',(-137.628168567003,2.61133924201346,
136.113676762384));
#170146=CARTESIAN_POINT('Ctrl Pts',(-137.620772210068,2.46990792513438,
136.183238479513));
#170147=CARTESIAN_POINT('Ctrl Pts',(-137.613375853132,2.32568639446254,
136.247149377567));
#170148=CARTESIAN_POINT('Ctrl Pts',(-137.605979496197,2.17916970584513,
136.305192368822));
#170149=CARTESIAN_POINT('Ctrl Pts',(-137.59858200686,2.0326305851495,136.363244246607));
#170150=CARTESIAN_POINT('Ctrl Pts',(-137.591184517524,1.88379595391424,
136.415426291281));
#170151=CARTESIAN_POINT('Ctrl Pts',(-137.583787028187,1.73317932133237,
136.461570177288));
#170152=CARTESIAN_POINT('Ctrl Pts',(-137.576386945672,1.58250989032193,
136.507730238962));
#170153=CARTESIAN_POINT('Ctrl Pts',(-137.568986863157,1.4300575709363,136.54784781842));
#170154=CARTESIAN_POINT('Ctrl Pts',(-137.561586780642,1.27634929796166,
136.581804951533));
#170155=CARTESIAN_POINT('Ctrl Pts',(-137.554178560976,1.12247200693996,
136.615799424005));
#170156=CARTESIAN_POINT('Ctrl Pts',(-137.546770341309,0.967336369014114,
136.643619841345));
#170157=CARTESIAN_POINT('Ctrl Pts',(-137.539362121642,0.811478465832407,
136.665199573039));
#170158=CARTESIAN_POINT('Ctrl Pts',(-137.53194934234,0.65552463471192,136.686792586698));
#170159=CARTESIAN_POINT('Ctrl Pts',(-137.524536563038,0.498848023188452,
136.70213722466));
#170160=CARTESIAN_POINT('Ctrl Pts',(-137.517123783736,0.341987519584247,
136.71121892795));
#170161=CARTESIAN_POINT('Ctrl Pts',(-137.509700412708,0.184902886336242,
136.720313607603));
#170162=CARTESIAN_POINT('Ctrl Pts',(-137.502277041679,0.0276342084789624,
136.723127473213));
#170163=CARTESIAN_POINT('Ctrl Pts',(-137.49485367065,-0.129281111182614,
136.719698051457));
#170164=CARTESIAN_POINT('Ctrl Pts',(-137.490917621209,-0.212481378797461,
136.717879689754));
#170165=CARTESIAN_POINT('Ctrl Pts',(-137.486981571768,-0.295582402394713,
136.714306981708));
#170166=CARTESIAN_POINT('Ctrl Pts',(-137.483045522328,-0.378505050477561,
136.708991384114));
#170167=CARTESIAN_POINT('Ctrl Pts',(-137.475622255922,-0.534894576835595,
136.698966332945));
#170168=CARTESIAN_POINT('Ctrl Pts',(-137.468198989517,-0.691122023178962,
136.682708652582));
#170169=CARTESIAN_POINT('Ctrl Pts',(-137.460775723111,-0.846650362243173,
136.660222102148));
#170170=CARTESIAN_POINT('Ctrl Pts',(-137.45336123039,-1.00199487972688,
136.637762128949));
#170171=CARTESIAN_POINT('Ctrl Pts',(-137.445946737669,-1.1566415688112,
136.60908799269));
#170172=CARTESIAN_POINT('Ctrl Pts',(-137.438532244948,-1.31005521482037,
136.574255408342));
#170173=CARTESIAN_POINT('Ctrl Pts',(-137.431124898595,-1.46332099498159,
136.53945639695));
#170174=CARTESIAN_POINT('Ctrl Pts',(-137.423717552241,-1.61535573645554,
136.498510836466));
#170175=CARTESIAN_POINT('Ctrl Pts',(-137.416310205887,-1.76563126010126,
136.451525996396));
#170176=CARTESIAN_POINT('Ctrl Pts',(-137.408908384212,-1.91579470259146,
136.404576199392));
#170177=CARTESIAN_POINT('Ctrl Pts',(-137.401506562536,-2.06420118504784,
136.351596202432));
#170178=CARTESIAN_POINT('Ctrl Pts',(-137.394104740861,-2.2103347188132,
136.292743894389));
#170179=CARTESIAN_POINT('Ctrl Pts',(-137.38670682655,-2.35639110982484,
136.233922654021));
#170180=CARTESIAN_POINT('Ctrl Pts',(-137.379308912238,-2.50017659635288,
136.169235415364));
#170181=CARTESIAN_POINT('Ctrl Pts',(-137.371910997927,-2.64119241240932,
136.098889227663));
#170182=CARTESIAN_POINT('Ctrl Pts',(-137.364514313015,-2.78218479419482,
136.028554730221));
#170183=CARTESIAN_POINT('Ctrl Pts',(-137.357117628103,-2.92040808529264,
135.952563316654));
#170184=CARTESIAN_POINT('Ctrl Pts',(-137.34972094319,-3.05538539446384,
135.871169342375));
#170185=CARTESIAN_POINT('Ctrl Pts',(-137.342324586255,-3.19035671859972,
135.789778977189));
#170186=CARTESIAN_POINT('Ctrl Pts',(-137.334928229319,-3.32208202731753,
135.702986720378));
#170187=CARTESIAN_POINT('Ctrl Pts',(-137.327531872384,-3.45011108879016,
135.611091735229));
#170188=CARTESIAN_POINT('Ctrl Pts',(-137.320134383047,-3.57815975183893,
135.519182680723));
#170189=CARTESIAN_POINT('Ctrl Pts',(-137.312736893711,-3.70251073756622,
135.422169560012));
#170190=CARTESIAN_POINT('Ctrl Pts',(-137.305339404374,-3.82274486465305,
135.32039341885));
#170191=CARTESIAN_POINT('Ctrl Pts',(-137.297939321859,-3.94302113962726,
135.218581600218));
#170192=CARTESIAN_POINT('Ctrl Pts',(-137.290539239344,-4.05917739789664,
135.112003677869));
#170193=CARTESIAN_POINT('Ctrl Pts',(-137.283139156829,-4.17082957177651,
135.001039214468));
#170194=CARTESIAN_POINT('Ctrl Pts',(-137.275730937163,-4.28260451869888,
134.889952734233));
#170195=CARTESIAN_POINT('Ctrl Pts',(-137.268322717496,-4.38986522541898,
134.774470343501));
#170196=CARTESIAN_POINT('Ctrl Pts',(-137.26091449783,-4.49226586857321,
134.655007047525));
#170197=CARTESIAN_POINT('Ctrl Pts',(-137.253501718528,-4.59472953761524,
134.535470223882));
#170198=CARTESIAN_POINT('Ctrl Pts',(-137.246088939226,-4.69232695168307,
134.411947904928));
#170199=CARTESIAN_POINT('Ctrl Pts',(-137.238676159924,-4.78475457959678,
134.284885603186));
#170200=CARTESIAN_POINT('Ctrl Pts',(-137.231252788895,-4.87731427243955,
134.15764174887));
#170201=CARTESIAN_POINT('Ctrl Pts',(-137.223829417866,-4.9646892191526,
134.026848119203));
#170202=CARTESIAN_POINT('Ctrl Pts',(-137.216406046837,-5.04662051265013,
133.892977130473));
#170203=CARTESIAN_POINT('Ctrl Pts',(-137.212469997396,-5.09006245037808,
133.821995520055));
#170204=CARTESIAN_POINT('Ctrl Pts',(-137.208533947955,-5.1319747630258,
133.75014913939));
#170205=CARTESIAN_POINT('Ctrl Pts',(-137.204597898515,-5.17232431701266,
133.677510756723));
#170206=CARTESIAN_POINT('Ctrl Pts',(-137.196816576985,-5.25209284071643,
133.533909254921));
#170207=CARTESIAN_POINT('Ctrl Pts',(-137.189035255457,-5.32597286795493,
133.386811640862));
#170208=CARTESIAN_POINT('Ctrl Pts',(-137.181253933927,-5.39366007775706,
133.236717813397));
#170209=CARTESIAN_POINT('Ctrl Pts',(-137.173485134107,-5.4612383652485,
133.086865517036));
#170210=CARTESIAN_POINT('Ctrl Pts',(-137.165716334287,-5.52264356596163,
132.934026908043));
#170211=CARTESIAN_POINT('Ctrl Pts',(-137.157947534466,-5.57761648533935,
132.778727580663));
#170212=CARTESIAN_POINT('Ctrl Pts',(-137.150066505945,-5.63338354789144,
132.621184786825));
#170213=CARTESIAN_POINT('Ctrl Pts',(-137.142185477423,-5.68253084916941,
132.461109897367));
#170214=CARTESIAN_POINT('Ctrl Pts',(-137.134304448901,-5.7248365729683,
132.299076903456));
#170215=CARTESIAN_POINT('Ctrl Pts',(-137.126562263329,-5.76639698142256,
132.139898503814));
#170216=CARTESIAN_POINT('Ctrl Pts',(-137.118820077758,-5.80135475029489,
131.978830741823));
#170217=CARTESIAN_POINT('Ctrl Pts',(-137.111077892186,-5.8295481012705,
131.816437441465));
#170218=CARTESIAN_POINT('Ctrl Pts',(-137.103127442189,-5.85849985205065,
131.649675769027));
#170219=CARTESIAN_POINT('Ctrl Pts',(-137.095176992192,-5.88031800224339,
131.481516547968));
#170220=CARTESIAN_POINT('Ctrl Pts',(-137.087226542196,-5.89488225293724,
131.312586735063));
#170221=CARTESIAN_POINT('Ctrl Pts',(-137.079276092199,-5.90944650363105,
131.143656922157));
#170222=CARTESIAN_POINT('Ctrl Pts',(-137.071325642203,-5.91675676133333,
130.973956878516));
#170223=CARTESIAN_POINT('Ctrl Pts',(-137.063375192206,-5.9167499953045,
130.80412489694));
#170224=CARTESIAN_POINT('',(-135.313375192206,-5.91688315261144,130.799007197003));
#170225=CARTESIAN_POINT('Ctrl Pts',(-137.063375192162,-5.91674999530446,
130.804124896005));
#170226=CARTESIAN_POINT('Ctrl Pts',(-137.05560354086,-5.9167433814115,130.638112287751));
#170227=CARTESIAN_POINT('Ctrl Pts',(-137.047831889558,-5.90974547835622,
130.472243404385));
#170228=CARTESIAN_POINT('Ctrl Pts',(-137.040060238256,-5.89581823969249,
130.307110331483));
#170229=CARTESIAN_POINT('Ctrl Pts',(-137.032278021656,-5.8818720674173,
130.141752765736));
#170230=CARTESIAN_POINT('Ctrl Pts',(-137.024495805056,-5.86097778122643,
129.97713331967));
#170231=CARTESIAN_POINT('Ctrl Pts',(-137.016713588456,-5.83324875759858,
129.813835759486));
#170232=CARTESIAN_POINT('Ctrl Pts',(-137.008912554227,-5.80545268437448,
129.650143340989));
#170233=CARTESIAN_POINT('Ctrl Pts',(-137.001111519998,-5.77078887560722,
129.487779511236));
#170234=CARTESIAN_POINT('Ctrl Pts',(-136.993310485769,-5.72942165030861,
129.327316909521));
#170235=CARTESIAN_POINT('Ctrl Pts',(-136.985499742625,-5.68800294069421,
129.166654601222));
#170236=CARTESIAN_POINT('Ctrl Pts',(-136.97768899948,-5.63986425109469,
129.007898544551));
#170237=CARTESIAN_POINT('Ctrl Pts',(-136.969878256335,-5.58521897036779,
128.851603690669));
#170238=CARTESIAN_POINT('Ctrl Pts',(-136.962049208225,-5.53044562501072,
128.69494255003));
#170239=CARTESIAN_POINT('Ctrl Pts',(-136.954220160116,-5.46913530667103,
128.540754440993));
#170240=CARTESIAN_POINT('Ctrl Pts',(-136.946391112006,-5.40154943985235,
128.3895740408));
#170241=CARTESIAN_POINT('Ctrl Pts',(-136.939644166238,-5.34330504388798,
128.259289241545));
#170242=CARTESIAN_POINT('Ctrl Pts',(-136.93289722047,-5.28040079509976,
128.13123788636));
#170243=CARTESIAN_POINT('Ctrl Pts',(-136.926150274702,-5.21303021830327,
128.005745512633));
#170244=CARTESIAN_POINT('Ctrl Pts',(-136.918727008296,-5.13890634705246,
127.867673657005));
#170245=CARTESIAN_POINT('Ctrl Pts',(-136.911303741891,-5.05918116475427,
127.732339912249));
#170246=CARTESIAN_POINT('Ctrl Pts',(-136.903880475485,-4.97408131473932,
127.600231151258));
#170247=CARTESIAN_POINT('Ctrl Pts',(-136.896465982764,-4.88908204567975,
127.468278531852));
#170248=CARTESIAN_POINT('Ctrl Pts',(-136.889051490043,-4.79872095359227,
127.339543619835));
#170249=CARTESIAN_POINT('Ctrl Pts',(-136.881636997322,-4.70327118310432,
127.214490043203));
#170250=CARTESIAN_POINT('Ctrl Pts',(-136.874229650968,-4.60791341069906,
127.089556997916));
#170251=CARTESIAN_POINT('Ctrl Pts',(-136.866822304615,-4.50747694907607,
126.968298518974));
#170252=CARTESIAN_POINT('Ctrl Pts',(-136.859414958261,-4.40227890815001,
126.851150405933));
#170253=CARTESIAN_POINT('Ctrl Pts',(-136.852013136585,-4.29715932789146,
126.734089666374));
#170254=CARTESIAN_POINT('Ctrl Pts',(-136.84461131491,-4.18728548791909,
126.621133465114));
#170255=CARTESIAN_POINT('Ctrl Pts',(-136.837209493234,-4.0730154701462,
126.51268547347));
#170256=CARTESIAN_POINT('Ctrl Pts',(-136.829811578923,-3.95880577462622,
126.404294730677));
#170257=CARTESIAN_POINT('Ctrl Pts',(-136.822413664612,-3.8402047931907,
126.300407714242));
#170258=CARTESIAN_POINT('Ctrl Pts',(-136.8150157503,-3.71760816105667,126.201391996845));
#170259=CARTESIAN_POINT('Ctrl Pts',(-136.807619065388,-3.59503190225895,
126.102392734063));
#170260=CARTESIAN_POINT('Ctrl Pts',(-136.800222380476,-3.46846160074031,
126.008263397979));
#170261=CARTESIAN_POINT('Ctrl Pts',(-136.792825695563,-3.33832682488041,
125.919332002216));
#170262=CARTESIAN_POINT('Ctrl Pts',(-136.785429338628,-3.20819781933284,
125.830404549765));
#170263=CARTESIAN_POINT('Ctrl Pts',(-136.778032981692,-3.07450496191039,
125.74667478998));
#170264=CARTESIAN_POINT('Ctrl Pts',(-136.770636624757,-2.9377074930873,
125.668427864155));
#170265=CARTESIAN_POINT('Ctrl Pts',(-136.76323913542,-2.80088908022252,
125.590168958526));
#170266=CARTESIAN_POINT('Ctrl Pts',(-136.755841646084,-2.66096543357956,
125.517394743643));
#170267=CARTESIAN_POINT('Ctrl Pts',(-136.748444156747,-2.51842097978532,
125.45034471069));
#170268=CARTESIAN_POINT('Ctrl Pts',(-136.741044074232,-2.37582655725316,
125.383271173452));
#170269=CARTESIAN_POINT('Ctrl Pts',(-136.733643991717,-2.23060983598848,
125.321925972068));
#170270=CARTESIAN_POINT('Ctrl Pts',(-136.726243909202,-2.08327567883836,
125.266500651075));
#170271=CARTESIAN_POINT('Ctrl Pts',(-136.718835689535,-1.93577951263676,
125.211014384245));
#170272=CARTESIAN_POINT('Ctrl Pts',(-136.711427469869,-1.7861616103125,
125.161461129258));
#170273=CARTESIAN_POINT('Ctrl Pts',(-136.704019250202,-1.63494317345788,
125.117982914488));
#170274=CARTESIAN_POINT('Ctrl Pts',(-136.6966064709,-1.4836316641786,125.074477939602));
#170275=CARTESIAN_POINT('Ctrl Pts',(-136.689193691598,-1.33071801918584,
125.037055544064));
#170276=CARTESIAN_POINT('Ctrl Pts',(-136.681780912296,-1.17673360750333,
125.00580660993));
#170277=CARTESIAN_POINT('Ctrl Pts',(-136.674357541267,-1.02252917567203,
124.974513025853));
#170278=CARTESIAN_POINT('Ctrl Pts',(-136.666934170238,-0.867251289011637,
124.949410579975));
#170279=CARTESIAN_POINT('Ctrl Pts',(-136.659510799209,-0.711437237224342,
124.930538384983));
#170280=CARTESIAN_POINT('Ctrl Pts',(-136.655574749769,-0.62882088827053,
124.920531894367));
#170281=CARTESIAN_POINT('Ctrl Pts',(-136.651638700329,-0.546053830252986,
124.912276079976));
#170282=CARTESIAN_POINT('Ctrl Pts',(-136.647702650889,-0.463216019656414,
124.905770830029));
#170283=CARTESIAN_POINT('Ctrl Pts',(-136.640279384483,-0.306986494131329,
124.89350213165));
#170284=CARTESIAN_POINT('Ctrl Pts',(-136.632856118078,-0.150032973389701,
124.887425990701));
#170285=CARTESIAN_POINT('Ctrl Pts',(-136.625432851672,0.00711241635787892,
124.88761489242));
#170286=CARTESIAN_POINT('Ctrl Pts',(-136.618018358951,0.164072073305337,
124.887803570873));
#170287=CARTESIAN_POINT('Ctrl Pts',(-136.61060386623,0.321222778213059,
124.894242552335));
#170288=CARTESIAN_POINT('Ctrl Pts',(-136.603189373509,0.478026826373297,
124.906952634751));
#170289=CARTESIAN_POINT('Ctrl Pts',(-136.595782027155,0.634679740887905,
124.919650466712));
#170290=CARTESIAN_POINT('Ctrl Pts',(-136.588374680802,0.790986294244059,
124.938607336612));
#170291=CARTESIAN_POINT('Ctrl Pts',(-136.580967334448,0.946408430277538,
124.963792011206));
#170292=CARTESIAN_POINT('Ctrl Pts',(-136.573565512772,1.10171464661822,
124.988957902119));
#170293=CARTESIAN_POINT('Ctrl Pts',(-136.566163691097,1.25613739214663,
125.020342289586));
#170294=CARTESIAN_POINT('Ctrl Pts',(-136.558761869422,1.40914349472865,
125.057862103361));
#170295=CARTESIAN_POINT('Ctrl Pts',(-136.55136395511,1.56206882657967,125.095362110717));
#170296=CARTESIAN_POINT('Ctrl Pts',(-136.543966040799,1.71357864319441,
125.138991005388));
#170297=CARTESIAN_POINT('Ctrl Pts',(-136.536568126488,1.86314984476834,
125.188614610272));
#170298=CARTESIAN_POINT('Ctrl Pts',(-136.529171441575,2.01269619032228,
125.238229968613));
#170299=CARTESIAN_POINT('Ctrl Pts',(-136.521774756663,2.16030420627278,
125.293837942547));
#170300=CARTESIAN_POINT('Ctrl Pts',(-136.514378071751,2.30546573326601,
125.355254423406));
#170301=CARTESIAN_POINT('Ctrl Pts',(-136.506981714815,2.45062082364502,
125.416668180993));
#170302=CARTESIAN_POINT('Ctrl Pts',(-136.49958535788,2.59332929696827,125.483889787944));
#170303=CARTESIAN_POINT('Ctrl Pts',(-136.492189000945,2.73310302509495,
125.556686998074));
#170304=CARTESIAN_POINT('Ctrl Pts',(-136.484791511608,2.87289815293663,
125.629495353642));
#170305=CARTESIAN_POINT('Ctrl Pts',(-136.477394022271,3.00975730982586,
125.707880839653));
#170306=CARTESIAN_POINT('Ctrl Pts',(-136.469996532935,3.14321716062246,
125.791565345099));
#170307=CARTESIAN_POINT('Ctrl Pts',(-136.46259645042,3.27672379556305,125.875279186019));
#170308=CARTESIAN_POINT('Ctrl Pts',(-136.455196367905,3.40682843583282,
125.964295546581));
#170309=CARTESIAN_POINT('Ctrl Pts',(-136.44779628539,3.53309703888642,126.058293205875));
#170310=CARTESIAN_POINT('Ctrl Pts',(-136.440388065723,3.65950448724962,
126.152394225259));
#170311=CARTESIAN_POINT('Ctrl Pts',(-136.432979846057,3.78206717491825,
126.251487259157));
#170312=CARTESIAN_POINT('Ctrl Pts',(-136.42557162639,3.90038388720675,126.355210575713));
#170313=CARTESIAN_POINT('Ctrl Pts',(-136.418158847088,4.01877342145743,
126.45899773224));
#170314=CARTESIAN_POINT('Ctrl Pts',(-136.410746067786,4.13291150292322,
126.56742059363));
#170315=CARTESIAN_POINT('Ctrl Pts',(-136.403333288484,4.24243445201907,
126.680081228046));
#170316=CARTESIAN_POINT('Ctrl Pts',(-136.395909917455,4.35211389264055,
126.792902837259));
#170317=CARTESIAN_POINT('Ctrl Pts',(-136.388486546426,4.45716478190906,
126.909974035845));
#170318=CARTESIAN_POINT('Ctrl Pts',(-136.381063175398,4.55726379500535,
127.030863928124));
#170319=CARTESIAN_POINT('Ctrl Pts',(-136.377127125957,4.61033869359071,
127.094962649721));
#170320=CARTESIAN_POINT('Ctrl Pts',(-136.373191076516,4.66202216061623,
127.160134450385));
#170321=CARTESIAN_POINT('Ctrl Pts',(-136.369255027076,4.71227107169331,
127.22631200004));
#170322=CARTESIAN_POINT('Ctrl Pts',(-136.36183176067,4.80703894977178,127.35112079336));
#170323=CARTESIAN_POINT('Ctrl Pts',(-136.354408494265,4.89698819100115,
127.479885932913));
#170324=CARTESIAN_POINT('Ctrl Pts',(-136.346985227859,4.98177018428258,
127.61219890589));
#170325=CARTESIAN_POINT('Ctrl Pts',(-136.339570735138,5.06645197228865,
127.74435549592));
#170326=CARTESIAN_POINT('Ctrl Pts',(-136.332156242417,5.14597846944518,
127.880051261458));
#170327=CARTESIAN_POINT('Ctrl Pts',(-136.324741749696,5.22004153532217,
128.018845058103));
#170328=CARTESIAN_POINT('Ctrl Pts',(-136.317334403343,5.29403321642806,
128.157505080061));
#170329=CARTESIAN_POINT('Ctrl Pts',(-136.309927056989,5.36257177498328,
128.29925686146));
#170330=CARTESIAN_POINT('Ctrl Pts',(-136.302519710635,5.42539265590344,
128.443630838076));
#170331=CARTESIAN_POINT('Ctrl Pts',(-136.29511788896,5.48816668264034,128.587897135134));
#170332=CARTESIAN_POINT('Ctrl Pts',(-136.287716067284,5.54523137455547,
128.734781392458));
#170333=CARTESIAN_POINT('Ctrl Pts',(-136.280314245609,5.59636842843825,
128.883790135735));
#170334=CARTESIAN_POINT('Ctrl Pts',(-136.272916331298,5.64747848746834,
129.032720218457));
#170335=CARTESIAN_POINT('Ctrl Pts',(-136.265518416986,5.69266701946077,
129.18377220142));
#170336=CARTESIAN_POINT('Ctrl Pts',(-136.258120502675,5.73176416318901,
129.336433459945));
#170337=CARTESIAN_POINT('Ctrl Pts',(-136.250723817763,5.77085480968132,
129.489069348938));
#170338=CARTESIAN_POINT('Ctrl Pts',(-136.24332713285,5.80385598445876,129.643313621445));
#170339=CARTESIAN_POINT('Ctrl Pts',(-136.235930447938,5.83064791081451,
129.798639233377));
#170340=CARTESIAN_POINT('Ctrl Pts',(-136.228534091003,5.85743864918818,
129.95395795801));
#170341=CARTESIAN_POINT('Ctrl Pts',(-136.221137734067,5.87802062312581,
130.110357558866));
#170342=CARTESIAN_POINT('Ctrl Pts',(-136.213741377132,5.89232538273506,
130.267301825183));
#170343=CARTESIAN_POINT('Ctrl Pts',(-136.206343887795,5.90663233243953,
130.424270120067));
#170344=CARTESIAN_POINT('Ctrl Pts',(-136.198946398459,5.91466012033609,
130.581782874671));
#170345=CARTESIAN_POINT('Ctrl Pts',(-136.191548909122,5.91639228512992,
130.739299946227));
#170346=CARTESIAN_POINT('Ctrl Pts',(-136.184148826607,5.91812505713144,
130.896872235147));
#170347=CARTESIAN_POINT('Ctrl Pts',(-136.176748744092,5.91355780796466,
131.054448470989));
#170348=CARTESIAN_POINT('Ctrl Pts',(-136.169348661577,5.90272617928099,
131.211489853719));
#170349=CARTESIAN_POINT('Ctrl Pts',(-136.161940441911,5.89188264010805,
131.368703919594));
#170350=CARTESIAN_POINT('Ctrl Pts',(-136.154532222244,5.87476099067463,
131.525381585189));
#170351=CARTESIAN_POINT('Ctrl Pts',(-136.147124002578,5.85144869989751,
131.680989772322));
#170352=CARTESIAN_POINT('Ctrl Pts',(-136.139711223276,5.82812206079434,
131.836693733698));
#170353=CARTESIAN_POINT('Ctrl Pts',(-136.132298443974,5.79859725782218,
131.99132653915));
#170354=CARTESIAN_POINT('Ctrl Pts',(-136.124885664672,5.76301250460659,
132.144367122867));
#170355=CARTESIAN_POINT('Ctrl Pts',(-136.117462293643,5.7273769062269,132.297626378146));
#170356=CARTESIAN_POINT('Ctrl Pts',(-136.110038922614,5.68566416288823,
132.449288508942));
#170357=CARTESIAN_POINT('Ctrl Pts',(-136.102615551585,5.63806203436787,
132.598848583288));
#170358=CARTESIAN_POINT('Ctrl Pts',(-136.098679502145,5.61282224362844,
132.678148923352));
#170359=CARTESIAN_POINT('Ctrl Pts',(-136.094743452704,5.58592753833369,
132.756858638084));
#170360=CARTESIAN_POINT('Ctrl Pts',(-136.090807403263,5.55741125539755,
132.834905052165));
#170361=CARTESIAN_POINT('Ctrl Pts',(-136.083384136857,5.50363043574379,
132.982098153372));
#170362=CARTESIAN_POINT('Ctrl Pts',(-136.075960870452,5.44391643903607,
133.127375700706));
#170363=CARTESIAN_POINT('Ctrl Pts',(-136.068537604047,5.37842452585654,
133.270223586623));
#170364=CARTESIAN_POINT('Ctrl Pts',(-136.061123111326,5.31301001867962,
133.412902638201));
#170365=CARTESIAN_POINT('Ctrl Pts',(-136.053708618605,5.24183134228407,
133.553157408393));
#170366=CARTESIAN_POINT('Ctrl Pts',(-136.046294125884,5.16509308651932,
133.690490200605));
#170367=CARTESIAN_POINT('Ctrl Pts',(-136.03888677953,5.08842879397484,133.8276906263));
#170368=CARTESIAN_POINT('Ctrl Pts',(-136.031479433176,5.00621577071171,
133.96197435705));
#170369=CARTESIAN_POINT('Ctrl Pts',(-136.024072086822,4.9187060759237,134.09286500424));
#170370=CARTESIAN_POINT('Ctrl Pts',(-136.016670265147,4.83126164916737,
134.223658028246));
#170371=CARTESIAN_POINT('Ctrl Pts',(-136.009268443472,4.73852862336444,
134.351062698642));
#170372=CARTESIAN_POINT('Ctrl Pts',(-136.001866621796,4.64080417421365,
134.474628615833));
#170373=CARTESIAN_POINT('Ctrl Pts',(-135.994468707485,4.54313131303917,
134.598129303537));
#170374=CARTESIAN_POINT('Ctrl Pts',(-135.987070793174,4.44047250709058,
134.71779498175));
#170375=CARTESIAN_POINT('Ctrl Pts',(-135.979672878862,4.33316722788835,
134.833205655248));
#170376=CARTESIAN_POINT('Ctrl Pts',(-135.97227619395,4.22587978087665,134.948597149586));
#170377=CARTESIAN_POINT('Ctrl Pts',(-135.964879509038,4.11394764705738,
135.059734769484));
#170378=CARTESIAN_POINT('Ctrl Pts',(-135.957482824126,3.99774950131289,
135.166232863202));
#170379=CARTESIAN_POINT('Ctrl Pts',(-135.95008646719,3.88155650791595,135.272726234684));
#170380=CARTESIAN_POINT('Ctrl Pts',(-135.942690110255,3.76109815390441,
135.374580236805));
#170381=CARTESIAN_POINT('Ctrl Pts',(-135.93529375332,3.6367885697415,135.471447445717));
#170382=CARTESIAN_POINT('Ctrl Pts',(-135.927896263983,3.5124599534639,135.568329485246));
#170383=CARTESIAN_POINT('Ctrl Pts',(-135.920498774646,3.38427922747028,
135.660222981888));
#170384=CARTESIAN_POINT('Ctrl Pts',(-135.91310128531,3.25269193143695,135.746822125931));
#170385=CARTESIAN_POINT('Ctrl Pts',(-135.905701202795,3.12105850768117,
135.833451627169));
#170386=CARTESIAN_POINT('Ctrl Pts',(-135.89830112028,2.98601644794011,135.91478287558));
#170387=CARTESIAN_POINT('Ctrl Pts',(-135.890901037765,2.84803832512546,
135.990554622915));
#170388=CARTESIAN_POINT('Ctrl Pts',(-135.883492818099,2.70990848118009,
136.066409689076));
#170389=CARTESIAN_POINT('Ctrl Pts',(-135.876084598432,2.56883645403495,
136.136692865816));
#170390=CARTESIAN_POINT('Ctrl Pts',(-135.868676378766,2.42531801654775,
136.201189601433));
#170391=CARTESIAN_POINT('Ctrl Pts',(-135.861263599464,2.28171124585702,
136.265726033715));
#170392=CARTESIAN_POINT('Ctrl Pts',(-135.853850820162,2.13565541001169,
136.324468789252));
#170393=CARTESIAN_POINT('Ctrl Pts',(-135.84643804086,1.98766360427814,136.377252502282));
#170394=CARTESIAN_POINT('Ctrl Pts',(-135.839014669831,1.83946034091221,
136.430111635156));
#170395=CARTESIAN_POINT('Ctrl Pts',(-135.831591298802,1.68931593831358,
136.476994609067));
#170396=CARTESIAN_POINT('Ctrl Pts',(-135.824167927773,1.53775669879329,
136.517786463573));
#170397=CARTESIAN_POINT('Ctrl Pts',(-135.820231878333,1.45739635338431,
136.539415283619));
#170398=CARTESIAN_POINT('Ctrl Pts',(-135.816295828892,1.37663839605393,
136.559332529761));
#170399=CARTESIAN_POINT('Ctrl Pts',(-135.812359779451,1.29556199002331,
136.577526966504));
#170400=CARTESIAN_POINT('Ctrl Pts',(-135.804936513045,1.14265441856021,
136.611841106371));
#170401=CARTESIAN_POINT('Ctrl Pts',(-135.79751324664,0.988151429699113,
136.640128092688));
#170402=CARTESIAN_POINT('Ctrl Pts',(-135.790089980234,0.832569478813058,
136.662240662894));
#170403=CARTESIAN_POINT('Ctrl Pts',(-135.782675487514,0.677171412872674,
136.684327097878));
#170404=CARTESIAN_POINT('Ctrl Pts',(-135.775260994793,0.520697289261222,
136.700253590744));
#170405=CARTESIAN_POINT('Ctrl Pts',(-135.767846502072,0.363676420030692,
136.709923251559));
#170406=CARTESIAN_POINT('Ctrl Pts',(-135.760439155718,0.206806893425211,
136.719583592391));
#170407=CARTESIAN_POINT('Ctrl Pts',(-135.753031809364,0.0493920403929515,
136.722999084059));
#170408=CARTESIAN_POINT('Ctrl Pts',(-135.74562446301,-0.108031095679464,
136.720124291418));
#170409=CARTESIAN_POINT('Ctrl Pts',(-135.738222641335,-0.265336819637314,
136.717251642906));
#170410=CARTESIAN_POINT('Ctrl Pts',(-135.730820819659,-0.422650442705173,
136.708098058343));
#170411=CARTESIAN_POINT('Ctrl Pts',(-135.723418997984,-0.579432400224242,
136.692670108079));
#170412=CARTESIAN_POINT('Ctrl Pts',(-135.716021083673,-0.736131593768324,
136.677250302111));
#170413=CARTESIAN_POINT('Ctrl Pts',(-135.708623169361,-0.892299310152501,
136.655562763288));
#170414=CARTESIAN_POINT('Ctrl Pts',(-135.70122525505,-1.04739870285251,
136.62766608094));
#170415=CARTESIAN_POINT('Ctrl Pts',(-135.693828570138,-1.20247232084702,
136.599774034515));
#170416=CARTESIAN_POINT('Ctrl Pts',(-135.686431885226,-1.35647760047121,
136.565674958492));
#170417=CARTESIAN_POINT('Ctrl Pts',(-135.679035200313,-1.50888539897116,
136.52547898859));
#170418=CARTESIAN_POINT('Ctrl Pts',(-135.671638843378,-1.66128643954961,
136.48528480102));
#170419=CARTESIAN_POINT('Ctrl Pts',(-135.664242486442,-1.81208977889087,
136.438994352301));
#170420=CARTESIAN_POINT('Ctrl Pts',(-135.656846129507,-1.96077927184045,
136.386768271045));
#170421=CARTESIAN_POINT('Ctrl Pts',(-135.64944864017,-2.10949152953099,
136.334534193842));
#170422=CARTESIAN_POINT('Ctrl Pts',(-135.642051150834,-2.25608894420267,
136.276362798356));
#170423=CARTESIAN_POINT('Ctrl Pts',(-135.634653661497,-2.40007340440478,
136.212463632115));
#170424=CARTESIAN_POINT('Ctrl Pts',(-135.627253578982,-2.54410833813682,
136.148542066119));
#170425=CARTESIAN_POINT('Ctrl Pts',(-135.619853496467,-2.68552815272177,
136.078888883061));
#170426=CARTESIAN_POINT('Ctrl Pts',(-135.612453413952,-2.82385761540701,
136.003760460856));
#170427=CARTESIAN_POINT('Ctrl Pts',(-135.605045194286,-2.96233918555689,
135.928549427228));
#170428=CARTESIAN_POINT('Ctrl Pts',(-135.597636974619,-3.09772328921889,
135.847851309213));
#170429=CARTESIAN_POINT('Ctrl Pts',(-135.590228754953,-3.22956144063075,
135.761967244124));
#170430=CARTESIAN_POINT('Ctrl Pts',(-135.582815975651,-3.36148073622497,
135.676030318825));
#170431=CARTESIAN_POINT('Ctrl Pts',(-135.575403196349,-3.48984942702584,
135.584901301852));
#170432=CARTESIAN_POINT('Ctrl Pts',(-135.567990417047,-3.61425104560988,
135.488922490549));
#170433=CARTESIAN_POINT('Ctrl Pts',(-135.560567046018,-3.73883041506059,
135.39280654022));
#170434=CARTESIAN_POINT('Ctrl Pts',(-135.553143674989,-3.85943110589282,
135.291827194583));
#170435=CARTESIAN_POINT('Ctrl Pts',(-135.54572030396,-3.97567191937431,
135.186365107751));
#170436=CARTESIAN_POINT('Ctrl Pts',(-135.54178425452,-4.03730558784453,
135.130446578782));
#170437=CARTESIAN_POINT('Ctrl Pts',(-135.537848205079,-4.09771417967086,
135.07326838014));
#170438=CARTESIAN_POINT('Ctrl Pts',(-135.533912155638,-4.15684545245782,
135.014891041026));
#170439=CARTESIAN_POINT('Ctrl Pts',(-135.526593680781,-4.26679090401356,
134.906347412467));
#170440=CARTESIAN_POINT('Ctrl Pts',(-135.519275205925,-4.37267110236618,
134.793307590097));
#170441=CARTESIAN_POINT('Ctrl Pts',(-135.511956731068,-4.47408803446405,
134.676113040225));
#170442=CARTESIAN_POINT('Ctrl Pts',(-135.504647058547,-4.57538298679652,
134.559059446733));
#170443=CARTESIAN_POINT('Ctrl Pts',(-135.497337386025,-4.67222510440882,
134.437861356091));
#170444=CARTESIAN_POINT('Ctrl Pts',(-135.490027713504,-4.76425133291557,
134.312898746091));
#170445=CARTESIAN_POINT('Ctrl Pts',(-135.482667191783,-4.85691773511574,
134.18706684288));
#170446=CARTESIAN_POINT('Ctrl Pts',(-135.475306670063,-4.94470068521811,
134.057418097223));
#170447=CARTESIAN_POINT('Ctrl Pts',(-135.467946148342,-5.02726830169465,
133.924377281829));
#170448=CARTESIAN_POINT('Ctrl Pts',(-135.460649442483,-5.10912005538388,
133.792489932805));
#170449=CARTESIAN_POINT('Ctrl Pts',(-135.453352736624,-5.18584633495802,
133.657269427338));
#170450=CARTESIAN_POINT('Ctrl Pts',(-135.446056030765,-5.2571654720375,
133.519161118914));
#170451=CARTESIAN_POINT('Ctrl Pts',(-135.438762445043,-5.32845411241422,
133.381111866841));
#170452=CARTESIAN_POINT('Ctrl Pts',(-135.43146885932,-5.3943400341916,133.240177609734));
#170453=CARTESIAN_POINT('Ctrl Pts',(-135.424175273598,-5.45458667183857,
133.096829767173));
#170454=CARTESIAN_POINT('Ctrl Pts',(-135.416883271381,-5.51482022938264,
132.953513046757));
#170455=CARTESIAN_POINT('Ctrl Pts',(-135.409591269164,-5.56941679093975,
132.807784138428));
#170456=CARTESIAN_POINT('Ctrl Pts',(-135.402299266947,-5.61818737844745,
132.660135696382));
#170457=CARTESIAN_POINT('Ctrl Pts',(-135.394888927385,-5.66774943332515,
132.510091160089));
#170458=CARTESIAN_POINT('Ctrl Pts',(-135.387478587823,-5.71129462244642,
132.358064624372));
#170459=CARTESIAN_POINT('Ctrl Pts',(-135.380068248262,-5.74867703636407,
132.20459020377));
#170460=CARTESIAN_POINT('Ctrl Pts',(-135.372772483496,-5.78548146294015,
132.053488724427));
#170461=CARTESIAN_POINT('Ctrl Pts',(-135.365476718731,-5.81631227136727,
131.900984201993));
#170462=CARTESIAN_POINT('Ctrl Pts',(-135.358180953966,-5.84108172357949,
131.747596993543));
#170463=CARTESIAN_POINT('Ctrl Pts',(-135.350713327006,-5.8664346557357,
131.590596529578));
#170464=CARTESIAN_POINT('Ctrl Pts',(-135.343245700046,-5.88543705467267,
131.432671700418));
#170465=CARTESIAN_POINT('Ctrl Pts',(-135.335778073086,-5.89805111906382,
131.2743856801));
#170466=CARTESIAN_POINT('Ctrl Pts',(-135.328310446126,-5.91066518345497,
131.116099659782));
#170467=CARTESIAN_POINT('Ctrl Pts',(-135.320842819166,-5.91689093509487,
130.957452878542));
#170468=CARTESIAN_POINT('Ctrl Pts',(-135.313375192206,-5.91674757824783,
130.799007319666));
#170469=CARTESIAN_POINT('',(-133.563375192206,-5.92503606369206,130.807060657761));
#170470=CARTESIAN_POINT('Ctrl Pts',(-135.313375192206,-5.91823652768249,
130.799005972509));
#170471=CARTESIAN_POINT('Ctrl Pts',(-135.294071638746,-5.92204404516267,
130.389322916598));
#170472=CARTESIAN_POINT('Ctrl Pts',(-135.274768085285,-5.88314771307888,
129.980358143981));
#170473=CARTESIAN_POINT('Ctrl Pts',(-135.16264865722,-5.39374310559234,
127.660585609891));
#170474=CARTESIAN_POINT('Ctrl Pts',(-134.977016908012,-2.48589836884803,
124.262352529057));
#170475=CARTESIAN_POINT('Ctrl Pts',(-134.698569284199,4.16028789435366,
125.176788746284));
#170476=CARTESIAN_POINT('Ctrl Pts',(-134.420121660386,6.9833728240057,131.262688591048));
#170477=CARTESIAN_POINT('Ctrl Pts',(-134.141674036573,3.38907928512634,
136.927407418748));
#170478=CARTESIAN_POINT('Ctrl Pts',(-133.86322641276,-3.31961255106015,
136.965345363627));
#170479=CARTESIAN_POINT('Ctrl Pts',(-133.670460131305,-5.8520964766113,
133.072114422921));
#170480=CARTESIAN_POINT('Ctrl Pts',(-133.570509724453,-5.9258914963796,
130.95802645762));
#170481=CARTESIAN_POINT('Ctrl Pts',(-133.563375192206,-5.92503606369206,
130.807060657761));
#170482=CARTESIAN_POINT('',(-131.813375192206,-5.90991206338681,130.808405239875));
#170483=CARTESIAN_POINT('Ctrl Pts',(-133.563375192206,-5.92503606369206,
130.807060657761));
#170484=CARTESIAN_POINT('Ctrl Pts',(-133.477693849849,-5.91476284346878,
128.994054291817));
#170485=CARTESIAN_POINT('Ctrl Pts',(-133.299196632889,-4.0536518896767,
125.19884575645));
#170486=CARTESIAN_POINT('Ctrl Pts',(-133.027883541321,2.41175106234068,
124.234656107945));
#170487=CARTESIAN_POINT('Ctrl Pts',(-132.749435917509,6.83088882713039,
129.282349329258));
#170488=CARTESIAN_POINT('Ctrl Pts',(-132.470988293696,4.97277346725347,
135.728696570128));
#170489=CARTESIAN_POINT('Ctrl Pts',(-132.192540669883,-1.45507777553816,
137.649819637784));
#170490=CARTESIAN_POINT('Ctrl Pts',(-131.97333630272,-5.46267151731689,
134.20997083825));
#170491=CARTESIAN_POINT('Ctrl Pts',(-131.846947810161,-5.91438909886242,
131.523472343736));
#170492=CARTESIAN_POINT('Ctrl Pts',(-131.813375192206,-5.90991206338681,
130.808405239875));
#170493=CARTESIAN_POINT('',(-130.063375158615,-5.91342694435326,130.800133359548));
#170494=CARTESIAN_POINT('Ctrl Pts',(-131.813375192206,-5.90991206338681,
130.808405239875));
#170495=CARTESIAN_POINT('Ctrl Pts',(-131.754131935556,-5.90201175123154,
129.546576209652));
#170496=CARTESIAN_POINT('Ctrl Pts',(-131.602072804305,-4.88693589981136,
126.296249162835));
#170497=CARTESIAN_POINT('Ctrl Pts',(-131.357197798442,0.468954947398858,
123.821693377335));
#170498=CARTESIAN_POINT('Ctrl Pts',(-131.078750174631,6.12819731254553,
127.424603491846));
#170499=CARTESIAN_POINT('Ctrl Pts',(-130.800302550819,6.15592572653701,
134.133345294561));
#170500=CARTESIAN_POINT('Ctrl Pts',(-130.521854927006,0.52665913153656,
137.782912809069));
#170501=CARTESIAN_POINT('Ctrl Pts',(-130.276212474135,-4.86635301707174,
135.345098168375));
#170502=CARTESIAN_POINT('Ctrl Pts',(-130.123385895868,-5.90187158747846,
132.078122015566));
#170503=CARTESIAN_POINT('Ctrl Pts',(-130.063375192206,-5.91026073634778,
130.800136338677));
#170504=CARTESIAN_POINT('',(-128.313375192206,-5.92111332573527,130.80192758));
#170505=CARTESIAN_POINT('Ctrl Pts',(-130.063375123377,-5.916748487671,130.800130234262));
#170506=CARTESIAN_POINT('Ctrl Pts',(-130.054904464835,-5.91661937012662,
130.619542334627));
#170507=CARTESIAN_POINT('Ctrl Pts',(-130.046433806292,-5.90821859595855,
130.43928493431));
#170508=CARTESIAN_POINT('Ctrl Pts',(-130.03796314775,-5.89166059700865,
130.260057418829));
#170509=CARTESIAN_POINT('Ctrl Pts',(-130.029453540339,-5.87502646285285,
130.080005798705));
#170510=CARTESIAN_POINT('Ctrl Pts',(-130.020943932927,-5.8501600223074,
129.900993696451));
#170511=CARTESIAN_POINT('Ctrl Pts',(-130.012434325516,-5.81722686199573,
129.723711646542));
#170512=CARTESIAN_POINT('Ctrl Pts',(-130.003872284472,-5.78409077749085,
129.545337238152));
#170513=CARTESIAN_POINT('Ctrl Pts',(-129.995310243429,-5.742788341951,129.368714407466));
#170514=CARTESIAN_POINT('Ctrl Pts',(-129.986748202385,-5.69353686693738,
129.194525685865));
#170515=CARTESIAN_POINT('Ctrl Pts',(-129.979485361383,-5.65175878735304,
129.046768278159));
#170516=CARTESIAN_POINT('Ctrl Pts',(-129.972222520382,-5.60426186830998,
128.900762007714));
#170517=CARTESIAN_POINT('Ctrl Pts',(-129.96495967938,-5.55120523506474,
128.756910740111));
#170518=CARTESIAN_POINT('Ctrl Pts',(-129.957536412975,-5.49697665935459,
128.609882011014));
#170519=CARTESIAN_POINT('Ctrl Pts',(-129.950113146569,-5.43682076436011,
128.464786885468));
#170520=CARTESIAN_POINT('Ctrl Pts',(-129.942689880164,-5.37089437471072,
128.322138996074));
#170521=CARTESIAN_POINT('Ctrl Pts',(-129.935275387444,-5.30504590457888,
128.179659704639));
#170522=CARTESIAN_POINT('Ctrl Pts',(-129.927860894723,-5.23344067060665,
128.039622227509));
#170523=CARTESIAN_POINT('Ctrl Pts',(-129.920446402002,-5.15628477651301,
127.902523636273));
#170524=CARTESIAN_POINT('Ctrl Pts',(-129.913039055649,-5.07920324817518,
127.765557185821));
#170525=CARTESIAN_POINT('Ctrl Pts',(-129.905631709295,-4.99658189223649,
127.63152430523));
#170526=CARTESIAN_POINT('Ctrl Pts',(-129.898224362942,-4.90867421668623,
127.500900613731));
#170527=CARTESIAN_POINT('Ctrl Pts',(-129.890822541267,-4.82083210599671,
127.370374346308));
#170528=CARTESIAN_POINT('Ctrl Pts',(-129.883420719591,-4.72771173374014,
127.243252513477));
#170529=CARTESIAN_POINT('Ctrl Pts',(-129.876018897916,-4.62961164510019,
127.119984608246));
#170530=CARTESIAN_POINT('Ctrl Pts',(-129.868620983605,-4.5315633427337,
126.996781775183));
#170531=CARTESIAN_POINT('Ctrl Pts',(-129.861223069294,-4.42854079113761,
126.877429109349));
#170532=CARTESIAN_POINT('Ctrl Pts',(-129.853825154983,-4.32088473858091,
126.762345570786));
#170533=CARTESIAN_POINT('Ctrl Pts',(-129.846428470071,-4.21324657650723,
126.647281157019));
#170534=CARTESIAN_POINT('Ctrl Pts',(-129.839031785159,-4.10097669647058,
126.536484734818));
#170535=CARTESIAN_POINT('Ctrl Pts',(-129.831635100247,-3.98445494539054,
126.430340801578));
#170536=CARTESIAN_POINT('Ctrl Pts',(-129.824238743312,-3.86793836100704,
126.324201574872));
#170537=CARTESIAN_POINT('Ctrl Pts',(-129.816842386377,-3.74717055641044,
126.222714678327));
#170538=CARTESIAN_POINT('Ctrl Pts',(-129.809446029442,-3.62256671758438,
126.126226273712));
#170539=CARTESIAN_POINT('Ctrl Pts',(-129.802048540105,-3.49794380159249,
126.029723096475));
#170540=CARTESIAN_POINT('Ctrl Pts',(-129.794651050769,-3.369483977136,125.938220163515));
#170541=CARTESIAN_POINT('Ctrl Pts',(-129.787253561433,-3.23763371260702,
125.852021927059));
#170542=CARTESIAN_POINT('Ctrl Pts',(-129.779853478918,-3.10573722817201,
125.765793473945));
#170543=CARTESIAN_POINT('Ctrl Pts',(-129.772453396403,-2.97044824959946,
125.684873623831));
#170544=CARTESIAN_POINT('Ctrl Pts',(-129.765053313888,-2.83224014276189,
125.609522185408));
#170545=CARTESIAN_POINT('Ctrl Pts',(-129.757645094222,-2.69388006190291,
125.534087890332));
#170546=CARTESIAN_POINT('Ctrl Pts',(-129.750236874556,-2.55259477038696,
125.464234413861));
#170547=CARTESIAN_POINT('Ctrl Pts',(-129.742828654889,-2.40888069179691,
125.400174797742));
#170548=CARTESIAN_POINT('Ctrl Pts',(-129.735415875588,-2.26507815958949,
125.336075753998));
#170549=CARTESIAN_POINT('Ctrl Pts',(-129.728003096286,-2.11884420753047,
125.277777814274));
#170550=CARTESIAN_POINT('Ctrl Pts',(-129.720590316984,-1.97069243182606,
125.225444781882));
#170551=CARTESIAN_POINT('Ctrl Pts',(-129.713166945956,-1.82232896991667,
125.173036973599));
#170552=CARTESIAN_POINT('Ctrl Pts',(-129.705743574927,-1.67204256713796,
125.126611204757));
#170553=CARTESIAN_POINT('Ctrl Pts',(-129.698320203899,-1.52035987326319,
125.086280833384));
#170554=CARTESIAN_POINT('Ctrl Pts',(-129.694384154454,-1.43993406932512,
125.06489670275));
#170555=CARTESIAN_POINT('Ctrl Pts',(-129.69044810501,-1.35911586474888,
125.045225348288));
#170556=CARTESIAN_POINT('Ctrl Pts',(-129.686512055566,-1.27798445658614,
125.027277764497));
#170557=CARTESIAN_POINT('Ctrl Pts',(-129.679088789161,-1.12497315294235,
124.99342918162));
#170558=CARTESIAN_POINT('Ctrl Pts',(-129.671665522755,-0.970384783872578,
124.965612580278));
#170559=CARTESIAN_POINT('Ctrl Pts',(-129.66424225635,-0.81473625057424,
124.943973650437));
#170560=CARTESIAN_POINT('Ctrl Pts',(-129.656827763629,-0.659271680916454,
124.922360296013));
#170561=CARTESIAN_POINT('Ctrl Pts',(-129.649413270908,-0.502749807316699,
124.906910130325));
#170562=CARTESIAN_POINT('Ctrl Pts',(-129.641998778187,-0.345700234274841,
124.897718431813));
#170563=CARTESIAN_POINT('Ctrl Pts',(-129.634591431833,-0.188802031523845,
124.888535592605));
#170564=CARTESIAN_POINT('Ctrl Pts',(-129.627184085479,-0.0313775120446858,
124.885599233421));
#170565=CARTESIAN_POINT('Ctrl Pts',(-129.619776739126,0.126036144974603,
124.888953154621));
#170566=CARTESIAN_POINT('Ctrl Pts',(-129.61237491745,0.283332396949609,
124.892304574341));
#170567=CARTESIAN_POINT('Ctrl Pts',(-129.604973095775,0.440617430989262,
124.90193692506));
#170568=CARTESIAN_POINT('Ctrl Pts',(-129.597571274099,0.597351704931872,
124.91784199421));
#170569=CARTESIAN_POINT('Ctrl Pts',(-129.590173359788,0.754003240070838,
124.933738667199));
#170570=CARTESIAN_POINT('Ctrl Pts',(-129.582775445477,0.910104223688883,
124.955901426375));
#170571=CARTESIAN_POINT('Ctrl Pts',(-129.575377531165,1.06511799007414,
124.984270048707));
#170572=CARTESIAN_POINT('Ctrl Pts',(-129.567980846253,1.22010599598387,
125.012633956689));
#170573=CARTESIAN_POINT('Ctrl Pts',(-129.560584161341,1.37400677640881,
125.047201613863));
#170574=CARTESIAN_POINT('Ctrl Pts',(-129.553187476429,1.5262915262612,125.087861274492));
#170575=CARTESIAN_POINT('Ctrl Pts',(-129.545791119493,1.6785695236482,125.12851913223));
#170576=CARTESIAN_POINT('Ctrl Pts',(-129.538394762558,1.82923127227653,
125.175268360025));
#170577=CARTESIAN_POINT('Ctrl Pts',(-129.530998405623,1.97776111828071,
125.227946759044));
#170578=CARTESIAN_POINT('Ctrl Pts',(-129.523600916286,2.1263137045835,125.28063322326));
#170579=CARTESIAN_POINT('Ctrl Pts',(-129.51620342695,2.27273338650872,125.339250541403));
#170580=CARTESIAN_POINT('Ctrl Pts',(-129.508805937613,2.41652269270348,
125.403587650837));
#170581=CARTESIAN_POINT('Ctrl Pts',(-129.501405855098,2.56036240401683,
125.467947313545));
#170582=CARTESIAN_POINT('Ctrl Pts',(-129.494005772583,2.7015695632254,125.538030607243));
#170583=CARTESIAN_POINT('Ctrl Pts',(-129.486605690068,2.83966972010401,
125.61357970876));
#170584=CARTESIAN_POINT('Ctrl Pts',(-129.479197470402,2.97792173230195,
125.68921188428));
#170585=CARTESIAN_POINT('Ctrl Pts',(-129.471789250735,3.11305959156186,
125.770321691148));
#170586=CARTESIAN_POINT('Ctrl Pts',(-129.464381031069,3.24463573075725,
125.856606628412));
#170587=CARTESIAN_POINT('Ctrl Pts',(-129.456968251767,3.37629285287084,
125.942944672614));
#170588=CARTESIAN_POINT('Ctrl Pts',(-129.449555472465,3.50438358369619,
126.034463977622));
#170589=CARTESIAN_POINT('Ctrl Pts',(-129.442142693163,3.62849249957423,
126.130820980093));
#170590=CARTESIAN_POINT('Ctrl Pts',(-129.434719322134,3.75277874809159,
126.227315661967));
#170591=CARTESIAN_POINT('Ctrl Pts',(-129.427295951105,3.87307153391706,
126.328661606893));
#170592=CARTESIAN_POINT('Ctrl Pts',(-129.419872580076,3.98899081866422,
126.434477002284));
#170593=CARTESIAN_POINT('Ctrl Pts',(-129.415936530635,4.05045400488321,
126.490582863926));
#170594=CARTESIAN_POINT('Ctrl Pts',(-129.412000481195,4.11068828613165,
126.547944660695));
#170595=CARTESIAN_POINT('Ctrl Pts',(-129.408064431754,4.16964160448611,
126.606501704663));
#170596=CARTESIAN_POINT('Ctrl Pts',(-129.400641165348,4.28082572303124,
126.716938462082));
#170597=CARTESIAN_POINT('Ctrl Pts',(-129.393217898943,4.38778740706093,
126.831962482668));
#170598=CARTESIAN_POINT('Ctrl Pts',(-129.385794632537,4.49012468575821,
126.951217631789));
#170599=CARTESIAN_POINT('Ctrl Pts',(-129.378380139816,4.59234101029095,
127.070331831227));
#170600=CARTESIAN_POINT('Ctrl Pts',(-129.370965647095,4.68994356819628,
127.193666924472));
#170601=CARTESIAN_POINT('Ctrl Pts',(-129.363551154374,4.78256593485623,
127.320828840583));
#170602=CARTESIAN_POINT('Ctrl Pts',(-129.35614380802,4.87509902859202,127.447868193251));
#170603=CARTESIAN_POINT('Ctrl Pts',(-129.348736461667,4.96266126882164,
127.578726726121));
#170604=CARTESIAN_POINT('Ctrl Pts',(-129.341329115313,5.04492544658949,
127.712976170291));
#170605=CARTESIAN_POINT('Ctrl Pts',(-129.333927293637,5.12712826862991,
127.847125486161));
#170606=CARTESIAN_POINT('Ctrl Pts',(-129.326525471962,5.20404070196677,
127.98466036069));
#170607=CARTESIAN_POINT('Ctrl Pts',(-129.319123650286,5.27537802034888,
128.125122422683));
#170608=CARTESIAN_POINT('Ctrl Pts',(-129.311725735975,5.34667768031591,
128.265510335847));
#170609=CARTESIAN_POINT('Ctrl Pts',(-129.304327821663,5.41240791796292,
128.408822027066));
#170610=CARTESIAN_POINT('Ctrl Pts',(-129.296929907352,5.47232931970685,
128.554573432258));
#170611=CARTESIAN_POINT('Ctrl Pts',(-129.28953322244,5.53224076360098,128.700300616211));
#170612=CARTESIAN_POINT('Ctrl Pts',(-129.282136537528,5.58634514566882,
128.848466364544));
#170613=CARTESIAN_POINT('Ctrl Pts',(-129.274739852615,5.63445064869656,
128.998565377262));
#170614=CARTESIAN_POINT('Ctrl Pts',(-129.26734349568,5.68255401867576,129.148657734433));
#170615=CARTESIAN_POINT('Ctrl Pts',(-129.259947138744,5.72465892457534,
129.300682830054));
#170616=CARTESIAN_POINT('Ctrl Pts',(-129.252550781809,5.76062310535929,
129.454119157493));
#170617=CARTESIAN_POINT('Ctrl Pts',(-129.245153292472,5.79659279235124,
129.607578976426));
#170618=CARTESIAN_POINT('Ctrl Pts',(-129.237755803135,5.82641979704802,
129.762450093916));
#170619=CARTESIAN_POINT('Ctrl Pts',(-129.230358313799,5.85001279700647,
129.918199888713));
#170620=CARTESIAN_POINT('Ctrl Pts',(-129.222958231284,5.87361406745445,
130.07400428136));
#170621=CARTESIAN_POINT('Ctrl Pts',(-129.215558148769,5.89097692633214,
130.230687595721));
#170622=CARTESIAN_POINT('Ctrl Pts',(-129.208158066254,5.90206183564049,
130.387711303663));
#170623=CARTESIAN_POINT('Ctrl Pts',(-129.200749846587,5.9131589339462,130.544907675314));
#170624=CARTESIAN_POINT('Ctrl Pts',(-129.193341626921,5.91796427013394,
130.702444815443));
#170625=CARTESIAN_POINT('Ctrl Pts',(-129.185933407254,5.91649042585801,
130.859782663996));
#170626=CARTESIAN_POINT('Ctrl Pts',(-129.178520627952,5.91501567445552,
131.01721735137));
#170627=CARTESIAN_POINT('Ctrl Pts',(-129.17110784865,5.90725405999082,131.174452130773));
#170628=CARTESIAN_POINT('Ctrl Pts',(-129.163695069348,5.89327008540014,
131.330951790135));
#170629=CARTESIAN_POINT('Ctrl Pts',(-129.156271698319,5.87926612985076,
131.48767506355));
#170630=CARTESIAN_POINT('Ctrl Pts',(-129.14884832729,5.85902210517054,131.643660749879));
#170631=CARTESIAN_POINT('Ctrl Pts',(-129.141424956261,5.83265382107117,
131.798382733036));
#170632=CARTESIAN_POINT('Ctrl Pts',(-129.137488906821,5.81867272414561,
131.880420040996));
#170633=CARTESIAN_POINT('Ctrl Pts',(-129.133552857381,5.80297072027464,
131.962102300013));
#170634=CARTESIAN_POINT('Ctrl Pts',(-129.129616807941,5.7855707293513,132.043352908976));
#170635=CARTESIAN_POINT('Ctrl Pts',(-129.122193541535,5.75275488950022,
132.196589021757));
#170636=CARTESIAN_POINT('Ctrl Pts',(-129.11477027513,5.7137973262347,132.348752208587));
#170637=CARTESIAN_POINT('Ctrl Pts',(-129.107347008724,5.66878039066167,
132.499311780564));
#170638=CARTESIAN_POINT('Ctrl Pts',(-129.099932516003,5.62381666136794,
132.649693403632));
#170639=CARTESIAN_POINT('Ctrl Pts',(-129.092518023282,5.57280792101309,
132.79847483037));
#170640=CARTESIAN_POINT('Ctrl Pts',(-129.085103530561,5.51588765118415,
132.945134772402));
#170641=CARTESIAN_POINT('Ctrl Pts',(-129.077696184208,5.45902224325428,
133.09165335806));
#170642=CARTESIAN_POINT('Ctrl Pts',(-129.070288837854,5.39625678311652,
133.236054184069));
#170643=CARTESIAN_POINT('Ctrl Pts',(-129.0628814915,5.32777472109283,133.377830470466));
#170644=CARTESIAN_POINT('Ctrl Pts',(-129.055479669825,5.25934373557468,
133.519501014759));
#170645=CARTESIAN_POINT('Ctrl Pts',(-129.048077848149,5.1852047993536,133.658550582357));
#170646=CARTESIAN_POINT('Ctrl Pts',(-129.040676026474,5.1055896516041,133.794491864173));
#170647=CARTESIAN_POINT('Ctrl Pts',(-129.033278112163,5.02601653207136,
133.930361383644));
#170648=CARTESIAN_POINT('Ctrl Pts',(-129.025880197851,4.94097314645032,
134.063125563839));
#170649=CARTESIAN_POINT('Ctrl Pts',(-129.01848228354,4.85073734267355,134.19232133087));
#170650=CARTESIAN_POINT('Ctrl Pts',(-129.011085598628,4.76051653445046,
134.321495627908));
#170651=CARTESIAN_POINT('Ctrl Pts',(-129.003688913716,4.66510523418736,
134.447102382981));
#170652=CARTESIAN_POINT('Ctrl Pts',(-128.996292228803,4.56482488319306,
134.568707087842));
#170653=CARTESIAN_POINT('Ctrl Pts',(-128.988895871868,4.46454897873461,
134.690306400624));
#170654=CARTESIAN_POINT('Ctrl Pts',(-128.981499514933,4.3594046903236,134.807903728032));
#170655=CARTESIAN_POINT('Ctrl Pts',(-128.974103157997,4.24975388069575,
134.921097494755));
#170656=CARTESIAN_POINT('Ctrl Pts',(-128.966705668661,4.14008628324903,
135.034308591733));
#170657=CARTESIAN_POINT('Ctrl Pts',(-128.959308179324,4.02591105053221,
135.14311451747));
#170658=CARTESIAN_POINT('Ctrl Pts',(-128.951910689988,3.90762692987578,
135.247150545011));
#170659=CARTESIAN_POINT('Ctrl Pts',(-128.944510607473,3.78930134490406,
135.351223042221));
#170660=CARTESIAN_POINT('Ctrl Pts',(-128.937110524958,3.66686428436636,
135.450522065752));
#170661=CARTESIAN_POINT('Ctrl Pts',(-128.929710442443,3.54074745597937,
135.544723263554));
#170662=CARTESIAN_POINT('Ctrl Pts',(-128.922302222776,3.41449194917462,
135.639028045257));
#170663=CARTESIAN_POINT('Ctrl Pts',(-128.91489400311,3.28454889308884,135.728223582984));
#170664=CARTESIAN_POINT('Ctrl Pts',(-128.907485783443,3.15137945623144,
135.812028546387));
#170665=CARTESIAN_POINT('Ctrl Pts',(-128.900073004141,3.01812805580732,
135.895885090347));
#170666=CARTESIAN_POINT('Ctrl Pts',(-128.892660224839,2.88164664057096,
135.974344263218));
#170667=CARTESIAN_POINT('Ctrl Pts',(-128.885247445537,2.74242036500662,
136.047171037951));
#170668=CARTESIAN_POINT('Ctrl Pts',(-128.877824074509,2.60299515641088,
136.120101870995));
#170669=CARTESIAN_POINT('Ctrl Pts',(-128.87040070348,2.46081759093237,136.187384073314));
#170670=CARTESIAN_POINT('Ctrl Pts',(-128.862977332451,2.31639290291346,
136.248830700304));
#170671=CARTESIAN_POINT('Ctrl Pts',(-128.85904128301,2.23981546789787,136.281411176328));
#170672=CARTESIAN_POINT('Ctrl Pts',(-128.855105233569,2.16260655337318,
136.312351891974));
#170673=CARTESIAN_POINT('Ctrl Pts',(-128.851169184128,2.0848429947869,136.341630725624));
#170674=CARTESIAN_POINT('Ctrl Pts',(-128.843745917723,1.93818335021957,
136.396849692123));
#170675=CARTESIAN_POINT('Ctrl Pts',(-128.836322651317,1.78910663711666,
136.446321510086));
#170676=CARTESIAN_POINT('Ctrl Pts',(-128.828899384912,1.63810385186479,
136.489828613519));
#170677=CARTESIAN_POINT('Ctrl Pts',(-128.821484892191,1.48727953936466,
136.533284295169));
#170678=CARTESIAN_POINT('Ctrl Pts',(-128.81407039947,1.33453404121955,136.570789192606));
#170679=CARTESIAN_POINT('Ctrl Pts',(-128.806655906749,1.18037808216392,
136.60217383857));
#170680=CARTESIAN_POINT('Ctrl Pts',(-128.799248560395,1.02637070442594,
136.63352823483));
#170681=CARTESIAN_POINT('Ctrl Pts',(-128.791841214041,0.870955935523697,
136.65877404925));
#170682=CARTESIAN_POINT('Ctrl Pts',(-128.784433867687,0.71465930317291,
136.677791696832));
#170683=CARTESIAN_POINT('Ctrl Pts',(-128.777032046012,0.558479242747264,
136.696795160335));
#170684=CARTESIAN_POINT('Ctrl Pts',(-128.769630224336,0.40141899746631,
136.709579661329));
#170685=CARTESIAN_POINT('Ctrl Pts',(-128.762228402661,0.244013814949968,
136.716076766081));
#170686=CARTESIAN_POINT('Ctrl Pts',(-128.75483048835,0.0866917254037876,
136.722570441062));
#170687=CARTESIAN_POINT('Ctrl Pts',(-128.747432574038,-0.0709745667012892,
136.722783314525));
#170688=CARTESIAN_POINT('Ctrl Pts',(-128.740034659727,-0.228445280593447,
136.716698845059));
#170689=CARTESIAN_POINT('Ctrl Pts',(-128.732637974815,-0.385889825709542,
136.710615386721));
#170690=CARTESIAN_POINT('Ctrl Pts',(-128.725241289902,-0.543138484464353,
136.698236676853));
#170691=CARTESIAN_POINT('Ctrl Pts',(-128.71784460499,-0.699651945885949,
136.679598290811));
#170692=CARTESIAN_POINT('Ctrl Pts',(-128.710448248055,-0.856158467336651,
136.660960731215));
#170693=CARTESIAN_POINT('Ctrl Pts',(-128.703051891119,-1.01192948559431,
136.636064091472));
#170694=CARTESIAN_POINT('Ctrl Pts',(-128.695655534184,-1.16643154832761,
136.604995755684));
#170695=CARTESIAN_POINT('Ctrl Pts',(-128.688258044847,-1.32095726572113,
136.573922663254));
#170696=CARTESIAN_POINT('Ctrl Pts',(-128.68086055551,-1.47421327475679,
136.536676066951));
#170697=CARTESIAN_POINT('Ctrl Pts',(-128.673463066174,-1.62567718764724,
136.493394300369));
#170698=CARTESIAN_POINT('Ctrl Pts',(-128.666062983659,-1.77719419597778,
136.45009736143));
#170699=CARTESIAN_POINT('Ctrl Pts',(-128.658662901144,-1.92691749868164,
136.400761142532));
#170700=CARTESIAN_POINT('Ctrl Pts',(-128.651262818629,-2.07434086062793,
136.345573531399));
#170701=CARTESIAN_POINT('Ctrl Pts',(-128.643854598962,-2.22192632971596,
136.290325235814));
#170702=CARTESIAN_POINT('Ctrl Pts',(-128.636446379296,-2.3672064576057,
136.229212829412));
#170703=CARTESIAN_POINT('Ctrl Pts',(-128.629038159629,-2.5096952802634,
136.162472240398));
#170704=CARTESIAN_POINT('Ctrl Pts',(-128.621625380327,-2.65227180241389,
136.095690573664));
#170705=CARTESIAN_POINT('Ctrl Pts',(-128.614212601025,-2.79205326530924,
136.023273993078));
#170706=CARTESIAN_POINT('Ctrl Pts',(-128.606799821723,-2.92857969618707,
135.945503634987));
#170707=CARTESIAN_POINT('Ctrl Pts',(-128.599376450694,-3.06530120243159,
135.867622154962));
#170708=CARTESIAN_POINT('Ctrl Pts',(-128.591953079665,-3.19875807179573,
135.784371816258));
#170709=CARTESIAN_POINT('Ctrl Pts',(-128.584529708637,-3.32851993098497,
135.696076638712));
#170710=CARTESIAN_POINT('Ctrl Pts',(-128.580593659196,-3.3973227823126,
135.649260416968));
#170711=CARTESIAN_POINT('Ctrl Pts',(-128.576657609756,-3.46508738689326,
135.601026583092));
#170712=CARTESIAN_POINT('Ctrl Pts',(-128.572721560316,-3.53175360174764,
135.551427823646));
#170713=CARTESIAN_POINT('Ctrl Pts',(-128.565370856845,-3.65625497916728,
135.458800487854));
#170714=CARTESIAN_POINT('Ctrl Pts',(-128.558020153374,-3.77731613250596,
135.361118238744));
#170715=CARTESIAN_POINT('Ctrl Pts',(-128.550669449903,-3.89449339699107,
135.258667717811));
#170716=CARTESIAN_POINT('Ctrl Pts',(-128.543327467855,-4.01153163363528,
135.156338751813));
#170717=CARTESIAN_POINT('Ctrl Pts',(-128.535985485806,-4.12469486664513,
135.049253019551));
#170718=CARTESIAN_POINT('Ctrl Pts',(-128.528643503758,-4.23356883529318,
134.937740043573));
#170719=CARTESIAN_POINT('Ctrl Pts',(-128.521308553125,-4.34233853535686,
134.826333863555));
#170720=CARTESIAN_POINT('Ctrl Pts',(-128.513973602492,-4.44682688166327,
134.710509148898));
#170721=CARTESIAN_POINT('Ctrl Pts',(-128.506638651858,-4.54665329278074,
134.590635092264));
#170722=CARTESIAN_POINT('Ctrl Pts',(-128.499309049148,-4.64640692032246,
134.470848435971));
#170723=CARTESIAN_POINT('Ctrl Pts',(-128.491979446438,-4.7415051355231,
134.347018606272));
#170724=CARTESIAN_POINT('Ctrl Pts',(-128.484649843727,-4.83160495263324,
134.219550823717));
#170725=CARTESIAN_POINT('Ctrl Pts',(-128.477323379202,-4.92166619330557,
134.092137616778));
#170726=CARTESIAN_POINT('Ctrl Pts',(-128.469996914678,-5.00673307380124,
133.961089866465));
#170727=CARTESIAN_POINT('Ctrl Pts',(-128.462670450153,-5.08650365374587,
133.826844884346));
#170728=CARTESIAN_POINT('Ctrl Pts',(-128.455345514147,-5.16625759116744,
133.692627909735));
#170729=CARTESIAN_POINT('Ctrl Pts',(-128.448020578142,-5.24071723147476,
133.555215357894));
#170730=CARTESIAN_POINT('Ctrl Pts',(-128.440695642136,-5.30962478121342,
133.415072253351));
#170731=CARTESIAN_POINT('Ctrl Pts',(-128.433370718813,-5.37853221164376,
133.274929391456));
#170732=CARTESIAN_POINT('Ctrl Pts',(-128.42604579549,-5.441887402354,133.132056328493));
#170733=CARTESIAN_POINT('Ctrl Pts',(-128.418720872167,-5.49947933825294,
132.986941101908));
#170734=CARTESIAN_POINT('Ctrl Pts',(-128.411394445916,-5.55708309087056,
132.841796100567));
#170735=CARTESIAN_POINT('Ctrl Pts',(-128.404068019664,-5.60892109517581,
132.69440837462));
#170736=CARTESIAN_POINT('Ctrl Pts',(-128.396741593413,-5.65483123213515,
132.545284021559));
#170737=CARTESIAN_POINT('Ctrl Pts',(-128.389408124028,-5.70078550401455,
132.396016310367));
#170738=CARTESIAN_POINT('Ctrl Pts',(-128.382074654642,-5.74080041454549,
132.245009002581));
#170739=CARTESIAN_POINT('Ctrl Pts',(-128.374741185257,-5.77476415054914,
132.092781964809));
#170740=CARTESIAN_POINT('Ctrl Pts',(-128.367404016875,-5.80874501783938,
131.940478143818));
#170741=CARTESIAN_POINT('Ctrl Pts',(-128.360066848492,-5.83666856210573,
131.786953741942));
#170742=CARTESIAN_POINT('Ctrl Pts',(-128.35272968011,-5.85847460091912,
131.632736083696));
#170743=CARTESIAN_POINT('Ctrl Pts',(-128.345382085172,-5.8803116274182,
131.478299272931));
#170744=CARTESIAN_POINT('Ctrl Pts',(-128.338034490234,-5.89601374437728,
131.323167616817));
#170745=CARTESIAN_POINT('Ctrl Pts',(-128.330686895297,-5.90557281670467,
131.167871647796));
#170746=CARTESIAN_POINT('Ctrl Pts',(-128.3249163276,-5.91308020850467,131.045907126086));
#170747=CARTESIAN_POINT('Ctrl Pts',(-128.319145759903,-5.91679959518812,
130.923841335279));
#170748=CARTESIAN_POINT('Ctrl Pts',(-128.313375192206,-5.91674950049016,
130.801929373134));
#170749=CARTESIAN_POINT('',(-126.563375192206,-5.9177375725148,130.809766839768));
#170750=CARTESIAN_POINT('Ctrl Pts',(-128.313375192206,-5.92532190149327,
130.801925850659));
#170751=CARTESIAN_POINT('Ctrl Pts',(-128.307008106971,-5.9260213244518,
130.66721635484));
#170752=CARTESIAN_POINT('Ctrl Pts',(-128.300641021737,-5.92182725011439,
130.532551188858));
#170753=CARTESIAN_POINT('Ctrl Pts',(-128.294273936502,-5.91260101588379,
130.398231675452));
#170754=CARTESIAN_POINT('Ctrl Pts',(-128.201458061898,-5.77810603617641,
128.440195517006));
#170755=CARTESIAN_POINT('Ctrl Pts',(-128.01582631269,-3.37042713891619,
124.671026986366));
#170756=CARTESIAN_POINT('Ctrl Pts',(-127.737378688876,3.3383490931192,124.653508167472));
#170757=CARTESIAN_POINT('Ctrl Pts',(-127.458931065064,6.97934559599797,
130.288322264368));
#170758=CARTESIAN_POINT('Ctrl Pts',(-127.180483441251,4.20666445614103,
136.397350397977));
#170759=CARTESIAN_POINT('Ctrl Pts',(-126.902035817438,-2.43173581192483,
137.366694156127));
#170760=CARTESIAN_POINT('Ctrl Pts',(-126.696333067756,-5.68500213269131,
133.627799485708));
#170761=CARTESIAN_POINT('Ctrl Pts',(-126.583446192679,-5.92170083184643,
131.235829725967));
#170762=CARTESIAN_POINT('Ctrl Pts',(-126.563375192206,-5.9177375725148,
130.809766839768));
#170763=CARTESIAN_POINT('',(-124.813375192206,-5.90693489644606,130.804324882377));
#170764=CARTESIAN_POINT('Ctrl Pts',(-126.563375192206,-5.9177375725148,
130.809766839768));
#170765=CARTESIAN_POINT('Ctrl Pts',(-126.490630318075,-5.90337322622243,
129.265554279451));
#170766=CARTESIAN_POINT('Ctrl Pts',(-126.325069569338,-4.49401215403822,
125.727844952722));
#170767=CARTESIAN_POINT('Ctrl Pts',(-126.066692945999,1.47590625823722,
123.963362061268));
#170768=CARTESIAN_POINT('Ctrl Pts',(-125.788245322187,6.55328921615238,
128.348355532103));
#170769=CARTESIAN_POINT('Ctrl Pts',(-125.509797698372,5.60851953039534,
134.990297693958));
#170770=CARTESIAN_POINT('Ctrl Pts',(-125.231350074562,-0.49020561238188,
137.785568177001));
#170771=CARTESIAN_POINT('Ctrl Pts',(-124.999209239171,-5.19913250634134,
134.767487955326));
#170772=CARTESIAN_POINT('Ctrl Pts',(-124.859884278386,-5.90688169119504,
131.796176362661));
#170773=CARTESIAN_POINT('Ctrl Pts',(-124.813375192206,-5.90693489644606,
130.804324882377));
#170774=CARTESIAN_POINT('',(-123.063375192206,-5.91786917663301,130.798966564578));
#170775=CARTESIAN_POINT('Ctrl Pts',(-124.813375192206,-5.90693489644606,
130.804324882377));
#170776=CARTESIAN_POINT('Ctrl Pts',(-124.767068403782,-5.90698787027343,
129.816787598437));
#170777=CARTESIAN_POINT('Ctrl Pts',(-124.627945740753,-5.20365792411555,
126.849932484951));
#170778=CARTESIAN_POINT('Ctrl Pts',(-124.396007203122,-0.505416379733264,
123.824237781003));
#170779=CARTESIAN_POINT('Ctrl Pts',(-124.117559579308,5.59938513102161,
126.606212611025));
#170780=CARTESIAN_POINT('Ctrl Pts',(-123.839111955496,6.55862525153711,
133.246080368117));
#170781=CARTESIAN_POINT('Ctrl Pts',(-123.560664331683,1.49080917254681,
137.642126959098));
#170782=CARTESIAN_POINT('Ctrl Pts',(-123.302085410586,-4.48761703300956,
135.889285280182));
#170783=CARTESIAN_POINT('Ctrl Pts',(-123.136322364094,-5.90346559078905,
132.347385160215));
#170784=CARTESIAN_POINT('Ctrl Pts',(-123.063375192206,-5.91786917663301,
130.798966564578));
#170785=CARTESIAN_POINT('',(-121.313375192206,-5.92147242173306,130.806864541253));
#170786=CARTESIAN_POINT('Ctrl Pts',(-123.063375192206,-5.91786917663301,
130.798966564578));
#170787=CARTESIAN_POINT('Ctrl Pts',(-123.04350648949,-5.92179229740345,
130.377222061529));
#170788=CARTESIAN_POINT('Ctrl Pts',(-122.930821912165,-5.68794946591629,
127.989632006443));
#170789=CARTESIAN_POINT('Ctrl Pts',(-122.725321460248,-2.44602925083019,
124.247341368356));
#170790=CARTESIAN_POINT('Ctrl Pts',(-122.44687383643,4.19446744113016,125.202217865403));
#170791=CARTESIAN_POINT('Ctrl Pts',(-122.16842621262,6.98045346581883,131.305189871789));
#170792=CARTESIAN_POINT('Ctrl Pts',(-121.889978588805,3.35174376952896,
136.947924260418));
#170793=CARTESIAN_POINT('Ctrl Pts',(-121.611530964993,-3.35705470917186,
136.945023791032));
#170794=CARTESIAN_POINT('Ctrl Pts',(-121.419329832793,-5.85843743252595,
133.0479081345));
#170795=CARTESIAN_POINT('Ctrl Pts',(-121.319944575197,-5.9259884994246,
130.945860215635));
#170796=CARTESIAN_POINT('Ctrl Pts',(-121.313375192206,-5.92524902604646,
130.806866138209));
#170797=CARTESIAN_POINT('',(-119.563375221739,-5.91298467060509,130.808541148921));
#170798=CARTESIAN_POINT('Ctrl Pts',(-121.313375192206,-5.91674947102406,
130.80686254413));
#170799=CARTESIAN_POINT('Ctrl Pts',(-121.306028534646,-5.91681510495363,
130.651646350502));
#170800=CARTESIAN_POINT('Ctrl Pts',(-121.298681877086,-5.91076878111168,
130.496180606544));
#170801=CARTESIAN_POINT('Ctrl Pts',(-121.291335219526,-5.89857784810465,
130.340992586354));
#170802=CARTESIAN_POINT('Ctrl Pts',(-121.283996845679,-5.88640066096616,
130.185979548188));
#170803=CARTESIAN_POINT('Ctrl Pts',(-121.276658471832,-5.86809268057159,
130.03124398736));
#170804=CARTESIAN_POINT('Ctrl Pts',(-121.269320097985,-5.84367323058927,
129.877314913949));
#170805=CARTESIAN_POINT('Ctrl Pts',(-121.261988318462,-5.81927572412734,
129.723524162481));
#170806=CARTESIAN_POINT('Ctrl Pts',(-121.254656538938,-5.78877773718004,
129.57053883055));
#170807=CARTESIAN_POINT('Ctrl Pts',(-121.247324759415,-5.75225051416586,
129.41888431507));
#170808=CARTESIAN_POINT('Ctrl Pts',(-121.239997890939,-5.71574775819199,
129.267331382377));
#170809=CARTESIAN_POINT('Ctrl Pts',(-121.232671022464,-5.67322389422861,
129.117107861219));
#170810=CARTESIAN_POINT('Ctrl Pts',(-121.225344153989,-5.62480147257169,
128.968730219949));
#170811=CARTESIAN_POINT('Ctrl Pts',(-121.21801976663,-5.57639544832839,
128.820402824195));
#170812=CARTESIAN_POINT('Ctrl Pts',(-121.210695379272,-5.52209495599299,
128.673920427593));
#170813=CARTESIAN_POINT('Ctrl Pts',(-121.203370991913,-5.46207273869829,
128.529785501271));
#170814=CARTESIAN_POINT('Ctrl Pts',(-121.19604772567,-5.40205970876471,
128.385672637106));
#170815=CARTESIAN_POINT('Ctrl Pts',(-121.188724459426,-5.3363268424924,
128.24390688063));
#170816=CARTESIAN_POINT('Ctrl Pts',(-121.181401193182,-5.26509537115889,
128.104971557964));
#170817=CARTESIAN_POINT('Ctrl Pts',(-121.174077531278,-5.19386005134228,
127.96602872892));
#170818=CARTESIAN_POINT('Ctrl Pts',(-121.166753869374,-5.11712570923675,
127.829916977633));
#170819=CARTESIAN_POINT('Ctrl Pts',(-121.15943020747,-5.03515983296668,
127.697095579147));
#170820=CARTESIAN_POINT('Ctrl Pts',(-121.152104633067,-4.9531725521544,
127.564239495725));
#170821=CARTESIAN_POINT('Ctrl Pts',(-121.144779058665,-4.86595121890948,
127.434675799529));
#170822=CARTESIAN_POINT('Ctrl Pts',(-121.137453484262,-4.77380683854971,
127.308835073286));
#170823=CARTESIAN_POINT('Ctrl Pts',(-121.130120271257,-4.68156637639744,
127.182863129029));
#170824=CARTESIAN_POINT('Ctrl Pts',(-121.122787058251,-4.58439284068438,
127.060622215841));
#170825=CARTESIAN_POINT('Ctrl Pts',(-121.115453845246,-4.48263815387548,
126.942510575951));
#170826=CARTESIAN_POINT('Ctrl Pts',(-121.108116577606,-4.38082720550211,
126.824333630512));
#170827=CARTESIAN_POINT('Ctrl Pts',(-121.100779309966,-4.27443032048298,
126.710290784522));
#170828=CARTESIAN_POINT('Ctrl Pts',(-121.093442042326,-4.16383600305346,
126.600743091889));
#170829=CARTESIAN_POINT('Ctrl Pts',(-121.086093879819,-4.05307746776123,
126.491032735493));
#170830=CARTESIAN_POINT('Ctrl Pts',(-121.078745717313,-3.93810933173165,
126.385831121878));
#170831=CARTESIAN_POINT('Ctrl Pts',(-121.071397554806,-3.81935351503993,
126.285459280996));
#170832=CARTESIAN_POINT('Ctrl Pts',(-121.065810275659,-3.72905585253458,
126.20914013415));
#170833=CARTESIAN_POINT('Ctrl Pts',(-121.060222996513,-3.63656901350179,
126.135612506084));
#170834=CARTESIAN_POINT('Ctrl Pts',(-121.054635717367,-3.54208899513348,
126.065000311253));
#170835=CARTESIAN_POINT('Ctrl Pts',(-121.047212450962,-3.41656271874957,
125.971184856541));
#170836=CARTESIAN_POINT('Ctrl Pts',(-121.039789184556,-3.28711687605227,
125.88221800333));
#170837=CARTESIAN_POINT('Ctrl Pts',(-121.032365918151,-3.15416262063407,
125.798445244221));
#170838=CARTESIAN_POINT('Ctrl Pts',(-121.02495142543,-3.02136550610423,
125.714771497555));
#170839=CARTESIAN_POINT('Ctrl Pts',(-121.017536932709,-2.88506854553574,
125.63627982236));
#170840=CARTESIAN_POINT('Ctrl Pts',(-121.010122439988,-2.74571521522359,
125.563274993443));
#170841=CARTESIAN_POINT('Ctrl Pts',(-121.002715093634,-2.60649619889814,
125.490340529328));
#170842=CARTESIAN_POINT('Ctrl Pts',(-120.99530774728,-2.46422700587418,
125.42288255534));
#170843=CARTESIAN_POINT('Ctrl Pts',(-120.987900400926,-2.31937919980076,
125.361162045951));
#170844=CARTESIAN_POINT('Ctrl Pts',(-120.980498579251,-2.1746394266855,
125.299487570047));
#170845=CARTESIAN_POINT('Ctrl Pts',(-120.973096757575,-2.02732521186773,
125.243542183947));
#170846=CARTESIAN_POINT('Ctrl Pts',(-120.9656949359,-1.87793167646206,125.193540429658));
#170847=CARTESIAN_POINT('Ctrl Pts',(-120.958297021589,-1.72861700474086,
125.143565070905));
#170848=CARTESIAN_POINT('Ctrl Pts',(-120.950899107277,-1.57722555156876,
125.099527213471));
#170849=CARTESIAN_POINT('Ctrl Pts',(-120.943501192966,-1.42427121927405,
125.061592813062));
#170850=CARTESIAN_POINT('Ctrl Pts',(-120.936104508054,-1.2713423052147,
125.023664716662));
#170851=CARTESIAN_POINT('Ctrl Pts',(-120.928707823141,-1.11685138947067,
124.991838154007));
#170852=CARTESIAN_POINT('Ctrl Pts',(-120.921311138229,-0.961326412262909,
124.966228888015));
#170853=CARTESIAN_POINT('Ctrl Pts',(-120.913914781294,-0.805808331195621,
124.940620757565));
#170854=CARTESIAN_POINT('Ctrl Pts',(-120.906518424358,-0.649256648170021,
124.921229436283));
#170855=CARTESIAN_POINT('Ctrl Pts',(-120.899122067423,-0.492208079267675,
124.908119292009));
#170856=CARTESIAN_POINT('Ctrl Pts',(-120.891724578086,-0.335135465828503,
124.895007140539));
#170857=CARTESIAN_POINT('Ctrl Pts',(-120.88432708875,-0.177566187066021,
124.888178111935));
#170858=CARTESIAN_POINT('Ctrl Pts',(-120.876929599413,-0.0200404953665216,
124.887644557027));
#170859=CARTESIAN_POINT('Ctrl Pts',(-120.869529516898,0.137540416720232,
124.887110815081));
#170860=CARTESIAN_POINT('Ctrl Pts',(-120.862129434383,0.295077338259973,
124.892876941955));
#170861=CARTESIAN_POINT('Ctrl Pts',(-120.854729351868,0.452031756016429,
124.904903197256));
#170862=CARTESIAN_POINT('Ctrl Pts',(-120.847321132202,0.609158761290738,
124.916942676661));
#170863=CARTESIAN_POINT('Ctrl Pts',(-120.839912912535,0.765701611180409,
124.935256003066));
#170864=CARTESIAN_POINT('Ctrl Pts',(-120.832504692869,0.921127908494123,
124.959751653855));
#170865=CARTESIAN_POINT('Ctrl Pts',(-120.825091913566,1.07664986809996,
124.984262381307));
#170866=CARTESIAN_POINT('Ctrl Pts',(-120.817679134264,1.23105354047714,
125.014962942686));
#170867=CARTESIAN_POINT('Ctrl Pts',(-120.810266354962,1.38381892657568,
125.051711163536));
#170868=CARTESIAN_POINT('Ctrl Pts',(-120.802842983934,1.53680259102208,
125.088511891967));
#170869=CARTESIAN_POINT('Ctrl Pts',(-120.795419612905,1.68814293574958,
125.131377436782));
#170870=CARTESIAN_POINT('Ctrl Pts',(-120.787996241876,1.83733647208646,
125.180116201572));
#170871=CARTESIAN_POINT('Ctrl Pts',(-120.784060192435,1.91644246490247,
125.205958664134));
#170872=CARTESIAN_POINT('Ctrl Pts',(-120.780124142994,1.99494525711013,
125.233451499228));
#170873=CARTESIAN_POINT('Ctrl Pts',(-120.776188093554,2.0727724291567,125.262560817914));
#170874=CARTESIAN_POINT('Ctrl Pts',(-120.768764827148,2.21955204673268,
125.317460084483));
#170875=CARTESIAN_POINT('Ctrl Pts',(-120.761341560743,2.36437101987972,
125.378277780744));
#170876=CARTESIAN_POINT('Ctrl Pts',(-120.753918294337,2.50671643732821,
125.444854738725));
#170877=CARTESIAN_POINT('Ctrl Pts',(-120.746503801616,2.64889361431474,
125.511353008271));
#170878=CARTESIAN_POINT('Ctrl Pts',(-120.739089308895,2.78860272008164,
125.583596833619));
#170879=CARTESIAN_POINT('Ctrl Pts',(-120.731674816174,2.92534762918201,
125.661377843831));
#170880=CARTESIAN_POINT('Ctrl Pts',(-120.72426746982,3.06196073839064,125.739083885776));
#170881=CARTESIAN_POINT('Ctrl Pts',(-120.716860123467,3.19561501636462,
125.822316304446));
#170882=CARTESIAN_POINT('Ctrl Pts',(-120.709452777113,3.3258360062163,125.910819423067));
#170883=CARTESIAN_POINT('Ctrl Pts',(-120.702050955438,3.45595987234043,
125.999256532723));
#170884=CARTESIAN_POINT('Ctrl Pts',(-120.694649133762,3.58265524158026,
126.092956306076));
#170885=CARTESIAN_POINT('Ctrl Pts',(-120.687247312087,3.70547398861345,
126.191618148903));
#170886=CARTESIAN_POINT('Ctrl Pts',(-120.679849397775,3.82822790058681,
126.290227908912));
#170887=CARTESIAN_POINT('Ctrl Pts',(-120.672451483464,3.94710897564502,
126.393794288467));
#170888=CARTESIAN_POINT('Ctrl Pts',(-120.665053569153,4.06169981378983,
126.501974630098));
#170889=CARTESIAN_POINT('Ctrl Pts',(-120.65765688424,4.17627160901574,126.610136994119));
#170890=CARTESIAN_POINT('Ctrl Pts',(-120.650260199328,4.28655431116285,
126.722911542422));
#170891=CARTESIAN_POINT('Ctrl Pts',(-120.642863514416,4.39216516102326,
126.839916676634));
#170892=CARTESIAN_POINT('Ctrl Pts',(-120.635467157481,4.49777132798792,
126.956916622715));
#170893=CARTESIAN_POINT('Ctrl Pts',(-120.628070800545,4.59870580443632,
127.078146504606));
#170894=CARTESIAN_POINT('Ctrl Pts',(-120.62067444361,4.69462432772869,127.203189560257));
#170895=CARTESIAN_POINT('Ctrl Pts',(-120.613276954273,4.79055753639185,
127.328251760319));
#170896=CARTESIAN_POINT('Ctrl Pts',(-120.605879464937,4.88147303557931,
127.457128000367));
#170897=CARTESIAN_POINT('Ctrl Pts',(-120.5984819756,4.96706841457714,127.589370426693));
#170898=CARTESIAN_POINT('Ctrl Pts',(-120.591081893085,5.05269379890177,
127.721659210395));
#170899=CARTESIAN_POINT('Ctrl Pts',(-120.58368181057,5.13299514720268,127.857316216583));
#170900=CARTESIAN_POINT('Ctrl Pts',(-120.576281728055,5.20771481463843,
127.995866898168));
#170901=CARTESIAN_POINT('Ctrl Pts',(-120.568873508389,5.28251664403043,
128.134569930472));
#170902=CARTESIAN_POINT('Ctrl Pts',(-120.561465288722,5.35172435800186,
128.276172663858));
#170903=CARTESIAN_POINT('Ctrl Pts',(-120.554057069056,5.41512718343709,
128.42017770728));
#170904=CARTESIAN_POINT('Ctrl Pts',(-120.546644289754,5.47856903225344,
128.564271383403));
#170905=CARTESIAN_POINT('Ctrl Pts',(-120.539231510452,5.53619873691977,
128.710769969241));
#170906=CARTESIAN_POINT('Ctrl Pts',(-120.53181873115,5.58785484064342,128.859159126101));
#170907=CARTESIAN_POINT('Ctrl Pts',(-120.524395360121,5.63958475303057,
129.007760308347));
#170908=CARTESIAN_POINT('Ctrl Pts',(-120.516971989092,5.68532390918129,
129.158257100569));
#170909=CARTESIAN_POINT('Ctrl Pts',(-120.509548618064,5.72496135665502,
129.310122340949));
#170910=CARTESIAN_POINT('Ctrl Pts',(-120.505612568623,5.74597808239354,
129.390644935357));
#170911=CARTESIAN_POINT('Ctrl Pts',(-120.501676519182,5.7652802583171,129.471552106675));
#170912=CARTESIAN_POINT('Ctrl Pts',(-120.497740469741,5.78285725161436,
129.552764608483));
#170913=CARTESIAN_POINT('Ctrl Pts',(-120.490317203336,5.81600691241305,
129.705928852335));
#170914=CARTESIAN_POINT('Ctrl Pts',(-120.48289393693,5.84311745448787,129.860642606314));
#170915=CARTESIAN_POINT('Ctrl Pts',(-120.475470670525,5.86404554929174,
130.016388309466));
#170916=CARTESIAN_POINT('Ctrl Pts',(-120.468056177804,5.88494890882558,
130.171949934132));
#170917=CARTESIAN_POINT('Ctrl Pts',(-120.460641685083,5.89968431676038,
130.328540713836));
#170918=CARTESIAN_POINT('Ctrl Pts',(-120.453227192362,5.90815891354594,
130.485630614605));
#170919=CARTESIAN_POINT('Ctrl Pts',(-120.445819846008,5.91662534219603,
130.642569106213));
#170920=CARTESIAN_POINT('Ctrl Pts',(-120.438412499654,5.91884295303603,
130.800005390914));
#170921=CARTESIAN_POINT('Ctrl Pts',(-120.431005153301,5.91477039864094,
130.957402095149));
#170922=CARTESIAN_POINT('Ctrl Pts',(-120.423603331625,5.91070088171053,
131.114681406986));
#170923=CARTESIAN_POINT('Ctrl Pts',(-120.41620150995,5.90035055045421,131.271920825569));
#170924=CARTESIAN_POINT('Ctrl Pts',(-120.408799688274,5.883730080621,131.428580851855));
#170925=CARTESIAN_POINT('Ctrl Pts',(-120.401401773963,5.86711838460459,
131.585158178531));
#170926=CARTESIAN_POINT('Ctrl Pts',(-120.394003859652,5.84424318123347,
131.741156351762));
#170927=CARTESIAN_POINT('Ctrl Pts',(-120.38660594534,5.81516714304668,131.896038986377));
#170928=CARTESIAN_POINT('Ctrl Pts',(-120.379209260428,5.78609593676982,
132.050895882309));
#170929=CARTESIAN_POINT('Ctrl Pts',(-120.371812575516,5.75082600965621,
132.204637241024));
#170930=CARTESIAN_POINT('Ctrl Pts',(-120.364415890604,5.70947152052425,
132.356734773117));
#170931=CARTESIAN_POINT('Ctrl Pts',(-120.357019533668,5.66811886509379,
132.508825561046));
#170932=CARTESIAN_POINT('Ctrl Pts',(-120.349623176733,5.62068228203217,
132.659272307061));
#170933=CARTESIAN_POINT('Ctrl Pts',(-120.342226819798,5.56732632268922,
132.807560103187));
#170934=CARTESIAN_POINT('Ctrl Pts',(-120.334829330461,5.51396219441252,
132.955870602553));
#170935=CARTESIAN_POINT('Ctrl Pts',(-120.327431841124,5.45467701174053,
133.102021142604));
#170936=CARTESIAN_POINT('Ctrl Pts',(-120.320034351788,5.38968410630416,
133.245515220772));
#170937=CARTESIAN_POINT('Ctrl Pts',(-120.312634269273,5.32466841770544,
133.389059600567));
#170938=CARTESIAN_POINT('Ctrl Pts',(-120.305234186758,5.25394117661835,
133.529945324598));
#170939=CARTESIAN_POINT('Ctrl Pts',(-120.297834104243,5.1777623696189,133.667699124669));
#170940=CARTESIAN_POINT('Ctrl Pts',(-120.290425884576,5.10149979619011,
133.805604399204));
#170941=CARTESIAN_POINT('Ctrl Pts',(-120.28301766491,5.0197738660886,133.940370545267));
#170942=CARTESIAN_POINT('Ctrl Pts',(-120.275609445243,4.93288912047083,
134.071551381455));
#170943=CARTESIAN_POINT('Ctrl Pts',(-120.268196665941,4.84595089874188,
134.202812957259));
#170944=CARTESIAN_POINT('Ctrl Pts',(-120.260783886639,4.7538477524764,134.330484524025));
#170945=CARTESIAN_POINT('Ctrl Pts',(-120.253371107337,4.65692513804388,
134.454152230954));
#170946=CARTESIAN_POINT('Ctrl Pts',(-120.245947736308,4.5598640360345,134.577996640102));
#170947=CARTESIAN_POINT('Ctrl Pts',(-120.23852436528,4.45796995358772,134.697825479856));
#170948=CARTESIAN_POINT('Ctrl Pts',(-120.231100994251,4.35162643436671,
134.813260458947));
#170949=CARTESIAN_POINT('Ctrl Pts',(-120.22716494481,4.29524054879861,134.874466854684));
#170950=CARTESIAN_POINT('Ctrl Pts',(-120.223228895369,4.23760435172856,
134.934438624318));
#170951=CARTESIAN_POINT('Ctrl Pts',(-120.219292845929,4.17877876812081,
134.993123987536));
#170952=CARTESIAN_POINT('Ctrl Pts',(-120.211869579523,4.06783555331918,
135.103802751059));
#170953=CARTESIAN_POINT('Ctrl Pts',(-120.204446313118,3.95232440057861,
135.210238181037));
#170954=CARTESIAN_POINT('Ctrl Pts',(-120.197023046713,3.83260327600736,
135.312029936764));
#170955=CARTESIAN_POINT('Ctrl Pts',(-120.189608553992,3.7130236518628,135.413701383089));
#170956=CARTESIAN_POINT('Ctrl Pts',(-120.18219406127,3.58924424193811,135.510739840486));
#170957=CARTESIAN_POINT('Ctrl Pts',(-120.174779568549,3.46166078596998,
135.602780687274));
#170958=CARTESIAN_POINT('Ctrl Pts',(-120.167372222196,3.33420029974052,
135.694732821629));
#170959=CARTESIAN_POINT('Ctrl Pts',(-120.159964875842,3.20294336742124,
135.781696717911));
#170960=CARTESIAN_POINT('Ctrl Pts',(-120.152557529488,3.06831974731346,
135.863347125825));
#170961=CARTESIAN_POINT('Ctrl Pts',(-120.145155707813,2.93379653457985,
135.944936635785));
#170962=CARTESIAN_POINT('Ctrl Pts',(-120.137753886137,2.79591195160947,
136.021220355493));
#170963=CARTESIAN_POINT('Ctrl Pts',(-120.130352064462,2.6551256647309,136.091915654347));
#170964=CARTESIAN_POINT('Ctrl Pts',(-120.12295415015,2.51441369783769,136.162573633703));
#170965=CARTESIAN_POINT('Ctrl Pts',(-120.115556235839,2.37080341041977,
136.227648900347));
#170966=CARTESIAN_POINT('Ctrl Pts',(-120.108158321528,2.22477995455184,
136.286904253172));
#170967=CARTESIAN_POINT('Ctrl Pts',(-120.100761636616,2.07878076513294,
136.346149758833));
#170968=CARTESIAN_POINT('Ctrl Pts',(-120.093364951703,1.93036954874399,
136.399577129983));
#170969=CARTESIAN_POINT('Ctrl Pts',(-120.085968266791,1.78005247585254,
136.446996858341));
#170970=CARTESIAN_POINT('Ctrl Pts',(-120.078571909856,1.62974206817806,
136.494414484059));
#170971=CARTESIAN_POINT('Ctrl Pts',(-120.07117555292,1.47752632803416,136.535824884343));
#170972=CARTESIAN_POINT('Ctrl Pts',(-120.063779195985,1.32392740610855,
136.571088180565));
#170973=CARTESIAN_POINT('Ctrl Pts',(-120.056381706648,1.17030496779544,
136.606356875688));
#170974=CARTESIAN_POINT('Ctrl Pts',(-120.048984217312,1.01529928989712,
136.635476509285));
#170975=CARTESIAN_POINT('Ctrl Pts',(-120.041586727975,0.859443405042454,
136.658358191534));
#170976=CARTESIAN_POINT('Ctrl Pts',(-120.03418664546,0.703532885148287,
136.681247894922));
#170977=CARTESIAN_POINT('Ctrl Pts',(-120.026786562945,0.546771934013165,
136.69789523906));
#170978=CARTESIAN_POINT('Ctrl Pts',(-120.01938648043,0.389699254668284,
136.708263144997));
#170979=CARTESIAN_POINT('Ctrl Pts',(-120.011978260763,0.232453857765671,
136.718642451513));
#170980=CARTESIAN_POINT('Ctrl Pts',(-120.004570041097,0.0748964208206027,
136.722728505713));
#170981=CARTESIAN_POINT('Ctrl Pts',(-119.99716182143,-0.0824330591834801,
136.720536354751));
#170982=CARTESIAN_POINT('Ctrl Pts',(-119.989749042128,-0.239859372857322,
136.718342854556));
#170983=CARTESIAN_POINT('Ctrl Pts',(-119.982336262826,-0.397057078125725,
136.709863469495));
#170984=CARTESIAN_POINT('Ctrl Pts',(-119.974923483524,-0.553491262984103,
136.695165145328));
#170985=CARTESIAN_POINT('Ctrl Pts',(-119.967500112495,-0.71014896834162,
136.680445819506));
#170986=CARTESIAN_POINT('Ctrl Pts',(-119.960076741466,-0.866040605419736,
136.659489857023));
#170987=CARTESIAN_POINT('Ctrl Pts',(-119.952653370438,-1.02064059234089,
136.632415468352));
#170988=CARTESIAN_POINT('Ctrl Pts',(-119.948717320997,-1.10261321498006,
136.618059977838));
#170989=CARTESIAN_POINT('Ctrl Pts',(-119.944781271556,-1.1842229356191,
136.60198521928));
#170990=CARTESIAN_POINT('Ctrl Pts',(-119.940845222116,-1.26539325858399,
136.584214462053));
#170991=CARTESIAN_POINT('Ctrl Pts',(-119.93342195571,-1.41847795446017,
136.550699368529));
#170992=CARTESIAN_POINT('Ctrl Pts',(-119.925998689305,-1.57046169568063,
136.511047514015));
#170993=CARTESIAN_POINT('Ctrl Pts',(-119.918575422899,-1.72081417484769,
136.465343671607));
#170994=CARTESIAN_POINT('Ctrl Pts',(-119.911160930178,-1.87098894987038,
136.419693847346));
#170995=CARTESIAN_POINT('Ctrl Pts',(-119.903746437457,-2.01953594689331,
136.36800638068));
#170996=CARTESIAN_POINT('Ctrl Pts',(-119.896331944736,-2.16593449237795,
136.310417131735));
#170997=CARTESIAN_POINT('Ctrl Pts',(-119.888924598383,-2.31219193343265,
136.252883389477));
#170998=CARTESIAN_POINT('Ctrl Pts',(-119.881517252029,-2.45630470036704,
136.189459325079));
#170999=CARTESIAN_POINT('Ctrl Pts',(-119.874109905675,-2.59776685603759,
136.120330700643));
#171000=CARTESIAN_POINT('Ctrl Pts',(-119.866708084,-2.73912350389537,136.051253634944));
#171001=CARTESIAN_POINT('Ctrl Pts',(-119.859306262324,-2.87783314286533,
135.976480644033));
#171002=CARTESIAN_POINT('Ctrl Pts',(-119.851904440649,-3.01340952693938,
135.896245689467));
#171003=CARTESIAN_POINT('Ctrl Pts',(-119.844506526338,-3.14891434129483,
135.81605309031));
#171004=CARTESIAN_POINT('Ctrl Pts',(-119.837108612027,-3.28128887437365,
135.730404459425));
#171005=CARTESIAN_POINT('Ctrl Pts',(-119.829710697715,-3.41007132562115,
135.639579756));
#171006=CARTESIAN_POINT('Ctrl Pts',(-119.822314012803,-3.53883237556252,
135.548770145992));
#171007=CARTESIAN_POINT('Ctrl Pts',(-119.814917327891,-3.66400222365588,
135.452786385564));
#171008=CARTESIAN_POINT('Ctrl Pts',(-119.807520642979,-3.7851478337164,
135.351951896409));
#171009=CARTESIAN_POINT('Ctrl Pts',(-119.800124286043,-3.90628807205363,
135.251121878362));
#171010=CARTESIAN_POINT('Ctrl Pts',(-119.792727929108,-4.02340414023981,
135.145441798064));
#171011=CARTESIAN_POINT('Ctrl Pts',(-119.785331572172,-4.13609611922292,
135.035275347864));
#171012=CARTESIAN_POINT('Ctrl Pts',(-119.777934082836,-4.24880535163569,
134.925092030898));
#171013=CARTESIAN_POINT('Ctrl Pts',(-119.770536593499,-4.35708887921984,
134.81042123734));
#171014=CARTESIAN_POINT('Ctrl Pts',(-119.763139104163,-4.46058379929442,
134.691663375517));
#171015=CARTESIAN_POINT('Ctrl Pts',(-119.755739021648,-4.56411499935235,
134.57286388331));
#171016=CARTESIAN_POINT('Ctrl Pts',(-119.748338939133,-4.66285400463935,
134.449974751562));
#171017=CARTESIAN_POINT('Ctrl Pts',(-119.740938856618,-4.75647843743766,
134.323429164311));
#171018=CARTESIAN_POINT('Ctrl Pts',(-119.733530636952,-4.85020581992532,
134.196744427177));
#171019=CARTESIAN_POINT('Ctrl Pts',(-119.726122417285,-4.93880717627017,
134.06639550532));
#171020=CARTESIAN_POINT('Ctrl Pts',(-119.718714197619,-5.02200328450927,
133.93284484685));
#171021=CARTESIAN_POINT('Ctrl Pts',(-119.711301418317,-5.10525059856455,
133.799211990178));
#171022=CARTESIAN_POINT('Ctrl Pts',(-119.703888639014,-5.1830858512289,
133.662373793921));
#171023=CARTESIAN_POINT('Ctrl Pts',(-119.696475859712,-5.25527623286301,
133.522816480516));
#171024=CARTESIAN_POINT('Ctrl Pts',(-119.689052488684,-5.32756976349968,
133.383059761077));
#171025=CARTESIAN_POINT('Ctrl Pts',(-119.681629117655,-5.39420215646452,
133.240576502124));
#171026=CARTESIAN_POINT('Ctrl Pts',(-119.674205746626,-5.4549887757349,
133.095872786224));
#171027=CARTESIAN_POINT('Ctrl Pts',(-119.670269697185,-5.48721929983094,
133.019147403926));
#171028=CARTESIAN_POINT('Ctrl Pts',(-119.666333647744,-5.51780719763373,
132.941798034986));
#171029=CARTESIAN_POINT('Ctrl Pts',(-119.662397598302,-5.54673069854685,
132.863901615045));
#171030=CARTESIAN_POINT('Ctrl Pts',(-119.653853459437,-5.60951609084795,
132.694808762161));
#171031=CARTESIAN_POINT('Ctrl Pts',(-119.645309320571,-5.6646129739838,
132.522714853274));
#171032=CARTESIAN_POINT('Ctrl Pts',(-119.636765181705,-5.71176372379817,
132.34827956816));
#171033=CARTESIAN_POINT('Ctrl Pts',(-119.628251478122,-5.75874651679441,
132.174465643164));
#171034=CARTESIAN_POINT('Ctrl Pts',(-119.619737774538,-5.79783959119408,
131.998327121539));
#171035=CARTESIAN_POINT('Ctrl Pts',(-119.611224070954,-5.82883457131893,
131.820538802087));
#171036=CARTESIAN_POINT('Ctrl Pts',(-119.602770336281,-5.8596112286944,
131.64400278977));
#171037=CARTESIAN_POINT('Ctrl Pts',(-119.594316601608,-5.882403397313,131.465840283061));
#171038=CARTESIAN_POINT('Ctrl Pts',(-119.585862866934,-5.89705423531172,
131.286731748846));
#171039=CARTESIAN_POINT('Ctrl Pts',(-119.578366998354,-5.91004503292618,
131.127917439438));
#171040=CARTESIAN_POINT('Ctrl Pts',(-119.570871129774,-5.91663550731186,
130.96835967698));
#171041=CARTESIAN_POINT('Ctrl Pts',(-119.563375261194,-5.91674852062905,
130.808544650777));
#171042=CARTESIAN_POINT('',(-117.813375192206,-5.91000238445492,130.800267657125));
#171043=CARTESIAN_POINT('Ctrl Pts',(-119.563375192206,-5.91016724854547,
130.808538527613));
#171044=CARTESIAN_POINT('Ctrl Pts',(-119.5035667863,-5.90190641363403,129.534810380383));
#171045=CARTESIAN_POINT('Ctrl Pts',(-119.35094250579,-4.87179864722807,
126.272220221406));
#171046=CARTESIAN_POINT('Ctrl Pts',(-119.105502350678,0.511451736149495,
123.824677411885));
#171047=CARTESIAN_POINT('Ctrl Pts',(-118.827054726865,6.14865731213414,
127.461970187318));
#171048=CARTESIAN_POINT('Ctrl Pts',(-118.54860710305,6.13554719689485,134.170756483371));
#171049=CARTESIAN_POINT('Ctrl Pts',(-118.270159479238,0.484168945789873,
137.785989436281));
#171050=CARTESIAN_POINT('Ctrl Pts',(-118.025082175625,-4.88153028890003,
135.32107526904));
#171051=CARTESIAN_POINT('Ctrl Pts',(-117.872820746612,-5.90197269538057,
132.066356888141));
#171052=CARTESIAN_POINT('Ctrl Pts',(-117.813375192206,-5.91000238445492,
130.800267657125));
#171053=CARTESIAN_POINT('',(-116.063375192205,-5.92511385651394,130.801729663424));
#171054=CARTESIAN_POINT('Ctrl Pts',(-117.813375192206,-5.91000238445492,
130.800267657125));
#171055=CARTESIAN_POINT('Ctrl Pts',(-117.780004872008,-5.9145099258207,
130.089536577909));
#171056=CARTESIAN_POINT('Ctrl Pts',(-117.653818677207,-5.46638774170925,
127.407478954535));
#171057=CARTESIAN_POINT('Ctrl Pts',(-117.4348166078,-1.46999045857098,123.962088437774));
#171058=CARTESIAN_POINT('Ctrl Pts',(-117.156368983987,4.96203161869359,
125.869200767536));
#171059=CARTESIAN_POINT('Ctrl Pts',(-116.877921360174,6.83418904709124,
132.311483903476));
#171060=CARTESIAN_POINT('Ctrl Pts',(-116.599473736361,2.42606060991088,
137.368794366749));
#171061=CARTESIAN_POINT('Ctrl Pts',(-116.327958347038,-4.04625026551561,
136.417986591368));
#171062=CARTESIAN_POINT('Ctrl Pts',(-116.14925883232,-5.91503838326621,
132.618953446528));
#171063=CARTESIAN_POINT('Ctrl Pts',(-116.063375192205,-5.92511385651394,
130.801729663424));
#171064=CARTESIAN_POINT('',(-114.313375192205,-5.91789950705419,130.809730098004));
#171065=CARTESIAN_POINT('Ctrl Pts',(-116.063375192205,-5.92511385651394,
130.801729663424));
#171066=CARTESIAN_POINT('Ctrl Pts',(-116.056442957715,-5.92592711434814,
130.655049558007));
#171067=CARTESIAN_POINT('Ctrl Pts',(-116.049510723225,-5.92095444110238,
130.508425518448));
#171068=CARTESIAN_POINT('Ctrl Pts',(-116.042578488735,-5.91001924693745,
130.3622475195));
#171069=CARTESIAN_POINT('Ctrl Pts',(-115.949762614131,-5.7636076372569,
128.405066348045));
#171070=CARTESIAN_POINT('Ctrl Pts',(-115.764130864921,-3.33302935004614,
124.650623876197));
#171071=CARTESIAN_POINT('Ctrl Pts',(-115.48568324111,3.37572922592766,124.673943606988));
#171072=CARTESIAN_POINT('Ctrl Pts',(-115.207235617296,6.98235755681463,
130.330817082983));
#171073=CARTESIAN_POINT('Ctrl Pts',(-114.928787993484,4.17254040011804,
136.422853933367));
#171074=CARTESIAN_POINT('Ctrl Pts',(-114.650340369671,-2.47163754435426,
137.351769905191));
#171075=CARTESIAN_POINT('Ctrl Pts',(-114.445202769245,-5.69320852440163,
133.603467437331));
#171076=CARTESIAN_POINT('Ctrl Pts',(-114.332881043423,-5.92195457526042,
131.22373034605));
#171077=CARTESIAN_POINT('Ctrl Pts',(-114.313375192205,-5.91810510348369,
130.809730284548));
#171078=CARTESIAN_POINT('',(-112.563375192235,-5.91674999772218,130.804524796032));
#171079=CARTESIAN_POINT('Ctrl Pts',(-114.313375192205,-5.91674756453265,
130.809729052814));
#171080=CARTESIAN_POINT('Ctrl Pts',(-114.306070857519,-5.91688819427679,
130.654735901592));
#171081=CARTESIAN_POINT('Ctrl Pts',(-114.298766522834,-5.91093444397203,
130.499551867607));
#171082=CARTESIAN_POINT('Ctrl Pts',(-114.291462188148,-5.89886813750953,
130.344702854905));
#171083=CARTESIAN_POINT('Ctrl Pts',(-114.284163478904,-5.88681112392603,
130.189973099337));
#171084=CARTESIAN_POINT('Ctrl Pts',(-114.27686476966,-5.86865095246589,
130.035578233295));
#171085=CARTESIAN_POINT('Ctrl Pts',(-114.269566060416,-5.84442151256597,
129.882044106841));
#171086=CARTESIAN_POINT('Ctrl Pts',(-114.262227687984,-5.82006040324443,
129.727675633835));
#171087=CARTESIAN_POINT('Ctrl Pts',(-114.254889315551,-5.78956386125597,
129.574177676706));
#171088=CARTESIAN_POINT('Ctrl Pts',(-114.247550943119,-5.75301928217937,
129.422080001565));
#171089=CARTESIAN_POINT('Ctrl Pts',(-114.240257380979,-5.71669785520761,
129.270911080214));
#171090=CARTESIAN_POINT('Ctrl Pts',(-114.232963818839,-5.67440215317019,
129.12112576259));
#171091=CARTESIAN_POINT('Ctrl Pts',(-114.225670256699,-5.62626920573315,
128.973233809527));
#171092=CARTESIAN_POINT('Ctrl Pts',(-114.218376881327,-5.57813749085329,
128.825345643585));
#171093=CARTESIAN_POINT('Ctrl Pts',(-114.211083505956,-5.52416894682227,
128.679351111731));
#171094=CARTESIAN_POINT('Ctrl Pts',(-114.203790130584,-5.46455023345578,
128.53574401079));
#171095=CARTESIAN_POINT('Ctrl Pts',(-114.196495407217,-5.40492050107706,
128.392110367707));
#171096=CARTESIAN_POINT('Ctrl Pts',(-114.189200683849,-5.33963866932655,
128.250865388737));
#171097=CARTESIAN_POINT('Ctrl Pts',(-114.181905960482,-5.26893909120866,
128.112481828387));
#171098=CARTESIAN_POINT('Ctrl Pts',(-114.174534223945,-5.19749311075687,
127.972637300162));
#171099=CARTESIAN_POINT('Ctrl Pts',(-114.167162487409,-5.12051451299327,
127.835715315378));
#171100=CARTESIAN_POINT('Ctrl Pts',(-114.159790750873,-5.03829170692901,
127.702176348637));
#171101=CARTESIAN_POINT('Ctrl Pts',(-114.152485137341,-4.95680642302291,
127.569835199772));
#171102=CARTESIAN_POINT('Ctrl Pts',(-114.14517952381,-4.870170894451,127.440816910365));
#171103=CARTESIAN_POINT('Ctrl Pts',(-114.137873910279,-4.77870783924653,
127.315538187343));
#171104=CARTESIAN_POINT('Ctrl Pts',(-114.13046911224,-4.68600303780323,
127.188558620383));
#171105=CARTESIAN_POINT('Ctrl Pts',(-114.123064314201,-4.5883389364067,
127.065421216274));
#171106=CARTESIAN_POINT('Ctrl Pts',(-114.115659516162,-4.486091339419,126.946522485025));
#171107=CARTESIAN_POINT('Ctrl Pts',(-114.108254718123,-4.3838437424313,
126.827623753776));
#171108=CARTESIAN_POINT('Ctrl Pts',(-114.100849920084,-4.27701297370974,
126.71296394576));
#171109=CARTESIAN_POINT('Ctrl Pts',(-114.093445122045,-4.16601025747249,
126.602897884525));
#171110=CARTESIAN_POINT('Ctrl Pts',(-114.086021855639,-4.05473068846847,
126.492557306642));
#171111=CARTESIAN_POINT('Ctrl Pts',(-114.078598589234,-3.9388961179316,
126.386473945882));
#171112=CARTESIAN_POINT('Ctrl Pts',(-114.071175322828,-3.81886572881143,
126.285047051568));
#171113=CARTESIAN_POINT('Ctrl Pts',(-114.063760830108,-3.69897720564364,
126.183740035422));
#171114=CARTESIAN_POINT('Ctrl Pts',(-114.056346337387,-3.57490301737353,
126.087078769448));
#171115=CARTESIAN_POINT('Ctrl Pts',(-114.048931844666,-3.44704001168771,
125.99542666914));
#171116=CARTESIAN_POINT('Ctrl Pts',(-114.041524498312,-3.31930024518073,
125.903862906577));
#171117=CARTESIAN_POINT('Ctrl Pts',(-114.034117151958,-3.18777923264967,
125.817298914059));
#171118=CARTESIAN_POINT('Ctrl Pts',(-114.026709805605,-3.05290772035521,
125.736058632335));
#171119=CARTESIAN_POINT('Ctrl Pts',(-114.019307983929,-2.91813680032266,
125.654878942679));
#171120=CARTESIAN_POINT('Ctrl Pts',(-114.011906162254,-2.78002067462342,
125.579015249553));
#171121=CARTESIAN_POINT('Ctrl Pts',(-114.004504340578,-2.63901986768726,
125.508748783184));
#171122=CARTESIAN_POINT('Ctrl Pts',(-113.997106426267,-2.49809349397873,
125.438519409935));
#171123=CARTESIAN_POINT('Ctrl Pts',(-113.989708511956,-2.35428580502743,
125.37388154503));
#171124=CARTESIAN_POINT('Ctrl Pts',(-113.982310597644,-2.20808267261941,
125.315070911841));
#171125=CARTESIAN_POINT('Ctrl Pts',(-113.974913912732,-2.06190383652064,
125.256270051913));
#171126=CARTESIAN_POINT('Ctrl Pts',(-113.96751722782,-1.91333069302429,
125.203294640926));
#171127=CARTESIAN_POINT('Ctrl Pts',(-113.960120542908,-1.76286998705137,
125.156332645676));
#171128=CARTESIAN_POINT('Ctrl Pts',(-113.952724185972,-1.61241595266338,
125.109372732769));
#171129=CARTESIAN_POINT('Ctrl Pts',(-113.945327829037,-1.46007487855918,
125.068425816648));
#171130=CARTESIAN_POINT('Ctrl Pts',(-113.937931472102,-1.30636933875029,
125.033630186046));
#171131=CARTESIAN_POINT('Ctrl Pts',(-113.930533982765,-1.15264026623131,
124.998829228143));
#171132=CARTESIAN_POINT('Ctrl Pts',(-113.923136493428,-0.997546676162303,
124.97018151339));
#171133=CARTESIAN_POINT('Ctrl Pts',(-113.915739004092,-0.841621869253158,
124.947774308828));
#171134=CARTESIAN_POINT('Ctrl Pts',(-113.908338921577,-0.685642403144888,
124.925359249456));
#171135=CARTESIAN_POINT('Ctrl Pts',(-113.900938839062,-0.528831509329074,
124.909189108839));
#171136=CARTESIAN_POINT('Ctrl Pts',(-113.893538756547,-0.371728001197229,
124.899299326129));
#171137=CARTESIAN_POINT('Ctrl Pts',(-113.886130536881,-0.214451741607334,
124.889398668587));
#171138=CARTESIAN_POINT('Ctrl Pts',(-113.878722317214,-0.0568825979155635,
124.885792183953));
#171139=CARTESIAN_POINT('Ctrl Pts',(-113.871314097548,0.100439481194228,
124.888463181579));
#171140=CARTESIAN_POINT('Ctrl Pts',(-113.863901318246,0.2578583894191,124.891135823159));
#171141=CARTESIAN_POINT('Ctrl Pts',(-113.856488538944,0.415029558226182,
124.900093624685));
#171142=CARTESIAN_POINT('Ctrl Pts',(-113.849075759642,0.571418281848443,
124.915268012617));
#171143=CARTESIAN_POINT('Ctrl Pts',(-113.841652388613,0.728030461012253,
124.930464082425));
#171144=CARTESIAN_POINT('Ctrl Pts',(-113.834229017584,0.883857593268391,
124.95189442836));
#171145=CARTESIAN_POINT('Ctrl Pts',(-113.826805646555,1.03837445896579,
124.979439240803));
#171146=CARTESIAN_POINT('Ctrl Pts',(-113.822869597114,1.1203030087511,124.994044161291));
#171147=CARTESIAN_POINT('Ctrl Pts',(-113.818933547673,1.2018634253566,125.010367237311));
#171148=CARTESIAN_POINT('Ctrl Pts',(-113.814997498232,1.2829792842865,125.02838496677));
#171149=CARTESIAN_POINT('Ctrl Pts',(-113.807574231826,1.43596126266911,
125.06236584221));
#171150=CARTESIAN_POINT('Ctrl Pts',(-113.800150965421,1.58782361330608,
125.102480099287));
#171151=CARTESIAN_POINT('Ctrl Pts',(-113.792727699015,1.7380362892762,125.148641351225));
#171152=CARTESIAN_POINT('Ctrl Pts',(-113.785313206294,1.8880714263377,125.194748044397));
#171153=CARTESIAN_POINT('Ctrl Pts',(-113.777898713573,2.0364604164326,125.246887397611));
#171154=CARTESIAN_POINT('Ctrl Pts',(-113.770484220852,2.18268300194557,
125.30492196662));
#171155=CARTESIAN_POINT('Ctrl Pts',(-113.763076874499,2.32876465262585,
125.362900599727));
#171156=CARTESIAN_POINT('Ctrl Pts',(-113.755669528145,2.47268371100539,
125.426763000039));
#171157=CARTESIAN_POINT('Ctrl Pts',(-113.748262181791,2.61393480768006,
125.496321866417));
#171158=CARTESIAN_POINT('Ctrl Pts',(-113.740860360116,2.75508055395652,
125.565828853168));
#171159=CARTESIAN_POINT('Ctrl Pts',(-113.73345853844,2.89356196716893,125.641023682162));
#171160=CARTESIAN_POINT('Ctrl Pts',(-113.726056716765,3.02889351565995,
125.721670912961));
#171161=CARTESIAN_POINT('Ctrl Pts',(-113.718658802454,3.16415362367994,
125.802275570715));
#171162=CARTESIAN_POINT('Ctrl Pts',(-113.711260888142,3.29626685863876,
125.888326707427));
#171163=CARTESIAN_POINT('Ctrl Pts',(-113.703862973831,3.42477227422022,
125.97954295964));
#171164=CARTESIAN_POINT('Ctrl Pts',(-113.696466288919,3.55325633453347,
126.070744053368));
#171165=CARTESIAN_POINT('Ctrl Pts',(-113.689069604007,3.67813346129888,
126.167108343168));
#171166=CARTESIAN_POINT('Ctrl Pts',(-113.681672919095,3.7989716047218,126.268311090828));
#171167=CARTESIAN_POINT('Ctrl Pts',(-113.674276562159,3.91980439005481,
126.369509351053));
#171168=CARTESIAN_POINT('Ctrl Pts',(-113.666880205224,4.03659826195533,
126.475545402873));
#171169=CARTESIAN_POINT('Ctrl Pts',(-113.659483848288,4.14895441017811,
126.58605433841));
#171170=CARTESIAN_POINT('Ctrl Pts',(-113.652086358952,4.26132776041402,
126.696580193148));
#171171=CARTESIAN_POINT('Ctrl Pts',(-113.644688869615,4.36926176798573,
126.811580033369));
#171172=CARTESIAN_POINT('Ctrl Pts',(-113.637291380279,4.47239475059848,
126.93065234805));
#171173=CARTESIAN_POINT('Ctrl Pts',(-113.629891297764,4.57556388631827,
127.049766403346));
#171174=CARTESIAN_POINT('Ctrl Pts',(-113.622491215249,4.67392840200823,
127.172955493448));
#171175=CARTESIAN_POINT('Ctrl Pts',(-113.615091132734,4.76716723990703,
127.299785455117));
#171176=CARTESIAN_POINT('Ctrl Pts',(-113.607682913067,4.86050860349341,
127.426754879367));
#171177=CARTESIAN_POINT('Ctrl Pts',(-113.600274693401,4.94871281216255,
127.557372869507));
#171178=CARTESIAN_POINT('Ctrl Pts',(-113.592866473734,5.03150205277778,
127.691176129716));
#171179=CARTESIAN_POINT('Ctrl Pts',(-113.585453694432,5.11434224878921,
127.825061743598));
#171180=CARTESIAN_POINT('Ctrl Pts',(-113.57804091513,5.19176065252689,127.962136209765));
#171181=CARTESIAN_POINT('Ctrl Pts',(-113.570628135828,5.26352593532371,
128.10191259944));
#171182=CARTESIAN_POINT('Ctrl Pts',(-113.5632047648,5.33539375972193,128.241888708175));
#171183=CARTESIAN_POINT('Ctrl Pts',(-113.555781393771,5.40159217402192,
128.384574113239));
#171184=CARTESIAN_POINT('Ctrl Pts',(-113.548358022742,5.46193808339751,
128.529462172441));
#171185=CARTESIAN_POINT('Ctrl Pts',(-113.544421973301,5.49393493253177,
128.606285297979));
#171186=CARTESIAN_POINT('Ctrl Pts',(-113.54048592386,5.52428726378068,128.683727407679));
#171187=CARTESIAN_POINT('Ctrl Pts',(-113.536549874419,5.55297354081431,
128.761711499994));
#171188=CARTESIAN_POINT('Ctrl Pts',(-113.529126608013,5.60707496402698,
128.908787064288));
#171189=CARTESIAN_POINT('Ctrl Pts',(-113.521703341608,5.65541101341678,
129.05823589664));
#171190=CARTESIAN_POINT('Ctrl Pts',(-113.514280075202,5.69776786531719,
129.209565359403));
#171191=CARTESIAN_POINT('Ctrl Pts',(-113.506865582481,5.74007465493617,
129.360715963308));
#171192=CARTESIAN_POINT('Ctrl Pts',(-113.49945108976,5.77641621416304,129.513742417257));
#171193=CARTESIAN_POINT('Ctrl Pts',(-113.492036597039,5.80662696678625,
129.668132721811));
#171194=CARTESIAN_POINT('Ctrl Pts',(-113.484629250685,5.83680860114866,
129.822374219178));
#171195=CARTESIAN_POINT('Ctrl Pts',(-113.477221904332,5.86087112156129,
129.977976586287));
#171196=CARTESIAN_POINT('Ctrl Pts',(-113.469814557978,5.87869894527026,
130.134413400706));
#171197=CARTESIAN_POINT('Ctrl Pts',(-113.462412736302,5.89651347231566,
130.290733538646));
#171198=CARTESIAN_POINT('Ctrl Pts',(-113.455010914627,5.90810251949215,
130.447886515388));
#171199=CARTESIAN_POINT('Ctrl Pts',(-113.447609092951,5.91340172778835,
130.605336578089));
#171200=CARTESIAN_POINT('Ctrl Pts',(-113.44021117864,5.91869813867371,130.762703524127));
#171201=CARTESIAN_POINT('Ctrl Pts',(-113.432813264329,5.91771131080386,
130.920366871648));
#171202=CARTESIAN_POINT('Ctrl Pts',(-113.425415350017,5.91042881047856,
131.077786729642));
#171203=CARTESIAN_POINT('Ctrl Pts',(-113.418018665105,5.90314752037266,
131.235180427313));
#171204=CARTESIAN_POINT('Ctrl Pts',(-113.410621980193,5.88957265149538,
131.39233034323));
#171205=CARTESIAN_POINT('Ctrl Pts',(-113.403225295281,5.86974388183291,
131.548697452732));
#171206=CARTESIAN_POINT('Ctrl Pts',(-113.395828938345,5.84991599139886,
131.705057628752));
#171207=CARTESIAN_POINT('Ctrl Pts',(-113.38843258141,5.82383479851612,131.860634697041));
#171208=CARTESIAN_POINT('Ctrl Pts',(-113.381036224474,5.79159174383815,
132.014895885621));
#171209=CARTESIAN_POINT('Ctrl Pts',(-113.373638735138,5.75934375266629,
132.169180691983));
#171210=CARTESIAN_POINT('Ctrl Pts',(-113.366241245801,5.72093209765044,
132.32214885207));
#171211=CARTESIAN_POINT('Ctrl Pts',(-113.358843756465,5.67649908327068,
132.473279045808));
#171212=CARTESIAN_POINT('Ctrl Pts',(-113.35144367395,5.63205049296629,132.624462218003));
#171213=CARTESIAN_POINT('Ctrl Pts',(-113.344043591435,5.58157644598328,
132.773805783143));
#171214=CARTESIAN_POINT('Ctrl Pts',(-113.33664350892,5.52526867658858,132.920804950406));
#171215=CARTESIAN_POINT('Ctrl Pts',(-113.329235289253,5.4688989910131,133.067965758364));
#171216=CARTESIAN_POINT('Ctrl Pts',(-113.321827069587,5.40668290590618,
133.212776671384));
#171217=CARTESIAN_POINT('Ctrl Pts',(-113.31441884992,5.33886004037904,133.354753534695));
#171218=CARTESIAN_POINT('Ctrl Pts',(-113.307006070618,5.27099543100986,
133.496817782398));
#171219=CARTESIAN_POINT('Ctrl Pts',(-113.299593291316,5.19751733874125,
133.636044175259));
#171220=CARTESIAN_POINT('Ctrl Pts',(-113.292180512014,5.11871039175003,
133.771974893022));
#171221=CARTESIAN_POINT('Ctrl Pts',(-113.284757140985,5.03979084169739,
133.908099834969));
#171222=CARTESIAN_POINT('Ctrl Pts',(-113.277333769957,4.9555274292701,134.040919382478));
#171223=CARTESIAN_POINT('Ctrl Pts',(-113.269910398928,4.8662474396675,134.170005640207));
#171224=CARTESIAN_POINT('Ctrl Pts',(-113.265974349487,4.8189090469383,134.238450271434));
#171225=CARTESIAN_POINT('Ctrl Pts',(-113.262038300047,4.77016098321603,
134.305845899249));
#171226=CARTESIAN_POINT('Ctrl Pts',(-113.258102250606,4.7200563911717,134.37213278331));
#171227=CARTESIAN_POINT('Ctrl Pts',(-113.250678984201,4.62556069428295,
134.497147777911));
#171228=CARTESIAN_POINT('Ctrl Pts',(-113.243255717795,4.52595197438324,
134.618595009587));
#171229=CARTESIAN_POINT('Ctrl Pts',(-113.23583245139,4.42152912456444,134.73602829975));
#171230=CARTESIAN_POINT('Ctrl Pts',(-113.228417958669,4.31722969388176,
134.853322793516));
#171231=CARTESIAN_POINT('Ctrl Pts',(-113.221003465948,4.20812770469415,
134.966612512778));
#171232=CARTESIAN_POINT('Ctrl Pts',(-113.213588973227,4.09456441864342,
135.075481405378));
#171233=CARTESIAN_POINT('Ctrl Pts',(-113.206181626873,3.9811105891637,135.18424536604));
#171234=CARTESIAN_POINT('Ctrl Pts',(-113.198774280519,3.8632042908697,135.28859672617));
#171235=CARTESIAN_POINT('Ctrl Pts',(-113.191366934165,3.74122594256215,
135.388153698542));
#171236=CARTESIAN_POINT('Ctrl Pts',(-113.18396511249,3.61933857030841,135.487636417567));
#171237=CARTESIAN_POINT('Ctrl Pts',(-113.176563290815,3.49338548324887,
135.58233163378));
#171238=CARTESIAN_POINT('Ctrl Pts',(-113.169161469139,3.36378263780546,
135.671895612622));
#171239=CARTESIAN_POINT('Ctrl Pts',(-113.161763554828,3.23424820869645,
135.761412311337));
#171240=CARTESIAN_POINT('Ctrl Pts',(-113.154365640517,3.10106816460101,
135.845802955578));
#171241=CARTESIAN_POINT('Ctrl Pts',(-113.146967726205,2.96469001039799,
135.924765260243));
#171242=CARTESIAN_POINT('Ctrl Pts',(-113.139571041293,2.82833451976945,
136.003714442805));
#171243=CARTESIAN_POINT('Ctrl Pts',(-113.132174356381,2.68878229657856,
136.077236889312));
#171244=CARTESIAN_POINT('Ctrl Pts',(-113.124777671469,2.54650828446141,
136.14507462598));
#171245=CARTESIAN_POINT('Ctrl Pts',(-113.117381314533,2.40424058092304,
136.212909354651));
#171246=CARTESIAN_POINT('Ctrl Pts',(-113.109984957598,2.25925166537939,
136.275059714012));
#171247=CARTESIAN_POINT('Ctrl Pts',(-113.102588600663,2.11203919988923,
136.331314659408));
#171248=CARTESIAN_POINT('Ctrl Pts',(-113.095191111326,1.96480419579437,
136.387578217579));
#171249=CARTESIAN_POINT('Ctrl Pts',(-113.087793621989,1.81534531263664,
136.437944431322));
#171250=CARTESIAN_POINT('Ctrl Pts',(-113.080396132653,1.66417807080576,
136.482251239192));
#171251=CARTESIAN_POINT('Ctrl Pts',(-113.072996050138,1.51295783753238,
136.526573578745));
#171252=CARTESIAN_POINT('Ctrl Pts',(-113.065595967623,1.36002841125942,
136.564832178397));
#171253=CARTESIAN_POINT('Ctrl Pts',(-113.058195885108,1.20591812385754,
136.596915497846));
#171254=CARTESIAN_POINT('Ctrl Pts',(-113.050787665441,1.05163837635196,
136.629034096203));
#171255=CARTESIAN_POINT('Ctrl Pts',(-113.043379445775,0.896175540257714,
136.654963777442));
#171256=CARTESIAN_POINT('Ctrl Pts',(-113.035971226108,0.740066468676722,
136.674644442428));
#171257=CARTESIAN_POINT('Ctrl Pts',(-113.028558446806,0.583861314566547,
136.694337220536));
#171258=CARTESIAN_POINT('Ctrl Pts',(-113.021145667504,0.427009503482,136.707773286638));
#171259=CARTESIAN_POINT('Ctrl Pts',(-113.013732888202,0.270050061054221,
136.714944643449));
#171260=CARTESIAN_POINT('Ctrl Pts',(-113.006309517173,0.112866347614659,
136.722126247031));
#171261=CARTESIAN_POINT('Ctrl Pts',(-112.998886146144,-0.0444249320157711,
136.723025261419));
#171262=CARTESIAN_POINT('Ctrl Pts',(-112.991462775116,-0.201286871721675,
136.717685753035));
#171263=CARTESIAN_POINT('Ctrl Pts',(-112.987526725675,-0.284458836002299,
136.714854617571));
#171264=CARTESIAN_POINT('Ctrl Pts',(-112.983590676234,-0.367510205607769,
136.710270474008));
#171265=CARTESIAN_POINT('Ctrl Pts',(-112.979654626794,-0.450361994384643,
136.703945741667));
#171266=CARTESIAN_POINT('Ctrl Pts',(-112.972231360388,-0.60661788230606,
136.69201749386));
#171267=CARTESIAN_POINT('Ctrl Pts',(-112.964808093983,-0.762635824064563,
136.673859051977));
#171268=CARTESIAN_POINT('Ctrl Pts',(-112.957384827577,-0.917878877959609,
136.649480712816));
#171269=CARTESIAN_POINT('Ctrl Pts',(-112.949970334856,-1.07293844745841,
136.625131186827));
#171270=CARTESIAN_POINT('Ctrl Pts',(-112.942555842135,-1.22722458692694,
136.594576453911));
#171271=CARTESIAN_POINT('Ctrl Pts',(-112.935141349414,-1.38020279964729,
136.557878740797));
#171272=CARTESIAN_POINT('Ctrl Pts',(-112.92773400306,-1.53303356620713,
136.52121639832));
#171273=CARTESIAN_POINT('Ctrl Pts',(-112.920326656706,-1.68455855512059,
136.478422949359));
#171274=CARTESIAN_POINT('Ctrl Pts',(-112.912919310352,-1.83425093232574,
136.429612085702));
#171275=CARTESIAN_POINT('Ctrl Pts',(-112.905517488676,-1.98383166330756,
136.380837627028));
#171276=CARTESIAN_POINT('Ctrl Pts',(-112.898115667001,-2.13158215074669,
136.326054805129));
#171277=CARTESIAN_POINT('Ctrl Pts',(-112.890713845326,-2.27698836641902,
136.265427779));
#171278=CARTESIAN_POINT('Ctrl Pts',(-112.883315931014,-2.42231782328193,
136.204832757406));
#171279=CARTESIAN_POINT('Ctrl Pts',(-112.875918016703,-2.5653051292881,
136.13839981902));
#171280=CARTESIAN_POINT('Ctrl Pts',(-112.868520102391,-2.70545407610144,
136.06634206989));
#171281=CARTESIAN_POINT('Ctrl Pts',(-112.861123417479,-2.84557973270179,
135.994296295452));
#171282=CARTESIAN_POINT('Ctrl Pts',(-112.853726732567,-2.98286763459972,
135.916627735978));
#171283=CARTESIAN_POINT('Ctrl Pts',(-112.846330047654,-3.11684402250852,
135.833596533871));
#171284=CARTESIAN_POINT('Ctrl Pts',(-112.838933690719,-3.25081446976426,
135.750569013454));
#171285=CARTESIAN_POINT('Ctrl Pts',(-112.831537333783,-3.38147337768759,
135.662179519848));
#171286=CARTESIAN_POINT('Ctrl Pts',(-112.824140976848,-3.50837418993428,
135.568732675446));
#171287=CARTESIAN_POINT('Ctrl Pts',(-112.816743487511,-3.63529443101929,
135.475271524093));
#171288=CARTESIAN_POINT('Ctrl Pts',(-112.809345998174,-3.75845513016968,
135.376751701586));
#171289=CARTESIAN_POINT('Ctrl Pts',(-112.801948508838,-3.87744128913971,
135.273519331661));
#171290=CARTESIAN_POINT('Ctrl Pts',(-112.794548426322,-3.99646915852248,
135.17025077379));
#171291=CARTESIAN_POINT('Ctrl Pts',(-112.787148343807,-4.11131929235792,
135.062266623909));
#171292=CARTESIAN_POINT('Ctrl Pts',(-112.779748261292,-4.22161227235034,
134.949951092328));
#171293=CARTESIAN_POINT('Ctrl Pts',(-112.772340041626,-4.33202653081314,
134.837512058274));
#171294=CARTESIAN_POINT('Ctrl Pts',(-112.764931821959,-4.43787336630588,
134.720732397407));
#171295=CARTESIAN_POINT('Ctrl Pts',(-112.757523602293,-4.53881203350988,
134.600031294398));
#171296=CARTESIAN_POINT('Ctrl Pts',(-112.750110822991,-4.63981282677959,
134.479255901874));
#171297=CARTESIAN_POINT('Ctrl Pts',(-112.742698043688,-4.73589920493002,
134.354554552856));
#171298=CARTESIAN_POINT('Ctrl Pts',(-112.735285264386,-4.82677308309787,
134.226376422144));
#171299=CARTESIAN_POINT('Ctrl Pts',(-112.727861893357,-4.91777680612428,
134.098015144508));
#171300=CARTESIAN_POINT('Ctrl Pts',(-112.720438522329,-5.00355295108318,
133.966167475469));
#171301=CARTESIAN_POINT('Ctrl Pts',(-112.7130151513,-5.08384838143384,133.831308948326));
#171302=CARTESIAN_POINT('Ctrl Pts',(-112.70907910186,-5.12642294526084,
133.759803721361));
#171303=CARTESIAN_POINT('Ctrl Pts',(-112.705143052419,-5.16745746935994,
133.687452410416));
#171304=CARTESIAN_POINT('Ctrl Pts',(-112.701207002979,-5.20691970851158,
133.614328181723));
#171305=CARTESIAN_POINT('Ctrl Pts',(-112.693383344829,-5.28535852734934,
133.468979659936));
#171306=CARTESIAN_POINT('Ctrl Pts',(-112.685559686679,-5.35779890327574,
133.320175471554));
#171307=CARTESIAN_POINT('Ctrl Pts',(-112.677736028528,-5.4239404560296,
133.168425018538));
#171308=CARTESIAN_POINT('Ctrl Pts',(-112.669925520726,-5.48997083515598,
133.01692963435));
#171309=CARTESIAN_POINT('Ctrl Pts',(-112.662115012924,-5.54972337017719,
132.86249814332));
#171310=CARTESIAN_POINT('Ctrl Pts',(-112.654304505122,-5.60294318882384,
132.705664955465));
#171311=CARTESIAN_POINT('Ctrl Pts',(-112.646511917776,-5.65604089973241,
132.549191606224));
#171312=CARTESIAN_POINT('Ctrl Pts',(-112.63871933043,-5.70263569018409,
132.390327847665));
#171313=CARTESIAN_POINT('Ctrl Pts',(-112.630926743085,-5.74252069389382,
132.229627835565));
#171314=CARTESIAN_POINT('Ctrl Pts',(-112.623144694277,-5.78235175792649,
132.069145150929));
#171315=CARTESIAN_POINT('Ctrl Pts',(-112.61536264547,-5.81549104384244,
131.906831464921));
#171316=CARTESIAN_POINT('Ctrl Pts',(-112.607580596663,-5.8417807737891,
131.743257818269));
#171317=CARTESIAN_POINT('Ctrl Pts',(-112.599813085406,-5.86802139221372,
131.57998974154));
#171318=CARTESIAN_POINT('Ctrl Pts',(-112.592045574148,-5.88743792681151,
131.41546670787));
#171319=CARTESIAN_POINT('Ctrl Pts',(-112.584278062891,-5.89992324519862,
131.250271217647));
#171320=CARTESIAN_POINT('Ctrl Pts',(-112.577310439339,-5.91112284254257,
131.102087333491));
#171321=CARTESIAN_POINT('Ctrl Pts',(-112.570342815787,-5.91674586775566,
130.95336270369));
#171322=CARTESIAN_POINT('Ctrl Pts',(-112.563375192235,-5.91674999772218,
130.804524796032));
#171323=CARTESIAN_POINT('',(-110.813375192205,-5.91674751312338,130.798935818188));
#171324=CARTESIAN_POINT('Ctrl Pts',(-112.563375192205,-5.9167499977222,
130.804524795383));
#171325=CARTESIAN_POINT('Ctrl Pts',(-112.555642867804,-5.91675458093688,
130.639351838401));
#171326=CARTESIAN_POINT('Ctrl Pts',(-112.547910543403,-5.90983835624213,
130.474306327478));
#171327=CARTESIAN_POINT('Ctrl Pts',(-112.540178219002,-5.89605913921249,
130.309974948873));
#171328=CARTESIAN_POINT('Ctrl Pts',(-112.532436725038,-5.88226358176701,
130.145448693951));
#171329=CARTESIAN_POINT('Ctrl Pts',(-112.524695231074,-5.8615888162922,
129.9816385811));
#171330=CARTESIAN_POINT('Ctrl Pts',(-112.51695373711,-5.83414414635372,
129.819123264404));
#171331=CARTESIAN_POINT('Ctrl Pts',(-112.509104207281,-5.80631647428949,
129.654339976844));
#171332=CARTESIAN_POINT('Ctrl Pts',(-112.501254677453,-5.77152862197727,
129.490888229268));
#171333=CARTESIAN_POINT('Ctrl Pts',(-112.493405147624,-5.72994687374479,
129.329355740773));
#171334=CARTESIAN_POINT('Ctrl Pts',(-112.485637347382,-5.68879807616569,
129.16950513434));
#171335=CARTESIAN_POINT('Ctrl Pts',(-112.477869547139,-5.64099635216969,
129.011534291415));
#171336=CARTESIAN_POINT('Ctrl Pts',(-112.470101746897,-5.58675172779189,
128.855993174163));
#171337=CARTESIAN_POINT('Ctrl Pts',(-112.462211352275,-5.53165099411291,
128.697997247816));
#171338=CARTESIAN_POINT('Ctrl Pts',(-112.454320957654,-5.4699024378795,
128.542508702172));
#171339=CARTESIAN_POINT('Ctrl Pts',(-112.446430563032,-5.40177507766933,
128.390078825237));
#171340=CARTESIAN_POINT('Ctrl Pts',(-112.438540168411,-5.33364771745899,
128.237648948302));
#171341=CARTESIAN_POINT('Ctrl Pts',(-112.430649773789,-5.25914176213731,
128.088278016487));
#171342=CARTESIAN_POINT('Ctrl Pts',(-112.422759379168,-5.17857258267913,
127.94248770487));
#171343=CARTESIAN_POINT('Ctrl Pts',(-112.415336112762,-5.10277327074935,
127.805328491124));
#171344=CARTESIAN_POINT('Ctrl Pts',(-112.407912846357,-5.02140639758439,
127.670975377606));
#171345=CARTESIAN_POINT('Ctrl Pts',(-112.400489579952,-4.93470451707544,
127.539912441893));
#171346=CARTESIAN_POINT('Ctrl Pts',(-112.393075087231,-4.84810511098886,
127.409004411686));
#171347=CARTESIAN_POINT('Ctrl Pts',(-112.38566059451,-4.75618345271013,
127.28137912707));
#171348=CARTESIAN_POINT('Ctrl Pts',(-112.378246101789,-4.65921831098971,
127.157496856327));
#171349=CARTESIAN_POINT('Ctrl Pts',(-112.370838755436,-4.56234662792355,
127.033733987981));
#171350=CARTESIAN_POINT('Ctrl Pts',(-112.363431409082,-4.46044136744951,
126.913707243357));
#171351=CARTESIAN_POINT('Ctrl Pts',(-112.356024062729,-4.35382492155404,
126.797848529109));
#171352=CARTESIAN_POINT('Ctrl Pts',(-112.348622241053,-4.24728799422634,
126.682076226661));
#171353=CARTESIAN_POINT('Ctrl Pts',(-112.341220419378,-4.13604712957681,
126.570466038308));
#171354=CARTESIAN_POINT('Ctrl Pts',(-112.333818597703,-4.020465297414,126.463417246041));
#171355=CARTESIAN_POINT('Ctrl Pts',(-112.326420683392,-3.90494448000071,
126.356424963998));
#171356=CARTESIAN_POINT('Ctrl Pts',(-112.31902276908,-3.78508753201583,
126.253989535557));
#171357=CARTESIAN_POINT('Ctrl Pts',(-112.311624854769,-3.66129453431139,
126.156473689561));
#171358=CARTESIAN_POINT('Ctrl Pts',(-112.304228169857,-3.53752210875751,
126.058974048929));
#171359=CARTESIAN_POINT('Ctrl Pts',(-112.296831484945,-3.40981522463513,
125.966392598926));
#171360=CARTESIAN_POINT('Ctrl Pts',(-112.289434800033,-3.27860741183864,
125.879052099155));
#171361=CARTESIAN_POINT('Ctrl Pts',(-112.282038443098,-3.14740541693406,
125.791715472153));
#171362=CARTESIAN_POINT('Ctrl Pts',(-112.274642086162,-3.01270311276057,
125.709619540167));
#171363=CARTESIAN_POINT('Ctrl Pts',(-112.267245729227,-2.87496317716572,
125.63304383241));
#171364=CARTESIAN_POINT('Ctrl Pts',(-112.259848239891,-2.73720215323548,
125.556456400716));
#171365=CARTESIAN_POINT('Ctrl Pts',(-112.252450750554,-2.59640289815762,
125.485391057476));
#171366=CARTESIAN_POINT('Ctrl Pts',(-112.245053261218,-2.45305271830573,
125.420081378549));
#171367=CARTESIAN_POINT('Ctrl Pts',(-112.237653178703,-2.3096522872699,
125.354748805414));
#171368=CARTESIAN_POINT('Ctrl Pts',(-112.230253096188,-2.16369949056062,
125.295176068368));
#171369=CARTESIAN_POINT('Ctrl Pts',(-112.222853013673,-2.01570148553828,
125.241548551381));
#171370=CARTESIAN_POINT('Ctrl Pts',(-112.215444794007,-1.86754074149505,
125.187862065425));
#171371=CARTESIAN_POINT('Ctrl Pts',(-112.20803657434,-1.71733064908698,
125.140133982357));
#171372=CARTESIAN_POINT('Ctrl Pts',(-112.200628354674,-1.56559410038212,
125.09849997474));
#171373=CARTESIAN_POINT('Ctrl Pts',(-112.193215575372,-1.41376416036338,
125.056840342086));
#171374=CARTESIAN_POINT('Ctrl Pts',(-112.18580279607,-1.26040625476733,
125.021282342947));
#171375=CARTESIAN_POINT('Ctrl Pts',(-112.178390016768,-1.10605281966712,
124.991910383576));
#171376=CARTESIAN_POINT('Ctrl Pts',(-112.17096664574,-0.951478837140164,
124.962496456172));
#171377=CARTESIAN_POINT('Ctrl Pts',(-112.163543274711,-0.795906852372275,
124.939286276748));
#171378=CARTESIAN_POINT('Ctrl Pts',(-112.156119903682,-0.639874591418284,
124.922312413942));
#171379=CARTESIAN_POINT('Ctrl Pts',(-112.15218385424,-0.557142542677966,
124.913312464596));
#171380=CARTESIAN_POINT('Ctrl Pts',(-112.148247804797,-0.474281109374064,
124.906064896517));
#171381=CARTESIAN_POINT('Ctrl Pts',(-112.144311755355,-0.391370240704987,
124.900568624517));
#171382=CARTESIAN_POINT('Ctrl Pts',(-112.136888488949,-0.235002930027058,
124.890202827062));
#171383=CARTESIAN_POINT('Ctrl Pts',(-112.129465222544,-0.0779870681005315,
124.886037942271));
#171384=CARTESIAN_POINT('Ctrl Pts',(-112.122041956138,0.0791443758398206,
124.888139971725));
#171385=CARTESIAN_POINT('Ctrl Pts',(-112.114627463417,0.23609010346239,
124.890239516755));
#171386=CARTESIAN_POINT('Ctrl Pts',(-112.107212970696,0.393150771559606,
124.898591227467));
#171387=CARTESIAN_POINT('Ctrl Pts',(-112.099798477975,0.54978846207174,
124.913209354063));
#171388=CARTESIAN_POINT('Ctrl Pts',(-112.092391131621,0.706275179280899,
124.927813391159));
#171389=CARTESIAN_POINT('Ctrl Pts',(-112.084983785268,0.862339361331365,
124.948671785618));
#171390=CARTESIAN_POINT('Ctrl Pts',(-112.077576438914,1.01744337217851,
124.975746756028));
#171391=CARTESIAN_POINT('Ctrl Pts',(-112.070174617238,1.17243170060306,
125.002801532904));
#171392=CARTESIAN_POINT('Ctrl Pts',(-112.062772795563,1.32646091758501,
125.036063589805));
#171393=CARTESIAN_POINT('Ctrl Pts',(-112.055370973887,1.47899890182926,
125.075443371621));
#171394=CARTESIAN_POINT('Ctrl Pts',(-112.047973059576,1.63145636245767,
125.114802365156));
#171395=CARTESIAN_POINT('Ctrl Pts',(-112.040575145265,1.78242379758288,
125.160272558826));
#171396=CARTESIAN_POINT('Ctrl Pts',(-112.033177230954,1.93137977968521,
125.211713417078));
#171397=CARTESIAN_POINT('Ctrl Pts',(-112.025780546041,2.08031100800629,
125.263145726793));
#171398=CARTESIAN_POINT('Ctrl Pts',(-112.018383861129,2.22723109422135,
125.320546610101));
#171399=CARTESIAN_POINT('Ctrl Pts',(-112.010987176217,2.37163415803816,
125.383725785471));
#171400=CARTESIAN_POINT('Ctrl Pts',(-112.003590819282,2.5160308188718,125.44690215941));
#171401=CARTESIAN_POINT('Ctrl Pts',(-111.996194462346,2.65791033722359,
125.515856166338));
#171402=CARTESIAN_POINT('Ctrl Pts',(-111.988798105411,2.7967874485724,125.590349634646));
#171403=CARTESIAN_POINT('Ctrl Pts',(-111.981400616074,2.93568582236149,
125.664854508095));
#171404=CARTESIAN_POINT('Ctrl Pts',(-111.974003126738,3.07158054488917,
125.744900355148));
#171405=CARTESIAN_POINT('Ctrl Pts',(-111.966605637401,3.20401170117158,
125.830203444611));
#171406=CARTESIAN_POINT('Ctrl Pts',(-111.959205554886,3.33648928099109,
125.915536436941));
#171407=CARTESIAN_POINT('Ctrl Pts',(-111.951805472371,3.46550056357364,
126.006130138896));
#171408=CARTESIAN_POINT('Ctrl Pts',(-111.944405389856,3.59061544919406,
126.101658069189));
#171409=CARTESIAN_POINT('Ctrl Pts',(-111.936997170189,3.71586791149281,
126.197291042262));
#171410=CARTESIAN_POINT('Ctrl Pts',(-111.929588950523,3.83721512353996,
126.297868852459));
#171411=CARTESIAN_POINT('Ctrl Pts',(-111.922180730857,3.95426030423132,
126.403024910206));
#171412=CARTESIAN_POINT('Ctrl Pts',(-111.914767951555,4.0713775242784,126.508245689753));
#171413=CARTESIAN_POINT('Ctrl Pts',(-111.907355172252,4.18418716995908,
126.618050071969));
#171414=CARTESIAN_POINT('Ctrl Pts',(-111.89994239295,4.29233043319898,126.73203572695));
#171415=CARTESIAN_POINT('Ctrl Pts',(-111.892519021922,4.40062821660466,
126.846184249979));
#171416=CARTESIAN_POINT('Ctrl Pts',(-111.885095650893,4.50424605572476,
126.964525697877));
#171417=CARTESIAN_POINT('Ctrl Pts',(-111.877672279864,4.60286589557306,
127.086625270628));
#171418=CARTESIAN_POINT('Ctrl Pts',(-111.873736230423,4.65515650101219,
127.151365393841));
#171419=CARTESIAN_POINT('Ctrl Pts',(-111.869800180983,4.70604271397878,
127.217161576831));
#171420=CARTESIAN_POINT('Ctrl Pts',(-111.865864131542,4.75548223297956,
127.2839459695));
#171421=CARTESIAN_POINT('Ctrl Pts',(-111.858440865136,4.84872362285936,
127.409899249804));
#171422=CARTESIAN_POINT('Ctrl Pts',(-111.851017598731,4.93709856708689,
127.539749919401));
#171423=CARTESIAN_POINT('Ctrl Pts',(-111.843594332325,5.02026345377358,
127.673085251648));
#171424=CARTESIAN_POINT('Ctrl Pts',(-111.836179839604,5.1033300464711,127.806262992605));
#171425=CARTESIAN_POINT('Ctrl Pts',(-111.828765346883,5.1811986432444,127.942916884508));
#171426=CARTESIAN_POINT('Ctrl Pts',(-111.821350854162,5.25356649714264,
128.082602064241));
#171427=CARTESIAN_POINT('Ctrl Pts',(-111.813943507808,5.32586460017808,
128.222152610137));
#171428=CARTESIAN_POINT('Ctrl Pts',(-111.806536161455,5.3926723446569,128.364728298163));
#171429=CARTESIAN_POINT('Ctrl Pts',(-111.799128815101,5.45373091173638,
128.509856378112));
#171430=CARTESIAN_POINT('Ctrl Pts',(-111.791726993425,5.51474393903293,
128.654876216064));
#171431=CARTESIAN_POINT('Ctrl Pts',(-111.78432517175,5.57001618268286,128.802444312871));
#171432=CARTESIAN_POINT('Ctrl Pts',(-111.776923350075,5.61933536337916,
128.952064573091));
#171433=CARTESIAN_POINT('Ctrl Pts',(-111.769525435763,5.66862850886386,
129.101605849941));
#171434=CARTESIAN_POINT('Ctrl Pts',(-111.762127521452,5.71197473341609,
129.253196779083));
#171435=CARTESIAN_POINT('Ctrl Pts',(-111.75472960714,5.74921042926596,129.406322705877));
#171436=CARTESIAN_POINT('Ctrl Pts',(-111.747332922228,5.78643993721887,
129.559423185921));
#171437=CARTESIAN_POINT('Ctrl Pts',(-111.739936237316,5.81756084373676,
129.71405779497));
#171438=CARTESIAN_POINT('Ctrl Pts',(-111.732539552404,5.84245979740451,
129.869698069792));
#171439=CARTESIAN_POINT('Ctrl Pts',(-111.725143195468,5.86735764702656,
130.025331443361));
#171440=CARTESIAN_POINT('Ctrl Pts',(-111.717746838533,5.88603403338742,
130.181970025428));
#171441=CARTESIAN_POINT('Ctrl Pts',(-111.710350481597,5.89842703968086,
130.339076811635));
#171442=CARTESIAN_POINT('Ctrl Pts',(-111.702952992261,5.91082194337521,
130.496207651292));
#171443=CARTESIAN_POINT('Ctrl Pts',(-111.695555502924,5.91693152217169,
130.653806465655));
#171444=CARTESIAN_POINT('Ctrl Pts',(-111.688158013587,5.91674589187827,
130.81133295158));
#171445=CARTESIAN_POINT('Ctrl Pts',(-111.680757931072,5.91656019651245,
130.968914658171));
#171446=CARTESIAN_POINT('Ctrl Pts',(-111.673357848557,5.91007489882196,
131.126423612777));
#171447=CARTESIAN_POINT('Ctrl Pts',(-111.665957766042,5.89733219735277,
131.28332148921));
#171448=CARTESIAN_POINT('Ctrl Pts',(-111.658549546376,5.88457548397331,
131.440391890988));
#171449=CARTESIAN_POINT('Ctrl Pts',(-111.651141326709,5.86554765592489,
131.596849500377));
#171450=CARTESIAN_POINT('Ctrl Pts',(-111.643733107043,5.84034266551811,
131.752162343577));
#171451=CARTESIAN_POINT('Ctrl Pts',(-111.636320327741,5.81512216186016,
131.907570779241));
#171452=CARTESIAN_POINT('Ctrl Pts',(-111.628907548438,5.78371699429802,
132.061832679798));
#171453=CARTESIAN_POINT('Ctrl Pts',(-111.621494769136,5.74627170984768,
132.214428700711));
#171454=CARTESIAN_POINT('Ctrl Pts',(-111.614071398108,5.70877292181908,
132.367242757974));
#171455=CARTESIAN_POINT('Ctrl Pts',(-111.606648027079,5.66521688314878,
132.518385823875));
#171456=CARTESIAN_POINT('Ctrl Pts',(-111.59922465605,5.61579748691372,132.66735528972));
#171457=CARTESIAN_POINT('Ctrl Pts',(-111.595288606609,5.58959413723057,
132.746342474975));
#171458=CARTESIAN_POINT('Ctrl Pts',(-111.591352557169,5.56174318611317,
132.824718931174));
#171459=CARTESIAN_POINT('Ctrl Pts',(-111.587416507729,5.53227885277902,
132.902412394237));
#171460=CARTESIAN_POINT('Ctrl Pts',(-111.579993241323,5.47671003965574,
133.048939840859));
#171461=CARTESIAN_POINT('Ctrl Pts',(-111.572569974918,5.4152318097948,133.193479643042));
#171462=CARTESIAN_POINT('Ctrl Pts',(-111.565146708512,5.34800567119306,
133.335519621538));
#171463=CARTESIAN_POINT('Ctrl Pts',(-111.557732215791,5.28085898830436,
133.477391720575));
#171464=CARTESIAN_POINT('Ctrl Pts',(-111.55031772307,5.20797807741091,133.616769542922));
#171465=CARTESIAN_POINT('Ctrl Pts',(-111.54290323035,5.12957357232856,133.753157919614));
#171466=CARTESIAN_POINT('Ctrl Pts',(-111.535495883996,5.05124463646009,
133.889414840055));
#171467=CARTESIAN_POINT('Ctrl Pts',(-111.528088537642,4.96740288993177,
134.022687729561));
#171468=CARTESIAN_POINT('Ctrl Pts',(-111.520681191288,4.87830617297523,
134.152503303476));
#171469=CARTESIAN_POINT('Ctrl Pts',(-111.513279369613,4.78927590771137,
134.282222056039));
#171470=CARTESIAN_POINT('Ctrl Pts',(-111.505877547938,4.69499868631527,
134.408488320888));
#171471=CARTESIAN_POINT('Ctrl Pts',(-111.498475726262,4.59577714578074,
134.530855349726));
#171472=CARTESIAN_POINT('Ctrl Pts',(-111.491077811951,4.49660798352456,
134.653157781964));
#171473=CARTESIAN_POINT('Ctrl Pts',(-111.483679897639,4.39249993472033,
134.771564788325));
#171474=CARTESIAN_POINT('Ctrl Pts',(-111.476281983328,4.2837975588958,134.885660537555));
#171475=CARTESIAN_POINT('Ctrl Pts',(-111.468885298416,4.17511324743484,
134.99973732614));
#171476=CARTESIAN_POINT('Ctrl Pts',(-111.461488613504,4.06183638150699,
135.109504009534));
#171477=CARTESIAN_POINT('Ctrl Pts',(-111.454091928591,3.94435030298717,
135.214579574696));
#171478=CARTESIAN_POINT('Ctrl Pts',(-111.446695571656,3.8268694339232,135.319650480696));
#171479=CARTESIAN_POINT('Ctrl Pts',(-111.439299214721,3.70518000162044,
135.420030433202));
#171480=CARTESIAN_POINT('Ctrl Pts',(-111.431902857785,3.57970033550769,
135.515377075876));
#171481=CARTESIAN_POINT('Ctrl Pts',(-111.424505368449,3.45420145813773,
135.610738316365));
#171482=CARTESIAN_POINT('Ctrl Pts',(-111.417107879112,3.32491148875949,
135.701064486766));
#171483=CARTESIAN_POINT('Ctrl Pts',(-111.409710389775,3.19227965706237,
135.786055224184));
#171484=CARTESIAN_POINT('Ctrl Pts',(-111.40231030726,3.05960133148206,135.871075754973));
#171485=CARTESIAN_POINT('Ctrl Pts',(-111.394910224745,2.92357912527311,
135.950756927688));
#171486=CARTESIAN_POINT('Ctrl Pts',(-111.38751014223,2.78468875685034,136.024843266706));
#171487=CARTESIAN_POINT('Ctrl Pts',(-111.380101922564,2.64564566418941,
136.09901107127));
#171488=CARTESIAN_POINT('Ctrl Pts',(-111.372693702898,2.503728440462,136.167571580201));
#171489=CARTESIAN_POINT('Ctrl Pts',(-111.365285483231,2.35943543380992,
136.230316293406));
#171490=CARTESIAN_POINT('Ctrl Pts',(-111.357872703929,2.21505361721908,
136.293099624936));
#171491=CARTESIAN_POINT('Ctrl Pts',(-111.350459924627,2.06829345117668,
136.350059893333));
#171492=CARTESIAN_POINT('Ctrl Pts',(-111.343047145325,1.91967000614294,
136.401037991689));
#171493=CARTESIAN_POINT('Ctrl Pts',(-111.335623774296,1.77083420096182,
136.452088929941));
#171494=CARTESIAN_POINT('Ctrl Pts',(-111.328200403268,1.62013015620956,
136.497140520032));
#171495=CARTESIAN_POINT('Ctrl Pts',(-111.320777032239,1.46808553476072,
136.53608421742));
#171496=CARTESIAN_POINT('Ctrl Pts',(-111.316840982798,1.38746782820295,
136.556733100218));
#171497=CARTESIAN_POINT('Ctrl Pts',(-111.312904933357,1.30647337647703,
136.575665695293));
#171498=CARTESIAN_POINT('Ctrl Pts',(-111.308968883916,1.22518147372208,
136.592871731743));
#171499=CARTESIAN_POINT('Ctrl Pts',(-111.30154561751,1.07186748216805,136.625321779503));
#171500=CARTESIAN_POINT('Ctrl Pts',(-111.294122351105,0.917031568081696,
136.651725697228));
#171501=CARTESIAN_POINT('Ctrl Pts',(-111.286699084699,0.761191941386301,
136.671942520775));
#171502=CARTESIAN_POINT('Ctrl Pts',(-111.279284591978,0.60553650418754,
136.692135449717));
#171503=CARTESIAN_POINT('Ctrl Pts',(-111.271870099257,0.448880082307066,
136.706155792758));
#171504=CARTESIAN_POINT('Ctrl Pts',(-111.264455606536,0.291753128140704,
136.713913111175));
#171505=CARTESIAN_POINT('Ctrl Pts',(-111.257048260182,0.134777618849387,
136.721662952796));
#171506=CARTESIAN_POINT('Ctrl Pts',(-111.249640913829,-0.0226671495244484,
136.723161769069));
#171507=CARTESIAN_POINT('Ctrl Pts',(-111.242233567475,-0.180043620251498,
136.718370666366));
#171508=CARTESIAN_POINT('Ctrl Pts',(-111.234831745799,-0.337302713669653,
136.713583137048));
#171509=CARTESIAN_POINT('Ctrl Pts',(-111.227429924124,-0.494493239348228,
136.702515040993));
#171510=CARTESIAN_POINT('Ctrl Pts',(-111.220028102449,-0.65107575260525,
136.685179516909));
#171511=CARTESIAN_POINT('Ctrl Pts',(-111.212630188137,-0.807575607171467,
136.667853144113));
#171512=CARTESIAN_POINT('Ctrl Pts',(-111.205232273826,-0.963467718441625,
136.644265973351));
#171513=CARTESIAN_POINT('Ctrl Pts',(-111.197834359514,-1.1182159929637,
136.61448312536));
#171514=CARTESIAN_POINT('Ctrl Pts',(-111.190437674602,-1.27293855113108,
136.584705226739));
#171515=CARTESIAN_POINT('Ctrl Pts',(-111.18304098969,-1.42651728360098,
136.54873376484));
#171516=CARTESIAN_POINT('Ctrl Pts',(-111.175644304778,-1.57842442766419,
136.506685309185));
#171517=CARTESIAN_POINT('Ctrl Pts',(-111.168247947842,-1.73032483600501,
136.464638718003));
#171518=CARTESIAN_POINT('Ctrl Pts',(-111.160851590907,-1.88055344354558,
136.416515768428));
#171519=CARTESIAN_POINT('Ctrl Pts',(-111.153455233971,-2.02859609893061,
136.362483360894));
#171520=CARTESIAN_POINT('Ctrl Pts',(-111.146057744635,-2.17666142002453,
136.308442680861));
#171521=CARTESIAN_POINT('Ctrl Pts',(-111.138660255298,-2.32253977188676,
136.248490869381));
#171522=CARTESIAN_POINT('Ctrl Pts',(-111.131262765961,-2.46573563108488,
136.182843522633));
#171523=CARTESIAN_POINT('Ctrl Pts',(-111.123862683446,-2.60898168737048,
136.117173163309));
#171524=CARTESIAN_POINT('Ctrl Pts',(-111.116462600931,-2.74954303964861,
136.045803449048));
#171525=CARTESIAN_POINT('Ctrl Pts',(-111.109062518416,-2.88694761161864,
135.968996524411));
#171526=CARTESIAN_POINT('Ctrl Pts',(-111.10165429875,-3.0245032740401,135.892105142665));
#171527=CARTESIAN_POINT('Ctrl Pts',(-111.094246079083,-3.15889489788458,
135.809764792797));
#171528=CARTESIAN_POINT('Ctrl Pts',(-111.086837859417,-3.28967769677574,
135.722282049821));
#171529=CARTESIAN_POINT('Ctrl Pts',(-111.079425080115,-3.4205409902974,
135.634745462677));
#171530=CARTESIAN_POINT('Ctrl Pts',(-111.072012300812,-3.54779073186089,
135.542060394921));
#171531=CARTESIAN_POINT('Ctrl Pts',(-111.06459952151,-3.67101465215211,
135.444574188748));
#171532=CARTESIAN_POINT('Ctrl Pts',(-111.057176150481,-3.7944146405591,
135.346948689713));
#171533=CARTESIAN_POINT('Ctrl Pts',(-111.049752779453,-3.9137770365694,
135.244508593591));
#171534=CARTESIAN_POINT('Ctrl Pts',(-111.042329408424,-4.02872530391475,
135.137639167128));
#171535=CARTESIAN_POINT('Ctrl Pts',(-111.038393358983,-4.08967363340134,
135.080974432926));
#171536=CARTESIAN_POINT('Ctrl Pts',(-111.034457309543,-4.1493816413853,
135.023065036908));
#171537=CARTESIAN_POINT('Ctrl Pts',(-111.030521260103,-4.20779782624605,
134.963972139804));
#171538=CARTESIAN_POINT('Ctrl Pts',(-111.023198451068,-4.3164780074149,
134.854032971776));
#171539=CARTESIAN_POINT('Ctrl Pts',(-111.015875642033,-4.42103274883604,
134.739643052212));
#171540=CARTESIAN_POINT('Ctrl Pts',(-111.008552832998,-4.52106797482426,
134.621149179894));
#171541=CARTESIAN_POINT('Ctrl Pts',(-111.00123885966,-4.62098249836996,
134.50279828221));
#171542=CARTESIAN_POINT('Ctrl Pts',(-110.993924886322,-4.71638811132162,
134.380353575008));
#171543=CARTESIAN_POINT('Ctrl Pts',(-110.986610912985,-4.80692618199845,
134.254199924449));
#171544=CARTESIAN_POINT('Ctrl Pts',(-110.979305281407,-4.89736099185748,
134.128190155122));
#171545=CARTESIAN_POINT('Ctrl Pts',(-110.971999649829,-4.98293909235842,
133.99848017652));
#171546=CARTESIAN_POINT('Ctrl Pts',(-110.964694018251,-5.06334123005648,
133.865488865534));
#171547=CARTESIAN_POINT('Ctrl Pts',(-110.957393102566,-5.14369146699154,
133.732583402397));
#171548=CARTESIAN_POINT('Ctrl Pts',(-110.950092186881,-5.21887218919547,
133.596401147546));
#171549=CARTESIAN_POINT('Ctrl Pts',(-110.942791271196,-5.28860661020286,
133.457391089502));
#171550=CARTESIAN_POINT('Ctrl Pts',(-110.935493534486,-5.35831066734712,
133.318441559419));
#171551=CARTESIAN_POINT('Ctrl Pts',(-110.928195797777,-5.42257296965475,
133.176667018737));
#171552=CARTESIAN_POINT('Ctrl Pts',(-110.920898061067,-5.48116212836772,
133.032542002698));
#171553=CARTESIAN_POINT('Ctrl Pts',(-110.91360196904,-5.53973808290514,
132.888449467958));
#171554=CARTESIAN_POINT('Ctrl Pts',(-110.906305877013,-5.59264329444742,
132.74200786814));
#171555=CARTESIAN_POINT('Ctrl Pts',(-110.899009784987,-5.63969419815228,
132.593712431444));
#171556=CARTESIAN_POINT('Ctrl Pts',(-110.891711309516,-5.6867604721658,
132.445368550479));
#171557=CARTESIAN_POINT('Ctrl Pts',(-110.884412834046,-5.72796849501785,
132.295169987417));
#171558=CARTESIAN_POINT('Ctrl Pts',(-110.877114358575,-5.76318429015178,
132.143628104011));
#171559=CARTESIAN_POINT('Ctrl Pts',(-110.86981486775,-5.79840498446254,
131.992065138289));
#171560=CARTESIAN_POINT('Ctrl Pts',(-110.862515376925,-5.82763171215511,
131.839158856489));
#171561=CARTESIAN_POINT('Ctrl Pts',(-110.855215886099,-5.85078163412601,
131.685430894147));
#171562=CARTESIAN_POINT('Ctrl Pts',(-110.847909803773,-5.87395246067146,
131.53156411416));
#171563=CARTESIAN_POINT('Ctrl Pts',(-110.840603721446,-5.89103546933593,
131.376874552918));
#171564=CARTESIAN_POINT('Ctrl Pts',(-110.833297639119,-5.90199966949726,
131.221889615067));
#171565=CARTESIAN_POINT('Ctrl Pts',(-110.826656823481,-5.91196550736092,
131.081017071772));
#171566=CARTESIAN_POINT('Ctrl Pts',(-110.820016007843,-5.91687675752732,
130.939900755746));
#171567=CARTESIAN_POINT('Ctrl Pts',(-110.813375192205,-5.91674751312338,
130.798935818188));
#171568=CARTESIAN_POINT('',(-109.063375192205,-5.92157197187691,130.806665548282));
#171569=CARTESIAN_POINT('Ctrl Pts',(-110.813375192205,-5.91750148305884,
130.798935126907));
#171570=CARTESIAN_POINT('Ctrl Pts',(-110.792941340233,-5.92153502060429,
130.365125357009));
#171571=CARTESIAN_POINT('Ctrl Pts',(-110.772507488262,-5.87789815567871,
129.932120052829));
#171572=CARTESIAN_POINT('Ctrl Pts',(-110.659257761686,-5.3550699825935,
127.595153321436));
#171573=CARTESIAN_POINT('Ctrl Pts',(-110.473626012476,-2.40606949429832,
124.232573180426));
#171574=CARTESIAN_POINT('Ctrl Pts',(-110.195178388666,4.22849156037399,
125.227854573977));
#171575=CARTESIAN_POINT('Ctrl Pts',(-109.916730764851,6.9772754443608,131.34767259412));
#171576=CARTESIAN_POINT('Ctrl Pts',(-109.638283141039,3.31428405383379,
136.968213450076));
#171577=CARTESIAN_POINT('Ctrl Pts',(-109.359835517226,-3.39437247038935,
136.924474673905));
#171578=CARTESIAN_POINT('Ctrl Pts',(-109.168199534281,-5.86470081146466,
133.023708255532));
#171579=CARTESIAN_POINT('Ctrl Pts',(-109.069379425941,-5.92607768413121,
130.933692464336));
#171580=CARTESIAN_POINT('Ctrl Pts',(-109.063375192205,-5.92544804556881,
130.806667057017));
#171581=CARTESIAN_POINT('',(-107.313375206758,-5.91311659137678,130.808668519379));
#171582=CARTESIAN_POINT('Ctrl Pts',(-109.063375192205,-5.91674955177621,
130.806663671189));
#171583=CARTESIAN_POINT('Ctrl Pts',(-109.056023423059,-5.91681000323962,
130.651358486149));
#171584=CARTESIAN_POINT('Ctrl Pts',(-109.048671653912,-5.9107514836903,
130.495803539147));
#171585=CARTESIAN_POINT('Ctrl Pts',(-109.041319884766,-5.89854122567361,
130.340526626219));
#171586=CARTESIAN_POINT('Ctrl Pts',(-109.033976470725,-5.88634484431719,
130.185426181713));
#171587=CARTESIAN_POINT('Ctrl Pts',(-109.026633056685,-5.86801066591285,
130.030603518659));
#171588=CARTESIAN_POINT('Ctrl Pts',(-109.019289642645,-5.8435578953709,
129.876588185367));
#171589=CARTESIAN_POINT('Ctrl Pts',(-109.011952897582,-5.81912733179754,
129.722712722265));
#171590=CARTESIAN_POINT('Ctrl Pts',(-109.004616152518,-5.78858929435041,
129.569643503627));
#171591=CARTESIAN_POINT('Ctrl Pts',(-108.997279407455,-5.75201490861492,
129.417906487935));
#171592=CARTESIAN_POINT('Ctrl Pts',(-108.989947651338,-5.71546539326063,
129.266272652579));
#171593=CARTESIAN_POINT('Ctrl Pts',(-108.982615895221,-5.67288778935029,
129.115969585884));
#171594=CARTESIAN_POINT('Ctrl Pts',(-108.975284139104,-5.62440453236753,
128.967514347792));
#171595=CARTESIAN_POINT('Ctrl Pts',(-108.96795496801,-5.57593836955698,
128.819111451881));
#171596=CARTESIAN_POINT('Ctrl Pts',(-108.960625796915,-5.52157081217014,
128.672555450604));
#171597=CARTESIAN_POINT('Ctrl Pts',(-108.95329662582,-5.46147449631298,
128.528349438195));
#171598=CARTESIAN_POINT('Ctrl Pts',(-108.945968652129,-5.40138799868857,
128.384166985436));
#171599=CARTESIAN_POINT('Ctrl Pts',(-108.938640678437,-5.33557475075789,
128.242334109451));
#171600=CARTESIAN_POINT('Ctrl Pts',(-108.931312704745,-5.26425589327723,
128.103334802696));
#171601=CARTESIAN_POINT('Ctrl Pts',(-108.923984414724,-5.19293395714485,
127.964329495698));
#171602=CARTESIAN_POINT('Ctrl Pts',(-108.916656124702,-5.1161061122852,
127.828158340491));
#171603=CARTESIAN_POINT('Ctrl Pts',(-108.909327834681,-5.03403978129622,
127.695281325745));
#171604=CARTESIAN_POINT('Ctrl Pts',(-108.901997714597,-4.95195295623358,
127.562371128192));
#171605=CARTESIAN_POINT('Ctrl Pts',(-108.894667594513,-4.86462524191013,
127.432757032239));
#171606=CARTESIAN_POINT('Ctrl Pts',(-108.887337474429,-4.77236761262287,
127.3068703842));
#171607=CARTESIAN_POINT('Ctrl Pts',(-108.879999739041,-4.68001413635613,
127.180852951802));
#171608=CARTESIAN_POINT('Ctrl Pts',(-108.872662003654,-4.58272074116282,
127.058571009372));
#171609=CARTESIAN_POINT('Ctrl Pts',(-108.865324268266,-4.48083937209908,
126.940423624815));
#171610=CARTESIAN_POINT('Ctrl Pts',(-108.857982558186,-4.37890281609824,
126.822212242373));
#171611=CARTESIAN_POINT('Ctrl Pts',(-108.850640848105,-4.27237359538035,
126.708140157104));
#171612=CARTESIAN_POINT('Ctrl Pts',(-108.843299138025,-4.16164029524909,
126.598569298984));
#171613=CARTESIAN_POINT('Ctrl Pts',(-108.835946378891,-4.05074034482209,
126.488833540008));
#171614=CARTESIAN_POINT('Ctrl Pts',(-108.828593619757,-3.93562395658254,
126.383612797555));
#171615=CARTESIAN_POINT('Ctrl Pts',(-108.821240860623,-3.81671324254075,
126.283229057136));
#171616=CARTESIAN_POINT('Ctrl Pts',(-108.815140663615,-3.71805928573641,
126.199945954592));
#171617=CARTESIAN_POINT('Ctrl Pts',(-108.809040466607,-3.6167943011096,
126.119991532806));
#171618=CARTESIAN_POINT('Ctrl Pts',(-108.802940269599,-3.51317353705052,
126.043526419543));
#171619=CARTESIAN_POINT('Ctrl Pts',(-108.795517003194,-3.38707850507706,
125.950476817087));
#171620=CARTESIAN_POINT('Ctrl Pts',(-108.788093736788,-3.25709349422422,
125.862299585812));
#171621=CARTESIAN_POINT('Ctrl Pts',(-108.780670470383,-3.1236317535783,
125.779337709107));
#171622=CARTESIAN_POINT('Ctrl Pts',(-108.773255977662,-2.99032775362614,
125.696473886451));
#171623=CARTESIAN_POINT('Ctrl Pts',(-108.765841484941,-2.85355551721927,
125.61881334381));
#171624=CARTESIAN_POINT('Ctrl Pts',(-108.75842699222,-2.71376036768682,
125.546658150778));
#171625=CARTESIAN_POINT('Ctrl Pts',(-108.751019645866,-2.57409995798308,
125.474572503637));
#171626=CARTESIAN_POINT('Ctrl Pts',(-108.743612299512,-2.43142276504334,
125.407981812447));
#171627=CARTESIAN_POINT('Ctrl Pts',(-108.736204953159,-2.28620193240537,
125.347144176305));
#171628=CARTESIAN_POINT('Ctrl Pts',(-108.728803131483,-2.14108941094326,
125.286351915167));
#171629=CARTESIAN_POINT('Ctrl Pts',(-108.721401309808,-1.99343737007284,
125.231304309045));
#171630=CARTESIAN_POINT('Ctrl Pts',(-108.713999488133,-1.84374222771336,
125.182212882025));
#171631=CARTESIAN_POINT('Ctrl Pts',(-108.706601573821,-1.69412610825474,
125.133147369988));
#171632=CARTESIAN_POINT('Ctrl Pts',(-108.69920365951,-1.54246938907896,
125.090031891219));
#171633=CARTESIAN_POINT('Ctrl Pts',(-108.691805745199,-1.3892869732124,
125.053029270081));
#171634=CARTESIAN_POINT('Ctrl Pts',(-108.684409060287,-1.23613001348369,
125.016032798108));
#171635=CARTESIAN_POINT('Ctrl Pts',(-108.677012375374,-1.08144822277829,
124.985147255178));
#171636=CARTESIAN_POINT('Ctrl Pts',(-108.669615690462,-0.925770236217381,
124.960485188347));
#171637=CARTESIAN_POINT('Ctrl Pts',(-108.662219333527,-0.770099152581536,
124.935824215057));
#171638=CARTESIAN_POINT('Ctrl Pts',(-108.654822976591,-0.613432329619568,
124.91738622758));
#171639=CARTESIAN_POINT('Ctrl Pts',(-108.647426619656,-0.45630686529425,
124.905232325421));
#171640=CARTESIAN_POINT('Ctrl Pts',(-108.640029130319,-0.299157344659222,
124.893076562469));
#171641=CARTESIAN_POINT('Ctrl Pts',(-108.632631640983,-0.141549415055182,
124.887206829314));
#171642=CARTESIAN_POINT('Ctrl Pts',(-108.625234151646,0.0159766059581922,
124.887632187888));
#171643=CARTESIAN_POINT('Ctrl Pts',(-108.617834069131,0.173557847473812,
124.88805769557));
#171644=CARTESIAN_POINT('Ctrl Pts',(-108.610433986616,0.331056750167858,
124.894782687566));
#171645=CARTESIAN_POINT('Ctrl Pts',(-108.603033904101,0.4879350526925,124.907764146138));
#171646=CARTESIAN_POINT('Ctrl Pts',(-108.595625684435,0.644985859038026,
124.920759879158));
#171647=CARTESIAN_POINT('Ctrl Pts',(-108.588217464768,0.80141433013455,
124.94002578702));
#171648=CARTESIAN_POINT('Ctrl Pts',(-108.580809245102,0.956688635779004,
124.965467107947));
#171649=CARTESIAN_POINT('Ctrl Pts',(-108.5733964658,1.11205851016769,124.990924087583));
#171650=CARTESIAN_POINT('Ctrl Pts',(-108.565983686498,1.26627243877102,
125.02256397913));
#171651=CARTESIAN_POINT('Ctrl Pts',(-108.558570907196,1.41881129762964,
125.060241445385));
#171652=CARTESIAN_POINT('Ctrl Pts',(-108.551147536167,1.57156811116338,
125.097972746971));
#171653=CARTESIAN_POINT('Ctrl Pts',(-108.543724165138,1.72264471716643,
125.14175874922));
#171654=CARTESIAN_POINT('Ctrl Pts',(-108.53630079411,1.87153880259726,125.191404794395));
#171655=CARTESIAN_POINT('Ctrl Pts',(-108.532364744669,1.95048601936168,
125.217728318788));
#171656=CARTESIAN_POINT('Ctrl Pts',(-108.528428695228,2.02882000040759,
125.245698513283));
#171657=CARTESIAN_POINT('Ctrl Pts',(-108.524492645787,2.10646853381558,
125.275281048728));
#171658=CARTESIAN_POINT('Ctrl Pts',(-108.517069379381,2.25291124448683,
125.331072787334));
#171659=CARTESIAN_POINT('Ctrl Pts',(-108.509646112976,2.39735731989397,
125.392770910978));
#171660=CARTESIAN_POINT('Ctrl Pts',(-108.502222846571,2.53929482717109,
125.4602131324));
#171661=CARTESIAN_POINT('Ctrl Pts',(-108.49480835385,2.68106457610179,125.527575642718));
#171662=CARTESIAN_POINT('Ctrl Pts',(-108.487393861129,2.8203313247116,125.600668578536));
#171663=CARTESIAN_POINT('Ctrl Pts',(-108.479979368408,2.95660022515872,
125.679280552719));
#171664=CARTESIAN_POINT('Ctrl Pts',(-108.472572022054,3.09273778450955,
125.757816757722));
#171665=CARTESIAN_POINT('Ctrl Pts',(-108.4651646757,3.22588292682234,125.841861225814));
#171666=CARTESIAN_POINT('Ctrl Pts',(-108.457757329346,3.35556276037715,
125.931155396803));
#171667=CARTESIAN_POINT('Ctrl Pts',(-108.450355507671,3.48514587381992,
126.020382968831));
#171668=CARTESIAN_POINT('Ctrl Pts',(-108.442953685995,3.61126851857284,
126.114852236817));
#171669=CARTESIAN_POINT('Ctrl Pts',(-108.43555186432,3.73348440741865,126.214259884242));
#171670=CARTESIAN_POINT('Ctrl Pts',(-108.428153950009,3.85563577944772,
126.313615055144));
#171671=CARTESIAN_POINT('Ctrl Pts',(-108.420756035697,3.97388421396637,
126.417903178699));
#171672=CARTESIAN_POINT('Ctrl Pts',(-108.413358121386,4.08781440456307,
126.526779062955));
#171673=CARTESIAN_POINT('Ctrl Pts',(-108.405961436474,4.20172566202916,
126.635636854015));
#171674=CARTESIAN_POINT('Ctrl Pts',(-108.398564751562,4.3113198302086,126.749080634977));
#171675=CARTESIAN_POINT('Ctrl Pts',(-108.391168066649,4.41621647988275,
126.866726484573));
#171676=CARTESIAN_POINT('Ctrl Pts',(-108.383771709714,4.52110847832952,
126.984367117629));
#171677=CARTESIAN_POINT('Ctrl Pts',(-108.376375352779,4.62130312399578,
127.106209170218));
#171678=CARTESIAN_POINT('Ctrl Pts',(-108.368978995843,4.71645869756903,
127.231833792387));
#171679=CARTESIAN_POINT('Ctrl Pts',(-108.361581506507,4.81162883970351,
127.357477648006));
#171680=CARTESIAN_POINT('Ctrl Pts',(-108.35418401717,4.9017581481849,127.486904928724));
#171681=CARTESIAN_POINT('Ctrl Pts',(-108.346786527833,4.98654694411484,
127.619665948271));
#171682=CARTESIAN_POINT('Ctrl Pts',(-108.339386445318,5.07136546262564,
127.752473506986));
#171683=CARTESIAN_POINT('Ctrl Pts',(-108.331986362803,5.15083954042843,
127.888616816865));
#171684=CARTESIAN_POINT('Ctrl Pts',(-108.324586280288,5.22471442615815,
128.027619771251));
#171685=CARTESIAN_POINT('Ctrl Pts',(-108.317178060622,5.29867054491936,
128.166775573676));
#171686=CARTESIAN_POINT('Ctrl Pts',(-108.309769840955,5.36701500060249,
128.308796970489));
#171687=CARTESIAN_POINT('Ctrl Pts',(-108.302361621289,5.42954005175752,
128.453185296825));
#171688=CARTESIAN_POINT('Ctrl Pts',(-108.294948841987,5.4921035860386,128.597662491768));
#171689=CARTESIAN_POINT('Ctrl Pts',(-108.287536062685,5.54884044448712,
128.744509171697));
#171690=CARTESIAN_POINT('Ctrl Pts',(-108.280123283383,5.59959230422747,
128.893210024615));
#171691=CARTESIAN_POINT('Ctrl Pts',(-108.272699912354,5.65041668060468,
129.042123348284));
#171692=CARTESIAN_POINT('Ctrl Pts',(-108.265276541325,5.69523887262437,
129.192895779375));
#171693=CARTESIAN_POINT('Ctrl Pts',(-108.257853170296,5.73395113888528,
129.344999490437));
#171694=CARTESIAN_POINT('Ctrl Pts',(-108.253917120855,5.75447731134562,
129.425648527723));
#171695=CARTESIAN_POINT('Ctrl Pts',(-108.249981071415,5.77328662472877,
129.506671697843));
#171696=CARTESIAN_POINT('Ctrl Pts',(-108.246045021974,5.79036892881588,
129.58798969112));
#171697=CARTESIAN_POINT('Ctrl Pts',(-108.238621755568,5.82258562120263,
129.741352888587));
#171698=CARTESIAN_POINT('Ctrl Pts',(-108.231198489163,5.84875387444842,
129.896228805643));
#171699=CARTESIAN_POINT('Ctrl Pts',(-108.223775222757,5.86873351320218,
130.052099018441));
#171700=CARTESIAN_POINT('Ctrl Pts',(-108.216360730036,5.88868953768214,
130.207785005593));
#171701=CARTESIAN_POINT('Ctrl Pts',(-108.208946237315,5.90247146008212,
130.364462582642));
#171702=CARTESIAN_POINT('Ctrl Pts',(-108.201531744594,5.90998964903964,
130.521601160174));
#171703=CARTESIAN_POINT('Ctrl Pts',(-108.194124398241,5.91750059168362,
130.678588281631));
#171704=CARTESIAN_POINT('Ctrl Pts',(-108.186717051887,5.91875980208571,
130.83603514863));
#171705=CARTESIAN_POINT('Ctrl Pts',(-108.179309705533,5.91372920473236,
130.993404145875));
#171706=CARTESIAN_POINT('Ctrl Pts',(-108.171907883857,5.90870235938832,
131.150655771385));
#171707=CARTESIAN_POINT('Ctrl Pts',(-108.164506062182,5.89739505892894,
131.307829271281));
#171708=CARTESIAN_POINT('Ctrl Pts',(-108.157104240507,5.87982126298926,
131.464385221501));
#171709=CARTESIAN_POINT('Ctrl Pts',(-108.149706326195,5.86225674411971,
131.620858527053));
#171710=CARTESIAN_POINT('Ctrl Pts',(-108.142308411884,5.83843235941513,
131.776714562144));
#171711=CARTESIAN_POINT('Ctrl Pts',(-108.134910497573,5.80841404538217,
131.931417333045));
#171712=CARTESIAN_POINT('Ctrl Pts',(-108.12751381266,5.77840071984838,132.086094395153));
#171713=CARTESIAN_POINT('Ctrl Pts',(-108.120117127748,5.74219557891749,
132.239618207339));
#171714=CARTESIAN_POINT('Ctrl Pts',(-108.112720442836,5.69991599514033,
132.391461184904));
#171715=CARTESIAN_POINT('Ctrl Pts',(-108.105324085901,5.65763828608422,
132.543297429592));
#171716=CARTESIAN_POINT('Ctrl Pts',(-108.097927728965,5.60928676986781,
132.693452628232));
#171717=CARTESIAN_POINT('Ctrl Pts',(-108.09053137203,5.55502912918315,132.84141288406));
#171718=CARTESIAN_POINT('Ctrl Pts',(-108.083133882693,5.50076318151534,
132.989395792979));
#171719=CARTESIAN_POINT('Ctrl Pts',(-108.075736393357,5.44058943744113,
133.135182739464));
#171720=CARTESIAN_POINT('Ctrl Pts',(-108.06833890402,5.37472424699098,133.278278528756));
#171721=CARTESIAN_POINT('Ctrl Pts',(-108.060938821505,5.30883596759976,
133.421424480057));
#171722=CARTESIAN_POINT('Ctrl Pts',(-108.05353873899,5.23725242553421,133.56187705701));
#171723=CARTESIAN_POINT('Ctrl Pts',(-108.046138656475,5.16023648347125,
133.699164582803));
#171724=CARTESIAN_POINT('Ctrl Pts',(-108.038730436808,5.0831358544629,133.836603070343));
#171725=CARTESIAN_POINT('Ctrl Pts',(-108.031322217142,5.00059107877114,
133.970869230568));
#171726=CARTESIAN_POINT('Ctrl Pts',(-108.023913997475,4.91290940794283,
134.101518744172));
#171727=CARTESIAN_POINT('Ctrl Pts',(-108.016501218173,4.82517377050918,
134.232248670372));
#171728=CARTESIAN_POINT('Ctrl Pts',(-108.009088438871,4.73229515763702,
134.359357213687));
#171729=CARTESIAN_POINT('Ctrl Pts',(-108.001675659569,4.63462153852264,
134.482432633876));
#171730=CARTESIAN_POINT('Ctrl Pts',(-107.994252288541,4.53680835876098,
134.605683909997));
#171731=CARTESIAN_POINT('Ctrl Pts',(-107.986828917512,4.43418673201651,
134.724890271399));
#171732=CARTESIAN_POINT('Ctrl Pts',(-107.979405546483,4.32714249761254,
134.839675768562));
#171733=CARTESIAN_POINT('Ctrl Pts',(-107.975469497042,4.27038507604071,
134.900537793397));
#171734=CARTESIAN_POINT('Ctrl Pts',(-107.971533447601,4.21238488165182,
134.960157604002));
#171735=CARTESIAN_POINT('Ctrl Pts',(-107.967597398161,4.15320315348277,
135.018483791893));
#171736=CARTESIAN_POINT('Ctrl Pts',(-107.960174131755,4.041588261154,135.128485161957));
#171737=CARTESIAN_POINT('Ctrl Pts',(-107.95275086535,3.92543134589529,135.23421547076));
#171738=CARTESIAN_POINT('Ctrl Pts',(-107.945327598944,3.80509280417013,
135.335276564055));
#171739=CARTESIAN_POINT('Ctrl Pts',(-107.937913106223,3.68489649260779,
135.436218211531));
#171740=CARTESIAN_POINT('Ctrl Pts',(-107.930498613502,3.56052867539627,
135.532501390628));
#171741=CARTESIAN_POINT('Ctrl Pts',(-107.923084120781,3.43238730449575,
135.623763895404));
#171742=CARTESIAN_POINT('Ctrl Pts',(-107.915676774428,3.30436944107258,
135.714938437942));
#171743=CARTESIAN_POINT('Ctrl Pts',(-107.908269428074,3.17258556671991,
135.801101724782));
#171744=CARTESIAN_POINT('Ctrl Pts',(-107.90086208172,3.03746741166749,135.881931127717));
#171745=CARTESIAN_POINT('Ctrl Pts',(-107.893460260045,2.90245003283244,
135.962700245034));
#171746=CARTESIAN_POINT('Ctrl Pts',(-107.886058438369,2.76410364389025,
136.038143208789));
#171747=CARTESIAN_POINT('Ctrl Pts',(-107.878656616694,2.62288962310563,
136.107980191735));
#171748=CARTESIAN_POINT('Ctrl Pts',(-107.871258702382,2.48175014810378,
136.177780308281));
#171749=CARTESIAN_POINT('Ctrl Pts',(-107.863860788071,2.33774638983323,
136.241980172649));
#171750=CARTESIAN_POINT('Ctrl Pts',(-107.85646287376,2.19136493529039,136.300345541388));
#171751=CARTESIAN_POINT('Ctrl Pts',(-107.849066188847,2.04500780668987,
136.358701210861));
#171752=CARTESIAN_POINT('Ctrl Pts',(-107.841669503935,1.89627411244474,
136.411224170927));
#171753=CARTESIAN_POINT('Ctrl Pts',(-107.834272819023,1.74567116723508,
136.45772799802));
#171754=CARTESIAN_POINT('Ctrl Pts',(-107.826876462088,1.59507489991783,
136.504229763085));
#171755=CARTESIAN_POINT('Ctrl Pts',(-107.819480105152,1.44260990311884,
136.544712815716));
#171756=CARTESIAN_POINT('Ctrl Pts',(-107.812083748217,1.28879916933246,
136.579040458356));
#171757=CARTESIAN_POINT('Ctrl Pts',(-107.80468625888,1.13496488673009,136.613373356646));
#171758=CARTESIAN_POINT('Ctrl Pts',(-107.797288769544,0.979784821253583,
136.641548887167));
#171759=CARTESIAN_POINT('Ctrl Pts',(-107.789891280207,0.823792536753465,
136.663481406463));
#171760=CARTESIAN_POINT('Ctrl Pts',(-107.782491197692,0.667745569400947,
136.68542161417));
#171761=CARTESIAN_POINT('Ctrl Pts',(-107.775091115177,0.510886185576555,
136.701114401467));
#171762=CARTESIAN_POINT('Ctrl Pts',(-107.767691032662,0.353753304040651,
136.71052596933));
#171763=CARTESIAN_POINT('Ctrl Pts',(-107.760282812996,0.196447638746722,
136.719947886179));
#171764=CARTESIAN_POINT('Ctrl Pts',(-107.752874593329,0.0388682480047973,
136.723074767836));
#171765=CARTESIAN_POINT('Ctrl Pts',(-107.745466373663,-0.11844497280288,
136.719924948289));
#171766=CARTESIAN_POINT('Ctrl Pts',(-107.738053594361,-0.275855017273053,
136.71677319008));
#171767=CARTESIAN_POINT('Ctrl Pts',(-107.730640815059,-0.432998193608058,
136.707337055073));
#171768=CARTESIAN_POINT('Ctrl Pts',(-107.723228035757,-0.589340007231835,
136.691686743948));
#171769=CARTESIAN_POINT('Ctrl Pts',(-107.715804664728,-0.745905209370844,
136.676014070924));
#171770=CARTESIAN_POINT('Ctrl Pts',(-107.708381293699,-0.901666393246402,
136.654109540064));
#171771=CARTESIAN_POINT('Ctrl Pts',(-107.70095792267,-1.05609870629948,
136.626094559018));
#171772=CARTESIAN_POINT('Ctrl Pts',(-107.69702187323,-1.13798242423446,
136.611240343857));
#171773=CARTESIAN_POINT('Ctrl Pts',(-107.693085823789,-1.21949278122046,
136.594669101593));
#171774=CARTESIAN_POINT('Ctrl Pts',(-107.689149774348,-1.30055342464799,
136.576404566821));
#171775=CARTESIAN_POINT('Ctrl Pts',(-107.681726507942,-1.4534312683332,
136.54195822426));
#171776=CARTESIAN_POINT('Ctrl Pts',(-107.674303241537,-1.60517082155485,
136.501381936232));
#171777=CARTESIAN_POINT('Ctrl Pts',(-107.666879975132,-1.7552423027785,
136.454763702394));
#171778=CARTESIAN_POINT('Ctrl Pts',(-107.659465482411,-1.90513641197444,
136.408200567438));
#171779=CARTESIAN_POINT('Ctrl Pts',(-107.65205098969,-2.05336602048654,
136.355609810687));
#171780=CARTESIAN_POINT('Ctrl Pts',(-107.644636496969,-2.19941129144228,
136.297130459238));
#171781=CARTESIAN_POINT('Ctrl Pts',(-107.637229150615,-2.34531579846778,
136.238707472389));
#171782=CARTESIAN_POINT('Ctrl Pts',(-107.629821804261,-2.48903981504603,
136.174407327774));
#171783=CARTESIAN_POINT('Ctrl Pts',(-107.622414457907,-2.63007854419395,
136.104418863838));
#171784=CARTESIAN_POINT('Ctrl Pts',(-107.615012636232,-2.77101208133618,
136.034482599938));
#171785=CARTESIAN_POINT('Ctrl Pts',(-107.607610814556,-2.90926398592004,
135.958866629453));
#171786=CARTESIAN_POINT('Ctrl Pts',(-107.600208992881,-3.04434944513681,
135.877807869524));
#171787=CARTESIAN_POINT('Ctrl Pts',(-107.59281107857,-3.17936359379116,
135.796791899882));
#171788=CARTESIAN_POINT('Ctrl Pts',(-107.585413164258,-3.3112143067519,
135.71033905451));
#171789=CARTESIAN_POINT('Ctrl Pts',(-107.578015249947,-3.43944149621148,
135.618732098522));
#171790=CARTESIAN_POINT('Ctrl Pts',(-107.570618565035,-3.5676473766379,
135.527140365947));
#171791=CARTESIAN_POINT('Ctrl Pts',(-107.563221880122,-3.69223062523073,
135.430396439482));
#171792=CARTESIAN_POINT('Ctrl Pts',(-107.55582519521,-3.81276018258793,
135.328826370843));
#171793=CARTESIAN_POINT('Ctrl Pts',(-107.548428838275,-3.93328439553861,
135.227260805926));
#171794=CARTESIAN_POINT('Ctrl Pts',(-107.541032481339,-4.04975498919121,
135.120869764886));
#171795=CARTESIAN_POINT('Ctrl Pts',(-107.533636124404,-4.16177426580181,
135.010019367751));
#171796=CARTESIAN_POINT('Ctrl Pts',(-107.526238635067,-4.27381069284995,
134.899151999137));
#171797=CARTESIAN_POINT('Ctrl Pts',(-107.518841145731,-4.3813941805237,
134.783824177595));
#171798=CARTESIAN_POINT('Ctrl Pts',(-107.511443656394,-4.48416427026502,
134.664438513124));
#171799=CARTESIAN_POINT('Ctrl Pts',(-107.504043573879,-4.58697038590184,
134.545010998194));
#171800=CARTESIAN_POINT('Ctrl Pts',(-107.496643491364,-4.68495950075922,
134.421523090944));
#171801=CARTESIAN_POINT('Ctrl Pts',(-107.489243408849,-4.77781188000648,
134.294409929792));
#171802=CARTESIAN_POINT('Ctrl Pts',(-107.481835189183,-4.87076635999004,
134.167156994652));
#171803=CARTESIAN_POINT('Ctrl Pts',(-107.474426969516,-4.95857260387171,
134.036271146253));
#171804=CARTESIAN_POINT('Ctrl Pts',(-107.46701874985,-5.04095420991477,
133.902216523841));
#171805=CARTESIAN_POINT('Ctrl Pts',(-107.459605970548,-5.12338652046197,
133.768079393045));
#171806=CARTESIAN_POINT('Ctrl Pts',(-107.452193191246,-5.20038735807925,
133.630769926805));
#171807=CARTESIAN_POINT('Ctrl Pts',(-107.444780411944,-5.27172687721469,
133.490775755729));
#171808=CARTESIAN_POINT('Ctrl Pts',(-107.437357040915,-5.34316832960026,
133.350581554417));
#171809=CARTESIAN_POINT('Ctrl Pts',(-107.429933669886,-5.40893215198175,
133.207695325058));
#171810=CARTESIAN_POINT('Ctrl Pts',(-107.422510298857,-5.46883679242566,
133.062624264776));
#171811=CARTESIAN_POINT('Ctrl Pts',(-107.418574249417,-5.50059967017909,
132.985704107687));
#171812=CARTESIAN_POINT('Ctrl Pts',(-107.414638199976,-5.53071615369011,
132.90816997465));
#171813=CARTESIAN_POINT('Ctrl Pts',(-107.410702150536,-5.55916494109477,
132.830098932404));
#171814=CARTESIAN_POINT('Ctrl Pts',(-107.402111129881,-5.621258703863,132.65969712556));
#171815=CARTESIAN_POINT('Ctrl Pts',(-107.393520109225,-5.67555971971428,
132.486312339245));
#171816=CARTESIAN_POINT('Ctrl Pts',(-107.38492908857,-5.72181188622781,
132.310614016275));
#171817=CARTESIAN_POINT('Ctrl Pts',(-107.376370430877,-5.767889817669,132.135577560896));
#171818=CARTESIAN_POINT('Ctrl Pts',(-107.367811773184,-5.80597933618538,
131.958245083306));
#171819=CARTESIAN_POINT('Ctrl Pts',(-107.359253115491,-5.83587378478307,
131.779300477548));
#171820=CARTESIAN_POINT('Ctrl Pts',(-107.350757783627,-5.86554704323359,
131.601679889645));
#171821=CARTESIAN_POINT('Ctrl Pts',(-107.342262451764,-5.8871459811393,
131.422471073596));
#171822=CARTESIAN_POINT('Ctrl Pts',(-107.3337671199,-5.90051563382055,131.242362692378));
#171823=CARTESIAN_POINT('Ctrl Pts',(-107.32696982208,-5.91121298060858,
131.098254101133));
#171824=CARTESIAN_POINT('Ctrl Pts',(-107.32017252426,-5.91664285591595,
130.953570016966));
#171825=CARTESIAN_POINT('Ctrl Pts',(-107.31337522644,-5.91674842950609,
130.80867158466));
#171826=CARTESIAN_POINT('',(-105.563375192205,-5.90975296513838,130.800404415155));
#171827=CARTESIAN_POINT('Ctrl Pts',(-107.313375192205,-5.91043119270566,
130.808666252895));
#171828=CARTESIAN_POINT('Ctrl Pts',(-107.253001637044,-5.90181299183432,
129.523046449566));
#171829=CARTESIAN_POINT('Ctrl Pts',(-107.099812207279,-4.8565494805829,
126.248208310993));
#171830=CARTESIAN_POINT('Ctrl Pts',(-106.85380690291,0.553929572890924,
123.827920081116));
#171831=CARTESIAN_POINT('Ctrl Pts',(-106.575359279096,6.16888947100959,
127.499460736355));
#171832=CARTESIAN_POINT('Ctrl Pts',(-106.296911655284,6.11494131227265,
134.208042929093));
#171833=CARTESIAN_POINT('Ctrl Pts',(-106.018464031471,0.441660819049746,
137.78880735666));
#171834=CARTESIAN_POINT('Ctrl Pts',(-105.773951877111,-4.8965958753672,
135.297035641043));
#171835=CARTESIAN_POINT('Ctrl Pts',(-105.622255597356,-5.90208552014624,
132.054589738716));
#171836=CARTESIAN_POINT('Ctrl Pts',(-105.563375192205,-5.90975296513838,
130.800404415155));
#171837=CARTESIAN_POINT('',(-103.813375192205,-5.92489227885479,130.801538229806));
#171838=CARTESIAN_POINT('Ctrl Pts',(-105.563375192205,-5.90975296513838,
130.800404415155));
#171839=CARTESIAN_POINT('Ctrl Pts',(-105.529439722752,-5.91417206423678,
130.077560072841));
#171840=CARTESIAN_POINT('Ctrl Pts',(-105.402688378692,-5.45597557692382,
127.383094551451));
#171841=CARTESIAN_POINT('Ctrl Pts',(-105.183121160033,-1.42831237022071,
123.953266960094));
#171842=CARTESIAN_POINT('Ctrl Pts',(-104.90467353622,4.99198140251171,125.899497499463));
#171843=CARTESIAN_POINT('Ctrl Pts',(-104.626225912407,6.82488813818383,
132.353057628482));
#171844=CARTESIAN_POINT('Ctrl Pts',(-104.347778288594,2.38605608918648,
137.383440862523));
#171845=CARTESIAN_POINT('Ctrl Pts',(-104.076828048526,-4.06688745323623,
136.395312951788));
#171846=CARTESIAN_POINT('Ctrl Pts',(-103.898693683064,-5.91427678181791,
132.606982621728));
#171847=CARTESIAN_POINT('Ctrl Pts',(-103.813375192205,-5.92489227885479,
130.801538229806));
#171848=CARTESIAN_POINT('',(-102.063375192205,-5.91808296072073,130.809685412516));
#171849=CARTESIAN_POINT('Ctrl Pts',(-103.813375192205,-5.92489227885479,
130.801538229806));
#171850=CARTESIAN_POINT('Ctrl Pts',(-103.805877808459,-5.92582511831476,
130.642884351829));
#171851=CARTESIAN_POINT('Ctrl Pts',(-103.798380424714,-5.92000731493553,
130.484299960519));
#171852=CARTESIAN_POINT('Ctrl Pts',(-103.698067166363,-5.74889566573683,
128.370026085815));
#171853=CARTESIAN_POINT('Ctrl Pts',(-103.512435417155,-3.29550805454775,
124.630448795005));
#171854=CARTESIAN_POINT('Ctrl Pts',(-103.233987793341,3.41298426984717,
124.694606211362));
#171855=CARTESIAN_POINT('Ctrl Pts',(-102.955540169529,6.98511078380345,
130.373329448925));
#171856=CARTESIAN_POINT('Ctrl Pts',(-102.677092545716,4.13826172907665,
136.448149273423));
#171857=CARTESIAN_POINT('Ctrl Pts',(-102.398644921904,-2.51144768934695,
137.336603037595));
#171858=CARTESIAN_POINT('Ctrl Pts',(-102.194072470733,-5.70132967268059,
133.57913972058));
#171859=CARTESIAN_POINT('Ctrl Pts',(-102.082315894167,-5.92220269805738,
131.211626874956));
#171860=CARTESIAN_POINT('Ctrl Pts',(-102.063375192205,-5.91847197029493,
130.809685762527));
#171861=CARTESIAN_POINT('',(-100.313375192239,-5.9167499888071,130.804724555984));
#171862=CARTESIAN_POINT('Ctrl Pts',(-102.063375192205,-5.91674760504896,
130.809684211029));
#171863=CARTESIAN_POINT('Ctrl Pts',(-102.056072017781,-5.91688700715738,
130.654749936505));
#171864=CARTESIAN_POINT('Ctrl Pts',(-102.048768843358,-5.91093665927345,
130.499620358955));
#171865=CARTESIAN_POINT('Ctrl Pts',(-102.041465668934,-5.89887734654449,
130.344821051343));
#171866=CARTESIAN_POINT('Ctrl Pts',(-102.034168273018,-5.88682757553336,
130.190144225944));
#171867=CARTESIAN_POINT('Ctrl Pts',(-102.026870877102,-5.86867848847835,
130.035797532258));
#171868=CARTESIAN_POINT('Ctrl Pts',(-102.019573481186,-5.84446293334446,
129.882306615209));
#171869=CARTESIAN_POINT('Ctrl Pts',(-102.012164155899,-5.8198759536767,
129.72646141423));
#171870=CARTESIAN_POINT('Ctrl Pts',(-102.004754830611,-5.78903486896265,
129.571498861028));
#171871=CARTESIAN_POINT('Ctrl Pts',(-101.997345505323,-5.75202887664798,
129.417964438724));
#171872=CARTESIAN_POINT('Ctrl Pts',(-101.990053608961,-5.71560938496194,
129.266863353011));
#171873=CARTESIAN_POINT('Ctrl Pts',(-101.982761712599,-5.67321906097977,
129.117145848256));
#171874=CARTESIAN_POINT('Ctrl Pts',(-101.975469816238,-5.62499442660723,
128.969321581704));
#171875=CARTESIAN_POINT('Ctrl Pts',(-101.96817822644,-5.57677181968034,
128.821503529935));
#171876=CARTESIAN_POINT('Ctrl Pts',(-101.960886636642,-5.52271550949202,
128.6755789241));
#171877=CARTESIAN_POINT('Ctrl Pts',(-101.953595046844,-5.46301166816555,
128.532041521139));
#171878=CARTESIAN_POINT('Ctrl Pts',(-101.94630222786,-5.40329776221654,
128.388479921246));
#171879=CARTESIAN_POINT('Ctrl Pts',(-101.939009408877,-5.33793457897994,
128.24730668025));
#171880=CARTESIAN_POINT('Ctrl Pts',(-101.931716589893,-5.26715601040432,
128.108994571078));
#171881=CARTESIAN_POINT('Ctrl Pts',(-101.924219346925,-5.19439345771586,
127.966805454603));
#171882=CARTESIAN_POINT('Ctrl Pts',(-101.916722103957,-5.11590766486404,
127.82764061171));
#171883=CARTESIAN_POINT('Ctrl Pts',(-101.909224860989,-5.03200221987744,
127.691984640656));
#171884=CARTESIAN_POINT('Ctrl Pts',(-101.901921253736,-4.95026385029387,
127.559832336357));
#171885=CARTESIAN_POINT('Ctrl Pts',(-101.894617646483,-4.86338260310448,
127.431010168018));
#171886=CARTESIAN_POINT('Ctrl Pts',(-101.88731403923,-4.7716815209098,127.305934396319));
#171887=CARTESIAN_POINT('Ctrl Pts',(-101.879719978405,-4.67633362338209,
127.175884547639));
#171888=CARTESIAN_POINT('Ctrl Pts',(-101.872125917579,-4.57577495020364,
127.049885568865));
#171889=CARTESIAN_POINT('Ctrl Pts',(-101.864531856754,-4.47041207257545,
126.928364427698));
#171890=CARTESIAN_POINT('Ctrl Pts',(-101.856937795929,-4.36504919494726,
126.806843286531));
#171891=CARTESIAN_POINT('Ctrl Pts',(-101.849343735103,-4.25488248181308,
126.68980026642));
#171892=CARTESIAN_POINT('Ctrl Pts',(-101.841749674278,-4.14035757478254,
126.577616041011));
#171893=CARTESIAN_POINT('Ctrl Pts',(-101.834326407872,-4.02840839311396,
126.467954897803));
#171894=CARTESIAN_POINT('Ctrl Pts',(-101.826903141467,-3.91193020919505,
126.362578620429));
#171895=CARTESIAN_POINT('Ctrl Pts',(-101.819479875061,-3.79128462966451,
126.261884264367));
#171896=CARTESIAN_POINT('Ctrl Pts',(-101.81206538234,-3.67078164318999,
126.161308920672));
#171897=CARTESIAN_POINT('Ctrl Pts',(-101.804650889619,-3.54612134916366,
126.065404720407));
#171898=CARTESIAN_POINT('Ctrl Pts',(-101.797236396898,-3.41770280013275,
125.974532656607));
#171899=CARTESIAN_POINT('Ctrl Pts',(-101.789829050545,-3.28940802573428,
125.883748178723));
#171900=CARTESIAN_POINT('Ctrl Pts',(-101.782421704191,-3.15736251038875,
125.797986395767));
#171901=CARTESIAN_POINT('Ctrl Pts',(-101.775014357837,-3.02199896429545,
125.717568620413));
#171902=CARTESIAN_POINT('Ctrl Pts',(-101.767612536161,-2.88673637744179,
125.637210823671));
#171903=CARTESIAN_POINT('Ctrl Pts',(-101.760210714486,-2.74816100688009,
125.562189288182));
#171904=CARTESIAN_POINT('Ctrl Pts',(-101.752808892811,-2.60673508043586,
125.49278243562));
#171905=CARTESIAN_POINT('Ctrl Pts',(-101.745410978499,-2.46538381163774,
125.423412222395));
#171906=CARTESIAN_POINT('Ctrl Pts',(-101.738013064188,-2.32118531807934,
125.359650953302));
#171907=CARTESIAN_POINT('Ctrl Pts',(-101.730615149876,-2.17462689745969,
125.301731389702));
#171908=CARTESIAN_POINT('Ctrl Pts',(-101.723218464964,-2.0280928321905,
125.243821451283));
#171909=CARTESIAN_POINT('Ctrl Pts',(-101.715821780052,-1.87919996504587,
125.191751428703));
#171910=CARTESIAN_POINT('Ctrl Pts',(-101.70842509514,-1.72845617576522,
125.145706200573));
#171911=CARTESIAN_POINT('Ctrl Pts',(-101.701028738204,-1.57771907062215,
125.099663014136));
#171912=CARTESIAN_POINT('Ctrl Pts',(-101.693632381269,-1.42513156354348,
125.059644200025));
#171913=CARTESIAN_POINT('Ctrl Pts',(-101.686236024333,-1.27121706066143,
125.025784863353));
#171914=CARTESIAN_POINT('Ctrl Pts',(-101.678838534997,-1.11727899307607,
124.99192034273));
#171915=CARTESIAN_POINT('Ctrl Pts',(-101.67144104566,-0.962013889759597,
124.964217257456));
#171916=CARTESIAN_POINT('Ctrl Pts',(-101.664043556324,-0.805955572760337,
124.942759626605));
#171917=CARTESIAN_POINT('Ctrl Pts',(-101.656643473808,-0.649842549759751,
124.921294473814));
#171918=CARTESIAN_POINT('Ctrl Pts',(-101.649243391293,-0.492936129049061,
124.906079185212));
#171919=CARTESIAN_POINT('Ctrl Pts',(-101.641843308778,-0.335775329764997,
124.897145919384));
#171920=CARTESIAN_POINT('Ctrl Pts',(-101.634435089112,-0.178441716025822,
124.888202830511));
#171921=CARTESIAN_POINT('Ctrl Pts',(-101.627026869445,-0.0208535380282623,
124.885555580799));
#171922=CARTESIAN_POINT('Ctrl Pts',(-101.619618649779,0.136449367148529,
124.889184193088));
#171923=CARTESIAN_POINT('Ctrl Pts',(-101.612205870477,0.293849089638717,
124.892815038726));
#171924=CARTESIAN_POINT('Ctrl Pts',(-101.604793091175,0.450962817748566,
124.902729419801));
#171925=CARTESIAN_POINT('Ctrl Pts',(-101.597380311873,0.607256273044526,
124.918855509137));
#171926=CARTESIAN_POINT('Ctrl Pts',(-101.589956940844,0.763773047759072,
124.935004640185));
#171927=CARTESIAN_POINT('Ctrl Pts',(-101.582533569815,0.919466840302727,
124.95738315305));
#171928=CARTESIAN_POINT('Ctrl Pts',(-101.575110198786,1.07381317007064,
124.985868043172));
#171929=CARTESIAN_POINT('Ctrl Pts',(-101.571174149346,1.15565129759787,
125.000971415399));
#171930=CARTESIAN_POINT('Ctrl Pts',(-101.567238099905,1.23711083986569,
125.017790670393));
#171931=CARTESIAN_POINT('Ctrl Pts',(-101.563302050465,1.31811551685823,
125.036301841278));
#171932=CARTESIAN_POINT('Ctrl Pts',(-101.555878784059,1.47088780960643,
125.071213331855));
#171933=CARTESIAN_POINT('Ctrl Pts',(-101.548455517654,1.62250315971815,
125.11225127494));
#171934=CARTESIAN_POINT('Ctrl Pts',(-101.541032251248,1.77243205595355,
125.159326058812));
#171935=CARTESIAN_POINT('Ctrl Pts',(-101.533617758527,1.92218374868442,
125.206345204198));
#171936=CARTESIAN_POINT('Ctrl Pts',(-101.526203265806,2.07025260243396,
125.259386877292));
#171937=CARTESIAN_POINT('Ctrl Pts',(-101.518788773085,2.21611920588817,
125.318310469436));
#171938=CARTESIAN_POINT('Ctrl Pts',(-101.511381426731,2.36184521761778,
125.377177268804));
#171939=CARTESIAN_POINT('Ctrl Pts',(-101.503974080378,2.50537286095345,
125.441914562052));
#171940=CARTESIAN_POINT('Ctrl Pts',(-101.496566734024,2.64619791600956,
125.512331975183));
#171941=CARTESIAN_POINT('Ctrl Pts',(-101.489164912348,2.78691793842699,
125.58269686835));
#171942=CARTESIAN_POINT('Ctrl Pts',(-101.481763090673,2.92493905363406,
125.658733279828));
#171943=CARTESIAN_POINT('Ctrl Pts',(-101.474361268997,3.05977717216197,
125.740202817969));
#171944=CARTESIAN_POINT('Ctrl Pts',(-101.466963354686,3.19454411069669,
125.821629348976));
#171945=CARTESIAN_POINT('Ctrl Pts',(-101.459565440375,3.3261310802111,125.908483102119));
#171946=CARTESIAN_POINT('Ctrl Pts',(-101.452167526063,3.45407885566847,
126.000479913247));
#171947=CARTESIAN_POINT('Ctrl Pts',(-101.444770841151,3.58200536852621,
126.092461436174));
#171948=CARTESIAN_POINT('Ctrl Pts',(-101.437374156239,3.70629358482421,
126.189584103082));
#171949=CARTESIAN_POINT('Ctrl Pts',(-101.429977471327,3.82651343954635,
126.291520551768));
#171950=CARTESIAN_POINT('Ctrl Pts',(-101.422581114391,3.9467279635945,126.393452480485));
#171951=CARTESIAN_POINT('Ctrl Pts',(-101.415184757456,4.06287420003124,
126.500197525152));
#171952=CARTESIAN_POINT('Ctrl Pts',(-101.40778840052,4.17455556729817,126.61138835698));
#171953=CARTESIAN_POINT('Ctrl Pts',(-101.400390911184,4.28625403326721,
126.722596212409));
#171954=CARTESIAN_POINT('Ctrl Pts',(-101.392993421847,4.39348600440325,
126.838250946889));
#171955=CARTESIAN_POINT('Ctrl Pts',(-101.385595932511,4.4958922492242,126.957948855174));
#171956=CARTESIAN_POINT('Ctrl Pts',(-101.378195849996,4.59833439239568,
127.077688723376));
#171957=CARTESIAN_POINT('Ctrl Pts',(-101.370795767481,4.69594719866225,
127.201474303797));
#171958=CARTESIAN_POINT('Ctrl Pts',(-101.363395684966,4.7884122590859,127.328869486872));
#171959=CARTESIAN_POINT('Ctrl Pts',(-101.355987465299,4.88097899434926,
127.456404754047));
#171960=CARTESIAN_POINT('Ctrl Pts',(-101.348579245633,4.96838646001872,
127.587557248193));
#171961=CARTESIAN_POINT('Ctrl Pts',(-101.341171025966,5.05035966831803,
127.721861990944));
#171962=CARTESIAN_POINT('Ctrl Pts',(-101.333758246664,5.1323833297595,127.856249396023));
#171963=CARTESIAN_POINT('Ctrl Pts',(-101.326345467362,5.20896588793141,
127.993792590317));
#171964=CARTESIAN_POINT('Ctrl Pts',(-101.31893268806,5.2798789825263,128.134003245906));
#171965=CARTESIAN_POINT('Ctrl Pts',(-101.311509317031,5.35089340107615,
128.274414241055));
#171966=CARTESIAN_POINT('Ctrl Pts',(-101.304085946002,5.41622202231293,
128.417499971028));
#171967=CARTESIAN_POINT('Ctrl Pts',(-101.296662574974,5.47568483887766,
128.56275268847));
#171968=CARTESIAN_POINT('Ctrl Pts',(-101.292726525533,5.50721345100937,
128.639769164545));
#171969=CARTESIAN_POINT('Ctrl Pts',(-101.288790476092,5.53709380779301,
128.717394602667));
#171970=CARTESIAN_POINT('Ctrl Pts',(-101.284854426652,5.56530484202796,
128.795551871617));
#171971=CARTESIAN_POINT('Ctrl Pts',(-101.277431160246,5.61850997216148,
128.94295404166));
#171972=CARTESIAN_POINT('Ctrl Pts',(-101.270007893841,5.6659353885349,129.092694340323));
#171973=CARTESIAN_POINT('Ctrl Pts',(-101.262584627435,5.70737027026856,
129.244278837481));
#171974=CARTESIAN_POINT('Ctrl Pts',(-101.255170134714,5.74875617941298,
129.395684174351));
#171975=CARTESIAN_POINT('Ctrl Pts',(-101.247755641993,5.78416554985556,
129.54892901446));
#171976=CARTESIAN_POINT('Ctrl Pts',(-101.240341149272,5.81343592513844,
129.703500359945));
#171977=CARTESIAN_POINT('Ctrl Pts',(-101.232933802919,5.84267808853162,
129.857922723748));
#171978=CARTESIAN_POINT('Ctrl Pts',(-101.225526456565,5.86579296734766,
130.013668683297));
#171979=CARTESIAN_POINT('Ctrl Pts',(-101.218119110211,5.88266818545696,
130.170211122327));
#171980=CARTESIAN_POINT('Ctrl Pts',(-101.210717288536,5.89953081739189,
130.326636806099));
#171981=CARTESIAN_POINT('Ctrl Pts',(-101.20331546686,5.9101630150755,130.483857416979));
#171982=CARTESIAN_POINT('Ctrl Pts',(-101.195913645185,5.91450368196843,
130.641336820279));
#171983=CARTESIAN_POINT('Ctrl Pts',(-101.188515730873,5.91884205745711,
130.798733091428));
#171984=CARTESIAN_POINT('Ctrl Pts',(-101.181117816562,5.91689550632446,
130.956387510711));
#171985=CARTESIAN_POINT('Ctrl Pts',(-101.173719902251,5.90865488157045,
131.113760121434));
#171986=CARTESIAN_POINT('Ctrl Pts',(-101.166323217338,5.90041562625877,
131.271106579684));
#171987=CARTESIAN_POINT('Ctrl Pts',(-101.158926532426,5.88588439274989,
131.428170949897));
#171988=CARTESIAN_POINT('Ctrl Pts',(-101.151529847514,5.865104139491,131.584414458929));
#171989=CARTESIAN_POINT('Ctrl Pts',(-101.144133490579,5.84432480765031,
131.74065103996));
#171990=CARTESIAN_POINT('Ctrl Pts',(-101.136737133643,5.81729705621921,
131.896066462142));
#171991=CARTESIAN_POINT('Ctrl Pts',(-101.129340776708,5.78411556729121,
132.050128519994));
#171992=CARTESIAN_POINT('Ctrl Pts',(-101.121943287371,5.75092899819263,
132.20421416514));
#171993=CARTESIAN_POINT('Ctrl Pts',(-101.114545798035,5.7115868942481,132.356945668434));
#171994=CARTESIAN_POINT('Ctrl Pts',(-101.107148308698,5.66623473072437,
132.50780258571));
#171995=CARTESIAN_POINT('Ctrl Pts',(-101.099748226183,5.62086666906996,
132.658712385644));
#171996=CARTESIAN_POINT('Ctrl Pts',(-101.092348143668,5.56948446058505,
132.807745933942));
#171997=CARTESIAN_POINT('Ctrl Pts',(-101.084948061153,5.51228290878922,
132.954399616275));
#171998=CARTESIAN_POINT('Ctrl Pts',(-101.077539841487,5.45501845800665,
133.101214559408));
#171999=CARTESIAN_POINT('Ctrl Pts',(-101.07013162182,5.39192202049038,133.245644062448));
#172000=CARTESIAN_POINT('Ctrl Pts',(-101.062723402154,5.32323615809954,
133.387205438224));
#172001=CARTESIAN_POINT('Ctrl Pts',(-101.055310622852,5.25450802070668,
133.528853942665));
#172002=CARTESIAN_POINT('Ctrl Pts',(-101.04789784355,5.18018377924718,133.66763047398));
#172003=CARTESIAN_POINT('Ctrl Pts',(-101.040485064248,5.1005508435062,133.803078953007));
#172004=CARTESIAN_POINT('Ctrl Pts',(-101.033061693219,5.02080412449189,
133.938720967173));
#172005=CARTESIAN_POINT('Ctrl Pts',(-101.02563832219,4.93573376298643,134.071025118535));
#172006=CARTESIAN_POINT('Ctrl Pts',(-101.018214951161,4.84566964284574,
134.199565511958));
#172007=CARTESIAN_POINT('Ctrl Pts',(-101.01427890172,4.79791548528698,134.267720712837));
#172008=CARTESIAN_POINT('Ctrl Pts',(-101.01034285228,4.7487580684344,134.334818348671));
#172009=CARTESIAN_POINT('Ctrl Pts',(-101.006406802839,4.69825089763084,
134.400799003721));
#172010=CARTESIAN_POINT('Ctrl Pts',(-100.998983536433,4.60299594977255,
134.525236459956));
#172011=CARTESIAN_POINT('Ctrl Pts',(-100.991560270028,4.50264979162134,
134.646075094947));
#172012=CARTESIAN_POINT('Ctrl Pts',(-100.984137003622,4.39751402674697,
134.762870557817));
#172013=CARTESIAN_POINT('Ctrl Pts',(-100.976722510901,4.2925025236157,134.879527978149));
#172014=CARTESIAN_POINT('Ctrl Pts',(-100.96930801818,4.18271292915891,134.99215146364));
#172015=CARTESIAN_POINT('Ctrl Pts',(-100.961893525459,4.06848903132321,
135.100327047195));
#172016=CARTESIAN_POINT('Ctrl Pts',(-100.954486179105,3.95437522678069,
135.208398367051));
#172017=CARTESIAN_POINT('Ctrl Pts',(-100.947078832752,3.83583589666972,
135.312030064689));
#172018=CARTESIAN_POINT('Ctrl Pts',(-100.939671486398,3.71325377678995,
135.410842675672));
#172019=CARTESIAN_POINT('Ctrl Pts',(-100.932269664722,3.59076308327994,
135.509581588483));
#172020=CARTESIAN_POINT('Ctrl Pts',(-100.924867843047,3.46423589318093,
135.603508338021));
#172021=CARTESIAN_POINT('Ctrl Pts',(-100.917466021372,3.33409024761793,
135.692281728145));
#172022=CARTESIAN_POINT('Ctrl Pts',(-100.91006810706,3.20401330492928,135.781008255485));
#172023=CARTESIAN_POINT('Ctrl Pts',(-100.902670192749,3.07032201854756,
135.864586631434));
#172024=CARTESIAN_POINT('Ctrl Pts',(-100.895272278438,2.93346572515558,
135.942717300576));
#172025=CARTESIAN_POINT('Ctrl Pts',(-100.887875593526,2.79663217479577,
136.02083498582));
#172026=CARTESIAN_POINT('Ctrl Pts',(-100.880478908613,2.6566349851843,136.093506576134));
#172027=CARTESIAN_POINT('Ctrl Pts',(-100.873082223701,2.51395066151732,
136.160476993631));
#172028=CARTESIAN_POINT('Ctrl Pts',(-100.865685866766,2.37127266462237,
136.227444441591));
#172029=CARTESIAN_POINT('Ctrl Pts',(-100.85828950983,2.22590810850929,136.288711060768));
#172030=CARTESIAN_POINT('Ctrl Pts',(-100.850893152895,2.07835593070503,
136.344068839829));
#172031=CARTESIAN_POINT('Ctrl Pts',(-100.843495663558,1.93078116228609,
136.399435094306));
#172032=CARTESIAN_POINT('Ctrl Pts',(-100.836098174222,1.78101845481702,
136.448890576236));
#172033=CARTESIAN_POINT('Ctrl Pts',(-100.828700684885,1.62958430565016,
136.492276365296));
#172034=CARTESIAN_POINT('Ctrl Pts',(-100.82130060237,1.47809707147727,136.535677363177));
#172035=CARTESIAN_POINT('Ctrl Pts',(-100.813900519855,1.32493758767808,
136.573004329161));
#172036=CARTESIAN_POINT('Ctrl Pts',(-100.80650043734,1.17063485531195,136.60414894112));
#172037=CARTESIAN_POINT('Ctrl Pts',(-100.799092217674,1.01616245122866,
136.635327799781));
#172038=CARTESIAN_POINT('Ctrl Pts',(-100.791683998007,0.860544654171698,
136.660310654194));
#172039=CARTESIAN_POINT('Ctrl Pts',(-100.784275778341,0.704318673136859,
136.679040674316));
#172040=CARTESIAN_POINT('Ctrl Pts',(-100.776862999039,0.547996537617463,
136.697782222452));
#172041=CARTESIAN_POINT('Ctrl Pts',(-100.769450219737,0.391065843486597,
136.710263238121));
#172042=CARTESIAN_POINT('Ctrl Pts',(-100.762037440434,0.23406565507024,
136.716479005387));
#172043=CARTESIAN_POINT('Ctrl Pts',(-100.754614069406,0.0768411374218717,
136.722703654033));
#172044=CARTESIAN_POINT('Ctrl Pts',(-100.747190698377,-0.0804527005207835,
136.722645175101));
#172045=CARTESIAN_POINT('Ctrl Pts',(-100.739767327348,-0.237279230834789,
136.716350902497));
#172046=CARTESIAN_POINT('Ctrl Pts',(-100.735831277907,-0.32043242020955,
136.713013528133));
#172047=CARTESIAN_POINT('Ctrl Pts',(-100.731895228467,-0.40345434608564,
136.707923912244));
#172048=CARTESIAN_POINT('Ctrl Pts',(-100.727959179026,-0.486266099372952,
136.701094954731));
#172049=CARTESIAN_POINT('Ctrl Pts',(-100.72053591262,-0.642446481603767,
136.688215753986));
#172050=CARTESIAN_POINT('Ctrl Pts',(-100.713112646215,-0.798350997120586,
136.669107923043));
#172051=CARTESIAN_POINT('Ctrl Pts',(-100.705689379809,-0.95344277685068,
136.643785027024));
#172052=CARTESIAN_POINT('Ctrl Pts',(-100.698274887088,-1.10835125097626,
136.618492060565));
#172053=CARTESIAN_POINT('Ctrl Pts',(-100.690860394367,-1.26244853654563,
136.586998710235));
#172054=CARTESIAN_POINT('Ctrl Pts',(-100.683445901647,-1.4152005255357,
136.549370455245));
#172055=CARTESIAN_POINT('Ctrl Pts',(-100.676038555293,-1.56780528640776,
136.511778467783));
#172056=CARTESIAN_POINT('Ctrl Pts',(-100.668631208939,-1.71906697204115,
136.468063436071));
#172057=CARTESIAN_POINT('Ctrl Pts',(-100.661223862585,-1.86845945020915,
136.418342256779));
#172058=CARTESIAN_POINT('Ctrl Pts',(-100.65382204091,-2.01774050583068,
136.368658161419));
#172059=CARTESIAN_POINT('Ctrl Pts',(-100.646420219234,-2.16515477720742,
136.312976955367));
#172060=CARTESIAN_POINT('Ctrl Pts',(-100.639018397559,-2.31018924492142,
136.251465923612));
#172061=CARTESIAN_POINT('Ctrl Pts',(-100.631620483248,-2.45514715007052,
136.18998736305));
#172062=CARTESIAN_POINT('Ctrl Pts',(-100.624222568936,-2.59772741070102,
136.122685251198));
#172063=CARTESIAN_POINT('Ctrl Pts',(-100.616824654625,-2.73743512490741,
136.049775710714));
#172064=CARTESIAN_POINT('Ctrl Pts',(-100.609427969713,-2.87711962222447,
135.976878286474));
#172065=CARTESIAN_POINT('Ctrl Pts',(-100.602031284801,-3.01393218992775,
135.898375455595));
#172066=CARTESIAN_POINT('Ctrl Pts',(-100.594634599888,-3.14740066106887,
135.814530239565));
#172067=CARTESIAN_POINT('Ctrl Pts',(-100.587238242953,-3.28086321407848,
135.73068874132));
#172068=CARTESIAN_POINT('Ctrl Pts',(-100.579841886018,-3.41098164925822,
135.64150552751));
#172069=CARTESIAN_POINT('Ctrl Pts',(-100.572445529082,-3.53731127286047,
135.547287933201));
#172070=CARTESIAN_POINT('Ctrl Pts',(-100.565048039746,-3.66366023785095,
135.453055913937));
#172071=CARTESIAN_POINT('Ctrl Pts',(-100.557650550409,-3.78621893699536,
135.353788202643));
#172072=CARTESIAN_POINT('Ctrl Pts',(-100.550253061073,-3.90457448669035,
135.249833442855));
#172073=CARTESIAN_POINT('Ctrl Pts',(-100.542852978558,-4.02297152573998,
135.145842241887));
#172074=CARTESIAN_POINT('Ctrl Pts',(-100.535452896042,-4.13716220149907,
135.037160967341));
#172075=CARTESIAN_POINT('Ctrl Pts',(-100.528052813527,-4.24676944149886,
134.924176132034));
#172076=CARTESIAN_POINT('Ctrl Pts',(-100.520644593861,-4.35649720592646,
134.811067058286));
#172077=CARTESIAN_POINT('Ctrl Pts',(-100.513236374195,-4.46163120938045,
134.693645241348));
#172078=CARTESIAN_POINT('Ctrl Pts',(-100.505828154528,-4.56183326455146,
134.572331932336));
#172079=CARTESIAN_POINT('Ctrl Pts',(-100.498415375226,-4.66209699241603,
134.450943957007));
#172080=CARTESIAN_POINT('Ctrl Pts',(-100.491002595924,-4.75742249780265,
134.325660013361));
#172081=CARTESIAN_POINT('Ctrl Pts',(-100.483589816622,-4.84751443562534,
134.196931082406));
#172082=CARTESIAN_POINT('Ctrl Pts',(-100.476166445593,-4.9377351010333,
134.068018217518));
#172083=CARTESIAN_POINT('Ctrl Pts',(-100.468743074565,-5.02270706257476,
133.935650847573));
#172084=CARTESIAN_POINT('Ctrl Pts',(-100.461319703536,-5.10218008310522,
133.800306037974));
#172085=CARTESIAN_POINT('Ctrl Pts',(-100.457383654095,-5.14431858552158,
133.728542972367));
#172086=CARTESIAN_POINT('Ctrl Pts',(-100.453447604654,-5.18491192638941,
133.655943213113));
#172087=CARTESIAN_POINT('Ctrl Pts',(-100.449511555213,-5.22392830647022,
133.582580121378));
#172088=CARTESIAN_POINT('Ctrl Pts',(-100.441665730885,-5.30170061818242,
133.436343663079));
#172089=CARTESIAN_POINT('Ctrl Pts',(-100.433819906556,-5.37341784873034,
133.286671693839));
#172090=CARTESIAN_POINT('Ctrl Pts',(-100.425974082228,-5.43878157850147,
133.134078519771));
#172091=CARTESIAN_POINT('Ctrl Pts',(-100.418141753343,-5.50403287744844,
132.981747818122));
#172092=CARTESIAN_POINT('Ctrl Pts',(-100.410309424458,-5.56295233934166,
132.826506211912));
#172093=CARTESIAN_POINT('Ctrl Pts',(-100.402477095573,-5.61528724153757,
132.668892665434));
#172094=CARTESIAN_POINT('Ctrl Pts',(-100.394663328559,-5.66749811501631,
132.511652647999));
#172095=CARTESIAN_POINT('Ctrl Pts',(-100.386849561545,-5.71315545719033,
132.352052196133));
#172096=CARTESIAN_POINT('Ctrl Pts',(-100.379035794531,-5.75205470421961,
132.190649635832));
#172097=CARTESIAN_POINT('Ctrl Pts',(-100.371233019106,-5.7908992318609,
132.029474119754));
#172098=CARTESIAN_POINT('Ctrl Pts',(-100.363430243681,-5.82300453863767,
131.866501847538));
#172099=CARTESIAN_POINT('Ctrl Pts',(-100.355627468256,-5.84821524401388,
131.702307733038));
#172100=CARTESIAN_POINT('Ctrl Pts',(-100.347839976852,-5.87337656684029,
131.538435240797));
#172101=CARTESIAN_POINT('Ctrl Pts',(-100.340052485449,-5.89167017837645,
131.373345985616));
#172102=CARTESIAN_POINT('Ctrl Pts',(-100.332264994045,-5.90299140926265,
131.20762601984));
#172103=CARTESIAN_POINT('Ctrl Pts',(-100.325968393443,-5.91214522600743,
131.073632621692));
#172104=CARTESIAN_POINT('Ctrl Pts',(-100.319671792841,-5.91674171556739,
130.939227231668));
#172105=CARTESIAN_POINT('Ctrl Pts',(-100.313375192239,-5.9167499888071,
130.804724555984));
#172106=CARTESIAN_POINT('',(-98.563375192205,-5.91674749124866,130.798912011994));
#172107=CARTESIAN_POINT('Ctrl Pts',(-100.313375192205,-5.91674998880715,
130.804724555263));
#172108=CARTESIAN_POINT('Ctrl Pts',(-100.305661661453,-5.91676012376195,
130.639954611816));
#172109=CARTESIAN_POINT('Ctrl Pts',(-100.297948130701,-5.90988315404377,
130.475303996975));
#172110=CARTESIAN_POINT('Ctrl Pts',(-100.29023459995,-5.89617484706362,
130.311356829189));
#172111=CARTESIAN_POINT('Ctrl Pts',(-100.282512544976,-5.88245139103566,
130.147228483414));
#172112=CARTESIAN_POINT('Ctrl Pts',(-100.274790490003,-5.8618815601619,
129.983805458956));
#172113=CARTESIAN_POINT('Ctrl Pts',(-100.267068435029,-5.83457264172292,
129.821663995531));
#172114=CARTESIAN_POINT('Ctrl Pts',(-100.259068059727,-5.8062794480888,
129.65367858699));
#172115=CARTESIAN_POINT('Ctrl Pts',(-100.251067684424,-5.77075242492543,
129.487069227152));
#172116=CARTESIAN_POINT('Ctrl Pts',(-100.243067309122,-5.72816741204176,
129.322460262575));
#172117=CARTESIAN_POINT('Ctrl Pts',(-100.235319847535,-5.68692862773064,
129.163055036975));
#172118=CARTESIAN_POINT('Ctrl Pts',(-100.227572385948,-5.63907146202288,
129.00552593413));
#172119=CARTESIAN_POINT('Ctrl Pts',(-100.219824924361,-5.584805069566,128.850420266007));
#172120=CARTESIAN_POINT('Ctrl Pts',(-100.2116980922,-5.52788141031746,128.687719526194));
#172121=CARTESIAN_POINT('Ctrl Pts',(-100.20357126004,-5.46390524848292,
128.527685917589));
#172122=CARTESIAN_POINT('Ctrl Pts',(-100.19544442788,-5.39317272883823,
128.370923032705));
#172123=CARTESIAN_POINT('Ctrl Pts',(-100.18731759572,-5.32244020919354,
128.21416014782));
#172124=CARTESIAN_POINT('Ctrl Pts',(-100.17919076356,-5.24495157963472,
128.060668314391));
#172125=CARTESIAN_POINT('Ctrl Pts',(-100.1710639314,-5.16105560301029,127.911017287587));
#172126=CARTESIAN_POINT('Ctrl Pts',(-100.163640664995,-5.08442276839887,
127.774322027004));
#172127=CARTESIAN_POINT('Ctrl Pts',(-100.156217398589,-5.00223955723448,
127.640466705985));
#172128=CARTESIAN_POINT('Ctrl Pts',(-100.148794132184,-4.9147414658173,
127.509933977515));
#172129=CARTESIAN_POINT('Ctrl Pts',(-100.141379639462,-4.82734678987766,
127.379555527891));
#172130=CARTESIAN_POINT('Ctrl Pts',(-100.133965146741,-4.73464994335874,
127.252492161096));
#172131=CARTESIAN_POINT('Ctrl Pts',(-100.12655065402,-4.63693249162979,
127.12920243994));
#172132=CARTESIAN_POINT('Ctrl Pts',(-100.119143307666,-4.53930922365981,
127.00603155006));
#172133=CARTESIAN_POINT('Ctrl Pts',(-100.111735961313,-4.43667521438776,
126.886627355494));
#172134=CARTESIAN_POINT('Ctrl Pts',(-100.104328614959,-4.32935547896536,
126.771419792405));
#172135=CARTESIAN_POINT('Ctrl Pts',(-100.096926793283,-4.22211578665059,
126.656298155462));
#172136=CARTESIAN_POINT('Ctrl Pts',(-100.089524971608,-4.11019758013669,
126.545367189702));
#172137=CARTESIAN_POINT('Ctrl Pts',(-100.082123149932,-3.99396625305007,
126.439023960217));
#172138=CARTESIAN_POINT('Ctrl Pts',(-100.074725235621,-3.87779628357628,
126.332736868495));
#172139=CARTESIAN_POINT('Ctrl Pts',(-100.067327321309,-3.75731800273049,
126.231032941206));
#172140=CARTESIAN_POINT('Ctrl Pts',(-100.059929406998,-3.63293369198555,
126.134272465064));
#172141=CARTESIAN_POINT('Ctrl Pts',(-100.052532722085,-3.50857005165668,
126.037528068759));
#172142=CARTESIAN_POINT('Ctrl Pts',(-100.045136037173,-3.3803019640779,
125.945725722126));
#172143=CARTESIAN_POINT('Ctrl Pts',(-100.037739352261,-3.24856491584063,
125.859185539769));
#172144=CARTESIAN_POINT('Ctrl Pts',(-100.030342995325,-3.11683370896214,
125.772649194694));
#172145=CARTESIAN_POINT('Ctrl Pts',(-100.02294663839,-2.98163415926531,
125.691374754914));
#172146=CARTESIAN_POINT('Ctrl Pts',(-100.015550281454,-2.84343063759905,
125.615638928011));
#172147=CARTESIAN_POINT('Ctrl Pts',(-100.008152792118,-2.70520595662081,
125.539891505759));
#172148=CARTESIAN_POINT('Ctrl Pts',(-100.000755302781,-2.56397671530603,
125.469684564225));
#172149=CARTESIAN_POINT('Ctrl Pts',(-99.9933578134444,-2.42023163284223,
125.405248708567));
#172150=CARTESIAN_POINT('Ctrl Pts',(-99.9859577309293,-2.27643616076282,
125.340790265021));
#172151=CARTESIAN_POINT('Ctrl Pts',(-99.9785576484144,-2.13012343205648,
125.282107087822));
#172152=CARTESIAN_POINT('Ctrl Pts',(-99.9711575658993,-1.98180172317201,
125.229381470293));
#172153=CARTESIAN_POINT('Ctrl Pts',(-99.9637493462328,-1.83331691932058,
125.176597875527));
#172154=CARTESIAN_POINT('Ctrl Pts',(-99.9563411265662,-1.68281907556357,
125.12978504822));
#172155=CARTESIAN_POINT('Ctrl Pts',(-99.9489329068996,-1.53083190015848,
125.089075475427));
#172156=CARTESIAN_POINT('Ctrl Pts',(-99.9415201275975,-1.37875117918209,
125.048340846571));
#172157=CARTESIAN_POINT('Ctrl Pts',(-99.9341073482953,-1.22517966331314,
125.013717039342));
#172158=CARTESIAN_POINT('Ctrl Pts',(-99.9266945689931,-1.07065029256481,
124.985285217339));
#172159=CARTESIAN_POINT('Ctrl Pts',(-99.9192711979643,-0.915900123005516,
124.956812770615));
#172160=CARTESIAN_POINT('Ctrl Pts',(-99.9118478269355,-0.760189733670803,
124.934550032053));
#172161=CARTESIAN_POINT('Ctrl Pts',(-99.9044244559067,-0.604057038907278,
124.918526296397));
#172162=CARTESIAN_POINT('Ctrl Pts',(-99.9004884064669,-0.521271737812884,
124.910030127271));
#172163=CARTESIAN_POINT('Ctrl Pts',(-99.8965523570271,-0.438367721794466,
124.903287094543));
#172164=CARTESIAN_POINT('Ctrl Pts',(-99.8926163075873,-0.355424931963131,
124.898295626369));
#172165=CARTESIAN_POINT('Ctrl Pts',(-99.8851930411819,-0.198997418857412,
124.888881873171));
#172166=CARTESIAN_POINT('Ctrl Pts',(-99.8777697747764,-0.0419591132346854,
124.885672865664));
#172167=CARTESIAN_POINT('Ctrl Pts',(-99.870346508371,0.1151566237746,124.888731359871));
#172168=CARTESIAN_POINT('Ctrl Pts',(-99.86293201565,0.272086663030391,124.891786239192));
#172169=CARTESIAN_POINT('Ctrl Pts',(-99.8555175229289,0.429093581924141,
124.901093868031));
#172170=CARTESIAN_POINT('Ctrl Pts',(-99.8481030302079,0.585639385617466,
124.916665221869));
#172171=CARTESIAN_POINT('Ctrl Pts',(-99.8406956838542,0.742034304571345,
124.93222156745));
#172172=CARTESIAN_POINT('Ctrl Pts',(-99.8332883375003,0.897968624146639,
124.954029582423));
#172173=CARTESIAN_POINT('Ctrl Pts',(-99.8258809911466,1.05290494824604,
124.982048213335));
#172174=CARTESIAN_POINT('Ctrl Pts',(-99.8184791694712,1.20772571498951,
125.010045946895));
#172175=CARTESIAN_POINT('Ctrl Pts',(-99.8110773477957,1.36154960258513,
125.04424500709));
#172176=CARTESIAN_POINT('Ctrl Pts',(-99.8036755261203,1.51384504474415,
125.084552601295));
#172177=CARTESIAN_POINT('Ctrl Pts',(-99.796277611809,1.66606009132429,125.124838917434));
#172178=CARTESIAN_POINT('Ctrl Pts',(-99.7888796974977,1.81674793939811,
125.171227250274));
#172179=CARTESIAN_POINT('Ctrl Pts',(-99.7814817831863,1.96538802658662,
125.223573892789));
#172180=CARTESIAN_POINT('Ctrl Pts',(-99.7740850982741,2.11400341248988,
125.275911836241));
#172181=CARTESIAN_POINT('Ctrl Pts',(-99.7666884133618,2.26057136114734,
125.334206000309));
#172182=CARTESIAN_POINT('Ctrl Pts',(-99.7592917284496,2.40458715993728,
125.398263027551));
#172183=CARTESIAN_POINT('Ctrl Pts',(-99.7518953715142,2.54859657291577,
125.462317214438));
#172184=CARTESIAN_POINT('Ctrl Pts',(-99.7444990145787,2.69005371995732,
125.532133604707));
#172185=CARTESIAN_POINT('Ctrl Pts',(-99.7371026576432,2.8284747953498,125.607471077219));
#172186=CARTESIAN_POINT('Ctrl Pts',(-99.7297051683066,2.96691706336229,
125.68282008409));
#172187=CARTESIAN_POINT('Ctrl Pts',(-99.7223076789701,3.10232200628499,
125.763691677827));
#172188=CARTESIAN_POINT('Ctrl Pts',(-99.7149101896335,3.23423144480751,
125.849799332859));
#172189=CARTESIAN_POINT('Ctrl Pts',(-99.7075101071185,3.36618712397941,
125.935937172796));
#172190=CARTESIAN_POINT('Ctrl Pts',(-99.7001100246035,3.49464454670415,
126.027314524554));
#172191=CARTESIAN_POINT('Ctrl Pts',(-99.6927099420885,3.61917560860956,
126.123602294757));
#172192=CARTESIAN_POINT('Ctrl Pts',(-99.685301722422,3.74384360521946,126.219995943262));
#172193=CARTESIAN_POINT('Ctrl Pts',(-99.6778935027555,3.86457632330588,
126.321310564907));
#172194=CARTESIAN_POINT('Ctrl Pts',(-99.670485283089,3.98097922065087,126.427177161593));
#172195=CARTESIAN_POINT('Ctrl Pts',(-99.6630725037869,4.09745376203722,
126.533108917403));
#172196=CARTESIAN_POINT('Ctrl Pts',(-99.6556597244847,4.20959290717608,
126.643597969532));
#172197=CARTESIAN_POINT('Ctrl Pts',(-99.6482469451826,4.31704030373725,
126.758239811361));
#172198=CARTESIAN_POINT('Ctrl Pts',(-99.6408235741538,4.42464122617726,
126.873045458829));
#172199=CARTESIAN_POINT('Ctrl Pts',(-99.633400203125,4.52753676751639,126.992015465332));
#172200=CARTESIAN_POINT('Ctrl Pts',(-99.6259768320962,4.62541152541234,
127.114713102818));
#172201=CARTESIAN_POINT('Ctrl Pts',(-99.6220407826556,4.67730707051926,
127.179770334301));
#172202=CARTESIAN_POINT('Ctrl Pts',(-99.618104733215,4.72779182063832,127.245875057057));
#172203=CARTESIAN_POINT('Ctrl Pts',(-99.6141686837743,4.77682388808281,
127.312959164748));
#172204=CARTESIAN_POINT('Ctrl Pts',(-99.6067454173689,4.86929683704776,
127.439477698233));
#172205=CARTESIAN_POINT('Ctrl Pts',(-99.5993221509635,4.95687970600967,
127.569863925366));
#172206=CARTESIAN_POINT('Ctrl Pts',(-99.5918988845581,5.03923140183056,
127.703703035487));
#172207=CARTESIAN_POINT('Ctrl Pts',(-99.5844843918371,5.12148576478588,
127.837383958894));
#172208=CARTESIAN_POINT('Ctrl Pts',(-99.5770698991162,5.19852106780652,
127.974509327165));
#172209=CARTESIAN_POINT('Ctrl Pts',(-99.5696554063952,5.27003727755891,
128.114632442519));
#172210=CARTESIAN_POINT('Ctrl Pts',(-99.5622480600415,5.3414845572958,128.25462050194));
#172211=CARTESIAN_POINT('Ctrl Pts',(-99.5548407136876,5.407423165301,128.397600226071));
#172212=CARTESIAN_POINT('Ctrl Pts',(-99.5474333673339,5.46759716529179,
128.543097297961));
#172213=CARTESIAN_POINT('Ctrl Pts',(-99.5400315456585,5.52772628524315,
128.688485852645));
#172214=CARTESIAN_POINT('Ctrl Pts',(-99.5326297239832,5.58209921593647,
128.83638767319));
#172215=CARTESIAN_POINT('Ctrl Pts',(-99.5252279023078,5.63050670187152,
128.986305381144));
#172216=CARTESIAN_POINT('Ctrl Pts',(-99.5178299879965,5.67888863387169,
129.136143948708));
#172217=CARTESIAN_POINT('Ctrl Pts',(-99.5104320736852,5.72131127830683,
129.287995929992));
#172218=CARTESIAN_POINT('Ctrl Pts',(-99.5030341593739,5.7576141632872,129.441345683967));
#172219=CARTESIAN_POINT('Ctrl Pts',(-99.4956374744617,5.79391101538663,
129.594669953994));
#172220=CARTESIAN_POINT('Ctrl Pts',(-99.4882407895495,5.82409004055069,
129.749491139811));
#172221=CARTESIAN_POINT('Ctrl Pts',(-99.4808441046373,5.84804110637009,
129.905280097976));
#172222=CARTESIAN_POINT('Ctrl Pts',(-99.4734477477019,5.87199111017406,
130.061062148295));
#172223=CARTESIAN_POINT('Ctrl Pts',(-99.4660513907665,5.88971364699685,
130.217811516675));
#172224=CARTESIAN_POINT('Ctrl Pts',(-99.4586550338311,5.90115007007733,
130.374990831803));
#172225=CARTESIAN_POINT('Ctrl Pts',(-99.4512575444945,5.91258824410341,
130.532194211485));
#172226=CARTESIAN_POINT('Ctrl Pts',(-99.4438600551579,5.91773836098938,
130.689827296646));
#172227=CARTESIAN_POINT('Ctrl Pts',(-99.4364625658214,5.91659382570492,
130.847349733985));
#172228=CARTESIAN_POINT('Ctrl Pts',(-99.4290624833064,5.91544888920539,
131.00492739057));
#172229=CARTESIAN_POINT('Ctrl Pts',(-99.4216624007915,5.90800490996031,
131.162393949051));
#172230=CARTESIAN_POINT('Ctrl Pts',(-99.4142623182765,5.8943073626781,131.319211350088));
#172231=CARTESIAN_POINT('Ctrl Pts',(-99.4068540986101,5.88059475353448,
131.476201187979));
#172232=CARTESIAN_POINT('Ctrl Pts',(-99.3994458789437,5.86061487615244,
131.632540070779));
#172233=CARTESIAN_POINT('Ctrl Pts',(-99.3920376592772,5.83446491937734,
131.787696606461));
#172234=CARTESIAN_POINT('Ctrl Pts',(-99.3846248799751,5.80829886774011,
131.942948638401));
#172235=CARTESIAN_POINT('Ctrl Pts',(-99.3772121006731,5.77595524607093,
132.097016508672));
#172236=CARTESIAN_POINT('Ctrl Pts',(-99.3697993213711,5.73758176010527,
132.249381762258));
#172237=CARTESIAN_POINT('Ctrl Pts',(-99.3623759503424,5.69915344430339,
132.401964722463));
#172238=CARTESIAN_POINT('Ctrl Pts',(-99.3549525793136,5.65467816188542,
132.552839850063));
#172239=CARTESIAN_POINT('Ctrl Pts',(-99.3475292082849,5.60435286185769,
132.701505725956));
#172240=CARTESIAN_POINT('Ctrl Pts',(-99.3435931588437,5.57766918024148,
132.78033194055));
#172241=CARTESIAN_POINT('Ctrl Pts',(-99.3396571094026,5.54934164539772,
132.858537407986));
#172242=CARTESIAN_POINT('Ctrl Pts',(-99.3357210599614,5.51940491580191,
132.936050073824));
#172243=CARTESIAN_POINT('Ctrl Pts',(-99.328297793556,5.46294517808277,133.082236542494));
#172244=CARTESIAN_POINT('Ctrl Pts',(-99.3208745271506,5.4005882324696,133.226399431254));
#172245=CARTESIAN_POINT('Ctrl Pts',(-99.3134512607452,5.33249870174735,
133.368027553493));
#172246=CARTESIAN_POINT('Ctrl Pts',(-99.3060367680242,5.26448964719574,
133.509488283052));
#172247=CARTESIAN_POINT('Ctrl Pts',(-99.2986222753032,5.19076165425145,
133.648419876261));
#172248=CARTESIAN_POINT('Ctrl Pts',(-99.2912077825821,5.11152836706183,
133.784328455517));
#172249=CARTESIAN_POINT('Ctrl Pts',(-99.2838004362284,5.03237144789747,
133.920106040968));
#172250=CARTESIAN_POINT('Ctrl Pts',(-99.2763930898745,4.94771998485609,
134.052866092728));
#172251=CARTESIAN_POINT('Ctrl Pts',(-99.2689857435207,4.85783469441018,
134.182136904457));
#172252=CARTESIAN_POINT('Ctrl Pts',(-99.2615839218453,4.76801644380481,
134.311311301138));
#172253=CARTESIAN_POINT('Ctrl Pts',(-99.2541821001699,4.67297235055375,
134.437001334361));
#172254=CARTESIAN_POINT('Ctrl Pts',(-99.2467802784945,4.57300776552732,
134.558762106342));
#172255=CARTESIAN_POINT('Ctrl Pts',(-99.2393823641832,4.47309595102777,
134.68045860176));
#172256=CARTESIAN_POINT('Ctrl Pts',(-99.2319844498718,4.36826905404935,
134.79822967907));
#172257=CARTESIAN_POINT('Ctrl Pts',(-99.2245865355605,4.25887415901876,
134.911661612154));
#172258=CARTESIAN_POINT('Ctrl Pts',(-99.2171898506483,4.14949744343463,
135.025074694909));
#172259=CARTESIAN_POINT('Ctrl Pts',(-99.209793165736,4.03555449530661,135.134149796146));
#172260=CARTESIAN_POINT('Ctrl Pts',(-99.2023964808238,3.91743096874174,
135.238508243395));
#172261=CARTESIAN_POINT('Ctrl Pts',(-99.1950001238883,3.79931267989816,
135.34286206328));
#172262=CARTESIAN_POINT('Ctrl Pts',(-99.187603766953,3.67701446095609,135.442499397863));
#172263=CARTESIAN_POINT('Ctrl Pts',(-99.1802074100175,3.55095671761385,
135.537080443642));
#172264=CARTESIAN_POINT('Ctrl Pts',(-99.1728099206809,3.42487967450857,
135.631675970021));
#172265=CARTESIAN_POINT('Ctrl Pts',(-99.1654124313443,3.29504225953587,
135.721213442148));
#172266=CARTESIAN_POINT('Ctrl Pts',(-99.1580149420076,3.16189552245616,
135.805395237279));
#172267=CARTESIAN_POINT('Ctrl Pts',(-99.1506148594926,3.02870211099436,
135.889606542208));
#172268=CARTESIAN_POINT('Ctrl Pts',(-99.1432147769776,2.89219738304632,
135.968458232839));
#172269=CARTESIAN_POINT('Ctrl Pts',(-99.1358146944626,2.75285860336558,
136.041697734114));
#172270=CARTESIAN_POINT('Ctrl Pts',(-99.1284064747961,2.61336660637241,
136.11501776975));
#172271=CARTESIAN_POINT('Ctrl Pts',(-99.1209982551296,2.47103466476383,
136.182713117992));
#172272=CARTESIAN_POINT('Ctrl Pts',(-99.1135900354632,2.32636238664759,
136.244578316196));
#172273=CARTESIAN_POINT('Ctrl Pts',(-99.1061772561611,2.18160106515775,
136.306481591398));
#172274=CARTESIAN_POINT('Ctrl Pts',(-99.098764476859,2.03449688491973,136.362547433667));
#172275=CARTESIAN_POINT('Ctrl Pts',(-99.0913516975569,1.8855658753796,136.412619874421));
#172276=CARTESIAN_POINT('Ctrl Pts',(-99.0839283265281,1.73642206622908,
136.462763861027));
#172277=CARTESIAN_POINT('Ctrl Pts',(-99.0765049554993,1.58544657185666,
136.506897238121));
#172278=CARTESIAN_POINT('Ctrl Pts',(-99.0690815844706,1.43316770610195,
136.544914675206));
#172279=CARTESIAN_POINT('Ctrl Pts',(-99.0651455350299,1.35242579760083,
136.565072432564));
#172280=CARTESIAN_POINT('Ctrl Pts',(-99.0612094855892,1.27131759844237,
136.583511640643));
#172281=CARTESIAN_POINT('Ctrl Pts',(-99.0572734361486,1.18992246381842,
136.600222511418));
#172282=CARTESIAN_POINT('Ctrl Pts',(-99.0498501697432,1.03641378016814,
136.631738692171));
#172283=CARTESIAN_POINT('Ctrl Pts',(-99.0424269033378,0.881420006692884,
136.657199590535));
#172284=CARTESIAN_POINT('Ctrl Pts',(-99.0350036369325,0.725460201803441,
136.676467399471));
#172285=CARTESIAN_POINT('Ctrl Pts',(-99.0275891442115,0.56968472845128,
136.695712435458));
#172286=CARTESIAN_POINT('Ctrl Pts',(-99.0201746514904,0.412945863245716,
136.708778906631));
#172287=CARTESIAN_POINT('Ctrl Pts',(-99.0127601587695,0.255774599280688,
136.715579604955));
#172288=CARTESIAN_POINT('Ctrl Pts',(-99.0053528124158,0.0987548228977118,
136.722373748509));
#172289=CARTESIAN_POINT('Ctrl Pts',(-98.997945466062,-0.0586961521079571,
136.72291412602));
#172290=CARTESIAN_POINT('Ctrl Pts',(-98.9905381197083,-0.216040542210129,
136.717165116839));
#172291=CARTESIAN_POINT('Ctrl Pts',(-98.983136298033,-0.373267578930346,
136.711420395486));
#172292=CARTESIAN_POINT('Ctrl Pts',(-98.9757344763576,-0.53038781758902,
136.699395641152));
#172293=CARTESIAN_POINT('Ctrl Pts',(-98.9683326546823,-0.686861903477895,
136.681107276054));
#172294=CARTESIAN_POINT('Ctrl Pts',(-98.960934740371,-0.843253387914375,
136.662828565242));
#172295=CARTESIAN_POINT('Ctrl Pts',(-98.9535368260596,-0.998999029060612,
136.638292871967));
#172296=CARTESIAN_POINT('Ctrl Pts',(-98.9461389117483,-1.15356313980562,
136.607568579115));
#172297=CARTESIAN_POINT('Ctrl Pts',(-98.9387422268362,-1.30810156479972,
136.576849392083));
#172298=CARTESIAN_POINT('Ctrl Pts',(-98.931345541924,-1.46145848331121,
136.539943719318));
#172299=CARTESIAN_POINT('Ctrl Pts',(-98.9239488570119,-1.61310685200084,
136.496971340822));
#172300=CARTESIAN_POINT('Ctrl Pts',(-98.9165525000764,-1.76474849644289,
136.454000867767));
#172301=CARTESIAN_POINT('Ctrl Pts',(-98.909156143141,-1.91468138254109,
136.404964325625));
#172302=CARTESIAN_POINT('Ctrl Pts',(-98.9017597862056,-2.06239238443654,
136.350031741525));
#172303=CARTESIAN_POINT('Ctrl Pts',(-98.8943622968691,-2.21012600126262,
136.295090747107));
#172304=CARTESIAN_POINT('Ctrl Pts',(-98.8869648075328,-2.35563670664166,
136.234252043465));
#172305=CARTESIAN_POINT('Ctrl Pts',(-98.8795673181963,-2.49843029871731,
136.167734239173));
#172306=CARTESIAN_POINT('Ctrl Pts',(-98.8721672356813,-2.64127394686632,
136.101193117168));
#172307=CARTESIAN_POINT('Ctrl Pts',(-98.8647671531664,-2.78139824715815,
136.028969088377));
#172308=CARTESIAN_POINT('Ctrl Pts',(-98.8573670706515,-2.918332727787,135.951327166168));
#172309=CARTESIAN_POINT('Ctrl Pts',(-98.8499588509851,-3.0554177819547,
135.873599868683));
#172310=CARTESIAN_POINT('Ctrl Pts',(-98.8425506313185,-3.18930568675224,
135.790442964435));
#172311=CARTESIAN_POINT('Ctrl Pts',(-98.8351424116521,-3.31955353025329,
135.702165730296));
#172312=CARTESIAN_POINT('Ctrl Pts',(-98.82772963235,-3.44988153912945,135.613834162992));
#172313=CARTESIAN_POINT('Ctrl Pts',(-98.8203168530479,-3.57656472273543,
135.520376207183));
#172314=CARTESIAN_POINT('Ctrl Pts',(-98.8129040737459,-3.69919293376609,
135.422141708228));
#172315=CARTESIAN_POINT('Ctrl Pts',(-98.8054807027171,-3.82199636173483,
135.323766847215));
#172316=CARTESIAN_POINT('Ctrl Pts',(-98.7980573316884,-3.94073296429517,
135.220602056289));
#172317=CARTESIAN_POINT('Ctrl Pts',(-98.7906339606597,-4.05502855738327,
135.113034887142));
#172318=CARTESIAN_POINT('Ctrl Pts',(-98.7866979112184,-4.11563082333166,
135.056000193014));
#172319=CARTESIAN_POINT('Ctrl Pts',(-98.7827618617771,-4.17498521414741,
134.997728410319));
#172320=CARTESIAN_POINT('Ctrl Pts',(-98.7788258123359,-4.23304060146686,
134.938281012159));
#172321=CARTESIAN_POINT('Ctrl Pts',(-98.771500395973,-4.34108799532415,
134.827642934639));
#172322=CARTESIAN_POINT('Ctrl Pts',(-98.76417497961,-4.44497946114729,134.712576679298));
#172323=CARTESIAN_POINT('Ctrl Pts',(-98.7568495632472,-4.54432289261208,
134.593431745188));
#172324=CARTESIAN_POINT('Ctrl Pts',(-98.7495330015686,-4.64354624152007,
134.474430828938));
#172325=CARTESIAN_POINT('Ctrl Pts',(-98.7422164398901,-4.73823225107807,
134.351361335499));
#172326=CARTESIAN_POINT('Ctrl Pts',(-98.7348998782115,-4.82802450097346,
134.224610605579));
#172327=CARTESIAN_POINT('Ctrl Pts',(-98.7275917009874,-4.9177138529426,
134.098005126359));
#172328=CARTESIAN_POINT('Ctrl Pts',(-98.7202835237632,-5.00252039296936,
133.967727122969));
#172329=CARTESIAN_POINT('Ctrl Pts',(-98.712975346539,-5.0821272954591,133.83419769491));
#172330=CARTESIAN_POINT('Ctrl Pts',(-98.7056719100402,-5.16168255792281,
133.700754885761));
#172331=CARTESIAN_POINT('Ctrl Pts',(-98.6983684735414,-5.23604469649038,
133.564065175827));
#172332=CARTESIAN_POINT('Ctrl Pts',(-98.6910650370426,-5.3049395390632,
133.424579510976));
#172333=CARTESIAN_POINT('Ctrl Pts',(-98.6837648057947,-5.37380414583459,
133.285155062041));
#172334=CARTESIAN_POINT('Ctrl Pts',(-98.6764645745468,-5.43720606106764,
133.142937443257));
#172335=CARTESIAN_POINT('Ctrl Pts',(-98.6691643432989,-5.49491666632617,
132.998402867075));
#172336=CARTESIAN_POINT('Ctrl Pts',(-98.6618657844603,-5.55261405066784,
132.853901402305));
#172337=CARTESIAN_POINT('Ctrl Pts',(-98.6545672256217,-5.60462257837086,
132.707084393212));
#172338=CARTESIAN_POINT('Ctrl Pts',(-98.647268666783,-5.650761579237,132.55844845377));
#172339=CARTESIAN_POINT('Ctrl Pts',(-98.6399678669216,-5.69691474708537,
132.409766875656));
#172340=CARTESIAN_POINT('Ctrl Pts',(-98.6326670670602,-5.73719466763828,
132.259265616628));
#172341=CARTESIAN_POINT('Ctrl Pts',(-98.6253662671987,-5.77147035984798,
132.107457102058));
#172342=CARTESIAN_POINT('Ctrl Pts',(-98.6180644732092,-5.80575071927642,
131.955627916176));
#172343=CARTESIAN_POINT('Ctrl Pts',(-98.6107626792195,-5.83402514580646,
131.802491496868));
#172344=CARTESIAN_POINT('Ctrl Pts',(-98.6034608852299,-5.85621385145219,
131.648570241155));
#172345=CARTESIAN_POINT('Ctrl Pts',(-98.5961528071448,-5.87842165321974,
131.494516517189));
#172346=CARTESIAN_POINT('Ctrl Pts',(-98.5888447290596,-5.89453322471738,
131.339676989102));
#172347=CARTESIAN_POINT('Ctrl Pts',(-98.5815366509744,-5.90452065747652,
131.184579459725));
#172348=CARTESIAN_POINT('Ctrl Pts',(-98.5754828313846,-5.9127939839769,
131.056100747439));
#172349=CARTESIAN_POINT('Ctrl Pts',(-98.5694290117949,-5.91686585467058,
130.927445169786));
#172350=CARTESIAN_POINT('Ctrl Pts',(-98.5633751922051,-5.91674749124866,
130.798912011994));
#172351=CARTESIAN_POINT('',(-96.8133751922048,-5.92166422711087,130.806462316915));
#172352=CARTESIAN_POINT('Ctrl Pts',(-98.563375192205,-5.91713394122631,
130.798911656121));
#172353=CARTESIAN_POINT('Ctrl Pts',(-98.5423761909776,-5.9212723605073,
130.353032893676));
#172354=CARTESIAN_POINT('Ctrl Pts',(-98.5213771897503,-5.87515968389772,
129.908001828249));
#172355=CARTESIAN_POINT('Ctrl Pts',(-98.4075623139186,-5.33543540985616,
127.56261494968));
#172356=CARTESIAN_POINT('Ctrl Pts',(-98.2219305647096,-2.36602057997696,
124.21804851249));
#172357=CARTESIAN_POINT('Ctrl Pts',(-97.9434829408973,4.26235899130877,
125.253697922036));
#172358=CARTESIAN_POINT('Ctrl Pts',(-97.6650353170831,6.97383887740406,
131.390135183845));
#172359=CARTESIAN_POINT('Ctrl Pts',(-97.3865876932723,3.27670152612622,
136.988274235881));
#172360=CARTESIAN_POINT('Ctrl Pts',(-97.1081400694582,-3.43156445187626,
136.903698773712));
#172361=CARTESIAN_POINT('Ctrl Pts',(-96.91706923577,-5.87088692384846,132.999514831838));
#172362=CARTESIAN_POINT('Ctrl Pts',(-96.818814276685,-5.92615900346599,
130.921523331019));
#172363=CARTESIAN_POINT('Ctrl Pts',(-96.8133751922048,-5.9256324804525,
130.806463725316));
#172364=CARTESIAN_POINT('',(-95.063375206451,-5.91325275216486,130.808790442179));
#172365=CARTESIAN_POINT('Ctrl Pts',(-96.8133751922048,-5.91674962734513,
130.80646057264));
#172366=CARTESIAN_POINT('Ctrl Pts',(-96.8060180359455,-5.916804781926,130.651059226289));
#172367=CARTESIAN_POINT('Ctrl Pts',(-96.7986608796862,-5.91073338293157,
130.49540813547));
#172368=CARTESIAN_POINT('Ctrl Pts',(-96.7913037234269,-5.89850259791408,
130.340035661419));
#172369=CARTESIAN_POINT('Ctrl Pts',(-96.7839549889756,-5.88628581359465,
130.184841043744));
#172370=CARTESIAN_POINT('Ctrl Pts',(-96.7766062545244,-5.86792370315422,
130.029924783744));
#172371=CARTESIAN_POINT('Ctrl Pts',(-96.7692575200732,-5.84343540412144,
129.875817005041));
#172372=CARTESIAN_POINT('Ctrl Pts',(-96.7619155248804,-5.81896956242183,
129.721850553008));
#172373=CARTESIAN_POINT('Ctrl Pts',(-96.7545735296877,-5.78838877287601,
129.568691479954));
#172374=CARTESIAN_POINT('Ctrl Pts',(-96.7472315344949,-5.75176409327423,
129.416866337282));
#172375=CARTESIAN_POINT('Ctrl Pts',(-96.7398946020873,-5.71516466878055,
129.265145887959));
#172376=CARTESIAN_POINT('Ctrl Pts',(-96.7325576696796,-5.67252973937426,
129.114757906376));
#172377=CARTESIAN_POINT('Ctrl Pts',(-96.725220737272,-5.62398167587752,
128.966220070194));
#172378=CARTESIAN_POINT('Ctrl Pts',(-96.7178864892326,-5.57545137469236,
128.817736579647));
#172379=CARTESIAN_POINT('Ctrl Pts',(-96.7105522411932,-5.52101235978126,
128.671102249299));
#172380=CARTESIAN_POINT('Ctrl Pts',(-96.7032179931538,-5.46083720911901,
128.526820818133));
#172381=CARTESIAN_POINT('Ctrl Pts',(-96.6958850156969,-5.40067248317853,
128.382564382231));
#172382=CARTESIAN_POINT('Ctrl Pts',(-96.6885520382401,-5.33477374453361,
128.240660385716));
#172383=CARTESIAN_POINT('Ctrl Pts',(-96.6812190607832,-5.26336209064202,
128.101593504903));
#172384=CARTESIAN_POINT('Ctrl Pts',(-96.6738858434829,-5.19194810105341,
127.962522075559));
#172385=CARTESIAN_POINT('Ctrl Pts',(-96.6665526261826,-5.11502101097641,
127.826288285204));
#172386=CARTESIAN_POINT('Ctrl Pts',(-96.6592194088823,-5.03284822279007,
127.69335285016));
#172387=CARTESIAN_POINT('Ctrl Pts',(-96.6518844413729,-4.95065582253505,
127.560385687595));
#172388=CARTESIAN_POINT('Ctrl Pts',(-96.6445494738636,-4.86321543263135,
127.430718770531));
#172389=CARTESIAN_POINT('Ctrl Pts',(-96.6372145063542,-4.77083803961927,
127.304784220026));
#172390=CARTESIAN_POINT('Ctrl Pts',(-96.6298719452267,-4.67836501173922,
127.178719294179));
#172391=CARTESIAN_POINT('Ctrl Pts',(-96.6225293840991,-4.58094499712026,
127.056394760042));
#172392=CARTESIAN_POINT('Ctrl Pts',(-96.6151868229715,-4.47893000454518,
126.938210520003));
#172393=CARTESIAN_POINT('Ctrl Pts',(-96.60784036526,-4.37686087418683,126.81996356141));
#172394=CARTESIAN_POINT('Ctrl Pts',(-96.6004939075486,-4.27019216761278,
126.705861551566));
#172395=CARTESIAN_POINT('Ctrl Pts',(-96.5931474498371,-4.1593125902904,
126.596267303635));
#172396=CARTESIAN_POINT('Ctrl Pts',(-96.5857897877326,-4.04826390584006,
126.486505908886));
#172397=CARTESIAN_POINT('Ctrl Pts',(-96.5784321256281,-3.93299180058921,
126.381266267863));
#172398=CARTESIAN_POINT('Ctrl Pts',(-96.5710744635236,-3.8139186156817,
126.280871327708));
#172399=CARTESIAN_POINT('Ctrl Pts',(-96.5644645829599,-3.70694720011512,
126.190679830165));
#172400=CARTESIAN_POINT('Ctrl Pts',(-96.5578547023961,-3.59690865649137,
126.104397861297));
#172401=CARTESIAN_POINT('Ctrl Pts',(-96.5512448218323,-3.48412789702929,
126.022228942294));
#172402=CARTESIAN_POINT('Ctrl Pts',(-96.5438215554269,-3.35746878196404,
125.929948640082));
#172403=CARTESIAN_POINT('Ctrl Pts',(-96.5363982890215,-3.22694941959803,
125.842564298181));
#172404=CARTESIAN_POINT('Ctrl Pts',(-96.5289750226161,-3.09298513919825,
125.760416378065));
#172405=CARTESIAN_POINT('Ctrl Pts',(-96.5215605298952,-2.95917919345286,
125.678365549968));
#172406=CARTESIAN_POINT('Ctrl Pts',(-96.5141460371742,-2.82193674935347,
125.60153901762));
#172407=CARTESIAN_POINT('Ctrl Pts',(-96.5067315444532,-2.68170496076179,
125.530236134211));
#172408=CARTESIAN_POINT('Ctrl Pts',(-96.4993241980994,-2.54160833284718,
125.459001975205));
#172409=CARTESIAN_POINT('Ctrl Pts',(-96.4919168517456,-2.39852842694709,
125.393281034356));
#172410=CARTESIAN_POINT('Ctrl Pts',(-96.4845095053919,-2.25293994895548,
125.333328525821));
#172411=CARTESIAN_POINT('Ctrl Pts',(-96.4771076837166,-2.10746005634475,
125.27342073213));
#172412=CARTESIAN_POINT('Ctrl Pts',(-96.4697058620412,-1.95947566072277,
125.219272945793));
#172413=CARTESIAN_POINT('Ctrl Pts',(-96.4623040403659,-1.80948445841844,
125.171093665145));
#172414=CARTESIAN_POINT('Ctrl Pts',(-96.4549061260546,-1.65957243530142,
125.122939817963));
#172415=CARTESIAN_POINT('Ctrl Pts',(-96.4475082117432,-1.50765606981616,
125.080748315519));
#172416=CARTESIAN_POINT('Ctrl Pts',(-96.4401102974319,-1.35425124660715,
125.044678844797));
#172417=CARTESIAN_POINT('Ctrl Pts',(-96.4327136125197,-1.20087191649693,
125.008615368168));
#172418=CARTESIAN_POINT('Ctrl Pts',(-96.4253169276075,-1.04600498262119,
124.97867198944));
#172419=CARTESIAN_POINT('Ctrl Pts',(-96.4179202426953,-0.890179755412589,
124.954958035631));
#172420=CARTESIAN_POINT('Ctrl Pts',(-96.4105238857599,-0.734361437657853,
124.931245133322));
#172421=CARTESIAN_POINT('Ctrl Pts',(-96.4031275288246,-0.577585280106661,
124.913761162877));
#172422=CARTESIAN_POINT('Ctrl Pts',(-96.3957311718892,-0.420388742700662,
124.902563953201));
#172423=CARTESIAN_POINT('Ctrl Pts',(-96.3883336825526,-0.263168138103033,
124.891365029203));
#172424=CARTESIAN_POINT('Ctrl Pts',(-96.380936193216,-0.105527397877214,
124.886454809003));
#172425=CARTESIAN_POINT('Ctrl Pts',(-96.3735387038794,0.0519931152654158,
124.887839065297));
#172426=CARTESIAN_POINT('Ctrl Pts',(-96.3661386213645,0.209568846979065,
124.88922380684));
#172427=CARTESIAN_POINT('Ctrl Pts',(-96.3587385388496,0.367023894647666,
124.896907414761));
#172428=CARTESIAN_POINT('Ctrl Pts',(-96.3513384563346,0.523820268757316,
124.910843595571));
#172429=CARTESIAN_POINT('Ctrl Pts',(-96.3439302366681,0.680789056599582,
124.924795100645));
#172430=CARTESIAN_POINT('Ctrl Pts',(-96.3365220170017,0.837097352389349,
124.945012876057));
#172431=CARTESIAN_POINT('Ctrl Pts',(-96.3291137973353,0.992213912618926,
124.971398924386));
#172432=CARTESIAN_POINT('Ctrl Pts',(-96.3217010180332,1.14742594450307,
124.997801212887));
#172433=CARTESIAN_POINT('Ctrl Pts',(-96.3142882387312,1.30144441487911,
125.030379262175));
#172434=CARTESIAN_POINT('Ctrl Pts',(-96.3068754594292,1.45375109411471,
125.068984577683));
#172435=CARTESIAN_POINT('Ctrl Pts',(-96.2994520884005,1.60627539627629,
125.107645054277));
#172436=CARTESIAN_POINT('Ctrl Pts',(-96.2920287173717,1.75708266535607,
125.152349891454));
#172437=CARTESIAN_POINT('Ctrl Pts',(-96.284605346343,1.90567178255613,125.202901377362));
#172438=CARTESIAN_POINT('Ctrl Pts',(-96.2806692969019,1.98445729784823,
125.229704988158));
#172439=CARTESIAN_POINT('Ctrl Pts',(-96.2767332474608,2.06261956503536,
125.258151505607));
#172440=CARTESIAN_POINT('Ctrl Pts',(-96.2727971980198,2.14008658250731,
125.288206161618));
#172441=CARTESIAN_POINT('Ctrl Pts',(-96.2653739316143,2.28618695978618,
125.344888304878));
#172442=CARTESIAN_POINT('Ctrl Pts',(-96.257950665209,2.43025478495182,125.407464569658));
#172443=CARTESIAN_POINT('Ctrl Pts',(-96.2505273988036,2.57177912251184,
125.475769555427));
#172444=CARTESIAN_POINT('Ctrl Pts',(-96.2431129060826,2.71313619005773,
125.543993810374));
#172445=CARTESIAN_POINT('Ctrl Pts',(-96.2356984133615,2.85195542093101,
125.617933148177));
#172446=CARTESIAN_POINT('Ctrl Pts',(-96.2282839206405,2.98774326323177,
125.697373173337));
#172447=CARTESIAN_POINT('Ctrl Pts',(-96.2208765742867,3.12340022809819,
125.77673663121));
#172448=CARTESIAN_POINT('Ctrl Pts',(-96.2134692279329,3.25603130100827,
125.861590034426));
#172449=CARTESIAN_POINT('Ctrl Pts',(-96.2060618815792,3.38516517293291,
125.951671948955));
#172450=CARTESIAN_POINT('Ctrl Pts',(-96.1986600599038,3.51420273194319,
126.041686676994));
#172451=CARTESIAN_POINT('Ctrl Pts',(-96.1912582382283,3.63974797868707,
126.136921939019));
#172452=CARTESIAN_POINT('Ctrl Pts',(-96.1838564165529,3.76135648058971,
126.237071707455));
#172453=CARTESIAN_POINT('Ctrl Pts',(-96.1764585022416,3.88290078631044,
126.337168607607));
#172454=CARTESIAN_POINT('Ctrl Pts',(-96.1690605879304,4.00051219855026,
126.442174610728));
#172455=CARTESIAN_POINT('Ctrl Pts',(-96.1616626736191,4.11377751987369,
126.551742003173));
#172456=CARTESIAN_POINT('Ctrl Pts',(-96.1542659887069,4.22702401855604,
126.661291187505));
#172457=CARTESIAN_POINT('Ctrl Pts',(-96.1468693037948,4.33592559171524,
126.775399997425));
#172458=CARTESIAN_POINT('Ctrl Pts',(-96.1394726188826,4.44010415421885,
126.893682202995));
#172459=CARTESIAN_POINT('Ctrl Pts',(-96.1320762619471,4.54427809733583,
127.011959163809));
#172460=CARTESIAN_POINT('Ctrl Pts',(-96.1246799050117,4.64372919947019,
127.134408872193));
#172461=CARTESIAN_POINT('Ctrl Pts',(-96.1172835480763,4.73811829729925,
127.260610405813));
#172462=CARTESIAN_POINT('Ctrl Pts',(-96.1098860587397,4.83252184633989,
127.38683126121));
#172463=CARTESIAN_POINT('Ctrl Pts',(-96.1024885694032,4.92186162434002,
127.516804786622));
#172464=CARTESIAN_POINT('Ctrl Pts',(-96.0950910800667,5.00584069532163,
127.65007947988));
#172465=CARTESIAN_POINT('Ctrl Pts',(-96.0876909975517,5.08984920503626,
127.783400892375));
#172466=CARTESIAN_POINT('Ctrl Pts',(-96.0802909150367,5.16849306739893,
127.920025461101));
#172467=CARTESIAN_POINT('Ctrl Pts',(-96.0728908325218,5.24152043396087,
128.059475537481));
#172468=CARTESIAN_POINT('Ctrl Pts',(-96.0654826128554,5.31462810162006,
128.199078953557));
#172469=CARTESIAN_POINT('Ctrl Pts',(-96.0580743931889,5.38210676648592,
128.341513751143));
#172470=CARTESIAN_POINT('Ctrl Pts',(-96.0506661735224,5.44375172647199,
128.48628001003));
#172471=CARTESIAN_POINT('Ctrl Pts',(-96.0432533942204,5.50543462790214,
128.631135370134));
#172472=CARTESIAN_POINT('Ctrl Pts',(-96.0358406149184,5.56127653772704,
128.778324702694));
#172473=CARTESIAN_POINT('Ctrl Pts',(-96.0284278356164,5.61112227285479,
128.927331741503));
#172474=CARTESIAN_POINT('Ctrl Pts',(-96.0210044645877,5.66103922990663,
129.076551688558));
#172475=CARTESIAN_POINT('Ctrl Pts',(-96.013581093559,5.70494279689298,129.22759417159));
#172476=CARTESIAN_POINT('Ctrl Pts',(-96.0061577225302,5.74272844744428,
129.379930717075));
#172477=CARTESIAN_POINT('Ctrl Pts',(-96.0022216730891,5.76276330602281,
129.460703208764));
#172478=CARTESIAN_POINT('Ctrl Pts',(-95.9982856236479,5.78107905988061,
129.541839375347));
#172479=CARTESIAN_POINT('Ctrl Pts',(-95.9943495742067,5.79766604176739,
129.623259846828));
#172480=CARTESIAN_POINT('Ctrl Pts',(-95.9869263078013,5.8289485719409,129.776816314981));
#172481=CARTESIAN_POINT('Ctrl Pts',(-95.9795030413958,5.85417356668348,
129.931848656131));
#172482=CARTESIAN_POINT('Ctrl Pts',(-95.9720797749903,5.87320400903427,
130.087837602748));
#172483=CARTESIAN_POINT('Ctrl Pts',(-95.9646652822693,5.89221195898259,
130.243642183384));
#172484=CARTESIAN_POINT('Ctrl Pts',(-95.9572507895483,5.90503988515356,
130.400400752035));
#172485=CARTESIAN_POINT('Ctrl Pts',(-95.9498362968273,5.91160138769369,
130.557582183504));
#172486=CARTESIAN_POINT('Ctrl Pts',(-95.9424289504735,5.91815656601064,
130.714612117592));
#172487=CARTESIAN_POINT('Ctrl Pts',(-95.9350216041198,5.91845732931424,
130.872063732636));
#172488=CARTESIAN_POINT('Ctrl Pts',(-95.927614257766,5.91246887541329,131.029399191524));
#172489=CARTESIAN_POINT('Ctrl Pts',(-95.9202124360906,5.9064848879272,131.186617303691));
#172490=CARTESIAN_POINT('Ctrl Pts',(-95.9128106144152,5.89422103726083,
131.343719060779));
#172491=CARTESIAN_POINT('Ctrl Pts',(-95.9054087927398,5.87569456641797,
131.500165133696));
#172492=CARTESIAN_POINT('Ctrl Pts',(-95.8980108784284,5.85717787555485,
131.656528619948));
#172493=CARTESIAN_POINT('Ctrl Pts',(-95.8906129641171,5.83240519233798,
131.812236741597));
#172494=CARTESIAN_POINT('Ctrl Pts',(-95.8832150498057,5.80144571479833,
131.966753916217));
#172495=CARTESIAN_POINT('Ctrl Pts',(-95.8758183648935,5.77049138216213,
132.121245412886));
#172496=CARTESIAN_POINT('Ctrl Pts',(-95.8684216799813,5.73335236900841,
132.274545989662));
#172497=CARTESIAN_POINT('Ctrl Pts',(-95.861024995069,5.69014925727116,132.426128786102));
#172498=CARTESIAN_POINT('Ctrl Pts',(-95.8536286381336,5.64694806120516,
132.577704861202));
#172499=CARTESIAN_POINT('Ctrl Pts',(-95.8462322811981,5.59768340351682,
132.727562948412));
#172500=CARTESIAN_POINT('Ctrl Pts',(-95.8388359242626,5.54252609202692,
132.875190181219));
#172501=CARTESIAN_POINT('Ctrl Pts',(-95.8314384349261,5.48736033581182,
133.022840016133));
#172502=CARTESIAN_POINT('Ctrl Pts',(-95.8240409455895,5.42630026009468,
133.168257966865));
#172503=CARTESIAN_POINT('Ctrl Pts',(-95.8166434562529,5.35956522528852,
133.310950164815));
#172504=CARTESIAN_POINT('Ctrl Pts',(-95.8092433737379,5.29280679661984,
133.453692383293));
#172505=CARTESIAN_POINT('Ctrl Pts',(-95.801843291223,5.22036960613111,133.593706608646));
#172506=CARTESIAN_POINT('Ctrl Pts',(-95.794443208708,5.14251938285965,133.730522772918));
#172507=CARTESIAN_POINT('Ctrl Pts',(-95.7870349890415,5.06458355526396,
133.867489380629));
#172508=CARTESIAN_POINT('Ctrl Pts',(-95.7796267693751,4.98122299270906,
134.001250579734));
#172509=CARTESIAN_POINT('Ctrl Pts',(-95.7722185497086,4.89274764574691,
134.131363929488));
#172510=CARTESIAN_POINT('Ctrl Pts',(-95.7648057704065,4.804217843685,134.261557361837));
#172511=CARTESIAN_POINT('Ctrl Pts',(-95.7573929911045,4.7105672058575,134.388098171646));
#172512=CARTESIAN_POINT('Ctrl Pts',(-95.7499802118024,4.61214620139334,
134.51057674449));
#172513=CARTESIAN_POINT('Ctrl Pts',(-95.7425568407737,4.51358456838238,
134.633230320463));
#172514=CARTESIAN_POINT('Ctrl Pts',(-95.7351334697449,4.41023920002195,
134.751809786278));
#172515=CARTESIAN_POINT('Ctrl Pts',(-95.7277100987161,4.3024982169981,134.865941548094));
#172516=CARTESIAN_POINT('Ctrl Pts',(-95.7237740492754,4.24537136259084,
134.926456946761));
#172517=CARTESIAN_POINT('Ctrl Pts',(-95.7198379998347,4.18700932010286,
134.985722589103));
#172518=CARTESIAN_POINT('Ctrl Pts',(-95.715901950394,4.12747364037448,135.043687440366));
#172519=CARTESIAN_POINT('Ctrl Pts',(-95.7084786839886,4.01519120644945,
135.15300734083));
#172520=CARTESIAN_POINT('Ctrl Pts',(-95.7010554175831,3.89839283290984,
135.258028610583));
#172521=CARTESIAN_POINT('Ctrl Pts',(-95.6936321511777,3.77744133321969,
135.358355296591));
#172522=CARTESIAN_POINT('Ctrl Pts',(-95.6862176584567,3.65663278815709,
135.458563404788));
#172523=CARTESIAN_POINT('Ctrl Pts',(-95.6788031657356,3.53168117215285,
135.554087737778));
#172524=CARTESIAN_POINT('Ctrl Pts',(-95.6713886730146,3.40298663464442,
135.644568518776));
#172525=CARTESIAN_POINT('Ctrl Pts',(-95.6639813266608,3.27441613777687,
135.73496209099));
#172526=CARTESIAN_POINT('Ctrl Pts',(-95.656573980307,3.14211020469109,135.820321575576));
#172527=CARTESIAN_POINT('Ctrl Pts',(-95.6491666339533,3.00650252154732,
135.900326978368));
#172528=CARTESIAN_POINT('Ctrl Pts',(-95.6417648122779,2.87099597973021,
135.980272710113));
#172529=CARTESIAN_POINT('Ctrl Pts',(-95.6343629906025,2.73219291129334,
136.054872122346));
#172530=CARTESIAN_POINT('Ctrl Pts',(-95.6269611689271,2.59055638934099,
136.123848201549));
#172531=CARTESIAN_POINT('Ctrl Pts',(-95.6195632546157,2.44899463620569,
136.192787868816));
#172532=CARTESIAN_POINT('Ctrl Pts',(-95.6121653403044,2.30460274319476,
136.25610995196));
#172533=CARTESIAN_POINT('Ctrl Pts',(-95.604767425993,2.15786871419567,136.313583173862));
#172534=CARTESIAN_POINT('Ctrl Pts',(-95.5973707410808,2.01115906973039,
136.371046844757));
#172535=CARTESIAN_POINT('Ctrl Pts',(-95.5899740561686,1.86210840901045,
136.422663447481));
#172536=CARTESIAN_POINT('Ctrl Pts',(-95.5825773712564,1.7112251721297,136.468249650092));
#172537=CARTESIAN_POINT('Ctrl Pts',(-95.5751810143209,1.56034862556979,
136.513833831363));
#172538=CARTESIAN_POINT('Ctrl Pts',(-95.5677846573855,1.40764002176226,
136.553388036227));
#172539=CARTESIAN_POINT('Ctrl Pts',(-95.5603883004501,1.25362317562847,
136.586778753262));
#172540=CARTESIAN_POINT('Ctrl Pts',(-95.5529908111135,1.09958274912191,
136.620174582502));
#172541=CARTESIAN_POINT('Ctrl Pts',(-95.5455933217769,0.944234046320716,
136.647404965891));
#172542=CARTESIAN_POINT('Ctrl Pts',(-95.5381958324403,0.788111142525765,
136.668387509517));
#172543=CARTESIAN_POINT('Ctrl Pts',(-95.5307957499253,0.631933510089578,
136.689377408541));
#172544=CARTESIAN_POINT('Ctrl Pts',(-95.5233956674102,0.474981506054996,
136.704115057496));
#172545=CARTESIAN_POINT('Ctrl Pts',(-95.5159955848952,0.317794244941677,
136.712569938535));
#172546=CARTESIAN_POINT('Ctrl Pts',(-95.5085873652287,0.160434140275297,
136.721034116584));
#172547=CARTESIAN_POINT('Ctrl Pts',(-95.5011791455624,0.00283863489836503,
136.723201709829));
#172548=CARTESIAN_POINT('Ctrl Pts',(-95.4937709258959,-0.154452497414042,
136.719094338415));
#172549=CARTESIAN_POINT('Ctrl Pts',(-95.4863581465939,-0.311840439794293,
136.714984438982));
#172550=CARTESIAN_POINT('Ctrl Pts',(-95.4789453672918,-0.468923264198511,
136.704591903687));
#172551=CARTESIAN_POINT('Ctrl Pts',(-95.4715325879897,-0.625166913285077,
136.687990185531));
#172552=CARTESIAN_POINT('Ctrl Pts',(-95.4641092169609,-0.781633810624336,
136.671364746062));
#172553=CARTESIAN_POINT('Ctrl Pts',(-95.4566858459322,-0.937258769509263,
136.648512458505));
#172554=CARTESIAN_POINT('Ctrl Pts',(-95.4492624749034,-1.09151768614798,
136.619557923189));
#172555=CARTESIAN_POINT('Ctrl Pts',(-95.4453264254626,-1.17330946514215,
136.60420553381));
#172556=CARTESIAN_POINT('Ctrl Pts',(-95.4413903760218,-1.25471743807355,
136.587138421895));
#172557=CARTESIAN_POINT('Ctrl Pts',(-95.437454326581,-1.33566539822654,
136.568380786379));
#172558=CARTESIAN_POINT('Ctrl Pts',(-95.4300310601755,-1.48833072477601,
136.533004471201));
#172559=CARTESIAN_POINT('Ctrl Pts',(-95.42260779377,-1.63982046723384,136.491505253228));
#172560=CARTESIAN_POINT('Ctrl Pts',(-95.4151845273645,-1.78960538956013,
136.443974355417));
#172561=CARTESIAN_POINT('Ctrl Pts',(-95.4077700346434,-1.93921327854795,
136.396499635179));
#172562=CARTESIAN_POINT('Ctrl Pts',(-95.4003555419223,-2.08712000584653,
136.343007537113));
#172563=CARTESIAN_POINT('Ctrl Pts',(-95.3929410492012,-2.23280659051213,
136.283640250133));
#172564=CARTESIAN_POINT('Ctrl Pts',(-95.3855337028474,-2.37835275696242,
136.224330183579));
#172565=CARTESIAN_POINT('Ctrl Pts',(-95.3781263564934,-2.52168269743741,
136.159156341415));
#172566=CARTESIAN_POINT('Ctrl Pts',(-95.3707190101396,-2.66229277381995,
136.088310631426));
#172567=CARTESIAN_POINT('Ctrl Pts',(-95.3633171884641,-2.80279797790181,
136.01751776084));
#172568=CARTESIAN_POINT('Ctrl Pts',(-95.3559153667888,-2.94058702512365,
135.94106161276));
#172569=CARTESIAN_POINT('Ctrl Pts',(-95.3485135451133,-3.07517655384108,
135.859182051129));
#172570=CARTESIAN_POINT('Ctrl Pts',(-95.3411156308019,-3.20969503379471,
135.77734571308));
#172571=CARTESIAN_POINT('Ctrl Pts',(-95.3337177164903,-3.34101704086007,
135.690091856765));
#172572=CARTESIAN_POINT('Ctrl Pts',(-95.3263198021788,-3.46868421702546,
135.597706042742));
#172573=CARTESIAN_POINT('Ctrl Pts',(-95.3189231172666,-3.59633017722139,
135.505335581566));
#172574=CARTESIAN_POINT('Ctrl Pts',(-95.3115264323544,-3.72032220983606,
135.407835073946));
#172575=CARTESIAN_POINT('Ctrl Pts',(-95.3041297474421,-3.84023124822334,
135.305533189538));
#172576=CARTESIAN_POINT('Ctrl Pts',(-95.2967333905066,-3.96013496971821,
135.203235841302));
#172577=CARTESIAN_POINT('Ctrl Pts',(-95.2893370335711,-4.07595577297636,
135.096137781879));
#172578=CARTESIAN_POINT('Ctrl Pts',(-95.2819406766356,-4.18729819629881,
134.984607545413));
#172579=CARTESIAN_POINT('Ctrl Pts',(-95.274543187299,-4.29865766643019,
134.873060233383));
#172580=CARTESIAN_POINT('Ctrl Pts',(-95.2671456979625,-4.40553712764686,
134.757079657373));
#172581=CARTESIAN_POINT('Ctrl Pts',(-95.2597482086259,-4.50757857887058,
134.637070614136));
#172582=CARTESIAN_POINT('Ctrl Pts',(-95.2523481261108,-4.60965580056727,
134.517019501914));
#172583=CARTESIAN_POINT('Ctrl Pts',(-95.2449480435957,-4.70689139397183,
134.392937395054));
#172584=CARTESIAN_POINT('Ctrl Pts',(-95.2375479610807,-4.79896827898857,
134.265261370226));
#172585=CARTESIAN_POINT('Ctrl Pts',(-95.2301397414141,-4.89114641200624,
134.137444952483));
#172586=CARTESIAN_POINT('Ctrl Pts',(-95.2227315217475,-4.9781542897327,
134.006027027566));
#172587=CARTESIAN_POINT('Ctrl Pts',(-95.215323302081,-5.05971834089961,
133.871473408655));
#172588=CARTESIAN_POINT('Ctrl Pts',(-95.2079105227789,-5.14133259337882,
133.736836974238));
#172589=CARTESIAN_POINT('Ctrl Pts',(-95.2004977434769,-5.21749616265445,
133.59906132607));
#172590=CARTESIAN_POINT('Ctrl Pts',(-95.1930849641748,-5.28798217577897,
133.458635484859));
#172591=CARTESIAN_POINT('Ctrl Pts',(-95.1856615931459,-5.35856890262481,
133.318008996621));
#172592=CARTESIAN_POINT('Ctrl Pts',(-95.1782382221169,-5.42346171752098,
133.174725091558));
#172593=CARTESIAN_POINT('Ctrl Pts',(-95.1708148510881,-5.48248215935056,
133.029292062555));
#172594=CARTESIAN_POINT('Ctrl Pts',(-95.1668788016479,-5.51377621377919,
132.952179980974));
#172595=CARTESIAN_POINT('Ctrl Pts',(-95.1629427522078,-5.54342016702373,
132.874463956889));
#172596=CARTESIAN_POINT('Ctrl Pts',(-95.1590067027677,-5.57139318674206,
132.796221185283));
#172597=CARTESIAN_POINT('Ctrl Pts',(-95.1503669630726,-5.63279475512309,
132.624476091636));
#172598=CARTESIAN_POINT('Ctrl Pts',(-95.1417272233776,-5.68629543393868,
132.449765875302));
#172599=CARTESIAN_POINT('Ctrl Pts',(-95.1330874836826,-5.73164059706365,
132.272770175078));
#172600=CARTESIAN_POINT('Ctrl Pts',(-95.1244822298778,-5.77680476303202,
132.096480960756));
#172601=CARTESIAN_POINT('Ctrl Pts',(-95.1158769760729,-5.81387830329087,
131.917924575233));
#172602=CARTESIAN_POINT('Ctrl Pts',(-95.1072717222681,-5.84265624027591,
131.737794396934));
#172603=CARTESIAN_POINT('Ctrl Pts',(-95.0987334134545,-5.87121029789798,
131.559065550134));
#172604=CARTESIAN_POINT('Ctrl Pts',(-95.0901951046409,-5.89159725125045,
131.378787421531));
#172605=CARTESIAN_POINT('Ctrl Pts',(-95.0816567958273,-5.90366397735691,
131.197657204073));
#172606=CARTESIAN_POINT('Ctrl Pts',(-95.0755629392138,-5.91227609250675,
131.068383175965));
#172607=CARTESIAN_POINT('Ctrl Pts',(-95.0694690826003,-5.91665103111156,
130.938675529287));
#172608=CARTESIAN_POINT('Ctrl Pts',(-95.0633752259867,-5.91674833943923,
130.808793477043));
#172609=CARTESIAN_POINT('',(-93.3133751922047,-5.90951273974424,130.800546416903));
#172610=CARTESIAN_POINT('Ctrl Pts',(-95.0633751922047,-5.91070361657871,
130.808788229024));
#172611=CARTESIAN_POINT('Ctrl Pts',(-95.0024364877883,-5.90173179602721,
129.511284220283));
#172612=CARTESIAN_POINT('Ctrl Pts',(-94.8486819087681,-4.84118804501417,
126.224213906414));
#172613=CARTESIAN_POINT('Ctrl Pts',(-94.6021114551422,0.596386883552906,
123.831421264929));
#172614=CARTESIAN_POINT('Ctrl Pts',(-94.3236638313295,6.18889303939605,
127.537073749649));
#172615=CARTESIAN_POINT('Ctrl Pts',(-94.0452162075165,6.09410883626184,
134.245203250136));
#172616=CARTESIAN_POINT('Ctrl Pts',(-93.7667685837036,0.399136326374221,
137.791366465805));
#172617=CARTESIAN_POINT('Ctrl Pts',(-93.5228215785999,-4.91155013382791,
135.272979751163));
#172618=CARTESIAN_POINT('Ctrl Pts',(-93.3716904481001,-5.90220975232409,
132.042820379345));
#172619=CARTESIAN_POINT('Ctrl Pts',(-93.3133751922047,-5.90951273974424,
130.800546416903));
#172620=CARTESIAN_POINT('',(-91.5633765517166,-5.92117668185514,130.801382376507));
#172621=CARTESIAN_POINT('Ctrl Pts',(-93.3133751922047,-5.90951273974424,
130.800546416903));
#172622=CARTESIAN_POINT('Ctrl Pts',(-93.2788745734958,-5.913833351573,130.065589163398));
#172623=CARTESIAN_POINT('Ctrl Pts',(-93.1515580801835,-5.44546871744137,
127.358710712193));
#172624=CARTESIAN_POINT('Ctrl Pts',(-92.9314257122645,-1.38658135523596,
123.944699352184));
#172625=CARTESIAN_POINT('Ctrl Pts',(-92.6529780884523,5.02174620662583,
125.929975982911));
#172626=CARTESIAN_POINT('Ctrl Pts',(-92.3745304646391,6.81533433053491,
132.394573965943));
#172627=CARTESIAN_POINT('Ctrl Pts',(-92.0960828408264,2.34596315227786,
137.397843568065));
#172628=CARTESIAN_POINT('Ctrl Pts',(-91.8256985594628,-4.08737977375717,
136.37259907124));
#172629=CARTESIAN_POINT('Ctrl Pts',(-91.6481301527034,-5.91352381113235,
132.595058967895));
#172630=CARTESIAN_POINT('Ctrl Pts',(-91.5633776205484,-5.9246574854241,
130.801403228907));
#172631=CARTESIAN_POINT('',(-89.8133744894949,-5.9182659565827,130.809617868958));
#172632=CARTESIAN_POINT('Ctrl Pts',(-91.5633751922047,-5.9167492370296,
130.801355853076));
#172633=CARTESIAN_POINT('Ctrl Pts',(-91.5553126592033,-5.91666269968621,
130.630953226781));
#172634=CARTESIAN_POINT('Ctrl Pts',(-91.5472501262019,-5.90921545676705,
130.460742668894));
#172635=CARTESIAN_POINT('Ctrl Pts',(-91.5391875932004,-5.89445284654217,
130.291178191531));
#172636=CARTESIAN_POINT('Ctrl Pts',(-91.531764326795,-5.88086074235885,
130.135058236659));
#172637=CARTESIAN_POINT('Ctrl Pts',(-91.5243410603895,-5.86104133235314,
129.979242582282));
#172638=CARTESIAN_POINT('Ctrl Pts',(-91.5169177939841,-5.83501063256916,
129.824268029947));
#172639=CARTESIAN_POINT('Ctrl Pts',(-91.5095033012632,-5.80901069891061,
129.669476644664));
#172640=CARTESIAN_POINT('Ctrl Pts',(-91.5020888085421,-5.77681414946191,
129.515524747181));
#172641=CARTESIAN_POINT('Ctrl Pts',(-91.4946743158212,-5.7384889012075,
129.362946141012));
#172642=CARTESIAN_POINT('Ctrl Pts',(-91.4872669694674,-5.70020059227029,
129.210514595849));
#172643=CARTESIAN_POINT('Ctrl Pts',(-91.4798596231137,-5.6557954346729,
129.059454066533));
#172644=CARTESIAN_POINT('Ctrl Pts',(-91.4724522767599,-5.60539272591123,
128.910290146121));
#172645=CARTESIAN_POINT('Ctrl Pts',(-91.4650504550845,-5.55502760939134,
128.761237477787));
#172646=CARTESIAN_POINT('Ctrl Pts',(-91.4576486334092,-5.49867396743771,
128.614078953904));
#172647=CARTESIAN_POINT('Ctrl Pts',(-91.4502468117338,-5.4365014254727,
128.469326824806));
#172648=CARTESIAN_POINT('Ctrl Pts',(-91.4428488974224,-5.37436170390846,
128.324651109229));
#172649=CARTESIAN_POINT('Ctrl Pts',(-91.4354509831112,-5.30640934682248,
128.182379600671));
#172650=CARTESIAN_POINT('Ctrl Pts',(-91.4280530687998,-5.23286273408415,
128.043006209176));
#172651=CARTESIAN_POINT('Ctrl Pts',(-91.4206563838876,-5.15932834345889,
127.903655979011));
#172652=CARTESIAN_POINT('Ctrl Pts',(-91.4132596989754,-5.08020171633685,
127.767203239874));
#172653=CARTESIAN_POINT('Ctrl Pts',(-91.4058630140632,-4.99574802713157,
127.634118952975));
#172654=CARTESIAN_POINT('Ctrl Pts',(-91.3984666571278,-4.91129808269137,
127.501040567172));
#172655=CARTESIAN_POINT('Ctrl Pts',(-91.3910703001923,-4.82152174584406,
127.371330651817));
#172656=CARTESIAN_POINT('Ctrl Pts',(-91.3836739432569,-4.72672837868967,
127.245432492893));
#172657=CARTESIAN_POINT('Ctrl Pts',(-91.3762764539203,-4.63192049842851,
127.119515058639));
#172658=CARTESIAN_POINT('Ctrl Pts',(-91.3688789645838,-4.53209428298416,
126.997410841056));
#172659=CARTESIAN_POINT('Ctrl Pts',(-91.3614814752472,-4.4276002572672,
126.879531127722));
#172660=CARTESIAN_POINT('Ctrl Pts',(-91.3540813927322,-4.32306960133165,
126.761610091838));
#172661=CARTESIAN_POINT('Ctrl Pts',(-91.3466813102172,-4.2138681247446,
126.64791678782));
#172662=CARTESIAN_POINT('Ctrl Pts',(-91.3392812277023,-4.10038405780983,
126.538826519594));
#172663=CARTESIAN_POINT('Ctrl Pts',(-91.3318730080358,-3.98677520347685,
126.429616295404));
#172664=CARTESIAN_POINT('Ctrl Pts',(-91.3244647883694,-3.8688746236027,
126.325019474033));
#172665=CARTESIAN_POINT('Ctrl Pts',(-91.3170565687029,-3.74710510889896,
126.225372316056));
#172666=CARTESIAN_POINT('Ctrl Pts',(-91.3096437894009,-3.62526064709075,
126.125663826916));
#172667=CARTESIAN_POINT('Ctrl Pts',(-91.3022310100988,-3.49954280290225,
126.030911295736));
#172668=CARTESIAN_POINT('Ctrl Pts',(-91.2948182307967,-3.37040390103012,
125.94140800558));
#172669=CARTESIAN_POINT('Ctrl Pts',(-91.287394859768,-3.24108047943916,
125.851776828926));
#172670=CARTESIAN_POINT('Ctrl Pts',(-91.2799714887392,-3.10832655162119,
125.767410072895));
#172671=CARTESIAN_POINT('Ctrl Pts',(-91.2725481177105,-2.97262032045786,
125.688555793992));
#172672=CARTESIAN_POINT('Ctrl Pts',(-91.2686120682695,-2.90066562046546,
125.646745363234));
#172673=CARTESIAN_POINT('Ctrl Pts',(-91.2646760188286,-2.82788128994348,
125.606483897824));
#172674=CARTESIAN_POINT('Ctrl Pts',(-91.2607399693877,-2.75434083446996,
125.567802861743));
#172675=CARTESIAN_POINT('Ctrl Pts',(-91.2533167029822,-2.61564583057169,
125.49485163489));
#172676=CARTESIAN_POINT('Ctrl Pts',(-91.2458934365767,-2.47384083239129,
125.427304098643));
#172677=CARTESIAN_POINT('Ctrl Pts',(-91.2384701701713,-2.32938612333577,
125.365436932598));
#172678=CARTESIAN_POINT('Ctrl Pts',(-91.2310556774503,-2.18510214775013,
125.303642888405));
#172679=CARTESIAN_POINT('Ctrl Pts',(-91.2236411847293,-2.03817503483164,
125.247515996236));
#172680=CARTESIAN_POINT('Ctrl Pts',(-91.2162266920083,-1.88909059938297,
125.197287649446));
#172681=CARTESIAN_POINT('Ctrl Pts',(-91.2088193456545,-1.74014985712612,
125.147107714627));
#172682=CARTESIAN_POINT('Ctrl Pts',(-91.2014119993007,-1.5890562832183,
125.10281512538));
#172683=CARTESIAN_POINT('Ctrl Pts',(-91.1940046529469,-1.43631655719245,
125.064593609225));
#172684=CARTESIAN_POINT('Ctrl Pts',(-91.1866028312715,-1.28369075021637,
125.02640060012));
#172685=CARTESIAN_POINT('Ctrl Pts',(-91.1792010095962,-1.12942159633595,
124.994269738407));
#172686=CARTESIAN_POINT('Ctrl Pts',(-91.1717991879207,-0.974031752950555,
124.968335197235));
#172687=CARTESIAN_POINT('Ctrl Pts',(-91.1644012736094,-0.818723938654372,
124.942414346706));
#172688=CARTESIAN_POINT('Ctrl Pts',(-91.157003359298,-0.662296980332273,
124.922683363683));
#172689=CARTESIAN_POINT('Ctrl Pts',(-91.1496054449866,-0.505284458147056,
124.909225489441));
#172690=CARTESIAN_POINT('Ctrl Pts',(-91.1422087600744,-0.348298028594753,
124.895769851653));
#172691=CARTESIAN_POINT('Ctrl Pts',(-91.1348120751622,-0.190726599881081,
124.888585285487));
#172692=CARTESIAN_POINT('Ctrl Pts',(-91.12741539025,-0.0331097382576597,
124.887703258234));
#172693=CARTESIAN_POINT('Ctrl Pts',(-91.1200190333145,0.124500134469396,
124.886821270092));
#172694=CARTESIAN_POINT('Ctrl Pts',(-91.1126226763791,0.28215506280889,
124.89224126729));
#172695=CARTESIAN_POINT('Ctrl Pts',(-91.1052263194436,0.439314879937609,
124.903942581633));
#172696=CARTESIAN_POINT('Ctrl Pts',(-91.097828830107,0.596498758635541,
124.915645687477));
#172697=CARTESIAN_POINT('Ctrl Pts',(-91.0904313407705,0.753187002897855,
124.933631997591));
#172698=CARTESIAN_POINT('Ctrl Pts',(-91.0830338514339,0.908844117561575,
124.957828916423));
#172699=CARTESIAN_POINT('Ctrl Pts',(-91.0756337689189,1.06455579758532,
124.982034317447));
#172700=CARTESIAN_POINT('Ctrl Pts',(-91.0682336864038,1.2192352597069,125.012454604511));
#172701=CARTESIAN_POINT('Ctrl Pts',(-91.0608336038888,1.37235690214343,
125.048966009406));
#172702=CARTESIAN_POINT('Ctrl Pts',(-91.0534253842223,1.52564691756732,
125.085517562343));
#172703=CARTESIAN_POINT('Ctrl Pts',(-91.0460171645559,1.67737532902632,
125.12817352244));
#172704=CARTESIAN_POINT('Ctrl Pts',(-91.0386089448894,1.82703070226985,
125.176759940949));
#172705=CARTESIAN_POINT('Ctrl Pts',(-91.0311961655873,1.97677818589847,
125.225376263588));
#172706=CARTESIAN_POINT('Ctrl Pts',(-91.0237833862852,2.12444973952501,
125.279930188856));
#172707=CARTESIAN_POINT('Ctrl Pts',(-91.0163706069831,2.26955412325322,
125.340199689837));
#172708=CARTESIAN_POINT('Ctrl Pts',(-91.0089472359544,2.4148658389294,125.400555306707));
#172709=CARTESIAN_POINT('Ctrl Pts',(-91.0015238649257,2.55760272085013,
125.466642653559));
#172710=CARTESIAN_POINT('Ctrl Pts',(-90.9941004938969,2.69729759171301,
125.538193485368));
#172711=CARTESIAN_POINT('Ctrl Pts',(-90.9901644444562,2.77136716417534,
125.576131453231));
#172712=CARTESIAN_POINT('Ctrl Pts',(-90.9862283950155,2.84458198378661,
125.615604666362));
#172713=CARTESIAN_POINT('Ctrl Pts',(-90.9822923455748,2.91687584745019,
125.656568289484));
#172714=CARTESIAN_POINT('Ctrl Pts',(-90.9748690791694,3.05321981810821,
125.733824404263));
#172715=CARTESIAN_POINT('Ctrl Pts',(-90.9674458127639,3.18669853869445,
125.816617872076));
#172716=CARTESIAN_POINT('Ctrl Pts',(-90.9600225463585,3.316830436404,125.904710995537));
#172717=CARTESIAN_POINT('Ctrl Pts',(-90.9526080536375,3.44680852901723,
125.992700000242));
#172718=CARTESIAN_POINT('Ctrl Pts',(-90.9451935609166,3.57344736642153,
126.08597598534));
#172719=CARTESIAN_POINT('Ctrl Pts',(-90.9377790681956,3.6962896760663,126.184255294837));
#172720=CARTESIAN_POINT('Ctrl Pts',(-90.9303717218418,3.81901358566811,
126.282439879036));
#172721=CARTESIAN_POINT('Ctrl Pts',(-90.922964375488,3.93794796279608,126.385617955562));
#172722=CARTESIAN_POINT('Ctrl Pts',(-90.9155570291342,4.05266435961837,
126.493462549787));
#172723=CARTESIAN_POINT('Ctrl Pts',(-90.9081552074588,4.1672951966239,126.601226709445));
#172724=CARTESIAN_POINT('Ctrl Pts',(-90.9007533857834,4.27771404648123,
126.713650202138));
#172725=CARTESIAN_POINT('Ctrl Pts',(-90.8933515641081,4.38352551643076,
126.830365825257));
#172726=CARTESIAN_POINT('Ctrl Pts',(-90.8859536497967,4.48928112932924,
126.947019835107));
#172727=CARTESIAN_POINT('Ctrl Pts',(-90.8785557354854,4.59043395607122,
127.067961187105));
#172728=CARTESIAN_POINT('Ctrl Pts',(-90.871157821174,4.68662555030327,127.19278595909));
#172729=CARTESIAN_POINT('Ctrl Pts',(-90.8637611362618,4.78280115923731,
127.317589987463));
#172730=CARTESIAN_POINT('Ctrl Pts',(-90.8563644513495,4.87401694434677,
127.446275859589));
#172731=CARTESIAN_POINT('Ctrl Pts',(-90.8489677664373,4.95995478256792,
127.578406631939));
#172732=CARTESIAN_POINT('Ctrl Pts',(-90.8415714095019,5.04588881021528,
127.710531545473));
#172733=CARTESIAN_POINT('Ctrl Pts',(-90.8341750525665,5.12654515277362,
127.84610074258));
#172734=CARTESIAN_POINT('Ctrl Pts',(-90.826778695631,5.2016492256185,127.98464859395));
#172735=CARTESIAN_POINT('Ctrl Pts',(-90.8193812062945,5.27676479708867,
128.12321765735));
#172736=CARTESIAN_POINT('Ctrl Pts',(-90.8119837169579,5.34632622833766,
128.264765954846));
#172737=CARTESIAN_POINT('Ctrl Pts',(-90.8045862276214,5.41010514784449,
128.408803719522));
#172738=CARTESIAN_POINT('Ctrl Pts',(-90.7971861451064,5.47390642495259,
128.552891976413));
#172739=CARTESIAN_POINT('Ctrl Pts',(-90.7897860625913,5.53192100343032,
128.69947109686));
#172740=CARTESIAN_POINT('Ctrl Pts',(-90.7823859800764,5.58396891237707,
128.848031977458));
#172741=CARTESIAN_POINT('Ctrl Pts',(-90.7749777604099,5.63607405335044,
128.996756216017));
#172742=CARTESIAN_POINT('Ctrl Pts',(-90.7675695407434,5.68219929860803,
129.14746621411));
#172743=CARTESIAN_POINT('Ctrl Pts',(-90.7601613210769,5.72221455345155,
129.299637664073));
#172744=CARTESIAN_POINT('Ctrl Pts',(-90.7527485417748,5.76225443701674,
129.451902773025));
#172745=CARTESIAN_POINT('Ctrl Pts',(-90.7453357624728,5.7961767564546,129.605630762527));
#172746=CARTESIAN_POINT('Ctrl Pts',(-90.7379229831707,5.82390278213553,
129.760288327572));
#172747=CARTESIAN_POINT('Ctrl Pts',(-90.730499612142,5.8516684240622,129.915166874598));
#172748=CARTESIAN_POINT('Ctrl Pts',(-90.7230762411133,5.87322003868459,
130.070977281123));
#172749=CARTESIAN_POINT('Ctrl Pts',(-90.7156528700845,5.88853078739758,
130.227181504664));
#172750=CARTESIAN_POINT('Ctrl Pts',(-90.7117168206436,5.89664891374179,
130.310004732056));
#172751=CARTESIAN_POINT('Ctrl Pts',(-90.7077807712027,5.90301337996738,
130.392938669234));
#172752=CARTESIAN_POINT('Ctrl Pts',(-90.7038447217618,5.90762612287072,
130.475903383096));
#172753=CARTESIAN_POINT('Ctrl Pts',(-90.6964214553564,5.91632561202739,
130.632372244197));
#172754=CARTESIAN_POINT('Ctrl Pts',(-90.688998188951,5.91881763159911,130.789423563835));
#172755=CARTESIAN_POINT('Ctrl Pts',(-90.6815749225456,5.91504186126461,
130.94652369993));
#172756=CARTESIAN_POINT('Ctrl Pts',(-90.6741604298246,5.91127055357707,
131.103438156711));
#172757=CARTESIAN_POINT('Ctrl Pts',(-90.6667459371035,5.90124621054413,
131.260400945556));
#172758=CARTESIAN_POINT('Ctrl Pts',(-90.6593314443825,5.88496031300223,
131.416874027124));
#172759=CARTESIAN_POINT('Ctrl Pts',(-90.6519240980287,5.86869011242153,
131.573196294046));
#172760=CARTESIAN_POINT('Ctrl Pts',(-90.6445167516749,5.84617041045668,
131.729029424547));
#172761=CARTESIAN_POINT('Ctrl Pts',(-90.6371094053211,5.81744471360352,
131.883836215561));
#172762=CARTESIAN_POINT('Ctrl Pts',(-90.6297075836457,5.78874044145883,
132.038527545829));
#172763=CARTESIAN_POINT('Ctrl Pts',(-90.6223057619704,5.75383945853556,
132.192193695336));
#172764=CARTESIAN_POINT('Ctrl Pts',(-90.614903940295,5.71283698334393,132.344303526975));
#172765=CARTESIAN_POINT('Ctrl Pts',(-90.6075060259836,5.6718561530398,132.496333061017));
#172766=CARTESIAN_POINT('Ctrl Pts',(-90.6001081116723,5.62478034201596,
132.646807553864));
#172767=CARTESIAN_POINT('Ctrl Pts',(-90.5927101973609,5.57175563241608,
132.795207104651));
#172768=CARTESIAN_POINT('Ctrl Pts',(-90.5853135124487,5.51873973456104,
132.943581994125));
#172769=CARTESIAN_POINT('Ctrl Pts',(-90.5779168275365,5.4597770256894,133.089882274714));
#172770=CARTESIAN_POINT('Ctrl Pts',(-90.5705201426243,5.39506316547971,
133.233604121825));
#172771=CARTESIAN_POINT('Ctrl Pts',(-90.5631237856889,5.3303521747504,133.377319596158));
#172772=CARTESIAN_POINT('Ctrl Pts',(-90.5557274287534,5.25989069299819,
133.518456523957));
#172773=CARTESIAN_POINT('Ctrl Pts',(-90.548331071818,5.18392204765302,133.656532205384));
#172774=CARTESIAN_POINT('Ctrl Pts',(-90.5409335824814,5.10794177131432,
133.794629026551));
#172775=CARTESIAN_POINT('Ctrl Pts',(-90.5335360931448,5.02645283249731,
133.929663341048));
#172776=CARTESIAN_POINT('Ctrl Pts',(-90.5261386038082,4.9397438455942,134.061178282467));
#172777=CARTESIAN_POINT('Ctrl Pts',(-90.5187385212932,4.85300446299003,
134.192739326246));
#172778=CARTESIAN_POINT('Ctrl Pts',(-90.5113384387783,4.7610415943726,134.320778229174));
#172779=CARTESIAN_POINT('Ctrl Pts',(-90.5039383562633,4.66418628418919,
134.444868393808));
#172780=CARTESIAN_POINT('Ctrl Pts',(-90.4965301365968,4.56722447163513,
134.569095008336));
#172781=CARTESIAN_POINT('Ctrl Pts',(-90.4891219169303,4.46535970364301,
134.689363918773));
#172782=CARTESIAN_POINT('Ctrl Pts',(-90.4817136972638,4.3589627757391,134.805282271663));
#172783=CARTESIAN_POINT('Ctrl Pts',(-90.4743009179617,4.2525003623014,134.921271970365));
#172784=CARTESIAN_POINT('Ctrl Pts',(-90.4668881386597,4.14150049318447,
135.032905511779));
#172785=CARTESIAN_POINT('Ctrl Pts',(-90.4594753593577,4.0263692977088,135.139828394054));
#172786=CARTESIAN_POINT('Ctrl Pts',(-90.4520519883289,3.91107359738209,
135.246904052757));
#172787=CARTESIAN_POINT('Ctrl Pts',(-90.4446286173001,3.79163506372278,
135.34925536712));
#172788=CARTESIAN_POINT('Ctrl Pts',(-90.4372052462713,3.66849186019001,
135.446568931959));
#172789=CARTESIAN_POINT('Ctrl Pts',(-90.4332691968306,3.60319837889668,
135.498166919043));
#172790=CARTESIAN_POINT('Ctrl Pts',(-90.4293331473898,3.53686385819526,
135.548349343547));
#172791=CARTESIAN_POINT('Ctrl Pts',(-90.425397097949,3.46955659495388,135.597074629158));
#172792=CARTESIAN_POINT('Ctrl Pts',(-90.4179738315436,3.34261719706789,
135.688968997157));
#172793=CARTESIAN_POINT('Ctrl Pts',(-90.4105505651382,3.2118324713806,135.775955678257));
#172794=CARTESIAN_POINT('Ctrl Pts',(-90.4031272987328,3.07761878148282,
135.857695476683));
#172795=CARTESIAN_POINT('Ctrl Pts',(-90.3957128060118,2.94356372102037,
135.939338665455));
#172796=CARTESIAN_POINT('Ctrl Pts',(-90.3882983132907,2.80608807908072,
136.015747123157));
#172797=CARTESIAN_POINT('Ctrl Pts',(-90.3808838205697,2.66563991858251,
136.08662285897));
#172798=CARTESIAN_POINT('Ctrl Pts',(-90.3734764742159,2.52532712730916,
136.15743028208));
#172799=CARTESIAN_POINT('Ctrl Pts',(-90.3660691278622,2.38204785220827,
136.222715432498));
#172800=CARTESIAN_POINT('Ctrl Pts',(-90.3586617815084,2.23627757375913,
136.28222454209));
#172801=CARTESIAN_POINT('Ctrl Pts',(-90.351259959833,2.09061601628326,136.341689267543));
#172802=CARTESIAN_POINT('Ctrl Pts',(-90.3438581381575,1.94246749887782,
136.395386389476));
#172803=CARTESIAN_POINT('Ctrl Pts',(-90.336456316482,1.79233035016364,136.443108925336));
#172804=CARTESIAN_POINT('Ctrl Pts',(-90.3290584021707,1.64227245768204,
136.490806268842));
#172805=CARTESIAN_POINT('Ctrl Pts',(-90.3216604878594,1.49022837944259,
136.532535194698));
#172806=CARTESIAN_POINT('Ctrl Pts',(-90.314262573548,1.33671448373252,136.568137586835));
#172807=CARTESIAN_POINT('Ctrl Pts',(-90.3068658886358,1.18322609924668,
136.603734062501));
#172808=CARTESIAN_POINT('Ctrl Pts',(-90.2994692037237,1.02826874535859,
136.633205940858));
#172809=CARTESIAN_POINT('Ctrl Pts',(-90.2920725188115,0.87237206280302,
136.656445506436));
#172810=CARTESIAN_POINT('Ctrl Pts',(-90.284676161876,0.716482292869719,
136.679684041548));
#172811=CARTESIAN_POINT('Ctrl Pts',(-90.2772798049405,0.559653646302565,
136.696690758313));
#172812=CARTESIAN_POINT('Ctrl Pts',(-90.2698834480051,0.402423756565,136.707409463938));
#172813=CARTESIAN_POINT('Ctrl Pts',(-90.2624859586685,0.245169794529927,
136.718129810624));
#172814=CARTESIAN_POINT('Ctrl Pts',(-90.255088469332,0.0875148394638481,
136.722560203893));
#172815=CARTESIAN_POINT('Ctrl Pts',(-90.2476909799954,-0.0700007308546633,
136.720696515753));
#172816=CARTESIAN_POINT('Ctrl Pts',(-90.2402908974804,-0.227571518012394,
136.718832174301));
#172817=CARTESIAN_POINT('Ctrl Pts',(-90.2328908149653,-0.385002450101525,
136.710669362966));
#172818=CARTESIAN_POINT('Ctrl Pts',(-90.2254907324503,-0.541755681001532,
136.696256012479));
#172819=CARTESIAN_POINT('Ctrl Pts',(-90.2180825127839,-0.698681278193312,
136.681826813033));
#172820=CARTESIAN_POINT('Ctrl Pts',(-90.2106742931175,-0.854927314020519,
136.661133382583));
#172821=CARTESIAN_POINT('Ctrl Pts',(-90.203266073451,-1.00996284570659,
136.63427533502));
#172822=CARTESIAN_POINT('Ctrl Pts',(-90.1958532941489,-1.16509379917596,
136.607400756778));
#172823=CARTESIAN_POINT('Ctrl Pts',(-90.1884405148468,-1.31901239977424,
136.574354079145));
#172824=CARTESIAN_POINT('Ctrl Pts',(-90.1810277355448,-1.47120087223584,
136.535285373313));
#172825=CARTESIAN_POINT('Ctrl Pts',(-90.173604364516,-1.62360679872362,
136.496160844282));
#172826=CARTESIAN_POINT('Ctrl Pts',(-90.1661809934872,-1.7742773031283,
136.450997208722));
#172827=CARTESIAN_POINT('Ctrl Pts',(-90.1587576224584,-1.92271187073998,
136.399993702804));
#172828=CARTESIAN_POINT('Ctrl Pts',(-90.1548215730176,-2.00141544012667,
136.372950420155));
#172829=CARTESIAN_POINT('Ctrl Pts',(-90.1508855235768,-2.07949076385258,
136.344266135415));
#172830=CARTESIAN_POINT('Ctrl Pts',(-90.146949474136,-2.15686594646315,
136.313975835663));
#172831=CARTESIAN_POINT('Ctrl Pts',(-90.1395262077306,-2.30279312606935,
136.256849275659));
#172832=CARTESIAN_POINT('Ctrl Pts',(-90.1321029413251,-2.4466698232985,
136.193834807825));
#172833=CARTESIAN_POINT('Ctrl Pts',(-90.1246796749197,-2.58798560844716,
136.125099387039));
#172834=CARTESIAN_POINT('Ctrl Pts',(-90.1172651821987,-2.72913437007332,
136.056445205812));
#172835=CARTESIAN_POINT('Ctrl Pts',(-90.1098506894776,-2.86772791203561,
135.982083692504));
#172836=CARTESIAN_POINT('Ctrl Pts',(-90.1024361967566,-3.00327333726637,
135.902230743821));
#172837=CARTESIAN_POINT('Ctrl Pts',(-90.0950288504028,-3.13868811871309,
135.822454760417));
#172838=CARTESIAN_POINT('Ctrl Pts',(-90.0876215040491,-3.27106031271403,
135.737198066874));
#172839=CARTESIAN_POINT('Ctrl Pts',(-90.0802141576953,-3.39991940813838,
135.646723530511));
#172840=CARTESIAN_POINT('Ctrl Pts',(-90.0728123360199,-3.52868239558817,
135.556316473471));
#172841=CARTESIAN_POINT('Ctrl Pts',(-90.0654105143445,-3.65393719743797,
135.460699536022));
#172842=CARTESIAN_POINT('Ctrl Pts',(-90.0580086926691,-3.77524031461416,
135.360180097024));
#172843=CARTESIAN_POINT('Ctrl Pts',(-90.0506107783577,-3.89647939681867,
135.259713721456));
#172844=CARTESIAN_POINT('Ctrl Pts',(-90.0432128640463,-4.0137706621383,
135.154350236032));
#172845=CARTESIAN_POINT('Ctrl Pts',(-90.0358149497349,-4.12670197337219,
135.044438610418));
#172846=CARTESIAN_POINT('Ctrl Pts',(-90.0284182648227,-4.2396145174711,
134.934545250122));
#172847=CARTESIAN_POINT('Ctrl Pts',(-90.0210215799105,-4.34816827824035,
134.820105509818));
#172848=CARTESIAN_POINT('Ctrl Pts',(-90.0136248949983,-4.45198634784982,
134.701506768413));
#172849=CARTESIAN_POINT('Ctrl Pts',(-90.0062285380629,-4.5557998140573,
134.5829132858));
#172850=CARTESIAN_POINT('Ctrl Pts',(-89.9988321811274,-4.65487776074972,
134.460161449648));
#172851=CARTESIAN_POINT('Ctrl Pts',(-89.9914358241919,-4.74888230731818,
134.333673212639));
#172852=CARTESIAN_POINT('Ctrl Pts',(-89.9840383348553,-4.8429012462227,
134.207165609957));
#172853=CARTESIAN_POINT('Ctrl Pts',(-89.9766408455187,-4.93184501570499,
134.07692076702));
#172854=CARTESIAN_POINT('Ctrl Pts',(-89.9692433561821,-5.01541805537971,
133.943391087675));
#172855=CARTESIAN_POINT('Ctrl Pts',(-89.9618432736671,-5.09902039145382,
133.809814599708));
#172856=CARTESIAN_POINT('Ctrl Pts',(-89.9544431911521,-5.1772480513532,
133.672951298951));
#172857=CARTESIAN_POINT('Ctrl Pts',(-89.9470431086371,-5.2498506415936,
133.533279598309));
#172858=CARTESIAN_POINT('Ctrl Pts',(-89.9396348889706,-5.32253306584581,
133.393454314273));
#172859=CARTESIAN_POINT('Ctrl Pts',(-89.9322266693041,-5.3895778956264,
133.25081479459));
#172860=CARTESIAN_POINT('Ctrl Pts',(-89.9248184496376,-5.45078195138222,
133.105861580196));
#172861=CARTESIAN_POINT('Ctrl Pts',(-89.9174056703355,-5.51202367721328,
132.960819149516));
#172862=CARTESIAN_POINT('Ctrl Pts',(-89.9099928910334,-5.56741733468471,
132.81346053516));
#172863=CARTESIAN_POINT('Ctrl Pts',(-89.9025801117313,-5.61680931276014,
132.664302473268));
#172864=CARTESIAN_POINT('Ctrl Pts',(-89.8951567407025,-5.66627186441004,
132.514931287341));
#172865=CARTESIAN_POINT('Ctrl Pts',(-89.8877333696738,-5.70971550667538,
132.363755876572));
#172866=CARTESIAN_POINT('Ctrl Pts',(-89.880309998645,-5.74703732216239,
132.211305030175));
#172867=CARTESIAN_POINT('Ctrl Pts',(-89.8763739492043,-5.76682624425736,
132.130471933412));
#172868=CARTESIAN_POINT('Ctrl Pts',(-89.8724378997637,-5.78489496269358,
132.049280395803));
#172869=CARTESIAN_POINT('Ctrl Pts',(-89.8685018503231,-5.80123405184049,
131.9678098164));
#172870=CARTESIAN_POINT('Ctrl Pts',(-89.8577895132931,-5.84570245406606,
131.746079800615));
#172871=CARTESIAN_POINT('Ctrl Pts',(-89.847077176263,-5.87746997319479,
131.521724546966));
#172872=CARTESIAN_POINT('Ctrl Pts',(-89.836364839233,-5.89629390879888,
131.295938387162));
#172873=CARTESIAN_POINT('Ctrl Pts',(-89.8287016235569,-5.90975986660081,
131.134419193508));
#172874=CARTESIAN_POINT('Ctrl Pts',(-89.8210384078808,-5.91660286006169,
130.972168001611));
#172875=CARTESIAN_POINT('Ctrl Pts',(-89.8133751922047,-5.91674765230671,
130.809631426141));
#172876=CARTESIAN_POINT('',(-88.0633751922046,-5.90698262932298,130.80492291423));
#172877=CARTESIAN_POINT('Ctrl Pts',(-89.8133742249814,-5.91883747551114,
130.809612765774));
#172878=CARTESIAN_POINT('Ctrl Pts',(-89.7389342254909,-5.90421827380185,
129.230170522338));
#172879=CARTESIAN_POINT('Ctrl Pts',(-89.5716783513963,-4.43993236803427,
125.657485558116));
#172880=CARTESIAN_POINT('Ctrl Pts',(-89.3116066026975,1.60058328561251,
123.991454213087));
#172881=CARTESIAN_POINT('Ctrl Pts',(-89.0331589788845,6.59704547191749,
128.468434340518));
#172882=CARTESIAN_POINT('Ctrl Pts',(-88.7547113550716,5.5311451531159,135.092016600209));
#172883=CARTESIAN_POINT('Ctrl Pts',(-88.4762637312587,-0.617607349934246,
137.775452475492));
#172884=CARTESIAN_POINT('Ctrl Pts',(-88.2458183436364,-5.23665250507847,
134.694553022179));
#172885=CARTESIAN_POINT('Ctrl Pts',(-88.1081888306183,-5.9077896589492,
131.760598074561));
#172886=CARTESIAN_POINT('Ctrl Pts',(-88.0633751922046,-5.90698262932298,
130.80492291423));
#172887=CARTESIAN_POINT('',(-86.3133751922044,-5.91676703712452,130.798896138361));
#172888=CARTESIAN_POINT('Ctrl Pts',(-88.0633751922046,-5.90698262932298,
130.80492291423));
#172889=CARTESIAN_POINT('Ctrl Pts',(-88.015372956014,-5.90611817760466,
129.781249175799));
#172890=CARTESIAN_POINT('Ctrl Pts',(-87.8745548452193,-5.16532046994545,
126.777054825752));
#172891=CARTESIAN_POINT('Ctrl Pts',(-87.6409208598199,-0.377868435225309,
123.81617229898));
#172892=CARTESIAN_POINT('Ctrl Pts',(-87.3624732360072,5.67511362901596,
126.709162719037));
#172893=CARTESIAN_POINT('Ctrl Pts',(-87.0840256121942,6.51294351290233,
133.365439946302));
#172894=CARTESIAN_POINT('Ctrl Pts',(-86.8055779883815,1.36569648341219,
137.668210386139));
#172895=CARTESIAN_POINT('Ctrl Pts',(-86.5486945150514,-4.54074141890726,
135.818696162511));
#172896=CARTESIAN_POINT('Ctrl Pts',(-86.3846269163258,-5.90276582907417,
132.312047574845));
#172897=CARTESIAN_POINT('Ctrl Pts',(-86.3133751922044,-5.91676703712452,
130.798896138361));
#172898=CARTESIAN_POINT('',(-84.5633751922045,-5.92580168545033,130.806256469132));
#172899=CARTESIAN_POINT('Ctrl Pts',(-86.3133751922044,-5.91676703712452,
130.798896138361));
#172900=CARTESIAN_POINT('Ctrl Pts',(-86.2918110417214,-5.92100446661924,
130.340944759889));
#172901=CARTESIAN_POINT('Ctrl Pts',(-86.1774310166342,-5.66290769290208,
127.916615574322));
#172902=CARTESIAN_POINT('Ctrl Pts',(-85.9702351169427,-2.3258839918925,
124.203767902776));
#172903=CARTESIAN_POINT('Ctrl Pts',(-85.6917874931298,4.29606847896242,
125.279746951938));
#172904=CARTESIAN_POINT('Ctrl Pts',(-85.4133398693169,6.97014389226581,
131.432576067439));
#172905=CARTESIAN_POINT('Ctrl Pts',(-85.134892245504,3.23899757903464,137.008105874533));
#172906=CARTESIAN_POINT('Ctrl Pts',(-84.8564446216911,-3.46862927549987,
136.88269686028));
#172907=CARTESIAN_POINT('Ctrl Pts',(-84.6659389372578,-5.87699607777005,
132.975327905718));
#172908=CARTESIAN_POINT('Ctrl Pts',(-84.5682491274291,-5.92623241459706,
130.909352943666));
#172909=CARTESIAN_POINT('Ctrl Pts',(-84.5633751922045,-5.92580168545033,
130.806256469132));
#172910=CARTESIAN_POINT('',(-82.813376411914,-5.91339316048575,130.808932093645));
#172911=CARTESIAN_POINT('Ctrl Pts',(-84.5633751922045,-5.92580168545033,
130.806256469132));
#172912=CARTESIAN_POINT('Ctrl Pts',(-84.4754332528247,-5.91802990458645,
128.946054497649));
#172913=CARTESIAN_POINT('Ctrl Pts',(-84.2946754388405,-3.9700232261154,
125.108533355109));
#172914=CARTESIAN_POINT('Ctrl Pts',(-84.0211017502524,2.57098795437597,
124.295322173311));
#172915=CARTESIAN_POINT('Ctrl Pts',(-83.7426541264397,6.86592017791128,
129.449111326519));
#172916=CARTESIAN_POINT('Ctrl Pts',(-83.4642065026265,4.85140717679743,
135.848308370593));
#172917=CARTESIAN_POINT('Ctrl Pts',(-83.1857588788137,-1.62131201537933,
137.612363840181));
#172918=CARTESIAN_POINT('Ctrl Pts',(-82.9688158071183,-5.50350238343903,
134.112443556921));
#172919=CARTESIAN_POINT('Ctrl Pts',(-82.8446886100276,-5.91572502166291,
131.475548415697));
#172920=CARTESIAN_POINT('Ctrl Pts',(-82.8133772875409,-5.91098454745023,
130.808948883669));
#172921=CARTESIAN_POINT('',(-81.0633739991884,-5.91254220191759,130.800666021097));
#172922=CARTESIAN_POINT('Ctrl Pts',(-82.8133751922044,-5.91674825198712,
130.808908705884));
#172923=CARTESIAN_POINT('Ctrl Pts',(-82.8056872104954,-5.91687418582307,
130.645077497767));
#172924=CARTESIAN_POINT('Ctrl Pts',(-82.7979992287864,-5.91019052118769,
130.48117042425));
#172925=CARTESIAN_POINT('Ctrl Pts',(-82.7903112470773,-5.89670961218577,
130.317794782292));
#172926=CARTESIAN_POINT('Ctrl Pts',(-82.7829152084456,-5.88374062662591,
130.160623159734));
#172927=CARTESIAN_POINT('Ctrl Pts',(-82.7755191698139,-5.86448120197058,
130.003943747025));
#172928=CARTESIAN_POINT('Ctrl Pts',(-82.7681231311822,-5.83899539068648,
129.848293993296));
#172929=CARTESIAN_POINT('Ctrl Pts',(-82.7607265983148,-5.81350787632902,
129.692633838371));
#172930=CARTESIAN_POINT('Ctrl Pts',(-82.7533300654475,-5.78179320650162,
129.538003847396));
#172931=CARTESIAN_POINT('Ctrl Pts',(-82.7459335325802,-5.74396684664459,
129.384932765526));
#172932=CARTESIAN_POINT('Ctrl Pts',(-82.7385350509601,-5.70613052073683,
129.231821354262));
#172933=CARTESIAN_POINT('Ctrl Pts',(-82.73113656934,-5.66217938781907,129.080270031722));
#172934=CARTESIAN_POINT('Ctrl Pts',(-82.7237380877199,-5.61227917682799,
128.930793697533));
#172935=CARTESIAN_POINT('Ctrl Pts',(-82.71633620194,-5.56235600595053,128.781248586888));
#172936=CARTESIAN_POINT('Ctrl Pts',(-82.70893431616,-5.50647842441477,128.633780718771));
#172937=CARTESIAN_POINT('Ctrl Pts',(-82.70153243038,-5.44486074827377,128.488886153356));
#172938=CARTESIAN_POINT('Ctrl Pts',(-82.6941216520159,-5.38316904500114,
128.343817512421));
#172939=CARTESIAN_POINT('Ctrl Pts',(-82.6867108736518,-5.31572362347877,
128.201328689992));
#172940=CARTESIAN_POINT('Ctrl Pts',(-82.6793000952876,-5.24278564009095,
128.061892879459));
#172941=CARTESIAN_POINT('Ctrl Pts',(-82.6718840542683,-5.16979586086856,
127.922358050639));
#172942=CARTESIAN_POINT('Ctrl Pts',(-82.664468013249,-5.09130593352807,
127.785880875214));
#172943=CARTESIAN_POINT('Ctrl Pts',(-82.6570519722298,-5.00762070700942,
127.652906125235));
#172944=CARTESIAN_POINT('Ctrl Pts',(-82.6496253628503,-4.92381622338038,
127.519741877241));
#172945=CARTESIAN_POINT('Ctrl Pts',(-82.6421987534708,-4.83480186949621,
127.390090325031));
#172946=CARTESIAN_POINT('Ctrl Pts',(-82.6347721440912,-4.74092356084927,
127.26436424007));
#172947=CARTESIAN_POINT('Ctrl Pts',(-82.6328026397902,-4.71602744430311,
127.231022232644));
#172948=CARTESIAN_POINT('Ctrl Pts',(-82.6308331354891,-4.69078945681863,
127.197956101158));
#172949=CARTESIAN_POINT('Ctrl Pts',(-82.6288636311881,-4.6652164826873,
127.165173107673));
#172950=CARTESIAN_POINT('Ctrl Pts',(-82.6214403647826,-4.56882928533186,
127.041610598019));
#172951=CARTESIAN_POINT('Ctrl Pts',(-82.6140170983771,-4.46738395023727,
126.92169324669));
#172952=CARTESIAN_POINT('Ctrl Pts',(-82.6065938319717,-4.36118612570389,
126.805862632138));
#172953=CARTESIAN_POINT('Ctrl Pts',(-82.5991793392506,-4.25511381817993,
126.690168919754));
#172954=CARTESIAN_POINT('Ctrl Pts',(-82.5917648465296,-4.1443004517905,
126.578552602109));
#172955=CARTESIAN_POINT('Ctrl Pts',(-82.5843503538085,-4.0290935800243,
126.471424489961));
#172956=CARTESIAN_POINT('Ctrl Pts',(-82.5769430074547,-3.91399774897824,
126.36439963192));
#172957=CARTESIAN_POINT('Ctrl Pts',(-82.5695356611009,-3.79451711439902,
126.261854619855));
#172958=CARTESIAN_POINT('Ctrl Pts',(-82.5621283147471,-3.67103786096599,
126.164165407679));
#172959=CARTESIAN_POINT('Ctrl Pts',(-82.5547264930717,-3.54765070301914,
126.066549055804));
#172960=CARTESIAN_POINT('Ctrl Pts',(-82.5473246713962,-3.42027115591953,
125.973781523261));
#172961=CARTESIAN_POINT('Ctrl Pts',(-82.5399228497208,-3.28932035877788,
125.886200174897));
#172962=CARTESIAN_POINT('Ctrl Pts',(-82.5325249354094,-3.15843868954236,
125.798665060046));
#172963=CARTESIAN_POINT('Ctrl Pts',(-82.5251270210979,-3.02398983431051,
125.716310884025));
#172964=CARTESIAN_POINT('Ctrl Pts',(-82.5177291067865,-2.88642584623075,
125.639433086931));
#172965=CARTESIAN_POINT('Ctrl Pts',(-82.5103324218743,-2.74888471878994,
125.562568065532));
#172966=CARTESIAN_POINT('Ctrl Pts',(-82.502935736962,-2.60822981148502,
125.491177798763));
#172967=CARTESIAN_POINT('Ctrl Pts',(-82.4955390520497,-2.46493993872728,
125.425513002977));
#172968=CARTESIAN_POINT('Ctrl Pts',(-82.4881426951142,-2.32165641959307,
125.359851118837));
#172969=CARTESIAN_POINT('Ctrl Pts',(-82.4807463381788,-2.17573850667814,
125.299914356412));
#172970=CARTESIAN_POINT('Ctrl Pts',(-82.4733499812433,-2.02768701603159,
125.245906162637));
#172971=CARTESIAN_POINT('Ctrl Pts',(-82.4659524919067,-1.87961285832387,
125.191889700071));
#172972=CARTESIAN_POINT('Ctrl Pts',(-82.4585550025701,-1.72940482318353,
125.143803741403));
#172973=CARTESIAN_POINT('Ctrl Pts',(-82.4511575132335,-1.57758083751009,
125.10180248427));
#172974=CARTESIAN_POINT('Ctrl Pts',(-82.4437574307184,-1.42570363017317,
125.059786503661));
#172975=CARTESIAN_POINT('Ctrl Pts',(-82.4363573482033,-1.27220970402733,
125.02385957081));
#172976=CARTESIAN_POINT('Ctrl Pts',(-82.4289572656882,-1.11762902715309,
124.994125173097));
#172977=CARTESIAN_POINT('Ctrl Pts',(-82.4215490460217,-0.962878372933568,
124.964358079357));
#172978=CARTESIAN_POINT('Ctrl Pts',(-82.4141408263552,-0.807038948306534,
124.940797189989));
#172979=CARTESIAN_POINT('Ctrl Pts',(-82.4067326066886,-0.650648458779961,
124.923494427489));
#172980=CARTESIAN_POINT('Ctrl Pts',(-82.3993198273866,-0.494161713517491,
124.906181015428));
#172981=CARTESIAN_POINT('Ctrl Pts',(-82.3919070480845,-0.337123599028448,
124.895133431512));
#172982=CARTESIAN_POINT('Ctrl Pts',(-82.3844942687825,-0.180073200227318,
124.89035146936));
#172983=CARTESIAN_POINT('Ctrl Pts',(-82.3770708977537,-0.0227984004507772,
124.885562674517));
#172984=CARTESIAN_POINT('Ctrl Pts',(-82.3696475267249,0.134488346401762,
124.88705737828));
#172985=CARTESIAN_POINT('Ctrl Pts',(-82.3622241556961,0.291250866976861,
124.894783348845));
#172986=CARTESIAN_POINT('Ctrl Pts',(-82.3582881062558,0.374370116840544,
124.89887984382));
#172987=CARTESIAN_POINT('Ctrl Pts',(-82.3543520568154,0.457342109213834,
124.904727308725));
#172988=CARTESIAN_POINT('Ctrl Pts',(-82.3504160073751,0.540088056083287,
124.912312123691));
#172989=CARTESIAN_POINT('Ctrl Pts',(-82.3429927409696,0.696144329485136,
124.926616848003));
#172990=CARTESIAN_POINT('Ctrl Pts',(-82.3355694745642,0.851867874952232,
124.947147423962));
#172991=CARTESIAN_POINT('Ctrl Pts',(-82.3281462081587,1.00672196965357,
124.973885384936));
#172992=CARTESIAN_POINT('Ctrl Pts',(-82.3207317154377,1.16139303967481,
125.00059174386));
#172993=CARTESIAN_POINT('Ctrl Pts',(-82.3133172227167,1.31519634014826,
125.033490821333));
#172994=CARTESIAN_POINT('Ctrl Pts',(-82.3059027299957,1.46759838319741,
125.072512264012));
#172995=CARTESIAN_POINT('Ctrl Pts',(-82.2984953836419,1.61985353541964,
125.111496096356));
#172996=CARTESIAN_POINT('Ctrl Pts',(-82.2910880372882,1.77070975976131,
125.156590454272));
#172997=CARTESIAN_POINT('Ctrl Pts',(-82.2836806909344,1.91964201329523,
125.207673641927));
#172998=CARTESIAN_POINT('Ctrl Pts',(-82.276278869259,2.06846318753557,125.258718729812));
#172999=CARTESIAN_POINT('Ctrl Pts',(-82.2688770475836,2.21536289660225,
125.315743633051));
#173000=CARTESIAN_POINT('Ctrl Pts',(-82.2614752259082,2.35982966991864,
125.378576389321));
#173001=CARTESIAN_POINT('Ctrl Pts',(-82.2540773115968,2.50422018034952,
125.441375976668));
#173002=CARTESIAN_POINT('Ctrl Pts',(-82.2466793972855,2.64617997137505,
125.509977162612));
#173003=CARTESIAN_POINT('Ctrl Pts',(-82.2392814829741,2.78521613510553,
125.584159314623));
#173004=CARTESIAN_POINT('Ctrl Pts',(-82.2318847980619,2.92422919354856,
125.658329138907));
#173005=CARTESIAN_POINT('Ctrl Pts',(-82.2244881131497,3.06031925994357,
125.738077912983));
#173006=CARTESIAN_POINT('Ctrl Pts',(-82.2170914282374,3.19301658863656,
125.823138315039));
#173007=CARTESIAN_POINT('Ctrl Pts',(-82.209695071302,3.32570803339095,125.908194945428));
#173008=CARTESIAN_POINT('Ctrl Pts',(-82.2022987143665,3.45500672529041,
125.998562534045));
#173009=CARTESIAN_POINT('Ctrl Pts',(-82.1949023574311,3.58047079535733,
126.093929698203));
#173010=CARTESIAN_POINT('Ctrl Pts',(-82.1875048680945,3.70595407429368,
126.189311463317));
#173011=CARTESIAN_POINT('Ctrl Pts',(-82.1801073787579,3.82760126521419,
126.289694102168));
#173012=CARTESIAN_POINT('Ctrl Pts',(-82.1727098894213,3.94500268514106,
126.394725215775));
#173013=CARTESIAN_POINT('Ctrl Pts',(-82.1653098069063,4.06244525995419,
126.499793147876));
#173014=CARTESIAN_POINT('Ctrl Pts',(-82.1579097243912,4.17563882244492,
126.609512550346));
#173015=CARTESIAN_POINT('Ctrl Pts',(-82.1505096418762,4.28420984505616,
126.723493483485));
#173016=CARTESIAN_POINT('Ctrl Pts',(-82.1431014222097,4.39290025266797,
126.837599750377));
#173017=CARTESIAN_POINT('Ctrl Pts',(-82.1356932025431,4.49695771177296,
126.955976635707));
#173018=CARTESIAN_POINT('Ctrl Pts',(-82.1282849828766,4.59604789554275,
127.078199817979));
#173019=CARTESIAN_POINT('Ctrl Pts',(-82.1208722035745,4.69519906766723,
127.200498226581));
#173020=CARTESIAN_POINT('Ctrl Pts',(-82.1134594242724,4.78937664965125,
127.326647350892));
#173021=CARTESIAN_POINT('Ctrl Pts',(-82.1060466449703,4.8782894265632,127.456193531953));
#173022=CARTESIAN_POINT('Ctrl Pts',(-82.0986232739415,4.96732924622026,
127.585924814673));
#173023=CARTESIAN_POINT('Ctrl Pts',(-82.0911999029128,5.05108903822848,
127.719062533285));
#173024=CARTESIAN_POINT('Ctrl Pts',(-82.083776531884,5.12932293189013,127.855127357397));
#173025=CARTESIAN_POINT('Ctrl Pts',(-82.0798404824434,5.17080441950393,
127.927272191968));
#173026=CARTESIAN_POINT('Ctrl Pts',(-82.0759044330027,5.21073317025427,
128.00023957666));
#173027=CARTESIAN_POINT('Ctrl Pts',(-82.0719683835621,5.24907805607844,
128.073955863011));
#173028=CARTESIAN_POINT('Ctrl Pts',(-82.0645451171567,5.32139531404309,
128.21298247847));
#173029=CARTESIAN_POINT('Ctrl Pts',(-82.0571218507514,5.38829473911661,
128.355094385383));
#173030=CARTESIAN_POINT('Ctrl Pts',(-82.0496985843459,5.44950175599861,
128.499830041968));
#173031=CARTESIAN_POINT('Ctrl Pts',(-82.042284091625,5.51063643126958,128.644394633025));
#173032=CARTESIAN_POINT('Ctrl Pts',(-82.0348695989041,5.56609194640114,
128.791576460628));
#173033=CARTESIAN_POINT('Ctrl Pts',(-82.0274551061831,5.61563912842514,
128.940888658614));
#173034=CARTESIAN_POINT('Ctrl Pts',(-82.0200477598293,5.66513855500982,
129.090056943883));
#173035=CARTESIAN_POINT('Ctrl Pts',(-82.0126404134756,5.70874086868112,
129.241351159836));
#173036=CARTESIAN_POINT('Ctrl Pts',(-82.0052330671218,5.74626465706431,
129.394263793418));
#173037=CARTESIAN_POINT('Ctrl Pts',(-81.9978312454464,5.78376045879044,
129.547062378988));
#173038=CARTESIAN_POINT('Ctrl Pts',(-81.9904294237709,5.81518667364236,
129.701476617752));
#173039=CARTESIAN_POINT('Ctrl Pts',(-81.9830276020955,5.84041151605071,
129.856983245194));
#173040=CARTESIAN_POINT('Ctrl Pts',(-81.9756296877842,5.86562304246124,
130.012407781899));
#173041=CARTESIAN_POINT('Ctrl Pts',(-81.9682317734728,5.88463965645102,
130.168923191279));
#173042=CARTESIAN_POINT('Ctrl Pts',(-81.9608338591614,5.89738055365975,
130.325995518697));
#173043=CARTESIAN_POINT('Ctrl Pts',(-81.9534371742492,5.91011933356242,
130.483041743543));
#173044=CARTESIAN_POINT('Ctrl Pts',(-81.9460404893371,5.91658443640106,
130.640644331031));
#173045=CARTESIAN_POINT('Ctrl Pts',(-81.9386438044249,5.91674685858663,
130.798263576871));
#173046=CARTESIAN_POINT('Ctrl Pts',(-81.9312474474895,5.91690927357023,
130.955875833708));
#173047=CARTESIAN_POINT('Ctrl Pts',(-81.9238510905539,5.91076956319177,
131.113504374131));
#173048=CARTESIAN_POINT('Ctrl Pts',(-81.9164547336185,5.89835086154906,
131.270609131305));
#173049=CARTESIAN_POINT('Ctrl Pts',(-81.9090572442819,5.8859302585715,131.427737941617));
#173050=CARTESIAN_POINT('Ctrl Pts',(-81.9016597549455,5.86722877961298,
131.584342436846));
#173051=CARTESIAN_POINT('Ctrl Pts',(-81.8942622656089,5.84232146425987,
131.739887458842));
#173052=CARTESIAN_POINT('Ctrl Pts',(-81.8868621830939,5.81740541768579,
131.895487006906));
#173053=CARTESIAN_POINT('Ctrl Pts',(-81.879462100579,5.78627926240652,132.050025973917));
#173054=CARTESIAN_POINT('Ctrl Pts',(-81.872062018064,5.74906916496555,132.202979328631));
#173055=CARTESIAN_POINT('Ctrl Pts',(-81.8646537983976,5.7118181511972,132.356100871283));
#173056=CARTESIAN_POINT('Ctrl Pts',(-81.857245578731,5.66846992335339,132.507632956724));
#173057=CARTESIAN_POINT('Ctrl Pts',(-81.8498373590646,5.61920076330784,
132.657064950195));
#173058=CARTESIAN_POINT('Ctrl Pts',(-81.8424245797625,5.56990127891637,
132.806588916563));
#173059=CARTESIAN_POINT('Ctrl Pts',(-81.8350118004604,5.51467373138314,
132.954009866587));
#173060=CARTESIAN_POINT('Ctrl Pts',(-81.8275990211583,5.45374238805491,
133.098837579149));
#173061=CARTESIAN_POINT('Ctrl Pts',(-81.8201756501296,5.39272398316602,
133.243872228337));
#173062=CARTESIAN_POINT('Ctrl Pts',(-81.812752279101,5.32598566336909,133.386305902533));
#173063=CARTESIAN_POINT('Ctrl Pts',(-81.8053289080722,5.25379780378184,
133.52567265397));
#173064=CARTESIAN_POINT('Ctrl Pts',(-81.8013928586312,5.21552206850281,
133.599568249645));
#173065=CARTESIAN_POINT('Ctrl Pts',(-81.7974568091902,5.17571500630908,
133.672602092252));
#173066=CARTESIAN_POINT('Ctrl Pts',(-81.7935207597492,5.13442175425764,
133.74470818408));
#173067=CARTESIAN_POINT('Ctrl Pts',(-81.7860974933438,5.05654396961077,
133.880698022907));
#173068=CARTESIAN_POINT('Ctrl Pts',(-81.7786742269383,4.9731419708674,134.013797360875));
#173069=CARTESIAN_POINT('Ctrl Pts',(-81.7712509605329,4.88445565154512,
134.143525715399));
#173070=CARTESIAN_POINT('Ctrl Pts',(-81.7638364678119,4.79587415208708,
134.273100741783));
#173071=CARTESIAN_POINT('Ctrl Pts',(-81.756421975091,4.70202097262363,134.39931241018));
#173072=CARTESIAN_POINT('Ctrl Pts',(-81.74900748237,4.60318185385699,134.521704747832));
#173073=CARTESIAN_POINT('Ctrl Pts',(-81.7416001360162,4.50443799995396,
134.643979119141));
#173074=CARTESIAN_POINT('Ctrl Pts',(-81.7341927896623,4.40071800678207,
134.762441199804));
#173075=CARTESIAN_POINT('Ctrl Pts',(-81.7267854433085,4.29235080162894,
134.87666403925));
#173076=CARTESIAN_POINT('Ctrl Pts',(-81.7193836216332,4.18406442082649,
134.990801686992));
#173077=CARTESIAN_POINT('Ctrl Pts',(-81.7119817999577,4.07113798527085,
135.100706119413));
#173078=CARTESIAN_POINT('Ctrl Pts',(-81.7045799782824,3.9539404989001,135.205983624328));
#173079=CARTESIAN_POINT('Ctrl Pts',(-81.6971820639711,3.83680488017047,
135.311205554068));
#173080=CARTESIAN_POINT('Ctrl Pts',(-81.6897841496598,3.71540297788113,
135.411805171867));
#173081=CARTESIAN_POINT('Ctrl Pts',(-81.6823862353485,3.59014034646083,
135.507425879203));
#173082=CARTESIAN_POINT('Ctrl Pts',(-81.6749895504363,3.46489853141684,
135.603030696113));
#173083=CARTESIAN_POINT('Ctrl Pts',(-81.6675928655241,3.33579755702844,
135.693658018427));
#173084=CARTESIAN_POINT('Ctrl Pts',(-81.6601961806119,3.20327581465295,
135.778991721252));
#173085=CARTESIAN_POINT('Ctrl Pts',(-81.6527998236765,3.07075994843001,
135.864321640292));
#173086=CARTESIAN_POINT('Ctrl Pts',(-81.645403466741,2.93482392966964,135.944358204454));
#173087=CARTESIAN_POINT('Ctrl Pts',(-81.6380071098055,2.79593463643932,
136.018828957796));
#173088=CARTESIAN_POINT('Ctrl Pts',(-81.630609620469,2.65702407890404,136.0933111128));
#173089=CARTESIAN_POINT('Ctrl Pts',(-81.6232121311324,2.51515967561123,
136.162225583847));
#173090=CARTESIAN_POINT('Ctrl Pts',(-81.6158146417959,2.37083223099745,
136.225346237817));
#173091=CARTESIAN_POINT('Ctrl Pts',(-81.6084145592809,2.22645419262149,
136.288489018633));
#173092=CARTESIAN_POINT('Ctrl Pts',(-81.6010144767658,2.0796117356769,136.345833789152));
#173093=CARTESIAN_POINT('Ctrl Pts',(-81.5936143942508,1.93081477991784,
136.397202904646));
#173094=CARTESIAN_POINT('Ctrl Pts',(-81.5862061745844,1.78185420660943,
136.448628505764));
#173095=CARTESIAN_POINT('Ctrl Pts',(-81.578797954918,1.63093519552675,136.494065207551));
#173096=CARTESIAN_POINT('Ctrl Pts',(-81.5713897352515,1.47858264281552,
136.533385310379));
#173097=CARTESIAN_POINT('Ctrl Pts',(-81.5639769559494,1.3261363196498,136.572729614075));
#173098=CARTESIAN_POINT('Ctrl Pts',(-81.5565641766474,1.17225506076626,
136.605949738655));
#173099=CARTESIAN_POINT('Ctrl Pts',(-81.5491513973453,1.01747252505441,
136.6329693901));
#173100=CARTESIAN_POINT('Ctrl Pts',(-81.5417280263166,0.86246882879718,
136.66002764849));
#173101=CARTESIAN_POINT('Ctrl Pts',(-81.5343046552877,0.706561652739749,
136.680867689957));
#173102=CARTESIAN_POINT('Ctrl Pts',(-81.526881284259,0.550289156290671,
136.695465132593));
#173103=CARTESIAN_POINT('Ctrl Pts',(-81.5229452348182,0.467429728965848,
136.703205046939));
#173104=CARTESIAN_POINT('Ctrl Pts',(-81.5190091853774,0.384467599300527,
136.709190814001));
#173105=CARTESIAN_POINT('Ctrl Pts',(-81.5150731359366,0.301482690721084,
136.713424735487));
#173106=CARTESIAN_POINT('Ctrl Pts',(-81.5076498695312,0.144975743012964,
136.721409779272));
#173107=CARTESIAN_POINT('Ctrl Pts',(-81.5002266031259,-0.0120853171151492,
136.723184758965));
#173108=CARTESIAN_POINT('Ctrl Pts',(-81.4928033367206,-0.169166577750935,
136.718691791204));
#173109=CARTESIAN_POINT('Ctrl Pts',(-81.4853888439996,-0.326062181382328,
136.714204133758));
#173110=CARTESIAN_POINT('Ctrl Pts',(-81.4779743512786,-0.482977568495968,
136.703463285476));
#173111=CARTESIAN_POINT('Ctrl Pts',(-81.4705598585576,-0.639374666465414,
136.686463183688));
#173112=CARTESIAN_POINT('Ctrl Pts',(-81.4631525122038,-0.795621023024034,
136.669479467239));
#173113=CARTESIAN_POINT('Ctrl Pts',(-81.4557451658501,-0.951349716316779,
136.646248547676));
#173114=CARTESIAN_POINT('Ctrl Pts',(-81.4483378194963,-1.106023747502,136.616816383631));
#173115=CARTESIAN_POINT('Ctrl Pts',(-81.4409359978209,-1.26058241695881,
136.587406171204));
#173116=CARTESIAN_POINT('Ctrl Pts',(-81.4335341761455,-1.41408762540887,
136.551803993017));
#173117=CARTESIAN_POINT('Ctrl Pts',(-81.4261323544702,-1.56600867599897,
136.510107491481));
#173118=CARTESIAN_POINT('Ctrl Pts',(-81.4187344401589,-1.7178495286477,
136.468433001205));
#173119=CARTESIAN_POINT('Ctrl Pts',(-81.4113365258476,-1.86810752982338,
136.420670693231));
#173120=CARTESIAN_POINT('Ctrl Pts',(-81.4039386115364,-2.01626345101585,
136.366969021777));
#173121=CARTESIAN_POINT('Ctrl Pts',(-81.3965419266242,-2.16439475138309,
136.313276274566));
#173122=CARTESIAN_POINT('Ctrl Pts',(-81.3891452417121,-2.31042431446803,
136.25364624989));
#173123=CARTESIAN_POINT('Ctrl Pts',(-81.3817485567999,-2.45384921420774,
136.188276905588));
#173124=CARTESIAN_POINT('Ctrl Pts',(-81.3743521998645,-2.59726775433709,
136.122910459832));
#173125=CARTESIAN_POINT('Ctrl Pts',(-81.3669558429291,-2.73808152108111,
136.051805355273));
#173126=CARTESIAN_POINT('Ctrl Pts',(-81.3595594859937,-2.87580893053838,
135.975207120561));
#173127=CARTESIAN_POINT('Ctrl Pts',(-81.3521619966572,-3.01355742641404,
135.898597158463));
#173128=CARTESIAN_POINT('Ctrl Pts',(-81.3447645073206,-3.14821829787595,
135.816492573096));
#173129=CARTESIAN_POINT('Ctrl Pts',(-81.337367017984,-3.27933600093747,
135.729184061656));
#173130=CARTESIAN_POINT('Ctrl Pts',(-81.3299669354691,-3.41049966710672,
135.641844944352));
#173131=CARTESIAN_POINT('Ctrl Pts',(-81.3225668529541,-3.53811738143704,
135.54929847572));
#173132=CARTESIAN_POINT('Ctrl Pts',(-81.3151667704391,-3.6617640623067,
135.451877644377));
#173133=CARTESIAN_POINT('Ctrl Pts',(-81.3077585507727,-3.78554670541263,
135.354349688815));
#173134=CARTESIAN_POINT('Ctrl Pts',(-81.3003503311062,-3.90534930135215,
135.251936897714));
#173135=CARTESIAN_POINT('Ctrl Pts',(-81.2929421114398,-4.02078069362285,
135.145011856296));
#173136=CARTESIAN_POINT('Ctrl Pts',(-81.2855293321378,-4.13628313198974,
135.0380210043));
#173137=CARTESIAN_POINT('Ctrl Pts',(-81.2781165528358,-4.24740874282639,
134.92651263184));
#173138=CARTESIAN_POINT('Ctrl Pts',(-81.2707037735337,-4.35380488214927,
134.810894482476));
#173139=CARTESIAN_POINT('Ctrl Pts',(-81.263280402505,-4.46035304526566,
134.695111132478));
#173140=CARTESIAN_POINT('Ctrl Pts',(-81.2558570314763,-4.56215799927547,
134.5752065612));
#173141=CARTESIAN_POINT('Ctrl Pts',(-81.2484336604476,-4.65890834268524,
134.451620358379));
#173142=CARTESIAN_POINT('Ctrl Pts',(-81.2444976110063,-4.71020769626048,
134.386091988225));
#173143=CARTESIAN_POINT('Ctrl Pts',(-81.240561561565,-4.76008674916817,
134.319529052227));
#173144=CARTESIAN_POINT('Ctrl Pts',(-81.2366255121237,-4.80850423733689,
134.252000036359));
#173145=CARTESIAN_POINT('Ctrl Pts',(-81.2291362145993,-4.90063036016376,
134.123509553982));
#173146=CARTESIAN_POINT('Ctrl Pts',(-81.2216469170749,-4.98773943234449,
133.991133385634));
#173147=CARTESIAN_POINT('Ctrl Pts',(-81.2141576195505,-5.06948932391224,
133.855296303096));
#173148=CARTESIAN_POINT('Ctrl Pts',(-81.206677475249,-5.15113930290757,
133.719625237076));
#173149=CARTESIAN_POINT('Ctrl Pts',(-81.1991973309475,-5.2274429538628,
133.580501986051));
#173150=CARTESIAN_POINT('Ctrl Pts',(-81.191717186646,-5.29809939888114,
133.438382888177));
#173151=CARTESIAN_POINT('Ctrl Pts',(-81.184244796432,-5.36868259982376,
133.296411114188));
#173152=CARTESIAN_POINT('Ctrl Pts',(-81.176772406218,-5.43363008903948,
133.151450000467));
#173153=CARTESIAN_POINT('Ctrl Pts',(-81.169300016004,-5.49268521580541,
133.003983240329));
#173154=CARTESIAN_POINT('Ctrl Pts',(-81.1618339858426,-5.55169007837193,
132.856641995097));
#173155=CARTESIAN_POINT('Ctrl Pts',(-81.1543679556812,-5.60481243076715,
132.706799687089));
#173156=CARTESIAN_POINT('Ctrl Pts',(-81.1469019255198,-5.65184238195513,
132.554962871659));
#173157=CARTESIAN_POINT('Ctrl Pts',(-81.1394413679871,-5.69883786000854,
132.403237353197));
#173158=CARTESIAN_POINT('Ctrl Pts',(-81.1319808104545,-5.7397497277019,
132.249520587567));
#173159=CARTESIAN_POINT('Ctrl Pts',(-81.1245202529218,-5.77441694790665,
132.094337157751));
#173160=CARTESIAN_POINT('Ctrl Pts',(-81.1170629530263,-5.80906903074052,
131.939221488464));
#173161=CARTESIAN_POINT('Ctrl Pts',(-81.1096056531308,-5.83748181760578,
131.782640785632));
#173162=CARTESIAN_POINT('Ctrl Pts',(-81.1021483532353,-5.85954464004648,
131.625132920828));
#173163=CARTESIAN_POINT('Ctrl Pts',(-81.0946921811703,-5.88160412574032,
131.467648877269));
#173164=CARTESIAN_POINT('Ctrl Pts',(-81.0872360091052,-5.897315504748,131.309238311168));
#173165=CARTESIAN_POINT('Ctrl Pts',(-81.0797798370402,-5.90661954331391,
131.150447504116));
#173166=CARTESIAN_POINT('Ctrl Pts',(-81.0743116220949,-5.91344294844644,
131.033993342823));
#173167=CARTESIAN_POINT('Ctrl Pts',(-81.0688434071496,-5.91682124838117,
130.917334873091));
#173168=CARTESIAN_POINT('Ctrl Pts',(-81.0633751922043,-5.91674886068838,
130.800688827439));
#173169=CARTESIAN_POINT('',(-79.3133766006371,-5.92105326280497,130.80120237523));
#173170=CARTESIAN_POINT('Ctrl Pts',(-81.0633730746496,-5.90928221278149,
130.800648347112));
#173171=CARTESIAN_POINT('Ctrl Pts',(-81.0283080125366,-5.91348873412656,
130.053593847611));
#173172=CARTESIAN_POINT('Ctrl Pts',(-80.9004270758182,-5.43485370113081,
127.334316820743));
#173173=CARTESIAN_POINT('Ctrl Pts',(-80.6797302644982,-1.34479895996363,
123.936385931571));
#173174=CARTESIAN_POINT('Ctrl Pts',(-80.4012826406847,5.05132492808504,
125.96063508846));
#173175=CARTESIAN_POINT('Ctrl Pts',(-80.1228350168721,6.80552797816757,
132.43603137747));
#173176=CARTESIAN_POINT('Ctrl Pts',(-79.8443873930591,2.30578328483937,
137.412001949667));
#173177=CARTESIAN_POINT('Ctrl Pts',(-79.5745682871991,-4.107765378118,136.349839717701));
#173178=CARTESIAN_POINT('Ctrl Pts',(-79.3975650559447,-5.91281211476802,
132.583114278618));
#173179=CARTESIAN_POINT('Ctrl Pts',(-79.3133776992939,-5.92441071902747,
130.801223821324));
#173180=CARTESIAN_POINT('',(-77.5633744091961,-5.91844797605931,130.809555611699));
#173181=CARTESIAN_POINT('Ctrl Pts',(-79.3133751922043,-5.91674914235768,
130.801174882221));
#173182=CARTESIAN_POINT('Ctrl Pts',(-79.3047475099473,-5.91665094697026,
130.618800199036));
#173183=CARTESIAN_POINT('Ctrl Pts',(-79.2961198276903,-5.90812140161666,
130.436657192634));
#173184=CARTESIAN_POINT('Ctrl Pts',(-79.2874921454338,-5.89121974889844,
130.255306492102));
#173185=CARTESIAN_POINT('Ctrl Pts',(-79.2800688790283,-5.87667755006802,
130.099272168765));
#173186=CARTESIAN_POINT('Ctrl Pts',(-79.2726456126227,-5.8559100131561,
129.943580047664));
#173187=CARTESIAN_POINT('Ctrl Pts',(-79.2652223462172,-5.82893642157347,
129.788766822905));
#173188=CARTESIAN_POINT('Ctrl Pts',(-79.2578078534961,-5.80199471053601,
129.634136574521));
#173189=CARTESIAN_POINT('Ctrl Pts',(-79.250393360775,-5.76886160871769,
129.480383518943));
#173190=CARTESIAN_POINT('Ctrl Pts',(-79.242978868054,-5.72960828125813,
129.328041036365));
#173191=CARTESIAN_POINT('Ctrl Pts',(-79.2355715217001,-5.69039278763345,
129.175845387207));
#173192=CARTESIAN_POINT('Ctrl Pts',(-79.2281641753463,-5.64506890444209,
129.025057963489));
#173193=CARTESIAN_POINT('Ctrl Pts',(-79.2207568289924,-5.59375912640378,
128.876203622331));
#173194=CARTESIAN_POINT('Ctrl Pts',(-79.2133550073169,-5.54248761713374,
128.727460302356));
#173195=CARTESIAN_POINT('Ctrl Pts',(-79.2059531856416,-5.48523922357823,
128.580647545591));
#173196=CARTESIAN_POINT('Ctrl Pts',(-79.1985513639661,-5.42218668623004,
128.436276560323));
#173197=CARTESIAN_POINT('Ctrl Pts',(-79.1911534496546,-5.35916743382533,
128.291981787373));
#173198=CARTESIAN_POINT('Ctrl Pts',(-79.1837555353432,-5.29035028868397,
128.15012656006));
#173199=CARTESIAN_POINT('Ctrl Pts',(-79.1763576210317,-5.21595663319991,
128.011203449937));
#173200=CARTESIAN_POINT('Ctrl Pts',(-79.1689609361195,-5.14157534059186,
127.872303426314));
#173201=CARTESIAN_POINT('Ctrl Pts',(-79.1615642512072,-5.06161955294839,
127.736334881567));
#173202=CARTESIAN_POINT('Ctrl Pts',(-79.1541675662949,-4.97635730664454,
127.603767153987));
#173203=CARTESIAN_POINT('Ctrl Pts',(-79.1467712093594,-4.89109884095829,
127.471205304599));
#173204=CARTESIAN_POINT('Ctrl Pts',(-79.1393748524239,-4.80053458638627,
127.342044286512));
#173205=CARTESIAN_POINT('Ctrl Pts',(-79.1319784954885,-4.70497659770437,
127.216725494319));
#173206=CARTESIAN_POINT('Ctrl Pts',(-79.1245810061518,-4.60940397885045,
127.0913875155));
#173207=CARTESIAN_POINT('Ctrl Pts',(-79.1171835168151,-4.50883632992364,
126.969893230733));
#173208=CARTESIAN_POINT('Ctrl Pts',(-79.1097860274785,-4.40362667296433,
126.85265178623));
#173209=CARTESIAN_POINT('Ctrl Pts',(-79.1023859449634,-4.29838013492272,
126.735369242921));
#173210=CARTESIAN_POINT('Ctrl Pts',(-79.0949858624484,-4.1884885981729,
126.62234278576));
#173211=CARTESIAN_POINT('Ctrl Pts',(-79.0875857799334,-4.07434257040716,
126.51394534845));
#173212=CARTESIAN_POINT('Ctrl Pts',(-79.0801775602668,-3.96007102734923,
126.405428717013));
#173213=CARTESIAN_POINT('Ctrl Pts',(-79.0727693406003,-3.84153592135824,
126.301551527873));
#173214=CARTESIAN_POINT('Ctrl Pts',(-79.0653611209337,-3.71916208222599,
126.202647461726));
#173215=CARTESIAN_POINT('Ctrl Pts',(-79.0579483416316,-3.59671292403768,
126.103682521776));
#173216=CARTESIAN_POINT('Ctrl Pts',(-79.0505355623296,-3.47042062355663,
126.009697026341));
#173217=CARTESIAN_POINT('Ctrl Pts',(-79.0431227830275,-3.34073928239624,
125.920981499624));
#173218=CARTESIAN_POINT('Ctrl Pts',(-79.0356994119986,-3.21087264645396,
125.832139212001));
#173219=CARTESIAN_POINT('Ctrl Pts',(-79.0282760409698,-3.07760761386653,
125.748582129929));
#173220=CARTESIAN_POINT('Ctrl Pts',(-79.020852669941,-2.94142388864598,
125.670555394361));
#173221=CARTESIAN_POINT('Ctrl Pts',(-79.0169166205008,-2.86921600986188,
125.629183746944));
#173222=CARTESIAN_POINT('Ctrl Pts',(-79.0129805710606,-2.79618794491139,
125.589366086373));
#173223=CARTESIAN_POINT('Ctrl Pts',(-79.0090445216204,-2.7224133895408,
125.551133428595));
#173224=CARTESIAN_POINT('Ctrl Pts',(-79.0016212552149,-2.58327688051581,
125.479027829214));
#173225=CARTESIAN_POINT('Ctrl Pts',(-78.9941979888094,-2.44106332862814,
125.412344751739));
#173226=CARTESIAN_POINT('Ctrl Pts',(-78.986774722404,-2.29623469298405,
125.351358068764));
#173227=CARTESIAN_POINT('Ctrl Pts',(-78.979360229683,-2.15157723276002,
125.290443466984));
#173228=CARTESIAN_POINT('Ctrl Pts',(-78.9719457369619,-2.00431118173726,
125.235212001756));
#173229=CARTESIAN_POINT('Ctrl Pts',(-78.9645312442409,-1.85492375427443,
125.185892104855));
#173230=CARTESIAN_POINT('Ctrl Pts',(-78.9571238978871,-1.70568031203854,
125.136619744327));
#173231=CARTESIAN_POINT('Ctrl Pts',(-78.9497165515334,-1.55431991598217,
125.093247725188));
#173232=CARTESIAN_POINT('Ctrl Pts',(-78.9423092051796,-1.40135035465225,
125.055956687255));
#173233=CARTESIAN_POINT('Ctrl Pts',(-78.9349073835042,-1.24849488379239,
125.018693462385));
#173234=CARTESIAN_POINT('Ctrl Pts',(-78.9275055618289,-1.09403299848743,
124.987502276109));
#173235=CARTESIAN_POINT('Ctrl Pts',(-78.9201037401535,-0.938488163203133,
124.962514117526));
#173236=CARTESIAN_POINT('Ctrl Pts',(-78.9127058258421,-0.783025438826628,
124.937539149997));
#173237=CARTESIAN_POINT('Ctrl Pts',(-78.9053079115308,-0.62648127063976,
124.918760747838));
#173238=CARTESIAN_POINT('Ctrl Pts',(-78.8979099972194,-0.469389735632584,
124.906258902727));
#173239=CARTESIAN_POINT('Ctrl Pts',(-78.8905133123072,-0.31232430638882,
124.893759135196));
#173240=CARTESIAN_POINT('Ctrl Pts',(-78.8831166273949,-0.154712062615261,
124.887533884154));
#173241=CARTESIAN_POINT('Ctrl Pts',(-78.8757199424827,0.00290724788302974,
124.887611331817));
#173242=CARTESIAN_POINT('Ctrl Pts',(-78.8683235855473,0.16051956937592,
124.887688776046));
#173243=CARTESIAN_POINT('Ctrl Pts',(-78.8609272286119,0.318138583672985,
124.894068363121));
#173244=CARTESIAN_POINT('Ctrl Pts',(-78.8535308716765,0.475224259772234,
124.906726137079));
#173245=CARTESIAN_POINT('Ctrl Pts',(-78.8461333823399,0.632333986089963,
124.919385848976));
#173246=CARTESIAN_POINT('Ctrl Pts',(-78.8387358930033,0.788909839507255,
124.938325631662));
#173247=CARTESIAN_POINT('Ctrl Pts',(-78.8313384036667,0.944416776692353,
124.963469631218));
#173248=CARTESIAN_POINT('Ctrl Pts',(-78.8239383211517,1.09997822659299,
124.988622444964));
#173249=CARTESIAN_POINT('Ctrl Pts',(-78.8165382386367,1.25446964594075,
125.019983746201));
#173250=CARTESIAN_POINT('Ctrl Pts',(-78.8091381561217,1.40736619610315,
125.057426569522));
#173251=CARTESIAN_POINT('Ctrl Pts',(-78.8017299364552,1.56043087174082,
125.094910565077));
#173252=CARTESIAN_POINT('Ctrl Pts',(-78.7943217167887,1.71189681308749,
125.138489348763));
#173253=CARTESIAN_POINT('Ctrl Pts',(-78.7869134971222,1.86125365424366,
125.187985861813));
#173254=CARTESIAN_POINT('Ctrl Pts',(-78.7795007178201,2.0107024220434,125.23751283914));
#173255=CARTESIAN_POINT('Ctrl Pts',(-78.772087938518,2.15803915443074,125.292964672311));
#173256=CARTESIAN_POINT('Ctrl Pts',(-78.7646751592159,2.30277397215182,
125.354116348207));
#173257=CARTESIAN_POINT('Ctrl Pts',(-78.7572517881872,2.44771559376764,
125.415355400485));
#173258=CARTESIAN_POINT('Ctrl Pts',(-78.7498284171585,2.59004753866645,
125.482310402806));
#173259=CARTESIAN_POINT('Ctrl Pts',(-78.7424050461297,2.72930427108517,
125.554710271273));
#173260=CARTESIAN_POINT('Ctrl Pts',(-78.738468996689,2.80314153203182,125.593098418744));
#173261=CARTESIAN_POINT('Ctrl Pts',(-78.7345329472482,2.87611471049029,
125.633016579915));
#173262=CARTESIAN_POINT('Ctrl Pts',(-78.7305968978075,2.9481578775156,125.674419517344));
#173263=CARTESIAN_POINT('Ctrl Pts',(-78.7231736314021,3.08402904213746,
125.752504165195));
#173264=CARTESIAN_POINT('Ctrl Pts',(-78.7157503649966,3.21700130233436,
125.836108621896));
#173265=CARTESIAN_POINT('Ctrl Pts',(-78.7083270985912,3.34659454115527,
125.924992262993));
#173266=CARTESIAN_POINT('Ctrl Pts',(-78.7009126058701,3.47603461152995,
126.013770851008));
#173267=CARTESIAN_POINT('Ctrl Pts',(-78.6934981131491,3.60210330521407,
126.107815994465));
#173268=CARTESIAN_POINT('Ctrl Pts',(-78.6860836204281,3.72434508482375,
126.20684125908));
#173269=CARTESIAN_POINT('Ctrl Pts',(-78.6786762740744,3.84646904320358,
126.305771079418));
#173270=CARTESIAN_POINT('Ctrl Pts',(-78.6712689277205,3.96477314251573,
126.409671231604));
#173271=CARTESIAN_POINT('Ctrl Pts',(-78.6638615813667,4.07883093325383,
126.518212138986));
#173272=CARTESIAN_POINT('Ctrl Pts',(-78.6564597596913,4.19280365538877,
126.626672092465));
#173273=CARTESIAN_POINT('Ctrl Pts',(-78.649057938016,4.30253610573119,126.739765653091));
#173274=CARTESIAN_POINT('Ctrl Pts',(-78.6416561163406,4.4076351341137,126.857123218191));
#173275=CARTESIAN_POINT('Ctrl Pts',(-78.6342582020292,4.51267868153692,
126.974418831145));
#173276=CARTESIAN_POINT('Ctrl Pts',(-78.6268602877179,4.61309342981408,
127.095973688346));
#173277=CARTESIAN_POINT('Ctrl Pts',(-78.6194623734066,4.70852339802178,
127.221381693154));
#173278=CARTESIAN_POINT('Ctrl Pts',(-78.6120656884944,4.80393750750017,
127.346768857426));
#173279=CARTESIAN_POINT('Ctrl Pts',(-78.6046690035822,4.8943682551633,127.476007601675));
#173280=CARTESIAN_POINT('Ctrl Pts',(-78.59727231867,4.9795001836408,127.608659053962));
#173281=CARTESIAN_POINT('Ctrl Pts',(-78.5898759617346,5.06462833727939,
127.741304624344));
#173282=CARTESIAN_POINT('Ctrl Pts',(-78.5824796047991,5.14445793728053,
127.877362287719));
#173283=CARTESIAN_POINT('Ctrl Pts',(-78.5750832478636,5.21871723852496,
128.016364751927));
#173284=CARTESIAN_POINT('Ctrl Pts',(-78.5676857585271,5.29298790905799,
128.155388497767));
#173285=CARTESIAN_POINT('Ctrl Pts',(-78.5602882691905,5.36168640683164,
128.297357612876));
#173286=CARTESIAN_POINT('Ctrl Pts',(-78.552890779854,5.42458734590637,128.441780949252));
#173287=CARTESIAN_POINT('Ctrl Pts',(-78.5454906973389,5.48751033480787,
128.586254913004));
#173288=CARTESIAN_POINT('Ctrl Pts',(-78.5380906148239,5.54463156969961,
128.733184468886));
#173289=CARTESIAN_POINT('Ctrl Pts',(-78.5306905323089,5.59577418207239,
128.88205942739));
#173290=CARTESIAN_POINT('Ctrl Pts',(-78.5232823126425,5.64697303100499,
129.031098089215));
#173291=CARTESIAN_POINT('Ctrl Pts',(-78.515874092976,5.6921800071335,129.182086072462));
#173292=CARTESIAN_POINT('Ctrl Pts',(-78.5084658733095,5.73126820977958,
129.334498287254));
#173293=CARTESIAN_POINT('Ctrl Pts',(-78.5010530940075,5.77038047056217,
129.487004309222));
#173294=CARTESIAN_POINT('Ctrl Pts',(-78.4936403147054,5.8033663755926,129.640935945287));
#173295=CARTESIAN_POINT('Ctrl Pts',(-78.4862275354033,5.83015044307889,
129.795759421073));
#173296=CARTESIAN_POINT('Ctrl Pts',(-78.4788041643746,5.85697278089689,
129.950804115902));
#173297=CARTESIAN_POINT('Ctrl Pts',(-78.4713807933459,5.87757553404887,
130.106742826417));
#173298=CARTESIAN_POINT('Ctrl Pts',(-78.4639574223171,5.89193513964429,
130.263037356727));
#173299=CARTESIAN_POINT('Ctrl Pts',(-78.4600213728763,5.89954894708507,
130.345908466935));
#173300=CARTESIAN_POINT('Ctrl Pts',(-78.4560853234354,5.90540845297665,
130.42887960985));
#173301=CARTESIAN_POINT('Ctrl Pts',(-78.4521492739946,5.90951608065499,
130.511870865643));
#173302=CARTESIAN_POINT('Ctrl Pts',(-78.4447260075892,5.91726293826161,
130.668389783998));
#173303=CARTESIAN_POINT('Ctrl Pts',(-78.4373027411837,5.91879889570283,
130.82545336347));
#173304=CARTESIAN_POINT('Ctrl Pts',(-78.4298794747783,5.91406688220579,
130.982527604678));
#173305=CARTESIAN_POINT('Ctrl Pts',(-78.4224649820572,5.90934046155575,
131.139416197177));
#173306=CARTESIAN_POINT('Ctrl Pts',(-78.4150504893362,5.89836082720356,
131.296315056844));
#173307=CARTESIAN_POINT('Ctrl Pts',(-78.4076359966152,5.8811227353417,131.452686102448));
#173308=CARTESIAN_POINT('Ctrl Pts',(-78.4002286502615,5.86390125820179,
131.608906431751));
#173309=CARTESIAN_POINT('Ctrl Pts',(-78.3928213039077,5.84043337297872,
131.764599591207));
#173310=CARTESIAN_POINT('Ctrl Pts',(-78.3854139575539,5.81076585546984,
131.91922865254));
#173311=CARTESIAN_POINT('Ctrl Pts',(-78.3780121358785,5.7811204651148,132.073742385684));
#173312=CARTESIAN_POINT('Ctrl Pts',(-78.3706103142031,5.74528471935816,
132.227193235924));
#173313=CARTESIAN_POINT('Ctrl Pts',(-78.3632084925277,5.70335706812827,
132.379050655615));
#173314=CARTESIAN_POINT('Ctrl Pts',(-78.3558105782163,5.66145155017911,
132.530827910957));
#173315=CARTESIAN_POINT('Ctrl Pts',(-78.348412663905,5.61346063041326,132.681013052036));
#173316=CARTESIAN_POINT('Ctrl Pts',(-78.3410147495937,5.55953355305193,
132.829087076866));
#173317=CARTESIAN_POINT('Ctrl Pts',(-78.3336180646815,5.5056154373926,132.977136494479));
#173318=CARTESIAN_POINT('Ctrl Pts',(-78.3262213797692,5.44576324963043,
133.123075141718));
#173319=CARTESIAN_POINT('Ctrl Pts',(-78.318824694857,5.38017571274215,133.266400394361));
#173320=CARTESIAN_POINT('Ctrl Pts',(-78.3114283379215,5.31459108407399,
133.409719291811));
#173321=CARTESIAN_POINT('Ctrl Pts',(-78.3040319809862,5.24327176727085,
133.550424685631));
#173322=CARTESIAN_POINT('Ctrl Pts',(-78.2966356240507,5.16646402358529,
133.688035366129));
#173323=CARTESIAN_POINT('Ctrl Pts',(-78.2892381347142,5.08964452043788,
133.825667115174));
#173324=CARTESIAN_POINT('Ctrl Pts',(-78.2818406453775,5.00733509922222,
133.960202881499));
#173325=CARTESIAN_POINT('Ctrl Pts',(-78.2744431560409,4.91982715005869,
134.091187564037));
#173326=CARTESIAN_POINT('Ctrl Pts',(-78.2670430735259,4.83228852511911,
134.222218163052));
#173327=CARTESIAN_POINT('Ctrl Pts',(-78.2596429910109,4.7395479512164,134.349694889633));
#173328=CARTESIAN_POINT('Ctrl Pts',(-78.2522429084959,4.64193906348408,
134.473193169401));
#173329=CARTESIAN_POINT('Ctrl Pts',(-78.2448346888294,4.54422284474539,
134.596827248223));
#173330=CARTESIAN_POINT('Ctrl Pts',(-78.2374264691629,4.44162785307719,
134.716473850599));
#173331=CARTESIAN_POINT('Ctrl Pts',(-78.2300182494964,4.33452726854626,
134.831742387492));
#173332=CARTESIAN_POINT('Ctrl Pts',(-78.2226054701944,4.22736076539261,
134.947081870245));
#173333=CARTESIAN_POINT('Ctrl Pts',(-78.2151926908923,4.11568340779413,
135.05803765564));
#173334=CARTESIAN_POINT('Ctrl Pts',(-78.2077799115902,3.99990347550006,
135.164257720616));
#173335=CARTESIAN_POINT('Ctrl Pts',(-78.2003565405614,3.88395811140934,
135.270629557802));
#173336=CARTESIAN_POINT('Ctrl Pts',(-78.1929331695327,3.76389874916808,
135.372251919577));
#173337=CARTESIAN_POINT('Ctrl Pts',(-78.185509798504,3.64016545190354,135.468814073789));
#173338=CARTESIAN_POINT('Ctrl Pts',(-78.1815737490633,3.57455908875558,
135.520013644928));
#173339=CARTESIAN_POINT('Ctrl Pts',(-78.1776376996226,3.50792032241883,
135.569791342611));
#173340=CARTESIAN_POINT('Ctrl Pts',(-78.1737016501818,3.44031770158284,
135.618106007039));
#173341=CARTESIAN_POINT('Ctrl Pts',(-78.1662783837764,3.31282126848915,
135.709225956304));
#173342=CARTESIAN_POINT('Ctrl Pts',(-78.158855117371,3.1815094533223,135.795414901996));
#173343=CARTESIAN_POINT('Ctrl Pts',(-78.1514318509655,3.04680067673981,
135.876336189147));
#173344=CARTESIAN_POINT('Ctrl Pts',(-78.1440173582445,2.912251114744,135.957161834058));
#173345=CARTESIAN_POINT('Ctrl Pts',(-78.1366028655235,2.77431289994026,
136.032732022835));
#173346=CARTESIAN_POINT('Ctrl Pts',(-78.1291883728024,2.63343590090035,
136.102751497668));
#173347=CARTESIAN_POINT('Ctrl Pts',(-78.1217810264487,2.49269468441605,
136.172703485095));
#173348=CARTESIAN_POINT('Ctrl Pts',(-78.1143736800949,2.34902065470756,
136.237115244315));
#173349=CARTESIAN_POINT('Ctrl Pts',(-78.1069663337411,2.20289082820329,
136.295735906282));
#173350=CARTESIAN_POINT('Ctrl Pts',(-78.0995645120657,2.05686999083637,
136.354312846747));
#173351=CARTESIAN_POINT('Ctrl Pts',(-78.0921626903903,1.90839734865715,
136.407107151722));
#173352=CARTESIAN_POINT('Ctrl Pts',(-78.0847608687149,1.75797248101512,
136.453914875956));
#173353=CARTESIAN_POINT('Ctrl Pts',(-78.0773629544035,1.60762702149025,
136.500697890757));
#173354=CARTESIAN_POINT('Ctrl Pts',(-78.069965040092,1.45533174445921,136.541500508014));
#173355=CARTESIAN_POINT('Ctrl Pts',(-78.0625671257807,1.30160397113954,
136.576167757866));
#173356=CARTESIAN_POINT('Ctrl Pts',(-78.0551704408685,1.1479017445871,136.610829246649));
#173357=CARTESIAN_POINT('Ctrl Pts',(-78.0477737559563,0.992767858011212,
136.639357309565));
#173358=CARTESIAN_POINT('Ctrl Pts',(-78.0403770710441,0.836732598028245,
136.661647457213));
#173359=CARTESIAN_POINT('Ctrl Pts',(-78.0329807141087,0.680704256812219,
136.683936616492));
#173360=CARTESIAN_POINT('Ctrl Pts',(-78.0255843571732,0.523774991204623,
136.699988357677));
#173361=CARTESIAN_POINT('Ctrl Pts',(-78.0181880002378,0.366482766769292,
136.709749761743));
#173362=CARTESIAN_POINT('Ctrl Pts',(-78.0107905109012,0.209166460492403,
136.719512660305));
#173363=CARTESIAN_POINT('Ctrl Pts',(-78.0033930215645,0.0514874573457338,
136.722983281029));
#173364=CARTESIAN_POINT('Ctrl Pts',(-77.9959955322279,-0.106013849775836,
136.720160785435));
#173365=CARTESIAN_POINT('Ctrl Pts',(-77.9885954497129,-0.263570368735784,
136.717337300419));
#173366=CARTESIAN_POINT('Ctrl Pts',(-77.981195367198,-0.420948694644431,
136.708216313554));
#173367=CARTESIAN_POINT('Ctrl Pts',(-77.973795284683,-0.577611283114258,
136.692849028705));
#173368=CARTESIAN_POINT('Ctrl Pts',(-77.9663870650165,-0.734446138206083,
136.677464845947));
#173369=CARTESIAN_POINT('Ctrl Pts',(-77.9589788453501,-0.890563312371909,
136.65582068493));
#173370=CARTESIAN_POINT('Ctrl Pts',(-77.9515706256836,-1.04543247905034,
136.628019389699));
#173371=CARTESIAN_POINT('Ctrl Pts',(-77.9441578463815,-1.20039696511673,
136.600200983235));
#173372=CARTESIAN_POINT('Ctrl Pts',(-77.9367450670794,-1.35411154945329,
136.566217971672));
#173373=CARTESIAN_POINT('Ctrl Pts',(-77.9293322877774,-1.50605937991354,
136.526223575264));
#173374=CARTESIAN_POINT('Ctrl Pts',(-77.9219089167486,-1.65822432055937,
136.486172032987));
#173375=CARTESIAN_POINT('Ctrl Pts',(-77.9144855457198,-1.80861710951992,
136.440092060079));
#173376=CARTESIAN_POINT('Ctrl Pts',(-77.907062174691,-1.95673845416578,
136.388185935794));
#173377=CARTESIAN_POINT('Ctrl Pts',(-77.9031261252503,-2.03527594521947,
136.360664063229));
#173378=CARTESIAN_POINT('Ctrl Pts',(-77.8991900758095,-2.11317521300684,
136.331505043287));
#173379=CARTESIAN_POINT('Ctrl Pts',(-77.8952540263687,-2.19036457638164,
136.300744300046));
#173380=CARTESIAN_POINT('Ctrl Pts',(-77.8878307599634,-2.3359413067075,
136.242730498304));
#173381=CARTESIAN_POINT('Ctrl Pts',(-77.8804074935581,-2.47943175128092,
136.17884137969));
#173382=CARTESIAN_POINT('Ctrl Pts',(-77.8729842271528,-2.62032650615729,
136.109247003119));
#173383=CARTESIAN_POINT('Ctrl Pts',(-77.8655697344319,-2.76105473513398,
136.039734881322));
#173384=CARTESIAN_POINT('Ctrl Pts',(-77.858155241711,-2.89919304963888,
135.964531087535));
#173385=CARTESIAN_POINT('Ctrl Pts',(-77.8507407489901,-3.03424987596111,
135.883854514868));
#173386=CARTESIAN_POINT('Ctrl Pts',(-77.8433334026365,-3.16917652942933,
135.80325570132));
#173387=CARTESIAN_POINT('Ctrl Pts',(-77.8359260562828,-3.30102728918574,
135.717194800271));
#173388=CARTESIAN_POINT('Ctrl Pts',(-77.8285187099291,-3.42933325296503,
135.625937538306));
#173389=CARTESIAN_POINT('Ctrl Pts',(-77.8211168882539,-3.55754352131619,
135.534748339449));
#173390=CARTESIAN_POINT('Ctrl Pts',(-77.8137150665785,-3.68221395504526,
135.438370712033));
#173391=CARTESIAN_POINT('Ctrl Pts',(-77.8063132449032,-3.802902934398,135.337114728926));
#173392=CARTESIAN_POINT('Ctrl Pts',(-77.798915330592,-3.92352820297763,
135.235912198064));
#173393=CARTESIAN_POINT('Ctrl Pts',(-77.7915174162808,-4.04017591771877,
135.12983667956));
#173394=CARTESIAN_POINT('Ctrl Pts',(-77.7841195019696,-4.15243607333393,
135.019239645412));
#173395=CARTESIAN_POINT('Ctrl Pts',(-77.7767228170575,-4.264677573348,134.908660990484));
#173396=CARTESIAN_POINT('Ctrl Pts',(-77.7693261321454,-4.37253269568519,
134.793562572933));
#173397=CARTESIAN_POINT('Ctrl Pts',(-77.7619294472333,-4.47562689758401,
134.674334058834));
#173398=CARTESIAN_POINT('Ctrl Pts',(-77.754533090298,-4.57871652817789,
134.555110831453));
#173399=CARTESIAN_POINT('Ctrl Pts',(-77.7471367333627,-4.67704541391682,
134.431758154029));
#173400=CARTESIAN_POINT('Ctrl Pts',(-77.7397403764274,-4.77027824899781,
134.3047000282));
#173401=CARTESIAN_POINT('Ctrl Pts',(-77.7323428870909,-4.86352535826413,
134.177622449448));
#173402=CARTESIAN_POINT('Ctrl Pts',(-77.7249453977545,-4.95167464249734,
134.046838593678));
#173403=CARTESIAN_POINT('Ctrl Pts',(-77.7175479084181,-5.03443330069878,
133.912802655519));
#173404=CARTESIAN_POINT('Ctrl Pts',(-77.7101478259032,-5.11722096981968,
133.77871973127));
#173405=CARTESIAN_POINT('Ctrl Pts',(-77.7027477433882,-5.19461405458396,
133.641382772306));
#173406=CARTESIAN_POINT('Ctrl Pts',(-77.6953476608733,-5.26636507838174,
133.501271706887));
#173407=CARTESIAN_POINT('Ctrl Pts',(-77.687939441207,-5.33819499980626,
133.361006574947));
#173408=CARTESIAN_POINT('Ctrl Pts',(-77.6805312215408,-5.4043703001598,
133.217961577139));
#173409=CARTESIAN_POINT('Ctrl Pts',(-77.6731230018744,-5.46469085058839,
133.072638481937));
#173410=CARTESIAN_POINT('Ctrl Pts',(-77.6657102225725,-5.52504852730944,
132.927225942794));
#173411=CARTESIAN_POINT('Ctrl Pts',(-77.6582974432705,-5.5795441447548,
132.77953286174));
#173412=CARTESIAN_POINT('Ctrl Pts',(-77.6508846639686,-5.62802724025374,
132.630076900416));
#173413=CARTESIAN_POINT('Ctrl Pts',(-77.64346129294,-5.6765796106731,132.480407389404));
#173414=CARTESIAN_POINT('Ctrl Pts',(-77.6360379219114,-5.71910220039589,
132.328970325788));
#173415=CARTESIAN_POINT('Ctrl Pts',(-77.6286145508828,-5.75549531282523,
132.176295115473));
#173416=CARTESIAN_POINT('Ctrl Pts',(-77.6246785014408,-5.77479181428223,
132.095343055546));
#173417=CARTESIAN_POINT('Ctrl Pts',(-77.6207424519988,-5.79236596201951,
132.014043032783));
#173418=CARTESIAN_POINT('Ctrl Pts',(-77.6168064025568,-5.80820881390571,
131.93247450214));
#173419=CARTESIAN_POINT('Ctrl Pts',(-77.6059178851201,-5.85203579615075,
131.70682683656));
#173420=CARTESIAN_POINT('Ctrl Pts',(-77.5950293676835,-5.88272376379399,
131.478551115798));
#173421=CARTESIAN_POINT('Ctrl Pts',(-77.5841408502469,-5.9000270659515,
131.248895412087));
#173422=CARTESIAN_POINT('Ctrl Pts',(-77.5772189642326,-5.9110268632979,
131.102902111082));
#173423=CARTESIAN_POINT('Ctrl Pts',(-77.5702970782184,-5.91661845541344,
130.956351474934));
#173424=CARTESIAN_POINT('Ctrl Pts',(-77.5633751922042,-5.91674770606937,
130.809570725322));
#173425=CARTESIAN_POINT('',(-75.8133751922041,-5.90702258126614,130.805121151015));
#173426=CARTESIAN_POINT('Ctrl Pts',(-77.5633740622052,-5.9192014526658,
130.809548914079));
#173427=CARTESIAN_POINT('Ctrl Pts',(-77.4883689677179,-5.90454020598336,
129.218368607907));
#173428=CARTESIAN_POINT('Ctrl Pts',(-77.3205479986255,-4.42166650021555,
125.634093850048));
#173429=CARTESIAN_POINT('Ctrl Pts',(-77.0599111549303,1.64202572553403,
124.00132364523));
#173430=CARTESIAN_POINT('Ctrl Pts',(-76.7814635311171,6.61114269020578,
128.508635708072));
#173431=CARTESIAN_POINT('Ctrl Pts',(-76.5030159073044,5.50494249485923,
135.125606810351));
#173432=CARTESIAN_POINT('Ctrl Pts',(-76.2245682834915,-0.66003092187362,
137.771563766067));
#173433=CARTESIAN_POINT('Ctrl Pts',(-75.9946880451241,-5.24895454444059,
134.670228436097));
#173434=CARTESIAN_POINT('Ctrl Pts',(-75.8576236813622,-5.90810076479692,
131.748728288428));
#173435=CARTESIAN_POINT('Ctrl Pts',(-75.8133751922041,-5.90702258126614,
130.805121151015));
#173436=CARTESIAN_POINT('',(-74.063375192204,-5.91640124831382,130.798888549479));
#173437=CARTESIAN_POINT('Ctrl Pts',(-75.8133751922041,-5.90702258126614,
130.805121151015));
#173438=CARTESIAN_POINT('Ctrl Pts',(-75.764807806758,-5.90583916108351,
129.76941275906));
#173439=CARTESIAN_POINT('Ctrl Pts',(-75.6234245467082,-5.1523334128451,
126.75277827436));
#173440=CARTESIAN_POINT('Ctrl Pts',(-75.3892254120525,-0.335322348419818,
123.814001581503));
#173441=CARTESIAN_POINT('Ctrl Pts',(-75.11077778824,5.69993711426887,126.743784621021));
#173442=CARTESIAN_POINT('Ctrl Pts',(-74.8323301644269,6.49723282634914,
133.405038631191));
#173443=CARTESIAN_POINT('Ctrl Pts',(-74.5538825406141,1.32388897848506,
137.676396597024));
#173444=CARTESIAN_POINT('Ctrl Pts',(-74.2975642165399,-4.55821169044833,
135.795110472929));
#173445=CARTESIAN_POINT('Ctrl Pts',(-74.1340617670698,-5.90256935525085,
132.300275173225));
#173446=CARTESIAN_POINT('Ctrl Pts',(-74.063375192204,-5.91640124831382,
130.798888549479));
#173447=CARTESIAN_POINT('',(-72.3133751922041,-5.92595501209889,130.806045629526));
#173448=CARTESIAN_POINT('Ctrl Pts',(-74.063375192204,-5.91640124831382,
130.798888549479));
#173449=CARTESIAN_POINT('Ctrl Pts',(-74.0412458924655,-5.92073149218436,
130.328861041661));
#173450=CARTESIAN_POINT('Ctrl Pts',(-73.9263007181233,-5.65438782062924,
127.892268950583));
#173451=CARTESIAN_POINT('Ctrl Pts',(-73.7185396691751,-2.28566121732441,
124.189731880434));
#173452=CARTESIAN_POINT('Ctrl Pts',(-73.4400920453628,4.32961877422029,
125.306000698443));
#173453=CARTESIAN_POINT('Ctrl Pts',(-73.1616444215496,6.96619062589002,
131.474993672292));
#173454=CARTESIAN_POINT('Ctrl Pts',(-72.8831967977369,3.20117360970058,
137.027707631104));
#173455=CARTESIAN_POINT('Ctrl Pts',(-72.6047491739239,-3.5055655677807,
136.861469711872));
#173456=CARTESIAN_POINT('Ctrl Pts',(-72.4148086387464,-5.88302857893171,
132.951147516027));
#173457=CARTESIAN_POINT('Ctrl Pts',(-72.3176839781731,-5.92629787890155,
130.897181430883));
#173458=CARTESIAN_POINT('Ctrl Pts',(-72.3133751922041,-5.92595501209889,
130.806045629526));
#173459=CARTESIAN_POINT('',(-70.5633763914996,-5.91353738369623,130.809041528552));
#173460=CARTESIAN_POINT('Ctrl Pts',(-72.3133751922041,-5.92595501209889,
130.806045629526));
#173461=CARTESIAN_POINT('Ctrl Pts',(-72.2248681035687,-5.9189121599564,
128.934018449121));
#173462=CARTESIAN_POINT('Ctrl Pts',(-72.0435451403292,-3.9487999677908,
125.086069876051));
#173463=CARTESIAN_POINT('Ctrl Pts',(-71.7694063024852,2.61056268441707,
124.311093104128));
#173464=CARTESIAN_POINT('Ctrl Pts',(-71.4909586786723,6.87404275541449,
129.490931241054));
#173465=CARTESIAN_POINT('Ctrl Pts',(-71.2125110548594,4.82061334984184,
135.877746810402));
#173466=CARTESIAN_POINT('Ctrl Pts',(-70.9340634310466,-1.66272422418068,
137.602368317227));
#173467=CARTESIAN_POINT('Ctrl Pts',(-70.717685491852,-5.51348031185306,
134.088059501253));
#173468=CARTESIAN_POINT('Ctrl Pts',(-70.5941234272619,-5.91605620421693,
131.463545541928));
#173469=CARTESIAN_POINT('Ctrl Pts',(-70.5633772372761,-5.91127305061012,
130.809057749741));
#173470=CARTESIAN_POINT('',(-68.8133740211525,-5.91243167929344,130.800818385325));
#173471=CARTESIAN_POINT('Ctrl Pts',(-70.5633751922041,-5.91674816655043,
130.809018527203));
#173472=CARTESIAN_POINT('Ctrl Pts',(-70.5556165668381,-5.91687830402043,
130.643710331672));
#173473=CARTESIAN_POINT('Ctrl Pts',(-70.547857941472,-5.91007539724289,
130.478317204947));
#173474=CARTESIAN_POINT('Ctrl Pts',(-70.5400993161061,-5.89635065780119,
130.313464006509));
#173475=CARTESIAN_POINT('Ctrl Pts',(-70.5327111471719,-5.88328124295133,
130.156482167337));
#173476=CARTESIAN_POINT('Ctrl Pts',(-70.5253229782378,-5.86393568336394,
129.9999903029));
#173477=CARTESIAN_POINT('Ctrl Pts',(-70.5179348093037,-5.83837699622299,
129.844524895958));
#173478=CARTESIAN_POINT('Ctrl Pts',(-70.5105463541655,-5.81281731898565,
129.689053466573));
#173479=CARTESIAN_POINT('Ctrl Pts',(-70.5031578990273,-5.78104409495704,
129.534608942759));
#173480=CARTESIAN_POINT('Ctrl Pts',(-70.4957694438891,-5.74317177248523,
129.381719217132));
#173481=CARTESIAN_POINT('Ctrl Pts',(-70.4883792401909,-5.70529048710717,
129.228793308451));
#173482=CARTESIAN_POINT('Ctrl Pts',(-70.4809890364927,-5.66130731908094,
129.077423293322));
#173483=CARTESIAN_POINT('Ctrl Pts',(-70.4735988327945,-5.61138700801363,
128.928123316797));
#173484=CARTESIAN_POINT('Ctrl Pts',(-70.4662054173999,-5.56144500216118,
128.778758456244));
#173485=CARTESIAN_POINT('Ctrl Pts',(-70.4588120020053,-5.50556083423948,
128.631465779532));
#173486=CARTESIAN_POINT('Ctrl Pts',(-70.4514185866107,-5.44394786519913,
128.486740673854));
#173487=CARTESIAN_POINT('Ctrl Pts',(-70.4440164177111,-5.38226194889408,
128.341844219501));
#173488=CARTESIAN_POINT('Ctrl Pts',(-70.4366142488115,-5.31483383449027,
128.199521749961));
#173489=CARTESIAN_POINT('Ctrl Pts',(-70.429212079912,-5.24192376487584,
128.060245859446));
#173490=CARTESIAN_POINT('Ctrl Pts',(-70.4218048048358,-5.16896340031444,
127.920873893403));
#173491=CARTESIAN_POINT('Ctrl Pts',(-70.4143975297596,-5.09051373203574,
127.784553016251));
#173492=CARTESIAN_POINT('Ctrl Pts',(-70.4069902546835,-5.00687873761646,
127.651727453161));
#173493=CARTESIAN_POINT('Ctrl Pts',(-70.3995723268131,-4.92312346328625,
127.518710866601));
#173494=CARTESIAN_POINT('Ctrl Pts',(-70.3921543989427,-4.83416818413982,
127.389199937277));
#173495=CARTESIAN_POINT('Ctrl Pts',(-70.3847364710722,-4.74035801715883,
127.263606964506));
#173496=CARTESIAN_POINT('Ctrl Pts',(-70.3822137085218,-4.70845412428677,
127.220894059522));
#173497=CARTESIAN_POINT('Ctrl Pts',(-70.3796909459713,-4.67598903149527,
127.178634002934));
#173498=CARTESIAN_POINT('Ctrl Pts',(-70.3771681834209,-4.6429772797318,
127.13684203651));
#173499=CARTESIAN_POINT('Ctrl Pts',(-70.3697449170155,-4.54583970814075,
127.013868552412));
#173500=CARTESIAN_POINT('Ctrl Pts',(-70.3623216506099,-4.44366628163952,
126.894570949422));
#173501=CARTESIAN_POINT('Ctrl Pts',(-70.3548983842045,-4.33676533087885,
126.779388937245));
#173502=CARTESIAN_POINT('Ctrl Pts',(-70.3474838914835,-4.22999072816441,
126.66434306064));
#173503=CARTESIAN_POINT('Ctrl Pts',(-70.3400693987625,-4.11849997468444,
126.553403363401));
#173504=CARTESIAN_POINT('Ctrl Pts',(-70.3326549060415,-4.00264311820997,
126.446978533017));
#173505=CARTESIAN_POINT('Ctrl Pts',(-70.3252475596877,-3.8868979289357,
126.340656278892));
#173506=CARTESIAN_POINT('Ctrl Pts',(-70.3178402133339,-3.76679528746255,
126.238840479285));
#173507=CARTESIAN_POINT('Ctrl Pts',(-70.3104328669801,-3.64272365985294,
126.141904730327));
#173508=CARTESIAN_POINT('Ctrl Pts',(-70.3030310453047,-3.51874456954415,
126.045041279709));
#173509=CARTESIAN_POINT('Ctrl Pts',(-70.2956292236293,-3.39080268019189,
125.953050861391));
#173510=CARTESIAN_POINT('Ctrl Pts',(-70.2882274019539,-3.25932117673971,
125.866268270378));
#173511=CARTESIAN_POINT('Ctrl Pts',(-70.2808294876426,-3.12790908134993,
125.779531491219));
#173512=CARTESIAN_POINT('Ctrl Pts',(-70.2734315733312,-2.99296140390075,
125.697997269374));
#173513=CARTESIAN_POINT('Ctrl Pts',(-70.2660336590199,-2.85493198759279,
125.621958287689));
#173514=CARTESIAN_POINT('Ctrl Pts',(-70.2586369741076,-2.71692550926932,
125.545931942302));
#173515=CARTESIAN_POINT('Ctrl Pts',(-70.2512402891954,-2.57583863515824,
125.475399204573));
#173516=CARTESIAN_POINT('Ctrl Pts',(-70.2438436042831,-2.4321516969811,
125.41060787153));
#173517=CARTESIAN_POINT('Ctrl Pts',(-70.2364472473477,-2.28847113003338,
125.345819411402));
#173518=CARTESIAN_POINT('Ctrl Pts',(-70.2290508904122,-2.14219106855501,
125.286772003218));
#173519=CARTESIAN_POINT('Ctrl Pts',(-70.2216545334767,-1.99381355775538,
125.233666041536));
#173520=CARTESIAN_POINT('Ctrl Pts',(-70.2142570441401,-1.84541332998005,
125.180551949195));
#173521=CARTESIAN_POINT('Ctrl Pts',(-70.2068595548035,-1.69491536496844,
125.133381240393));
#173522=CARTESIAN_POINT('Ctrl Pts',(-70.1994620654669,-1.54283851866879,
125.092304957139));
#173523=CARTESIAN_POINT('Ctrl Pts',(-70.1920619829519,-1.39070836206665,
125.051214274658));
#173524=CARTESIAN_POINT('Ctrl Pts',(-70.1846619004369,-1.23699858237161,
125.016222368545));
#173525=CARTESIAN_POINT('Ctrl Pts',(-70.1772618179219,-1.08223976780218,
124.987429498197));
#173526=CARTESIAN_POINT('Ctrl Pts',(-70.1698535982554,-0.927310780006325,
124.958604967127));
#173527=CARTESIAN_POINT('Ctrl Pts',(-70.1624453785889,-0.771330820902878,
124.935993153098));
#173528=CARTESIAN_POINT('Ctrl Pts',(-70.1550371589224,-0.61483790210435,
124.919642704477));
#173529=CARTESIAN_POINT('Ctrl Pts',(-70.1476243796204,-0.458248664525749,
124.903282192427));
#173530=CARTESIAN_POINT('Ctrl Pts',(-70.1402116003183,-0.301146209810517,
124.893190748772));
#173531=CARTESIAN_POINT('Ctrl Pts',(-70.1327988210163,-0.144069611628858,
124.889364885572));
#173532=CARTESIAN_POINT('Ctrl Pts',(-70.1253754499875,0.0132314249628933,
124.8855335558));
#173533=CARTESIAN_POINT('Ctrl Pts',(-70.1179520789587,0.170506158969827,
124.88798568094));
#173534=CARTESIAN_POINT('Ctrl Pts',(-70.1105287079299,0.327218744922378,
124.896665766317));
#173535=CARTESIAN_POINT('Ctrl Pts',(-70.1065926584892,0.410311518258836,
124.90126815586));
#173536=CARTESIAN_POINT('Ctrl Pts',(-70.1026566090485,0.493246378182262,
124.907620586494));
#173537=CARTESIAN_POINT('Ctrl Pts',(-70.0987205596078,0.575944621046976,
124.915708958995));
#173538=CARTESIAN_POINT('Ctrl Pts',(-70.0912972932024,0.731910926170226,
124.930963377105));
#173539=CARTESIAN_POINT('Ctrl Pts',(-70.0838740267969,0.887506610997351,
124.9524415061));
#173540=CARTESIAN_POINT('Ctrl Pts',(-70.0764507603915,1.04219507505318,
124.980121612508));
#173541=CARTESIAN_POINT('Ctrl Pts',(-70.0690362676705,1.19670071019079,
125.007769003329));
#173542=CARTESIAN_POINT('Ctrl Pts',(-70.0616217749495,1.35030089502287,
125.041603715604));
#173543=CARTESIAN_POINT('Ctrl Pts',(-70.0542072822284,1.50246257981797,
125.081552149799));
#173544=CARTESIAN_POINT('Ctrl Pts',(-70.0467999358747,1.65447760545227,
125.121462080189));
#173545=CARTESIAN_POINT('Ctrl Pts',(-70.0393925895208,1.80505653262137,
125.167473907267));
#173546=CARTESIAN_POINT('Ctrl Pts',(-70.0319852431671,1.95367506892302,
125.219462741367));
#173547=CARTESIAN_POINT('Ctrl Pts',(-70.0245834214917,2.10218275991302,
125.271412800234));
#173548=CARTESIAN_POINT('Ctrl Pts',(-70.0171815998163,2.24873262049636,
125.329330867157));
#173549=CARTESIAN_POINT('Ctrl Pts',(-70.0097797781409,2.39281423635623,
125.393041869535));
#173550=CARTESIAN_POINT('Ctrl Pts',(-70.0023818638296,2.53681979265281,
125.456719239371));
#173551=CARTESIAN_POINT('Ctrl Pts',(-69.9949839495182,2.67835935860231,
125.526183303835));
#173552=CARTESIAN_POINT('Ctrl Pts',(-69.9875860352068,2.81694137850027,
125.601210434014));
#173553=CARTESIAN_POINT('Ctrl Pts',(-69.9801893502947,2.95550036858065,
125.676225096046));
#173554=CARTESIAN_POINT('Ctrl Pts',(-69.9727926653825,3.09110246011843,
125.756800811423));
#173555=CARTESIAN_POINT('Ctrl Pts',(-69.9653959804703,3.22327954342664,
125.842667403811));
#173556=CARTESIAN_POINT('Ctrl Pts',(-69.9579996235349,3.35545076586466,
125.928530188783));
#173557=CARTESIAN_POINT('Ctrl Pts',(-69.9506032665994,3.48419696899745,
126.019683180935));
#173558=CARTESIAN_POINT('Ctrl Pts',(-69.9432069096639,3.60907818750902,
126.115812313565));
#173559=CARTESIAN_POINT('Ctrl Pts',(-69.9358094203273,3.73397852565341,
126.211956163811));
#173560=CARTESIAN_POINT('Ctrl Pts',(-69.9284119309909,3.85501240511799,
126.313077443782));
#173561=CARTESIAN_POINT('Ctrl Pts',(-69.9210144416543,3.97177229566804,
126.418821267171));
#173562=CARTESIAN_POINT('Ctrl Pts',(-69.9136143591393,4.08857311621772,
126.524602158894));
#173563=CARTESIAN_POINT('Ctrl Pts',(-69.9062142766242,4.20109668834899,
126.63500856986));
#173564=CARTESIAN_POINT('Ctrl Pts',(-69.8988141941091,4.308971865099,126.749648293826));
#173565=CARTESIAN_POINT('Ctrl Pts',(-69.8914059744427,4.41696566169522,
126.864414075955));
#173566=CARTESIAN_POINT('Ctrl Pts',(-69.8839977547763,4.52030059915588,
126.983422195323));
#173567=CARTESIAN_POINT('Ctrl Pts',(-69.8765895351098,4.61864493981229,
127.106246303156));
#173568=CARTESIAN_POINT('Ctrl Pts',(-69.8691767558078,4.71704980976927,
127.229146007177));
#173569=CARTESIAN_POINT('Ctrl Pts',(-69.8617639765057,4.81045774133546,
127.355866079909));
#173570=CARTESIAN_POINT('Ctrl Pts',(-69.8543511972036,4.89858028652564,
127.485951098088));
#173571=CARTESIAN_POINT('Ctrl Pts',(-69.8469278261749,4.98682874534118,
127.616221987842));
#173572=CARTESIAN_POINT('Ctrl Pts',(-69.8395044551461,5.06977653839243,
127.749867109348));
#173573=CARTESIAN_POINT('Ctrl Pts',(-69.8320810841174,5.14718071735724,
127.88640564441));
#173574=CARTESIAN_POINT('Ctrl Pts',(-69.8281450346766,5.18822227033221,
127.958801651897));
#173575=CARTESIAN_POINT('Ctrl Pts',(-69.8242089852357,5.22770610811614,
128.032010742314));
#173576=CARTESIAN_POINT('Ctrl Pts',(-69.8202729357949,5.26560155154211,
128.105959079081));
#173577=CARTESIAN_POINT('Ctrl Pts',(-69.8128496693895,5.33707117516701,
128.245423334375));
#173578=CARTESIAN_POINT('Ctrl Pts',(-69.8054264029841,5.40310428523581,
128.387939844073));
#173579=CARTESIAN_POINT('Ctrl Pts',(-69.7980031365786,5.46342912107124,
128.533045403526));
#173580=CARTESIAN_POINT('Ctrl Pts',(-69.7905886438576,5.52368265796054,
128.677979460258));
#173581=CARTESIAN_POINT('Ctrl Pts',(-69.7831741511366,5.57824120807032,
128.825496134384));
#173582=CARTESIAN_POINT('Ctrl Pts',(-69.7757596584156,5.62687856637098,
128.975107173722));
#173583=CARTESIAN_POINT('Ctrl Pts',(-69.7683523120618,5.67546904615455,
129.124574012308));
#173584=CARTESIAN_POINT('Ctrl Pts',(-69.760944965708,5.71814958114104,129.27613084479));
#173585=CARTESIAN_POINT('Ctrl Pts',(-69.7535376193542,5.7547418516929,129.429269063205));
#173586=CARTESIAN_POINT('Ctrl Pts',(-69.7461357976788,5.79130683034868,
129.582293065359));
#173587=CARTESIAN_POINT('Ctrl Pts',(-69.7387339760035,5.82179249964607,
129.736895743475));
#173588=CARTESIAN_POINT('Ctrl Pts',(-69.7313321543281,5.84607026171702,
129.892553040515));
#173589=CARTESIAN_POINT('Ctrl Pts',(-69.7239342400167,5.87033520774649,
130.04812816728));
#173590=CARTESIAN_POINT('Ctrl Pts',(-69.7165363257053,5.88839871568098,
130.204756436319));
#173591=CARTESIAN_POINT('Ctrl Pts',(-69.709138411394,5.90018323299076,130.361903411008));
#173592=CARTESIAN_POINT('Ctrl Pts',(-69.7017417264817,5.91196579192751,
130.519024270721));
#173593=CARTESIAN_POINT('Ctrl Pts',(-69.6943450415694,5.91747140329958,
130.676663293115));
#173594=CARTESIAN_POINT('Ctrl Pts',(-69.6869483566572,5.91667434938848,
130.834280607346));
#173595=CARTESIAN_POINT('Ctrl Pts',(-69.6795519997218,5.91587733081959,
130.991890932659));
#173596=CARTESIAN_POINT('Ctrl Pts',(-69.6721556427864,5.90877820452963,
131.14947917843));
#173597=CARTESIAN_POINT('Ctrl Pts',(-69.664759285851,5.89540339172789,131.306505428655));
#173598=CARTESIAN_POINT('Ctrl Pts',(-69.6573617965144,5.88202653120816,
131.463555719999));
#173599=CARTESIAN_POINT('Ctrl Pts',(-69.6499643071779,5.86237210273223,
131.6200434725));
#173600=CARTESIAN_POINT('Ctrl Pts',(-69.6425668178413,5.83651840215569,
131.77543399471));
#173601=CARTESIAN_POINT('Ctrl Pts',(-69.6351667353263,5.81065563860442,
131.930878988827));
#173602=CARTESIAN_POINT('Ctrl Pts',(-69.6277666528113,5.77858933746478,
132.085225618848));
#173603=CARTESIAN_POINT('Ctrl Pts',(-69.6203665702963,5.74044885895687,
132.237949631266));
#173604=CARTESIAN_POINT('Ctrl Pts',(-69.6129583506298,5.70226644107197,
132.390841579436));
#173605=CARTESIAN_POINT('Ctrl Pts',(-69.6055501309633,5.65799659755602,
132.542106984372));
#173606=CARTESIAN_POINT('Ctrl Pts',(-69.5981419112969,5.60781871539539,
132.691236293852));
#173607=CARTESIAN_POINT('Ctrl Pts',(-69.5907291319948,5.55760994958561,
132.840457389934));
#173608=CARTESIAN_POINT('Ctrl Pts',(-69.5833163526927,5.50148603212475,
132.987539422832));
#173609=CARTESIAN_POINT('Ctrl Pts',(-69.5759035733907,5.43967421031951,
133.13199354569));
#173610=CARTESIAN_POINT('Ctrl Pts',(-69.5684802023619,5.37777406888441,
133.276654071373));
#173611=CARTESIAN_POINT('Ctrl Pts',(-69.5610568313332,5.31016995139102,
133.418678851508));
#173612=CARTESIAN_POINT('Ctrl Pts',(-69.5536334603044,5.23713506430395,
133.557603592811));
#173613=CARTESIAN_POINT('Ctrl Pts',(-69.5496974108637,5.1984102147228,133.631264824103));
#173614=CARTESIAN_POINT('Ctrl Pts',(-69.5457613614229,5.1581593123346,133.704054996672));
#173615=CARTESIAN_POINT('Ctrl Pts',(-69.5418253119821,5.11642789510683,
133.775908388791));
#173616=CARTESIAN_POINT('Ctrl Pts',(-69.5344020455767,5.03772374460734,
133.911421643862));
#173617=CARTESIAN_POINT('Ctrl Pts',(-69.5269787791712,4.95351307766139,
134.044010824169));
#173618=CARTESIAN_POINT('Ctrl Pts',(-69.5195555127658,4.86403870817574,
134.17319691633));
#173619=CARTESIAN_POINT('Ctrl Pts',(-69.5121410200448,4.77467008996419,
134.302230321259));
#173620=CARTESIAN_POINT('Ctrl Pts',(-69.5047265273237,4.68005036313393,
134.427868340304));
#173621=CARTESIAN_POINT('Ctrl Pts',(-69.4973120346027,4.58046803872867,
134.54965674854));
#173622=CARTESIAN_POINT('Ctrl Pts',(-69.4899046882489,4.48098169551717,
134.671327772521));
#173623=CARTESIAN_POINT('Ctrl Pts',(-69.4824973418952,4.37654251172839,
134.789156285318));
#173624=CARTESIAN_POINT('Ctrl Pts',(-69.4750899955415,4.26748200752502,
134.902717346543));
#173625=CARTESIAN_POINT('Ctrl Pts',(-69.4676881738661,4.1585028447603,135.016193709644));
#173626=CARTESIAN_POINT('Ctrl Pts',(-69.4602863521906,4.04490948199505,
135.125408690525));
#173627=CARTESIAN_POINT('Ctrl Pts',(-69.4528845305152,3.92707331296834,
135.229970830528));
#173628=CARTESIAN_POINT('Ctrl Pts',(-69.4454866162039,3.80929934873836,
135.334477772991));
#173629=CARTESIAN_POINT('Ctrl Pts',(-69.4380887018926,3.68728731731776,
135.434336519075));
#173630=CARTESIAN_POINT('Ctrl Pts',(-69.4306907875812,3.56144493633774,
135.529192945589));
#173631=CARTESIAN_POINT('Ctrl Pts',(-69.423294102669,3.43562346807806,135.624033608687));
#173632=CARTESIAN_POINT('Ctrl Pts',(-69.4158974177568,3.30597321139763,
135.713873377613));
#173633=CARTESIAN_POINT('Ctrl Pts',(-69.4085007328446,3.17293447387337,
135.798398801942));
#173634=CARTESIAN_POINT('Ctrl Pts',(-69.4011043759092,3.03990163542576,
135.882920478326));
#173635=CARTESIAN_POINT('Ctrl Pts',(-69.3937080189737,2.90348092996179,
135.962128078467));
#173636=CARTESIAN_POINT('Ctrl Pts',(-69.3863116620382,2.76414088541546,
136.035751993488));
#173637=CARTESIAN_POINT('Ctrl Pts',(-69.3789141727016,2.62477950755278,
136.109387180519));
#173638=CARTESIAN_POINT('Ctrl Pts',(-69.371516683365,2.48249823073304,136.177436805853));
#173639=CARTESIAN_POINT('Ctrl Pts',(-69.3641191940284,2.33778922683581,
136.239677728222));
#173640=CARTESIAN_POINT('Ctrl Pts',(-69.3567191115135,2.19302949542282,
136.30194046905));
#173641=CARTESIAN_POINT('Ctrl Pts',(-69.3493190289986,2.04584068523556,
136.358390305388));
#173642=CARTESIAN_POINT('Ctrl Pts',(-69.3419189464837,1.89673378795444,
136.408852699828));
#173643=CARTESIAN_POINT('Ctrl Pts',(-69.3345107268172,1.74746293230992,
136.459370582858));
#173644=CARTESIAN_POINT('Ctrl Pts',(-69.3271025071507,1.59627013130651,
136.503887755952));
#173645=CARTESIAN_POINT('Ctrl Pts',(-69.3196942874842,1.44368104870872,
136.542279717039));
#173646=CARTESIAN_POINT('Ctrl Pts',(-69.3122815081821,1.29099805007645,
136.580695307738));
#173647=CARTESIAN_POINT('Ctrl Pts',(-69.30486872888,1.13691742192892,136.612978097926));
#173648=CARTESIAN_POINT('Ctrl Pts',(-69.297455949578,0.98197327769154,136.639055043532));
#173649=CARTESIAN_POINT('Ctrl Pts',(-69.2900325785492,0.826807741994932,
136.665169249101));
#173650=CARTESIAN_POINT('Ctrl Pts',(-69.2826092075204,0.670776595288852,
136.685059853217));
#173651=CARTESIAN_POINT('Ctrl Pts',(-69.2751858364916,0.514418135430624,
136.698705750356));
#173652=CARTESIAN_POINT('Ctrl Pts',(-69.2712497870508,0.431513128242939,
136.705941132447));
#173653=CARTESIAN_POINT('Ctrl Pts',(-69.26731373761,0.348516098610012,136.711421774576));
#173654=CARTESIAN_POINT('Ctrl Pts',(-69.2633776881692,0.26550695446625,
136.715150464924));
#173655=CARTESIAN_POINT('Ctrl Pts',(-69.2559544217638,0.108954299240561,
136.722182658552));
#173656=CARTESIAN_POINT('Ctrl Pts',(-69.2485311553583,-0.0481146557159442,
136.723001530107));
#173657=CARTESIAN_POINT('Ctrl Pts',(-69.2411078889529,-0.205165656030647,
136.717552447372));
#173658=CARTESIAN_POINT('Ctrl Pts',(-69.2336933962319,-0.362031035105474,
136.712109805));
#173659=CARTESIAN_POINT('Ctrl Pts',(-69.226278903511,-0.518878132348524,
136.700413967222));
#173660=CARTESIAN_POINT('Ctrl Pts',(-69.21886441079,-0.675168848197389,
136.68246214688));
#173661=CARTESIAN_POINT('Ctrl Pts',(-69.2114570644362,-0.831308925170076,
136.664527629179));
#173662=CARTESIAN_POINT('Ctrl Pts',(-69.2040497180825,-0.986893319969474,
136.640349175274));
#173663=CARTESIAN_POINT('Ctrl Pts',(-69.1966423717287,-1.14138532346651,
136.609976011809));
#173664=CARTESIAN_POINT('Ctrl Pts',(-69.1892405500533,-1.29576210099913,
136.579625501795));
#173665=CARTESIAN_POINT('Ctrl Pts',(-69.181838728378,-1.44904774479013,
136.54308955346));
#173666=CARTESIAN_POINT('Ctrl Pts',(-69.1744369067026,-1.60071216219591,
136.500469037909));
#173667=CARTESIAN_POINT('Ctrl Pts',(-69.1670389923912,-1.75229651713629,
136.457871021395));
#173668=CARTESIAN_POINT('Ctrl Pts',(-69.1596410780798,-1.9022609916559,
136.409194935244));
#173669=CARTESIAN_POINT('Ctrl Pts',(-69.1522431637685,-2.05008727054761,
136.354592391613));
#173670=CARTESIAN_POINT('Ctrl Pts',(-69.1448464788563,-2.19788898339319,
136.299998921933));
#173671=CARTESIAN_POINT('Ctrl Pts',(-69.1374497939441,-2.34355285600365,
136.239481078665));
#173672=CARTESIAN_POINT('Ctrl Pts',(-69.130053109032,-2.48657717665965,
136.173239877432));
#173673=CARTESIAN_POINT('Ctrl Pts',(-69.1226567520966,-2.6295951554672,
136.107001613403));
#173674=CARTESIAN_POINT('Ctrl Pts',(-69.1152603951612,-2.76997347630487,
136.035040652891));
#173675=CARTESIAN_POINT('Ctrl Pts',(-69.1078640382258,-2.90723205879644,
135.957605451533));
#173676=CARTESIAN_POINT('Ctrl Pts',(-69.1004665488893,-3.0445116559274,
135.880158394648));
#173677=CARTESIAN_POINT('Ctrl Pts',(-69.0930690595527,-3.17867023851975,
135.797235611542));
#173678=CARTESIAN_POINT('Ctrl Pts',(-69.0856715702162,-3.30925404058336,
135.709130567052));
#173679=CARTESIAN_POINT('Ctrl Pts',(-69.0782714877013,-3.43988361859653,
135.620994637475));
#173680=CARTESIAN_POINT('Ctrl Pts',(-69.0708714051863,-3.5669356118435,
135.527673038265));
#173681=CARTESIAN_POINT('Ctrl Pts',(-69.0634713226713,-3.68998697357453,
135.429501339463));
#173682=CARTESIAN_POINT('Ctrl Pts',(-69.0560631030049,-3.81317364292777,
135.331221690786));
#173683=CARTESIAN_POINT('Ctrl Pts',(-69.0486548833384,-3.93235060347521,
135.228081524749));
#173684=CARTESIAN_POINT('Ctrl Pts',(-69.0412466636719,-4.04712897399369,
135.120455800757));
#173685=CARTESIAN_POINT('Ctrl Pts',(-69.0338338843699,-4.1619779886842,
135.012763834926));
#173686=CARTESIAN_POINT('Ctrl Pts',(-69.0264211050679,-4.27242275750764,
134.900581075324));
#173687=CARTESIAN_POINT('Ctrl Pts',(-69.0190083257659,-4.37811312506494,
134.784317404597));
#173688=CARTESIAN_POINT('Ctrl Pts',(-69.0115849547371,-4.48395450797564,
134.667887610885));
#173689=CARTESIAN_POINT('Ctrl Pts',(-69.0041615837084,-4.58502768261678,
134.54736554551));
#173690=CARTESIAN_POINT('Ctrl Pts',(-68.9967382126797,-4.68102392917194,
134.423192685654));
#173691=CARTESIAN_POINT('Ctrl Pts',(-68.9928021632386,-4.73192344249798,
134.357353255865));
#173692=CARTESIAN_POINT('Ctrl Pts',(-68.9888661137975,-4.78139638377557,
134.290487925176));
#173693=CARTESIAN_POINT('Ctrl Pts',(-68.9849300643564,-4.82940190659136,
134.222665429474));
#173694=CARTESIAN_POINT('Ctrl Pts',(-68.9774294548569,-4.92088212955422,
134.093421611996));
#173695=CARTESIAN_POINT('Ctrl Pts',(-68.9699288453573,-5.00730510338989,
133.960313065865));
#173696=CARTESIAN_POINT('Ctrl Pts',(-68.9624282358577,-5.08833070564033,
133.823768041637));
#173697=CARTESIAN_POINT('Ctrl Pts',(-68.9549368819826,-5.16925632367674,
133.687391511645));
#173698=CARTESIAN_POINT('Ctrl Pts',(-68.9474455281075,-5.24479764593728,
133.547587254532));
#173699=CARTESIAN_POINT('Ctrl Pts',(-68.9399541742324,-5.31465601959238,
133.404814800187));
#173700=CARTESIAN_POINT('Ctrl Pts',(-68.9324706909269,-5.38444099861082,
133.262192345503));
#173701=CARTESIAN_POINT('Ctrl Pts',(-68.9249872076214,-5.44855475875408,
133.116608226452));
#173702=CARTESIAN_POINT('Ctrl Pts',(-68.917503724316,-5.50674305299424,
132.968549036073));
#173703=CARTESIAN_POINT('Ctrl Pts',(-68.9100267317162,-5.5648808783445,
132.820618262982));
#173704=CARTESIAN_POINT('Ctrl Pts',(-68.9025497391166,-5.61710334055933,
132.670217029963));
#173705=CARTESIAN_POINT('Ctrl Pts',(-68.8950727465169,-5.66320309338228,
132.517854500136));
#173706=CARTESIAN_POINT('Ctrl Pts',(-68.8876014915568,-5.70926747051557,
132.365608889148));
#173707=CARTESIAN_POINT('Ctrl Pts',(-68.8801302365967,-5.7492183963796,
132.211405327029));
#173708=CARTESIAN_POINT('Ctrl Pts',(-68.8726589816366,-5.7828974908347,
132.055770691442));
#173709=CARTESIAN_POINT('Ctrl Pts',(-68.8651911165758,-5.81656130422431,
131.900206671264));
#173710=CARTESIAN_POINT('Ctrl Pts',(-68.8577232515151,-5.84395887749384,
131.743213225079));
#173711=CARTESIAN_POINT('Ctrl Pts',(-68.8502553864543,-5.86498226780924,
131.585330246158));
#173712=CARTESIAN_POINT('Ctrl Pts',(-68.8427890124123,-5.88600146063689,
131.427478789834));
#173713=CARTESIAN_POINT('Ctrl Pts',(-68.8353226383703,-5.90064895462738,
131.268738513768));
#173714=CARTESIAN_POINT('Ctrl Pts',(-68.8278562643284,-5.90886828661765,
131.109657413986));
#173715=CARTESIAN_POINT('Ctrl Pts',(-68.823029240287,-5.9141820993062,131.006811201236));
#173716=CARTESIAN_POINT('Ctrl Pts',(-68.8182022162455,-5.91681021654618,
130.903822693668));
#173717=CARTESIAN_POINT('Ctrl Pts',(-68.8133751922041,-5.91674895302827,
130.80084076829));
#173718=CARTESIAN_POINT('',(-67.0633766192359,-5.92092402712534,130.801027289785));
#173719=CARTESIAN_POINT('Ctrl Pts',(-68.8133731068898,-5.90906110029032,
130.800800910513));
#173720=CARTESIAN_POINT('Ctrl Pts',(-68.7777428847743,-5.91314900340379,
130.04163462849));
#173721=CARTESIAN_POINT('Ctrl Pts',(-68.6492967880541,-5.42415644322105,
127.3099351127));
#173722=CARTESIAN_POINT('Ctrl Pts',(-68.4280348167307,-1.30296673267659,
123.928327006259));
#173723=CARTESIAN_POINT('Ctrl Pts',(-68.1495871929176,5.08071647084124,
125.991473680054));
#173724=CARTESIAN_POINT('Ctrl Pts',(-67.8711395691046,6.79546944445906,
132.477428326834));
#173725=CARTESIAN_POINT('Ctrl Pts',(-67.592691945292,2.26551797575204,137.425915482692));
#173726=CARTESIAN_POINT('Ctrl Pts',(-67.3234379964852,-4.12802629246645,
136.327038353622));
#173727=CARTESIAN_POINT('Ctrl Pts',(-67.146999922283,-5.91212555947519,
132.571180631677));
#173728=CARTESIAN_POINT('Ctrl Pts',(-67.0633777226851,-5.92415232255569,
130.801048813814));
#173729=CARTESIAN_POINT('',(-65.3133743315069,-5.91862889358278,130.80948552551));
#173730=CARTESIAN_POINT('Ctrl Pts',(-67.0633751922041,-5.91674904530173,
130.800999453909));
#173731=CARTESIAN_POINT('Ctrl Pts',(-67.0541823606914,-5.9166386387428,
130.60664774455));
#173732=CARTESIAN_POINT('Ctrl Pts',(-67.0449895291787,-5.90695304333343,
130.412571862945));
#173733=CARTESIAN_POINT('Ctrl Pts',(-67.035796697666,-5.88776834993849,
130.219455138055));
#173734=CARTESIAN_POINT('Ctrl Pts',(-67.0283734312605,-5.87227659532702,
130.063512228163));
#173735=CARTESIAN_POINT('Ctrl Pts',(-67.020950164855,-5.85056170105724,
129.907949409567));
#173736=CARTESIAN_POINT('Ctrl Pts',(-67.0135268984495,-5.822646217192,129.753303249046));
#173737=CARTESIAN_POINT('Ctrl Pts',(-67.0061124057283,-5.79476372711042,
129.598839867444));
#173738=CARTESIAN_POINT('Ctrl Pts',(-66.9986979130071,-5.76069530068166,
129.445291351149));
#173739=CARTESIAN_POINT('Ctrl Pts',(-66.991283420286,-5.72051534856346,
129.293190637269));
#173740=CARTESIAN_POINT('Ctrl Pts',(-66.9838760739322,-5.6803741233958,
129.141236523784));
#173741=CARTESIAN_POINT('Ctrl Pts',(-66.9764687275783,-5.63413319410368,
128.990727793149));
#173742=CARTESIAN_POINT('Ctrl Pts',(-66.9690613812244,-5.58191824809153,
128.842188547098));
#173743=CARTESIAN_POINT('Ctrl Pts',(-66.9616595595489,-5.52974224595615,
128.693760087222));
#173744=CARTESIAN_POINT('Ctrl Pts',(-66.9542577378734,-5.47160122215931,
128.547298537778));
#173745=CARTESIAN_POINT('Ctrl Pts',(-66.9468559161979,-5.40767102586325,
128.40331404606));
#173746=CARTESIAN_POINT('Ctrl Pts',(-66.9394580018865,-5.34377457782018,
128.259405562635));
#173747=CARTESIAN_POINT('Ctrl Pts',(-66.932060087575,-5.2740951946687,128.117971873066));
#173748=CARTESIAN_POINT('Ctrl Pts',(-66.9246621732635,-5.1988572531239,
127.979504192163));
#173749=CARTESIAN_POINT('Ctrl Pts',(-66.9172654883512,-5.12363181476004,
127.841059522076));
#173750=CARTESIAN_POINT('Ctrl Pts',(-66.9098688034391,-5.04284982938717,
127.705580210085));
#173751=CARTESIAN_POINT('Ctrl Pts',(-66.9024721185268,-4.95678218540968,
127.573533954171));
#173752=CARTESIAN_POINT('Ctrl Pts',(-66.8950757615912,-4.87071835776171,
127.441493553326));
#173753=CARTESIAN_POINT('Ctrl Pts',(-66.8876794046558,-4.77936954135731,
127.312886218616));
#173754=CARTESIAN_POINT('Ctrl Pts',(-66.8802830477202,-4.68305047208488,
127.18815143689));
#173755=CARTESIAN_POINT('Ctrl Pts',(-66.8728855583836,-4.58671665611692,
127.06339755795));
#173756=CARTESIAN_POINT('Ctrl Pts',(-66.8654880690468,-4.48541130027901,
126.942517708014));
#173757=CARTESIAN_POINT('Ctrl Pts',(-66.8580905797102,-4.37948991066,126.825918876768));
#173758=CARTESIAN_POINT('Ctrl Pts',(-66.8506904971951,-4.2735313904619,
126.709279171981));
#173759=CARTESIAN_POINT('Ctrl Pts',(-66.8432904146799,-4.16295386562101,
126.596923749914));
#173760=CARTESIAN_POINT('Ctrl Pts',(-66.8358903321648,-4.04815010674773,
126.489223160226));
#173761=CARTESIAN_POINT('Ctrl Pts',(-66.8284821124982,-3.93322010933962,
126.381404142669));
#173762=CARTESIAN_POINT('Ctrl Pts',(-66.8210738928317,-3.81405486959446,
126.278250434967));
#173763=CARTESIAN_POINT('Ctrl Pts',(-66.8136656731651,-3.69108124064205,
126.180093125575));
#173764=CARTESIAN_POINT('Ctrl Pts',(-66.806252893863,-3.56803192347277,
126.081875401998));
#173765=CARTESIAN_POINT('Ctrl Pts',(-66.7988401145608,-3.44116984650735,
125.988660424976));
#173766=CARTESIAN_POINT('Ctrl Pts',(-66.7914273352586,-3.31095087144901,
125.900735949083));
#173767=CARTESIAN_POINT('Ctrl Pts',(-66.7840039642298,-3.18054583341263,
125.812685842577));
#173768=CARTESIAN_POINT('Ctrl Pts',(-66.776580593201,-3.04677463424182,
125.729941530703));
#173769=CARTESIAN_POINT('Ctrl Pts',(-66.7691572221722,-2.91011846130336,
125.652745229779));
#173770=CARTESIAN_POINT('Ctrl Pts',(-66.7652211727325,-2.83766007941345,
125.611813898742));
#173771=CARTESIAN_POINT('Ctrl Pts',(-66.7612851232929,-2.76439098611254,
125.572441518465));
#173772=CARTESIAN_POINT('Ctrl Pts',(-66.7573490738532,-2.69038506458434,
125.534658655713));
#173773=CARTESIAN_POINT('Ctrl Pts',(-66.7499258074478,-2.55081220618745,
125.463401355704));
#173774=CARTESIAN_POINT('Ctrl Pts',(-66.7425025410424,-2.40819537036832,
125.397585207967));
#173775=CARTESIAN_POINT('Ctrl Pts',(-66.735079274637,-2.26299817481437,
125.337481267947));
#173776=CARTESIAN_POINT('Ctrl Pts',(-66.727664781916,-2.11797259028748,
125.277448365793));
#173777=CARTESIAN_POINT('Ctrl Pts',(-66.7202502891949,-1.97037305815825,
125.223114374127));
#173778=CARTESIAN_POINT('Ctrl Pts',(-66.7128357964739,-1.82068817428747,
125.174704754682));
#173779=CARTESIAN_POINT('Ctrl Pts',(-66.7054284501201,-1.67114756234329,
125.12634179425));
#173780=CARTESIAN_POINT('Ctrl Pts',(-66.6980211037663,-1.51952595285366,
125.083891952386));
#173781=CARTESIAN_POINT('Ctrl Pts',(-66.6906137574126,-1.36633222456315,
125.047532774507));
#173782=CARTESIAN_POINT('Ctrl Pts',(-66.6832119357372,-1.2132527539351,
125.011200714675));
#173783=CARTESIAN_POINT('Ctrl Pts',(-66.6758101140618,-1.05860386084746,
124.980950359637));
#173784=CARTESIAN_POINT('Ctrl Pts',(-66.6684082923864,-0.902909797435244,
124.956909509588));
#173785=CARTESIAN_POINT('Ctrl Pts',(-66.6610103780751,-0.747297923707401,
124.932881350516));
#173786=CARTESIAN_POINT('Ctrl Pts',(-66.6536124637637,-0.590642346458045,
124.915056225062));
#173787=CARTESIAN_POINT('Ctrl Pts',(-66.6462145494524,-0.433477619714073,
124.903510872342));
#173788=CARTESIAN_POINT('Ctrl Pts',(-66.6388178645402,-0.276339010896203,
124.891967438251));
#173789=CARTESIAN_POINT('Ctrl Pts',(-66.631421179628,-0.118691792442532,
124.886701733012));
#173790=CARTESIAN_POINT('Ctrl Pts',(-66.6240244947158,0.0389241262890107,
124.88773865272));
#173791=CARTESIAN_POINT('Ctrl Pts',(-66.6166281377804,0.196533056165548,
124.888775526451));
#173792=CARTESIAN_POINT('Ctrl Pts',(-66.6092317808449,0.354110315790006,
124.896114467004));
#173793=CARTESIAN_POINT('Ctrl Pts',(-66.6018354239094,0.511116029992645,
124.90972823154));
#173794=CARTESIAN_POINT('Ctrl Pts',(-66.5944379345729,0.668145782170946,
124.923344080378));
#173795=CARTESIAN_POINT('Ctrl Pts',(-66.5870404452363,0.824603442766855,
124.943236633815));
#173796=CARTESIAN_POINT('Ctrl Pts',(-66.5796429558997,0.979954440106066,
124.969326782376));
#173797=CARTESIAN_POINT('Ctrl Pts',(-66.5722428733847,1.13535989549657,
124.995426076798));
#173798=CARTESIAN_POINT('Ctrl Pts',(-66.5648427908696,1.28965754733386,
125.027727230101));
#173799=CARTESIAN_POINT('Ctrl Pts',(-66.5574427083546,1.44232333958396,
125.066100084391));
#173800=CARTESIAN_POINT('Ctrl Pts',(-66.5500344886882,1.59515700356729,
125.10451513358));
#173801=CARTESIAN_POINT('Ctrl Pts',(-66.5426262690219,1.74635486217521,
125.149015126028));
#173802=CARTESIAN_POINT('Ctrl Pts',(-66.5352180493554,1.8954076367711,125.199419899506));
#173803=CARTESIAN_POINT('Ctrl Pts',(-66.5278052700533,2.04455215086288,
125.249855696281));
#173804=CARTESIAN_POINT('Ctrl Pts',(-66.5203924907512,2.1915486023942,125.306203382567));
#173805=CARTESIAN_POINT('Ctrl Pts',(-66.5129797114491,2.33590849090625,
125.36823496738));
#173806=CARTESIAN_POINT('Ctrl Pts',(-66.5055563404204,2.4804746475966,125.43035518583));
#173807=CARTESIAN_POINT('Ctrl Pts',(-66.4981329693916,2.62239638131092,
125.498175362577));
#173808=CARTESIAN_POINT('Ctrl Pts',(-66.4907095983629,2.76120981507606,
125.571421584897));
#173809=CARTESIAN_POINT('Ctrl Pts',(-66.4867735489219,2.83481202844313,
125.610258489492));
#173810=CARTESIAN_POINT('Ctrl Pts',(-66.482837499481,2.90754086170374,125.650620119523));
#173811=CARTESIAN_POINT('Ctrl Pts',(-66.4789014500401,2.97933066250755,
125.69246083706));
#173812=CARTESIAN_POINT('Ctrl Pts',(-66.4714781836347,3.11472398633657,
125.771371124527));
#173813=CARTESIAN_POINT('Ctrl Pts',(-66.4640549172293,3.24718485880746,
125.85578347212));
#173814=CARTESIAN_POINT('Ctrl Pts',(-66.4566316508239,3.37623463661398,
125.945454337236));
#173815=CARTESIAN_POINT('Ctrl Pts',(-66.4492171581029,3.50513188830024,
126.035019218837));
#173816=CARTESIAN_POINT('Ctrl Pts',(-66.4418026653818,3.63062576674194,
126.129830035777));
#173817=CARTESIAN_POINT('Ctrl Pts',(-66.4343881726608,3.75226248660205,
126.229597586092));
#173818=CARTESIAN_POINT('Ctrl Pts',(-66.426980826307,3.87378196841203,126.329268976687));
#173819=CARTESIAN_POINT('Ctrl Pts',(-66.4195734799533,3.99145140610673,
126.433887354475));
#173820=CARTESIAN_POINT('Ctrl Pts',(-66.4121661335995,4.10484636430756,
126.543120552992));
#173821=CARTESIAN_POINT('Ctrl Pts',(-66.4047643119241,4.21815674827041,
126.652272281268));
#173822=CARTESIAN_POINT('Ctrl Pts',(-66.3973624902487,4.32719873292128,
126.766031719103));
#173823=CARTESIAN_POINT('Ctrl Pts',(-66.3899606685733,4.43158142525334,
126.884026877455));
#173824=CARTESIAN_POINT('Ctrl Pts',(-66.3825627542619,4.53590901477448,
127.001959747082));
#173825=CARTESIAN_POINT('Ctrl Pts',(-66.3751648399506,4.63558196368183,
127.124123605227));
#173826=CARTESIAN_POINT('Ctrl Pts',(-66.3677669256392,4.730246769673,127.250110195818));
#173827=CARTESIAN_POINT('Ctrl Pts',(-66.360370240727,4.82489584409095,127.376075849723));
#173828=CARTESIAN_POINT('Ctrl Pts',(-66.3529735558148,4.91453820336326,
127.505862677105));
#173829=CARTESIAN_POINT('Ctrl Pts',(-66.3455768709026,4.99886106750231,
127.63902989388));
#173830=CARTESIAN_POINT('Ctrl Pts',(-66.3381805139672,5.08318019267708,
127.772191205881));
#173831=CARTESIAN_POINT('Ctrl Pts',(-66.3307841570318,5.16218009200584,
127.908732293855));
#173832=CARTESIAN_POINT('Ctrl Pts',(-66.3233878000963,5.23559186994411,
128.048184220113));
#173833=CARTESIAN_POINT('Ctrl Pts',(-66.3159903107598,5.309014887413,128.187657496817));
#173834=CARTESIAN_POINT('Ctrl Pts',(-66.3085928214232,5.37684790606324,
128.330042168823));
#173835=CARTESIAN_POINT('Ctrl Pts',(-66.3011953320866,5.43886853388846,
128.474845725238));
#173836=CARTESIAN_POINT('Ctrl Pts',(-66.2937952495716,5.50091090294861,
128.619700042315));
#173837=CARTESIAN_POINT('Ctrl Pts',(-66.2863951670566,5.55713667760582,
128.766974589103));
#173838=CARTESIAN_POINT('Ctrl Pts',(-66.2789950845416,5.60737209829619,
128.916158108896));
#173839=CARTESIAN_POINT('Ctrl Pts',(-66.2715868648752,5.65766275799601,
129.065505671305));
#173840=CARTESIAN_POINT('Ctrl Pts',(-66.2641786452088,5.70194978983447,
129.216766044789));
#173841=CARTESIAN_POINT('Ctrl Pts',(-66.2567704255423,5.74010949185553,
129.369413376721));
#173842=CARTESIAN_POINT('Ctrl Pts',(-66.2493576462402,5.77829268053645,
129.522154660538));
#173843=CARTESIAN_POINT('Ctrl Pts',(-66.2419448669381,5.81034094885473,
129.676284239173));
#173844=CARTESIAN_POINT('Ctrl Pts',(-66.2345320876361,5.83618206565302,
129.83126788866));
#173845=CARTESIAN_POINT('Ctrl Pts',(-66.2271087166073,5.86206010545083,
129.986472986053));
#173846=CARTESIAN_POINT('Ctrl Pts',(-66.2196853455785,5.88171323368988,
130.142534222191));
#173847=CARTESIAN_POINT('Ctrl Pts',(-66.2122619745498,5.89512116406734,
130.298913267721));
#173848=CARTESIAN_POINT('Ctrl Pts',(-66.208325925109,5.90223037047237,130.381829189925));
#173849=CARTESIAN_POINT('Ctrl Pts',(-66.2043898756682,5.90758469890388,
130.464834464052));
#173850=CARTESIAN_POINT('Ctrl Pts',(-66.2004538262274,5.91118705914763,
130.547849186504));
#173851=CARTESIAN_POINT('Ctrl Pts',(-66.1930305598219,5.91798099814152,
130.704412362246));
#173852=CARTESIAN_POINT('Ctrl Pts',(-66.1856072934165,5.91856083653682,
130.861482381503));
#173853=CARTESIAN_POINT('Ctrl Pts',(-66.1781840270111,5.91287275522387,
131.018524907379));
#173854=CARTESIAN_POINT('Ctrl Pts',(-66.1707695342901,5.90719139675067,
131.175381822032));
#173855=CARTESIAN_POINT('Ctrl Pts',(-66.1633550415692,5.89525687793374,
131.332210938575));
#173856=CARTESIAN_POINT('Ctrl Pts',(-66.1559405488482,5.87706723051589,
131.488474153828));
#173857=CARTESIAN_POINT('Ctrl Pts',(-66.1485332024944,5.85889511496505,
131.64458675671));
#173858=CARTESIAN_POINT('Ctrl Pts',(-66.1411258561406,5.83447991609504,
131.800134175855));
#173859=CARTESIAN_POINT('Ctrl Pts',(-66.1337185097868,5.80387167727135,
131.954579777669));
#173860=CARTESIAN_POINT('Ctrl Pts',(-66.1263166881114,5.77328626722696,
132.108910188126));
#173861=CARTESIAN_POINT('Ctrl Pts',(-66.1189148664361,5.73651708654385,
132.262140052921));
#173862=CARTESIAN_POINT('Ctrl Pts',(-66.1115130447607,5.69366581292043,
132.413739433532));
#173863=CARTESIAN_POINT('Ctrl Pts',(-66.1041151304493,5.65083716015079,
132.565258786011));
#173864=CARTESIAN_POINT('Ctrl Pts',(-66.0967172161379,5.6019329099643,132.715149010157));
#173865=CARTESIAN_POINT('Ctrl Pts',(-66.0893193018265,5.54710546312941,
132.862892022092));
#173866=CARTESIAN_POINT('Ctrl Pts',(-66.0819226169143,5.49228712762151,
133.010610481819));
#173867=CARTESIAN_POINT('Ctrl Pts',(-66.0745259320022,5.43154767881375,
133.156182087898));
#173868=CARTESIAN_POINT('Ctrl Pts',(-66.06712924709,5.36508889561729,133.299105435102));
#173869=CARTESIAN_POINT('Ctrl Pts',(-66.0597328901545,5.29863305927292,
133.442022444936));
#173870=CARTESIAN_POINT('Ctrl Pts',(-66.052336533219,5.22645855018246,133.582291090886));
#173871=CARTESIAN_POINT('Ctrl Pts',(-66.0449401762836,5.14881455429579,
133.719431671241));
#173872=CARTESIAN_POINT('Ctrl Pts',(-66.037542686947,5.07115867091514,133.856593248168));
#173873=CARTESIAN_POINT('Ctrl Pts',(-66.0301451976104,4.98803181730729,
133.990625481047));
#173874=CARTESIAN_POINT('Ctrl Pts',(-66.0227477082739,4.89972814852321,
134.121075051018));
#173875=CARTESIAN_POINT('Ctrl Pts',(-66.0153476257589,4.8113935250248,134.251570349883));
#173876=CARTESIAN_POINT('Ctrl Pts',(-66.0079475432438,4.71787868237357,
134.378480176419));
#173877=CARTESIAN_POINT('Ctrl Pts',(-66.0005474607288,4.6195198340263,134.501381995045));
#173878=CARTESIAN_POINT('Ctrl Pts',(-65.9931392410623,4.52105283001387,
134.624418956855));
#173879=CARTESIAN_POINT('Ctrl Pts',(-65.9857310213959,4.41773141636521,
134.743438817623));
#173880=CARTESIAN_POINT('Ctrl Pts',(-65.9783228017295,4.30993114385929,
134.858053267199));
#173881=CARTESIAN_POINT('Ctrl Pts',(-65.9709100224274,4.20206452208423,
134.972738260057));
#173882=CARTESIAN_POINT('Ctrl Pts',(-65.9634972431253,4.08971381425009,
135.083012177924));
#173883=CARTESIAN_POINT('Ctrl Pts',(-65.9560844638232,3.97328943540592,
135.188525489579));
#173884=CARTESIAN_POINT('Ctrl Pts',(-65.9486610927945,3.85669870394948,
135.294189563601));
#173885=CARTESIAN_POINT('Ctrl Pts',(-65.9412377217657,3.73602296197024,
135.395079207134));
#173886=CARTESIAN_POINT('Ctrl Pts',(-65.933814350737,3.61170415595693,135.490886372573));
#173887=CARTESIAN_POINT('Ctrl Pts',(-65.9298783012961,3.54578734201899,
135.541685630551));
#173888=CARTESIAN_POINT('Ctrl Pts',(-65.9259422518553,3.47884679936752,
135.591056756885));
#173889=CARTESIAN_POINT('Ctrl Pts',(-65.9220062024144,3.41095132597342,
135.638959009815));
#173890=CARTESIAN_POINT('Ctrl Pts',(-65.914582936009,3.28290258209922,135.729301163862));
#173891=CARTESIAN_POINT('Ctrl Pts',(-65.9071596696035,3.15106854326037,
135.814689180383));
#173892=CARTESIAN_POINT('Ctrl Pts',(-65.8997364031981,3.01586967167639,
135.894788957692));
#173893=CARTESIAN_POINT('Ctrl Pts',(-65.8923219104771,2.88083059393067,
135.974794063717));
#173894=CARTESIAN_POINT('Ctrl Pts',(-65.8849074177562,2.74243491761407,
136.049523183289));
#173895=CARTESIAN_POINT('Ctrl Pts',(-65.8774929250351,2.60113430028143,
136.118683802544));
#173896=CARTESIAN_POINT('Ctrl Pts',(-65.8700855786814,2.45996987380385,
136.187777762191));
#173897=CARTESIAN_POINT('Ctrl Pts',(-65.8626782323275,2.31590641338194,
136.251313743412));
#173898=CARTESIAN_POINT('Ctrl Pts',(-65.8552708859738,2.16942245371716,
136.309043785543));
#173899=CARTESIAN_POINT('Ctrl Pts',(-65.8478690642984,2.02304774731602,
136.366730770431));
#173900=CARTESIAN_POINT('Ctrl Pts',(-65.840467242623,1.87425648207241,136.418620302134));
#173901=CARTESIAN_POINT('Ctrl Pts',(-65.8330654209476,1.72354946955238,
136.464511480264));
#173902=CARTESIAN_POINT('Ctrl Pts',(-65.8256675066363,1.57292201409094,
136.510378432799));
#173903=CARTESIAN_POINT('Ctrl Pts',(-65.8182695923248,1.42038118162624,
136.550253229501));
#173904=CARTESIAN_POINT('Ctrl Pts',(-65.8108716780135,1.26644522713655,
136.583984052459));
#173905=CARTESIAN_POINT('Ctrl Pts',(-65.8034749931013,1.11253485401004,
136.617709269966));
#173906=CARTESIAN_POINT('Ctrl Pts',(-65.7960783081892,0.957230183289539,
136.645292460324));
#173907=CARTESIAN_POINT('Ctrl Pts',(-65.788681623277,0.801062127823096,
136.666632364071));
#173908=CARTESIAN_POINT('Ctrl Pts',(-65.7812852663416,0.644900997011886,
136.687971321584));
#173909=CARTESIAN_POINT('Ctrl Pts',(-65.773888909406,0.487876927435477,
136.703067492386));
#173910=CARTESIAN_POINT('Ctrl Pts',(-65.7664925524706,0.330528196823573,
136.711871233181));
#173911=CARTESIAN_POINT('Ctrl Pts',(-65.759095063134,0.173155375719321,
136.720676321851));
#173912=CARTESIAN_POINT('Ctrl Pts',(-65.7516975737974,0.0154581673463709,
136.723187041426));
#173913=CARTESIAN_POINT('Ctrl Pts',(-65.7443000844609,-0.142023040308535,
136.719405842966));
#173914=CARTESIAN_POINT('Ctrl Pts',(-65.7369000019459,-0.299559452756658,
136.715623319011));
#173915=CARTESIAN_POINT('Ctrl Pts',(-65.7294999194308,-0.456879340773783,
136.705544494598));
#173916=CARTESIAN_POINT('Ctrl Pts',(-65.7220998369158,-0.613445481624306,
136.689223844828));
#173917=CARTESIAN_POINT('Ctrl Pts',(-65.7146916172494,-0.770183783042085,
136.672885248825));
#173918=CARTESIAN_POINT('Ctrl Pts',(-65.707283397583,-0.926166310566384,
136.650291159274));
#173919=CARTESIAN_POINT('Ctrl Pts',(-65.6998751779165,-1.08086337350242,
136.621547646562));
#173920=CARTESIAN_POINT('Ctrl Pts',(-65.6924623986145,-1.23565564989943,
136.592786442698));
#173921=CARTESIAN_POINT('Ctrl Pts',(-65.6850496193124,-1.38916052202344,
136.557868356457));
#173922=CARTESIAN_POINT('Ctrl Pts',(-65.6776368400104,-1.54086207999922,
136.516949751481));
#173923=CARTESIAN_POINT('Ctrl Pts',(-65.6702134689816,-1.69278039627535,
136.475972680083));
#173924=CARTESIAN_POINT('Ctrl Pts',(-65.662790097953,-1.84288989693174,
136.428978077337));
#173925=CARTESIAN_POINT('Ctrl Pts',(-65.6553667269242,-1.99069252992094,
136.376171258086));
#173926=CARTESIAN_POINT('Ctrl Pts',(-65.6514306774834,-2.06906103240837,
136.348171815437));
#173927=CARTESIAN_POINT('Ctrl Pts',(-65.6474946280425,-2.14678135767349,
136.31853914079));
#173928=CARTESIAN_POINT('Ctrl Pts',(-65.6435585786016,-2.22378204153457,
136.28730909391));
#173929=CARTESIAN_POINT('Ctrl Pts',(-65.6361353121962,-2.36900292818556,
136.228410200152));
#173930=CARTESIAN_POINT('Ctrl Pts',(-65.6287120457907,-2.51210180301667,
136.163648798191));
#173931=CARTESIAN_POINT('Ctrl Pts',(-65.6212887793853,-2.65257030671823,
136.093198044678));
#173932=CARTESIAN_POINT('Ctrl Pts',(-65.6138742866643,-2.7928727883138,
136.022830558105));
#173933=CARTESIAN_POINT('Ctrl Pts',(-65.6064597939433,-2.9305507565997,
135.946787270539));
#173934=CARTESIAN_POINT('Ctrl Pts',(-65.5990453012222,-3.06511397943727,
135.865290063385));
#173935=CARTESIAN_POINT('Ctrl Pts',(-65.5916379548685,-3.19954750517444,
135.783871406308));
#173936=CARTESIAN_POINT('Ctrl Pts',(-65.5842306085147,-3.33087194491194,
135.697009486768));
#173937=CARTESIAN_POINT('Ctrl Pts',(-65.5768232621609,-3.45862002262525,
135.604972880767));
#173938=CARTESIAN_POINT('Ctrl Pts',(-65.5694214404855,-3.58627282100237,
135.513004919139));
#173939=CARTESIAN_POINT('Ctrl Pts',(-65.5620196188102,-3.71035426690494,
135.41587017306));
#173940=CARTESIAN_POINT('Ctrl Pts',(-65.5546177971348,-3.83042463626246,
135.313881397917));
#173941=CARTESIAN_POINT('Ctrl Pts',(-65.5472198828235,-3.95043162140679,
135.211946461853));
#173942=CARTESIAN_POINT('Ctrl Pts',(-65.539821968512,-4.06643146314844,
135.105162840933));
#173943=CARTESIAN_POINT('Ctrl Pts',(-65.5324240542006,-4.17801630330618,
134.993884496458));
#173944=CARTESIAN_POINT('Ctrl Pts',(-65.5250273692884,-4.28958260008783,
134.882624644425));
#173945=CARTESIAN_POINT('Ctrl Pts',(-65.5176306843763,-4.39673508738394,
134.766871814636));
#173946=CARTESIAN_POINT('Ctrl Pts',(-65.510233999464,-4.4991016013804,134.647017945894));
#173947=CARTESIAN_POINT('Ctrl Pts',(-65.5028376425286,-4.60146357633835,
134.527169391599));
#173948=CARTESIAN_POINT('Ctrl Pts',(-65.4954412855931,-4.69903975751229,
134.403220443774));
#173949=CARTESIAN_POINT('Ctrl Pts',(-65.4880449286577,-4.79149742632994,
134.275597137306));
#173950=CARTESIAN_POINT('Ctrl Pts',(-65.4806474393211,-4.88396925065285,
134.147954291383));
#173951=CARTESIAN_POINT('Ctrl Pts',(-65.4732499499844,-4.9713207832332,
134.016636269019));
#173952=CARTESIAN_POINT('Ctrl Pts',(-65.4658524606479,-5.05326199330886,
133.88209903879));
#173953=CARTESIAN_POINT('Ctrl Pts',(-65.4584523781328,-5.13523192774869,
133.747514646744));
#173954=CARTESIAN_POINT('Ctrl Pts',(-65.4510522956179,-5.21178756954797,
133.609709118639));
#173955=CARTESIAN_POINT('Ctrl Pts',(-65.4436522131028,-5.2826843681415,
133.469163880303));
#173956=CARTESIAN_POINT('Ctrl Pts',(-65.4362439934364,-5.35365912505335,
133.328464098029));
#173957=CARTESIAN_POINT('Ctrl Pts',(-65.4288357737699,-5.41896244382849,
133.185018922674));
#173958=CARTESIAN_POINT('Ctrl Pts',(-65.4214275541034,-5.47839725372801,
133.039331331657));
#173959=CARTESIAN_POINT('Ctrl Pts',(-65.4140147748013,-5.53786864476129,
132.893554072359));
#173960=CARTESIAN_POINT('Ctrl Pts',(-65.4066019954993,-5.59146420282318,
132.745531997422));
#173961=CARTESIAN_POINT('Ctrl Pts',(-65.3991892161972,-5.63903661918401,
132.595783674803));
#173962=CARTESIAN_POINT('Ctrl Pts',(-65.3917658451685,-5.68667700924425,
132.445821384759));
#173963=CARTESIAN_POINT('Ctrl Pts',(-65.3843424741398,-5.72827697073119,
132.294128279844));
#173964=CARTESIAN_POINT('Ctrl Pts',(-65.376919103111,-5.76374003153909,
132.141234363039));
#173965=CARTESIAN_POINT('Ctrl Pts',(-65.3729830536703,-5.7825433973037,
132.06016633971));
#173966=CARTESIAN_POINT('Ctrl Pts',(-65.3690470042294,-5.79962232311235,
131.978760844448));
#173967=CARTESIAN_POINT('Ctrl Pts',(-65.3651109547887,-5.81496835066423,
131.89709738517));
#173968=CARTESIAN_POINT('Ctrl Pts',(-65.3540312620643,-5.8581663013949,
131.667220690471));
#173969=CARTESIAN_POINT('Ctrl Pts',(-65.34295156934,-5.8877428756825,131.434710068976));
#173970=CARTESIAN_POINT('Ctrl Pts',(-65.3318718766157,-5.90344880502964,
131.200873882028));
#173971=CARTESIAN_POINT('Ctrl Pts',(-65.3257063151452,-5.91218874712461,
131.070750112306));
#173972=CARTESIAN_POINT('Ctrl Pts',(-65.3195407536746,-5.91663417826577,
130.940216236482));
#173973=CARTESIAN_POINT('Ctrl Pts',(-65.3133751922041,-5.91674776606,130.809502146914));
#173974=CARTESIAN_POINT('',(-63.5633751922041,-5.90707449789702,130.805318407263));
#173975=CARTESIAN_POINT('Ctrl Pts',(-65.3133739040115,-5.91956322123172,
130.80947726991));
#173976=CARTESIAN_POINT('Ctrl Pts',(-65.2378037129995,-5.90488233384873,
129.206561386044));
#173977=CARTESIAN_POINT('Ctrl Pts',(-65.0694176473834,-4.40327992023266,
125.61073367988));
#173978=CARTESIAN_POINT('Ctrl Pts',(-64.8082157071628,1.68340731958302,
124.011445166397));
#173979=CARTESIAN_POINT('Ctrl Pts',(-64.5297680833501,6.62499493017222,
128.54892214456));
#173980=CARTESIAN_POINT('Ctrl Pts',(-64.2513204595371,5.47853584893362,
135.159036895121));
#173981=CARTESIAN_POINT('Ctrl Pts',(-63.9728728357242,-0.702430036122883,
137.767416884371));
#173982=CARTESIAN_POINT('Ctrl Pts',(-63.7435577466132,-5.2611549065832,
134.645897948005));
#173983=CARTESIAN_POINT('Ctrl Pts',(-63.6070585321065,-5.90841563450014,
131.736853223252));
#173984=CARTESIAN_POINT('Ctrl Pts',(-63.5633751922041,-5.90707449789702,
130.805318407263));
#173985=CARTESIAN_POINT('',(-61.813375192204,-5.91603704377717,130.798888855257));
#173986=CARTESIAN_POINT('Ctrl Pts',(-63.5633751922041,-5.90707449789702,
130.805318407263));
#173987=CARTESIAN_POINT('Ctrl Pts',(-63.5142426575023,-5.90556606376996,
129.757581059916));
#173988=CARTESIAN_POINT('Ctrl Pts',(-63.3722942481961,-5.13924177134339,
126.728510338679));
#173989=CARTESIAN_POINT('Ctrl Pts',(-63.1375299642854,-0.292763836116973,
123.812089894358));
#173990=CARTESIAN_POINT('Ctrl Pts',(-62.8590823404728,5.72454938625507,
126.778556989137));
#173991=CARTESIAN_POINT('Ctrl Pts',(-62.5806347166597,6.48128138244416,
133.444540947002));
#173992=CARTESIAN_POINT('Ctrl Pts',(-62.3021870928469,1.2820324163645,137.68432816209));
#173993=CARTESIAN_POINT('Ctrl Pts',(-62.0464339180284,-4.57556355584588,
135.771497744683));
#173994=CARTESIAN_POINT('Ctrl Pts',(-61.883496617814,-5.90239076361927,
132.288505652477));
#173995=CARTESIAN_POINT('Ctrl Pts',(-61.813375192204,-5.91603704377717,
130.798888855257));
#173996=CARTESIAN_POINT('',(-60.0633743488977,-5.92189398088504,130.805812684987));
#173997=CARTESIAN_POINT('Ctrl Pts',(-61.8133751713904,-5.9167474688621,
130.798887755983));
#173998=CARTESIAN_POINT('Ctrl Pts',(-61.8037869858401,-5.91655904331685,
130.595179631626));
#173999=CARTESIAN_POINT('Ctrl Pts',(-61.7941988002899,-5.9058470097901,
130.391941306513));
#174000=CARTESIAN_POINT('Ctrl Pts',(-61.7846106147396,-5.88477711978155,
130.190089656999));
#174001=CARTESIAN_POINT('Ctrl Pts',(-61.7747945288506,-5.86320642229021,
129.983440221809));
#174002=CARTESIAN_POINT('Ctrl Pts',(-61.7649784429615,-5.83077960451583,
129.778243866767));
#174003=CARTESIAN_POINT('Ctrl Pts',(-61.7551623570725,-5.78772236815066,
129.575458525571));
#174004=CARTESIAN_POINT('Ctrl Pts',(-61.7518721864553,-5.77329037809414,
129.507488626089));
#174005=CARTESIAN_POINT('Ctrl Pts',(-61.7485820158383,-5.75766448883687,
129.439789405312));
#174006=CARTESIAN_POINT('Ctrl Pts',(-61.7452918452211,-5.74085438261084,
129.372396400081));
#174007=CARTESIAN_POINT('Ctrl Pts',(-61.7378685788157,-5.70292750545467,
129.220344640489));
#174008=CARTESIAN_POINT('Ctrl Pts',(-61.7304453124103,-5.65889826191603,
129.069570793701));
#174009=CARTESIAN_POINT('Ctrl Pts',(-61.7230220460048,-5.60886672123866,
128.920602494589));
#174010=CARTESIAN_POINT('Ctrl Pts',(-61.7156075532838,-5.55889431368752,
128.771810263636));
#174011=CARTESIAN_POINT('Ctrl Pts',(-61.7081930605627,-5.50293384776418,
128.624819683024));
#174012=CARTESIAN_POINT('Ctrl Pts',(-61.7007785678417,-5.44113617986515,
128.48014728083));
#174013=CARTESIAN_POINT('Ctrl Pts',(-61.693371221488,-5.37939807488507,
128.335614319344));
#174014=CARTESIAN_POINT('Ctrl Pts',(-61.6859638751342,-5.31183411407088,
128.193395429116));
#174015=CARTESIAN_POINT('Ctrl Pts',(-61.6785565287805,-5.23864460889609,
128.053990965286));
#174016=CARTESIAN_POINT('Ctrl Pts',(-61.6711547071051,-5.16550969121563,
127.914690474564));
#174017=CARTESIAN_POINT('Ctrl Pts',(-61.6637528854297,-5.08675775624425,
127.77820055973));
#174018=CARTESIAN_POINT('Ctrl Pts',(-61.6563510637543,-5.00263672547793,
127.645000499536));
#174019=CARTESIAN_POINT('Ctrl Pts',(-61.648953149443,-4.91856010154895,
127.511870754617));
#174020=CARTESIAN_POINT('Ctrl Pts',(-61.6415552351315,-4.82912022530189,
127.382027720465));
#174021=CARTESIAN_POINT('Ctrl Pts',(-61.6341573208202,-4.73461028990158,
127.255924910771));
#174022=CARTESIAN_POINT('Ctrl Pts',(-61.626760635908,-4.64011606033782,
127.129843057076));
#174023=CARTESIAN_POINT('Ctrl Pts',(-61.6193639509958,-4.54055366749458,
127.007500492655));
#174024=CARTESIAN_POINT('Ctrl Pts',(-61.6119672660836,-4.436258917276,126.889320722317));
#174025=CARTESIAN_POINT('Ctrl Pts',(-61.6045709091481,-4.33196879159592,
126.771146192195));
#174026=CARTESIAN_POINT('Ctrl Pts',(-61.5971745522127,-4.22294697277507,
126.657134369035));
#174027=CARTESIAN_POINT('Ctrl Pts',(-61.5897781952773,-4.10956856309439,
126.547674490104));
#174028=CARTESIAN_POINT('Ctrl Pts',(-61.5823807059407,-3.99617279488974,
126.438197852587));
#174029=CARTESIAN_POINT('Ctrl Pts',(-61.5749832166041,-3.87841937630812,
126.333274806244));
#174030=CARTESIAN_POINT('Ctrl Pts',(-61.5675857272675,-3.75671904009221,
126.233256525959));
#174031=CARTESIAN_POINT('Ctrl Pts',(-61.5601856447525,-3.63497604201228,
126.13320318442));
#174032=CARTESIAN_POINT('Ctrl Pts',(-61.5527855622375,-3.50928365980766,
126.038058269039));
#174033=CARTESIAN_POINT('Ctrl Pts',(-61.5453854797225,-3.38008421662579,
125.948131499102));
#174034=CARTESIAN_POINT('Ctrl Pts',(-61.537977260056,-3.25074270537393,
125.858105845437));
#174035=CARTESIAN_POINT('Ctrl Pts',(-61.5305690403896,-3.1178867382884,
125.773310009541));
#174036=CARTESIAN_POINT('Ctrl Pts',(-61.5231608207231,-2.98198664269018,
125.69400972694));
#174037=CARTESIAN_POINT('Ctrl Pts',(-61.515748041421,-2.84600290285074,
125.614660636339));
#174038=CARTESIAN_POINT('Ctrl Pts',(-61.5083352621189,-2.70697163000957,
125.540814013635));
#174039=CARTESIAN_POINT('Ctrl Pts',(-61.5009224828169,-2.56538557406321,
125.472688514099));
#174040=CARTESIAN_POINT('Ctrl Pts',(-61.4934991117881,-2.4235972133204,
125.404465673654));
#174041=CARTESIAN_POINT('Ctrl Pts',(-61.4860757407594,-2.27924712048853,
125.341980430805));
#174042=CARTESIAN_POINT('Ctrl Pts',(-61.4786523697306,-2.13284650455696,
125.28540271317));
#174043=CARTESIAN_POINT('Ctrl Pts',(-61.4747163202899,-2.05522138515569,
125.255403849716));
#174044=CARTESIAN_POINT('Ctrl Pts',(-61.4707802708491,-1.97702002949481,
125.227064965853));
#174045=CARTESIAN_POINT('Ctrl Pts',(-61.4668442214083,-1.89831997046167,
125.200405598809));
#174046=CARTESIAN_POINT('Ctrl Pts',(-61.4594209550028,-1.74989411526949,
125.150126864576));
#174047=CARTESIAN_POINT('Ctrl Pts',(-61.4519976885974,-1.5992449262225,
125.105672967093));
#174048=CARTESIAN_POINT('Ctrl Pts',(-61.444574422192,-1.44687040735415,
125.067244914809));
#174049=CARTESIAN_POINT('Ctrl Pts',(-61.437159929471,-1.29467598251319,
125.028862281291));
#174050=CARTESIAN_POINT('Ctrl Pts',(-61.42974543675,-1.14076064531272,124.99649140689));
#174051=CARTESIAN_POINT('Ctrl Pts',(-61.4223309440289,-0.985640507020434,
124.970284567889));
#174052=CARTESIAN_POINT('Ctrl Pts',(-61.4149235976752,-0.830669879357381,
124.944102988025));
#174053=CARTESIAN_POINT('Ctrl Pts',(-61.4075162513212,-0.674497127998955,
124.924073677711));
#174054=CARTESIAN_POINT('Ctrl Pts',(-61.4001089049675,-0.517651489138725,
124.910298563406));
#174055=CARTESIAN_POINT('Ctrl Pts',(-61.3927070832921,-0.360922831673627,
124.8965337231));
#174056=CARTESIAN_POINT('Ctrl Pts',(-61.3853052616168,-0.203522656253442,
124.889013823443));
#174057=CARTESIAN_POINT('Ctrl Pts',(-61.3779034399413,-0.0459882012907073,
124.88778934293));
#174058=CARTESIAN_POINT('Ctrl Pts',(-61.37050552563,0.111463092459498,124.886565508812));
#174059=CARTESIAN_POINT('Ctrl Pts',(-61.3631076113186,0.269048152239418,
124.891630478216));
#174060=CARTESIAN_POINT('Ctrl Pts',(-61.3557096970073,0.426226946069279,
124.902982714657));
#174061=CARTESIAN_POINT('Ctrl Pts',(-61.3483130120951,0.583379619635344,
124.914333064562));
#174062=CARTESIAN_POINT('Ctrl Pts',(-61.340916327183,0.740125789283221,
124.931968580961));
#174063=CARTESIAN_POINT('Ctrl Pts',(-61.3335196422707,0.895927637127192,
124.955835655532));
#174064=CARTESIAN_POINT('Ctrl Pts',(-61.3261232853353,1.05172257655374,
124.979701671812));
#174065=CARTESIAN_POINT('Ctrl Pts',(-61.3187269283998,1.20657290843936,
125.009798640333));
#174066=CARTESIAN_POINT('Ctrl Pts',(-61.3113305714643,1.35994840450235,
125.046021369172));
#174067=CARTESIAN_POINT('Ctrl Pts',(-61.3039330821278,1.51334738274533,
125.082249643804));
#174068=CARTESIAN_POINT('Ctrl Pts',(-61.2965355927911,1.66527071223876,
125.124605460371));
#174069=CARTESIAN_POINT('Ctrl Pts',(-61.2891381034545,1.81520092852823,
125.172933076385));
#174070=CARTESIAN_POINT('Ctrl Pts',(-61.2817380209395,1.9651837026228,125.22127763357));
#174071=CARTESIAN_POINT('Ctrl Pts',(-61.2743379384246,2.11317161736641,
125.275598043705));
#174072=CARTESIAN_POINT('Ctrl Pts',(-61.2669378559096,2.25866501068448,
125.335689578638));
#174073=CARTESIAN_POINT('Ctrl Pts',(-61.2595296362431,2.40431838894559,
125.395847190391));
#174074=CARTESIAN_POINT('Ctrl Pts',(-61.2521214165766,2.54747142262499,
125.461788457622));
#174075=CARTESIAN_POINT('Ctrl Pts',(-61.2447131969101,2.68764631749271,
125.533261317176));
#174076=CARTESIAN_POINT('Ctrl Pts',(-61.2373004176081,2.82790748766928,
125.604778167084));
#174077=CARTESIAN_POINT('Ctrl Pts',(-61.229887638306,2.96518654179332,125.68183321112));
#174078=CARTESIAN_POINT('Ctrl Pts',(-61.222474859004,3.09903317563845,125.764130073356));
#174079=CARTESIAN_POINT('Ctrl Pts',(-61.2150514879752,3.23307105583081,
125.846544525207));
#174080=CARTESIAN_POINT('Ctrl Pts',(-61.2076281169464,3.36366641143666,
125.934215546467));
#174081=CARTESIAN_POINT('Ctrl Pts',(-61.2002047459177,3.49039995659213,
126.026804892562));
#174082=CARTESIAN_POINT('Ctrl Pts',(-61.1962686964769,3.55759712316341,
126.075897985512));
#174083=CARTESIAN_POINT('Ctrl Pts',(-61.1923326470361,3.62370917166573,
126.126373141864));
#174084=CARTESIAN_POINT('Ctrl Pts',(-61.1883965975953,3.68867775645533,
126.178175691352));
#174085=CARTESIAN_POINT('Ctrl Pts',(-61.1809733311899,3.81120647976808,
126.275873682984));
#174086=CARTESIAN_POINT('Ctrl Pts',(-61.1735500647845,3.93003636921133,
126.3785906949));
#174087=CARTESIAN_POINT('Ctrl Pts',(-61.166126798379,4.04472912733981,126.486016392177));
#174088=CARTESIAN_POINT('Ctrl Pts',(-61.158712305658,4.15928632815297,126.593315121202));
#174089=CARTESIAN_POINT('Ctrl Pts',(-61.151297812937,4.26971586092583,126.705311205181));
#174090=CARTESIAN_POINT('Ctrl Pts',(-61.143883320216,4.37561064056104,126.821652734139));
#174091=CARTESIAN_POINT('Ctrl Pts',(-61.1364759738622,4.48140335482078,
126.937882128752));
#174092=CARTESIAN_POINT('Ctrl Pts',(-61.1290686275084,4.58266976768811,
127.058448356044));
#174093=CARTESIAN_POINT('Ctrl Pts',(-61.1216612811546,4.67903806045666,
127.182961248358));
#174094=CARTESIAN_POINT('Ctrl Pts',(-61.1142594594792,4.7753344781167,127.30738127426));
#174095=CARTESIAN_POINT('Ctrl Pts',(-61.1068576378038,4.86673982220071,
127.435741810197));
#174096=CARTESIAN_POINT('Ctrl Pts',(-61.0994558161284,4.95292123323519,
127.567618147139));
#174097=CARTESIAN_POINT('Ctrl Pts',(-61.0920579018171,5.0390571497735,127.699424867588));
#174098=CARTESIAN_POINT('Ctrl Pts',(-61.0846599875057,5.11997442160667,
127.834743381103));
#174099=CARTESIAN_POINT('Ctrl Pts',(-61.0772620731944,5.1953824409474,127.973118512977));
#174100=CARTESIAN_POINT('Ctrl Pts',(-61.0698653882822,5.27077792884347,
128.111470649415));
#174101=CARTESIAN_POINT('Ctrl Pts',(-61.0624687033699,5.34066580286567,
128.252878068607));
#174102=CARTESIAN_POINT('Ctrl Pts',(-61.0550720184577,5.40480046150981,
128.396859312527));
#174103=CARTESIAN_POINT('Ctrl Pts',(-61.0476756615223,5.46893227635599,
128.540834172168));
#174104=CARTESIAN_POINT('Ctrl Pts',(-61.0402793045868,5.52731123116298,
128.687382288618));
#174105=CARTESIAN_POINT('Ctrl Pts',(-61.0328829476514,5.57973922553615,
128.836000707003));
#174106=CARTESIAN_POINT('Ctrl Pts',(-61.0254854583148,5.63217524676911,
128.984641879247));
#174107=CARTESIAN_POINT('Ctrl Pts',(-61.0180879689783,5.67865836923736,
129.135353632495));
#174108=CARTESIAN_POINT('Ctrl Pts',(-61.0106904796417,5.71903992132884,
129.287616426627));
#174109=CARTESIAN_POINT('Ctrl Pts',(-61.0032903971267,5.75943562911081,
129.439932596246));
#174110=CARTESIAN_POINT('Ctrl Pts',(-60.9958903146117,5.79372541235539,
129.593800528683));
#174111=CARTESIAN_POINT('Ctrl Pts',(-60.9884902320967,5.82181143509756,
129.748689183517));
#174112=CARTESIAN_POINT('Ctrl Pts',(-60.9810820124302,5.84992834130905,
129.90374815435));
#174113=CARTESIAN_POINT('Ctrl Pts',(-60.9736737927637,5.87182779704541,
130.059829721532));
#174114=CARTESIAN_POINT('Ctrl Pts',(-60.9662655730972,5.8874636107235,130.216395656955));
#174115=CARTESIAN_POINT('Ctrl Pts',(-60.9588527937952,5.90310904798401,
130.373057956098));
#174116=CARTESIAN_POINT('Ctrl Pts',(-60.9514400144931,5.91248313910554,
130.530204845753));
#174117=CARTESIAN_POINT('Ctrl Pts',(-60.944027235191,5.91559183311733,130.687297273792));
#174118=CARTESIAN_POINT('Ctrl Pts',(-60.9366038641623,5.9187049689769,130.844614162859));
#174119=CARTESIAN_POINT('Ctrl Pts',(-60.9291804931335,5.91553483549277,
131.001876062657));
#174120=CARTESIAN_POINT('Ctrl Pts',(-60.9217571221048,5.90613937315212,
131.158547386662));
#174121=CARTESIAN_POINT('Ctrl Pts',(-60.917821072664,5.90115767357812,131.241618281925));
#174122=CARTESIAN_POINT('Ctrl Pts',(-60.9138850232233,5.89442667210103,
131.324523275652));
#174123=CARTESIAN_POINT('Ctrl Pts',(-60.9099489737825,5.88596082711695,
131.407183729386));
#174124=CARTESIAN_POINT('Ctrl Pts',(-60.9025257073771,5.86999450768682,
131.563078765387));
#174125=CARTESIAN_POINT('Ctrl Pts',(-60.8951024409717,5.84780623429085,
131.718574770755));
#174126=CARTESIAN_POINT('Ctrl Pts',(-60.8876791745662,5.81942019001215,
131.873135249834));
#174127=CARTESIAN_POINT('Ctrl Pts',(-60.8802646818452,5.79106769568043,
132.027513051261));
#174128=CARTESIAN_POINT('Ctrl Pts',(-60.8728501891242,5.75653207818981,
132.180957163757));
#174129=CARTESIAN_POINT('Ctrl Pts',(-60.8654356964032,5.71588936993058,
132.332934879162));
#174130=CARTESIAN_POINT('Ctrl Pts',(-60.8580283500494,5.67528583464374,
132.484766112723));
#174131=CARTESIAN_POINT('Ctrl Pts',(-60.8506210036956,5.62858702273421,
132.635133404728));
#174132=CARTESIAN_POINT('Ctrl Pts',(-60.8432136573418,5.57592021620963,
132.783513038418));
#174133=CARTESIAN_POINT('Ctrl Pts',(-60.8358118356664,5.52329269057643,
132.93178200498));
#174134=CARTESIAN_POINT('Ctrl Pts',(-60.828410013991,5.46470615751025,133.078065914746));
#174135=CARTESIAN_POINT('Ctrl Pts',(-60.8210081923156,5.40033801807167,
133.221855158009));
#174136=CARTESIAN_POINT('Ctrl Pts',(-60.8136102780043,5.33600385807286,
133.365568496049));
#174137=CARTESIAN_POINT('Ctrl Pts',(-60.806212363693,5.26589432217311,133.506789450432));
#174138=CARTESIAN_POINT('Ctrl Pts',(-60.7988144493816,5.19023528113713,
133.645027491548));
#174139=CARTESIAN_POINT('Ctrl Pts',(-60.7914177644694,5.11458881326108,
133.78324256001));
#174140=CARTESIAN_POINT('Ctrl Pts',(-60.7840210795571,5.03339484964367,
133.918475371894));
#174141=CARTESIAN_POINT('Ctrl Pts',(-60.7766243946449,4.94692570094628,
134.050259055875));
#174142=CARTESIAN_POINT('Ctrl Pts',(-60.7692280377095,4.86046038638169,
134.18203689643));
#174143=CARTESIAN_POINT('Ctrl Pts',(-60.7618316807741,4.76872055661285,
134.310365601064));
#174144=CARTESIAN_POINT('Ctrl Pts',(-60.7544353238386,4.67202228371712,
134.434806642912));
#174145=CARTESIAN_POINT('Ctrl Pts',(-60.747037834502,4.57530920606894,134.559266737001));
#174146=CARTESIAN_POINT('Ctrl Pts',(-60.7396403451654,4.47363640279043,
134.679837688373));
#174147=CARTESIAN_POINT('Ctrl Pts',(-60.7322428558288,4.36736061706032,
134.796113591267));
#174148=CARTESIAN_POINT('Ctrl Pts',(-60.7248427733138,4.26104757651828,
134.912430254498));
#174149=CARTESIAN_POINT('Ctrl Pts',(-60.7174426907989,4.1501285926113,135.024448596194));
#174150=CARTESIAN_POINT('Ctrl Pts',(-60.7100426082839,4.03499756195621,
135.131799263868));
#174151=CARTESIAN_POINT('Ctrl Pts',(-60.7026343886174,3.91973993289699,
135.239267974637));
#174152=CARTESIAN_POINT('Ctrl Pts',(-60.6952261689509,3.80026128071653,
135.342058506539));
#174153=CARTESIAN_POINT('Ctrl Pts',(-60.6878179492845,3.67698946428683,
135.439841071847));
#174154=CARTESIAN_POINT('Ctrl Pts',(-60.6804051699824,3.55364177611101,
135.537683820693));
#174155=CARTESIAN_POINT('Ctrl Pts',(-60.6729923906803,3.42649657243919,
135.630512241426));
#174156=CARTESIAN_POINT('Ctrl Pts',(-60.6655796113782,3.29601058868899,
135.718039968292));
#174157=CARTESIAN_POINT('Ctrl Pts',(-60.6581562403495,3.16533816044602,
135.805692758878));
#174158=CARTESIAN_POINT('Ctrl Pts',(-60.6507328693208,3.03131573567422,
135.888029533972));
#174159=CARTESIAN_POINT('Ctrl Pts',(-60.643309498292,2.89442523673469,135.964809542946));
#174160=CARTESIAN_POINT('Ctrl Pts',(-60.6393734488512,2.82184260955433,
136.005520146015));
#174161=CARTESIAN_POINT('Ctrl Pts',(-60.6354373994104,2.7484540196275,136.044669338017));
#174162=CARTESIAN_POINT('Ctrl Pts',(-60.6315013499696,2.67433344283047,
136.082226777205));
#174163=CARTESIAN_POINT('Ctrl Pts',(-60.6240780835642,2.53454434821584,
136.153058935384));
#174164=CARTESIAN_POINT('Ctrl Pts',(-60.6166548171588,2.3917278512743,136.218440701675));
#174165=CARTESIAN_POINT('Ctrl Pts',(-60.6092315507533,2.24634839254537,
136.27810243298));
#174166=CARTESIAN_POINT('Ctrl Pts',(-60.6018170580324,2.10114076026364,
136.337693649073));
#174167=CARTESIAN_POINT('Ctrl Pts',(-60.5944025653114,1.95337653782512,
136.391578146863));
#174168=CARTESIAN_POINT('Ctrl Pts',(-60.5869880725904,1.8035450050554,136.439531952782));
#174169=CARTESIAN_POINT('Ctrl Pts',(-60.5795807262366,1.65385788555803,
136.487439539017));
#174170=CARTESIAN_POINT('Ctrl Pts',(-60.5721733798828,1.50210777565312,
136.529427700232));
#174171=CARTESIAN_POINT('Ctrl Pts',(-60.564766033529,1.34880409211538,136.565320440685));
#174172=CARTESIAN_POINT('Ctrl Pts',(-60.5573642118536,1.19561474824843,
136.601186410978));
#174173=CARTESIAN_POINT('Ctrl Pts',(-60.5499623901782,1.04087449980872,
136.630965927865));
#174174=CARTESIAN_POINT('Ctrl Pts',(-60.5425605685028,0.885107985482796,
136.654532787386));
#174175=CARTESIAN_POINT('Ctrl Pts',(-60.5351626541915,0.72942369908752,
136.678087206145));
#174176=CARTESIAN_POINT('Ctrl Pts',(-60.5277647398802,0.572714593905674,
136.695435443345));
#174177=CARTESIAN_POINT('Ctrl Pts',(-60.5203668255688,0.415515455055614,
136.706502387221));
#174178=CARTESIAN_POINT('Ctrl Pts',(-60.5129701406566,0.258342439850548,
136.717567491972));
#174179=CARTESIAN_POINT('Ctrl Pts',(-60.5055734557445,0.100679924612702,
136.722353348917));
#174180=CARTESIAN_POINT('Ctrl Pts',(-60.4981767708323,-0.0569321080256532,
136.720836705372));
#174181=CARTESIAN_POINT('Ctrl Pts',(-60.4907804138969,-0.214537151981316,
136.719320129076));
#174182=CARTESIAN_POINT('Ctrl Pts',(-60.4833840569614,-0.372091344508002,
136.711501611543));
#174183=CARTESIAN_POINT('Ctrl Pts',(-60.475987700026,-0.529054895854471,
136.697410038678));
#174184=CARTESIAN_POINT('Ctrl Pts',(-60.4685902106894,-0.68604247872136,
136.683316308358));
#174185=CARTESIAN_POINT('Ctrl Pts',(-60.4611927213528,-0.84243886852604,
136.662947643763));
#174186=CARTESIAN_POINT('Ctrl Pts',(-60.4537952320163,-0.997709736852333,
136.636384781052));
#174187=CARTESIAN_POINT('Ctrl Pts',(-60.4463951495013,-1.15303503514082,
136.609812606772));
#174188=CARTESIAN_POINT('Ctrl Pts',(-60.4389950669864,-1.30723365868226,
136.577041974109));
#174189=CARTESIAN_POINT('Ctrl Pts',(-60.4315949844714,-1.45978195002596,
136.538204635402));
#174190=CARTESIAN_POINT('Ctrl Pts',(-60.424186764805,-1.61249798389834,
136.499324591049));
#174191=CARTESIAN_POINT('Ctrl Pts',(-60.4167785451385,-1.76355969949811,
136.45436461045));
#174192=CARTESIAN_POINT('Ctrl Pts',(-60.4093703254721,-1.91245836889943,
136.40350640507));
#174193=CARTESIAN_POINT('Ctrl Pts',(-60.40195754617,-2.06144868294747,136.352616897313));
#174194=CARTESIAN_POINT('Ctrl Pts',(-60.3945447668679,-2.20827295062666,
136.295822065392));
#174195=CARTESIAN_POINT('Ctrl Pts',(-60.3871319875659,-2.35244336766703,
136.233351386062));
#174196=CARTESIAN_POINT('Ctrl Pts',(-60.3797086165371,-2.49681978215999,
136.170791445697));
#174197=CARTESIAN_POINT('Ctrl Pts',(-60.3722852455084,-2.63853443721335,
136.10253962215));
#174198=CARTESIAN_POINT('Ctrl Pts',(-60.3648618744796,-2.77712429169874,
136.028871238759));
#174199=CARTESIAN_POINT('Ctrl Pts',(-60.3609258250386,-2.85060795796856,
135.989810494234));
#174200=CARTESIAN_POINT('Ctrl Pts',(-60.3569897755977,-2.92321360743758,
135.949227689603));
#174201=CARTESIAN_POINT('Ctrl Pts',(-60.3530537261567,-2.9948757269657,
135.907168662411));
#174202=CARTESIAN_POINT('Ctrl Pts',(-60.3456304597512,-3.13002824789162,
135.827846649746));
#174203=CARTESIAN_POINT('Ctrl Pts',(-60.3382071933459,-3.26223158466391,
135.743031527813));
#174204=CARTESIAN_POINT('Ctrl Pts',(-60.3307839269404,-3.39100783745323,
135.652968294913));
#174205=CARTESIAN_POINT('Ctrl Pts',(-60.3233694342194,-3.51963188740615,
135.563011509275));
#174206=CARTESIAN_POINT('Ctrl Pts',(-60.3159549414983,-3.64483661305601,
135.467819171294));
#174207=CARTESIAN_POINT('Ctrl Pts',(-60.3085404487773,-3.76616911139899,
135.367681862761));
#174208=CARTESIAN_POINT('Ctrl Pts',(-60.3011331024234,-3.88738466491198,
135.267641070335));
#174209=CARTESIAN_POINT('Ctrl Pts',(-60.2937257560696,-4.00473513521546,
135.162665031839));
#174210=CARTESIAN_POINT('Ctrl Pts',(-60.2863184097158,-4.11779709989725,
135.053087204036));
#174211=CARTESIAN_POINT('Ctrl Pts',(-60.2789165880403,-4.23077473870035,
134.943591103511));
#174212=CARTESIAN_POINT('Ctrl Pts',(-60.2715147663649,-4.33946997367944,
134.829500306308));
#174213=CARTESIAN_POINT('Ctrl Pts',(-60.2641129446894,-4.44349304584495,
134.711187989492));
#174214=CARTESIAN_POINT('Ctrl Pts',(-60.256715030378,-4.54746120504037,
134.592938128826));
#174215=CARTESIAN_POINT('Ctrl Pts',(-60.2493171160666,-4.64676186750825,
134.470471466364));
#174216=CARTESIAN_POINT('Ctrl Pts',(-60.2419192017553,-4.74104277517465,
134.344197332227));
#174217=CARTESIAN_POINT('Ctrl Pts',(-60.234522516843,-4.83530801506436,
134.217944182561));
#174218=CARTESIAN_POINT('Ctrl Pts',(-60.2271258319308,-4.92455493266152,
134.087885115836));
#174219=CARTESIAN_POINT('Ctrl Pts',(-60.2197291470186,-5.00847209102242,
133.95446186609));
#174220=CARTESIAN_POINT('Ctrl Pts',(-60.2123327900831,-5.09238552840858,
133.82104453247));
#174221=CARTESIAN_POINT('Ctrl Pts',(-60.2049364331476,-5.1709694777115,
133.684263628425));
#174222=CARTESIAN_POINT('Ctrl Pts',(-60.1975400762121,-5.24395647191723,
133.544588907898));
#174223=CARTESIAN_POINT('Ctrl Pts',(-60.1901425868755,-5.31695464061809,
133.404892802816));
#174224=CARTESIAN_POINT('Ctrl Pts',(-60.1827450975389,-5.38435397510693,
133.26230232995));
#174225=CARTESIAN_POINT('Ctrl Pts',(-60.1753476082023,-5.44593358344121,
133.117310674797));
#174226=CARTESIAN_POINT('Ctrl Pts',(-60.1679475256873,-5.50753477841182,
132.972268193045));
#174227=CARTESIAN_POINT('Ctrl Pts',(-60.1605474431723,-5.56331203957477,
132.824823196505));
#174228=CARTESIAN_POINT('Ctrl Pts',(-60.1531473606573,-5.61309316426054,
132.675487468379));
#174229=CARTESIAN_POINT('Ctrl Pts',(-60.1457391409908,-5.66292902841053,
132.525987530267));
#174230=CARTESIAN_POINT('Ctrl Pts',(-60.1383309213242,-5.70675547056859,
132.374593062919));
#174231=CARTESIAN_POINT('Ctrl Pts',(-60.1309227016577,-5.74445038986613,
132.221830293032));
#174232=CARTESIAN_POINT('Ctrl Pts',(-60.1235099223556,-5.78216850975747,
132.06897350021));
#174233=CARTESIAN_POINT('Ctrl Pts',(-60.1160971430536,-5.81374751221079,
131.914747091587));
#174234=CARTESIAN_POINT('Ctrl Pts',(-60.1086843637515,-5.83911679239732,
131.759685508503));
#174235=CARTESIAN_POINT('Ctrl Pts',(-60.1012609927227,-5.86452232140111,
131.604402366157));
#174236=CARTESIAN_POINT('Ctrl Pts',(-60.093837621694,-5.88370036188762,
131.448282035521));
#174237=CARTESIAN_POINT('Ctrl Pts',(-60.0864142506652,-5.89663226613734,
131.2918629052));
#174238=CARTESIAN_POINT('Ctrl Pts',(-60.0824782012247,-5.90348907206677,
131.208925729084));
#174239=CARTESIAN_POINT('Ctrl Pts',(-60.0785421517842,-5.90859073619492,
131.125904542705));
#174240=CARTESIAN_POINT('Ctrl Pts',(-60.0746061023437,-5.91194041149315,
131.042879240433));
#174241=CARTESIAN_POINT('Ctrl Pts',(-60.0708624656306,-5.91512633880762,
130.963912607924));
#174242=CARTESIAN_POINT('Ctrl Pts',(-60.0671188289174,-5.916730195719,130.884881716305));
#174243=CARTESIAN_POINT('Ctrl Pts',(-60.0633751922041,-5.91674981773242,
130.80582924392));
#174244=CARTESIAN_POINT('',(-58.3133751922041,-5.91156881184207,130.80911788525));
#174245=CARTESIAN_POINT('Ctrl Pts',(-60.0633736607459,-5.92609170103476,
130.80579917263));
#174246=CARTESIAN_POINT('Ctrl Pts',(-59.9743019333409,-5.91980991597853,
128.921945335877));
#174247=CARTESIAN_POINT('Ctrl Pts',(-59.7924143313318,-3.92743761287679,
125.063652292068));
#174248=CARTESIAN_POINT('Ctrl Pts',(-59.5177108547178,2.6500406791028,124.327104645363));
#174249=CARTESIAN_POINT('Ctrl Pts',(-59.2392632309052,6.8819106127336,129.532799825198));
#174250=CARTESIAN_POINT('Ctrl Pts',(-58.960815607092,4.78964089328673,135.906997254022));
#174251=CARTESIAN_POINT('Ctrl Pts',(-58.6823679832794,-1.70407482012499,
137.5921208916));
#174252=CARTESIAN_POINT('Ctrl Pts',(-58.4665545116499,-5.52337744944411,
134.063665339323));
#174253=CARTESIAN_POINT('Ctrl Pts',(-58.3435569146249,-5.9163895394015,
131.451508990351));
#174254=CARTESIAN_POINT('Ctrl Pts',(-58.3133751922041,-5.91156881184207,
130.80911788525));
#174255=CARTESIAN_POINT('',(-56.5633751922042,-5.90884967465456,130.801001847959));
#174256=CARTESIAN_POINT('Ctrl Pts',(-58.3133751922041,-5.91156881184207,
130.80911788525));
#174257=CARTESIAN_POINT('Ctrl Pts',(-58.2507410400206,-5.90156467160833,
129.476005689816));
#174258=CARTESIAN_POINT('Ctrl Pts',(-58.095291013233,-4.79442660150182,
126.152340551137));
#174259=CARTESIAN_POINT('Ctrl Pts',(-57.8470251118403,0.723619930605998,
123.843474558564));
#174260=CARTESIAN_POINT('Ctrl Pts',(-57.5685774880279,6.24752483186355,
127.65063361518));
#174261=CARTESIAN_POINT('Ctrl Pts',(-57.2901298642149,6.03025962119851,
134.355913718856));
#174262=CARTESIAN_POINT('Ctrl Pts',(-57.0116822404018,0.271480413209222,
137.797490025462));
#174263=CARTESIAN_POINT('Ctrl Pts',(-56.7694306830652,-4.95574853847363,
135.200719103271));
#174264=CARTESIAN_POINT('Ctrl Pts',(-56.6199950003325,-5.90264780731658,
132.007497243329));
#174265=CARTESIAN_POINT('Ctrl Pts',(-56.5633751922042,-5.90884967465456,
130.801001847959));
#174266=CARTESIAN_POINT('',(-54.8133751922042,-5.92388329333877,130.80082555441));
#174267=CARTESIAN_POINT('Ctrl Pts',(-56.5633751922042,-5.90884967465456,
130.801001847959));
#174268=CARTESIAN_POINT('Ctrl Pts',(-56.5271791257282,-5.91281442144304,
130.02971015734));
#174269=CARTESIAN_POINT('Ctrl Pts',(-56.3981671846476,-5.41337615916817,
127.285565116781));
#174270=CARTESIAN_POINT('Ctrl Pts',(-56.1763393689635,-1.26108622347638,
123.9205228749));
#174271=CARTESIAN_POINT('Ctrl Pts',(-55.8978917451504,5.10991974578196,
126.022490614944));
#174272=CARTESIAN_POINT('Ctrl Pts',(-55.6194441213376,6.78515910212911,
132.518763280054));
#174273=CARTESIAN_POINT('Ctrl Pts',(-55.3409964975246,2.22516871706598,
137.439583651567));
#174274=CARTESIAN_POINT('Ctrl Pts',(-55.0723068544802,-4.14818251483082,
136.304192128701));
#174275=CARTESIAN_POINT('Ctrl Pts',(-54.89643308604,-5.91148057148662,132.559222115526));
#174276=CARTESIAN_POINT('Ctrl Pts',(-54.8133751922042,-5.92388329333877,
130.80082555441));
#174277=CARTESIAN_POINT('',(-53.0633751922041,-5.91880835334059,130.809427504538));
#174278=CARTESIAN_POINT('Ctrl Pts',(-54.8133751922042,-5.92388329333877,
130.80082555441));
#174279=CARTESIAN_POINT('Ctrl Pts',(-54.8036172114357,-5.92534041578338,
130.59424194105));
#174280=CARTESIAN_POINT('Ctrl Pts',(-54.7010433560634,-5.82163645082206,
128.424157715391));
#174281=CARTESIAN_POINT('Ctrl Pts',(-54.5056536260855,-3.14421568114513,
124.552043584596));
#174282=CARTESIAN_POINT('Ctrl Pts',(-54.2272060022732,3.56072601726273,
124.779512838547));
#174283=CARTESIAN_POINT('Ctrl Pts',(-53.9487583784601,6.99353445694264,
130.543522871244));
#174284=CARTESIAN_POINT('Ctrl Pts',(-53.6703107546473,3.99962638384432,
136.547230050173));
#174285=CARTESIAN_POINT('Ctrl Pts',(-53.3918631308343,-2.66974294339494,
137.27352077531));
#174286=CARTESIAN_POINT('Ctrl Pts',(-53.1895512766867,-5.7329688978399,
133.481874791569));
#174287=CARTESIAN_POINT('Ctrl Pts',(-53.0800552971433,-5.92313625057596,
131.163173995511));
#174288=CARTESIAN_POINT('Ctrl Pts',(-53.0633751922041,-5.9199225285852,
130.809428458345));
#174289=CARTESIAN_POINT('',(-51.313375216539,-5.9114707548659,130.80551579402));
#174290=CARTESIAN_POINT('Ctrl Pts',(-53.0633751922041,-5.91674783196214,
130.809425740597));
#174291=CARTESIAN_POINT('Ctrl Pts',(-53.0560738687434,-5.91688031615351,
130.654666310814));
#174292=CARTESIAN_POINT('Ctrl Pts',(-53.0487725452826,-5.91093678929377,
130.499695394686));
#174293=CARTESIAN_POINT('Ctrl Pts',(-53.0414712218218,-5.89889421094919,
130.345037582513));
#174294=CARTESIAN_POINT('Ctrl Pts',(-53.0341762556043,-5.88686211804603,
130.190514430493));
#174295=CARTESIAN_POINT('Ctrl Pts',(-53.0268812893869,-5.86874157038524,
130.036304221831));
#174296=CARTESIAN_POINT('Ctrl Pts',(-53.0195863231694,-5.84456157651281,
129.882932084879));
#174297=CARTESIAN_POINT('Ctrl Pts',(-53.0122960072682,-5.82039699664201,
129.729657717942));
#174298=CARTESIAN_POINT('Ctrl Pts',(-53.0050056913671,-5.79018071829052,
129.577220738767));
#174299=CARTESIAN_POINT('Ctrl Pts',(-52.9977153754659,-5.75399360318452,
129.426141412573));
#174300=CARTESIAN_POINT('Ctrl Pts',(-52.9904271935296,-5.71781708049078,
129.27510630915));
#174301=CARTESIAN_POINT('Ctrl Pts',(-52.9831390115933,-5.67567328381649,
129.125428443235));
#174302=CARTESIAN_POINT('Ctrl Pts',(-52.975850829657,-5.62769420842712,
128.977618036101));
#174303=CARTESIAN_POINT('Ctrl Pts',(-52.9685634929614,-5.57972069737013,
128.829824771154));
#174304=CARTESIAN_POINT('Ctrl Pts',(-52.9612761562658,-5.52591337242735,
128.683898900805));
#174305=CARTESIAN_POINT('Ctrl Pts',(-52.9539888195702,-5.46645404004436,
128.540335266431));
#174306=CARTESIAN_POINT('Ctrl Pts',(-52.9467007900094,-5.40698905438916,
128.396757982319));
#174307=CARTESIAN_POINT('Ctrl Pts',(-52.9394127604487,-5.34187113974337,
128.255543737113));
#174308=CARTESIAN_POINT('Ctrl Pts',(-52.9321247308879,-5.27133003934232,
128.117166880816));
#174309=CARTESIAN_POINT('Ctrl Pts',(-52.9248344699682,-5.20076734153747,
127.978747658001));
#174310=CARTESIAN_POINT('Ctrl Pts',(-52.9175442090485,-5.12477832970221,
127.843167895492));
#174311=CARTESIAN_POINT('Ctrl Pts',(-52.9102539481288,-5.04363827206326,
127.71087657153));
#174312=CARTESIAN_POINT('Ctrl Pts',(-52.9029560283258,-4.96241297162721,
127.578446267109));
#174313=CARTESIAN_POINT('Ctrl Pts',(-52.8956581085228,-4.8760260235918,
127.44931162676));
#174314=CARTESIAN_POINT('Ctrl Pts',(-52.8883601887198,-4.78479581982511,
127.323892326505));
#174315=CARTESIAN_POINT('Ctrl Pts',(-52.8810578861492,-4.69351082773637,
127.198397705657));
#174316=CARTESIAN_POINT('Ctrl Pts',(-52.8737555835786,-4.59737702659977,
127.076623169065));
#174317=CARTESIAN_POINT('Ctrl Pts',(-52.866453281008,-4.49675195989873,
126.958953958492));
#174318=CARTESIAN_POINT('Ctrl Pts',(-52.8591408388067,-4.39598717000699,
126.84112135804));
#174319=CARTESIAN_POINT('Ctrl Pts',(-52.8518283966053,-4.29071892636813,
126.727405744225));
#174320=CARTESIAN_POINT('Ctrl Pts',(-52.844515954404,-4.18134074351241,
126.618154680307));
#174321=CARTESIAN_POINT('Ctrl Pts',(-52.8413332640055,-4.13373463835684,
126.570603902799));
#174322=CARTESIAN_POINT('Ctrl Pts',(-52.8381505736071,-4.08535037470118,
126.523898349799));
#174323=CARTESIAN_POINT('Ctrl Pts',(-52.8349678832086,-4.03622221003705,
126.478064183697));
#174324=CARTESIAN_POINT('Ctrl Pts',(-52.8275446168032,-3.92163630671296,
126.371161160517));
#174325=CARTESIAN_POINT('Ctrl Pts',(-52.8201213503977,-3.8026270667802,
126.268652000085));
#174326=CARTESIAN_POINT('Ctrl Pts',(-52.8126980839923,-3.67956565674869,
126.170924836186));
#174327=CARTESIAN_POINT('Ctrl Pts',(-52.8052835912713,-3.55664969508404,
126.073313177678));
#174328=CARTESIAN_POINT('Ctrl Pts',(-52.7978690985503,-3.42969138598225,
125.980472495404));
#174329=CARTESIAN_POINT('Ctrl Pts',(-52.7904546058293,-3.29909845275371,
125.892753959706));
#174330=CARTESIAN_POINT('Ctrl Pts',(-52.7830472594756,-3.16863138991114,
125.805119970434));
#174331=CARTESIAN_POINT('Ctrl Pts',(-52.7756399131217,-3.0345369849,125.722598506056));
#174332=CARTESIAN_POINT('Ctrl Pts',(-52.7682325667679,-2.89725564261266,
125.645500248856));
#174333=CARTESIAN_POINT('Ctrl Pts',(-52.7608307450925,-2.76007668992973,
125.568459494444));
#174334=CARTESIAN_POINT('Ctrl Pts',(-52.7534289234172,-2.61971585685554,
125.49683407541));
#174335=CARTESIAN_POINT('Ctrl Pts',(-52.7460271017418,-2.47664201289675,
125.430891077087));
#174336=CARTESIAN_POINT('Ctrl Pts',(-52.7386291874304,-2.3336436965067,
125.36498288956));
#174337=CARTESIAN_POINT('Ctrl Pts',(-52.731231273119,-2.18793555964505,
125.304751304547));
#174338=CARTESIAN_POINT('Ctrl Pts',(-52.7238333588077,-2.04001042257452,
125.250417150237));
#174339=CARTESIAN_POINT('Ctrl Pts',(-52.7164366738955,-1.89210986797813,
125.196092025277));
#174340=CARTESIAN_POINT('Ctrl Pts',(-52.7090399889834,-1.74199339445259,
125.147662514501));
#174341=CARTESIAN_POINT('Ctrl Pts',(-52.7016433040712,-1.59017323240424,
125.105301076427));
#174342=CARTESIAN_POINT('Ctrl Pts',(-52.6942469471357,-1.43835980222074,
125.062941516704));
#174343=CARTESIAN_POINT('Ctrl Pts',(-52.6868505902002,-1.28484319328321,
125.02664959502));
#174344=CARTESIAN_POINT('Ctrl Pts',(-52.6794542332648,-1.13014994595898,
124.996547633133));
#174345=CARTESIAN_POINT('Ctrl Pts',(-52.6720567439282,-0.97543301470345,
124.966441062559));
#174346=CARTESIAN_POINT('Ctrl Pts',(-52.6646592545916,-0.819539452814311,
124.942526410084));
#174347=CARTESIAN_POINT('Ctrl Pts',(-52.657261765255,-0.663004969701697,
124.924874672974));
#174348=CARTESIAN_POINT('Ctrl Pts',(-52.64986168274,-0.50641561366891,124.907216748076));
#174349=CARTESIAN_POINT('Ctrl Pts',(-52.6424616002251,-0.349185259803934,
124.895826151482));
#174350=CARTESIAN_POINT('Ctrl Pts',(-52.6350615177101,-0.191853550423675,
124.890721908811));
#174351=CARTESIAN_POINT('Ctrl Pts',(-52.6276532980436,-0.034348838654634,
124.8856120535));
#174352=CARTESIAN_POINT('Ctrl Pts',(-52.6202450783771,0.123257077873727,
124.886802368925));
#174353=CARTESIAN_POINT('Ctrl Pts',(-52.6128368587106,0.280425008487276,
124.894259740498));
#174354=CARTESIAN_POINT('Ctrl Pts',(-52.6054240794086,0.43768967333963,
124.90172170196));
#174355=CARTESIAN_POINT('Ctrl Pts',(-52.5980113001065,0.594515444107284,
124.915458373162));
#174356=CARTESIAN_POINT('Ctrl Pts',(-52.5905985208045,0.750369949499985,
124.935384940211));
#174357=CARTESIAN_POINT('Ctrl Pts',(-52.5831751497757,0.906447147118842,
124.955339979273));
#174358=CARTESIAN_POINT('Ctrl Pts',(-52.5757517787469,1.06154994051297,
124.981502516532));
#174359=CARTESIAN_POINT('Ctrl Pts',(-52.5683284077181,1.21515699932609,
125.013736814426));
#174360=CARTESIAN_POINT('Ctrl Pts',(-52.5643923582773,1.29660314766047,
125.030828212621));
#174361=CARTESIAN_POINT('Ctrl Pts',(-52.5604563088365,1.37762904656777,
125.049625767575));
#174362=CARTESIAN_POINT('Ctrl Pts',(-52.5565202593957,1.45815902216238,
125.070103662338));
#174363=CARTESIAN_POINT('Ctrl Pts',(-52.5490969929903,1.61003604287771,
125.108724332765));
#174364=CARTESIAN_POINT('Ctrl Pts',(-52.5416737265848,1.76060730390585,
125.153441471698));
#174365=CARTESIAN_POINT('Ctrl Pts',(-52.5342504601794,1.90934563273537,
125.204152602032));
#174366=CARTESIAN_POINT('Ctrl Pts',(-52.5268359674584,2.05790816521238,
125.254803796021));
#174367=CARTESIAN_POINT('Ctrl Pts',(-52.5194214747373,2.204641727793,125.311434760585));
#174368=CARTESIAN_POINT('Ctrl Pts',(-52.5120069820163,2.34903048651398,
125.373892282705));
#174369=CARTESIAN_POINT('Ctrl Pts',(-52.5045996356626,2.49328007791296,
125.436289605913));
#174370=CARTESIAN_POINT('Ctrl Pts',(-52.4971922893088,2.63518902437024,
125.504502159405));
#174371=CARTESIAN_POINT('Ctrl Pts',(-52.489784942955,2.77425789047849,125.578327349434));
#174372=CARTESIAN_POINT('Ctrl Pts',(-52.4823831212796,2.91322303377983,
125.652097477852));
#174373=CARTESIAN_POINT('Ctrl Pts',(-52.4749812996041,3.04935198613164,
125.731471733407));
#174374=CARTESIAN_POINT('Ctrl Pts',(-52.4675794779287,3.18216660565613,
125.81620000905));
#174375=CARTESIAN_POINT('Ctrl Pts',(-52.4601815636174,3.31491111337623,
125.900883557297));
#174376=CARTESIAN_POINT('Ctrl Pts',(-52.4527836493061,3.44434445878719,
125.990915296569));
#174377=CARTESIAN_POINT('Ctrl Pts',(-52.4453857349948,3.57001447149046,
126.085999966254));
#174378=CARTESIAN_POINT('Ctrl Pts',(-52.4379890500826,3.69566360011804,
126.181068834592));
#174379=CARTESIAN_POINT('Ctrl Pts',(-52.4305923651704,3.8175503398691,126.281188741757));
#174380=CARTESIAN_POINT('Ctrl Pts',(-52.4231956802582,3.93525272345958,
126.386021951845));
#174381=CARTESIAN_POINT('Ctrl Pts',(-52.4157993233228,4.05294988800302,
126.490850513518));
#174382=CARTESIAN_POINT('Ctrl Pts',(-52.4084029663873,4.16646278653926,
126.600391714284));
#174383=CARTESIAN_POINT('Ctrl Pts',(-52.4010066094519,4.27540389837806,
126.714268678717));
#174384=CARTESIAN_POINT('Ctrl Pts',(-52.3936091201153,4.38436168937888,
126.828163078004));
#174385=CARTESIAN_POINT('Ctrl Pts',(-52.3862116307787,4.48874604191685,
126.946394292946));
#174386=CARTESIAN_POINT('Ctrl Pts',(-52.3788141414421,4.58820765995969,
127.0685499918));
#174387=CARTESIAN_POINT('Ctrl Pts',(-52.3714140589272,4.68770414411854,
127.190748512145));
#174388=CARTESIAN_POINT('Ctrl Pts',(-52.3640139764122,4.78227422246028,
127.316873966156));
#174389=CARTESIAN_POINT('Ctrl Pts',(-52.3566138938972,4.8716101983397,127.446482621281));
#174390=CARTESIAN_POINT('Ctrl Pts',(-52.3492056742307,4.96104440830883,
127.576233794447));
#174391=CARTESIAN_POINT('Ctrl Pts',(-52.3417974545643,5.04523280985229,
127.709475510216));
#174392=CARTESIAN_POINT('Ctrl Pts',(-52.3343892348978,5.12391181748065,
127.845736232961));
#174393=CARTESIAN_POINT('Ctrl Pts',(-52.3269764555957,5.20263925072538,
127.982080821906));
#174394=CARTESIAN_POINT('Ctrl Pts',(-52.3195636762936,5.27585035998211,
128.121447790711));
#174395=CARTESIAN_POINT('Ctrl Pts',(-52.3121508969916,5.34332874189719,
128.26334339635));
#174396=CARTESIAN_POINT('Ctrl Pts',(-52.3047275259628,5.41090354008868,
128.405441749085));
#174397=CARTESIAN_POINT('Ctrl Pts',(-52.2973041549342,5.47272910495652,
128.55007561235));
#174398=CARTESIAN_POINT('Ctrl Pts',(-52.2898807839054,5.52863784456495,
128.696733006686));
#174399=CARTESIAN_POINT('Ctrl Pts',(-52.2859447344646,5.55828199981758,
128.77449427616));
#174400=CARTESIAN_POINT('Ctrl Pts',(-52.2820086850237,5.58626356198724,
128.852824197292));
#174401=CARTESIAN_POINT('Ctrl Pts',(-52.2780726355828,5.61256334802277,
128.931645148806));
#174402=CARTESIAN_POINT('Ctrl Pts',(-52.2706493691774,5.6621639236969,129.080299003443));
#174403=CARTESIAN_POINT('Ctrl Pts',(-52.2632261027721,5.70592957275061,
129.231149575616));
#174404=CARTESIAN_POINT('Ctrl Pts',(-52.2558028363666,5.74366156245514,
129.383697948782));
#174405=CARTESIAN_POINT('Ctrl Pts',(-52.2483883436456,5.78134895608134,
129.53606602244));
#174406=CARTESIAN_POINT('Ctrl Pts',(-52.2409738509246,5.81301679646227,
129.690127543985));
#174407=CARTESIAN_POINT('Ctrl Pts',(-52.2335593582035,5.83851516519413,
129.845365712315));
#174408=CARTESIAN_POINT('Ctrl Pts',(-52.2261520118498,5.86398895763818,
130.000454256253));
#174409=CARTESIAN_POINT('Ctrl Pts',(-52.2187446654959,5.88330505638482,
130.156716823324));
#174410=CARTESIAN_POINT('Ctrl Pts',(-52.2113373191421,5.89636395225233,
130.313623717507));
#174411=CARTESIAN_POINT('Ctrl Pts',(-52.2039354974668,5.90941310830254,
130.470413584608));
#174412=CARTESIAN_POINT('Ctrl Pts',(-52.1965336757915,5.91621432298951,
130.627846451544));
#174413=CARTESIAN_POINT('Ctrl Pts',(-52.1891318541161,5.91671957109146,
130.785384855043));
#174414=CARTESIAN_POINT('Ctrl Pts',(-52.1817339398047,5.91722455247687,
130.942840095246));
#174415=CARTESIAN_POINT('Ctrl Pts',(-52.1743360254934,5.91144018517517,
131.100400388709));
#174416=CARTESIAN_POINT('Ctrl Pts',(-52.166938111182,5.89937047115848,131.257525716093));
#174417=CARTESIAN_POINT('Ctrl Pts',(-52.1595414262698,5.88730276290932,
131.414624932099));
#174418=CARTESIAN_POINT('Ctrl Pts',(-52.1521447413576,5.86895180955259,
131.571288953651));
#174419=CARTESIAN_POINT('Ctrl Pts',(-52.1447480564454,5.84437367424631,
131.726980213216));
#174420=CARTESIAN_POINT('Ctrl Pts',(-52.1373516995099,5.81979662876026,
131.882664569267));
#174421=CARTESIAN_POINT('Ctrl Pts',(-52.1299553425744,5.78899300855361,
132.037375880365));
#174422=CARTESIAN_POINT('Ctrl Pts',(-52.122558985639,5.75207042519614,132.190584404003));
#174423=CARTESIAN_POINT('Ctrl Pts',(-52.1151614963024,5.71514218889695,
132.343816384257));
#174424=CARTESIAN_POINT('Ctrl Pts',(-52.1077640069658,5.6720932115609,132.495544756));
#174425=CARTESIAN_POINT('Ctrl Pts',(-52.1003665176293,5.62308159652317,
132.645252771208));
#174426=CARTESIAN_POINT('Ctrl Pts',(-52.0929664351143,5.57405280053977,
132.79501326633));
#174427=CARTESIAN_POINT('Ctrl Pts',(-52.0855663525993,5.51905732136755,
132.942751640281));
#174428=CARTESIAN_POINT('Ctrl Pts',(-52.0781662700843,5.45830216621815,
133.087969170878));
#174429=CARTESIAN_POINT('Ctrl Pts',(-52.0707580504178,5.3974802045298,133.233346383078));
#174430=CARTESIAN_POINT('Ctrl Pts',(-52.0633498307514,5.33088606290201,
133.376196871619));
#174431=CARTESIAN_POINT('Ctrl Pts',(-52.0559416110849,5.25877398321794,
133.516043998038));
#174432=CARTESIAN_POINT('Ctrl Pts',(-52.0485288317828,5.18661751975208,
133.655977198031));
#174433=CARTESIAN_POINT('Ctrl Pts',(-52.0411160524808,5.1089365346525,133.792903028561));
#174434=CARTESIAN_POINT('Ctrl Pts',(-52.0337032731787,5.02602945661223,
133.926372543194));
#174435=CARTESIAN_POINT('Ctrl Pts',(-52.02627990215,4.94300391705102,134.060032765329));
#174436=CARTESIAN_POINT('Ctrl Pts',(-52.0188565311212,4.85473757962601,
134.190226500017));
#174437=CARTESIAN_POINT('Ctrl Pts',(-52.0114331600925,4.76157059962359,
134.316536010012));
#174438=CARTESIAN_POINT('Ctrl Pts',(-52.0074971106516,4.71217123131458,
134.383508342967));
#174439=CARTESIAN_POINT('Ctrl Pts',(-52.0035610612108,4.66139476808778,
134.449389259386));
#174440=CARTESIAN_POINT('Ctrl Pts',(-51.9996250117699,4.60929614601334,
134.514120663829));
#174441=CARTESIAN_POINT('Ctrl Pts',(-51.9922017453645,4.51103977072458,
134.636202072408));
#174442=CARTESIAN_POINT('Ctrl Pts',(-51.9847784789591,4.40778131439432,
134.754561771454));
#174443=CARTESIAN_POINT('Ctrl Pts',(-51.9773552125536,4.29983310974557,
134.868762884915));
#174444=CARTESIAN_POINT('Ctrl Pts',(-51.9699407198326,4.19201249091017,
134.982829022145));
#174445=CARTESIAN_POINT('Ctrl Pts',(-51.9625262271117,4.07951341084149,
135.092746088694));
#174446=CARTESIAN_POINT('Ctrl Pts',(-51.9551117343906,3.96268963438439,
135.198108610344));
#174447=CARTESIAN_POINT('Ctrl Pts',(-51.9477043880368,3.84597845708105,
135.30336957963));
#174448=CARTESIAN_POINT('Ctrl Pts',(-51.9402970416831,3.72495115701242,
135.404084494993));
#174449=CARTESIAN_POINT('Ctrl Pts',(-51.9328896953293,3.5999995952991,135.499883322904));
#174450=CARTESIAN_POINT('Ctrl Pts',(-51.9254878736538,3.47514122717394,
135.595610700435));
#174451=CARTESIAN_POINT('Ctrl Pts',(-51.9180860519783,3.3463647201556,135.686429065064));
#174452=CARTESIAN_POINT('Ctrl Pts',(-51.9106842303029,3.21409629851096,
135.772007499783));
#174453=CARTESIAN_POINT('Ctrl Pts',(-51.9032863159915,3.08189770033766,
135.857540758312));
#174454=CARTESIAN_POINT('Ctrl Pts',(-51.8958884016802,2.94621117129102,
135.937839393519));
#174455=CARTESIAN_POINT('Ctrl Pts',(-51.8884904873688,2.80749320809699,
136.012614878735));
#174456=CARTESIAN_POINT('Ctrl Pts',(-51.8810938024566,2.66879829731183,
136.087377937623));
#174457=CARTESIAN_POINT('Ctrl Pts',(-51.8736971175444,2.52707328048832,
136.156619491218));
#174458=CARTESIAN_POINT('Ctrl Pts',(-51.8663004326322,2.38280073192316,
136.220096138661));
#174459=CARTESIAN_POINT('Ctrl Pts',(-51.8589040756968,2.23853458055379,
136.283569971483));
#174460=CARTESIAN_POINT('Ctrl Pts',(-51.8515077187613,2.09172146373359,
136.341279256081));
#174461=CARTESIAN_POINT('Ctrl Pts',(-51.8441113618258,1.94286523551681,
136.393028190353));
#174462=CARTESIAN_POINT('Ctrl Pts',(-51.8367138724892,1.79398621703191,
136.444785047519));
#174463=CARTESIAN_POINT('Ctrl Pts',(-51.8293163831528,1.64306381693422,
136.490579614774));
#174464=CARTESIAN_POINT('Ctrl Pts',(-51.8219188938162,1.49061824868513,
136.530265594003));
#174465=CARTESIAN_POINT('Ctrl Pts',(-51.8145188113012,1.33811924087842,
136.569965485091));
#174466=CARTESIAN_POINT('Ctrl Pts',(-51.8071187287862,1.18409636287308,
136.603552430741));
#174467=CARTESIAN_POINT('Ctrl Pts',(-51.7997186462712,1.02908109622292,
136.630931020461));
#174468=CARTESIAN_POINT('Ctrl Pts',(-51.7923104266047,0.87389537435112,
136.658339715755));
#174469=CARTESIAN_POINT('Ctrl Pts',(-51.7849022069383,0.717715452403777,
136.679526356733));
#174470=CARTESIAN_POINT('Ctrl Pts',(-51.7774939872719,0.561079763766469,
136.69444720956));
#174471=CARTESIAN_POINT('Ctrl Pts',(-51.7700812079698,0.404347668476189,
136.709377245923));
#174472=CARTESIAN_POINT('Ctrl Pts',(-51.7626684286677,0.247159619399972,
136.718033789121));
#174473=CARTESIAN_POINT('Ctrl Pts',(-51.7552556493657,0.0900546358877009,
136.720425249148));
#174474=CARTESIAN_POINT('Ctrl Pts',(-51.7478322783369,-0.0672748265925056,
136.722820126206));
#174475=CARTESIAN_POINT('Ctrl Pts',(-51.7404089073082,-0.224520614267026,
136.718932050455));
#174476=CARTESIAN_POINT('Ctrl Pts',(-51.7329855362795,-0.381147410718013,
136.708821406986));
#174477=CARTESIAN_POINT('Ctrl Pts',(-51.7290494868387,-0.464194696405279,
136.703460501218));
#174478=CARTESIAN_POINT('Ctrl Pts',(-51.7251134373979,-0.54706809589055,
136.696351069196));
#174479=CARTESIAN_POINT('Ctrl Pts',(-51.7211773879571,-0.629689037547038,
136.687507928189));
#174480=CARTESIAN_POINT('Ctrl Pts',(-51.7137541215516,-0.785509554999487,
136.670830040235));
#174481=CARTESIAN_POINT('Ctrl Pts',(-51.7063308551461,-0.940902639802616,
136.647932084924));
#174482=CARTESIAN_POINT('Ctrl Pts',(-51.6989075887406,-1.09533191229578,
136.618840694444));
#174483=CARTESIAN_POINT('Ctrl Pts',(-51.6914930960196,-1.24957866221319,
136.589783687571));
#174484=CARTESIAN_POINT('Ctrl Pts',(-51.6840786032987,-1.40286350403403,
136.554547884713));
#174485=CARTESIAN_POINT('Ctrl Pts',(-51.6766641105777,-1.55465408227488,
136.513211749533));
#174486=CARTESIAN_POINT('Ctrl Pts',(-51.6692567642239,-1.7062983590414,
136.471915455677));
#174487=CARTESIAN_POINT('Ctrl Pts',(-51.6618494178702,-1.85645088167409,
136.424530632311));
#174488=CARTESIAN_POINT('Ctrl Pts',(-51.6544420715164,-2.00458851997636,
136.371186951132));
#174489=CARTESIAN_POINT('Ctrl Pts',(-51.6470402498409,-2.15261567164096,
136.317883055682));
#174490=CARTESIAN_POINT('Ctrl Pts',(-51.6396384281654,-2.2986305814974,
136.25862927763));
#174491=CARTESIAN_POINT('Ctrl Pts',(-51.6322366064899,-2.44212445506916,
136.193605342799));
#174492=CARTESIAN_POINT('Ctrl Pts',(-51.6248386921785,-2.58554257934057,
136.128615733598));
#174493=CARTESIAN_POINT('Ctrl Pts',(-51.6174407778672,-2.72644197859387,
136.057862187601));
#174494=CARTESIAN_POINT('Ctrl Pts',(-51.6100428635558,-2.86433315953933,
135.981572812721));
#174495=CARTESIAN_POINT('Ctrl Pts',(-51.6026461786436,-3.00220142547232,
135.905296115751));
#174496=CARTESIAN_POINT('Ctrl Pts',(-51.5952494937313,-3.13706213895409,
135.823485596273));
#174497=CARTESIAN_POINT('Ctrl Pts',(-51.587852808819,-3.26844967675284,
135.7364156936));
#174498=CARTESIAN_POINT('Ctrl Pts',(-51.5804564518836,-3.39983138869029,
135.649349651698));
#174499=CARTESIAN_POINT('Ctrl Pts',(-51.5730600949482,-3.52773991998567,
135.557024896506));
#174500=CARTESIAN_POINT('Ctrl Pts',(-51.5656637380127,-3.65173819136145,
135.459759498892));
#174501=CARTESIAN_POINT('Ctrl Pts',(-51.5582662486762,-3.77575544718895,
135.362479209697));
#174502=CARTESIAN_POINT('Ctrl Pts',(-51.5508687593395,-3.89586095732777,
135.260257002346));
#174503=CARTESIAN_POINT('Ctrl Pts',(-51.543471270003,-4.01165044894745,
135.153451469452));
#174504=CARTESIAN_POINT('Ctrl Pts',(-51.5360711874879,-4.12748053039493,
135.046608496043));
#174505=CARTESIAN_POINT('Ctrl Pts',(-51.5286711049729,-4.23899130678344,
134.935179251152));
#174506=CARTESIAN_POINT('Ctrl Pts',(-51.5212710224578,-4.34581522780061,
134.819559313561));
#174507=CARTESIAN_POINT('Ctrl Pts',(-51.5138628027913,-4.45275661269994,
134.703812239962));
#174508=CARTESIAN_POINT('Ctrl Pts',(-51.5064545831248,-4.55500059651085,
134.583865545343));
#174509=CARTESIAN_POINT('Ctrl Pts',(-51.4990463634584,-4.65221934832278,
134.460148589754));
#174510=CARTESIAN_POINT('Ctrl Pts',(-51.4916335841563,-4.74949793665456,
134.336355488442));
#174511=CARTESIAN_POINT('Ctrl Pts',(-51.4842208048541,-4.84174491166975,
134.208787804002));
#174512=CARTESIAN_POINT('Ctrl Pts',(-51.476808025552,-4.92867599581161,
134.077903574488));
#174513=CARTESIAN_POINT('Ctrl Pts',(-51.4693846545233,-5.01573129116279,
133.946832331448));
#174514=CARTESIAN_POINT('Ctrl Pts',(-51.4619612834945,-5.09745533209747,
133.812435396931));
#174515=CARTESIAN_POINT('Ctrl Pts',(-51.4545379124658,-5.1736095707027,
133.675195787414));
#174516=CARTESIAN_POINT('Ctrl Pts',(-51.4506018630252,-5.21398837530511,
133.602428053432));
#174517=CARTESIAN_POINT('Ctrl Pts',(-51.4466658135846,-5.25280210551076,
133.528861493687));
#174518=CARTESIAN_POINT('Ctrl Pts',(-51.442729764144,-5.29002075762279,
133.454570221809));
#174519=CARTESIAN_POINT('Ctrl Pts',(-51.4347880966952,-5.3651158910625,
133.304674600701));
#174520=CARTESIAN_POINT('Ctrl Pts',(-51.4268464292464,-5.43391710599038,
133.151423594091));
#174521=CARTESIAN_POINT('Ctrl Pts',(-51.4189047617976,-5.49613374452766,
132.995352270851));
#174522=CARTESIAN_POINT('Ctrl Pts',(-51.4109782153217,-5.55823192228682,
132.839578108159));
#174523=CARTESIAN_POINT('Ctrl Pts',(-51.4030516688456,-5.61377041282377,
132.680994606987));
#174524=CARTESIAN_POINT('Ctrl Pts',(-51.3951251223697,-5.66250500041385,
132.520160047216));
#174525=CARTESIAN_POINT('Ctrl Pts',(-51.3872200850336,-5.71110734389741,
132.359761921275));
#174526=CARTESIAN_POINT('Ctrl Pts',(-51.3793150476975,-5.75294252721499,
132.197125200942));
#174527=CARTESIAN_POINT('Ctrl Pts',(-51.3714100103613,-5.78781509037246,
132.03282593745));
#174528=CARTESIAN_POINT('Ctrl Pts',(-51.3635181584019,-5.82262948708961,
131.868800720441));
#174529=CARTESIAN_POINT('Ctrl Pts',(-51.3556263064426,-5.85050435298047,
131.70311877322));
#174530=CARTESIAN_POINT('Ctrl Pts',(-51.3477344544831,-5.87129377485024,
131.536371527256));
#174531=CARTESIAN_POINT('Ctrl Pts',(-51.3398611043402,-5.89203445758117,
131.370015206889));
#174532=CARTESIAN_POINT('Ctrl Pts',(-51.3319877541973,-5.90572279094747,
131.202598859044));
#174533=CARTESIAN_POINT('Ctrl Pts',(-51.3241144040543,-5.91226381036876,
131.034723807125));
#174534=CARTESIAN_POINT('Ctrl Pts',(-51.3205346847667,-5.9152377684626,
130.958397268821));
#174535=CARTESIAN_POINT('Ctrl Pts',(-51.3169549654791,-5.91673493774469,
130.881976074287));
#174536=CARTESIAN_POINT('Ctrl Pts',(-51.3133752461914,-5.91674988690743,
130.805517458505));
#174537=CARTESIAN_POINT('',(-49.5633751912882,-5.91573782775675,130.798896933973));
#174538=CARTESIAN_POINT('Ctrl Pts',(-51.3133751922042,-5.9071383279532,
130.805514428026));
#174539=CARTESIAN_POINT('Ctrl Pts',(-51.2636775082465,-5.90529917539433,
129.745753984472));
#174540=CARTESIAN_POINT('Ctrl Pts',(-51.1211639496847,-5.12604516750494,
126.704251395053));
#174541=CARTESIAN_POINT('Ctrl Pts',(-50.8858345165182,-0.250194475344861,
123.810437308373));
#174542=CARTESIAN_POINT('Ctrl Pts',(-50.6073868927055,5.74894953295976,
126.81347853489));
#174543=CARTESIAN_POINT('Ctrl Pts',(-50.3289392688926,6.46508977227328,
133.483945429956));
#174544=CARTESIAN_POINT('Ctrl Pts',(-50.0504916450797,1.24012834806205,
137.692004787431));
#174545=CARTESIAN_POINT('Ctrl Pts',(-49.7953036195168,-4.59279733233232,
135.747858542419));
#174546=CARTESIAN_POINT('Ctrl Pts',(-49.6329314685584,-5.902229748077,132.27673871186));
#174547=CARTESIAN_POINT('Ctrl Pts',(-49.5633751922042,-5.91567488377501,
130.798897011574));
#174548=CARTESIAN_POINT('',(-47.8133744782874,-5.92195381510691,130.805598640966));
#174549=CARTESIAN_POINT('Ctrl Pts',(-49.5633751765939,-5.91674747619486,
130.798895689225));
#174550=CARTESIAN_POINT('Ctrl Pts',(-49.5538760923211,-5.91656103173357,
130.597036721113));
#174551=CARTESIAN_POINT('Ctrl Pts',(-49.5443770080484,-5.9060410641023,
130.395639713077));
#174552=CARTESIAN_POINT('Ctrl Pts',(-49.5348779237755,-5.88534989114146,
130.195601862934));
#174553=CARTESIAN_POINT('Ctrl Pts',(-49.5251696431194,-5.86420304072518,
129.991158620273));
#174554=CARTESIAN_POINT('Ctrl Pts',(-49.5154613624632,-5.83243204681259,
129.788134809279));
#174555=CARTESIAN_POINT('Ctrl Pts',(-49.5057530818071,-5.79025820845633,
129.587462741036));
#174556=CARTESIAN_POINT('Ctrl Pts',(-49.5017008536894,-5.77265488407041,
129.503702389828));
#174557=CARTESIAN_POINT('Ctrl Pts',(-49.4976486255716,-5.7532397230529,
129.420351485477));
#174558=CARTESIAN_POINT('Ctrl Pts',(-49.4935963974539,-5.73203124524393,
129.337476720985));
#174559=CARTESIAN_POINT('Ctrl Pts',(-49.4861731310485,-5.69317948856694,
129.185658650227));
#174560=CARTESIAN_POINT('Ctrl Pts',(-49.4787498646431,-5.64823325758814,
129.035155615431));
#174561=CARTESIAN_POINT('Ctrl Pts',(-49.4713265982376,-5.59729583156049,
128.886494632546));
#174562=CARTESIAN_POINT('Ctrl Pts',(-49.4639121055166,-5.54641860934023,
128.738009354597));
#174563=CARTESIAN_POINT('Ctrl Pts',(-49.4564976127956,-5.48956440684963,
128.591362144619));
#174564=CARTESIAN_POINT('Ctrl Pts',(-49.4490831200745,-5.42688722194317,
128.447068602815));
#174565=CARTESIAN_POINT('Ctrl Pts',(-49.4416757737207,-5.36427044766719,
128.302914136558));
#174566=CARTESIAN_POINT('Ctrl Pts',(-49.434268427367,-5.29584201190525,
128.161109162323));
#174567=CARTESIAN_POINT('Ctrl Pts',(-49.4268610810132,-5.2218052682233,
128.022152806626));
#174568=CARTESIAN_POINT('Ctrl Pts',(-49.4194592593378,-5.14782374393836,
127.883300089822));
#174569=CARTESIAN_POINT('Ctrl Pts',(-49.4120574376624,-5.06824241520598,
127.747292089211));
#174570=CARTESIAN_POINT('Ctrl Pts',(-49.4046556159871,-4.98331211643455,
127.614606565496));
#174571=CARTESIAN_POINT('Ctrl Pts',(-49.3972577016757,-4.89842665170675,
127.481991085436));
#174572=CARTESIAN_POINT('Ctrl Pts',(-49.3898597873643,-4.80819804117083,
127.352694902888));
#174573=CARTESIAN_POINT('Ctrl Pts',(-49.382461873053,-4.71292223322602,
127.227169738389));
#174574=CARTESIAN_POINT('Ctrl Pts',(-49.3750651881408,-4.61766225839188,
127.101665433896));
#174575=CARTESIAN_POINT('Ctrl Pts',(-49.3676685032286,-4.51735697629474,
126.979931200743));
#174576=CARTESIAN_POINT('Ctrl Pts',(-49.3602718183164,-4.41234476461102,
126.86238849175));
#174577=CARTESIAN_POINT('Ctrl Pts',(-49.352875461381,-4.30733720927881,
126.744850994724));
#174578=CARTESIAN_POINT('Ctrl Pts',(-49.3454791044454,-4.19762338805193,
126.631504930694));
#174579=CARTESIAN_POINT('Ctrl Pts',(-49.33808274751,-4.0835807656593,126.522737246362));
#174580=CARTESIAN_POINT('Ctrl Pts',(-49.3306852581734,-3.96952068304989,
126.41395290942));
#174581=CARTESIAN_POINT('Ctrl Pts',(-49.3232877688369,-3.85113074980261,
126.30974860554));
#174582=CARTESIAN_POINT('Ctrl Pts',(-49.3158902795003,-3.72882382875141,
126.210473002851));
#174583=CARTESIAN_POINT('Ctrl Pts',(-49.3084901969853,-3.60647403319846,
126.111162599253));
#174584=CARTESIAN_POINT('Ctrl Pts',(-49.3010901144702,-3.48020480567695,
126.016784571892));
#174585=CARTESIAN_POINT('Ctrl Pts',(-49.2936900319552,-3.35046034648829,
125.927645941771));
#174586=CARTESIAN_POINT('Ctrl Pts',(-49.2862818122888,-3.22057321992887,
125.838409294564));
#174587=CARTESIAN_POINT('Ctrl Pts',(-49.2788735926223,-3.08720353803567,
125.754423761719));
#174588=CARTESIAN_POINT('Ctrl Pts',(-49.2714653729558,-2.95082323702318,
125.675952210824));
#174589=CARTESIAN_POINT('Ctrl Pts',(-49.2640525936537,-2.81435899621084,
125.597432361999));
#174590=CARTESIAN_POINT('Ctrl Pts',(-49.2566398143518,-2.67488077394437,
125.524433430321));
#174591=CARTESIAN_POINT('Ctrl Pts',(-49.2492270350497,-2.5328826420075,
125.457171067502));
#174592=CARTESIAN_POINT('Ctrl Pts',(-49.2418036640209,-2.39068161648087,
125.389812597064));
#174593=CARTESIAN_POINT('Ctrl Pts',(-49.2343802929921,-2.24595383271325,
125.328207211908));
#174594=CARTESIAN_POINT('Ctrl Pts',(-49.2269569219633,-2.09921152462009,
125.27252172463));
#174595=CARTESIAN_POINT('Ctrl Pts',(-49.2230208725225,-2.02140523183575,
125.24299594312));
#174596=CARTESIAN_POINT('Ctrl Pts',(-49.2190848230818,-1.94303281823506,
125.215133618159));
#174597=CARTESIAN_POINT('Ctrl Pts',(-49.215148773641,-1.86417193419749,
125.188953814649));
#174598=CARTESIAN_POINT('Ctrl Pts',(-49.2077255072355,-1.71544276806656,
125.139579522273));
#174599=CARTESIAN_POINT('Ctrl Pts',(-49.2003022408301,-1.56452576670862,
125.09604349279));
#174600=CARTESIAN_POINT('Ctrl Pts',(-49.1928789744247,-1.41192014852576,
125.058543699434));
#174601=CARTESIAN_POINT('Ctrl Pts',(-49.1854644817037,-1.25949489751027,
125.02108822772));
#174602=CARTESIAN_POINT('Ctrl Pts',(-49.1780499889827,-1.10538536130388,
124.98965487942));
#174603=CARTESIAN_POINT('Ctrl Pts',(-49.1706354962616,-0.950108568560871,
124.964392786281));
#174604=CARTESIAN_POINT('Ctrl Pts',(-49.1632281499079,-0.794981437436779,
124.939155041698));
#174605=CARTESIAN_POINT('Ctrl Pts',(-49.155820803554,-0.638689655500852,
124.920076770346));
#174606=CARTESIAN_POINT('Ctrl Pts',(-49.1484134572003,-0.481763069596425,
124.907256675183));
#174607=CARTESIAN_POINT('Ctrl Pts',(-49.1410116355249,-0.324953525460267,
124.89444614173));
#174608=CARTESIAN_POINT('Ctrl Pts',(-49.1336098138495,-0.167510490536946,
124.887884520943));
#174609=CARTESIAN_POINT('Ctrl Pts',(-49.1262079921741,-0.00997150056215477,
124.887619020058));
#174610=CARTESIAN_POINT('Ctrl Pts',(-49.1188100778627,0.14748432580611,
124.88735365933));
#174611=CARTESIAN_POINT('Ctrl Pts',(-49.1114121635514,0.305035633993691,
124.893377799879));
#174612=CARTESIAN_POINT('Ctrl Pts',(-49.10401424924,0.46214241137939,124.90568661792));
#174613=CARTESIAN_POINT('Ctrl Pts',(-49.0966175643278,0.61922308046867,
124.917993390458));
#174614=CARTESIAN_POINT('Ctrl Pts',(-49.0892208794156,0.775858993578949,
124.936582738537));
#174615=CARTESIAN_POINT('Ctrl Pts',(-49.0818241945034,0.931512669118098,
124.961397780976));
#174616=CARTESIAN_POINT('Ctrl Pts',(-49.0744278375679,1.08715944281038,
124.98621172309));
#174617=CARTESIAN_POINT('Ctrl Pts',(-49.0670314806325,1.24182369688828,
125.017250751906));
#174618=CARTESIAN_POINT('Ctrl Pts',(-49.059635123697,1.39497585322708,125.0544064498));
#174619=CARTESIAN_POINT('Ctrl Pts',(-49.0522376343605,1.54815145755176,
125.091567836326));
#174620=CARTESIAN_POINT('Ctrl Pts',(-49.0448401450239,1.69981414038029,
125.134847668565));
#174621=CARTESIAN_POINT('Ctrl Pts',(-49.0374426556873,1.84944739489439,
125.184087056963));
#174622=CARTESIAN_POINT('Ctrl Pts',(-49.0300425731723,1.99913310311389,
125.233343706151));
#174623=CARTESIAN_POINT('Ctrl Pts',(-49.0226424906573,2.1467876122295,125.288563954295));
#174624=CARTESIAN_POINT('Ctrl Pts',(-49.0152424081423,2.29191251566261,
125.349540035453));
#174625=CARTESIAN_POINT('Ctrl Pts',(-49.0078341884759,2.43719699884644,
125.410583166079));
#174626=CARTESIAN_POINT('Ctrl Pts',(-49.0004259688094,2.57994597702167,
125.477394624718));
#174627=CARTESIAN_POINT('Ctrl Pts',(-48.9930177491429,2.71968319919072,
125.549719444418));
#174628=CARTESIAN_POINT('Ctrl Pts',(-48.9856049698408,2.85950642728856,
125.622088778838));
#174629=CARTESIAN_POINT('Ctrl Pts',(-48.9781921905387,2.99631388202598,
125.699978051789));
#174630=CARTESIAN_POINT('Ctrl Pts',(-48.9707794112367,3.12965707164409,
125.783088151706));
#174631=CARTESIAN_POINT('Ctrl Pts',(-48.9633560402079,3.26319078826452,
125.86631700323));
#174632=CARTESIAN_POINT('Ctrl Pts',(-48.9559326691793,3.39325004585048,
125.954781371145));
#174633=CARTESIAN_POINT('Ctrl Pts',(-48.9485092981505,3.51941762529719,
126.048140464835));
#174634=CARTESIAN_POINT('Ctrl Pts',(-48.9445732487097,3.58631470326899,
126.097641696429));
#174635=CARTESIAN_POINT('Ctrl Pts',(-48.9406371992689,3.65211827026437,
126.148518360397));
#174636=CARTESIAN_POINT('Ctrl Pts',(-48.9367011498281,3.71677031451401,
126.200715432319));
#174637=CARTESIAN_POINT('Ctrl Pts',(-48.9292778834227,3.83870205224826,
126.29915748095));
#174638=CARTESIAN_POINT('Ctrl Pts',(-48.9218546170173,3.9569044724428,126.402595941023));
#174639=CARTESIAN_POINT('Ctrl Pts',(-48.9144313506119,4.07094117486974,
126.510717815323));
#174640=CARTESIAN_POINT('Ctrl Pts',(-48.9070168578909,4.18484309538457,
126.618711898548));
#174641=CARTESIAN_POINT('Ctrl Pts',(-48.8996023651697,4.29458883020234,
126.731378123408));
#174642=CARTESIAN_POINT('Ctrl Pts',(-48.8921878724487,4.39977344394399,
126.848362108407));
#174643=CARTESIAN_POINT('Ctrl Pts',(-48.884780526095,4.50485667679494,126.965233339838));
#174644=CARTESIAN_POINT('Ctrl Pts',(-48.8773731797412,4.6053872925839,127.086413770715));
#174645=CARTESIAN_POINT('Ctrl Pts',(-48.8699658333874,4.70099585455471,
127.211510977244));
#174646=CARTESIAN_POINT('Ctrl Pts',(-48.862564011712,4.79653310805277,127.336514881557));
#174647=CARTESIAN_POINT('Ctrl Pts',(-48.8551621900366,4.88715539159204,
127.465429449544));
#174648=CARTESIAN_POINT('Ctrl Pts',(-48.8477603683612,4.97253243719055,
127.597827953833));
#174649=CARTESIAN_POINT('Ctrl Pts',(-48.8403624540499,5.05786441291127,
127.730156565981));
#174650=CARTESIAN_POINT('Ctrl Pts',(-48.8329645397386,5.1379564633351,127.865965138759));
#174651=CARTESIAN_POINT('Ctrl Pts',(-48.8255666254272,5.21252075683664,
128.004796736879));
#174652=CARTESIAN_POINT('Ctrl Pts',(-48.818169940515,5.28707265910534,128.143605263706));
#174653=CARTESIAN_POINT('Ctrl Pts',(-48.8107732556028,5.3560984511702,128.285435490272));
#174654=CARTESIAN_POINT('Ctrl Pts',(-48.8033765706906,5.41935546684912,
128.429804472424));
#174655=CARTESIAN_POINT('Ctrl Pts',(-48.7959802137552,5.48260967764568,
128.574167053104));
#174656=CARTESIAN_POINT('Ctrl Pts',(-48.7885838568196,5.54009547084567,
128.721067823624));
#174657=CARTESIAN_POINT('Ctrl Pts',(-48.7811874998842,5.59161781135387,
128.870002632536));
#174658=CARTESIAN_POINT('Ctrl Pts',(-48.7737900105476,5.64314804006392,
129.018960243747));
#174659=CARTESIAN_POINT('Ctrl Pts',(-48.7663925212111,5.68871287608846,
129.169952160615));
#174660=CARTESIAN_POINT('Ctrl Pts',(-48.7589950318745,5.7281668131581,129.32245794764));
#174661=CARTESIAN_POINT('Ctrl Pts',(-48.7515949493595,5.76763458074427,
129.475017195332));
#174662=CARTESIAN_POINT('Ctrl Pts',(-48.7441948668445,5.80098709090098,
129.629091008595));
#174663=CARTESIAN_POINT('Ctrl Pts',(-48.7367947843294,5.82812974206965,
129.784147761294));
#174664=CARTESIAN_POINT('Ctrl Pts',(-48.729386564663,5.85530223937357,129.939375014832));
#174665=CARTESIAN_POINT('Ctrl Pts',(-48.7219783449966,5.8762511765631,130.095586998386));
#174666=CARTESIAN_POINT('Ctrl Pts',(-48.7145701253302,5.89093363925821,
130.252245212641));
#174667=CARTESIAN_POINT('Ctrl Pts',(-48.7071573460281,5.90562513876414,
130.408999847412));
#174668=CARTESIAN_POINT('Ctrl Pts',(-48.6997445667261,5.91404245848461,
130.566200888252));
#174669=CARTESIAN_POINT('Ctrl Pts',(-48.692331787424,5.91619482870196,130.723309329235));
#174670=CARTESIAN_POINT('Ctrl Pts',(-48.6849084163952,5.91835027432682,
130.880642254125));
#174671=CARTESIAN_POINT('Ctrl Pts',(-48.6774850453664,5.91422290175767,
131.037881942723));
#174672=CARTESIAN_POINT('Ctrl Pts',(-48.6700616743377,5.90387391067542,
131.194493171125));
#174673=CARTESIAN_POINT('Ctrl Pts',(-48.6661256248968,5.89838662728293,
131.277532202259));
#174674=CARTESIAN_POINT('Ctrl Pts',(-48.662189575456,5.89115108428755,131.360394686433));
#174675=CARTESIAN_POINT('Ctrl Pts',(-48.6582535260152,5.8821822185121,131.443002074661));
#174676=CARTESIAN_POINT('Ctrl Pts',(-48.6508302596098,5.86526721756844,
131.598797030769));
#174677=CARTESIAN_POINT('Ctrl Pts',(-48.6434069932043,5.84213280695006,
131.754155088839));
#174678=CARTESIAN_POINT('Ctrl Pts',(-48.6359837267989,5.81280643509335,
131.908539910361));
#174679=CARTESIAN_POINT('Ctrl Pts',(-48.6285692340779,5.78351472457273,
132.062742261845));
#174680=CARTESIAN_POINT('Ctrl Pts',(-48.6211547413569,5.74804568908171,
132.215973303271));
#174681=CARTESIAN_POINT('Ctrl Pts',(-48.6137402486358,5.70647860234763,
132.36770079918));
#174682=CARTESIAN_POINT('Ctrl Pts',(-48.6063329022821,5.66495157953671,
132.519282054416));
#174683=CARTESIAN_POINT('Ctrl Pts',(-48.5989255559283,5.61733830446223,
132.66936229154));
#174684=CARTESIAN_POINT('Ctrl Pts',(-48.5915182095745,5.56376924478614,
132.817418578299));
#174685=CARTESIAN_POINT('Ctrl Pts',(-48.5841163878991,5.51024013893581,
132.965364439094));
#174686=CARTESIAN_POINT('Ctrl Pts',(-48.5767145662237,5.45076421966322,
133.111289005703));
#174687=CARTESIAN_POINT('Ctrl Pts',(-48.5693127445483,5.38552198688106,
133.25468375775));
#174688=CARTESIAN_POINT('Ctrl Pts',(-48.5619148302369,5.32031419496584,
133.398002812823));
#174689=CARTESIAN_POINT('Ctrl Pts',(-48.5545169159256,5.24934630600076,
133.538794374064));
#174690=CARTESIAN_POINT('Ctrl Pts',(-48.5471190016142,5.17284717255866,
133.676569295892));
#174691=CARTESIAN_POINT('Ctrl Pts',(-48.539722316702,5.09636075188458,133.814321322027));
#174692=CARTESIAN_POINT('Ctrl Pts',(-48.5323256317898,5.01434509209365,
133.949057377659));
#174693=CARTESIAN_POINT('Ctrl Pts',(-48.5249289468776,4.92707534078023,
134.080312257743));
#174694=CARTESIAN_POINT('Ctrl Pts',(-48.5175325899421,4.83980945909903,
134.211561317848));
#174695=CARTESIAN_POINT('Ctrl Pts',(-48.5101362330066,4.74729015580746,
134.339329198466));
#174696=CARTESIAN_POINT('Ctrl Pts',(-48.5027398760712,4.64983616656427,
134.463179304876));
#174697=CARTESIAN_POINT('Ctrl Pts',(-48.4953423867346,4.55236725686655,
134.587048373054));
#174698=CARTESIAN_POINT('Ctrl Pts',(-48.487944897398,4.44996238774628,134.706998179314));
#174699=CARTESIAN_POINT('Ctrl Pts',(-48.4805474080615,4.34298076663618,
134.822624997012));
#174700=CARTESIAN_POINT('Ctrl Pts',(-48.4731473255465,4.23596164328465,
134.938292347512));
#174701=CARTESIAN_POINT('Ctrl Pts',(-48.4657472430314,4.12436282700883,
135.04963341843));
#174702=CARTESIAN_POINT('Ctrl Pts',(-48.4583471605164,4.00858045548097,
135.156281261883));
#174703=CARTESIAN_POINT('Ctrl Pts',(-48.45093894085,3.89267076933289,135.263046375604));
#174704=CARTESIAN_POINT('Ctrl Pts',(-48.4435307211835,3.77256861567195,
135.365107702568));
#174705=CARTESIAN_POINT('Ctrl Pts',(-48.436122501517,3.6487038529544,135.462138065656));
#174706=CARTESIAN_POINT('Ctrl Pts',(-48.4287097222149,3.52476285354219,
135.559228149314));
#174707=CARTESIAN_POINT('Ctrl Pts',(-48.4212969429129,3.3970549326316,135.651280881209));
#174708=CARTESIAN_POINT('Ctrl Pts',(-48.4138841636108,3.26603856036764,
135.738012681169));
#174709=CARTESIAN_POINT('Ctrl Pts',(-48.4064607925821,3.13483498576692,
135.824868407592));
#174710=CARTESIAN_POINT('Ctrl Pts',(-48.3990374215534,3.00031383680022,
135.906387824636));
#174711=CARTESIAN_POINT('Ctrl Pts',(-48.3916140505246,2.86295849241714,
135.982333119733));
#174712=CARTESIAN_POINT('Ctrl Pts',(-48.3876780010838,2.79012939302957,
136.022601137475));
#174713=CARTESIAN_POINT('Ctrl Pts',(-48.3837419516431,2.71650385058052,
136.061302866956));
#174714=CARTESIAN_POINT('Ctrl Pts',(-48.3798059022023,2.64215602427448,
136.098408417302));
#174715=CARTESIAN_POINT('Ctrl Pts',(-48.3723826357969,2.50193834417637,
136.16838832723));
#174716=CARTESIAN_POINT('Ctrl Pts',(-48.3649593693915,2.35872649592454,
136.232899517595));
#174717=CARTESIAN_POINT('Ctrl Pts',(-48.357536102986,2.21298655284755,136.291675177477));
#174718=CARTESIAN_POINT('Ctrl Pts',(-48.350121610265,2.06741886228034,136.350381369411));
#174719=CARTESIAN_POINT('Ctrl Pts',(-48.342707117544,1.91932936733809,136.403365386084));
#174720=CARTESIAN_POINT('Ctrl Pts',(-48.335292624823,1.76920870217187,136.450406236462));
#174721=CARTESIAN_POINT('Ctrl Pts',(-48.3278852784692,1.61923272895446,
136.497401747098));
#174722=CARTESIAN_POINT('Ctrl Pts',(-48.3204779321155,1.46722983677219,
136.538465384379));
#174723=CARTESIAN_POINT('Ctrl Pts',(-48.3130705857617,1.31371050429746,
136.573424256788));
#174724=CARTESIAN_POINT('Ctrl Pts',(-48.3056687640863,1.16030567233307,
136.608357055552));
#174725=CARTESIAN_POINT('Ctrl Pts',(-48.2982669424109,1.00538701450003,
136.63719407288));
#174726=CARTESIAN_POINT('Ctrl Pts',(-48.2908651207355,0.849479928003844,
136.659812300777));
#174727=CARTESIAN_POINT('Ctrl Pts',(-48.2834672064241,0.693655143644823,
136.682418588688));
#174728=CARTESIAN_POINT('Ctrl Pts',(-48.2760692921128,0.536843338275426,
136.698812571662));
#174729=CARTESIAN_POINT('Ctrl Pts',(-48.2686713778014,0.379579744332311,
136.708922394717));
#174730=CARTESIAN_POINT('Ctrl Pts',(-48.2612746928892,0.222342284745682,
136.719030537702));
#174731=CARTESIAN_POINT('Ctrl Pts',(-48.253878007977,0.0646535577592358,
136.722856569496));
#174732=CARTESIAN_POINT('Ctrl Pts',(-48.2464813230648,-0.092946322453696,
136.720380524872));
#174733=CARTESIAN_POINT('Ctrl Pts',(-48.2390849661294,-0.250539214522786,
136.717904590039));
#174734=CARTESIAN_POINT('Ctrl Pts',(-48.2316886091939,-0.408042894400034,
136.709127140275));
#174735=CARTESIAN_POINT('Ctrl Pts',(-48.2242922522585,-0.56491775817197,
136.694080346806));
#174736=CARTESIAN_POINT('Ctrl Pts',(-48.2168947629219,-0.721816639886255,
136.679031249635));
#174737=CARTESIAN_POINT('Ctrl Pts',(-48.2094972735853,-0.87808614218579,
136.657710933208));
#174738=CARTESIAN_POINT('Ctrl Pts',(-48.2020997842487,-1.03319243801818,
136.630203384799));
#174739=CARTESIAN_POINT('Ctrl Pts',(-48.1946997017337,-1.18835310612214,
136.602686193662));
#174740=CARTESIAN_POINT('Ctrl Pts',(-48.1872996192187,-1.34234938857821,
136.568977517374));
#174741=CARTESIAN_POINT('Ctrl Pts',(-48.1798995367037,-1.49465843965174,
136.529212293485));
#174742=CARTESIAN_POINT('Ctrl Pts',(-48.1724913170373,-1.64713497018445,
136.489403343645));
#174743=CARTESIAN_POINT('Ctrl Pts',(-48.1650830973708,-1.7979202027976,
136.443524640511));
#174744=CARTESIAN_POINT('Ctrl Pts',(-48.1576748777043,-1.94650652512017,
136.391760988952));
#174745=CARTESIAN_POINT('Ctrl Pts',(-48.1502620984023,-2.09518429984484,
136.339965477729));
#174746=CARTESIAN_POINT('Ctrl Pts',(-48.1428493191002,-2.24166012094816,
136.282277937093));
#174747=CARTESIAN_POINT('Ctrl Pts',(-48.1354365397981,-2.38544759008819,
136.218930808952));
#174748=CARTESIAN_POINT('Ctrl Pts',(-48.1280131687694,-2.5294405095073,
136.155493167463));
#174749=CARTESIAN_POINT('Ctrl Pts',(-48.1205897977406,-2.67073707069456,
136.086379951135));
#174750=CARTESIAN_POINT('Ctrl Pts',(-48.1131664267119,-2.80887591707196,
136.011869296867));
#174751=CARTESIAN_POINT('Ctrl Pts',(-48.109230377271,-2.88212044801796,
135.972361960115));
#174752=CARTESIAN_POINT('Ctrl Pts',(-48.1052943278302,-2.95447771321897,
135.931337936195));
#174753=CARTESIAN_POINT('Ctrl Pts',(-48.1013582783894,-3.02588247977486,
135.888843460598));
#174754=CARTESIAN_POINT('Ctrl Pts',(-48.093935011984,-3.16054964103153,
135.808700205831));
#174755=CARTESIAN_POINT('Ctrl Pts',(-48.0865117455786,-3.2922342346609,
135.723081896093));
#174756=CARTESIAN_POINT('Ctrl Pts',(-48.0790884791732,-3.42045986106223,
135.632236434254));
#174757=CARTESIAN_POINT('Ctrl Pts',(-48.0716739864521,-3.54853393542182,
135.541498344207));
#174758=CARTESIAN_POINT('Ctrl Pts',(-48.0642594937311,-3.67315687853743,
135.445545613218));
#174759=CARTESIAN_POINT('Ctrl Pts',(-48.0568450010101,-3.79387756465029,
135.344671574642));
#174760=CARTESIAN_POINT('Ctrl Pts',(-48.0494376546563,-3.91448189562082,
135.243894762262));
#174761=CARTESIAN_POINT('Ctrl Pts',(-48.0420303083026,-4.03119117274931,
135.138206323109));
#174762=CARTESIAN_POINT('Ctrl Pts',(-48.0346229619488,-4.14358401131458,
135.02794228526));
#174763=CARTESIAN_POINT('Ctrl Pts',(-48.0272211402734,-4.2558930230605,
134.91776048649));
#174764=CARTESIAN_POINT('Ctrl Pts',(-48.019819318598,-4.36389174110269,
134.80301014438));
#174765=CARTESIAN_POINT('Ctrl Pts',(-48.0124174969226,-4.46719268530761,
134.684066801652));
#174766=CARTESIAN_POINT('Ctrl Pts',(-48.0050195826113,-4.57043909774833,
134.565186248188));
#174767=CARTESIAN_POINT('Ctrl Pts',(-47.9976216682999,-4.66899243107006,
134.442117383433));
#174768=CARTESIAN_POINT('Ctrl Pts',(-47.9902237539885,-4.76250292543401,
134.31527167422));
#174769=CARTESIAN_POINT('Ctrl Pts',(-47.9828270690763,-4.85599788005013,
134.188447044462));
#174770=CARTESIAN_POINT('Ctrl Pts',(-47.9754303841641,-4.94445143765424,
134.057847116112));
#174771=CARTESIAN_POINT('Ctrl Pts',(-47.9680336992519,-5.0275548560333,
133.923915510828));
#174772=CARTESIAN_POINT('Ctrl Pts',(-47.9606373423165,-5.11065458951971,
133.789989844212));
#174773=CARTESIAN_POINT('Ctrl Pts',(-47.953240985381,-5.18840445865811,
133.652733111597));
#174774=CARTESIAN_POINT('Ctrl Pts',(-47.9458446284456,-5.26053986091569,
133.512616686371));
#174775=CARTESIAN_POINT('Ctrl Pts',(-47.938447139109,-5.33268630728741,
133.372478808962));
#174776=CARTESIAN_POINT('Ctrl Pts',(-47.9310496497725,-5.39921640434239,
133.229480699089));
#174777=CARTESIAN_POINT('Ctrl Pts',(-47.9236521604359,-5.45991226639079,
133.084116877743));
#174778=CARTESIAN_POINT('Ctrl Pts',(-47.9162520779209,-5.52062940527981,
132.938702099334));
#174779=CARTESIAN_POINT('Ctrl Pts',(-47.9088519954058,-5.57550809347577,
132.790920302588));
#174780=CARTESIAN_POINT('Ctrl Pts',(-47.9014519128908,-5.62437924686929,
132.641284309472));
#174781=CARTESIAN_POINT('Ctrl Pts',(-47.8940436932243,-5.67330413911991,
132.491483776199));
#174782=CARTESIAN_POINT('Ctrl Pts',(-47.8866354735579,-5.71620818818213,
132.339825329848));
#174783=CARTESIAN_POINT('Ctrl Pts',(-47.8792272538914,-5.75297249874091,
132.18683593063));
#174784=CARTESIAN_POINT('Ctrl Pts',(-47.8718144745894,-5.78975943711944,
132.033752368989));
#174785=CARTESIAN_POINT('Ctrl Pts',(-47.8644016952873,-5.82039903456348,
131.879336587473));
#174786=CARTESIAN_POINT('Ctrl Pts',(-47.8569889159853,-5.84482394084855,
131.724123447313));
#174787=CARTESIAN_POINT('Ctrl Pts',(-47.8495655449565,-5.86928374658509,
131.568688531339));
#174788=CARTESIAN_POINT('Ctrl Pts',(-47.8421421739278,-5.88751108298261,
131.412454351077));
#174789=CARTESIAN_POINT('Ctrl Pts',(-47.8347188028991,-5.89949057999138,
131.255959398668));
#174790=CARTESIAN_POINT('Ctrl Pts',(-47.8307827534583,-5.9058423967496,
131.172982019855));
#174791=CARTESIAN_POINT('Ctrl Pts',(-47.8268467040173,-5.91043859283062,
131.089931316381));
#174792=CARTESIAN_POINT('Ctrl Pts',(-47.8229106545765,-5.91328280748709,
131.006887161944));
#174793=CARTESIAN_POINT('Ctrl Pts',(-47.8197321671191,-5.91557960297907,
130.939826316479));
#174794=CARTESIAN_POINT('Ctrl Pts',(-47.8165536796616,-5.91673566589503,
130.872726177956));
#174795=CARTESIAN_POINT('Ctrl Pts',(-47.8133751922042,-5.91674986753237,
130.805612638189));
#174796=CARTESIAN_POINT('',(-46.0633751922042,-5.91187214664006,130.80921511903));
#174797=CARTESIAN_POINT('Ctrl Pts',(-47.8133738942076,-5.92621134272425,
130.805587189359));
#174798=CARTESIAN_POINT('Ctrl Pts',(-47.7237369397262,-5.92074740615048,
128.909881288281));
#174799=CARTESIAN_POINT('Ctrl Pts',(-47.5412841106406,-3.90596225253313,
125.041284327674));
#174800=CARTESIAN_POINT('Ctrl Pts',(-47.2660154069507,2.68942047555363,
124.343356203699));
#174801=CARTESIAN_POINT('Ctrl Pts',(-46.9875677831378,6.88952345832453,
129.574715527493));
#174802=CARTESIAN_POINT('Ctrl Pts',(-46.7091201593249,4.75849095482671,
135.936058617563));
#174803=CARTESIAN_POINT('Ctrl Pts',(-46.4306725355122,-1.74536227095043,
137.58162194302));
#174804=CARTESIAN_POINT('Ctrl Pts',(-46.2154242131385,-5.53317027689218,
134.039283239287));
#174805=CARTESIAN_POINT('Ctrl Pts',(-46.0929917653692,-5.91671613064816,
131.43949600246));
#174806=CARTESIAN_POINT('Ctrl Pts',(-46.0633751922042,-5.91187214664006,
130.80921511903));
#174807=CARTESIAN_POINT('',(-44.3133751922042,-5.90864861670285,130.801162763788));
#174808=CARTESIAN_POINT('Ctrl Pts',(-46.0633751922042,-5.91187214664006,
130.80921511903));
#174809=CARTESIAN_POINT('Ctrl Pts',(-46.0001758907649,-5.90153548804726,
129.464248187122));
#174810=CARTESIAN_POINT('Ctrl Pts',(-45.8441607147213,-4.77861257565497,
126.128421018115));
#174811=CARTESIAN_POINT('Ctrl Pts',(-45.5953296640732,0.765979412781536,
123.848008407568));
#174812=CARTESIAN_POINT('Ctrl Pts',(-45.3168820402607,6.26660671109677,
127.688722503348));
#174813=CARTESIAN_POINT('Ctrl Pts',(-45.0384344164476,6.00852858267546,
134.39255581871));
#174814=CARTESIAN_POINT('Ctrl Pts',(-44.7599867926347,0.228906219712464,
137.799013037303));
#174815=CARTESIAN_POINT('Ctrl Pts',(-44.5183003845536,-4.97026108933638,
135.176602734102));
#174816=CARTESIAN_POINT('Ctrl Pts',(-44.3694298510767,-5.90281458641276,
131.995717272823));
#174817=CARTESIAN_POINT('Ctrl Pts',(-44.3133751922042,-5.90864861670285,
130.801162763788));
#174818=CARTESIAN_POINT('',(-42.5633751922041,-5.92360350378115,130.800661905678));
#174819=CARTESIAN_POINT('Ctrl Pts',(-44.3133751922042,-5.90864861670285,
130.801162763788));
#174820=CARTESIAN_POINT('Ctrl Pts',(-44.2766139764725,-5.9124746331374,
130.017761760318));
#174821=CARTESIAN_POINT('Ctrl Pts',(-44.1470368861364,-5.4024867072948,
127.261186095784));
#174822=CARTESIAN_POINT('Ctrl Pts',(-43.924643921196,-1.21915898426497,
123.912973826689));
#174823=CARTESIAN_POINT('Ctrl Pts',(-43.6461962973832,5.13893367076999,
126.053684743782));
#174824=CARTESIAN_POINT('Ctrl Pts',(-43.3677486735701,6.77459733323286,
132.560034705456));
#174825=CARTESIAN_POINT('Ctrl Pts',(-43.0893010497574,2.18473700393284,
137.453005949813));
#174826=CARTESIAN_POINT('Ctrl Pts',(-42.8211765559688,-4.16819407011025,
136.281308753027));
#174827=CARTESIAN_POINT('Ctrl Pts',(-42.6458679367842,-5.91084275337813,
132.547310458652));
#174828=CARTESIAN_POINT('Ctrl Pts',(-42.5633751922041,-5.92360350378115,
130.800661905678));
#174829=CARTESIAN_POINT('',(-40.8133751922042,-5.91898627828404,130.809343451928));
#174830=CARTESIAN_POINT('Ctrl Pts',(-42.5633751922041,-5.92360350378115,
130.800661905678));
#174831=CARTESIAN_POINT('Ctrl Pts',(-42.55305206218,-5.92520038222528,130.582086560529));
#174832=CARTESIAN_POINT('Ctrl Pts',(-42.4499130575518,-5.81485187816171,
128.399916294978));
#174833=CARTESIAN_POINT('Ctrl Pts',(-42.2539581783187,-3.10609779771171,
124.533019692256));
#174834=CARTESIAN_POINT('Ctrl Pts',(-41.9755105545057,3.59733500374434,
124.801299614947));
#174835=CARTESIAN_POINT('Ctrl Pts',(-41.697062930693,6.99499267634301,130.586099333203));
#174836=CARTESIAN_POINT('Ctrl Pts',(-41.4186153068799,3.96459380377209,
136.571470509137));
#174837=CARTESIAN_POINT('Ctrl Pts',(-41.1401676830672,-2.70907309328813,
137.257149433693));
#174838=CARTESIAN_POINT('Ctrl Pts',(-40.9384209781752,-5.74066911494575,
133.457570663198));
#174839=CARTESIAN_POINT('Ctrl Pts',(-40.8294901478875,-5.92335425468506,
131.151051523995));
#174840=CARTESIAN_POINT('Ctrl Pts',(-40.8133751922042,-5.92027830700173,
130.809344539608));
#174841=CARTESIAN_POINT('',(-39.0633752204132,-5.91150858312851,130.805710542273));
#174842=CARTESIAN_POINT('Ctrl Pts',(-40.8133751922042,-5.91674790342102,
130.809341567576));
#174843=CARTESIAN_POINT('Ctrl Pts',(-40.806073639501,-5.9168781620269,130.654610576157));
#174844=CARTESIAN_POINT('Ctrl Pts',(-40.7987720867977,-5.91093464250606,
130.499664442865));
#174845=CARTESIAN_POINT('Ctrl Pts',(-40.7914705340945,-5.89889343352436,
130.345027598479));
#174846=CARTESIAN_POINT('Ctrl Pts',(-40.7841754751059,-5.88686293352173,
130.190528282039));
#174847=CARTESIAN_POINT('Ctrl Pts',(-40.7768804161173,-5.8687455646891,
130.036338088981));
#174848=CARTESIAN_POINT('Ctrl Pts',(-40.7695853571287,-5.84456946063665,
129.882982094757));
#174849=CARTESIAN_POINT('Ctrl Pts',(-40.762295084242,-5.82040921790863,
129.729726713484));
#174850=CARTESIAN_POINT('Ctrl Pts',(-40.7550048113552,-5.79019821096416,
129.577304821114));
#174851=CARTESIAN_POINT('Ctrl Pts',(-40.7477145384685,-5.75401643453495,
129.426236735761));
#174852=CARTESIAN_POINT('Ctrl Pts',(-40.7404265740672,-5.71784611516684,
129.275216486541));
#174853=CARTESIAN_POINT('Ctrl Pts',(-40.7331386096659,-5.67570887379195,
129.125549566526));
#174854=CARTESIAN_POINT('Ctrl Pts',(-40.7258506452646,-5.62773585583999,
128.977746345369));
#174855=CARTESIAN_POINT('Ctrl Pts',(-40.7185636482984,-5.57976920602881,
128.829962744236));
#174856=CARTESIAN_POINT('Ctrl Pts',(-40.7112766513322,-5.5259684392141,
128.684042716502));
#174857=CARTESIAN_POINT('Ctrl Pts',(-40.703989654366,-5.46651454289294,
128.540481355141));
#174858=CARTESIAN_POINT('Ctrl Pts',(-40.6967020865158,-5.40705598878513,
128.396908746776));
#174859=CARTESIAN_POINT('Ctrl Pts',(-40.6894145186656,-5.3419435716094,
128.255695528562));
#174860=CARTESIAN_POINT('Ctrl Pts',(-40.6821269508155,-5.27140625812483,
128.117316400531));
#174861=CARTESIAN_POINT('Ctrl Pts',(-40.6748372734662,-5.20084852652484,
127.978897216523));
#174862=CARTESIAN_POINT('Ctrl Pts',(-40.6675475961168,-5.12486294960536,
127.843314097973));
#174863=CARTESIAN_POINT('Ctrl Pts',(-40.6602579187675,-5.04372407249495,
127.711016465514));
#174864=CARTESIAN_POINT('Ctrl Pts',(-40.6529606389673,-4.96250057513231,
127.578580859011));
#174865=CARTESIAN_POINT('Ctrl Pts',(-40.645663359167,-4.87611324910678,
127.449437908301));
#174866=CARTESIAN_POINT('Ctrl Pts',(-40.6383660793667,-4.78487983439095,
127.324007828991));
#174867=CARTESIAN_POINT('Ctrl Pts',(-40.6310645260418,-4.69359299041688,
127.198504293743));
#174868=CARTESIAN_POINT('Ctrl Pts',(-40.6237629727168,-4.59745464492467,
127.07671826108));
#174869=CARTESIAN_POINT('Ctrl Pts',(-40.6164614193919,-4.49682176573284,
126.959035589726));
#174870=CARTESIAN_POINT('Ctrl Pts',(-40.6091495810276,-4.39604713408348,
126.841187149411));
#174871=CARTESIAN_POINT('Ctrl Pts',(-40.6018377426631,-4.2907655900787,
126.727453891566));
#174872=CARTESIAN_POINT('Ctrl Pts',(-40.5945259042988,-4.18137019794758,
126.618184100717));
#174873=CARTESIAN_POINT('Ctrl Pts',(-40.590774748013,-4.12524762078129,
126.562125960156));
#174874=CARTESIAN_POINT('Ctrl Pts',(-40.5870235917272,-4.06804283219271,
126.507241923182));
#174875=CARTESIAN_POINT('Ctrl Pts',(-40.5832724354414,-4.00981203384433,
126.45357470974));
#174876=CARTESIAN_POINT('Ctrl Pts',(-40.575849169036,-3.89457750448703,
126.347371184142));
#174877=CARTESIAN_POINT('Ctrl Pts',(-40.5684259026306,-3.77494646716493,
126.24558836599));
#174878=CARTESIAN_POINT('Ctrl Pts',(-40.5610026362251,-3.6512924441916,
126.148612122481));
#174879=CARTESIAN_POINT('Ctrl Pts',(-40.5535881435041,-3.52778457000442,
126.051750496838));
#174880=CARTESIAN_POINT('Ctrl Pts',(-40.5461736507831,-3.40026346556194,
125.959684365949));
#174881=CARTESIAN_POINT('Ctrl Pts',(-40.5387591580621,-3.26913898429393,
125.872762411723));
#174882=CARTESIAN_POINT('Ctrl Pts',(-40.5313518117083,-3.13814088573771,
125.78592423615));
#174883=CARTESIAN_POINT('Ctrl Pts',(-40.5239444653546,-3.0035466336093,
125.704220571407));
#174884=CARTESIAN_POINT('Ctrl Pts',(-40.5165371190008,-2.86579851585264,
125.627959413154));
#174885=CARTESIAN_POINT('Ctrl Pts',(-40.5091352973254,-2.72815313583895,
125.55175513335));
#174886=CARTESIAN_POINT('Ctrl Pts',(-40.50173347565,-2.58735889907036,125.480985457599));
#174887=CARTESIAN_POINT('Ctrl Pts',(-40.4943316539745,-2.44388629219069,
125.415914612145));
#174888=CARTESIAN_POINT('Ctrl Pts',(-40.4869337396632,-2.30048942338301,
125.350878117083));
#174889=CARTESIAN_POINT('Ctrl Pts',(-40.4795358253518,-2.1544173394011,
125.291534614808));
#174890=CARTESIAN_POINT('Ctrl Pts',(-40.4721379110404,-2.00616419562074,
125.238101929479));
#174891=CARTESIAN_POINT('Ctrl Pts',(-40.4647412261282,-1.85793568882392,
125.184678123693));
#174892=CARTESIAN_POINT('Ctrl Pts',(-40.4573445412159,-1.70752719243071,
125.137163311785));
#174893=CARTESIAN_POINT('Ctrl Pts',(-40.4499478563037,-1.55545197716094,
125.095726830989));
#174894=CARTESIAN_POINT('Ctrl Pts',(-40.4425514993683,-1.40338350506558,
125.05429218753));
#174895=CARTESIAN_POINT('Ctrl Pts',(-40.4351551424328,-1.24964882120708,
125.018935437423));
#174896=CARTESIAN_POINT('Ctrl Pts',(-40.4277587854974,-1.09477520080447,
124.989775694959));
#174897=CARTESIAN_POINT('Ctrl Pts',(-40.4203612961608,-0.939877868855211,
124.960611488065));
#174898=CARTESIAN_POINT('Ctrl Pts',(-40.4129638068242,-0.783841620035531,
124.937646247032));
#174899=CARTESIAN_POINT('Ctrl Pts',(-40.4055663174876,-0.627202586010622,
124.920947706797));
#174900=CARTESIAN_POINT('Ctrl Pts',(-40.3981662349727,-0.470508642415827,
124.904243312915));
#174901=CARTESIAN_POINT('Ctrl Pts',(-40.3907661524578,-0.313211863871322,
124.893810033153));
#174902=CARTESIAN_POINT('Ctrl Pts',(-40.3833660699428,-0.155851998510028,
124.889663607823));
#174903=CARTESIAN_POINT('Ctrl Pts',(-40.3759578502763,0.0016809002008922,
124.885512623072));
#174904=CARTESIAN_POINT('Ctrl Pts',(-40.3685496306099,0.15927665086858,
124.887662308391));
#174905=CARTESIAN_POINT('Ctrl Pts',(-40.3611414109434,0.316396274386738,
124.8960762676));
#174906=CARTESIAN_POINT('Ctrl Pts',(-40.3537286316413,0.473612602411938,
124.90449540546));
#174907=CARTESIAN_POINT('Ctrl Pts',(-40.3463158523392,0.630351848544956,
124.919186465133));
#174908=CARTESIAN_POINT('Ctrl Pts',(-40.3389030730371,0.7860821676454,124.9400613936));
#174909=CARTESIAN_POINT('Ctrl Pts',(-40.3314797020083,0.94203500152858,
124.960966149143));
#174910=CARTESIAN_POINT('Ctrl Pts',(-40.3240563309797,1.09697566243705,
124.988072356398));
#174911=CARTESIAN_POINT('Ctrl Pts',(-40.316632959951,1.25038365594666,125.021241106831));
#174912=CARTESIAN_POINT('Ctrl Pts',(-40.3126969105101,1.33172425508061,
125.038827974184));
#174913=CARTESIAN_POINT('Ctrl Pts',(-40.3087608610692,1.41263422671327,
125.058118408508));
#174914=CARTESIAN_POINT('Ctrl Pts',(-40.3048248116284,1.49303805551621,
125.079086132681));
#174915=CARTESIAN_POINT('Ctrl Pts',(-40.2974015452229,1.64467716731935,
125.11863060609));
#174916=CARTESIAN_POINT('Ctrl Pts',(-40.2899782788175,1.79497343269383,
125.164263486521));
#174917=CARTESIAN_POINT('Ctrl Pts',(-40.282555012412,1.94340031270272,125.215879089719));
#174918=CARTESIAN_POINT('Ctrl Pts',(-40.275140519691,2.09165176446553,125.267433687561));
#174919=CARTESIAN_POINT('Ctrl Pts',(-40.26772602697,2.2380378796578,125.324956811728));
#174920=CARTESIAN_POINT('Ctrl Pts',(-40.260311534249,2.3820437665246,125.388292112011));
#174921=CARTESIAN_POINT('Ctrl Pts',(-40.2529041878953,2.52591085509611,
125.451566367348));
#174922=CARTESIAN_POINT('Ctrl Pts',(-40.2454968415414,2.66740194313536,
125.520641497054));
#174923=CARTESIAN_POINT('Ctrl Pts',(-40.2380894951876,2.80601883773402,
125.595311870935));
#174924=CARTESIAN_POINT('Ctrl Pts',(-40.2306876735123,2.94453234662277,
125.669926552833));
#174925=CARTESIAN_POINT('Ctrl Pts',(-40.2232858518369,3.08017560319755,
125.750127993337));
#174926=CARTESIAN_POINT('Ctrl Pts',(-40.2158840301616,3.21247199691197,
125.835663179448));
#174927=CARTESIAN_POINT('Ctrl Pts',(-40.2084861158502,3.34469855238976,
125.921153212201));
#174928=CARTESIAN_POINT('Ctrl Pts',(-40.2010882015388,3.47358145094979,
126.011971180905));
#174929=CARTESIAN_POINT('Ctrl Pts',(-40.1936902872275,3.59867032790635,
126.107819077928));
#174930=CARTESIAN_POINT('Ctrl Pts',(-40.1862936023153,3.7237384173609,126.203651046769));
#174931=CARTESIAN_POINT('Ctrl Pts',(-40.1788969174032,3.84501344054032,
126.304511058125));
#174932=CARTESIAN_POINT('Ctrl Pts',(-40.171500232491,3.96207549387292,126.410058813712));
#174933=CARTESIAN_POINT('Ctrl Pts',(-40.1641038755556,4.07913235655157,
126.515601889202));
#174934=CARTESIAN_POINT('Ctrl Pts',(-40.1567075186201,4.19197634357601,
126.625832045655));
#174935=CARTESIAN_POINT('Ctrl Pts',(-40.1493111616847,4.30022223558357,
126.740370055681));
#174936=CARTESIAN_POINT('Ctrl Pts',(-40.1419136723481,4.40848470031338,
126.854925601768));
#174937=CARTESIAN_POINT('Ctrl Pts',(-40.1345161830116,4.51214741188774,
126.973790043341));
#174938=CARTESIAN_POINT('Ctrl Pts',(-40.1271186936751,4.61086359072635,
127.096548930032));
#174939=CARTESIAN_POINT('Ctrl Pts',(-40.1197186111601,4.70961437436899,
127.219350849661));
#174940=CARTESIAN_POINT('Ctrl Pts',(-40.112318528645,4.8034149391095,127.34604964177));
#174941=CARTESIAN_POINT('Ctrl Pts',(-40.1049184461299,4.89196029512963,
127.47619970899));
#174942=CARTESIAN_POINT('Ctrl Pts',(-40.0975102264635,4.98060301587099,
127.606492889587));
#174943=CARTESIAN_POINT('Ctrl Pts',(-40.090102006797,5.06397877745584,127.740244615392));
#174944=CARTESIAN_POINT('Ctrl Pts',(-40.0826937871306,5.14182686964955,
127.876981754991));
#174945=CARTESIAN_POINT('Ctrl Pts',(-40.0752810078285,5.21972287604515,
128.013803054019));
#174946=CARTESIAN_POINT('Ctrl Pts',(-40.0678682285265,5.29208426257341,
128.153613097479));
#174947=CARTESIAN_POINT('Ctrl Pts',(-40.0604554492244,5.35869763544404,
128.295916834184));
#174948=CARTESIAN_POINT('Ctrl Pts',(-40.0530320781957,5.4254061886257,128.438423901142));
#174949=CARTESIAN_POINT('Ctrl Pts',(-40.0456087071669,5.48635018063139,
128.583431434439));
#174950=CARTESIAN_POINT('Ctrl Pts',(-40.0381853361381,5.54136513919476,
128.73042644392));
#174951=CARTESIAN_POINT('Ctrl Pts',(-40.0342492866973,5.57053539029118,
128.808366725044));
#174952=CARTESIAN_POINT('Ctrl Pts',(-40.0303132372565,5.5980396175646,128.886865526615));
#174953=CARTESIAN_POINT('Ctrl Pts',(-40.0263771878157,5.62385911082201,
128.965845112022));
#174954=CARTESIAN_POINT('Ctrl Pts',(-40.0189539214102,5.67255386930616,
129.11479814523));
#174955=CARTESIAN_POINT('Ctrl Pts',(-40.0115306550048,5.71540043723443,
129.265912336419));
#174956=CARTESIAN_POINT('Ctrl Pts',(-40.0041073885994,5.7522031226067,129.418687568548));
#174957=CARTESIAN_POINT('Ctrl Pts',(-39.9966928958784,5.78896231026119,
129.571282233041));
#174958=CARTESIAN_POINT('Ctrl Pts',(-39.9892784031574,5.81969174770084,
129.725533671315));
#174959=CARTESIAN_POINT('Ctrl Pts',(-39.9818639104363,5.84424466521449,
129.880924179249));
#174960=CARTESIAN_POINT('Ctrl Pts',(-39.9744565640826,5.86877391770181,
130.03616491596));
#174961=CARTESIAN_POINT('Ctrl Pts',(-39.9670492177287,5.88713844396749,
130.192542170424));
#174962=CARTESIAN_POINT('Ctrl Pts',(-39.9596418713749,5.89924196108349,
130.349525650691));
#174963=CARTESIAN_POINT('Ctrl Pts',(-39.9522400496995,5.91133645093981,
130.506392046757));
#174964=CARTESIAN_POINT('Ctrl Pts',(-39.9448382280241,5.91717920107018,
130.663863397752));
#174965=CARTESIAN_POINT('Ctrl Pts',(-39.9374364063487,5.9167254588341,130.821401958019));
#174966=CARTESIAN_POINT('Ctrl Pts',(-39.9300384920374,5.91627195612501,
130.978857354905));
#174967=CARTESIAN_POINT('Ctrl Pts',(-39.9226405777261,5.90952858176699,
131.136379518053));
#174968=CARTESIAN_POINT('Ctrl Pts',(-39.9152426634148,5.89650262490897,
131.293428462493));
#174969=CARTESIAN_POINT('Ctrl Pts',(-39.9078459785026,5.88347883272858,
131.450451308248));
#174970=CARTESIAN_POINT('Ctrl Pts',(-39.9004492935904,5.86417456100677,
131.607000719717));
#174971=CARTESIAN_POINT('Ctrl Pts',(-39.8930526086781,5.83864914418897,
131.762539480598));
#174972=CARTESIAN_POINT('Ctrl Pts',(-39.8856562517427,5.81312485919486,
131.918071344728));
#174973=CARTESIAN_POINT('Ctrl Pts',(-39.8782598948072,5.78138003804499,
132.072592279003));
#174974=CARTESIAN_POINT('Ctrl Pts',(-39.8708635378717,5.74352551500831,
132.225573205798));
#174975=CARTESIAN_POINT('Ctrl Pts',(-39.8634660485352,5.70566519634756,
132.378577554362));
#174976=CARTESIAN_POINT('Ctrl Pts',(-39.8560685591986,5.6616934029449,132.530041063586));
#174977=CARTESIAN_POINT('Ctrl Pts',(-39.8486710698621,5.61177138079809,
132.67944795744));
#174978=CARTESIAN_POINT('Ctrl Pts',(-39.841270987347,5.56183185856352,132.82890722565));
#174979=CARTESIAN_POINT('Ctrl Pts',(-39.833870904832,5.5059380729144,132.976308089261));
#174980=CARTESIAN_POINT('Ctrl Pts',(-39.8264708223169,5.44430006309049,
133.12115309544));
#174981=CARTESIAN_POINT('Ctrl Pts',(-39.8190626026505,5.3825942759386,133.266157373593));
#174982=CARTESIAN_POINT('Ctrl Pts',(-39.811654382984,5.31513179667647,133.408599838003));
#174983=CARTESIAN_POINT('Ctrl Pts',(-39.8042461633175,5.2421697639104,133.548005406682));
#174984=CARTESIAN_POINT('Ctrl Pts',(-39.7968333840154,5.16916282423029,
133.687496777163));
#174985=CARTESIAN_POINT('Ctrl Pts',(-39.7894206047134,5.09064977198451,
133.823947204571));
#174986=CARTESIAN_POINT('Ctrl Pts',(-39.7820078254113,5.00693176320131,
133.956909567407));
#174987=CARTESIAN_POINT('Ctrl Pts',(-39.7745844543825,4.9230941342013,134.090061913103));
#174988=CARTESIAN_POINT('Ctrl Pts',(-39.7671610833537,4.83403690593031,
134.219715933354));
#174989=CARTESIAN_POINT('Ctrl Pts',(-39.7597377123249,4.74010277025761,
134.345455969275));
#174990=CARTESIAN_POINT('Ctrl Pts',(-39.7558016628841,4.69029663760551,
134.412126353411));
#174991=CARTESIAN_POINT('Ctrl Pts',(-39.7518656134434,4.63912007931228,
134.477696958464));
#174992=CARTESIAN_POINT('Ctrl Pts',(-39.7479295640026,4.58662838407366,
134.542110024483));
#174993=CARTESIAN_POINT('Ctrl Pts',(-39.7405062975972,4.48763068506306,
134.663591056732));
#174994=CARTESIAN_POINT('Ctrl Pts',(-39.7330830311917,4.38365365279023,
134.781319999315));
#174995=CARTESIAN_POINT('Ctrl Pts',(-39.7256597647863,4.27501227357988,
134.894861885533));
#174996=CARTESIAN_POINT('Ctrl Pts',(-39.7182452720653,4.1664992994575,135.008269574671));
#174997=CARTESIAN_POINT('Ctrl Pts',(-39.7108307793442,4.05333320735376,
135.11749979088));
#174998=CARTESIAN_POINT('Ctrl Pts',(-39.7034162866232,3.93587022379573,
135.222149220922));
#174999=CARTESIAN_POINT('Ctrl Pts',(-39.6960089402695,3.81852045548382,
135.326697785902));
#175000=CARTESIAN_POINT('Ctrl Pts',(-39.6886015939158,3.69688231749495,
135.426674107724));
#175001=CARTESIAN_POINT('Ctrl Pts',(-39.681194247562,3.57134991618857,135.521710545082));
#175002=CARTESIAN_POINT('Ctrl Pts',(-39.6737924258866,3.4459111416828,135.616676100681));
#175003=CARTESIAN_POINT('Ctrl Pts',(-39.6663906042111,3.3165841834328,135.706708883505));
#175004=CARTESIAN_POINT('Ctrl Pts',(-39.6589887825357,3.18379727219426,
135.791480577229));
#175005=CARTESIAN_POINT('Ctrl Pts',(-39.6515908682243,3.05108045813274,
135.876207520635));
#175006=CARTESIAN_POINT('Ctrl Pts',(-39.644192953913,2.91490764245909,135.95567870568));
#175007=CARTESIAN_POINT('Ctrl Pts',(-39.6367950396016,2.77573706978512,
136.029608389865));
#175008=CARTESIAN_POINT('Ctrl Pts',(-39.6293983546894,2.63658962473572,
136.103525788278));
#175009=CARTESIAN_POINT('Ctrl Pts',(-39.6220016697772,2.4944457407587,136.171903338584));
#175010=CARTESIAN_POINT('Ctrl Pts',(-39.614604984865,2.34978946485991,136.234500581999));
#175011=CARTESIAN_POINT('Ctrl Pts',(-39.6072086279296,2.2051396031722,136.297095049787));
#175012=CARTESIAN_POINT('Ctrl Pts',(-39.5998122709942,2.05797791366424,
136.353909572053));
#175013=CARTESIAN_POINT('Ctrl Pts',(-39.5924159140587,1.90880943295803,
136.404751417425));
#175014=CARTESIAN_POINT('Ctrl Pts',(-39.5850184247221,1.75961811417598,
136.455601046815));
#175015=CARTESIAN_POINT('Ctrl Pts',(-39.5776209353856,1.60841974579123,
136.500476058116));
#175016=CARTESIAN_POINT('Ctrl Pts',(-39.5702234460491,1.45573542218498,
136.539233322613));
#175017=CARTESIAN_POINT('Ctrl Pts',(-39.562823363534,1.30299757532557,136.578004173409));
#175018=CARTESIAN_POINT('Ctrl Pts',(-39.555423281019,1.14877309773524,136.610652915796));
#175019=CARTESIAN_POINT('Ctrl Pts',(-39.548023198504,0.993594041911419,
136.637087376328));
#175020=CARTESIAN_POINT('Ctrl Pts',(-39.5406149788375,0.838244350763372,
136.663550904266));
#175021=CARTESIAN_POINT('Ctrl Pts',(-39.533206759171,0.681938353370654,
136.683786441191));
#175022=CARTESIAN_POINT('Ctrl Pts',(-39.5257985395045,0.525214739363178,
136.697753531674));
#175023=CARTESIAN_POINT('Ctrl Pts',(-39.5183857602024,0.36839466458613,
136.711729218668));
#175024=CARTESIAN_POINT('Ctrl Pts',(-39.5109729809004,0.211156833004429,
136.719428753209));
#175025=CARTESIAN_POINT('Ctrl Pts',(-39.5035602015983,0.0540402027871688,
136.720863826302));
#175026=CARTESIAN_POINT('Ctrl Pts',(-39.4961368305695,-0.103300923039385,
136.722300949894));
#175027=CARTESIAN_POINT('Ctrl Pts',(-39.4887134595408,-0.260520129493493,
136.717455746439));
#175028=CARTESIAN_POINT('Ctrl Pts',(-39.481290088512,-0.417082477656666,
136.706391858531));
#175029=CARTESIAN_POINT('Ctrl Pts',(-39.4773540390713,-0.500095591313523,
136.700525519688));
#175030=CARTESIAN_POINT('Ctrl Pts',(-39.4734179896306,-0.582924178214504,
136.692911745483));
#175031=CARTESIAN_POINT('Ctrl Pts',(-39.4694819401898,-0.665489758385496,
136.683565831197));
#175032=CARTESIAN_POINT('Ctrl Pts',(-39.4620586737844,-0.821205865806332,
136.665939728528));
#175033=CARTESIAN_POINT('Ctrl Pts',(-39.454635407379,-0.976456685181706,
136.64209627565));
#175034=CARTESIAN_POINT('Ctrl Pts',(-39.4472121409736,-1.13070600890658,
136.612065369352));
#175035=CARTESIAN_POINT('Ctrl Pts',(-39.4397976482526,-1.28477302274064,
136.582069957092));
#175036=CARTESIAN_POINT('Ctrl Pts',(-39.4323831555316,-1.43784053421516,
136.545901718732));
#175037=CARTESIAN_POINT('Ctrl Pts',(-39.4249686628106,-1.58937667534061,
136.503642357082));
#175038=CARTESIAN_POINT('Ctrl Pts',(-39.4175613164568,-1.74076676022715,
136.461423726596));
#175039=CARTESIAN_POINT('Ctrl Pts',(-39.410153970103,-1.89062805601135,
136.413125760138));
#175040=CARTESIAN_POINT('Ctrl Pts',(-39.4027466237493,-2.03843823153748,
136.358881311443));
#175041=CARTESIAN_POINT('Ctrl Pts',(-39.395344802074,-2.18613816465772,
136.304677320305));
#175042=CARTESIAN_POINT('Ctrl Pts',(-39.3879429803987,-2.33178967462792,
136.24453580589));
#175043=CARTESIAN_POINT('Ctrl Pts',(-39.3805411587234,-2.47488507044041,
136.178639587866));
#175044=CARTESIAN_POINT('Ctrl Pts',(-39.373143244412,-2.61790492730954,
136.112778155942));
#175045=CARTESIAN_POINT('Ctrl Pts',(-39.3657453301005,-2.7583710191074,
136.04116822621));
#175046=CARTESIAN_POINT('Ctrl Pts',(-39.3583474157891,-2.89579525017106,
135.964040882038));
#175047=CARTESIAN_POINT('Ctrl Pts',(-39.3509507308769,-3.03319664381967,
135.886926355033));
#175048=CARTESIAN_POINT('Ctrl Pts',(-39.3435540459648,-3.16755685479181,
135.804296415874));
#175049=CARTESIAN_POINT('Ctrl Pts',(-39.3361573610526,-3.29841193907253,
135.71642833317));
#175050=CARTESIAN_POINT('Ctrl Pts',(-39.3287610041172,-3.4292612211017,
135.62856414663));
#175051=CARTESIAN_POINT('Ctrl Pts',(-39.3213646471817,-3.5566053755584,
135.535462486468));
#175052=CARTESIAN_POINT('Ctrl Pts',(-39.3139682902462,-3.68000926745085,
135.437444078284));
#175053=CARTESIAN_POINT('Ctrl Pts',(-39.3065708009097,-3.80343205279366,
135.339410663231));
#175054=CARTESIAN_POINT('Ctrl Pts',(-39.2991733115732,-3.92291308206493,
135.236459233492));
#175055=CARTESIAN_POINT('Ctrl Pts',(-39.2917758222367,-4.03805027277946,
135.128950835957));
#175056=CARTESIAN_POINT('Ctrl Pts',(-39.2843757397216,-4.15322782465886,
135.02140475152));
#175057=CARTESIAN_POINT('Ctrl Pts',(-39.2769756572065,-4.2640582335698,
134.909298773409));
#175058=CARTESIAN_POINT('Ctrl Pts',(-39.2695755746915,-4.37017636401009,
134.79303071046));
#175059=CARTESIAN_POINT('Ctrl Pts',(-39.262167355025,-4.47641118224341,
134.676634798824));
#175060=CARTESIAN_POINT('Ctrl Pts',(-39.2547591353586,-4.57792312213516,
134.55606793839));
#175061=CARTESIAN_POINT('Ctrl Pts',(-39.2473509156921,-4.67438697248521,
134.431761476854));
#175062=CARTESIAN_POINT('Ctrl Pts',(-39.23993813639,-4.77091019472571,134.307378506764));
#175063=CARTESIAN_POINT('Ctrl Pts',(-39.232525357088,-4.86237891991497,
134.179251652339));
#175064=CARTESIAN_POINT('Ctrl Pts',(-39.225112577786,-4.94851166397086,
134.047840673624));
#175065=CARTESIAN_POINT('Ctrl Pts',(-39.2176892067572,-5.03476747853081,
133.916241928739));
#175066=CARTESIAN_POINT('Ctrl Pts',(-39.2102658357284,-5.11567189302207,
133.781350006852));
#175067=CARTESIAN_POINT('Ctrl Pts',(-39.2028424646996,-5.19098930420983,
133.643649367602));
#175068=CARTESIAN_POINT('Ctrl Pts',(-39.1989064152588,-5.23092440283896,
133.570637184588));
#175069=CARTESIAN_POINT('Ctrl Pts',(-39.1949703658178,-5.26928959338914,
133.496835717663));
#175070=CARTESIAN_POINT('Ctrl Pts',(-39.1910343163769,-5.30605532387013,
133.422319261726));
#175071=CARTESIAN_POINT('Ctrl Pts',(-39.1830667672712,-5.38047836337056,
133.271479306388));
#175072=CARTESIAN_POINT('Ctrl Pts',(-39.1750992181656,-5.44854441786373,
133.117303859407));
#175073=CARTESIAN_POINT('Ctrl Pts',(-39.1671316690599,-5.50996474576556,
132.960333498407));
#175074=CARTESIAN_POINT('Ctrl Pts',(-39.1591797189277,-5.57126482413259,
132.803670456067));
#175075=CARTESIAN_POINT('Ctrl Pts',(-39.1512277687956,-5.62594501497068,
132.644223678088));
#175076=CARTESIAN_POINT('Ctrl Pts',(-39.1432758186635,-5.67376320284541,
132.482556577678));
#175077=CARTESIAN_POINT('Ctrl Pts',(-39.1353462269315,-5.72144694091106,
132.321344034661));
#175078=CARTESIAN_POINT('Ctrl Pts',(-39.1274166351995,-5.76230707955355,
132.157923897655));
#175079=CARTESIAN_POINT('Ctrl Pts',(-39.1194870434675,-5.79615040522259,
131.992876937411));
#175080=CARTESIAN_POINT('Ctrl Pts',(-39.1115712989339,-5.8299346313491,
131.828118193519));
#175081=CARTESIAN_POINT('Ctrl Pts',(-39.1036555544003,-5.85672641306675,
131.661738570411));
#175082=CARTESIAN_POINT('Ctrl Pts',(-39.0957398098666,-5.87638217084346,
131.494333910305));
#175083=CARTESIAN_POINT('Ctrl Pts',(-39.0878434404491,-5.8959898178472,
131.327339001259));
#175084=CARTESIAN_POINT('Ctrl Pts',(-39.0799470710314,-5.9084962433274,
131.159324344707));
#175085=CARTESIAN_POINT('Ctrl Pts',(-39.0720507016138,-5.91380886971371,
130.990895373029));
#175086=CARTESIAN_POINT('Ctrl Pts',(-39.0691588860228,-5.91575446458157,
130.929213161808));
#175087=CARTESIAN_POINT('Ctrl Pts',(-39.0662670704316,-5.91673573397632,
130.867475498038));
#175088=CARTESIAN_POINT('Ctrl Pts',(-39.0633752548405,-5.91674984556424,
130.805712473904));
#175089=CARTESIAN_POINT('',(-37.3133751886983,-5.91555801160614,130.798912666527));
#175090=CARTESIAN_POINT('Ctrl Pts',(-39.0633751922042,-5.90721400833861,
130.805708959537));
#175091=CARTESIAN_POINT('Ctrl Pts',(-39.0131123589908,-5.90503878728851,
129.733931433989));
#175092=CARTESIAN_POINT('Ctrl Pts',(-38.870033651173,-5.11274322411047,
126.68000182472));
#175093=CARTESIAN_POINT('Ctrl Pts',(-38.6341390687512,-0.207615843526837,
123.809043884792));
#175094=CARTESIAN_POINT('Ctrl Pts',(-38.3556914449382,5.77313665022518,
126.848547964243));
#175095=CARTESIAN_POINT('Ctrl Pts',(-38.0772438211253,6.44865859582369,
133.523250619913));
#175096=CARTESIAN_POINT('Ctrl Pts',(-37.7987961973124,1.19817832634459,
137.699426188581));
#175097=CARTESIAN_POINT('Ctrl Pts',(-37.5441733210053,-4.60991333961225,
135.724193425928));
#175098=CARTESIAN_POINT('Ctrl Pts',(-37.3823663193026,-5.90208600168968,
132.264974056485));
#175099=CARTESIAN_POINT('Ctrl Pts',(-37.3133751922042,-5.91531521970268,
130.798912964642));
#175100=CARTESIAN_POINT('',(-35.5633751921759,-5.91674990983146,130.805393579034));
#175101=CARTESIAN_POINT('Ctrl Pts',(-37.3133751715223,-5.91674749050639,
130.798911206011));
#175102=CARTESIAN_POINT('Ctrl Pts',(-37.3039607718894,-5.91656319311221,
130.598808656684));
#175103=CARTESIAN_POINT('Ctrl Pts',(-37.2945463722564,-5.90622431910606,
130.399160275082));
#175104=CARTESIAN_POINT('Ctrl Pts',(-37.2851319726236,-5.88588985533355,
130.20084493974));
#175105=CARTESIAN_POINT('Ctrl Pts',(-37.2755249102599,-5.86513925314817,
129.998471143363));
#175106=CARTESIAN_POINT('Ctrl Pts',(-37.2659178478962,-5.83397976607423,
129.797485305177));
#175107=CARTESIAN_POINT('Ctrl Pts',(-37.2563107855325,-5.7926285272159,
129.598796306472));
#175108=CARTESIAN_POINT('Ctrl Pts',(-37.2515075069172,-5.77195399489752,
129.499457030589));
#175109=CARTESIAN_POINT('Ctrl Pts',(-37.2467042283019,-5.74873253607829,
129.400691536482));
#175110=CARTESIAN_POINT('Ctrl Pts',(-37.2419009496867,-5.72299570535111,
129.302611397812));
#175111=CARTESIAN_POINT('Ctrl Pts',(-37.2344776832812,-5.68322050881899,
129.15103264156));
#175112=CARTESIAN_POINT('Ctrl Pts',(-37.2270544168757,-5.63735895589863,
129.0008059957));
#175113=CARTESIAN_POINT('Ctrl Pts',(-37.2196311504702,-5.5855175320251,
128.852457837728));
#175114=CARTESIAN_POINT('Ctrl Pts',(-37.2122166577491,-5.53373738040943,
128.704285014958));
#175115=CARTESIAN_POINT('Ctrl Pts',(-37.2048021650281,-5.4759915481044,
128.55798660968));
#175116=CARTESIAN_POINT('Ctrl Pts',(-37.197387672307,-5.41243716871604,
128.414077275114));
#175117=CARTESIAN_POINT('Ctrl Pts',(-37.1899803259532,-5.34894404543122,
128.270306645783));
#175118=CARTESIAN_POINT('Ctrl Pts',(-37.1825729795993,-5.27965367036182,
128.128920842176));
#175119=CARTESIAN_POINT('Ctrl Pts',(-37.1751656332455,-5.20477243163089,
127.99041774369));
#175120=CARTESIAN_POINT('Ctrl Pts',(-37.1677638115701,-5.12994704215301,
127.852017946041));
#175121=CARTESIAN_POINT('Ctrl Pts',(-37.1603619898947,-5.04953926857393,
127.716496899478));
#175122=CARTESIAN_POINT('Ctrl Pts',(-37.1529601682192,-4.96380284891965,
127.584330828953));
#175123=CARTESIAN_POINT('Ctrl Pts',(-37.1455622539078,-4.87811168885406,
127.452234527867));
#175124=CARTESIAN_POINT('Ctrl Pts',(-37.1381643395965,-4.7870976874825,
127.323489988039));
#175125=CARTESIAN_POINT('Ctrl Pts',(-37.1307664252851,-4.69105953747209,
127.198547120116));
#175126=CARTESIAN_POINT('Ctrl Pts',(-37.1233697403728,-4.59503734725976,
127.073625015431));
#175127=CARTESIAN_POINT('Ctrl Pts',(-37.1159730554605,-4.49399289275658,
126.952503624453));
#175128=CARTESIAN_POINT('Ctrl Pts',(-37.1085763705483,-4.38826711087254,
126.835602332392));
#175129=CARTESIAN_POINT('Ctrl Pts',(-37.1011800136128,-4.28254601698046,
126.718706223858));
#175130=CARTESIAN_POINT('Ctrl Pts',(-37.0937836566772,-4.1721442588322,
126.606030119038));
#175131=CARTESIAN_POINT('Ctrl Pts',(-37.0863872997417,-4.05744164961755,
126.497958659731));
#175132=CARTESIAN_POINT('Ctrl Pts',(-37.0789898104051,-3.94272147914044,
126.389870654407));
#175133=CARTESIAN_POINT('Ctrl Pts',(-37.0715923210685,-3.82369941820876,
126.286388954317));
#175134=CARTESIAN_POINT('Ctrl Pts',(-37.0641948317318,-3.70079044444893,
126.187859707919));
#175135=CARTESIAN_POINT('Ctrl Pts',(-37.0567947492168,-3.57783838513889,
126.089295922245));
#175136=CARTESIAN_POINT('Ctrl Pts',(-37.0493946667017,-3.4509969912524,
125.995688280118));
#175137=CARTESIAN_POINT('Ctrl Pts',(-37.0419945841867,-3.32071232378487,
125.907341092879));
#175138=CARTESIAN_POINT('Ctrl Pts',(-37.0345863645201,-3.19028439493188,
125.818896758826));
#175139=CARTESIAN_POINT('Ctrl Pts',(-37.0271781448536,-3.05640594029233,
125.735724641147));
#175140=CARTESIAN_POINT('Ctrl Pts',(-37.0197699251871,-2.91955048748648,
125.65808472975));
#175141=CARTESIAN_POINT('Ctrl Pts',(-37.012357145885,-2.78261080243258,
125.580397032283));
#175142=CARTESIAN_POINT('Ctrl Pts',(-37.0049443665829,-2.64269079915634,
125.508248496634));
#175143=CARTESIAN_POINT('Ctrl Pts',(-36.9975315872807,-2.50028585302065,
125.441851762964));
#175144=CARTESIAN_POINT('Ctrl Pts',(-36.9901082162519,-2.35767743202019,
125.375360158527));
#175145=CARTESIAN_POINT('Ctrl Pts',(-36.982684845223,-2.21257732025677,
125.314636913875));
#175146=CARTESIAN_POINT('Ctrl Pts',(-36.9752614741942,-2.06549875759093,
125.2598457204));
#175147=CARTESIAN_POINT('Ctrl Pts',(-36.9713254247541,-1.98751417457693,
125.230794114928));
#175148=CARTESIAN_POINT('Ctrl Pts',(-36.967389375314,-1.90897360716784,
125.203409381323));
#175149=CARTESIAN_POINT('Ctrl Pts',(-36.9634533258738,-1.82995482035788,
125.177710111452));
#175150=CARTESIAN_POINT('Ctrl Pts',(-36.9560300594683,-1.6809278545018,
125.129242090516));
#175151=CARTESIAN_POINT('Ctrl Pts',(-36.9486067930629,-1.52974863311755,
125.086625542278));
#175152=CARTESIAN_POINT('Ctrl Pts',(-36.9411835266575,-1.37691757047712,
125.050055397419));
#175153=CARTESIAN_POINT('Ctrl Pts',(-36.9337690339364,-1.22426714146091,
125.013528475434));
#175154=CARTESIAN_POINT('Ctrl Pts',(-36.9263545412154,-1.0699691168342,
124.983033818009));
#175155=CARTESIAN_POINT('Ctrl Pts',(-36.9189400484944,-0.914541423479221,
124.958717406829));
#175156=CARTESIAN_POINT('Ctrl Pts',(-36.9115327021406,-0.759263537186846,
124.93442443272));
#175157=CARTESIAN_POINT('Ctrl Pts',(-36.9041253557868,-0.60285851612274,
124.916297907282));
#175158=CARTESIAN_POINT('Ctrl Pts',(-36.896718009433,-0.445856798146332,
124.904433306315));
#175159=CARTESIAN_POINT('Ctrl Pts',(-36.8893161877575,-0.288972177974303,
124.892577554415));
#175160=CARTESIAN_POINT('Ctrl Pts',(-36.8819143660822,-0.131492117657274,
124.886974455641));
#175161=CARTESIAN_POINT('Ctrl Pts',(-36.8745125444067,0.0260455696644963,
124.887667944222));
#175162=CARTESIAN_POINT('Ctrl Pts',(-36.8671146300954,0.183500094066952,
124.888361066717));
#175163=CARTESIAN_POINT('Ctrl Pts',(-36.859716715784,0.341011812540219,
124.895344155183));
#175164=CARTESIAN_POINT('Ctrl Pts',(-36.8523188014726,0.498040751832022,
124.908609098717));
#175165=CARTESIAN_POINT('Ctrl Pts',(-36.8449221165604,0.655043595763134,
124.921871837857));
#175166=CARTESIAN_POINT('Ctrl Pts',(-36.8375254316482,0.811563448135018,
124.94141432878));
#175167=CARTESIAN_POINT('Ctrl Pts',(-36.830128746736,0.967063183565719,
124.967176419557));
#175168=CARTESIAN_POINT('Ctrl Pts',(-36.8227323898005,1.1225560239752,124.992937368015));
#175169=CARTESIAN_POINT('Ctrl Pts',(-36.8153360328651,1.27702846910446,
125.024917306963));
#175170=CARTESIAN_POINT('Ctrl Pts',(-36.8079396759296,1.42995161060948,
125.063004597094));
#175171=CARTESIAN_POINT('Ctrl Pts',(-36.8005421865931,1.58289816503785,
125.101097718485));
#175172=CARTESIAN_POINT('Ctrl Pts',(-36.7931446972564,1.73429458128532,
125.145299962647));
#175173=CARTESIAN_POINT('Ctrl Pts',(-36.7857472079199,1.88362532930908,
125.195449298844));
#175174=CARTESIAN_POINT('Ctrl Pts',(-36.7783471254048,2.03300842499507,
125.245616214813));
#175175=CARTESIAN_POINT('Ctrl Pts',(-36.7709470428898,2.18032405709106,
125.301734254761));
#175176=CARTESIAN_POINT('Ctrl Pts',(-36.7635469603748,2.32507509298301,
125.363592622651));
#175177=CARTESIAN_POINT('Ctrl Pts',(-36.7561387407084,2.46998529751969,
125.425519010176));
#175178=CARTESIAN_POINT('Ctrl Pts',(-36.7487305210419,2.61232493057494,
125.493198184501));
#175179=CARTESIAN_POINT('Ctrl Pts',(-36.7413223013754,2.7516193020312,125.566372284323));
#175180=CARTESIAN_POINT('Ctrl Pts',(-36.7339095220733,2.89099940684923,
125.639591421583));
#175181=CARTESIAN_POINT('Ctrl Pts',(-36.7264967427712,3.02733019274953,
125.718312037234));
#175182=CARTESIAN_POINT('Ctrl Pts',(-36.7190839634691,3.16016499705973,
125.802232295156));
#175183=CARTESIAN_POINT('Ctrl Pts',(-36.7116605924404,3.29318960196728,
125.886272462277));
#175184=CARTESIAN_POINT('Ctrl Pts',(-36.7042372214116,3.42270794213975,
125.975526898769));
#175185=CARTESIAN_POINT('Ctrl Pts',(-36.6968138503828,3.54830488069168,
126.069652280597));
#175186=CARTESIAN_POINT('Ctrl Pts',(-36.6928778009421,3.61489939116719,
126.119559816549));
#175187=CARTESIAN_POINT('Ctrl Pts',(-36.6889417515014,3.68039203827932,
126.170836102878));
#175188=CARTESIAN_POINT('Ctrl Pts',(-36.6850057020607,3.7447251462828,126.223425763052));
#175189=CARTESIAN_POINT('Ctrl Pts',(-36.6775824356553,3.86605538021307,
126.322608220877));
#175190=CARTESIAN_POINT('Ctrl Pts',(-36.6701591692499,3.98362595112466,
126.426764296155));
#175191=CARTESIAN_POINT('Ctrl Pts',(-36.6627359028445,4.09700237217803,
126.535578340983));
#175192=CARTESIAN_POINT('Ctrl Pts',(-36.6553214101235,4.21024479171705,
126.644263776647));
#175193=CARTESIAN_POINT('Ctrl Pts',(-36.6479069174025,4.31930266191125,
126.7575959675));
#175194=CARTESIAN_POINT('Ctrl Pts',(-36.6404924246815,4.42377321210486,
126.875218073656));
#175195=CARTESIAN_POINT('Ctrl Pts',(-36.6330850783277,4.52814306964896,
126.992726811197));
#175196=CARTESIAN_POINT('Ctrl Pts',(-36.6256777319739,4.62793416316039,
127.114516955274));
#175197=CARTESIAN_POINT('Ctrl Pts',(-36.6182703856201,4.72277945152285,
127.240193840495));
#175198=CARTESIAN_POINT('Ctrl Pts',(-36.6108685639448,4.81755400069094,
127.365776991154));
#175199=CARTESIAN_POINT('Ctrl Pts',(-36.6034667422694,4.9073898656435,127.495240814215));
#175200=CARTESIAN_POINT('Ctrl Pts',(-36.596064920594,4.99195938212829,127.628156579775));
#175201=CARTESIAN_POINT('Ctrl Pts',(-36.5886670062826,5.07648425502363,
127.761002180137));
#175202=CARTESIAN_POINT('Ctrl Pts',(-36.5812690919713,5.15574811619767,
127.89729577974));
#175203=CARTESIAN_POINT('Ctrl Pts',(-36.5738711776599,5.22946592085267,
128.03657869965));
#175204=CARTESIAN_POINT('Ctrl Pts',(-36.5664744927477,5.30317147494592,
128.175838473267));
#175205=CARTESIAN_POINT('Ctrl Pts',(-36.5590778078356,5.37133262727738,
128.318086251635));
#175206=CARTESIAN_POINT('Ctrl Pts',(-36.5516811229234,5.43370965597914,
128.462837622373));
#175207=CARTESIAN_POINT('Ctrl Pts',(-36.5442847659879,5.49608391881808,
128.607582574683));
#175208=CARTESIAN_POINT('Ctrl Pts',(-36.5368884090525,5.55267442025389,
128.754830555812));
#175209=CARTESIAN_POINT('Ctrl Pts',(-36.529492052117,5.60328919771785,128.904076236417));
#175210=CARTESIAN_POINT('Ctrl Pts',(-36.5220945627804,5.65391172443346,
129.053344766917));
#175211=CARTESIAN_POINT('Ctrl Pts',(-36.5146970734439,5.69855658559252,
129.204611252345));
#175212=CARTESIAN_POINT('Ctrl Pts',(-36.5072995841073,5.73708144566016,
129.357354381103));
#175213=CARTESIAN_POINT('Ctrl Pts',(-36.4998995015923,5.77561981055778,
129.510151053729));
#175214=CARTESIAN_POINT('Ctrl Pts',(-36.4924994190774,5.80803381173699,
129.664425038557));
#175215=CARTESIAN_POINT('Ctrl Pts',(-36.4850993365624,5.83423208555115,
129.819644143435));
#175216=CARTESIAN_POINT('Ctrl Pts',(-36.4776911168959,5.86045916706061,
129.975033927675));
#175217=CARTESIAN_POINT('Ctrl Pts',(-36.4702828972295,5.88045680943273,
130.13137053911));
#175218=CARTESIAN_POINT('Ctrl Pts',(-36.462874677563,5.89418537708077,130.288115227168));
#175219=CARTESIAN_POINT('Ctrl Pts',(-36.4554618982609,5.90792239443314,
130.444956388966));
#175220=CARTESIAN_POINT('Ctrl Pts',(-36.4480491189589,5.91538263084562,
130.60220575585));
#175221=CARTESIAN_POINT('Ctrl Pts',(-36.4406363396568,5.9165785975116,130.759324388065));
#175222=CARTESIAN_POINT('Ctrl Pts',(-36.4332129686281,5.91777627303084,
130.91666751875));
#175223=CARTESIAN_POINT('Ctrl Pts',(-36.4257895975994,5.91269181431795,
131.073879169572));
#175224=CARTESIAN_POINT('Ctrl Pts',(-36.4183662265706,5.90138967797973,
131.230424499084));
#175225=CARTESIAN_POINT('Ctrl Pts',(-36.4144301771298,5.89539701410207,
131.313428589046));
#175226=CARTESIAN_POINT('Ctrl Pts',(-36.4104941276889,5.88765719770414,
131.396245493168));
#175227=CARTESIAN_POINT('Ctrl Pts',(-36.406558078248,5.878185643482,131.478796754841));
#175228=CARTESIAN_POINT('Ctrl Pts',(-36.3991348118426,5.86032258781643,
131.634485858017));
#175229=CARTESIAN_POINT('Ctrl Pts',(-36.3917115454372,5.83624289722977,
131.789700211938));
#175230=CARTESIAN_POINT('Ctrl Pts',(-36.3842882790318,5.80597728449461,
131.943903655118));
#175231=CARTESIAN_POINT('Ctrl Pts',(-36.3768737863108,5.77574744320025,
132.097924842633));
#175232=CARTESIAN_POINT('Ctrl Pts',(-36.3694592935897,5.73934630402704,
132.250937134956));
#175233=CARTESIAN_POINT('Ctrl Pts',(-36.3620448008687,5.69685637910187,
132.402408789051));
#175234=CARTESIAN_POINT('Ctrl Pts',(-36.354637454515,5.65440740756607,132.553734449062));
#175235=CARTESIAN_POINT('Ctrl Pts',(-36.3472301081612,5.60588143365416,
132.703522070027));
#175236=CARTESIAN_POINT('Ctrl Pts',(-36.3398227618075,5.55141210584787,
132.851249523576));
#175237=CARTESIAN_POINT('Ctrl Pts',(-36.3324209401321,5.49698340332128,
132.998866796416));
#175238=CARTESIAN_POINT('Ctrl Pts',(-36.3250191184567,5.43662030174455,
133.144426612578));
#175239=CARTESIAN_POINT('Ctrl Pts',(-36.3176172967813,5.37050639319398,
133.287421559863));
#175240=CARTESIAN_POINT('Ctrl Pts',(-36.3102193824699,5.30442738566111,
133.430341021229));
#175241=CARTESIAN_POINT('Ctrl Pts',(-36.3028214681585,5.23260377337199,
133.570697972246));
#175242=CARTESIAN_POINT('Ctrl Pts',(-36.2954235538471,5.15526738222731,
133.708004669485));
#175243=CARTESIAN_POINT('Ctrl Pts',(-36.2880268689349,5.07794384298792,
133.845288548842));
#175244=CARTESIAN_POINT('Ctrl Pts',(-36.2806301840228,4.99510952614419,
133.979522855525));
#175245=CARTESIAN_POINT('Ctrl Pts',(-36.2732334991106,4.90704240602778,
134.110244068014));
#175246=CARTESIAN_POINT('Ctrl Pts',(-36.2658371421751,4.81897919089976,
134.240959484187));
#175247=CARTESIAN_POINT('Ctrl Pts',(-36.2584407852398,4.72568384242273,
134.368161806303));
#175248=CARTESIAN_POINT('Ctrl Pts',(-36.2510444283043,4.62747774802602,
134.491416387964));
#175249=CARTESIAN_POINT('Ctrl Pts',(-36.2436469389678,4.52925661802541,
134.614689840216));
#175250=CARTESIAN_POINT('Ctrl Pts',(-36.2362494496312,4.42612347771388,
134.73401405658));
#175251=CARTESIAN_POINT('Ctrl Pts',(-36.2288519602946,4.31843998546752,
134.848987504488));
#175252=CARTESIAN_POINT('Ctrl Pts',(-36.2214518777796,4.21071874494005,
134.96400125616));
#175253=CARTESIAN_POINT('Ctrl Pts',(-36.2140517952646,4.09844423163117,
135.074660930516));
#175254=CARTESIAN_POINT('Ctrl Pts',(-36.2066517127496,3.98201480958954,
135.180601997873));
#175255=CARTESIAN_POINT('Ctrl Pts',(-36.1992434930831,3.86545736142897,
135.286659558325));
#175256=CARTESIAN_POINT('Ctrl Pts',(-36.1918352734167,3.74473615671733,
135.38798789843));
#175257=CARTESIAN_POINT('Ctrl Pts',(-36.1844270537503,3.62028303756659,
135.484262463802));
#175258=CARTESIAN_POINT('Ctrl Pts',(-36.1770142744482,3.49575331959763,
135.580596284564));
#175259=CARTESIAN_POINT('Ctrl Pts',(-36.1696014951461,3.36748741371257,
135.671869916572));
#175260=CARTESIAN_POINT('Ctrl Pts',(-36.162188715844,3.23594550779504,135.757802575748));
#175261=CARTESIAN_POINT('Ctrl Pts',(-36.1547653448153,3.10421564863363,
135.843858019538));
#175262=CARTESIAN_POINT('Ctrl Pts',(-36.1473419737866,2.96920076020303,
135.9245570578));
#175263=CARTESIAN_POINT('Ctrl Pts',(-36.1399186027578,2.83138566012953,
135.999664824839));
#175264=CARTESIAN_POINT('Ctrl Pts',(-36.1359825533169,2.75831278724038,
136.039488765111));
#175265=CARTESIAN_POINT('Ctrl Pts',(-36.132046503876,2.68445302048714,136.077741597966));
#175266=CARTESIAN_POINT('Ctrl Pts',(-36.1281104544351,2.60988069965456,
136.114393884512));
#175267=CARTESIAN_POINT('Ctrl Pts',(-36.1206871880297,2.4692396298907,136.183518953057));
#175268=CARTESIAN_POINT('Ctrl Pts',(-36.1132639216242,2.3256377370963,136.24715717701));
#175269=CARTESIAN_POINT('Ctrl Pts',(-36.1058406552187,2.17954271011847,
136.305044587516));
#175270=CARTESIAN_POINT('Ctrl Pts',(-36.0984261624977,2.0336203553301,136.362863579911));
#175271=CARTESIAN_POINT('Ctrl Pts',(-36.0910116697768,1.88521107539483,
136.414945152124));
#175272=CARTESIAN_POINT('Ctrl Pts',(-36.0835971770557,1.73480684060859,
136.461071303846));
#175273=CARTESIAN_POINT('Ctrl Pts',(-36.0761898307019,1.58454757108623,
136.507152997447));
#175274=CARTESIAN_POINT('Ctrl Pts',(-36.0687824843481,1.4322975291499,136.547290589165));
#175275=CARTESIAN_POINT('Ctrl Pts',(-36.0613751379943,1.27856823645375,
136.581314298117));
#175276=CARTESIAN_POINT('Ctrl Pts',(-36.0539733163189,1.12495360086441,
136.615312630903));
#175277=CARTESIAN_POINT('Ctrl Pts',(-36.0465714946436,0.969862274205898,
136.643206080106));
#175278=CARTESIAN_POINT('Ctrl Pts',(-36.0391696729682,0.813820392733913,
136.664874838253));
#175279=CARTESIAN_POINT('Ctrl Pts',(-36.0317717586568,0.657860884556308,
136.68653215763));
#175280=CARTESIAN_POINT('Ctrl Pts',(-36.0243738443455,0.50095218971895,
136.701971278895));
#175281=CARTESIAN_POINT('Ctrl Pts',(-36.0169759300341,0.343629968143567,
136.711123606505));
#175282=CARTESIAN_POINT('Ctrl Pts',(-36.0095792451219,0.186333890667293,
136.720274413164));
#175283=CARTESIAN_POINT('Ctrl Pts',(-36.0021825602096,0.0286247951460516,
136.723140478031));
#175284=CARTESIAN_POINT('Ctrl Pts',(-35.9947858752974,-0.128957092719909,
136.719705124079));
#175285=CARTESIAN_POINT('Ctrl Pts',(-35.9873895183619,-0.286531993239603,
136.716269922455));
#175286=CARTESIAN_POINT('Ctrl Pts',(-35.9799931614266,-0.443979324110384,
136.706533865713));
#175287=CARTESIAN_POINT('Ctrl Pts',(-35.9725968044911,-0.600759687251767,
136.690532409204));
#175288=CARTESIAN_POINT('Ctrl Pts',(-35.9651993151545,-0.757564053867211,
136.674528502831));
#175289=CARTESIAN_POINT('Ctrl Pts',(-35.957801825818,-0.913700878037255,
136.652257324605));
#175290=CARTESIAN_POINT('Ctrl Pts',(-35.9504043364814,-1.06863685385445,
136.6238061098));
#175291=CARTESIAN_POINT('Ctrl Pts',(-35.9430042539664,-1.22362714223779,
136.595344921466));
#175292=CARTESIAN_POINT('Ctrl Pts',(-35.9356041714513,-1.37741537721916,
136.560699450641));
#175293=CARTESIAN_POINT('Ctrl Pts',(-35.9282040889363,-1.52947954415417,
136.520007815086));
#175294=CARTESIAN_POINT('Ctrl Pts',(-35.9207958692699,-1.68171092127329,
136.479271434894));
#175295=CARTESIAN_POINT('Ctrl Pts',(-35.9133876496034,-1.83221408349758,
136.432475709276));
#175296=CARTESIAN_POINT('Ctrl Pts',(-35.905979429937,-1.98048255282059,
136.37980852966));
#175297=CARTESIAN_POINT('Ctrl Pts',(-35.8985666506349,-2.12884227891269,
136.327108934273));
#175298=CARTESIAN_POINT('Ctrl Pts',(-35.8911538713328,-2.27496422572512,
136.268530822556));
#175299=CARTESIAN_POINT('Ctrl Pts',(-35.8837410920307,-2.41836341886766,
136.204309592953));
#175300=CARTESIAN_POINT('Ctrl Pts',(-35.8763177210019,-2.56196750750212,
136.139996601046));
#175301=CARTESIAN_POINT('Ctrl Pts',(-35.8688943499732,-2.70284073902702,
136.070024552953));
#175302=CARTESIAN_POINT('Ctrl Pts',(-35.8614709789445,-2.84052345851048,
135.994674388828));
#175303=CARTESIAN_POINT('Ctrl Pts',(-35.8575349295037,-2.91352614003103,
135.954721923807));
#175304=CARTESIAN_POINT('Ctrl Pts',(-35.8535988800629,-2.98563233974033,
135.913258200757));
#175305=CARTESIAN_POINT('Ctrl Pts',(-35.8496628306222,-3.05677710739541,
135.870329851405));
#175306=CARTESIAN_POINT('Ctrl Pts',(-35.8422395642167,-3.19095391884254,
135.789368324273));
#175307=CARTESIAN_POINT('Ctrl Pts',(-35.8348162978114,-3.3221148897088,
135.702949999345));
#175308=CARTESIAN_POINT('Ctrl Pts',(-35.827393031406,-3.4497851382752,135.61132567488));
#175309=CARTESIAN_POINT('Ctrl Pts',(-35.819978538685,-3.57730449121032,
135.519809642757));
#175310=CARTESIAN_POINT('Ctrl Pts',(-35.8125640459639,-3.70134103384341,
135.423100074323));
#175311=CARTESIAN_POINT('Ctrl Pts',(-35.8051495532429,-3.82144543437741,
135.321493043627));
#175312=CARTESIAN_POINT('Ctrl Pts',(-35.7977422068891,-3.94143407376832,
135.219983945614));
#175313=CARTESIAN_POINT('Ctrl Pts',(-35.7903348605353,-4.05749783301726,
135.113587022127));
#175314=CARTESIAN_POINT('Ctrl Pts',(-35.7829275141815,-4.16921738070859,
135.002640860105));
#175315=CARTESIAN_POINT('Ctrl Pts',(-35.7755256925061,-4.28085360374616,
134.891777445918));
#175316=CARTESIAN_POINT('Ctrl Pts',(-35.7681238708307,-4.38815180291972,
134.776371811015));
#175317=CARTESIAN_POINT('Ctrl Pts',(-35.7607220491553,-4.49072679131001,
134.656801849864));
#175318=CARTESIAN_POINT('Ctrl Pts',(-35.7533241348439,-4.59324763116238,
134.537295008765));
#175319=CARTESIAN_POINT('Ctrl Pts',(-35.7459262205326,-4.69104998340803,
134.413628502078));
#175320=CARTESIAN_POINT('Ctrl Pts',(-35.7385283062212,-4.78378659940384,
134.286215918101));
#175321=CARTESIAN_POINT('Ctrl Pts',(-35.731131621309,-4.87650780425661,
134.158824507784));
#175322=CARTESIAN_POINT('Ctrl Pts',(-35.7237349363968,-4.96416472418869,
134.027688557237));
#175323=CARTESIAN_POINT('Ctrl Pts',(-35.7163382514846,-5.04645132315826,
133.8932535593));
#175324=CARTESIAN_POINT('Ctrl Pts',(-35.7089418945492,-5.1287342734538,
133.758824522352));
#175325=CARTESIAN_POINT('Ctrl Pts',(-35.7015455376137,-5.20564718137771,
133.621097047265));
#175326=CARTESIAN_POINT('Ctrl Pts',(-35.6941491806782,-5.27692831868325,
133.480544109403));
#175327=CARTESIAN_POINT('Ctrl Pts',(-35.6867516913416,-5.34822036931299,
133.339969652527));
#175328=CARTESIAN_POINT('Ctrl Pts',(-35.6793542020051,-5.41387876363703,
133.196569204493));
#175329=CARTESIAN_POINT('Ctrl Pts',(-35.6719567126685,-5.4736886302921,
133.050838603461));
#175330=CARTESIAN_POINT('Ctrl Pts',(-35.6645566301535,-5.53351946320322,
132.905056916793));
#175331=CARTESIAN_POINT('Ctrl Pts',(-35.6571565476384,-5.58749754488179,
132.75694379595));
#175332=CARTESIAN_POINT('Ctrl Pts',(-35.6497564651234,-5.63545691604405,
132.607013082661));
#175333=CARTESIAN_POINT('Ctrl Pts',(-35.6423482454569,-5.68346902346516,
132.456917505138));
#175334=CARTESIAN_POINT('Ctrl Pts',(-35.6349400257905,-5.72544908960591,
132.305000699543));
#175335=CARTESIAN_POINT('Ctrl Pts',(-35.627531806124,-5.76128142911044,
132.15179034007));
#175336=CARTESIAN_POINT('Ctrl Pts',(-35.6201190268219,-5.79713582282209,
131.998485682177));
#175337=CARTESIAN_POINT('Ctrl Pts',(-35.6127062475199,-5.82683487989473,
131.843886249702));
#175338=CARTESIAN_POINT('Ctrl Pts',(-35.6052934682178,-5.85031450720381,
131.688527303944));
#175339=CARTESIAN_POINT('Ctrl Pts',(-35.597870097189,-5.87382768330547,
131.532946374039));
#175340=CARTESIAN_POINT('Ctrl Pts',(-35.5904467261602,-5.89110364019271,
131.376604133463));
#175341=CARTESIAN_POINT('Ctrl Pts',(-35.5830233551314,-5.90213028605508,
131.220039157945));
#175342=CARTESIAN_POINT('Ctrl Pts',(-35.5790873056907,-5.90797687827193,
131.137024651201));
#175343=CARTESIAN_POINT('Ctrl Pts',(-35.57515125625,-5.91206743599125,131.053947508116));
#175344=CARTESIAN_POINT('Ctrl Pts',(-35.5712152068093,-5.91440608461213,
130.970887578756));
#175345=CARTESIAN_POINT('Ctrl Pts',(-35.5686018686076,-5.91595882927992,
130.915739977158));
#175346=CARTESIAN_POINT('Ctrl Pts',(-35.5659885304059,-5.91674027688676,
130.86057055656));
#175347=CARTESIAN_POINT('Ctrl Pts',(-35.5633751922042,-5.91674990983136,
130.805393579632));
#175348=CARTESIAN_POINT('',(-33.8133752151521,-5.91399190468965,130.809307765289));
#175349=CARTESIAN_POINT('Ctrl Pts',(-35.5633751921759,-5.91674990983146,
130.805393579034));
#175350=CARTESIAN_POINT('Ctrl Pts',(-35.5559869379694,-5.91677714342954,
130.649400936515));
#175351=CARTESIAN_POINT('Ctrl Pts',(-35.5485986837629,-5.9106310999208,
130.493162228736));
#175352=CARTESIAN_POINT('Ctrl Pts',(-35.5412104295564,-5.89827942929397,
130.337209318234));
#175353=CARTESIAN_POINT('Ctrl Pts',(-35.5338308523911,-5.88594226492956,
130.181439564643));
#175354=CARTESIAN_POINT('Ctrl Pts',(-35.5264512752258,-5.8674140075802,
130.025955312578));
#175355=CARTESIAN_POINT('Ctrl Pts',(-35.5190716980605,-5.84271427044327,
129.871290139811));
#175356=CARTESIAN_POINT('Ctrl Pts',(-35.5116991387766,-5.81803802243363,
129.716772051602));
#175357=CARTESIAN_POINT('Ctrl Pts',(-35.5043265794927,-5.78720203589756,
129.563071862187));
#175358=CARTESIAN_POINT('Ctrl Pts',(-35.4969540202089,-5.75027783723711,
129.410719574442));
#175359=CARTESIAN_POINT('Ctrl Pts',(-35.489586825525,-5.71338050625557,
129.258478144955));
#175360=CARTESIAN_POINT('Ctrl Pts',(-35.4822196308411,-5.67040387116845,
129.107583029565));
#175361=CARTESIAN_POINT('Ctrl Pts',(-35.4748524361572,-5.6214707734391,
128.958555398733));
#175362=CARTESIAN_POINT('Ctrl Pts',(-35.4672655672755,-5.57107859400335,
128.805084078457));
#175363=CARTESIAN_POINT('Ctrl Pts',(-35.4596786983938,-5.51436926674348,
128.653593749841));
#175364=CARTESIAN_POINT('Ctrl Pts',(-35.4520918295121,-5.45153285809808,
128.504638882317));
#175365=CARTESIAN_POINT('Ctrl Pts',(-35.4447293484672,-5.39055488750217,
128.360089476522));
#175366=CARTESIAN_POINT('Ctrl Pts',(-35.4373668674222,-5.32380729160206,
128.217928046068));
#175367=CARTESIAN_POINT('Ctrl Pts',(-35.4300043863773,-5.25151313802298,
128.078642304227));
#175368=CARTESIAN_POINT('Ctrl Pts',(-35.4226419565869,-5.1792194877258,
127.939357532036));
#175369=CARTESIAN_POINT('Ctrl Pts',(-35.4152795267965,-5.10137952996784,
127.802948743642));
#175370=CARTESIAN_POINT('Ctrl Pts',(-35.4079170970061,-5.01826264884636,
127.669879711627));
#175371=CARTESIAN_POINT('Ctrl Pts',(-35.4005532295195,-4.93512953710119,
127.536784694598));
#175372=CARTESIAN_POINT('Ctrl Pts',(-35.3931893620328,-4.84671765065185,
127.407031052028));
#175373=CARTESIAN_POINT('Ctrl Pts',(-35.3858254945462,-4.75333999936162,
127.281054015385));
#175374=CARTESIAN_POINT('Ctrl Pts',(-35.3784586997688,-4.65992522850938,
127.155026900246));
#175375=CARTESIAN_POINT('Ctrl Pts',(-35.3710919049914,-4.5615409878702,
127.032779682138));
#175376=CARTESIAN_POINT('Ctrl Pts',(-35.363725110214,-4.45854075467284,
126.914714759468));
#175377=CARTESIAN_POINT('Ctrl Pts',(-35.356350135751,-4.35542615565569,
126.796518743971));
#175378=CARTESIAN_POINT('Ctrl Pts',(-35.348975161288,-4.24768557986087,
126.682514578862));
#175379=CARTESIAN_POINT('Ctrl Pts',(-35.341600186825,-4.13570998790208,
126.573068443954));
#175380=CARTESIAN_POINT('Ctrl Pts',(-35.3342202982419,-4.02365978395514,
126.463549382496));
#175381=CARTESIAN_POINT('Ctrl Pts',(-35.3268404096588,-3.90736922166183,
126.358594652872));
#175382=CARTESIAN_POINT('Ctrl Pts',(-35.3194605210757,-3.78726204666404,
126.258529917639));
#175383=CARTESIAN_POINT('Ctrl Pts',(-35.3120707249736,-3.66699362748174,
126.158330845248));
#175384=CARTESIAN_POINT('Ctrl Pts',(-35.3046809288715,-3.54289866613725,
126.063035098984));
#175385=CARTESIAN_POINT('Ctrl Pts',(-35.2972911327694,-3.41542997607893,
125.972925153752));
#175386=CARTESIAN_POINT('Ctrl Pts',(-35.2957832828451,-3.38942064483255,
125.95453868243));
#175387=CARTESIAN_POINT('Ctrl Pts',(-35.2942754329207,-3.36327093207583,
125.936367965198));
#175388=CARTESIAN_POINT('Ctrl Pts',(-35.2927675829964,-3.33698480487009,
125.918415164067));
#175389=CARTESIAN_POINT('Ctrl Pts',(-35.2853443165909,-3.20757608728912,
125.830032080732));
#175390=CARTESIAN_POINT('Ctrl Pts',(-35.2779210501855,-3.07445790372475,
125.746660164798));
#175391=CARTESIAN_POINT('Ctrl Pts',(-35.27049778378,-2.9380557519732,125.668627080787));
#175392=CARTESIAN_POINT('Ctrl Pts',(-35.263083291059,-2.80181481623773,
125.590686225401));
#175393=CARTESIAN_POINT('Ctrl Pts',(-35.2556687983381,-2.66229795907687,
125.518071825293));
#175394=CARTESIAN_POINT('Ctrl Pts',(-35.2482543056171,-2.51996123713822,
125.451069487259));
#175395=CARTESIAN_POINT('Ctrl Pts',(-35.2408469592633,-2.37776170469086,
125.384131728601));
#175396=CARTESIAN_POINT('Ctrl Pts',(-35.2334396129094,-2.23274805373423,
125.322795421452));
#175397=CARTESIAN_POINT('Ctrl Pts',(-35.2260322665556,-2.08540253695233,
125.267301215557));
#175398=CARTESIAN_POINT('Ctrl Pts',(-35.2186304448803,-1.93816691601608,
125.211848399335));
#175399=CARTESIAN_POINT('Ctrl Pts',(-35.2112286232049,-1.78860324006258,
125.162229139482));
#175400=CARTESIAN_POINT('Ctrl Pts',(-35.2038268015295,-1.63721531991091,
125.118636691912));
#175401=CARTESIAN_POINT('Ctrl Pts',(-35.1964288872181,-1.48590731626454,
125.075067256457));
#175402=CARTESIAN_POINT('Ctrl Pts',(-35.1890309729068,-1.33277734410326,
125.037518400195));
#175403=CARTESIAN_POINT('Ctrl Pts',(-35.1816330585955,-1.1783459087153,
125.006134036799));
#175404=CARTESIAN_POINT('Ctrl Pts',(-35.1742363736833,-1.02394013702934,
124.974754888914));
#175405=CARTESIAN_POINT('Ctrl Pts',(-35.1668396887712,-0.86823369682951,
124.949538274981));
#175406=CARTESIAN_POINT('Ctrl Pts',(-35.1594430038589,-0.711758980423895,
124.930577363454));
#175407=CARTESIAN_POINT('Ctrl Pts',(-35.1520466469235,-0.555291202270955,
124.911617292674));
#175408=CARTESIAN_POINT('Ctrl Pts',(-35.144650289988,-0.398055586234015,
124.898912417671));
#175409=CARTESIAN_POINT('Ctrl Pts',(-35.1372539330525,-0.24059110316989,
124.892504184636));
#175410=CARTESIAN_POINT('Ctrl Pts',(-35.129856443716,-0.0831025118918699,
124.886094970484));
#175411=CARTESIAN_POINT('Ctrl Pts',(-35.1224589543793,0.0746146431697645,
124.885984332997));
#175412=CARTESIAN_POINT('Ctrl Pts',(-35.1150614650428,0.232020073902628,
124.892161597928));
#175413=CARTESIAN_POINT('Ctrl Pts',(-35.1076613825278,0.389480682865451,
124.89834102829));
#175414=CARTESIAN_POINT('Ctrl Pts',(-35.1002613000128,0.546628977156729,
124.910812735017));
#175415=CARTESIAN_POINT('Ctrl Pts',(-35.0928612174978,0.70292862523581,
124.929514074011));
#175416=CARTESIAN_POINT('Ctrl Pts',(-35.0854529978313,0.859400140845949,
124.948235977049));
#175417=CARTESIAN_POINT('Ctrl Pts',(-35.0780447781649,1.01502077575306,
124.973201148121));
#175418=CARTESIAN_POINT('Ctrl Pts',(-35.0706365584984,1.16926251474753,
125.00429546844));
#175419=CARTESIAN_POINT('Ctrl Pts',(-35.0632237791963,1.32359918695913,
125.035408926794));
#175420=CARTESIAN_POINT('Ctrl Pts',(-35.0558109998942,1.47655491028574,
125.072658963228));
#175421=CARTESIAN_POINT('Ctrl Pts',(-35.0483982205921,1.62761621409,125.115881381238));
#175422=CARTESIAN_POINT('Ctrl Pts',(-35.0409748495634,1.778893361369,125.159165557466));
#175423=CARTESIAN_POINT('Ctrl Pts',(-35.0335514785346,1.9282703293981,125.208439042192));
#175424=CARTESIAN_POINT('Ctrl Pts',(-35.0261281075058,2.07525224822536,
125.263488965133));
#175425=CARTESIAN_POINT('Ctrl Pts',(-35.022192058065,2.15318558836977,125.292677755181));
#175426=CARTESIAN_POINT('Ctrl Pts',(-35.0182560086243,2.23044597228738,
125.323489724327));
#175427=CARTESIAN_POINT('Ctrl Pts',(-35.0143199591835,2.30696248977542,
125.355887929439));
#175428=CARTESIAN_POINT('Ctrl Pts',(-35.0068966927781,2.4512702537599,125.416989933166));
#175429=CARTESIAN_POINT('Ctrl Pts',(-34.9994734263727,2.59336703765948,
125.483921474066));
#175430=CARTESIAN_POINT('Ctrl Pts',(-34.9920501599673,2.73274717607931,
125.556501679472));
#175431=CARTESIAN_POINT('Ctrl Pts',(-34.9846356672463,2.87196257875034,
125.628996101103));
#175432=CARTESIAN_POINT('Ctrl Pts',(-34.9772211745252,3.00846739929175,
125.707125727391));
#175433=CARTESIAN_POINT('Ctrl Pts',(-34.9698066818042,3.14177483886011,
125.790661242413));
#175434=CARTESIAN_POINT('Ctrl Pts',(-34.9623993354504,3.27495379169927,
125.874116242761));
#175435=CARTESIAN_POINT('Ctrl Pts',(-34.9549919890966,3.40494118453581,
125.962966562074));
#175436=CARTESIAN_POINT('Ctrl Pts',(-34.9475846427429,3.53127388256734,
126.056936544577));
#175437=CARTESIAN_POINT('Ctrl Pts',(-34.9401828210675,3.65751235690642,
126.150836440721));
#175438=CARTESIAN_POINT('Ctrl Pts',(-34.9327809993921,3.78010126566057,
126.249848175196));
#175439=CARTESIAN_POINT('Ctrl Pts',(-34.9253791777167,3.89860569510034,
126.353652337232));
#175440=CARTESIAN_POINT('Ctrl Pts',(-34.9179812634053,4.01704756697493,
126.45740170186));
#175441=CARTESIAN_POINT('Ctrl Pts',(-34.9105833490939,4.13140897354866,
126.565938210315));
#175442=CARTESIAN_POINT('Ctrl Pts',(-34.9031854347825,4.24128749035135,
126.678901735612));
#175443=CARTESIAN_POINT('Ctrl Pts',(-34.8957887498703,4.35114774733716,
126.79184648842));
#175444=CARTESIAN_POINT('Ctrl Pts',(-34.8883920649582,4.45652633307937,
126.909216530615));
#175445=CARTESIAN_POINT('Ctrl Pts',(-34.880995380046,4.55705709127248,127.030614305294));
#175446=CARTESIAN_POINT('Ctrl Pts',(-34.8735990231105,4.65758339182656,
127.15200669707));
#175447=CARTESIAN_POINT('Ctrl Pts',(-34.8662026661751,4.75326205414824,
127.277426178712));
#175448=CARTESIAN_POINT('Ctrl Pts',(-34.8588063092396,4.84376688147076,
127.406441701455));
#175449=CARTESIAN_POINT('Ctrl Pts',(-34.851408819903,4.93428556531351,127.535476976803));
#175450=CARTESIAN_POINT('Ctrl Pts',(-34.8440113305665,5.01962862253187,
127.668109083874));
#175451=CARTESIAN_POINT('Ctrl Pts',(-34.8366138412299,5.09951299474849,
127.803877693287));
#175452=CARTESIAN_POINT('Ctrl Pts',(-34.8292137587149,5.17942537030761,
127.939693896174));
#175453=CARTESIAN_POINT('Ctrl Pts',(-34.8218136761999,5.25387506184623,
128.078648468956));
#175454=CARTESIAN_POINT('Ctrl Pts',(-34.8144135936849,5.32262487331873,
128.220256320052));
#175455=CARTESIAN_POINT('Ctrl Pts',(-34.8070053740185,5.3914502822767,128.362019883539));
#175456=CARTESIAN_POINT('Ctrl Pts',(-34.799597154352,5.45456313121603,128.506442215864));
#175457=CARTESIAN_POINT('Ctrl Pts',(-34.7921889346856,5.51177402638542,
128.653017398885));
#175458=CARTESIAN_POINT('Ctrl Pts',(-34.7847761553835,5.56902013390633,
128.799682796487));
#175459=CARTESIAN_POINT('Ctrl Pts',(-34.7773633760815,5.62035692788746,
128.948503333028));
#175460=CARTESIAN_POINT('Ctrl Pts',(-34.7699505967795,5.66564500807687,
129.098958258897));
#175461=CARTESIAN_POINT('Ctrl Pts',(-34.7625272257507,5.71099779799906,
129.24962816182));
#175462=CARTESIAN_POINT('Ctrl Pts',(-34.7551038547219,5.75028451975687,
129.401936757664));
#175463=CARTESIAN_POINT('Ctrl Pts',(-34.7476804836931,5.78341677785059,
129.555352636736));
#175464=CARTESIAN_POINT('Ctrl Pts',(-34.7437444342523,5.80098429608973,
129.636697416985));
#175465=CARTESIAN_POINT('Ctrl Pts',(-34.7398083848115,5.81682243850423,
129.718353388052));
#175466=CARTESIAN_POINT('Ctrl Pts',(-34.7358723353706,5.83092395770166,
129.800240922509));
#175467=CARTESIAN_POINT('Ctrl Pts',(-34.7284490689652,5.85751898281439,
129.954678256872));
#175468=CARTESIAN_POINT('Ctrl Pts',(-34.7210258025597,5.87801436445953,
130.110406438308));
#175469=CARTESIAN_POINT('Ctrl Pts',(-34.7136025361543,5.89228895143836,
130.266902270103));
#175470=CARTESIAN_POINT('Ctrl Pts',(-34.7061880434332,5.90654666704081,
130.423213136822));
#175471=CARTESIAN_POINT('Ctrl Pts',(-34.6987735507123,5.91459818951644,
130.580289479792));
#175472=CARTESIAN_POINT('Ctrl Pts',(-34.6913590579912,5.91637332218163,
130.737597790502));
#175473=CARTESIAN_POINT('Ctrl Pts',(-34.6839517116374,5.91814674390712,
130.89475448154));
#175474=CARTESIAN_POINT('Ctrl Pts',(-34.6765443652836,5.91365581484407,
131.052142324447));
#175475=CARTESIAN_POINT('Ctrl Pts',(-34.6691370189298,5.9028821163297,131.209222672117));
#175476=CARTESIAN_POINT('Ctrl Pts',(-34.6617351972544,5.8921164532462,131.366185863336));
#175477=CARTESIAN_POINT('Ctrl Pts',(-34.654333375579,5.87507737645693,131.522841645149));
#175478=CARTESIAN_POINT('Ctrl Pts',(-34.6469315539036,5.85179853379275,
131.678651462995));
#175479=CARTESIAN_POINT('Ctrl Pts',(-34.6395336395921,5.82853197984821,
131.834379030052));
#175480=CARTESIAN_POINT('Ctrl Pts',(-34.6321357252807,5.79903227505665,
131.989261154258));
#175481=CARTESIAN_POINT('Ctrl Pts',(-34.6247378109693,5.76338488419449,
132.142764607077));
#175482=CARTESIAN_POINT('Ctrl Pts',(-34.6173411260571,5.72774341728218,
132.296242550405));
#175483=CARTESIAN_POINT('Ctrl Pts',(-34.6099444411449,5.68595637629979,
132.448341913797));
#175484=CARTESIAN_POINT('Ctrl Pts',(-34.6025477562326,5.63816032070145,
132.598539750364));
#175485=CARTESIAN_POINT('Ctrl Pts',(-34.5951513992972,5.59036638443037,
132.748730927002));
#175486=CARTESIAN_POINT('Ctrl Pts',(-34.5877550423618,5.53656407652576,
132.897020388743));
#175487=CARTESIAN_POINT('Ctrl Pts',(-34.5803586854263,5.47693973320394,
133.042900704621));
#175488=CARTESIAN_POINT('Ctrl Pts',(-34.5729611960897,5.41730626124269,
133.188803355149));
#175489=CARTESIAN_POINT('Ctrl Pts',(-34.5655637067531,5.35184912027339,
133.332295779819));
#175490=CARTESIAN_POINT('Ctrl Pts',(-34.5581662174165,5.28080259847433,
133.472891014329));
#175491=CARTESIAN_POINT('Ctrl Pts',(-34.5507661349015,5.2097311714274,133.61353553428));
#175492=CARTESIAN_POINT('Ctrl Pts',(-34.5433660523864,5.13306663075884,
133.751280509039));
#175493=CARTESIAN_POINT('Ctrl Pts',(-34.5359659698714,5.0510888874963,133.885664175009));
#175494=CARTESIAN_POINT('Ctrl Pts',(-34.5285577502049,4.96902100127764,
134.020195609635));
#175495=CARTESIAN_POINT('Ctrl Pts',(-34.5211495305385,4.88162843930775,
134.151358035229));
#175496=CARTESIAN_POINT('Ctrl Pts',(-34.513741310872,4.78923447289869,134.278718648354));
#175497=CARTESIAN_POINT('Ctrl Pts',(-34.5063285315699,4.69678363954498,
134.40615764981));
#175498=CARTESIAN_POINT('Ctrl Pts',(-34.4989157522677,4.59932549845371,
134.529789883664));
#175499=CARTESIAN_POINT('Ctrl Pts',(-34.4915029729657,4.49722282177984,
134.64921659065));
#175500=CARTESIAN_POINT('Ctrl Pts',(-34.4840796019369,4.39497425601324,
134.768813940116));
#175501=CARTESIAN_POINT('Ctrl Pts',(-34.4766562309081,4.28806815346692,
134.884193488187));
#175502=CARTESIAN_POINT('Ctrl Pts',(-34.4692328598794,4.17690382423927,
134.994993625305));
#175503=CARTESIAN_POINT('Ctrl Pts',(-34.4652968104388,4.11796182953463,
135.053742516615));
#175504=CARTESIAN_POINT('Ctrl Pts',(-34.4613607609982,4.05782325130584,
135.111204641304));
#175505=CARTESIAN_POINT('Ctrl Pts',(-34.4574247115576,3.99655116497038,
135.167330861365));
#175506=CARTESIAN_POINT('Ctrl Pts',(-34.4500014451522,3.88099392237199,
135.273183160767));
#175507=CARTESIAN_POINT('Ctrl Pts',(-34.4425781787468,3.76105364728595,
135.374601391742));
#175508=CARTESIAN_POINT('Ctrl Pts',(-34.4351549123414,3.6371050347427,135.471200825753));
#175509=CARTESIAN_POINT('Ctrl Pts',(-34.4277404196204,3.513302919166,135.567686087255));
#175510=CARTESIAN_POINT('Ctrl Pts',(-34.4203259268994,3.38550218775947,
135.659363661323));
#175511=CARTESIAN_POINT('Ctrl Pts',(-34.4129114341784,3.25411375332225,
135.745886115116));
#175512=CARTESIAN_POINT('Ctrl Pts',(-34.4055040878246,3.12285195600464,
135.832325175311));
#175513=CARTESIAN_POINT('Ctrl Pts',(-34.3980967414708,2.98800964945674,
135.913618803003));
#175514=CARTESIAN_POINT('Ctrl Pts',(-34.3906893951171,2.8500300570067,135.989460350132));
#175515=CARTESIAN_POINT('Ctrl Pts',(-34.3832875734416,2.71215337494198,
136.065245331774));
#175516=CARTESIAN_POINT('Ctrl Pts',(-34.3758857517661,2.57114439177295,
136.1355861505));
#175517=CARTESIAN_POINT('Ctrl Pts',(-34.3684839300907,2.42747439617799,
136.200220013288));
#175518=CARTESIAN_POINT('Ctrl Pts',(-34.3610860157793,2.28388024285558,
136.264819756363));
#175519=CARTESIAN_POINT('Ctrl Pts',(-34.353688101468,2.13762821426212,136.323718390586));
#175520=CARTESIAN_POINT('Ctrl Pts',(-34.3462901871567,1.98921312646629,
136.376699596845));
#175521=CARTESIAN_POINT('Ctrl Pts',(-34.3388935022444,1.84082270256573,
136.429671998589));
#175522=CARTESIAN_POINT('Ctrl Pts',(-34.3314968173322,1.69027028411111,
136.476728798687));
#175523=CARTESIAN_POINT('Ctrl Pts',(-34.32410013242,1.5380696548491,136.517702222908));
#175524=CARTESIAN_POINT('Ctrl Pts',(-34.3167037754845,1.38587577432272,
136.558673830325));
#175525=CARTESIAN_POINT('Ctrl Pts',(-34.3093074185491,1.23203418876763,
136.593562501167));
#175526=CARTESIAN_POINT('Ctrl Pts',(-34.3019110616137,1.07707253350351,
136.622250726538));
#175527=CARTESIAN_POINT('Ctrl Pts',(-34.2945135722771,0.922087153214153,
136.65094334415));
#175528=CARTESIAN_POINT('Ctrl Pts',(-34.2871160829405,0.765981728849491,
136.673433558141));
#175529=CARTESIAN_POINT('Ctrl Pts',(-34.2797185936039,0.609292595753247,
136.689655265692));
#175530=CARTESIAN_POINT('Ctrl Pts',(-34.272318511089,0.452548535524518,
136.705882659737));
#175531=CARTESIAN_POINT('Ctrl Pts',(-34.264918428574,0.295220730252588,
136.715837133886));
#175532=CARTESIAN_POINT('Ctrl Pts',(-34.257518346059,0.137848973478393,
136.719504590709));
#175533=CARTESIAN_POINT('Ctrl Pts',(-34.2501101263925,-0.0196958297208099,
136.723176080278));
#175534=CARTESIAN_POINT('Ctrl Pts',(-34.242701906726,-0.177284307513279,
136.720546737662));
#175535=CARTESIAN_POINT('Ctrl Pts',(-34.2352936870595,-0.334377594066704,
136.711654599339));
#175536=CARTESIAN_POINT('Ctrl Pts',(-34.2278809077575,-0.491567568916312,
136.702756988053));
#175537=CARTESIAN_POINT('Ctrl Pts',(-34.2204681284555,-0.648261374510992,
136.687588936078));
#175538=CARTESIAN_POINT('Ctrl Pts',(-34.2130553491534,-0.803927436176936,
136.66624011478));
#175539=CARTESIAN_POINT('Ctrl Pts',(-34.2056319781247,-0.959815920812247,
136.644860789286));
#175540=CARTESIAN_POINT('Ctrl Pts',(-34.1982086070959,-1.11467336207536,
136.61728312151));
#175541=CARTESIAN_POINT('Ctrl Pts',(-34.1907852360671,-1.26797969074281,
136.58364760355));
#175542=CARTESIAN_POINT('Ctrl Pts',(-34.1868491866263,-1.34926638473693,
136.565813244854));
#175543=CARTESIAN_POINT('Ctrl Pts',(-34.1829131371856,-1.43011726815256,
136.546276637761));
#175544=CARTESIAN_POINT('Ctrl Pts',(-34.1789770877448,-1.51045690598956,
136.525064289113));
#175545=CARTESIAN_POINT('Ctrl Pts',(-34.1715538213394,-1.66197495563588,
136.485058461576));
#175546=CARTESIAN_POINT('Ctrl Pts',(-34.1641305549339,-1.81213163405688,
136.438968342382));
#175547=CARTESIAN_POINT('Ctrl Pts',(-34.1567072885285,-1.96040072642103,
136.386901217897));
#175548=CARTESIAN_POINT('Ctrl Pts',(-34.1492927958075,-2.1084945770312,
136.33489563243));
#175549=CARTESIAN_POINT('Ctrl Pts',(-34.1418783030866,-2.25470493356989,
136.276927225726));
#175550=CARTESIAN_POINT('Ctrl Pts',(-34.1344638103656,-2.39851738254339,
136.213153914424));
#175551=CARTESIAN_POINT('Ctrl Pts',(-34.1270564640119,-2.54219121966432,
136.14944207024));
#175552=CARTESIAN_POINT('Ctrl Pts',(-34.1196491176581,-2.68347141139231,
136.079936610284));
#175553=CARTESIAN_POINT('Ctrl Pts',(-34.1122417713044,-2.82186039299421,
136.004844680127));
#175554=CARTESIAN_POINT('Ctrl Pts',(-34.104839949629,-2.96014615887172,
135.929808756365));
#175555=CARTESIAN_POINT('Ctrl Pts',(-34.0974381279536,-3.09554468155867,
135.849194835935));
#175556=CARTESIAN_POINT('Ctrl Pts',(-34.0900363062783,-3.22758012280086,
135.763257381303));
#175557=CARTESIAN_POINT('Ctrl Pts',(-34.0826383919669,-3.35954586356231,
135.677365292384));
#175558=CARTESIAN_POINT('Ctrl Pts',(-34.0752404776555,-3.48815174648927,
135.586155469132));
#175559=CARTESIAN_POINT('Ctrl Pts',(-34.0678425633441,-3.61294831601482,
135.489927288557));
#175560=CARTESIAN_POINT('Ctrl Pts',(-34.0604458784319,-3.73772414661438,
135.393715099361));
#175561=CARTESIAN_POINT('Ctrl Pts',(-34.0530491935198,-3.85869162487618,
135.292486435728));
#175562=CARTESIAN_POINT('Ctrl Pts',(-34.0456525086076,-3.9754318849244,
135.186582872407));
#175563=CARTESIAN_POINT('Ctrl Pts',(-34.0382561516722,-4.09216696858683,
135.080684004962));
#175564=CARTESIAN_POINT('Ctrl Pts',(-34.0308597947367,-4.20467493024666,
134.970110900808));
#175565=CARTESIAN_POINT('Ctrl Pts',(-34.0234634378013,-4.31257170656327,
134.855243958055));
#175566=CARTESIAN_POINT('Ctrl Pts',(-34.0160659484648,-4.42048500215193,
134.740359428879));
#175567=CARTESIAN_POINT('Ctrl Pts',(-34.0086684591282,-4.52378545109523,
134.621180024243));
#175568=CARTESIAN_POINT('Ctrl Pts',(-34.0012709697916,-4.62212753686347,
134.498121248071));
#175569=CARTESIAN_POINT('Ctrl Pts',(-33.9938708872767,-4.72050409629728,
134.375019333836));
#175570=CARTESIAN_POINT('Ctrl Pts',(-33.9864708047617,-4.81391859901877,
134.248035631935));
#175571=CARTESIAN_POINT('Ctrl Pts',(-33.9790707222467,-4.90206741286746,
134.117616665958));
#175572=CARTESIAN_POINT('Ctrl Pts',(-33.9716625025803,-4.99031315539914,
133.987054290919));
#175573=CARTESIAN_POINT('Ctrl Pts',(-33.9642542829138,-5.07328143654858,
133.853049417505));
#175574=CARTESIAN_POINT('Ctrl Pts',(-33.9568460632474,-5.15071298733801,
133.716075968449));
#175575=CARTESIAN_POINT('Ctrl Pts',(-33.9494332839453,-5.22819219595495,
133.57901821452));
#175576=CARTESIAN_POINT('Ctrl Pts',(-33.9420205046432,-5.30012771363057,
133.438988575482));
#175577=CARTESIAN_POINT('Ctrl Pts',(-33.9346077253412,-5.36630765432855,
133.296482749725));
#175578=CARTESIAN_POINT('Ctrl Pts',(-33.9271843543124,-5.43258215602942,
133.153773304961));
#175579=CARTESIAN_POINT('Ctrl Pts',(-33.9197609832837,-5.49308451269598,
133.008580950781));
#175580=CARTESIAN_POINT('Ctrl Pts',(-33.9123376122549,-5.54765181418925,
132.861419175562));
#175581=CARTESIAN_POINT('Ctrl Pts',(-33.9084015628139,-5.57658470676673,
132.783390471238));
#175582=CARTESIAN_POINT('Ctrl Pts',(-33.904465513373,-5.60384988329389,
132.704808319859));
#175583=CARTESIAN_POINT('Ctrl Pts',(-33.900529463932,-5.62942887026787,
132.625750514621));
#175584=CARTESIAN_POINT('Ctrl Pts',(-33.891614366256,-5.68736492283714,
132.44668567656));
#175585=CARTESIAN_POINT('Ctrl Pts',(-33.88269926858,-5.73679017535818,132.264740894172));
#175586=CARTESIAN_POINT('Ctrl Pts',(-33.8737841709039,-5.77745654700139,
132.080654631503));
#175587=CARTESIAN_POINT('Ctrl Pts',(-33.864918132021,-5.81789913611463,
131.897581375107));
#175588=CARTESIAN_POINT('Ctrl Pts',(-33.856052093138,-5.84967891348687,
131.71239016528));
#175589=CARTESIAN_POINT('Ctrl Pts',(-33.847186054255,-5.87259860290424,
131.525828712264));
#175590=CARTESIAN_POINT('Ctrl Pts',(-33.8384101721643,-5.89528522705938,
131.341164361481));
#175591=CARTESIAN_POINT('Ctrl Pts',(-33.8296342900738,-5.90929097733084,
131.155157536546));
#175592=CARTESIAN_POINT('Ctrl Pts',(-33.8208584079831,-5.91447133257009,
130.968553853439));
#175593=CARTESIAN_POINT('Ctrl Pts',(-33.8183640220233,-5.91594375497067,
130.915515127262));
#175594=CARTESIAN_POINT('Ctrl Pts',(-33.8158696360635,-5.91670348892751,
130.862428307846));
#175595=CARTESIAN_POINT('Ctrl Pts',(-33.8133752501038,-5.91674792922998,
130.809310814809));
#175596=CARTESIAN_POINT('',(-32.0633751628002,-5.91238878816303,130.801325224237));
#175597=CARTESIAN_POINT('Ctrl Pts',(-33.8133751922042,-5.91218240422062,
130.80930576309));
#175598=CARTESIAN_POINT('Ctrl Pts',(-33.7496107415092,-5.90152008560987,
129.452491318376));
#175599=CARTESIAN_POINT('Ctrl Pts',(-33.5930304162097,-4.76268453244047,
126.104521439791));
#175600=CARTESIAN_POINT('Ctrl Pts',(-33.3436342163061,0.808310511306774,
123.852800026758));
#175601=CARTESIAN_POINT('Ctrl Pts',(-33.0651865924932,6.28545637891517,
127.726926842634));
#175602=CARTESIAN_POINT('Ctrl Pts',(-32.7867389686805,5.98657489591573,
134.429064956672));
#175603=CARTESIAN_POINT('Ctrl Pts',(-32.5082913448675,0.186323544011373,
137.800276859724));
#175604=CARTESIAN_POINT('Ctrl Pts',(-32.2671700860422,-4.98466412141571,
135.152472362352));
#175605=CARTESIAN_POINT('Ctrl Pts',(-32.118864701821,-5.90299123506428,
131.98393423347));
#175606=CARTESIAN_POINT('Ctrl Pts',(-32.0633751922042,-5.90845789250784,
130.801327869466));
#175607=CARTESIAN_POINT('',(-30.3133751922042,-5.92024601756991,130.800506515061));
#175608=CARTESIAN_POINT('Ctrl Pts',(-32.0633751301833,-5.9167492198897,
130.801322289959));
#175609=CARTESIAN_POINT('Ctrl Pts',(-32.0552226912489,-5.91665987366913,
130.627332105479));
#175610=CARTESIAN_POINT('Ctrl Pts',(-32.0470702523146,-5.90889181901625,
130.453606855061));
#175611=CARTESIAN_POINT('Ctrl Pts',(-32.0389178133802,-5.89353951184319,
130.280793444375));
#175612=CARTESIAN_POINT('Ctrl Pts',(-32.0307233044932,-5.87810798042311,
130.107088245101));
#175613=CARTESIAN_POINT('Ctrl Pts',(-32.0225287956061,-5.85501380044389,
129.934304547922));
#175614=CARTESIAN_POINT('Ctrl Pts',(-32.0143342867191,-5.82440321666261,
129.763083645656));
#175615=CARTESIAN_POINT('Ctrl Pts',(-32.0061184001803,-5.79371277667428,
129.591416066125));
#175616=CARTESIAN_POINT('Ctrl Pts',(-31.9979025136416,-5.75546677692304,
129.421319658769));
#175617=CARTESIAN_POINT('Ctrl Pts',(-31.9896866271029,-5.70986156687168,
129.253421724617));
#175618=CARTESIAN_POINT('Ctrl Pts',(-31.981440949994,-5.66409099363012,
129.084914997348));
#175619=CARTESIAN_POINT('Ctrl Pts',(-31.9731952728851,-5.61090785806304,
128.918622924254));
#175620=CARTESIAN_POINT('Ctrl Pts',(-31.9649495957763,-5.55055821384193,
128.755157338911));
#175621=CARTESIAN_POINT('Ctrl Pts',(-31.9604317629314,-5.51749245086869,
128.665594022192));
#175622=CARTESIAN_POINT('Ctrl Pts',(-31.9559139300866,-5.48227613873368,
128.576878802306));
#175623=CARTESIAN_POINT('Ctrl Pts',(-31.9513960972417,-5.44495557469001,
128.489109151277));
#175624=CARTESIAN_POINT('Ctrl Pts',(-31.9439728308363,-5.38363402986731,
128.344894541248));
#175625=CARTESIAN_POINT('Ctrl Pts',(-31.936549564431,-5.31648631935658,
128.202899780306));
#175626=CARTESIAN_POINT('Ctrl Pts',(-31.9291262980256,-5.24369408515371,
128.063630258004));
#175627=CARTESIAN_POINT('Ctrl Pts',(-31.9217118053046,-5.17098788532654,
127.924525340712));
#175628=CARTESIAN_POINT('Ctrl Pts',(-31.9142973125836,-5.09265061241143,
127.788139578232));
#175629=CARTESIAN_POINT('Ctrl Pts',(-31.9068828198626,-5.00891232289246,
127.654959419866));
#175630=CARTESIAN_POINT('Ctrl Pts',(-31.8994754735088,-4.92525474348962,
127.52190762555));
#175631=CARTESIAN_POINT('Ctrl Pts',(-31.8920681271552,-4.83620670838022,
127.392055598298));
#175632=CARTESIAN_POINT('Ctrl Pts',(-31.8846607808014,-4.74204457783254,
127.265866052875));
#175633=CARTESIAN_POINT('Ctrl Pts',(-31.8772589591261,-4.6479526769545,
127.139770624376));
#175634=CARTESIAN_POINT('Ctrl Pts',(-31.8698571374507,-4.54875449768384,
127.017332536583));
#175635=CARTESIAN_POINT('Ctrl Pts',(-31.8624553157753,-4.44477011228294,
126.898986216634));
#175636=CARTESIAN_POINT('Ctrl Pts',(-31.855057401464,-4.34084061942953,
126.780702370786));
#175637=CARTESIAN_POINT('Ctrl Pts',(-31.8476594871526,-4.2321301980658,
126.666506270731));
#175638=CARTESIAN_POINT('Ctrl Pts',(-31.8402615728413,-4.11899958718184,
126.556799792422));
#175639=CARTESIAN_POINT('Ctrl Pts',(-31.8328648879291,-4.00588777655302,
126.44711154534));
#175640=CARTESIAN_POINT('Ctrl Pts',(-31.8254682030169,-3.88835750200238,
126.341911698849));
#175641=CARTESIAN_POINT('Ctrl Pts',(-31.8180715181047,-3.7668068771992,
126.241565803816));
#175642=CARTESIAN_POINT('Ctrl Pts',(-31.8106751611693,-3.64526164207828,
126.141224358225));
#175643=CARTESIAN_POINT('Ctrl Pts',(-31.8032788042339,-3.51969669903321,
126.045736673799));
#175644=CARTESIAN_POINT('Ctrl Pts',(-31.7958824472985,-3.39054359274896,
125.955428290943));
#175645=CARTESIAN_POINT('Ctrl Pts',(-31.7884849579619,-3.26137071279423,
125.865106081643));
#175646=CARTESIAN_POINT('Ctrl Pts',(-31.7810874686253,-3.12860888170464,
125.779964966739));
#175647=CARTESIAN_POINT('Ctrl Pts',(-31.7736899792888,-2.9927188590947,
125.700287303739));
#175648=CARTESIAN_POINT('Ctrl Pts',(-31.7662898967738,-2.85678120044799,
125.620581709858));
#175649=CARTESIAN_POINT('Ctrl Pts',(-31.7588898142588,-2.71771348881668,
125.546343569736));
#175650=CARTESIAN_POINT('Ctrl Pts',(-31.7514897317438,-2.57600117619034,
125.477809340917));
#175651=CARTESIAN_POINT('Ctrl Pts',(-31.7440815120773,-2.43413303630788,
125.409199751669));
#175652=CARTESIAN_POINT('Ctrl Pts',(-31.736673292411,-2.28961482420962,
125.346306762018));
#175653=CARTESIAN_POINT('Ctrl Pts',(-31.7292650727446,-2.1429527456763,
125.289318995575));
#175654=CARTESIAN_POINT('Ctrl Pts',(-31.7218522934425,-1.99620039908083,
125.232296154112));
#175655=CARTESIAN_POINT('Ctrl Pts',(-31.7144395141404,-1.84730190901101,
125.1811858991));
#175656=CARTESIAN_POINT('Ctrl Pts',(-31.7070267348384,-1.6967782366183,
125.136126838139));
#175657=CARTESIAN_POINT('Ctrl Pts',(-31.6996033638096,-1.54603948894339,
125.091003394678));
#175658=CARTESIAN_POINT('Ctrl Pts',(-31.6921799927809,-1.39367128176785,
125.051948506168));
#175659=CARTESIAN_POINT('Ctrl Pts',(-31.6847566217521,-1.24020515869239,
125.019049759293));
#175660=CARTESIAN_POINT('Ctrl Pts',(-31.680820572311,-1.15883373786127,
125.001606054303));
#175661=CARTESIAN_POINT('Ctrl Pts',(-31.6768845228699,-1.07715375838786,
124.985892196715));
#175662=CARTESIAN_POINT('Ctrl Pts',(-31.6729484734287,-0.995244858637009,
124.971915312734));
#175663=CARTESIAN_POINT('Ctrl Pts',(-31.6655252070233,-0.840767230009799,
124.945555345751));
#175664=CARTESIAN_POINT('Ctrl Pts',(-31.6581019406178,-0.685008038423174,
124.925296979622));
#175665=CARTESIAN_POINT('Ctrl Pts',(-31.6506786742124,-0.52849066435613,
124.911260569188));
#175666=CARTESIAN_POINT('Ctrl Pts',(-31.6432641814914,-0.37215828082705,
124.897240748626));
#175667=CARTESIAN_POINT('Ctrl Pts',(-31.6358496887704,-0.21506986670196,
124.889428278929));
#175668=CARTESIAN_POINT('Ctrl Pts',(-31.6284351960493,-0.0577590367029607,
124.88789254479));
#175669=CARTESIAN_POINT('Ctrl Pts',(-31.6210278496956,0.0994001711954374,
124.886358290849));
#175670=CARTESIAN_POINT('Ctrl Pts',(-31.6136205033418,0.256780997419503,
124.891088732216));
#175671=CARTESIAN_POINT('Ctrl Pts',(-31.606213156988,0.413844767457253,
124.902101467804));
#175672=CARTESIAN_POINT('Ctrl Pts',(-31.5988113353126,0.570791393409633,
124.913105989678));
#175673=CARTESIAN_POINT('Ctrl Pts',(-31.5914095136372,0.727421063243341,
124.930383450169));
#175674=CARTESIAN_POINT('Ctrl Pts',(-31.5840076919618,0.88319527422838,
124.953899381896));
#175675=CARTESIAN_POINT('Ctrl Pts',(-31.5766097776504,1.03888725321998,
124.977402899745));
#175676=CARTESIAN_POINT('Ctrl Pts',(-31.5692118633392,1.19372430454489,
125.007138274604));
#175677=CARTESIAN_POINT('Ctrl Pts',(-31.5618139490278,1.34717333034709,
125.043019230311));
#175678=CARTESIAN_POINT('Ctrl Pts',(-31.5544172641156,1.50059685570483,
125.078894223254));
#175679=CARTESIAN_POINT('Ctrl Pts',(-31.5470205792033,1.65263245020395,
125.120912685186));
#175680=CARTESIAN_POINT('Ctrl Pts',(-31.5396238942911,1.80275737538391,
125.168937260976));
#175681=CARTESIAN_POINT('Ctrl Pts',(-31.5322275373557,1.95287564386758,
125.216959707306));
#175682=CARTESIAN_POINT('Ctrl Pts',(-31.5248311804202,2.10108305593801,
125.270987624226));
#175683=CARTESIAN_POINT('Ctrl Pts',(-31.5174348234848,2.24687246478841,
125.330833903511));
#175684=CARTESIAN_POINT('Ctrl Pts',(-31.5100373341482,2.39268419436928,
125.390689345414));
#175685=CARTESIAN_POINT('Ctrl Pts',(-31.5026398448117,2.5360768382514,125.456364781628));
#175686=CARTESIAN_POINT('Ctrl Pts',(-31.4952423554751,2.67656378924137,
125.527625183169));
#175687=CARTESIAN_POINT('Ctrl Pts',(-31.4878422729601,2.81709998771423,
125.598910564933));
#175688=CARTESIAN_POINT('Ctrl Pts',(-31.4804421904451,2.95472813258679,
125.675784641228));
#175689=CARTESIAN_POINT('Ctrl Pts',(-31.4730421079302,3.08898688677217,
125.757966798625));
#175690=CARTESIAN_POINT('Ctrl Pts',(-31.4656338882637,3.2233932722601,125.840239323752));
#175691=CARTESIAN_POINT('Ctrl Pts',(-31.4582256685972,3.35442254936867,
125.927831391406));
#175692=CARTESIAN_POINT('Ctrl Pts',(-31.4508174489307,3.48164240712283,
126.020419071997));
#175693=CARTESIAN_POINT('Ctrl Pts',(-31.4434046696286,3.60894056657666,
126.11306373876));
#175694=CARTESIAN_POINT('Ctrl Pts',(-31.4359918903266,3.73242434256604,
126.21070991421));
#175695=CARTESIAN_POINT('Ctrl Pts',(-31.4285791110246,3.85169552836548,
126.312994219768));
#175696=CARTESIAN_POINT('Ctrl Pts',(-31.4211557399958,3.97113713442844,
126.415424673939));
#175697=CARTESIAN_POINT('Ctrl Pts',(-31.413732368967,4.08635385600204,126.52250624072));
#175698=CARTESIAN_POINT('Ctrl Pts',(-31.4063089979383,4.19698469163003,
126.633839060168));
#175699=CARTESIAN_POINT('Ctrl Pts',(-31.4023729484975,4.25564381523029,
126.692870392433));
#175700=CARTESIAN_POINT('Ctrl Pts',(-31.3984368990568,4.31301435270298,
126.753096348597));
#175701=CARTESIAN_POINT('Ctrl Pts',(-31.394500849616,4.36904726208884,126.814453778537));
#175702=CARTESIAN_POINT('Ctrl Pts',(-31.3870775832105,4.47472358046362,
126.930171976502));
#175703=CARTESIAN_POINT('Ctrl Pts',(-31.3796543168051,4.57595916531729,
127.050266453983));
#175704=CARTESIAN_POINT('Ctrl Pts',(-31.3722310503997,4.67236985877937,
127.17436193089));
#175705=CARTESIAN_POINT('Ctrl Pts',(-31.3648165576787,4.76866660280833,
127.298310737249));
#175706=CARTESIAN_POINT('Ctrl Pts',(-31.3574020649576,4.86014957975774,
127.426250838326));
#175707=CARTESIAN_POINT('Ctrl Pts',(-31.3499875722366,4.94647198252855,
127.557770793064));
#175708=CARTESIAN_POINT('Ctrl Pts',(-31.3425802258828,5.03271118451759,
127.689163983918));
#175709=CARTESIAN_POINT('Ctrl Pts',(-31.3351728795291,5.11379951103673,
127.824129849383));
#175710=CARTESIAN_POINT('Ctrl Pts',(-31.3277655331753,5.1894309888911,127.962224699979));
#175711=CARTESIAN_POINT('Ctrl Pts',(-31.3203637114999,5.26500605793588,
128.100216554226));
#175712=CARTESIAN_POINT('Ctrl Pts',(-31.3129618898245,5.33513220353953,
128.24133242086));
#175713=CARTESIAN_POINT('Ctrl Pts',(-31.3055600681491,5.399547350206,128.385100611824));
#175714=CARTESIAN_POINT('Ctrl Pts',(-31.2981621538377,5.46392849261786,
128.528792908678));
#175715=CARTESIAN_POINT('Ctrl Pts',(-31.2907642395263,5.52260448794614,
128.675134401609));
#175716=CARTESIAN_POINT('Ctrl Pts',(-31.2833663252149,5.57535977035532,
128.823629945919));
#175717=CARTESIAN_POINT('Ctrl Pts',(-31.2759696403027,5.62810628579372,
128.972100812964));
#175718=CARTESIAN_POINT('Ctrl Pts',(-31.2685729553906,5.67493391624791,
129.12272466952));
#175719=CARTESIAN_POINT('Ctrl Pts',(-31.2611762704784,5.71567566957414,
129.274987477113));
#175720=CARTESIAN_POINT('Ctrl Pts',(-31.2537799135429,5.75641561636833,
129.427243533214));
#175721=CARTESIAN_POINT('Ctrl Pts',(-31.2463835566075,5.79107012610512,
129.581138035241));
#175722=CARTESIAN_POINT('Ctrl Pts',(-31.238987199672,5.8195224929958,129.736143169658));
#175723=CARTESIAN_POINT('Ctrl Pts',(-31.2315897103355,5.84797921601649,
129.891172035756));
#175724=CARTESIAN_POINT('Ctrl Pts',(-31.2241922209989,5.87023183808305,
130.04731150563));
#175725=CARTESIAN_POINT('Ctrl Pts',(-31.2167947316623,5.88621507266181,
130.204025143961));
#175726=CARTESIAN_POINT('Ctrl Pts',(-31.2093946491473,5.90220391013868,
130.360793718014));
#175727=CARTESIAN_POINT('Ctrl Pts',(-31.2019945666322,5.91191894662271,
130.518136490118));
#175728=CARTESIAN_POINT('Ctrl Pts',(-31.1945944841172,5.91534690617494,
130.675513645904));
#175729=CARTESIAN_POINT('Ctrl Pts',(-31.1871862644508,5.9187786351211,130.833063854051));
#175730=CARTESIAN_POINT('Ctrl Pts',(-31.1797780447843,5.91590947271245,
130.990648147946));
#175731=CARTESIAN_POINT('Ctrl Pts',(-31.1723698251179,5.90677827544612,
131.147727720268));
#175732=CARTESIAN_POINT('Ctrl Pts',(-31.1649570458158,5.89764145808025,
131.304903972445));
#175733=CARTESIAN_POINT('Ctrl Pts',(-31.1575442665136,5.88223496237197,
131.461574513398));
#175734=CARTESIAN_POINT('Ctrl Pts',(-31.1501314872116,5.86064926854897,
131.617207905534));
#175735=CARTESIAN_POINT('Ctrl Pts',(-31.1427081161828,5.83903273207435,
131.773063673959));
#175736=CARTESIAN_POINT('Ctrl Pts',(-31.1352847451541,5.81121942956898,
131.927878967384));
#175737=CARTESIAN_POINT('Ctrl Pts',(-31.1278613741253,5.7773506444235,132.081133930993));
#175738=CARTESIAN_POINT('Ctrl Pts',(-31.1239253246845,5.75939260186919,
132.16239339));
#175739=CARTESIAN_POINT('Ctrl Pts',(-31.1199892752438,5.73973297611782,
132.243214448401));
#175740=CARTESIAN_POINT('Ctrl Pts',(-31.1160532258031,5.71839838878044,
132.323521711622));
#175741=CARTESIAN_POINT('Ctrl Pts',(-31.1086299593976,5.67816202289149,
132.474978703754));
#175742=CARTESIAN_POINT('Ctrl Pts',(-31.1012066929921,5.6318434441649,132.625065066981));
#175743=CARTESIAN_POINT('Ctrl Pts',(-31.0937834265867,5.57955073965454,
132.773254750352));
#175744=CARTESIAN_POINT('Ctrl Pts',(-31.0863689338657,5.5273198407782,132.921269285825));
#175745=CARTESIAN_POINT('Ctrl Pts',(-31.0789544411448,5.46912899392726,
133.067391255007));
#175746=CARTESIAN_POINT('Ctrl Pts',(-31.0715399484237,5.40513689840729,
133.211106485325));
#175747=CARTESIAN_POINT('Ctrl Pts',(-31.06413260207,5.34120648087834,133.354683197493));
#175748=CARTESIAN_POINT('Ctrl Pts',(-31.0567252557161,5.27148609700651,
133.495857450143));
#175749=CARTESIAN_POINT('Ctrl Pts',(-31.0493179093623,5.19618364933253,
133.634131994358));
#175750=CARTESIAN_POINT('Ctrl Pts',(-31.0419160876869,5.1209373650649,133.772303408201));
#175751=CARTESIAN_POINT('Ctrl Pts',(-31.0345142660115,5.04011748448139,
133.907579093436));
#175752=CARTESIAN_POINT('Ctrl Pts',(-31.0271124443361,4.95397919389765,
134.039483599607));
#175753=CARTESIAN_POINT('Ctrl Pts',(-31.0197145300247,4.86788637504713,
134.171318474416));
#175754=CARTESIAN_POINT('Ctrl Pts',(-31.0123166157134,4.77648094115402,
134.299785402595));
#175755=CARTESIAN_POINT('Ctrl Pts',(-31.0049187014021,4.68006295287517,
134.424435384698));
#175756=CARTESIAN_POINT('Ctrl Pts',(-30.9975220164899,4.58366098751677,
134.549064652235));
#175757=CARTESIAN_POINT('Ctrl Pts',(-30.9901253315777,4.48224834919548,
134.669877937625));
#175758=CARTESIAN_POINT('Ctrl Pts',(-30.9827286466655,4.3761672497064,134.786456895294));
#175759=CARTESIAN_POINT('Ctrl Pts',(-30.97533228973,4.27009085396444,134.903030683731));
#175760=CARTESIAN_POINT('Ctrl Pts',(-30.9679359327946,4.15934665988656,
135.015370241667));
#175761=CARTESIAN_POINT('Ctrl Pts',(-30.9605395758591,4.04431564962055,
135.123092085108));
#175762=CARTESIAN_POINT('Ctrl Pts',(-30.9531420865225,3.92926702781321,
135.230830421038));
#175763=CARTESIAN_POINT('Ctrl Pts',(-30.9457445971859,3.80993055548604,
135.333949379595));
#175764=CARTESIAN_POINT('Ctrl Pts',(-30.9383471078494,3.68672226190013,
135.432104076976));
#175765=CARTESIAN_POINT('Ctrl Pts',(-30.9309470253344,3.5634707778379,135.530293182333));
#175766=CARTESIAN_POINT('Ctrl Pts',(-30.9235469428194,3.43634506201051,
135.623514329305));
#175767=CARTESIAN_POINT('Ctrl Pts',(-30.9161468603044,3.30579209956626,
135.711464565614));
#175768=CARTESIAN_POINT('Ctrl Pts',(-30.9087386406379,3.17509558071863,
135.799511512249));
#175769=CARTESIAN_POINT('Ctrl Pts',(-30.9013304209715,3.04096459888016,
135.882275764717));
#175770=CARTESIAN_POINT('Ctrl Pts',(-30.8939222013051,2.90387347079756,
135.959498775569));
#175771=CARTESIAN_POINT('Ctrl Pts',(-30.886509422003,2.76669796541292,136.036769315896));
#175772=CARTESIAN_POINT('Ctrl Pts',(-30.8790966427009,2.62655901491376,
136.108491648998));
#175773=CARTESIAN_POINT('Ctrl Pts',(-30.8716838633989,2.48395263957195,
136.174454643453));
#175774=CARTESIAN_POINT('Ctrl Pts',(-30.8642604923701,2.34114250155346,
136.240511888927));
#175775=CARTESIAN_POINT('Ctrl Pts',(-30.8568371213413,2.1958582412163,136.300793217486));
#175776=CARTESIAN_POINT('Ctrl Pts',(-30.8494137503126,2.04861359426401,
136.35513650062));
#175777=CARTESIAN_POINT('Ctrl Pts',(-30.8454777008717,1.97054094936247,
136.383950613288));
#175778=CARTESIAN_POINT('Ctrl Pts',(-30.8415416514309,1.89191739602549,
136.411096169584));
#175779=CARTESIAN_POINT('Ctrl Pts',(-30.8376056019901,1.81282075547442,
136.436554814415));
#175780=CARTESIAN_POINT('Ctrl Pts',(-30.8301823355846,1.66364695991792,
136.48456902403));
#175781=CARTESIAN_POINT('Ctrl Pts',(-30.8227590691793,1.51233872867243,
136.526725237324));
#175782=CARTESIAN_POINT('Ctrl Pts',(-30.8153358027739,1.359397066994,136.56283004761));
#175783=CARTESIAN_POINT('Ctrl Pts',(-30.8079213100529,1.20663616965867,
136.598892185008));
#175784=CARTESIAN_POINT('Ctrl Pts',(-30.8005068173318,1.05224604448269,
136.628917071073));
#175785=CARTESIAN_POINT('Ctrl Pts',(-30.7930923246108,0.896745060267345,
136.652760301188));
#175786=CARTESIAN_POINT('Ctrl Pts',(-30.785684978257,0.74139395375487,136.6765805503));
#175787=CARTESIAN_POINT('Ctrl Pts',(-30.7782776319032,0.584934486240059,
136.694230948695));
#175788=CARTESIAN_POINT('Ctrl Pts',(-30.7708702855494,0.427897383720886,
136.705617635482));
#175789=CARTESIAN_POINT('Ctrl Pts',(-30.7634684638741,0.270977405397665,
136.716995829649));
#175790=CARTESIAN_POINT('Ctrl Pts',(-30.7560666421986,0.113481020612778,
136.722119587338));
#175791=CARTESIAN_POINT('Ctrl Pts',(-30.7486648205232,-0.0440538262639501,
136.720946611439));
#175792=CARTESIAN_POINT('Ctrl Pts',(-30.7412669062119,-0.201505511721036,
136.719774254745));
#175793=CARTESIAN_POINT('Ctrl Pts',(-30.7338689919006,-0.358995246491254,
136.712311787134));
#175794=CARTESIAN_POINT('Ctrl Pts',(-30.7264710775893,-0.515983084510254,
136.698568962967));
#175795=CARTESIAN_POINT('Ctrl Pts',(-30.719074392677,-0.67294483399885,
136.684828422609));
#175796=CARTESIAN_POINT('Ctrl Pts',(-30.7116777077649,-0.829404480761122,
136.664809629616));
#175797=CARTESIAN_POINT('Ctrl Pts',(-30.7042810228527,-0.984825084984825,
136.638574370462));
#175798=CARTESIAN_POINT('Ctrl Pts',(-30.6968846659172,-1.14023879769607,
136.612340274608));
#175799=CARTESIAN_POINT('Ctrl Pts',(-30.6894883089817,-1.29461319138569,
136.579890322802));
#175800=CARTESIAN_POINT('Ctrl Pts',(-30.6820919520463,-1.44741969995118,
136.54133776365));
#175801=CARTESIAN_POINT('Ctrl Pts',(-30.6746944627097,-1.60024960358324,
136.502779302003));
#175802=CARTESIAN_POINT('Ctrl Pts',(-30.6672969733732,-1.75151078214626,
136.45811646397));
#175803=CARTESIAN_POINT('Ctrl Pts',(-30.6598994840366,-1.90068820115118,
136.407512848632));
#175804=CARTESIAN_POINT('Ctrl Pts',(-30.6524994015216,-2.04991791406908,
136.356891494276));
#175805=CARTESIAN_POINT('Ctrl Pts',(-30.6450993190067,-2.19706205979905,
136.300325336154));
#175806=CARTESIAN_POINT('Ctrl Pts',(-30.6376992364917,-2.34162414962036,
136.238026682426));
#175807=CARTESIAN_POINT('Ctrl Pts',(-30.6302910168252,-2.48634520032076,
136.175659524925));
#175808=CARTESIAN_POINT('Ctrl Pts',(-30.6228827971588,-2.62847818194231,
136.107547431205));
#175809=CARTESIAN_POINT('Ctrl Pts',(-30.6154745774923,-2.7675491914073,
136.033949706169));
#175810=CARTESIAN_POINT('Ctrl Pts',(-30.6080617981902,-2.90670579675828,
135.960306682962));
#175811=CARTESIAN_POINT('Ctrl Pts',(-30.6006490188882,-3.042796352708,135.881171487923));
#175812=CARTESIAN_POINT('Ctrl Pts',(-30.5932362395861,-3.17537511733832,
135.796847315264));
#175813=CARTESIAN_POINT('Ctrl Pts',(-30.5858128685574,-3.30814331672487,
135.712402656272));
#175814=CARTESIAN_POINT('Ctrl Pts',(-30.5783894975286,-3.43738939717479,
135.622754423926));
#175815=CARTESIAN_POINT('Ctrl Pts',(-30.5709661264999,-3.56269926868576,
135.528247204203));
#175816=CARTESIAN_POINT('Ctrl Pts',(-30.567030077059,-3.62914156933087,
135.478137208635));
#175817=CARTESIAN_POINT('Ctrl Pts',(-30.5630940276182,-3.69447784571092,
135.426661822723));
#175818=CARTESIAN_POINT('Ctrl Pts',(-30.5591579781774,-3.75865059089494,
135.373876598287));
#175819=CARTESIAN_POINT('Ctrl Pts',(-30.5518356192568,-3.87803320542091,
135.275678553566));
#175820=CARTESIAN_POINT('Ctrl Pts',(-30.5445132603363,-3.99376921053319,
135.172630614569));
#175821=CARTESIAN_POINT('Ctrl Pts',(-30.5371909014158,-4.10543114346578,
135.065037287857));
#175822=CARTESIAN_POINT('Ctrl Pts',(-30.5298772454647,-4.21696036091817,
134.957571840894));
#175823=CARTESIAN_POINT('Ctrl Pts',(-30.5225635895135,-4.32442486623985,
134.845572018463));
#175824=CARTESIAN_POINT('Ctrl Pts',(-30.5152499335623,-4.42742852318782,
134.729383832091));
#175825=CARTESIAN_POINT('Ctrl Pts',(-30.5079432704593,-4.53033369465485,
134.6133067374));
#175826=CARTESIAN_POINT('Ctrl Pts',(-30.5006366073561,-4.62878625187513,
134.493049533255));
#175827=CARTESIAN_POINT('Ctrl Pts',(-30.493329944253,-4.72242553994323,
134.368996304728));
#175828=CARTESIAN_POINT('Ctrl Pts',(-30.4858318295843,-4.8185183951257,
134.241692593117));
#175829=CARTESIAN_POINT('Ctrl Pts',(-30.4783337149157,-4.9095419668824,
134.110391462067));
#175830=CARTESIAN_POINT('Ctrl Pts',(-30.470835600247,-4.99514875989112,
133.975546425597));
#175831=CARTESIAN_POINT('Ctrl Pts',(-30.4635374611051,-5.078472410499,133.844297720791));
#175832=CARTESIAN_POINT('Ctrl Pts',(-30.4562393219631,-5.15666431666376,
133.709692083498));
#175833=CARTESIAN_POINT('Ctrl Pts',(-30.4489411828212,-5.22944681245081,
133.572178638724));
#175834=CARTESIAN_POINT('Ctrl Pts',(-30.441644464302,-5.30221514072616,
133.434691961696));
#175835=CARTESIAN_POINT('Ctrl Pts',(-30.4343477457829,-5.36957597382484,
133.294298942816));
#175836=CARTESIAN_POINT('Ctrl Pts',(-30.4270510272637,-5.43129716072561,
133.151474103189));
#175837=CARTESIAN_POINT('Ctrl Pts',(-30.4197541965348,-5.49301929678201,
133.008647067185));
#175838=CARTESIAN_POINT('Ctrl Pts',(-30.4124573658057,-5.54910146225589,
132.863388489118));
#175839=CARTESIAN_POINT('Ctrl Pts',(-30.4051605350768,-5.59935941978715,
132.716193416359));
#175840=CARTESIAN_POINT('Ctrl Pts',(-30.3975117565041,-5.65204146805617,
132.561898687544));
#175841=CARTESIAN_POINT('Ctrl Pts',(-30.3898629779314,-5.69832334402539,
132.405476452916));
#175842=CARTESIAN_POINT('Ctrl Pts',(-30.3822141993587,-5.73805168600958,
132.247514597979));
#175843=CARTESIAN_POINT('Ctrl Pts',(-30.3749091742947,-5.77599454592966,
132.096651908141));
#175844=CARTESIAN_POINT('Ctrl Pts',(-30.3676041492307,-5.80796004342863,
131.944385359264));
#175845=CARTESIAN_POINT('Ctrl Pts',(-30.3602991241668,-5.83386718326425,
131.791236623218));
#175846=CARTESIAN_POINT('Ctrl Pts',(-30.3529901493464,-5.8597883308398,
131.638005081133));
#175847=CARTESIAN_POINT('Ctrl Pts',(-30.345681174526,-5.87964454851776,
131.483890782082));
#175848=CARTESIAN_POINT('Ctrl Pts',(-30.3383721997057,-5.89340677965082,
131.329419749537));
#175849=CARTESIAN_POINT('Ctrl Pts',(-30.331054809785,-5.90718485576337,
131.174770868624));
#175850=CARTESIAN_POINT('Ctrl Pts',(-30.3237374198642,-5.91485492660111,
131.019764816672));
#175851=CARTESIAN_POINT('Ctrl Pts',(-30.3164200299435,-5.91643999844559,
130.86492717016));
#175852=CARTESIAN_POINT('Ctrl Pts',(-30.3154050840304,-5.9166598530943,
130.843450682202));
#175853=CARTESIAN_POINT('Ctrl Pts',(-30.3143901381173,-5.91676272238497,
130.821977425223));
#175854=CARTESIAN_POINT('Ctrl Pts',(-30.3133751922042,-5.91674874622358,
130.800508791798));
#175855=CARTESIAN_POINT('',(-28.5633751922042,-5.92063026149449,130.809252908732));
#175856=CARTESIAN_POINT('Ctrl Pts',(-30.3133751922042,-5.92331393100809,
130.800504517838));
#175857=CARTESIAN_POINT('Ctrl Pts',(-30.3024869129242,-5.92505294868337,
130.569933512729));
#175858=CARTESIAN_POINT('Ctrl Pts',(-30.1987827590407,-5.80798761008149,
128.375668861247));
#175859=CARTESIAN_POINT('Ctrl Pts',(-30.0022627305509,-3.06786481668135,
124.514228186764));
#175860=CARTESIAN_POINT('Ctrl Pts',(-29.7238151067389,3.63381068965364,
124.823308836979));
#175861=CARTESIAN_POINT('Ctrl Pts',(-29.4453674829254,6.99619169371812,
130.628683882915));
#175862=CARTESIAN_POINT('Ctrl Pts',(-29.166919859113,3.92941431422043,136.595497265716));
#175863=CARTESIAN_POINT('Ctrl Pts',(-28.8884722352998,-2.74830285748438,
137.240538981617));
#175864=CARTESIAN_POINT('Ctrl Pts',(-28.6872906796637,-5.74828619175598,
133.433271609878));
#175865=CARTESIAN_POINT('Ctrl Pts',(-28.5789249986318,-5.92356585908216,
131.138925557496));
#175866=CARTESIAN_POINT('Ctrl Pts',(-28.5633751922042,-5.92063026149449,
130.809252908732));
#175867=CARTESIAN_POINT('',(-26.8133751922042,-5.90730146414194,130.80590174944));
#175868=CARTESIAN_POINT('Ctrl Pts',(-28.5633751922042,-5.92063026149449,
130.809252908732));
#175869=CARTESIAN_POINT('Ctrl Pts',(-28.4861091240275,-5.90604345075803,
129.171129021212));
#175870=CARTESIAN_POINT('Ctrl Pts',(-28.3160271812466,-4.34740652689545,
125.540851770958));
#175871=CARTESIAN_POINT('Ctrl Pts',(-28.0531293638612,1.80717170404076,
124.043318466945));
#175872=CARTESIAN_POINT('Ctrl Pts',(-27.7746817400483,6.66507669263684,
128.670276923891));
#175873=CARTESIAN_POINT('Ctrl Pts',(-27.4962341162354,5.39810180779896,
135.258354039539));
#175874=CARTESIAN_POINT('Ctrl Pts',(-27.2177864924227,-0.829464926472844,
137.753428790069));
#175875=CARTESIAN_POINT('Ctrl Pts',(-26.9901668510788,-5.29714975403036,
134.572874387029));
#175876=CARTESIAN_POINT('Ctrl Pts',(-26.8553630843394,-5.90938010162537,
131.701195839402));
#175877=CARTESIAN_POINT('Ctrl Pts',(-26.8133751922042,-5.90730146414194,
130.80590174944));
#175878=CARTESIAN_POINT('',(-25.0633751922042,-5.91495849395119,130.798936651208));
#175879=CARTESIAN_POINT('Ctrl Pts',(-26.8133751922042,-5.90730146414194,
130.80590174944));
#175880=CARTESIAN_POINT('Ctrl Pts',(-26.7625472097351,-5.90478519232655,
129.722113304836));
#175881=CARTESIAN_POINT('Ctrl Pts',(-26.6189033526615,-5.09933556471253,
126.655762013877));
#175882=CARTESIAN_POINT('Ctrl Pts',(-26.3824436209839,-0.165029518421817,
123.807909675237));
#175883=CARTESIAN_POINT('Ctrl Pts',(-26.103995997171,5.79710984178776,126.883763977695));
#175884=CARTESIAN_POINT('Ctrl Pts',(-25.8255483733581,6.43198846195871,
133.562455060395));
#175885=CARTESIAN_POINT('Ctrl Pts',(-25.5471007495452,1.15618390569174,
137.706592090545));
#175886=CARTESIAN_POINT('Ctrl Pts',(-25.2930430224939,-4.62691189982062,
135.700502950123));
#175887=CARTESIAN_POINT('Ctrl Pts',(-25.1318011700469,-5.90195921676385,
132.253211397296));
#175888=CARTESIAN_POINT('Ctrl Pts',(-25.0633751922042,-5.91495849395119,
130.798936651208));
#175889=CARTESIAN_POINT('',(-23.3133751922042,-5.92204637845178,130.805173195123));
#175890=CARTESIAN_POINT('Ctrl Pts',(-25.0633751922042,-5.91495849395119,
130.798936651208));
#175891=CARTESIAN_POINT('Ctrl Pts',(-25.0389852954426,-5.9195919831401,
130.280571959342));
#175892=CARTESIAN_POINT('Ctrl Pts',(-24.9217795240766,-5.61943562007176,
127.794847517694));
#175893=CARTESIAN_POINT('Ctrl Pts',(-24.7117578781066,-2.12393811031069,
124.136043930883));
#175894=CARTESIAN_POINT('Ctrl Pts',(-24.4333102542936,4.46220325635265,
125.413043280463));
#175895=CARTESIAN_POINT('Ctrl Pts',(-24.1548626304806,6.9477978211794,131.644399882352));
#175896=CARTESIAN_POINT('Ctrl Pts',(-23.8764150066679,3.04870560713308,
137.103801438095));
#175897=CARTESIAN_POINT('Ctrl Pts',(-23.5979673828549,-3.65199812231858,
136.774324624571));
#175898=CARTESIAN_POINT('Ctrl Pts',(-23.4102874447005,-5.90639808632494,
132.854491977135));
#175899=CARTESIAN_POINT('Ctrl Pts',(-23.3154233811502,-5.92647964306893,
130.84848671572));
#175900=CARTESIAN_POINT('Ctrl Pts',(-23.3133751922042,-5.92639646612977,
130.805173792008));
#175901=CARTESIAN_POINT('',(-21.5633752135755,-5.91415027995088,130.809391528846));
#175902=CARTESIAN_POINT('Ctrl Pts',(-23.3133751922042,-5.91674994430204,
130.805172468387));
#175903=CARTESIAN_POINT('Ctrl Pts',(-23.3059798793106,-5.9167713677538,
130.649038849046));
#175904=CARTESIAN_POINT('Ctrl Pts',(-23.2985845664169,-5.91060834918149,
130.492660650871));
#175905=CARTESIAN_POINT('Ctrl Pts',(-23.2911892535234,-5.89822880539483,
130.336570577366));
#175906=CARTESIAN_POINT('Ctrl Pts',(-23.2838026511675,-5.88586384280095,
130.180664353886));
#175907=CARTESIAN_POINT('Ctrl Pts',(-23.2764160488116,-5.86729695721436,
130.025045951154));
#175908=CARTESIAN_POINT('Ctrl Pts',(-23.2690294464557,-5.84254802841723,
129.870249757904));
#175909=CARTESIAN_POINT('Ctrl Pts',(-23.2616499014213,-5.81782274528825,
129.715601460325));
#175910=CARTESIAN_POINT('Ctrl Pts',(-23.2542703563871,-5.78692723508014,
129.561774177723));
#175911=CARTESIAN_POINT('Ctrl Pts',(-23.2468908113527,-5.74993328836115,
129.409298704282));
#175912=CARTESIAN_POINT('Ctrl Pts',(-23.2395166762504,-5.71296646184232,
129.256935010354));
#175913=CARTESIAN_POINT('Ctrl Pts',(-23.2321425411481,-5.66991018801461,
129.105921516842));
#175914=CARTESIAN_POINT('Ctrl Pts',(-23.2247684060458,-5.62088757009435,
128.956780176324));
#175915=CARTESIAN_POINT('Ctrl Pts',(-23.2171143947618,-5.57000435931385,
128.801978360599));
#175916=CARTESIAN_POINT('Ctrl Pts',(-23.2094603834777,-5.51269307061477,
128.649194014824));
#175917=CARTESIAN_POINT('Ctrl Pts',(-23.2018063721937,-5.44914883316946,
128.498995666746));
#175918=CARTESIAN_POINT('Ctrl Pts',(-23.1944370770504,-5.38796833277387,
128.354384440561));
#175919=CARTESIAN_POINT('Ctrl Pts',(-23.187067781907,-5.32101042755766,
128.212170651381));
#175920=CARTESIAN_POINT('Ctrl Pts',(-23.1796984867637,-5.24849883706996,
128.072842629382));
#175921=CARTESIAN_POINT('Ctrl Pts',(-23.1723292880499,-5.17598819541877,
127.933516430533));
#175922=CARTESIAN_POINT('Ctrl Pts',(-23.1649600893362,-5.09792418648816,
127.797076257873));
#175923=CARTESIAN_POINT('Ctrl Pts',(-23.1575908906224,-5.01457683741423,
127.663986483141));
#175924=CARTESIAN_POINT('Ctrl Pts',(-23.1502203047479,-4.93121379922998,
127.5308716559));
#175925=CARTESIAN_POINT('Ctrl Pts',(-23.1428497188733,-4.84256564093685,
127.40110880106));
#175926=CARTESIAN_POINT('Ctrl Pts',(-23.1354791329987,-4.74894601112439,
127.27513374105));
#175927=CARTESIAN_POINT('Ctrl Pts',(-23.1281056757768,-4.65528991006212,
127.149109605136));
#175928=CARTESIAN_POINT('Ctrl Pts',(-23.1207322185549,-4.55665870647836,
127.026876503302));
#175929=CARTESIAN_POINT('Ctrl Pts',(-23.1133587613329,-4.45340651845562,
126.908837424993));
#175930=CARTESIAN_POINT('Ctrl Pts',(-23.1059771282012,-4.35003984132017,
126.790667461424));
#175931=CARTESIAN_POINT('Ctrl Pts',(-23.0985954950695,-4.24204219768873,
126.676701089374));
#175932=CARTESIAN_POINT('Ctrl Pts',(-23.0912138619378,-4.1298052089831,
126.567305095348));
#175933=CARTESIAN_POINT('Ctrl Pts',(-23.0838273751285,-4.01749442059947,
126.457837169696));
#175934=CARTESIAN_POINT('Ctrl Pts',(-23.0764408883193,-3.90093901295938,
126.352945859601));
#175935=CARTESIAN_POINT('Ctrl Pts',(-23.0690544015101,-3.78056341408622,
126.252957445513));
#175936=CARTESIAN_POINT('Ctrl Pts',(-23.0616578881235,-3.66002441476484,
126.152833304984));
#175937=CARTESIAN_POINT('Ctrl Pts',(-23.0542613747369,-3.53565517005978,
126.057625573558));
#175938=CARTESIAN_POINT('Ctrl Pts',(-23.0468648613503,-3.40790924259743,
125.967617378906));
#175939=CARTESIAN_POINT('Ctrl Pts',(-23.0449339526433,-3.37456032389313,
125.944120144781));
#175940=CARTESIAN_POINT('Ctrl Pts',(-23.0430030439361,-3.34098141257093,
125.92097701851));
#175941=CARTESIAN_POINT('Ctrl Pts',(-23.0410721352291,-3.30718084149768,
125.898192515663));
#175942=CARTESIAN_POINT('Ctrl Pts',(-23.0336488688237,-3.1772365086463,
125.810598817457));
#175943=CARTESIAN_POINT('Ctrl Pts',(-23.0262256024183,-3.04361328293765,
125.728038774378));
#175944=CARTESIAN_POINT('Ctrl Pts',(-23.0188023360128,-2.9067386488714,
125.650837454752));
#175945=CARTESIAN_POINT('Ctrl Pts',(-23.0113878432918,-2.7700257892559,
125.573727380675));
#175946=CARTESIAN_POINT('Ctrl Pts',(-23.0039733505708,-2.63006949255535,
125.501963604653));
#175947=CARTESIAN_POINT('Ctrl Pts',(-22.9965588578498,-2.48732754553731,
125.435828952044));
#175948=CARTESIAN_POINT('Ctrl Pts',(-22.989151511496,-2.34472317858195,
125.369758042503));
#175949=CARTESIAN_POINT('Ctrl Pts',(-22.9817441651423,-2.19933884288163,
125.309305611026));
#175950=CARTESIAN_POINT('Ctrl Pts',(-22.9743368187885,-2.05165824708864,
125.254709367293));
#175951=CARTESIAN_POINT('Ctrl Pts',(-22.9669349971132,-1.90408779705587,
125.200153843499));
#175952=CARTESIAN_POINT('Ctrl Pts',(-22.9595331754377,-1.75422484565269,
125.151445939522));
#175953=CARTESIAN_POINT('Ctrl Pts',(-22.9521313537623,-1.60257437076737,
125.108775840859));
#175954=CARTESIAN_POINT('Ctrl Pts',(-22.9447334394509,-1.45100395098642,
125.066128267408));
#175955=CARTESIAN_POINT('Ctrl Pts',(-22.9373355251395,-1.2976482454218,
125.029512252444));
#175956=CARTESIAN_POINT('Ctrl Pts',(-22.9299376108281,-1.14302862576133,
124.999068538507));
#175957=CARTESIAN_POINT('Ctrl Pts',(-22.9225409259159,-0.988434701077222,
124.968629883763));
#175958=CARTESIAN_POINT('Ctrl Pts',(-22.9151442410038,-0.832577645070909,
124.944361566332));
#175959=CARTESIAN_POINT('Ctrl Pts',(-22.9077475560916,-0.675990407329334,
124.926353512118));
#175960=CARTESIAN_POINT('Ctrl Pts',(-22.9003511991562,-0.519410112829972,
124.9083462564));
#175961=CARTESIAN_POINT('Ctrl Pts',(-22.8929548422207,-0.362100071825017,
124.896598754613));
#175962=CARTESIAN_POINT('Ctrl Pts',(-22.8855584852852,-0.204599497480111,
124.89114917131));
#175963=CARTESIAN_POINT('Ctrl Pts',(-22.8781609959487,-0.0470748093954174,
124.885698753662));
#175964=CARTESIAN_POINT('Ctrl Pts',(-22.8707635066121,0.110640097014221,
124.886548187313));
#175965=CARTESIAN_POINT('Ctrl Pts',(-22.8633660172756,0.268005008623873,
124.893683509328));
#175966=CARTESIAN_POINT('Ctrl Pts',(-22.8559659347606,0.425425084259119,
124.900821332619));
#175967=CARTESIAN_POINT('Ctrl Pts',(-22.8485658522456,0.582494548137099,
124.914249414544));
#175968=CARTESIAN_POINT('Ctrl Pts',(-22.8411657697306,0.738677459986535,
124.933901847367));
#175969=CARTESIAN_POINT('Ctrl Pts',(-22.8337575500642,0.895032111003989,
124.95357589006));
#175970=CARTESIAN_POINT('Ctrl Pts',(-22.8263493303977,1.05049789253869,
124.97948790556));
#175971=CARTESIAN_POINT('Ctrl Pts',(-22.8189411107313,1.20454749383738,
125.011520563017));
#175972=CARTESIAN_POINT('Ctrl Pts',(-22.8115283314292,1.35869191009564,
125.04357293604));
#175973=CARTESIAN_POINT('Ctrl Pts',(-22.8041155521271,1.51141804796216,
125.081753367219));
#175974=CARTESIAN_POINT('Ctrl Pts',(-22.796702772825,1.66221344582373,125.12589453745));
#175975=CARTESIAN_POINT('Ctrl Pts',(-22.7892794017963,1.81322430722093,
125.170098778655));
#175976=CARTESIAN_POINT('Ctrl Pts',(-22.7818560307675,1.96229856595337,
125.22028065046));
#175977=CARTESIAN_POINT('Ctrl Pts',(-22.7744326597387,2.10894265703972,
125.276224274112));
#175978=CARTESIAN_POINT('Ctrl Pts',(-22.7704966102979,2.18669687281173,
125.305886925721));
#175979=CARTESIAN_POINT('Ctrl Pts',(-22.7665605608571,2.26376826407334,
125.33716862988));
#175980=CARTESIAN_POINT('Ctrl Pts',(-22.7626245114162,2.34008614681892,
125.370032012488));
#175981=CARTESIAN_POINT('Ctrl Pts',(-22.7552012450108,2.48401929187543,
125.432011326455));
#175982=CARTESIAN_POINT('Ctrl Pts',(-22.7477779786054,2.62570601176396,
125.499806610725));
#175983=CARTESIAN_POINT('Ctrl Pts',(-22.7403547121999,2.76464175148176,
125.573233917852));
#175984=CARTESIAN_POINT('Ctrl Pts',(-22.7329402194789,2.9034132806931,125.646574439999));
#175985=CARTESIAN_POINT('Ctrl Pts',(-22.7255257267578,3.03943997490544,
125.725533562314));
#175986=CARTESIAN_POINT('Ctrl Pts',(-22.7181112340368,3.17223644020566,
125.809879009838));
#175987=CARTESIAN_POINT('Ctrl Pts',(-22.710703887683,3.3049049112733,125.894143162045));
#175988=CARTESIAN_POINT('Ctrl Pts',(-22.7032965413292,3.4343490386326,125.983783105323));
#175989=CARTESIAN_POINT('Ctrl Pts',(-22.6958891949754,3.56010737405691,
126.07852036977));
#175990=CARTESIAN_POINT('Ctrl Pts',(-22.6884873733,3.68577191416971,126.173186975592));
#175991=CARTESIAN_POINT('Ctrl Pts',(-22.6810855516246,3.80775583910473,
126.272943109091));
#175992=CARTESIAN_POINT('Ctrl Pts',(-22.6736837299492,3.9256261875345,126.377466717974));
#175993=CARTESIAN_POINT('Ctrl Pts',(-22.6662858156379,4.04343431312467,
126.481935149658));
#175994=CARTESIAN_POINT('Ctrl Pts',(-22.6588879013265,4.15713290831237,
126.591165797524));
#175995=CARTESIAN_POINT('Ctrl Pts',(-22.6514899870152,4.26632174827858,
126.704796091587));
#175996=CARTESIAN_POINT('Ctrl Pts',(-22.644093302103,4.37549244304063,126.818407502357));
#175997=CARTESIAN_POINT('Ctrl Pts',(-22.6366966171908,4.4801546116015,126.936416839318));
#175998=CARTESIAN_POINT('Ctrl Pts',(-22.6292999322785,4.57994452448142,
127.058424324038));
#175999=CARTESIAN_POINT('Ctrl Pts',(-22.6219035753431,4.67973001257203,
127.180426398817));
#176000=CARTESIAN_POINT('Ctrl Pts',(-22.6145072184076,4.7746434382067,127.306425979902));
#176001=CARTESIAN_POINT('Ctrl Pts',(-22.6071108614722,4.8643612345785,127.435990040858));
#176002=CARTESIAN_POINT('Ctrl Pts',(-22.5997133721356,4.95409276697384,
127.565573938403));
#176003=CARTESIAN_POINT('Ctrl Pts',(-22.5923158827991,5.03862687370157,
127.69872309552));
#176004=CARTESIAN_POINT('Ctrl Pts',(-22.5849183934625,5.11768330378438,
127.834975468303));
#176005=CARTESIAN_POINT('Ctrl Pts',(-22.5775183109475,5.19676744697631,
127.971275604143));
#176006=CARTESIAN_POINT('Ctrl Pts',(-22.5701182284326,5.27036990321027,
128.110680798823));
#176007=CARTESIAN_POINT('Ctrl Pts',(-22.5627181459176,5.33825643372543,
128.25270452587));
#176008=CARTESIAN_POINT('Ctrl Pts',(-22.5553099262511,5.40621761245989,
128.394884422606));
#176009=CARTESIAN_POINT('Ctrl Pts',(-22.5479017065846,5.46845015233561,
128.539688264945));
#176010=CARTESIAN_POINT('Ctrl Pts',(-22.5404934869181,5.52476774277762,
128.686608991226));
#176011=CARTESIAN_POINT('Ctrl Pts',(-22.533080707616,5.58111999575693,128.833620144763));
#176012=CARTESIAN_POINT('Ctrl Pts',(-22.5256679283139,5.63154992573988,
128.982750425641));
#176013=CARTESIAN_POINT('Ctrl Pts',(-22.5182551490118,5.67592130500799,
129.133478245328));
#176014=CARTESIAN_POINT('Ctrl Pts',(-22.510831777983,5.72035608418356,129.284421431992));
#176015=CARTESIAN_POINT('Ctrl Pts',(-22.5034084069543,5.75871493239599,
129.436966355337));
#176016=CARTESIAN_POINT('Ctrl Pts',(-22.4959850359255,5.79091269062497,
129.590581077428));
#176017=CARTESIAN_POINT('Ctrl Pts',(-22.4920489864848,5.80798471461218,
129.672031289013));
#176018=CARTESIAN_POINT('Ctrl Pts',(-22.4881129370441,5.82332550050936,
129.753782158449));
#176019=CARTESIAN_POINT('Ctrl Pts',(-22.4841768876034,5.83692828577312,
129.835754015667));
#176020=CARTESIAN_POINT('Ctrl Pts',(-22.476753621198,5.86258271425269,129.99035038013));
#176021=CARTESIAN_POINT('Ctrl Pts',(-22.4693303547925,5.88212975452446,
130.146200437488));
#176022=CARTESIAN_POINT('Ctrl Pts',(-22.4619070883871,5.89545144248125,
130.30278026324));
#176023=CARTESIAN_POINT('Ctrl Pts',(-22.4544925956661,5.90875738530923,
130.459175024642));
#176024=CARTESIAN_POINT('Ctrl Pts',(-22.4470781029451,5.91585259032555,
130.616297469254));
#176025=CARTESIAN_POINT('Ctrl Pts',(-22.439663610224,5.91667010976492,130.773613671142));
#176026=CARTESIAN_POINT('Ctrl Pts',(-22.4322562638703,5.91748684124827,
130.930778245751));
#176027=CARTESIAN_POINT('Ctrl Pts',(-22.4248489175164,5.91203793091999,
131.088135835065));
#176028=CARTESIAN_POINT('Ctrl Pts',(-22.4174415711627,5.9003082393564,131.245147689839));
#176029=CARTESIAN_POINT('Ctrl Pts',(-22.4100397494873,5.88858729623937,
131.402042439247));
#176030=CARTESIAN_POINT('Ctrl Pts',(-22.402637927812,5.87059492693678,131.558591596893));
#176031=CARTESIAN_POINT('Ctrl Pts',(-22.3952361061366,5.84636805699052,
131.714256823021));
#176032=CARTESIAN_POINT('Ctrl Pts',(-22.3878381918252,5.82215397622001,
131.869839874689));
#176033=CARTESIAN_POINT('Ctrl Pts',(-22.3804402775138,5.79171200653895,
132.024539556212));
#176034=CARTESIAN_POINT('Ctrl Pts',(-22.3730423632024,5.75513085705372,
132.177823169181));
#176035=CARTESIAN_POINT('Ctrl Pts',(-22.3656456782902,5.71855578669215,
132.331081309193));
#176036=CARTESIAN_POINT('Ctrl Pts',(-22.3582489933779,5.67584364793114,
132.482923484956));
#176037=CARTESIAN_POINT('Ctrl Pts',(-22.3508523084657,5.62713418102083,
132.632827590548));
#176038=CARTESIAN_POINT('Ctrl Pts',(-22.3434559515303,5.57842687393939,
132.782725049235));
#176039=CARTESIAN_POINT('Ctrl Pts',(-22.3360595945949,5.523722882824,132.930684253597));
#176040=CARTESIAN_POINT('Ctrl Pts',(-22.3286632376594,5.46321162931493,
133.076198916349));
#176041=CARTESIAN_POINT('Ctrl Pts',(-22.3212657483228,5.40269111137829,
133.221735857768));
#176042=CARTESIAN_POINT('Ctrl Pts',(-22.3138682589862,5.33636170406164,
133.36482716766));
#176043=CARTESIAN_POINT('Ctrl Pts',(-22.3064707696496,5.26446065549238,
133.504987316922));
#176044=CARTESIAN_POINT('Ctrl Pts',(-22.2990706871346,5.19253440212221,
133.645196599106));
#176045=CARTESIAN_POINT('Ctrl Pts',(-22.2916706046196,5.11503278911246,
133.782472342951));
#176046=CARTESIAN_POINT('Ctrl Pts',(-22.2842705221046,5.03223853319076,
133.916354497311));
#176047=CARTESIAN_POINT('Ctrl Pts',(-22.2768623024381,4.94935323647323,
134.050383868863));
#176048=CARTESIAN_POINT('Ctrl Pts',(-22.2694540827717,4.8611638707726,134.181011880992));
#176049=CARTESIAN_POINT('Ctrl Pts',(-22.2620458631052,4.76799633600885,
134.307807706121));
#176050=CARTESIAN_POINT('Ctrl Pts',(-22.2546330838032,4.67477145818217,
134.434681571965));
#176051=CARTESIAN_POINT('Ctrl Pts',(-22.2472203045011,4.57656253826667,
134.557718259832));
#176052=CARTESIAN_POINT('Ctrl Pts',(-22.2398075251991,4.47373476905679,
134.676521226145));
#176053=CARTESIAN_POINT('Ctrl Pts',(-22.2323841541703,4.37076007470783,
134.795493943708));
#176054=CARTESIAN_POINT('Ctrl Pts',(-22.2249607831415,4.26315360482678,
134.910220586273));
#176055=CARTESIAN_POINT('Ctrl Pts',(-22.2175374121128,4.15131686333376,
135.020341981697));
#176056=CARTESIAN_POINT('Ctrl Pts',(-22.213601362672,4.09201833950854,135.078730987877));
#176057=CARTESIAN_POINT('Ctrl Pts',(-22.2096653132312,4.03153108724262,
135.135825967334));
#176058=CARTESIAN_POINT('Ctrl Pts',(-22.2057292637905,3.96991847990183,
135.191578166928));
#176059=CARTESIAN_POINT('Ctrl Pts',(-22.198305997385,3.85371902532059,135.296725075398));
#176060=CARTESIAN_POINT('Ctrl Pts',(-22.1908827309796,3.73316361089217,
135.39741131683));
#176061=CARTESIAN_POINT('Ctrl Pts',(-22.1834594645742,3.60862926665662,
135.493254450692));
#176062=CARTESIAN_POINT('Ctrl Pts',(-22.1760449718532,3.48424211167366,
135.588984305929));
#176063=CARTESIAN_POINT('Ctrl Pts',(-22.1686304791322,3.35588568070393,
135.679882222098));
#176064=CARTESIAN_POINT('Ctrl Pts',(-22.1612159864112,3.22397299385564,
135.765603274138));
#176065=CARTESIAN_POINT('Ctrl Pts',(-22.1538086400574,3.09218744942174,
135.851241705));
#176066=CARTESIAN_POINT('Ctrl Pts',(-22.1464012937036,2.95685278380421,
135.931713003117));
#176067=CARTESIAN_POINT('Ctrl Pts',(-22.1389939473499,2.81841407877306,
136.006713224135));
#176068=CARTESIAN_POINT('Ctrl Pts',(-22.1315921256745,2.68007862655091,
136.081657507159));
#176069=CARTESIAN_POINT('Ctrl Pts',(-22.1241903039991,2.53864407142366,
136.151138660928));
#176070=CARTESIAN_POINT('Ctrl Pts',(-22.1167884823237,2.39458329303352,
136.214896766158));
#176071=CARTESIAN_POINT('Ctrl Pts',(-22.1093905680123,2.2505985632061,136.278621213982));
#176072=CARTESIAN_POINT('Ctrl Pts',(-22.1019926537009,2.10399071161964,
136.33662847934));
#176073=CARTESIAN_POINT('Ctrl Pts',(-22.0945947393895,1.95525586197085,
136.388705259216));
#176074=CARTESIAN_POINT('Ctrl Pts',(-22.0871980544773,1.8065457293568,136.440773384876));
#176075=CARTESIAN_POINT('Ctrl Pts',(-22.0798013695651,1.65570965219169,
136.486912857817));
#176076=CARTESIAN_POINT('Ctrl Pts',(-22.072404684653,1.50326242599239,136.526959034465));
#176077=CARTESIAN_POINT('Ctrl Pts',(-22.0650083277175,1.35082195946285,
136.567003435425));
#176078=CARTESIAN_POINT('Ctrl Pts',(-22.057611970782,1.19677084699426,136.600954982464));
#176079=CARTESIAN_POINT('Ctrl Pts',(-22.0502156138466,1.0416374294404,136.62869938073));
#176080=CARTESIAN_POINT('Ctrl Pts',(-22.04281812451,0.88648026056494,136.656448026734));
#176081=CARTESIAN_POINT('Ctrl Pts',(-22.0354206351736,0.730240824157295,
136.677987566008));
#176082=CARTESIAN_POINT('Ctrl Pts',(-22.028023145837,0.573455848010767,
136.693255161781));
#176083=CARTESIAN_POINT('Ctrl Pts',(-22.020623063322,0.416615911133003,
136.708528109586));
#176084=CARTESIAN_POINT('Ctrl Pts',(-22.0132229808071,0.259230425071346,
136.717524700296));
#176085=CARTESIAN_POINT('Ctrl Pts',(-22.0058228982921,0.101839259180674,
136.720234122619));
#176086=CARTESIAN_POINT('Ctrl Pts',(-21.9984146786257,-0.0557249744771007,
136.722946524231));
#176087=CARTESIAN_POINT('Ctrl Pts',(-21.9910064589591,-0.213294526965045,
136.719357944537));
#176088=CARTESIAN_POINT('Ctrl Pts',(-21.9835982392927,-0.370330773973643,
136.709509699541));
#176089=CARTESIAN_POINT('Ctrl Pts',(-21.9761854599906,-0.527463674171985,
136.699655393114));
#176090=CARTESIAN_POINT('Ctrl Pts',(-21.9687726806886,-0.684062244356029,
136.683533782499));
#176091=CARTESIAN_POINT('Ctrl Pts',(-21.9613599013866,-0.839595465555872,
136.661237773245));
#176092=CARTESIAN_POINT('Ctrl Pts',(-21.9539365303578,-0.99535091991573,
136.638909906408));
#176093=CARTESIAN_POINT('Ctrl Pts',(-21.9465131593291,-1.15003761893748,
136.610390088384));
#176094=CARTESIAN_POINT('Ctrl Pts',(-21.9390897883003,-1.30313635824861,
136.575821974476));
#176095=CARTESIAN_POINT('Ctrl Pts',(-21.9351537388594,-1.38431298338782,
136.557493131032));
#176096=CARTESIAN_POINT('Ctrl Pts',(-21.9312176894186,-1.46504344395392,
136.53746472363));
#176097=CARTESIAN_POINT('Ctrl Pts',(-21.9272816399777,-1.54525246769907,
136.515763717818));
#176098=CARTESIAN_POINT('Ctrl Pts',(-21.9198583735721,-1.69652418324068,
136.474836298123));
#176099=CARTESIAN_POINT('Ctrl Pts',(-21.9124351071667,-1.84639751596973,
136.42783298655));
#176100=CARTESIAN_POINT('Ctrl Pts',(-21.9050118407613,-1.99434691388684,
136.374864270699));
#176101=CARTESIAN_POINT('Ctrl Pts',(-21.8975973480402,-2.14212144790203,
136.321958159472));
#176102=CARTESIAN_POINT('Ctrl Pts',(-21.8901828553191,-2.28797622535719,
136.263100802848));
#176103=CARTESIAN_POINT('Ctrl Pts',(-21.8827683625981,-2.43139780357286,
136.198453245922));
#176104=CARTESIAN_POINT('Ctrl Pts',(-21.8753610162443,-2.5746811466707,
136.133867998745));
#176105=CARTESIAN_POINT('Ctrl Pts',(-21.8679536698907,-2.71553562134067,
136.063503813937));
#176106=CARTESIAN_POINT('Ctrl Pts',(-21.8605463235369,-2.85346493302224,
135.987570862049));
#176107=CARTESIAN_POINT('Ctrl Pts',(-21.8531445018615,-2.99129137182076,
135.911694543821));
#176108=CARTESIAN_POINT('Ctrl Pts',(-21.845742680186,-3.12619666607363,
135.830257907741));
#176109=CARTESIAN_POINT('Ctrl Pts',(-21.8383408585105,-3.25770653532805,
135.743518308122));
#176110=CARTESIAN_POINT('Ctrl Pts',(-21.8309429441991,-3.38914698154654,
135.656824497663));
#176111=CARTESIAN_POINT('Ctrl Pts',(-21.8235450298877,-3.51719526162264,
135.564833503806));
#176112=CARTESIAN_POINT('Ctrl Pts',(-21.8161471155763,-3.64140375070958,
135.467847433975));
#176113=CARTESIAN_POINT('Ctrl Pts',(-21.8087504306641,-3.7655915985983,
135.37087748147));
#176114=CARTESIAN_POINT('Ctrl Pts',(-21.8013537457518,-3.88594062800541,
135.268914329994));
#176115=CARTESIAN_POINT('Ctrl Pts',(-21.7939570608396,-4.0020340600782,
135.162302097723));
#176116=CARTESIAN_POINT('Ctrl Pts',(-21.7865607039042,-4.11812234444605,
135.055694592751));
#176117=CARTESIAN_POINT('Ctrl Pts',(-21.7791643469687,-4.22995513172452,
134.944438669363));
#176118=CARTESIAN_POINT('Ctrl Pts',(-21.7717679900333,-4.33715068128002,
134.828917056526));
#176119=CARTESIAN_POINT('Ctrl Pts',(-21.7643705006967,-4.44436264274842,
134.713377757034));
#176120=CARTESIAN_POINT('Ctrl Pts',(-21.75697301136,-4.54693569891078,134.593571741362));
#176121=CARTESIAN_POINT('Ctrl Pts',(-21.7495755220234,-4.64452686892937,
134.469916608994));
#176122=CARTESIAN_POINT('Ctrl Pts',(-21.7421754395084,-4.74215224938077,
134.346218129512));
#176123=CARTESIAN_POINT('Ctrl Pts',(-21.7347753569935,-4.83479203551193,
134.218668139732));
#176124=CARTESIAN_POINT('Ctrl Pts',(-21.7273752744785,-4.92214531890378,
134.087715003266));
#176125=CARTESIAN_POINT('Ctrl Pts',(-21.719967054812,-5.00959465621136,
133.956617870363));
#176126=CARTESIAN_POINT('Ctrl Pts',(-21.7125588351455,-5.09174567445106,
133.822110428272));
#176127=CARTESIAN_POINT('Ctrl Pts',(-21.705150615479,-5.16834199435097,
133.684668169188));
#176128=CARTESIAN_POINT('Ctrl Pts',(-21.697737836177,-5.24498545800748,
133.547141316687));
#176129=CARTESIAN_POINT('Ctrl Pts',(-21.690325056875,-5.31606724272622,
133.406676380159));
#176130=CARTESIAN_POINT('Ctrl Pts',(-21.6829122775729,-5.38137848385342,
133.263770338621));
#176131=CARTESIAN_POINT('Ctrl Pts',(-21.6754889065441,-5.446783044745,133.120660106229));
#176132=CARTESIAN_POINT('Ctrl Pts',(-21.6680655355153,-5.50640045337233,
132.975102147108));
#176133=CARTESIAN_POINT('Ctrl Pts',(-21.6606421644865,-5.56007092836429,
132.827610931803));
#176134=CARTESIAN_POINT('Ctrl Pts',(-21.6567061150459,-5.58852830200886,
132.749407550449));
#176135=CARTESIAN_POINT('Ctrl Pts',(-21.6527700656052,-5.61531462151302,
132.670660884153));
#176136=CARTESIAN_POINT('Ctrl Pts',(-21.6488340161646,-5.64041188726546,
132.591448837127));
#176137=CARTESIAN_POINT('Ctrl Pts',(-21.6398564824062,-5.69765495647397,
132.410778132406));
#176138=CARTESIAN_POINT('Ctrl Pts',(-21.6308789486478,-5.74624880988774,
132.227243494478));
#176139=CARTESIAN_POINT('Ctrl Pts',(-21.6219014148894,-5.78594647018682,
132.041597056826));
#176140=CARTESIAN_POINT('Ctrl Pts',(-21.6129769272198,-5.82540956655472,
131.857047559343));
#176141=CARTESIAN_POINT('Ctrl Pts',(-21.6040524395501,-5.85608123096748,
131.670411147484));
#176142=CARTESIAN_POINT('Ctrl Pts',(-21.5951279518804,-5.8777655631654,
131.482448035947));
#176143=CARTESIAN_POINT('Ctrl Pts',(-21.5862995925613,-5.8992163268758,
131.296509531821));
#176144=CARTESIAN_POINT('Ctrl Pts',(-21.5774712332422,-5.91187226502017,
131.109272779503));
#176145=CARTESIAN_POINT('Ctrl Pts',(-21.5686428739231,-5.91559043864777,
130.921494407222));
#176146=CARTESIAN_POINT('Ctrl Pts',(-21.5668869983483,-5.91632994754399,
130.884147098912));
#176147=CARTESIAN_POINT('Ctrl Pts',(-21.5651311227735,-5.91671605321219,
130.846778431061));
#176148=CARTESIAN_POINT('Ctrl Pts',(-21.5633752471987,-5.91674785866266,
130.809394454159));
#176149=CARTESIAN_POINT('',(-19.8133751630259,-5.91241589777291,130.801494312422));
#176150=CARTESIAN_POINT('Ctrl Pts',(-21.5633751922043,-5.91249924175333,
130.809389669497));
#176151=CARTESIAN_POINT('Ctrl Pts',(-21.4990455922534,-5.90151877568405,
129.440734853295));
#176152=CARTESIAN_POINT('Ctrl Pts',(-21.3419001176983,-4.74664212764213,
126.080642320765));
#176153=CARTESIAN_POINT('Ctrl Pts',(-21.0919387685389,0.850611657590301,
123.857849238585));
#176154=CARTESIAN_POINT('Ctrl Pts',(-20.813491144726,6.30407313683402,127.765245217356));
#176155=CARTESIAN_POINT('Ctrl Pts',(-20.5350435209133,5.96439937442269,
134.46543977988));
#176156=CARTESIAN_POINT('Ctrl Pts',(-20.2565958971003,0.143733964024427,
137.801281445897));
#176157=CARTESIAN_POINT('Ctrl Pts',(-20.0160397875307,-4.99895800061713,
135.128328424986));
#176158=CARTESIAN_POINT('Ctrl Pts',(-19.8682995525653,-5.90317744802826,
131.97214796945));
#176159=CARTESIAN_POINT('Ctrl Pts',(-19.8133751922042,-5.90827769618411,
130.801496940956));
#176160=CARTESIAN_POINT('',(-18.0633751922043,-5.91997941989959,130.800355646857));
#176161=CARTESIAN_POINT('Ctrl Pts',(-19.8133751324712,-5.91674930439072,
130.801491559896));
#176162=CARTESIAN_POINT('Ctrl Pts',(-19.805254061995,-5.91666525141781,
130.628152287518));
#176163=CARTESIAN_POINT('Ctrl Pts',(-19.7971329915187,-5.90895978560523,
130.455069894106));
#176164=CARTESIAN_POINT('Ctrl Pts',(-19.7890119210425,-5.89372508479234,
130.282886565106));
#176165=CARTESIAN_POINT('Ctrl Pts',(-19.780850939307,-5.8784155125575,130.109857035655));
#176166=CARTESIAN_POINT('Ctrl Pts',(-19.7726899575716,-5.85550259932545,
129.937735664064));
#176167=CARTESIAN_POINT('Ctrl Pts',(-19.764528975836,-5.82513029749076,
129.767158814755));
#176168=CARTESIAN_POINT('Ctrl Pts',(-19.7563478049367,-5.79468285869375,
129.596159981416));
#176169=CARTESIAN_POINT('Ctrl Pts',(-19.7481666340374,-5.75673919147736,
129.426713542274));
#176170=CARTESIAN_POINT('Ctrl Pts',(-19.7399854631381,-5.7114933612633,
129.259441801982));
#176171=CARTESIAN_POINT('Ctrl Pts',(-19.7317751853,-5.6660865556063,129.091574942928));
#176172=CARTESIAN_POINT('Ctrl Pts',(-19.7235649074619,-5.61332565032963,
128.925898501203));
#176173=CARTESIAN_POINT('Ctrl Pts',(-19.7153546296238,-5.5534544170368,
128.763019244744));
#176174=CARTESIAN_POINT('Ctrl Pts',(-19.7101366362407,-5.5154036098262,
128.659502299372));
#176175=CARTESIAN_POINT('Ctrl Pts',(-19.7049186428575,-5.47448177662029,
128.557114725779));
#176176=CARTESIAN_POINT('Ctrl Pts',(-19.6997006494744,-5.43076109945184,
128.456007057477));
#176177=CARTESIAN_POINT('Ctrl Pts',(-19.692277383069,-5.36856281551098,
128.312168401059));
#176178=CARTESIAN_POINT('Ctrl Pts',(-19.6848541166636,-5.30055198667891,
128.170585018124));
#176179=CARTESIAN_POINT('Ctrl Pts',(-19.6774308502582,-5.22691332803574,
128.031761183154));
#176180=CARTESIAN_POINT('Ctrl Pts',(-19.6700163575372,-5.15336170417167,
127.893101426428));
#176181=CARTESIAN_POINT('Ctrl Pts',(-19.6626018648161,-5.07419566381752,
127.757195052076));
#176182=CARTESIAN_POINT('Ctrl Pts',(-19.6551873720952,-4.98964822034993,
127.624527099965));
#176183=CARTESIAN_POINT('Ctrl Pts',(-19.6477800257414,-4.90518226689174,
127.491987018222));
#176184=CARTESIAN_POINT('Ctrl Pts',(-19.6403726793877,-4.81534543548999,
127.362679457492));
#176185=CARTESIAN_POINT('Ctrl Pts',(-19.632965333034,-4.72041689796875,
127.237065441684));
#176186=CARTESIAN_POINT('Ctrl Pts',(-19.6255635113586,-4.62555916173197,
127.111545113548));
#176187=CARTESIAN_POINT('Ctrl Pts',(-19.6181616896832,-4.52561750498102,
126.989713141722));
#176188=CARTESIAN_POINT('Ctrl Pts',(-19.6107598680078,-4.42091463852936,
126.872001996924));
#176189=CARTESIAN_POINT('Ctrl Pts',(-19.6033619536965,-4.31626704390605,
126.754352990923));
#176190=CARTESIAN_POINT('Ctrl Pts',(-19.5959640393852,-4.20686349262083,
126.640820757849));
#176191=CARTESIAN_POINT('Ctrl Pts',(-19.5885661250739,-4.09306716331315,
126.531804970286));
#176192=CARTESIAN_POINT('Ctrl Pts',(-19.5811694401617,-3.97928974489091,
126.422807299169));
#176193=CARTESIAN_POINT('Ctrl Pts',(-19.5737727552495,-3.86112126657913,
126.318324841927));
#176194=CARTESIAN_POINT('Ctrl Pts',(-19.5663760703374,-3.73896205988283,
126.218720719225));
#176195=CARTESIAN_POINT('Ctrl Pts',(-19.5589797134019,-3.61680826985394,
126.119121013074));
#176196=CARTESIAN_POINT('Ctrl Pts',(-19.5515833564665,-3.49066439259866,
126.024399447261));
#176197=CARTESIAN_POINT('Ctrl Pts',(-19.5441869995311,-3.36096394646326,
125.934878929226));
#176198=CARTESIAN_POINT('Ctrl Pts',(-19.5367895101945,-3.23124364285826,
125.845344705372));
#176199=CARTESIAN_POINT('Ctrl Pts',(-19.529392020858,-3.09796599340552,
125.761013326884));
#176200=CARTESIAN_POINT('Ctrl Pts',(-19.5219945315215,-2.96159346797302,
125.682164341264));
#176201=CARTESIAN_POINT('Ctrl Pts',(-19.5145944490065,-2.82517313736313,
125.603287715255));
#176202=CARTESIAN_POINT('Ctrl Pts',(-19.5071943664916,-2.68565609370416,
125.529897495227));
#176203=CARTESIAN_POINT('Ctrl Pts',(-19.4997942839766,-2.54352921937556,
125.462227179259));
#176204=CARTESIAN_POINT('Ctrl Pts',(-19.4923860643102,-2.40124606193763,
125.394482452821));
#176205=CARTESIAN_POINT('Ctrl Pts',(-19.4849778446437,-2.25634767994791,
125.332470351808));
#176206=CARTESIAN_POINT('Ctrl Pts',(-19.4775696249772,-2.10934141801378,
125.276376414916));
#176207=CARTESIAN_POINT('Ctrl Pts',(-19.4701568456752,-1.96224467617836,
125.220247953141));
#176208=CARTESIAN_POINT('Ctrl Pts',(-19.4627440663732,-1.81303782222359,
125.170045032456));
#176209=CARTESIAN_POINT('Ctrl Pts',(-19.4553312870711,-1.66224265139249,
125.125903086652));
#176210=CARTESIAN_POINT('Ctrl Pts',(-19.4479079160424,-1.51123201734951,
125.081698068766));
#176211=CARTESIAN_POINT('Ctrl Pts',(-19.4404845450136,-1.35862889501245,
125.043571412378));
#176212=CARTESIAN_POINT('Ctrl Pts',(-19.4330611739849,-1.20496535129876,
125.01160746689));
#176213=CARTESIAN_POINT('Ctrl Pts',(-19.4291251245438,-1.12348925330885,
124.994659416026));
#176214=CARTESIAN_POINT('Ctrl Pts',(-19.4251890751027,-1.04171513246566,
124.979443058799));
#176215=CARTESIAN_POINT('Ctrl Pts',(-19.4212530256616,-0.959722669037745,
124.965965036498));
#176216=CARTESIAN_POINT('Ctrl Pts',(-19.4138297592562,-0.805087441922301,
124.940545907076));
#176217=CARTESIAN_POINT('Ctrl Pts',(-19.4064064928507,-0.649207817768075,
124.921236066696));
#176218=CARTESIAN_POINT('Ctrl Pts',(-19.3989832264453,-0.492607899991114,
124.908152682006));
#176219=CARTESIAN_POINT('Ctrl Pts',(-19.3915687337243,-0.336193070312152,
124.895084760789));
#176220=CARTESIAN_POINT('Ctrl Pts',(-19.3841542410033,-0.179060009951245,
124.888228677603));
#176221=CARTESIAN_POINT('Ctrl Pts',(-19.3767397482823,-0.0217427461081744,
124.88765056759));
#176222=CARTESIAN_POINT('Ctrl Pts',(-19.3693324019285,0.135422889433114,
124.88707301478));
#176223=CARTESIAN_POINT('Ctrl Pts',(-19.3619250555747,0.292772004215519,
124.892761390263));
#176224=CARTESIAN_POINT('Ctrl Pts',(-19.354517709221,0.449765826577879,
124.904730013558));
#176225=CARTESIAN_POINT('Ctrl Pts',(-19.3471158875456,0.606642557024484,
124.916689710203));
#176226=CARTESIAN_POINT('Ctrl Pts',(-19.3397140658702,0.763164152067051,
124.93492029984));
#176227=CARTESIAN_POINT('Ctrl Pts',(-19.3323122441948,0.918792328765516,
124.959384037707));
#176228=CARTESIAN_POINT('Ctrl Pts',(-19.3249143298834,1.07433835056069,
124.983834861357));
#176229=CARTESIAN_POINT('Ctrl Pts',(-19.3175164155721,1.22899152544658,
125.014512222368));
#176230=CARTESIAN_POINT('Ctrl Pts',(-19.3101185012607,1.38221929063171,
125.051326601057));
#176231=CARTESIAN_POINT('Ctrl Pts',(-19.3027218163485,1.53542159214232,
125.088134861865));
#176232=CARTESIAN_POINT('Ctrl Pts',(-19.2953251314363,1.68719859146999,
125.13107802911));
#176233=CARTESIAN_POINT('Ctrl Pts',(-19.2879284465241,1.83702839595899,
125.180015568146));
#176234=CARTESIAN_POINT('Ctrl Pts',(-19.2805320895887,1.98685155683745,
125.22895093724));
#176235=CARTESIAN_POINT('Ctrl Pts',(-19.2731357326532,2.13472733970239,
125.283880033731));
#176236=CARTESIAN_POINT('Ctrl Pts',(-19.2657393757178,2.28014974612413,
125.344612665714));
#176237=CARTESIAN_POINT('Ctrl Pts',(-19.2583418863812,2.42559441708775,
125.405354596019));
#176238=CARTESIAN_POINT('Ctrl Pts',(-19.2509443970446,2.56858461921539,
125.471901687142));
#176239=CARTESIAN_POINT('Ctrl Pts',(-19.2435469077081,2.70863518501748,
125.544015952339));
#176240=CARTESIAN_POINT('Ctrl Pts',(-19.2361468251931,2.8487348453281,125.616155497079));
#176241=CARTESIAN_POINT('Ctrl Pts',(-19.228746742678,2.98589248594806,125.693865930657));
#176242=CARTESIAN_POINT('Ctrl Pts',(-19.2213466601631,3.11964848651157,
125.776863836552));
#176243=CARTESIAN_POINT('Ctrl Pts',(-19.2139384404966,3.25355156554814,
125.859953007177));
#176244=CARTESIAN_POINT('Ctrl Pts',(-19.2065302208301,3.38404521721012,
125.948341064354));
#176245=CARTESIAN_POINT('Ctrl Pts',(-19.1991220011637,3.51069911038355,
126.041701452892));
#176246=CARTESIAN_POINT('Ctrl Pts',(-19.1917092218616,3.63743095691508,
126.135119303192));
#176247=CARTESIAN_POINT('Ctrl Pts',(-19.1842964425595,3.76031804505089,
126.233515350278));
#176248=CARTESIAN_POINT('Ctrl Pts',(-19.1768836632575,3.87896438743185,
126.336523798306));
#176249=CARTESIAN_POINT('Ctrl Pts',(-19.1694602922287,3.99778025727076,
126.439679429635));
#176250=CARTESIAN_POINT('Ctrl Pts',(-19.1620369212,4.11234300825503,126.54746036933));
#176251=CARTESIAN_POINT('Ctrl Pts',(-19.1546135501712,4.2222940796779,126.659464567335));
#176252=CARTESIAN_POINT('Ctrl Pts',(-19.1506775007304,4.28059277598683,
126.718851880623));
#176253=CARTESIAN_POINT('Ctrl Pts',(-19.1467414512895,4.33759563802791,
126.779425951686));
#176254=CARTESIAN_POINT('Ctrl Pts',(-19.1428054018486,4.39325400916325,
126.841123333038));
#176255=CARTESIAN_POINT('Ctrl Pts',(-19.1353821354432,4.49822396008497,
126.957482668758));
#176256=CARTESIAN_POINT('Ctrl Pts',(-19.1279588690378,4.59872662010651,
127.078191170905));
#176257=CARTESIAN_POINT('Ctrl Pts',(-19.1205356026323,4.69438012291138,
127.202871227867));
#176258=CARTESIAN_POINT('Ctrl Pts',(-19.1131211099113,4.78992057121961,
127.327403923355));
#176259=CARTESIAN_POINT('Ctrl Pts',(-19.1057066171903,4.8806230454924,127.455898536846));
#176260=CARTESIAN_POINT('Ctrl Pts',(-19.0982921244693,4.96614324961477,
127.58794152379));
#176261=CARTESIAN_POINT('Ctrl Pts',(-19.0908847781155,5.0515810261445,127.719857242733));
#176262=CARTESIAN_POINT('Ctrl Pts',(-19.0834774317617,5.13184627475372,
127.855314215252));
#176263=CARTESIAN_POINT('Ctrl Pts',(-19.0760700854079,5.20663572878033,
127.993866897543));
#176264=CARTESIAN_POINT('Ctrl Pts',(-19.0686682637325,5.28136940201058,
128.132316242016));
#176265=CARTESIAN_POINT('Ctrl Pts',(-19.0612664420571,5.35063523600553,
128.273856371853));
#176266=CARTESIAN_POINT('Ctrl Pts',(-19.0538646203816,5.41417403142384,
128.418014012407));
#176267=CARTESIAN_POINT('Ctrl Pts',(-19.0464667060703,5.47767928520665,
128.562095553263));
#176268=CARTESIAN_POINT('Ctrl Pts',(-19.0390687917589,5.53546337120056,
128.708791512263));
#176269=CARTESIAN_POINT('Ctrl Pts',(-19.0316708774475,5.58731374165029,
128.857605441673));
#176270=CARTESIAN_POINT('Ctrl Pts',(-19.0242741925353,5.63915549550904,
129.006394640907));
#176271=CARTESIAN_POINT('Ctrl Pts',(-19.0168775076232,5.68506536818857,
129.157300759831));
#176272=CARTESIAN_POINT('Ctrl Pts',(-19.009480822711,5.72487949973719,129.309808752963));
#176273=CARTESIAN_POINT('Ctrl Pts',(-19.0020844657755,5.76469186588549,
129.462309983731));
#176274=CARTESIAN_POINT('Ctrl Pts',(-18.99468810884,5.79840893404005,129.616412586286));
#176275=CARTESIAN_POINT('Ctrl Pts',(-18.9872917519045,5.82591721352525,
129.77158804645));
#176276=CARTESIAN_POINT('Ctrl Pts',(-18.9798942625679,5.85342970459826,
129.926787264372));
#176277=CARTESIAN_POINT('Ctrl Pts',(-18.9724967732313,5.87473144910435,
130.083059299371));
#176278=CARTESIAN_POINT('Ctrl Pts',(-18.9650992838947,5.88976042715353,
130.239867328645));
#176279=CARTESIAN_POINT('Ctrl Pts',(-18.9576992013797,5.90479467358766,
130.396730326732));
#176280=CARTESIAN_POINT('Ctrl Pts',(-18.9502991188648,5.91355173996144,
130.554129321824));
#176281=CARTESIAN_POINT('Ctrl Pts',(-18.9428990363498,5.91602163658517,
130.711524428738));
#176282=CARTESIAN_POINT('Ctrl Pts',(-18.9354908166833,5.91849424911415,
130.869092607753));
#176283=CARTESIAN_POINT('Ctrl Pts',(-18.9280825970168,5.91466587953959,
131.026656516571));
#176284=CARTESIAN_POINT('Ctrl Pts',(-18.9206743773503,5.90457866351184,
131.183677594382));
#176285=CARTESIAN_POINT('Ctrl Pts',(-18.9132615980483,5.89448523897093,
131.340795316047));
#176286=CARTESIAN_POINT('Ctrl Pts',(-18.9058488187462,5.87812533065798,
131.497369170545));
#176287=CARTESIAN_POINT('Ctrl Pts',(-18.8984360394441,5.85559265213575,
131.65286828091));
#176288=CARTESIAN_POINT('Ctrl Pts',(-18.8910126684153,5.83302777786578,
131.808589575696));
#176289=CARTESIAN_POINT('Ctrl Pts',(-18.8835892973866,5.80427258604344,
131.963232693286));
#176290=CARTESIAN_POINT('Ctrl Pts',(-18.8761659263578,5.76947152194551,
132.116278648527));
#176291=CARTESIAN_POINT('Ctrl Pts',(-18.8722298769172,5.75101916272129,
132.19742728628));
#176292=CARTESIAN_POINT('Ctrl Pts',(-18.8682938274765,5.7308679204954,132.27812717353));
#176293=CARTESIAN_POINT('Ctrl Pts',(-18.8643577780358,5.70904487533382,
132.358303079154));
#176294=CARTESIAN_POINT('Ctrl Pts',(-18.8569345116303,5.66788729323179,
132.509512334959));
#176295=CARTESIAN_POINT('Ctrl Pts',(-18.8495112452249,5.62065595438862,
132.659313963098));
#176296=CARTESIAN_POINT('Ctrl Pts',(-18.8420879788194,5.56746214607701,
132.807182580322));
#176297=CARTESIAN_POINT('Ctrl Pts',(-18.8346734860984,5.51433120842935,
132.954876429122));
#176298=CARTESIAN_POINT('Ctrl Pts',(-18.8272589933775,5.45525195381932,
133.100641466801));
#176299=CARTESIAN_POINT('Ctrl Pts',(-18.8198445006565,5.39038620852657,
133.24396449636));
#176300=CARTESIAN_POINT('Ctrl Pts',(-18.8124371543027,5.32558298328118,
133.387149385787));
#176301=CARTESIAN_POINT('Ctrl Pts',(-18.8050298079489,5.25500452342057,
133.527896615039));
#176302=CARTESIAN_POINT('Ctrl Pts',(-18.7976224615952,5.17886175452877,
133.665710209975));
#176303=CARTESIAN_POINT('Ctrl Pts',(-18.7902206399198,5.10277577578681,
133.803421018332));
#176304=CARTESIAN_POINT('Ctrl Pts',(-18.7828188182444,5.02113393111676,
133.938202223669));
#176305=CARTESIAN_POINT('Ctrl Pts',(-18.775416996569,4.93419429630813,134.069579937731));
#176306=CARTESIAN_POINT('Ctrl Pts',(-18.7680190822576,4.84730055625585,
134.200888298521));
#176307=CARTESIAN_POINT('Ctrl Pts',(-18.7606211679462,4.7551148012385,134.328796435686));
#176308=CARTESIAN_POINT('Ctrl Pts',(-18.7532232536348,4.65793981954055,
134.452857184652));
#176309=CARTESIAN_POINT('Ctrl Pts',(-18.7458265687226,4.56078098656177,
134.576897316972));
#176310=CARTESIAN_POINT('Ctrl Pts',(-18.7384298838105,4.4586348024227,134.697091036458));
#176311=CARTESIAN_POINT('Ctrl Pts',(-18.7310331988983,4.3518460191663,134.813022088427));
#176312=CARTESIAN_POINT('Ctrl Pts',(-18.7236368419628,4.24506197103646,
134.928947999892));
#176313=CARTESIAN_POINT('Ctrl Pts',(-18.7162404850274,4.13363598601705,
135.040611345094));
#176314=CARTESIAN_POINT('Ctrl Pts',(-18.7088441280919,4.0179513735731,135.14763096629));
#176315=CARTESIAN_POINT('Ctrl Pts',(-18.7014466387554,3.90224904951965,
135.254666972462));
#176316=CARTESIAN_POINT('Ctrl Pts',(-18.6940491494187,3.78228707385151,
135.357057585485));
#176317=CARTESIAN_POINT('Ctrl Pts',(-18.6866516600822,3.65848356752733,
135.454460460433));
#176318=CARTESIAN_POINT('Ctrl Pts',(-18.6792515775672,3.53463666207592,
135.551897479808));
#176319=CARTESIAN_POINT('Ctrl Pts',(-18.6718514950523,3.40694583801266,
135.644343049292));
#176320=CARTESIAN_POINT('Ctrl Pts',(-18.6644514125373,3.27585991636076,
135.731496943149));
#176321=CARTESIAN_POINT('Ctrl Pts',(-18.6570431928708,3.14462985226186,
135.818746671672));
#176322=CARTESIAN_POINT('Ctrl Pts',(-18.6496349732043,3.00999754606355,
135.900692897353));
#176323=CARTESIAN_POINT('Ctrl Pts',(-18.6422267535379,2.87243887957627,
135.977079964834));
#176324=CARTESIAN_POINT('Ctrl Pts',(-18.6348139742358,2.73479554802506,
136.05351404728));
#176325=CARTESIAN_POINT('Ctrl Pts',(-18.6274011949337,2.59422259977726,
136.124381985966));
#176326=CARTESIAN_POINT('Ctrl Pts',(-18.6199884156316,2.45121733113151,
136.189475672796));
#176327=CARTESIAN_POINT('Ctrl Pts',(-18.6125650446028,2.30800772985163,
136.254662368538));
#176328=CARTESIAN_POINT('Ctrl Pts',(-18.6051416735741,2.1623592117385,136.314058193694));
#176329=CARTESIAN_POINT('Ctrl Pts',(-18.5977183025454,2.01478648989958,
136.367504150014));
#176330=CARTESIAN_POINT('Ctrl Pts',(-18.5937822531046,1.9365398918211,136.395842478473));
#176331=CARTESIAN_POINT('Ctrl Pts',(-18.5898462036637,1.85775255249047,
136.42250892794));
#176332=CARTESIAN_POINT('Ctrl Pts',(-18.5859101542229,1.77850240341984,
136.44748561738));
#176333=CARTESIAN_POINT('Ctrl Pts',(-18.5784868878175,1.62903909558629,
136.494590874169));
#176334=CARTESIAN_POINT('Ctrl Pts',(-18.571063621412,1.47747705089621,136.535825250256));
#176335=CARTESIAN_POINT('Ctrl Pts',(-18.5636403550066,1.32431844264458,
136.570998392298));
#176336=CARTESIAN_POINT('Ctrl Pts',(-18.5562258622856,1.17134085514886,
136.606129962608));
#176337=CARTESIAN_POINT('Ctrl Pts',(-18.5488113695646,1.01677082046078,
136.635214475868));
#176338=CARTESIAN_POINT('Ctrl Pts',(-18.5413968768436,0.861127576809288,
136.658110685596));
#176339=CARTESIAN_POINT('Ctrl Pts',(-18.5339895304898,0.705634347975893,
136.680984827095));
#176340=CARTESIAN_POINT('Ctrl Pts',(-18.526582184136,0.549070336308056,
136.697682485281));
#176341=CARTESIAN_POINT('Ctrl Pts',(-18.5191748377823,0.391966829328503,
136.708113031684));
#176342=CARTESIAN_POINT('Ctrl Pts',(-18.5117730161069,0.234980496071408,
136.718535798592));
#176343=CARTESIAN_POINT('Ctrl Pts',(-18.5043711944314,0.0774558395621827,
136.722700736153));
#176344=CARTESIAN_POINT('Ctrl Pts',(-18.496969372756,-0.0800689483216963,
136.720568822659));
#176345=CARTESIAN_POINT('Ctrl Pts',(-18.4895714584446,-0.237510580095773,
136.718438034587));
#176346=CARTESIAN_POINT('Ctrl Pts',(-18.4821735441333,-0.394951970787518,
136.710017020522));
#176347=CARTESIAN_POINT('Ctrl Pts',(-18.474775629822,-0.551853243714099,
136.695318821449));
#176348=CARTESIAN_POINT('Ctrl Pts',(-18.4673789449098,-0.708728442495824,
136.680623064951));
#176349=CARTESIAN_POINT('Ctrl Pts',(-18.4599822599976,-0.86506333034826,
136.659652228581));
#176350=CARTESIAN_POINT('Ctrl Pts',(-18.4525855750854,-1.02032135351922,
136.632471366175));
#176351=CARTESIAN_POINT('Ctrl Pts',(-18.4451892181499,-1.17557249238673,
136.605291708997));
#176352=CARTESIAN_POINT('Ctrl Pts',(-18.4377928612145,-1.32974649380934,
136.571902637663));
#176353=CARTESIAN_POINT('Ctrl Pts',(-18.430396504279,-1.48231549085407,
136.532420616211));
#176354=CARTESIAN_POINT('Ctrl Pts',(-18.4229990149425,-1.63490784660174,
136.492932549961));
#176355=CARTESIAN_POINT('Ctrl Pts',(-18.415601525606,-1.78589434727353,
136.4473497697));
#176356=CARTESIAN_POINT('Ctrl Pts',(-18.4082040362694,-1.9347609637968,
136.395839006639));
#176357=CARTESIAN_POINT('Ctrl Pts',(-18.4008039537544,-2.08367976528151,
136.344310186559));
#176358=CARTESIAN_POINT('Ctrl Pts',(-18.3934038712394,-2.23047685051118,
136.286849368298));
#176359=CARTESIAN_POINT('Ctrl Pts',(-18.3860037887244,-2.37465703234387,
136.223671878348));
#176360=CARTESIAN_POINT('Ctrl Pts',(-18.378595569058,-2.51899575510878,
136.160424918253));
#176361=CARTESIAN_POINT('Ctrl Pts',(-18.3711873493915,-2.66071148568839,
136.091448882692));
#176362=CARTESIAN_POINT('Ctrl Pts',(-18.3637791297251,-2.79933190824786,
136.017005956544));
#176363=CARTESIAN_POINT('Ctrl Pts',(-18.356366350423,-2.93803764936441,
135.942517212017));
#176364=CARTESIAN_POINT('Ctrl Pts',(-18.348953571121,-3.07364396547769,
135.862555061328));
#176365=CARTESIAN_POINT('Ctrl Pts',(-18.341540791819,-3.20570696855736,
135.77742540643));
#176366=CARTESIAN_POINT('Ctrl Pts',(-18.3341174207902,-3.33795866944916,
135.692174114289));
#176367=CARTESIAN_POINT('Ctrl Pts',(-18.3266940497614,-3.46665664103307,
135.601740785341));
#176368=CARTESIAN_POINT('Ctrl Pts',(-18.3192706787326,-3.59138889857157,
135.506472519862));
#176369=CARTESIAN_POINT('Ctrl Pts',(-18.3153346292918,-3.65752493442915,
135.455958999574));
#176370=CARTESIAN_POINT('Ctrl Pts',(-18.3113985798509,-3.72254665499518,
135.404086846922));
#176371=CARTESIAN_POINT('Ctrl Pts',(-18.30746253041,-3.78639689256382,135.35091196276));
#176372=CARTESIAN_POINT('Ctrl Pts',(-18.3001424141559,-3.9051431555055,
135.252019319332));
#176373=CARTESIAN_POINT('Ctrl Pts',(-18.2928222979017,-4.02021616790234,
135.148301554346));
#176374=CARTESIAN_POINT('Ctrl Pts',(-18.2855021816476,-4.13119046426338,
135.040065507012));
#176375=CARTESIAN_POINT('Ctrl Pts',(-18.2781907686664,-4.24203281742192,
134.931958147232));
#176376=CARTESIAN_POINT('Ctrl Pts',(-18.2708793556851,-4.34878587753108,
134.819343458631));
#176377=CARTESIAN_POINT('Ctrl Pts',(-18.2635679427039,-4.45105574861657,
134.702569601857));
#176378=CARTESIAN_POINT('Ctrl Pts',(-18.2562635213531,-4.55322782285328,
134.585907411551));
#176379=CARTESIAN_POINT('Ctrl Pts',(-18.2489591000023,-4.65092498734133,
134.465094254707));
#176380=CARTESIAN_POINT('Ctrl Pts',(-18.2416546786515,-4.74378905259512,
134.34051615529));
#176381=CARTESIAN_POINT('Ctrl Pts',(-18.2342263667162,-4.8382281889974,
134.213825081716));
#176382=CARTESIAN_POINT('Ctrl Pts',(-18.226798054781,-4.92766849113517,
134.083240461263));
#176383=CARTESIAN_POINT('Ctrl Pts',(-18.2193697428457,-5.01177438429781,
133.949205301075));
#176384=CARTESIAN_POINT('Ctrl Pts',(-18.212073836435,-5.09438113673903,
133.817559242996));
#176385=CARTESIAN_POINT('Ctrl Pts',(-18.2047779300244,-5.17184184502397,
133.682584966104));
#176386=CARTESIAN_POINT('Ctrl Pts',(-18.1974820236138,-5.24388129092448,
133.544732776451));
#176387=CARTESIAN_POINT('Ctrl Pts',(-18.1901875500544,-5.31590658891714,
133.406907659745));
#176388=CARTESIAN_POINT('Ctrl Pts',(-18.1828930764951,-5.38251256475605,
133.266206095432));
#176389=CARTESIAN_POINT('Ctrl Pts',(-18.1755986029358,-5.4434696449894,
133.123103549971));
#176390=CARTESIAN_POINT('Ctrl Pts',(-18.1683040281309,-5.50442757129209,
132.979999018282));
#176391=CARTESIAN_POINT('Ctrl Pts',(-18.161009453326,-5.55973629600026,
132.834493793265));
#176392=CARTESIAN_POINT('Ctrl Pts',(-18.1537148785212,-5.60921426509306,
132.687083616516));
#176393=CARTESIAN_POINT('Ctrl Pts',(-18.1461865713281,-5.66027760470986,
132.534950130517));
#176394=CARTESIAN_POINT('Ctrl Pts',(-18.138658264135,-5.70513013885221,
132.380787987925));
#176395=CARTESIAN_POINT('Ctrl Pts',(-18.1311299569419,-5.7436280871913,
132.225158618172));
#176396=CARTESIAN_POINT('Ctrl Pts',(-18.1238273542451,-5.78097183714094,
132.07419513779));
#176397=CARTESIAN_POINT('Ctrl Pts',(-18.1165247515484,-5.81233652687398,
131.921851535299));
#176398=CARTESIAN_POINT('Ctrl Pts',(-18.1092221488516,-5.83764314806235,
131.768649494605));
#176399=CARTESIAN_POINT('Ctrl Pts',(-18.1015809894104,-5.86412301222138,
131.608344837722));
#176400=CARTESIAN_POINT('Ctrl Pts',(-18.0939398299692,-5.88396960496991,
131.447100723953));
#176401=CARTESIAN_POINT('Ctrl Pts',(-18.086298670528,-5.89715334372373,
131.285518599011));
#176402=CARTESIAN_POINT('Ctrl Pts',(-18.0786575110868,-5.91033708247756,
131.123936474068));
#176403=CARTESIAN_POINT('Ctrl Pts',(-18.0710163516455,-5.91685801118231,
130.962016816047));
#176404=CARTESIAN_POINT('Ctrl Pts',(-18.0633751922043,-5.91674864602274,
130.800357832532));
#176405=CARTESIAN_POINT('',(-16.3133751922043,-5.92097783986537,130.809153648924));
#176406=CARTESIAN_POINT('Ctrl Pts',(-18.0633751922043,-5.92301518338556,
130.800353593109));
#176407=CARTESIAN_POINT('Ctrl Pts',(-18.0519217636686,-5.92489819397444,
130.557782917589));
#176408=CARTESIAN_POINT('Ctrl Pts',(-17.9476524605274,-5.80104331945593,
128.351415487931));
#176409=CARTESIAN_POINT('Ctrl Pts',(-17.7505672827852,-3.02951815479332,
124.495669764465));
#176410=CARTESIAN_POINT('Ctrl Pts',(-17.4721196589708,3.6701517233714,124.845539689074));
#176411=CARTESIAN_POINT('Ctrl Pts',(-17.1936720351586,6.99713146463687,
130.671274942398));
#176412=CARTESIAN_POINT('Ctrl Pts',(-16.9152244113454,3.89408921877592,
136.619309429597));
#176413=CARTESIAN_POINT('Ctrl Pts',(-16.6367767875328,-2.78743078230602,
137.223690034585));
#176414=CARTESIAN_POINT('Ctrl Pts',(-16.4361603811523,-5.75582047298202,
133.408977741301));
#176415=CARTESIAN_POINT('Ctrl Pts',(-16.3283598493761,-5.92377094759506,
131.126796202098));
#176416=CARTESIAN_POINT('Ctrl Pts',(-16.3133751922043,-5.92097783986537,
130.809153648924));
#176417=CARTESIAN_POINT('',(-14.5633751922042,-5.90740060865866,130.806092547028));
#176418=CARTESIAN_POINT('Ctrl Pts',(-16.3133751922043,-5.92097783986537,
130.809153648924));
#176419=CARTESIAN_POINT('Ctrl Pts',(-16.2355439747718,-5.90647026905285,
129.159298978353));
#176420=CARTESIAN_POINT('Ctrl Pts',(-16.064896882735,-4.32853530421092,
125.517624031903));
#176421=CARTESIAN_POINT('Ctrl Pts',(-15.8014339160941,1.84829460391826,
124.054444500495));
#176422=CARTESIAN_POINT('Ctrl Pts',(-15.522986292281,6.67794397737314,128.710888677124));
#176423=CARTESIAN_POINT('Ctrl Pts',(-15.2445386684683,5.37088907132037,
135.291131295225));
#176424=CARTESIAN_POINT('Ctrl Pts',(-14.9660910446553,-0.871750508755442,
137.748250851493));
#176425=CARTESIAN_POINT('Ctrl Pts',(-14.7390365525673,-5.30894723277776,
134.548523582037));
#176426=CARTESIAN_POINT('Ctrl Pts',(-14.6047979350836,-5.90970731248103,
131.689299166102));
#176427=CARTESIAN_POINT('Ctrl Pts',(-14.5633751922042,-5.90740060865866,
130.806092547028));
#176428=CARTESIAN_POINT('',(-12.8133751922043,-5.9146051397711,130.798967998767));
#176429=CARTESIAN_POINT('Ctrl Pts',(-14.5633751922042,-5.90740060865866,
130.806092547028));
#176430=CARTESIAN_POINT('Ctrl Pts',(-14.5119820604793,-5.90453868486625,
129.710299488454));
#176431=CARTESIAN_POINT('Ctrl Pts',(-14.3677730541501,-5.08582181367531,
126.631532353636));
#176432=CARTESIAN_POINT('Ctrl Pts',(-14.1307481732166,-0.122437078091865,
123.80703472175));
#176433=CARTESIAN_POINT('Ctrl Pts',(-13.8523005494037,5.82086821931613,
126.919125270293));
#176434=CARTESIAN_POINT('Ctrl Pts',(-13.5738529255909,6.41507998839504,
133.601557298682));
#176435=CARTESIAN_POINT('Ctrl Pts',(-13.2954053017781,1.11414664221958,
137.713502227777));
#176436=CARTESIAN_POINT('Ctrl Pts',(-13.0419127239824,-4.643793337457,135.676787665054));
#176437=CARTESIAN_POINT('Ctrl Pts',(-12.8812360207912,-5.90184908491918,
132.241450451055));
#176438=CARTESIAN_POINT('Ctrl Pts',(-12.8133751922043,-5.9146051397711,
130.798967998767));
#176439=CARTESIAN_POINT('',(-11.0633751922043,-5.92207844733352,130.804950250625));
#176440=CARTESIAN_POINT('Ctrl Pts',(-12.8133751922043,-5.9146051397711,
130.798967998767));
#176441=CARTESIAN_POINT('Ctrl Pts',(-12.7884201461869,-5.91929603350845,
130.268511522982));
#176442=CARTESIAN_POINT('Ctrl Pts',(-12.6706492255654,-5.61047757032242,
127.770484247143));
#176443=CARTESIAN_POINT('Ctrl Pts',(-12.4600624303391,-2.08330682229084,
124.123238465223));
#176444=CARTESIAN_POINT('Ctrl Pts',(-12.1816148065263,4.49493906093286,
125.440305866834));
#176445=CARTESIAN_POINT('Ctrl Pts',(-11.9031671827135,6.94255553713972,
131.686677535726));
#176446=CARTESIAN_POINT('Ctrl Pts',(-11.6247195589006,3.01030263740934,
137.122243060405));
#176447=CARTESIAN_POINT('Ctrl Pts',(-11.3462719350876,-3.6882713246427,
136.751983265833));
#176448=CARTESIAN_POINT('Ctrl Pts',(-11.159157146189,-5.91205182492537,
132.830344731594));
#176449=CARTESIAN_POINT('Ctrl Pts',(-11.0648582318944,-5.92650494164408,
130.836311522113));
#176450=CARTESIAN_POINT('Ctrl Pts',(-11.0633751922043,-5.92646057751854,
130.804950686933));
#176451=CARTESIAN_POINT('',(-9.31337521180815,-5.91431177079138,130.809468401107));
#176452=CARTESIAN_POINT('Ctrl Pts',(-11.0633751922043,-5.91674997067294,
130.804949720094));
#176453=CARTESIAN_POINT('Ctrl Pts',(-11.0559725385279,-5.91676553096338,
130.648667335256));
#176454=CARTESIAN_POINT('Ctrl Pts',(-11.0485698848515,-5.91058485695991,
130.492142119407));
#176455=CARTESIAN_POINT('Ctrl Pts',(-11.0411672311751,-5.89817619223044,
130.33590766592));
#176456=CARTESIAN_POINT('Ctrl Pts',(-11.0337733149295,-5.88578217357992,
130.17985761762));
#176457=CARTESIAN_POINT('Ctrl Pts',(-11.026379398684,-5.86717482433238,
130.024098019341));
#176458=CARTESIAN_POINT('Ctrl Pts',(-11.0189854824384,-5.8423743511813,
129.869164112462));
#176459=CARTESIAN_POINT('Ctrl Pts',(-11.0115986568399,-5.81759766128598,
129.714378784714));
#176460=CARTESIAN_POINT('Ctrl Pts',(-11.0042118312414,-5.78663972892824,
129.56041794053));
#176461=CARTESIAN_POINT('Ctrl Pts',(-10.9968250056428,-5.74957266881999,
129.407813200377));
#176462=CARTESIAN_POINT('Ctrl Pts',(-10.9894436296807,-5.71253295496425,
129.25532104449));
#176463=CARTESIAN_POINT('Ctrl Pts',(-10.9820622537184,-5.66939317491942,
129.104183364184));
#176464=CARTESIAN_POINT('Ctrl Pts',(-10.9746808777562,-5.62027675265298,
128.954922922998));
#176465=CARTESIAN_POINT('Ctrl Pts',(-10.9669598698273,-5.56890038492651,
128.798794708451));
#176466=CARTESIAN_POINT('Ctrl Pts',(-10.9592388618985,-5.51098439803554,
128.644721000573));
#176467=CARTESIAN_POINT('Ctrl Pts',(-10.9515178539696,-5.44672909903955,
128.493284529642));
#176468=CARTESIAN_POINT('Ctrl Pts',(-10.9441414338751,-5.38534150780139,
128.34860665371));
#176469=CARTESIAN_POINT('Ctrl Pts',(-10.9367650137806,-5.31816835142111,
128.206336096069));
#176470=CARTESIAN_POINT('Ctrl Pts',(-10.9293885936862,-5.24543405326975,
128.066961823949));
#176471=CARTESIAN_POINT('Ctrl Pts',(-10.9220123116993,-5.17270111691086,
127.92759016131));
#176472=CARTESIAN_POINT('Ctrl Pts',(-10.9146360297123,-5.0944074193427,
127.791115009524));
#176473=CARTESIAN_POINT('Ctrl Pts',(-10.9072597477254,-5.01082368071441,
127.658001355929));
#176474=CARTESIAN_POINT('Ctrl Pts',(-10.8998821260389,-4.92722476138972,
127.524863525884));
#176475=CARTESIAN_POINT('Ctrl Pts',(-10.8925045043525,-4.83833408803295,
127.395088727551));
#176476=CARTESIAN_POINT('Ctrl Pts',(-10.885126882666,-4.74446599590369,
127.269113387709));
#176477=CARTESIAN_POINT('Ctrl Pts',(-10.8777464429199,-4.65056204860439,
127.143089928563));
#176478=CARTESIAN_POINT('Ctrl Pts',(-10.8703660031739,-4.55167712190346,
127.020869117988));
#176479=CARTESIAN_POINT('Ctrl Pts',(-10.8629855634278,-4.4481660206591,
126.90285454745));
#176480=CARTESIAN_POINT('Ctrl Pts',(-10.8555969500128,-4.34454028322792,
126.784709278463));
#176481=CARTESIAN_POINT('Ctrl Pts',(-10.8482083365977,-4.23627838943202,
126.670779832888));
#176482=CARTESIAN_POINT('Ctrl Pts',(-10.8408197231827,-4.12377266546004,
126.561433612997));
#176483=CARTESIAN_POINT('Ctrl Pts',(-10.8334263149394,-4.01119393108678,
126.452016433059));
#176484=CARTESIAN_POINT('Ctrl Pts',(-10.8260329066962,-3.89436615855799,
126.34718865428));
#176485=CARTESIAN_POINT('Ctrl Pts',(-10.8186394984529,-3.77371450048516,
126.24727718281));
#176486=CARTESIAN_POINT('Ctrl Pts',(-10.8112359444123,-3.65289727502847,
126.147228605218));
#176487=CARTESIAN_POINT('Ctrl Pts',(-10.8038323903717,-3.52824598511995,
126.052110030891));
#176488=CARTESIAN_POINT('Ctrl Pts',(-10.7964288363311,-3.40021498322093,
125.96220524724));
#176489=CARTESIAN_POINT('Ctrl Pts',(-10.7940781200414,-3.35956362036101,
125.93365941124));
#176490=CARTESIAN_POINT('Ctrl Pts',(-10.7917274037517,-3.31857172301088,
125.905638850208));
#176491=CARTESIAN_POINT('Ctrl Pts',(-10.7893766874619,-3.27725432932366,
125.878151667123));
#176492=CARTESIAN_POINT('Ctrl Pts',(-10.7819534210565,-3.14677919633695,
125.791350599861));
#176493=CARTESIAN_POINT('Ctrl Pts',(-10.7745301546511,-3.01265587994184,
125.709605488931));
#176494=CARTESIAN_POINT('Ctrl Pts',(-10.7671068882456,-2.87531383550085,
125.633238794414));
#176495=CARTESIAN_POINT('Ctrl Pts',(-10.7596923955246,-2.73813411795046,
125.556962358988));
#176496=CARTESIAN_POINT('Ctrl Pts',(-10.7522779028036,-2.59774356784212,
125.486051866285));
#176497=CARTESIAN_POINT('Ctrl Pts',(-10.7448634100826,-2.45460168509987,
125.420787349744));
#176498=CARTESIAN_POINT('Ctrl Pts',(-10.7374560637288,-2.31159776789361,
125.355585737602));
#176499=CARTESIAN_POINT('Ctrl Pts',(-10.7300487173751,-2.16584813471945,
125.296019421885));
#176500=CARTESIAN_POINT('Ctrl Pts',(-10.7226413710213,-2.017837932274,125.242323163397));
#176501=CARTESIAN_POINT('Ctrl Pts',(-10.7152395493459,-1.86993812142143,
125.188666953605));
#176502=CARTESIAN_POINT('Ctrl Pts',(-10.7078377276705,-1.71978144779477,
125.140872210394));
#176503=CARTESIAN_POINT('Ctrl Pts',(-10.7004359059951,-1.56787403763929,
125.099126041793));
#176504=CARTESIAN_POINT('Ctrl Pts',(-10.6930379916837,-1.41604681822383,
125.05740191067));
#176505=CARTESIAN_POINT('Ctrl Pts',(-10.6856400773724,-1.26247106191039,
125.021720093822));
#176506=CARTESIAN_POINT('Ctrl Pts',(-10.678242163061,-1.10766898746678,
124.992218157448));
#176507=CARTESIAN_POINT('Ctrl Pts',(-10.6708454781488,-0.952892638319105,
124.96272112376));
#176508=CARTESIAN_POINT('Ctrl Pts',(-10.6634487932367,-0.796890741846708,
124.939402002103));
#176509=CARTESIAN_POINT('Ctrl Pts',(-10.6560521083244,-0.640196785166688,
124.922347472497));
#176510=CARTESIAN_POINT('Ctrl Pts',(-10.648655751389,-0.483509776461135,
124.905293699108));
#176511=CARTESIAN_POINT('Ctrl Pts',(-10.6412593944536,-0.326131139669395,
124.894504005844));
#176512=CARTESIAN_POINT('Ctrl Pts',(-10.6338630375182,-0.168600310285228,
124.890013274209));
#176513=CARTESIAN_POINT('Ctrl Pts',(-10.6264655481816,-0.0110453625287005,
124.885521855032));
#176514=CARTESIAN_POINT('Ctrl Pts',(-10.619068058845,0.146661451045509,
124.887331328345));
#176515=CARTESIAN_POINT('Ctrl Pts',(-10.6116705695084,0.303980012317705,
124.895424443041));
#176516=CARTESIAN_POINT('Ctrl Pts',(-10.6042704869934,0.461353721367905,
124.903520394766));
#176517=CARTESIAN_POINT('Ctrl Pts',(-10.5968704044785,0.61833853456716,
124.917904354309));
#176518=CARTESIAN_POINT('Ctrl Pts',(-10.5894703219635,0.774398922773036,
124.938507152732));
#176519=CARTESIAN_POINT('Ctrl Pts',(-10.582062102297,0.930630915418698,
124.959132606049));
#176520=CARTESIAN_POINT('Ctrl Pts',(-10.5746538826305,1.08593608273927,
124.985990505799));
#176521=CARTESIAN_POINT('Ctrl Pts',(-10.567245662964,1.23978783797754,125.018960313412));
#176522=CARTESIAN_POINT('Ctrl Pts',(-10.559832883662,1.39373428640401,125.051950413392));
#176523=CARTESIAN_POINT('Ctrl Pts',(-10.55242010436,1.54622517948682,125.091059824526));
#176524=CARTESIAN_POINT('Ctrl Pts',(-10.5450073250579,1.69674908362636,
125.136118111311));
#176525=CARTESIAN_POINT('Ctrl Pts',(-10.5375839540292,1.84748806337922,
125.181240779489));
#176526=CARTESIAN_POINT('Ctrl Pts',(-10.5301605830004,1.99625408881397,
125.232329178865));
#176527=CARTESIAN_POINT('Ctrl Pts',(-10.5227372119717,2.14255491820914,
125.289164430216));
#176528=CARTESIAN_POINT('Ctrl Pts',(-10.5188011625308,2.22012712839686,
125.319299844227));
#176529=CARTESIAN_POINT('Ctrl Pts',(-10.5148651130899,2.29700667109292,
125.351050124242));
#176530=CARTESIAN_POINT('Ctrl Pts',(-10.510929063649,2.37312309110805,125.384377466582));
#176531=CARTESIAN_POINT('Ctrl Pts',(-10.5035057972436,2.51667628374082,
125.447231794123));
#176532=CARTESIAN_POINT('Ctrl Pts',(-10.4960825308381,2.65794768936465,
125.515888309583));
#176533=CARTESIAN_POINT('Ctrl Pts',(-10.4886592644326,2.79643388206537,
125.590159997554));
#176534=CARTESIAN_POINT('Ctrl Pts',(-10.4812447717116,2.93475639558649,
125.664343902557));
#176535=CARTESIAN_POINT('Ctrl Pts',(-10.4738302789907,3.07029992295007,
125.744129595039));
#176536=CARTESIAN_POINT('Ctrl Pts',(-10.4664157862697,3.20258049315985,
125.829281849613));
#176537=CARTESIAN_POINT('Ctrl Pts',(-10.4590084399159,3.33473356637598,
125.914352031239));
#176538=CARTESIAN_POINT('Ctrl Pts',(-10.4516010935622,3.46362963165732,
126.00477827684));
#176539=CARTESIAN_POINT('Ctrl Pts',(-10.4441937472084,3.58880894445214,
126.100279312707));
#176540=CARTESIAN_POINT('Ctrl Pts',(-10.436791925533,3.71389489379274,126.195709120299));
#176541=CARTESIAN_POINT('Ctrl Pts',(-10.4293901038576,3.8352693147493,126.296205956322));
#176542=CARTESIAN_POINT('Ctrl Pts',(-10.4219882821822,3.95250121443982,
126.401445138891));
#176543=CARTESIAN_POINT('Ctrl Pts',(-10.4145903678708,4.06967122832319,
126.506628766516));
#176544=CARTESIAN_POINT('Ctrl Pts',(-10.4071924535595,4.18270279898259,
126.616549506211));
#176545=CARTESIAN_POINT('Ctrl Pts',(-10.3997945392481,4.29119791608063,
126.730842358429));
#176546=CARTESIAN_POINT('Ctrl Pts',(-10.3923978543359,4.39967500325837,
126.845116217247));
#176547=CARTESIAN_POINT('Ctrl Pts',(-10.3850011694237,4.50361687634247,
126.963760476095));
#176548=CARTESIAN_POINT('Ctrl Pts',(-10.3776044845115,4.60266224615703,
127.086373149822));
#176549=CARTESIAN_POINT('Ctrl Pts',(-10.3702081275761,4.70170322419625,
127.208980386774));
#176550=CARTESIAN_POINT('Ctrl Pts',(-10.3628117706406,4.79584789609205,
127.33555539834));
#176551=CARTESIAN_POINT('Ctrl Pts',(-10.3554154137051,4.88477533698727,
127.465663196466));
#176552=CARTESIAN_POINT('Ctrl Pts',(-10.3480179243686,4.97371639290084,
127.595790914427));
#176553=CARTESIAN_POINT('Ctrl Pts',(-10.340620435032,5.05743841669607,127.729452187701));
#176554=CARTESIAN_POINT('Ctrl Pts',(-10.3332229456954,5.13566397518045,
127.866183274972));
#176555=CARTESIAN_POINT('Ctrl Pts',(-10.3258228631804,5.21391695551287,
128.002962293113));
#176556=CARTESIAN_POINT('Ctrl Pts',(-10.3184227806654,5.28666944907581,
128.142812943979));
#176557=CARTESIAN_POINT('Ctrl Pts',(-10.3110226981504,5.3536901830731,128.285247284235));
#176558=CARTESIAN_POINT('Ctrl Pts',(-10.3036144784839,5.42078461325731,
128.427838245691));
#176559=CARTESIAN_POINT('Ctrl Pts',(-10.2962062588175,5.48213453801958,
128.573018232284));
#176560=CARTESIAN_POINT('Ctrl Pts',(-10.288798039151,5.53755673686508,128.720279057622));
#176561=CARTESIAN_POINT('Ctrl Pts',(-10.2813852598489,5.59301304714952,
128.867630519541));
#176562=CARTESIAN_POINT('Ctrl Pts',(-10.2739724805468,5.64253424443491,
129.017065018678));
#176563=CARTESIAN_POINT('Ctrl Pts',(-10.2665597012447,5.6859872785842,129.168060146907));
#176564=CARTESIAN_POINT('Ctrl Pts',(-10.2591363302159,5.72950240046618,
129.319271024056));
#176565=CARTESIAN_POINT('Ctrl Pts',(-10.2517129591872,5.76693195373218,
129.472046622293));
#176566=CARTESIAN_POINT('Ctrl Pts',(-10.2442895881585,5.79819401899688,
129.625854495151));
#176567=CARTESIAN_POINT('Ctrl Pts',(-10.2403535387177,5.81476991612321,
129.70740711991));
#176568=CARTESIAN_POINT('Ctrl Pts',(-10.2364174892769,5.82961277704559,
129.789249858412));
#176569=CARTESIAN_POINT('Ctrl Pts',(-10.2324814398361,5.84271632432023,
129.871303000898));
#176570=CARTESIAN_POINT('Ctrl Pts',(-10.2250581734307,5.86742920553252,
130.026052666836));
#176571=CARTESIAN_POINT('Ctrl Pts',(-10.2176349070252,5.88602718010824,
130.182018825036));
#176572=CARTESIAN_POINT('Ctrl Pts',(-10.2102116406198,5.89839547540299,
130.338676842623));
#176573=CARTESIAN_POINT('Ctrl Pts',(-10.2027971478988,5.91074915239983,
130.495149703442));
#176574=CARTESIAN_POINT('Ctrl Pts',(-10.1953826551778,5.91688777704139,
130.652312427466));
#176575=CARTESIAN_POINT('Ctrl Pts',(-10.1879681624568,5.91674765296144,
130.809630691122));
#176576=CARTESIAN_POINT('Ctrl Pts',(-10.180560816103,5.91660766393836,130.966797325512));
#176577=CARTESIAN_POINT('Ctrl Pts',(-10.1731534697492,5.91020097425619,
131.12411883029));
#176578=CARTESIAN_POINT('Ctrl Pts',(-10.1657461233955,5.89751572429131,
131.281056374036));
#176579=CARTESIAN_POINT('Ctrl Pts',(-10.1583443017201,5.8848399354645,131.43787686784));
#176580=CARTESIAN_POINT('Ctrl Pts',(-10.1509424800447,5.86589494036225,
131.594313600335));
#176581=CARTESIAN_POINT('Ctrl Pts',(-10.1435406583693,5.84072094086921,
131.749828466513));
#176582=CARTESIAN_POINT('Ctrl Pts',(-10.136142744058,5.81556023053434,131.905261237605));
#176583=CARTESIAN_POINT('Ctrl Pts',(-10.1287448297466,5.78417712400211,
132.05977274399));
#176584=CARTESIAN_POINT('Ctrl Pts',(-10.1213469154352,5.74666357142174,
132.212830837128));
#176585=CARTESIAN_POINT('Ctrl Pts',(-10.113950230523,5.70915625291342,132.365863494788));
#176586=CARTESIAN_POINT('Ctrl Pts',(-10.1065535456107,5.66552059908761,
132.517442856355));
#176587=CARTESIAN_POINT('Ctrl Pts',(-10.0991568606985,5.6158995258123,132.667047676221));
#176588=CARTESIAN_POINT('Ctrl Pts',(-10.0917605037631,5.56628065278753,
132.816645862452));
#176589=CARTESIAN_POINT('Ctrl Pts',(-10.0843641468277,5.5106770055377,132.964269326751));
#176590=CARTESIAN_POINT('Ctrl Pts',(-10.0769677898923,5.44928108410796,
133.109412944279));
#176591=CARTESIAN_POINT('Ctrl Pts',(-10.0695703005556,5.38787576280555,
133.254578783665));
#176592=CARTESIAN_POINT('Ctrl Pts',(-10.0621728112191,5.32067654700163,
133.397263676478));
#176593=CARTESIAN_POINT('Ctrl Pts',(-10.0547753218825,5.24792363598143,
133.536983546806));
#176594=CARTESIAN_POINT('Ctrl Pts',(-10.0473752393675,5.17514522154135,
133.676752395717));
#176595=CARTESIAN_POINT('Ctrl Pts',(-10.0399751568525,5.09680940804071,
133.813553821845));
#176596=CARTESIAN_POINT('Ctrl Pts',(-10.0325750743375,5.01320170743094,
133.946929503543));
#176597=CARTESIAN_POINT('Ctrl Pts',(-10.025166854671,4.92950207155915,134.080451845515));
#176598=CARTESIAN_POINT('Ctrl Pts',(-10.0177586350045,4.8405191700166,134.21054060371));
#176599=CARTESIAN_POINT('Ctrl Pts',(-10.010350415338,4.74658151925483,134.336766942378));
#176600=CARTESIAN_POINT('Ctrl Pts',(-10.002937636036,4.65258605143658,134.46307097125));
#176601=CARTESIAN_POINT('Ctrl Pts',(-9.99552485673399,4.55362999186371,
134.585507553963));
#176602=CARTESIAN_POINT('Ctrl Pts',(-9.98811207743194,4.45008094043782,
134.703682377315));
#176603=CARTESIAN_POINT('Ctrl Pts',(-9.98068870640318,4.34638393327112,
134.822026054397));
#176604=CARTESIAN_POINT('Ctrl Pts',(-9.97326533537441,4.23808108345211,
134.936095540218));
#176605=CARTESIAN_POINT('Ctrl Pts',(-9.96584196434566,4.12557607384473,
135.045534113359));
#176606=CARTESIAN_POINT('Ctrl Pts',(-9.96190591490489,4.06592321823056,
135.103561070781));
#176607=CARTESIAN_POINT('Ctrl Pts',(-9.95796986546407,4.00508953330804,
135.160286789327));
#176608=CARTESIAN_POINT('Ctrl Pts',(-9.9540338160233,3.94313868804302,135.215662902533));
#176609=CARTESIAN_POINT('Ctrl Pts',(-9.94661054961786,3.82630132729226,
135.320100523812));
#176610=CARTESIAN_POINT('Ctrl Pts',(-9.93918728321246,3.7051352407465,135.420051044737));
#176611=CARTESIAN_POINT('Ctrl Pts',(-9.93176401680702,3.58001977948435,
135.515134326948));
#176612=CARTESIAN_POINT('Ctrl Pts',(-9.924349524086,3.45505219430705,135.610105228615));
#176613=CARTESIAN_POINT('Ctrl Pts',(-9.91693503136498,3.32614482006905,
135.700220118628));
#176614=CARTESIAN_POINT('Ctrl Pts',(-9.90952053864396,3.193712768883,135.785136592489));
#176615=CARTESIAN_POINT('Ctrl Pts',(-9.90211319229019,3.06140836069405,
135.869971220656));
#176616=CARTESIAN_POINT('Ctrl Pts',(-9.89470584593635,2.92558635088209,
135.949617207303));
#176617=CARTESIAN_POINT('Ctrl Pts',(-9.88729849958258,2.78669366316633,
136.02377332305));
#176618=CARTESIAN_POINT('Ctrl Pts',(-9.87989667790721,2.64790456685758,
136.097874130368));
#176619=CARTESIAN_POINT('Ctrl Pts',(-9.87249485623189,2.50604968068134,
136.166493044531));
#176620=CARTESIAN_POINT('Ctrl Pts',(-9.86509303455651,2.36160345772091,
136.229373029624));
#176621=CARTESIAN_POINT('Ctrl Pts',(-9.85769512024507,2.21723348679515,
136.292219820863));
#176622=CARTESIAN_POINT('Ctrl Pts',(-9.85029720593362,2.07027524482308,
136.349333567877));
#176623=CARTESIAN_POINT('Ctrl Pts',(-9.84289929162219,1.9212261447454,136.400503991645));
#176624=CARTESIAN_POINT('Ctrl Pts',(-9.83550260670999,1.77220181392583,
136.451665911817));
#176625=CARTESIAN_POINT('Ctrl Pts',(-9.8281059217978,1.6210876673359,136.496886347886));
#176626=CARTESIAN_POINT('Ctrl Pts',(-9.82070923688559,1.46839949318662,
136.536003793036));
#176627=CARTESIAN_POINT('Ctrl Pts',(-9.81331287995015,1.315718089391,136.575119503677));
#176628=CARTESIAN_POINT('Ctrl Pts',(-9.80591652301471,1.16146315842902,
136.608132668826));
#176629=CARTESIAN_POINT('Ctrl Pts',(-9.79852016607927,1.00616372711077,
136.634932211908));
#176630=CARTESIAN_POINT('Ctrl Pts',(-9.7911226767427,0.850840519053114,
136.661735858068));
#176631=CARTESIAN_POINT('Ctrl Pts',(-9.78372518740613,0.694472860110188,
136.682323924469));
#176632=CARTESIAN_POINT('Ctrl Pts',(-9.77632769806957,0.537597850636254,
136.696636842718));
#176633=CARTESIAN_POINT('Ctrl Pts',(-9.76892761555455,0.380667848870265,
136.710954778338));
#176634=CARTESIAN_POINT('Ctrl Pts',(-9.76152753303949,0.223230513995242,
136.718993152237));
#176635=CARTESIAN_POINT('Ctrl Pts',(-9.75412745052446,0.0658257711749089,
136.720744439661));
#176636=CARTESIAN_POINT('Ctrl Pts',(-9.746719230858,-0.091752054341082,
136.722497652806));
#176637=CARTESIAN_POINT('Ctrl Pts',(-9.73931101119156,-0.249296842727074,
136.71794996901));
#176638=CARTESIAN_POINT('Ctrl Pts',(-9.7319027915251,-0.406270231155212,
136.707145982271));
#176639=CARTESIAN_POINT('Ctrl Pts',(-9.72449001222301,-0.563340234085357,
136.696335345859));
#176640=CARTESIAN_POINT('Ctrl Pts',(-9.71707723292087,-0.719837766041626,
136.679260773995));
#176641=CARTESIAN_POINT('Ctrl Pts',(-9.70966445361879,-0.875232383435107,
136.656018402971));
#176642=CARTESIAN_POINT('Ctrl Pts',(-9.70224108259003,-1.03084903594476,
136.632742822157));
#176643=CARTESIAN_POINT('Ctrl Pts',(-9.69481771156129,-1.18535926075348,
136.603281910697));
#176644=CARTESIAN_POINT('Ctrl Pts',(-9.68739434053253,-1.33824473757904,
136.567782481775));
#176645=CARTESIAN_POINT('Ctrl Pts',(-9.68345829109182,-1.41930828582709,
136.548959832764));
#176646=CARTESIAN_POINT('Ctrl Pts',(-9.67952224165109,-1.49991533204027,
136.528440367216));
#176647=CARTESIAN_POINT('Ctrl Pts',(-9.67558619221037,-1.5799907695123,
136.506251508381));
#176648=CARTESIAN_POINT('Ctrl Pts',(-9.66816292580495,-1.73101054551834,
136.464404013107));
#176649=CARTESIAN_POINT('Ctrl Pts',(-9.66073965939949,-1.88059497894224,
136.416489250882));
#176650=CARTESIAN_POINT('Ctrl Pts',(-9.65331639299407,-2.02821920009124,
136.362620906441));
#176651=CARTESIAN_POINT('Ctrl Pts',(-9.64590190027308,-2.17566894167027,
136.308816229909));
#176652=CARTESIAN_POINT('Ctrl Pts',(-9.63848740755215,-2.32116273533804,
136.249072104348));
#176653=CARTESIAN_POINT('Ctrl Pts',(-9.63107291483115,-2.4641881282552,
136.183552697337));
#176654=CARTESIAN_POINT('Ctrl Pts',(-9.62366556847732,-2.60707566791507,
136.118096440396));
#176655=CARTESIAN_POINT('Ctrl Pts',(-9.61625822212349,-2.7474992061147,
136.046876138106));
#176656=CARTESIAN_POINT('Ctrl Pts',(-9.60885087576966,-2.88496373685656,
135.97010497821));
#176657=CARTESIAN_POINT('Ctrl Pts',(-9.60144905409428,-3.02232574136377,
135.893391077142));
#176658=CARTESIAN_POINT('Ctrl Pts',(-9.59404723241887,-3.15673280821445,
135.811134743078));
#176659=CARTESIAN_POINT('Ctrl Pts',(-9.5866454107435,-3.2877122323319,135.723596212643));
#176660=CARTESIAN_POINT('Ctrl Pts',(-9.57924749643216,-3.41862251343128,
135.636103893117));
#176661=CARTESIAN_POINT('Ctrl Pts',(-9.57184958212081,-3.54610844577842,
135.543335137415));
#176662=CARTESIAN_POINT('Ctrl Pts',(-9.56445166780946,-3.66972425183371,
135.445594772185));
#176663=CARTESIAN_POINT('Ctrl Pts',(-9.55705498289727,-3.79331951518448,
135.347870649631));
#176664=CARTESIAN_POINT('Ctrl Pts',(-9.54965829798511,-3.91304563615874,
135.245176788596));
#176665=CARTESIAN_POINT('Ctrl Pts',(-9.54226161307292,-4.02848793837069,
135.137859837931));
#176666=CARTESIAN_POINT('Ctrl Pts',(-9.5348652561375,-4.14392512174999,
135.030547645812));
#176667=CARTESIAN_POINT('Ctrl Pts',(-9.52746889920204,-4.25507859064215,
134.918613025821));
#176668=CARTESIAN_POINT('Ctrl Pts',(-9.5200725422666,-4.36156894126619,
134.802441023596));
#176669=CARTESIAN_POINT('Ctrl Pts',(-9.51267505293002,-4.46807559583507,
134.68625123514));
#176670=CARTESIAN_POINT('Ctrl Pts',(-9.50527756359342,-4.56991745833369,
134.565823047891));
#176671=CARTESIAN_POINT('Ctrl Pts',(-9.49788007425684,-4.66675409632555,
134.441576141415));
#176672=CARTESIAN_POINT('Ctrl Pts',(-9.49047999174186,-4.76362468025047,
134.317285680379));
#176673=CARTESIAN_POINT('Ctrl Pts',(-9.48307990922691,-4.85548631699029,
134.189174129133));
#176674=CARTESIAN_POINT('Ctrl Pts',(-9.47567982671194,-4.94204083301768,
134.057691674696));
#176675=CARTESIAN_POINT('Ctrl Pts',(-9.4682716070455,-5.02869052463333,
133.926064641783));
#176676=CARTESIAN_POINT('Ctrl Pts',(-9.46086338737904,-5.11002123582678,
133.791059615239));
#176677=CARTESIAN_POINT('Ctrl Pts',(-9.4534551677126,-5.1857794865322,133.653153639104));
#176678=CARTESIAN_POINT('Ctrl Pts',(-9.44604238841058,-5.26158436517683,
133.515162784141));
#176679=CARTESIAN_POINT('Ctrl Pts',(-9.43862960910857,-5.33180978297738,
133.374267755105));
#176680=CARTESIAN_POINT('Ctrl Pts',(-9.43121682980654,-5.39624990440219,
133.230966793224));
#176681=CARTESIAN_POINT('Ctrl Pts',(-9.42379345877782,-5.46078210089444,
133.087461076208));
#176682=CARTESIAN_POINT('Ctrl Pts',(-9.41637008774905,-5.51951235233774,
132.941542905853));
#176683=CARTESIAN_POINT('Ctrl Pts',(-9.40894671672032,-5.57228401204957,
132.793727715805));
#176684=CARTESIAN_POINT('Ctrl Pts',(-9.40501066727938,-5.60026481226855,
132.715352555262));
#176685=CARTESIAN_POINT('Ctrl Pts',(-9.4010746178385,-5.62657128217795,
132.636444292024));
#176686=CARTESIAN_POINT('Ctrl Pts',(-9.39713856839757,-5.651185896725,132.557080938426));
#176687=CARTESIAN_POINT('Ctrl Pts',(-9.38809573540457,-5.70773646903769,
132.374748484753));
#176688=CARTESIAN_POINT('Ctrl Pts',(-9.37905290241155,-5.75549286966623,
132.189567681947));
#176689=CARTESIAN_POINT('Ctrl Pts',(-9.37001006941856,-5.7942091403477,
132.00230510727));
#176690=CARTESIAN_POINT('Ctrl Pts',(-9.36057093182716,-5.83462216204914,
131.806835699677));
#176691=CARTESIAN_POINT('Ctrl Pts',(-9.35113179423582,-5.86518480503675,
131.609097826369));
#176692=CARTESIAN_POINT('Ctrl Pts',(-9.34169265664443,-5.8856728759424,
131.409988688164));
#176693=CARTESIAN_POINT('Ctrl Pts',(-9.3328127637492,-5.90494708118736,
131.222676255793));
#176694=CARTESIAN_POINT('Ctrl Pts',(-9.32393287085396,-5.91530547341419,
131.034150421048));
#176695=CARTESIAN_POINT('Ctrl Pts',(-9.31505297795874,-5.91660919492221,
130.845179694748));
#176696=CARTESIAN_POINT('Ctrl Pts',(-9.31449373326259,-5.9166913016939,
130.833278551608));
#176697=CARTESIAN_POINT('Ctrl Pts',(-9.31393448856645,-5.91673751044455,
130.821375650849));
#176698=CARTESIAN_POINT('Ctrl Pts',(-9.3133752438703,-5.91674779288229,
130.809471187257));
#176699=CARTESIAN_POINT('',(-7.56337516349587,-5.91244826925484,130.801667160838));
#176700=CARTESIAN_POINT('Ctrl Pts',(-9.3133751922043,-5.9128223061593,130.809466697563));
#176701=CARTESIAN_POINT('Ctrl Pts',(-9.24848044299772,-5.90153186961771,
129.428978555947));
#176702=CARTESIAN_POINT('Ctrl Pts',(-9.09076981918684,-4.73048501898084,
126.056784170589));
#176703=CARTESIAN_POINT('Ctrl Pts',(-8.84024332077167,0.892881284146524,
123.863155855944));
#176704=CARTESIAN_POINT('Ctrl Pts',(-8.56179569695882,6.32245629500537,
127.80367620762));
#176705=CARTESIAN_POINT('Ctrl Pts',(-8.28334807314588,5.9420028399166,134.501678940454));
#176706=CARTESIAN_POINT('Ctrl Pts',(-8.00490044933302,0.101139057920626,
137.802026758594));
#176707=CARTESIAN_POINT('Ctrl Pts',(-7.76490948901916,-5.01314309408,135.104171354005));
#176708=CARTESIAN_POINT('Ctrl Pts',(-7.61773440330959,-5.90337292098504,
131.960358330193));
#176709=CARTESIAN_POINT('Ctrl Pts',(-7.56337519220432,-5.90810821042033,
130.801669750358));
#176710=CARTESIAN_POINT('',(-5.81337519220429,-5.91970862835117,130.800211422335));
#176711=CARTESIAN_POINT('Ctrl Pts',(-7.56337513504499,-5.9167493857658,
130.801664594553));
#176712=CARTESIAN_POINT('Ctrl Pts',(-7.55528446404787,-5.91667068981716,
130.628956793656));
#176713=CARTESIAN_POINT('Ctrl Pts',(-7.5471937930507,-5.90902596019284,
130.456497795035));
#176714=CARTESIAN_POINT('Ctrl Pts',(-7.53910312205358,-5.89390511114336,
130.284925247825));
#176715=CARTESIAN_POINT('Ctrl Pts',(-7.53097456335621,-5.87871345286232,
130.112549245717));
#176716=CARTESIAN_POINT('Ctrl Pts',(-7.52284600465886,-5.85597557211895,
129.941068258802));
#176717=CARTESIAN_POINT('Ctrl Pts',(-7.51471744596151,-5.82583314817139,
129.771113942194));
#176718=CARTESIAN_POINT('Ctrl Pts',(-7.50656981588184,-5.79562000348323,
129.600760875467));
#176719=CARTESIAN_POINT('Ctrl Pts',(-7.49842218580217,-5.75796764258631,
129.431941879387));
#176720=CARTESIAN_POINT('Ctrl Pts',(-7.49027455572249,-5.71306787093264,
129.265274504115));
#176721=CARTESIAN_POINT('Ctrl Pts',(-7.48209847134111,-5.66801129397036,
129.098025069553));
#176722=CARTESIAN_POINT('Ctrl Pts',(-7.47392238695973,-5.61565671350522,
128.932942534547));
#176723=CARTESIAN_POINT('Ctrl Pts',(-7.46574630257834,-5.55624564874628,
128.770628862076));
#176724=CARTESIAN_POINT('Ctrl Pts',(-7.45983260228799,-5.51327407280285,
128.653228604539));
#176725=CARTESIAN_POINT('Ctrl Pts',(-7.45391890199762,-5.46661188495489,
128.53727643129));
#176726=CARTESIAN_POINT('Ctrl Pts',(-7.44800520170728,-5.41636538536468,
128.422991982784));
#176727=CARTESIAN_POINT('Ctrl Pts',(-7.4405819353018,-5.35329266708549,
128.27953460997));
#176728=CARTESIAN_POINT('Ctrl Pts',(-7.43315866889636,-5.28442124009781,
128.138367851464));
#176729=CARTESIAN_POINT('Ctrl Pts',(-7.42573540249089,-5.20993888572132,
127.999994847994));
#176730=CARTESIAN_POINT('Ctrl Pts',(-7.41832090976983,-5.13554456330222,
127.861785389922));
#176731=CARTESIAN_POINT('Ctrl Pts',(-7.41090641704874,-5.05555268903511,
127.726363439756));
#176732=CARTESIAN_POINT('Ctrl Pts',(-7.40349192432768,-4.97019922455477,
127.59421260996));
#176733=CARTESIAN_POINT('Ctrl Pts',(-7.39608457797386,-4.884928026957,127.462189152109));
#176734=CARTESIAN_POINT('Ctrl Pts',(-7.38867723162001,-4.79430572819841,
127.333430849439));
#176735=CARTESIAN_POINT('Ctrl Pts',(-7.38126988526619,-4.69861430131405,
127.208397017919));
#176736=CARTESIAN_POINT('Ctrl Pts',(-7.37386806359074,-4.60299424470596,
127.083456441347));
#176737=CARTESIAN_POINT('Ctrl Pts',(-7.36646624191535,-4.50231281384863,
126.962235100016));
#176738=CARTESIAN_POINT('Ctrl Pts',(-7.35906442023989,-4.39689534614848,
126.845163492199));
#176739=CARTESIAN_POINT('Ctrl Pts',(-7.35166650592851,-4.29153352750941,
126.728153685572));
#176740=CARTESIAN_POINT('Ctrl Pts',(-7.34426859161715,-4.18144090029054,
126.615289526455));
#176741=CARTESIAN_POINT('Ctrl Pts',(-7.33687067730577,-4.06698306932293,
126.506968469258));
#176742=CARTESIAN_POINT('Ctrl Pts',(-7.32947399239352,-3.95254425917018,
126.398665413055));
#176743=CARTESIAN_POINT('Ctrl Pts',(-7.32207730748121,-3.83374195587244,
126.294904216699));
#176744=CARTESIAN_POINT('Ctrl Pts',(-7.31468062256897,-3.71097869393608,
126.196045557194));
#176745=CARTESIAN_POINT('Ctrl Pts',(-7.30728426563349,-3.58822087545141,
126.097191281186));
#176746=CARTESIAN_POINT('Ctrl Pts',(-7.29988790869808,-3.46150273829219,
126.003239343929));
#176747=CARTESIAN_POINT('Ctrl Pts',(-7.29249155176259,-3.33125975840187,
125.914510007931));
#176748=CARTESIAN_POINT('Ctrl Pts',(-7.28509406242597,-3.20099683797864,
125.825767087244));
#176749=CARTESIAN_POINT('Ctrl Pts',(-7.27769657308931,-3.06720830881352,
125.742248570103));
#176750=CARTESIAN_POINT('Ctrl Pts',(-7.27029908375269,-2.93035833389096,
125.664231183642));
#176751=CARTESIAN_POINT('Ctrl Pts',(-7.26289900123764,-2.79346038642164,
125.586186448306));
#176752=CARTESIAN_POINT('Ctrl Pts',(-7.25549891872264,-2.65349918058857,
125.513646867873));
#176753=CARTESIAN_POINT('Ctrl Pts',(-7.24809883620759,-2.51096301111948,
125.446842972304));
#176754=CARTESIAN_POINT('Ctrl Pts',(-7.24069061654108,-2.36827010847918,
125.379965618985));
#176755=CARTESIAN_POINT('Ctrl Pts',(-7.23328239687457,-2.2229969258592,
125.31883670449));
#176756=CARTESIAN_POINT('Ctrl Pts',(-7.22587417720806,-2.07565192789372,
125.263638675731));
#176757=CARTESIAN_POINT('Ctrl Pts',(-7.21846139790595,-1.92821624154057,
125.208406673506));
#176758=CARTESIAN_POINT('Ctrl Pts',(-7.21104861860382,-1.77870655261404,
125.159112947436));
#176759=CARTESIAN_POINT('Ctrl Pts',(-7.20363583930171,-1.62764547111343,
125.115889752486));
#176760=CARTESIAN_POINT('Ctrl Pts',(-7.19621246827291,-1.47636854645551,
125.072604798209));
#176761=CARTESIAN_POINT('Ctrl Pts',(-7.18878909724414,-1.32353616372034,
125.035407786739));
#176762=CARTESIAN_POINT('Ctrl Pts',(-7.18136572621535,-1.16968089342613,
125.004379827076));
#176763=CARTESIAN_POINT('Ctrl Pts',(-7.17742967677499,-1.08810313741903,
124.987928058359));
#176764=CARTESIAN_POINT('Ctrl Pts',(-7.17349362733462,-1.00623790539112,
124.973209765342));
#176765=CARTESIAN_POINT('Ctrl Pts',(-7.16955757789427,-0.924164916562035,
124.960231104157));
#176766=CARTESIAN_POINT('Ctrl Pts',(-7.16213431148884,-0.769377821023641,
124.935753754211));
#176767=CARTESIAN_POINT('Ctrl Pts',(-7.15471104508342,-0.613383540478684,
124.917393155114));
#176768=CARTESIAN_POINT('Ctrl Pts',(-7.14728777867799,-0.456706881859427,
124.905263280976));
#176769=CARTESIAN_POINT('Ctrl Pts',(-7.13987328595699,-0.30021540203947,
124.893147743342));
#176770=CARTESIAN_POINT('Ctrl Pts',(-7.13245879323596,-0.143043518065936,
124.887248300721));
#176771=CARTESIAN_POINT('Ctrl Pts',(-7.12504430051496,0.0142743501722947,
124.887627836256));
#176772=CARTESIAN_POINT('Ctrl Pts',(-7.11763695416119,0.171440589526204,
124.88800700598));
#176773=CARTESIAN_POINT('Ctrl Pts',(-7.11022960780743,0.328752162237795,
124.894653104793));
#176774=CARTESIAN_POINT('Ctrl Pts',(-7.10282226145367,0.4856702194611,124.907577172294));
#176775=CARTESIAN_POINT('Ctrl Pts',(-7.09542043977828,0.642471241277148,
124.920491600539));
#176776=CARTESIAN_POINT('Ctrl Pts',(-7.08801861810287,0.798878961563464,
124.93967464378));
#176777=CARTESIAN_POINT('Ctrl Pts',(-7.08061679642748,0.954355337116193,
124.965085281275));
#176778=CARTESIAN_POINT('Ctrl Pts',(-7.07321888211614,1.10974963790049,
124.990482504692));
#176779=CARTESIAN_POINT('Ctrl Pts',(-7.06582096780479,1.26421320561768,
125.022100715093));
#176780=CARTESIAN_POINT('Ctrl Pts',(-7.05842305349344,1.41721403227515,
125.059847152596));
#176781=CARTESIAN_POINT('Ctrl Pts',(-7.05102636858124,1.57018943297094,
125.097587317325));
#176782=CARTESIAN_POINT('Ctrl Pts',(-7.04362968366908,1.72170221297456,
125.141453598607));
#176783=CARTESIAN_POINT('Ctrl Pts',(-7.03623299875687,1.87123134477403,
125.19130228749));
#176784=CARTESIAN_POINT('Ctrl Pts',(-7.02883664182143,2.02075384629509,
125.24114876603));
#176785=CARTESIAN_POINT('Ctrl Pts',(-7.02144028488599,2.16829252036316,
125.296977006675));
#176786=CARTESIAN_POINT('Ctrl Pts',(-7.01404392795055,2.31334253567563,
125.358593740887));
#176787=CARTESIAN_POINT('Ctrl Pts',(-7.00664643861397,2.45841475851594,
125.420219908779));
#176788=CARTESIAN_POINT('Ctrl Pts',(-6.9992489492774,2.60099722033429,125.487636188884));
#176789=CARTESIAN_POINT('Ctrl Pts',(-6.99185145994082,2.74060621132301,
125.560601645516));
#176790=CARTESIAN_POINT('Ctrl Pts',(-6.98445137742582,2.8802641420271,125.633592680075));
#176791=CARTESIAN_POINT('Ctrl Pts',(-6.97705129491078,3.01694619596777,
125.712136591347));
#176792=CARTESIAN_POINT('Ctrl Pts',(-6.96965121239577,3.15019448653172,
125.795947170223));
#176793=CARTESIAN_POINT('Ctrl Pts',(-6.96224299272931,3.28358929728922,
125.879849907447));
#176794=CARTESIAN_POINT('Ctrl Pts',(-6.95483477306293,3.41354248801447,
125.969030678893));
#176795=CARTESIAN_POINT('Ctrl Pts',(-6.94742655339647,3.53962572340069,
126.063160315877));
#176796=CARTESIAN_POINT('Ctrl Pts',(-6.94001377409441,3.66578656091466,
126.157347888081));
#176797=CARTESIAN_POINT('Ctrl Pts',(-6.93260099479233,3.78807240757056,
126.256490160701));
#176798=CARTESIAN_POINT('Ctrl Pts',(-6.92518821549027,3.90608951004912,
126.360218934183));
#176799=CARTESIAN_POINT('Ctrl Pts',(-6.91776484446151,4.02427524089816,
126.464095920201));
#176800=CARTESIAN_POINT('Ctrl Pts',(-6.91034147343269,4.13817977612814,
126.572572238946));
#176801=CARTESIAN_POINT('Ctrl Pts',(-6.90291810240393,4.24744700906844,
126.685243665153));
#176802=CARTESIAN_POINT('Ctrl Pts',(-6.89898205296311,4.30538311780511,
126.744984758842));
#176803=CARTESIAN_POINT('Ctrl Pts',(-6.89504600352228,4.36201619215133,
126.805904700208));
#176804=CARTESIAN_POINT('Ctrl Pts',(-6.89110995408146,4.41729796259356,
126.867939746754));
#176805=CARTESIAN_POINT('Ctrl Pts',(-6.88368668767603,4.52155765636165,
126.98493590849));
#176806=CARTESIAN_POINT('Ctrl Pts',(-6.8762634212706,4.62132366738767,127.106253962405));
#176807=CARTESIAN_POINT('Ctrl Pts',(-6.86884015486518,4.7162164350593,127.231513979355));
#176808=CARTESIAN_POINT('Ctrl Pts',(-6.86142566214419,4.81099704735989,
127.356625949367));
#176809=CARTESIAN_POINT('Ctrl Pts',(-6.85401116942323,4.90091565794216,
127.485670313854));
#176810=CARTESIAN_POINT('Ctrl Pts',(-6.84659667670223,4.98563049443313,
127.618231440103));
#176811=CARTESIAN_POINT('Ctrl Pts',(-6.83918933034846,5.07026367957537,
127.750664798949));
#176812=CARTESIAN_POINT('Ctrl Pts',(-6.83178198399465,5.14970287601641,
127.886607859114));
#176813=CARTESIAN_POINT('Ctrl Pts',(-6.82437463764089,5.22364753486462,
128.025613238979));
#176814=CARTESIAN_POINT('Ctrl Pts',(-6.81697281596549,5.29753704299648,
128.164514943387));
#176815=CARTESIAN_POINT('Ctrl Pts',(-6.80957099429009,5.36593999871168,
128.306474091605));
#176816=CARTESIAN_POINT('Ctrl Pts',(-6.8021691726147,5.42860008842839,128.451015839932));
#176817=CARTESIAN_POINT('Ctrl Pts',(-6.79477125830335,5.49122710037147,
128.595481285796));
#176818=CARTESIAN_POINT('Ctrl Pts',(-6.78737334399204,5.5481171358204,128.742526274992));
#176819=CARTESIAN_POINT('Ctrl Pts',(-6.77997542968069,5.59906067297614,
128.891653075146));
#176820=CARTESIAN_POINT('Ctrl Pts',(-6.7725787447685,5.64999574424015,129.04075509313));
#176821=CARTESIAN_POINT('Ctrl Pts',(-6.76518205985623,5.69498615793799,
129.191937882538));
#176822=CARTESIAN_POINT('Ctrl Pts',(-6.75778537494404,5.73387119238194,
129.344685409969));
#176823=CARTESIAN_POINT('Ctrl Pts',(-6.7503890180086,5.77275450262271,129.497426164415));
#176824=CARTESIAN_POINT('Ctrl Pts',(-6.7429926610732,5.80553287979693,129.65173115717));
#176825=CARTESIAN_POINT('Ctrl Pts',(-6.73559630413777,5.83209605254753,
129.807071192996));
#176826=CARTESIAN_POINT('Ctrl Pts',(-6.7281988148012,5.85866329218773,129.962435011778));
#176827=CARTESIAN_POINT('Ctrl Pts',(-6.72080132546463,5.87901336978973,
130.118833821182));
#176828=CARTESIAN_POINT('Ctrl Pts',(-6.71340383612807,5.89308753440536,
130.275730430823));
#176829=CARTESIAN_POINT('Ctrl Pts',(-6.70600375361309,5.90716663269756,
130.432682040326));
#176830=CARTESIAN_POINT('Ctrl Pts',(-6.69860367109814,5.91496540446514,
130.590131425927));
#176831=CARTESIAN_POINT('Ctrl Pts',(-6.69120358858316,5.91647714663784,
130.747538651636));
#176832=CARTESIAN_POINT('Ctrl Pts',(-6.6837953689167,5.91799055112647,130.905118962771));
#176833=CARTESIAN_POINT('Ctrl Pts',(-6.67638714925018,5.9132031162481,131.062656647922));
#176834=CARTESIAN_POINT('Ctrl Pts',(-6.66897892958372,5.9021602552449,131.219613412749));
#176835=CARTESIAN_POINT('Ctrl Pts',(-6.66156615028166,5.89111059754501,
131.376666781846));
#176836=CARTESIAN_POINT('Ctrl Pts',(-6.65415337097965,5.87379788285035,
131.533138147988));
#176837=CARTESIAN_POINT('Ctrl Pts',(-6.6467405916776,5.85031905458617,131.688497214504));
#176838=CARTESIAN_POINT('Ctrl Pts',(-6.63931722064885,5.82680667867113,
131.844078265341));
#176839=CARTESIAN_POINT('Ctrl Pts',(-6.6318938496201,5.7971106630666,131.998543476737));
#176840=CARTESIAN_POINT('Ctrl Pts',(-6.62447047859135,5.76137860958308,
132.151374752436));
#176841=CARTESIAN_POINT('Ctrl Pts',(-6.62053442915043,5.74243261744663,
132.23240956195));
#176842=CARTESIAN_POINT('Ctrl Pts',(-6.61659837970951,5.72179050545635,
132.312985287692));
#176843=CARTESIAN_POINT('Ctrl Pts',(-6.61266233026859,5.6994798111297,132.393026864776));
#176844=CARTESIAN_POINT('Ctrl Pts',(-6.60523906386315,5.65740253792386,
132.54398278114));
#176845=CARTESIAN_POINT('Ctrl Pts',(-6.59781579745767,5.60926018913864,
132.693494123237));
#176846=CARTESIAN_POINT('Ctrl Pts',(-6.59039253105223,5.55516724814181,
132.841036194989));
#176847=CARTESIAN_POINT('Ctrl Pts',(-6.58297803833122,5.5011382405091,132.988403884266));
#176848=CARTESIAN_POINT('Ctrl Pts',(-6.57556354561025,5.44117276734328,
133.133806589066));
#176849=CARTESIAN_POINT('Ctrl Pts',(-6.56814905288923,5.37543577590156,
133.276732106978));
#176850=CARTESIAN_POINT('Ctrl Pts',(-6.56074170653544,5.30976214424714,
133.419519867895));
#176851=CARTESIAN_POINT('Ctrl Pts',(-6.55333436018166,5.23832822370858,
133.55983485831));
#176852=CARTESIAN_POINT('Ctrl Pts',(-6.54592701382788,5.16134795509735,
133.697182397232));
#176853=CARTESIAN_POINT('Ctrl Pts',(-6.53852519215247,5.08442510127475,
133.834427497179));
#176854=CARTESIAN_POINT('Ctrl Pts',(-6.53112337047707,5.00196431778647,
133.968709228251));
#176855=CARTESIAN_POINT('Ctrl Pts',(-6.52372154880166,4.91422656033279,
134.099555281955));
#176856=CARTESIAN_POINT('Ctrl Pts',(-6.51632363449031,4.82653511895844,
134.230332263046));
#176857=CARTESIAN_POINT('Ctrl Pts',(-6.50892572017889,4.73357245879413,
134.357676869513));
#176858=CARTESIAN_POINT('Ctrl Pts',(-6.50152780586754,4.63564408453204,
134.481143788225));
#176859=CARTESIAN_POINT('Ctrl Pts',(-6.49413112095533,4.53773198418901,
134.604590188976));
#176860=CARTESIAN_POINT('Ctrl Pts',(-6.48673443604315,4.43485603929642,
134.724159888735));
#176861=CARTESIAN_POINT('Ctrl Pts',(-6.47933775113094,4.32736352937015,
134.839438739137));
#176862=CARTESIAN_POINT('Ctrl Pts',(-6.47194139419549,4.21987578577442,
134.954712477953));
#176863=CARTESIAN_POINT('Ctrl Pts',(-6.46454503726002,4.10777213874416,
135.065695472695));
#176864=CARTESIAN_POINT('Ctrl Pts',(-6.45714868032456,3.99143821085792,
135.172008905993));
#176865=CARTESIAN_POINT('Ctrl Pts',(-6.44975119098798,3.87508647195033,
135.27833861615));
#176866=CARTESIAN_POINT('Ctrl Pts',(-6.44235370165139,3.75450343817615,
135.379997089517));
#176867=CARTESIAN_POINT('Ctrl Pts',(-6.4349562123148,3.63010930669793,135.476644532733));
#176868=CARTESIAN_POINT('Ctrl Pts',(-6.4275561297998,3.50567156904975,135.57332585556));
#176869=CARTESIAN_POINT('Ctrl Pts',(-6.42015604728487,3.37742036838085,
135.664992421953));
#176870=CARTESIAN_POINT('Ctrl Pts',(-6.41275596476987,3.24580634495809,
135.751346743838));
#176871=CARTESIAN_POINT('Ctrl Pts',(-6.4053477451034,3.11404759838633,135.837796021178));
#176872=CARTESIAN_POINT('Ctrl Pts',(-6.39793952543684,2.97891895667795,
135.918921183524));
#176873=CARTESIAN_POINT('Ctrl Pts',(-6.39053130577037,2.84089784907312,
135.994469477083));
#176874=CARTESIAN_POINT('Ctrl Pts',(-6.38311852646829,2.70279179177936,
136.070064269356));
#176875=CARTESIAN_POINT('Ctrl Pts',(-6.37570574716627,2.56179005476495,
136.140075187587));
#176876=CARTESIAN_POINT('Ctrl Pts',(-6.36829296786419,2.41839119192782,
136.204297154721));
#176877=CARTESIAN_POINT('Ctrl Pts',(-6.36086959683542,2.27478743407074,
136.268610885214));
#176878=CARTESIAN_POINT('Ctrl Pts',(-6.35344622580663,2.12878005524076,
136.327119006033));
#176879=CARTESIAN_POINT('Ctrl Pts',(-6.34602285477786,1.98088472687642,
136.37966565508));
#176880=CARTESIAN_POINT('Ctrl Pts',(-6.34208680533712,1.90246707507912,
136.407527149243));
#176881=CARTESIAN_POINT('Ctrl Pts',(-6.33815075589638,1.82351886925034,
136.433713503745));
#176882=CARTESIAN_POINT('Ctrl Pts',(-6.33421470645564,1.74411814830525,
136.458207312273));
#176883=CARTESIAN_POINT('Ctrl Pts',(-6.32679144005021,1.59437086661246,
136.504401870733));
#176884=CARTESIAN_POINT('Ctrl Pts',(-6.31936817364477,1.44256062466505,
136.544712881658));
#176885=CARTESIAN_POINT('Ctrl Pts',(-6.31194490723934,1.28919074518874,
136.578953052104));
#176886=CARTESIAN_POINT('Ctrl Pts',(-6.30453041451832,1.13600213617317,
136.613152753511));
#176887=CARTESIAN_POINT('Ctrl Pts',(-6.29711592179732,0.981257919622204,
136.641295816229));
#176888=CARTESIAN_POINT('Ctrl Pts',(-6.2897014290763,0.82547818395196,136.663244157142));
#176889=CARTESIAN_POINT('Ctrl Pts',(-6.28229408272252,0.669848594655958,
136.685171343418));
#176890=CARTESIAN_POINT('Ctrl Pts',(-6.27488673636877,0.513185840371659,
136.700915642659));
#176891=CARTESIAN_POINT('Ctrl Pts',(-6.26747939001498,0.356021750459489,
136.710389662169));
#176892=CARTESIAN_POINT('Ctrl Pts',(-6.26007756833959,0.198974879455262,
136.719856615599));
#176893=CARTESIAN_POINT('Ctrl Pts',(-6.25267574666416,0.0414277883562145,
136.723062578698));
#176894=CARTESIAN_POINT('Ctrl Pts',(-6.24527392498877,-0.116081103395428,
136.719971806609));
#176895=CARTESIAN_POINT('Ctrl Pts',(-6.23787601067742,-0.273506847429162,
136.716882666115));
#176896=CARTESIAN_POINT('Ctrl Pts',(-6.23047809636608,-0.430894059994037,
136.70750341764));
#176897=CARTESIAN_POINT('Ctrl Pts',(-6.22308018205473,-0.587702953794054,
136.691850388309));
#176898=CARTESIAN_POINT('Ctrl Pts',(-6.21568349714252,-0.744485788800949,
136.676199960227));
#176899=CARTESIAN_POINT('Ctrl Pts',(-6.20828681223032,-0.900690124697001,
136.654277857563));
#176900=CARTESIAN_POINT('Ctrl Pts',(-6.2008901273181,-1.05577981367228,
136.6261523991));
#176901=CARTESIAN_POINT('Ctrl Pts',(-6.19349377038265,-1.21086262580822,
136.59802818775));
#176902=CARTESIAN_POINT('Ctrl Pts',(-6.18609741344724,-1.36483052198972,
136.563701234132));
#176903=CARTESIAN_POINT('Ctrl Pts',(-6.17870105651178,-1.51715635401359,
136.523291213401));
#176904=CARTESIAN_POINT('Ctrl Pts',(-6.1713035671752,-1.66950550751121,
136.482875005793));
#176905=CARTESIAN_POINT('Ctrl Pts',(-6.16390607783857,-1.82021173543165,
136.436373972391));
#176906=CARTESIAN_POINT('Ctrl Pts',(-6.15650858850199,-1.96876203316624,
136.383957970356));
#176907=CARTESIAN_POINT('Ctrl Pts',(-6.14910850598699,-2.11736440497743,
136.331523593973));
#176908=CARTESIAN_POINT('Ctrl Pts',(-6.14170842347198,-2.26380899008739,
136.273170244804));
#176909=CARTESIAN_POINT('Ctrl Pts',(-6.13430834095698,-2.40760192128238,
136.209116259696));
#176910=CARTESIAN_POINT('Ctrl Pts',(-6.1269001212905,-2.55155296758749,
136.144991840647));
#176911=CARTESIAN_POINT('Ctrl Pts',(-6.11949190162403,-2.69284619579678,
136.075154419176));
#176912=CARTESIAN_POINT('Ctrl Pts',(-6.11208368195756,-2.83101089482012,
135.999869050425));
#176913=CARTESIAN_POINT('Ctrl Pts',(-6.10467090265549,-2.96926063191031,
135.924537344786));
#176914=CARTESIAN_POINT('Ctrl Pts',(-6.09725812335342,-3.10437768324554,
135.843751201475));
#176915=CARTESIAN_POINT('Ctrl Pts',(-6.08984534405135,-3.23592003113169,
135.757819218849));
#176916=CARTESIAN_POINT('Ctrl Pts',(-6.0824219730226,-3.36765033289323,
135.671764452575));
#176917=CARTESIAN_POINT('Ctrl Pts',(-6.07499860199389,-3.49579542666038,
135.580549378065));
#176918=CARTESIAN_POINT('Ctrl Pts',(-6.06757523096513,-3.61994544822661,
135.484523597032));
#176919=CARTESIAN_POINT('Ctrl Pts',(-6.06363918152437,-3.68577276859955,
135.433608423821));
#176920=CARTESIAN_POINT('Ctrl Pts',(-6.05970313208357,-3.75047752394584,
135.381341426573));
#176921=CARTESIAN_POINT('Ctrl Pts',(-6.0557670826428,-3.8140028879032,135.327778853101));
#176922=CARTESIAN_POINT('Ctrl Pts',(-6.04844892319008,-3.93211338161724,
135.228191828275));
#176923=CARTESIAN_POINT('Ctrl Pts',(-6.04113076373738,-4.04652378683626,
135.123804285533));
#176924=CARTESIAN_POINT('Ctrl Pts',(-6.03381260428466,-4.15681063084074,
135.014925418377));
#176925=CARTESIAN_POINT('Ctrl Pts',(-6.02650314913099,-4.26696629846438,
134.906176052939));
#176926=CARTESIAN_POINT('Ctrl Pts',(-6.01919369397733,-4.37300789179196,
134.792946258656));
#176927=CARTESIAN_POINT('Ctrl Pts',(-6.01188423882365,-4.4745437509958,
134.675586364397));
#176928=CARTESIAN_POINT('Ctrl Pts',(-6.0045817750019,-4.57598249339982,
134.558338722276));
#176929=CARTESIAN_POINT('Ctrl Pts',(-5.99727931118016,-4.67292382734191,
134.436969129899));
#176930=CARTESIAN_POINT('Ctrl Pts',(-5.98997684735841,-4.76501202442191,
134.311865566902));
#176931=CARTESIAN_POINT('Ctrl Pts',(-5.98261844506032,-4.85780563731206,
134.185803683142));
#176932=CARTESIAN_POINT('Ctrl Pts',(-5.97526004276216,-4.94567115456138,
134.055950647106));
#176933=CARTESIAN_POINT('Ctrl Pts',(-5.96790164046408,-5.02828466217561,
133.922739029278));
#176934=CARTESIAN_POINT('Ctrl Pts',(-5.96060768547709,-5.11017461347822,
133.790694122677));
#176935=CARTESIAN_POINT('Ctrl Pts',(-5.95331373049013,-5.18690398224569,
133.655349566142));
#176936=CARTESIAN_POINT('Ctrl Pts',(-5.94601977550315,-5.25819998616286,
133.517156862774));
#176937=CARTESIAN_POINT('Ctrl Pts',(-5.93872726715306,-5.32948184968156,
133.378991567674));
#176938=CARTESIAN_POINT('Ctrl Pts',(-5.93143475880301,-5.39533231605664,
133.237979591406));
#176939=CARTESIAN_POINT('Ctrl Pts',(-5.92414225045292,-5.45552437627061,
133.094597361315));
#176940=CARTESIAN_POINT('Ctrl Pts',(-5.91684965354754,-5.51571716741625,
132.951213390087));
#176941=CARTESIAN_POINT('Ctrl Pts',(-5.90955705664208,-5.5702512675601,
132.805459462894));
#176942=CARTESIAN_POINT('Ctrl Pts',(-5.9022644597367,-5.61894779131388,
132.657832031154));
#176943=CARTESIAN_POINT('Ctrl Pts',(-5.89485702077567,-5.6684111761685,
132.507879798256));
#176944=CARTESIAN_POINT('Ctrl Pts',(-5.88744958181468,-5.71185143378304,
132.355994940758));
#176945=CARTESIAN_POINT('Ctrl Pts',(-5.88004214285365,-5.74913392966919,
132.202713084302));
#176946=CARTESIAN_POINT('Ctrl Pts',(-5.87274168883747,-5.78587795797063,
132.051645063295));
#176947=CARTESIAN_POINT('Ctrl Pts',(-5.86544123482127,-5.8166408791501,
131.899220517167));
#176948=CARTESIAN_POINT('Ctrl Pts',(-5.85814078080509,-5.84134564715325,
131.745961166092));
#176949=CARTESIAN_POINT('Ctrl Pts',(-5.85067984937163,-5.86659347143138,
131.589332892374));
#176950=CARTESIAN_POINT('Ctrl Pts',(-5.84321891793812,-5.88551366306476,
131.431833112249));
#176951=CARTESIAN_POINT('Ctrl Pts',(-5.83575798650466,-5.89808008625693,
131.274022047321));
#176952=CARTESIAN_POINT('Ctrl Pts',(-5.82829705507119,-5.91064650944911,
131.116210982393));
#176953=CARTESIAN_POINT('Ctrl Pts',(-5.82083612363776,-5.91685920350292,
130.958089057843));
#176954=CARTESIAN_POINT('Ctrl Pts',(-5.81337519220429,-5.91674854661678,
130.800213497092));
#176955=CARTESIAN_POINT('',(-4.06337519220434,-5.92132048307296,130.809046855528));
#176956=CARTESIAN_POINT('Ctrl Pts',(-5.81337519220429,-5.92270786400364,
130.800209320135));
#176957=CARTESIAN_POINT('Ctrl Pts',(-5.80135661441281,-5.92473620102161,
130.545634893806));
#176958=CARTESIAN_POINT('Ctrl Pts',(-5.69652216201681,-5.79401867711778,
128.327156252607));
#176959=CARTESIAN_POINT('Ctrl Pts',(-5.49887183501715,-2.99105923299359,
124.477345113001));
#176960=CARTESIAN_POINT('Ctrl Pts',(-5.22042421120391,3.70635675827079,
124.86799134748));
#176961=CARTESIAN_POINT('Ctrl Pts',(-4.94197658739132,6.99781195427446,
130.713870933415));
#176962=CARTESIAN_POINT('Ctrl Pts',(-4.66352896357833,3.85861982642432,
136.642906118412));
#176963=CARTESIAN_POINT('Ctrl Pts',(-4.38508133976539,-2.82645541785551,
137.20660321694));
#176964=CARTESIAN_POINT('Ctrl Pts',(-4.18503008264081,-5.7632723015822,
133.384689163164));
#176965=CARTESIAN_POINT('Ctrl Pts',(-4.07779470012041,-5.92396940801648,
131.114663565642));
#176966=CARTESIAN_POINT('Ctrl Pts',(-4.06337519220434,-5.92132048307296,
130.809046855528));
#176967=CARTESIAN_POINT('',(-2.31337593551284,-5.91165713928214,130.806298299166));
#176968=CARTESIAN_POINT('Ctrl Pts',(-4.06337519220434,-5.92132048307296,
130.809046855528));
#176969=CARTESIAN_POINT('Ctrl Pts',(-3.98497882551612,-5.90691873702097,
129.147461743774));
#176970=CARTESIAN_POINT('Ctrl Pts',(-3.81376658422367,-4.30954189761841,
125.494430884269));
#176971=CARTESIAN_POINT('Ctrl Pts',(-3.54973846832673,1.88934901456002,
124.065820654671));
#176972=CARTESIAN_POINT('Ctrl Pts',(-3.27129084451378,6.6905638084388,128.751578004728));
#176973=CARTESIAN_POINT('Ctrl Pts',(-2.99284322070105,5.34347731457243,
135.323742291973));
#176974=CARTESIAN_POINT('Ctrl Pts',(-2.7143955968881,-0.914003788003028,
137.74281560451));
#176975=CARTESIAN_POINT('Ctrl Pts',(-2.48790670352819,-5.32063620302637,
134.524174883853));
#176976=CARTESIAN_POINT('Ctrl Pts',(-2.35423368477254,-5.91003297744418,
131.677416134064));
#176977=CARTESIAN_POINT('Ctrl Pts',(-2.31337654062121,-5.90751142670208,
130.806309852799));
#176978=CARTESIAN_POINT('',(-0.563374439001446,-5.91502852340845,130.79899021336));
#176979=CARTESIAN_POINT('Ctrl Pts',(-2.31337519220432,-5.91674968734432,
130.80628410681));
#176980=CARTESIAN_POINT('Ctrl Pts',(-2.3057930075727,-5.91680232326788,
130.644373357754));
#176981=CARTESIAN_POINT('Ctrl Pts',(-2.29821082294107,-5.91020461859756,
130.482517862187));
#176982=CARTESIAN_POINT('Ctrl Pts',(-2.29062863830944,-5.89699648063777,
130.321283946792));
#176983=CARTESIAN_POINT('Ctrl Pts',(-2.28304210500759,-5.88378076731029,
130.159957557637));
#176984=CARTESIAN_POINT('Ctrl Pts',(-2.27545557170574,-5.86394708961438,
129.999253804566));
#176985=CARTESIAN_POINT('Ctrl Pts',(-2.26786903840389,-5.83758710464856,
129.839732524392));
#176986=CARTESIAN_POINT('Ctrl Pts',(-2.26027699856307,-5.81120798679575,
129.680095458771));
#176987=CARTESIAN_POINT('Ctrl Pts',(-2.25268495872227,-5.77829317310447,
129.521642918593));
#176988=CARTESIAN_POINT('Ctrl Pts',(-2.24509291888145,-5.73898519239538,
129.364923392826));
#176989=CARTESIAN_POINT('Ctrl Pts',(-2.23748852633052,-5.6996132552133,
129.207948874869));
#176990=CARTESIAN_POINT('Ctrl Pts',(-2.22988413377958,-5.65382744716086,
129.052713342816));
#176991=CARTESIAN_POINT('Ctrl Pts',(-2.22227974122865,-5.60182027501037,
128.899750376865));
#176992=CARTESIAN_POINT('Ctrl Pts',(-2.2146688457404,-5.54976862864605,
128.746656603808));
#176993=CARTESIAN_POINT('Ctrl Pts',(-2.20705795025213,-5.49148513093914,
128.595839595603));
#176994=CARTESIAN_POINT('Ctrl Pts',(-2.19944705476388,-5.4272100320278,
128.447811905836));
#176995=CARTESIAN_POINT('Ctrl Pts',(-2.191821899877,-5.36281451045945,128.299506878686));
#176996=CARTESIAN_POINT('Ctrl Pts',(-2.18419674499019,-5.29240509848426,
128.154001928447));
#176997=CARTESIAN_POINT('Ctrl Pts',(-2.17657159010332,-5.21626825515832,
128.011785452467));
#176998=CARTESIAN_POINT('Ctrl Pts',(-2.170214509823,-5.15279308219536,127.89321978811));
#176999=CARTESIAN_POINT('Ctrl Pts',(-2.16385742954263,-5.08533789991428,
127.776939382873));
#177000=CARTESIAN_POINT('Ctrl Pts',(-2.15750034926231,-5.01409095860777,
127.663210761015));
#177001=CARTESIAN_POINT('Ctrl Pts',(-2.15007708285687,-4.93089474233096,
127.530407992961));
#177002=CARTESIAN_POINT('Ctrl Pts',(-2.14265381645139,-4.84229297604232,
127.400711986189));
#177003=CARTESIAN_POINT('Ctrl Pts',(-2.13523055004595,-4.7485443720732,
127.274593357682));
#177004=CARTESIAN_POINT('Ctrl Pts',(-2.12781605732493,-4.65490657116863,
127.148623790919));
#177005=CARTESIAN_POINT('Ctrl Pts',(-2.12040156460396,-4.55613426162116,
127.026223482906));
#177006=CARTESIAN_POINT('Ctrl Pts',(-2.11298707188294,-4.45253099752081,
126.907836746394));
#177007=CARTESIAN_POINT('Ctrl Pts',(-2.10557972552916,-4.349027590147,126.789564115475));
#177008=CARTESIAN_POINT('Ctrl Pts',(-2.09817237917537,-4.24070274209709,
126.675297633804));
#177009=CARTESIAN_POINT('Ctrl Pts',(-2.09076503282159,-4.12790201220618,
126.565450906317));
#177010=CARTESIAN_POINT('Ctrl Pts',(-2.08336321114618,-4.01518541335518,
126.455686106663));
#177011=CARTESIAN_POINT('Ctrl Pts',(-2.07596138947079,-3.89799984592126,
126.350334756892));
#177012=CARTESIAN_POINT('Ctrl Pts',(-2.06855956779538,-3.77672959920243,
126.249775664246));
#177013=CARTESIAN_POINT('Ctrl Pts',(-2.06116165348401,-3.65552337010287,
126.149269655962));
#177014=CARTESIAN_POINT('Ctrl Pts',(-2.0537637391726,-3.53023704266339,
126.053551104272));
#177015=CARTESIAN_POINT('Ctrl Pts',(-2.04636582486123,-3.40128995994975,
125.962960285963));
#177016=CARTESIAN_POINT('Ctrl Pts',(-2.03896913994901,-3.27236430590211,
125.872384522205));
#177017=CARTESIAN_POINT('Ctrl Pts',(-2.03157245503679,-3.13977940913043,
125.786935014975));
#177018=CARTESIAN_POINT('Ctrl Pts',(-2.02417577012457,-3.00398582290172,
125.706910300171));
#177019=CARTESIAN_POINT('Ctrl Pts',(-2.0167794131891,-2.86819825790272,
125.626889133748));
#177020=CARTESIAN_POINT('Ctrl Pts',(-2.00938305625366,-2.72920260794733,
125.552292471002));
#177021=CARTESIAN_POINT('Ctrl Pts',(-2.00198669931819,-2.58747616329207,
125.483374086208));
#177022=CARTESIAN_POINT('Ctrl Pts',(-1.99458920998161,-2.44572801995653,
125.414445149833));
#177023=CARTESIAN_POINT('Ctrl Pts',(-1.98719172064502,-2.30124858517679,
125.351196385678));
#177024=CARTESIAN_POINT('Ctrl Pts',(-1.97979423130843,-2.15453722444724,
125.293834334989));
#177025=CARTESIAN_POINT('Ctrl Pts',(-1.97239414879345,-2.00777443427803,
125.236452176123));
#177026=CARTESIAN_POINT('Ctrl Pts',(-1.96499406627848,-1.85877850786164,
125.184960975141));
#177027=CARTESIAN_POINT('Ctrl Pts',(-1.9575939837635,-1.70806599298024,
125.139518066698));
#177028=CARTESIAN_POINT('Ctrl Pts',(-1.95018576409703,-1.55718775419468,
125.094025189105));
#177029=CARTESIAN_POINT('Ctrl Pts',(-1.94277754443058,-1.40458951497581,
125.054593993804));
#177030=CARTESIAN_POINT('Ctrl Pts',(-1.93536932476411,-1.25080081208395,
125.021331317019));
#177031=CARTESIAN_POINT('Ctrl Pts',(-1.92795654546203,-1.09691745481113,
124.98804816761));
#177032=CARTESIAN_POINT('Ctrl Pts',(-1.92054376615991,-0.941842540717448,
124.960941166087));
#177033=CARTESIAN_POINT('Ctrl Pts',(-1.91313098685782,-0.786112328983106,
124.940065436667));
#177034=CARTESIAN_POINT('Ctrl Pts',(-1.90570761582904,-0.630159602619215,
124.919159879025));
#177035=CARTESIAN_POINT('Ctrl Pts',(-1.89828424480029,-0.473550079262816,
124.904503410531));
#177036=CARTESIAN_POINT('Ctrl Pts',(-1.89086087377152,-0.316822461589335,
124.896099105892));
#177037=CARTESIAN_POINT('Ctrl Pts',(-1.88692482433083,-0.233721718073758,
124.891642941914));
#177038=CARTESIAN_POINT('Ctrl Pts',(-1.88298877489015,-0.150587741872396,
124.888943614882));
#177039=CARTESIAN_POINT('Ctrl Pts',(-1.87905272544947,-0.0675003028066515,
124.887995663338));
#177040=CARTESIAN_POINT('Ctrl Pts',(-1.87162945904403,0.0892000142053658,
124.886207856309));
#177041=CARTESIAN_POINT('Ctrl Pts',(-1.86420619263863,0.246208356781524,
124.890647171959));
#177042=CARTESIAN_POINT('Ctrl Pts',(-1.85678292623319,0.402988941192107,
124.901350328249));
#177043=CARTESIAN_POINT('Ctrl Pts',(-1.84936843351219,0.559584223971734,
124.912040834298));
#177044=CARTESIAN_POINT('Ctrl Pts',(-1.84195394079111,0.715951915618239,
124.928980419423));
#177045=CARTESIAN_POINT('Ctrl Pts',(-1.8345394480701,0.871554124829254,
124.952153856865));
#177046=CARTESIAN_POINT('Ctrl Pts',(-1.82713210171632,1.02700635877293,
124.975304958876));
#177047=CARTESIAN_POINT('Ctrl Pts',(-1.81972475536254,1.18169421235017,
125.004677897003));
#177048=CARTESIAN_POINT('Ctrl Pts',(-1.81231740900876,1.33508292502333,
125.04020550638));
#177049=CARTESIAN_POINT('Ctrl Pts',(-1.80491558733332,1.4883572346082,125.075706617926));
#177050=CARTESIAN_POINT('Ctrl Pts',(-1.79751376565783,1.64033397049057,
125.117353176775));
#177051=CARTESIAN_POINT('Ctrl Pts',(-1.7901119439824,1.79048671365771,125.165026624024));
#177052=CARTESIAN_POINT('Ctrl Pts',(-1.78271402967108,1.94056019235902,
125.212674904831));
#177053=CARTESIAN_POINT('Ctrl Pts',(-1.77531611535977,2.08881124105536,
125.266343625154));
#177054=CARTESIAN_POINT('Ctrl Pts',(-1.76791820104845,2.2347269100769,125.325863907712));
#177055=CARTESIAN_POINT('Ctrl Pts',(-1.76052151613624,2.38061833056206,
125.38537429908));
#177056=CARTESIAN_POINT('Ctrl Pts',(-1.75312483122411,2.52417479632223,
125.450734181854));
#177057=CARTESIAN_POINT('Ctrl Pts',(-1.7457281463119,2.66490160560296,125.521725858759));
#177058=CARTESIAN_POINT('Ctrl Pts',(-1.73833178937645,2.8056221749097,125.592714387819));
#177059=CARTESIAN_POINT('Ctrl Pts',(-1.73093543244098,2.94351300392341,
125.669334046348));
#177060=CARTESIAN_POINT('Ctrl Pts',(-1.72353907550553,3.07810259811792,
125.751320447732));
#177061=CARTESIAN_POINT('Ctrl Pts',(-1.71614158616895,3.2127127983229,125.833319401442));
#177062=CARTESIAN_POINT('Ctrl Pts',(-1.70874409683235,3.34402043850989,
125.92068653983));
#177063=CARTESIAN_POINT('Ctrl Pts',(-1.70134660749576,3.47158183043043,
126.01311337315));
#177064=CARTESIAN_POINT('Ctrl Pts',(-1.69394652498075,3.59918793879934,
126.105572606553));
#177065=CARTESIAN_POINT('Ctrl Pts',(-1.6865464424657,3.7230448821481,126.203094847359));
#177066=CARTESIAN_POINT('Ctrl Pts',(-1.67914635995069,3.84274108368343,
126.305330552511));
#177067=CARTESIAN_POINT('Ctrl Pts',(-1.67173814028423,3.96256890349707,
126.40767867633));
#177068=CARTESIAN_POINT('Ctrl Pts',(-1.6643299206178,4.07822656056999,126.514750372571));
#177069=CARTESIAN_POINT('Ctrl Pts',(-1.65692170095133,4.18933794300868,
126.626157874547));
#177070=CARTESIAN_POINT('Ctrl Pts',(-1.64950892164925,4.30051771264958,
126.737633945983));
#177071=CARTESIAN_POINT('Ctrl Pts',(-1.64209614234712,4.40714537972399,
126.853450866711));
#177072=CARTESIAN_POINT('Ctrl Pts',(-1.63468336304504,4.50888470548128,
126.973187262682));
#177073=CARTESIAN_POINT('Ctrl Pts',(-1.62725999201627,4.61076940115831,
127.09309474363));
#177074=CARTESIAN_POINT('Ctrl Pts',(-1.61983662098756,4.70775157596957,
127.216932591816));
#177075=CARTESIAN_POINT('Ctrl Pts',(-1.61241324995879,4.79953746112196,
127.344249243378));
#177076=CARTESIAN_POINT('Ctrl Pts',(-1.60847720051802,4.8482045398015,127.411755586956));
#177077=CARTESIAN_POINT('Ctrl Pts',(-1.60454115107726,4.89541150488017,
127.480239503417));
#177078=CARTESIAN_POINT('Ctrl Pts',(-1.60060510163649,4.94111983370151,
127.549630928098));
#177079=CARTESIAN_POINT('Ctrl Pts',(-1.59318183523107,5.02732431535081,
127.680500989416));
#177080=CARTESIAN_POINT('Ctrl Pts',(-1.5857585688257,5.10845623767103,127.814996113277));
#177081=CARTESIAN_POINT('Ctrl Pts',(-1.57833530242027,5.18419510460719,
127.952685376613));
#177082=CARTESIAN_POINT('Ctrl Pts',(-1.57092080969925,5.25984445449256,
128.090211902674));
#177083=CARTESIAN_POINT('Ctrl Pts',(-1.56350631697814,5.33011325860168,
128.230924729751));
#177084=CARTESIAN_POINT('Ctrl Pts',(-1.55609182425712,5.39472358424925,
128.374363084225));
#177085=CARTESIAN_POINT('Ctrl Pts',(-1.54868447790336,5.45927163603234,
128.517663187412));
#177086=CARTESIAN_POINT('Ctrl Pts',(-1.54127713154963,5.51817191462117,
128.663683250145));
#177087=CARTESIAN_POINT('Ctrl Pts',(-1.53386978519586,5.57119187658512,
128.811937058989));
#177088=CARTESIAN_POINT('Ctrl Pts',(-1.52646796352046,5.62417229426118,
128.96008029455));
#177089=CARTESIAN_POINT('Ctrl Pts',(-1.51906614184496,5.67128100279193,
129.110453608984));
#177090=CARTESIAN_POINT('Ctrl Pts',(-1.51166432016956,5.71233320680563,
129.262550027083));
#177091=CARTESIAN_POINT('Ctrl Pts',(-1.50426640585821,5.75336373968031,
129.414566154667));
#177092=CARTESIAN_POINT('Ctrl Pts',(-1.49686849154693,5.78834403834904,
129.56830321489));
#177093=CARTESIAN_POINT('Ctrl Pts',(-1.48947057723558,5.81713892222552,
129.723238366371));
#177094=CARTESIAN_POINT('Ctrl Pts',(-1.48207389232338,5.84592902091465,
129.878147770441));
#177095=CARTESIAN_POINT('Ctrl Pts',(-1.47467720741118,5.86853567675316,
130.034254503959));
#177096=CARTESIAN_POINT('Ctrl Pts',(-1.46728052249898,5.88487464624398,
130.191024689632));
#177097=CARTESIAN_POINT('Ctrl Pts',(-1.45988416556353,5.90121289124782,
130.347787923951));
#177098=CARTESIAN_POINT('Ctrl Pts',(-1.45248780862806,5.911283963798,130.505214180646));
#177099=CARTESIAN_POINT('Ctrl Pts',(-1.4450914516926,5.91505544553447,130.662763870594));
#177100=CARTESIAN_POINT('Ctrl Pts',(-1.43769396235606,5.91882750469441,
130.820337681801));
#177101=CARTESIAN_POINT('Ctrl Pts',(-1.43029647301953,5.91629804369174,
130.978034590675));
#177102=CARTESIAN_POINT('Ctrl Pts',(-1.42289898368298,5.90748677934887,
131.135314563483));
#177103=CARTESIAN_POINT('Ctrl Pts',(-1.41549890116797,5.89867242623088,
131.292649670544));
#177104=CARTESIAN_POINT('Ctrl Pts',(-1.40809881865298,5.88357190632204,
131.449567178063));
#177105=CARTESIAN_POINT('Ctrl Pts',(-1.40069873613797,5.86225683278428,
131.605531878268));
#177106=CARTESIAN_POINT('Ctrl Pts',(-1.3932905164715,5.84091832113198,131.761668077693));
#177107=CARTESIAN_POINT('Ctrl Pts',(-1.38588229680507,5.81335165939988,
131.916849007374));
#177108=CARTESIAN_POINT('Ctrl Pts',(-1.37847407713861,5.77967978901732,
132.070548636355));
#177109=CARTESIAN_POINT('Ctrl Pts',(-1.37106129783653,5.74598719416029,
132.224342864894));
#177110=CARTESIAN_POINT('Ctrl Pts',(-1.36364851853442,5.70618199722547,
132.376653615695));
#177111=CARTESIAN_POINT('Ctrl Pts',(-1.35623573923235,5.6604369668774,132.526970238608));
#177112=CARTESIAN_POINT('Ctrl Pts',(-1.34881236820361,5.61462657388495,
132.677501640961));
#177113=CARTESIAN_POINT('Ctrl Pts',(-1.34138899717489,5.56285951934267,
132.826032873159));
#177114=CARTESIAN_POINT('Ctrl Pts',(-1.33396562614615,5.50535692750925,
132.9720726979));
#177115=CARTESIAN_POINT('Ctrl Pts',(-1.3300295767053,5.47486767356284,133.049506517156));
#177116=CARTESIAN_POINT('Ctrl Pts',(-1.32609352726445,5.44276673279752,
133.126240303509));
#177117=CARTESIAN_POINT('Ctrl Pts',(-1.32215747782359,5.40909223016113,
133.202203775095));
#177118=CARTESIAN_POINT('Ctrl Pts',(-1.31473421141816,5.34558316913515,
133.345468511766));
#177119=CARTESIAN_POINT('Ctrl Pts',(-1.30731094501272,5.27628239810198,
133.486424995463));
#177120=CARTESIAN_POINT('Ctrl Pts',(-1.29988767860729,5.2013792288988,133.624570659332));
#177121=CARTESIAN_POINT('Ctrl Pts',(-1.29247318588628,5.1265645890212,133.7625530465));
#177122=CARTESIAN_POINT('Ctrl Pts',(-1.2850586931653,5.04616090743831,133.89773090165));
#177123=CARTESIAN_POINT('Ctrl Pts',(-1.27764420044429,4.96040561664195,
134.029621332747));
#177124=CARTESIAN_POINT('Ctrl Pts',(-1.27023685409053,4.87473298002385,
134.161384642879));
#177125=CARTESIAN_POINT('Ctrl Pts',(-1.26282950773677,4.78371920504016,
134.289866526044));
#177126=CARTESIAN_POINT('Ctrl Pts',(-1.25542216138302,4.68764766141966,
134.414608526628));
#177127=CARTESIAN_POINT('Ctrl Pts',(-1.24802033970763,4.59164777158069,
134.539257489922));
#177128=CARTESIAN_POINT('Ctrl Pts',(-1.24061851803223,4.49059785100919,
134.660171830121));
#177129=CARTESIAN_POINT('Ctrl Pts',(-1.23321669635683,4.38482454589331,
134.776922041161));
#177130=CARTESIAN_POINT('Ctrl Pts',(-1.22581878204542,4.27910707768095,
134.893610620674));
#177131=CARTESIAN_POINT('Ctrl Pts',(-1.21842086773407,4.1686714407265,135.006139172925));
#177132=CARTESIAN_POINT('Ctrl Pts',(-1.21102295342266,4.05388444788204,
135.114111358122));
#177133=CARTESIAN_POINT('Ctrl Pts',(-1.20362626851044,3.93911653055418,
135.222065600299));
#177134=CARTESIAN_POINT('Ctrl Pts',(-1.19622958359819,3.81999896415178,
135.325464722696));
#177135=CARTESIAN_POINT('Ctrl Pts',(-1.18883289868597,3.69693537909345,
135.423949275153));
#177136=CARTESIAN_POINT('Ctrl Pts',(-1.18143654175054,3.57387725080378,
135.522429460702));
#177137=CARTESIAN_POINT('Ctrl Pts',(-1.17404018481509,3.44687374321637,
135.615995276359));
#177138=CARTESIAN_POINT('Ctrl Pts',(-1.16664382787965,3.31636130502646,
135.70432778654));
#177139=CARTESIAN_POINT('Ctrl Pts',(-1.15924633854305,3.18582888504832,
135.792673820654));
#177140=CARTESIAN_POINT('Ctrl Pts',(-1.15184884920649,3.05178677394595,
135.875784744682));
#177141=CARTESIAN_POINT('Ctrl Pts',(-1.14445135986989,2.91469997481603,
135.953385245523));
#177142=CARTESIAN_POINT('Ctrl Pts',(-1.13705127735488,2.77756512012139,
136.031012949099));
#177143=CARTESIAN_POINT('Ctrl Pts',(-1.12965119483986,2.63738377704964,
136.103126199768));
#177144=CARTESIAN_POINT('Ctrl Pts',(-1.12225111232485,2.49464493972069,
136.169495954836));
#177145=CARTESIAN_POINT('Ctrl Pts',(-1.11484289265838,2.35174914636659,
136.235938690273));
#177146=CARTESIAN_POINT('Ctrl Pts',(-1.10743467299194,2.20629058125491,
136.296625160027));
#177147=CARTESIAN_POINT('Ctrl Pts',(-1.10002645332548,2.0587782619703,136.351374465623));
#177148=CARTESIAN_POINT('Ctrl Pts',(-1.09261367402341,1.91117515131413,
136.406157468504));
#177149=CARTESIAN_POINT('Ctrl Pts',(-1.0852008947213,1.76151612176115,136.454995910186));
#177150=CARTESIAN_POINT('Ctrl Pts',(-1.07778811541922,1.6103241834286,136.49775912696));
#177151=CARTESIAN_POINT('Ctrl Pts',(-1.07036474439047,1.45891621496458,
136.540583445823));
#177152=CARTESIAN_POINT('Ctrl Pts',(-1.06294137336175,1.30597132523184,
136.577315115797));
#177153=CARTESIAN_POINT('Ctrl Pts',(-1.055518002333,1.15202232914964,136.607874649223));
#177154=CARTESIAN_POINT('Ctrl Pts',(-1.05158195289228,1.07039487747272,
136.624078047111));
#177155=CARTESIAN_POINT('Ctrl Pts',(-1.04764590345148,0.988485227210227,
136.638547102349));
#177156=CARTESIAN_POINT('Ctrl Pts',(-1.04370985401076,0.906373115949746,
136.651275901473));
#177157=CARTESIAN_POINT('Ctrl Pts',(-1.03628658760532,0.751512236741009,
136.675282019368));
#177158=CARTESIAN_POINT('Ctrl Pts',(-1.02886332119983,0.595462795402828,
136.693167740489));
#177159=CARTESIAN_POINT('Ctrl Pts',(-1.0214400547944,0.438749943334577,
136.704820688588));
#177160=CARTESIAN_POINT('Ctrl Pts',(-1.01402556207338,0.282222312843054,
136.716459863869));
#177161=CARTESIAN_POINT('Ctrl Pts',(-1.00661106935241,0.125033201004514,
136.721880902015));
#177162=CARTESIAN_POINT('Ctrl Pts',(-0.999196576631391,-0.0322827833728939,
136.721022546762));
#177163=CARTESIAN_POINT('Ctrl Pts',(-0.991789230277595,-0.189447140681941,
136.720165018825));
#177164=CARTESIAN_POINT('Ctrl Pts',(-0.984381883923756,-0.346737756299064,
136.713040148482));
#177165=CARTESIAN_POINT('Ctrl Pts',(-0.976974537569959,-0.503615750273477,
136.699638536255));
#177166=CARTESIAN_POINT('Ctrl Pts',(-0.969572715894546,-0.660376738721094,
136.686246919456));
#177167=CARTESIAN_POINT('Ctrl Pts',(-0.962170894219245,-0.816725347952993,
136.66658791377));
#177168=CARTESIAN_POINT('Ctrl Pts',(-0.954769072543826,-0.972123662110491,
136.64070417737));
#177169=CARTESIAN_POINT('Ctrl Pts',(-0.94737115823238,-1.12743994270911,
136.614834104792));
#177170=CARTESIAN_POINT('Ctrl Pts',(-0.939973243920947,-1.28180656000724,
136.582745906877));
#177171=CARTESIAN_POINT('Ctrl Pts',(-0.932575329609506,-1.43469179080562,
136.544533962326));
#177172=CARTESIAN_POINT('Ctrl Pts',(-0.925178644697286,-1.58755161485074,
136.506328367908));
#177173=CARTESIAN_POINT('Ctrl Pts',(-0.917781959785012,-1.73893017918694,
136.462001137028));
#177174=CARTESIAN_POINT('Ctrl Pts',(-0.910385274872795,-1.88830689611621,
136.411697563798));
#177175=CARTESIAN_POINT('Ctrl Pts',(-0.902988917937337,-2.03767698952532,
136.361396221082));
#177176=CARTESIAN_POINT('Ctrl Pts',(-0.895592561001907,-2.18504505824414,
136.305119182057));
#177177=CARTESIAN_POINT('Ctrl Pts',(-0.888196204066446,-2.32990686155138,
136.243061250897));
#177178=CARTESIAN_POINT('Ctrl Pts',(-0.880798714729856,-2.47479084357051,
136.18099381851));
#177179=CARTESIAN_POINT('Ctrl Pts',(-0.873401225393216,-2.6171674529902,
136.113143878704));
#177180=CARTESIAN_POINT('Ctrl Pts',(-0.866003736056626,-2.75655371556865,
136.039753838298));
#177181=CARTESIAN_POINT('Ctrl Pts',(-0.858603653541681,-2.89598883978418,
135.966338071128));
#177182=CARTESIAN_POINT('Ctrl Pts',(-0.851203571026781,-3.03243119997379,
135.887378510511));
#177183=CARTESIAN_POINT('Ctrl Pts',(-0.843803488511838,-3.16542378276714,
135.803162757878));
#177184=CARTESIAN_POINT('Ctrl Pts',(-0.836395268845371,-3.29856260457818,
135.718854401368));
#177185=CARTESIAN_POINT('Ctrl Pts',(-0.828987049178865,-3.42824375777772,
135.62927851019));
#177186=CARTESIAN_POINT('Ctrl Pts',(-0.82157882951239,-3.55403991091922,
135.534765555211));
#177187=CARTESIAN_POINT('Ctrl Pts',(-0.814166050210334,-3.67991348949378,
135.440194429085));
#177188=CARTESIAN_POINT('Ctrl Pts',(-0.806753270908295,-3.80189701475527,
135.340680419632));
#177189=CARTESIAN_POINT('Ctrl Pts',(-0.799340491606245,-3.91959785588101,
135.236592923151));
#177190=CARTESIAN_POINT('Ctrl Pts',(-0.791917120577471,-4.03746687348868,
135.132356701573));
#177191=CARTESIAN_POINT('Ctrl Pts',(-0.78449374954874,-4.15104071652076,
135.023534199059));
#177192=CARTESIAN_POINT('Ctrl Pts',(-0.777070378519966,-4.25996451027873,
134.910530722867));
#177193=CARTESIAN_POINT('Ctrl Pts',(-0.773134329079252,-4.31771851931851,
134.85061356831));
#177194=CARTESIAN_POINT('Ctrl Pts',(-0.769198279638492,-4.37416591199664,
134.789521537525));
#177195=CARTESIAN_POINT('Ctrl Pts',(-0.765262230197777,-4.42925861303343,
134.72731851963));
#177196=CARTESIAN_POINT('Ctrl Pts',(-0.757905128544479,-4.53223562284684,
134.611051198123));
#177197=CARTESIAN_POINT('Ctrl Pts',(-0.750548026891183,-4.63080249576435,
134.490533175901));
#177198=CARTESIAN_POINT('Ctrl Pts',(-0.743190925237883,-4.72458291754208,
134.366136413117));
#177199=CARTESIAN_POINT('Ctrl Pts',(-0.735698603028151,-4.8200869855888,
134.239453288083));
#177200=CARTESIAN_POINT('Ctrl Pts',(-0.728206280818478,-4.91062661734549,
134.108747682586));
#177201=CARTESIAN_POINT('Ctrl Pts',(-0.720713958608741,-4.99584315379781,
133.974452374148));
#177202=CARTESIAN_POINT('Ctrl Pts',(-0.71337486278037,-5.07931691662832,
133.842903555193));
#177203=CARTESIAN_POINT('Ctrl Pts',(-0.706035766951913,-5.15768296477155,
133.707910767536));
#177204=CARTESIAN_POINT('Ctrl Pts',(-0.698696671123543,-5.23064471034456,
133.569914174568));
#177205=CARTESIAN_POINT('Ctrl Pts',(-0.691362564756517,-5.30355685310305,
133.432011398151));
#177206=CARTESIAN_POINT('Ctrl Pts',(-0.68402845838953,-5.37107182671326,
133.291109214693));
#177207=CARTESIAN_POINT('Ctrl Pts',(-0.676694352022508,-5.43293719121724,
133.147675372094));
#177208=CARTESIAN_POINT('Ctrl Pts',(-0.669363719094841,-5.4947732562291,
133.004309459891));
#177209=CARTESIAN_POINT('Ctrl Pts',(-0.66203308616718,-5.55096488716106,
132.858414623623));
#177210=CARTESIAN_POINT('Ctrl Pts',(-0.654702453239508,-5.60130642736868,
132.710481513317));
#177211=CARTESIAN_POINT('Ctrl Pts',(-0.647091848153241,-5.6535706159776,
132.556898529033));
#177212=CARTESIAN_POINT('Ctrl Pts',(-0.639481243066946,-5.69952882857686,
132.401118882871));
#177213=CARTESIAN_POINT('Ctrl Pts',(-0.631870637980683,-5.73900659669919,
132.243712501416));
#177214=CARTESIAN_POINT('Ctrl Pts',(-0.624540907355159,-5.77702741143781,
132.092115307537));
#177215=CARTESIAN_POINT('Ctrl Pts',(-0.617211176729692,-5.80903751536817,
131.939009708147));
#177216=CARTESIAN_POINT('Ctrl Pts',(-0.609881446104168,-5.83493256653342,
131.784917860417));
#177217=CARTESIAN_POINT('Ctrl Pts',(-0.60255090713329,-5.86083047348497,
131.630809018962));
#177218=CARTESIAN_POINT('Ctrl Pts',(-0.595220368162337,-5.88061192932304,
131.475714089102));
#177219=CARTESIAN_POINT('Ctrl Pts',(-0.587889829191454,-5.8942242033676,
131.320162520369));
#177220=CARTESIAN_POINT('Ctrl Pts',(-0.580555320412306,-5.9078438490554,
131.164526713642));
#177221=CARTESIAN_POINT('Ctrl Pts',(-0.57322081163314,-5.91528762124507,
131.008434154064));
#177222=CARTESIAN_POINT('Ctrl Pts',(-0.565886302853983,-5.91655484099832,
130.852416584515));
#177223=CARTESIAN_POINT('Ctrl Pts',(-0.565049265970727,-5.9166994600457,
130.83461137573));
#177224=CARTESIAN_POINT('Ctrl Pts',(-0.564212229087517,-5.91676369097117,
130.816807141521));
#177225=CARTESIAN_POINT('Ctrl Pts',(-0.563375192204262,-5.91674757584986,
130.79900466996));
#177226=CARTESIAN_POINT('',(1.18662480779564,-5.92210060015532,130.804726096251));
#177227=CARTESIAN_POINT('Ctrl Pts',(-0.563374100425627,-5.91425578389467,
130.798983714904));
#177228=CARTESIAN_POINT('Ctrl Pts',(-0.537854269078733,-5.91899404643966,
130.256440525358));
#177229=CARTESIAN_POINT('Ctrl Pts',(-0.419518563127545,-5.60142465403446,
127.746111889883));
#177230=CARTESIAN_POINT('Ctrl Pts',(-0.2083669825721,-2.04259833657134,
124.110680571));
#177231=CARTESIAN_POINT('Ctrl Pts',(0.0700806412408244,4.5275083038907,
125.467767220224));
#177232=CARTESIAN_POINT('Ctrl Pts',(0.348528265053751,6.93705599415352,
131.728922494524));
#177233=CARTESIAN_POINT('Ctrl Pts',(0.626975888866651,2.97178811981426,
137.140450571258));
#177234=CARTESIAN_POINT('Ctrl Pts',(0.905423512679459,-3.72440785671249,
136.72942151575));
#177235=CARTESIAN_POINT('Ctrl Pts',(1.09197315232256,-5.91763069388933,
132.806204183693));
#177236=CARTESIAN_POINT('Ctrl Pts',(1.18570691736122,-5.92652215037093,
130.824135984152));
#177237=CARTESIAN_POINT('Ctrl Pts',(1.18662480779563,-5.92650486509969,
130.804726368057));
#177238=CARTESIAN_POINT('',(2.93662479004875,-5.91447619583082,130.809538251585));
#177239=CARTESIAN_POINT('Ctrl Pts',(1.18662480779565,-5.91674998873255,
130.804725766041));
#177240=CARTESIAN_POINT('Ctrl Pts',(1.1940350854322,-5.91675964326844,130.648286730755));
#177241=CARTESIAN_POINT('Ctrl Pts',(1.20144536306876,-5.91056063453475,
130.491606878693));
#177242=CARTESIAN_POINT('Ctrl Pts',(1.20885564070531,-5.89812159424516,
130.335220742903));
#177243=CARTESIAN_POINT('Ctrl Pts',(1.21625716100478,-5.88569725419679,
130.179019421525));
#177244=CARTESIAN_POINT('Ctrl Pts',(1.2236586813042,-5.86704758979576,130.023111495431));
#177245=CARTESIAN_POINT('Ctrl Pts',(1.23106020160367,-5.84219319642566,
129.868033101075));
#177246=CARTESIAN_POINT('Ctrl Pts',(1.23845460439431,-5.817362703735,129.713103834439));
#177247=CARTESIAN_POINT('Ctrl Pts',(1.24584900718498,-5.78633941867362,
129.559002879114));
#177248=CARTESIAN_POINT('Ctrl Pts',(1.25324340997562,-5.74919584151621,
129.40626271742));
#177249=CARTESIAN_POINT('Ctrl Pts',(1.2606323293674,-5.71207980857768,129.253635821835));
#177250=CARTESIAN_POINT('Ctrl Pts',(1.26802124875918,-5.66885260811299,
129.102368073306));
#177251=CARTESIAN_POINT('Ctrl Pts',(1.27541016815096,-5.61963804525913,
128.952983075632));
#177252=CARTESIAN_POINT('Ctrl Pts',(1.28279523383285,-5.57044915038689,
128.803675990088));
#177253=CARTESIAN_POINT('Ctrl Pts',(1.29018029951475,-5.51527922885192,
128.656250054947));
#177254=CARTESIAN_POINT('Ctrl Pts',(1.29756536519665,-5.45430225584897,
128.51121486024));
#177255=CARTESIAN_POINT('Ctrl Pts',(1.30494927592191,-5.39333481908606,
128.366202347709));
#177256=CARTESIAN_POINT('Ctrl Pts',(1.31233318664717,-5.32656227780676,
128.223580178958));
#177257=CARTESIAN_POINT('Ctrl Pts',(1.31971709737243,-5.2542072203174,128.083839151291));
#177258=CARTESIAN_POINT('Ctrl Pts',(1.3271007517007,-5.18185467526619,127.944102975955));
#177259=CARTESIAN_POINT('Ctrl Pts',(1.33448440602898,-5.10392017165668,
127.807248075647));
#177260=CARTESIAN_POINT('Ctrl Pts',(1.34186806035726,-5.02067271393934,
127.673741499563));
#177261=CARTESIAN_POINT('Ctrl Pts',(1.34925292985532,-4.93741155571667,
127.540212951547));
#177262=CARTESIAN_POINT('Ctrl Pts',(1.35663779935341,-4.84883590086788,
127.410034142876));
#177263=CARTESIAN_POINT('Ctrl Pts',(1.36402266885148,-4.75525851876446,
127.283643789672));
#177264=CARTESIAN_POINT('Ctrl Pts',(1.37141022555093,-4.66164708578567,
127.15720744563));
#177265=CARTESIAN_POINT('Ctrl Pts',(1.37879778225042,-4.56303052504015,
127.034562602469));
#177266=CARTESIAN_POINT('Ctrl Pts',(1.38618533894987,-4.45976225609666,
126.916115360179));
#177267=CARTESIAN_POINT('Ctrl Pts',(1.39358103742541,-4.35638017589496,
126.797537577986));
#177268=CARTESIAN_POINT('Ctrl Pts',(1.40097673590085,-4.24833639680506,
126.683166916957));
#177269=CARTESIAN_POINT('Ctrl Pts',(1.40837243437639,-4.13602208551581,
126.57337351399));
#177270=CARTESIAN_POINT('Ctrl Pts',(1.41577279822131,-4.02363692388693,
126.463510850928));
#177271=CARTESIAN_POINT('Ctrl Pts',(1.42317316206625,-3.90697614011333,
126.358231449219));
#177272=CARTESIAN_POINT('Ctrl Pts',(1.43057352591117,-3.78646397365026,
126.257865138766));
#177273=CARTESIAN_POINT('Ctrl Pts',(1.43798426079176,-3.66578291873755,
126.157358172717));
#177274=CARTESIAN_POINT('Ctrl Pts',(1.44539499567228,-3.54123999963713,
126.061778274154));
#177275=CARTESIAN_POINT('Ctrl Pts',(1.45280573055285,-3.41328899580607,
125.971412366901));
#177276=CARTESIAN_POINT('Ctrl Pts',(1.45597674047032,-3.35853951297656,
125.932745326085));
#177277=CARTESIAN_POINT('Ctrl Pts',(1.45914775038788,-3.30316634952253,
125.895032363853));
#177278=CARTESIAN_POINT('Ctrl Pts',(1.46231876030535,-3.24720637728398,
125.858293361066));
#177279=CARTESIAN_POINT('Ctrl Pts',(1.46974202671077,-3.11620527896578,
125.772288141195));
#177280=CARTESIAN_POINT('Ctrl Pts',(1.4771652931162,-2.9815868418728,125.691360991508));
#177281=CARTESIAN_POINT('Ctrl Pts',(1.48458855952163,-2.84378247631683,
125.615831751896));
#177282=CARTESIAN_POINT('Ctrl Pts',(1.49200305224264,-2.7061409840766,125.540391781573));
#177283=CARTESIAN_POINT('Ctrl Pts',(1.49941754496364,-2.56532138278411,
125.470337199803));
#177284=CARTESIAN_POINT('Ctrl Pts',(1.50683203768466,-2.42178486849296,
125.405945237731));
#177285=CARTESIAN_POINT('Ctrl Pts',(1.51423938403844,-2.27838670009834,
125.341615339057));
#177286=CARTESIAN_POINT('Ctrl Pts',(1.52164673039226,-2.13227717025643,
125.282937346352));
#177287=CARTESIAN_POINT('Ctrl Pts',(1.52905407674604,-1.98394284573079,
125.230143062844));
#177288=CARTESIAN_POINT('Ctrl Pts',(1.53645589842143,-1.83571915454092,
125.177388155304));
#177289=CARTESIAN_POINT('Ctrl Pts',(1.54385772009686,-1.68527432280217,
125.130508343911));
#177290=CARTESIAN_POINT('Ctrl Pts',(1.55125954177225,-1.53311560636215,
125.089687652292));
#177291=CARTESIAN_POINT('Ctrl Pts',(1.5586574560836,-1.38103721332414,125.048888509599));
#177292=CARTESIAN_POINT('Ctrl Pts',(1.56605537039489,-1.22724709706649,
125.014142213072));
#177293=CARTESIAN_POINT('Ctrl Pts',(1.57345328470623,-1.072268304086,124.985583147465));
#177294=CARTESIAN_POINT('Ctrl Pts',(1.58084996961843,-0.917315265769306,
124.957028827857));
#177295=CARTESIAN_POINT('Ctrl Pts',(1.58824665453057,-0.76117430953846,
124.934659766071));
#177296=CARTESIAN_POINT('Ctrl Pts',(1.59564333944277,-0.604379440272201,
124.918559393036));
#177297=CARTESIAN_POINT('Ctrl Pts',(1.60303969637822,-0.447591523454532,
124.902459733909));
#177298=CARTESIAN_POINT('Ctrl Pts',(1.61043605331375,-0.290150122598635,
124.892628248985));
#177299=CARTESIAN_POINT('Ctrl Pts',(1.61783241024921,-0.132594875537374,
124.889096535424));
#177300=CARTESIAN_POINT('Ctrl Pts',(1.62522989958578,0.0249844936342075,
124.885564281149));
#177301=CARTESIAN_POINT('Ctrl Pts',(1.63262738892231,0.182677370488753,
124.888333727073));
#177302=CARTESIAN_POINT('Ctrl Pts',(1.64002487825888,0.339943751926087,
124.897384334557));
#177303=CARTESIAN_POINT('Ctrl Pts',(1.64742496077388,0.497265262849863,
124.906438114718));
#177304=CARTESIAN_POINT('Ctrl Pts',(1.6548250432889,0.654159608239698,124.921777418875));
#177305=CARTESIAN_POINT('Ctrl Pts',(1.6622251258039,0.810091689926226,124.943329819454));
#177306=CARTESIAN_POINT('Ctrl Pts',(1.66963334547036,0.966195234966553,
124.964905919114));
#177307=CARTESIAN_POINT('Ctrl Pts',(1.67704156513685,1.12133403318331,124.992708707882));
#177308=CARTESIAN_POINT('Ctrl Pts',(1.68444978480332,1.27498224132818,125.026614443945));
#177309=CARTESIAN_POINT('Ctrl Pts',(1.6918625641054,1.42872501738185,125.060541048421));
#177310=CARTESIAN_POINT('Ctrl Pts',(1.69927534340744,1.58097501507603,125.100577990297));
#177311=CARTESIAN_POINT('Ctrl Pts',(1.70668812270952,1.73122184777611,125.146551723985));
#177312=CARTESIAN_POINT('Ctrl Pts',(1.71411149373828,1.88168336019642,125.192591147099));
#177313=CARTESIAN_POINT('Ctrl Pts',(1.72153486476699,2.03013563975381,125.244584180947));
#177314=CARTESIAN_POINT('Ctrl Pts',(1.72895823579574,2.17608778622686,125.302308953947));
#177315=CARTESIAN_POINT('Ctrl Pts',(1.73289428523654,2.25347511636075,125.332916013678));
#177316=CARTESIAN_POINT('Ctrl Pts',(1.73683033467736,2.33015996168881,125.365133693031));
#177317=CARTESIAN_POINT('Ctrl Pts',(1.74076638411816,2.40607209844888,125.398923760145));
#177318=CARTESIAN_POINT('Ctrl Pts',(1.74818965052359,2.54924001924134,125.46265077217));
#177319=CARTESIAN_POINT('Ctrl Pts',(1.755612916929,2.69009087573639,125.532165974727));
#177320=CARTESIAN_POINT('Ctrl Pts',(1.76303618333444,2.82812238976302,125.607279291377));
#177321=CARTESIAN_POINT('Ctrl Pts',(1.77045067605546,2.96599076200327,125.682303830325));
#177322=CARTESIAN_POINT('Ctrl Pts',(1.77786516877653,3.10104609990376,125.762913136486));
#177323=CARTESIAN_POINT('Ctrl Pts',(1.78527966149755,3.2328058733188,125.848869042764));
#177324=CARTESIAN_POINT('Ctrl Pts',(1.79268700785134,3.36443865170356,125.934742101503));
#177325=CARTESIAN_POINT('Ctrl Pts',(1.80009435420517,3.49278187861667,126.025951298649));
#177326=CARTESIAN_POINT('Ctrl Pts',(1.80750170055896,3.61737753021731,126.122212567111));
#177327=CARTESIAN_POINT('Ctrl Pts',(1.81490352223436,3.74188025368009,126.218402040287));
#177328=CARTESIAN_POINT('Ctrl Pts',(1.82230534390971,3.86264067308458,126.319635854887));
#177329=CARTESIAN_POINT('Ctrl Pts',(1.82970716558512,3.97922977996487,126.425586711466));
#177330=CARTESIAN_POINT('Ctrl Pts',(1.83710507989642,4.09575734036218,126.531481637412));
#177331=CARTESIAN_POINT('Ctrl Pts',(1.84450299420769,4.20811769806562,126.642088395783));
#177332=CARTESIAN_POINT('Ctrl Pts',(1.85190090851899,4.31591507196789,126.75703957099));
#177333=CARTESIAN_POINT('Ctrl Pts',(1.8592975934312,4.42369453190318,126.871971643398));
#177334=CARTESIAN_POINT('Ctrl Pts',(1.86669427834345,4.52691225790639,126.991246427726));
#177335=CARTESIAN_POINT('Ctrl Pts',(1.87409096325567,4.62520941449318,127.114459747003));
#177336=CARTESIAN_POINT('Ctrl Pts',(1.88148732019112,4.72350221248104,127.237667602871));
#177337=CARTESIAN_POINT('Ctrl Pts',(1.88888367712659,4.81687464207243,127.364813354635));
#177338=CARTESIAN_POINT('Ctrl Pts',(1.89628003406204,4.90500843225194,127.495460068738));
#177339=CARTESIAN_POINT('Ctrl Pts',(1.90367752339863,4.99315571593972,127.626126785186));
#177340=CARTESIAN_POINT('Ctrl Pts',(1.9110750127352,5.07606255445162,127.760295221747));
#177341=CARTESIAN_POINT('Ctrl Pts',(1.91847250207178,5.15345434266035,127.897499956885));
#177342=CARTESIAN_POINT('Ctrl Pts',(1.92587258458679,5.23087326044057,128.03475278893));
#177343=CARTESIAN_POINT('Ctrl Pts',(1.93327266710181,5.30277309546234,128.175043713766));
#177344=CARTESIAN_POINT('Ctrl Pts',(1.94067274961682,5.36892554946398,128.317883389274));
#177345=CARTESIAN_POINT('Ctrl Pts',(1.9480809692833,5.43515074488934,128.46088013169));
#177346=CARTESIAN_POINT('Ctrl Pts',(1.95548918894971,5.49561578119426,128.60643088284));
#177347=CARTESIAN_POINT('Ctrl Pts',(1.96289740861619,5.55014053475337,128.754026350431));
#177348=CARTESIAN_POINT('Ctrl Pts',(1.97031018791826,5.60469884738858,128.90171266057));
#177349=CARTESIAN_POINT('Ctrl Pts',(1.97772296722037,5.6533094769499,129.051445840615));
#177350=CARTESIAN_POINT('Ctrl Pts',(1.98513574652245,5.69584255581191,129.202702682206));
#177351=CARTESIAN_POINT('Ctrl Pts',(1.99255911755121,5.73843640793154,129.354175646665));
#177352=CARTESIAN_POINT('Ctrl Pts',(1.99998248857994,5.77493527928529,129.507176258639));
#177353=CARTESIAN_POINT('Ctrl Pts',(2.0074058596087,5.80526049315837,129.661171582859));
#177354=CARTESIAN_POINT('Ctrl Pts',(2.01134190904947,5.82133964919735,129.742823598827));
#177355=CARTESIAN_POINT('Ctrl Pts',(2.0152779584903,5.83568403513684,129.82475517368));
#177356=CARTESIAN_POINT('Ctrl Pts',(2.01921400793108,5.84828785886529,129.906886560922));
#177357=CARTESIAN_POINT('Ctrl Pts',(2.02663727433653,5.87205827706538,130.061783794029));
#177358=CARTESIAN_POINT('Ctrl Pts',(2.03406054074194,5.88970649679028,130.217860273688));
#177359=CARTESIAN_POINT('Ctrl Pts',(2.04148380714739,5.90112094111124,130.374590678089));
#177360=CARTESIAN_POINT('Ctrl Pts',(2.04889829986839,5.91252189450691,130.531135840167));
#177361=CARTESIAN_POINT('Ctrl Pts',(2.05631279258944,5.9177037113047,130.68833301988));
#177362=CARTESIAN_POINT('Ctrl Pts',(2.06372728531045,5.9166059488978,130.845647515817));
#177363=CARTESIAN_POINT('Ctrl Pts',(2.07113463166422,5.91550924455563,131.00281038612));
#177364=CARTESIAN_POINT('Ctrl Pts',(2.07854197801803,5.90814501292183,131.160089976757));
#177365=CARTESIAN_POINT('Ctrl Pts',(2.0859493243718,5.89450467461231,131.316947394096));
#177366=CARTESIAN_POINT('Ctrl Pts',(2.09335114604718,5.88087450978173,131.473687821256));
#177367=CARTESIAN_POINT('Ctrl Pts',(2.10075296772251,5.86097759089359,131.630006331778));
#177368=CARTESIAN_POINT('Ctrl Pts',(2.1081547893979,5.83485739468559,131.785365075345));
#177369=CARTESIAN_POINT('Ctrl Pts',(2.11555270370928,5.80875098712571,131.940641806242));
#177370=CARTESIAN_POINT('Ctrl Pts',(2.12295061802067,5.77642790665482,132.09495941201));
#177371=CARTESIAN_POINT('Ctrl Pts',(2.13034853233205,5.73798334105775,132.247786313694));
#177372=CARTESIAN_POINT('Ctrl Pts',(2.13774521724426,5.69954516425014,132.400587818319));
#177373=CARTESIAN_POINT('Ctrl Pts',(2.14514190215647,5.65498761229471,132.551898748862));
#177374=CARTESIAN_POINT('Ctrl Pts',(2.15253858706868,5.60445677138152,132.70119873934));
#177375=CARTESIAN_POINT('Ctrl Pts',(2.1599349440041,5.55392817105891,132.8504921097));
#177376=CARTESIAN_POINT('Ctrl Pts',(2.16733130093954,5.49742692808816,132.997774363695));
#177377=CARTESIAN_POINT('Ctrl Pts',(2.17472765787497,5.43514861378607,133.142541557647));
#177378=CARTESIAN_POINT('Ctrl Pts',(2.18212514721153,5.37286076451498,133.287330915827));
#177379=CARTESIAN_POINT('Ctrl Pts',(2.18952263654819,5.30479423031583,133.429604104318));
#177380=CARTESIAN_POINT('Ctrl Pts',(2.19692012588476,5.231192152731,133.568878518341));
#177381=CARTESIAN_POINT('Ctrl Pts',(2.2043202083997,5.15756427405248,133.708201754793));
#177382=CARTESIAN_POINT('Ctrl Pts',(2.21172029091452,5.07839716282394,133.844523793975));
#177383=CARTESIAN_POINT('Ctrl Pts',(2.21912037342946,4.99397911564089,133.977388060725));
#177384=CARTESIAN_POINT('Ctrl Pts',(2.22652859309594,4.90946824213586,134.110398425397));
#177385=CARTESIAN_POINT('Ctrl Pts',(2.23393681276249,4.81969510204575,134.239943109171));
#177386=CARTESIAN_POINT('Ctrl Pts',(2.24134503242897,4.72499081618039,134.365595284014));
#177387=CARTESIAN_POINT('Ctrl Pts',(2.24875781173106,4.63022824140704,134.491324795675));
#177388=CARTESIAN_POINT('Ctrl Pts',(2.25617059103314,4.5305287090298,134.6131567363));
#177389=CARTESIAN_POINT('Ctrl Pts',(2.26358337033523,4.42626221243583,134.73069903768));
#177390=CARTESIAN_POINT('Ctrl Pts',(2.27100674136397,4.32184673498236,134.848409289012));
#177391=CARTESIAN_POINT('Ctrl Pts',(2.27843011239267,4.21285151842754,134.961817391203));
#177392=CARTESIAN_POINT('Ctrl Pts',(2.28585348342142,4.09968240962053,135.070569086775));
#177393=CARTESIAN_POINT('Ctrl Pts',(2.28978953286226,4.03967743267468,135.128231845229));
#177394=CARTESIAN_POINT('Ctrl Pts',(2.29372558230313,3.97849956930882,135.184586200873));
#177395=CARTESIAN_POINT('Ctrl Pts',(2.29766163174398,3.9162127817296,135.23958417571));
#177396=CARTESIAN_POINT('Ctrl Pts',(2.3050848981494,3.79874184426099,135.343308639825));
#177397=CARTESIAN_POINT('Ctrl Pts',(2.31250816455476,3.67696957545211,135.442519736538));
#177398=CARTESIAN_POINT('Ctrl Pts',(2.3199314309602,3.55127763336318,135.53683964375));
#177399=CARTESIAN_POINT('Ctrl Pts',(2.32734592368122,3.42573424871136,135.631048072665));
#177400=CARTESIAN_POINT('Ctrl Pts',(2.3347604164023,3.29628070791526,135.720376597284));
#177401=CARTESIAN_POINT('Ctrl Pts',(2.34217490912332,3.16333419970981,135.804485346355));
#177402=CARTESIAN_POINT('Ctrl Pts',(2.34958225547707,3.03051583035488,135.888513028247));
#177403=CARTESIAN_POINT('Ctrl Pts',(2.3569896018308,2.8942115092836,135.967330752114));
#177404=CARTESIAN_POINT('Ctrl Pts',(2.36439694818455,2.75486998560348,136.040640014707));
#177405=CARTESIAN_POINT('Ctrl Pts',(2.37179876985996,2.61563238808818,136.113894600486));
#177406=CARTESIAN_POINT('Ctrl Pts',(2.37920059153536,2.47336242734692,136.181648732345));
#177407=CARTESIAN_POINT('Ctrl Pts',(2.38660241321077,2.32853611232308,136.243648267259));
#177408=CARTESIAN_POINT('Ctrl Pts',(2.39400032752223,2.18378624998154,136.305615073103));
#177409=CARTESIAN_POINT('Ctrl Pts',(2.40139824183376,2.03648306321578,136.361833185401));
#177410=CARTESIAN_POINT('Ctrl Pts',(2.40879615614523,1.88712523577866,136.412095356923));
#177411=CARTESIAN_POINT('Ctrl Pts',(2.41619284105743,1.73779222890518,136.462349175782));
#177412=CARTESIAN_POINT('Ctrl Pts',(2.42358952596956,1.58640561248091,136.50664889932));
#177413=CARTESIAN_POINT('Ctrl Pts',(2.43098621088177,1.43348214829835,136.54483616346));
#177414=CARTESIAN_POINT('Ctrl Pts',(2.43838256781722,1.28056546490244,136.583021734337));
#177415=CARTESIAN_POINT('Ctrl Pts',(2.44577892475267,1.12611243142052,136.615095294281));
#177416=CARTESIAN_POINT('Ctrl Pts',(2.45317528168812,0.97065274101566,136.640948989111));
#177417=CARTESIAN_POINT('Ctrl Pts',(2.46057277102466,0.815169249335995,
136.666806642208));
#177418=CARTESIAN_POINT('Ctrl Pts',(2.46797026036123,0.658679162120519,
136.686442472838));
#177419=CARTESIAN_POINT('Ctrl Pts',(2.47536774969777,0.501719932381965,
136.699800183192));
#177420=CARTESIAN_POINT('Ctrl Pts',(2.48276783221279,0.3447056808274,136.713162576072));
#177421=CARTESIAN_POINT('Ctrl Pts',(2.49016791472778,0.187222331038063,
136.720242435294));
#177422=CARTESIAN_POINT('Ctrl Pts',(2.49756799724281,0.0298098439794243,
136.721035522925));
#177423=CARTESIAN_POINT('Ctrl Pts',(2.50497621690927,-0.127775734290234,
136.721829482636));
#177424=CARTESIAN_POINT('Ctrl Pts',(2.51238443657572,-0.285289920693903,
136.716322863255));
#177425=CARTESIAN_POINT('Ctrl Pts',(2.51979265624217,-0.442194633834676,
136.70456353512));
#177426=CARTESIAN_POINT('Ctrl Pts',(2.52720543554424,-0.599195919208739,
136.692796969314));
#177427=CARTESIAN_POINT('Ctrl Pts',(2.53461821484636,-0.755586613862468,
136.674770068906));
#177428=CARTESIAN_POINT('Ctrl Pts',(2.54203099414843,-0.910836869243758,
136.650582197367));
#177429=CARTESIAN_POINT('Ctrl Pts',(2.54945436517718,-1.06630895347023,
136.626359765062));
#177430=CARTESIAN_POINT('Ctrl Pts',(2.55687773620583,-1.22063697863208,
136.595958851851));
#177431=CARTESIAN_POINT('Ctrl Pts',(2.56430110723457,-1.37330352774386,
136.55952942336));
#177432=CARTESIAN_POINT('Ctrl Pts',(2.56823715667533,-1.45425099526594,
136.540213666262));
#177433=CARTESIAN_POINT('Ctrl Pts',(2.57217320611614,-1.5347316402072,136.519203902923));
#177434=CARTESIAN_POINT('Ctrl Pts',(2.5761092555569,-1.614670524186,136.49652801328));
#177435=CARTESIAN_POINT('Ctrl Pts',(2.58353252196235,-1.76543276456432,
136.453761993102));
#177436=CARTESIAN_POINT('Ctrl Pts',(2.59095578836782,-1.91472275577802,
136.404937555722));
#177437=CARTESIAN_POINT('Ctrl Pts',(2.59837905477326,-2.06201632989022,
136.350171578802));
#177438=CARTESIAN_POINT('Ctrl Pts',(2.60579354749427,-2.20913581522959,
136.295470330719));
#177439=CARTESIAN_POINT('Ctrl Pts',(2.61320804021524,-2.35426323378479,
136.234841650059));
#177440=CARTESIAN_POINT('Ctrl Pts',(2.62062253293624,-2.49688714154573,
136.168452820808));
#177441=CARTESIAN_POINT('Ctrl Pts',(2.62802987929002,-2.63937358301488,
136.102127979611));
#177442=CARTESIAN_POINT('Ctrl Pts',(2.63543722564383,-2.77936098129598,
136.030054198934));
#177443=CARTESIAN_POINT('Ctrl Pts',(2.64284457199761,-2.91635563729711,
135.952447675814));
#177444=CARTESIAN_POINT('Ctrl Pts',(2.65024639367301,-3.05324811751509,
135.874899034568));
#177445=CARTESIAN_POINT('Ctrl Pts',(2.65764821534844,-3.18715197646189,
135.791826050558));
#177446=CARTESIAN_POINT('Ctrl Pts',(2.66505003702383,-3.31759610195315,
135.703491833078));
#177447=CARTESIAN_POINT('Ctrl Pts',(2.67244795133514,-3.4479713670052,135.615204246545));
#177448=CARTESIAN_POINT('Ctrl Pts',(2.67984586564639,-3.57489022758569,
135.521661166579));
#177449=CARTESIAN_POINT('Ctrl Pts',(2.6872437799577,-3.69790876998053,135.423170127754));
#177450=CARTESIAN_POINT('Ctrl Pts',(2.6946404648699,-3.8209068689261,135.324695456352));
#177451=CARTESIAN_POINT('Ctrl Pts',(2.70203714978218,-3.94000564497269,
135.221274691116));
#177452=CARTESIAN_POINT('Ctrl Pts',(2.70943383469438,-4.05479253956745,
135.113256998725));
#177453=CARTESIAN_POINT('Ctrl Pts',(2.71683019162982,-4.16957434439101,
135.005244095952));
#177454=CARTESIAN_POINT('Ctrl Pts',(2.7242265485652,-4.28004437606428,134.892634927137));
#177455=CARTESIAN_POINT('Ctrl Pts',(2.73162290550064,-4.38582558171782,
134.77581684032));
#177456=CARTESIAN_POINT('Ctrl Pts',(2.73902039483721,-4.49162298274399,
134.658980868355));
#177457=CARTESIAN_POINT('Ctrl Pts',(2.74641788417378,-4.59272987779126,
134.537934972038));
#177458=CARTESIAN_POINT('Ctrl Pts',(2.75381537351035,-4.68880839543919,
134.413100895469));
#177459=CARTESIAN_POINT('Ctrl Pts',(2.76121545602542,-4.78492059326364,
134.288223058507));
#177460=CARTESIAN_POINT('Ctrl Pts',(2.76861553854049,-4.8760006766464,134.159554693013));
#177461=CARTESIAN_POINT('Ctrl Pts',(2.77601562105556,-4.96175321800073,
134.027547792733));
#177462=CARTESIAN_POINT('Ctrl Pts',(2.78342384072205,-5.04760005308911,
133.895395737296));
#177463=CARTESIAN_POINT('Ctrl Pts',(2.79083206038853,-5.1281074434976,133.759898128959));
#177464=CARTESIAN_POINT('Ctrl Pts',(2.79824028005501,-5.20302481775922,
133.621533545926));
#177465=CARTESIAN_POINT('Ctrl Pts',(2.80565305935704,-5.2779883024141,133.483083801801));
#177466=CARTESIAN_POINT('Ctrl Pts',(2.81306583865903,-5.34735475106751,
133.341763901173));
#177467=CARTESIAN_POINT('Ctrl Pts',(2.82047861796104,-5.41092136493723,
133.198073329018));
#177468=CARTESIAN_POINT('Ctrl Pts',(2.82790198898978,-5.4745788057661,133.054177445034));
#177469=CARTESIAN_POINT('Ctrl Pts',(2.83532536001858,-5.53241972375438,
132.907904470494));
#177470=CARTESIAN_POINT('Ctrl Pts',(2.84274873104732,-5.58429061271274,
132.759770783048));
#177471=CARTESIAN_POINT('Ctrl Pts',(2.84668478048813,-5.61179380266354,
132.681226747544));
#177472=CARTESIAN_POINT('Ctrl Pts',(2.8506208299289,-5.63761944817894,132.602159811346));
#177473=CARTESIAN_POINT('Ctrl Pts',(2.85455687936971,-5.66175049941405,
132.522648092026));
#177474=CARTESIAN_POINT('Ctrl Pts',(2.86366808789622,-5.71760930989739,
132.33859353023));
#177475=CARTESIAN_POINT('Ctrl Pts',(2.87277929642273,-5.76452188978835,
132.151705729902));
#177476=CARTESIAN_POINT('Ctrl Pts',(2.88189050494924,-5.80224320684398,
131.962766561583));
#177477=CARTESIAN_POINT('Ctrl Pts',(2.89101288072823,-5.84001075744482,
131.773595817903));
#177478=CARTESIAN_POINT('Ctrl Pts',(2.90013525650721,-5.86856438465176,
131.582368600916));
#177479=CARTESIAN_POINT('Ctrl Pts',(2.9092576322862,-5.88770617541872,131.38989161968));
#177480=CARTESIAN_POINT('Ctrl Pts',(2.91838000806519,-5.90684796618569,
131.197414638443));
#177481=CARTESIAN_POINT('Ctrl Pts',(2.92750238384411,-5.91657775146001,
131.00368782821));
#177482=CARTESIAN_POINT('Ctrl Pts',(2.9366247596231,-5.9167477322684,130.809540887515));
#177483=CARTESIAN_POINT('',(4.68662480779567,-5.90794960642534,130.801846066134));
#177484=CARTESIAN_POINT('Ctrl Pts',(2.93662480779568,-5.91315123421776,
130.809536714076));
#177485=CARTESIAN_POINT('Ctrl Pts',(3.002084706258,-5.90155967865228,129.41722218474));
#177486=CARTESIAN_POINT('Ctrl Pts',(3.16036047932472,-4.71421286616052,
126.032947503737));
#177487=CARTESIAN_POINT('Ctrl Pts',(3.41145212699552,0.935117824657439,
123.868719682199));
#177488=CARTESIAN_POINT('Ctrl Pts',(3.6898997508085,6.34060517223504,127.842218389349));
#177489=CARTESIAN_POINT('Ctrl Pts',(3.96834737462117,5.91938612231001,134.537781095536));
#177490=CARTESIAN_POINT('Ctrl Pts',(4.24679499843421,0.0585404040744741,
137.802512770201));
#177491=CARTESIAN_POINT('Ctrl Pts',(4.48622080949229,-5.02721977015144,
135.080001576444));
#177492=CARTESIAN_POINT('Ctrl Pts',(4.63283074594615,-5.90357735060225,
131.948565170342));
#177493=CARTESIAN_POINT('Ctrl Pts',(4.68662480779567,-5.90794960642534,
130.801846066134));
#177494=CARTESIAN_POINT('',(6.43662480779561,-5.92239257047651,130.800071874156));
#177495=CARTESIAN_POINT('Ctrl Pts',(4.68662480779567,-5.90794960642534,
130.801846066134));
#177496=CARTESIAN_POINT('Ctrl Pts',(4.72564662055044,-5.91112120831184,
129.970024548512));
#177497=CARTESIAN_POINT('Ctrl Pts',(4.85748430790944,-5.357959038813,127.163691475044));
#177498=CARTESIAN_POINT('Ctrl Pts',(5.082137869873,-1.05101382462193,123.885333917891));
#177499=CARTESIAN_POINT('Ctrl Pts',(5.36058549368563,5.25307447480259,126.180209982854));
#177500=CARTESIAN_POINT('Ctrl Pts',(5.63903311749881,6.72984395884472,132.724454578803));
#177501=CARTESIAN_POINT('Ctrl Pts',(5.91748074131143,2.02221561585842,137.504226626174));
#177502=CARTESIAN_POINT('Ctrl Pts',(6.18334463807725,-4.24699899157585,
136.189382608541));
#177503=CARTESIAN_POINT('Ctrl Pts',(6.35639266023856,-5.90852833851104,
132.49976478573));
#177504=CARTESIAN_POINT('Ctrl Pts',(6.43662480779561,-5.92239257047651,
130.800071874156));
#177505=CARTESIAN_POINT('',(8.18662480779565,-5.92165762541258,130.808932636213));
#177506=CARTESIAN_POINT('Ctrl Pts',(6.43662480779561,-5.92239257047651,
130.800071874156));
#177507=CARTESIAN_POINT('Ctrl Pts',(6.44920853484286,-5.92456705683997,
130.53348955878));
#177508=CARTESIAN_POINT('Ctrl Pts',(6.55460813649462,-5.78691335188716,
128.302891236576));
#177509=CARTESIAN_POINT('Ctrl Pts',(6.75282361275006,-2.95248947639563,
124.459254911432));
#177510=CARTESIAN_POINT('Ctrl Pts',(7.03127123656321,3.74242445275167,124.890662980229));
#177511=CARTESIAN_POINT('Ctrl Pts',(7.30971886037598,6.99823313741991,130.756470277563));
#177512=CARTESIAN_POINT('Ctrl Pts',(7.588166484189,3.82300745149239,136.66628645778));
#177513=CARTESIAN_POINT('Ctrl Pts',(7.86661410800171,-2.86537531805696,
137.189279161839));
#177514=CARTESIAN_POINT('Ctrl Pts',(8.06610021587067,-5.77064201872146,
133.360405977193));
#177515=CARTESIAN_POINT('Ctrl Pts',(8.17277044913534,-5.92416113212367,
131.102527757664));
#177516=CARTESIAN_POINT('Ctrl Pts',(8.18662480779565,-5.92165762541258,
130.808932636213));
#177517=CARTESIAN_POINT('',(9.93662400132317,-5.91171822603858,130.806485822397));
#177518=CARTESIAN_POINT('Ctrl Pts',(8.18662480779565,-5.92165762541258,
130.808932636213));
#177519=CARTESIAN_POINT('Ctrl Pts',(8.26558632373962,-5.90738914211935,
129.135616935941));
#177520=CARTESIAN_POINT('Ctrl Pts',(8.4373637142878,-4.29042602827262,125.471272957867));
#177521=CARTESIAN_POINT('Ctrl Pts',(8.70195697944047,1.93033341467937,124.077446507921));
#177522=CARTESIAN_POINT('Ctrl Pts',(8.98040460325343,6.7029357182005,128.792343398947));
#177523=CARTESIAN_POINT('Ctrl Pts',(9.25885222706628,5.3158675533077,135.356185821374));
#177524=CARTESIAN_POINT('Ctrl Pts',(9.53729985087913,-0.956223198505886,
137.737123250526));
#177525=CARTESIAN_POINT('Ctrl Pts',(9.76322355739578,-5.33223384913622,
134.499816419021));
#177526=CARTESIAN_POINT('Ctrl Pts',(9.89633138930801,-5.91036449412479,
131.665510020757));
#177527=CARTESIAN_POINT('Ctrl Pts',(9.93662334661598,-5.90763365731545,
130.806498324047));
#177528=CARTESIAN_POINT('',(11.6866256258633,-5.91485588054631,130.79903509886));
#177529=CARTESIAN_POINT('Ctrl Pts',(9.93662480779568,-5.91674962384094,
130.806470422784));
#177530=CARTESIAN_POINT('Ctrl Pts',(9.94419276580098,-5.91680724575811,
130.644875194101));
#177531=CARTESIAN_POINT('Ctrl Pts',(9.95176072380631,-5.91024040341668,
130.48332735637));
#177532=CARTESIAN_POINT('Ctrl Pts',(9.9593286818116,-5.89708709072551,130.322391316782));
#177533=CARTESIAN_POINT('Ctrl Pts',(9.96690056530931,-5.88392695542389,
130.161371799827));
#177534=CARTESIAN_POINT('Ctrl Pts',(9.97447244880701,-5.86417356697056,
130.000965061026));
#177535=CARTESIAN_POINT('Ctrl Pts',(9.98204433230472,-5.83791669394471,
129.841729204687));
#177536=CARTESIAN_POINT('Ctrl Pts',(9.98962133024956,-5.81164208565014,
129.682385792102));
#177537=CARTESIAN_POINT('Ctrl Pts',(9.99719832819441,-5.77885529158964,
129.524215182232));
#177538=CARTESIAN_POINT('Ctrl Pts',(10.0047753261393,-5.73969699141968,
129.367764289717));
#177539=CARTESIAN_POINT('Ctrl Pts',(10.0123643149607,-5.70047672180609,
129.211065807938));
#177540=CARTESIAN_POINT('Ctrl Pts',(10.0199533037822,-5.65486488004793,
129.056092820959));
#177541=CARTESIAN_POINT('Ctrl Pts',(10.0275422926037,-5.6030521688323,128.9033774625));
#177542=CARTESIAN_POINT('Ctrl Pts',(10.0351374993923,-5.5511970053554,128.750536978138));
#177543=CARTESIAN_POINT('Ctrl Pts',(10.042732706181,-5.49313096425641,128.599958136316));
#177544=CARTESIAN_POINT('Ctrl Pts',(10.0503279129696,-5.42909254872292,
128.452152153186));
#177545=CARTESIAN_POINT('Ctrl Pts',(10.0579373914952,-5.3649338021114,128.304068435931));
#177546=CARTESIAN_POINT('Ctrl Pts',(10.0655468700207,-5.2947803979279,128.158768307418));
#177547=CARTESIAN_POINT('Ctrl Pts',(10.0731563485463,-5.21891713299337,
128.016738957181));
#177548=CARTESIAN_POINT('Ctrl Pts',(10.0801692651992,-5.14900133623913,
127.885844311493));
#177549=CARTESIAN_POINT('Ctrl Pts',(10.0871821818521,-5.07423647615101,
127.75772757786));
#177550=CARTESIAN_POINT('Ctrl Pts',(10.0941950985049,-4.99487698837381,
127.632746764413));
#177551=CARTESIAN_POINT('Ctrl Pts',(10.1016183649104,-4.9108739053874,127.500452895869));
#177552=CARTESIAN_POINT('Ctrl Pts',(10.1090416313157,-4.82148428427923,
127.371298636164));
#177553=CARTESIAN_POINT('Ctrl Pts',(10.1164648977212,-4.72696969736647,
127.245753018704));
#177554=CARTESIAN_POINT('Ctrl Pts',(10.1238793904422,-4.63256681884621,
127.120355785738));
#177555=CARTESIAN_POINT('Ctrl Pts',(10.1312938831632,-4.53305125390469,
126.998559000602));
#177556=CARTESIAN_POINT('Ctrl Pts',(10.1387083758842,-4.4287292556656,126.880805119996));
#177557=CARTESIAN_POINT('Ctrl Pts',(10.146115722238,-4.32450780689622,126.763164735014));
#177558=CARTESIAN_POINT('Ctrl Pts',(10.1535230685917,-4.21548939334842,
126.649559774533));
#177559=CARTESIAN_POINT('Ctrl Pts',(10.1609304149455,-4.10202208518554,
126.54040173231));
#177560=CARTESIAN_POINT('Ctrl Pts',(10.1683322366209,-3.98863940522165,
126.431325104274));
#177561=CARTESIAN_POINT('Ctrl Pts',(10.1757340582964,-3.87081470539658,
126.32668904823));
#177562=CARTESIAN_POINT('Ctrl Pts',(10.1831358799718,-3.74893457379556,
126.226870025123));
#177563=CARTESIAN_POINT('Ctrl Pts',(10.1905337942832,-3.62711878176765,
126.127103695702));
#177564=CARTESIAN_POINT('Ctrl Pts',(10.1979317085945,-3.50125210960173,
126.032149570891));
#177565=CARTESIAN_POINT('Ctrl Pts',(10.2053296229059,-3.3717559639555,125.942345368512));
#177566=CARTESIAN_POINT('Ctrl Pts',(10.2127263078181,-3.24228133821939,
125.852556089963));
#177567=CARTESIAN_POINT('Ctrl Pts',(10.2201229927302,-3.10917874253501,
125.767915247813));
#177568=CARTESIAN_POINT('Ctrl Pts',(10.2275196776424,-2.97290053909443,
125.688718629785));
#177569=CARTESIAN_POINT('Ctrl Pts',(10.2349160345779,-2.8366283783722,125.609525523417));
#177570=CARTESIAN_POINT('Ctrl Pts',(10.2423123915133,-2.69718121262551,
125.535776348748));
#177571=CARTESIAN_POINT('Ctrl Pts',(10.2497087484487,-2.55503786806384,
125.467721969947));
#177572=CARTESIAN_POINT('Ctrl Pts',(10.2571062377853,-2.41287276099325,
125.399657171847));
#177573=CARTESIAN_POINT('Ctrl Pts',(10.2645037271219,-2.26801098990349,
125.337289066872));
#177574=CARTESIAN_POINT('Ctrl Pts',(10.2719012164585,-2.12095316831205,
125.280821152664));
#177575=CARTESIAN_POINT('Ctrl Pts',(10.2793012989735,-1.97384379582901,
125.224333443716));
#177576=CARTESIAN_POINT('Ctrl Pts',(10.2867013814885,-1.82453718840631,
125.173750177241));
#177577=CARTESIAN_POINT('Ctrl Pts',(10.2941014640035,-1.67355084199639,
125.129225540605));
#177578=CARTESIAN_POINT('Ctrl Pts',(10.30150968367,-1.52239847057702,125.084651944553));
#177579=CARTESIAN_POINT('Ctrl Pts',(10.3089179033365,-1.36956302977261,
125.046150388616));
#177580=CARTESIAN_POINT('Ctrl Pts',(10.3163261230029,-1.21557469687477,
125.013824483596));
#177581=CARTESIAN_POINT('Ctrl Pts',(10.323738902305,-1.06149158672746,124.98147868252));
#177582=CARTESIAN_POINT('Ctrl Pts',(10.331151681607,-0.90625453780127,124.955316168244));
#177583=CARTESIAN_POINT('Ctrl Pts',(10.3385644609091,-0.7504001348975,124.935388799603));
#177584=CARTESIAN_POINT('Ctrl Pts',(10.3459878319378,-0.59432303991357,
124.915432957802));
#177585=CARTESIAN_POINT('Ctrl Pts',(10.3534112029666,-0.437627200085401,
124.901730087478));
#177586=CARTESIAN_POINT('Ctrl Pts',(10.3608345739954,-0.280851326824123,
124.894279984045));
#177587=CARTESIAN_POINT('Ctrl Pts',(10.3647706234362,-0.197724997035228,
124.890329760442));
#177588=CARTESIAN_POINT('Ctrl Pts',(10.368706672877,-0.114576129541411,
124.888136543532));
#177589=CARTESIAN_POINT('Ctrl Pts',(10.3726427223178,-0.0314844594406813,
124.887694386375));
#177590=CARTESIAN_POINT('Ctrl Pts',(10.3800659887232,0.125223837166229,
124.886860491777));
#177591=CARTESIAN_POINT('Ctrl Pts',(10.3874892551287,0.28220224736707,124.892255479522));
#177592=CARTESIAN_POINT('Ctrl Pts',(10.3949125215341,0.438914773846293,
124.903912805425));
#177593=CARTESIAN_POINT('Ctrl Pts',(10.4023270142551,0.595442079133384,
124.915556353337));
#177594=CARTESIAN_POINT('Ctrl Pts',(10.4097415069761,0.751703757586047,
124.933447479131));
#177595=CARTESIAN_POINT('Ctrl Pts',(10.4171559996971,0.907162020557403,
124.957567682036));
#177596=CARTESIAN_POINT('Ctrl Pts',(10.4245633460509,1.06247044700223,124.981664636982));
#177597=CARTESIAN_POINT('Ctrl Pts',(10.4319706924046,1.2169766331604,125.011978659766));
#177598=CARTESIAN_POINT('Ctrl Pts',(10.4393780387584,1.37014623725376,125.04843933153));
#177599=CARTESIAN_POINT('Ctrl Pts',(10.4467798604338,1.52320160167784,125.08487280955));
#177600=CARTESIAN_POINT('Ctrl Pts',(10.4541816821093,1.67492200735845,125.127443722312));
#177601=CARTESIAN_POINT('Ctrl Pts',(10.4615835037847,1.82478176673787,125.176030308648));
#177602=CARTESIAN_POINT('Ctrl Pts',(10.4689814180961,1.97456241631661,125.224591246504));
#177603=CARTESIAN_POINT('Ctrl Pts',(10.4763793324075,2.1224840215316,125.279161418682));
#177604=CARTESIAN_POINT('Ctrl Pts',(10.4837772467188,2.26803467022076,125.339568828561));
#177605=CARTESIAN_POINT('Ctrl Pts',(10.491173931631,2.41356113103246,125.399966199824));
#177606=CARTESIAN_POINT('Ctrl Pts',(10.4985706165432,2.55671707286601,125.466198740585));
#177607=CARTESIAN_POINT('Ctrl Pts',(10.5059673014554,2.69700912831771,125.538045746209));
#177608=CARTESIAN_POINT('Ctrl Pts',(10.5133636583908,2.83729496307266,125.609889566063));
#177609=CARTESIAN_POINT('Ctrl Pts',(10.5207600153262,2.97471683167974,125.687347185622));
#177610=CARTESIAN_POINT('Ctrl Pts',(10.5281563722617,3.10880485774485,125.770151353048));
#177611=CARTESIAN_POINT('Ctrl Pts',(10.5355538615983,3.24291341302963,125.852968198003));
#177612=CARTESIAN_POINT('Ctrl Pts',(10.542951350935,3.37368679182139,125.941133024556));
#177613=CARTESIAN_POINT('Ctrl Pts',(10.5503488402716,3.5006831919568,126.03433464782));
#177614=CARTESIAN_POINT('Ctrl Pts',(10.5577489227866,3.62772411048287,126.127568942768));
#177615=CARTESIAN_POINT('Ctrl Pts',(10.5651490053016,3.75098511348906,126.225843329081));
#177616=CARTESIAN_POINT('Ctrl Pts',(10.5725490878166,3.87005675957541,126.328805764795));
#177617=CARTESIAN_POINT('Ctrl Pts',(10.579957307483,3.9892593371775,126.431881418291));
#177618=CARTESIAN_POINT('Ctrl Pts',(10.5873655271494,4.10426307557628,126.539655171727));
#177619=CARTESIAN_POINT('Ctrl Pts',(10.5947737468159,4.21469423029261,126.651736976103));
#177620=CARTESIAN_POINT('Ctrl Pts',(10.602186526118,4.32519335354219,126.763887764959));
#177621=CARTESIAN_POINT('Ctrl Pts',(10.60959930542,4.43111403458347,126.880351612742));
#177622=CARTESIAN_POINT('Ctrl Pts',(10.6170120847221,4.53212260591901,127.000705106427));
#177623=CARTESIAN_POINT('Ctrl Pts',(10.6244354557508,4.6332755030381,127.121230566828));
#177624=CARTESIAN_POINT('Ctrl Pts',(10.6318588267796,4.72950204486285,127.245656478611));
#177625=CARTESIAN_POINT('Ctrl Pts',(10.6392821978083,4.8205112168404,127.373529498024));
#177626=CARTESIAN_POINT('Ctrl Pts',(10.6432182472491,4.86876646355787,127.441330841188));
#177627=CARTESIAN_POINT('Ctrl Pts',(10.64715429669,4.91555567296337,127.510100850996));
#177628=CARTESIAN_POINT('Ctrl Pts',(10.6510903461308,4.96084074961768,127.579769229586));
#177629=CARTESIAN_POINT('Ctrl Pts',(10.6585136125362,5.04624699088922,127.711161617332));
#177630=CARTESIAN_POINT('Ctrl Pts',(10.6659368789416,5.12655870002981,127.84614812235));
#177631=CARTESIAN_POINT('Ctrl Pts',(10.6733601453471,5.20145801007354,127.984295878603));
#177632=CARTESIAN_POINT('Ctrl Pts',(10.6807746380681,5.2762687953528,128.122280355681));
#177633=CARTESIAN_POINT('Ctrl Pts',(10.6881891307891,5.34567973862619,128.263418321831));
#177634=CARTESIAN_POINT('Ctrl Pts',(10.6956036235102,5.40941571721768,128.407247320115));
#177635=CARTESIAN_POINT('Ctrl Pts',(10.7030109698639,5.47309026467339,128.550937690595));
#177636=CARTESIAN_POINT('Ctrl Pts',(10.7104183162176,5.5311005864092,128.697313590628));
#177637=CARTESIAN_POINT('Ctrl Pts',(10.7178256625714,5.58321710302218,128.84588740023));
#177638=CARTESIAN_POINT('Ctrl Pts',(10.7252274842468,5.63529474917068,128.99435039788));
#177639=CARTESIAN_POINT('Ctrl Pts',(10.7326293059222,5.68148721984,129.145007690324));
#177640=CARTESIAN_POINT('Ctrl Pts',(10.7400311275976,5.72161280918421,129.297351186846));
#177641=CARTESIAN_POINT('Ctrl Pts',(10.747429041909,5.76171721654226,129.449614262423));
#177642=CARTESIAN_POINT('Ctrl Pts',(10.7548269562203,5.79576102598574,129.603561409261));
#177643=CARTESIAN_POINT('Ctrl Pts',(10.7622248705317,5.82361224211681,129.758668972784));
#177644=CARTESIAN_POINT('Ctrl Pts',(10.7696215554439,5.85145882988107,129.913750760244));
#177645=CARTESIAN_POINT('Ctrl Pts',(10.7770182403562,5.87311480087535,130.069992214597));
#177646=CARTESIAN_POINT('Ctrl Pts',(10.7844149252684,5.88849916302601,130.226858955627));
#177647=CARTESIAN_POINT('Ctrl Pts',(10.7918112822038,5.90388284301787,130.383718741021));
#177648=CARTESIAN_POINT('Ctrl Pts',(10.7992076391392,5.91299543066692,130.541203386449));
#177649=CARTESIAN_POINT('Ctrl Pts',(10.8066039960746,5.91580779284587,130.698773115445));
#177650=CARTESIAN_POINT('Ctrl Pts',(10.8140014854112,5.91862058560467,130.856366968771));
#177651=CARTESIAN_POINT('Ctrl Pts',(10.8213989747479,5.9151312256229,131.01404555834));
#177652=CARTESIAN_POINT('Ctrl Pts',(10.8287964640845,5.90536271669626,131.171268980449));
#177653=CARTESIAN_POINT('Ctrl Pts',(10.8361965465995,5.89559078343395,131.328547516986));
#177654=CARTESIAN_POINT('Ctrl Pts',(10.8435966291146,5.87953534189579,131.485370196036));
#177655=CARTESIAN_POINT('Ctrl Pts',(10.8509967116296,5.85727126187853,131.641202255674));
#177656=CARTESIAN_POINT('Ctrl Pts',(10.8584049312961,5.83498270021658,131.797205668681));
#177657=CARTESIAN_POINT('Ctrl Pts',(10.8658131509625,5.80647191886609,131.952215917124));
#177658=CARTESIAN_POINT('Ctrl Pts',(10.873221370629,5.77186505907829,132.105707728175));
#177659=CARTESIAN_POINT('Ctrl Pts',(10.8806341499311,5.7372368993457,132.259294010875));
#177660=CARTESIAN_POINT('Ctrl Pts',(10.8880469292331,5.69650528113772,132.411359634179));
#177661=CARTESIAN_POINT('Ctrl Pts',(10.8954597085352,5.64984607839031,132.56139500909));
#177662=CARTESIAN_POINT('Ctrl Pts',(10.902883079564,5.60312020678591,132.71164476158));
#177663=CARTESIAN_POINT('Ctrl Pts',(10.9103064505928,5.55044995959825,132.859858121085));
#177664=CARTESIAN_POINT('Ctrl Pts',(10.9177298216216,5.49205944728994,133.005545205449));
#177665=CARTESIAN_POINT('Ctrl Pts',(10.9216658710623,5.46109939660376,133.08279199329));
#177666=CARTESIAN_POINT('Ctrl Pts',(10.9256019205029,5.42853195025858,133.159328950403));
#177667=CARTESIAN_POINT('Ctrl Pts',(10.9295379699436,5.39439566032155,133.235086028303));
#177668=CARTESIAN_POINT('Ctrl Pts',(10.936961236349,5.33001568285598,133.377961512929));
#177669=CARTESIAN_POINT('Ctrl Pts',(10.9443845027544,5.25985815368121,133.518493531566));
#177670=CARTESIAN_POINT('Ctrl Pts',(10.9518077691599,5.18411544039399,133.656180679065));
#177671=CARTESIAN_POINT('Ctrl Pts',(10.9592222618809,5.10846224870362,133.793705091791));
#177672=CARTESIAN_POINT('Ctrl Pts',(10.966636754602,5.02723719084237,133.928391002378));
#177673=CARTESIAN_POINT('Ctrl Pts',(10.974051247323,4.94068063440387,134.059756973054));
#177674=CARTESIAN_POINT('Ctrl Pts',(10.9814585936767,4.85420750443351,134.190996328262));
#177675=CARTESIAN_POINT('Ctrl Pts',(10.9888659400305,4.76241331003379,134.318921804274));
#177676=CARTESIAN_POINT('Ctrl Pts',(10.9962732863842,4.66558420643275,134.443076678924));
#177677=CARTESIAN_POINT('Ctrl Pts',(11.0036751080596,4.56882732163019,134.567138954184));
#177678=CARTESIAN_POINT('Ctrl Pts',(11.011076929735,4.46704323337127,134.687435934572));
#177679=CARTESIAN_POINT('Ctrl Pts',(11.0184787514104,4.36056119631744,134.803540110371));
#177680=CARTESIAN_POINT('Ctrl Pts',(11.0258766657218,4.25413537030136,134.919582995679));
#177681=CARTESIAN_POINT('Ctrl Pts',(11.0332745800332,4.14301678622663,135.03143720997));
#177682=CARTESIAN_POINT('Ctrl Pts',(11.0406724943446,4.02757466278196,135.138708653686));
#177683=CARTESIAN_POINT('Ctrl Pts',(11.0480691792568,3.9121517237247,135.245962270834));
#177684=CARTESIAN_POINT('Ctrl Pts',(11.0554658641691,3.79240694448886,135.348634375047));
#177685=CARTESIAN_POINT('Ctrl Pts',(11.0628625490813,3.6687461360898,135.446367979842));
#177686=CARTESIAN_POINT('Ctrl Pts',(11.0702589060167,3.54509081094057,135.544097251027));
#177687=CARTESIAN_POINT('Ctrl Pts',(11.0776552629521,3.41752009475671,135.636888226728));
#177688=CARTESIAN_POINT('Ctrl Pts',(11.0850516198875,3.28647236959852,135.724424634057));
#177689=CARTESIAN_POINT('Ctrl Pts',(11.0924491092241,3.15540458069868,135.811974443433));
#177690=CARTESIAN_POINT('Ctrl Pts',(11.0998465985608,3.02085903330203,135.894267875232));
#177691=CARTESIAN_POINT('Ctrl Pts',(11.1072440878974,2.88330239779886,135.971032452059));
#177692=CARTESIAN_POINT('Ctrl Pts',(11.1146441704124,2.74569754202996,136.04782393859));
#177693=CARTESIAN_POINT('Ctrl Pts',(11.1220442529274,2.60507982236836,136.119082529544));
#177694=CARTESIAN_POINT('Ctrl Pts',(11.1294443354424,2.46193961812188,136.184582163118));
#177695=CARTESIAN_POINT('Ctrl Pts',(11.1368525551089,2.31864201650667,136.250153820272));
#177696=CARTESIAN_POINT('Ctrl Pts',(11.1442607747753,2.17281673063916,136.309953718074));
#177697=CARTESIAN_POINT('Ctrl Pts',(11.1516689944418,2.02497386985343,136.363804059936));
#177698=CARTESIAN_POINT('Ctrl Pts',(11.1590817737438,1.87704001425334,136.417687545785));
#177699=CARTESIAN_POINT('Ctrl Pts',(11.166494553046,1.72708646407916,136.465614065613));
#177700=CARTESIAN_POINT('Ctrl Pts',(11.173907332348,1.57563701514503,136.507456141841));
#177701=CARTESIAN_POINT('Ctrl Pts',(11.1813307033768,1.42397116813621,136.54935800399));
#177702=CARTESIAN_POINT('Ctrl Pts',(11.1887540744055,1.27080551601733,136.585157974457));
#177703=CARTESIAN_POINT('Ctrl Pts',(11.1961774454342,1.11667334769981,136.61477981045));
#177704=CARTESIAN_POINT('Ctrl Pts',(11.200113494875,1.03494877370778,136.63048601866));
#177705=CARTESIAN_POINT('Ctrl Pts',(11.2040495443158,0.952952563794645,
136.64445619853));
#177706=CARTESIAN_POINT('Ctrl Pts',(11.2079855937565,0.870764490067564,
136.656684922091));
#177707=CARTESIAN_POINT('Ctrl Pts',(11.215408860162,0.71576034801899,136.679747913082));
#177708=CARTESIAN_POINT('Ctrl Pts',(11.2228321265674,0.559604922454607,
136.696683385581));
#177709=CARTESIAN_POINT('Ctrl Pts',(11.2302553929728,0.402824039110081,
136.707382162166));
#177710=CARTESIAN_POINT('Ctrl Pts',(11.2376698856938,0.246228457749604,
136.718068293686));
#177711=CARTESIAN_POINT('Ctrl Pts',(11.2450843784149,0.0890092588634893,
136.722532376653));
#177712=CARTESIAN_POINT('Ctrl Pts',(11.2524988711359,-0.0682985857609222,
136.720716410255));
#177713=CARTESIAN_POINT('Ctrl Pts',(11.2599062174897,-0.225454811162149,
136.718902194154));
#177714=CARTESIAN_POINT('Ctrl Pts',(11.2673135638434,-0.382699141440079,
136.710819983197));
#177715=CARTESIAN_POINT('Ctrl Pts',(11.2747209101972,-0.53949264941082,
136.696463658394));
#177716=CARTESIAN_POINT('Ctrl Pts',(11.2821227318726,-0.696169214867613,
136.68211804108));
#177717=CARTESIAN_POINT('Ctrl Pts',(11.2895245535481,-0.852395257374062,
136.661507661269));
#177718=CARTESIAN_POINT('Ctrl Pts',(11.2969263752234,-1.00763313071025,
136.634678450789));
#177719=CARTESIAN_POINT('Ctrl Pts',(11.3043242895348,-1.16278905518213,
136.60786340324));
#177720=CARTESIAN_POINT('Ctrl Pts',(11.3117222038461,-1.31695748245476,
136.574836126431));
#177721=CARTESIAN_POINT('Ctrl Pts',(11.3191201181575,-1.46960727369043,
136.535694234065));
#177722=CARTESIAN_POINT('Ctrl Pts',(11.3265168030697,-1.6222316972995,136.496558846373));
#177723=CARTESIAN_POINT('Ctrl Pts',(11.333913487982,-1.77333762450528,136.451310952486));
#177724=CARTESIAN_POINT('Ctrl Pts',(11.3413101728942,-1.92240536170159,
136.400099012792));
#177725=CARTESIAN_POINT('Ctrl Pts',(11.3487065298296,-2.07146648907822,
136.348889343888));
#177726=CARTESIAN_POINT('Ctrl Pts',(11.356102886765,-2.21848925309794,136.291716276284));
#177727=CARTESIAN_POINT('Ctrl Pts',(11.3634992437005,-2.36297060821013,
136.228777680001));
#177728=CARTESIAN_POINT('Ctrl Pts',(11.3708967330371,-2.50747408378725,
136.165829447658));
#177729=CARTESIAN_POINT('Ctrl Pts',(11.3782942223737,-2.64943503345679,
136.097114078121));
#177730=CARTESIAN_POINT('Ctrl Pts',(11.3856917117103,-2.78837196752447,
136.02287691372));
#177731=CARTESIAN_POINT('Ctrl Pts',(11.3930917942253,-2.927357605719,135.948613725596));
#177732=CARTESIAN_POINT('Ctrl Pts',(11.4004918767404,-3.0633167886923,135.868825064542));
#177733=CARTESIAN_POINT('Ctrl Pts',(11.4078919592554,-3.19579426225298,
135.783801308633));
#177734=CARTESIAN_POINT('Ctrl Pts',(11.4153001789218,-3.32841740841409,
135.698684060363));
#177735=CARTESIAN_POINT('Ctrl Pts',(11.4227083985882,-3.45755088504768,
135.608320422832));
#177736=CARTESIAN_POINT('Ctrl Pts',(11.4301166182547,-3.58276938029463,
135.51304346207));
#177737=CARTESIAN_POINT('Ctrl Pts',(11.4375293975567,-3.70806494543602,
135.417707859928));
#177738=CARTESIAN_POINT('Ctrl Pts',(11.4449421768588,-3.82944044060424,
135.317453145898));
#177739=CARTESIAN_POINT('Ctrl Pts',(11.4523549561609,-3.94650549087129,
135.21265109949));
#177740=CARTESIAN_POINT('Ctrl Pts',(11.4597783271896,-4.06373780917214,
135.107699307003));
#177741=CARTESIAN_POINT('Ctrl Pts',(11.4672016982183,-4.17664711448327,
134.998187464499));
#177742=CARTESIAN_POINT('Ctrl Pts',(11.474625069247,-4.28488100590149,134.884523031952));
#177743=CARTESIAN_POINT('Ctrl Pts',(11.4785611186878,-4.34226921216777,
134.824255422475));
#177744=CARTESIAN_POINT('Ctrl Pts',(11.4824971681286,-4.39834367447588,
134.762820912282));
#177745=CARTESIAN_POINT('Ctrl Pts',(11.4864332175694,-4.45305670734803,
134.700283681956));
#177746=CARTESIAN_POINT('Ctrl Pts',(11.4937956702431,-4.55539843887839,
134.583306645577));
#177747=CARTESIAN_POINT('Ctrl Pts',(11.5011581229168,-4.65329686455237,
134.462100747582));
#177748=CARTESIAN_POINT('Ctrl Pts',(11.5085205755906,-4.74637765054397,
134.337040869289));
#177749=CARTESIAN_POINT('Ctrl Pts',(11.5159415852658,-4.8401987512058,134.210986331771));
#177750=CARTESIAN_POINT('Ctrl Pts',(11.523362594941,-4.92912493136729,134.081016476417));
#177751=CARTESIAN_POINT('Ctrl Pts',(11.5307836046162,-5.01281050267483,
133.947553488959));
#177752=CARTESIAN_POINT('Ctrl Pts',(11.5381280065076,-5.09563217992484,
133.815468252527));
#177753=CARTESIAN_POINT('Ctrl Pts',(11.5454724083989,-5.1733207042299,133.679961977886));
#177754=CARTESIAN_POINT('Ctrl Pts',(11.5528168102903,-5.24558146672041,
133.541476917342));
#177755=CARTESIAN_POINT('Ctrl Pts',(11.5601561603024,-5.3177925243272,133.403087114356));
#177756=CARTESIAN_POINT('Ctrl Pts',(11.5674955103146,-5.38458307413891,
133.261722937933));
#177757=CARTESIAN_POINT('Ctrl Pts',(11.5748348603267,-5.44570279726505,
133.117853994768));
#177758=CARTESIAN_POINT('Ctrl Pts',(11.5821706709072,-5.50679304515347,
132.974054432993));
#177759=CARTESIAN_POINT('Ctrl Pts',(11.5895064814877,-5.56221776140611,
132.827752857696));
#177760=CARTESIAN_POINT('Ctrl Pts',(11.5968422920681,-5.61177352462589,
132.679441541368));
#177761=CARTESIAN_POINT('Ctrl Pts',(11.6043241683788,-5.66231600889853,
132.528177149784));
#177762=CARTESIAN_POINT('Ctrl Pts',(11.6118060446894,-5.70675318012188,
132.374822504533));
#177763=CARTESIAN_POINT('Ctrl Pts',(11.619287921,-5.74492160186354,132.21991928853));
#177764=CARTESIAN_POINT('Ctrl Pts',(11.6266225812379,-5.78233900809533,
132.068064003577));
#177765=CARTESIAN_POINT('Ctrl Pts',(11.6339572414757,-5.8137320057929,131.914720911414));
#177766=CARTESIAN_POINT('Ctrl Pts',(11.6412919017136,-5.83899770548043,
131.760413104564));
#177767=CARTESIAN_POINT('Ctrl Pts',(11.6488473860606,-5.86502407784319,
131.601459563231));
#177768=CARTESIAN_POINT('Ctrl Pts',(11.6564028704076,-5.88454831827244,
131.44148272438));
#177769=CARTESIAN_POINT('Ctrl Pts',(11.6639583547546,-5.8975152635197,131.28106207451));
#177770=CARTESIAN_POINT('Ctrl Pts',(11.6715138391016,-5.91048220876697,
131.120641424639));
#177771=CARTESIAN_POINT('Ctrl Pts',(11.6790693234486,-5.9168918570892,130.959777403725));
#177772=CARTESIAN_POINT('Ctrl Pts',(11.6866248077956,-5.91674761742372,
130.799050795463));
#177773=CARTESIAN_POINT('',(13.4366248077956,-5.9221125045945,130.804501180565));
#177774=CARTESIAN_POINT('Ctrl Pts',(11.6866260347045,-5.91391045748492,
130.799027254254));
#177775=CARTESIAN_POINT('Ctrl Pts',(11.7127109702638,-5.91868981499976,
130.244388001879));
#177776=CARTESIAN_POINT('Ctrl Pts',(11.8316117804274,-5.59228796829895,
127.72174242367));
#177777=CARTESIAN_POINT('Ctrl Pts',(12.0433284651951,-2.00181416161862,
124.098370713555));
#177778=CARTESIAN_POINT('Ctrl Pts',(12.3217760890081,4.55990977836376,125.495426323045));
#177779=CARTESIAN_POINT('Ctrl Pts',(12.600223712821,6.93129939600614,131.771133193343));
#177780=CARTESIAN_POINT('Ctrl Pts',(12.8786713366339,2.93316348151725,137.158423295966));
#177781=CARTESIAN_POINT('Ctrl Pts',(13.1571189604468,-3.76040637948188,
136.706640210358));
#177782=CARTESIAN_POINT('Ctrl Pts',(13.343103450834,-5.92313498158111,132.782070348646));
#177783=CARTESIAN_POINT('Ctrl Pts',(13.436272066617,-5.92653126023725,130.811960232984));
#177784=CARTESIAN_POINT('Ctrl Pts',(13.4366248077956,-5.92652866437588,
130.804501285384));
#177785=CARTESIAN_POINT('',(15.186624792037,-5.91464336866557,130.809600954502));
#177786=CARTESIAN_POINT('Ctrl Pts',(13.4366248077956,-5.91674999833336,
130.804501053285));
#177787=CARTESIAN_POINT('Ctrl Pts',(13.4440429936624,-5.9167537153653,130.647897384805));
#177788=CARTESIAN_POINT('Ctrl Pts',(13.4514611795291,-5.91053569384905,
130.491055185319));
#177789=CARTESIAN_POINT('Ctrl Pts',(13.4588793653959,-5.89806501653408,
130.334509978281));
#177790=CARTESIAN_POINT('Ctrl Pts',(13.4662887814253,-5.8856090821513,130.17814984021));
#177791=CARTESIAN_POINT('Ctrl Pts',(13.4736981974548,-5.86691523469698,
130.022086364759));
#177792=CARTESIAN_POINT('Ctrl Pts',(13.4811076134842,-5.84200452152495,
129.866856626651));
#177793=CARTESIAN_POINT('Ctrl Pts',(13.4885098919879,-5.81711780496167,
129.711776422089));
#177794=CARTESIAN_POINT('Ctrl Pts',(13.4959121704916,-5.78602620363372,
129.557528722674));
#177795=CARTESIAN_POINT('Ctrl Pts',(13.5033144489953,-5.7488026662856,129.404646908764));
#177796=CARTESIAN_POINT('Ctrl Pts',(13.5107112166218,-5.71160684126162,
129.251878912903));
#177797=CARTESIAN_POINT('Ctrl Pts',(13.5181079842483,-5.66828825786702,
129.100475139549));
#177798=CARTESIAN_POINT('Ctrl Pts',(13.5255047518748,-5.61897116429073,
128.95096006254));
#177799=CARTESIAN_POINT('Ctrl Pts',(13.5328976308802,-5.56967999764619,
128.801523588445));
#177800=CARTESIAN_POINT('Ctrl Pts',(13.5402905098857,-5.51439671792575,
128.653974187445));
#177801=CARTESIAN_POINT('Ctrl Pts',(13.5476833888911,-5.45329573856649,
128.508822303742));
#177802=CARTESIAN_POINT('Ctrl Pts',(13.5550750649302,-5.39220470153485,
128.363694039098));
#177803=CARTESIAN_POINT('Ctrl Pts',(13.5624667409693,-5.32529798838409,
128.220962861824));
#177804=CARTESIAN_POINT('Ctrl Pts',(13.5698584170083,-5.25279862348526,
128.081120418169));
#177805=CARTESIAN_POINT('Ctrl Pts',(13.5772497912476,-5.18030221871185,
127.941283684235));
#177806=CARTESIAN_POINT('Ctrl Pts',(13.5846411654869,-5.10221378826202,
127.804335781348));
#177807=CARTESIAN_POINT('Ctrl Pts',(13.5920325397262,-5.01880277670205,
127.670744615075));
#177808=CARTESIAN_POINT('Ctrl Pts',(13.5994250770067,-4.9353786403247,127.53713242808));
#177809=CARTESIAN_POINT('Ctrl Pts',(13.6068176142871,-4.84663045333017,
127.406878346496));
#177810=CARTESIAN_POINT('Ctrl Pts',(13.6142101515676,-4.75287143714511,
127.28042195969));
#177811=CARTESIAN_POINT('Ctrl Pts',(13.6216053171532,-4.65907908635613,
127.153920613224));
#177812=CARTESIAN_POINT('Ctrl Pts',(13.6290004827387,-4.56027258201902,
127.031219949844));
#177813=CARTESIAN_POINT('Ctrl Pts',(13.6363956483242,-4.4568058175647,126.912726967411));
#177814=CARTESIAN_POINT('Ctrl Pts',(13.6437989522555,-4.35322518841236,
126.794103583996));
#177815=CARTESIAN_POINT('Ctrl Pts',(13.6512022561868,-4.24497430347026,
126.67969741039));
#177816=CARTESIAN_POINT('Ctrl Pts',(13.658605560118,-4.13244484685284,126.569879521821));
#177817=CARTESIAN_POINT('Ctrl Pts',(13.6660134637275,-4.01984547560077,
126.459993403317));
#177818=CARTESIAN_POINT('Ctrl Pts',(13.673421367337,-3.90296251305144,126.354701499595));
#177819=CARTESIAN_POINT('Ctrl Pts',(13.6808292709464,-3.78222076458437,
126.254334612097));
#177820=CARTESIAN_POINT('Ctrl Pts',(13.6882476815014,-3.66130776294873,
126.153825369964));
#177821=CARTESIAN_POINT('Ctrl Pts',(13.6956660920563,-3.53652534116423,
126.058255321024));
#177822=CARTESIAN_POINT('Ctrl Pts',(13.7030845026112,-3.40832794592024,
125.967912419192));
#177823=CARTESIAN_POINT('Ctrl Pts',(13.706727737765,-3.34536927660466,125.923544365764));
#177824=CARTESIAN_POINT('Ctrl Pts',(13.7103709729188,-3.28158735658004,
125.88043633549));
#177825=CARTESIAN_POINT('Ctrl Pts',(13.7140142080725,-3.21703809881979,
125.838618333351));
#177826=CARTESIAN_POINT('Ctrl Pts',(13.721437474478,-3.08551588946378,125.753412147826));
#177827=CARTESIAN_POINT('Ctrl Pts',(13.7288607408834,-2.95040732000841,
125.673305958167));
#177828=CARTESIAN_POINT('Ctrl Pts',(13.7362840072888,-2.81214573972864,
125.598616972223));
#177829=CARTESIAN_POINT('Ctrl Pts',(13.7436985000098,-2.67404757315466,
125.524016262459));
#177830=CARTESIAN_POINT('Ctrl Pts',(13.7511129927308,-2.53280413880009,
125.45482018752));
#177831=CARTESIAN_POINT('Ctrl Pts',(13.7585274854519,-2.38887831175831,
125.391303165986));
#177832=CARTESIAN_POINT('Ctrl Pts',(13.7659348318056,-2.24509120584755,
125.327847364547));
#177833=CARTESIAN_POINT('Ctrl Pts',(13.7733421781595,-2.09862719348059,
125.270059869189));
#177834=CARTESIAN_POINT('Ctrl Pts',(13.7807495245132,-1.94997424345807,
125.218169516972));
#177835=CARTESIAN_POINT('Ctrl Pts',(13.7881513461886,-1.80143216441404,
125.166317866538));
#177836=CARTESIAN_POINT('Ctrl Pts',(13.795553167864,-1.65070474935151,125.120354724112));
#177837=CARTESIAN_POINT('Ctrl Pts',(13.8029549895394,-1.49830036492387,
125.080461022101));
#177838=CARTESIAN_POINT('Ctrl Pts',(13.8103529038507,-1.34597643358468,
125.040588379664));
#177839=CARTESIAN_POINT('Ctrl Pts',(13.8177508181621,-1.19197765613274,
125.006778890994));
#177840=CARTESIAN_POINT('Ctrl Pts',(13.8251487324734,-1.03682788741214,
124.979163754422));
#177841=CARTESIAN_POINT('Ctrl Pts',(13.8325454173856,-0.881703901768178,
124.951553206984));
#177842=CARTESIAN_POINT('Ctrl Pts',(13.8399421022978,-0.725429671639387,
124.930135033964));
#177843=CARTESIAN_POINT('Ctrl Pts',(13.84733878721,-0.568539699878368,124.914989414104));
#177844=CARTESIAN_POINT('Ctrl Pts',(13.8547351441455,-0.411656684782658,
124.899844465818));
#177845=CARTESIAN_POINT('Ctrl Pts',(13.8621315010809,-0.254158353911757,
124.890971553542));
#177846=CARTESIAN_POINT('Ctrl Pts',(13.8695278580164,-0.0965845274411798,
124.888398988924));
#177847=CARTESIAN_POINT('Ctrl Pts',(13.8769253473529,0.061013423984047,
124.88582603044));
#177848=CARTESIAN_POINT('Ctrl Pts',(13.8843228366896,0.218686520751447,
124.889555346353));
#177849=CARTESIAN_POINT('Ctrl Pts',(13.8917203260261,0.375894894790388,
124.899563111252));
#177850=CARTESIAN_POINT('Ctrl Pts',(13.8991204085411,0.533158377980696,
124.909574384358));
#177851=CARTESIAN_POINT('Ctrl Pts',(13.906520491056,0.689956441782852,124.925868464725));
#177852=CARTESIAN_POINT('Ctrl Pts',(13.913920573571,0.845754438828811,124.948369668828));
#177853=CARTESIAN_POINT('Ctrl Pts',(13.9213287932375,1.00172375178961,124.970895615318));
#177854=CARTESIAN_POINT('Ctrl Pts',(13.928737012904,1.15669043217741,124.999642262864));
#177855=CARTESIAN_POINT('Ctrl Pts',(13.9361452325704,1.3101293997381,125.034482670985));
#177856=CARTESIAN_POINT('Ctrl Pts',(13.9435580118725,1.46366280642284,125.069344522796));
#177857=CARTESIAN_POINT('Ctrl Pts',(13.9509707911745,1.61566626704777,125.110307511829));
#177858=CARTESIAN_POINT('Ctrl Pts',(13.9583835704766,1.76563046085579,125.157194988846));
#177859=CARTESIAN_POINT('Ctrl Pts',(13.9658069415053,1.91580893053656,125.204149460888));
#177860=CARTESIAN_POINT('Ctrl Pts',(13.973230312534,2.06394196326246,125.257045202587));
#177861=CARTESIAN_POINT('Ctrl Pts',(13.9806536835628,2.20954001850263,125.315657358222));
#177862=CARTESIAN_POINT('Ctrl Pts',(13.9845897330036,2.28673960096969,125.346734929519));
#177863=CARTESIAN_POINT('Ctrl Pts',(13.9885257824445,2.36322690734754,125.379418814373));
#177864=CARTESIAN_POINT('Ctrl Pts',(13.9924618318854,2.43893194790328,125.413670354158));
#177865=CARTESIAN_POINT('Ctrl Pts',(13.9998850982908,2.58170929171549,125.478267689239));
#177866=CARTESIAN_POINT('Ctrl Pts',(14.0073083646962,2.72213437980149,125.548639002982));
#177867=CARTESIAN_POINT('Ctrl Pts',(14.0147316311016,2.85970610034554,125.62459116496));
#177868=CARTESIAN_POINT('Ctrl Pts',(14.0221461238226,2.99711522254071,125.700453557791));
#177869=CARTESIAN_POINT('Ctrl Pts',(14.0295606165437,3.131677366452,125.781883490623));
#177870=CARTESIAN_POINT('Ctrl Pts',(14.0369751092647,3.26291146066457,125.868639863475));
#177871=CARTESIAN_POINT('Ctrl Pts',(14.0443824556184,3.39401906651588,125.955312617269));
#177872=CARTESIAN_POINT('Ctrl Pts',(14.0517898019722,3.52180469925431,126.04730138617));
#177873=CARTESIAN_POINT('Ctrl Pts',(14.0591971483259,3.64581207272215,126.144319320228));
#177874=CARTESIAN_POINT('Ctrl Pts',(14.0665989700013,3.76972695681267,126.241264894652));
#177875=CARTESIAN_POINT('Ctrl Pts',(14.0740007916767,3.88986889984315,126.343231936572));
#177876=CARTESIAN_POINT('Ctrl Pts',(14.0814026133521,4.00581089366082,126.449890541113));
#177877=CARTESIAN_POINT('Ctrl Pts',(14.0888005276634,4.12169168260212,126.556492841406));
#177878=CARTESIAN_POINT('Ctrl Pts',(14.0961984419748,4.23337666379677,126.667781519879));
#177879=CARTESIAN_POINT('Ctrl Pts',(14.1035963562861,4.34047230003337,126.783386758519));
#177880=CARTESIAN_POINT('Ctrl Pts',(14.1109930411983,4.44755013891845,126.898972785665));
#177881=CARTESIAN_POINT('Ctrl Pts',(14.1183897261105,4.55003989306975,127.018873675703));
#177882=CARTESIAN_POINT('Ctrl Pts',(14.1257864110227,4.64758519399128,127.142683074814));
#177883=CARTESIAN_POINT('Ctrl Pts',(14.1331827679581,4.74512616965181,127.266486984086));
#177884=CARTESIAN_POINT('Ctrl Pts',(14.1405791248936,4.8377228969889,127.394198764614));
#177885=CARTESIAN_POINT('Ctrl Pts',(14.147975481829,4.92505977062255,127.525379553532));
#177886=CARTESIAN_POINT('Ctrl Pts',(14.1553729711656,5.01241001575426,127.656580426562));
#177887=CARTESIAN_POINT('Ctrl Pts',(14.1627704605021,5.09449859683924,127.791251054751));
#177888=CARTESIAN_POINT('Ctrl Pts',(14.1701679498386,5.17105374699097,127.928924353583));
#177889=CARTESIAN_POINT('Ctrl Pts',(14.1775680323536,5.24763573343257,128.066645913577));
#177890=CARTESIAN_POINT('Ctrl Pts',(14.1849681148686,5.31868024563838,128.20737191385));
#177891=CARTESIAN_POINT('Ctrl Pts',(14.1923681973836,5.38396196834096,128.350611631635));
#177892=CARTESIAN_POINT('Ctrl Pts',(14.1997764170501,5.44931547500848,128.494008856214));
#177893=CARTESIAN_POINT('Ctrl Pts',(14.2071846367166,5.50889338230191,128.639924978483));
#177894=CARTESIAN_POINT('Ctrl Pts',(14.2145928563831,5.5625186701399,128.787849619122));
#177895=CARTESIAN_POINT('Ctrl Pts',(14.2220056356851,5.61617696344769,128.935865304909));
#177896=CARTESIAN_POINT('Ctrl Pts',(14.2294184149872,5.66387522400035,129.085891617444));
#177897=CARTESIAN_POINT('Ctrl Pts',(14.2368311942892,5.70548677149639,129.237404567519));
#177898=CARTESIAN_POINT('Ctrl Pts',(14.244254565318,5.74715777552295,129.389134006402));
#177899=CARTESIAN_POINT('Ctrl Pts',(14.2516779363467,5.7827246124855,129.542353962618));
#177900=CARTESIAN_POINT('Ctrl Pts',(14.2591013073754,5.8121118512552,129.696531031845));
#177901=CARTESIAN_POINT('Ctrl Pts',(14.2630373568164,5.82769367038867,129.77827941338));
#177902=CARTESIAN_POINT('Ctrl Pts',(14.2669734062573,5.84153904980948,129.860296788583));
#177903=CARTESIAN_POINT('Ctrl Pts',(14.2709094556983,5.85364268295297,129.942503377177));
#177904=CARTESIAN_POINT('Ctrl Pts',(14.2783327221038,5.87646975731931,130.09754243768));
#177905=CARTESIAN_POINT('Ctrl Pts',(14.2857559885092,5.89316756823212,130.253723455326));
#177906=CARTESIAN_POINT('Ctrl Pts',(14.2931792549146,5.90362773861287,130.410520438838));
#177907=CARTESIAN_POINT('Ctrl Pts',(14.3005937476357,5.9140755459409,130.567132101337));
#177908=CARTESIAN_POINT('Ctrl Pts',(14.3080082403568,5.9183003628808,130.72435791174));
#177909=CARTESIAN_POINT('Ctrl Pts',(14.3154227330778,5.91624500282486,130.881662810613));
#177910=CARTESIAN_POINT('Ctrl Pts',(14.3228300794316,5.91419162380233,131.038816093102));
#177911=CARTESIAN_POINT('Ctrl Pts',(14.3302374257853,5.9058701231011,131.196047941545));
#177912=CARTESIAN_POINT('Ctrl Pts',(14.3376447721391,5.89127520189453,131.352819420069));
#177913=CARTESIAN_POINT('Ctrl Pts',(14.3450465938145,5.8766911661309,131.509473972509));
#177914=CARTESIAN_POINT('Ctrl Pts',(14.3524484154899,5.85584306074447,131.665668468618));
#177915=CARTESIAN_POINT('Ctrl Pts',(14.3598502371653,5.82877763571499,131.8208653327));
#177916=CARTESIAN_POINT('Ctrl Pts',(14.3672481514766,5.80172649831251,131.975980269566));
#177917=CARTESIAN_POINT('Ctrl Pts',(14.374646065788,5.76846464164647,132.130098256421));
#177918=CARTESIAN_POINT('Ctrl Pts',(14.3820439800994,5.72909048761005,132.282688303594));
#177919=CARTESIAN_POINT('Ctrl Pts',(14.3894406650116,5.68972287684377,132.435252993069));
#177920=CARTESIAN_POINT('Ctrl Pts',(14.3968373499239,5.64424507785501,132.586289885705));
#177921=CARTESIAN_POINT('Ctrl Pts',(14.4042340348361,5.59280634174263,132.735279514429));
#177922=CARTESIAN_POINT('Ctrl Pts',(14.4116303917716,5.54136988647778,132.884262536797));
#177923=CARTESIAN_POINT('Ctrl Pts',(14.419026748707,5.48397314146012,133.031198122891));
#177924=CARTESIAN_POINT('Ctrl Pts',(14.4264231056425,5.42081474203117,133.175583528867));
#177925=CARTESIAN_POINT('Ctrl Pts',(14.4338205949791,5.35764667288985,133.319991040617));
#177926=CARTESIAN_POINT('Ctrl Pts',(14.4412180843157,5.28871534252514,133.461847252803));
#177927=CARTESIAN_POINT('Ctrl Pts',(14.4486155736523,5.21426682572683,133.600671049658));
#177928=CARTESIAN_POINT('Ctrl Pts',(14.4560156561673,5.13979221111637,133.739543510979));
#177929=CARTESIAN_POINT('Ctrl Pts',(14.4634157386823,5.05979673572452,133.875381111754));
#177930=CARTESIAN_POINT('Ctrl Pts',(14.4708158211974,4.97457147010795,134.007729040225));
#177931=CARTESIAN_POINT('Ctrl Pts',(14.4782240408639,4.88925249055057,134.140222498849));
#177932=CARTESIAN_POINT('Ctrl Pts',(14.4856322605304,4.79869243848905,134.269218307875));
#177933=CARTESIAN_POINT('Ctrl Pts',(14.4930404801969,4.70322502682163,134.394291662806));
#177934=CARTESIAN_POINT('Ctrl Pts',(14.5004532594989,4.60769885655543,134.5194419983));
#177935=CARTESIAN_POINT('Ctrl Pts',(14.507866038801,4.5072595457769,134.64066478231));
#177936=CARTESIAN_POINT('Ctrl Pts',(14.5152788181031,4.40227946764858,134.757570206143));
#177937=CARTESIAN_POINT('Ctrl Pts',(14.5227021891319,4.29714938906111,134.87464266993));
#177938=CARTESIAN_POINT('Ctrl Pts',(14.5301255601606,4.18746584462711,134.987385186112));
#177939=CARTESIAN_POINT('Ctrl Pts',(14.5375489311894,4.07363683014216,135.09544597428));
#177940=CARTESIAN_POINT('Ctrl Pts',(14.54148498063,4.01328195537579,135.152742397047));
#177941=CARTESIAN_POINT('Ctrl Pts',(14.5454210300707,3.95176218053971,135.208723301553));
#177942=CARTESIAN_POINT('Ctrl Pts',(14.5493570795113,3.88914175871114,135.263341100047));
#177943=CARTESIAN_POINT('Ctrl Pts',(14.5567803459167,3.77104159745337,135.366348563449));
#177944=CARTESIAN_POINT('Ctrl Pts',(14.564203612322,3.64866765869746,135.464816559647));
#177945=CARTESIAN_POINT('Ctrl Pts',(14.5716268787275,3.52240389334273,135.558369596803));
#177946=CARTESIAN_POINT('Ctrl Pts',(14.5790413714485,3.39628936127274,135.651812062038));
#177947=CARTESIAN_POINT('Ctrl Pts',(14.5864558641695,3.26629445086713,135.740350911159));
#177948=CARTESIAN_POINT('Ctrl Pts',(14.5938703568906,3.13283841202407,135.82364881876));
#177949=CARTESIAN_POINT('Ctrl Pts',(14.6012777032443,2.99951100313579,135.906866440701));
#177950=CARTESIAN_POINT('Ctrl Pts',(14.6086850495981,2.862729421611,135.984852981169));
#177951=CARTESIAN_POINT('Ctrl Pts',(14.6160923959519,2.72294422531694,136.057312674106));
#177952=CARTESIAN_POINT('Ctrl Pts',(14.6234942176273,2.58326328609667,136.129718323871));
#177953=CARTESIAN_POINT('Ctrl Pts',(14.6308960393026,2.44058352265737,136.19660516277));
#177954=CARTESIAN_POINT('Ctrl Pts',(14.638297860978,2.29538248216377,136.257721950091));
#177955=CARTESIAN_POINT('Ctrl Pts',(14.6456957752894,2.15025809216776,136.318806474335));
#177956=CARTESIAN_POINT('Ctrl Pts',(14.6530936896008,2.00261541898403,136.374126868734));
#177957=CARTESIAN_POINT('Ctrl Pts',(14.6604916039122,1.85295439869872,136.423478925525));
#177958=CARTESIAN_POINT('Ctrl Pts',(14.6678882888244,1.70331824936092,136.4728227809));
#177959=CARTESIAN_POINT('Ctrl Pts',(14.6752849737366,1.55166477278916,136.516200150363));
#177960=CARTESIAN_POINT('Ctrl Pts',(14.6826816586488,1.3985116852086,136.553455818451));
#177961=CARTESIAN_POINT('Ctrl Pts',(14.6900780155843,1.24536538859666,136.590709834583));
#177962=CARTESIAN_POINT('Ctrl Pts',(14.6974743725197,1.09071997590906,136.621842600824));
#177963=CARTESIAN_POINT('Ctrl Pts',(14.7048707294551,0.935105787033889,
136.646749489385));
#177964=CARTESIAN_POINT('Ctrl Pts',(14.7122682187917,0.779467773228917,
136.671660191255));
#177965=CARTESIAN_POINT('Ctrl Pts',(14.7196657081283,0.62286105653735,136.690343058499));
#177966=CARTESIAN_POINT('Ctrl Pts',(14.7270631974649,0.465823422714856,
136.702745065985));
#177967=CARTESIAN_POINT('Ctrl Pts',(14.7344632799798,0.30873073959416,136.715151420975));
#177968=CARTESIAN_POINT('Ctrl Pts',(14.7418633624948,0.151207210495546,
136.721272503175));
#177969=CARTESIAN_POINT('Ctrl Pts',(14.7492634450097,-0.00620718782220476,
136.721107361624));
#177970=CARTESIAN_POINT('Ctrl Pts',(14.7566716646762,-0.163794679454623,
136.720942038482));
#177971=CARTESIAN_POINT('Ctrl Pts',(14.7640798843426,-0.321272427130523,
136.714476687566));
#177972=CARTESIAN_POINT('Ctrl Pts',(14.7714881040091,-0.478102650822751,
136.70176245378));
#177973=CARTESIAN_POINT('Ctrl Pts',(14.7789008833112,-0.635029400900809,
136.689040394595));
#177974=CARTESIAN_POINT('Ctrl Pts',(14.7863136626133,-0.791307463137764,
136.670061833636));
#177975=CARTESIAN_POINT('Ctrl Pts',(14.7937264419153,-0.946407603652012,
136.644929357873));
#177976=CARTESIAN_POINT('Ctrl Pts',(14.8011498129441,-1.10172935852028,
136.61976097165));
#177977=CARTESIAN_POINT('Ctrl Pts',(14.8085731839728,-1.25586946535376,
136.588421183204));
#177978=CARTESIAN_POINT('Ctrl Pts',(14.8159965550016,-1.40831142963687,
136.55106310505));
#177979=CARTESIAN_POINT('Ctrl Pts',(14.8199326044424,-1.48913981689591,
136.531254955617));
#177980=CARTESIAN_POINT('Ctrl Pts',(14.8238686538833,-1.56949107832643,
136.509755673011));
#177981=CARTESIAN_POINT('Ctrl Pts',(14.8278047033241,-1.64929044664833,
136.486593592823));
#177982=CARTESIAN_POINT('Ctrl Pts',(14.8352279697296,-1.7997895648476,136.442910632452));
#177983=CARTESIAN_POINT('Ctrl Pts',(14.842651236135,-1.94877958185454,136.393178329126));
#177984=CARTESIAN_POINT('Ctrl Pts',(14.8500745025404,-2.09573705091141,
136.3375167491));
#177985=CARTESIAN_POINT('Ctrl Pts',(14.8574889952614,-2.24252082844392,
136.28192095644));
#177986=CARTESIAN_POINT('Ctrl Pts',(14.8649034879824,-2.38727649413616,
136.2204099673));
#177987=CARTESIAN_POINT('Ctrl Pts',(14.8723179807034,-2.52949363175903,
136.153154175873));
#177988=CARTESIAN_POINT('Ctrl Pts',(14.8797253270571,-2.67157369515048,
136.08596320811));
#177989=CARTESIAN_POINT('Ctrl Pts',(14.8871326734108,-2.81111976622904,
136.013038619768));
#177990=CARTESIAN_POINT('Ctrl Pts',(14.8945400197646,-2.94763947110261,
135.934599609163));
#177991=CARTESIAN_POINT('Ctrl Pts',(14.90194184144,-3.08405735442892,135.856219101331));
#177992=CARTESIAN_POINT('Ctrl Pts',(14.9093436631153,-3.21745304361395,
135.772332545676));
#177993=CARTESIAN_POINT('Ctrl Pts',(14.9167454847906,-3.34735703682289,
135.68320591441));
#177994=CARTESIAN_POINT('Ctrl Pts',(14.9241433991019,-3.4771924547259,135.594126332397));
#177995=CARTESIAN_POINT('Ctrl Pts',(14.9315413134133,-3.60353954051628,
135.499812394439));
#177996=CARTESIAN_POINT('Ctrl Pts',(14.9389392277246,-3.72595626075486,
135.40057433164));
#177997=CARTESIAN_POINT('Ctrl Pts',(14.9463359126368,-3.84835263755524,
135.301352760407));
#177998=CARTESIAN_POINT('Ctrl Pts',(14.9537325975491,-3.96681965542502,
135.197208923264));
#177999=CARTESIAN_POINT('Ctrl Pts',(14.9611292824613,-4.08094688893181,
135.088494491784));
#178000=CARTESIAN_POINT('Ctrl Pts',(14.9685256393967,-4.1950690619173,134.979784880815));
#178001=CARTESIAN_POINT('Ctrl Pts',(14.9759219963321,-4.30485156286373,
134.866505335949));
#178002=CARTESIAN_POINT('Ctrl Pts',(14.9833183532675,-4.40991970378503,
134.749045493278));
#178003=CARTESIAN_POINT('Ctrl Pts',(14.9907158426041,-4.51500393090708,
134.631567667204));
#178004=CARTESIAN_POINT('Ctrl Pts',(14.9981133319406,-4.61537211194998,
134.50990854722));
#178005=CARTESIAN_POINT('Ctrl Pts',(15.0055108212772,-4.71068894902936,
134.38449192633));
#178006=CARTESIAN_POINT('Ctrl Pts',(15.0129109037922,-4.80603919927794,
134.259031340839));
#178007=CARTESIAN_POINT('Ctrl Pts',(15.0203109863071,-4.89633435429538,
134.129810928955));
#178008=CARTESIAN_POINT('Ctrl Pts',(15.027711068822,-4.98128174338273,133.9972844744));
#178009=CARTESIAN_POINT('Ctrl Pts',(15.0351192884885,-5.06632254085743,
133.864612293385));
#178010=CARTESIAN_POINT('Ctrl Pts',(15.042527508155,-5.14600362724973,133.728627124168));
#178011=CARTESIAN_POINT('Ctrl Pts',(15.0499357278214,-5.22007734897655,
133.58980906139));
#178012=CARTESIAN_POINT('Ctrl Pts',(15.0573485071235,-5.29419666184331,
133.45090555841));
#178013=CARTESIAN_POINT('Ctrl Pts',(15.0647612864255,-5.36270157095136,
133.30916602285));
#178014=CARTESIAN_POINT('Ctrl Pts',(15.0721740657276,-5.4253923217827,133.165091164927));
#178015=CARTESIAN_POINT('Ctrl Pts',(15.0795974367563,-5.48817264809856,
133.02081044609));
#178016=CARTESIAN_POINT('Ctrl Pts',(15.0870208077851,-5.54512208931563,
132.874188087565));
#178017=CARTESIAN_POINT('Ctrl Pts',(15.0944441788138,-5.596090285426,132.725741391869));
#178018=CARTESIAN_POINT('Ctrl Pts',(15.0983802282549,-5.62311484597069,
132.647031391876));
#178019=CARTESIAN_POINT('Ctrl Pts',(15.1023162776959,-5.64845871011584,
132.567808712566));
#178020=CARTESIAN_POINT('Ctrl Pts',(15.1062523271369,-5.67210530385628,
132.488151573851));
#178021=CARTESIAN_POINT('Ctrl Pts',(15.1154352247266,-5.72727337324023,
132.302309561938));
#178022=CARTESIAN_POINT('Ctrl Pts',(15.1246181223163,-5.77333541830667,
132.113648895864));
#178023=CARTESIAN_POINT('Ctrl Pts',(15.1338010199059,-5.81004723006746,
131.922967674081));
#178024=CARTESIAN_POINT('Ctrl Pts',(15.1428586604398,-5.84625828339016,
131.734887392601));
#178025=CARTESIAN_POINT('Ctrl Pts',(15.1519163009736,-5.87337244800413,
131.544841256533));
#178026=CARTESIAN_POINT('Ctrl Pts',(15.1609739415075,-5.89120098166726,
131.353616073709));
#178027=CARTESIAN_POINT('Ctrl Pts',(15.1695242154695,-5.90803084443243,
131.173102429403));
#178028=CARTESIAN_POINT('Ctrl Pts',(15.1780744894315,-5.91658646534607,
130.991538235456));
#178029=CARTESIAN_POINT('Ctrl Pts',(15.1866247633935,-5.91674767718177,
130.80960342827));
#178030=CARTESIAN_POINT('',(16.9366248077956,-5.90780204387767,130.802025653359));
#178031=CARTESIAN_POINT('Ctrl Pts',(15.1866248077956,-5.91348565267583,
130.809599593522));
#178032=CARTESIAN_POINT('Ctrl Pts',(15.2526498555137,-5.9016025138533,129.405465492393));
#178033=CARTESIAN_POINT('Ctrl Pts',(15.4114907778362,-4.69782533091822,
126.00913283962));
#178034=CARTESIAN_POINT('Ctrl Pts',(15.6631475747628,0.977319714034647,
123.874540511177));
#178035=CARTESIAN_POINT('Ctrl Pts',(15.9415951985758,6.35851909600637,127.880870334347));
#178036=CARTESIAN_POINT('Ctrl Pts',(16.2200428223884,5.89655005967416,134.57374490735));
#178037=CARTESIAN_POINT('Ctrl Pts',(16.4984904462014,0.0159395809900309,
137.802739462705));
#178038=CARTESIAN_POINT('Ctrl Pts',(16.7373511080038,-5.04118839832629,
135.055819514375));
#178039=CARTESIAN_POINT('Ctrl Pts',(16.8833958952019,-5.90379043459487,
131.936768349731));
#178040=CARTESIAN_POINT('Ctrl Pts',(16.9366248077956,-5.90780204387767,
130.802025653359));
#178041=CARTESIAN_POINT('',(18.6866248077956,-5.92206989474538,130.799941417168));
#178042=CARTESIAN_POINT('Ctrl Pts',(16.9366248077956,-5.90780204387767,
130.802025653359));
#178043=CARTESIAN_POINT('Ctrl Pts',(16.9762117698061,-5.91078552440622,
129.958104298891));
#178044=CARTESIAN_POINT('Ctrl Pts',(17.1086146064211,-5.34658274166464,
127.139324596949));
#178045=CARTESIAN_POINT('Ctrl Pts',(17.33383331764,-1.00887627239691,123.879064291967));
#178046=CARTESIAN_POINT('Ctrl Pts',(17.6122809414531,5.28112566490743,126.212272612985));
#178047=CARTESIAN_POINT('Ctrl Pts',(17.8907285652659,6.7180311134912,132.765385474242));
#178048=CARTESIAN_POINT('Ctrl Pts',(18.1691761890789,1.98139416284149,137.516412293604));
#178049=CARTESIAN_POINT('Ctrl Pts',(18.4344749365886,-4.26639119716458,
136.166306194459));
#178050=CARTESIAN_POINT('Ctrl Pts',(18.6069578094943,-5.90800757224012,
132.487901526767));
#178051=CARTESIAN_POINT('Ctrl Pts',(18.6866248077956,-5.92206989474538,
130.799941417168));
#178052=CARTESIAN_POINT('',(20.4366248077956,-5.92198869469903,130.808811111152));
#178053=CARTESIAN_POINT('Ctrl Pts',(18.6866248077956,-5.92206989474538,
130.799941417168));
#178054=CARTESIAN_POINT('Ctrl Pts',(18.6997736840986,-5.92439085252084,
130.521347028541));
#178055=CARTESIAN_POINT('Ctrl Pts',(18.8057384350059,-5.7797270106078,128.27862052501));
#178056=CARTESIAN_POINT('Ctrl Pts',(19.0045190605175,-2.91381031421446,
124.441399830078));
#178057=CARTESIAN_POINT('Ctrl Pts',(19.2829666843302,3.77835347032134,124.913553747223));
#178058=CARTESIAN_POINT('Ctrl Pts',(19.5614143081434,6.99839499846111,130.799071396303));
#178059=CARTESIAN_POINT('Ctrl Pts',(19.839861931956,3.78725341361693,136.689449581327));
#178060=CARTESIAN_POINT('Ctrl Pts',(20.1183095557691,-2.9041890407256,137.171718511235));
#178061=CARTESIAN_POINT('Ctrl Pts',(20.3172305143822,-5.7779299637371,133.336128281175));
#178062=CARTESIAN_POINT('Ctrl Pts',(20.423335598391,-5.92434601569743,131.090388889328));
#178063=CARTESIAN_POINT('Ctrl Pts',(20.4366248077956,-5.92198869469903,
130.808811111152));
#178064=CARTESIAN_POINT('',(22.1866248077956,-5.90776713110451,130.806650508727));
#178065=CARTESIAN_POINT('Ctrl Pts',(20.4366248077956,-5.92198869469903,
130.808811111152));
#178066=CARTESIAN_POINT('Ctrl Pts',(20.5161514729953,-5.90788176989252,
129.123764167348));
#178067=CARTESIAN_POINT('Ctrl Pts',(20.6884940127994,-4.27118742048918,
125.448150887193));
#178068=CARTESIAN_POINT('Ctrl Pts',(20.9536524272077,1.97124628558328,124.089321629448));
#178069=CARTESIAN_POINT('Ctrl Pts',(21.2321000510206,6.71505924821413,128.8331833492));
#178070=CARTESIAN_POINT('Ctrl Pts',(21.5105476748335,5.28806081061698,135.388460681217));
#178071=CARTESIAN_POINT('Ctrl Pts',(21.7889952986464,-0.99840717580492,
137.731174000475));
#178072=CARTESIAN_POINT('Ctrl Pts',(22.0143543429672,-5.34374262142005,
134.475446717348));
#178073=CARTESIAN_POINT('Ctrl Pts',(22.1468975126835,-5.9107024042326,131.653576004858));
#178074=CARTESIAN_POINT('Ctrl Pts',(22.1866248077956,-5.90776713110451,
130.806650508727));
#178075=CARTESIAN_POINT('',(23.9366248230411,-5.91468528336671,130.799105832252));
#178076=CARTESIAN_POINT('Ctrl Pts',(22.1866248077956,-5.90776713110451,
130.806650508727));
#178077=CARTESIAN_POINT('Ctrl Pts',(22.2397133872878,-5.90384465210482,
129.674882755639));
#178078=CARTESIAN_POINT('Ctrl Pts',(22.3856178413844,-5.04464026757503,
126.558908262004));
#178079=CARTESIAN_POINT('Ctrl Pts',(22.6243381700852,0.00536115071223864,
123.805965673837));
#178080=CARTESIAN_POINT('Ctrl Pts',(22.9027857938979,5.89084570391381,127.026067693108));
#178081=CARTESIAN_POINT('Ctrl Pts',(23.1812334177107,6.36293083903494,133.718236330083));
#178082=CARTESIAN_POINT('Ctrl Pts',(23.4596810415237,0.987793379532795,
137.732695537999));
#178083=CARTESIAN_POINT('Ctrl Pts',(23.7114781715519,-4.69373819460421,
135.605498381351));
#178084=CARTESIAN_POINT('Ctrl Pts',(23.8704594269759,-5.90161551527517,
132.206175144537));
#178085=CARTESIAN_POINT('Ctrl Pts',(23.9366248077956,-5.91356949928869,
130.799107147868));
#178086=CARTESIAN_POINT('',(25.6866248077955,-5.92211383359681,130.804275968097));
#178087=CARTESIAN_POINT('Ctrl Pts',(23.9366248512203,-5.91674766439881,
130.799103400509));
#178088=CARTESIAN_POINT('Ctrl Pts',(23.9456716507033,-5.91657663065078,
130.606613054719));
#178089=CARTESIAN_POINT('Ctrl Pts',(23.9547184501863,-5.90700848198333,
130.414538242424));
#178090=CARTESIAN_POINT('Ctrl Pts',(23.9637652496693,-5.88818678512448,
130.22368261214));
#178091=CARTESIAN_POINT('Ctrl Pts',(23.9729451091623,-5.86908825940729,
130.030019883928));
#178092=CARTESIAN_POINT('Ctrl Pts',(23.9821249686552,-5.84046202858799,
129.837612422055));
#178093=CARTESIAN_POINT('Ctrl Pts',(23.9913048281483,-5.80250701712613,
129.647276835508));
#178094=CARTESIAN_POINT('Ctrl Pts',(23.999728648482,-5.76767792224026,129.472616996169));
#178095=CARTESIAN_POINT('Ctrl Pts',(24.0081524688158,-5.72499397722651,
129.299701495139));
#178096=CARTESIAN_POINT('Ctrl Pts',(24.0165762891496,-5.6746439613045,129.129145265759));
#178097=CARTESIAN_POINT('Ctrl Pts',(24.023999555555,-5.63027435619705,128.97884714951));
#178098=CARTESIAN_POINT('Ctrl Pts',(24.0314228219604,-5.57986236094382,
128.83008573685));
#178099=CARTESIAN_POINT('Ctrl Pts',(24.0388460883658,-5.52353043033182,
128.683383920924));
#178100=CARTESIAN_POINT('Ctrl Pts',(24.0462605810868,-5.46726507938364,
128.536855494361));
#178101=CARTESIAN_POINT('Ctrl Pts',(24.0536750738078,-5.40509385289825,
128.392382164185));
#178102=CARTESIAN_POINT('Ctrl Pts',(24.0610895665288,-5.33718947358348,
128.250473563374));
#178103=CARTESIAN_POINT('Ctrl Pts',(24.0684969128826,-5.26935054306615,
128.108701739416));
#178104=CARTESIAN_POINT('Ctrl Pts',(24.0759042592364,-5.19578962060363,
127.969490058064));
#178105=CARTESIAN_POINT('Ctrl Pts',(24.0833116055901,-5.11672815014872,
127.833329887335));
#178106=CARTESIAN_POINT('Ctrl Pts',(24.0907134272655,-5.03772564672119,
127.697271269999));
#178107=CARTESIAN_POINT('Ctrl Pts',(24.0981152489409,-4.95323095060532,
127.564259953031));
#178108=CARTESIAN_POINT('Ctrl Pts',(24.1055170706163,-4.86351217474033,
127.434764219086));
#178109=CARTESIAN_POINT('Ctrl Pts',(24.1129149849276,-4.77384076071849,
127.305336844929));
#178110=CARTESIAN_POINT('Ctrl Pts',(24.120312899239,-4.67895097119628,127.179421663853));
#178111=CARTESIAN_POINT('Ctrl Pts',(24.1277108135503,-4.57915505213842,
127.057459288337));
#178112=CARTESIAN_POINT('Ctrl Pts',(24.1351074984625,-4.47937571735225,
126.935517180756));
#178113=CARTESIAN_POINT('Ctrl Pts',(24.1425041833746,-4.37469210734596,
126.817526863637));
#178114=CARTESIAN_POINT('Ctrl Pts',(24.1499008682868,-4.26545776381407,
126.703897152588));
#178115=CARTESIAN_POINT('Ctrl Pts',(24.1572972252222,-4.15622826384744,
126.590272479999));
#178116=CARTESIAN_POINT('Ctrl Pts',(24.1646935821577,-4.04244869027558,
126.481008298142));
#178117=CARTESIAN_POINT('Ctrl Pts',(24.1720899390931,-3.92451038575863,
126.376477512224));
#178118=CARTESIAN_POINT('Ctrl Pts',(24.1794874284297,-3.80655402458584,
126.271930722375));
#178119=CARTESIAN_POINT('Ctrl Pts',(24.1868849177662,-3.68443794406968,
126.17211901905));
#178120=CARTESIAN_POINT('Ctrl Pts',(24.1942824071028,-3.55858746359443,
126.07737576182));
#178121=CARTESIAN_POINT('Ctrl Pts',(24.2016824896177,-3.4326928664287,125.982599292489));
#178122=CARTESIAN_POINT('Ctrl Pts',(24.2090825721327,-3.30306156096661,
125.892895031101));
#178123=CARTESIAN_POINT('Ctrl Pts',(24.2164826546477,-3.17014866238169,
125.808553573564));
#178124=CARTESIAN_POINT('Ctrl Pts',(24.2238908743141,-3.03708961240101,
125.724119373924));
#178125=CARTESIAN_POINT('Ctrl Pts',(24.2312990939805,-2.90074207837538,
125.645059954875));
#178126=CARTESIAN_POINT('Ctrl Pts',(24.238707313647,-2.76158728059598,125.571620775557));
#178127=CARTESIAN_POINT('Ctrl Pts',(24.246120092949,-2.62234683536006,125.498136395649));
#178128=CARTESIAN_POINT('Ctrl Pts',(24.2535328722511,-2.48029601952231,
125.430279308824));
#178129=CARTESIAN_POINT('Ctrl Pts',(24.2609456515532,-2.33593645005443,
125.368246981538));
#178130=CARTESIAN_POINT('Ctrl Pts',(24.2683690225819,-2.19137061286431,
125.306126019554));
#178131=CARTESIAN_POINT('Ctrl Pts',(24.2757923936106,-2.04448978115152,
125.249846572598));
#178132=CARTESIAN_POINT('Ctrl Pts',(24.2832157646394,-1.895811938507,125.19955663738));
#178133=CARTESIAN_POINT('Ctrl Pts',(24.2871518140804,-1.81697937885602,
125.172891707034));
#178134=CARTESIAN_POINT('Ctrl Pts',(24.2910878635214,-1.73764181840951,
125.147909796198));
#178135=CARTESIAN_POINT('Ctrl Pts',(24.2950239129624,-1.65787755193035,
125.124627121591));
#178136=CARTESIAN_POINT('Ctrl Pts',(24.3024471793678,-1.50744463471726,
125.080716723912));
#178137=CARTESIAN_POINT('Ctrl Pts',(24.3098704457732,-1.3550385302888,125.042720586018));
#178138=CARTESIAN_POINT('Ctrl Pts',(24.3172937121787,-1.20116535325871,
125.010818319746));
#178139=CARTESIAN_POINT('Ctrl Pts',(24.3247082048997,-1.04747404154529,
124.978953759303));
#178140=CARTESIAN_POINT('Ctrl Pts',(24.3321226976207,-0.892319470638296,
124.953168809008));
#178141=CARTESIAN_POINT('Ctrl Pts',(24.3395371903417,-0.736223770039259,
124.933593621429));
#178142=CARTESIAN_POINT('Ctrl Pts',(24.3469445366954,-0.580278520353359,
124.914037301153));
#178143=CARTESIAN_POINT('Ctrl Pts',(24.3543518830492,-0.423394314735643,
124.900678874369));
#178144=CARTESIAN_POINT('Ctrl Pts',(24.361759229403,-0.266104250879958,
124.893597630424));
#178145=CARTESIAN_POINT('Ctrl Pts',(24.3691610510784,-0.108931499888111,
124.886521667938));
#178146=CARTESIAN_POINT('Ctrl Pts',(24.3765628727537,0.0486461353012634,
124.885713582992));
#178147=CARTESIAN_POINT('Ctrl Pts',(24.3839646944291,0.206089753637759,
124.891200922788));
#178148=CARTESIAN_POINT('Ctrl Pts',(24.3913626087405,0.363450258713448,
124.89668536586));
#178149=CARTESIAN_POINT('Ctrl Pts',(24.3987605230519,0.520676515704192,
124.908458602183));
#178150=CARTESIAN_POINT('Ctrl Pts',(24.4061584373632,0.677229048280863,
124.926496092191));
#178151=CARTESIAN_POINT('Ctrl Pts',(24.4135551222754,0.833755564666995,
124.944530584695));
#178152=CARTESIAN_POINT('Ctrl Pts',(24.4209518071876,0.98960820836661,124.968827222111));
#178153=CARTESIAN_POINT('Ctrl Pts',(24.4283484920998,1.1442519333095,124.99930953462));
#178154=CARTESIAN_POINT('Ctrl Pts',(24.4357448490353,1.29888880118756,125.029790495511));
#178155=CARTESIAN_POINT('Ctrl Pts',(24.4431412059707,1.4523164906429,125.066456513942));
#178156=CARTESIAN_POINT('Ctrl Pts',(24.4505375629061,1.60400973569663,125.109179906624));
#178157=CARTESIAN_POINT('Ctrl Pts',(24.4579350522427,1.75572620537343,125.151909840366));
#178158=CARTESIAN_POINT('Ctrl Pts',(24.4653325415793,1.90570734256569,125.200698893727));
#178159=CARTESIAN_POINT('Ctrl Pts',(24.4727300309159,2.05344278690677,125.255369422457));
#178160=CARTESIAN_POINT('Ctrl Pts',(24.4801301134309,2.20123001967885,125.310059115855));
#178161=CARTESIAN_POINT('Ctrl Pts',(24.4875301959458,2.34676964236528,125.370634260061));
#178162=CARTESIAN_POINT('Ctrl Pts',(24.4949302784608,2.48957116752841,125.436869027977));
#178163=CARTESIAN_POINT('Ctrl Pts',(24.5023384981273,2.63252971764881,125.503176627829));
#178164=CARTESIAN_POINT('Ctrl Pts',(24.5097467177938,2.77274381858923,125.575156122638));
#178165=CARTESIAN_POINT('Ctrl Pts',(24.5171549374602,2.90974684729997,125.652535324805));
#178166=CARTESIAN_POINT('Ctrl Pts',(24.5245677167623,3.04683419908907,125.729962152581));
#178167=CARTESIAN_POINT('Ctrl Pts',(24.5319804960644,3.18070622379183,125.812795114103));
#178168=CARTESIAN_POINT('Ctrl Pts',(24.5393932753664,3.3109256510603,125.900718920251));
#178169=CARTESIAN_POINT('Ctrl Pts',(24.5468166463952,3.44133114195296,125.988768356055));
#178170=CARTESIAN_POINT('Ctrl Pts',(24.5542400174239,3.56807331189845,126.081922943875));
#178171=CARTESIAN_POINT('Ctrl Pts',(24.5616633884526,3.69074766429063,126.179826885282));
#178172=CARTESIAN_POINT('Ctrl Pts',(24.5655994378935,3.75579254946112,126.23173790419));
#178173=CARTESIAN_POINT('Ctrl Pts',(24.5695354873344,3.81969442791911,126.284983507724));
#178174=CARTESIAN_POINT('Ctrl Pts',(24.5734715367753,3.88239733584584,126.339506589816));
#178175=CARTESIAN_POINT('Ctrl Pts',(24.5808948031808,4.00065306330287,126.442335421033));
#178176=CARTESIAN_POINT('Ctrl Pts',(24.5883180695862,4.11499951238944,126.550021152415));
#178177=CARTESIAN_POINT('Ctrl Pts',(24.5957413359917,4.22501200326998,126.66223505999));
#178178=CARTESIAN_POINT('Ctrl Pts',(24.6031558287127,4.33489446852228,126.774316340045));
#178179=CARTESIAN_POINT('Ctrl Pts',(24.6105703214338,4.44045291290973,126.890914879288));
#178180=CARTESIAN_POINT('Ctrl Pts',(24.6179848141548,4.5412956116416,127.011661746025));
#178181=CARTESIAN_POINT('Ctrl Pts',(24.6253921605086,4.64204111438377,127.132292232387));
#178182=CARTESIAN_POINT('Ctrl Pts',(24.6327995068624,4.73807968241352,127.257062801791));
#178183=CARTESIAN_POINT('Ctrl Pts',(24.6402068532162,4.82905645503334,127.385567801878));
#178184=CARTESIAN_POINT('Ctrl Pts',(24.6476086748916,4.91996537374391,127.513976958088));
#178185=CARTESIAN_POINT('Ctrl Pts',(24.655010496567,5.0058197993633,127.646114695752));
#178186=CARTESIAN_POINT('Ctrl Pts',(24.6624123182425,5.08630526646846,127.78154251209));
#178187=CARTESIAN_POINT('Ctrl Pts',(24.6698102325539,5.16674824592203,127.916898837137));
#178188=CARTESIAN_POINT('Ctrl Pts',(24.6772081468652,5.24182772113697,128.055541461833));
#178189=CARTESIAN_POINT('Ctrl Pts',(24.6846060611766,5.31127273781135,128.197003245229));
#178190=CARTESIAN_POINT('Ctrl Pts',(24.6920027460888,5.38070621398372,128.338441520242));
#178191=CARTESIAN_POINT('Ctrl Pts',(24.6993994310011,5.44450692564126,128.482697689365));
#178192=CARTESIAN_POINT('Ctrl Pts',(24.7067961159133,5.50245000353816,128.62928026938));
#178193=CARTESIAN_POINT('Ctrl Pts',(24.7141924728488,5.56039051217835,128.775856349771));
#178194=CARTESIAN_POINT('Ctrl Pts',(24.7215888297843,5.61247376626662,128.924758288788));
#178195=CARTESIAN_POINT('Ctrl Pts',(24.7289851867198,5.65852327027925,129.07547514935));
#178196=CARTESIAN_POINT('Ctrl Pts',(24.7363826760564,5.70457982458843,129.226215085048));
#178197=CARTESIAN_POINT('Ctrl Pts',(24.743780165393,5.74460068036273,129.378770138535));
#178198=CARTESIAN_POINT('Ctrl Pts',(24.7511776547296,5.77845943249758,129.532614908126));
#178199=CARTESIAN_POINT('Ctrl Pts',(24.7585777372446,5.81233005376556,129.686513607762));
#178200=CARTESIAN_POINT('Ctrl Pts',(24.7659778197597,5.84003419043265,129.841702559298));
#178201=CARTESIAN_POINT('Ctrl Pts',(24.7733779022747,5.86149671679066,129.997647036701));
#178202=CARTESIAN_POINT('Ctrl Pts',(24.7807861219412,5.8829828434028,130.153762991088));
#178203=CARTESIAN_POINT('Ctrl Pts',(24.7881943416076,5.89821360233257,130.31063576042));
#178204=CARTESIAN_POINT('Ctrl Pts',(24.7956025612741,5.90716577155861,130.467725637467));
#178205=CARTESIAN_POINT('Ctrl Pts',(24.8030153405762,5.91612345069544,130.624912200711));
#178206=CARTESIAN_POINT('Ctrl Pts',(24.8104281198783,5.9187948335726,130.782315765558));
#178207=CARTESIAN_POINT('Ctrl Pts',(24.8178408991804,5.91520882655381,130.939398022606));
#178208=CARTESIAN_POINT('Ctrl Pts',(24.8252642702092,5.91161769568003,131.096704726149));
#178209=CARTESIAN_POINT('Ctrl Pts',(24.832687641238,5.90175134137646,131.253688833394));
#178210=CARTESIAN_POINT('Ctrl Pts',(24.8401110122668,5.885690466642,131.409817712148));
#178211=CARTESIAN_POINT('Ctrl Pts',(24.8440470617073,5.87717460548304,131.492600989918));
#178212=CARTESIAN_POINT('Ctrl Pts',(24.8479831111478,5.86691809743371,131.575143999358));
#178213=CARTESIAN_POINT('Ctrl Pts',(24.8519191605883,5.85493873763482,131.657368789299));
#178214=CARTESIAN_POINT('Ctrl Pts',(24.8593424269937,5.83234603891552,131.812442176991));
#178215=CARTESIAN_POINT('Ctrl Pts',(24.8667656933991,5.80355403208354,131.966851851249));
#178216=CARTESIAN_POINT('Ctrl Pts',(24.8741889598045,5.76860973210365,132.120062833563));
#178217=CARTESIAN_POINT('Ctrl Pts',(24.8816034525255,5.73370673338439,132.273092733219));
#178218=CARTESIAN_POINT('Ctrl Pts',(24.8890179452466,5.69266599767656,132.424926400591));
#178219=CARTESIAN_POINT('Ctrl Pts',(24.8964324379676,5.64558618084606,132.575034849925));
#178220=CARTESIAN_POINT('Ctrl Pts',(24.9038397843214,5.59855174131547,132.724998619084));
#178221=CARTESIAN_POINT('Ctrl Pts',(24.9112471306751,5.54548991948243,132.873240126774));
#178222=CARTESIAN_POINT('Ctrl Pts',(24.9186544770289,5.48655019129086,133.019241553631));
#178223=CARTESIAN_POINT('Ctrl Pts',(24.9260562987043,5.42765442257233,133.165134087116));
#178224=CARTESIAN_POINT('Ctrl Pts',(24.9334581203797,5.36288961569906,133.308789521764));
#178225=CARTESIAN_POINT('Ctrl Pts',(24.9408599420551,5.29245471923663,133.449706267444));
#178226=CARTESIAN_POINT('Ctrl Pts',(24.9482578563664,5.22205700480778,133.590548624272));
#178227=CARTESIAN_POINT('Ctrl Pts',(24.9556557706778,5.14599532836024,133.728654838313));
#178228=CARTESIAN_POINT('Ctrl Pts',(24.9630536849891,5.06451625138588,133.863544446947));
#178229=CARTESIAN_POINT('Ctrl Pts',(24.9704503699014,4.98305071475594,133.998411639375));
#178230=CARTESIAN_POINT('Ctrl Pts',(24.9778470548135,4.89616975719619,134.130062968087));
#178231=CARTESIAN_POINT('Ctrl Pts',(24.9852437397257,4.80416533013663,134.258043585531));
#178232=CARTESIAN_POINT('Ctrl Pts',(24.9926400966611,4.71216498264979,134.386018528181));
#178233=CARTESIAN_POINT('Ctrl Pts',(25.0000364535966,4.61504183527233,134.510322780091));
#178234=CARTESIAN_POINT('Ctrl Pts',(25.0074328105321,4.5131303536997,134.630531676603));
#178235=CARTESIAN_POINT('Ctrl Pts',(25.0148302998686,4.41120326921907,134.750758977405));
#178236=CARTESIAN_POINT('Ctrl Pts',(25.0222277892052,4.30448663224654,134.866889389592));
#178237=CARTESIAN_POINT('Ctrl Pts',(25.0296252785417,4.1933541530555,134.978532572523));
#178238=CARTESIAN_POINT('Ctrl Pts',(25.0370253610567,4.08218271654616,135.0902148918));
#178239=CARTESIAN_POINT('Ctrl Pts',(25.0444254435717,3.96659261901945,135.197406585606));
#178240=CARTESIAN_POINT('Ctrl Pts',(25.0518255260867,3.84699313335238,135.299755416073));
#178241=CARTESIAN_POINT('Ctrl Pts',(25.0592337457532,3.72726213575569,135.4022167896));
#178242=CARTESIAN_POINT('Ctrl Pts',(25.0666419654197,3.60351322928271,135.4998244221));
#178243=CARTESIAN_POINT('Ctrl Pts',(25.0740501850862,3.47618793284358,135.592267051286));
#178244=CARTESIAN_POINT('Ctrl Pts',(25.0814629643882,3.34878426980885,135.684766577367));
#178245=CARTESIAN_POINT('Ctrl Pts',(25.0888757436903,3.21780014050114,135.772094559034));
#178246=CARTESIAN_POINT('Ctrl Pts',(25.0962885229924,3.08370406445976,135.853984346651));
#178247=CARTESIAN_POINT('Ctrl Pts',(25.1037118940211,2.94941638565646,135.935991142236));
#178248=CARTESIAN_POINT('Ctrl Pts',(25.1111352650498,2.81200820471106,136.012544043446));
#178249=CARTESIAN_POINT('Ctrl Pts',(25.1185586360786,2.6719712621141,136.083423047291));
#178250=CARTESIAN_POINT('Ctrl Pts',(25.1224946855194,2.59772031500809,136.121004795849));
#178251=CARTESIAN_POINT('Ctrl Pts',(25.1264307349603,2.52273065029043,136.156992217978));
#178252=CARTESIAN_POINT('Ctrl Pts',(25.1303667844011,2.44707746919643,136.191358150724));
#178253=CARTESIAN_POINT('Ctrl Pts',(25.1377900508066,2.30439793070983,136.256171227358));
#178254=CARTESIAN_POINT('Ctrl Pts',(25.145213317212,2.15892591567081,136.315409897181));
#178255=CARTESIAN_POINT('Ctrl Pts',(25.1526365836174,2.01113692938864,136.368824546261));
#178256=CARTESIAN_POINT('Ctrl Pts',(25.1600510763384,1.86352261741495,136.422176063662));
#178257=CARTESIAN_POINT('Ctrl Pts',(25.1674655690594,1.71359713277626,136.469717136335));
#178258=CARTESIAN_POINT('Ctrl Pts',(25.1748800617804,1.56185885207399,136.511244836533));
#178259=CARTESIAN_POINT('Ctrl Pts',(25.1822874081341,1.41026682243951,136.552732510771));
#178260=CARTESIAN_POINT('Ctrl Pts',(25.189694754488,1.25686583279447,136.588218253181));
#178261=CARTESIAN_POINT('Ctrl Pts',(25.1971021008418,1.10217233463407,136.617547928093));
#178262=CARTESIAN_POINT('Ctrl Pts',(25.2045039225171,0.947594212721068,
136.646855727826));
#178263=CARTESIAN_POINT('Ctrl Pts',(25.2119057441925,0.791725866935453,
136.670016532975));
#178264=CARTESIAN_POINT('Ctrl Pts',(25.2193075658679,0.63509683581886,136.686926602885));
#178265=CARTESIAN_POINT('Ctrl Pts',(25.2267054801792,0.478550487948597,
136.7038277461));
#178266=CARTESIAN_POINT('Ctrl Pts',(25.2341033944905,0.321244624674761,
136.714484685648));
#178267=CARTESIAN_POINT('Ctrl Pts',(25.2415013088019,0.163716745317209,
136.71884515891));
#178268=CARTESIAN_POINT('Ctrl Pts',(25.2488979937141,0.00621504423535982,
136.723204907542));
#178269=CARTESIAN_POINT('Ctrl Pts',(25.2562946786262,-0.151508226914853,
136.721270256281));
#178270=CARTESIAN_POINT('Ctrl Pts',(25.2636913635384,-0.308912585129157,
136.713040975924));
#178271=CARTESIAN_POINT('Ctrl Pts',(25.2710877204738,-0.466309963869269,
136.704812060463));
#178272=CARTESIAN_POINT('Ctrl Pts',(25.2784840774093,-0.623388085001987,
136.690289090361));
#178273=CARTESIAN_POINT('Ctrl Pts',(25.2858804343447,-0.779608879247233,
136.669523919461));
#178274=CARTESIAN_POINT('Ctrl Pts',(25.2932779236813,-0.935853591294892,
136.648755569361));
#178275=CARTESIAN_POINT('Ctrl Pts',(25.3006754130179,-1.0912403450341,136.621743164734));
#178276=CARTESIAN_POINT('Ctrl Pts',(25.3080729023544,-1.24523873629802,
136.588590129966));
#178277=CARTESIAN_POINT('Ctrl Pts',(25.3154729848694,-1.39929111145949,
136.555425473454));
#178278=CARTESIAN_POINT('Ctrl Pts',(25.3228730673844,-1.5519537904435,136.516115979528));
#178279=CARTESIAN_POINT('Ctrl Pts',(25.3302731498994,-1.70270920356773,
136.470815587879));
#178280=CARTESIAN_POINT('Ctrl Pts',(25.3376813695658,-1.85363038776651,
136.425465383793));
#178281=CARTESIAN_POINT('Ctrl Pts',(25.3450895892323,-2.00263976006402,
136.374111233591));
#178282=CARTESIAN_POINT('Ctrl Pts',(25.3524978088987,-2.14923679492765,
136.316956354769));
#178283=CARTESIAN_POINT('Ctrl Pts',(25.3599105882008,-2.29592405782034,
136.259766298072));
#178284=CARTESIAN_POINT('Ctrl Pts',(25.3673233675028,-2.44019568341001,
136.196768547618));
#178285=CARTESIAN_POINT('Ctrl Pts',(25.3747361468049,-2.58157408554993,
136.128213151523));
#178286=CARTESIAN_POINT('Ctrl Pts',(25.3821595178337,-2.72315449578081,
136.059559800262));
#178287=CARTESIAN_POINT('Ctrl Pts',(25.3895828888624,-2.86183309784256,
135.985333119044));
#178288=CARTESIAN_POINT('Ctrl Pts',(25.3970062598912,-2.99715899924097,
135.905827906079));
#178289=CARTESIAN_POINT('Ctrl Pts',(25.4009423093321,-3.06891203926582,
135.863672334462));
#178290=CARTESIAN_POINT('Ctrl Pts',(25.404878358773,-3.13972302222651,135.820033486419));
#178291=CARTESIAN_POINT('Ctrl Pts',(25.408814408214,-3.20952844705469,135.774959948637));
#178292=CARTESIAN_POINT('Ctrl Pts',(25.4162346050843,-3.34112486183839,
135.68998781376));
#178293=CARTESIAN_POINT('Ctrl Pts',(25.4236548019546,-3.4695443034646,135.599657033977));
#178294=CARTESIAN_POINT('Ctrl Pts',(25.4310749988249,-3.59431996881035,
135.504232373722));
#178295=CARTESIAN_POINT('Ctrl Pts',(25.4384864234167,-3.71894812231803,
135.408920526065));
#178296=CARTESIAN_POINT('Ctrl Pts',(25.4458978480086,-3.83994078008817,
135.308527009478));
#178297=CARTESIAN_POINT('Ctrl Pts',(25.4533092726004,-3.9568580362525,135.203361077153));
#178298=CARTESIAN_POINT('Ctrl Pts',(25.4607135552692,-4.07366262662126,
135.098296486613));
#178299=CARTESIAN_POINT('Ctrl Pts',(25.4681178379381,-4.18639935763738,
134.988468883858));
#178300=CARTESIAN_POINT('Ctrl Pts',(25.4755221206069,-4.29465958995777,
134.874229112847));
#178301=CARTESIAN_POINT('Ctrl Pts',(25.4829208860585,-4.40283915339494,
134.760074466305));
#178302=CARTESIAN_POINT('Ctrl Pts',(25.4903196515101,-4.50654860379132,
134.64151446767));
#178303=CARTESIAN_POINT('Ctrl Pts',(25.4977184169617,-4.60541461751424,
134.518938219836));
#178304=CARTESIAN_POINT('Ctrl Pts',(25.5051132855161,-4.70422855894348,
134.396426532371));
#178305=CARTESIAN_POINT('Ctrl Pts',(25.5125081540706,-4.79820391012449,
134.269903098562));
#178306=CARTESIAN_POINT('Ctrl Pts',(25.519903022625,-4.88700634916399,134.139791550104));
#178307=CARTESIAN_POINT('Ctrl Pts',(25.527296676565,-4.97579420231431,134.009701372598));
#178308=CARTESIAN_POINT('Ctrl Pts',(25.5346903305049,-5.05941061909563,
133.876024558373));
#178309=CARTESIAN_POINT('Ctrl Pts',(25.5420839844448,-5.13756344001877,
133.739215377564));
#178310=CARTESIAN_POINT('Ctrl Pts',(25.5494773254721,-5.21571295337497,
133.602411986764));
#178311=CARTESIAN_POINT('Ctrl Pts',(25.5568706664994,-5.28839914527273,
133.462476817398));
#178312=CARTESIAN_POINT('Ctrl Pts',(25.5642640075267,-5.35537498064481,
133.319890259447));
#178313=CARTESIAN_POINT('Ctrl Pts',(25.5716584987318,-5.42236123540883,
133.177281519388));
#178314=CARTESIAN_POINT('Ctrl Pts',(25.5790529899368,-5.48363520598969,
133.032020907689));
#178315=CARTESIAN_POINT('Ctrl Pts',(25.5864474811419,-5.53899739066159,
132.884610234498));
#178316=CARTESIAN_POINT('Ctrl Pts',(25.5938445860284,-5.5943791438355,132.737147457039));
#178317=CARTESIAN_POINT('Ctrl Pts',(25.601241690915,-5.64384481952122,132.587533454593));
#178318=CARTESIAN_POINT('Ctrl Pts',(25.6086387958015,-5.68724435633118,
132.436286533127));
#178319=CARTESIAN_POINT('Ctrl Pts',(25.6160440377224,-5.73069163391611,
132.28487323557));
#178320=CARTESIAN_POINT('Ctrl Pts',(25.6234492796433,-5.76805934356134,
132.131823791191));
#178321=CARTESIAN_POINT('Ctrl Pts',(25.6308545215641,-5.79924809922357,
131.977668780902));
#178322=CARTESIAN_POINT('Ctrl Pts',(25.6382643467168,-5.83045615814433,
131.82341836142));
#178323=CARTESIAN_POINT('Ctrl Pts',(25.6456741718695,-5.85547758370099,
131.668061380605));
#178324=CARTESIAN_POINT('Ctrl Pts',(25.6530839970223,-5.87426478966554,
131.512134411511));
#178325=CARTESIAN_POINT('Ctrl Pts',(25.6605043622138,-5.89307871932133,
131.355985645511));
#178326=CARTESIAN_POINT('Ctrl Pts',(25.6679247274053,-5.90564068938807,
131.199265643398));
#178327=CARTESIAN_POINT('Ctrl Pts',(25.6753450925968,-5.91195518967298,
131.042512665214));
#178328=CARTESIAN_POINT('Ctrl Pts',(25.6791049976631,-5.91515475209332,
130.963085803919));
#178329=CARTESIAN_POINT('Ctrl Pts',(25.6828649027293,-5.91675113395662,
130.883650431332));
#178330=CARTESIAN_POINT('Ctrl Pts',(25.6866248077955,-5.91674999939557,
130.804276044766));
#178331=CARTESIAN_POINT('',(27.4366239742277,-5.91481336151323,130.809673827526));
#178332=CARTESIAN_POINT('Ctrl Pts',(25.6866248077955,-5.92653132131743,
130.804275904954));
#178333=CARTESIAN_POINT('Ctrl Pts',(25.6868372158726,-5.92653226647307,
130.799784399869));
#178334=CARTESIAN_POINT('Ctrl Pts',(25.6870496239497,-5.92652760397538,
130.795292896806));
#178335=CARTESIAN_POINT('Ctrl Pts',(25.7800779066311,-5.92202701559398,
128.828156677032));
#178336=CARTESIAN_POINT('Ctrl Pts',(25.9657096558399,-3.76932368489478,
124.907771816502));
#178337=CARTESIAN_POINT('Ctrl Pts',(26.2441572796525,2.92355563587315,124.445871569505));
#178338=CARTESIAN_POINT('Ctrl Pts',(26.5226049034657,6.92983015090643,129.827112128218));
#178339=CARTESIAN_POINT('Ctrl Pts',(26.8010525272784,4.56792929827948,136.1063963074));
#178340=CARTESIAN_POINT('Ctrl Pts',(27.0795001510913,-1.99167542371128,
137.513368706464));
#178341=CARTESIAN_POINT('Ctrl Pts',(27.2913571581557,-5.59000537624551,
133.893030412084));
#178342=CARTESIAN_POINT('Ctrl Pts',(27.4103982906157,-5.91861368694706,
131.367325223928));
#178343=CARTESIAN_POINT('Ctrl Pts',(27.4366235484716,-5.91382540835153,
130.809681996055));
#178344=CARTESIAN_POINT('',(29.1866256294184,-5.9117342771041,130.802189275152));
#178345=CARTESIAN_POINT('Ctrl Pts',(27.4366248077956,-5.91674762872223,
130.809657834746));
#178346=CARTESIAN_POINT('Ctrl Pts',(27.443965016876,-5.91688743308838,130.65350279638));
#178347=CARTESIAN_POINT('Ctrl Pts',(27.4513052259564,-5.91084113374822,
130.497219595639));
#178348=CARTESIAN_POINT('Ctrl Pts',(27.4586454350368,-5.89860518297208,
130.341340685042));
#178349=CARTESIAN_POINT('Ctrl Pts',(27.4660516835234,-5.88625914610499,
130.184059341544));
#178350=CARTESIAN_POINT('Ctrl Pts',(27.4734579320102,-5.86761150181308,
130.027189989693));
#178351=CARTESIAN_POINT('Ctrl Pts',(27.4808641804968,-5.84271241096424,
129.871278496172));
#178352=CARTESIAN_POINT('Ctrl Pts',(27.4882001791284,-5.81804949333168,
129.716845856602));
#178353=CARTESIAN_POINT('Ctrl Pts',(27.4955361777599,-5.78725328873107,
129.563353362203));
#178354=CARTESIAN_POINT('Ctrl Pts',(27.5028721763914,-5.75042446463643,
129.411324710272));
#178355=CARTESIAN_POINT('Ctrl Pts',(27.5102083131135,-5.71359494728757,
129.259293196601));
#178356=CARTESIAN_POINT('Ctrl Pts',(27.5175444498355,-5.67073267353985,
129.108725949671));
#178357=CARTESIAN_POINT('Ctrl Pts',(27.5248805865576,-5.62198896756605,
128.960134326932));
#178358=CARTESIAN_POINT('Ctrl Pts',(27.5322183682366,-5.57323433195728,
128.811509386));
#178359=CARTESIAN_POINT('Ctrl Pts',(27.5395561499156,-5.51859575789823,
128.664861311901));
#178360=CARTESIAN_POINT('Ctrl Pts',(27.5468939315946,-5.45827368163428,
128.520683981333));
#178361=CARTESIAN_POINT('Ctrl Pts',(27.5543523871881,-5.39695957516337,
128.374135574105));
#178362=CARTESIAN_POINT('Ctrl Pts',(27.5618108427816,-5.3297735441911,128.230140266825));
#178363=CARTESIAN_POINT('Ctrl Pts',(27.5692692983752,-5.25697551298712,
128.089192295278));
#178364=CARTESIAN_POINT('Ctrl Pts',(27.5766186203589,-5.18524267709565,
127.950306702565));
#178365=CARTESIAN_POINT('Ctrl Pts',(27.5839679423425,-5.10806120040344,
127.814380171892));
#178366=CARTESIAN_POINT('Ctrl Pts',(27.5913172643262,-5.02572412757875,
127.681857205883));
#178367=CARTESIAN_POINT('Ctrl Pts',(27.5988302867247,-4.94155306067873,
127.546382394172));
#178368=CARTESIAN_POINT('Ctrl Pts',(27.6063433091232,-4.85199427692997,
127.414464896858));
#178369=CARTESIAN_POINT('Ctrl Pts',(27.6138563315217,-4.75740460400089,
127.286544249941));
#178370=CARTESIAN_POINT('Ctrl Pts',(27.6213693539202,-4.66281493107167,
127.158623603023));
#178371=CARTESIAN_POINT('Ctrl Pts',(27.6288823763187,-4.56319468257101,
127.034700088833));
#178372=CARTESIAN_POINT('Ctrl Pts',(27.6363953987172,-4.45894050967834,
126.915173029695));
#178373=CARTESIAN_POINT('Ctrl Pts',(27.6438186651226,-4.3559318324494,126.797073927153));
#178374=CARTESIAN_POINT('Ctrl Pts',(27.651241931528,-4.2480722099351,126.68289148983));
#178375=CARTESIAN_POINT('Ctrl Pts',(27.6586651979334,-4.13569101201919,
126.573049896808));
#178376=CARTESIAN_POINT('Ctrl Pts',(27.6660796906545,-4.02344263934621,
126.463338127426));
#178377=CARTESIAN_POINT('Ctrl Pts',(27.6734941833755,-3.90668359313888,
126.357957248402));
#178378=CARTESIAN_POINT('Ctrl Pts',(27.6809086760965,-3.78578340080344,
126.257298422621));
#178379=CARTESIAN_POINT('Ctrl Pts',(27.6883160224503,-3.66499973662536,
126.156736615606));
#178380=CARTESIAN_POINT('Ctrl Pts',(27.6957233688041,-3.54008315735201,
126.060888038354));
#178381=CARTESIAN_POINT('Ctrl Pts',(27.7031307151579,-3.41143985491094,
125.970106933819));
#178382=CARTESIAN_POINT('Ctrl Pts',(27.7105325368333,-3.28289249949808,
125.879393537256));
#178383=CARTESIAN_POINT('Ctrl Pts',(27.7179343585087,-3.15062425902694,
125.793740302197));
#178384=CARTESIAN_POINT('Ctrl Pts',(27.7253361801841,-3.01507411433273,
125.713461026376));
#178385=CARTESIAN_POINT('Ctrl Pts',(27.7327340944955,-2.87959552550517,
125.633224129359));
#178386=CARTESIAN_POINT('Ctrl Pts',(27.7401320088068,-2.74083880317532,
125.558355731559));
#178387=CARTESIAN_POINT('Ctrl Pts',(27.7475299231182,-2.59927150009754,
125.489126076054));
#178388=CARTESIAN_POINT('Ctrl Pts',(27.7549266080304,-2.45772772293704,
125.419907925262));
#178389=CARTESIAN_POINT('Ctrl Pts',(27.7623232929426,-2.31337462703835,
125.356326820817));
#178390=CARTESIAN_POINT('Ctrl Pts',(27.7697199778548,-2.16670403726219,
125.298606883752));
#178391=CARTESIAN_POINT('Ctrl Pts',(27.7771163347903,-2.02003995101388,
125.240889506048));
#178392=CARTESIAN_POINT('Ctrl Pts',(27.7845126917257,-1.87105892257703,
125.189032915675));
#178393=CARTESIAN_POINT('Ctrl Pts',(27.7919090486611,-1.72027215703767,
125.143212830392));
#178394=CARTESIAN_POINT('Ctrl Pts',(27.7993065379977,-1.56946230565956,
125.097385729937));
#178395=CARTESIAN_POINT('Ctrl Pts',(27.8067040273342,-1.41684652389887,
125.057597083329));
#178396=CARTESIAN_POINT('Ctrl Pts',(27.8141015166708,-1.26295040520195,
125.023972495952));
#178397=CARTESIAN_POINT('Ctrl Pts',(27.8215015991858,-1.10900033845896,
124.990336121528));
#178398=CARTESIAN_POINT('Ctrl Pts',(27.8289016817008,-0.953769405649258,
124.962868188108));
#178399=CARTESIAN_POINT('Ctrl Pts',(27.8363017642158,-0.797792446516978,
124.941643007551));
#178400=CARTESIAN_POINT('Ctrl Pts',(27.8437099838823,-0.641643974683311,
124.920394487726));
#178401=CARTESIAN_POINT('Ctrl Pts',(27.8511182035487,-0.484748208384811,
124.905402480083));
#178402=CARTESIAN_POINT('Ctrl Pts',(27.8585264232152,-0.32764488956888,
124.896689385275));
#178403=CARTESIAN_POINT('Ctrl Pts',(27.8659392025172,-0.170444876281628,
124.887970927702));
#178404=CARTESIAN_POINT('Ctrl Pts',(27.8733519818193,-0.0130374283167435,
124.885539089349));
#178405=CARTESIAN_POINT('Ctrl Pts',(27.8807647611214,0.144039189540048,
124.88936414467));
#178406=CARTESIAN_POINT('Ctrl Pts',(27.8881881321502,0.301340245834596,
124.893194665409));
#178407=CARTESIAN_POINT('Ctrl Pts',(27.8956115031789,0.458309156382128,
124.903299911375));
#178408=CARTESIAN_POINT('Ctrl Pts',(27.9030348742077,0.614413412423298,
124.919598369086));
#178409=CARTESIAN_POINT('Ctrl Pts',(27.9069709236484,0.697183634646086,
124.928240202441));
#178410=CARTESIAN_POINT('Ctrl Pts',(27.9109069730892,0.779710939849281,
124.938622315023));
#178411=CARTESIAN_POINT('Ctrl Pts',(27.91484302253,0.861917404034309,124.950726793084));
#178412=CARTESIAN_POINT('Ctrl Pts',(27.9222662889354,1.01695622991221,124.973555460939));
#178413=CARTESIAN_POINT('Ctrl Pts',(27.9296895553408,1.17132190883347,125.002582419669));
#178414=CARTESIAN_POINT('Ctrl Pts',(27.9371128217462,1.32447953445568,125.037759840218));
#178415=CARTESIAN_POINT('Ctrl Pts',(27.9445273144673,1.47745614048356,125.072895683977));
#178416=CARTESIAN_POINT('Ctrl Pts',(27.9519418071883,1.62922717502141,125.114167437156));
#178417=CARTESIAN_POINT('Ctrl Pts',(27.9593562999093,1.7792638030657,125.161475638976));
#178418=CARTESIAN_POINT('Ctrl Pts',(27.9667636462631,1.92915582015953,125.20873824337));
#178419=CARTESIAN_POINT('Ctrl Pts',(27.9741709926169,2.0773164051288,125.262025602098));
#178420=CARTESIAN_POINT('Ctrl Pts',(27.9815783389707,2.22322796668605,125.321187451356));
#178421=CARTESIAN_POINT('Ctrl Pts',(27.9889801606462,2.36903070189555,125.380305175475));
#178422=CARTESIAN_POINT('Ctrl Pts',(27.9963819823215,2.51258740918187,125.445288526469));
#178423=CARTESIAN_POINT('Ctrl Pts',(28.003783803997,2.65339680176143,125.515937792668));
#178424=CARTESIAN_POINT('Ctrl Pts',(28.0111817183084,2.79413186215931,125.58654976367));
#178425=CARTESIAN_POINT('Ctrl Pts',(28.0185796326198,2.93212216335348,125.662821526187));
#178426=CARTESIAN_POINT('Ctrl Pts',(28.0259775469312,3.0668876185034,125.744505787833));
#178427=CARTESIAN_POINT('Ctrl Pts',(28.0333742318434,3.20163067807899,125.826176475036));
#178428=CARTESIAN_POINT('Ctrl Pts',(28.0407709167557,3.33314963631253,125.913257682901));
#178429=CARTESIAN_POINT('Ctrl Pts',(28.0481676016679,3.46099009048201,126.005456768135));
#178430=CARTESIAN_POINT('Ctrl Pts',(28.0555639586034,3.58882487607142,126.097651765164));
#178431=CARTESIAN_POINT('Ctrl Pts',(28.0629603155388,3.71298117914123,126.194963969986));
#178432=CARTESIAN_POINT('Ctrl Pts',(28.0703566724743,3.83303484452738,126.297058271024));
#178433=CARTESIAN_POINT('Ctrl Pts',(28.0777541618109,3.95310689043654,126.399168202961));
#178434=CARTESIAN_POINT('Ctrl Pts',(28.0851516511474,4.0690747635913,126.506061447077));
#178435=CARTESIAN_POINT('Ctrl Pts',(28.092549140484,4.1805486925268,126.617363699498));
#178436=CARTESIAN_POINT('Ctrl Pts',(28.099949222999,4.29206169847481,126.728704968751));
#178437=CARTESIAN_POINT('Ctrl Pts',(28.107349305514,4.3990773597029,126.844458059937));
#178438=CARTESIAN_POINT('Ctrl Pts',(28.114749388029,4.50124406159337,126.964213164607));
#178439=CARTESIAN_POINT('Ctrl Pts',(28.1221576076954,4.60352310627586,127.084099952326));
#178440=CARTESIAN_POINT('Ctrl Pts',(28.1295658273619,4.70094230097773,127.207997257701));
#178441=CARTESIAN_POINT('Ctrl Pts',(28.1369740470284,4.79319105568959,127.335463088645));
#178442=CARTESIAN_POINT('Ctrl Pts',(28.1443868263304,4.88549658797059,127.46300737268));
#178443=CARTESIAN_POINT('Ctrl Pts',(28.1517996056325,4.9726251329659,127.594124248633));
#178444=CARTESIAN_POINT('Ctrl Pts',(28.1592123849345,5.05431075435431,127.72834479171));
#178445=CARTESIAN_POINT('Ctrl Pts',(28.1666357559633,5.13611309198947,127.862757115393));
#178446=CARTESIAN_POINT('Ctrl Pts',(28.1740591269921,5.21245679269273,128.000281637707));
#178447=CARTESIAN_POINT('Ctrl Pts',(28.1814824980209,5.28312260207257,128.140426283921));
#178448=CARTESIAN_POINT('Ctrl Pts',(28.1854185474616,5.32059130980751,128.214734338067));
#178449=CARTESIAN_POINT('Ctrl Pts',(28.1893545969023,5.35646456875852,128.289778682676));
#178450=CARTESIAN_POINT('Ctrl Pts',(28.1932906463429,5.39071533044503,128.365484075261));
#178451=CARTESIAN_POINT('Ctrl Pts',(28.2007139127484,5.45531119805775,128.508262082997));
#178452=CARTESIAN_POINT('Ctrl Pts',(28.2081371791538,5.51432841563994,128.653824080753));
#178453=CARTESIAN_POINT('Ctrl Pts',(28.2155604455592,5.56751809318757,128.801694183901));
#178454=CARTESIAN_POINT('Ctrl Pts',(28.2229749382802,5.62064490495354,128.949389516867));
#178455=CARTESIAN_POINT('Ctrl Pts',(28.2303894310012,5.66795776150901,129.099387177314));
#178456=CARTESIAN_POINT('Ctrl Pts',(28.2378039237222,5.70925449378641,129.251188480396));
#178457=CARTESIAN_POINT('Ctrl Pts',(28.245211270076,5.75051142271838,129.402843471667));
#178458=CARTESIAN_POINT('Ctrl Pts',(28.2526186164298,5.78576367384332,129.556298286936));
#178459=CARTESIAN_POINT('Ctrl Pts',(28.2600259627835,5.81485789762128,129.711036240736));
#178460=CARTESIAN_POINT('Ctrl Pts',(28.2674277844589,5.84393042182966,129.865658785133));
#178461=CARTESIAN_POINT('Ctrl Pts',(28.2748296061344,5.8668539950702,130.021562197229));
#178462=CARTESIAN_POINT('Ctrl Pts',(28.2822314278098,5.88352568267587,130.17821678122));
#178463=CARTESIAN_POINT('Ctrl Pts',(28.2896293421211,5.90018856942726,130.334788668475));
#178464=CARTESIAN_POINT('Ctrl Pts',(28.2970272564324,5.91060610388832,130.492110567638));
#178465=CARTESIAN_POINT('Ctrl Pts',(28.3044251707437,5.91472684148525,130.649644900478));
#178466=CARTESIAN_POINT('Ctrl Pts',(28.3118218556558,5.91884689429037,130.807153053971));
#178467=CARTESIAN_POINT('Ctrl Pts',(28.3192185405681,5.9166722173005,130.964873198271));
#178468=CARTESIAN_POINT('Ctrl Pts',(28.3266152254803,5.90820340383502,131.122264850649));
#178469=CARTESIAN_POINT('Ctrl Pts',(28.3340115824157,5.89973496588562,131.279649524117));
#178470=CARTESIAN_POINT('Ctrl Pts',(28.3414079393512,5.88497296644016,131.436705361867));
#178471=CARTESIAN_POINT('Ctrl Pts',(28.3488042962866,5.8639700781312,131.592894374156));
#178472=CARTESIAN_POINT('Ctrl Pts',(28.3562017856231,5.84296397422646,131.749107299381));
#178473=CARTESIAN_POINT('Ctrl Pts',(28.3635992749596,5.81571512869173,131.904452764903));
#178474=CARTESIAN_POINT('Ctrl Pts',(28.3709967642961,5.78232777297846,132.058400524563));
#178475=CARTESIAN_POINT('Ctrl Pts',(28.3783968468111,5.7489287133792,132.212402250373));
#178476=CARTESIAN_POINT('Ctrl Pts',(28.3857969293261,5.70938693836345,132.365004930219));
#178477=CARTESIAN_POINT('Ctrl Pts',(28.3931970118411,5.66385717509631,132.515691229286));
#178478=CARTESIAN_POINT('Ctrl Pts',(28.4006052315076,5.61827734717395,132.66654322343));
#178479=CARTESIAN_POINT('Ctrl Pts',(28.408013451174,5.56669648954086,132.815474270903));
#178480=CARTESIAN_POINT('Ctrl Pts',(28.4154216708405,5.50931858117112,132.961984156014));
#178481=CARTESIAN_POINT('Ctrl Pts',(28.4228344501426,5.45190535765593,133.108584215514));
#178482=CARTESIAN_POINT('Ctrl Pts',(28.4302472294447,5.38868812329735,133.252759802188));
#178483=CARTESIAN_POINT('Ctrl Pts',(28.4376600087468,5.31991765272615,133.394033710972));
#178484=CARTESIAN_POINT('Ctrl Pts',(28.4450833797755,5.25104891968187,133.535509478542));
#178485=CARTESIAN_POINT('Ctrl Pts',(28.4525067508043,5.17661127919204,133.674074959643));
#178486=CARTESIAN_POINT('Ctrl Pts',(28.459930121833,5.09690021530756,133.809279710936));
#178487=CARTESIAN_POINT('Ctrl Pts',(28.4638661712739,5.05463549659387,133.880968514267));
#178488=CARTESIAN_POINT('Ctrl Pts',(28.4678022207148,5.01088893682213,133.951713004331));
#178489=CARTESIAN_POINT('Ctrl Pts',(28.4717382701558,4.96570921926207,134.021449754074));
#178490=CARTESIAN_POINT('Ctrl Pts',(28.4791615365612,4.88050168195686,134.152971087675));
#178491=CARTESIAN_POINT('Ctrl Pts',(28.4865848029667,4.78993649839303,134.281303759618));
#178492=CARTESIAN_POINT('Ctrl Pts',(28.4940080693721,4.69427951265969,134.405981144429));
#178493=CARTESIAN_POINT('Ctrl Pts',(28.5014225620932,4.59873558553967,134.530511170925));
#178494=CARTESIAN_POINT('Ctrl Pts',(28.5088370548142,4.49811206029958,134.651394216484));
#178495=CARTESIAN_POINT('Ctrl Pts',(28.5162515475352,4.39271921730441,134.768190639202));
#178496=CARTESIAN_POINT('Ctrl Pts',(28.523658893889,4.28742795589973,134.884874489131));
#178497=CARTESIAN_POINT('Ctrl Pts',(28.5310662402428,4.17737677656537,134.997479282392));
#178498=CARTESIAN_POINT('Ctrl Pts',(28.5384735865966,4.06291749224456,135.105596720562));
#178499=CARTESIAN_POINT('Ctrl Pts',(28.5458754082719,3.9485435759763,135.213633520666));
#178500=CARTESIAN_POINT('Ctrl Pts',(28.5532772299473,3.82976837124208,135.317189374453));
#178501=CARTESIAN_POINT('Ctrl Pts',(28.5606790516227,3.70698188742178,135.41589136655));
#178502=CARTESIAN_POINT('Ctrl Pts',(28.5680769659341,3.58426022163018,135.514541254634));
#178503=CARTESIAN_POINT('Ctrl Pts',(28.5754748802455,3.45753178411389,135.608342150716));
#178504=CARTESIAN_POINT('Ctrl Pts',(28.5828727945568,3.32722104761594,135.696960198852));
#178505=CARTESIAN_POINT('Ctrl Pts',(28.5902694794691,3.19693196639815,135.785563520277));
#178506=CARTESIAN_POINT('Ctrl Pts',(28.5976661643813,3.06306207609928,135.868985493458));
#178507=CARTESIAN_POINT('Ctrl Pts',(28.6050628492935,2.92606642084863,135.946934473456));
#178508=CARTESIAN_POINT('Ctrl Pts',(28.612459206229,2.7890768401287,136.024879997115));
#178509=CARTESIAN_POINT('Ctrl Pts',(28.6198555631645,2.64896209449349,136.097352825506));
#178510=CARTESIAN_POINT('Ctrl Pts',(28.6272519201,2.50620328079606,136.16410647701));
#178511=CARTESIAN_POINT('Ctrl Pts',(28.6346494094366,2.36342261035959,136.230870348669));
#178512=CARTESIAN_POINT('Ctrl Pts',(28.6420468987732,2.2179974040005,136.291913141832));
#178513=CARTESIAN_POINT('Ctrl Pts',(28.6494443881098,2.07043011247464,136.347035938371));
#178514=CARTESIAN_POINT('Ctrl Pts',(28.6568444706249,1.92281109146329,136.402178058121));
#178515=CARTESIAN_POINT('Ctrl Pts',(28.6642445531399,1.77304883971829,136.451395918903));
#178516=CARTESIAN_POINT('Ctrl Pts',(28.671644635655,1.62166223948166,136.494540064959));
#178517=CARTESIAN_POINT('Ctrl Pts',(28.6790528553215,1.47010917411581,136.53773165244));
#178518=CARTESIAN_POINT('Ctrl Pts',(28.6864610749879,1.31692855244665,136.574836085069));
#178519=CARTESIAN_POINT('Ctrl Pts',(28.6938692946544,1.16265147571948,136.605754597336));
#178520=CARTESIAN_POINT('Ctrl Pts',(28.7012820739565,1.0082794440254,136.636692139431));
#178521=CARTESIAN_POINT('Ctrl Pts',(28.7086948532586,0.852809980353635,
136.661436116041));
#178522=CARTESIAN_POINT('Ctrl Pts',(28.7161076325607,0.696780120652307,
136.679939569973));
#178523=CARTESIAN_POINT('Ctrl Pts',(28.7235310035895,0.540527318170587,
136.698469462507));
#178524=CARTESIAN_POINT('Ctrl Pts',(28.7309543746183,0.383712891615819,
136.710740994564));
#178525=CARTESIAN_POINT('Ctrl Pts',(28.7383777456471,0.226875528073778,
136.716759289616));
#178526=CARTESIAN_POINT('Ctrl Pts',(28.7423137950877,0.143716594668171,
136.71995033406));
#178527=CARTESIAN_POINT('Ctrl Pts',(28.7462498445283,0.0605511674709851,
136.721384239266));
#178528=CARTESIAN_POINT('Ctrl Pts',(28.7501858939688,-0.0225410760443611,
136.721067679978));
#178529=CARTESIAN_POINT('Ctrl Pts',(28.7576091603742,-0.179250454103204,
136.720470659038));
#178530=CARTESIAN_POINT('Ctrl Pts',(28.7650324267796,-0.336173059472607,
136.713642549052));
#178531=CARTESIAN_POINT('Ctrl Pts',(28.7724556931851,-0.492772611700997,
136.700554789713));
#178532=CARTESIAN_POINT('Ctrl Pts',(28.7798701859061,-0.649187076263437,
136.687482499018));
#178533=CARTESIAN_POINT('Ctrl Pts',(28.7872846786271,-0.805278879335282,
136.668165316284));
#178534=CARTESIAN_POINT('Ctrl Pts',(28.7946991713481,-0.960510423616398,
136.642626651983));
#178535=CARTESIAN_POINT('Ctrl Pts',(28.8021065177018,-1.11559234989033,
136.617112602807));
#178536=CARTESIAN_POINT('Ctrl Pts',(28.8095138640555,-1.26981530217414,
136.585389070105));
#178537=CARTESIAN_POINT('Ctrl Pts',(28.8169212104093,-1.42264560394922,
136.547531348797));
#178538=CARTESIAN_POINT('Ctrl Pts',(28.8243230320847,-1.57536191912015,
136.509701863205));
#178539=CARTESIAN_POINT('Ctrl Pts',(28.8317248537601,-1.72668729116989,
136.465747388037));
#178540=CARTESIAN_POINT('Ctrl Pts',(28.8391266754356,-1.87609716623874,
136.415794479364));
#178541=CARTESIAN_POINT('Ctrl Pts',(28.8465245897469,-2.02542816899692,
136.365867940442));
#178542=CARTESIAN_POINT('Ctrl Pts',(28.8539225040582,-2.17284533544077,
136.309949392371));
#178543=CARTESIAN_POINT('Ctrl Pts',(28.8613204183695,-2.31783834522459,
136.248215498797));
#178544=CARTESIAN_POINT('Ctrl Pts',(28.8687171032817,-2.46280725980105,
136.186491864277));
#178545=CARTESIAN_POINT('Ctrl Pts',(28.8761137881939,-2.60535247413135,
136.118954948376));
#178546=CARTESIAN_POINT('Ctrl Pts',(28.8835104731061,-2.74498265660099,
136.045829951394));
#178547=CARTESIAN_POINT('Ctrl Pts',(28.8909068300416,-2.88460664772181,
135.972708196851));
#178548=CARTESIAN_POINT('Ctrl Pts',(28.898303186977,-3.02131553329272,135.893999027086));
#178549=CARTESIAN_POINT('Ctrl Pts',(28.9056995439125,-3.15464189674526,
135.80997397317));
#178550=CARTESIAN_POINT('Ctrl Pts',(28.9130970332491,-3.28798867280498,
135.725936054803));
#178551=CARTESIAN_POINT('Ctrl Pts',(28.9204945225856,-3.41795157975971,
135.636580830796));
#178552=CARTESIAN_POINT('Ctrl Pts',(28.9278920119222,-3.54409167524775,
135.542223507091));
#178553=CARTESIAN_POINT('Ctrl Pts',(28.9352920944372,-3.67027598895036,
135.447833106573));
#178554=CARTESIAN_POINT('Ctrl Pts',(28.9426921769522,-3.79263452436216,
135.34843733866));
#178555=CARTESIAN_POINT('Ctrl Pts',(28.9500922594672,-3.91076107159585,
135.244391969188));
#178556=CARTESIAN_POINT('Ctrl Pts',(28.9575004791336,-4.02901751111209,
135.140232191137));
#178557=CARTESIAN_POINT('Ctrl Pts',(28.9649086988002,-4.143032388792,135.031412847989));
#178558=CARTESIAN_POINT('Ctrl Pts',(28.9723169184666,-4.25243553721774,
134.918327385092));
#178559=CARTESIAN_POINT('Ctrl Pts',(28.9797296977688,-4.36190602145663,
134.805172319978));
#178560=CARTESIAN_POINT('Ctrl Pts',(28.9871424770708,-4.46675887243248,
134.687746180831));
#178561=CARTESIAN_POINT('Ctrl Pts',(28.994555256373,-4.56666430268049,134.566475409691));
#178562=CARTESIAN_POINT('Ctrl Pts',(29.0019786274017,-4.66671248249163,
134.445031361187));
#178563=CARTESIAN_POINT('Ctrl Pts',(29.0094019984305,-4.761798897917,134.319732005737));
#178564=CARTESIAN_POINT('Ctrl Pts',(29.0168253694593,-4.85163668595149,
134.191033325406));
#178565=CARTESIAN_POINT('Ctrl Pts',(29.0207614189,-4.899270836795,134.122794197013));
#178566=CARTESIAN_POINT('Ctrl Pts',(29.0246974683408,-4.94543016668652,
134.053599828531));
#178567=CARTESIAN_POINT('Ctrl Pts',(29.0286335177815,-4.99007722365454,
133.983520862735));
#178568=CARTESIAN_POINT('Ctrl Pts',(29.0362400418879,-5.07635889267805,
133.848091328453));
#178569=CARTESIAN_POINT('Ctrl Pts',(29.0438465659943,-5.15724064230757,
133.708963349913));
#178570=CARTESIAN_POINT('Ctrl Pts',(29.0514530901007,-5.2323984196574,133.566594738792));
#178571=CARTESIAN_POINT('Ctrl Pts',(29.0590492970541,-5.30745425632099,
133.424419230161));
#178572=CARTESIAN_POINT('Ctrl Pts',(29.0666455040075,-5.37680142326697,
133.279012149228));
#178573=CARTESIAN_POINT('Ctrl Pts',(29.0742417109609,-5.44015902814017,
133.130860200855));
#178574=CARTESIAN_POINT('Ctrl Pts',(29.0818288199004,-5.50344074930285,
132.98288569479));
#178575=CARTESIAN_POINT('Ctrl Pts',(29.0894159288399,-5.56074706272857,
132.83217318864));
#178576=CARTESIAN_POINT('Ctrl Pts',(29.0970030377794,-5.61184284714001,
132.679234059029));
#178577=CARTESIAN_POINT('Ctrl Pts',(29.1045799859559,-5.66287020335803,
132.526499747652));
#178578=CARTESIAN_POINT('Ctrl Pts',(29.1121569341324,-5.7077035037439,132.371545087259));
#178579=CARTESIAN_POINT('Ctrl Pts',(29.1197338823088,-5.74615574642359,
132.214901187824));
#178580=CARTESIAN_POINT('Ctrl Pts',(29.1273048899565,-5.78457784152278,
132.05838010137));
#178581=CARTESIAN_POINT('Ctrl Pts',(29.1348758976042,-5.81662876103272,
131.900172750996));
#178582=CARTESIAN_POINT('Ctrl Pts',(29.1424469052518,-5.84217110628933,
131.740825954532));
#178583=CARTESIAN_POINT('Ctrl Pts',(29.1500122319244,-5.86769428561259,
131.5815987254));
#178584=CARTESIAN_POINT('Ctrl Pts',(29.1575775585969,-5.88671857053288,
131.421234097781));
#178585=CARTESIAN_POINT('Ctrl Pts',(29.1651428852695,-5.89915750936803,
131.260289605641));
#178586=CARTESIAN_POINT('Ctrl Pts',(29.1723035261115,-5.91093106222438,
131.107954385549));
#178587=CARTESIAN_POINT('Ctrl Pts',(29.1794641669536,-5.91680531166713,
130.955100016775));
#178588=CARTESIAN_POINT('Ctrl Pts',(29.1866248077956,-5.91674960731476,
130.802204964392));
#178589=CARTESIAN_POINT('',(30.9366248077955,-5.92174042288377,130.7998180981));
#178590=CARTESIAN_POINT('Ctrl Pts',(29.1866262959298,-5.90766577404403,
130.80217654783));
#178591=CARTESIAN_POINT('Ctrl Pts',(29.2267779111514,-5.91044712185902,
129.946168516127));
#178592=CARTESIAN_POINT('Ctrl Pts',(29.3597454009771,-5.33509832877074,
127.114953888422));
#178593=CARTESIAN_POINT('Ctrl Pts',(29.5855287654075,-0.96670133588667,
123.873051285443));
#178594=CARTESIAN_POINT('Ctrl Pts',(29.8639763892201,5.30898116095411,126.244505404626));
#178595=CARTESIAN_POINT('Ctrl Pts',(30.1424240130331,6.70596932902698,132.806243703186));
#178596=CARTESIAN_POINT('Ctrl Pts',(30.420871636846,1.94049928853783,137.528349243488));
#178597=CARTESIAN_POINT('Ctrl Pts',(30.6856052351002,-4.28566032468232,
136.143193126057));
#178598=CARTESIAN_POINT('Ctrl Pts',(30.85752295875,-5.90750938229346,132.476046720674));
#178599=CARTESIAN_POINT('Ctrl Pts',(30.9366248077955,-5.92174042288377,
130.7998180981));
#178600=CARTESIAN_POINT('',(32.6866248077956,-5.92231311245214,130.808682413197));
#178601=CARTESIAN_POINT('Ctrl Pts',(30.9366248077955,-5.92174042288377,
130.7998180981));
#178602=CARTESIAN_POINT('Ctrl Pts',(30.9503388333543,-5.92420768321634,
130.509207417696));
#178603=CARTESIAN_POINT('Ctrl Pts',(31.0568687335175,-5.77245931818093,
128.254344206899));
#178604=CARTESIAN_POINT('Ctrl Pts',(31.2562145082845,-2.87502317972114,
124.423780530593));
#178605=CARTESIAN_POINT('Ctrl Pts',(31.5346621320976,3.8141424796121,124.936662800225));
#178606=CARTESIAN_POINT('Ctrl Pts',(31.8131097559105,6.99829753140275,130.841672711039));
#178607=CARTESIAN_POINT('Ctrl Pts',(32.0915573797234,3.75135903767198,136.712394630739));
#178608=CARTESIAN_POINT('Ctrl Pts',(32.3700050035363,-2.94289514760019,
137.153921915842));
#178609=CARTESIAN_POINT('Ctrl Pts',(32.5683608128937,-5.78513647409968,
133.311856168978));
#178610=CARTESIAN_POINT('Ctrl Pts',(32.6739007476468,-5.92452395854052,
131.07824707337));
#178611=CARTESIAN_POINT('Ctrl Pts',(32.6866248077956,-5.92231311245214,
130.808682413197));
#178612=CARTESIAN_POINT('',(34.4366248077956,-5.90791192852897,130.806830871508));
#178613=CARTESIAN_POINT('Ctrl Pts',(32.6866248077956,-5.92231311245214,
130.808682413197));
#178614=CARTESIAN_POINT('Ctrl Pts',(32.7667166222511,-5.90839690389693,
129.111903044516));
#178615=CARTESIAN_POINT('Ctrl Pts',(32.939624311311,-4.25182580178573,125.425065311405));
#178616=CARTESIAN_POINT('Ctrl Pts',(33.2053478749749,2.01208611123176,124.101445579217));
#178617=CARTESIAN_POINT('Ctrl Pts',(33.4837954987878,6.7269339492388,128.874096342156));
#178618=CARTESIAN_POINT('Ctrl Pts',(33.7622431226007,5.26005811688714,135.420565675545));
#178619=CARTESIAN_POINT('Ctrl Pts',(34.0406907464136,-1.0405541567591,137.724968074804));
#178620=CARTESIAN_POINT('Ctrl Pts',(34.2654846414787,-5.35514334605665,
134.451080629057));
#178621=CARTESIAN_POINT('Ctrl Pts',(34.3974626619392,-5.91103772112295,
131.641657145399));
#178622=CARTESIAN_POINT('Ctrl Pts',(34.4366248077956,-5.90791192852897,
130.806830871508));
#178623=CARTESIAN_POINT('',(36.1866248250608,-5.91451745769036,130.799166741936));
#178624=CARTESIAN_POINT('Ctrl Pts',(34.4366248077956,-5.90791192852897,
130.806830871508));
#178625=CARTESIAN_POINT('Ctrl Pts',(34.4902785365435,-5.90362946585253,
129.663085004891));
#178626=CARTESIAN_POINT('Ctrl Pts',(34.6367481398959,-5.03069841154749,
126.53472321439));
#178627=CARTESIAN_POINT('Ctrl Pts',(34.8760336178522,0.047962267785614,
123.806127972732));
#178628=CARTESIAN_POINT('Ctrl Pts',(35.1544812416653,5.91373610162903,127.061996945949));
#178629=CARTESIAN_POINT('Ctrl Pts',(35.432928865478,6.34507536014334,133.756915308749));
#178630=CARTESIAN_POINT('Ctrl Pts',(35.711376489291,0.945600336853253,137.73858015067));
#178631=CARTESIAN_POINT('Ctrl Pts',(35.9626084700635,-4.71015443282379,
135.581689261836));
#178632=CARTESIAN_POINT('Ctrl Pts',(36.1210245762317,-5.90156890071962,
132.19441833346));
#178633=CARTESIAN_POINT('Ctrl Pts',(36.1866248077956,-5.91323377650414,
130.799168236558));
#178634=CARTESIAN_POINT('',(37.9366248077955,-5.92210452553072,130.804050934745));
#178635=CARTESIAN_POINT('Ctrl Pts',(36.1866248550572,-5.91674771806056,
130.799164145188));
#178636=CARTESIAN_POINT('Ctrl Pts',(36.1956075840384,-5.91657982411567,
130.607998669251));
#178637=CARTESIAN_POINT('Ctrl Pts',(36.2045903130197,-5.90714364554391,
130.417241009972));
#178638=CARTESIAN_POINT('Ctrl Pts',(36.2135730420009,-5.88857986329382,
130.227682409108));
#178639=CARTESIAN_POINT('Ctrl Pts',(36.2226894911536,-5.86973973382792,
130.035301969952));
#178640=CARTESIAN_POINT('Ctrl Pts',(36.2318059403062,-5.84149826826958,
129.8441565403));
#178641=CARTESIAN_POINT('Ctrl Pts',(36.2409223894589,-5.80405176354405,
129.655050525119));
#178642=CARTESIAN_POINT('Ctrl Pts',(36.2500388386115,-5.76660525881853,
129.465944509937));
#178643=CARTESIAN_POINT('Ctrl Pts',(36.2591552877641,-5.71995381969959,
129.278877833967));
#178644=CARTESIAN_POINT('Ctrl Pts',(36.2682717369168,-5.66434131196571,
129.09463313517));
#178645=CARTESIAN_POINT('Ctrl Pts',(36.2756950033222,-5.61905762163104,
128.944607893977));
#178646=CARTESIAN_POINT('Ctrl Pts',(36.2831182697276,-5.56774100745304,
128.796156109647));
#178647=CARTESIAN_POINT('Ctrl Pts',(36.290541536133,-5.51051710494887,128.649799920216));
#178648=CARTESIAN_POINT('Ctrl Pts',(36.297956028854,-5.45336083634523,128.503616711647));
#178649=CARTESIAN_POINT('Ctrl Pts',(36.305370521575,-5.3903113115816,128.359524512129));
#178650=CARTESIAN_POINT('Ctrl Pts',(36.3127850142959,-5.32154435244625,
128.218031893786));
#178651=CARTESIAN_POINT('Ctrl Pts',(36.3201923606497,-5.25284367349506,
128.076675651357));
#178652=CARTESIAN_POINT('Ctrl Pts',(36.3275997070035,-5.17843669292861,
127.937914335489));
#178653=CARTESIAN_POINT('Ctrl Pts',(36.3350070533572,-5.09854784169346,
127.802237957103));
#178654=CARTESIAN_POINT('Ctrl Pts',(36.3424088750326,-5.01871857457771,
127.66666277128));
#178655=CARTESIAN_POINT('Ctrl Pts',(36.3498106967079,-4.93341576631353,
127.534168261902));
#178656=CARTESIAN_POINT('Ctrl Pts',(36.3572125183833,-4.84291037544202,
127.405221070867));
#178657=CARTESIAN_POINT('Ctrl Pts',(36.3646104326946,-4.752452761662,127.27634195005));
#178658=CARTESIAN_POINT('Ctrl Pts',(36.3720083470059,-4.65679824878223,
127.151006722973));
#178659=CARTESIAN_POINT('Ctrl Pts',(36.3794062613172,-4.55626175911545,
127.029654093222));
#178660=CARTESIAN_POINT('Ctrl Pts',(36.3868029462294,-4.45574197678934,
126.908321630078));
#178661=CARTESIAN_POINT('Ctrl Pts',(36.3941996311416,-4.35034206577818,
126.790970737893));
#178662=CARTESIAN_POINT('Ctrl Pts',(36.4015963160537,-4.2404180498028,126.678008072593));
#178663=CARTESIAN_POINT('Ctrl Pts',(36.4089926729892,-4.13049890797349,
126.565050416175));
#178664=CARTESIAN_POINT('Ctrl Pts',(36.4163890299246,-4.01605632038603,
126.456480867289));
#178665=CARTESIAN_POINT('Ctrl Pts',(36.42378538686,-3.8974838924297,126.352669942019));
#178666=CARTESIAN_POINT('Ctrl Pts',(36.4311828761966,-3.77889331073178,
126.248843123031));
#178667=CARTESIAN_POINT('Ctrl Pts',(36.4385803655331,-3.65617191057611,
126.149776624228));
#178668=CARTESIAN_POINT('Ctrl Pts',(36.4459778548697,-3.52974703272114,
126.055801209967));
#178669=CARTESIAN_POINT('Ctrl Pts',(36.4533779373846,-3.40327783682139,
125.961792852771));
#178670=CARTESIAN_POINT('Ctrl Pts',(36.4607780198996,-3.27310287782725,
125.872879355944));
#178671=CARTESIAN_POINT('Ctrl Pts',(36.4681781024146,-3.13967903141979,
125.789348539598));
#178672=CARTESIAN_POINT('Ctrl Pts',(36.475586322081,-3.00610847177691,125.705725872533));
#178673=CARTESIAN_POINT('Ctrl Pts',(36.4829945417474,-2.86928220683207,
125.62749790441));
#178674=CARTESIAN_POINT('Ctrl Pts',(36.4904027614138,-2.72968294214001,
125.554907160501));
#178675=CARTESIAN_POINT('Ctrl Pts',(36.4978155407158,-2.58999775642967,
125.4822717382));
#178676=CARTESIAN_POINT('Ctrl Pts',(36.5052283200179,-2.44753650711736,
125.415280612245));
#178677=CARTESIAN_POINT('Ctrl Pts',(36.5126410993199,-2.30280200391537,
125.354128191947));
#178678=CARTESIAN_POINT('Ctrl Pts',(36.5200644703487,-2.15786069726782,
125.292888394204));
#178679=CARTESIAN_POINT('Ctrl Pts',(36.5274878413774,-2.01063999794909,
125.237504095288));
#178680=CARTESIAN_POINT('Ctrl Pts',(36.5349112124061,-1.86165878085102,
125.188120136053));
#178681=CARTESIAN_POINT('Ctrl Pts',(36.5388472618473,-1.78266536478243,
125.161935575913));
#178682=CARTESIAN_POINT('Ctrl Pts',(36.5427833112885,-1.7031772022922,125.137437078181));
#178683=CARTESIAN_POINT('Ctrl Pts',(36.5467193607296,-1.6232726854084,125.114640382677));
#178684=CARTESIAN_POINT('Ctrl Pts',(36.5541426271351,-1.47257526031468,
125.071646526421));
#178685=CARTESIAN_POINT('Ctrl Pts',(36.5615658935405,-1.31994068634216,
125.034578831723));
#178686=CARTESIAN_POINT('Ctrl Pts',(36.5689891599459,-1.16587616207567,
125.003613826229));
#178687=CARTESIAN_POINT('Ctrl Pts',(36.5764036526669,-1.01199372928239,
124.9726854188));
#178688=CARTESIAN_POINT('Ctrl Pts',(36.583818145388,-0.85668507271891,124.947845416152));
#178689=CARTESIAN_POINT('Ctrl Pts',(36.591232638109,-0.700473104488531,
124.929220790091));
#178690=CARTESIAN_POINT('Ctrl Pts',(36.5986399844627,-0.544411699234631,
124.910614115145));
#178691=CARTESIAN_POINT('Ctrl Pts',(36.6060473308166,-0.387449083782456,
124.898210934551));
#178692=CARTESIAN_POINT('Ctrl Pts',(36.6134546771703,-0.230118828605541,
124.892087291068));
#178693=CARTESIAN_POINT('Ctrl Pts',(36.6208564988457,-0.0729059162684447,
124.885968214829));
#178694=CARTESIAN_POINT('Ctrl Pts',(36.6282583205211,0.0846737184149918,
124.886119364646));
#178695=CARTESIAN_POINT('Ctrl Pts',(36.6356601421965,0.242081016691307,
124.892565006767));
#178696=CARTESIAN_POINT('Ctrl Pts',(36.6430580565079,0.399405220879894,
124.899007246284));
#178697=CARTESIAN_POINT('Ctrl Pts',(36.6504559708192,0.556556897801354,
124.911737345329));
#178698=CARTESIAN_POINT('Ctrl Pts',(36.6578538851306,0.712996730501101,
124.930727480844));
#178699=CARTESIAN_POINT('Ctrl Pts',(36.6652505700428,0.869410565738761,
124.949714460544));
#178700=CARTESIAN_POINT('Ctrl Pts',(36.672647254955,1.02511242132171,124.974959367078));
#178701=CARTESIAN_POINT('Ctrl Pts',(36.6800439398672,1.1795677265864,125.006382475067));
#178702=CARTESIAN_POINT('Ctrl Pts',(36.6874402968026,1.33401618314101,125.037804189723));
#178703=CARTESIAN_POINT('Ctrl Pts',(36.6948366537381,1.48721783347539,125.075403486711));
#178704=CARTESIAN_POINT('Ctrl Pts',(36.7022330106735,1.63864819858704,125.119049487666));
#178705=CARTESIAN_POINT('Ctrl Pts',(36.7096305000101,1.79010174807438,125.162702170934));
#178706=CARTESIAN_POINT('Ctrl Pts',(36.7170279893467,1.93978311364797,125.2124032981));
#178707=CARTESIAN_POINT('Ctrl Pts',(36.7244254786833,2.08718302576793,125.267972121493));
#178708=CARTESIAN_POINT('Ctrl Pts',(36.7318255611983,2.23463460869859,125.323560424452));
#178709=CARTESIAN_POINT('Ctrl Pts',(36.7392256437132,2.37980279677705,125.385020387333));
#178710=CARTESIAN_POINT('Ctrl Pts',(36.7466257262282,2.52219848632689,125.452123201488));
#178711=CARTESIAN_POINT('Ctrl Pts',(36.7540339458947,2.66475075457582,125.519299802084));
#178712=CARTESIAN_POINT('Ctrl Pts',(36.7614421655612,2.80452409805858,125.59213148631));
#178713=CARTESIAN_POINT('Ctrl Pts',(36.7688503852277,2.94105355925407,125.670343231142));
#178714=CARTESIAN_POINT('Ctrl Pts',(36.7762631645297,3.07766705205501,125.748603113999));
#178715=CARTESIAN_POINT('Ctrl Pts',(36.7836759438318,3.21103236867163,125.83224945783));
#178716=CARTESIAN_POINT('Ctrl Pts',(36.7910887231338,3.34071416611194,125.920964317568));
#178717=CARTESIAN_POINT('Ctrl Pts',(36.7985120941626,3.4705812589859,126.009805937257));
#178718=CARTESIAN_POINT('Ctrl Pts',(36.8059354651913,3.5967540222762,126.1037303147));
#178719=CARTESIAN_POINT('Ctrl Pts',(36.8133588362201,3.7188301327171,126.202379195777));
#178720=CARTESIAN_POINT('Ctrl Pts',(36.8172948856609,3.7835578156491,126.254685199571));
#178721=CARTESIAN_POINT('Ctrl Pts',(36.8212309351017,3.84713438905048,126.308318805457));
#178722=CARTESIAN_POINT('Ctrl Pts',(36.8251669845425,3.90950423776022,126.36322256776));
#178723=CARTESIAN_POINT('Ctrl Pts',(36.8325902509479,4.02713182593014,126.466769349974));
#178724=CARTESIAN_POINT('Ctrl Pts',(36.8400135173534,4.14082064282964,126.575149145481));
#178725=CARTESIAN_POINT('Ctrl Pts',(36.8474367837588,4.25014801752764,126.688030651248));
#178726=CARTESIAN_POINT('Ctrl Pts',(36.8548512764798,4.35934617634797,126.80077874045));
#178727=CARTESIAN_POINT('Ctrl Pts',(36.8622657692008,4.46419289657875,126.918017683605));
#178728=CARTESIAN_POINT('Ctrl Pts',(36.8696802619218,4.56429870647891,127.039376171312));
#178729=CARTESIAN_POINT('Ctrl Pts',(36.8770876082756,4.66430803063057,127.16061768914));
#178730=CARTESIAN_POINT('Ctrl Pts',(36.8844949546294,4.75958530541786,127.285970560856));
#178731=CARTESIAN_POINT('Ctrl Pts',(36.8919023009832,4.84977814603905,127.41502698148));
#178732=CARTESIAN_POINT('Ctrl Pts',(36.8993041226586,4.93990371743693,127.543987146957));
#178733=CARTESIAN_POINT('Ctrl Pts',(36.906705944334,5.02495219245812,127.676645056671));
#178734=CARTESIAN_POINT('Ctrl Pts',(36.9141077660094,5.10461178079674,127.812560301728));
#178735=CARTESIAN_POINT('Ctrl Pts',(36.9215056803208,5.18422931745863,127.948403798184));
#178736=CARTESIAN_POINT('Ctrl Pts',(36.9289035946321,5.25846344461655,128.087500884228));
#178737=CARTESIAN_POINT('Ctrl Pts',(36.9363015089434,5.32704605660825,128.229382778191));
#178738=CARTESIAN_POINT('Ctrl Pts',(36.9436981938556,5.39561727141405,128.371241093956));
#178739=CARTESIAN_POINT('Ctrl Pts',(36.9510948787679,5.45853867274588,128.515882963387));
#178740=CARTESIAN_POINT('Ctrl Pts',(36.9584915636801,5.51558838732208,128.662815543528));
#178741=CARTESIAN_POINT('Ctrl Pts',(36.9658879206155,5.57263557225415,128.809741608524));
#178742=CARTESIAN_POINT('Ctrl Pts',(36.973284277551,5.62381145299412,128.958957834283));
#178743=CARTESIAN_POINT('Ctrl Pts',(36.9806806344864,5.66894264750733,129.109952218811));
#178744=CARTESIAN_POINT('Ctrl Pts',(36.988078123823,5.71408075172164,129.260969720964));
#178745=CARTESIAN_POINT('Ctrl Pts',(36.9954756131596,5.75317222009143,129.413765566268));
#178746=CARTESIAN_POINT('Ctrl Pts',(37.0028731024962,5.78609384812336,129.567813593305));
#178747=CARTESIAN_POINT('Ctrl Pts',(37.0102731850112,5.81902701678101,129.721915621639));
#178748=CARTESIAN_POINT('Ctrl Pts',(37.0176732675261,5.84578596095896,129.877270340826));
#178749=CARTESIAN_POINT('Ctrl Pts',(37.0250733500411,5.86629881137007,130.033342577428));
#178750=CARTESIAN_POINT('Ctrl Pts',(37.0324815697076,5.88683421776897,130.189586431498));
#178751=CARTESIAN_POINT('Ctrl Pts',(37.0398897893741,5.90110976543565,130.346549008294));
#178752=CARTESIAN_POINT('Ctrl Pts',(37.0472980090406,5.9091055181301,130.503690469223));
#178753=CARTESIAN_POINT('Ctrl Pts',(37.0547107883427,5.91710619207691,130.6609286481));
#178754=CARTESIAN_POINT('Ctrl Pts',(37.0621235676446,5.91881936528427,130.818345558087));
#178755=CARTESIAN_POINT('Ctrl Pts',(37.0695363469467,5.91427722042245,130.975403075722));
#178756=CARTESIAN_POINT('Ctrl Pts',(37.0769597179755,5.90972858553104,131.132685004503));
#178757=CARTESIAN_POINT('Ctrl Pts',(37.0843830890043,5.89890680721048,131.289606143896));
#178758=CARTESIAN_POINT('Ctrl Pts',(37.091806460033,5.88189582924777,131.44563436284));
#178759=CARTESIAN_POINT('Ctrl Pts',(37.0957425094738,5.87287620055913,131.528364268369));
#178760=CARTESIAN_POINT('Ctrl Pts',(37.0996785589146,5.86211741981153,131.610843314209));
#178761=CARTESIAN_POINT('Ctrl Pts',(37.1036146083554,5.84963775632701,131.692993658958));
#178762=CARTESIAN_POINT('Ctrl Pts',(37.1110378747608,5.82610150047212,131.84792664533));
#178763=CARTESIAN_POINT('Ctrl Pts',(37.1184611411662,5.79637009157543,132.002158193617));
#178764=CARTESIAN_POINT('Ctrl Pts',(37.1258844075717,5.76049380029665,132.155153621414));
#178765=CARTESIAN_POINT('Ctrl Pts',(37.1332989002927,5.72465991181477,132.307968221321));
#178766=CARTESIAN_POINT('Ctrl Pts',(37.1407133930137,5.68269568186778,132.45954924896));
#178767=CARTESIAN_POINT('Ctrl Pts',(37.1481278857347,5.63470298458015,132.609368328924));
#178768=CARTESIAN_POINT('Ctrl Pts',(37.1555352320885,5.58675654446106,132.759043007619));
#178769=CARTESIAN_POINT('Ctrl Pts',(37.1629425784423,5.53279331760733,132.906958766367));
#178770=CARTESIAN_POINT('Ctrl Pts',(37.1703499247961,5.4729659293069,133.052598705302));
#178771=CARTESIAN_POINT('Ctrl Pts',(37.1777517464715,5.41318316252982,133.198130020475));
#178772=CARTESIAN_POINT('Ctrl Pts',(37.1851535681469,5.34754508419324,133.341388551759));
#178773=CARTESIAN_POINT('Ctrl Pts',(37.1925553898223,5.27625369249818,133.481873929372));
#178774=CARTESIAN_POINT('Ctrl Pts',(37.1999533041337,5.20499993497386,133.622285145848));
#178775=CARTESIAN_POINT('Ctrl Pts',(37.207351218445,5.12809897604868,133.759925792089));
#178776=CARTESIAN_POINT('Ctrl Pts',(37.2147491327564,5.04580029735864,133.894316915263));
#178777=CARTESIAN_POINT('Ctrl Pts',(37.2221458176686,4.96351529521606,134.02868570507));
#178778=CARTESIAN_POINT('Ctrl Pts',(37.2295425025809,4.87583454835409,134.159805725539));
#178779=CARTESIAN_POINT('Ctrl Pts',(37.2369391874931,4.78305277157969,134.287223914737));
#178780=CARTESIAN_POINT('Ctrl Pts',(37.2443355444285,4.69027510884636,134.41463645408));
#178781=CARTESIAN_POINT('Ctrl Pts',(37.251731901364,4.59239708567242,134.538347186755));
#178782=CARTESIAN_POINT('Ctrl Pts',(37.2591282582995,4.48975574661072,134.657933491961));
#178783=CARTESIAN_POINT('Ctrl Pts',(37.266525747636,4.38709869289799,134.777538106136));
#178784=CARTESIAN_POINT('Ctrl Pts',(37.2739232369726,4.27967711435648,134.893016752237));
#178785=CARTESIAN_POINT('Ctrl Pts',(37.2813207263092,4.16786709044987,135.003981371735));
#178786=CARTESIAN_POINT('Ctrl Pts',(37.2887208088242,4.05601787171271,135.114984889708));
#178787=CARTESIAN_POINT('Ctrl Pts',(37.2961208913392,3.93977740953756,135.221470967769));
#178788=CARTESIAN_POINT('Ctrl Pts',(37.3035209738543,3.81955711339041,135.323089865933));
#178789=CARTESIAN_POINT('Ctrl Pts',(37.3109291935207,3.69920462266887,135.424820504523));
#178790=CARTESIAN_POINT('Ctrl Pts',(37.3183374131872,3.57486384361288,135.521673033861));
#178791=CARTESIAN_POINT('Ctrl Pts',(37.3257456328536,3.44697818169413,135.61333888508));
#178792=CARTESIAN_POINT('Ctrl Pts',(37.3331584121557,3.31901380828399,135.705061155101));
#178793=CARTESIAN_POINT('Ctrl Pts',(37.3405711914578,3.18750051559732,135.791590181211));
#178794=CARTESIAN_POINT('Ctrl Pts',(37.3479839707599,3.05290843766486,135.872662170723));
#178795=CARTESIAN_POINT('Ctrl Pts',(37.3554073417886,2.91812404825991,135.953849999696));
#178796=CARTESIAN_POINT('Ctrl Pts',(37.3628307128174,2.78025241393159,136.02956503996));
#178797=CARTESIAN_POINT('Ctrl Pts',(37.3702540838461,2.63978660528028,136.099590285964));
#178798=CARTESIAN_POINT('Ctrl Pts',(37.3741901332869,2.56530826310386,136.136719351627));
#178799=CARTESIAN_POINT('Ctrl Pts',(37.3781261827276,2.49010092212003,136.172249623619));
#178800=CARTESIAN_POINT('Ctrl Pts',(37.3820622321684,2.41423994751945,136.206154397256));
#178801=CARTESIAN_POINT('Ctrl Pts',(37.3894854985738,2.27116851696018,136.270097742207));
#178802=CARTESIAN_POINT('Ctrl Pts',(37.3969087649793,2.12533859458309,136.328449785029));
#178803=CARTESIAN_POINT('Ctrl Pts',(37.4043320313847,1.97722719635829,136.380963810952));
#178804=CARTESIAN_POINT('Ctrl Pts',(37.4117465241057,1.8292908535063,136.433415769657));
#178805=CARTESIAN_POINT('Ctrl Pts',(37.4191610168267,1.67907875063627,136.480043322525));
#178806=CARTESIAN_POINT('Ctrl Pts',(37.4265755095477,1.52709049039462,136.520646579329));
#178807=CARTESIAN_POINT('Ctrl Pts',(37.4339828559015,1.37524872216024,136.561210701185));
#178808=CARTESIAN_POINT('Ctrl Pts',(37.4413902022553,1.22163456289373,136.595761990761));
#178809=CARTESIAN_POINT('Ctrl Pts',(37.4487975486091,1.06676539278921,136.624149459032));
#178810=CARTESIAN_POINT('Ctrl Pts',(37.4561993702845,0.912011729954633,
136.652515754857));
#178811=CARTESIAN_POINT('Ctrl Pts',(37.4636011919599,0.75600528565307,136.674727316029));
#178812=CARTESIAN_POINT('Ctrl Pts',(37.4710030136353,0.599276220113848,
136.690683627265));
#178813=CARTESIAN_POINT('Ctrl Pts',(37.4784009279467,0.44262989062857,136.706631515288));
#178814=CARTESIAN_POINT('Ctrl Pts',(37.485798842258,0.28526207005183,136.716330691948));
#178815=CARTESIAN_POINT('Ctrl Pts',(37.4931967565693,0.127710565882259,
136.719732167508));
#178816=CARTESIAN_POINT('Ctrl Pts',(37.5005934414816,-0.0298147560858202,
136.723133077804));
#178817=CARTESIAN_POINT('Ctrl Pts',(37.5079901263939,-0.187523328218363,
136.720238356069));
#178818=CARTESIAN_POINT('Ctrl Pts',(37.5153868113061,-0.344874676129766,
136.711051063176));
#178819=CARTESIAN_POINT('Ctrl Pts',(37.5227831682415,-0.50221904691751,
136.701864177658));
#178820=CARTESIAN_POINT('Ctrl Pts',(37.530179525177,-0.659205852315889,
136.686385297525));
#178821=CARTESIAN_POINT('Ctrl Pts',(37.5375758821124,-0.815297348663056,
136.664669551041));
#178822=CARTESIAN_POINT('Ctrl Pts',(37.544973371449,-0.971412743016796,
136.64295047982));
#178823=CARTESIAN_POINT('Ctrl Pts',(37.5523708607856,-1.12663218562586,
136.614992692396));
#178824=CARTESIAN_POINT('Ctrl Pts',(37.5597683501222,-1.28042591172418,
136.580902839959));
#178825=CARTESIAN_POINT('Ctrl Pts',(37.5671684326372,-1.43427354997455,
136.546801037377));
#178826=CARTESIAN_POINT('Ctrl Pts',(37.5745685151522,-1.58669411242584,
136.506562970707));
#178827=CARTESIAN_POINT('Ctrl Pts',(37.5819685976672,-1.73717097605971,
136.46034572738));
#178828=CARTESIAN_POINT('Ctrl Pts',(37.5893768173337,-1.88781330447453,
136.414077663443));
#178829=CARTESIAN_POINT('Ctrl Pts',(37.5967850370001,-2.03650730868539,
136.361817402371));
#178830=CARTESIAN_POINT('Ctrl Pts',(37.6041932566666,-2.18275370947581,
136.303771204735));
#178831=CARTESIAN_POINT('Ctrl Pts',(37.6116060359687,-2.32909012248588,
136.245689280633));
#178832=CARTESIAN_POINT('Ctrl Pts',(37.6190188152708,-2.47297558986873,
136.181814475047));
#178833=CARTESIAN_POINT('Ctrl Pts',(37.6264315945728,-2.61393405644007,
136.112399738662));
#178834=CARTESIAN_POINT('Ctrl Pts',(37.6338549656016,-2.75509393107895,
136.042885819246));
#178835=CARTESIAN_POINT('Ctrl Pts',(37.6412783366304,-2.8933181248711,135.967816337263));
#178836=CARTESIAN_POINT('Ctrl Pts',(37.6487017076592,-3.02815754819667,
135.887488830173));
#178837=CARTESIAN_POINT('Ctrl Pts',(37.6526377570999,-3.09965264586894,
135.844897258483));
#178838=CARTESIAN_POINT('Ctrl Pts',(37.6565738065405,-3.17019667480669,
135.800828172418));
#178839=CARTESIAN_POINT('Ctrl Pts',(37.6605098559812,-3.2397264308791,135.755330544314));
#178840=CARTESIAN_POINT('Ctrl Pts',(37.6679221115746,-3.37066287645052,
135.669650713946));
#178841=CARTESIAN_POINT('Ctrl Pts',(37.675334367168,-3.49839897233822,135.578641572179));
#178842=CARTESIAN_POINT('Ctrl Pts',(37.6827466227614,-3.62247011547864,
135.482569764768));
#178843=CARTESIAN_POINT('Ctrl Pts',(37.6901501101258,-3.74639449031427,
135.386611604221));
#178844=CARTESIAN_POINT('Ctrl Pts',(37.6975535974902,-3.86666224837065,
135.285602925195));
#178845=CARTESIAN_POINT('Ctrl Pts',(37.7049570848546,-3.98283590640176,
135.179854727398));
#178846=CARTESIAN_POINT('Ctrl Pts',(37.7123534420334,-4.09889767935609,
135.074208374077));
#178847=CARTESIAN_POINT('Ctrl Pts',(37.7197497992122,-4.21087292643776,
134.963831839071));
#178848=CARTESIAN_POINT('Ctrl Pts',(37.7271461563909,-4.3183556485216,134.849077548994));
#178849=CARTESIAN_POINT('Ctrl Pts',(37.734537015717,-4.42575847665778,134.734408557959));
#178850=CARTESIAN_POINT('Ctrl Pts',(37.7419278750431,-4.52867517368807,
134.615368563017));
#178851=CARTESIAN_POINT('Ctrl Pts',(37.7493187343692,-4.6267352650982,134.492348056427));
#178852=CARTESIAN_POINT('Ctrl Pts',(37.756705723756,-4.72474401111272,134.369391964794));
#178853=CARTESIAN_POINT('Ctrl Pts',(37.7640927131428,-4.81790098287275,
134.242459804359));
#178854=CARTESIAN_POINT('Ctrl Pts',(37.7714797025296,-4.90587490393759,
134.111976373577));
#178855=CARTESIAN_POINT('Ctrl Pts',(37.7788655139203,-4.9938347958847,133.981513750864));
#178856=CARTESIAN_POINT('Ctrl Pts',(37.7862513253109,-5.07661306799916,
133.847501291781));
#178857=CARTESIAN_POINT('Ctrl Pts',(37.7936371367016,-5.15392078710318,
133.710394182886));
#178858=CARTESIAN_POINT('Ctrl Pts',(37.8010226735015,-5.2312256320508,133.573292171376));
#178859=CARTESIAN_POINT('Ctrl Pts',(37.8084082103015,-5.30306014434898,
133.433096065046));
#178860=CARTESIAN_POINT('Ctrl Pts',(37.8157937471015,-5.36918067557369,
133.290286890718));
#178861=CARTESIAN_POINT('Ctrl Pts',(37.8231804792538,-5.43531190843543,
133.147454602662));
#178862=CARTESIAN_POINT('Ctrl Pts',(37.8305672114062,-5.49572716160444,
133.002008744488));
#178863=CARTESIAN_POINT('Ctrl Pts',(37.8379539435586,-5.55023045568705,
132.854451457325));
#178864=CARTESIAN_POINT('Ctrl Pts',(37.8453433414564,-5.60475341907727,
132.706840919258));
#178865=CARTESIAN_POINT('Ctrl Pts',(37.8527327393541,-5.65336004616993,
132.557117786319));
#178866=CARTESIAN_POINT('Ctrl Pts',(37.8601221372519,-5.69590390508168,
132.405800365598));
#178867=CARTESIAN_POINT('Ctrl Pts',(37.8675196661198,-5.7384945773941,132.254316441808));
#178868=CARTESIAN_POINT('Ctrl Pts',(37.8749171949877,-5.77500905850871,
132.101235087859));
#178869=CARTESIAN_POINT('Ctrl Pts',(37.8823147238556,-5.80535167515036,
131.947086520978));
#178870=CARTESIAN_POINT('Ctrl Pts',(37.8897168959795,-5.83571333714352,
131.792841198643));
#178871=CARTESIAN_POINT('Ctrl Pts',(37.8971190681034,-5.85989535865037,
131.637527697812));
#178872=CARTESIAN_POINT('Ctrl Pts',(37.9045212402273,-5.87785390268125,
131.481681856887));
#178873=CARTESIAN_POINT('Ctrl Pts',(37.911933808771,-5.89583766965469,131.325617129025));
#178874=CARTESIAN_POINT('Ctrl Pts',(37.9193463773147,-5.90758047647729,
131.16901894028));
#178875=CARTESIAN_POINT('Ctrl Pts',(37.9267589458584,-5.91309056511575,
131.012424384809));
#178876=CARTESIAN_POINT('Ctrl Pts',(37.9300475665041,-5.91553514166833,
130.94295047909));
#178877=CARTESIAN_POINT('Ctrl Pts',(37.9333361871498,-5.91675362238445,
130.873477241184));
#178878=CARTESIAN_POINT('Ctrl Pts',(37.9366248077955,-5.91674999191025,
130.804051214748));
#178879=CARTESIAN_POINT('',(39.6866240381297,-5.91498544959244,130.809720579457));
#178880=CARTESIAN_POINT('Ctrl Pts',(37.9366248077955,-5.92651271267239,
130.804050704229));
#178881=CARTESIAN_POINT('Ctrl Pts',(37.9374023651284,-5.92652516855156,
130.787608616101));
#178882=CARTESIAN_POINT('Ctrl Pts',(37.9381799224613,-5.92646268754296,
130.771166625385));
#178883=CARTESIAN_POINT('Ctrl Pts',(38.0317733543984,-5.90988757984946,
128.792144232197));
#178884=CARTESIAN_POINT('Ctrl Pts',(38.217405103607,-3.7333596383727,124.884936123503));
#178885=CARTESIAN_POINT('Ctrl Pts',(38.4958527274199,2.96220739674919,124.46378589054));
#178886=CARTESIAN_POINT('Ctrl Pts',(38.7743003512328,6.93565054613509,129.869314077418));
#178887=CARTESIAN_POINT('Ctrl Pts',(39.0527479750457,4.53556966898844,136.134104355128));
#178888=CARTESIAN_POINT('Ctrl Pts',(39.3311955988587,-2.03247815906468,
137.501120510476));
#178889=CARTESIAN_POINT('Ctrl Pts',(39.5424875011082,-5.59916423616403,
133.868660331039));
#178890=CARTESIAN_POINT('Ctrl Pts',(39.6609635287535,-5.91891885957568,
131.355273964503));
#178891=CARTESIAN_POINT('Ctrl Pts',(39.6866236817946,-5.9141696267495,130.80972741823));
#178892=CARTESIAN_POINT('',(41.4366255671013,-5.91167177449429,130.80237612265));
#178893=CARTESIAN_POINT('Ctrl Pts',(39.6866248077955,-5.91674758557763,
130.809705808054));
#178894=CARTESIAN_POINT('Ctrl Pts',(39.6939603857742,-5.91688853801437,
130.653681435918));
#178895=CARTESIAN_POINT('Ctrl Pts',(39.701295963753,-5.91085373526745,130.497522968287));
#178896=CARTESIAN_POINT('Ctrl Pts',(39.7086315417317,-5.89863824892961,
130.34176211912));
#178897=CARTESIAN_POINT('Ctrl Pts',(39.716109012763,-5.88618647682792,130.182988367297));
#178898=CARTESIAN_POINT('Ctrl Pts',(39.7235864837944,-5.86731242361618,
130.024628175413));
#178899=CARTESIAN_POINT('Ctrl Pts',(39.7310639548258,-5.84206663858188,
129.867243787673));
#178900=CARTESIAN_POINT('Ctrl Pts',(39.7383948603265,-5.81731569490013,
129.712944283338));
#178901=CARTESIAN_POINT('Ctrl Pts',(39.7457257658273,-5.78644057510626,
129.55958307169));
#178902=CARTESIAN_POINT('Ctrl Pts',(39.7530566713281,-5.74954111903638,
129.407683316609));
#178903=CARTESIAN_POINT('Ctrl Pts',(39.7603875560361,-5.71264176762486,
129.255783992362));
#178904=CARTESIAN_POINT('Ctrl Pts',(39.7677184407442,-5.66971820337799,
129.105346486387));
#178905=CARTESIAN_POINT('Ctrl Pts',(39.7750493254522,-5.62092094437509,
128.956881713874));
#178906=CARTESIAN_POINT('Ctrl Pts',(39.7823816999613,-5.57211376866862,
128.808386769972));
#178907=CARTESIAN_POINT('Ctrl Pts',(39.7897140744705,-5.51743064147151,
128.661865718906));
#178908=CARTESIAN_POINT('Ctrl Pts',(39.7970464489796,-5.45707122236629,
128.517812075216));
#178909=CARTESIAN_POINT('Ctrl Pts',(39.804633482105,-5.39461547742173,128.368755345348));
#178910=CARTESIAN_POINT('Ctrl Pts',(39.8122205152304,-5.32608221199373,
128.222340914693));
#178911=CARTESIAN_POINT('Ctrl Pts',(39.8198075483558,-5.2517452856169,128.079089618656));
#178912=CARTESIAN_POINT('Ctrl Pts',(39.8271512980281,-5.17979202408456,
127.940431774284));
#178913=CARTESIAN_POINT('Ctrl Pts',(39.8344950477005,-5.10240180354443,
127.804737635045));
#178914=CARTESIAN_POINT('Ctrl Pts',(39.8418387973729,-5.01986775780857,
127.672450935501));
#178915=CARTESIAN_POINT('Ctrl Pts',(39.8495474722248,-4.93323243509578,
127.533590653014));
#178916=CARTESIAN_POINT('Ctrl Pts',(39.8572561470767,-4.84092929066518,
127.398485515014));
#178917=CARTESIAN_POINT('Ctrl Pts',(39.8649648219286,-4.74334534328168,
127.267609917154));
#178918=CARTESIAN_POINT('Ctrl Pts',(39.8726734967805,-4.64576139589804,
127.136734319293));
#178919=CARTESIAN_POINT('Ctrl Pts',(39.8803821716324,-4.54289700502975,
127.010088583274));
#178920=CARTESIAN_POINT('Ctrl Pts',(39.8880908464843,-4.43518330710743,
126.888102250852));
#178921=CARTESIAN_POINT('Ctrl Pts',(39.8955141128897,-4.33145763563316,
126.770632379469));
#178922=CARTESIAN_POINT('Ctrl Pts',(39.9029373792952,-4.22290495060319,
126.657108629819));
#178923=CARTESIAN_POINT('Ctrl Pts',(39.9103606457006,-4.10985719789727,
126.547953168156));
#178924=CARTESIAN_POINT('Ctrl Pts',(39.9177751384216,-3.99694305824686,
126.438926719184));
#178925=CARTESIAN_POINT('Ctrl Pts',(39.9251896311426,-3.87954469199329,
126.334258538078));
#178926=CARTESIAN_POINT('Ctrl Pts',(39.9326041238636,-3.75803400081586,
126.234337531058));
#178927=CARTESIAN_POINT('Ctrl Pts',(39.9400114702173,-3.63664042621773,
126.134512831667));
#178928=CARTESIAN_POINT('Ctrl Pts',(39.9474188165711,-3.51114270386505,
126.039426432942));
#178929=CARTESIAN_POINT('Ctrl Pts',(39.9548261629248,-3.38194917453696,
125.949430098666));
#178930=CARTESIAN_POINT('Ctrl Pts',(39.9622279846002,-3.25285200261651,
125.859500887051));
#178931=CARTESIAN_POINT('Ctrl Pts',(39.9696298062757,-3.12006481721647,
125.77465439327));
#178932=CARTESIAN_POINT('Ctrl Pts',(39.9770316279511,-2.98402850121463,
125.695201737042));
#178933=CARTESIAN_POINT('Ctrl Pts',(39.9844295422624,-2.84806399772568,
125.615791023253));
#178934=CARTESIAN_POINT('Ctrl Pts',(39.9918274565738,-2.70885410104915,
125.541768664143));
#178935=CARTESIAN_POINT('Ctrl Pts',(39.9992253708851,-2.56686800032308,
125.473402051659));
#178936=CARTESIAN_POINT('Ctrl Pts',(40.0066220557973,-2.42490549511085,
125.405046800465));
#178937=CARTESIAN_POINT('Ctrl Pts',(40.0140187407095,-2.28016803751169,
125.342345592298));
#178938=CARTESIAN_POINT('Ctrl Pts',(40.0214154256217,-2.13314880756229,
125.285519550159));
#178939=CARTESIAN_POINT('Ctrl Pts',(40.0288117825571,-1.98613609659962,
125.228696027746));
#178940=CARTESIAN_POINT('Ctrl Pts',(40.0362081394926,-1.83684216265196,
125.177747287962));
#178941=CARTESIAN_POINT('Ctrl Pts',(40.0436044964281,-1.68577927097773,
125.132845933459));
#178942=CARTESIAN_POINT('Ctrl Pts',(40.0510019857646,-1.53469325118937,
125.087937704444));
#178943=CARTESIAN_POINT('Ctrl Pts',(40.0583994751012,-1.3818380922606,125.049078810608));
#178944=CARTESIAN_POINT('Ctrl Pts',(40.0657969644377,-1.22774014249539,
125.016391655572));
#178945=CARTESIAN_POINT('Ctrl Pts',(40.0731970469527,-1.07358817393255,
124.983693042105));
#178946=CARTESIAN_POINT('Ctrl Pts',(40.0805971294677,-0.918192912085663,
124.95717055235));
#178947=CARTESIAN_POINT('Ctrl Pts',(40.0879972119827,-0.762089639146931,
124.936895241068));
#178948=CARTESIAN_POINT('Ctrl Pts',(40.0954054316492,-0.605814714611795,
124.916597634997));
#178949=CARTESIAN_POINT('Ctrl Pts',(40.1028136513156,-0.448830594622927,
124.902560974183));
#178950=CARTESIAN_POINT('Ctrl Pts',(40.1102218709821,-0.291677147486677,
124.894804373301));
#178951=CARTESIAN_POINT('Ctrl Pts',(40.1176346502841,-0.134426975026185,
124.88704299836));
#178952=CARTESIAN_POINT('Ctrl Pts',(40.1250474295862,0.0229923598331128,
124.885569388876));
#178953=CARTESIAN_POINT('Ctrl Pts',(40.1324602088882,0.180042783226127,
124.890350543284));
#178954=CARTESIAN_POINT('Ctrl Pts',(40.1398835799169,0.337317607629243,
124.89513852923));
#178955=CARTESIAN_POINT('Ctrl Pts',(40.1473069509458,0.494222096405806,
124.90619910228));
#178956=CARTESIAN_POINT('Ctrl Pts',(40.1547303219745,0.650224246858324,
124.923447508932));
#178957=CARTESIAN_POINT('Ctrl Pts',(40.1586663714154,0.732940330251242,
124.93259302801));
#178958=CARTESIAN_POINT('Ctrl Pts',(40.1626024208563,0.81540290755164,124.943477315367));
#178959=CARTESIAN_POINT('Ctrl Pts',(40.1665384702972,0.897534165250741,
124.956081983241));
#178960=CARTESIAN_POINT('Ctrl Pts',(40.1739617367026,1.05243115403726,124.979853993472));
#178961=CARTESIAN_POINT('Ctrl Pts',(40.1813850031081,1.20661727758316,125.009820082102));
#178962=CARTESIAN_POINT('Ctrl Pts',(40.1888082695135,1.35955793060564,125.045929164833));
#178963=CARTESIAN_POINT('Ctrl Pts',(40.1962227622345,1.51231782047762,125.081995569627));
#178964=CARTESIAN_POINT('Ctrl Pts',(40.2036372549555,1.66383481017379,125.1241904315));
#178965=CARTESIAN_POINT('Ctrl Pts',(40.2110517476765,1.81358067993473,125.172411072349));
#178966=CARTESIAN_POINT('Ctrl Pts',(40.2184590940303,1.96318221898834,125.220585236329));
#178967=CARTESIAN_POINT('Ctrl Pts',(40.2258664403841,2.11101568360718,125.274773503299));
#178968=CARTESIAN_POINT('Ctrl Pts',(40.2332737867379,2.25656440679198,125.334822461515));
#178969=CARTESIAN_POINT('Ctrl Pts',(40.2406756084133,2.40200457424758,125.394826632952));
#178970=CARTESIAN_POINT('Ctrl Pts',(40.2480774300886,2.54516304965807,125.460682650378));
#178971=CARTESIAN_POINT('Ctrl Pts',(40.255479251764,2.68553977122917,125.532187754349));
#178972=CARTESIAN_POINT('Ctrl Pts',(40.2628771660754,2.82584238902285,125.603655111332));
#178973=CARTESIAN_POINT('Ctrl Pts',(40.2702750803868,2.96336584570946,125.68076544684));
#178974=CARTESIAN_POINT('Ctrl Pts',(40.2776729946982,3.09763156868231,125.763268550642));
#178975=CARTESIAN_POINT('Ctrl Pts',(40.2850696796104,3.23187497912706,125.845757943925));
#178976=CARTESIAN_POINT('Ctrl Pts',(40.2924663645227,3.36286141258997,125.933638131604));
#178977=CARTESIAN_POINT('Ctrl Pts',(40.2998630494349,3.4901382561708,126.026613709732));
#178978=CARTESIAN_POINT('Ctrl Pts',(40.3072594063703,3.61740945616265,126.119585165226));
#178979=CARTESIAN_POINT('Ctrl Pts',(40.3146557633057,3.74097109189239,126.217651341734));
#178980=CARTESIAN_POINT('Ctrl Pts',(40.3220521202412,3.8604010559739,126.320474551938));
#178981=CARTESIAN_POINT('Ctrl Pts',(40.3294496095777,3.97984930508813,126.423313504638));
#178982=CARTESIAN_POINT('Ctrl Pts',(40.3368470989143,4.0951643401099,126.530910697628));
#178983=CARTESIAN_POINT('Ctrl Pts',(40.3442445882509,4.20595867528984,126.642889461322));
#178984=CARTESIAN_POINT('Ctrl Pts',(40.3516446707659,4.3167918492519,126.754907478997));
#178985=CARTESIAN_POINT('Ctrl Pts',(40.3590447532808,4.42310090580708,126.871309860251));
#178986=CARTESIAN_POINT('Ctrl Pts',(40.3664448357958,4.52453673147266,126.991684663849));
#178987=CARTESIAN_POINT('Ctrl Pts',(40.3738530554623,4.62608409625671,127.112191831918));
#178988=CARTESIAN_POINT('Ctrl Pts',(40.3812612751288,4.7227472879426,127.236679860052));
#178989=CARTESIAN_POINT('Ctrl Pts',(40.3886694947953,4.81421841280676,127.364704873703));
#178990=CARTESIAN_POINT('Ctrl Pts',(40.3960822740973,4.905745836622,127.492808684613));
#178991=CARTESIAN_POINT('Ctrl Pts',(40.4034950533994,4.99207462168811,127.624453507457));
#178992=CARTESIAN_POINT('Ctrl Pts',(40.4109078327014,5.07294169108934,127.759168807301));
#178993=CARTESIAN_POINT('Ctrl Pts',(40.4183312037302,5.15392430715175,127.894076594683));
#178994=CARTESIAN_POINT('Ctrl Pts',(40.425754574759,5.22942944258174,128.03206329476));
#178995=CARTESIAN_POINT('Ctrl Pts',(40.4331779457878,5.29924084244862,128.172635507258));
#178996=CARTESIAN_POINT('Ctrl Pts',(40.4371139952286,5.33625652175943,128.247170267308));
#178997=CARTESIAN_POINT('Ctrl Pts',(40.4410500446693,5.37167229983716,128.32243159223));
#178998=CARTESIAN_POINT('Ctrl Pts',(40.4449860941101,5.40546158672476,128.39834407628));
#178999=CARTESIAN_POINT('Ctrl Pts',(40.4524093605156,5.46918712726751,128.541512652051));
#179000=CARTESIAN_POINT('Ctrl Pts',(40.459832626921,5.5273171742017,128.687431207435));
#179001=CARTESIAN_POINT('Ctrl Pts',(40.4672558933265,5.57960573897948,128.835622351557));
#179002=CARTESIAN_POINT('Ctrl Pts',(40.4746703860475,5.63183250301585,128.983638346053));
#179003=CARTESIAN_POINT('Ctrl Pts',(40.4820848787685,5.67823140463998,129.133921234178));
#179004=CARTESIAN_POINT('Ctrl Pts',(40.4894993714894,5.71860331416626,129.285971109664));
#179005=CARTESIAN_POINT('Ctrl Pts',(40.4969067178432,5.75893631172639,129.437874433757));
#179006=CARTESIAN_POINT('Ctrl Pts',(40.504314064197,5.79325378669266,129.591540996322));
#179007=CARTESIAN_POINT('Ctrl Pts',(40.5117214105508,5.82140553757743,129.746453187985));
#179008=CARTESIAN_POINT('Ctrl Pts',(40.5191232322262,5.84953629182421,129.901249840291));
#179009=CARTESIAN_POINT('Ctrl Pts',(40.5265250539017,5.87151041202376,130.057289906154));
#179010=CARTESIAN_POINT('Ctrl Pts',(40.5339268755771,5.88722818982492,130.214043072993));
#179011=CARTESIAN_POINT('Ctrl Pts',(40.5413247898884,5.90293767033347,130.370713491055));
#179012=CARTESIAN_POINT('Ctrl Pts',(40.5487227041997,5.91239734872819,130.528095889897));
#179013=CARTESIAN_POINT('Ctrl Pts',(40.5561206185111,5.9155590537797,130.685652388091));
#179014=CARTESIAN_POINT('Ctrl Pts',(40.5635173034233,5.9187202334132,130.843182703254));
#179015=CARTESIAN_POINT('Ctrl Pts',(40.5709139883355,5.91558550943023,131.000886687489));
#179016=CARTESIAN_POINT('Ctrl Pts',(40.5783106732477,5.90615876521095,131.158223871694));
#179017=CARTESIAN_POINT('Ctrl Pts',(40.5857070301832,5.8967324389834,131.315554079403));
#179018=CARTESIAN_POINT('Ctrl Pts',(40.5931033871186,5.88101466958121,131.472517146792));
#179019=CARTESIAN_POINT('Ctrl Pts',(40.600499744054,5.85906140355735,131.628575414718));
#179020=CARTESIAN_POINT('Ctrl Pts',(40.6078972333906,5.83710477643234,131.784657575564));
#179021=CARTESIAN_POINT('Ctrl Pts',(40.6152947227272,5.80891080381423,131.939834291438));
#179022=CARTESIAN_POINT('Ctrl Pts',(40.6226922120638,5.77458694298216,132.093575960494));
#179023=CARTESIAN_POINT('Ctrl Pts',(40.6300922945788,5.74025104997384,132.247371523453));
#179024=CARTESIAN_POINT('Ctrl Pts',(40.6374923770939,5.69978107174915,132.399730673917));
#179025=CARTESIAN_POINT('Ctrl Pts',(40.6448924596089,5.65333488177034,132.550137028524));
#179026=CARTESIAN_POINT('Ctrl Pts',(40.6523006792754,5.60683761943092,132.700708770381));
#179027=CARTESIAN_POINT('Ctrl Pts',(40.6597088989418,5.55435113191353,132.849323071186));
#179028=CARTESIAN_POINT('Ctrl Pts',(40.6671171186083,5.4960824393679,132.995480966194));
#179029=CARTESIAN_POINT('Ctrl Pts',(40.6745298979104,5.43777788341435,133.141728818948));
#179030=CARTESIAN_POINT('Ctrl Pts',(40.6819426772125,5.37368418260655,133.285516913133));
#179031=CARTESIAN_POINT('Ctrl Pts',(40.6893554565146,5.30405501181169,133.426369579064));
#179032=CARTESIAN_POINT('Ctrl Pts',(40.6967788275433,5.23432635159222,133.56742350189));
#179033=CARTESIAN_POINT('Ctrl Pts',(40.7042021985721,5.15904660284588,133.705533292648));
#179034=CARTESIAN_POINT('Ctrl Pts',(40.7116255696009,5.07851398612542,133.84025031504));
#179035=CARTESIAN_POINT('Ctrl Pts',(40.7155616190416,5.03581366038748,133.911680512801));
#179036=CARTESIAN_POINT('Ctrl Pts',(40.7194976684823,4.99163726934961,133.982157394404));
#179037=CARTESIAN_POINT('Ctrl Pts',(40.723433717923,4.94603388147802,134.051617830318));
#179038=CARTESIAN_POINT('Ctrl Pts',(40.7308569843284,4.86002731518371,134.182618044669));
#179039=CARTESIAN_POINT('Ctrl Pts',(40.7382802507339,4.76868261218417,134.310397042927));
#179040=CARTESIAN_POINT('Ctrl Pts',(40.7457035171393,4.67226845212472,134.434489826531));
#179041=CARTESIAN_POINT('Ctrl Pts',(40.7531180098603,4.57596824559563,134.55843594277));
#179042=CARTESIAN_POINT('Ctrl Pts',(40.7605325025813,4.4746107352678,134.678704224687));
#179043=CARTESIAN_POINT('Ctrl Pts',(40.7679469953023,4.36850887198248,134.794856927289));
#179044=CARTESIAN_POINT('Ctrl Pts',(40.7753543416561,4.26250927366765,134.910897677542));
#179045=CARTESIAN_POINT('Ctrl Pts',(40.7827616880099,4.15177467598909,135.022830471733));
#179046=CARTESIAN_POINT('Ctrl Pts',(40.7901690343636,4.03665937080015,135.130249160586));
#179047=CARTESIAN_POINT('Ctrl Pts',(40.797570856039,3.92162992294871,135.237587732528));
#179048=CARTESIAN_POINT('Ctrl Pts',(40.8049726777144,3.80222654496907,135.340418649281));
#179049=CARTESIAN_POINT('Ctrl Pts',(40.8123744993898,3.67884150905682,135.438371376481));
#179050=CARTESIAN_POINT('Ctrl Pts',(40.8197724137012,3.55552160714426,135.536272395199));
#179051=CARTESIAN_POINT('Ctrl Pts',(40.8271703280126,3.42822452493381,135.629300121399));
#179052=CARTESIAN_POINT('Ctrl Pts',(40.834568242324,3.29737675957992,135.717123289208));
#179053=CARTESIAN_POINT('Ctrl Pts',(40.8419649272362,3.16655073875137,135.8049318624));
#179054=CARTESIAN_POINT('Ctrl Pts',(40.8493616121484,3.03217551552328,135.887537385946));
#179055=CARTESIAN_POINT('Ctrl Pts',(40.8567582970606,2.89470790091954,135.964650990293));
#179056=CARTESIAN_POINT('Ctrl Pts',(40.864154653996,2.75724638177389,136.041761175341));
#179057=CARTESIAN_POINT('Ctrl Pts',(40.8715510109314,2.61669306946448,136.113379742752));
#179058=CARTESIAN_POINT('Ctrl Pts',(40.8789473678669,2.47353055233435,136.179263144047));
#179059=CARTESIAN_POINT('Ctrl Pts',(40.8863448572035,2.33034611665716,136.245156632258));
#179060=CARTESIAN_POINT('Ctrl Pts',(40.8937423465401,2.18455201988314,136.305313049932));
#179061=CARTESIAN_POINT('Ctrl Pts',(40.9011398358766,2.03665191433,136.359536541185));
#179062=CARTESIAN_POINT('Ctrl Pts',(40.9085399183916,1.88869996262476,136.413779040399));
#179063=CARTESIAN_POINT('Ctrl Pts',(40.9159400009066,1.73864088254088,136.462084343953));
#179064=CARTESIAN_POINT('Ctrl Pts',(40.9233400834216,1.58699445648627,136.504306157445));
#179065=CARTESIAN_POINT('Ctrl Pts',(40.930748303088,1.43518127959615,136.54657439816));
#179066=CARTESIAN_POINT('Ctrl Pts',(40.9381565227545,1.2817776307969,136.582745689409));
#179067=CARTESIAN_POINT('Ctrl Pts',(40.9455647424209,1.12731520270745,136.612724500472));
#179068=CARTESIAN_POINT('Ctrl Pts',(40.952977521723,0.972757705570631,136.642721762993));
#179069=CARTESIAN_POINT('Ctrl Pts',(40.9603903010251,0.817140498780058,
136.666518894402));
#179070=CARTESIAN_POINT('Ctrl Pts',(40.9678030803271,0.661000894175588,
136.684072207466));
#179071=CARTESIAN_POINT('Ctrl Pts',(40.9752264513559,0.504638189981837,
136.701650601526));
#179072=CARTESIAN_POINT('Ctrl Pts',(40.9826498223847,0.347751968537191,
136.712967332296));
#179073=CARTESIAN_POINT('Ctrl Pts',(40.9900731934134,0.190880875758771,
136.718030802296));
#179074=CARTESIAN_POINT('Ctrl Pts',(40.9940092428542,0.107704058296784,
136.720715575587));
#179075=CARTESIAN_POINT('Ctrl Pts',(40.9979452922951,0.0245314433688089,
136.721643202666));
#179076=CARTESIAN_POINT('Ctrl Pts',(41.0018813417359,-0.0585573336590143,
136.720820843172));
#179077=CARTESIAN_POINT('Ctrl Pts',(41.0093046081413,-0.215260174020292,
136.71926989883));
#179078=CARTESIAN_POINT('Ctrl Pts',(41.0167278745468,-0.372138307333893,
136.711486682914));
#179079=CARTESIAN_POINT('Ctrl Pts',(41.0241511409522,-0.528655289229605,
136.697445900138));
#179080=CARTESIAN_POINT('Ctrl Pts',(41.0315656336732,-0.684987281050643,
136.683421712401));
#179081=CARTESIAN_POINT('Ctrl Pts',(41.0389801263942,-0.840958602928902,
136.663154712461));
#179082=CARTESIAN_POINT('Ctrl Pts',(41.0463946191152,-0.996031810030865,
136.636671582862));
#179083=CARTESIAN_POINT('Ctrl Pts',(41.053801965469,-1.15095555173808,136.6102139787));
#179084=CARTESIAN_POINT('Ctrl Pts',(41.0612093118228,-1.30498253648128,
136.577552234876));
#179085=CARTESIAN_POINT('Ctrl Pts',(41.0686166581766,-1.45757955597116,
136.538764893558));
#179086=CARTESIAN_POINT('Ctrl Pts',(41.076018479852,-1.61006276284655,136.500006481302));
#179087=CARTESIAN_POINT('Ctrl Pts',(41.0834203015274,-1.76111776782164,
136.455131660018));
#179088=CARTESIAN_POINT('Ctrl Pts',(41.0908221232029,-1.91022079713827,
136.404270176539));
#179089=CARTESIAN_POINT('Ctrl Pts',(41.0982200375142,-2.05924511612529,
136.353435542442));
#179090=CARTESIAN_POINT('Ctrl Pts',(41.1056179518255,-2.20631915919651,
136.296620660277));
#179091=CARTESIAN_POINT('Ctrl Pts',(41.1130158661368,-2.35093369086305,
136.234005296886));
#179092=CARTESIAN_POINT('Ctrl Pts',(41.120412551049,-2.49552419021863,136.171400339031));
#179093=CARTESIAN_POINT('Ctrl Pts',(41.1278092359612,-2.63765564713984,
136.102996961254));
#179094=CARTESIAN_POINT('Ctrl Pts',(41.1352059208734,-2.77683810997354,
136.029023350556));
#179095=CARTESIAN_POINT('Ctrl Pts',(41.1426022778088,-2.91601440131099,
135.955053019926));
#179096=CARTESIAN_POINT('Ctrl Pts',(41.1499986347443,-3.05224162892631,
135.87551312267));
#179097=CARTESIAN_POINT('Ctrl Pts',(41.1573949916798,-3.1850540377979,135.790678030127));
#179098=CARTESIAN_POINT('Ctrl Pts',(41.1647924810163,-3.31788678058872,
135.705829949114));
#179099=CARTESIAN_POINT('Ctrl Pts',(41.1721899703529,-3.44730334902115,
135.615685259549));
#179100=CARTESIAN_POINT('Ctrl Pts',(41.1795874596895,-3.5728667276141,135.520561833503));
#179101=CARTESIAN_POINT('Ctrl Pts',(41.1869875422044,-3.69847412225334,
135.425405062089));
#179102=CARTESIAN_POINT('Ctrl Pts',(41.1943876247194,-3.82022534039261,
135.325266304615));
#179103=CARTESIAN_POINT('Ctrl Pts',(41.2017877072343,-3.9377163453184,135.220503793043));
#179104=CARTESIAN_POINT('Ctrl Pts',(41.2091959269008,-4.0553365436833,135.115626084319));
#179105=CARTESIAN_POINT('Ctrl Pts',(41.2166041465672,-4.16868689470295,
135.00611471642));
#179106=CARTESIAN_POINT('Ctrl Pts',(41.2240123662337,-4.27739963283134,
134.892365380718));
#179107=CARTESIAN_POINT('Ctrl Pts',(41.2314251455357,-4.38617928183638,
134.778546034198));
#179108=CARTESIAN_POINT('Ctrl Pts',(41.2388379248378,-4.49031538389258,
134.660483801621));
#179109=CARTESIAN_POINT('Ctrl Pts',(41.2462507041399,-4.5894807535191,134.538607124638));
#179110=CARTESIAN_POINT('Ctrl Pts',(41.2536740751686,-4.68878781527613,
134.416556304543));
#179111=CARTESIAN_POINT('Ctrl Pts',(41.2610974461973,-4.78310973622976,
134.290680452602));
#179112=CARTESIAN_POINT('Ctrl Pts',(41.2685208172261,-4.87216243438203,
134.161437288644));
#179113=CARTESIAN_POINT('Ctrl Pts',(41.272456866667,-4.91938031173366,134.092909461965));
#179114=CARTESIAN_POINT('Ctrl Pts',(41.2763929161079,-4.96511758064068,
134.023435390549));
#179115=CARTESIAN_POINT('Ctrl Pts',(41.2803289655488,-5.00933721984806,
133.953085943844));
#179116=CARTESIAN_POINT('Ctrl Pts',(41.2879507990617,-5.09496488614177,
133.816860071033));
#179117=CARTESIAN_POINT('Ctrl Pts',(41.2955726325746,-5.17514684997344,
133.676956375135));
#179118=CARTESIAN_POINT('Ctrl Pts',(41.3031944660875,-5.24956106473146,
133.533836609429));
#179119=CARTESIAN_POINT('Ctrl Pts',(41.3108058128407,-5.32387289415342,
133.390913759935));
#179120=CARTESIAN_POINT('Ctrl Pts',(41.3184171595939,-5.39243262360372,
133.244783959347));
#179121=CARTESIAN_POINT('Ctrl Pts',(41.3260285063472,-5.45496157201488,
133.095937544126));
#179122=CARTESIAN_POINT('Ctrl Pts',(41.3336305557737,-5.51741414076793,
132.947272946105));
#179123=CARTESIAN_POINT('Ctrl Pts',(41.3412326052003,-5.57385047090191,
132.795898661498));
#179124=CARTESIAN_POINT('Ctrl Pts',(41.3488346546268,-5.62403781503907,
132.642329392467));
#179125=CARTESIAN_POINT('Ctrl Pts',(41.3564261680854,-5.67415560263751,
132.488972960895));
#179126=CARTESIAN_POINT('Ctrl Pts',(41.3640176815441,-5.7180415659947,132.333427938303));
#179127=CARTESIAN_POINT('Ctrl Pts',(41.3716091950027,-5.75551120804998,
132.176228430626));
#179128=CARTESIAN_POINT('Ctrl Pts',(41.3791945469146,-5.79295043838896,
132.019156511754));
#179129=CARTESIAN_POINT('Ctrl Pts',(41.3867798988264,-5.823983640756,131.860433118151));
#179130=CARTESIAN_POINT('Ctrl Pts',(41.3943652507382,-5.84847600411157,
131.700607788737));
#179131=CARTESIAN_POINT('Ctrl Pts',(41.4019444458498,-5.87294848775788,
131.5409121847));
#179132=CARTESIAN_POINT('Ctrl Pts',(41.4095236409613,-5.89089066382546,
131.380116769395));
#179133=CARTESIAN_POINT('Ctrl Pts',(41.4171028360728,-5.90221872705661,
131.218781491174));
#179134=CARTESIAN_POINT('Ctrl Pts',(41.4236101599804,-5.91194474355384,
131.080262704199));
#179135=CARTESIAN_POINT('Ctrl Pts',(41.430117483888,-5.91679593767829,130.941346268479));
#179136=CARTESIAN_POINT('Ctrl Pts',(41.4366248077955,-5.91674967204228,
130.802390620728));
#179137=CARTESIAN_POINT('',(43.1866248077955,-5.92140473490589,130.799702052978));
#179138=CARTESIAN_POINT('Ctrl Pts',(41.4366261848254,-5.90754071104223,
130.802364327911));
#179139=CARTESIAN_POINT('Ctrl Pts',(41.4773429863376,-5.91011510315806,
129.934261000353));
#179140=CARTESIAN_POINT('Ctrl Pts',(41.6108756624536,-5.32352528808913,
127.090594479252));
#179141=CARTESIAN_POINT('Ctrl Pts',(41.8372242131748,-0.924490577904954,
123.867295121138));
#179142=CARTESIAN_POINT('Ctrl Pts',(42.1156718369874,5.33663993075326,126.276907163378));
#179143=CARTESIAN_POINT('Ctrl Pts',(42.3941194608004,6.69365905240206,132.847027751616));
#179144=CARTESIAN_POINT('Ctrl Pts',(42.6725670846133,1.8995325083189,137.540037033501));
#179145=CARTESIAN_POINT('Ctrl Pts',(42.9367355336118,-4.30480664579817,
136.120044043652));
#179146=CARTESIAN_POINT('Ctrl Pts',(43.1080881080057,-5.90703348562082,
132.464199972487));
#179147=CARTESIAN_POINT('Ctrl Pts',(43.1866248077955,-5.92140473490589,
130.799702052978));
#179148=CARTESIAN_POINT('',(44.9366248077955,-5.92016258122845,130.808544943896));
#179149=CARTESIAN_POINT('Ctrl Pts',(43.1866248077955,-5.92140473490589,
130.799702052978));
#179150=CARTESIAN_POINT('Ctrl Pts',(43.20090398261,-5.92401764812218,130.497070839358));
#179151=CARTESIAN_POINT('Ctrl Pts',(43.3079990320291,-5.76510993760414,
128.23006237518));
#179152=CARTESIAN_POINT('Ctrl Pts',(43.5079099560517,-2.83612951018477,
124.406397665834));
#179153=CARTESIAN_POINT('Ctrl Pts',(43.786357579865,3.84979015445499,124.959989282935));
#179154=CARTESIAN_POINT('Ctrl Pts',(44.0648052036776,6.99794073985275,130.884272643158));
#179155=CARTESIAN_POINT('Ctrl Pts',(44.3432528274906,3.71532565374068,136.735120755777));
#179156=CARTESIAN_POINT('Ctrl Pts',(44.6217004513035,-2.981492204414,137.135890035122));
#179157=CARTESIAN_POINT('Ctrl Pts',(44.8194911114051,-5.79226188538465,
133.287589730583));
#179158=CARTESIAN_POINT('Ctrl Pts',(44.9244658969025,-5.92469486449521,
131.06610242403));
#179159=CARTESIAN_POINT('Ctrl Pts',(44.9366248077955,-5.92263029408517,
130.808546688057));
#179160=CARTESIAN_POINT('',(46.6866247826357,-5.91193532425354,130.807010291797));
#179161=CARTESIAN_POINT('Ctrl Pts',(44.9366248077955,-5.91674852212777,
130.808542530865));
#179162=CARTESIAN_POINT('Ctrl Pts',(44.9439356290697,-5.91685786750848,
130.653836042839));
#179163=CARTESIAN_POINT('Ctrl Pts',(44.9512464503438,-5.91089535321625,
130.498893564097));
#179164=CARTESIAN_POINT('Ctrl Pts',(44.9585572716179,-5.89883200535206,
130.344239399696));
#179165=CARTESIAN_POINT('Ctrl Pts',(44.9658607352432,-5.88678079810431,
130.189740880055));
#179166=CARTESIAN_POINT('Ctrl Pts',(44.9731641988686,-5.86864100352846,
130.035530478046));
#179167=CARTESIAN_POINT('Ctrl Pts',(44.9804676624939,-5.84443566142174,
129.882133768032));
#179168=CARTESIAN_POINT('Ctrl Pts',(44.9877654758338,-5.82024904564804,
129.728855732559));
#179169=CARTESIAN_POINT('Ctrl Pts',(44.9950632891737,-5.79000628061789,
129.576390514602));
#179170=CARTESIAN_POINT('Ctrl Pts',(45.0023611025136,-5.75378230755912,
129.425259562632));
#179171=CARTESIAN_POINT('Ctrl Pts',(45.0097042106975,-5.71733350561856,
129.273190596412));
#179172=CARTESIAN_POINT('Ctrl Pts',(45.0170473188815,-5.67482902238523,
129.122472908791));
#179173=CARTESIAN_POINT('Ctrl Pts',(45.0243904270655,-5.62639776554055,
128.973628865938));
#179174=CARTESIAN_POINT('Ctrl Pts',(45.0316830372035,-5.57829956709244,
128.82580841325));
#179175=CARTESIAN_POINT('Ctrl Pts',(45.0389756473414,-5.52435599133673,
128.679836282438));
#179176=CARTESIAN_POINT('Ctrl Pts',(45.0462682574794,-5.46474358155259,
128.536209795777));
#179177=CARTESIAN_POINT('Ctrl Pts',(45.0535606612411,-5.40513285876214,
128.392587373657));
#179178=CARTESIAN_POINT('Ctrl Pts',(45.0608530650027,-5.33985376844323,
128.251310819223));
#179179=CARTESIAN_POINT('Ctrl Pts',(45.0681454687644,-5.26913108006282,
128.112857650149));
#179180=CARTESIAN_POINT('Ctrl Pts',(45.0754392015105,-5.19839550301742,
127.974379249052));
#179181=CARTESIAN_POINT('Ctrl Pts',(45.0827329342566,-5.12221452936977,
127.838725599691));
#179182=CARTESIAN_POINT('Ctrl Pts',(45.0900266670027,-5.04085882516912,
127.7063495028));
#179183=CARTESIAN_POINT('Ctrl Pts',(45.0974074196632,-4.95853248403015,
127.572394055934));
#179184=CARTESIAN_POINT('Ctrl Pts',(45.1047881723237,-4.87090734677987,
127.441795221017));
#179185=CARTESIAN_POINT('Ctrl Pts',(45.1121689249843,-4.77830835698527,
127.314991074502));
#179186=CARTESIAN_POINT('Ctrl Pts',(45.1194735190076,-4.68666485414325,
127.189495362429));
#179187=CARTESIAN_POINT('Ctrl Pts',(45.126778113031,-4.59014995067122,127.067716658515));
#179188=CARTESIAN_POINT('Ctrl Pts',(45.1340827070544,-4.48911806096891,
126.950044906939));
#179189=CARTESIAN_POINT('Ctrl Pts',(45.1415015390335,-4.38650611404346,
126.830532864129));
#179190=CARTESIAN_POINT('Ctrl Pts',(45.1489203710127,-4.27923500777099,
126.715257603372));
#179191=CARTESIAN_POINT('Ctrl Pts',(45.1563392029919,-4.16771300727604,
126.604586950869));
#179192=CARTESIAN_POINT('Ctrl Pts',(45.163758034971,-4.05619100678108,126.493916298365));
#179193=CARTESIAN_POINT('Ctrl Pts',(45.1711768669501,-3.94041845823231,
126.387850480556));
#179194=CARTESIAN_POINT('Ctrl Pts',(45.1785956989293,-3.82083591173472,
126.286712612453));
#179195=CARTESIAN_POINT('Ctrl Pts',(45.1860189653347,-3.70118188768014,
126.185514291651));
#179196=CARTESIAN_POINT('Ctrl Pts',(45.1934422317401,-3.5773236613378,126.088919949533));
#179197=CARTESIAN_POINT('Ctrl Pts',(45.2008654981455,-3.44965085327522,
125.997299191601));
#179198=CARTESIAN_POINT('Ctrl Pts',(45.2082799908665,-3.32212894386903,
125.905786721796));
#179199=CARTESIAN_POINT('Ctrl Pts',(45.2156944835875,-3.19080172729827,
125.819236350781));
#179200=CARTESIAN_POINT('Ctrl Pts',(45.2231089763085,-3.05609353823588,
125.737978984877));
#179201=CARTESIAN_POINT('Ctrl Pts',(45.2305163226623,-2.92151518599797,
125.65679993788));
#179202=CARTESIAN_POINT('Ctrl Pts',(45.2379236690161,-2.78356266621654,
125.580903931238));
#179203=CARTESIAN_POINT('Ctrl Pts',(45.2453310153699,-2.64269098546984,
125.510579840294));
#179204=CARTESIAN_POINT('Ctrl Pts',(45.2527328370453,-2.50192437213682,
125.44030819971));
#179205=CARTESIAN_POINT('Ctrl Pts',(45.2601346587207,-2.35824326553433,
125.37560036619));
#179206=CARTESIAN_POINT('Ctrl Pts',(45.2675364803961,-2.21212898083884,
125.316700284179));
#179207=CARTESIAN_POINT('Ctrl Pts',(45.2749343947074,-2.06609182873709,
125.257831295062));
#179208=CARTESIAN_POINT('Ctrl Pts',(45.2823323090188,-1.91762440194704,
125.204764090846));
#179209=CARTESIAN_POINT('Ctrl Pts',(45.2897302233302,-1.76722968623992,
125.157695247759));
#179210=CARTESIAN_POINT('Ctrl Pts',(45.2971269082424,-1.61685996340631,
125.110634226661));
#179211=CARTESIAN_POINT('Ctrl Pts',(45.3045235931546,-1.46456394322652,
125.069569699691));
#179212=CARTESIAN_POINT('Ctrl Pts',(45.3119202780668,-1.31086164400109,
125.034648985882));
#179213=CARTESIAN_POINT('Ctrl Pts',(45.3193166350022,-1.15716616009645,
124.999729820494));
#179214=CARTESIAN_POINT('Ctrl Pts',(45.3267129919377,-1.00206488515139,
124.970954009303));
#179215=CARTESIAN_POINT('Ctrl Pts',(45.3341093488732,-0.846089689838693,
124.94841809742));
#179216=CARTESIAN_POINT('Ctrl Pts',(45.3415068382097,-0.690090614325849,
124.925878735232));
#179217=CARTESIAN_POINT('Ctrl Pts',(45.3489043275463,-0.533217721518071,
124.909581227955));
#179218=CARTESIAN_POINT('Ctrl Pts',(45.3563018168828,-0.376009541818982,
124.899570410712));
#179219=CARTESIAN_POINT('Ctrl Pts',(45.3637018993978,-0.218746253035978,
124.889556084192));
#179220=CARTESIAN_POINT('Ctrl Pts',(45.3711019819128,-0.0611478156626729,
124.885832859144));
#179221=CARTESIAN_POINT('Ctrl Pts',(45.3785020644278,0.096245841597927,
124.888393469206));
#179222=CARTESIAN_POINT('Ctrl Pts',(45.3859102840943,0.253812569365371,
124.890956894922));
#179223=CARTESIAN_POINT('Ctrl Pts',(45.3933185037608,0.411173693849745,
124.899817948841));
#179224=CARTESIAN_POINT('Ctrl Pts',(45.4007267234272,0.567792275605391,
124.914917308198));
#179225=CARTESIAN_POINT('Ctrl Pts',(45.4081395027293,0.724507253484786,
124.930025960958));
#179226=CARTESIAN_POINT('Ctrl Pts',(45.4155522820314,0.88047840897048,124.951380519465));
#179227=CARTESIAN_POINT('Ctrl Pts',(45.4229650613335,1.03517813060349,124.9788703549));
#179228=CARTESIAN_POINT('Ctrl Pts',(45.4303884323622,1.19009889445346,125.0063994691));
#179229=CARTESIAN_POINT('Ctrl Pts',(45.437811803391,1.3437442324516,125.040081288913));
#179230=CARTESIAN_POINT('Ctrl Pts',(45.4452351744197,1.49560003991316,125.07975485969));
#179231=CARTESIAN_POINT('Ctrl Pts',(45.4491712238606,1.57611763276001,125.10079073887));
#179232=CARTESIAN_POINT('Ctrl Pts',(45.4531072733014,1.65613241984305,125.123510294631));
#179233=CARTESIAN_POINT('Ctrl Pts',(45.4570433227422,1.73557007374295,125.147884056877));
#179234=CARTESIAN_POINT('Ctrl Pts',(45.4644665891476,1.88538700983267,125.193852211792));
#179235=CARTESIAN_POINT('Ctrl Pts',(45.4718898555531,2.03360296229411,125.245846044098));
#179236=CARTESIAN_POINT('Ctrl Pts',(45.4793131219585,2.17969637211682,125.30373753578));
#179237=CARTESIAN_POINT('Ctrl Pts',(45.4867276146795,2.32561711166163,125.361560604525));
#179238=CARTESIAN_POINT('Ctrl Pts',(45.4941421074005,2.46941995843265,125.425267321563));
#179239=CARTESIAN_POINT('Ctrl Pts',(45.5015566001215,2.61059714831543,125.494679545062));
#179240=CARTESIAN_POINT('Ctrl Pts',(45.5089639464753,2.75163826630716,125.564024866447));
#179241=CARTESIAN_POINT('Ctrl Pts',(45.5163712928292,2.890058432802,125.639064582904));
#179242=CARTESIAN_POINT('Ctrl Pts',(45.5237786391829,3.0253686666206,125.719572028693));
#179243=CARTESIAN_POINT('Ctrl Pts',(45.5311804608583,3.16057798096165,125.800019428992));
#179244=CARTESIAN_POINT('Ctrl Pts',(45.5385822825336,3.29268166164688,125.885926248643));
#179245=CARTESIAN_POINT('Ctrl Pts',(45.545984104209,3.4212143086976,125.977019401486));
#179246=CARTESIAN_POINT('Ctrl Pts',(45.5533820185204,3.54967910436535,126.068064466964));
#179247=CARTESIAN_POINT('Ctrl Pts',(45.5607799328318,3.67457631691279,126.164290197822));
#179248=CARTESIAN_POINT('Ctrl Pts',(45.5681778471432,3.79546868509539,126.265379672138));
#179249=CARTESIAN_POINT('Ctrl Pts',(45.5755745320554,3.91634096315892,126.366452347217));
#179250=CARTESIAN_POINT('Ctrl Pts',(45.5829712169676,4.03320943165098,126.472386922357));
#179251=CARTESIAN_POINT('Ctrl Pts',(45.5903679018798,4.14566906430304,126.582825520971));
#179252=CARTESIAN_POINT('Ctrl Pts',(45.5977642588152,4.25812371037713,126.693259222622));
#179253=CARTESIAN_POINT('Ctrl Pts',(45.6051606157507,4.3661696429725,126.808196289093));
#179254=CARTESIAN_POINT('Ctrl Pts',(45.6125569726861,4.46943814686197,126.927241427513));
#179255=CARTESIAN_POINT('Ctrl Pts',(45.6199544620227,4.57272246142317,127.046304792049));
#179256=CARTESIAN_POINT('Ctrl Pts',(45.6273519513593,4.67122764626124,127.169477198867));
#179257=CARTESIAN_POINT('Ctrl Pts',(45.6347494406959,4.76462489147967,127.296329801568));
#179258=CARTESIAN_POINT('Ctrl Pts',(45.6421495232109,4.85805487695762,127.423226872252));
#179259=CARTESIAN_POINT('Ctrl Pts',(45.6495496057259,4.94637313659405,127.55380640695));
#179260=CARTESIAN_POINT('Ctrl Pts',(45.6569496882409,5.02929393913205,127.687610220709));
#179261=CARTESIAN_POINT('Ctrl Pts',(45.6643579079074,5.11230592161691,127.821561165516));
#179262=CARTESIAN_POINT('Ctrl Pts',(45.6717661275738,5.18990839753916,127.95874315233));
#179263=CARTESIAN_POINT('Ctrl Pts',(45.6791743472403,5.26186104793697,128.098672373384));
#179264=CARTESIAN_POINT('Ctrl Pts',(45.6865871265424,5.3338579839904,128.238687718539));
#179265=CARTESIAN_POINT('Ctrl Pts',(45.6939999058444,5.40019800847263,128.381453329469));
#179266=CARTESIAN_POINT('Ctrl Pts',(45.7014126851465,5.46068900966242,128.526465514131));
#179267=CARTESIAN_POINT('Ctrl Pts',(45.7088360561752,5.52126644323154,128.671684899004));
#179268=CARTESIAN_POINT('Ctrl Pts',(45.716259427204,5.57597803248774,128.819156919657));
#179269=CARTESIAN_POINT('Ctrl Pts',(45.7236827982327,5.6246813069971,128.96836204534));
#179270=CARTESIAN_POINT('Ctrl Pts',(45.7276188476735,5.65050495176093,129.047474183104));
#179271=CARTESIAN_POINT('Ctrl Pts',(45.7315548971143,5.67464029293529,129.127073364458));
#179272=CARTESIAN_POINT('Ctrl Pts',(45.7354909465551,5.69707194876263,129.20708112633));
#179273=CARTESIAN_POINT('Ctrl Pts',(45.7429142129605,5.73937735158505,129.357973268265));
#179274=CARTESIAN_POINT('Ctrl Pts',(45.750337479366,5.77574781060515,129.510775483146));
#179275=CARTESIAN_POINT('Ctrl Pts',(45.7577607457714,5.80600911562059,129.664979771742));
#179276=CARTESIAN_POINT('Ctrl Pts',(45.7651752384924,5.83623465428658,129.819001803675));
#179277=CARTESIAN_POINT('Ctrl Pts',(45.7725897312134,5.86036534023474,129.974422248053));
#179278=CARTESIAN_POINT('Ctrl Pts',(45.7800042239344,5.87827659032461,130.130717618536));
#179279=CARTESIAN_POINT('Ctrl Pts',(45.7874115702882,5.89617057687732,130.286862345657));
#179280=CARTESIAN_POINT('Ctrl Pts',(45.794818916642,5.90785701927774,130.443879951684));
#179281=CARTESIAN_POINT('Ctrl Pts',(45.8022262629957,5.91326231156118,130.601236524534));
#179282=CARTESIAN_POINT('Ctrl Pts',(45.8096280846711,5.9186635723737,130.758475734914));
#179283=CARTESIAN_POINT('Ctrl Pts',(45.8170299063465,5.91779299821617,130.916053037257));
#179284=CARTESIAN_POINT('Ctrl Pts',(45.8244317280219,5.91062878415207,131.073429267641));
#179285=CARTESIAN_POINT('Ctrl Pts',(45.8318296423332,5.90346835202084,131.230722420336));
#179286=CARTESIAN_POINT('Ctrl Pts',(45.8392275566445,5.89002091356227,131.387814340496));
#179287=CARTESIAN_POINT('Ctrl Pts',(45.8466254709558,5.87031675378085,131.544165843811));
#179288=CARTESIAN_POINT('Ctrl Pts',(45.854022155868,5.85061586847319,131.700491364344));
#179289=CARTESIAN_POINT('Ctrl Pts',(45.8614188407802,5.82466037207562,131.856076342233));
#179290=CARTESIAN_POINT('Ctrl Pts',(45.8688155256924,5.79253242970573,132.010386576369));
#179291=CARTESIAN_POINT('Ctrl Pts',(45.8762118826278,5.76040591192252,132.164689968228));
#179292=CARTESIAN_POINT('Ctrl Pts',(45.8836082395633,5.72210756845078,132.317718363261));
#179293=CARTESIAN_POINT('Ctrl Pts',(45.8910045964987,5.67777067078999,132.468947885455));
#179294=CARTESIAN_POINT('Ctrl Pts',(45.8984020858353,5.63342698503679,132.620200561275));
#179295=CARTESIAN_POINT('Ctrl Pts',(45.9057995751719,5.58304300928447,132.76965345763));
#179296=CARTESIAN_POINT('Ctrl Pts',(45.9131970645085,5.52680181437526,132.916798135487));
#179297=CARTESIAN_POINT('Ctrl Pts',(45.9205971470234,5.47054090420276,133.063994394681));
#179298=CARTESIAN_POINT('Ctrl Pts',(45.9279972295384,5.40841882008364,133.208880475903));
#179299=CARTESIAN_POINT('Ctrl Pts',(45.9353973120533,5.34066660127346,133.350968325192));
#179300=CARTESIAN_POINT('Ctrl Pts',(45.9428055317198,5.27283988193331,133.49321241468));
#179301=CARTESIAN_POINT('Ctrl Pts',(45.9502137513862,5.19937082501298,133.632651790219));
#179302=CARTESIAN_POINT('Ctrl Pts',(45.9576219710527,5.12053657342015,133.768822754745));
#179303=CARTESIAN_POINT('Ctrl Pts',(45.9650347503548,5.04165380066066,133.905077530227));
#179304=CARTESIAN_POINT('Ctrl Pts',(45.9724475296569,4.95739945253087,134.038059571623));
#179305=CARTESIAN_POINT('Ctrl Pts',(45.9798603089589,4.86809345833394,134.167334992049));
#179306=CARTESIAN_POINT('Ctrl Pts',(45.9872836799877,4.77865985954472,134.296795127256));
#179307=CARTESIAN_POINT('Ctrl Pts',(45.9947070510164,4.68416042234265,134.422537766178));
#179308=CARTESIAN_POINT('Ctrl Pts',(46.0021304220451,4.58495523391334,134.54416222534));
#179309=CARTESIAN_POINT('Ctrl Pts',(46.0060664714861,4.53235426261025,134.60865043193));
#179310=CARTESIAN_POINT('Ctrl Pts',(46.010002520927,4.47843095841243,134.67198147985));
#179311=CARTESIAN_POINT('Ctrl Pts',(46.0139385703679,4.42324302030786,134.734100016788));
#179312=CARTESIAN_POINT('Ctrl Pts',(46.0213618367734,4.31916029140282,134.851253638795));
#179313=CARTESIAN_POINT('Ctrl Pts',(46.0287851031789,4.2102625819376,134.964446465579));
#179314=CARTESIAN_POINT('Ctrl Pts',(46.0362083695843,4.09688312118325,135.073257343169));
#179315=CARTESIAN_POINT('Ctrl Pts',(46.0436228623053,3.98363766553642,135.181939615337));
#179316=CARTESIAN_POINT('Ctrl Pts',(46.0510373550263,3.86592126912529,135.286249991384));
#179317=CARTESIAN_POINT('Ctrl Pts',(46.0584518477473,3.74410701560329,135.38580069883));
#179318=CARTESIAN_POINT('Ctrl Pts',(46.0658591941011,3.62241017124454,135.485255455557));
#179319=CARTESIAN_POINT('Ctrl Pts',(46.0732665404548,3.49662361989866,135.579959441951));
#179320=CARTESIAN_POINT('Ctrl Pts',(46.0806738868086,3.36715677110134,135.669562138708));
#179321=CARTESIAN_POINT('Ctrl Pts',(46.088075708484,3.23778648356381,135.759098006394));
#179322=CARTESIAN_POINT('Ctrl Pts',(46.0954775301595,3.10474166968327,135.843539948656));
#179323=CARTESIAN_POINT('Ctrl Pts',(46.1028793518349,2.96846415723677,135.922578189114));
#179324=CARTESIAN_POINT('Ctrl Pts',(46.1102772661463,2.83225858462753,136.0015747059));
#179325=CARTESIAN_POINT('Ctrl Pts',(46.1176751804578,2.69282403416121,136.075173015105));
#179326=CARTESIAN_POINT('Ctrl Pts',(46.1250730947692,2.55063050665169,136.14310715407));
#179327=CARTESIAN_POINT('Ctrl Pts',(46.1324697796814,2.40846060912821,136.211030003614));
#179328=CARTESIAN_POINT('Ctrl Pts',(46.1398664645937,2.26353298103326,136.27329039032));
#179329=CARTESIAN_POINT('Ctrl Pts',(46.1472631495059,2.1163414731415,136.329668693281));
#179330=CARTESIAN_POINT('Ctrl Pts',(46.1546595064414,1.96915649187545,136.386044496369));
#179331=CARTESIAN_POINT('Ctrl Pts',(46.1620558633768,1.81970817900835,136.436538600782));
#179332=CARTESIAN_POINT('Ctrl Pts',(46.1694522203123,1.66850932276898,136.480979963826));
#179333=CARTESIAN_POINT('Ctrl Pts',(46.1768497096488,1.51728731759851,136.525428130956));
#179334=CARTESIAN_POINT('Ctrl Pts',(46.1842471989854,1.36431459357758,136.563821606276));
#179335=CARTESIAN_POINT('Ctrl Pts',(46.191644688322,1.21011786912664,136.596039588756));
#179336=CARTESIAN_POINT('Ctrl Pts',(46.199044770837,1.05586709125386,136.628268865198));
#179337=CARTESIAN_POINT('Ctrl Pts',(46.206444853352,0.900391823851985,136.654318262379));
#179338=CARTESIAN_POINT('Ctrl Pts',(46.213844935867,0.744227562900071,136.674118355081));
#179339=CARTESIAN_POINT('Ctrl Pts',(46.2212531555334,0.587891583288495,
136.693940220021));
#179340=CARTESIAN_POINT('Ctrl Pts',(46.2286613751999,0.430865467671833,
136.707499010156));
#179341=CARTESIAN_POINT('Ctrl Pts',(46.2360695948664,0.27368914003429,136.714777254075));
#179342=CARTESIAN_POINT('Ctrl Pts',(46.2434823741684,0.116416072989489,
136.722059977632));
#179343=CARTESIAN_POINT('Ctrl Pts',(46.2508951534706,-0.0410070178754066,
136.723054449985));
#179344=CARTESIAN_POINT('Ctrl Pts',(46.2583079327727,-0.198042161633038,
136.717795310257));
#179345=CARTESIAN_POINT('Ctrl Pts',(46.2657313038014,-0.355301684568288,
136.712528656023));
#179346=CARTESIAN_POINT('Ctrl Pts',(46.2731546748302,-0.512171781994873,
136.700990570913));
#179347=CARTESIAN_POINT('Ctrl Pts',(46.280578045859,-0.668120711639999,
136.683267427269));
#179348=CARTESIAN_POINT('Ctrl Pts',(46.2845140952996,-0.750808576077483,
136.673870191249));
#179349=CARTESIAN_POINT('Ctrl Pts',(46.2884501447402,-0.833237643384159,
136.662734966589));
#179350=CARTESIAN_POINT('Ctrl Pts',(46.2923861941809,-0.915330156377743,
136.649880377803));
#179351=CARTESIAN_POINT('Ctrl Pts',(46.2998094605863,-1.07015407387049,
136.625637024531));
#179352=CARTESIAN_POINT('Ctrl Pts',(46.3072327269918,-1.22424827677132,
136.595201785179));
#179353=CARTESIAN_POINT('Ctrl Pts',(46.3146559933972,-1.37707831775669,
136.558627370964));
#179354=CARTESIAN_POINT('Ctrl Pts',(46.3220704861182,-1.52972772632494,
136.52209618467));
#179355=CARTESIAN_POINT('Ctrl Pts',(46.3294849788391,-1.68111558755918,
136.479440352643));
#179356=CARTESIAN_POINT('Ctrl Pts',(46.3368994715601,-1.83071399666345,
136.430764160232));
#179357=CARTESIAN_POINT('Ctrl Pts',(46.3443068179139,-1.98016821718939,
136.382134883767));
#179358=CARTESIAN_POINT('Ctrl Pts',(46.3517141642678,-2.12783606660938,
136.327496913579));
#179359=CARTESIAN_POINT('Ctrl Pts',(46.3591215106215,-2.27320134724993,
136.267005233259));
#179360=CARTESIAN_POINT('Ctrl Pts',(46.3665233322969,-2.41845820897882,
136.206558669917));
#179361=CARTESIAN_POINT('Ctrl Pts',(46.3739251539723,-2.56141557822503,
136.140267232377));
#179362=CARTESIAN_POINT('Ctrl Pts',(46.3813269756476,-2.7015740126405,136.06833520116));
#179363=CARTESIAN_POINT('Ctrl Pts',(46.3887248899591,-2.84165845851243,
135.996441142302));
#179364=CARTESIAN_POINT('Ctrl Pts',(46.3961228042706,-2.97894658086459,
135.918912589866));
#179365=CARTESIAN_POINT('Ctrl Pts',(46.4035207185821,-3.11296057086087,
135.836001209537));
#179366=CARTESIAN_POINT('Ctrl Pts',(46.4109174034943,-3.24695229016116,
135.753103607576));
#179367=CARTESIAN_POINT('Ctrl Pts',(46.4183140884065,-3.3776706398419,135.664825149305));
#179368=CARTESIAN_POINT('Ctrl Pts',(46.4257107733187,-3.50466390820735,
135.571462614902));
#179369=CARTESIAN_POINT('Ctrl Pts',(46.4331071302542,-3.63165154555802,
135.478104220293));
#179370=CARTESIAN_POINT('Ctrl Pts',(46.4405034871896,-3.75491412925077,
135.379662418904));
#179371=CARTESIAN_POINT('Ctrl Pts',(46.4478998441251,-3.87403058165865,
135.276476181242));
#179372=CARTESIAN_POINT('Ctrl Pts',(46.4552973334616,-3.99316527109948,
135.173274145503));
#179373=CARTESIAN_POINT('Ctrl Pts',(46.4626948227982,-4.10815228314594,
135.065326471596));
#179374=CARTESIAN_POINT('Ctrl Pts',(46.4700923121348,-4.21860528029612,
134.953011006736));
#179375=CARTESIAN_POINT('Ctrl Pts',(46.4774923946498,-4.32909699657292,
134.840656169864));
#179376=CARTESIAN_POINT('Ctrl Pts',(46.4848924771647,-4.43505127190368,
134.723930759578));
#179377=CARTESIAN_POINT('Ctrl Pts',(46.4922925596797,-4.53612024823016,
134.603247777788));
#179378=CARTESIAN_POINT('Ctrl Pts',(46.4997007793462,-4.63730036028668,
134.482432092651));
#179379=CARTESIAN_POINT('Ctrl Pts',(46.5071089990127,-4.73358420549952,
134.357650431633));
#179380=CARTESIAN_POINT('Ctrl Pts',(46.5145172186791,-4.8246652425727,134.229347604346));
#179381=CARTESIAN_POINT('Ctrl Pts',(46.5219299979812,-4.91580233850455,
134.100965808809));
#179382=CARTESIAN_POINT('Ctrl Pts',(46.5293427772834,-5.00173004214471,
133.969058840609));
#179383=CARTESIAN_POINT('Ctrl Pts',(46.5367555565854,-5.08218670994251,
133.834098033215));
#179384=CARTESIAN_POINT('Ctrl Pts',(46.5441789276142,-5.16275833800006,
133.698944387491));
#179385=CARTESIAN_POINT('Ctrl Pts',(46.5516022986429,-5.23784313964544,
133.560728514899));
#179386=CARTESIAN_POINT('Ctrl Pts',(46.5590256696716,-5.30722636269027,
133.419944471635));
#179387=CARTESIAN_POINT('Ctrl Pts',(46.5629617191124,-5.34401501237569,
133.345297393831));
#179388=CARTESIAN_POINT('Ctrl Pts',(46.5668977685531,-5.37920155682514,
133.269928624069));
#179389=CARTESIAN_POINT('Ctrl Pts',(46.5708338179938,-5.41275963571393,
133.193913648676));
#179390=CARTESIAN_POINT('Ctrl Pts',(46.5790075004481,-5.48244704303539,
133.036059363562));
#179391=CARTESIAN_POINT('Ctrl Pts',(46.5871811829024,-5.54529049275333,
132.875006885446));
#179392=CARTESIAN_POINT('Ctrl Pts',(46.5953548653567,-5.60101427766594,
132.711339805675));
#179393=CARTESIAN_POINT('Ctrl Pts',(46.6034977581387,-5.65652815509931,
132.548289247991));
#179394=CARTESIAN_POINT('Ctrl Pts',(46.6116406509207,-5.70497578329349,
132.382643967415));
#179395=CARTESIAN_POINT('Ctrl Pts',(46.6197835437026,-5.74613022296392,
132.215005159341));
#179396=CARTESIAN_POINT('Ctrl Pts',(46.6279070867468,-5.78718686844328,
132.04776470687));
#179397=CARTESIAN_POINT('Ctrl Pts',(46.6360306297911,-5.8209848249271,131.878540410804));
#179398=CARTESIAN_POINT('Ctrl Pts',(46.6441541728353,-5.84734612825664,
131.707950025905));
#179399=CARTESIAN_POINT('Ctrl Pts',(46.6522457214236,-5.87360360797701,
131.538031508751));
#179400=CARTESIAN_POINT('Ctrl Pts',(46.6603372700119,-5.89248280272631,
131.366757875198));
#179401=CARTESIAN_POINT('Ctrl Pts',(46.6684288186002,-5.90385647684864,
131.1947569076));
#179402=CARTESIAN_POINT('Ctrl Pts',(46.6744941295062,-5.91238202284796,
131.065827403781));
#179403=CARTESIAN_POINT('Ctrl Pts',(46.6805594404121,-5.91669136066497,
130.936489603205));
#179404=CARTESIAN_POINT('Ctrl Pts',(46.6866247513181,-5.91674940543741,
130.807013117524));
#179405=CARTESIAN_POINT('',(48.4366248414426,-5.9154484603631,130.799233570558));
#179406=CARTESIAN_POINT('Ctrl Pts',(46.6866248077955,-5.90806780525821,
130.807008021674));
#179407=CARTESIAN_POINT('Ctrl Pts',(46.7408436857992,-5.90342285908467,
129.651290948913));
#179408=CARTESIAN_POINT('Ctrl Pts',(46.8878784384072,-5.01664859954711,
126.510550347247));
#179409=CARTESIAN_POINT('Ctrl Pts',(47.1277290656195,0.0905616076009186,
123.806549593712));
#179410=CARTESIAN_POINT('Ctrl Pts',(47.4061766894324,5.9364073636732,127.098064873448));
#179411=CARTESIAN_POINT('Ctrl Pts',(47.6846243132453,6.32698476215336,133.795484879415));
#179412=CARTESIAN_POINT('Ctrl Pts',(47.9630719370583,0.903372254600805,
137.744207813289));
#179413=CARTESIAN_POINT('Ctrl Pts',(48.2137387685748,-4.72645520494283,
135.557858009853));
#179414=CARTESIAN_POINT('Ctrl Pts',(48.3715897254874,-5.9015373895361,132.182661905809));
#179415=CARTESIAN_POINT('Ctrl Pts',(48.4366248077955,-5.91290344989438,
130.799236492267));
#179416=CARTESIAN_POINT('',(50.1866248077955,-5.92098875812942,130.803826647697));
#179417=CARTESIAN_POINT('Ctrl Pts',(48.4366248586207,-5.91674777733439,
130.799232078923));
#179418=CARTESIAN_POINT('Ctrl Pts',(48.445546196015,-5.91658317823966,130.609335619975));
#179419=CARTESIAN_POINT('Ctrl Pts',(48.4544675334093,-5.90727285882511,
130.419839250733));
#179420=CARTESIAN_POINT('Ctrl Pts',(48.4633888708036,-5.88895466743454,
130.231522518797));
#179421=CARTESIAN_POINT('Ctrl Pts',(48.4728185897837,-5.86959261560288,
130.03247457532));
#179422=CARTESIAN_POINT('Ctrl Pts',(48.4822483087638,-5.84016649034169,
129.834744725379));
#179423=CARTESIAN_POINT('Ctrl Pts',(48.4916780277439,-5.80089613338642,
129.639227744387));
#179424=CARTESIAN_POINT('Ctrl Pts',(48.501107746724,-5.76162577643119,129.443710763395));
#179425=CARTESIAN_POINT('Ctrl Pts',(48.5105374657041,-5.71251132052502,
129.250406591543));
#179426=CARTESIAN_POINT('Ctrl Pts',(48.5199671846841,-5.6538287683761,129.060184359161));
#179427=CARTESIAN_POINT('Ctrl Pts',(48.5273904510895,-5.6076326708179,128.910437552264));
#179428=CARTESIAN_POINT('Ctrl Pts',(48.5348137174949,-5.555413339271,128.762300897197));
#179429=CARTESIAN_POINT('Ctrl Pts',(48.5422369839003,-5.49729958532726,
128.616295757545));
#179430=CARTESIAN_POINT('Ctrl Pts',(48.5496514766213,-5.43925451701456,
128.470463183842));
#179431=CARTESIAN_POINT('Ctrl Pts',(48.5570659693423,-5.37532903029584,
128.326757454371));
#179432=CARTESIAN_POINT('Ctrl Pts',(48.5644804620632,-5.3057020395247,128.185686061558));
#179433=CARTESIAN_POINT('Ctrl Pts',(48.571887808417,-5.23614215786867,128.044750638665));
#179434=CARTESIAN_POINT('Ctrl Pts',(48.5792951547707,-5.16089187637648,
127.906444830133));
#179435=CARTESIAN_POINT('Ctrl Pts',(48.5867025011244,-5.08017860467204,
127.771257271629));
#179436=CARTESIAN_POINT('Ctrl Pts',(48.5941043227998,-4.99952553197077,
127.636170541107));
#179437=CARTESIAN_POINT('Ctrl Pts',(48.6015061444752,-4.91341777248504,
127.504197748952));
#179438=CARTESIAN_POINT('Ctrl Pts',(48.6089079661506,-4.82212912031739,
127.375803879012));
#179439=CARTESIAN_POINT('Ctrl Pts',(48.6163058804619,-4.73088865871902,
127.247477787197));
#179440=CARTESIAN_POINT('Ctrl Pts',(48.6237037947732,-4.63447296699451,
127.122727158461));
#179441=CARTESIAN_POINT('Ctrl Pts',(48.6311017090845,-4.53319963213509,
127.001988771243));
#179442=CARTESIAN_POINT('Ctrl Pts',(48.6384983939967,-4.43194312706619,
126.881270448554));
#179443=CARTESIAN_POINT('Ctrl Pts',(48.6458950789088,-4.32583082068225,
126.764563329783));
#179444=CARTESIAN_POINT('Ctrl Pts',(48.653291763821,-4.21522120553785,126.652271896105));
#179445=CARTESIAN_POINT('Ctrl Pts',(48.6606881207564,-4.1046164949397,126.539985441546));
#179446=CARTESIAN_POINT('Ctrl Pts',(48.6680844776919,-3.98951513404839,
126.432114548716));
#179447=CARTESIAN_POINT('Ctrl Pts',(48.6754808346273,-3.87031297639719,
126.329027330845));
#179448=CARTESIAN_POINT('Ctrl Pts',(48.6828783239638,-3.75109256859135,
126.225924330058));
#179449=CARTESIAN_POINT('Ctrl Pts',(48.6902758133004,-3.62777039628237,
126.127606706723));
#179450=CARTESIAN_POINT('Ctrl Pts',(48.697673302637,-3.50077580576758,126.034402617724));
#179451=CARTESIAN_POINT('Ctrl Pts',(48.7050733851519,-3.37373669749576,
125.941165856177));
#179452=CARTESIAN_POINT('Ctrl Pts',(48.7124734676669,-3.2430229086499,125.853046418634));
#179453=CARTESIAN_POINT('Ctrl Pts',(48.7198735501819,-3.10909305848895,
125.770329338744));
#179454=CARTESIAN_POINT('Ctrl Pts',(48.7272817698484,-2.97501593868961,
125.687521302921));
#179455=CARTESIAN_POINT('Ctrl Pts',(48.7346899895148,-2.83771601297265,
125.610127684493));
#179456=CARTESIAN_POINT('Ctrl Pts',(48.7420982091813,-2.69767745426955,
125.538388065869));
#179457=CARTESIAN_POINT('Ctrl Pts',(48.7495109884833,-2.55755270417024,
125.466604292707));
#179458=CARTESIAN_POINT('Ctrl Pts',(48.7569237677852,-2.41468630033689,
125.400481610002));
#179459=CARTESIAN_POINT('Ctrl Pts',(48.7643365470873,-2.26958222659054,
125.340211362719));
#179460=CARTESIAN_POINT('Ctrl Pts',(48.771759918116,-2.12427082133892,125.27985499848));
#179461=CARTESIAN_POINT('Ctrl Pts',(48.7791832891448,-1.97671570973133,
125.22536789989));
#179462=CARTESIAN_POINT('Ctrl Pts',(48.7866066601735,-1.82743663873346,
125.17689174658));
#179463=CARTESIAN_POINT('Ctrl Pts',(48.7905427096146,-1.7482852933807,125.151188526923));
#179464=CARTESIAN_POINT('Ctrl Pts',(48.7944787590558,-1.66864947431325,
125.127174350099));
#179465=CARTESIAN_POINT('Ctrl Pts',(48.7984148084969,-1.58860766791951,
125.104864478439));
#179466=CARTESIAN_POINT('Ctrl Pts',(48.8058380749024,-1.43765131909392,
125.062788756759));
#179467=CARTESIAN_POINT('Ctrl Pts',(48.8132613413078,-1.28479393150785,
125.026650878815));
#179468=CARTESIAN_POINT('Ctrl Pts',(48.8206846077132,-1.13054376892283,
124.996624281518));
#179469=CARTESIAN_POINT('Ctrl Pts',(48.8280991004342,-0.976475917220308,
124.966633173166));
#179470=CARTESIAN_POINT('Ctrl Pts',(48.8355135931552,-0.821018930020202,
124.94273903862));
#179471=CARTESIAN_POINT('Ctrl Pts',(48.8429280858763,-0.664696482650895,
124.925065664219));
#179472=CARTESIAN_POINT('Ctrl Pts',(48.85033543223,-0.508524704741576,124.907409324081));
#179473=CARTESIAN_POINT('Ctrl Pts',(48.8577427785838,-0.351489495762193,
124.895961849281));
#179474=CARTESIAN_POINT('Ctrl Pts',(48.8651501249376,-0.194124879194325,
124.890796033174));
#179475=CARTESIAN_POINT('Ctrl Pts',(48.872551946613,-0.0368776310945197,
124.885634069927));
#179476=CARTESIAN_POINT('Ctrl Pts',(48.8799537682885,0.120698163911409,
124.886744448906));
#179477=CARTESIAN_POINT('Ctrl Pts',(48.8873555899639,0.278063309341962,
124.894148154507));
#179478=CARTESIAN_POINT('Ctrl Pts',(48.8947535042752,0.435345382937171,
124.901547951749));
#179479=CARTESIAN_POINT('Ctrl Pts',(48.9021514185865,0.592416656476129,
124.915234441797));
#179480=CARTESIAN_POINT('Ctrl Pts',(48.9095493328979,0.74873799236339,124.935176519134));
#179481=CARTESIAN_POINT('Ctrl Pts',(48.9169460178101,0.905033350480361,
124.955115282459));
#179482=CARTESIAN_POINT('Ctrl Pts',(48.9243427027223,1.0605786483571,124.981307522652));
#179483=CARTESIAN_POINT('Ctrl Pts',(48.9317393876345,1.21483981054544,125.013670261726));
#179484=CARTESIAN_POINT('Ctrl Pts',(48.9391357445699,1.36909413263219,125.046031565803));
#179485=CARTESIAN_POINT('Ctrl Pts',(48.9465321015054,1.52206406690208,125.084562748093));
#179486=CARTESIAN_POINT('Ctrl Pts',(48.9539284584408,1.67322594076375,125.129129740002));
#179487=CARTESIAN_POINT('Ctrl Pts',(48.9613259477774,1.82441095789421,125.173703555231));
#179488=CARTESIAN_POINT('Ctrl Pts',(48.968723437114,1.97378700535063,125.224314914506));
#179489=CARTESIAN_POINT('Ctrl Pts',(48.9761209264506,2.12084592329109,125.28077997344));
#179490=CARTESIAN_POINT('Ctrl Pts',(48.9835210089656,2.26795639250747,125.337264826113));
#179491=CARTESIAN_POINT('Ctrl Pts',(48.9909210914806,2.41274776671714,125.399607330248));
#179492=CARTESIAN_POINT('Ctrl Pts',(48.9983211739956,2.55473234412884,125.467575704122));
#179493=CARTESIAN_POINT('Ctrl Pts',(49.0057293936621,2.69687304817977,125.53561881621));
#179494=CARTESIAN_POINT('Ctrl Pts',(49.0131376133285,2.83620045485241,125.609299991048));
#179495=CARTESIAN_POINT('Ctrl Pts',(49.020545832995,2.97225128938345,125.68834138038));
#179496=CARTESIAN_POINT('Ctrl Pts',(49.027958612297,3.10838586093301,125.767431418368));
#179497=CARTESIAN_POINT('Ctrl Pts',(49.0353713915991,3.24123952756261,125.851888044962));
#179498=CARTESIAN_POINT('Ctrl Pts',(49.0427841709011,3.37037888976805,125.941390670928));
#179499=CARTESIAN_POINT('Ctrl Pts',(49.0502075419299,3.49970277235025,126.031021182443));
#179500=CARTESIAN_POINT('Ctrl Pts',(49.0576309129587,3.62530145360704,126.125711869107));
#179501=CARTESIAN_POINT('Ctrl Pts',(49.0650542839875,3.74677479852134,126.225102034382));
#179502=CARTESIAN_POINT('Ctrl Pts',(49.0689903334282,3.81118288070779,126.277801084845));
#179503=CARTESIAN_POINT('Ctrl Pts',(49.072926382869,3.87443179320028,126.331820705672));
#179504=CARTESIAN_POINT('Ctrl Pts',(49.0768624323098,3.93646627155632,126.387103113707));
#179505=CARTESIAN_POINT('Ctrl Pts',(49.0842856987152,4.05346136170605,126.491364009955));
#179506=CARTESIAN_POINT('Ctrl Pts',(49.0917089651207,4.16648833363798,126.600433853532));
#179507=CARTESIAN_POINT('Ctrl Pts',(49.0991322315261,4.27512654098774,126.713978774627));
#179508=CARTESIAN_POINT('Ctrl Pts',(49.1065467242471,4.3836363469984,126.827389495055));
#179509=CARTESIAN_POINT('Ctrl Pts',(49.1139612169682,4.48776745793892,126.945264497789));
#179510=CARTESIAN_POINT('Ctrl Pts',(49.1213757096892,4.58713266954996,127.067230109483));
#179511=CARTESIAN_POINT('Ctrl Pts',(49.128783056043,4.68640210922901,127.189078166128));
#179512=CARTESIAN_POINT('Ctrl Pts',(49.1361904023967,4.78091456023954,127.315008695161));
#179513=CARTESIAN_POINT('Ctrl Pts',(49.1435977487505,4.87032012673337,127.444611754089));
#179514=CARTESIAN_POINT('Ctrl Pts',(49.1509995704259,4.95965901118264,127.574118150166));
#179515=CARTESIAN_POINT('Ctrl Pts',(49.1584013921013,5.04389838410333,127.707291316244));
#179516=CARTESIAN_POINT('Ctrl Pts',(49.1658032137767,5.12272914186027,127.84368895363));
#179517=CARTESIAN_POINT('Ctrl Pts',(49.1732011280881,5.20151828547382,127.980014587765));
#179518=CARTESIAN_POINT('Ctrl Pts',(49.1805990423994,5.27490431380218,128.119560980864));
#179519=CARTESIAN_POINT('Ctrl Pts',(49.1879969567108,5.34262197975757,128.26185772791));
#179520=CARTESIAN_POINT('Ctrl Pts',(49.195393641623,5.4103283922654,128.404130827817));
#179521=CARTESIAN_POINT('Ctrl Pts',(49.2027903265353,5.47236815169598,128.549153037798));
#179522=CARTESIAN_POINT('Ctrl Pts',(49.2101870114475,5.52852238895339,128.696430173424));
#179523=CARTESIAN_POINT('Ctrl Pts',(49.2175833683829,5.58467413627307,128.843700778627));
#179524=CARTESIAN_POINT('Ctrl Pts',(49.2249797253184,5.63494074732371,128.993225761867));
#179525=CARTESIAN_POINT('Ctrl Pts',(49.2323760822538,5.67915195998449,129.14449207521));
#179526=CARTESIAN_POINT('Ctrl Pts',(49.2397735715904,5.72336994149479,129.295781547811));
#179527=CARTESIAN_POINT('Ctrl Pts',(49.247171060927,5.7615305739112,129.448812523025));
#179528=CARTESIAN_POINT('Ctrl Pts',(49.2545685502636,5.79351385791696,129.603058099203));
#179529=CARTESIAN_POINT('Ctrl Pts',(49.2619686327786,5.82550835361335,129.757357745929));
#179530=CARTESIAN_POINT('Ctrl Pts',(49.2693687152936,5.85132111373933,129.912872476042));
#179531=CARTESIAN_POINT('Ctrl Pts',(49.2767687978086,5.87088352809197,130.069066688529));
#179532=CARTESIAN_POINT('Ctrl Pts',(49.2841770174751,5.89046745333025,130.22543265261));
#179533=CARTESIAN_POINT('Ctrl Pts',(49.2915852371415,5.90378726074775,130.382479220564));
#179534=CARTESIAN_POINT('Ctrl Pts',(49.2989934568079,5.91082630062458,130.539666442442));
#179535=CARTESIAN_POINT('Ctrl Pts',(49.30640623611,5.917869672913,130.696950410432));
#179536=CARTESIAN_POINT('Ctrl Pts',(49.3138190154121,5.91862457296778,130.854374832421));
#179537=CARTESIAN_POINT('Ctrl Pts',(49.3212317947142,5.91312645857319,131.011401790818));
#179538=CARTESIAN_POINT('Ctrl Pts',(49.328655165743,5.90762048821491,131.168653116698));
#179539=CARTESIAN_POINT('Ctrl Pts',(49.3360785367717,5.8958436868817,131.32550547347));
#179540=CARTESIAN_POINT('Ctrl Pts',(49.3435019078005,5.87788323603809,131.481427250921));
#179541=CARTESIAN_POINT('Ctrl Pts',(49.3474379572412,5.86836017404581,131.564100718616));
#179542=CARTESIAN_POINT('Ctrl Pts',(49.351374006682,5.8570995192712,131.646512744557));
#179543=CARTESIAN_POINT('Ctrl Pts',(49.3553100561227,5.84412001454051,131.728585599996));
#179544=CARTESIAN_POINT('Ctrl Pts',(49.3627333225281,5.81964107369463,131.883372443948));
#179545=CARTESIAN_POINT('Ctrl Pts',(49.3701565889336,5.7889713644415,132.037420151157));
#179546=CARTESIAN_POINT('Ctrl Pts',(49.377579855339,5.75216441127301,132.190194355135));
#179547=CARTESIAN_POINT('Ctrl Pts',(49.38499434806,5.71540096086654,132.342787992691));
#179548=CARTESIAN_POINT('Ctrl Pts',(49.392408840781,5.67251479168054,132.494110763706));
#179549=CARTESIAN_POINT('Ctrl Pts',(49.399823333502,5.62361099232305,132.643634922699));
#179550=CARTESIAN_POINT('Ctrl Pts',(49.4072306798558,5.57475432828858,132.793014964679));
#179551=CARTESIAN_POINT('Ctrl Pts',(49.4146380262096,5.51989169604158,132.940599493412));
#179552=CARTESIAN_POINT('Ctrl Pts',(49.4220453725634,5.45917886455839,133.085872547681));
#179553=CARTESIAN_POINT('Ctrl Pts',(49.4294471942388,5.39851131499548,133.231037251826));
#179554=CARTESIAN_POINT('Ctrl Pts',(49.4368490159141,5.33200239743908,133.373893571248));
#179555=CARTESIAN_POINT('Ctrl Pts',(49.4442508375895,5.25985715224054,133.513942375056));
#179556=CARTESIAN_POINT('Ctrl Pts',(49.4516487519009,5.18774999195535,133.653917248191));
#179557=CARTESIAN_POINT('Ctrl Pts',(49.4590466662122,5.1100126001463,133.791087226305));
#179558=CARTESIAN_POINT('Ctrl Pts',(49.4664445805236,5.02689736934888,133.924974884106));
#179559=CARTESIAN_POINT('Ctrl Pts',(49.4738412654358,4.94379595079495,134.058840292208));
#179560=CARTESIAN_POINT('Ctrl Pts',(49.481237950348,4.85531866367337,134.189424145733));
#179561=CARTESIAN_POINT('Ctrl Pts',(49.4886346352602,4.76176297524727,134.316275185158));
#179562=CARTESIAN_POINT('Ctrl Pts',(49.4960309921956,4.66821143517857,134.443120599875));
#179563=CARTESIAN_POINT('Ctrl Pts',(49.503427349131,4.56958216311505,134.566233229168));
#179564=CARTESIAN_POINT('Ctrl Pts',(49.5108237060665,4.46621476997766,134.685192511752));
#179565=CARTESIAN_POINT('Ctrl Pts',(49.518221195403,4.36283155102836,134.804170007307));
#179566=CARTESIAN_POINT('Ctrl Pts',(49.5256186847396,4.25470901146467,134.918992608217));
#179567=CARTESIAN_POINT('Ctrl Pts',(49.5330161740762,4.14222558600479,135.029274552446));
#179568=CARTESIAN_POINT('Ctrl Pts',(49.5404162565912,4.02970272965449,135.139595155841));
#179569=CARTESIAN_POINT('Ctrl Pts',(49.5478163391062,3.91281621016474,135.245371672274));
#179570=CARTESIAN_POINT('Ctrl Pts',(49.5552164216212,3.79197955834561,135.346256872611));
#179571=CARTESIAN_POINT('Ctrl Pts',(49.5626246412877,3.67101003420549,135.447253006596));
#179572=CARTESIAN_POINT('Ctrl Pts',(49.5700328609541,3.54608199006025,135.543346843867));
#179573=CARTESIAN_POINT('Ctrl Pts',(49.5774410806205,3.41764070151259,135.634232520408));
#179574=CARTESIAN_POINT('Ctrl Pts',(49.5848538599226,3.28912035949482,135.725174135567));
#179575=CARTESIAN_POINT('Ctrl Pts',(49.5922666392247,3.15708277670348,135.810900999753));
#179576=CARTESIAN_POINT('Ctrl Pts',(49.5996794185268,3.0219996842398,135.891152187009));
#179577=CARTESIAN_POINT('Ctrl Pts',(49.6071027895555,2.88672357871883,135.971518040925));
#179578=CARTESIAN_POINT('Ctrl Pts',(49.6145261605842,2.74839359989224,136.046392414594));
#179579=CARTESIAN_POINT('Ctrl Pts',(49.621949531613,2.60750413019932,136.115561307946));
#179580=CARTESIAN_POINT('Ctrl Pts',(49.6258855810538,2.53280115277032,136.152236314887));
#179581=CARTESIAN_POINT('Ctrl Pts',(49.6298216304947,2.4573789223514,136.187308120155));
#179582=CARTESIAN_POINT('Ctrl Pts',(49.6337576799356,2.38131296529585,136.220750478332));
#179583=CARTESIAN_POINT('Ctrl Pts',(49.641180946341,2.23785494422899,136.283821722154));
#179584=CARTESIAN_POINT('Ctrl Pts',(49.6486042127465,2.09167251829583,136.341284975719));
#179585=CARTESIAN_POINT('Ctrl Pts',(49.6560274791519,1.94324419645132,136.392896432559));
#179586=CARTESIAN_POINT('Ctrl Pts',(49.6634419718729,1.79499130455702,136.444446888943));
#179587=CARTESIAN_POINT('Ctrl Pts',(49.6708564645939,1.64449814962074,136.490159194205));
#179588=CARTESIAN_POINT('Ctrl Pts',(49.6782709573149,1.49226554182097,136.529836503044));
#179589=CARTESIAN_POINT('Ctrl Pts',(49.6856783036687,1.34017966153985,136.5694755694));
#179590=CARTESIAN_POINT('Ctrl Pts',(49.6930856500225,1.18635802488163,136.603091125833));
#179591=CARTESIAN_POINT('Ctrl Pts',(49.7004929963763,1.03131892156764,136.630535335554));
#179592=CARTESIAN_POINT('Ctrl Pts',(49.7078948180517,0.87639545226619,136.657959076347));
#179593=CARTESIAN_POINT('Ctrl Pts',(49.7152966397271,0.720256690325655,
136.679220570484));
#179594=CARTESIAN_POINT('Ctrl Pts',(49.7226984614025,0.563433398017768,
136.694222531779));
#179595=CARTESIAN_POINT('Ctrl Pts',(49.7300963757139,0.406692891505404,
136.709216573656));
#179596=CARTESIAN_POINT('Ctrl Pts',(49.7374942900252,0.249268944948803,
136.717957628023));
#179597=CARTESIAN_POINT('Ctrl Pts',(49.7448922043366,0.0916996540967001,
136.720399979837));
#179598=CARTESIAN_POINT('Ctrl Pts',(49.7522888892488,-0.0658434515980862,
136.722841925776));
#179599=CARTESIAN_POINT('Ctrl Pts',(49.759685574161,-0.223531480763051,
136.718987240832));
#179600=CARTESIAN_POINT('Ctrl Pts',(49.7670822590732,-0.380823987658732,
136.708842275842));
#179601=CARTESIAN_POINT('Ctrl Pts',(49.7744786160086,-0.538109520039827,
136.698697760691));
#179602=CARTESIAN_POINT('Ctrl Pts',(49.7818749729441,-0.694999192499319,
136.682263544104));
#179603=CARTESIAN_POINT('Ctrl Pts',(49.7892713298795,-0.850955606919887,
136.65959802672));
#179604=CARTESIAN_POINT('Ctrl Pts',(49.7966688192161,-1.00693589866586,
136.636929039187));
#179605=CARTESIAN_POINT('Ctrl Pts',(49.8040663085527,-1.16198227843079,
136.608026904952));
#179606=CARTESIAN_POINT('Ctrl Pts',(49.8114637978893,-1.31556564047997,
136.573001498058));
#179607=CARTESIAN_POINT('Ctrl Pts',(49.8188638804043,-1.4692028409384,136.537963813063));
#179608=CARTESIAN_POINT('Ctrl Pts',(49.8262639629193,-1.62137563885699,
136.496798664685));
#179609=CARTESIAN_POINT('Ctrl Pts',(49.8336640454343,-1.77156837702499,
136.449666282278));
#179610=CARTESIAN_POINT('Ctrl Pts',(49.8410722651008,-1.92192626754878,
136.40248207297));
#179611=CARTESIAN_POINT('Ctrl Pts',(49.8484804847673,-2.0702993937618,136.349317637552));
#179612=CARTESIAN_POINT('Ctrl Pts',(49.8558887044338,-2.21618974126468,
136.290382272027));
#179613=CARTESIAN_POINT('Ctrl Pts',(49.8633014837358,-2.36216988184215,
136.231410632767));
#179614=CARTESIAN_POINT('Ctrl Pts',(49.8707142630379,-2.50566385928894,
136.166661138954));
#179615=CARTESIAN_POINT('Ctrl Pts',(49.87812704234,-2.64619716702359,136.096389634468));
#179616=CARTESIAN_POINT('Ctrl Pts',(49.8855504133687,-2.78693127533868,
136.026017722762));
#179617=CARTESIAN_POINT('Ctrl Pts',(49.8929737843975,-2.92469593891223,
135.950108221743));
#179618=CARTESIAN_POINT('Ctrl Pts',(49.9003971554262,-3.05904388763994,
135.868961397094));
#179619=CARTESIAN_POINT('Ctrl Pts',(49.904333204867,-3.13027839368957,135.825935403574));
#179620=CARTESIAN_POINT('Ctrl Pts',(49.9082692543077,-3.20055285457639,
135.781437712479));
#179621=CARTESIAN_POINT('Ctrl Pts',(49.9122053037485,-3.26980436544908,
135.735517679979));
#179622=CARTESIAN_POINT('Ctrl Pts',(49.9196099432231,-3.40008282836062,
135.649131243417));
#179623=CARTESIAN_POINT('Ctrl Pts',(49.9270145826977,-3.52713740843895,
135.557444507087));
#179624=CARTESIAN_POINT('Ctrl Pts',(49.9344192221724,-3.65050568465854,
135.460726025132));
#179625=CARTESIAN_POINT('Ctrl Pts',(49.9418150978359,-3.77372794752092,
135.36412201499));
#179626=CARTESIAN_POINT('Ctrl Pts',(49.9492109734994,-3.89327229771408,
135.262498341619));
#179627=CARTESIAN_POINT('Ctrl Pts',(49.956606849163,-4.00870365838643,135.156167775718));
#179628=CARTESIAN_POINT('Ctrl Pts',(49.963995606204,-4.12402391493515,135.049939554311));
#179629=CARTESIAN_POINT('Ctrl Pts',(49.971384363245,-4.23523878823535,134.939013711422));
#179630=CARTESIAN_POINT('Ctrl Pts',(49.978773120286,-4.34194490417043,134.823744278234));
#179631=CARTESIAN_POINT('Ctrl Pts',(49.9861563981161,-4.44857189105712,
134.708560324314));
#179632=CARTESIAN_POINT('Ctrl Pts',(49.9935396759461,-4.55069652350319,
134.589039467391));
#179633=CARTESIAN_POINT('Ctrl Pts',(50.0009229537762,-4.64795116117806,
134.465573608612));
#179634=CARTESIAN_POINT('Ctrl Pts',(50.008660531027,-4.74987273169511,134.336183025985));
#179635=CARTESIAN_POINT('Ctrl Pts',(50.0163981082779,-4.84644505124757,
134.202459754589));
#179636=CARTESIAN_POINT('Ctrl Pts',(50.0241356855287,-4.93729087406291,
134.06489575576));
#179637=CARTESIAN_POINT('Ctrl Pts',(50.0315139282383,-5.02391779979922,
133.933720254881));
#179638=CARTESIAN_POINT('Ctrl Pts',(50.0388921709478,-5.10533787375355,
133.799053048601));
#179639=CARTESIAN_POINT('Ctrl Pts',(50.0462704136574,-5.18126751669558,
133.661351601615));
#179640=CARTESIAN_POINT('Ctrl Pts',(50.0536484892962,-5.25719544030873,
133.5236532727));
#179641=CARTESIAN_POINT('Ctrl Pts',(50.061026564935,-5.3276329986223,133.38292116834));
#179642=CARTESIAN_POINT('Ctrl Pts',(50.0684046405738,-5.39234218173474,
133.239638087914));
#179643=CARTESIAN_POINT('Ctrl Pts',(50.0757840254405,-5.45706284739009,
133.096329582131));
#179644=CARTESIAN_POINT('Ctrl Pts',(50.0831634103072,-5.51605295970531,
132.950469541257));
#179645=CARTESIAN_POINT('Ctrl Pts',(50.090542795174,-5.56912241309877,132.802561335818));
#179646=CARTESIAN_POINT('Ctrl Pts',(50.0979249660981,-5.62221190265312,
132.654597288224));
#179647=CARTESIAN_POINT('Ctrl Pts',(50.1053071370221,-5.66937615664302,
132.504583889727));
#179648=CARTESIAN_POINT('Ctrl Pts',(50.1126893079463,-5.71047479811216,
132.35304010107));
#179649=CARTESIAN_POINT('Ctrl Pts',(50.1200796238243,-5.75161878485249,
132.201329109947));
#179650=CARTESIAN_POINT('Ctrl Pts',(50.1274699397025,-5.78668369838023,
132.048084719622));
#179651=CARTESIAN_POINT('Ctrl Pts',(50.1348602555805,-5.81558005653692,
131.893837174684));
#179652=CARTESIAN_POINT('Ctrl Pts',(50.1422553353984,-5.84449504184223,
131.73949019881));
#179653=CARTESIAN_POINT('Ctrl Pts',(50.1496504152164,-5.86723349559764,
131.584139150302));
#179654=CARTESIAN_POINT('Ctrl Pts',(50.1570454950343,-5.88375782693143,
131.428319267256));
#179655=CARTESIAN_POINT('Ctrl Pts',(50.1644507263577,-5.90030484183908,
131.272285484371));
#179656=CARTESIAN_POINT('Ctrl Pts',(50.171855957681,-5.91062067882276,131.115781955036));
#179657=CARTESIAN_POINT('Ctrl Pts',(50.1792611890044,-5.91471982211213,
130.959344450316));
#179658=CARTESIAN_POINT('Ctrl Pts',(50.1817157286014,-5.91607852504501,
130.907491640724));
#179659=CARTESIAN_POINT('Ctrl Pts',(50.1841702681985,-5.91675464911097,
130.855646046806));
#179660=CARTESIAN_POINT('Ctrl Pts',(50.1866248077955,-5.91674997593985,
130.803827029961));
#179661=CARTESIAN_POINT('',(51.9366241057987,-5.91515969554757,130.80975978087));
#179662=CARTESIAN_POINT('Ctrl Pts',(50.1866248077955,-5.92647345050323,
130.803826153073));
#179663=CARTESIAN_POINT('Ctrl Pts',(50.1879675143841,-5.92650997018912,
130.775433012952));
#179664=CARTESIAN_POINT('Ctrl Pts',(50.1893102209727,-5.92632365013767,
130.747040365475));
#179665=CARTESIAN_POINT('Ctrl Pts',(50.2834688021656,-5.89752915104776,
128.756206350782));
#179666=CARTESIAN_POINT('Ctrl Pts',(50.4691005513741,-3.69725725083763,
124.862319776956));
#179667=CARTESIAN_POINT('Ctrl Pts',(50.7475481751871,3.00074939194039,124.481935163904));
#179668=CARTESIAN_POINT('Ctrl Pts',(51.025995799,6.94121393828233,129.911550675113));
#179669=CARTESIAN_POINT('Ctrl Pts',(51.3044434228129,4.50304197249439,136.161614907245));
#179670=CARTESIAN_POINT('Ctrl Pts',(51.5828910466258,-2.07320558018495,
137.488624163583));
#179671=CARTESIAN_POINT('Ctrl Pts',(51.7936178464117,-5.60823393350386,
133.844292795978));
#179672=CARTESIAN_POINT('Ctrl Pts',(51.9115287715932,-5.91922017290752,
131.343217642334));
#179673=CARTESIAN_POINT('Ctrl Pts',(51.9366238221706,-5.91451815454292,
130.809765226023));
#179674=CARTESIAN_POINT('',(53.686625479034,-5.9116149950419,130.802566075556));
#179675=CARTESIAN_POINT('Ctrl Pts',(51.9366248077955,-5.9167475488552,130.809746303783));
#179676=CARTESIAN_POINT('Ctrl Pts',(51.9439560591643,-5.91688945578099,
130.653846494255));
#179677=CARTESIAN_POINT('Ctrl Pts',(51.951287310533,-5.91086546482152,130.497806767427));
#179678=CARTESIAN_POINT('Ctrl Pts',(51.9586185619018,-5.89866929285895,
130.342158133818));
#179679=CARTESIAN_POINT('Ctrl Pts',(51.9661672174164,-5.88611145026003,
130.181893827313));
#179680=CARTESIAN_POINT('Ctrl Pts',(51.9737158729309,-5.86700965347304,
130.022044579614));
#179681=CARTESIAN_POINT('Ctrl Pts',(51.9812645284455,-5.84141482151809,
129.863189301891));
#179682=CARTESIAN_POINT('Ctrl Pts',(51.9885906513572,-5.81657451923583,
129.709017040682));
#179683=CARTESIAN_POINT('Ctrl Pts',(51.9959167742689,-5.78561867600374,
129.555781372117));
#179684=CARTESIAN_POINT('Ctrl Pts',(52.0032428971806,-5.74864632721248,
129.404004960197));
#179685=CARTESIAN_POINT('Ctrl Pts',(52.010568844207,-5.71167486605228,129.25223219212));
#179686=CARTESIAN_POINT('Ctrl Pts',(52.0178947912334,-5.66868727655011,
129.101918981409));
#179687=CARTESIAN_POINT('Ctrl Pts',(52.0252207382597,-5.61983329325566,
128.953575833072));
#179688=CARTESIAN_POINT('Ctrl Pts',(52.0325480234181,-5.57097038646265,
128.805205588892));
#179689=CARTESIAN_POINT('Ctrl Pts',(52.0398753085765,-5.51623907267722,
128.658806485197));
#179690=CARTESIAN_POINT('Ctrl Pts',(52.0472025937348,-5.45583825678566,
128.514871705539));
#179691=CARTESIAN_POINT('Ctrl Pts',(52.0549179021112,-5.39223885936663,
128.363314725409));
#179692=CARTESIAN_POINT('Ctrl Pts',(52.0626332104877,-5.32235333157764,
128.214490617775));
#179693=CARTESIAN_POINT('Ctrl Pts',(52.0703485188641,-5.24646991932888,
128.068947678341));
#179694=CARTESIAN_POINT('Ctrl Pts',(52.0776870150263,-5.17429261903222,
127.930512991046));
#179695=CARTESIAN_POINT('Ctrl Pts',(52.0850255111885,-5.09668961357051,
127.79504689232));
#179696=CARTESIAN_POINT('Ctrl Pts',(52.0923640073507,-5.01395414508074,
127.662992381665));
#179697=CARTESIAN_POINT('Ctrl Pts',(52.0997074671847,-4.93116271530131,
127.530848550905));
#179698=CARTESIAN_POINT('Ctrl Pts',(52.1070509270187,-4.84323212316322,
127.402121216907));
#179699=CARTESIAN_POINT('Ctrl Pts',(52.1143943868527,-4.75049683159906,
127.277221491381));
#179700=CARTESIAN_POINT('Ctrl Pts',(52.1217476746734,-4.65763742943423,
127.152154608565));
#179701=CARTESIAN_POINT('Ctrl Pts',(52.1291009624941,-4.55996073382341,
127.030925851244));
#179702=CARTESIAN_POINT('Ctrl Pts',(52.1364542503148,-4.45783936112482,
126.913910927247));
#179703=CARTESIAN_POINT('Ctrl Pts',(52.1375649316271,-4.44241438348144,
126.89623634514));
#179704=CARTESIAN_POINT('Ctrl Pts',(52.1386756129393,-4.42688806529473,
126.878657827617));
#179705=CARTESIAN_POINT('Ctrl Pts',(52.1397862942516,-4.41126175718772,
126.861176590403));
#179706=CARTESIAN_POINT('Ctrl Pts',(52.147209560657,-4.30682293506047,126.744340303067));
#179707=CARTESIAN_POINT('Ctrl Pts',(52.1546328270625,-4.19758120997391,
126.631479447753));
#179708=CARTESIAN_POINT('Ctrl Pts',(52.1620560934679,-4.08387109150341,
126.523014162246));
#179709=CARTESIAN_POINT('Ctrl Pts',(52.1694705861889,-3.97029536895008,
126.414677073698));
#179710=CARTESIAN_POINT('Ctrl Pts',(52.1768850789099,-3.85226203288944,
126.310725469028));
#179711=CARTESIAN_POINT('Ctrl Pts',(52.1842995716309,-3.73014534549287,
126.211545983379));
#179712=CARTESIAN_POINT('Ctrl Pts',(52.1917069179847,-3.60814635875687,
126.112462090653));
#179713=CARTESIAN_POINT('Ctrl Pts',(52.1991142643386,-3.48207214368769,
126.018141393914));
#179714=CARTESIAN_POINT('Ctrl Pts',(52.2065216106924,-3.35233317478483,
125.928933164743));
#179715=CARTESIAN_POINT('Ctrl Pts',(52.2139234323678,-3.22269097010012,
125.839791470436));
#179716=CARTESIAN_POINT('Ctrl Pts',(52.2213252540432,-3.08938976024935,
125.755754861952));
#179717=CARTESIAN_POINT('Ctrl Pts',(52.2287270757186,-2.9528723138158,125.677131769465));
#179718=CARTESIAN_POINT('Ctrl Pts',(52.2361249900299,-2.81642693387919,
125.598550181496));
#179719=CARTESIAN_POINT('Ctrl Pts',(52.2435229043413,-2.67676902132893,
125.525376604003));
#179720=CARTESIAN_POINT('Ctrl Pts',(52.2509208186527,-2.53436938430073,
125.457875567889));
#179721=CARTESIAN_POINT('Ctrl Pts',(52.2583175035649,-2.39199341150901,
125.390385749223));
#179722=CARTESIAN_POINT('Ctrl Pts',(52.2657141884771,-2.24687695550852,
125.32856676075));
#179723=CARTESIAN_POINT('Ctrl Pts',(52.2731108733894,-2.09951453323692,
125.272636719248));
#179724=CARTESIAN_POINT('Ctrl Pts',(52.2805072303248,-1.95215864516933,
125.216709157742));
#179725=CARTESIAN_POINT('Ctrl Pts',(52.2879035872603,-1.80255733785183,
125.16667015647));
#179726=CARTESIAN_POINT('Ctrl Pts',(52.2952999441957,-1.65122391773314,
125.122689196584));
#179727=CARTESIAN_POINT('Ctrl Pts',(52.3026974335323,-1.49986732808149,
125.0787015031));
#179728=CARTESIAN_POINT('Ctrl Pts',(52.3100949228689,-1.34677845608772,
125.040773801967));
#179729=CARTESIAN_POINT('Ctrl Pts',(52.3174924122055,-1.19248438540936,
125.009025290507));
#179730=CARTESIAN_POINT('Ctrl Pts',(52.3248924947206,-1.03813622718349,
124.977265649656));
#179731=CARTESIAN_POINT('Ctrl Pts',(52.3322925772356,-0.88258239452695,
124.951689586367));
#179732=CARTESIAN_POINT('Ctrl Pts',(52.3396926597507,-0.726358592244894,
124.932364895669));
#179733=CARTESIAN_POINT('Ctrl Pts',(52.3471008794171,-0.569963005832477,
124.913018955488));
#179734=CARTESIAN_POINT('Ctrl Pts',(52.3545090990836,-0.412896349256926,
124.899938161637));
#179735=CARTESIAN_POINT('Ctrl Pts',(52.36191731875,-0.255698597178542,124.893138342105));
#179736=CARTESIAN_POINT('Ctrl Pts',(52.3693300980521,-0.098404092506292,
124.886334337398));
#179737=CARTESIAN_POINT('Ctrl Pts',(52.3767428773542,0.0590212960175399,
124.88581901139));
#179738=CARTESIAN_POINT('Ctrl Pts',(52.3841556566563,0.216039705387039,
124.891556087718));
#179739=CARTESIAN_POINT('Ctrl Pts',(52.3915790276851,0.37328247002283,124.897301361449));
#179740=CARTESIAN_POINT('Ctrl Pts',(52.3990023987139,0.53011672287545,124.909316851731));
#179741=CARTESIAN_POINT('Ctrl Pts',(52.4064257697426,0.686010987022784,
124.92751456818));
#179742=CARTESIAN_POINT('Ctrl Pts',(52.4103618191833,0.768669866501998,
124.937163434089));
#179743=CARTESIAN_POINT('Ctrl Pts',(52.4142978686239,0.851064660209557,
124.948549492898));
#179744=CARTESIAN_POINT('Ctrl Pts',(52.4182339180645,0.933117668009956,
124.961653883513));
#179745=CARTESIAN_POINT('Ctrl Pts',(52.42565718447,1.08786707994086,124.98636835524));
#179746=CARTESIAN_POINT('Ctrl Pts',(52.4330804508755,1.24186793468851,125.017272463365));
#179747=CARTESIAN_POINT('Ctrl Pts',(52.4405037172809,1.39458594783973,125.054311870243));
#179748=CARTESIAN_POINT('Ctrl Pts',(52.4479182100019,1.54712346098142,125.091307499619));
#179749=CARTESIAN_POINT('Ctrl Pts',(52.4553327027228,1.69838079131768,125.134423906641));
#179750=CARTESIAN_POINT('Ctrl Pts',(52.4627471954438,1.84783035390649,125.183555199685));
#179751=CARTESIAN_POINT('Ctrl Pts',(52.4701545417976,1.99713587138085,125.232639138139));
#179752=CARTESIAN_POINT('Ctrl Pts',(52.4775618881514,2.14463673762683,125.287726305386));
#179753=CARTESIAN_POINT('Ctrl Pts',(52.4849692345052,2.28981722907865,125.348660147423));
#179754=CARTESIAN_POINT('Ctrl Pts',(52.4923710561806,2.43488943944198,125.409548542702));
#179755=CARTESIAN_POINT('Ctrl Pts',(52.499772877856,2.57764437818717,125.476274786242));
#179756=CARTESIAN_POINT('Ctrl Pts',(52.5071746995314,2.71758322703924,125.548633078337));
#179757=CARTESIAN_POINT('Ctrl Pts',(52.5145726138428,2.85744820326268,125.620953173052));
#179758=CARTESIAN_POINT('Ctrl Pts',(52.5219705281541,2.99449971945855,125.698899224199));
#179759=CARTESIAN_POINT('Ctrl Pts',(52.5293684424655,3.1282607349877,125.782218112974));
#179760=CARTESIAN_POINT('Ctrl Pts',(52.5367651273777,3.26199952186255,125.865523155661));
#179761=CARTESIAN_POINT('Ctrl Pts',(52.5441618122898,3.39244857680424,125.954199066723));
#179762=CARTESIAN_POINT('Ctrl Pts',(52.551558497202,3.51915709350606,126.047947692501));
#179763=CARTESIAN_POINT('Ctrl Pts',(52.5589548541375,3.64585999181964,126.141692161367));
#179764=CARTESIAN_POINT('Ctrl Pts',(52.5663512110729,3.76882238158787,126.240508675684));
#179765=CARTESIAN_POINT('Ctrl Pts',(52.5737475680084,3.88762421884382,126.344056984902));
#179766=CARTESIAN_POINT('Ctrl Pts',(52.581145057345,4.00644424496435,126.44762114763));
#179767=CARTESIAN_POINT('Ctrl Pts',(52.5885425466816,4.12110216881211,126.555918302442));
#179768=CARTESIAN_POINT('Ctrl Pts',(52.5959400360182,4.23121280471162,126.668569427994));
#179769=CARTESIAN_POINT('Ctrl Pts',(52.6033401185331,4.34136203972353,126.781260043223));
#179770=CARTESIAN_POINT('Ctrl Pts',(52.6107402010482,4.44696055228445,126.898307401211));
#179771=CARTESIAN_POINT('Ctrl Pts',(52.6181402835632,4.54766174298314,127.019297443205));
#179772=CARTESIAN_POINT('Ctrl Pts',(52.6255485032296,4.64847366499349,127.140420526187));
#179773=CARTESIAN_POINT('Ctrl Pts',(52.632956722896,4.74437727177301,127.26549466413));
#179774=CARTESIAN_POINT('Ctrl Pts',(52.6403649425625,4.83506737729302,127.394074116473));
#179775=CARTESIAN_POINT('Ctrl Pts',(52.6477777218646,4.92581330106,127.522732707324));
#179776=CARTESIAN_POINT('Ctrl Pts',(52.6551905011666,5.01133912725185,127.654900598912));
#179777=CARTESIAN_POINT('Ctrl Pts',(52.6626032804687,5.09138464810678,127.790105663598));
#179778=CARTESIAN_POINT('Ctrl Pts',(52.6700266514975,5.17154454175555,127.92550391562));
#179779=CARTESIAN_POINT('Ctrl Pts',(52.6774500225262,5.24620831404149,128.063947680314));
#179780=CARTESIAN_POINT('Ctrl Pts',(52.684873393555,5.3151627175081,128.20494225014));
#179781=CARTESIAN_POINT('Ctrl Pts',(52.6888094429958,5.35172399676439,128.27970095418));
#179782=CARTESIAN_POINT('Ctrl Pts',(52.6927454924366,5.38668098162346,128.355176470578));
#179783=CARTESIAN_POINT('Ctrl Pts',(52.6966815418774,5.42000754163706,128.431293233125));
#179784=CARTESIAN_POINT('Ctrl Pts',(52.7041048082828,5.48286039373613,128.574847071766));
#179785=CARTESIAN_POINT('Ctrl Pts',(52.7115280746882,5.54010111599179,128.721116777712));
#179786=CARTESIAN_POINT('Ctrl Pts',(52.7189513410937,5.59148663042751,128.86962347153));
#179787=CARTESIAN_POINT('Ctrl Pts',(52.7263658338147,5.64281141145248,129.017954642769));
#179788=CARTESIAN_POINT('Ctrl Pts',(52.7337803265356,5.68829463881708,129.168517189784));
#179789=CARTESIAN_POINT('Ctrl Pts',(52.7411948192566,5.72774022959643,129.32081000341));
#179790=CARTESIAN_POINT('Ctrl Pts',(52.7486021656104,5.76714780123039,129.472956031489));
#179791=CARTESIAN_POINT('Ctrl Pts',(52.7560095119642,5.80052922839119,129.626828647179));
#179792=CARTESIAN_POINT('Ctrl Pts',(52.763416858318,5.82773746320924,129.781909336376));
#179793=CARTESIAN_POINT('Ctrl Pts',(52.7708186799934,5.85492540509926,129.936874360544));
#179794=CARTESIAN_POINT('Ctrl Pts',(52.7782205016688,5.87594925799897,130.093045298053));
#179795=CARTESIAN_POINT('Ctrl Pts',(52.7856223233442,5.89071254356778,130.249891239193));
#179796=CARTESIAN_POINT('Ctrl Pts',(52.7930202376556,5.90546803571309,130.406654382583));
#179797=CARTESIAN_POINT('Ctrl Pts',(52.8004181519669,5.91396950750976,130.564091449242));
#179798=CARTESIAN_POINT('Ctrl Pts',(52.8078160662783,5.91617206285784,130.721664274476));
#179799=CARTESIAN_POINT('Ctrl Pts',(52.8152127511905,5.91837425218116,130.879210913964));
#179800=CARTESIAN_POINT('Ctrl Pts',(52.8226094361027,5.91427959736362,131.036892894355));
#179801=CARTESIAN_POINT('Ctrl Pts',(52.8300061210149,5.90389527170223,131.194169780198));
#179802=CARTESIAN_POINT('Ctrl Pts',(52.8374024779504,5.89351140649271,131.35143969222));
#179803=CARTESIAN_POINT('Ctrl Pts',(52.8447988348858,5.87683844956178,131.508304172924));
#179804=CARTESIAN_POINT('Ctrl Pts',(52.8521951918212,5.8539356193096,131.66422591369));
#179805=CARTESIAN_POINT('Ctrl Pts',(52.8595926811578,5.83102928257562,131.820171526473));
#179806=CARTESIAN_POINT('Ctrl Pts',(52.8669901704944,5.80189122761264,131.975173742568));
#179807=CARTESIAN_POINT('Ctrl Pts',(52.874387659831,5.76663213354565,132.128703624063));
#179808=CARTESIAN_POINT('Ctrl Pts',(52.881787742346,5.731360679458,132.28228732522));
#179809=CARTESIAN_POINT('Ctrl Pts',(52.8891878248609,5.68996399765501,132.434397300576));
#179810=CARTESIAN_POINT('Ctrl Pts',(52.8965879073759,5.64260310204595,132.584518137361));
#179811=CARTESIAN_POINT('Ctrl Pts',(52.9039961270424,5.59519012826335,132.734804047438));
#179812=CARTESIAN_POINT('Ctrl Pts',(52.9114043467088,5.54179995576858,132.883096094616));
#179813=CARTESIAN_POINT('Ctrl Pts',(52.9188125663753,5.48264263821576,133.028896583586));
#179814=CARTESIAN_POINT('Ctrl Pts',(52.9262253456773,5.42344891032091,133.174786810325));
#179815=CARTESIAN_POINT('Ctrl Pts',(52.9336381249794,5.35848111807983,133.318182083901));
#179816=CARTESIAN_POINT('Ctrl Pts',(52.9410509042814,5.28799582719607,133.458608287633));
#179817=CARTESIAN_POINT('Ctrl Pts',(52.9484742753102,5.21740982362327,133.59923513891));
#179818=CARTESIAN_POINT('Ctrl Pts',(52.955897646339,5.14129075613998,133.736884121616));
#179819=CARTESIAN_POINT('Ctrl Pts',(52.9633210173677,5.05993957075007,133.871108423118));
#179820=CARTESIAN_POINT('Ctrl Pts',(52.9672570668085,5.01680522026109,133.942277368443));
#179821=CARTESIAN_POINT('Ctrl Pts',(52.9711931162494,4.97220063492622,134.012484030043));
#179822=CARTESIAN_POINT('Ctrl Pts',(52.9751291656902,4.92617526658991,134.081665578252));
#179823=CARTESIAN_POINT('Ctrl Pts',(52.9825524320956,4.83937285831089,134.212139819091));
#179824=CARTESIAN_POINT('Ctrl Pts',(52.9899756985011,4.74725202068656,134.339360408767));
#179825=CARTESIAN_POINT('Ctrl Pts',(52.9973989649065,4.6500842589625,134.462863992862));
#179826=CARTESIAN_POINT('Ctrl Pts',(53.0048134576275,4.55303134146338,134.586221605976));
#179827=CARTESIAN_POINT('Ctrl Pts',(53.0122279503485,4.45094360188705,134.705870667667));
#179828=CARTESIAN_POINT('Ctrl Pts',(53.0196424430696,4.34413664995451,134.821375346071));
#179829=CARTESIAN_POINT('Ctrl Pts',(53.0270497894233,4.23743264258361,134.936768696717));
#179830=CARTESIAN_POINT('Ctrl Pts',(53.0344571357771,4.12601872987208,135.048025344126));
#179831=CARTESIAN_POINT('Ctrl Pts',(53.0418644821309,4.01025166945499,135.154741303223));
#179832=CARTESIAN_POINT('Ctrl Pts',(53.0492663038063,3.89457095247904,135.261377669531));
#179833=CARTESIAN_POINT('Ctrl Pts',(53.0566681254817,3.77454382579025,135.363479838813));
#179834=CARTESIAN_POINT('Ctrl Pts',(53.0640699471571,3.65056480986416,135.460679671441));
#179835=CARTESIAN_POINT('Ctrl Pts',(53.0714678614684,3.52665124149642,135.557828193034));
#179836=CARTESIAN_POINT('Ctrl Pts',(53.0788657757797,3.39879023163356,135.650079302173));
#179837=CARTESIAN_POINT('Ctrl Pts',(53.086263690091,3.26741028603743,135.737104335336));
#179838=CARTESIAN_POINT('Ctrl Pts',(53.0936603750032,3.13605217340384,135.824114906517));
#179839=CARTESIAN_POINT('Ctrl Pts',(53.1010570599155,3.00117659656919,135.90590091945));
#179840=CARTESIAN_POINT('Ctrl Pts',(53.1084537448277,2.8632421165247,135.982176290672));
#179841=CARTESIAN_POINT('Ctrl Pts',(53.1158501017631,2.7253137526396,136.058448279764));
#179842=CARTESIAN_POINT('Ctrl Pts',(53.1232464586986,2.58432708190977,136.129209932343));
#179843=CARTESIAN_POINT('Ctrl Pts',(53.130642815634,2.4407661662857,136.194220642095));
#179844=CARTESIAN_POINT('Ctrl Pts',(53.1380403049706,2.29718327111916,136.259241305152));
#179845=CARTESIAN_POINT('Ctrl Pts',(53.1454377943071,2.1510256863835,136.318509118218));
#179846=CARTESIAN_POINT('Ctrl Pts',(53.1528352836437,2.00279824729528,136.371831294914));
#179847=CARTESIAN_POINT('Ctrl Pts',(53.1602353661587,1.85451884730828,136.425172163616));
#179848=CARTESIAN_POINT('Ctrl Pts',(53.1676354486737,1.70416849937797,136.472563119973));
#179849=CARTESIAN_POINT('Ctrl Pts',(53.1750355311887,1.5522678668175,136.513861036354));
#179850=CARTESIAN_POINT('Ctrl Pts',(53.1824437508552,1.40020020389534,136.55520436404));
#179851=CARTESIAN_POINT('Ctrl Pts',(53.1898519705216,1.24657921239373,136.590441173567));
#179852=CARTESIAN_POINT('Ctrl Pts',(53.1972601901881,1.09193715660315,136.619479172551));
#179853=CARTESIAN_POINT('Ctrl Pts',(53.2046729694902,0.937199921207133,
136.648535043939));
#179854=CARTESIAN_POINT('Ctrl Pts',(53.2120857487923,0.781440737749198,
136.671384448335));
#179855=CARTESIAN_POINT('Ctrl Pts',(53.2194985280944,0.62519717405066,136.687986970085));
#179856=CARTESIAN_POINT('Ctrl Pts',(53.2269218991231,0.468730362221436,
136.704613214297));
#179857=CARTESIAN_POINT('Ctrl Pts',(53.2343452701519,0.311778159362604,
136.714974724435));
#179858=CARTESIAN_POINT('Ctrl Pts',(53.2417686411807,0.154879150262876,
136.719083181754));
#179859=CARTESIAN_POINT('Ctrl Pts',(53.2457046906215,0.0716875308978307,
136.721261584405));
#179860=CARTESIAN_POINT('Ctrl Pts',(53.2496407400623,-0.0114891897633528,
136.721682898984));
#179861=CARTESIAN_POINT('Ctrl Pts',(53.2535767895031,-0.0945714214127198,
136.720354769756));
#179862=CARTESIAN_POINT('Ctrl Pts',(53.2610000559085,-0.251261917394923,
136.717849959484));
#179863=CARTESIAN_POINT('Ctrl Pts',(53.268423322314,-0.408089765475678,
136.709111926048));
#179864=CARTESIAN_POINT('Ctrl Pts',(53.2758465887194,-0.564518377244247,
136.694118640121));
#179865=CARTESIAN_POINT('Ctrl Pts',(53.2832610814404,-0.72076210338496,
136.679143075013));
#179866=CARTESIAN_POINT('Ctrl Pts',(53.2906755741615,-0.87660716449545,
136.657927008867));
#179867=CARTESIAN_POINT('Ctrl Pts',(53.2980900668825,-1.03151628812405,
136.630500395312));
#179868=CARTESIAN_POINT('Ctrl Pts',(53.3054974132363,-1.18627610450663,
136.60310021656));
#179869=CARTESIAN_POINT('Ctrl Pts',(53.3129047595901,-1.34010141418094,
136.569501471909));
#179870=CARTESIAN_POINT('Ctrl Pts',(53.3203121059439,-1.49245949684531,
136.52978594786));
#179871=CARTESIAN_POINT('Ctrl Pts',(53.3277139276193,-1.64470394510392,
136.490100045148));
#179872=CARTESIAN_POINT('Ctrl Pts',(53.3351157492948,-1.79548298560572,
136.444306540601));
#179873=CARTESIAN_POINT('Ctrl Pts',(53.3425175709702,-1.94427364410263,
136.392538367007));
#179874=CARTESIAN_POINT('Ctrl Pts',(53.3499154852815,-2.09298575716804,
136.34079752143));
#179875=CARTESIAN_POINT('Ctrl Pts',(53.3573133995928,-2.23971122698436,
136.283088410468));
#179876=CARTESIAN_POINT('Ctrl Pts',(53.3647113139041,-2.38394192178945,
136.219593897494));
#179877=CARTESIAN_POINT('Ctrl Pts',(53.3721079988163,-2.52814864807028,
136.156109936155));
#179878=CARTESIAN_POINT('Ctrl Pts',(53.3795046837286,-2.66986108084924,
136.086842631213));
#179879=CARTESIAN_POINT('Ctrl Pts',(53.3869013686408,-2.8085906665899,136.012023147919));
#179880=CARTESIAN_POINT('Ctrl Pts',(53.3942977255762,-2.94731410091516,
135.937206982199));
#179881=CARTESIAN_POINT('Ctrl Pts',(53.4016940825117,-3.08305462262472,
135.856839304833));
#179882=CARTESIAN_POINT('Ctrl Pts',(53.4090904394471,-3.21534815550256,
135.771197317258));
#179883=CARTESIAN_POINT('Ctrl Pts',(53.4164879287837,-3.34766194285783,
135.685542217676));
#179884=CARTESIAN_POINT('Ctrl Pts',(53.4238854181202,-3.47652737718893,
135.594611402899));
#179885=CARTESIAN_POINT('Ctrl Pts',(53.4312829074568,-3.60150938608916,
135.498725399346));
#179886=CARTESIAN_POINT('Ctrl Pts',(53.4386829899718,-3.72653520723922,
135.402805783102));
#179887=CARTESIAN_POINT('Ctrl Pts',(53.4460830724868,-3.84767459657205,
135.301927746744));
#179888=CARTESIAN_POINT('Ctrl Pts',(53.4534831550018,-3.96452570551961,
135.196451975083));
#179889=CARTESIAN_POINT('Ctrl Pts',(53.4608913746683,-4.08150530427405,
135.090860221967));
#179890=CARTESIAN_POINT('Ctrl Pts',(53.4682995943347,-4.19418692839497,
134.980660887301));
#179891=CARTESIAN_POINT('Ctrl Pts',(53.4757078140012,-4.30220522783594,
134.866251893817));
#179892=CARTESIAN_POINT('Ctrl Pts',(53.4831205933033,-4.41029001073799,
134.751772483506));
#179893=CARTESIAN_POINT('Ctrl Pts',(53.4905333726054,-4.51370550507364,
134.633078532338));
#179894=CARTESIAN_POINT('Ctrl Pts',(53.4979461519075,-4.61212713946999,
134.510600465696));
#179895=CARTESIAN_POINT('Ctrl Pts',(53.5053695229362,-4.7106894033128,134.387947396649));
#179896=CARTESIAN_POINT('Ctrl Pts',(53.5127928939649,-4.8042433346608,134.26149971259));
#179897=CARTESIAN_POINT('Ctrl Pts',(53.5202162649937,-4.89250764304995,
134.13171685416));
#179898=CARTESIAN_POINT('Ctrl Pts',(53.5241523144345,-4.93930749723082,
134.062902868523));
#179899=CARTESIAN_POINT('Ctrl Pts',(53.5280883638753,-4.9846210103391,133.993151668565));
#179900=CARTESIAN_POINT('Ctrl Pts',(53.532024413316,-5.02841159320816,133.922534347779));
#179901=CARTESIAN_POINT('Ctrl Pts',(53.5396620524379,-5.11338427302963,
133.785506187936));
#179902=CARTESIAN_POINT('Ctrl Pts',(53.5472996915599,-5.1928647323864,133.644820790303));
#179903=CARTESIAN_POINT('Ctrl Pts',(53.5549373306818,-5.26653292943453,
133.500943912345));
#179904=CARTESIAN_POINT('Ctrl Pts',(53.5625643034415,-5.34009824499512,
133.357267965967));
#179905=CARTESIAN_POINT('Ctrl Pts',(53.5701912762012,-5.40786731261599,
133.21040972157));
#179906=CARTESIAN_POINT('Ctrl Pts',(53.5778182489609,-5.46956365958501,
133.060863207028));
#179907=CARTESIAN_POINT('Ctrl Pts',(53.5854357124241,-5.53118308365448,
132.911503146823));
#179908=CARTESIAN_POINT('Ctrl Pts',(53.5930531758872,-5.58674474131301,
132.759461810151));
#179909=CARTESIAN_POINT('Ctrl Pts',(53.6006706393504,-5.63601825436551,
132.60525728283));
#179910=CARTESIAN_POINT('Ctrl Pts',(53.608277176095,-5.68522108800988,132.451273951118));
#179911=CARTESIAN_POINT('Ctrl Pts',(53.6158837128396,-5.72815365873106,
132.295133942283));
#179912=CARTESIAN_POINT('Ctrl Pts',(53.6234902495842,-5.76463396731877,
132.137374415445));
#179913=CARTESIAN_POINT('Ctrl Pts',(53.631090387928,-5.80108358971582,131.979747591401));
#179914=CARTESIAN_POINT('Ctrl Pts',(53.6386905262718,-5.83109168432949,
131.82050429686));
#179915=CARTESIAN_POINT('Ctrl Pts',(53.6462906646155,-5.85452601886792,
131.660196850089));
#179916=CARTESIAN_POINT('Ctrl Pts',(53.6538841673983,-5.8779398932582,131.500029365223));
#179917=CARTESIAN_POINT('Ctrl Pts',(53.6614776701811,-5.89479140087716,
131.33879992004));
#179918=CARTESIAN_POINT('Ctrl Pts',(53.6690711729639,-5.90499937150216,
131.177070940819));
#179919=CARTESIAN_POINT('Ctrl Pts',(53.6749223845744,-5.91286517440627,
131.052449865664));
#179920=CARTESIAN_POINT('Ctrl Pts',(53.680773596185,-5.91678736038817,130.927532467533));
#179921=CARTESIAN_POINT('Ctrl Pts',(53.6866248077955,-5.91674973171695,
130.802578841105));
#179922=CARTESIAN_POINT('',(55.4366248077955,-5.92106340457748,130.79959340511));
#179923=CARTESIAN_POINT('Ctrl Pts',(53.686626026497,-5.90742709745722,130.802555663958));
#179924=CARTESIAN_POINT('Ctrl Pts',(53.727908030041,-5.90978532495469,129.922359697697));
#179925=CARTESIAN_POINT('Ctrl Pts',(53.8620059081893,-5.31185327642548,
127.066239178578));
#179926=CARTESIAN_POINT('Ctrl Pts',(54.0889196609419,-0.882245562582123,
123.861796012345));
#179927=CARTESIAN_POINT('Ctrl Pts',(54.3673672847546,5.36410094939406,126.309476688583));
#179928=CARTESIAN_POINT('Ctrl Pts',(54.6458149085676,6.68110073978089,132.887736108264));
#179929=CARTESIAN_POINT('Ctrl Pts',(54.9242625323805,1.858495340223,137.551475230548));
#179930=CARTESIAN_POINT('Ctrl Pts',(55.1878658321232,-4.32383043540707,
136.096859582895));
#179931=CARTESIAN_POINT('Ctrl Pts',(55.3586532572615,-5.90657959716367,
132.452360893221));
#179932=CARTESIAN_POINT('Ctrl Pts',(55.4366248077955,-5.92106340457748,
130.79959340511));
#179933=CARTESIAN_POINT('',(57.1866248077955,-5.92031730829855,130.808402304245));
#179934=CARTESIAN_POINT('Ctrl Pts',(55.4366248077955,-5.92106340457748,
130.79959340511));
#179935=CARTESIAN_POINT('Ctrl Pts',(55.4514691318657,-5.92382085046061,
130.48493740509));
#179936=CARTESIAN_POINT('Ctrl Pts',(55.5591293305407,-5.75767852999927,
128.205775126642));
#179937=CARTESIAN_POINT('Ctrl Pts',(55.7596054038189,-2.79713074682738,
124.389251879948));
#179938=CARTESIAN_POINT('Ctrl Pts',(56.0380530276321,3.88529517390352,124.983532330973));
#179939=CARTESIAN_POINT('Ctrl Pts',(56.3165006514451,6.99732463703978,130.926869614113));
#179940=CARTESIAN_POINT('Ctrl Pts',(56.5949482752577,3.6791545970478,136.757627114317));
#179941=CARTESIAN_POINT('Ctrl Pts',(56.8733958990709,-3.01997878093501,
137.117623537249));
#179942=CARTESIAN_POINT('Ctrl Pts',(57.0706214099165,-5.7993065312336,133.263329052102));
#179943=CARTESIAN_POINT('Ctrl Pts',(57.1750310461582,-5.92485864146025,
131.053955056992));
#179944=CARTESIAN_POINT('Ctrl Pts',(57.1866248077955,-5.9229396490959,130.808404094467));
#179945=CARTESIAN_POINT('',(58.9366247815215,-5.91201869214909,130.807184091162));
#179946=CARTESIAN_POINT('Ctrl Pts',(57.1866248077955,-5.91674862124091,
130.808399867971));
#179947=CARTESIAN_POINT('Ctrl Pts',(57.1939380426069,-5.91685425135328,
130.653671450818));
#179948=CARTESIAN_POINT('Ctrl Pts',(57.2012512774183,-5.91088629876316,
130.498704782712));
#179949=CARTESIAN_POINT('Ctrl Pts',(57.2085645122297,-5.89881522288282,
130.344024296181));
#179950=CARTESIAN_POINT('Ctrl Pts',(57.2158702793011,-5.88675647310165,
130.189501758042));
#179951=CARTESIAN_POINT('Ctrl Pts',(57.2231760463724,-5.86860702960594,
130.035265200377));
#179952=CARTESIAN_POINT('Ctrl Pts',(57.2304818134437,-5.84438936097259,
129.881840395646));
#179953=CARTESIAN_POINT('Ctrl Pts',(57.2377818193403,-5.82019078988507,
129.728536578501));
#179954=CARTESIAN_POINT('Ctrl Pts',(57.2450818252368,-5.78993357634959,
129.576043618411));
#179955=CARTESIAN_POINT('Ctrl Pts',(57.2523818311334,-5.75369209415274,
129.4248832353));
#179956=CARTESIAN_POINT('Ctrl Pts',(57.2597947192818,-5.71689019869302,
129.271385412372));
#179957=CARTESIAN_POINT('Ctrl Pts',(57.2672076074303,-5.67391745113027,
129.119262122311));
#179958=CARTESIAN_POINT('Ctrl Pts',(57.2746204955787,-5.62490602073945,
128.96905061096));
#179959=CARTESIAN_POINT('Ctrl Pts',(57.281915036378,-5.57667706173495,128.82123723834));
#179960=CARTESIAN_POINT('Ctrl Pts',(57.2892095771774,-5.52260093667172,
128.675275429644));
#179961=CARTESIAN_POINT('Ctrl Pts',(57.2965041179767,-5.46285411060139,
128.53166276506));
#179962=CARTESIAN_POINT('Ctrl Pts',(57.3037983637164,-5.40310970125243,
128.388055909517));
#179963=CARTESIAN_POINT('Ctrl Pts',(57.3110926094561,-5.33769519475609,
128.246798364337));
#179964=CARTESIAN_POINT('Ctrl Pts',(57.3183868551958,-5.26683529508206,
128.108367936386));
#179965=CARTESIAN_POINT('Ctrl Pts',(57.3256823401667,-5.19596335690571,
127.969913990266));
#179966=CARTESIAN_POINT('Ctrl Pts',(57.3329778251376,-5.11964436033471,
127.834288459341));
#179967=CARTESIAN_POINT('Ctrl Pts',(57.3402733101084,-5.03814892406815,
127.701944465369));
#179968=CARTESIAN_POINT('Ctrl Pts',(57.3477747964908,-4.95435231454629,
127.565863495766));
#179969=CARTESIAN_POINT('Ctrl Pts',(57.3552762828731,-4.86508283881317,
127.433252493631));
#179970=CARTESIAN_POINT('Ctrl Pts',(57.3627777692554,-4.77068175052153,
127.304571167079));
#179971=CARTESIAN_POINT('Ctrl Pts',(57.370084061884,-4.6787370424514,127.179238215753));
#179972=CARTESIAN_POINT('Ctrl Pts',(57.3773903545127,-4.58192475377393,
127.057633233637));
#179973=CARTESIAN_POINT('Ctrl Pts',(57.3846966471413,-4.48059993087497,
126.940145972655));
#179974=CARTESIAN_POINT('Ctrl Pts',(57.3922957304005,-4.37521464115621,
126.817950555159));
#179975=CARTESIAN_POINT('Ctrl Pts',(57.3998948136597,-4.26494798228707,
126.700210065349));
#179976=CARTESIAN_POINT('Ctrl Pts',(57.4074938969189,-4.15023953349525,
126.587318718662));
#179977=CARTESIAN_POINT('Ctrl Pts',(57.4150929801781,-4.03553108470327,
126.474427371975));
#179978=CARTESIAN_POINT('Ctrl Pts',(57.4226920634373,-3.91638123640206,
126.366385422119));
#179979=CARTESIAN_POINT('Ctrl Pts',(57.4302911466965,-3.79326491482562,
126.26353780133));
#179980=CARTESIAN_POINT('Ctrl Pts',(57.437714413102,-3.67299708478074,126.163069723505));
#179981=CARTESIAN_POINT('Ctrl Pts',(57.4451376795074,-3.54855315606726,
126.067231131235));
#179982=CARTESIAN_POINT('Ctrl Pts',(57.4525609459128,-3.42032499192752,
125.976389251444));
#179983=CARTESIAN_POINT('Ctrl Pts',(57.4599754386338,-3.29224838282892,
125.885654739211));
#179984=CARTESIAN_POINT('Ctrl Pts',(57.4673899313548,-3.16039674277302,
125.799905397816));
#179985=CARTESIAN_POINT('Ctrl Pts',(57.4748044240758,-3.02519641289154,
125.719469544403));
#179986=CARTESIAN_POINT('Ctrl Pts',(57.4822117704296,-2.89012639417781,
125.639111218095));
#179987=CARTESIAN_POINT('Ctrl Pts',(57.4896191167834,-2.75171442980218,
125.564056373772));
#179988=CARTESIAN_POINT('Ctrl Pts',(57.4970264631372,-2.6104172763789,125.494591111676));
#179989=CARTESIAN_POINT('Ctrl Pts',(57.5044282848126,-2.46922550770409,
125.425177659393));
#179990=CARTESIAN_POINT('Ctrl Pts',(57.511830106488,-2.32515316823143,125.361345652437));
#179991=CARTESIAN_POINT('Ctrl Pts',(57.5192319281634,-2.17868304917881,
125.303336100831));
#179992=CARTESIAN_POINT('Ctrl Pts',(57.5266298424747,-2.03229025056129,
125.245357172015));
#179993=CARTESIAN_POINT('Ctrl Pts',(57.5340277567861,-1.88350253939427,
125.193194714378));
#179994=CARTESIAN_POINT('Ctrl Pts',(57.5414256710974,-1.73282408874509,
125.14704223869));
#179995=CARTESIAN_POINT('Ctrl Pts',(57.5488223560096,-1.58217067812126,
125.100897432707));
#179996=CARTESIAN_POINT('Ctrl Pts',(57.5562190409218,-1.42962750820282,
125.060760735669));
#179997=CARTESIAN_POINT('Ctrl Pts',(57.563615725834,-1.27571548442838,125.026776298381));
#179998=CARTESIAN_POINT('Ctrl Pts',(57.5710120827695,-1.12181028527413,
124.992793367999));
#179999=CARTESIAN_POINT('Ctrl Pts',(57.578408439705,-0.966536717466216,
124.964962235441));
#180000=CARTESIAN_POINT('Ctrl Pts',(57.5858047966404,-0.810427229520558,
124.943376206381));
#180001=CARTESIAN_POINT('Ctrl Pts',(57.593202285977,-0.65429384081399,124.921786872445));
#180002=CARTESIAN_POINT('Ctrl Pts',(57.6005997753136,-0.497324646944804,
124.906444596948));
#180003=CARTESIAN_POINT('Ctrl Pts',(57.6079972646502,-0.340058441262998,
124.897390935993));
#180004=CARTESIAN_POINT('Ctrl Pts',(57.6153973471651,-0.182737106157256,
124.888334101291));
#180005=CARTESIAN_POINT('Ctrl Pts',(57.6227974296801,-0.0251189243910171,
124.885570291646));
#180006=CARTESIAN_POINT('Ctrl Pts',(57.630197512195,0.132256229568732,124.889088954131));
#180007=CARTESIAN_POINT('Ctrl Pts',(57.6376057318615,0.289804433689493,
124.892611485747));
#180008=CARTESIAN_POINT('Ctrl Pts',(57.645013951528,0.447108702886177,124.902430277321));
#180009=CARTESIAN_POINT('Ctrl Pts',(57.6524221711944,0.603632468775904,
124.918482738682));
#180010=CARTESIAN_POINT('Ctrl Pts',(57.6598349504965,0.760252572432243,
124.934545080065));
#180011=CARTESIAN_POINT('Ctrl Pts',(57.6672477297986,0.916090846875104,
124.956848683615));
#180012=CARTESIAN_POINT('Ctrl Pts',(57.6746605091007,1.07062036384995,124.985279710841));
#180013=CARTESIAN_POINT('Ctrl Pts',(57.6820838801294,1.22537067984492,125.013751361652));
#180014=CARTESIAN_POINT('Ctrl Pts',(57.6895072511581,1.37880814035333,125.048367840201));
#180015=CARTESIAN_POINT('Ctrl Pts',(57.6969306221869,1.53041962999226,125.08896506532));
#180016=CARTESIAN_POINT('Ctrl Pts',(57.7008666716277,1.61080767966777,125.110490688195));
#180017=CARTESIAN_POINT('Ctrl Pts',(57.7048027210686,1.69068268387806,125.133696895736));
#180018=CARTESIAN_POINT('Ctrl Pts',(57.7087387705094,1.76997049597375,125.158553765939));
#180019=CARTESIAN_POINT('Ctrl Pts',(57.7161620369149,1.91950483509634,125.205433047384));
#180020=CARTESIAN_POINT('Ctrl Pts',(57.7235853033203,2.06740154024459,125.258328148936));
#180021=CARTESIAN_POINT('Ctrl Pts',(57.7310085697257,2.21313984135335,125.317107880074));
#180022=CARTESIAN_POINT('Ctrl Pts',(57.7384230624467,2.35870589189342,125.375818138451));
#180023=CARTESIAN_POINT('Ctrl Pts',(57.7458375551678,2.50211827346222,125.440399043895));
#180024=CARTESIAN_POINT('Ctrl Pts',(57.7532520478888,2.64287031575285,125.510669366972));
#180025=CARTESIAN_POINT('Ctrl Pts',(57.7606593942426,2.7834866959255,125.580871960867));
#180026=CARTESIAN_POINT('Ctrl Pts',(57.7680667405963,2.92144750976236,125.656752889853));
#180027=CARTESIAN_POINT('Ctrl Pts',(57.7754740869501,3.05626516492244,125.738082515825));
#180028=CARTESIAN_POINT('Ctrl Pts',(57.7828759086255,3.19098226798874,125.819351483093));
#180029=CARTESIAN_POINT('Ctrl Pts',(57.7902777303009,3.32256056190424,125.906060863689));
#180030=CARTESIAN_POINT('Ctrl Pts',(57.7976795519763,3.45053631766601,125.997934743492));
#180031=CARTESIAN_POINT('Ctrl Pts',(57.8050774662877,3.57844451602229,126.089760123789));
#180032=CARTESIAN_POINT('Ctrl Pts',(57.812475380599,3.70275366117676,126.186744356588));
#180033=CARTESIAN_POINT('Ctrl Pts',(57.8198732949103,3.82302842918003,126.288567864108));
#180034=CARTESIAN_POINT('Ctrl Pts',(57.8272699798225,3.94328320969938,126.390374450409));
#180035=CARTESIAN_POINT('Ctrl Pts',(57.8346666647347,4.05950465906293,126.497018474366));
#180036=CARTESIAN_POINT('Ctrl Pts',(57.8420633496469,4.17128993700269,126.608139600513));
#180037=CARTESIAN_POINT('Ctrl Pts',(57.8494597065824,4.28307025826609,126.719255799432));
#180038=CARTESIAN_POINT('Ctrl Pts',(57.8568560635178,4.39041453447414,126.834848442644));
#180039=CARTESIAN_POINT('Ctrl Pts',(57.8642524204533,4.492956463491,126.954520000128));
#180040=CARTESIAN_POINT('Ctrl Pts',(57.8716499097899,4.59551409193883,127.074209879633));
#180041=CARTESIAN_POINT('Ctrl Pts',(57.8790473991264,4.69326766630308,127.197979633371));
#180042=CARTESIAN_POINT('Ctrl Pts',(57.886444888463,4.7858909932891,127.325398421328));
#180043=CARTESIAN_POINT('Ctrl Pts',(57.893844970978,4.87854678923855,127.452861875742));
#180044=CARTESIAN_POINT('Ctrl Pts',(57.9012450534929,4.96606853785129,127.583976609418));
#180045=CARTESIAN_POINT('Ctrl Pts',(57.9086451360079,5.04817330226624,127.718282706562));
#180046=CARTESIAN_POINT('Ctrl Pts',(57.9160533556744,5.13036834931048,127.852736487067));
#180047=CARTESIAN_POINT('Ctrl Pts',(57.9234615753408,5.20713432174797,127.990388320514));
#180048=CARTESIAN_POINT('Ctrl Pts',(57.9308697950073,5.27823385014464,128.130752945209));
#180049=CARTESIAN_POINT('Ctrl Pts',(57.9382825743094,5.34937713911489,128.271203961989));
#180050=CARTESIAN_POINT('Ctrl Pts',(57.9456953536114,5.41484687967498,128.414370758362));
#180051=CARTESIAN_POINT('Ctrl Pts',(57.9531081329135,5.4744540297795,128.559748482178));
#180052=CARTESIAN_POINT('Ctrl Pts',(57.9605315039422,5.53414634937529,128.705333928504));
#180053=CARTESIAN_POINT('Ctrl Pts',(57.967954874971,5.5879592209053,128.853136261815));
#180054=CARTESIAN_POINT('Ctrl Pts',(57.9753782459998,5.6357533391064,129.002635093728));
#180055=CARTESIAN_POINT('Ctrl Pts',(57.9793142954406,5.66109492738108,129.081902961584));
#180056=CARTESIAN_POINT('Ctrl Pts',(57.9832503448815,5.68474527857404,129.161647586823));
#180057=CARTESIAN_POINT('Ctrl Pts',(57.9871863943223,5.70668948883968,129.241790414194));
#180058=CARTESIAN_POINT('Ctrl Pts',(57.9946096607278,5.74807558454479,129.392937285441));
#180059=CARTESIAN_POINT('Ctrl Pts',(58.0020329271332,5.78351521925214,129.545958066559));
#180060=CARTESIAN_POINT('Ctrl Pts',(58.0094561935386,5.81283727832263,129.700343707259));
#180061=CARTESIAN_POINT('Ctrl Pts',(58.0168706862596,5.84212468115439,129.854546876954));
#180062=CARTESIAN_POINT('Ctrl Pts',(58.0242851789807,5.86530883165831,130.010111332086));
#180063=CARTESIAN_POINT('Ctrl Pts',(58.0316996717017,5.88226833561215,130.166512837641));
#180064=CARTESIAN_POINT('Ctrl Pts',(58.0391070180555,5.89921149335756,130.322763597537));
#180065=CARTESIAN_POINT('Ctrl Pts',(58.0465143644092,5.90994190850043,130.479849433084));
#180066=CARTESIAN_POINT('Ctrl Pts',(58.053921710763,5.91438922651423,130.637235994029));
#180067=CARTESIAN_POINT('Ctrl Pts',(58.0613235324384,5.91883322755047,130.794505170139));
#180068=CARTESIAN_POINT('Ctrl Pts',(58.0687253541138,5.91700345175747,130.952074253508));
#180069=CARTESIAN_POINT('Ctrl Pts',(58.0761271757892,5.90888137664651,131.10940395747));
#180070=CARTESIAN_POINT('Ctrl Pts',(58.0835250901006,5.90076358911575,131.266650608307));
#180071=CARTESIAN_POINT('Ctrl Pts',(58.090923004412,5.88636013670069,131.423657759545));
#180072=CARTESIAN_POINT('Ctrl Pts',(58.0983209187234,5.86570458601269,131.579886421218));
#180073=CARTESIAN_POINT('Ctrl Pts',(58.1057176036356,5.84505246790256,131.736089120521));
#180074=CARTESIAN_POINT('Ctrl Pts',(58.1131142885478,5.81815036247924,131.891513217307));
#180075=CARTESIAN_POINT('Ctrl Pts',(58.12051097346,5.78508368517174,132.045625020528));
#180076=CARTESIAN_POINT('Ctrl Pts',(58.1279073303955,5.75201847407532,132.19972999027));
#180077=CARTESIAN_POINT('Ctrl Pts',(58.1353036873309,5.71278931290752,132.352522417155));
#180078=CARTESIAN_POINT('Ctrl Pts',(58.1427000442664,5.66753265968059,132.503479246136));
#180079=CARTESIAN_POINT('Ctrl Pts',(58.150097533603,5.62226907754451,132.654459186993));
#180080=CARTESIAN_POINT('Ctrl Pts',(58.1574950229396,5.57097627309034,132.803602612771));
#180081=CARTESIAN_POINT('Ctrl Pts',(58.1648925122762,5.51384040878113,132.950402208261));
#180082=CARTESIAN_POINT('Ctrl Pts',(58.1722925947912,5.45668451558301,133.097253264122));
#180083=CARTESIAN_POINT('Ctrl Pts',(58.1796926773062,5.39368161974116,133.241758506183));
#180084=CARTESIAN_POINT('Ctrl Pts',(58.1870927598213,5.32506572715347,133.38343129593));
#180085=CARTESIAN_POINT('Ctrl Pts',(58.1945009794877,5.25637438433838,133.525259869472));
#180086=CARTESIAN_POINT('Ctrl Pts',(58.2019091991542,5.18205788157243,133.66424943452));
#180087=CARTESIAN_POINT('Ctrl Pts',(58.2093174188207,5.10239617928412,133.799937989648));
#180088=CARTESIAN_POINT('Ctrl Pts',(58.2167301981228,5.02268544654705,133.935710058817));
#180089=CARTESIAN_POINT('Ctrl Pts',(58.2241429774249,4.93762316002383,134.068176756233));
#180090=CARTESIAN_POINT('Ctrl Pts',(58.231555756727,4.84753188428267,134.196906150549));
#180091=CARTESIAN_POINT('Ctrl Pts',(58.2389791277557,4.75731188190199,134.32581947946));
#180092=CARTESIAN_POINT('Ctrl Pts',(58.2464024987845,4.66204876442175,134.450984543766));
#180093=CARTESIAN_POINT('Ctrl Pts',(58.2538258698133,4.56210505142999,134.572002859369));
#180094=CARTESIAN_POINT('Ctrl Pts',(58.2577619192539,4.50911249668749,134.636169674094));
#180095=CARTESIAN_POINT('Ctrl Pts',(58.2616979686946,4.45480467750348,134.699171302174));
#180096=CARTESIAN_POINT('Ctrl Pts',(58.2656340181352,4.39923962874216,134.760952743551));
#180097=CARTESIAN_POINT('Ctrl Pts',(58.2730572845406,4.29444568089989,134.877470613859));
#180098=CARTESIAN_POINT('Ctrl Pts',(58.2804805509461,4.18486095219262,134.989998452176));
#180099=CARTESIAN_POINT('Ctrl Pts',(58.2879038173515,4.07082122940121,135.098117140793));
#180100=CARTESIAN_POINT('Ctrl Pts',(58.2953183100725,3.95691629209141,135.2061080421));
#180101=CARTESIAN_POINT('Ctrl Pts',(58.3027328027936,3.83856710982604,135.3096999124));
#180102=CARTESIAN_POINT('Ctrl Pts',(58.3101472955146,3.71614911982727,135.408507257467));
#180103=CARTESIAN_POINT('Ctrl Pts',(58.3175546418684,3.59384912089656,135.507219368293));
#180104=CARTESIAN_POINT('Ctrl Pts',(58.3249619882221,3.46748841003899,135.601155901602));
#180105=CARTESIAN_POINT('Ctrl Pts',(58.3323693345759,3.33747852291532,135.689968836773));
#180106=CARTESIAN_POINT('Ctrl Pts',(58.3397711562512,3.20756560207102,135.778715531905));
#180107=CARTESIAN_POINT('Ctrl Pts',(58.3471729779266,3.07400923113412,135.862346028108));
#180108=CARTESIAN_POINT('Ctrl Pts',(58.3545747996019,2.9372531153924,135.940553244271));
#180109=CARTESIAN_POINT('Ctrl Pts',(58.3619727139134,2.80056919213752,136.018719175454));
#180110=CARTESIAN_POINT('Ctrl Pts',(58.3693706282249,2.66068921127279,136.091467343368));
#180111=CARTESIAN_POINT('Ctrl Pts',(58.3767685425363,2.51808478389424,136.15853465131));
#180112=CARTESIAN_POINT('Ctrl Pts',(58.3841652274485,2.37550405478604,136.225590813882));
#180113=CARTESIAN_POINT('Ctrl Pts',(58.3915619123607,2.23020011521923,136.286967831439));
#180114=CARTESIAN_POINT('Ctrl Pts',(58.3989585972729,2.08266814371336,136.342449093355));
#180115=CARTESIAN_POINT('Ctrl Pts',(58.4063549542083,1.9351427139295,136.397927895172));
#180116=CARTESIAN_POINT('Ctrl Pts',(58.4137513111438,1.78538979804815,136.447511329748));
#180117=CARTESIAN_POINT('Ctrl Pts',(58.4211476680793,1.63392321598273,136.491031479043));
#180118=CARTESIAN_POINT('Ctrl Pts',(58.4285451574158,1.48243344399757,136.534558291384));
#180119=CARTESIAN_POINT('Ctrl Pts',(58.4359426467523,1.32922984222628,136.572019866972));
#180120=CARTESIAN_POINT('Ctrl Pts',(58.4433401360889,1.17483985468064,136.603298613299));
#180121=CARTESIAN_POINT('Ctrl Pts',(58.4507402186039,1.02039574596376,136.634588324342));
#180122=CARTESIAN_POINT('Ctrl Pts',(58.4581403011189,0.86476478908387,136.659690816806));
#180123=CARTESIAN_POINT('Ctrl Pts',(58.4655403836339,0.708482892709509,
136.678539926477));
#180124=CARTESIAN_POINT('Ctrl Pts',(58.4729486033004,0.552029148323692,
136.697409762682));
#180125=CARTESIAN_POINT('Ctrl Pts',(58.4803568229668,0.394923405833401,
136.71001243907));
#180126=CARTESIAN_POINT('Ctrl Pts',(58.4877650426333,0.23770568557277,136.716333771222));
#180127=CARTESIAN_POINT('Ctrl Pts',(58.4951778219354,0.08039120042774,136.722658994048));
#180128=CARTESIAN_POINT('Ctrl Pts',(58.5025906012376,-0.0770350273878875,
136.72269516894));
#180129=CARTESIAN_POINT('Ctrl Pts',(58.5100033805397,-0.234035247772293,
136.716480209159));
#180130=CARTESIAN_POINT('Ctrl Pts',(58.5174267515684,-0.391259797433267,
136.710256369153));
#180131=CARTESIAN_POINT('Ctrl Pts',(58.5248501225971,-0.548056752820933,
136.697763585009));
#180132=CARTESIAN_POINT('Ctrl Pts',(58.5322734936259,-0.703894907287435,
136.679091464336));
#180133=CARTESIAN_POINT('Ctrl Pts',(58.5362095430666,-0.78652403606943,
136.669191057924));
#180134=CARTESIAN_POINT('Ctrl Pts',(58.5401455925074,-0.868883792885377,
136.657554270445));
#180135=CARTESIAN_POINT('Ctrl Pts',(58.5440816419481,-0.950896535366328,
136.644200199398));
#180136=CARTESIAN_POINT('Ctrl Pts',(58.5515049083535,-1.10557000815762,
136.619014838168));
#180137=CARTESIAN_POINT('Ctrl Pts',(58.5589281747589,-1.25947608810888,
136.587642147561));
#180138=CARTESIAN_POINT('Ctrl Pts',(58.5663514411644,-1.41208065866681,
136.550138091148));
#180139=CARTESIAN_POINT('Ctrl Pts',(58.5737659338854,-1.56450486329579,
136.512678361414));
#180140=CARTESIAN_POINT('Ctrl Pts',(58.5811804266064,-1.71563026150735,
136.469101778821));
#180141=CARTESIAN_POINT('Ctrl Pts',(58.5885949193274,-1.8649295931009,136.419515840289));
#180142=CARTESIAN_POINT('Ctrl Pts',(58.5960022656812,-2.01408502437742,
136.369977694552));
#180143=CARTESIAN_POINT('Ctrl Pts',(58.603409612035,-2.16141754102118,136.314441840567));
#180144=CARTESIAN_POINT('Ctrl Pts',(58.6108169583887,-2.30641189835171,
136.253066401295));
#180145=CARTESIAN_POINT('Ctrl Pts',(58.6182187800641,-2.45129811342042,
136.191736738141));
#180146=CARTESIAN_POINT('Ctrl Pts',(58.6256206017395,-2.59384929920243,
136.124576306744));
#180147=CARTESIAN_POINT('Ctrl Pts',(58.633022423415,-2.73356726611679,136.05179242409));
#180148=CARTESIAN_POINT('Ctrl Pts',(58.6404203377263,-2.87321147700378,
135.97904696348));
#180149=CARTESIAN_POINT('Ctrl Pts',(58.6478182520377,-3.01002511741883,
135.900684135702));
#180150=CARTESIAN_POINT('Ctrl Pts',(58.655216166349,-3.14353191933897,135.816958510335));
#180151=CARTESIAN_POINT('Ctrl Pts',(58.6626128512612,-3.27701653485051,
135.733246798649));
#180152=CARTESIAN_POINT('Ctrl Pts',(58.6700095361734,-3.40719508659085,
135.644174256277));
#180153=CARTESIAN_POINT('Ctrl Pts',(58.6774062210856,-3.5336176778186,135.550040407597));
#180154=CARTESIAN_POINT('Ctrl Pts',(58.684802578021,-3.66003466333635,135.45591073291));
#180155=CARTESIAN_POINT('Ctrl Pts',(58.6921989349565,-3.78269572007288,
135.356720421088));
#180156=CARTESIAN_POINT('Ctrl Pts',(58.6995952918919,-3.90118184161253,
135.252810999572));
#180157=CARTESIAN_POINT('Ctrl Pts',(58.7069927812285,-4.01968610367937,
135.14888566926));
#180158=CARTESIAN_POINT('Ctrl Pts',(58.714390270565,-4.13401387715223,135.040240036794));
#180159=CARTESIAN_POINT('Ctrl Pts',(58.7217877599015,-4.24378113175039,
134.927254294136));
#180160=CARTESIAN_POINT('Ctrl Pts',(58.7291878424165,-4.35358686508995,
134.8142289445));
#180161=CARTESIAN_POINT('Ctrl Pts',(58.7365879249314,-4.45882863663084,
134.696860723119));
#180162=CARTESIAN_POINT('Ctrl Pts',(58.7439880074464,-4.55916110881966,
134.575564741758));
#180163=CARTESIAN_POINT('Ctrl Pts',(58.7513962271129,-4.65960390687621,
134.454135382997));
#180164=CARTESIAN_POINT('Ctrl Pts',(58.7588044467794,-4.7551263867847,134.328769926799));
#180165=CARTESIAN_POINT('Ctrl Pts',(58.7662126664459,-4.84542472061101,
134.199915040542));
#180166=CARTESIAN_POINT('Ctrl Pts',(58.773625445748,-4.93577863155494,134.070980846253));
#180167=CARTESIAN_POINT('Ctrl Pts',(58.78103822505,-5.02090178799864,133.938553255662));
#180168=CARTESIAN_POINT('Ctrl Pts',(58.7884510043521,-5.10053542037966,
133.803105186207));
#180169=CARTESIAN_POINT('Ctrl Pts',(58.7958743753808,-5.18028283702907,
133.667463582198));
#180170=CARTESIAN_POINT('Ctrl Pts',(58.8032977464095,-5.25452488828037,
133.528793207927));
#180171=CARTESIAN_POINT('Ctrl Pts',(58.8107211174382,-5.32304983338438,
133.387589417693));
#180172=CARTESIAN_POINT('Ctrl Pts',(58.8146571668791,-5.35938340351294,
133.312719779971));
#180173=CARTESIAN_POINT('Ctrl Pts',(58.81859321632,-5.39411050494493,133.237138216132));
#180174=CARTESIAN_POINT('Ctrl Pts',(58.8225292657609,-5.42720523735072,
133.160920371566));
#180175=CARTESIAN_POINT('Ctrl Pts',(58.8307364137368,-5.49621183143824,
133.001996776182));
#180176=CARTESIAN_POINT('Ctrl Pts',(58.8389435617126,-5.55829734966145,
132.839894260625));
#180177=CARTESIAN_POINT('Ctrl Pts',(58.8471507096885,-5.61318787800807,
132.67520331771));
#180178=CARTESIAN_POINT('Ctrl Pts',(58.8553258331378,-5.66786422194073,
132.511155003572));
#180179=CARTESIAN_POINT('Ctrl Pts',(58.8635009565872,-5.71540149870125,
132.344538634856));
#180180=CARTESIAN_POINT('Ctrl Pts',(58.8716760800365,-5.75557476425497,
132.1759617606));
#180181=CARTESIAN_POINT('Ctrl Pts',(58.879830802216,-5.79564777619953,132.007805575074));
#180182=CARTESIAN_POINT('Ctrl Pts',(58.8879855243955,-5.8283933671508,131.837698871199));
#180183=CARTESIAN_POINT('Ctrl Pts',(58.896140246575,-5.85363568991775,131.666265352569));
#180184=CARTESIAN_POINT('Ctrl Pts',(58.9042614198469,-5.87877416459087,
131.495537119436));
#180185=CARTESIAN_POINT('Ctrl Pts',(58.9123825931188,-5.89647088813332,
131.323493192654));
#180186=CARTESIAN_POINT('Ctrl Pts',(58.9205037663907,-5.90660082279266,
131.150766856951));
#180187=CARTESIAN_POINT('Ctrl Pts',(58.9258774271522,-5.91330365138323,
131.036476384186));
#180188=CARTESIAN_POINT('Ctrl Pts',(58.9312510879138,-5.91669453246377,
130.921887482986));
#180189=CARTESIAN_POINT('Ctrl Pts',(58.9366247486753,-5.91674932490583,
130.807187051078));
#180190=CARTESIAN_POINT('',(60.6866248421796,-5.91522241010308,130.799308802059));
#180191=CARTESIAN_POINT('Ctrl Pts',(58.9366248077955,-5.90823460448425,
130.807181723492));
#180192=CARTESIAN_POINT('Ctrl Pts',(58.9914088350549,-5.90322513381588,
129.639500448815));
#180193=CARTESIAN_POINT('Ctrl Pts',(59.1390087369187,-5.00249046179937,
126.486390081414));
#180194=CARTESIAN_POINT('Ctrl Pts',(59.3794245133868,0.133157591622454,
123.807230521151));
#180195=CARTESIAN_POINT('Ctrl Pts',(59.6578721371997,5.95885864996216,127.134270139101));
#180196=CARTESIAN_POINT('Ctrl Pts',(59.9363197610124,6.30865971541475,133.83394361287));
#180197=CARTESIAN_POINT('Ctrl Pts',(60.2147673848254,0.861110697562879,
137.749578317314));
#180198=CARTESIAN_POINT('Ctrl Pts',(60.4648690670865,-4.74264084872292,
135.534005146028));
#180199=CARTESIAN_POINT('Ctrl Pts',(60.6221548747431,-5.90152067071388,
132.170905612889));
#180200=CARTESIAN_POINT('Ctrl Pts',(60.6866248077955,-5.91257889518605,
130.79931179142));
#180201=CARTESIAN_POINT('',(62.4366248077954,-5.92102293431065,130.803603394944));
#180202=CARTESIAN_POINT('Ctrl Pts',(60.6866248620209,-5.9167478418662,130.799307077057));
#180203=CARTESIAN_POINT('Ctrl Pts',(60.6954873200923,-5.91658668901759,
130.610627325191));
#180204=CARTESIAN_POINT('Ctrl Pts',(60.7043497781637,-5.90739656084578,
130.422339921947));
#180205=CARTESIAN_POINT('Ctrl Pts',(60.7132122362351,-5.88931252189037,
130.235213376507));
#180206=CARTESIAN_POINT('Ctrl Pts',(60.7221443094069,-5.87108643180472,
130.04661694166));
#180207=CARTESIAN_POINT('Ctrl Pts',(60.7310763825786,-5.84382625345664,
129.859199684484));
#180208=CARTESIAN_POINT('Ctrl Pts',(60.7400084557503,-5.80771882203087,
129.673726880793));
#180209=CARTESIAN_POINT('Ctrl Pts',(60.7490150007341,-5.77131034226002,
129.486707684064));
#180210=CARTESIAN_POINT('Ctrl Pts',(60.7580215457179,-5.72590651421125,
129.30166550607));
#180211=CARTESIAN_POINT('Ctrl Pts',(60.7670280907016,-5.67174697298224,
129.119363039833));
#180212=CARTESIAN_POINT('Ctrl Pts',(60.7685729379515,-5.66245725994887,
129.088093616972));
#180213=CARTESIAN_POINT('Ctrl Pts',(60.7701177852014,-5.65291005942039,
129.056904746874));
#180214=CARTESIAN_POINT('Ctrl Pts',(60.7716626324512,-5.64310672008258,
129.025800214246));
#180215=CARTESIAN_POINT('Ctrl Pts',(60.7790858988566,-5.59599992711428,
128.876337390568));
#180216=CARTESIAN_POINT('Ctrl Pts',(60.786509165262,-5.54287981320506,128.728521354023));
#180217=CARTESIAN_POINT('Ctrl Pts',(60.7939324316674,-5.48387836124831,
128.582872674422));
#180218=CARTESIAN_POINT('Ctrl Pts',(60.8013469243884,-5.42494664410802,
128.437396139466));
#180219=CARTESIAN_POINT('Ctrl Pts',(60.8087614171094,-5.36014756421678,
128.294082205112));
#180220=CARTESIAN_POINT('Ctrl Pts',(60.8161759098303,-5.28966312186374,
128.15343726528));
#180221=CARTESIAN_POINT('Ctrl Pts',(60.8235832561841,-5.21924661506993,
128.012927884337));
#180222=CARTESIAN_POINT('Ctrl Pts',(60.8309906025378,-5.1431558210789,127.875082708114));
#180223=CARTESIAN_POINT('Ctrl Pts',(60.8383979488915,-5.06162111976517,
127.740388978917));
#180224=CARTESIAN_POINT('Ctrl Pts',(60.8457997705669,-4.98014723010781,
127.605795709385));
#180225=CARTESIAN_POINT('Ctrl Pts',(60.8532015922422,-4.8932377101554,127.474349524752));
#180226=CARTESIAN_POINT('Ctrl Pts',(60.8606034139176,-4.80116917942636,
127.346513733589));
#180227=CARTESIAN_POINT('Ctrl Pts',(60.8680013282289,-4.70914925095804,
127.218745425946));
#180228=CARTESIAN_POINT('Ctrl Pts',(60.8753992425403,-4.61197595310718,
127.094584018232));
#180229=CARTESIAN_POINT('Ctrl Pts',(60.8827971568516,-4.50996952577516,
126.97446434755));
#180230=CARTESIAN_POINT('Ctrl Pts',(60.8901938417637,-4.40798005006093,
126.854364638579));
#180231=CARTESIAN_POINT('Ctrl Pts',(60.8975905266759,-4.3011592803352,126.738305617849));
#180232=CARTESIAN_POINT('Ctrl Pts',(60.9049872115881,-4.18986816470222,
126.626689576793));
#180233=CARTESIAN_POINT('Ctrl Pts',(60.9123835685235,-4.07858198383394,
126.515078484909));
#180234=CARTESIAN_POINT('Ctrl Pts',(60.9197799254589,-3.96282611476256,
126.40791024533));
#180235=CARTESIAN_POINT('Ctrl Pts',(60.9271762823943,-3.84299864449683,
126.305550554794));
#180236=CARTESIAN_POINT('Ctrl Pts',(60.9345737717309,-3.72315282833915,
126.203175192728));
#180237=CARTESIAN_POINT('Ctrl Pts',(60.9419712610674,-3.59923445362533,
126.105610088057));
#180238=CARTESIAN_POINT('Ctrl Pts',(60.949368750404,-3.471674856282,126.013180778032));
#180239=CARTESIAN_POINT('Ctrl Pts',(60.9567688329189,-3.34407054311992,
125.920719067056));
#180240=CARTESIAN_POINT('Ctrl Pts',(60.9641689154339,-3.21282276807083,
125.833396954096));
#180241=CARTESIAN_POINT('Ctrl Pts',(60.9715689979489,-3.07839187697724,
125.751496675774));
#180242=CARTESIAN_POINT('Ctrl Pts',(60.9789772176153,-2.94381316529887,
125.669506339676));
#180243=CARTESIAN_POINT('Ctrl Pts',(60.9863854372817,-2.80604466650949,
125.59294993879));
#180244=CARTESIAN_POINT('Ctrl Pts',(60.9937936569482,-2.6655720029761,125.52206410379));
#180245=CARTESIAN_POINT('Ctrl Pts',(61.0012064362502,-2.52501288086183,
125.451134639741));
#180246=CARTESIAN_POINT('Ctrl Pts',(61.0086192155523,-2.38174661647441,
125.385882850486));
#180247=CARTESIAN_POINT('Ctrl Pts',(61.0160319948543,-2.23627834906836,
125.326497009553));
#180248=CARTESIAN_POINT('Ctrl Pts',(61.023455365883,-2.09060222978048,125.267026315346));
#180249=CARTESIAN_POINT('Ctrl Pts',(61.0308787369117,-1.9427181735932,125.213438436121));
#180250=CARTESIAN_POINT('Ctrl Pts',(61.0383021079405,-1.79314678028665,
125.165871885038));
#180251=CARTESIAN_POINT('Ctrl Pts',(61.0422381573817,-1.7138404386294,125.140650958306));
#180252=CARTESIAN_POINT('Ctrl Pts',(61.046174206823,-1.63405991391674,125.117121992242));
#180253=CARTESIAN_POINT('Ctrl Pts',(61.0501102562642,-1.55388378398904,
125.095299771126));
#180254=CARTESIAN_POINT('Ctrl Pts',(61.0575335226697,-1.40267410517459,
125.054143743153));
#180255=CARTESIAN_POINT('Ctrl Pts',(61.0649567890751,-1.24959956816168,
125.018937021065));
#180256=CARTESIAN_POINT('Ctrl Pts',(61.0723800554806,-1.09516948305461,
124.989849944613));
#180257=CARTESIAN_POINT('Ctrl Pts',(61.0797945482016,-0.940921921483288,
124.96079724667));
#180258=CARTESIAN_POINT('Ctrl Pts',(61.0872090409226,-0.785322364161935,
124.937849865632));
#180259=CARTESIAN_POINT('Ctrl Pts',(61.0946235336436,-0.628895230239016,
124.921128397784));
#180260=CARTESIAN_POINT('Ctrl Pts',(61.1020308799974,-0.47261886667715,
124.904423046716));
#180261=CARTESIAN_POINT('Ctrl Pts',(61.1094382263512,-0.315516883168193,
124.8939317019));
#180262=CARTESIAN_POINT('Ctrl Pts',(61.116845572705,-0.158123736413326,
124.88972390459));
#180263=CARTESIAN_POINT('Ctrl Pts',(61.1242473943804,-0.00084797940541162,
124.885519245614));
#180264=CARTESIAN_POINT('Ctrl Pts',(61.1316492160557,0.156718136893979,
124.88758881261));
#180265=CARTESIAN_POINT('Ctrl Pts',(61.1390510377312,0.314035298255438,
124.895950307343));
#180266=CARTESIAN_POINT('Ctrl Pts',(61.1464489520425,0.47126941311197,124.904307388108));
#180267=CARTESIAN_POINT('Ctrl Pts',(61.1538468663538,0.628254462934403,
124.918949762001));
#180268=CARTESIAN_POINT('Ctrl Pts',(61.1612447806652,0.784451509464366,
124.939843042198));
#180269=CARTESIAN_POINT('Ctrl Pts',(61.1686414655774,0.940622598878676,
124.960732850311));
#180270=CARTESIAN_POINT('Ctrl Pts',(61.1760381504896,1.096005575261,124.9878714536));
#180271=CARTESIAN_POINT('Ctrl Pts',(61.1834348354018,1.25006687816888,125.021172624546));
#180272=CARTESIAN_POINT('Ctrl Pts',(61.1908311923373,1.40412134983736,125.054472318884));
#180273=CARTESIAN_POINT('Ctrl Pts',(61.1982275492727,1.55685389968581,125.093933958689));
#180274=CARTESIAN_POINT('Ctrl Pts',(61.2056239062081,1.70774168093889,125.139420290106));
#180275=CARTESIAN_POINT('Ctrl Pts',(61.2130213955447,1.85865256349626,125.184913585596));
#180276=CARTESIAN_POINT('Ctrl Pts',(61.2204188848813,2.00771775765134,125.236433301559));
#180277=CARTESIAN_POINT('Ctrl Pts',(61.2278163742178,2.1544302320902,125.2937925037));
#180278=CARTESIAN_POINT('Ctrl Pts',(61.2352164567328,2.30119413635954,125.351171813021));
#180279=CARTESIAN_POINT('Ctrl Pts',(61.2426165392478,2.44560333140259,125.414394548285));
#180280=CARTESIAN_POINT('Ctrl Pts',(61.2500166217628,2.5871715353852,125.483225963285));
#180281=CARTESIAN_POINT('Ctrl Pts',(61.2574248414292,2.72889540816165,125.552133065502));
#180282=CARTESIAN_POINT('Ctrl Pts',(61.2648330610957,2.86777171519548,125.626661000668));
#180283=CARTESIAN_POINT('Ctrl Pts',(61.2722412807622,3.00333888164796,125.706529105591));
#180284=CARTESIAN_POINT('Ctrl Pts',(61.2796540600642,3.13898948742954,125.786446368001));
#180285=CARTESIAN_POINT('Ctrl Pts',(61.2870668393663,3.27132658113066,125.871710147787));
#180286=CARTESIAN_POINT('Ctrl Pts',(61.2944796186683,3.39991872279468,125.961997223428));
#180287=CARTESIAN_POINT('Ctrl Pts',(61.3019029896971,3.52869460294108,126.052413305476));
#180288=CARTESIAN_POINT('Ctrl Pts',(61.3093263607259,3.65371454805904,126.147866792564));
#180289=CARTESIAN_POINT('Ctrl Pts',(61.3167497317546,3.77458062620727,126.247994559098));
#180290=CARTESIAN_POINT('Ctrl Pts',(61.3206857811954,3.83866672098319,126.301084703447));
#180291=CARTESIAN_POINT('Ctrl Pts',(61.3246218306362,3.90158562885523,126.355488337498));
#180292=CARTESIAN_POINT('Ctrl Pts',(61.328557880077,3.96328243814734,126.411147342755));
#180293=CARTESIAN_POINT('Ctrl Pts',(61.3359811464824,4.07964069498093,126.516118489612));
#180294=CARTESIAN_POINT('Ctrl Pts',(61.3434044128879,4.19200163368944,126.625874339636));
#180295=CARTESIAN_POINT('Ctrl Pts',(61.3508276792933,4.29994664806236,126.740078468611));
#180296=CARTESIAN_POINT('Ctrl Pts',(61.3582421720143,4.40776408039256,126.854147617789));
#180297=CARTESIAN_POINT('Ctrl Pts',(61.3656566647354,4.51117572342619,126.9726543122));
#180298=CARTESIAN_POINT('Ctrl Pts',(61.3730711574564,4.60979665473362,127.095222528399));
#180299=CARTESIAN_POINT('Ctrl Pts',(61.3804785038101,4.70832253147444,127.217672608738));
#180300=CARTESIAN_POINT('Ctrl Pts',(61.3878858501639,4.80206665651455,127.344176128685));
#180301=CARTESIAN_POINT('Ctrl Pts',(61.3952931965177,4.89068163592486,127.474321023428));
#180302=CARTESIAN_POINT('Ctrl Pts',(61.4026950181931,4.97923052294039,127.604368851199));
#180303=CARTESIAN_POINT('Ctrl Pts',(61.4100968398685,5.06265767223972,127.738052338859));
#180304=CARTESIAN_POINT('Ctrl Pts',(61.4174986615439,5.14065667831233,127.87492731431));
#180305=CARTESIAN_POINT('Ctrl Pts',(61.4248965758553,5.21861450931679,128.011730034527));
#180306=CARTESIAN_POINT('Ctrl Pts',(61.4322944901667,5.29114971946928,128.15172056374));
#180307=CARTESIAN_POINT('Ctrl Pts',(61.4396924044781,5.35799993008529,128.294426891009));
#180308=CARTESIAN_POINT('Ctrl Pts',(61.4470890893903,5.42483903140899,128.437109503076));
#180309=CARTESIAN_POINT('Ctrl Pts',(61.4544857743025,5.48599485003209,128.582506679756));
#180310=CARTESIAN_POINT('Ctrl Pts',(61.4618824592147,5.54125152915468,128.730122913459));
#180311=CARTESIAN_POINT('Ctrl Pts',(61.4692788161501,5.59650575813822,128.877732601703));
#180312=CARTESIAN_POINT('Ctrl Pts',(61.4766751730856,5.64586123685168,129.027560801719));
#180313=CARTESIAN_POINT('Ctrl Pts',(61.4840715300211,5.68915082939721,129.179093438648));
#180314=CARTESIAN_POINT('Ctrl Pts',(61.4914690193577,5.73244704968986,129.33064927561));
#180315=CARTESIAN_POINT('Ctrl Pts',(61.4988665086943,5.76967543209657,129.483909710115));
#180316=CARTESIAN_POINT('Ctrl Pts',(61.5062639980309,5.80071918692378,129.638347119808));
#180317=CARTESIAN_POINT('Ctrl Pts',(61.5136640805459,5.83177382409111,129.792838667295));
#180318=CARTESIAN_POINT('Ctrl Pts',(61.5210641630609,5.85663944366383,129.948507645677));
#180319=CARTESIAN_POINT('Ctrl Pts',(61.5284642455759,5.87525069706555,130.104818046216));
#180320=CARTESIAN_POINT('Ctrl Pts',(61.5358724652423,5.8938824154537,130.26130032611));
#180321=CARTESIAN_POINT('Ctrl Pts',(61.5432806849089,5.90624598905169,130.418425065803));
#180322=CARTESIAN_POINT('Ctrl Pts',(61.5506889045753,5.91232805527671,130.575652223999));
#180323=CARTESIAN_POINT('Ctrl Pts',(61.5581016838774,5.918413864912,130.732976152888));
#180324=CARTESIAN_POINT('Ctrl Pts',(61.5655144631794,5.91821046384112,130.890402253458));
#180325=CARTESIAN_POINT('Ctrl Pts',(61.5729272424815,5.91175658364844,131.047392833927));
#180326=CARTESIAN_POINT('Ctrl Pts',(61.5803506135103,5.90529348184907,131.2046077299));
#180327=CARTESIAN_POINT('Ctrl Pts',(61.5877739845391,5.89256209389692,131.361385491828));
#180328=CARTESIAN_POINT('Ctrl Pts',(61.5951973555678,5.87365283570351,131.517195050048));
#180329=CARTESIAN_POINT('Ctrl Pts',(61.5991334050085,5.8636266932882,131.599809016413));
#180330=CARTESIAN_POINT('Ctrl Pts',(61.6030694544492,5.85186458175435,131.682150968647));
#180331=CARTESIAN_POINT('Ctrl Pts',(61.6070055038899,5.83838571673788,131.764143293535));
#180332=CARTESIAN_POINT('Ctrl Pts',(61.6144287702953,5.81296499797722,131.918778259385));
#180333=CARTESIAN_POINT('Ctrl Pts',(61.6218520367008,5.78135812484507,132.072636417221));
#180334=CARTESIAN_POINT('Ctrl Pts',(61.6292753031062,5.74362187368212,132.225183736276));
#180335=CARTESIAN_POINT('Ctrl Pts',(61.6366897958272,5.7059302236342,132.377550757068));
#180336=CARTESIAN_POINT('Ctrl Pts',(61.6441042885482,5.66212370437189,132.528609664138));
#180337=CARTESIAN_POINT('Ctrl Pts',(61.6515187812692,5.61231061509273,132.677833361488));
#180338=CARTESIAN_POINT('Ctrl Pts',(61.658926127623,5.56254553754444,132.82691323142));
#180339=CARTESIAN_POINT('Ctrl Pts',(61.6663334739767,5.50678553285906,132.974161061339));
#180340=CARTESIAN_POINT('Ctrl Pts',(61.6737408203305,5.44518950792927,133.119061847798));
#180341=CARTESIAN_POINT('Ctrl Pts',(61.6811426420059,5.38363942363875,133.263854561783));
#180342=CARTESIAN_POINT('Ctrl Pts',(61.6885444636813,5.31626213137478,133.406303375749));
#180343=CARTESIAN_POINT('Ctrl Pts',(61.6959462853567,5.24326570604115,133.545910416193));
#180344=CARTESIAN_POINT('Ctrl Pts',(61.703344199668,5.17030781495226,133.685443759167));
#180345=CARTESIAN_POINT('Ctrl Pts',(61.7107421139794,5.09173687084677,133.82213798627));
#180346=CARTESIAN_POINT('Ctrl Pts',(61.7181400282907,5.00780816780718,133.955517217442));
#180347=CARTESIAN_POINT('Ctrl Pts',(61.7255367132029,4.92389341219542,134.088874283406));
#180348=CARTESIAN_POINT('Ctrl Pts',(61.7329333981151,4.83462286337252,134.218917131155));
#180349=CARTESIAN_POINT('Ctrl Pts',(61.7403300830273,4.74029673003504,134.345196320295));
#180350=CARTESIAN_POINT('Ctrl Pts',(61.7477264399628,4.64597477921716,134.471469910083));
#180351=CARTESIAN_POINT('Ctrl Pts',(61.7551227968982,4.54659791300742,134.59397987401));
#180352=CARTESIAN_POINT('Ctrl Pts',(61.7625191538336,4.44250829611049,134.712307725894));
#180353=CARTESIAN_POINT('Ctrl Pts',(61.7699166431702,4.33840274282749,134.830653694074));
#180354=CARTESIAN_POINT('Ctrl Pts',(61.7773141325067,4.22958324876174,134.944815995));
#180355=CARTESIAN_POINT('Ctrl Pts',(61.7847116218433,4.11643058986292,135.054411177423));
#180356=CARTESIAN_POINT('Ctrl Pts',(61.7921117043583,4.00323826547494,135.164044778268));
#180357=CARTESIAN_POINT('Ctrl Pts',(61.7995117868733,3.88571001994317,135.269107813487));
#180358=CARTESIAN_POINT('Ctrl Pts',(61.8069118693883,3.76426149009823,135.369255577657));
#180359=CARTESIAN_POINT('Ctrl Pts',(61.8143200890548,3.64267941510951,135.469513464589));
#180360=CARTESIAN_POINT('Ctrl Pts',(61.8217283087212,3.51716873512941,135.564845049001));
#180361=CARTESIAN_POINT('Ctrl Pts',(61.8291365283877,3.38817657939181,135.654947183061));
#180362=CARTESIAN_POINT('Ctrl Pts',(61.8365493076898,3.25910503113451,135.745104773482));
#180363=CARTESIAN_POINT('Ctrl Pts',(61.8439620869918,3.12654805093928,135.830026299104));
#180364=CARTESIAN_POINT('Ctrl Pts',(61.8513748662939,2.99097894949759,135.909453710367));
#180365=CARTESIAN_POINT('Ctrl Pts',(61.8587982373226,2.8552161405664,135.988994611239));
#180366=CARTESIAN_POINT('Ctrl Pts',(61.8662216083514,2.71643294310971,136.063025543815));
#180367=CARTESIAN_POINT('Ctrl Pts',(61.8736449793801,2.57512503308625,136.131335521437));
#180368=CARTESIAN_POINT('Ctrl Pts',(61.877581028821,2.50020018855354,136.167555110648));
#180369=CARTESIAN_POINT('Ctrl Pts',(61.8815170782618,2.42456586350064,136.202167149593));
#180370=CARTESIAN_POINT('Ctrl Pts',(61.8854531277027,2.34829774264479,136.23514585309));
#180371=CARTESIAN_POINT('Ctrl Pts',(61.8928763941081,2.2044584469599,136.297342658656));
#180372=CARTESIAN_POINT('Ctrl Pts',(61.9002996605136,2.05792893431406,136.353914993641));
#180373=CARTESIAN_POINT('Ctrl Pts',(61.907722926919,1.90918918891571,136.404621968916));
#180374=CARTESIAN_POINT('Ctrl Pts',(61.91513741964,1.76062524154414,136.455269012758));
#180375=CARTESIAN_POINT('Ctrl Pts',(61.922551912361,1.60985661112041,136.500064376527));
#180376=CARTESIAN_POINT('Ctrl Pts',(61.929966405082,1.45738529679739,136.538814267146));
#180377=CARTESIAN_POINT('Ctrl Pts',(61.9373737514358,1.30506094006778,136.577526809161));
#180378=CARTESIAN_POINT('Ctrl Pts',(61.9447810977896,1.15103752593519,136.610205386813));
#180379=CARTESIAN_POINT('Ctrl Pts',(61.9521884441434,0.99583423444274,136.636705321029));
#180380=CARTESIAN_POINT('Ctrl Pts',(61.9595902658188,0.840746699420133,
136.663185490594));
#180381=CARTESIAN_POINT('Ctrl Pts',(61.9669920874942,0.684481405619452,
136.683496129843));
#180382=CARTESIAN_POINT('Ctrl Pts',(61.9743939091696,0.527569697687247,
136.697543185295));
#180383=CARTESIAN_POINT('Ctrl Pts',(61.981791823481,0.370740822224485,136.711582825415));
#180384=CARTESIAN_POINT('Ctrl Pts',(61.9891897377924,0.213266583089832,
136.719365433586));
#180385=CARTESIAN_POINT('Ctrl Pts',(61.9965876521038,0.0556853443427907,
136.720848571152));
#180386=CARTESIAN_POINT('Ctrl Pts',(62.003984337016,-0.10186970726096,136.722331462247));
#180387=CARTESIAN_POINT('Ctrl Pts',(62.0113810219281,-0.259531350270411,
136.717516956931));
#180388=CARTESIAN_POINT('Ctrl Pts',(62.0187777068403,-0.416759187618657,
136.706414695769));
#180389=CARTESIAN_POINT('Ctrl Pts',(62.0261740637758,-0.573980053319833,
136.695312926894));
#180390=CARTESIAN_POINT('Ctrl Pts',(62.0335704207112,-0.730766779235901,
136.677923982828));
#180391=CARTESIAN_POINT('Ctrl Pts',(62.0409667776467,-0.886582332707555,
136.654309534423));
#180392=CARTESIAN_POINT('Ctrl Pts',(62.0483642669833,-1.04242174193845,
136.630691470585));
#180393=CARTESIAN_POINT('Ctrl Pts',(62.0557617563198,-1.19728931355836,
136.600846060519));
#180394=CARTESIAN_POINT('Ctrl Pts',(62.0631592456564,-1.3506566204702,136.564886397048));
#180395=CARTESIAN_POINT('Ctrl Pts',(62.0705593281714,-1.50407769005373,
136.528914127973));
#180396=CARTESIAN_POINT('Ctrl Pts',(62.0779594106865,-1.6559970846206,136.486823423278));
#180397=CARTESIAN_POINT('Ctrl Pts',(62.0853594932015,-1.80590013187556,
136.438777648297));
#180398=CARTESIAN_POINT('Ctrl Pts',(62.092767712868,-1.95596801294138,136.390679042047));
#180399=CARTESIAN_POINT('Ctrl Pts',(62.1001759325344,-2.10401476313579,
136.336612402311));
#180400=CARTESIAN_POINT('Ctrl Pts',(62.1075841522009,-2.24954365133065,
136.276790052767));
#180401=CARTESIAN_POINT('Ctrl Pts',(62.1149969315029,-2.39516211012792,
136.216930883566));
#180402=CARTESIAN_POINT('Ctrl Pts',(62.122409710805,-2.53825928041674,136.151309100842));
#180403=CARTESIAN_POINT('Ctrl Pts',(62.1298224901071,-2.67836222180148,
136.080183432192));
#180404=CARTESIAN_POINT('Ctrl Pts',(62.1372458611359,-2.81866534883903,
136.008956135851));
#180405=CARTESIAN_POINT('Ctrl Pts',(62.1446692321646,-2.95596537727408,
135.93220942865));
#180406=CARTESIAN_POINT('Ctrl Pts',(62.1520926031934,-3.08981687309164,
135.850246293367));
#180407=CARTESIAN_POINT('Ctrl Pts',(62.1560286526342,-3.16078814789647,
135.806787472362));
#180408=CARTESIAN_POINT('Ctrl Pts',(62.1599647020749,-3.23079043668502,
135.761862825116));
#180409=CARTESIAN_POINT('Ctrl Pts',(62.1639007515157,-3.2997611362165,135.715522089806));
#180410=CARTESIAN_POINT('Ctrl Pts',(62.1712980963833,-3.4293835044989,135.628430094224));
#180411=CARTESIAN_POINT('Ctrl Pts',(62.1786954412508,-3.55575829884785,
135.536066499443));
#180412=CARTESIAN_POINT('Ctrl Pts',(62.1860927861183,-3.67842526326733,
135.43870179459));
#180413=CARTESIAN_POINT('Ctrl Pts',(62.1934813718664,-3.80094697900442,
135.341452378275));
#180414=CARTESIAN_POINT('Ctrl Pts',(62.2008699576145,-3.91976931110266,
135.239213869239));
#180415=CARTESIAN_POINT('Ctrl Pts',(62.2082585433626,-4.03445957380163,
135.132300833172));
#180416=CARTESIAN_POINT('Ctrl Pts',(62.2156400218208,-4.14903951268851,
135.025490639782));
#180417=CARTESIAN_POINT('Ctrl Pts',(62.223021500279,-4.25949502084972,134.914015124824));
#180418=CARTESIAN_POINT('Ctrl Pts',(62.2304029787372,-4.36542533481602,
134.798229945504));
#180419=CARTESIAN_POINT('Ctrl Pts',(62.2377789958862,-4.47127727448394,
134.682530431769));
#180420=CARTESIAN_POINT('Ctrl Pts',(62.2451550130352,-4.57261043273816,
134.562527878227));
#180421=CARTESIAN_POINT('Ctrl Pts',(62.2525310301842,-4.6690599892814,134.438615613984));
#180422=CARTESIAN_POINT('Ctrl Pts',(62.2602016042513,-4.76936120228845,
134.309754986156));
#180423=CARTESIAN_POINT('Ctrl Pts',(62.2678721783185,-4.86438039852302,
134.176666214058));
#180424=CARTESIAN_POINT('Ctrl Pts',(62.2755427523856,-4.95375217877916,
134.0398312037));
#180425=CARTESIAN_POINT('Ctrl Pts',(62.2829137966036,-5.03963406171821,
133.908339492247));
#180426=CARTESIAN_POINT('Ctrl Pts',(62.2902848408216,-5.1203010331985,133.773388936696));
#180427=CARTESIAN_POINT('Ctrl Pts',(62.2976558850396,-5.19547235895497,
133.635437714686));
#180428=CARTESIAN_POINT('Ctrl Pts',(62.3050267840442,-5.27064220379776,
133.497489210385));
#180429=CARTESIAN_POINT('Ctrl Pts',(62.3123976830489,-5.34031643794952,
133.356540487433));
#180430=CARTESIAN_POINT('Ctrl Pts',(62.3197685820535,-5.40426003168304,
133.213074812412));
#180431=CARTESIAN_POINT('Ctrl Pts',(62.3271408180326,-5.4682152238599,133.069583114792));
#180432=CARTESIAN_POINT('Ctrl Pts',(62.3345130540117,-5.52643755324915,
132.923573899925));
#180433=CARTESIAN_POINT('Ctrl Pts',(62.3418852899909,-5.57874000795137,
132.775550736804));
#180434=CARTESIAN_POINT('Ctrl Pts',(62.3492603456933,-5.63106246722916,
132.627470957975));
#180435=CARTESIAN_POINT('Ctrl Pts',(62.3566354013958,-5.677460419311,132.477376051935));
#180436=CARTESIAN_POINT('Ctrl Pts',(62.3640104570983,-5.71779666927694,
132.32578488821));
#180437=CARTESIAN_POINT('Ctrl Pts',(62.3713936318705,-5.75817732471455,
132.174026840426));
#180438=CARTESIAN_POINT('Ctrl Pts',(62.3787768066428,-5.79248285793303,
132.020769609828));
#180439=CARTESIAN_POINT('Ctrl Pts',(62.386159981415,-5.82062703583033,131.866543027635));
#180440=CARTESIAN_POINT('Ctrl Pts',(62.3935479622602,-5.84878953416268,
131.712216051745));
#180441=CARTESIAN_POINT('Ctrl Pts',(62.4009359431054,-5.87078263465548,
131.556918838468));
#180442=CARTESIAN_POINT('Ctrl Pts',(62.4083239239507,-5.8865720210988,131.401185887571));
#180443=CARTESIAN_POINT('Ctrl Pts',(62.415721914078,-5.90238279910038,131.245241948711));
#180444=CARTESIAN_POINT('Ctrl Pts',(62.4231199042053,-5.91197306176435,
131.088861467507));
#180445=CARTESIAN_POINT('Ctrl Pts',(62.4305178943326,-5.91536056244642,
130.932579098112));
#180446=CARTESIAN_POINT('Ctrl Pts',(62.4325535321535,-5.91629267027411,
130.889576296485));
#180447=CARTESIAN_POINT('Ctrl Pts',(62.4345891699745,-5.91675544781438,
130.846580893109));
#180448=CARTESIAN_POINT('Ctrl Pts',(62.4366248077954,-5.91674995161543,
130.803603941404));
#180449=CARTESIAN_POINT('',(64.1866248077954,-5.91487042073829,130.809777511898));
#180450=CARTESIAN_POINT('Ctrl Pts',(62.4366248077954,-5.92641419966217,
130.803602705471));
#180451=CARTESIAN_POINT('Ctrl Pts',(62.4385326636398,-5.9264866793447,130.763257721606));
#180452=CARTESIAN_POINT('Ctrl Pts',(62.4404405194842,-5.9261104867987,130.722914125487));
#180453=CARTESIAN_POINT('Ctrl Pts',(62.5351642499328,-5.88495218713434,
128.720344364475));
#180454=CARTESIAN_POINT('Ctrl Pts',(62.7207959991417,-3.66101786007206,
124.839923614913));
#180455=CARTESIAN_POINT('Ctrl Pts',(62.9992436229541,3.03918019325866,124.50031871707));
#180456=CARTESIAN_POINT('Ctrl Pts',(63.2776912467674,6.94652012119423,129.953820356205));
#180457=CARTESIAN_POINT('Ctrl Pts',(63.55613887058,4.4703474141243,136.188926944336));
#180458=CARTESIAN_POINT('Ctrl Pts',(63.8345864943932,-2.113856177913,137.475880128848));
#180459=CARTESIAN_POINT('Ctrl Pts',(64.0447484734647,-5.61721949372411,
133.819923126594));
#180460=CARTESIAN_POINT('Ctrl Pts',(64.1620945779322,-5.91951888618433,
131.331144473255));
#180461=CARTESIAN_POINT('Ctrl Pts',(64.1866248077954,-5.91487042073829,
130.809777511898));
#180462=CARTESIAN_POINT('',(65.9366248077954,-5.90732499563075,130.802771912788));
#180463=CARTESIAN_POINT('Ctrl Pts',(64.1866248077954,-5.91487042073829,
130.809777511898));
#180464=CARTESIAN_POINT('Ctrl Pts',(64.2549104525365,-5.90193032756302,
129.358430365884));
#180465=CARTESIAN_POINT('Ctrl Pts',(64.416011971882,-4.63111467414602,125.91410477066));
#180466=CARTESIAN_POINT('Ctrl Pts',(64.6699293658316,1.14574950453723,123.90038939781));
#180467=CARTESIAN_POINT('Ctrl Pts',(64.9483769896447,6.42781211149671,128.036547041898));
#180468=CARTESIAN_POINT('Ctrl Pts',(65.2268246134574,5.80302940406682,134.716190146808));
#180469=CARTESIAN_POINT('Ctrl Pts',(65.5052722372703,-0.154453831949839,
137.801053017846));
#180470=CARTESIAN_POINT('Ctrl Pts',(65.7418723020498,-5.0959898596557,134.958976688939));
#180471=CARTESIAN_POINT('Ctrl Pts',(65.8856564922247,-5.90472330876078,
131.889541835793));
#180472=CARTESIAN_POINT('Ctrl Pts',(65.9366248077954,-5.90732499563075,
130.802771912788));
#180473=CARTESIAN_POINT('',(67.6866248077955,-5.92071699922957,130.79949226525));
#180474=CARTESIAN_POINT('Ctrl Pts',(65.9366248077954,-5.90732499563075,
130.802771912788));
#180475=CARTESIAN_POINT('Ctrl Pts',(65.978472366829,-5.90946111183665,129.910478965698));
#180476=CARTESIAN_POINT('Ctrl Pts',(66.1131358004669,-5.30008853599008,
127.041893018253));
#180477=CARTESIAN_POINT('Ctrl Pts',(66.3406151087089,-0.839967855329431,
123.856554162838));
#180478=CARTESIAN_POINT('Ctrl Pts',(66.619062732522,5.39136319930542,126.342212773363));
#180479=CARTESIAN_POINT('Ctrl Pts',(66.8975103563348,6.66829485651329,132.928367264669));
#180480=CARTESIAN_POINT('Ctrl Pts',(67.1759579801478,1.81738930489791,137.562663410783));
#180481=CARTESIAN_POINT('Ctrl Pts',(67.4389961306345,-4.3427319715742,136.073640374768));
#180482=CARTESIAN_POINT('Ctrl Pts',(67.6092184065172,-5.90614742993307,
132.440529099857));
#180483=CARTESIAN_POINT('Ctrl Pts',(67.6866248077955,-5.92071699922957,
130.79949226525));
#180484=CARTESIAN_POINT('',(69.4366248077955,-5.9204678244194,130.808252981436));
#180485=CARTESIAN_POINT('Ctrl Pts',(67.6866248077955,-5.92071699922957,
130.79949226525));
#180486=CARTESIAN_POINT('Ctrl Pts',(67.7020342811215,-5.92361739746199,
130.472807224837));
#180487=CARTESIAN_POINT('Ctrl Pts',(67.8102596290518,-5.75016475465227,
128.181482562032));
#180488=CARTESIAN_POINT('Ctrl Pts',(68.0113008515862,-2.75802833476207,
124.372343808279));
#180489=CARTESIAN_POINT('Ctrl Pts',(68.2897484753995,3.92065622231303,125.00729107194));
#180490=CARTESIAN_POINT('Ctrl Pts',(68.5681960992121,6.99644924578514,130.969462045448));
#180491=CARTESIAN_POINT('Ctrl Pts',(68.8466437230252,3.64284720793011,136.77991287238));
#180492=CARTESIAN_POINT('Ctrl Pts',(69.1250913468378,-3.05835345103424,
137.099123099097));
#180493=CARTESIAN_POINT('Ctrl Pts',(69.3217517084282,-5.80627074332086,
133.239074215812));
#180494=CARTESIAN_POINT('Ctrl Pts',(69.4255961954139,-5.92501520140697,
131.041805089321));
#180495=CARTESIAN_POINT('Ctrl Pts',(69.4366248077955,-5.92324058126049,
130.808254804363));
#180496=CARTESIAN_POINT('',(71.1866247805454,-5.91210743526078,130.807354196885));
#180497=CARTESIAN_POINT('Ctrl Pts',(69.4366248077955,-5.91674872130226,
130.808250536342));
#180498=CARTESIAN_POINT('Ctrl Pts',(69.4439407278742,-5.91685046494537,
130.653493687942));
#180499=CARTESIAN_POINT('Ctrl Pts',(69.451256647953,-5.91087639187094,130.498496518504));
#180500=CARTESIAN_POINT('Ctrl Pts',(69.4585725680317,-5.89879643630179,
130.343783625551));
#180501=CARTESIAN_POINT('Ctrl Pts',(69.4658809137479,-5.88672898742519,
130.189230910885));
#180502=CARTESIAN_POINT('Ctrl Pts',(69.473189259464,-5.86856826374107,130.034962267138));
#180503=CARTESIAN_POINT('Ctrl Pts',(69.4804976051802,-5.84433620417594,
129.881503697422));
#180504=CARTESIAN_POINT('Ctrl Pts',(69.4878000820948,-5.82012360361777,
129.728168359136));
#180505=CARTESIAN_POINT('Ctrl Pts',(69.4951025590094,-5.78984942927961,
129.575642178058));
#180506=CARTESIAN_POINT('Ctrl Pts',(69.5024050359239,-5.75358752863028,
129.424447173581));
#180507=CARTESIAN_POINT('Ctrl Pts',(69.5098876008631,-5.71643136509835,
129.269523515115));
#180508=CARTESIAN_POINT('Ctrl Pts',(69.5173701658022,-5.67298833895637,
129.115997951889));
#180509=CARTESIAN_POINT('Ctrl Pts',(69.5248527307414,-5.62339394741176,
128.964422826576));
#180510=CARTESIAN_POINT('Ctrl Pts',(69.5321494851218,-5.57503110703688,
128.8166116858));
#180511=CARTESIAN_POINT('Ctrl Pts',(69.5394462395022,-5.52081893454438,
128.670655641708));
#180512=CARTESIAN_POINT('Ctrl Pts',(69.5467429938826,-5.46093385327126,
128.527052554809));
#180513=CARTESIAN_POINT('Ctrl Pts',(69.5540393668669,-5.40105190214901,
128.383456973943));
#180514=CARTESIAN_POINT('Ctrl Pts',(69.5613357398511,-5.3354977798605,128.242214460549));
#180515=CARTESIAN_POINT('Ctrl Pts',(69.5686321128354,-5.26449616021194,
128.103803130377));
#180516=CARTESIAN_POINT('Ctrl Pts',(69.5759296374804,-5.19348333365522,
127.965369953336));
#180517=CARTESIAN_POINT('Ctrl Pts',(69.5832271621254,-5.11702147458102,
127.829769190646));
#180518=CARTESIAN_POINT('Ctrl Pts',(69.5905246867704,-5.03538118839708,
127.69745430259));
#180519=CARTESIAN_POINT('Ctrl Pts',(69.5981465124115,-4.95011281907282,
127.559259359025));
#180520=CARTESIAN_POINT('Ctrl Pts',(69.6057683380526,-4.85919544818148,
127.424649435827));
#180521=CARTESIAN_POINT('Ctrl Pts',(69.6133901636938,-4.76298711651232,
127.294106454341));
#180522=CARTESIAN_POINT('Ctrl Pts',(69.6206984429048,-4.6707366002486,127.168933746034));
#180523=CARTESIAN_POINT('Ctrl Pts',(69.6280067221158,-4.57362205408285,
127.047500299789));
#180524=CARTESIAN_POINT('Ctrl Pts',(69.6353150013268,-4.47199918411649,
126.930195693384));
#180525=CARTESIAN_POINT('Ctrl Pts',(69.6426281226757,-4.37030898339657,
126.812813366211));
#180526=CARTESIAN_POINT('Ctrl Pts',(69.6499412440246,-4.26410477346076,
126.699565604616));
#180527=CARTESIAN_POINT('Ctrl Pts',(69.6572543653735,-4.15377803744627,
126.5908040939));
#180528=CARTESIAN_POINT('Ctrl Pts',(69.6645770915714,-4.04330640138201,
126.481899738858));
#180529=CARTESIAN_POINT('Ctrl Pts',(69.6718998177694,-3.92870171892136,
126.377493647466));
#180530=CARTESIAN_POINT('Ctrl Pts',(69.6792225439673,-3.8103876164212,126.277896569866));
#180531=CARTESIAN_POINT('Ctrl Pts',(69.6801438941328,-3.79550125921326,
126.265365200885));
#180532=CARTESIAN_POINT('Ctrl Pts',(69.6810652442983,-3.78055621475712,
126.252909905282));
#180533=CARTESIAN_POINT('Ctrl Pts',(69.6819865944638,-3.76555335708998,
126.240531252065));
#180534=CARTESIAN_POINT('Ctrl Pts',(69.6894098608692,-3.64467617762322,
126.140797140098));
#180535=CARTESIAN_POINT('Ctrl Pts',(69.6968331272747,-3.51965115785384,
126.045717849011));
#180536=CARTESIAN_POINT('Ctrl Pts',(69.7042563936801,-3.3908723891784,125.95565821354));
#180537=CARTESIAN_POINT('Ctrl Pts',(69.7116708864011,-3.26224582631312,
125.865705021079));
#180538=CARTESIAN_POINT('Ctrl Pts',(69.7190853791222,-3.12987464858298,
125.780759886778));
#180539=CARTESIAN_POINT('Ctrl Pts',(69.7264998718432,-2.99418718778021,
125.701148526438));
#180540=CARTESIAN_POINT('Ctrl Pts',(69.7339072181969,-2.8586305076609,125.621613898525));
#180541=CARTESIAN_POINT('Ctrl Pts',(69.7413145645506,-2.71976422759838,
125.547402997708));
#180542=CARTESIAN_POINT('Ctrl Pts',(69.7487219109044,-2.57804683731763,
125.47879913852));
#180543=CARTESIAN_POINT('Ctrl Pts',(69.7561237325798,-2.43643514521304,
125.410246446678));
#180544=CARTESIAN_POINT('Ctrl Pts',(69.7635255542552,-2.29197691152282,
125.347292631605));
#180545=CARTESIAN_POINT('Ctrl Pts',(69.7709273759306,-2.14515638561624,
125.290175759969));
#180546=CARTESIAN_POINT('Ctrl Pts',(69.778325290242,-1.99841336512276,125.233089039885));
#180547=CARTESIAN_POINT('Ctrl Pts',(69.7857232045533,-1.84931088296295,
125.181833261727));
#180548=CARTESIAN_POINT('Ctrl Pts',(69.7931211188647,-1.69835428081799,
125.136598863635));
#180549=CARTESIAN_POINT('Ctrl Pts',(69.8005178037769,-1.54742276492156,
125.091371982678));
#180550=CARTESIAN_POINT('Ctrl Pts',(69.807914488689,-1.39463809780787,125.052164602853));
#180551=CARTESIAN_POINT('Ctrl Pts',(69.8153111736012,-1.24052205275116,
125.019117701392));
#180552=CARTESIAN_POINT('Ctrl Pts',(69.8227075305367,-1.08641284136107,
124.986072265266));
#180553=CARTESIAN_POINT('Ctrl Pts',(69.8301038874722,-0.930972734409442,
124.959186842633));
#180554=CARTESIAN_POINT('Ctrl Pts',(69.8375002444076,-0.774734738525306,
124.938551496275));
#180555=CARTESIAN_POINT('Ctrl Pts',(69.8448977337442,-0.618472822205254,
124.917912990592));
#180556=CARTESIAN_POINT('Ctrl Pts',(69.8522952230807,-0.461413143825941,
124.903526515388));
#180557=CARTESIAN_POINT('Ctrl Pts',(69.8596927124173,-0.304094739718604,
124.895430346208));
#180558=CARTESIAN_POINT('Ctrl Pts',(69.8670927949323,-0.14672118788802,
124.887331338928));
#180559=CARTESIAN_POINT('Ctrl Pts',(69.8744928774473,0.0109108976734853,
124.885527047099));
#180560=CARTESIAN_POINT('Ctrl Pts',(69.8818929599623,0.168261716740211,
124.890003631622));
#180561=CARTESIAN_POINT('Ctrl Pts',(69.8893011796288,0.325785559207997,
124.89448513861));
#180562=CARTESIAN_POINT('Ctrl Pts',(69.8967093992953,0.483027144149797,
124.905261304));
#180563=CARTESIAN_POINT('Ctrl Pts',(69.9041176189618,0.639450294128235,
124.922266272536));
#180564=CARTESIAN_POINT('Ctrl Pts',(69.9115303982638,0.795969719945647,
124.939281707346));
#180565=CARTESIAN_POINT('Ctrl Pts',(69.9189431775659,0.951669338700781,
124.962533529471));
#180566=CARTESIAN_POINT('Ctrl Pts',(69.926355956868,1.10602292486905,124.991904694966));
#180567=CARTESIAN_POINT('Ctrl Pts',(69.9337793278967,1.26059705867981,125.02131782736));
#180568=CARTESIAN_POINT('Ctrl Pts',(69.9412026989255,1.4138209560176,125.05686768192));
#180569=CARTESIAN_POINT('Ctrl Pts',(69.9486260699543,1.56518250981502,125.098387057036));
#180570=CARTESIAN_POINT('Ctrl Pts',(69.9525621193951,1.64543803750871,125.120401625966));
#180571=CARTESIAN_POINT('Ctrl Pts',(69.9564981688358,1.72517029904688,125.144093625371));
#180572=CARTESIAN_POINT('Ctrl Pts',(69.9604342182766,1.80430533129763,125.16943268245));
#180573=CARTESIAN_POINT('Ctrl Pts',(69.967857484682,1.95355153240296,125.217221353296));
#180574=CARTESIAN_POINT('Ctrl Pts',(69.9752807510875,2.10112350987105,125.271015764047));
#180575=CARTESIAN_POINT('Ctrl Pts',(69.9827040174929,2.24650130187933,125.330681556536));
#180576=CARTESIAN_POINT('Ctrl Pts',(69.9901185102139,2.39170726941065,125.390276829014));
#180577=CARTESIAN_POINT('Ctrl Pts',(69.9975330029349,2.53472387157822,125.455729529795));
#180578=CARTESIAN_POINT('Ctrl Pts',(70.0049474956559,2.67504555065757,125.526855348558));
#180579=CARTESIAN_POINT('Ctrl Pts',(70.0123548420097,2.81523198241931,125.597912613578));
#180580=CARTESIAN_POINT('Ctrl Pts',(70.0197621883634,2.95272833140933,125.674631943299));
#180581=CARTESIAN_POINT('Ctrl Pts',(70.0271695347172,3.08704841219299,125.756780735754));
#180582=CARTESIAN_POINT('Ctrl Pts',(70.0345713563926,3.22126831199298,125.83886825854));
#180583=CARTESIAN_POINT('Ctrl Pts',(70.041973178068,3.35231634345692,125.926376987033));
#180584=CARTESIAN_POINT('Ctrl Pts',(70.0493749997434,3.47973046574129,126.019028189375));
#180585=CARTESIAN_POINT('Ctrl Pts',(70.0567729140548,3.60707732710293,126.11163048187));
#180586=CARTESIAN_POINT('Ctrl Pts',(70.0641708283662,3.73079379854535,126.209369622826));
#180587=CARTESIAN_POINT('Ctrl Pts',(70.0715687426776,3.85044650954543,126.311923390444));
#180588=CARTESIAN_POINT('Ctrl Pts',(70.0789654275898,3.9700793364348,126.414460115486));
#180589=CARTESIAN_POINT('Ctrl Pts',(70.086362112502,4.08564946004065,126.521809636526));
#180590=CARTESIAN_POINT('Ctrl Pts',(70.0937587974142,4.19675624102293,126.63360917257));
#180591=CARTESIAN_POINT('Ctrl Pts',(70.1011551543496,4.30785809541419,126.745403751306));
#180592=CARTESIAN_POINT('Ctrl Pts',(70.108551511285,4.41449673755278,126.861647687931));
#180593=CARTESIAN_POINT('Ctrl Pts',(70.1159478682204,4.51630829196768,126.981941230005));
#180594=CARTESIAN_POINT('Ctrl Pts',(70.123345357557,4.61813543399169,127.102253189327));
#180595=CARTESIAN_POINT('Ctrl Pts',(70.1307428468936,4.71513377558765,127.226615703652));
#180596=CARTESIAN_POINT('Ctrl Pts',(70.1381403362302,4.80697975214996,127.354595955314));
#180597=CARTESIAN_POINT('Ctrl Pts',(70.1455404187452,4.89885792517665,127.482621070255));
#180598=CARTESIAN_POINT('Ctrl Pts',(70.1529405012601,4.98557991961542,127.614266144404));
#180599=CARTESIAN_POINT('Ctrl Pts',(70.1603405837751,5.06686560348531,127.749069548172));
#180600=CARTESIAN_POINT('Ctrl Pts',(70.1677488034416,5.14824066932122,127.884021182141));
#180601=CARTESIAN_POINT('Ctrl Pts',(70.175157023108,5.2241672936826,128.022137761481));
#180602=CARTESIAN_POINT('Ctrl Pts',(70.1825652427745,5.29441106545892,128.162932588555));
#180603=CARTESIAN_POINT('Ctrl Pts',(70.1899780220765,5.36469807110454,128.303814072495));
#180604=CARTESIAN_POINT('Ctrl Pts',(70.1973908013786,5.42929510173657,128.447376749211));
#180605=CARTESIAN_POINT('Ctrl Pts',(70.2048035806806,5.4880161919904,128.593114625156));
#180606=CARTESIAN_POINT('Ctrl Pts',(70.2122269517094,5.54682118569186,128.739060738212));
#180607=CARTESIAN_POINT('Ctrl Pts',(70.2196503227381,5.5997333454398,128.887187907311));
#180608=CARTESIAN_POINT('Ctrl Pts',(70.2270736937669,5.64661653630389,129.036974905719));
#180609=CARTESIAN_POINT('Ctrl Pts',(70.2310097432078,5.67147512904752,129.116395566368));
#180610=CARTESIAN_POINT('Ctrl Pts',(70.2349457926487,5.69463961388656,129.196282680525));
#180611=CARTESIAN_POINT('Ctrl Pts',(70.2388818420896,5.71609556543968,129.276557603673));
#180612=CARTESIAN_POINT('Ctrl Pts',(70.246305108495,5.75656082045037,129.42795360343));
#180613=CARTESIAN_POINT('Ctrl Pts',(70.2537283749005,5.79106831761621,129.581187280543));
#180614=CARTESIAN_POINT('Ctrl Pts',(70.2611516413059,5.81945004420199,129.735748552531));
#180615=CARTESIAN_POINT('Ctrl Pts',(70.2685661340269,5.84779822594401,129.890127145933));
#180616=CARTESIAN_POINT('Ctrl Pts',(70.275980626748,5.87003498190646,130.045829847321));
#180617=CARTESIAN_POINT('Ctrl Pts',(70.283395119469,5.88604211128355,130.202331692433));
#180618=CARTESIAN_POINT('Ctrl Pts',(70.2908024658228,5.90203381238663,130.358682695174));
#180619=CARTESIAN_POINT('Ctrl Pts',(70.2982098121765,5.91180780265241,130.515830939367));
#180620=CARTESIAN_POINT('Ctrl Pts',(70.3056171585303,5.91529698159951,130.67324165639));
#180621=CARTESIAN_POINT('Ctrl Pts',(70.3130189802057,5.91878355818531,130.830534970562));
#180622=CARTESIAN_POINT('Ctrl Pts',(70.3204208018811,5.91599464855981,130.988089996177));
#180623=CARTESIAN_POINT('Ctrl Pts',(70.3278226235566,5.90691501336847,131.145367343808));
#180624=CARTESIAN_POINT('Ctrl Pts',(70.3352205378679,5.8978401712459,131.302561665951));
#180625=CARTESIAN_POINT('Ctrl Pts',(70.3426184521793,5.88248123859997,131.459478230305));
#180626=CARTESIAN_POINT('Ctrl Pts',(70.3500163664906,5.86087506240501,131.615578261222));
#180627=CARTESIAN_POINT('Ctrl Pts',(70.3574130514028,5.83927247676453,131.771652351146));
#180628=CARTESIAN_POINT('Ctrl Pts',(70.3648097363151,5.81142475918317,131.926909807532));
#180629=CARTESIAN_POINT('Ctrl Pts',(70.3722064212272,5.77742057223629,132.080817469168));
#180630=CARTESIAN_POINT('Ctrl Pts',(70.3796027781627,5.74341789307072,132.234718306376));
#180631=CARTESIAN_POINT('Ctrl Pts',(70.3869991350981,5.70325936785843,132.387269103333));
#180632=CARTESIAN_POINT('Ctrl Pts',(70.3943954920335,5.65708463606796,132.537947645339));
#180633=CARTESIAN_POINT('Ctrl Pts',(70.4017929813701,5.61090283480805,132.688649256616));
#180634=CARTESIAN_POINT('Ctrl Pts',(70.4091904707067,5.55870310232612,132.837477685252));
#180635=CARTESIAN_POINT('Ctrl Pts',(70.4165879600433,5.50067468580775,132.983926758662));
#180636=CARTESIAN_POINT('Ctrl Pts',(70.4239880425583,5.44262592751775,133.130427169569));
#180637=CARTESIAN_POINT('Ctrl Pts',(70.4313881250733,5.37874455454987,133.274546217773));
#180638=CARTESIAN_POINT('Ctrl Pts',(70.4387882075884,5.30926753077319,133.415798698237));
#180639=CARTESIAN_POINT('Ctrl Pts',(70.4461964272549,5.23971410986665,133.557206500324));
#180640=CARTESIAN_POINT('Ctrl Pts',(70.4536046469213,5.16455291508093,133.695741104571));
#180641=CARTESIAN_POINT('Ctrl Pts',(70.4610128665878,5.08406671399133,133.830942222312));
#180642=CARTESIAN_POINT('Ctrl Pts',(70.4684256458899,5.00353097498771,133.966226554085));
#180643=CARTESIAN_POINT('Ctrl Pts',(70.475838425192,4.91766390208587,134.098172998918));
#180644=CARTESIAN_POINT('Ctrl Pts',(70.4832512044941,4.82679068316633,134.22635159701));
#180645=CARTESIAN_POINT('Ctrl Pts',(70.4906745755229,4.73578762033045,134.354713342694));
#180646=CARTESIAN_POINT('Ctrl Pts',(70.4980979465516,4.63976435258281,134.479296194346));
#180647=CARTESIAN_POINT('Ctrl Pts',(70.5055213175804,4.53908581848059,134.599703882011));
#180648=CARTESIAN_POINT('Ctrl Pts',(70.509457367021,4.48570364395298,134.663546927152));
#180649=CARTESIAN_POINT('Ctrl Pts',(70.5133934164617,4.43101332217446,134.726216800849));
#180650=CARTESIAN_POINT('Ctrl Pts',(70.5173294659024,4.37507322173496,134.787658857336));
#180651=CARTESIAN_POINT('Ctrl Pts',(70.5247527323078,4.26957193813348,134.903536658334));
#180652=CARTESIAN_POINT('Ctrl Pts',(70.5321759987133,4.15930425088632,135.015395338423));
#180653=CARTESIAN_POINT('Ctrl Pts',(70.5395992651187,4.04460849184142,135.122817831691));
#180654=CARTESIAN_POINT('Ctrl Pts',(70.5470137578397,3.93004829365897,135.230113360492));
#180655=CARTESIAN_POINT('Ctrl Pts',(70.5544282505607,3.81107071101288,135.33298288641));
#180656=CARTESIAN_POINT('Ctrl Pts',(70.5618427432817,3.68805352078212,135.431043207754));
#180657=CARTESIAN_POINT('Ctrl Pts',(70.5692500896354,3.56515489915108,135.529009014867));
#180658=CARTESIAN_POINT('Ctrl Pts',(70.5766574359892,3.4382247111246,135.622174614237));
#180659=CARTESIAN_POINT('Ctrl Pts',(70.5840647823429,3.30767660323895,135.710194496825));
#180660=CARTESIAN_POINT('Ctrl Pts',(70.5914666040183,3.17722586305691,135.798148730865));
#180661=CARTESIAN_POINT('Ctrl Pts',(70.5988684256938,3.04316288404195,135.880964682051));
#180662=CARTESIAN_POINT('Ctrl Pts',(70.6062702473692,2.90593323255091,135.958337975923));
#180663=CARTESIAN_POINT('Ctrl Pts',(70.6136681616805,2.76877602352488,136.035670425036));
#180664=CARTESIAN_POINT('Ctrl Pts',(70.6210660759918,2.62845579556738,136.107565755947));
#180665=CARTESIAN_POINT('Ctrl Pts',(70.6284639903032,2.48544575258087,136.173763747661));
#180666=CARTESIAN_POINT('Ctrl Pts',(70.6358606752154,2.34245947526874,136.239950738471));
#180667=CARTESIAN_POINT('Ctrl Pts',(70.6432573601277,2.1967846085204,136.300442112532));
#180668=CARTESIAN_POINT('Ctrl Pts',(70.6506540450399,2.04891764025126,136.355024277523));
#180669=CARTESIAN_POINT('Ctrl Pts',(70.6580504019754,1.90105722855834,136.409604022284));
#180670=CARTESIAN_POINT('Ctrl Pts',(70.6654467589108,1.75100525881178,136.458274949689));
#180671=CARTESIAN_POINT('Ctrl Pts',(70.6728431158463,1.59927656356989,136.500872272581));
#180672=CARTESIAN_POINT('Ctrl Pts',(70.6802406051828,1.44752463827816,136.54347611723));
#180673=CARTESIAN_POINT('Ctrl Pts',(70.6876380945194,1.29409583577123,136.580004404934));
#180674=CARTESIAN_POINT('Ctrl Pts',(70.6950355838559,1.13951830610753,136.610342756063));
#180675=CARTESIAN_POINT('Ctrl Pts',(70.7024356663709,0.984886589529773,
136.640691742254));
#180676=CARTESIAN_POINT('Ctrl Pts',(70.709835748886,0.829105710134168,136.664846399819));
#180677=CARTESIAN_POINT('Ctrl Pts',(70.717235831401,0.672711969420469,136.682743827999));
#180678=CARTESIAN_POINT('Ctrl Pts',(70.7246440510675,0.516146257711301,
136.700660936241));
#180679=CARTESIAN_POINT('Ctrl Pts',(70.732052270734,0.358966709958309,136.712307031883));
#180680=CARTESIAN_POINT('Ctrl Pts',(70.7394604904004,0.201713422834879,
136.717671218029));
#180681=CARTESIAN_POINT('Ctrl Pts',(70.7468732697025,0.0443633489371363,
136.723038705742));
#180682=CARTESIAN_POINT('Ctrl Pts',(70.7542860490046,-0.113060182341062,
136.722116581831));
#180683=CARTESIAN_POINT('Ctrl Pts',(70.7616988283066,-0.270019661649939,
136.714946032296));
#180684=CARTESIAN_POINT('Ctrl Pts',(70.7691221993354,-0.427203412023969,
136.707765237144));
#180685=CARTESIAN_POINT('Ctrl Pts',(70.7765455703642,-0.583921415204719,
136.694318216891));
#180686=CARTESIAN_POINT('Ctrl Pts',(70.783968941393,-0.739643019853316,
136.674697811091));
#180687=CARTESIAN_POINT('Ctrl Pts',(70.7879049908338,-0.822210351126378,
136.664294601151));
#180688=CARTESIAN_POINT('Ctrl Pts',(70.7918410402745,-0.904497745579814,
136.652156682058));
#180689=CARTESIAN_POINT('Ctrl Pts',(70.7957770897153,-0.98642767853512,
136.638303623589));
#180690=CARTESIAN_POINT('Ctrl Pts',(70.8032003561208,-1.14094497514307,
136.612177187655));
#180691=CARTESIAN_POINT('Ctrl Pts',(70.8106236225262,-1.29465722909891,
136.579868208319));
#180692=CARTESIAN_POINT('Ctrl Pts',(70.8180468889316,-1.4470306744114,136.541435899433));
#180693=CARTESIAN_POINT('Ctrl Pts',(70.8254613816527,-1.59922402696579,
136.503049014345));
#180694=CARTESIAN_POINT('Ctrl Pts',(70.8328758743737,-1.7500813621471,136.458553295931));
#180695=CARTESIAN_POINT('Ctrl Pts',(70.8402903670947,-1.89907608388792,
136.408059448705));
#180696=CARTESIAN_POINT('Ctrl Pts',(70.8476977134485,-2.04792719890596,
136.357614269349));
#180697=CARTESIAN_POINT('Ctrl Pts',(70.8551050598022,-2.19491892331317,
136.301182589468));
#180698=CARTESIAN_POINT('Ctrl Pts',(70.862512406156,-2.3395369845147,136.238925665533));
#180699=CARTESIAN_POINT('Ctrl Pts',(70.8699142278314,-2.48404718411098,
136.176715175161));
#180700=CARTESIAN_POINT('Ctrl Pts',(70.8773160495068,-2.62618690414198,
136.108688238563));
#180701=CARTESIAN_POINT('Ctrl Pts',(70.8847178711823,-2.76545922625434,
136.035055201503));
#180702=CARTESIAN_POINT('Ctrl Pts',(70.8921157854936,-2.90465802759125,
135.96146103475));
#180703=CARTESIAN_POINT('Ctrl Pts',(70.899513699805,-3.04099211639179,135.882266835393));
#180704=CARTESIAN_POINT('Ctrl Pts',(70.9069116141163,-3.17398678309439,
135.797730067471));
#180705=CARTESIAN_POINT('Ctrl Pts',(70.9143082990285,-3.30695934849587,
135.713207348026));
#180706=CARTESIAN_POINT('Ctrl Pts',(70.9217049839407,-3.43659327848189,
135.623344022168));
#180707=CARTESIAN_POINT('Ctrl Pts',(70.9291016688529,-3.5624405079365,135.528442347375));
#180708=CARTESIAN_POINT('Ctrl Pts',(70.9364980257884,-3.68828215719317,
135.433544880621));
#180709=CARTESIAN_POINT('Ctrl Pts',(70.9438943827238,-3.81033714172265,
135.333609733897));
#180710=CARTESIAN_POINT('Ctrl Pts',(70.9512907396592,-3.928188541847,135.228980978931));
#180711=CARTESIAN_POINT('Ctrl Pts',(70.9586882289958,-4.04605798532149,
135.124336205035));
#180712=CARTESIAN_POINT('Ctrl Pts',(70.9660857183324,-4.15972228376363,
135.014996639913));
#180713=CARTESIAN_POINT('Ctrl Pts',(70.9734832076689,-4.26879972834428,
134.901344806184));
#180714=CARTESIAN_POINT('Ctrl Pts',(70.9808832901838,-4.37791540985311,
134.787653131982));
#180715=CARTESIAN_POINT('Ctrl Pts',(70.9882833726988,-4.48244077783003,
134.669646448629));
#180716=CARTESIAN_POINT('Ctrl Pts',(70.9956834552137,-4.58203302802309,
134.547741962367));
#180717=CARTESIAN_POINT('Ctrl Pts',(71.0030916748801,-4.68173479013442,
134.42570342959));
#180718=CARTESIAN_POINT('Ctrl Pts',(71.0104998945465,-4.77649236511753,
134.299758823676));
#180719=CARTESIAN_POINT('Ctrl Pts',(71.017908114213,-4.86600464965862,134.170356653214));
#180720=CARTESIAN_POINT('Ctrl Pts',(71.025320893515,-4.95557202751718,134.040874837876));
#180721=CARTESIAN_POINT('Ctrl Pts',(71.0327336728171,-5.03988748249446,
133.907931532048));
#180722=CARTESIAN_POINT('Ctrl Pts',(71.0401464521191,-5.11869512860509,
133.772001219609));
#180723=CARTESIAN_POINT('Ctrl Pts',(71.0475698231479,-5.19761537877647,
133.635876683564));
#180724=CARTESIAN_POINT('Ctrl Pts',(71.0549931941766,-5.27101192856715,
133.496756946096));
#180725=CARTESIAN_POINT('Ctrl Pts',(71.0624165652054,-5.33867605651321,
133.355138641251));
#180726=CARTESIAN_POINT('Ctrl Pts',(71.0663526146463,-5.37455320072993,
133.280049217935));
#180727=CARTESIAN_POINT('Ctrl Pts',(71.0702886640872,-5.40881957231786,
133.204257660723));
#180728=CARTESIAN_POINT('Ctrl Pts',(71.0742247135281,-5.44144973190216,
133.127839771267));
#180729=CARTESIAN_POINT('Ctrl Pts',(71.0824664643207,-5.50977449449734,
132.967827248446));
#180730=CARTESIAN_POINT('Ctrl Pts',(71.0907082151132,-5.57109886347091,
132.804654973488));
#180731=CARTESIAN_POINT('Ctrl Pts',(71.0989499659057,-5.62515069641183,
132.638920566207));
#180732=CARTESIAN_POINT('Ctrl Pts',(71.1071583725541,-5.67898384861912,
132.473856680531));
#180733=CARTESIAN_POINT('Ctrl Pts',(71.1153667792024,-5.72560307789162,
132.306251557788));
#180734=CARTESIAN_POINT('Ctrl Pts',(71.1235751858508,-5.76478541520492,
132.136719307687));
#180735=CARTESIAN_POINT('Ctrl Pts',(71.1317620467689,-5.80386490526583,
131.967632052125));
#180736=CARTESIAN_POINT('Ctrl Pts',(71.139948907687,-5.83554637754198,131.796627980267));
#180737=CARTESIAN_POINT('Ctrl Pts',(71.1481357686052,-5.85965608173033,
131.624336938164));
#180738=CARTESIAN_POINT('Ctrl Pts',(71.1562874406351,-5.88366215722719,
131.452786439997));
#180739=CARTESIAN_POINT('Ctrl Pts',(71.164439112665,-5.90016132245018,131.279960230598));
#180740=CARTESIAN_POINT('Ctrl Pts',(71.172590784695,-5.90903071560393,131.106497282917));
#180741=CARTESIAN_POINT('Ctrl Pts',(71.1772687719017,-5.91412058030319,
131.006952373956));
#180742=CARTESIAN_POINT('Ctrl Pts',(71.1819467591085,-5.91669867470891,
130.907198071244));
#180743=CARTESIAN_POINT('Ctrl Pts',(71.1866247463153,-5.91674924113994,
130.807357277356));
#180744=CARTESIAN_POINT('',(72.9366248426605,-5.91499535916685,130.799390962839));
#180745=CARTESIAN_POINT('Ctrl Pts',(71.1866248077955,-5.90841215785675,
130.807351744564));
#180746=CARTESIAN_POINT('Ctrl Pts',(71.2419739843107,-5.90303659312473,
129.627713360534));
#180747=CARTESIAN_POINT('Ctrl Pts',(71.3901390354303,-4.98822362966825,
126.46224284269));
#180748=CARTESIAN_POINT('Ctrl Pts',(71.6311199611539,0.175748641439395,
123.808170729825));
#180749=CARTESIAN_POINT('Ctrl Pts',(71.9095675849669,5.98108912855082,127.170611401303));
#180750=CARTESIAN_POINT('Ctrl Pts',(72.1880152087798,6.29010089897139,133.872290084015));
#180751=CARTESIAN_POINT('Ctrl Pts',(72.4664628325927,0.818817231748582,
137.754691463744));
#180752=CARTESIAN_POINT('Ctrl Pts',(72.7159993655978,-4.75871170394957,
135.510131186065));
#180753=CARTESIAN_POINT('Ctrl Pts',(72.8727200239988,-5.90151843304881,
132.159149211696));
#180754=CARTESIAN_POINT('Ctrl Pts',(72.9366248077954,-5.91226047810136,
130.799394002698));
#180755=CARTESIAN_POINT('',(74.6866248077955,-5.92105151543396,130.803381673069));
#180756=CARTESIAN_POINT('Ctrl Pts',(72.9366248650027,-5.91674791128255,
130.799389014852));
#180757=CARTESIAN_POINT('Ctrl Pts',(72.945430803682,-5.91659035247599,130.611876899878));
#180758=CARTESIAN_POINT('Ctrl Pts',(72.9542367423612,-5.90751514879322,
130.424749374994));
#180759=CARTESIAN_POINT('Ctrl Pts',(72.9630426810405,-5.88965462586106,
130.238764515587));
#180760=CARTESIAN_POINT('Ctrl Pts',(72.9719130074933,-5.87166350932068,
130.051419761291));
#180761=CARTESIAN_POINT('Ctrl Pts',(72.9807833339461,-5.84475822811481,
129.865234475));
#180762=CARTESIAN_POINT('Ctrl Pts',(72.989653660399,-5.80912273554289,129.680962377449));
#180763=CARTESIAN_POINT('Ctrl Pts',(72.998594956327,-5.77320213145674,129.495215960533));
#180764=CARTESIAN_POINT('Ctrl Pts',(73.007536252255,-5.72841111589955,129.311413496325));
#180765=CARTESIAN_POINT('Ctrl Pts',(73.0164775481831,-5.67498623746573,
129.130305132501));
#180766=CARTESIAN_POINT('Ctrl Pts',(73.0187710588615,-5.66128234821181,
129.083849454294));
#180767=CARTESIAN_POINT('Ctrl Pts',(73.02106456954,-5.64701062660013,129.037570925487));
#180768=CARTESIAN_POINT('Ctrl Pts',(73.0233580802185,-5.63217556439491,
128.991481974542));
#180769=CARTESIAN_POINT('Ctrl Pts',(73.0307813466239,-5.58415982157597,
128.842308672483));
#180770=CARTESIAN_POINT('Ctrl Pts',(73.0382046130293,-5.53014089368967,
128.694818731837));
#180771=CARTESIAN_POINT('Ctrl Pts',(73.0456278794347,-5.4702539300403,128.549531909354));
#180772=CARTESIAN_POINT('Ctrl Pts',(73.0530423721557,-5.41043774780861,
128.404416803829));
#180773=CARTESIAN_POINT('Ctrl Pts',(73.0604568648767,-5.34476747589827,
128.261499975141));
#180774=CARTESIAN_POINT('Ctrl Pts',(73.0678713575977,-5.27342819378993,
128.121286699941));
#180775=CARTESIAN_POINT('Ctrl Pts',(73.0752787039515,-5.20215767116756,
127.981208567574));
#180776=CARTESIAN_POINT('Ctrl Pts',(73.0826860503052,-5.12522918424966,
127.843829131562));
#180777=CARTESIAN_POINT('Ctrl Pts',(73.090093396659,-5.04287607462456,127.709634222797));
#180778=CARTESIAN_POINT('Ctrl Pts',(73.0974952183343,-4.96058438705569,
127.575539401658));
#180779=CARTESIAN_POINT('Ctrl Pts',(73.1048970400097,-4.87287632710042,
127.444624695334));
#180780=CARTESIAN_POINT('Ctrl Pts',(73.1122988616851,-4.78003132944284,
127.317351719951));
#180781=CARTESIAN_POINT('Ctrl Pts',(73.1196967759964,-4.6872353439367,127.190145930981));
#180782=CARTESIAN_POINT('Ctrl Pts',(73.1270946903077,-4.58930804075162,
127.066578345136));
#180783=CARTESIAN_POINT('Ctrl Pts',(73.1344926046191,-4.48657230083255,
126.947081842069));
#180784=CARTESIAN_POINT('Ctrl Pts',(73.1418892895313,-4.38385363372979,
126.827605197153));
#180785=CARTESIAN_POINT('Ctrl Pts',(73.1492859744434,-4.27632835894441,
126.712198575072));
#180786=CARTESIAN_POINT('Ctrl Pts',(73.1566826593556,-4.16435986675526,
126.601262062612));
#180787=CARTESIAN_POINT('Ctrl Pts',(73.164079016291,-4.05239633936639,126.490330469193));
#180788=CARTESIAN_POINT('Ctrl Pts',(73.1714753732265,-3.9359902514904,126.383868854023));
#180789=CARTESIAN_POINT('Ctrl Pts',(73.1788717301619,-3.81554190886022,
126.282240483798));
#180790=CARTESIAN_POINT('Ctrl Pts',(73.1862692194984,-3.6950751252813,126.18059655401));
#180791=CARTESIAN_POINT('Ctrl Pts',(73.193666708835,-3.57056514000339,126.083787583313));
#180792=CARTESIAN_POINT('Ctrl Pts',(73.2010641981715,-3.44244526259913,
125.992136477264));
#180793=CARTESIAN_POINT('Ctrl Pts',(73.2084642806865,-3.31428047297036,
125.900453243061));
#180794=CARTESIAN_POINT('Ctrl Pts',(73.2158643632015,-3.1825035751514,125.813931690438));
#180795=CARTESIAN_POINT('Ctrl Pts',(73.2232644457165,-3.04757662451002,
125.732851248528));
#180796=CARTESIAN_POINT('Ctrl Pts',(73.2306726653829,-2.91250130781558,
125.651681650337));
#180797=CARTESIAN_POINT('Ctrl Pts',(73.2380808850493,-2.77426934101548,
125.57596530382));
#180798=CARTESIAN_POINT('Ctrl Pts',(73.2454891047157,-2.63336777791731,
125.505935879144));
#180799=CARTESIAN_POINT('Ctrl Pts',(73.2529018840178,-2.49237949225783,
125.435863352525));
#180800=CARTESIAN_POINT('Ctrl Pts',(73.2603146633198,-2.34871867610027,
125.37148487465));
#180801=CARTESIAN_POINT('Ctrl Pts',(73.2677274426219,-2.2028916054145,125.312985640632));
#180802=CARTESIAN_POINT('Ctrl Pts',(73.2751508136506,-2.05685617017173,
125.254402820165));
#180803=CARTESIAN_POINT('Ctrl Pts',(73.2825741846794,-1.90864864930206,
125.201716146024));
#180804=CARTESIAN_POINT('Ctrl Pts',(73.2899975557081,-1.75879047610902,
125.155060959763));
#180805=CARTESIAN_POINT('Ctrl Pts',(73.2939336051492,-1.67933207687891,
125.13032326053));
#180806=CARTESIAN_POINT('Ctrl Pts',(73.2978696545902,-1.59940980282377,
125.107280377103));
#180807=CARTESIAN_POINT('Ctrl Pts',(73.3018057040313,-1.51910232032421,
125.085946615162));
#180808=CARTESIAN_POINT('Ctrl Pts',(73.3092289704367,-1.36764491465122,
125.045711805949));
#180809=CARTESIAN_POINT('Ctrl Pts',(73.3166522368422,-1.2143589004448,125.011437544314));
#180810=CARTESIAN_POINT('Ctrl Pts',(73.3240755032476,-1.05975461527935,
124.983291066539));
#180811=CARTESIAN_POINT('Ctrl Pts',(73.3314899959686,-0.905333059539768,
124.955177855563));
#180812=CARTESIAN_POINT('Ctrl Pts',(73.3389044886896,-0.749596697896401,
124.933178078357));
#180813=CARTESIAN_POINT('Ctrl Pts',(73.3463189814106,-0.593070673885265,
124.917409136682));
#180814=CARTESIAN_POINT('Ctrl Pts',(73.3537263277644,-0.436695515549284,
124.901655393708));
#180815=CARTESIAN_POINT('Ctrl Pts',(73.3611336741181,-0.27953257898284,
124.892120567636));
#180816=CARTESIAN_POINT('Ctrl Pts',(73.3685410204719,-0.122116734302222,
124.888870945045));
#180817=CARTESIAN_POINT('Ctrl Pts',(73.3759428421473,0.0351817037025853,
124.885623746145));
#180818=CARTESIAN_POINT('Ctrl Pts',(73.3833446638227,0.192732302624848,
124.888652424469));
#180819=CARTESIAN_POINT('Ctrl Pts',(73.3907464854981,0.349995650471745,
124.897971398496));
#180820=CARTESIAN_POINT('Ctrl Pts',(73.3981443998094,0.507175980221113,
124.907285453109));
#180821=CARTESIAN_POINT('Ctrl Pts',(73.4055423141208,0.664068989187735,
124.922883168268));
#180822=CARTESIAN_POINT('Ctrl Pts',(73.4129402284321,0.820135958420872,
124.944726877117));
#180823=CARTESIAN_POINT('Ctrl Pts',(73.4203369133443,0.976176992155399,
124.966566955938));
#180824=CARTESIAN_POINT('Ctrl Pts',(73.4277335982566,1.13139188926999,124.994650916692));
#180825=CARTESIAN_POINT('Ctrl Pts',(73.4351302831688,1.28524762409922,125.028889285523));
#180826=CARTESIAN_POINT('Ctrl Pts',(73.4425266401042,1.43909653680393,125.06312613619));
#180827=CARTESIAN_POINT('Ctrl Pts',(73.4499229970396,1.59158604266972,125.103516771243));
#180828=CARTESIAN_POINT('Ctrl Pts',(73.457319353975,1.7421941401116,125.149920756655));
#180829=CARTESIAN_POINT('Ctrl Pts',(73.4647168433116,1.89282529603757,125.196331846635));
#180830=CARTESIAN_POINT('Ctrl Pts',(73.4721143326482,2.04157411322565,125.248758010204));
#180831=CARTESIAN_POINT('Ctrl Pts',(73.4795118219848,2.18793470767816,125.307009230085));
#180832=CARTESIAN_POINT('Ctrl Pts',(73.4869119044998,2.33434660861027,125.365280869842));
#180833=CARTESIAN_POINT('Ctrl Pts',(73.4943119870148,2.47836827335111,125.429381493493));
#180834=CARTESIAN_POINT('Ctrl Pts',(73.5017120695298,2.61951485804302,125.499073399046));
#180835=CARTESIAN_POINT('Ctrl Pts',(73.5091202891963,2.76081664791502,125.568841938013));
#180836=CARTESIAN_POINT('Ctrl Pts',(73.5165285088627,2.89923670919764,125.644213871848));
#180837=CARTESIAN_POINT('Ctrl Pts',(73.5239367285292,3.0343151840806,125.724905732821));
#180838=CARTESIAN_POINT('Ctrl Pts',(73.5313495078312,3.16947679751105,125.805647258289));
#180839=CARTESIAN_POINT('Ctrl Pts',(73.5387622871333,3.30129241448396,125.891715031785));
#180840=CARTESIAN_POINT('Ctrl Pts',(73.5461750664354,3.42933257057741,125.98278321148));
#180841=CARTESIAN_POINT('Ctrl Pts',(73.5535984374641,3.55755567645037,126.073981513662));
#180842=CARTESIAN_POINT('Ctrl Pts',(73.5610218084928,3.68199225276942,126.170194264108));
#180843=CARTESIAN_POINT('Ctrl Pts',(73.5684451795216,3.80224658541458,126.271055921629));
#180844=CARTESIAN_POINT('Ctrl Pts',(73.5723812289625,3.86600831804772,126.324535192591));
#180845=CARTESIAN_POINT('Ctrl Pts',(73.5763172784034,3.92859488981757,126.379320823921));
#180846=CARTESIAN_POINT('Ctrl Pts',(73.5802533278442,3.98995174384923,126.435354363936));
#180847=CARTESIAN_POINT('Ctrl Pts',(73.5876765942497,4.10566885566872,126.541031871657));
#180848=CARTESIAN_POINT('Ctrl Pts',(73.5950998606552,4.21735959757791,126.651469661085));
#180849=CARTESIAN_POINT('Ctrl Pts',(73.6025231270606,4.32460741903181,126.766328766063));
#180850=CARTESIAN_POINT('Ctrl Pts',(73.6099376197817,4.4317284824672,126.881052117117));
#180851=CARTESIAN_POINT('Ctrl Pts',(73.6173521125027,4.53441682563771,127.000186111896));
#180852=CARTESIAN_POINT('Ctrl Pts',(73.6247666052237,4.63228982220687,127.123352390792));
#180853=CARTESIAN_POINT('Ctrl Pts',(73.6321739515775,4.73006848509707,127.246399957391));
#180854=CARTESIAN_POINT('Ctrl Pts',(73.6395812979313,4.82304081044393,127.373471780618));
#180855=CARTESIAN_POINT('Ctrl Pts',(73.6469886442851,4.91086191911022,127.504153688609));
#180856=CARTESIAN_POINT('Ctrl Pts',(73.6543904659605,4.99861752748036,127.634738129104));
#180857=CARTESIAN_POINT('Ctrl Pts',(73.661792287636,5.08122936173455,127.768926984656));
#180858=CARTESIAN_POINT('Ctrl Pts',(73.6691941093114,5.15839372584091,127.90627422622));
#180859=CARTESIAN_POINT('Ctrl Pts',(73.6765920236228,5.23551735548016,128.043548963244));
#180860=CARTESIAN_POINT('Ctrl Pts',(73.6839899379341,5.30719905963787,128.183978441169));
#180861=CARTESIAN_POINT('Ctrl Pts',(73.6913878522455,5.37317933775536,128.327089060627));
#180862=CARTESIAN_POINT('Ctrl Pts',(73.6987845371577,5.43914865114758,128.470175897697));
#180863=CARTESIAN_POINT('Ctrl Pts',(73.70618122207,5.49941826281195,128.61594265333));
#180864=CARTESIAN_POINT('Ctrl Pts',(73.7135779069822,5.55377533624324,128.763892515136));
#180865=CARTESIAN_POINT('Ctrl Pts',(73.7209742639176,5.6081299994249,128.911835816689));
#180866=CARTESIAN_POINT('Ctrl Pts',(73.7283706208531,5.6565725169158,129.061961681544));
#180867=CARTESIAN_POINT('Ctrl Pts',(73.7357669777886,5.6989388852343,129.213755026961));
#180868=CARTESIAN_POINT('Ctrl Pts',(73.7431644671252,5.74131173995197,129.365571612326));
#180869=CARTESIAN_POINT('Ctrl Pts',(73.7505619564618,5.7776064928376,129.519055827002));
#180870=CARTESIAN_POINT('Ctrl Pts',(73.7579594457983,5.80770956814848,129.673679347474));
#180871=CARTESIAN_POINT('Ctrl Pts',(73.7653595283134,5.83782319604574,129.828357070982));
#180872=CARTESIAN_POINT('Ctrl Pts',(73.7727596108284,5.86174075366047,129.984174529263));
#180873=CARTESIAN_POINT('Ctrl Pts',(73.7801596933434,5.87940015646438,130.140595325715));
#180874=CARTESIAN_POINT('Ctrl Pts',(73.7875679130099,5.89707897759708,130.297188122912));
#180875=CARTESIAN_POINT('Ctrl Pts',(73.7949761326763,5.90848585923868,130.454385212029));
#180876=CARTESIAN_POINT('Ctrl Pts',(73.8023843523428,5.91361072643859,130.611646480434));
#180877=CARTESIAN_POINT('Ctrl Pts',(73.8097971316449,5.91873874790875,130.769004540526));
#180878=CARTESIAN_POINT('Ctrl Pts',(73.817209910947,5.9175770532492,130.926426486195));
#180879=CARTESIAN_POINT('Ctrl Pts',(73.8246226902491,5.91016764640917,131.083374871392));
#180880=CARTESIAN_POINT('Ctrl Pts',(73.8320460612779,5.90274765266118,131.240547511802));
#180881=CARTESIAN_POINT('Ctrl Pts',(73.8394694323067,5.88906214985623,131.39724486943));
#180882=CARTESIAN_POINT('Ctrl Pts',(73.8468928033354,5.86920478500243,131.552936434838));
#180883=CARTESIAN_POINT('Ctrl Pts',(73.850828852776,5.85867593368659,131.635487838581));
#180884=CARTESIAN_POINT('Ctrl Pts',(73.8547649022166,5.84641280124301,131.717756665896));
#180885=CARTESIAN_POINT('Ctrl Pts',(73.8587009516572,5.83243507540528,131.799665421976));
#180886=CARTESIAN_POINT('Ctrl Pts',(73.8661242180626,5.80607352070382,131.954142779668));
#180887=CARTESIAN_POINT('Ctrl Pts',(73.873547484468,5.77353065489684,132.107805686861));
#180888=CARTESIAN_POINT('Ctrl Pts',(73.8809707508734,5.73486650406995,132.260120468296));
#180889=CARTESIAN_POINT('Ctrl Pts',(73.8883852435944,5.69624805105844,132.412255226308));
#180890=CARTESIAN_POINT('Ctrl Pts',(73.8957997363155,5.65152280498643,132.56304467189));
#180891=CARTESIAN_POINT('Ctrl Pts',(73.9032142290365,5.60080227162785,132.711962378057));
#180892=CARTESIAN_POINT('Ctrl Pts',(73.9106215753903,5.55013062462896,132.860736551732));
#180893=CARTESIAN_POINT('Ctrl Pts',(73.918028921744,5.49347531371264,133.007642226515));
#180894=CARTESIAN_POINT('Ctrl Pts',(73.9254362680978,5.43099837779956,133.152165375811));
#180895=CARTESIAN_POINT('Ctrl Pts',(73.9328380897732,5.36856803954236,133.29658073429));
#180896=CARTESIAN_POINT('Ctrl Pts',(73.9402399114486,5.30032486926107,133.438616764308));
#180897=CARTESIAN_POINT('Ctrl Pts',(73.947641733124,5.22647996870166,133.577776868196));
#180898=CARTESIAN_POINT('Ctrl Pts',(73.9550396474354,5.1526740502905,133.716863510549));
#180899=CARTESIAN_POINT('Ctrl Pts',(73.9624375617467,5.07327246536376,133.853076921387));
#180900=CARTESIAN_POINT('Ctrl Pts',(73.9698354760581,4.98853340009094,133.985942783514));
#180901=CARTESIAN_POINT('Ctrl Pts',(73.9772321609703,4.90380841691344,134.118786565745));
#180902=CARTESIAN_POINT('Ctrl Pts',(73.9846288458825,4.8137479143422,134.248283588933));
#180903=CARTESIAN_POINT('Ctrl Pts',(73.9920255307947,4.71865483138288,134.373986248464));
#180904=CARTESIAN_POINT('Ctrl Pts',(73.9994218877301,4.6235659649505,134.499683334209));
#180905=CARTESIAN_POINT('Ctrl Pts',(74.0068182446656,4.523445187041,134.621586093119));
#180906=CARTESIAN_POINT('Ctrl Pts',(74.014214601601,4.4186372034637,134.73927812962));
#180907=CARTESIAN_POINT('Ctrl Pts',(74.0216120909376,4.31381317351656,134.856988185071));
#180908=CARTESIAN_POINT('Ctrl Pts',(74.0290095802742,4.20430075729512,134.970485955687));
#180909=CARTESIAN_POINT('Ctrl Pts',(74.0364070696108,4.09048305787075,135.079390315214));
#180910=CARTESIAN_POINT('Ctrl Pts',(74.0438071521258,3.97662545982813,135.188332850996));
#180911=CARTESIAN_POINT('Ctrl Pts',(74.0512072346407,3.85845984330652,135.292678511851));
#180912=CARTESIAN_POINT('Ctrl Pts',(74.0586073171557,3.73640393575553,135.392085128843));
#180913=CARTESIAN_POINT('Ctrl Pts',(74.0660155368222,3.61421381518662,135.491601053629));
#180914=CARTESIAN_POINT('Ctrl Pts',(74.0734237564887,3.48812515021597,135.586166852634));
#180915=CARTESIAN_POINT('Ctrl Pts',(74.0808319761552,3.35858690714007,135.675482105446));
#180916=CARTESIAN_POINT('Ctrl Pts',(74.0882447554572,3.22896893543684,135.764852330306));
#180917=CARTESIAN_POINT('Ctrl Pts',(74.0956575347593,3.09589746978524,135.848965370567));
#180918=CARTESIAN_POINT('Ctrl Pts',(74.1030703140613,2.95984738292835,135.927566062624));
#180919=CARTESIAN_POINT('Ctrl Pts',(74.1104936850901,2.82360290132734,136.006279063036));
#180920=CARTESIAN_POINT('Ctrl Pts',(74.1179170561189,2.68437162790257,136.079463811276));
#180921=CARTESIAN_POINT('Ctrl Pts',(74.1253404271476,2.5426505137647,136.146912341916));
#180922=CARTESIAN_POINT('Ctrl Pts',(74.1292764765885,2.46750657849685,136.182675171266));
#180923=CARTESIAN_POINT('Ctrl Pts',(74.1332125260293,2.3916629614686,136.216826161325));
#180924=CARTESIAN_POINT('Ctrl Pts',(74.1371485754701,2.31519550295665,136.249339988104));
#180925=CARTESIAN_POINT('Ctrl Pts',(74.1445718418755,2.17098026267194,136.310660050688));
#180926=CARTESIAN_POINT('Ctrl Pts',(74.1519951082809,2.0241090930186,136.366339370785));
#180927=CARTESIAN_POINT('Ctrl Pts',(74.1594183746864,1.87506343567259,136.41613998553));
#180928=CARTESIAN_POINT('Ctrl Pts',(74.1668328674074,1.726193937916,136.465881740083));
#180929=CARTESIAN_POINT('Ctrl Pts',(74.1742473601283,1.57515541879241,136.509758502452));
#180930=CARTESIAN_POINT('Ctrl Pts',(74.1816618528493,1.4224510478273,136.547579538958));
#180931=CARTESIAN_POINT('Ctrl Pts',(74.1890691992031,1.26989385908415,136.585364122125));
#180932=CARTESIAN_POINT('Ctrl Pts',(74.1964765455569,1.11567437487134,136.61710451008));
#180933=CARTESIAN_POINT('Ctrl Pts',(74.2038838919107,0.960312646315376,
136.642659186826));
#180934=CARTESIAN_POINT('Ctrl Pts',(74.2112857135861,0.805066792397916,
136.668194803931));
#180935=CARTESIAN_POINT('Ctrl Pts',(74.2186875352614,0.648680757205681,
136.687553835673));
#180936=CARTESIAN_POINT('Ctrl Pts',(74.2260893569368,0.491686448070869,
136.700645464763));
#180937=CARTESIAN_POINT('Ctrl Pts',(74.2334872712482,0.334775015009695,
136.713730182883));
#180938=CARTESIAN_POINT('Ctrl Pts',(74.2408851855595,0.177256318563158,
136.72055405647));
#180939=CARTESIAN_POINT('Ctrl Pts',(74.2482830998709,0.0196689711522565,
136.72107792483));
#180940=CARTESIAN_POINT('Ctrl Pts',(74.2556797847831,-0.137892188100206,
136.721601706132));
#180941=CARTESIAN_POINT('Ctrl Pts',(74.2630764696953,-0.295521602744105,
136.715827558846));
#180942=CARTESIAN_POINT('Ctrl Pts',(74.2704731546075,-0.452678944409718,
136.703768412912));
#180943=CARTESIAN_POINT('Ctrl Pts',(74.2778695115429,-0.609829317554113,
136.691709801693));
#180944=CARTESIAN_POINT('Ctrl Pts',(74.2852658684783,-0.76650728713711,
136.673366774501));
#180945=CARTESIAN_POINT('Ctrl Pts',(74.2926622254137,-0.922176205857355,
136.648804270118));
#180946=CARTESIAN_POINT('Ctrl Pts',(74.3000597147503,-1.07786895788646,
136.624238005152));
#180947=CARTESIAN_POINT('Ctrl Pts',(74.3074572040869,-1.23255198268647,
136.593450425187));
#180948=CARTESIAN_POINT('Ctrl Pts',(74.3148546934235,-1.38569755137894,
136.556557837638));
#180949=CARTESIAN_POINT('Ctrl Pts',(74.3222547759385,-1.53889680501311,
136.519652317449));
#180950=CARTESIAN_POINT('Ctrl Pts',(74.3296548584534,-1.69055716679896,
136.476637616123));
#180951=CARTESIAN_POINT('Ctrl Pts',(74.3370549409684,-1.84016496842807,
136.427680228923));
#180952=CARTESIAN_POINT('Ctrl Pts',(74.3444631606348,-1.98993727921513,
136.378669008043));
#180953=CARTESIAN_POINT('Ctrl Pts',(74.3518713803013,-2.13765216746389,
136.323702167447));
#180954=CARTESIAN_POINT('Ctrl Pts',(74.3592795999678,-2.28281420372402,
136.262995050625));
#180955=CARTESIAN_POINT('Ctrl Pts',(74.3666923792698,-2.42806558479541,
136.202250569585));
#180956=CARTESIAN_POINT('Ctrl Pts',(74.3741051585719,-2.57076064540786,
136.13575892959));
#180957=CARTESIAN_POINT('Ctrl Pts',(74.3815179378739,-2.71042802887655,
136.063781732364));
#180958=CARTESIAN_POINT('Ctrl Pts',(74.3889413089027,-2.85029497565258,
135.991701690743));
#180959=CARTESIAN_POINT('Ctrl Pts',(74.3963646799315,-2.98712528124606,
135.914120621237));
#180960=CARTESIAN_POINT('Ctrl Pts',(74.4037880509602,-3.12047536423706,
135.831344212495));
#180961=CARTESIAN_POINT('Ctrl Pts',(74.4077241004011,-3.19118077793225,
135.787454174387));
#180962=CARTESIAN_POINT('Ctrl Pts',(74.411660149842,-3.26090830066379,135.742104235688));
#180963=CARTESIAN_POINT('Ctrl Pts',(74.4155961992829,-3.32959563312116,
135.695344514738));
#180964=CARTESIAN_POINT('Ctrl Pts',(74.4229865676082,-3.45856369964765,
135.607547964975));
#180965=CARTESIAN_POINT('Ctrl Pts',(74.4303769359336,-3.58426034178358,
135.514508215958));
#180966=CARTESIAN_POINT('Ctrl Pts',(74.4377673042589,-3.70622745252568,
135.41649771794));
#180967=CARTESIAN_POINT('Ctrl Pts',(74.4451489183431,-3.82805008745028,
135.318603317997));
#180968=CARTESIAN_POINT('Ctrl Pts',(74.4525305324272,-3.94615169233114,
135.215750121195));
#180969=CARTESIAN_POINT('Ctrl Pts',(74.4599121465114,-4.06010195808091,
135.108254511761));
#180970=CARTESIAN_POINT('Ctrl Pts',(74.4672866643554,-4.1739426788938,135.000862242145));
#180971=CARTESIAN_POINT('Ctrl Pts',(74.4746611821994,-4.2836397319908,134.888836700284));
#180972=CARTESIAN_POINT('Ctrl Pts',(74.4820357000435,-4.38879495099896,
134.772535190413));
#180973=CARTESIAN_POINT('Ctrl Pts',(74.4894047737232,-4.49387254021456,
134.656319538972));
#180974=CARTESIAN_POINT('Ctrl Pts',(74.4967738474029,-4.59441471883195,
134.53583448246));
#180975=CARTESIAN_POINT('Ctrl Pts',(74.5041429210826,-4.69005947318445,
134.411474796587));
#180976=CARTESIAN_POINT('Ctrl Pts',(74.511746333029,-4.7887457530969,134.283160443615));
#180977=CARTESIAN_POINT('Ctrl Pts',(74.5193497449753,-4.88221766942739,
134.1507212306));
#180978=CARTESIAN_POINT('Ctrl Pts',(74.5269531569216,-4.97012145377866,
134.014629032697));
#180979=CARTESIAN_POINT('Ctrl Pts',(74.5343173147514,-5.05525919803919,
133.882819204185));
#180980=CARTESIAN_POINT('Ctrl Pts',(74.5416814725812,-5.13517372494517,
133.747583154343));
#180981=CARTESIAN_POINT('Ctrl Pts',(74.549045630411,-5.20958712413971,133.609379790138));
#180982=CARTESIAN_POINT('Ctrl Pts',(74.5564096624141,-5.28399925187906,
133.471178787328));
#180983=CARTESIAN_POINT('Ctrl Pts',(74.5637736944171,-5.35291025985287,
133.330010902823));
#180984=CARTESIAN_POINT('Ctrl Pts',(74.5711377264201,-5.41608807588343,
133.18635988641));
#180985=CARTESIAN_POINT('Ctrl Pts',(74.5785031202411,-5.47927757528023,
133.042682304859));
#180986=CARTESIAN_POINT('Ctrl Pts',(74.585868514062,-5.53673162053088,132.896521022438));
#180987=CARTESIAN_POINT('Ctrl Pts',(74.593233907883,-5.58826626889062,132.748379822841));
#180988=CARTESIAN_POINT('Ctrl Pts',(74.6006021517574,-5.63982085868267,
132.60018129972));
#180989=CARTESIAN_POINT('Ctrl Pts',(74.6079703956318,-5.68545136843434,
132.450001690142));
#180990=CARTESIAN_POINT('Ctrl Pts',(74.6153386395062,-5.72502375860916,
132.298359789541));
#180991=CARTESIAN_POINT('Ctrl Pts',(74.6227149696233,-5.76463957730755,
132.146551470286));
#180992=CARTESIAN_POINT('Ctrl Pts',(74.6300912997405,-5.79818390819066,
131.993278020939));
#180993=CARTESIAN_POINT('Ctrl Pts',(74.6374676298576,-5.82557373822989,
131.839068877389));
#180994=CARTESIAN_POINT('Ctrl Pts',(74.6448488045965,-5.85298155734553,
131.684758452449));
#180995=CARTESIAN_POINT('Ctrl Pts',(74.6522299793354,-5.87422677263048,
131.529511481286));
#180996=CARTESIAN_POINT('Ctrl Pts',(74.6596111540743,-5.88927831124794,
131.373861745892));
#180997=CARTESIAN_POINT('Ctrl Pts',(74.6670021893174,-5.9043499572014,131.218004078166));
#180998=CARTESIAN_POINT('Ctrl Pts',(74.6743932245606,-5.91321138974546,
131.061742946688));
#180999=CARTESIAN_POINT('Ctrl Pts',(74.6817842598037,-5.91588359738916,
130.905611912086));
#181000=CARTESIAN_POINT('Ctrl Pts',(74.683397775801,-5.91646695948111,130.871527387562));
#181001=CARTESIAN_POINT('Ctrl Pts',(74.6850112917982,-5.91675555147155,
130.837449041975));
#181002=CARTESIAN_POINT('Ctrl Pts',(74.6866248077955,-5.91674991913294,
130.803382384264));
#181003=CARTESIAN_POINT('',(76.4366248077954,-5.91522634936544,130.8098031079));
#181004=CARTESIAN_POINT('Ctrl Pts',(74.6866248077955,-5.92633562348113,
130.803380799432));
#181005=CARTESIAN_POINT('Ctrl Pts',(74.6890978128956,-5.92645530821839,
130.751082873092));
#181006=CARTESIAN_POINT('Ctrl Pts',(74.6915708179957,-5.92582318992127,
130.698787913914));
#181007=CARTESIAN_POINT('Ctrl Pts',(74.7868596977001,-5.87215715415332,
128.684559602157));
#181008=CARTESIAN_POINT('Ctrl Pts',(74.9724914469087,-3.62464280894678,
124.817748467285));
#181009=CARTESIAN_POINT('Ctrl Pts',(75.2509390707216,3.07749837663965,124.518935868821));
#181010=CARTESIAN_POINT('Ctrl Pts',(75.5293866945345,6.95156889824953,129.996121554386));
#181011=CARTESIAN_POINT('Ctrl Pts',(75.8078343183472,4.43748720538687,136.216039454336));
#181012=CARTESIAN_POINT('Ctrl Pts',(76.0862819421603,-2.1544284459224,137.462888878506));
#181013=CARTESIAN_POINT('Ctrl Pts',(76.2958787719761,-5.62611108597975,
133.795562092127));
#181014=CARTESIAN_POINT('Ctrl Pts',(76.412659727188,-5.91981165034088,131.319080415719));
#181015=CARTESIAN_POINT('Ctrl Pts',(76.4366248077954,-5.91522634936544,
130.8098031079));
#181016=CARTESIAN_POINT('',(78.1866248462858,-5.91289176011554,130.802962071976));
#181017=CARTESIAN_POINT('Ctrl Pts',(76.4366248077954,-5.91522634936544,
130.8098031079));
#181018=CARTESIAN_POINT('Ctrl Pts',(76.5054756017923,-5.9020529485309,129.346668158248));
#181019=CARTESIAN_POINT('Ctrl Pts',(76.6671422703935,-4.61414522720397,
125.890408083284));
#181020=CARTESIAN_POINT('Ctrl Pts',(76.9216248135988,1.18775470884825,123.907491814845));
#181021=CARTESIAN_POINT('Ctrl Pts',(77.200072437412,6.444541485859,128.075726239824));
#181022=CARTESIAN_POINT('Ctrl Pts',(77.4785200612247,5.77910947071827,134.751442356751));
#181023=CARTESIAN_POINT('Ctrl Pts',(77.7569676850376,-0.197041822817637,
137.799983181025));
#181024=CARTESIAN_POINT('Ctrl Pts',(77.9930026005611,-5.10942382781107,
134.934739361913));
#181025=CARTESIAN_POINT('Ctrl Pts',(78.1362216414804,-5.9049751713417,131.877724787875));
#181026=CARTESIAN_POINT('Ctrl Pts',(78.1866248077954,-5.90723462883533,
130.802964231305));
#181027=CARTESIAN_POINT('',(79.9366248077955,-5.91765730409607,130.799401002026));
#181028=CARTESIAN_POINT('Ctrl Pts',(78.1866248725357,-5.91674983436422,
130.802960599348));
#181029=CARTESIAN_POINT('Ctrl Pts',(78.1945270335779,-5.91670989979542,
130.634189328837));
#181030=CARTESIAN_POINT('Ctrl Pts',(78.2024291946202,-5.90944460636754,
130.465609897226));
#181031=CARTESIAN_POINT('Ctrl Pts',(78.2103313556624,-5.89502840903797,
130.297832613271));
#181032=CARTESIAN_POINT('Ctrl Pts',(78.2182492070647,-5.88058358721903,
130.129722194372));
#181033=CARTESIAN_POINT('Ctrl Pts',(78.2261670584669,-5.85895952068674,
129.962417391742));
#181034=CARTESIAN_POINT('Ctrl Pts',(78.2340849098691,-5.83028189352874,
129.79651955644));
#181035=CARTESIAN_POINT('Ctrl Pts',(78.2420266193473,-5.80151785492241,
129.630121837653));
#181036=CARTESIAN_POINT('Ctrl Pts',(78.2499683288254,-5.76565778336446,
129.465139853294));
#181037=CARTESIAN_POINT('Ctrl Pts',(78.2579100383036,-5.72287817090009,
129.302163558743));
#181038=CARTESIAN_POINT('Ctrl Pts',(78.2658646621798,-5.68002899243783,
129.138922240554));
#181039=CARTESIAN_POINT('Ctrl Pts',(78.2738192860561,-5.63023788296061,
128.977693401605));
#181040=CARTESIAN_POINT('Ctrl Pts',(78.2817739099323,-5.57373019043886,
128.819048972839));
#181041=CARTESIAN_POINT('Ctrl Pts',(78.2897479198207,-5.51708478445259,
128.660017915758));
#181042=CARTESIAN_POINT('Ctrl Pts',(78.2977219297091,-5.45369016527998,
128.503584133401));
#181043=CARTESIAN_POINT('Ctrl Pts',(78.3056959395974,-5.38381942457843,
128.350298889322));
#181044=CARTESIAN_POINT('Ctrl Pts',(78.3084182706194,-5.35996551825003,
128.297967229215));
#181045=CARTESIAN_POINT('Ctrl Pts',(78.3111406016414,-5.33535717654536,
128.246002314849));
#181046=CARTESIAN_POINT('Ctrl Pts',(78.3138629326633,-5.31000644233234,
128.19442534157));
#181047=CARTESIAN_POINT('Ctrl Pts',(78.3212861990688,-5.24087992828296,
128.05378498228));
#181048=CARTESIAN_POINT('Ctrl Pts',(78.3287094654741,-5.1660575455445,127.915680173518));
#181049=CARTESIAN_POINT('Ctrl Pts',(78.3361327318796,-5.08574833795125,
127.780605600121));
#181050=CARTESIAN_POINT('Ctrl Pts',(78.3435472246006,-5.0055340491721,127.645690673652));
#181051=CARTESIAN_POINT('Ctrl Pts',(78.3509617173216,-4.91984603282031,
127.513799171315));
#181052=CARTESIAN_POINT('Ctrl Pts',(78.3583762100426,-4.82894063743904,
127.385404215008));
#181053=CARTESIAN_POINT('Ctrl Pts',(78.3657835563964,-4.73812286010017,
127.257133010595));
#181054=CARTESIAN_POINT('Ctrl Pts',(78.3731909027502,-4.64209792915583,
127.132351945622));
#181055=CARTESIAN_POINT('Ctrl Pts',(78.380598249104,-4.54116712779319,127.01150790754));
#181056=CARTESIAN_POINT('Ctrl Pts',(78.3880000707794,-4.44031160443018,
126.890753999501));
#181057=CARTESIAN_POINT('Ctrl Pts',(78.3954018924548,-4.33455773444595,
126.773931556894));
#181058=CARTESIAN_POINT('Ctrl Pts',(78.4028037141302,-4.22424889844974,
126.661456828381));
#181059=CARTESIAN_POINT('Ctrl Pts',(78.4102016284416,-4.11399829362917,
126.549041474401));
#181060=CARTESIAN_POINT('Ctrl Pts',(78.417599542753,-3.99919777225675,126.440969529504));
#181061=CARTESIAN_POINT('Ctrl Pts',(78.4249974570644,-3.88022953820049,
126.337622513157));
#181062=CARTESIAN_POINT('Ctrl Pts',(78.4323941419766,-3.76128107450676,
126.23429267121));
#181063=CARTESIAN_POINT('Ctrl Pts',(78.4397908268889,-3.63816655426999,
126.135686443999));
#181064=CARTESIAN_POINT('Ctrl Pts',(78.4471875118011,-3.51130351085463,
126.042147033826));
#181065=CARTESIAN_POINT('Ctrl Pts',(78.4545838687365,-3.38444609267964,
125.948611771288));
#181066=CARTESIAN_POINT('Ctrl Pts',(78.461980225672,-3.2538407822705,125.860143100606));
#181067=CARTESIAN_POINT('Ctrl Pts',(78.4693765826074,-3.11993630293593,
125.77704244302));
#181068=CARTESIAN_POINT('Ctrl Pts',(78.476774071944,-2.98601132248373,125.69392906251));
#181069=CARTESIAN_POINT('Ctrl Pts',(78.4841715612806,-2.84878648456505,
125.616185528377));
#181070=CARTESIAN_POINT('Ctrl Pts',(78.4915690506172,-2.7087373189545,125.544068543983));
#181071=CARTESIAN_POINT('Ctrl Pts',(78.4989691331322,-2.56863905932585,
125.471926279092));
#181072=CARTESIAN_POINT('Ctrl Pts',(78.5063692156472,-2.42571483246961,
125.405414661724));
#181073=CARTESIAN_POINT('Ctrl Pts',(78.5137692981623,-2.28046231007505,
125.34474321203));
#181074=CARTESIAN_POINT('Ctrl Pts',(78.5211775178287,-2.1350500675999,125.284005047841));
#181075=CARTESIAN_POINT('Ctrl Pts',(78.5285857374952,-1.98730476136634,
125.229120020179));
#181076=CARTESIAN_POINT('Ctrl Pts',(78.5359939571617,-1.83774216640246,
125.180248750584));
#181077=CARTESIAN_POINT('Ctrl Pts',(78.5434067364638,-1.68808751815687,
125.131347401538));
#181078=CARTESIAN_POINT('Ctrl Pts',(78.5508195157658,-1.53661371075818,
125.088467287444));
#181079=CARTESIAN_POINT('Ctrl Pts',(78.5582322950679,-1.38384851366532,
125.051718280889));
#181080=CARTESIAN_POINT('Ctrl Pts',(78.5656556660967,-1.23086503849498,
125.014916765631));
#181081=CARTESIAN_POINT('Ctrl Pts',(78.5730790371254,-1.07658685352688,
124.984263926978));
#181082=CARTESIAN_POINT('Ctrl Pts',(78.5805024081542,-0.921549500963253,
124.959818113676));
#181083=CARTESIAN_POINT('Ctrl Pts',(78.5844384575949,-0.839344976565465,
124.946856356895));
#181084=CARTESIAN_POINT('Ctrl Pts',(78.5883745070356,-0.756927080310396,
124.935638748306));
#181085=CARTESIAN_POINT('Ctrl Pts',(78.5923105564763,-0.674375721295938,
124.926168042545));
#181086=CARTESIAN_POINT('Ctrl Pts',(78.5997338228818,-0.518686434531233,
124.908306587052));
#181087=CARTESIAN_POINT('Ctrl Pts',(78.6071570892872,-0.362051622079567,
124.896607754196));
#181088=CARTESIAN_POINT('Ctrl Pts',(78.6145803556926,-0.205000469604143,
124.891163058718));
#181089=CARTESIAN_POINT('Ctrl Pts',(78.6219948484136,-0.0481349385484352,
124.885724798418));
#181090=CARTESIAN_POINT('Ctrl Pts',(78.6294093411346,0.109145583613756,
124.886525974743));
#181091=CARTESIAN_POINT('Ctrl Pts',(78.6368238338557,0.266304483379695,
124.893606648348));
#181092=CARTESIAN_POINT('Ctrl Pts',(78.6442311802094,0.423311907481,124.900680497332));
#181093=CARTESIAN_POINT('Ctrl Pts',(78.6516385265633,0.580197572140323,
124.914021777738));
#181094=CARTESIAN_POINT('Ctrl Pts',(78.659045872917,0.736422647367805,124.93361856507));
#181095=CARTESIAN_POINT('Ctrl Pts',(78.6664476945924,0.892531204040482,
124.953200736379));
#181096=CARTESIAN_POINT('Ctrl Pts',(78.6738495162679,1.04797978349757,124.979029078526));
#181097=CARTESIAN_POINT('Ctrl Pts',(78.6812513379433,1.20223257834504,125.011039688249));
#181098=CARTESIAN_POINT('Ctrl Pts',(78.6886492522546,1.35640394434237,125.04303339982));
#181099=CARTESIAN_POINT('Ctrl Pts',(78.696047166566,1.50938041830019,125.081202803749));
#181100=CARTESIAN_POINT('Ctrl Pts',(78.7034450808773,1.66063442655972,125.125432561689));
#181101=CARTESIAN_POINT('Ctrl Pts',(78.7108417657895,1.81186329914721,125.169654969446));
#181102=CARTESIAN_POINT('Ctrl Pts',(78.7182384507017,1.96136991620067,125.219935627707));
#181103=CARTESIAN_POINT('Ctrl Pts',(78.7256351356139,2.10863984492123,125.276108763054));
#181104=CARTESIAN_POINT('Ctrl Pts',(78.7330314925494,2.25590324353882,125.332279407626));
#181105=CARTESIAN_POINT('Ctrl Pts',(78.7404278494848,2.40092980223452,125.394341876737));
#181106=CARTESIAN_POINT('Ctrl Pts',(78.7478242064203,2.54322338087415,125.462081572301));
#181107=CARTESIAN_POINT('Ctrl Pts',(78.7552216957569,2.68553874502392,125.529831638986));
#181108=CARTESIAN_POINT('Ctrl Pts',(78.7626191850934,2.82511995890015,125.603260502345));
#181109=CARTESIAN_POINT('Ctrl Pts',(78.77001667443,2.96149401523343,125.682106840152));
#181110=CARTESIAN_POINT('Ctrl Pts',(78.777416756945,3.09791587728085,125.76098081742));
#181111=CARTESIAN_POINT('Ctrl Pts',(78.78481683946,3.23112802041357,125.845275863474));
#181112=CARTESIAN_POINT('Ctrl Pts',(78.792216921975,3.36068516568954,125.934686523788));
#181113=CARTESIAN_POINT('Ctrl Pts',(78.7996251416415,3.49038477236554,126.024195500314));
#181114=CARTESIAN_POINT('Ctrl Pts',(78.807033361308,3.61642104746169,126.11883111272));
#181115=CARTESIAN_POINT('Ctrl Pts',(78.8144415809744,3.73838006652545,126.218246244733));
#181116=CARTESIAN_POINT('Ctrl Pts',(78.8218543602765,3.86041414933046,126.317722565101));
#181117=CARTESIAN_POINT('Ctrl Pts',(78.8292671395786,3.97836569659867,126.421984020153));
#181118=CARTESIAN_POINT('Ctrl Pts',(78.8366799188806,4.09185699712507,126.530645971315));
#181119=CARTESIAN_POINT('Ctrl Pts',(78.8441032899094,4.20551045934395,126.639463183769));
#181120=CARTESIAN_POINT('Ctrl Pts',(78.8515266609381,4.31469068806539,126.752693182139));
#181121=CARTESIAN_POINT('Ctrl Pts',(78.8589500319669,4.41905911919642,126.869916938525));
#181122=CARTESIAN_POINT('Ctrl Pts',(78.8628860814077,4.47439776566789,126.932071786906));
#181123=CARTESIAN_POINT('Ctrl Pts',(78.8668221308484,4.52838434356865,126.995348905774));
#181124=CARTESIAN_POINT('Ctrl Pts',(78.8707581802892,4.5809733425261,127.059682554292));
#181125=CARTESIAN_POINT('Ctrl Pts',(78.8781814466946,4.68015455331391,127.181013807612));
#181126=CARTESIAN_POINT('Ctrl Pts',(78.8856047131,4.77466205487176,127.306471606538));
#181127=CARTESIAN_POINT('Ctrl Pts',(78.8930279795055,4.86413281547984,127.435660198135));
#181128=CARTESIAN_POINT('Ctrl Pts',(78.9004424722265,4.95349782907904,127.564696099546));
#181129=CARTESIAN_POINT('Ctrl Pts',(78.9078569649475,5.03783774076514,127.69745371263));
#181130=CARTESIAN_POINT('Ctrl Pts',(78.9152714576685,5.11682879366983,127.833503223013));
#181131=CARTESIAN_POINT('Ctrl Pts',(78.9226788040223,5.19574371202383,127.969421603755));
#181132=CARTESIAN_POINT('Ctrl Pts',(78.9300861503761,5.2693198488673,128.108625244604));
#181133=CARTESIAN_POINT('Ctrl Pts',(78.9374934967298,5.33727598584508,128.250654367149));
#181134=CARTESIAN_POINT('Ctrl Pts',(78.9448953184052,5.40518143857207,128.392577559015));
#181135=CARTESIAN_POINT('Ctrl Pts',(78.9522971400807,5.46747507706612,128.537321701267));
#181136=CARTESIAN_POINT('Ctrl Pts',(78.9596989617561,5.52392104796787,128.684401462696));
#181137=CARTESIAN_POINT('Ctrl Pts',(78.9670968760674,5.58033722148095,128.831403581864));
#181138=CARTESIAN_POINT('Ctrl Pts',(78.9744947903788,5.63091174177378,128.980738517087));
#181139=CARTESIAN_POINT('Ctrl Pts',(78.9818927046902,5.67545647981579,129.13190006251));
#181140=CARTESIAN_POINT('Ctrl Pts',(78.9892893896024,5.71999381533041,129.283036487627));
#181141=CARTESIAN_POINT('Ctrl Pts',(78.9966860745146,5.75850325193283,129.435998562765));
#181142=CARTESIAN_POINT('Ctrl Pts',(79.0040827594268,5.79084619600052,129.590263876459));
#181143=CARTESIAN_POINT('Ctrl Pts',(79.0114791163622,5.82318770594818,129.744522349868));
#181144=CARTESIAN_POINT('Ctrl Pts',(79.0188754732976,5.84936319043042,129.900083581578));
#181145=CARTESIAN_POINT('Ctrl Pts',(79.0262718302331,5.86928502103311,130.056414159338));
#181146=CARTESIAN_POINT('Ctrl Pts',(79.0336693195697,5.88920990171894,130.212768671708));
#181147=CARTESIAN_POINT('Ctrl Pts',(79.0410668089063,5.90287917492191,130.369892394333));
#181148=CARTESIAN_POINT('Ctrl Pts',(79.0484642982428,5.91025702645075,130.527246121753));
#181149=CARTESIAN_POINT('Ctrl Pts',(79.0558643807578,5.91763746427399,130.684655009279));
#181150=CARTESIAN_POINT('Ctrl Pts',(79.0632644632728,5.91872207191936,130.842293689474));
#181151=CARTESIAN_POINT('Ctrl Pts',(79.0706645457878,5.91352715278672,130.99962243092));
#181152=CARTESIAN_POINT('Ctrl Pts',(79.0780727654543,5.90832652130644,131.157124171491));
#181153=CARTESIAN_POINT('Ctrl Pts',(79.0854809851207,5.89683258566624,131.314314919371));
#181154=CARTESIAN_POINT('Ctrl Pts',(79.0928892047872,5.87911364833969,131.47065880337));
#181155=CARTESIAN_POINT('Ctrl Pts',(79.1003019840893,5.86138380530286,131.627098914422));
#181156=CARTESIAN_POINT('Ctrl Pts',(79.1077147633914,5.83742138275471,131.782690754884));
#181157=CARTESIAN_POINT('Ctrl Pts',(79.1151275426934,5.80734582588931,131.936908639076));
#181158=CARTESIAN_POINT('Ctrl Pts',(79.1225509137222,5.77722729565787,132.091346877013));
#181159=CARTESIAN_POINT('Ctrl Pts',(79.129974284751,5.74097827168832,132.244406875497));
#181160=CARTESIAN_POINT('Ctrl Pts',(79.1373976557797,5.69876829185863,132.395577296151));
#181161=CARTESIAN_POINT('Ctrl Pts',(79.1413337052205,5.67638754773837,132.475731480466));
#181162=CARTESIAN_POINT('Ctrl Pts',(79.1452697546613,5.65233177958366,132.555354745812));
#181163=CARTESIAN_POINT('Ctrl Pts',(79.1492058041021,5.62663169755628,132.634373268494));
#181164=CARTESIAN_POINT('Ctrl Pts',(79.1566290705075,5.57816214492473,132.783399736188));
#181165=CARTESIAN_POINT('Ctrl Pts',(79.1640523369129,5.52369455860523,132.930724578636));
#181166=CARTESIAN_POINT('Ctrl Pts',(79.1714756033183,5.4633656692368,133.075828452844));
#181167=CARTESIAN_POINT('Ctrl Pts',(79.1788900960393,5.40310808360552,133.220760826324));
#181168=CARTESIAN_POINT('Ctrl Pts',(79.1863045887604,5.33700312620981,133.363477115313));
#181169=CARTESIAN_POINT('Ctrl Pts',(79.1937190814814,5.26523741356136,133.50347260882));
#181170=CARTESIAN_POINT('Ctrl Pts',(79.2011264278352,5.19354087140873,133.6433331694));
#181171=CARTESIAN_POINT('Ctrl Pts',(79.208533774189,5.11619460507125,133.780477825228));
#181172=CARTESIAN_POINT('Ctrl Pts',(79.2159411205427,5.03343343375855,133.914421457875));
#181173=CARTESIAN_POINT('Ctrl Pts',(79.2233429422181,4.95073398884981,134.048265190307));
#181174=CARTESIAN_POINT('Ctrl Pts',(79.2307447638935,4.86262787581848,134.178912337079));
#181175=CARTESIAN_POINT('Ctrl Pts',(79.2381465855689,4.76939593305506,134.305902134706));
#181176=CARTESIAN_POINT('Ctrl Pts',(79.2455444998803,4.67621320670851,134.432824895408));
#181177=CARTESIAN_POINT('Ctrl Pts',(79.2529424141917,4.57791025988974,134.556093851872));
#181178=CARTESIAN_POINT('Ctrl Pts',(79.260340328503,4.47481128958491,134.675277109187));
#181179=CARTESIAN_POINT('Ctrl Pts',(79.2677370134152,4.37172945245855,134.794440560407));
#181180=CARTESIAN_POINT('Ctrl Pts',(79.2751336983274,4.26385341766289,134.909519377983));
#181181=CARTESIAN_POINT('Ctrl Pts',(79.2825303832396,4.15154779152017,135.020114583018));
#181182=CARTESIAN_POINT('Ctrl Pts',(79.289926740175,4.03924714512659,135.130704884146));
#181183=CARTESIAN_POINT('Ctrl Pts',(79.2973230971105,3.9225175638997,135.236811706103));
#181184=CARTESIAN_POINT('Ctrl Pts',(79.3047194540459,3.80176045737709,135.338073002271));
#181185=CARTESIAN_POINT('Ctrl Pts',(79.3121169433825,3.68098486263312,135.439349801801));
#181186=CARTESIAN_POINT('Ctrl Pts',(79.3195144327191,3.5561808008703,135.53577935852));
#181187=CARTESIAN_POINT('Ctrl Pts',(79.3269119220557,3.42778256246763,135.627040087212));
#181188=CARTESIAN_POINT('Ctrl Pts',(79.3343120045707,3.29933931426163,135.718332807211));
#181189=CARTESIAN_POINT('Ctrl Pts',(79.3417120870857,3.16729968497964,135.804452875525));
#181190=CARTESIAN_POINT('Ctrl Pts',(79.3491121696007,3.03212657833541,135.88512227065));
#181191=CARTESIAN_POINT('Ctrl Pts',(79.3565203892671,2.89680483496421,135.965880370069));
#181192=CARTESIAN_POINT('Ctrl Pts',(79.3639286089336,2.75834305393096,136.041175635316));
#181193=CARTESIAN_POINT('Ctrl Pts',(79.3713368286001,2.61722899799891,136.110775879731));
#181194=CARTESIAN_POINT('Ctrl Pts',(79.3787496079022,2.47602808871995,136.180418961934));
#181195=CARTESIAN_POINT('Ctrl Pts',(79.3861623872043,2.3321719920476,136.244359887505));
#181196=CARTESIAN_POINT('Ctrl Pts',(79.3935751665063,2.18616754527691,136.302415003117));
#181197=CARTESIAN_POINT('Ctrl Pts',(79.4009985375351,2.03995448050585,136.360553070601));
#181198=CARTESIAN_POINT('Ctrl Pts',(79.4084219085638,1.89158728601007,136.412788407988));
#181199=CARTESIAN_POINT('Ctrl Pts',(79.4158452795926,1.741587804611,136.458987261415));
#181200=CARTESIAN_POINT('Ctrl Pts',(79.4197813290334,1.66205448038528,136.483483002028));
#181201=CARTESIAN_POINT('Ctrl Pts',(79.4237173784741,1.58206244191956,136.506282522811));
#181202=CARTESIAN_POINT('Ctrl Pts',(79.4276534279149,1.50169039877162,136.527371757581));
#181203=CARTESIAN_POINT('Ctrl Pts',(79.4350766943203,1.35011123372,136.567145396185));
#181204=CARTESIAN_POINT('Ctrl Pts',(79.4424999607257,1.19672161046144,136.600952949165));
#181205=CARTESIAN_POINT('Ctrl Pts',(79.4499232271312,1.04203237321619,136.628628734306));
#181206=CARTESIAN_POINT('Ctrl Pts',(79.4573377198522,0.887525965802995,
136.656271808966));
#181207=CARTESIAN_POINT('Ctrl Pts',(79.4647522125732,0.731723365765574,
136.677797476357));
#181208=CARTESIAN_POINT('Ctrl Pts',(79.4721667052942,0.575150071538092,
136.693089933616));
#181209=CARTESIAN_POINT('Ctrl Pts',(79.479574051648,0.418727688546467,136.708367651429));
#181210=CARTESIAN_POINT('Ctrl Pts',(79.4869813980017,0.261536459217152,
136.717424083419));
#181211=CARTESIAN_POINT('Ctrl Pts',(79.4943887443555,0.104111452942493,
136.720194571276));
#181212=CARTESIAN_POINT('Ctrl Pts',(79.5017905660309,-0.0531961398232929,
136.722962992798));
#181213=CARTESIAN_POINT('Ctrl Pts',(79.5091923877063,-0.210736790727082,
136.719454798675));
#181214=CARTESIAN_POINT('Ctrl Pts',(79.5165942093817,-0.367971046389676,
136.709657212278));
#181215=CARTESIAN_POINT('Ctrl Pts',(79.5239921236931,-0.525122299312614,
136.699864797951));
#181216=CARTESIAN_POINT('Ctrl Pts',(79.5313900380044,-0.681967107482434,
136.683789626689));
#181217=CARTESIAN_POINT('Ctrl Pts',(79.5387879523158,-0.837966869088659,
136.661471004848));
#181218=CARTESIAN_POINT('Ctrl Pts',(79.546184637228,-0.993940706364406,
136.639156091958));
#181219=CARTESIAN_POINT('Ctrl Pts',(79.5535813221401,-1.14906940661803,
136.610599840533));
#181220=CARTESIAN_POINT('Ctrl Pts',(79.5609780070523,-1.30282021898066,
136.575893346358));
#181221=CARTESIAN_POINT('Ctrl Pts',(79.5683743639878,-1.45656421387115,
136.541188391105));
#181222=CARTESIAN_POINT('Ctrl Pts',(79.5757707209233,-1.60893007821654,
136.500333817537));
#181223=CARTESIAN_POINT('Ctrl Pts',(79.5831670778587,-1.75939624028258,
136.453471647824));
#181224=CARTESIAN_POINT('Ctrl Pts',(79.5905645671953,-1.90988543910226,
136.406602303393));
#181225=CARTESIAN_POINT('Ctrl Pts',(79.5979620565318,-2.058474000088,136.353723642426));
#181226=CARTESIAN_POINT('Ctrl Pts',(79.6053595458684,-2.20465661993256,
136.295027221057));
#181227=CARTESIAN_POINT('Ctrl Pts',(79.6127596283834,-2.350890483868,136.236310223747));
#181228=CARTESIAN_POINT('Ctrl Pts',(79.6201597108984,-2.49471638126169,
136.171771544599));
#181229=CARTESIAN_POINT('Ctrl Pts',(79.6275597934134,-2.63565019398481,
136.101650360203));
#181230=CARTESIAN_POINT('Ctrl Pts',(79.6349680130798,-2.77673897792317,
136.031452070356));
#181231=CARTESIAN_POINT('Ctrl Pts',(79.6423762327463,-2.91492899181364,
135.955659182587));
#181232=CARTESIAN_POINT('Ctrl Pts',(79.6497844524127,-3.04976124275421,
135.87455656296));
#181233=CARTESIAN_POINT('Ctrl Pts',(79.6571972317148,-3.18467648069582,
135.793404026024));
#181234=CARTESIAN_POINT('Ctrl Pts',(79.6646100110169,-3.31622952641147,
135.706935449793));
#181235=CARTESIAN_POINT('Ctrl Pts',(79.672022790319,-3.4439919092189,135.615477981727));
#181236=CARTESIAN_POINT('Ctrl Pts',(79.6794461613477,-3.57193684491018,
135.523889834943));
#181237=CARTESIAN_POINT('Ctrl Pts',(79.6868695323765,-3.69608000633086,
135.427298788013));
#181238=CARTESIAN_POINT('Ctrl Pts',(79.6942929034052,-3.81602679377552,
135.326071584853));
#181239=CARTESIAN_POINT('Ctrl Pts',(79.6982289528461,-3.87962545856341,
135.272398492824));
#181240=CARTESIAN_POINT('Ctrl Pts',(79.702165002287,-3.94204499181968,135.217422623261));
#181241=CARTESIAN_POINT('Ctrl Pts',(79.7061010517278,-4.00323101482898,
135.161202593632));
#181242=CARTESIAN_POINT('Ctrl Pts',(79.7134134904188,-4.11690312406568,
135.056756364984));
#181243=CARTESIAN_POINT('Ctrl Pts',(79.7207259291098,-4.22668148481328,
134.947677566942));
#181244=CARTESIAN_POINT('Ctrl Pts',(79.7280383678008,-4.3321564831283,134.834292474085));
#181245=CARTESIAN_POINT('Ctrl Pts',(79.7353420711127,-4.43750548187835,
134.721042830127));
#181246=CARTESIAN_POINT('Ctrl Pts',(79.7426457744246,-4.53856108607832,
134.60349740517));
#181247=CARTESIAN_POINT('Ctrl Pts',(79.7499494777365,-4.63494720400953,
134.482022235843));
#181248=CARTESIAN_POINT('Ctrl Pts',(79.7572461627114,-4.73124070176747,
134.360663795474));
#181249=CARTESIAN_POINT('Ctrl Pts',(79.7645428476862,-4.82287340406486,
134.235383424818));
#181250=CARTESIAN_POINT('Ctrl Pts',(79.771839532661,-4.90950671483698,134.106583259889));
#181251=CARTESIAN_POINT('Ctrl Pts',(79.7791305735189,-4.99607301318684,
133.977882724201));
#181252=CARTESIAN_POINT('Ctrl Pts',(79.7864216143768,-5.07764740490519,
133.845668133241));
#181253=CARTESIAN_POINT('Ctrl Pts',(79.7937126552347,-5.15393239403828,
133.71037359761));
#181254=CARTESIAN_POINT('Ctrl Pts',(79.8010006578554,-5.23018559458332,
133.575135440335));
#181255=CARTESIAN_POINT('Ctrl Pts',(79.8082886604761,-5.30115358817978,
133.436820226451));
#181256=CARTESIAN_POINT('Ctrl Pts',(79.8155766630968,-5.36658298783485,
133.295889786005));
#181257=CARTESIAN_POINT('Ctrl Pts',(79.8228631672246,-5.43199893449135,
133.154988322395));
#181258=CARTESIAN_POINT('Ctrl Pts',(79.8301496713525,-5.49187839129512,
133.011473051662));
#181259=CARTESIAN_POINT('Ctrl Pts',(79.8374361754803,-5.54601474745979,
132.865828779692));
#181260=CARTESIAN_POINT('Ctrl Pts',(79.8447227195084,-5.60015140007108,
132.720183710184));
#181261=CARTESIAN_POINT('Ctrl Pts',(79.8520092635366,-5.64854475669413,
132.572409977985));
#181262=CARTESIAN_POINT('Ctrl Pts',(79.8592958075647,-5.69103712586775,
132.423010361796));
#181263=CARTESIAN_POINT('Ctrl Pts',(79.866586863467,-5.733555806585,132.273518236419));
#181264=CARTESIAN_POINT('Ctrl Pts',(79.8738779193693,-5.77016609637652,
132.122398587331));
#181265=CARTESIAN_POINT('Ctrl Pts',(79.8811689752716,-5.80076069769532,
131.970167587254));
#181266=CARTESIAN_POINT('Ctrl Pts',(79.8884625230659,-5.83136575544766,
131.817884558608));
#181267=CARTESIAN_POINT('Ctrl Pts',(79.8957560708601,-5.85595096667871,
131.664489802451));
#181268=CARTESIAN_POINT('Ctrl Pts',(79.9030496186544,-5.87446066816507,
131.510506792718));
#181269=CARTESIAN_POINT('Ctrl Pts',(79.9103508269902,-5.89298981071651,
131.356362051921));
#181270=CARTESIAN_POINT('Ctrl Pts',(79.917652035326,-5.90543066925387,131.201628207417));
#181271=CARTESIAN_POINT('Ctrl Pts',(79.9249532436618,-5.91177963798963,
131.046831387663));
#181272=CARTESIAN_POINT('Ctrl Pts',(79.9288437650397,-5.91516274903892,
130.964346364803));
#181273=CARTESIAN_POINT('Ctrl Pts',(79.9327342864175,-5.91681701672771,
130.88184344256));
#181274=CARTESIAN_POINT('Ctrl Pts',(79.9366248077954,-5.91674792198156,
130.799401764183));
#181275=CARTESIAN_POINT('',(81.6866248077954,-5.92353248883006,130.808099003046));
#181276=CARTESIAN_POINT('Ctrl Pts',(79.9366248077954,-5.92036607957503,
130.799398731789));
#181277=CARTESIAN_POINT('Ctrl Pts',(79.9525994303772,-5.92340740034602,
130.460680406864));
#181278=CARTESIAN_POINT('Ctrl Pts',(80.061389927564,-5.74256826904676,128.157184786054));
#181279=CARTESIAN_POINT('Ctrl Pts',(80.2629962993529,-2.71882372294293,
124.355674077366));
#181280=CARTESIAN_POINT('Ctrl Pts',(80.5414439231668,3.95587198936288,125.031264625449));
#181281=CARTESIAN_POINT('Ctrl Pts',(80.8198915469792,6.99531459853266,131.012048358891));
#181282=CARTESIAN_POINT('Ctrl Pts',(81.0983391707924,3.60640483176838,136.801977204155));
#181283=CARTESIAN_POINT('Ctrl Pts',(81.3767867946052,-3.09661479272062,
137.080389406207));
#181284=CARTESIAN_POINT('Ctrl Pts',(81.5728820069396,-5.81315485131558,
133.214825300187));
#181285=CARTESIAN_POINT('Ctrl Pts',(81.6761613446696,-5.92516446039476,
131.029652639399));
#181286=CARTESIAN_POINT('Ctrl Pts',(81.6866248077954,-5.92353248883006,
130.808099003046));
#181287=CARTESIAN_POINT('',(83.4366248077954,-5.90860028553273,130.807517856062));
#181288=CARTESIAN_POINT('Ctrl Pts',(81.6866248077954,-5.92353248883006,
130.808099003046));
#181289=CARTESIAN_POINT('Ctrl Pts',(81.7689772192739,-5.91068809952968,
129.064366932107));
#181290=CARTESIAN_POINT('Ctrl Pts',(81.944145505357,-4.17314388298674,125.333100902792));
#181291=CARTESIAN_POINT('Ctrl Pts',(82.2121296660436,2.17468473634867,124.152420537573));
#181292=CARTESIAN_POINT('Ctrl Pts',(82.4905772898569,6.77193580165642,129.038448380621));
#181293=CARTESIAN_POINT('Ctrl Pts',(82.7690249136695,5.1461086926968,135.547263299818));
#181294=CARTESIAN_POINT('Ctrl Pts',(83.0474725374827,-1.20874090346615,
137.697582357697));
#181295=CARTESIAN_POINT('Ctrl Pts',(83.2700058355244,-5.39976777314671,
134.353588453385));
#181296=CARTESIAN_POINT('Ctrl Pts',(83.3997232589621,-5.91239030108813,
131.593925525655));
#181297=CARTESIAN_POINT('Ctrl Pts',(83.4366248077954,-5.90860028553273,
130.807517856062));
#181298=CARTESIAN_POINT('',(85.1866248077954,-5.91194855424759,130.79948298725));
#181299=CARTESIAN_POINT('Ctrl Pts',(83.4366248077954,-5.90860028553273,
130.807517856062));
#181300=CARTESIAN_POINT('Ctrl Pts',(83.4925391335664,-5.90285754109132,
129.615929534796));
#181301=CARTESIAN_POINT('Ctrl Pts',(83.6412693339418,-4.97384773570943,
126.438109061856));
#181302=CARTESIAN_POINT('Ctrl Pts',(83.8828154089211,0.218333178828223,
123.80937018488));
#181303=CARTESIAN_POINT('Ctrl Pts',(84.1612630327344,6.00309797568514,127.207087313424));
#181304=CARTESIAN_POINT('Ctrl Pts',(84.4397106565468,6.27130900052438,133.910522871902));
#181305=CARTESIAN_POINT('Ctrl Pts',(84.71815828036,0.776493424362582,137.759547063109));
#181306=CARTESIAN_POINT('Ctrl Pts',(84.9671296641093,-4.7746681124197,135.486236640735));
#181307=CARTESIAN_POINT('Ctrl Pts',(85.1232851732545,-5.90153036521254,
132.147392464895));
#181308=CARTESIAN_POINT('Ctrl Pts',(85.1866248077954,-5.91194855424759,
130.79948298725));
#181309=CARTESIAN_POINT('',(86.9366241207765,-5.92196730184553,130.803176251173));
#181310=CARTESIAN_POINT('Ctrl Pts',(85.1866248077954,-5.91194855424759,
130.79948298725));
#181311=CARTESIAN_POINT('Ctrl Pts',(85.2161010478588,-5.91679684620963,
130.172209027827));
#181312=CARTESIAN_POINT('Ctrl Pts',(85.3383931625264,-5.53558770671179,
127.575492174767));
#181313=CARTESIAN_POINT('Ctrl Pts',(85.5535011517986,-1.75560445854355,
124.029745239887));
#181314=CARTESIAN_POINT('Ctrl Pts',(85.8319487756115,4.7507286914536,125.665475774475));
#181315=CARTESIAN_POINT('Ctrl Pts',(86.1103963994243,6.8913742600039,132.023590431382));
#181316=CARTESIAN_POINT('Ctrl Pts',(86.3888440232373,2.69918354595779,137.261292452082));
#181317=CARTESIAN_POINT('Ctrl Pts',(86.6642530762223,-3.90060987699965,
136.572983623696));
#181318=CARTESIAN_POINT('Ctrl Pts',(86.846846254603,-5.92098433078664,132.701838245013));
#181319=CARTESIAN_POINT('Ctrl Pts',(86.9366235583794,-5.9262383104758,130.803187280332));
#181320=CARTESIAN_POINT('',(88.6866248062304,-5.91569305183782,130.809821120246));
#181321=CARTESIAN_POINT('Ctrl Pts',(86.9366248077953,-5.91674987874936,
130.803162778058));
#181322=CARTESIAN_POINT('Ctrl Pts',(86.9396629621512,-5.91673689178478,
130.739013432001));
#181323=CARTESIAN_POINT('Ctrl Pts',(86.9427011165071,-5.91568067838148,
130.67487583135));
#181324=CARTESIAN_POINT('Ctrl Pts',(86.945739270863,-5.91358218154266,130.610772537765));
#181325=CARTESIAN_POINT('Ctrl Pts',(86.9531625372684,-5.90845482484487,
130.454145925023));
#181326=CARTESIAN_POINT('Ctrl Pts',(86.9605858036738,-5.89709281915318,
130.297486319545));
#181327=CARTESIAN_POINT('Ctrl Pts',(86.9680090700793,-5.87948312036875,
130.141330603314));
#181328=CARTESIAN_POINT('Ctrl Pts',(86.9754235628003,-5.86189423478589,
129.985359450172));
#181329=CARTESIAN_POINT('Ctrl Pts',(86.9828380555213,-5.83807239593259,
129.829891368147));
#181330=CARTESIAN_POINT('Ctrl Pts',(86.9902525482423,-5.80805654683473,
129.675463053006));
#181331=CARTESIAN_POINT('Ctrl Pts',(86.9976598945961,-5.77806962814226,
129.521183581689));
#181332=CARTESIAN_POINT('Ctrl Pts',(87.0050672409499,-5.74190065508616,
129.367942246121));
#181333=CARTESIAN_POINT('Ctrl Pts',(87.0124745873037,-5.69964032010081,
129.21627032291));
#181334=CARTESIAN_POINT('Ctrl Pts',(87.0198764089791,-5.65741150446767,
129.064711522341));
#181335=CARTESIAN_POINT('Ctrl Pts',(87.0272782306545,-5.60910047272904,
128.914720161505));
#181336=CARTESIAN_POINT('Ctrl Pts',(87.0346800523299,-5.55484889329824,
128.766816916164));
#181337=CARTESIAN_POINT('Ctrl Pts',(87.0420779666413,-5.50062595285393,
128.618991747795));
#181338=CARTESIAN_POINT('Ctrl Pts',(87.0494758809526,-5.44046883837646,
128.473252849217));
#181339=CARTESIAN_POINT('Ctrl Pts',(87.056873795264,-5.37456889341132,128.330105219982));
#181340=CARTESIAN_POINT('Ctrl Pts',(87.0642704801762,-5.30867989982158,
128.186981379285));
#181341=CARTESIAN_POINT('Ctrl Pts',(87.0716671650885,-5.23705012580709,
128.046448292034));
#181342=CARTESIAN_POINT('Ctrl Pts',(87.0790638500007,-5.15991888229762,
127.908990573753));
#181343=CARTESIAN_POINT('Ctrl Pts',(87.0864602069362,-5.08279105886826,
127.771538950492));
#181344=CARTESIAN_POINT('Ctrl Pts',(87.0938565638716,-5.00016243365457,
127.637162750611));
#181345=CARTESIAN_POINT('Ctrl Pts',(87.1012529208071,-4.91231793758966,
127.506321345129));
#181346=CARTESIAN_POINT('Ctrl Pts',(87.1086504101436,-4.82445999230827,
127.375459907495));
#181347=CARTESIAN_POINT('Ctrl Pts',(87.1160478994802,-4.73138479422256,
127.248134651781));
#181348=CARTESIAN_POINT('Ctrl Pts',(87.1234453888168,-4.63342010767118,
127.124775224029));
#181349=CARTESIAN_POINT('Ctrl Pts',(87.1308454713318,-4.53542107975067,
127.001372552822));
#181350=CARTESIAN_POINT('Ctrl Pts',(87.1382455538468,-4.4325293828044,126.881938769633));
#181351=CARTESIAN_POINT('Ctrl Pts',(87.1456456363618,-4.32511237779127,
126.766869629096));
#181352=CARTESIAN_POINT('Ctrl Pts',(87.1530538560283,-4.21757725673839,
126.65167395821));
#181353=CARTESIAN_POINT('Ctrl Pts',(87.1604620756948,-4.10550714502573,
126.540852787686));
#181354=CARTESIAN_POINT('Ctrl Pts',(87.1678702953613,-3.9893060253567,126.434764755412));
#181355=CARTESIAN_POINT('Ctrl Pts',(87.1752830746634,-3.87303338583718,
126.328611427724));
#181356=CARTESIAN_POINT('Ctrl Pts',(87.1826958539654,-3.75262495683606,
126.227197283059));
#181357=CARTESIAN_POINT('Ctrl Pts',(87.1901086332675,-3.62851653654409,
126.130839642271));
#181358=CARTESIAN_POINT('Ctrl Pts',(87.1975320042963,-3.50423078432128,
126.034344321167));
#181359=CARTESIAN_POINT('Ctrl Pts',(87.204955375325,-3.37623478500182,125.942920150223));
#181360=CARTESIAN_POINT('Ctrl Pts',(87.2123787463538,-3.2449926234718,125.856840689752));
#181361=CARTESIAN_POINT('Ctrl Pts',(87.2163147957945,-3.17540488031723,
125.811199294363));
#181362=CARTESIAN_POINT('Ctrl Pts',(87.2202508452353,-3.10490493454365,
125.767059720152));
#181363=CARTESIAN_POINT('Ctrl Pts',(87.224186894676,-3.03356448216249,125.724457361099));
#181364=CARTESIAN_POINT('Ctrl Pts',(87.2316101610815,-2.89901861542882,
125.644110641499));
#181365=CARTESIAN_POINT('Ctrl Pts',(87.2390334274869,-2.76107501090047,
125.568991475291));
#181366=CARTESIAN_POINT('Ctrl Pts',(87.2464566938924,-2.62017831194225,
125.499401034673));
#181367=CARTESIAN_POINT('Ctrl Pts',(87.2538711866134,-2.47944814118135,
125.429892844177));
#181368=CARTESIAN_POINT('Ctrl Pts',(87.2612856793344,-2.33577215490723,
125.36590053602));
#181369=CARTESIAN_POINT('Ctrl Pts',(87.2687001720554,-2.18962294012674,
125.307681443504));
#181370=CARTESIAN_POINT('Ctrl Pts',(87.2761075184092,-2.04361458946177,
125.249518464741));
#181371=CARTESIAN_POINT('Ctrl Pts',(87.2835148647629,-1.89513810041531,
125.19711776113));
#181372=CARTESIAN_POINT('Ctrl Pts',(87.2909222111167,-1.74468947252004,
125.150690198539));
#181373=CARTESIAN_POINT('Ctrl Pts',(87.2983240327921,-1.59435305488766,
125.104297263377));
#181374=CARTESIAN_POINT('Ctrl Pts',(87.3057258544675,-1.44204778232258,
125.063868708343));
#181375=CARTESIAN_POINT('Ctrl Pts',(87.3131276761429,-1.28828828932917,
125.029566781759));
#181376=CARTESIAN_POINT('Ctrl Pts',(87.3205255904543,-1.13460996477558,
124.995282962894));
#181377=CARTESIAN_POINT('Ctrl Pts',(87.3279235047656,-0.979479312067915,
124.96711941249));
#181378=CARTESIAN_POINT('Ctrl Pts',(87.335321419077,-0.823424627491789,
124.945188112396));
#181379=CARTESIAN_POINT('Ctrl Pts',(87.3427181039892,-0.667395876372897,
124.923260456886));
#181380=CARTESIAN_POINT('Ctrl Pts',(87.3501147889014,-0.510443767454701,
124.907563048054));
#181381=CARTESIAN_POINT('Ctrl Pts',(87.3575114738136,-0.353105374908404,
124.898156493367));
#181382=CARTESIAN_POINT('Ctrl Pts',(87.364907830749,-0.195773958911312,
124.888750355776));
#181383=CARTESIAN_POINT('Ctrl Pts',(87.3723041876844,-0.0380566659750203,
124.885634539975));
#181384=CARTESIAN_POINT('Ctrl Pts',(87.3797005446199,0.119506009921639,
124.888817626758));
#181385=CARTESIAN_POINT('Ctrl Pts',(87.3870980339564,0.277092809066217,
124.89200120088));
#181386=CARTESIAN_POINT('Ctrl Pts',(87.3944955232931,0.434524570790814,
124.90148559025));
#181387=CARTESIAN_POINT('Ctrl Pts',(87.4018930126296,0.591262657080174,
124.917227271629));
#181388=CARTESIAN_POINT('Ctrl Pts',(87.4092930951446,0.748055687662819,
124.93297447123));
#181389=CARTESIAN_POINT('Ctrl Pts',(87.4166931776596,0.904154187469182,
124.954983292769));
#181390=CARTESIAN_POINT('Ctrl Pts',(87.4240932601746,1.05902662934586,124.983158580114));
#181391=CARTESIAN_POINT('Ctrl Pts',(87.4315014798411,1.21406936939365,125.011364849084));
#181392=CARTESIAN_POINT('Ctrl Pts',(87.4389096995075,1.36788299161932,125.045751058433));
#181393=CARTESIAN_POINT('Ctrl Pts',(87.446317919174,1.51994740129198,125.086171178608));
#181394=CARTESIAN_POINT('Ctrl Pts',(87.4537306984761,1.67210540407156,125.126616176694));
#181395=CARTESIAN_POINT('Ctrl Pts',(87.4611434777781,1.82251169319055,125.173102375787));
#181396=CARTESIAN_POINT('Ctrl Pts',(87.4685562570802,1.97066373806021,125.225434646199));
#181397=CARTESIAN_POINT('Ctrl Pts',(87.4759796281089,2.11902746951911,125.277841691413));
#181398=CARTESIAN_POINT('Ctrl Pts',(87.4834029991377,2.26513017790937,125.336111353121));
#181399=CARTESIAN_POINT('Ctrl Pts',(87.4908263701665,2.40849085997515,125.400001049595));
#181400=CARTESIAN_POINT('Ctrl Pts',(87.4947624196073,2.48450413349837,125.433876899678));
#181401=CARTESIAN_POINT('Ctrl Pts',(87.498698469048,2.55974695012835,125.46933198269));
#181402=CARTESIAN_POINT('Ctrl Pts',(87.5026345184888,2.63415077846103,125.506325110056));
#181403=CARTESIAN_POINT('Ctrl Pts',(87.5100577848942,2.77447407663323,125.576092993754));
#181404=CARTESIAN_POINT('Ctrl Pts',(87.5174810512996,2.91223584635632,125.651545110787));
#181405=CARTESIAN_POINT('Ctrl Pts',(87.5249043177051,3.04694236233204,125.732470161027));
#181406=CARTESIAN_POINT('Ctrl Pts',(87.5323188104261,3.18148966639265,125.813299564579));
#181407=CARTESIAN_POINT('Ctrl Pts',(87.5397333031471,3.31298858766372,125.899588835289));
#181408=CARTESIAN_POINT('Ctrl Pts',(87.5471477958681,3.44096717952954,125.991079467259));
#181409=CARTESIAN_POINT('Ctrl Pts',(87.5545551422219,3.56882242081021,126.082481917114));
#181410=CARTESIAN_POINT('Ctrl Pts',(87.5619624885757,3.69316378589292,126.179075532161));
#181411=CARTESIAN_POINT('Ctrl Pts',(87.5693698349295,3.81354576748629,126.280556992099));
#181412=CARTESIAN_POINT('Ctrl Pts',(87.5767716566049,3.93383796365611,126.381962763336));
#181413=CARTESIAN_POINT('Ctrl Pts',(87.5841734782803,4.05017637208661,126.488248881137));
#181414=CARTESIAN_POINT('Ctrl Pts',(87.5915752999557,4.1621463161506,126.599070068097));
#181415=CARTESIAN_POINT('Ctrl Pts',(87.598973214267,4.27405715215269,126.709832753415));
#181416=CARTESIAN_POINT('Ctrl Pts',(87.6063711285784,4.38160385180637,126.825125478141));
#181417=CARTESIAN_POINT('Ctrl Pts',(87.6137690428898,4.48440664456365,126.94456430057));
#181418=CARTESIAN_POINT('Ctrl Pts',(87.621165727802,4.58719235336167,127.063983274434));
#181419=CARTESIAN_POINT('Ctrl Pts',(87.6285624127141,4.68523547662453,127.187546695878));
#181420=CARTESIAN_POINT('Ctrl Pts',(87.6359590976264,4.7781947218654,127.314835469005));
#181421=CARTESIAN_POINT('Ctrl Pts',(87.6433554545618,4.87114984519592,127.442118598015));
#181422=CARTESIAN_POINT('Ctrl Pts',(87.6507518114973,4.95902131856453,127.5731264488));
#181423=CARTESIAN_POINT('Ctrl Pts',(87.6581481684327,5.04150977250863,127.707408926596));
#181424=CARTESIAN_POINT('Ctrl Pts',(87.6655456577693,5.12401085564567,127.841711963383));
#181425=CARTESIAN_POINT('Ctrl Pts',(87.6729431471059,5.20112708295338,127.979290307344));
#181426=CARTESIAN_POINT('Ctrl Pts',(87.6803406364425,5.272603924762,128.11966726169));
#181427=CARTESIAN_POINT('Ctrl Pts',(87.6877407189575,5.34410582266671,128.260093424959));
#181428=CARTESIAN_POINT('Ctrl Pts',(87.6951408014724,5.40996422984681,128.403319819423));
#181429=CARTESIAN_POINT('Ctrl Pts',(87.7025408839874,5.46997190044179,128.548847822019));
#181430=CARTESIAN_POINT('Ctrl Pts',(87.7099491036539,5.53004555563953,128.694535847614));
#181431=CARTESIAN_POINT('Ctrl Pts',(87.7173573233204,5.58425548376604,128.842530190304));
#181432=CARTESIAN_POINT('Ctrl Pts',(87.7247655429869,5.63244341971258,128.99231434712));
#181433=CARTESIAN_POINT('Ctrl Pts',(87.7321783222889,5.68066101452968,129.142190693586));
#181434=CARTESIAN_POINT('Ctrl Pts',(87.739591101591,5.72284913182212,129.293858690448));
#181435=CARTESIAN_POINT('Ctrl Pts',(87.7470038808931,5.75890030966424,129.446790072125));
#181436=CARTESIAN_POINT('Ctrl Pts',(87.7544272519218,5.79500299911989,129.599939969332));
#181437=CARTESIAN_POINT('Ctrl Pts',(87.7618506229506,5.82495116508458,129.754356491213));
#181438=CARTESIAN_POINT('Ctrl Pts',(87.7692739939793,5.84868890442652,129.909503834758));
#181439=CARTESIAN_POINT('Ctrl Pts',(87.7732100434201,5.86127522340487,129.991766679014));
#181440=CARTESIAN_POINT('Ctrl Pts',(87.7771460928609,5.87211643822368,130.074234930039));
#181441=CARTESIAN_POINT('Ctrl Pts',(87.7810821423017,5.88121015909862,130.156828666991));
#181442=CARTESIAN_POINT('Ctrl Pts',(87.7885054087072,5.89836063286343,130.31259787722));
#181443=CARTESIAN_POINT('Ctrl Pts',(87.7959286751126,5.90934423144243,130.469284467981));
#181444=CARTESIAN_POINT('Ctrl Pts',(87.8033519415181,5.91407185703321,130.626358841317));
#181445=CARTESIAN_POINT('Ctrl Pts',(87.8107664342391,5.91879389496316,130.783247565789));
#181446=CARTESIAN_POINT('Ctrl Pts',(87.8181809269601,5.91727466666259,130.940522791048));
#181447=CARTESIAN_POINT('Ctrl Pts',(87.8255954196811,5.90947656179092,131.09764772629));
#181448=CARTESIAN_POINT('Ctrl Pts',(87.8330027660349,5.90168597302632,131.254621218604));
#181449=CARTESIAN_POINT('Ctrl Pts',(87.8404101123887,5.88762857404784,131.411444338941));
#181450=CARTESIAN_POINT('Ctrl Pts',(87.8478174587424,5.86731874924192,131.56757831737));
#181451=CARTESIAN_POINT('Ctrl Pts',(87.8552192804178,5.84702407226958,131.723595845187));
#181452=CARTESIAN_POINT('Ctrl Pts',(87.8626211020932,5.82048630266507,131.878924885928));
#181453=CARTESIAN_POINT('Ctrl Pts',(87.8700229237686,5.78777178924067,132.033029929533));
#181454=CARTESIAN_POINT('Ctrl Pts',(87.87742083808,5.75507454555326,132.187053622285));
#181455=CARTESIAN_POINT('Ctrl Pts',(87.8848187523914,5.71620712911922,132.33985424048));
#181456=CARTESIAN_POINT('Ctrl Pts',(87.8922166667027,5.67128728570899,132.490904742531));
#181457=CARTESIAN_POINT('Ctrl Pts',(87.8996133516149,5.62637490716184,132.64193014273));
#181458=CARTESIAN_POINT('Ctrl Pts',(87.9070100365271,5.57541220416368,132.791205646551));
#181459=CARTESIAN_POINT('Ctrl Pts',(87.9144067214393,5.51856729703439,132.938217583392));
#181460=CARTESIAN_POINT('Ctrl Pts',(87.9218030783748,5.46172491046786,133.085223001569));
#181461=CARTESIAN_POINT('Ctrl Pts',(87.9291994353102,5.39900097300319,133.229964704157));
#181462=CARTESIAN_POINT('Ctrl Pts',(87.9365957922457,5.33061234560512,133.371947535936));
#181463=CARTESIAN_POINT('Ctrl Pts',(87.9439932815823,5.26221324773357,133.513952105648));
#181464=CARTESIAN_POINT('Ctrl Pts',(87.9513907709188,5.18814789506565,133.653196627176));
#181465=CARTESIAN_POINT('Ctrl Pts',(87.9587882602554,5.10867976660914,133.789209291241));
#181466=CARTESIAN_POINT('Ctrl Pts',(87.9661883427704,5.0291837807234,133.925269634334));
#181467=CARTESIAN_POINT('Ctrl Pts',(87.9735884252854,4.94428143644078,134.058095542208));
#181468=CARTESIAN_POINT('Ctrl Pts',(87.9809885078004,4.85428021801495,134.187243135108));
#181469=CARTESIAN_POINT('Ctrl Pts',(87.9883967274669,4.76418003399711,134.316532739062));
#181470=CARTESIAN_POINT('Ctrl Pts',(87.9958049471333,4.66896999237839,134.442135644086));
#181471=CARTESIAN_POINT('Ctrl Pts',(88.0032131667998,4.56899909557546,134.563639514792));
#181472=CARTESIAN_POINT('Ctrl Pts',(88.0106259461019,4.46896666835359,134.685218169103));
#181473=CARTESIAN_POINT('Ctrl Pts',(88.018038725404,4.3641677950318,134.802692484011));
#181474=CARTESIAN_POINT('Ctrl Pts',(88.0254515047061,4.25498883460737,134.915686508306));
#181475=CARTESIAN_POINT('Ctrl Pts',(88.0328748757348,4.14565387416439,135.028841983761));
#181476=CARTESIAN_POINT('Ctrl Pts',(88.0402982467635,4.03192659623113,135.137504125873));
#181477=CARTESIAN_POINT('Ctrl Pts',(88.0477216177923,3.91422757004694,135.241336287139));
#181478=CARTESIAN_POINT('Ctrl Pts',(88.051657667233,3.85182072221531,135.296390590461));
#181479=CARTESIAN_POINT('Ctrl Pts',(88.0555937166738,3.7882977884274,135.350087715604));
#181480=CARTESIAN_POINT('Ctrl Pts',(88.0595297661146,3.72372471661368,135.40238245281));
#181481=CARTESIAN_POINT('Ctrl Pts',(88.06695303252,3.60194191842861,135.501008695118));
#181482=CARTESIAN_POINT('Ctrl Pts',(88.0743762989254,3.47605395534822,135.594942437263));
#181483=CARTESIAN_POINT('Ctrl Pts',(88.0817995653309,3.34645823359367,135.683822458109));
#181484=CARTESIAN_POINT('Ctrl Pts',(88.0892140580519,3.2170156832198,135.772597430151));
#181485=CARTESIAN_POINT('Ctrl Pts',(88.0966285507728,3.0838744019375,135.856330361269));
#181486=CARTESIAN_POINT('Ctrl Pts',(88.1040430434938,2.94746567774693,135.934699460275));
#181487=CARTESIAN_POINT('Ctrl Pts',(88.1114503898476,2.81118842942062,136.012993024192));
#181488=CARTESIAN_POINT('Ctrl Pts',(88.1188577362013,2.67165032930038,136.085932863465));
#181489=CARTESIAN_POINT('Ctrl Pts',(88.1262650825551,2.52931243490207,136.153239861777));
#181490=CARTESIAN_POINT('Ctrl Pts',(88.1336669042305,2.38708070147531,136.22049665999));
#181491=CARTESIAN_POINT('Ctrl Pts',(88.1410687259059,2.24205366766045,136.282128823476));
#181492=CARTESIAN_POINT('Ctrl Pts',(88.1484705475813,2.09471773639211,136.337902717103));
#181493=CARTESIAN_POINT('Ctrl Pts',(88.1558684618926,1.94745958261503,136.393647168125));
#181494=CARTESIAN_POINT('Ctrl Pts',(88.163266376204,1.79789530701756,136.443539376393));
#181495=CARTESIAN_POINT('Ctrl Pts',(88.1706642905153,1.64653196907772,136.487393525909));
#181496=CARTESIAN_POINT('Ctrl Pts',(88.1780609754275,1.49519378497874,136.53124038766));
#181497=CARTESIAN_POINT('Ctrl Pts',(88.1854576603397,1.34205749010861,136.569051078361));
#181498=CARTESIAN_POINT('Ctrl Pts',(88.1928543452519,1.18764612323309,136.60068939089));
#181499=CARTESIAN_POINT('Ctrl Pts',(88.2002507021873,1.0332416031195,136.632326300544));
#181500=CARTESIAN_POINT('Ctrl Pts',(88.2076470591228,0.877562489117202,
136.657791301282));
#181501=CARTESIAN_POINT('Ctrl Pts',(88.2150434160582,0.721142587985943,
136.676999200886));
#181502=CARTESIAN_POINT('Ctrl Pts',(88.2224409053948,0.564698738568276,
136.696210041267));
#181503=CARTESIAN_POINT('Ctrl Pts',(88.2298383947314,0.407514246733144,
136.709161827551));
#181504=CARTESIAN_POINT('Ctrl Pts',(88.2372358840679,0.250128475829376,
136.715821207647));
#181505=CARTESIAN_POINT('Ctrl Pts',(88.2446359665829,0.0926875335874854,
136.722482922179));
#181506=CARTESIAN_POINT('Ctrl Pts',(88.2520360490979,-0.0649544554721071,
136.722847823034));
#181507=CARTESIAN_POINT('Ctrl Pts',(88.2594361316129,-0.222257839989229,
136.716934677573));
#181508=CARTESIAN_POINT('Ctrl Pts',(88.2668443512794,-0.379734195748697,
136.71101503));
#181509=CARTESIAN_POINT('Ctrl Pts',(88.2742525709459,-0.536870830133897,
136.698803563685));
#181510=CARTESIAN_POINT('Ctrl Pts',(88.2816607906123,-0.693132189373962,
136.680371026896));
#181511=CARTESIAN_POINT('Ctrl Pts',(88.2890735699144,-0.849489724873278,
136.661927145188));
#181512=CARTESIAN_POINT('Ctrl Pts',(88.2964863492164,-1.00497054393579,
136.637254621682));
#181513=CARTESIAN_POINT('Ctrl Pts',(88.3038991285185,-1.15904951168507,
136.606475300331));
#181514=CARTESIAN_POINT('Ctrl Pts',(88.3113224995472,-1.31334863468906,
136.575652000044));
#181515=CARTESIAN_POINT('Ctrl Pts',(88.318745870576,-1.46624154398572,136.538704562227));
#181516=CARTESIAN_POINT('Ctrl Pts',(88.3261692416047,-1.61721768054957,
136.495804857495));
#181517=CARTESIAN_POINT('Ctrl Pts',(88.3301052910456,-1.69726885078065,
136.473058404681));
#181518=CARTESIAN_POINT('Ctrl Pts',(88.3340413404865,-1.77678146029476,
136.448639369187));
#181519=CARTESIAN_POINT('Ctrl Pts',(88.3379773899274,-1.85568182637297,
136.422578797894));
#181520=CARTESIAN_POINT('Ctrl Pts',(88.3454006563329,-2.00448545439682,
136.37342937376));
#181521=CARTESIAN_POINT('Ctrl Pts',(88.3528239227383,-2.15156009103515,
136.318289747177));
#181522=CARTESIAN_POINT('Ctrl Pts',(88.3602471891438,-2.2963870229461,136.257299018405));
#181523=CARTESIAN_POINT('Ctrl Pts',(88.3676616818648,-2.44104278145067,
136.19638037561));
#181524=CARTESIAN_POINT('Ctrl Pts',(88.3750761745858,-2.5834557825298,136.12962453947));
#181525=CARTESIAN_POINT('Ctrl Pts',(88.3824906673068,-2.72312217244512,
136.057220428796));
#181526=CARTESIAN_POINT('Ctrl Pts',(88.3898980136606,-2.86265394663559,
135.984886103931));
#181527=CARTESIAN_POINT('Ctrl Pts',(88.3973053600144,-2.9994440507029,135.906914513157));
#181528=CARTESIAN_POINT('Ctrl Pts',(88.4047127063682,-3.13300844333492,
135.823542688032));
#181529=CARTESIAN_POINT('Ctrl Pts',(88.4121145280437,-3.26647321860391,
135.740233044761));
#181530=CARTESIAN_POINT('Ctrl Pts',(88.4195163497191,-3.39671675751825,
135.651531383647));
#181531=CARTESIAN_POINT('Ctrl Pts',(88.4269181713945,-3.52327958355582,
135.557720643758));
#181532=CARTESIAN_POINT('Ctrl Pts',(88.4343160857059,-3.64977559806242,
135.463959425829));
#181533=CARTESIAN_POINT('Ctrl Pts',(88.4417140000172,-3.77259447017055,
135.365094722142));
#181534=CARTESIAN_POINT('Ctrl Pts',(88.4491119143286,-3.89130578958367,
135.261452698111));
#181535=CARTESIAN_POINT('Ctrl Pts',(88.4565085992408,-4.00999738132931,
135.157827897503));
#181536=CARTESIAN_POINT('Ctrl Pts',(88.463905284153,-4.12458249421014,135.049427597485));
#181537=CARTESIAN_POINT('Ctrl Pts',(88.4713019690653,-4.23466381808838,
134.936618222105));
#181538=CARTESIAN_POINT('Ctrl Pts',(88.4786983260007,-4.34474026084537,
134.823813848812));
#181539=CARTESIAN_POINT('Ctrl Pts',(88.4860946829362,-4.45031305096526,
134.706601056056));
#181540=CARTESIAN_POINT('Ctrl Pts',(88.4934910398717,-4.55102197822761,
134.585382902106));
#181541=CARTESIAN_POINT('Ctrl Pts',(88.5008885292083,-4.65174632428396,
134.464146189347));
#181542=CARTESIAN_POINT('Ctrl Pts',(88.5082860185449,-4.74760508617959,
134.338903181521));
#181543=CARTESIAN_POINT('Ctrl Pts',(88.5156835078815,-4.83827866479283,
134.210089632668));
#181544=CARTESIAN_POINT('Ctrl Pts',(88.5230835903965,-4.92898402888836,
134.081230928426));
#181545=CARTESIAN_POINT('Ctrl Pts',(88.5304836729115,-5.0145003760186,133.948799496202));
#181546=CARTESIAN_POINT('Ctrl Pts',(88.5378837554266,-5.09455180095346,
133.813259504186));
#181547=CARTESIAN_POINT('Ctrl Pts',(88.5452919750931,-5.17469125065952,
133.677570472014));
#181548=CARTESIAN_POINT('Ctrl Pts',(88.5527001947595,-5.24935358736278,
133.53876637534));
#181549=CARTESIAN_POINT('Ctrl Pts',(88.560108414426,-5.31830885369035,133.397336031884));
#181550=CARTESIAN_POINT('Ctrl Pts',(88.5675211937281,-5.38730656083386,
133.255818640412));
#181551=CARTESIAN_POINT('Ctrl Pts',(88.5749339730302,-5.45059004857925,
133.111672122273));
#181552=CARTESIAN_POINT('Ctrl Pts',(88.5823467523323,-5.50797797946812,
132.965404147945));
#181553=CARTESIAN_POINT('Ctrl Pts',(88.5897701233611,-5.56544790892379,
132.818927179077));
#181554=CARTESIAN_POINT('Ctrl Pts',(88.5971934943899,-5.61700533517418,
132.670323051701));
#181555=CARTESIAN_POINT('Ctrl Pts',(88.6046168654186,-5.66251888820989,
132.520114213851));
#181556=CARTESIAN_POINT('Ctrl Pts',(88.6085529148593,-5.68665126611114,
132.440469883815));
#181557=CARTESIAN_POINT('Ctrl Pts',(88.6124889642999,-5.70908534761106,
132.360374588369));
#181558=CARTESIAN_POINT('Ctrl Pts',(88.6164250137405,-5.72980742602137,
132.27990710047));
#181559=CARTESIAN_POINT('Ctrl Pts',(88.6261250355039,-5.78087502936128,
132.081602583305));
#181560=CARTESIAN_POINT('Ctrl Pts',(88.6358250572672,-5.82166799180386,
131.880551790034));
#181561=CARTESIAN_POINT('Ctrl Pts',(88.6455250790304,-5.85194413610283,
131.677676362547));
#181562=CARTESIAN_POINT('Ctrl Pts',(88.6550245796708,-5.88159440485232,
131.478994823436));
#181563=CARTESIAN_POINT('Ctrl Pts',(88.6645240803113,-5.90115822620598,
131.278563068723));
#181564=CARTESIAN_POINT('Ctrl Pts',(88.6740235809517,-5.91045275283364,
131.077268695536));
#181565=CARTESIAN_POINT('Ctrl Pts',(88.678223984272,-5.91456252259787,130.988262169246));
#181566=CARTESIAN_POINT('Ctrl Pts',(88.6824243875923,-5.91666507788678,
130.899087300844));
#181567=CARTESIAN_POINT('Ctrl Pts',(88.6866247909126,-5.9167474790821,130.80982241906));
#181568=CARTESIAN_POINT('',(90.4366248408691,-5.91280601562254,130.803156497514));
#181569=CARTESIAN_POINT('Ctrl Pts',(88.6866248077954,-5.91558532475283,
130.809820987551));
#181570=CARTESIAN_POINT('Ctrl Pts',(88.756040751048,-5.90219245444721,129.3349040253));
#181571=CARTESIAN_POINT('Ctrl Pts',(88.918272568905,-4.59705841354693,125.866736618183));
#181572=CARTESIAN_POINT('Ctrl Pts',(89.1733202613661,1.22971590047256,123.914849797887));
#181573=CARTESIAN_POINT('Ctrl Pts',(89.451767885179,6.46103205536798,128.115006548304));
#181574=CARTESIAN_POINT('Ctrl Pts',(89.7302155089922,5.75497539034297,134.786548306122));
#181575=CARTESIAN_POINT('Ctrl Pts',(90.0086631328047,-0.239622512229257,
137.79865411884));
#181576=CARTESIAN_POINT('Ctrl Pts',(90.2441328990728,-5.12275198661228,
134.910492178741));
#181577=CARTESIAN_POINT('Ctrl Pts',(90.3867867907362,-5.90523390002275,
131.865903345122));
#181578=CARTESIAN_POINT('Ctrl Pts',(90.4366248077954,-5.90715601702778,
130.803158353846));
#181579=CARTESIAN_POINT('',(92.1866248077953,-5.91752627892735,130.799315009708));
#181580=CARTESIAN_POINT('Ctrl Pts',(90.4366248639554,-5.91674987721069,
130.80315520174));
#181581=CARTESIAN_POINT('Ctrl Pts',(90.4445032138975,-5.91671559555037,
130.634884630583));
#181582=CARTESIAN_POINT('Ctrl Pts',(90.4523815638397,-5.90949872441783,
130.466797726228));
#181583=CARTESIAN_POINT('Ctrl Pts',(90.4602599137817,-5.89517156383314,
130.29950143376));
#181584=CARTESIAN_POINT('Ctrl Pts',(90.4681529579633,-5.88081768106298,
130.131893109991));
#181585=CARTESIAN_POINT('Ctrl Pts',(90.4760460021448,-5.85932704389707,
129.965078635201));
#181586=CARTESIAN_POINT('Ctrl Pts',(90.4839390463263,-5.83082321380477,
129.799656077985));
#181587=CARTESIAN_POINT('Ctrl Pts',(90.491854985065,-5.80223670552753,129.633753696242));
#181588=CARTESIAN_POINT('Ctrl Pts',(90.4997709238037,-5.76659635918975,
129.46925159903));
#181589=CARTESIAN_POINT('Ctrl Pts',(90.5076868625424,-5.72407656219687,
129.306736474929));
#181590=CARTESIAN_POINT('Ctrl Pts',(90.5156151112129,-5.6814906434436,129.143968626525));
#181591=CARTESIAN_POINT('Ctrl Pts',(90.5235433598835,-5.6320039940697,128.983194201965));
#181592=CARTESIAN_POINT('Ctrl Pts',(90.531471608554,-5.57583988714239,128.824981898005));
#181593=CARTESIAN_POINT('Ctrl Pts',(90.5394190372223,-5.5195399081597,128.666386847268));
#181594=CARTESIAN_POINT('Ctrl Pts',(90.5473664658905,-5.45653027275169,
128.510366586071));
#181595=CARTESIAN_POINT('Ctrl Pts',(90.5553138945588,-5.38708203898443,
128.357469188068));
#181596=CARTESIAN_POINT('Ctrl Pts',(90.5587287231827,-5.3572417187441,128.291772667468));
#181597=CARTESIAN_POINT('Ctrl Pts',(90.5621435518066,-5.32621325346571,
128.226652364695));
#181598=CARTESIAN_POINT('Ctrl Pts',(90.5655583804305,-5.2940206433992,128.162150181253));
#181599=CARTESIAN_POINT('Ctrl Pts',(90.572981646836,-5.22403929231815,128.021933220414));
#181600=CARTESIAN_POINT('Ctrl Pts',(90.5804049132415,-5.14837761269494,
127.884286435494));
#181601=CARTESIAN_POINT('Ctrl Pts',(90.5878281796469,-5.06724765577779,
127.749703229656));
#181602=CARTESIAN_POINT('Ctrl Pts',(90.595242672368,-4.98621358773235,127.615279089991));
#181603=CARTESIAN_POINT('Ctrl Pts',(90.6026571650891,-4.89972429797056,
127.483911638574));
#181604=CARTESIAN_POINT('Ctrl Pts',(90.6100716578101,-4.80803901031332,
127.356072428072));
#181605=CARTESIAN_POINT('Ctrl Pts',(90.6174790041639,-4.71644209238809,
127.228356433814));
#181606=CARTESIAN_POINT('Ctrl Pts',(90.6248863505178,-4.61965936280325,
127.104162211755));
#181607=CARTESIAN_POINT('Ctrl Pts',(90.6322936968716,-4.51799481949465,
126.983934807068));
#181608=CARTESIAN_POINT('Ctrl Pts',(90.639695518547,-4.41640610143804,126.863797072516));
#181609=CARTESIAN_POINT('Ctrl Pts',(90.6470973402225,-4.30994305946116,
126.747620548181));
#181610=CARTESIAN_POINT('Ctrl Pts',(90.6544991618979,-4.19895160163495,
126.635819384757));
#181611=CARTESIAN_POINT('Ctrl Pts',(90.6618970762093,-4.08801873533561,
126.524077240298));
#181612=CARTESIAN_POINT('Ctrl Pts',(90.6692949905207,-3.97256247634775,
126.416706121082));
#181613=CARTESIAN_POINT('Ctrl Pts',(90.6766929048321,-3.85296734387529,
126.314085212924));
#181614=CARTESIAN_POINT('Ctrl Pts',(90.6840895897443,-3.73339208594409,
126.2114813585));
#181615=CARTESIAN_POINT('Ctrl Pts',(90.6914862746566,-3.60967960264082,
126.113626391262));
#181616=CARTESIAN_POINT('Ctrl Pts',(90.6988829595688,-3.48224950876385,
126.020860965511));
#181617=CARTESIAN_POINT('Ctrl Pts',(90.7062793165043,-3.35482506527059,
125.928099653075));
#181618=CARTESIAN_POINT('Ctrl Pts',(90.7136756734398,-3.22368364076562,
125.840427653108));
#181619=CARTESIAN_POINT('Ctrl Pts',(90.7210720303753,-3.08927578508048,
125.758143649756));
#181620=CARTESIAN_POINT('Ctrl Pts',(90.7284695197119,-2.9548473512095,125.675847048513));
#181621=CARTESIAN_POINT('Ctrl Pts',(90.7358670090485,-2.81715180878977,
125.598940281324));
#181622=CARTESIAN_POINT('Ctrl Pts',(90.7432644983851,-2.67666624141168,
125.527677152113));
#181623=CARTESIAN_POINT('Ctrl Pts',(90.7506645809002,-2.53613142703582,
125.456389041722));
#181624=CARTESIAN_POINT('Ctrl Pts',(90.7580646634152,-2.39280497314063,
125.390748676996));
#181625=CARTESIAN_POINT('Ctrl Pts',(90.7654647459302,-2.24718581760332,
125.330962544736));
#181626=CARTESIAN_POINT('Ctrl Pts',(90.7728729655967,-2.10140653883449,
125.271110671477));
#181627=CARTESIAN_POINT('Ctrl Pts',(90.7802811852632,-1.95332986923686,
125.217126028321));
#181628=CARTESIAN_POINT('Ctrl Pts',(90.7876894049297,-1.80347255203134,
125.169166094165));
#181629=CARTESIAN_POINT('Ctrl Pts',(90.7951021842319,-1.65352300014715,
125.121176641469));
#181630=CARTESIAN_POINT('Ctrl Pts',(90.802514963534,-1.50179097578084,125.079219385903));
#181631=CARTESIAN_POINT('Ctrl Pts',(90.8099277428361,-1.34880490743863,
125.043400985337));
#181632=CARTESIAN_POINT('Ctrl Pts',(90.8173511138649,-1.19560024542797,
125.007531405761));
#181633=CARTESIAN_POINT('Ctrl Pts',(90.8247744848937,-1.04113832634722,
124.977818270137));
#181634=CARTESIAN_POINT('Ctrl Pts',(90.8321978559225,-0.885955037661632,
124.954316666129));
#181635=CARTESIAN_POINT('Ctrl Pts',(90.8361339053628,-0.803673134438044,
124.941855551773));
#181636=CARTESIAN_POINT('Ctrl Pts',(90.8400699548032,-0.721188480435601,
124.931139852149));
#181637=CARTESIAN_POINT('Ctrl Pts',(90.8440060042436,-0.63858100003989,
124.922171835413));
#181638=CARTESIAN_POINT('Ctrl Pts',(90.851429270649,-0.48278587008773,124.905258435729));
#181639=CARTESIAN_POINT('Ctrl Pts',(90.8588525370545,-0.326082745600167,
124.894513300188));
#181640=CARTESIAN_POINT('Ctrl Pts',(90.8662758034599,-0.16900135951202,
124.890024720529));
#181641=CARTESIAN_POINT('Ctrl Pts',(90.8736902961809,-0.0121056305772075,
124.885541445998));
#181642=CARTESIAN_POINT('Ctrl Pts',(90.881104788902,0.14516710055356,124.88730001866));
#181643=CARTESIAN_POINT('Ctrl Pts',(90.888519281623,0.302279986459184,124.895337231905));
#181644=CARTESIAN_POINT('Ctrl Pts',(90.8959266279768,0.459241441050176,
124.903366698582));
#181645=CARTESIAN_POINT('Ctrl Pts',(90.9033339743306,0.616042986821128,
124.917662739376));
#181646=CARTESIAN_POINT('Ctrl Pts',(90.9107413206843,0.772145876353247,
124.93821015));
#181647=CARTESIAN_POINT('Ctrl Pts',(90.9181431423597,0.928132338460816,
124.958742235589));
#181648=CARTESIAN_POINT('Ctrl Pts',(90.9255449640351,1.08342081336588,124.985516358822));
#181649=CARTESIAN_POINT('Ctrl Pts',(90.9329467857105,1.23747589259897,125.018465356007));
#181650=CARTESIAN_POINT('Ctrl Pts',(90.9403447000218,1.39144964735457,125.051396959672));
#181651=CARTESIAN_POINT('Ctrl Pts',(90.9477426143332,1.54419093901699,125.090496867628));
#181652=CARTESIAN_POINT('Ctrl Pts',(90.9551405286445,1.69517290579942,125.135646532172));
#181653=CARTESIAN_POINT('Ctrl Pts',(90.9625372135568,1.84612978211828,125.180788693661));
#181654=CARTESIAN_POINT('Ctrl Pts',(90.969933898469,1.99532755652216,125.231978509551));
#181655=CARTESIAN_POINT('Ctrl Pts',(90.9773305833812,2.14225281485328,125.289047077997));
#181656=CARTESIAN_POINT('Ctrl Pts',(90.9847269403166,2.28917155836448,125.346113115963));
#181657=CARTESIAN_POINT('Ctrl Pts',(90.992123297252,2.43381763818899,125.409057253026));
#181658=CARTESIAN_POINT('Ctrl Pts',(90.9995196541875,2.5756962297044,125.477661874931));
#181659=CARTESIAN_POINT('Ctrl Pts',(91.006917143524,2.71759654319447,125.546277000379));
#181660=CARTESIAN_POINT('Ctrl Pts',(91.0143146328607,2.85672818862127,125.620554173739));
#181661=CARTESIAN_POINT('Ctrl Pts',(91.0217121221972,2.9926197582217,125.700229198294));
#181662=CARTESIAN_POINT('Ctrl Pts',(91.0291122047122,3.12855896440119,125.779932152805));
#181663=CARTESIAN_POINT('Ctrl Pts',(91.0365122872273,3.26125551155026,125.865036537193));
#181664=CARTESIAN_POINT('Ctrl Pts',(91.0439123697423,3.39026598836524,125.95523419205));
#181665=CARTESIAN_POINT('Ctrl Pts',(91.0513205894087,3.51941832546209,126.045531028502));
#181666=CARTESIAN_POINT('Ctrl Pts',(91.0587288090752,3.64487619156441,126.140932106109));
#181667=CARTESIAN_POINT('Ctrl Pts',(91.0661370287417,3.76622778288404,126.241087795355));
#181668=CARTESIAN_POINT('Ctrl Pts',(91.0735498080438,3.88765406408343,126.341305128756));
#181669=CARTESIAN_POINT('Ctrl Pts',(91.0809625873458,4.00496875691294,126.446282656632));
#181670=CARTESIAN_POINT('Ctrl Pts',(91.0883753666479,4.11779649856984,126.555633448299));
#181671=CARTESIAN_POINT('Ctrl Pts',(91.0957987376766,4.23078545379503,126.665140485505));
#181672=CARTESIAN_POINT('Ctrl Pts',(91.1032221087054,4.33927439652106,126.779032997027));
#181673=CARTESIAN_POINT('Ctrl Pts',(91.1106454797341,4.44292731966955,126.896889901792));
#181674=CARTESIAN_POINT('Ctrl Pts',(91.1145815291749,4.49788658664,126.959380460635));
#181675=CARTESIAN_POINT('Ctrl Pts',(91.1185175786157,4.55148697851146,127.022985038748));
#181676=CARTESIAN_POINT('Ctrl Pts',(91.1224536280564,4.60368338593768,127.087637619475));
#181677=CARTESIAN_POINT('Ctrl Pts',(91.1298768944618,4.70212418135033,127.209570368989));
#181678=CARTESIAN_POINT('Ctrl Pts',(91.1373001608672,4.79586623467169,127.335601137458));
#181679=CARTESIAN_POINT('Ctrl Pts',(91.1447234272727,4.88454892996854,127.465331969405));
#181680=CARTESIAN_POINT('Ctrl Pts',(91.1521379199937,4.97312680968425,127.594909470281));
#181681=CARTESIAN_POINT('Ctrl Pts',(91.1595524127147,5.05665702547508,127.728178024655));
#181682=CARTESIAN_POINT('Ctrl Pts',(91.1669669054357,5.13481844287327,127.864705855314));
#181683=CARTESIAN_POINT('Ctrl Pts',(91.1743742517894,5.21290452535465,128.00110209531));
#181684=CARTESIAN_POINT('Ctrl Pts',(91.1817815981432,5.28563192693006,128.140751035867));
#181685=CARTESIAN_POINT('Ctrl Pts',(91.189188944497,5.35272223325634,128.283191195234));
#181686=CARTESIAN_POINT('Ctrl Pts',(91.1965907661724,5.41976250110099,128.425525117356));
#181687=CARTESIAN_POINT('Ctrl Pts',(91.2039925878478,5.48117388676096,128.570645776893));
#181688=CARTESIAN_POINT('Ctrl Pts',(91.2113944095231,5.53672349559555,128.71806641592));
#181689=CARTESIAN_POINT('Ctrl Pts',(91.2187923238345,5.59224378022399,128.86540923274));
#181690=CARTESIAN_POINT('Ctrl Pts',(91.2261902381458,5.64190831935104,129.015049262592));
#181691=CARTESIAN_POINT('Ctrl Pts',(91.2335881524572,5.68553206885048,129.166479163805));
#181692=CARTESIAN_POINT('Ctrl Pts',(91.2409848373694,5.72914856887417,129.317883900117));
#181693=CARTESIAN_POINT('Ctrl Pts',(91.2483815222816,5.76672616841884,129.471077559092));
#181694=CARTESIAN_POINT('Ctrl Pts',(91.2557782071938,5.79812945649661,129.625536895288));
#181695=CARTESIAN_POINT('Ctrl Pts',(91.2631745641292,5.82953135211968,129.779989382594));
#181696=CARTESIAN_POINT('Ctrl Pts',(91.2705709210646,5.85475940625998,129.935707069719));
#181697=CARTESIAN_POINT('Ctrl Pts',(91.277967278,5.8737292391587,130.092156020872));
#181698=CARTESIAN_POINT('Ctrl Pts',(91.2853647673366,5.89270197638728,130.248628924759));
#181699=CARTESIAN_POINT('Ctrl Pts',(91.2927622566732,5.90541453963378,130.405832944991));
#181700=CARTESIAN_POINT('Ctrl Pts',(91.3001597460097,5.91183439766716,130.563228668087));
#181701=CARTESIAN_POINT('Ctrl Pts',(91.3075598285247,5.91825650617181,130.72067956601));
#181702=CARTESIAN_POINT('Ctrl Pts',(91.3149599110397,5.91838150233257,130.87832192784));
#181703=CARTESIAN_POINT('Ctrl Pts',(91.3223599935547,5.91222897474555,131.035616131401));
#181704=CARTESIAN_POINT('Ctrl Pts',(91.3297682132211,5.90606968182196,131.19308329611));
#181705=CARTESIAN_POINT('Ctrl Pts',(91.3371764328876,5.89361909443958,131.35020116476));
#181706=CARTESIAN_POINT('Ctrl Pts',(91.344584652554,5.87494877580655,131.506434291869));
#181707=CARTESIAN_POINT('Ctrl Pts',(91.3519974318561,5.85626696590393,131.66276357786));
#181708=CARTESIAN_POINT('Ctrl Pts',(91.3594102111581,5.83135785562912,131.818206669498));
#181709=CARTESIAN_POINT('Ctrl Pts',(91.3668229904602,5.8003440879611,131.972238617939));
#181710=CARTESIAN_POINT('Ctrl Pts',(91.3742463614889,5.76928600636741,132.126490654451));
#181711=CARTESIAN_POINT('Ctrl Pts',(91.3816697325177,5.73210593435422,132.27932715899));
#181712=CARTESIAN_POINT('Ctrl Pts',(91.3890931035464,5.6889765193202,132.430237834678));
#181713=CARTESIAN_POINT('Ctrl Pts',(91.3930291529874,5.6661082685921,132.510254295983));
#181714=CARTESIAN_POINT('Ctrl Pts',(91.3969652024283,5.64156825671818,132.589729651809));
#181715=CARTESIAN_POINT('Ctrl Pts',(91.4009012518693,5.61538764267704,132.66859026677));
#181716=CARTESIAN_POINT('Ctrl Pts',(91.4083245182747,5.56601182166638,132.817318925424));
#181717=CARTESIAN_POINT('Ctrl Pts',(91.4157477846802,5.51064843637328,132.964309478627));
#181718=CARTESIAN_POINT('Ctrl Pts',(91.4231710510857,5.44943737629167,133.109043425324));
#181719=CARTESIAN_POINT('Ctrl Pts',(91.4305855438067,5.38829866259978,133.253606308515));
#181720=CARTESIAN_POINT('Ctrl Pts',(91.4380000365277,5.32132617541701,133.395917553664));
#181721=CARTESIAN_POINT('Ctrl Pts',(91.4454145292487,5.24870960011652,133.535473595116));
#181722=CARTESIAN_POINT('Ctrl Pts',(91.4528218756025,5.17616301540528,133.674895127202));
#181723=CARTESIAN_POINT('Ctrl Pts',(91.4602292219562,5.09798334366856,133.811566413381));
#181724=CARTESIAN_POINT('Ctrl Pts',(91.46763656831,5.01440835281893,133.945003773622));
#181725=CARTESIAN_POINT('Ctrl Pts',(91.4750383899854,4.93089569535057,134.078341611245));
#181726=CARTESIAN_POINT('Ctrl Pts',(91.4824402116608,4.84199592845688,134.208450010511));
#181727=CARTESIAN_POINT('Ctrl Pts',(91.4898420333362,4.74799269012315,134.334869926014));
#181728=CARTESIAN_POINT('Ctrl Pts',(91.4972399476476,4.65403907536715,134.461223105428));
#181729=CARTESIAN_POINT('Ctrl Pts',(91.504637861959,4.55498757674822,134.583891380064));
#181730=CARTESIAN_POINT('Ctrl Pts',(91.5120357762703,4.45116501431281,134.702444836494));
#181731=CARTESIAN_POINT('Ctrl Pts',(91.5194324611825,4.34735970530389,134.82097859149));
#181732=CARTESIAN_POINT('Ctrl Pts',(91.5268291460947,4.23878515177542,134.93539860488));
#181733=CARTESIAN_POINT('Ctrl Pts',(91.5342258310069,4.12580838199207,135.04530812462));
#181734=CARTESIAN_POINT('Ctrl Pts',(91.5416221879424,4.01283662171701,135.155212770856));
#181735=CARTESIAN_POINT('Ctrl Pts',(91.5490185448779,3.8954633008768,135.260607060807));
#181736=CARTESIAN_POINT('Ctrl Pts',(91.5564149018133,3.77409202545241,135.361131398055));
#181737=CARTESIAN_POINT('Ctrl Pts',(91.5638123911499,3.65270216777599,135.461671125835));
#181738=CARTESIAN_POINT('Ctrl Pts',(91.5712098804865,3.5273134242617,135.55733917819));
#181739=CARTESIAN_POINT('Ctrl Pts',(91.578607369823,3.39836203482263,135.647816619511));
#181740=CARTESIAN_POINT('Ctrl Pts',(91.5860074523381,3.2693654416738,135.738325777559));
#181741=CARTESIAN_POINT('Ctrl Pts',(91.5934075348531,3.13680402148058,135.823640487567));
#181742=CARTESIAN_POINT('Ctrl Pts',(91.6008076173681,3.00114236177598,135.903485551008));
#181743=CARTESIAN_POINT('Ctrl Pts',(91.6082158370345,2.86533152813027,135.983418412306));
#181744=CARTESIAN_POINT('Ctrl Pts',(91.615624056701,2.7264139688223,136.057869426345));
#181745=CARTESIAN_POINT('Ctrl Pts',(91.6230322763675,2.58487885096429,136.126609379916));
#181746=CARTESIAN_POINT('Ctrl Pts',(91.6304450556695,2.44325662060257,136.195391641782));
#181747=CARTESIAN_POINT('Ctrl Pts',(91.6378578349716,2.29901396268784,136.258455689784));
#181748=CARTESIAN_POINT('Ctrl Pts',(91.6452706142737,2.15265882307452,136.315620959261));
#181749=CARTESIAN_POINT('Ctrl Pts',(91.6526939853025,2.00609456437444,136.372867909156));
#181750=CARTESIAN_POINT('Ctrl Pts',(91.6601173563312,1.85741214745418,136.424199125519));
#181751=CARTESIAN_POINT('Ctrl Pts',(91.66754072736,1.70713421966435,136.46948403357));
#181752=CARTESIAN_POINT('Ctrl Pts',(91.6714767768007,1.62745325648183,136.493495178414));
#181753=CARTESIAN_POINT('Ctrl Pts',(91.6754128262415,1.54732391292978,136.515807342531));
#181754=CARTESIAN_POINT('Ctrl Pts',(91.6793488756822,1.46682498273252,136.536406939128));
#181755=CARTESIAN_POINT('Ctrl Pts',(91.6867721420876,1.31500651266434,136.575257135418));
#181756=CARTESIAN_POINT('Ctrl Pts',(91.6941954084931,1.1614139351894,136.608130335848));
#181757=CARTESIAN_POINT('Ctrl Pts',(91.7016186748985,1.00655909361785,136.634863970927));
#181758=CARTESIAN_POINT('Ctrl Pts',(91.7090331676195,0.851887277608911,
136.661566009069));
#181759=CARTESIAN_POINT('Ctrl Pts',(91.7164476603405,0.695956531385569,
136.682142862991));
#181760=CARTESIAN_POINT('Ctrl Pts',(91.7238621530615,0.539293048570612,
136.696481930834));
#181761=CARTESIAN_POINT('Ctrl Pts',(91.7312694994153,0.382780563918668,
136.710807178143));
#181762=CARTESIAN_POINT('Ctrl Pts',(91.7386768457691,0.225537117906594,
136.718906574708));
#181763=CARTESIAN_POINT('Ctrl Pts',(91.7460841921229,0.0680981636066172,
136.720718720539));
#181764=CARTESIAN_POINT('Ctrl Pts',(91.7534860137983,-0.0892233667816346,
136.722529514803));
#181765=CARTESIAN_POINT('Ctrl Pts',(91.7608878354737,-0.246739743448905,
136.71806239102));
#181766=CARTESIAN_POINT('Ctrl Pts',(91.7682896571491,-0.403911445235869,
136.707307856607));
#181767=CARTESIAN_POINT('Ctrl Pts',(91.7756875714605,-0.561000177304546,
136.69655899943));
#181768=CARTESIAN_POINT('Ctrl Pts',(91.7830854857718,-0.717744225373094,
136.679529367138));
#181769=CARTESIAN_POINT('Ctrl Pts',(91.7904834000831,-0.873605236879032,
136.656261543983));
#181770=CARTESIAN_POINT('Ctrl Pts',(91.7978800849954,-1.02944034711246,
136.632997587518));
#181771=CARTESIAN_POINT('Ctrl Pts',(91.8052767699075,-1.18439234318304,
136.603497552744));
#181772=CARTESIAN_POINT('Ctrl Pts',(91.8126734548197,-1.33792903861843,
136.567855776766));
#181773=CARTESIAN_POINT('Ctrl Pts',(91.8200698117552,-1.49145892607585,
136.532215581181));
#181774=CARTESIAN_POINT('Ctrl Pts',(91.8274661686906,-1.64357327404957,
136.49043427029));
#181775=CARTESIAN_POINT('Ctrl Pts',(91.8348625256261,-1.79375138499813,
136.442657038589));
#181776=CARTESIAN_POINT('Ctrl Pts',(91.8422600149627,-1.94395248859886,
136.394872492071));
#181777=CARTESIAN_POINT('Ctrl Pts',(91.8496575042993,-2.09221640916468,
136.341090310078));
#181778=CARTESIAN_POINT('Ctrl Pts',(91.8570549936358,-2.23803901880698,
136.281505121119));
#181779=CARTESIAN_POINT('Ctrl Pts',(91.8644550761508,-2.38391274633883,
136.221899044663));
#181780=CARTESIAN_POINT('Ctrl Pts',(91.8718551586658,-2.52734311371323,
136.156486052207));
#181781=CARTESIAN_POINT('Ctrl Pts',(91.8792552411808,-2.66784746770677,
136.085508262875));
#181782=CARTESIAN_POINT('Ctrl Pts',(91.8866634608472,-2.80850632068193,
136.014452426166));
#181783=CARTESIAN_POINT('Ctrl Pts',(91.8940716805137,-2.94623240141119,
135.937819740826));
#181784=CARTESIAN_POINT('Ctrl Pts',(91.9014799001802,-3.08056845955723,
135.855897861661));
#181785=CARTESIAN_POINT('Ctrl Pts',(91.9088926794822,-3.21498719930563,
135.773925560947));
#181786=CARTESIAN_POINT('Ctrl Pts',(91.9163054587843,-3.34601144888164,
135.686657786049));
#181787=CARTESIAN_POINT('Ctrl Pts',(91.9237182380863,-3.47321473698105,
135.594424286591));
#181788=CARTESIAN_POINT('Ctrl Pts',(91.9311416091151,-3.60059977910374,
135.502058999584));
#181789=CARTESIAN_POINT('Ctrl Pts',(91.9385649801439,-3.72415266332074,
135.404714047604));
#181790=CARTESIAN_POINT('Ctrl Pts',(91.9459883511726,-3.84348102971194,
135.302758569809));
#181791=CARTESIAN_POINT('Ctrl Pts',(91.9499244006134,-3.90675179281829,
135.248699329093));
#181792=CARTESIAN_POINT('Ctrl Pts',(91.9538604500543,-3.968835515863,135.193344512691));
#181793=CARTESIAN_POINT('Ctrl Pts',(91.9577964994951,-4.02967817795937,
135.136753068));
#181794=CARTESIAN_POINT('Ctrl Pts',(91.9651092607808,-4.14271737387972,
135.031612181927));
#181795=CARTESIAN_POINT('Ctrl Pts',(91.9724220220665,-4.25183428317431,
134.921862168348));
#181796=CARTESIAN_POINT('Ctrl Pts',(91.9797347833521,-4.35662126326586,
134.807831827773));
#181797=CARTESIAN_POINT('Ctrl Pts',(91.9870388008535,-4.46128295077362,
134.693937831962));
#181798=CARTESIAN_POINT('Ctrl Pts',(91.9943428183548,-4.5616247513243,134.575773972212));
#181799=CARTESIAN_POINT('Ctrl Pts',(92.0016468358561,-4.6572727888953,134.453708604853));
#181800=CARTESIAN_POINT('Ctrl Pts',(92.008943826474,-4.7528288075724,134.331760671373));
#181801=CARTESIAN_POINT('Ctrl Pts',(92.0162408170919,-4.84369981294541,
134.205919000611));
#181802=CARTESIAN_POINT('Ctrl Pts',(92.0235378077098,-4.92954964602831,
134.076587817783));
#181803=CARTESIAN_POINT('Ctrl Pts',(92.030829124937,-5.01533273109574,133.947357189604));
#181804=CARTESIAN_POINT('Ctrl Pts',(92.0381204421642,-5.09610220423257,
133.814642770773));
#181805=CARTESIAN_POINT('Ctrl Pts',(92.0454117593914,-5.17156320462958,
133.67888050496));
#181806=CARTESIAN_POINT('Ctrl Pts',(92.0527000265024,-5.24699263805258,
133.543175031448));
#181807=CARTESIAN_POINT('Ctrl Pts',(92.0599882936134,-5.31711782937492,
133.404424583361));
#181808=CARTESIAN_POINT('Ctrl Pts',(92.0672765607244,-5.38168819565519,
133.263092552374));
#181809=CARTESIAN_POINT('Ctrl Pts',(92.0745633173205,-5.44624517953679,
133.121789812867));
#181810=CARTESIAN_POINT('Ctrl Pts',(92.0818500739167,-5.50524946949846,
132.97790690556));
#181811=CARTESIAN_POINT('Ctrl Pts',(92.0891368305128,-5.55849739808825,
132.831929910573));
#181812=CARTESIAN_POINT('Ctrl Pts',(92.0964236148311,-5.61174552925784,
132.685952360223));
#181813=CARTESIAN_POINT('Ctrl Pts',(92.1037103991495,-5.65923712502633,
132.537881068885));
#181814=CARTESIAN_POINT('Ctrl Pts',(92.1109971834678,-5.70081754541245,
132.388219789468));
#181815=CARTESIAN_POINT('Ctrl Pts',(92.1182883586633,-5.74242302136636,
132.23846832702));
#181816=CARTESIAN_POINT('Ctrl Pts',(92.1255795338589,-5.7781101049333,132.08712533467));
#181817=CARTESIAN_POINT('Ctrl Pts',(92.1328707090544,-5.80777463398576,
131.934707627706));
#181818=CARTESIAN_POINT('Ctrl Pts',(92.140164370051,-5.8374492766502,131.78223795654));
#181819=CARTESIAN_POINT('Ctrl Pts',(92.1474580310474,-5.86109721452016,
131.628693221285));
#181820=CARTESIAN_POINT('Ctrl Pts',(92.154751692044,-5.87866595867811,131.474597224131));
#181821=CARTESIAN_POINT('Ctrl Pts',(92.1620527420383,-5.89625250122448,
131.320345116762));
#181822=CARTESIAN_POINT('Ctrl Pts',(92.1693537920326,-5.90774752402002,
131.16554101612));
#181823=CARTESIAN_POINT('Ctrl Pts',(92.1766548420269,-5.91315060519789,
131.010711005857));
#181824=CARTESIAN_POINT('Ctrl Pts',(92.1799781639497,-5.91561000187961,
130.940234845878));
#181825=CARTESIAN_POINT('Ctrl Pts',(92.1833014858725,-5.91680790818329,
130.869753291447));
#181826=CARTESIAN_POINT('Ctrl Pts',(92.1866248077953,-5.91674784920219,
130.79931567344));
#181827=CARTESIAN_POINT('',(93.9366248077954,-5.92381476472989,130.807936889348));
#181828=CARTESIAN_POINT('Ctrl Pts',(92.1866248077953,-5.92001119952791,
130.799312890928));
#181829=CARTESIAN_POINT('Ctrl Pts',(92.2031645796329,-5.92319097430219,
130.448557057701));
#181830=CARTESIAN_POINT('Ctrl Pts',(92.3125202260744,-5.73488872890447,
128.132881907437));
#181831=CARTESIAN_POINT('Ctrl Pts',(92.514691747121,-2.67951836410898,124.339243304882));
#181832=CARTESIAN_POINT('Ctrl Pts',(92.7931393709338,3.99094117012314,125.055452103163));
#181833=CARTESIAN_POINT('Ctrl Pts',(93.0715869947465,6.99392073732381,131.054626976383));
#181834=CARTESIAN_POINT('Ctrl Pts',(93.3500346185597,3.56982881895088,136.823819292042));
#181835=CARTESIAN_POINT('Ctrl Pts',(93.6284822423723,-3.13476138820806,
137.061423152762));
#181836=CARTESIAN_POINT('Ctrl Pts',(93.8240123054511,-5.8199591828543,133.190582379912));
#181837=CARTESIAN_POINT('Ctrl Pts',(93.9267264939254,-5.92530633858584,
131.017497826861));
#181838=CARTESIAN_POINT('Ctrl Pts',(93.9366248077954,-5.92381476472989,
130.807936889348));
#181839=CARTESIAN_POINT('',(95.6866248077953,-5.90879879622959,130.807679832969));
#181840=CARTESIAN_POINT('Ctrl Pts',(93.9366248077954,-5.92381476472989,
130.807936889348));
#181841=CARTESIAN_POINT('Ctrl Pts',(94.0195423685297,-5.91131994314571,
129.052457926775));
#181842=CARTESIAN_POINT('Ctrl Pts',(94.1952758038683,-4.15316323793241,
125.310207551055));
#181843=CARTESIAN_POINT('Ctrl Pts',(94.463825113811,2.21513669179455,124.165781705854));
#181844=CARTESIAN_POINT('Ctrl Pts',(94.7422727376241,6.78255994238161,129.079703794217));
#181845=CARTESIAN_POINT('Ctrl Pts',(95.0207203614368,5.11714195239869,135.578501249066));
#181846=CARTESIAN_POINT('Ctrl Pts',(95.2991679852499,-1.25067950555994,
137.690096693304));
#181847=CARTESIAN_POINT('Ctrl Pts',(95.521136134036,-5.41068117704307,134.329209871018));
#181848=CARTESIAN_POINT('Ctrl Pts',(95.6502884082178,-5.91273003071525,
131.581978529553));
#181849=CARTESIAN_POINT('Ctrl Pts',(95.6866248077953,-5.90879879622959,
130.807679832969));
#181850=CARTESIAN_POINT('',(97.4366248077953,-5.91164346900976,130.799578598919));
#181851=CARTESIAN_POINT('Ctrl Pts',(95.6866248077953,-5.90879879622959,
130.807679832969));
#181852=CARTESIAN_POINT('Ctrl Pts',(95.743104282822,-5.90268828273519,129.60414881709));
#181853=CARTESIAN_POINT('Ctrl Pts',(95.8923996324532,-4.95936241370667,
126.413989174633));
#181854=CARTESIAN_POINT('Ctrl Pts',(96.1345108566885,0.26090962579987,123.810828841882));
#181855=CARTESIAN_POINT('Ctrl Pts',(96.4129584805014,6.02488437581224,127.243696523827));
#181856=CARTESIAN_POINT('Ctrl Pts',(96.6914061043143,6.25228471641837,133.94864055981));
#181857=CARTESIAN_POINT('Ctrl Pts',(96.969853728127,0.734140843724936,137.764144935481));
#181858=CARTESIAN_POINT('Ctrl Pts',(97.2182599626209,-4.79051041786796,
135.462322015875));
#181859=CARTESIAN_POINT('Ctrl Pts',(97.3738503225103,-5.90155615582126,
132.135635140803));
#181860=CARTESIAN_POINT('Ctrl Pts',(97.4366248077953,-5.91164346900976,
130.799578598919));
#181861=CARTESIAN_POINT('',(99.1866239901644,-5.92190965301424,130.802961585215));
#181862=CARTESIAN_POINT('Ctrl Pts',(97.4366248077953,-5.91164346900976,
130.799578598919));
#181863=CARTESIAN_POINT('Ctrl Pts',(97.4666661971145,-5.9164708586937,130.160194706803));
#181864=CARTESIAN_POINT('Ctrl Pts',(97.5895234610379,-5.52581770990293,
127.551110354335));
#181865=CARTESIAN_POINT('Ctrl Pts',(97.8051965995659,-1.71433292458932,
124.019183895178));
#181866=CARTESIAN_POINT('Ctrl Pts',(98.0836442233787,4.78192252208498,125.694490020073));
#181867=CARTESIAN_POINT('Ctrl Pts',(98.3620918471916,6.88382478086414,132.065517593005));
#181868=CARTESIAN_POINT('Ctrl Pts',(98.6405394710045,2.6598283595664,137.277603516453));
#181869=CARTESIAN_POINT('Ctrl Pts',(98.9153832961096,-3.92211680638712,
136.550627681392));
#181870=CARTESIAN_POINT('Ctrl Pts',(99.0974112466104,-5.92004009495408,
132.689770205197));
#181871=CARTESIAN_POINT('Ctrl Pts',(99.1866233225069,-5.92612303819684,
130.802974698158));
#181872=CARTESIAN_POINT('',(100.936624807795,-5.91594690676652,130.809831085281));
#181873=CARTESIAN_POINT('Ctrl Pts',(99.1866248077953,-5.91674983077855,
130.802945526759));
#181874=CARTESIAN_POINT('Ctrl Pts',(99.190228111407,-5.91673163312845,130.7268578703));
#181875=CARTESIAN_POINT('Ctrl Pts',(99.1938314150186,-5.91524580007589,
130.650789527188));
#181876=CARTESIAN_POINT('Ctrl Pts',(99.1974347186303,-5.91229419097278,
130.574778471288));
#181877=CARTESIAN_POINT('Ctrl Pts',(99.2048579850357,-5.90621349862531,
130.41818597215));
#181878=CARTESIAN_POINT('Ctrl Pts',(99.2122812514411,-5.89389807196139,
130.261598432965));
#181879=CARTESIAN_POINT('Ctrl Pts',(99.2197045178466,-5.8753381352769,130.105552805173));
#181880=CARTESIAN_POINT('Ctrl Pts',(99.2271190105676,-5.85680013489626,
129.949691610355));
#181881=CARTESIAN_POINT('Ctrl Pts',(99.2345335032886,-5.83203235906404,
129.794371419087));
#181882=CARTESIAN_POINT('Ctrl Pts',(99.2419479960096,-5.80107701710407,
129.640128680138));
#181883=CARTESIAN_POINT('Ctrl Pts',(99.2493553423634,-5.77015151106811,
129.486034606148));
#181884=CARTESIAN_POINT('Ctrl Pts',(99.2567626887172,-5.73305038463465,
129.333016280592));
#181885=CARTESIAN_POINT('Ctrl Pts',(99.264170035071,-5.68986756258922,129.181604418165));
#181886=CARTESIAN_POINT('Ctrl Pts',(99.2715718567464,-5.64671694792167,
129.030305484417));
#181887=CARTESIAN_POINT('Ctrl Pts',(99.2789736784218,-5.59749377128855,
128.880610985535));
#181888=CARTESIAN_POINT('Ctrl Pts',(99.2863755000972,-5.54234286797957,
128.733040725262));
#181889=CARTESIAN_POINT('Ctrl Pts',(99.2937734144086,-5.48722107840303,
128.585548366179));
#181890=CARTESIAN_POINT('Ctrl Pts',(99.3011713287199,-5.42617792445619,
128.440178361236));
#181891=CARTESIAN_POINT('Ctrl Pts',(99.3085692430313,-5.35940782021498,
128.297434535864));
#181892=CARTESIAN_POINT('Ctrl Pts',(99.3159659279435,-5.29264881195401,
128.154714431927));
#181893=CARTESIAN_POINT('Ctrl Pts',(99.3233626128557,-5.22016490028322,
128.014619979193));
#181894=CARTESIAN_POINT('Ctrl Pts',(99.3307592977679,-5.14219834169077,
127.877634327457));
#181895=CARTESIAN_POINT('Ctrl Pts',(99.3381556547034,-5.06423524021717,
127.740654749809));
#181896=CARTESIAN_POINT('Ctrl Pts',(99.3455520116389,-4.98079015985139,
127.606784023502));
#181897=CARTESIAN_POINT('Ctrl Pts',(99.3529483685743,-4.8921508225692,127.47647977659));
#181898=CARTESIAN_POINT('Ctrl Pts',(99.3603458579109,-4.80349791437826,
127.346155579765));
#181899=CARTESIAN_POINT('Ctrl Pts',(99.3677433472474,-4.70964937578964,
127.219399258241));
#181900=CARTESIAN_POINT('Ctrl Pts',(99.375140836584,-4.61093558044671,127.096638454907));
#181901=CARTESIAN_POINT('Ctrl Pts',(99.382540919099,-4.51218718113584,126.973834617964));
#181902=CARTESIAN_POINT('Ctrl Pts',(99.389941001614,-4.40857036319694,126.85502937857));
#181903=CARTESIAN_POINT('Ctrl Pts',(99.397341084129,-4.30045488985332,126.740616247796));
#181904=CARTESIAN_POINT('Ctrl Pts',(99.4047493037955,-4.19222053243215,
126.626077308023));
#181905=CARTESIAN_POINT('Ctrl Pts',(99.4121575234619,-4.0794778971994,126.515940393338));
#181906=CARTESIAN_POINT('Ctrl Pts',(99.4195657431284,-3.96263314250425,
126.410561675827));
#181907=CARTESIAN_POINT('Ctrl Pts',(99.4269785224305,-3.84571647181216,
126.305118099473));
#181908=CARTESIAN_POINT('Ctrl Pts',(99.4343913017325,-3.72469293701729,
126.204438794061));
#181909=CARTESIAN_POINT('Ctrl Pts',(99.4418040810346,-3.60000025985815,
126.108838421737));
#181910=CARTESIAN_POINT('Ctrl Pts',(99.4492274520634,-3.47512941595448,
126.013101451118));
#181911=CARTESIAN_POINT('Ctrl Pts',(99.4566508230921,-3.34657926322684,
125.92245812203));
#181912=CARTESIAN_POINT('Ctrl Pts',(99.4640741941209,-3.21481554320218,
125.837179164701));
#181913=CARTESIAN_POINT('Ctrl Pts',(99.4680102435616,-3.14495125721809,
125.791962215285));
#181914=CARTESIAN_POINT('Ctrl Pts',(99.4719462930024,-3.07418392752774,
125.748252612057));
#181915=CARTESIAN_POINT('Ctrl Pts',(99.4758823424432,-3.00258546426742,
125.706085311909));
#181916=CARTESIAN_POINT('Ctrl Pts',(99.4833056088486,-2.8675529970698,125.626559099827));
#181917=CARTESIAN_POINT('Ctrl Pts',(99.4907288752541,-2.72915467663098,
125.552281027277));
#181918=CARTESIAN_POINT('Ctrl Pts',(99.4981521416595,-2.58783697139819,
125.483549554207));
#181919=CARTESIAN_POINT('Ctrl Pts',(99.5055666343805,-2.44668629195717,
125.41489931603));
#181920=CARTESIAN_POINT('Ctrl Pts',(99.5129811271015,-2.30262342832347,
125.35178279001));
#181921=CARTESIAN_POINT('Ctrl Pts',(99.5203956198226,-2.15612252520884,
125.294454427912));
#181922=CARTESIAN_POINT('Ctrl Pts',(99.5278029661763,-2.00976282518029,
125.237181321047));
#181923=CARTESIAN_POINT('Ctrl Pts',(99.5352103125301,-1.86097010910352,
125.185685406831));
#181924=CARTESIAN_POINT('Ctrl Pts',(99.5426176588839,-1.71024165092188,
125.140174527937));
#181925=CARTESIAN_POINT('Ctrl Pts',(99.5500194805593,-1.5596256117108,125.094697592772));
#181926=CARTESIAN_POINT('Ctrl Pts',(99.5574213022347,-1.40707706092008,
125.05519691221));
#181927=CARTESIAN_POINT('Ctrl Pts',(99.5648231239101,-1.25311161117067,
125.021831598836));
#181928=CARTESIAN_POINT('Ctrl Pts',(99.5722210382215,-1.09922743858373,
124.988483898752));
#181929=CARTESIAN_POINT('Ctrl Pts',(99.5796189525328,-0.943928220562229,
124.961265194468));
#181930=CARTESIAN_POINT('Ctrl Pts',(99.5870168668442,-0.787742925268995,
124.940284249868));
#181931=CARTESIAN_POINT('Ctrl Pts',(99.5944135517564,-0.631583585138571,
124.919306791921));
#181932=CARTESIAN_POINT('Ctrl Pts',(99.6018102366686,-0.474538829596409,
124.904565085961));
#181933=CARTESIAN_POINT('Ctrl Pts',(99.6092069215808,-0.317146091797828,
124.896116469009));
#181934=CARTESIAN_POINT('Ctrl Pts',(99.6166032785163,-0.159760332958178,
124.887668226678));
#181935=CARTESIAN_POINT('Ctrl Pts',(99.6239996354517,-0.00202699530287781,
124.885512538533));
#181936=CARTESIAN_POINT('Ctrl Pts',(99.6313959923871,0.155513384969617,
124.889654695071));
#181937=CARTESIAN_POINT('Ctrl Pts',(99.6387934817237,0.313077885076512,
124.893797485784));
#181938=CARTESIAN_POINT('Ctrl Pts',(99.6461909710603,0.470448995785109,
124.904240031248));
#181939=CARTESIAN_POINT('Ctrl Pts',(99.6535884603969,0.627088353998179,
124.920935530189));
#181940=CARTESIAN_POINT('Ctrl Pts',(99.6609885429119,0.783782621895561,
124.937636881711));
#181941=CARTESIAN_POINT('Ctrl Pts',(99.6683886254269,0.939744255614704,
124.960595511352));
#181942=CARTESIAN_POINT('Ctrl Pts',(99.6757887079419,1.09444231709256,124.989713029186));
#181943=CARTESIAN_POINT('Ctrl Pts',(99.6831969276084,1.24931048499225,125.018862564724));
#181944=CARTESIAN_POINT('Ctrl Pts',(99.6906051472749,1.40291193879136,125.054184444152));
#181945=CARTESIAN_POINT('Ctrl Pts',(99.6980133669413,1.55472748231848,125.095529474659));
#181946=CARTESIAN_POINT('Ctrl Pts',(99.7054261462434,1.70663646577957,125.136899952343));
#181947=CARTESIAN_POINT('Ctrl Pts',(99.7128389255454,1.85675699353004,125.184300855926));
#181948=CARTESIAN_POINT('Ctrl Pts',(99.7202517048475,2.00458773210166,125.23753400029));
#181949=CARTESIAN_POINT('Ctrl Pts',(99.7276750758762,2.15262969816523,125.290843206668));
#181950=CARTESIAN_POINT('Ctrl Pts',(99.735098446905,2.29837499564107,125.350001157429));
#181951=CARTESIAN_POINT('Ctrl Pts',(99.7425218179338,2.44134410684905,125.414762347337));
#181952=CARTESIAN_POINT('Ctrl Pts',(99.7464578673746,2.51714976010779,125.44910028415));
#181953=CARTESIAN_POINT('Ctrl Pts',(99.7503939168153,2.592175357509,125.485012734642));
#181954=CARTESIAN_POINT('Ctrl Pts',(99.7543299662561,2.66635261964488,125.522458093833));
#181955=CARTESIAN_POINT('Ctrl Pts',(99.7617532326615,2.8062486210409,125.593078872639));
#181956=CARTESIAN_POINT('Ctrl Pts',(99.7691764990669,2.9435485399053,125.669368186712));
#181957=CARTESIAN_POINT('Ctrl Pts',(99.7765997654724,3.07775994633127,125.751111734396));
#181958=CARTESIAN_POINT('Ctrl Pts',(99.7840142581934,3.2118127260205,125.832758667995));
#181959=CARTESIAN_POINT('Ctrl Pts',(99.7914287509144,3.34278394363856,125.919846811222));
#181960=CARTESIAN_POINT('Ctrl Pts',(99.7988432436354,3.4702032349126,126.012114790096));
#181961=CARTESIAN_POINT('Ctrl Pts',(99.8062505899892,3.59749971467655,126.104293837619));
#181962=CARTESIAN_POINT('Ctrl Pts',(99.813657936343,3.72125078325056,126.201642564191));
#181963=CARTESIAN_POINT('Ctrl Pts',(99.8210652826968,3.84101278799423,126.303854943204));
#181964=CARTESIAN_POINT('Ctrl Pts',(99.8284671043722,3.96068546971632,126.405991088368));
#181965=CARTESIAN_POINT('Ctrl Pts',(99.8358689260476,4.07637472889887,126.512983421846));
#181966=CARTESIAN_POINT('Ctrl Pts',(99.843270747723,4.18766799839924,126.624484148377));
#181967=CARTESIAN_POINT('Ctrl Pts',(99.8506686620344,4.29890251704895,126.735926014542));
#181968=CARTESIAN_POINT('Ctrl Pts',(99.8580665763457,4.40574540457195,126.851871270446));
#181969=CARTESIAN_POINT('Ctrl Pts',(99.865464490657,4.50781923461863,126.97193366973));
#181970=CARTESIAN_POINT('Ctrl Pts',(99.8728611755693,4.60987610184649,127.09197611682));
#181971=CARTESIAN_POINT('Ctrl Pts',(99.8802578604815,4.70716524297956,127.216134065239));
#181972=CARTESIAN_POINT('Ctrl Pts',(99.8876545453937,4.79934792301003,127.343986349311));
#181973=CARTESIAN_POINT('Ctrl Pts',(99.8950509023291,4.89152651556394,127.47183296428));
#181974=CARTESIAN_POINT('Ctrl Pts',(99.9024472592646,4.97859887890554,127.603373286392));
#181975=CARTESIAN_POINT('Ctrl Pts',(99.9098436162,5.06026838897342,127.738155406877));
#181976=CARTESIAN_POINT('Ctrl Pts',(99.9172411055366,5.14195040285179,127.872958162849));
#181977=CARTESIAN_POINT('Ctrl Pts',(99.9246385948732,5.21822772294531,128.011003386167));
#181978=CARTESIAN_POINT('Ctrl Pts',(99.9320360842097,5.28884872608873,128.151812839476));
#181979=CARTESIAN_POINT('Ctrl Pts',(99.9394361667247,5.35949448531528,128.292671653321));
#181980=CARTESIAN_POINT('Ctrl Pts',(99.9468362492398,5.42447981257595,128.436296292949));
#181981=CARTESIAN_POINT('Ctrl Pts',(99.9542363317547,5.48360050111013,128.582186882971));
#181982=CARTESIAN_POINT('Ctrl Pts',(99.9616445514212,5.54278619891914,128.728237894695));
#181983=CARTESIAN_POINT('Ctrl Pts',(99.9690527710876,5.59609423909144,128.876559486611));
#181984=CARTESIAN_POINT('Ctrl Pts',(99.9764609907541,5.64336950355073,129.026634201918));
#181985=CARTESIAN_POINT('Ctrl Pts',(99.9838737700562,5.69067386514649,129.176801285708));
#181986=CARTESIAN_POINT('Ctrl Pts',(99.9912865493583,5.73193795464536,129.328723283557));
#181987=CARTESIAN_POINT('Ctrl Pts',(99.9986993286603,5.76705752781521,129.481871285522));
#181988=CARTESIAN_POINT('Ctrl Pts',(100.006122699689,5.80222728147815,129.635238112534));
#181989=CARTESIAN_POINT('Ctrl Pts',(100.013546070718,5.83123491537528,129.789834076422));
#181990=CARTESIAN_POINT('Ctrl Pts',(100.020969441747,5.85402778899558,129.945123043802));
#181991=CARTESIAN_POINT('Ctrl Pts',(100.024905491187,5.86611311749639,130.027460980414));
#181992=CARTESIAN_POINT('Ctrl Pts',(100.028841540628,5.87645212380115,130.109993697044));
#181993=CARTESIAN_POINT('Ctrl Pts',(100.032777590069,5.88504290467065,130.192641259784));
#181994=CARTESIAN_POINT('Ctrl Pts',(100.040200856474,5.90124484928165,130.348511983771));
#181995=CARTESIAN_POINT('Ctrl Pts',(100.04762412288,5.91127444860908,130.505262531775));
#181996=CARTESIAN_POINT('Ctrl Pts',(100.055047389285,5.91504583031439,130.662362773285));
#181997=CARTESIAN_POINT('Ctrl Pts',(100.062461882006,5.91881275455972,130.819277335357));
#181998=CARTESIAN_POINT('Ctrl Pts',(100.069876374727,5.91633617547076,130.976540398697));
#181999=CARTESIAN_POINT('Ctrl Pts',(100.077290867448,5.90758175100173,131.1336149535));
#182000=CARTESIAN_POINT('Ctrl Pts',(100.084698213802,5.89883576437661,131.290538113933));
#182001=CARTESIAN_POINT('Ctrl Pts',(100.092105560156,5.88382399900399,131.447272757324));
#182002=CARTESIAN_POINT('Ctrl Pts',(100.099512906509,5.86256411864931,131.603280211283));
#182003=CARTESIAN_POINT('Ctrl Pts',(100.106914728185,5.8413200947155,131.759171308998));
#182004=CARTESIAN_POINT('Ctrl Pts',(100.11431654986,5.81383728483579,131.914335928916));
#182005=CARTESIAN_POINT('Ctrl Pts',(100.121718371535,5.78018529639496,132.068238974782));
#182006=CARTESIAN_POINT('Ctrl Pts',(100.129116285847,5.7465510725769,132.222060776429));
#182007=CARTESIAN_POINT('Ctrl Pts',(100.136514200158,5.70675423553321,132.374621966586));
#182008=CARTESIAN_POINT('Ctrl Pts',(100.14391211447,5.66091573710451,132.525396230185));
#182009=CARTESIAN_POINT('Ctrl Pts',(100.151308799382,5.61508485620265,132.676145437837));
#182010=CARTESIAN_POINT('Ctrl Pts',(100.158705484294,5.56321441506422,132.82510795149));
#182011=CARTESIAN_POINT('Ctrl Pts',(100.166102169206,5.50547565775297,132.971771133456));
#182012=CARTESIAN_POINT('Ctrl Pts',(100.173498526141,5.44773946063873,133.118427812222));
#182013=CARTESIAN_POINT('Ctrl Pts',(100.180894883077,5.38413560147719,133.262785014671));
#182014=CARTESIAN_POINT('Ctrl Pts',(100.188291240012,5.31488395136552,133.404348914851));
#182015=CARTESIAN_POINT('Ctrl Pts',(100.195688729349,5.24562169864942,133.545934488824));
#182016=CARTESIAN_POINT('Ctrl Pts',(100.203086218685,5.17071009731625,133.68472557365));
#182017=CARTESIAN_POINT('Ctrl Pts',(100.210483708022,5.09041549352912,133.820251972661));
#182018=CARTESIAN_POINT('Ctrl Pts',(100.217883790537,5.01009274259305,133.955825880242));
#182019=CARTESIAN_POINT('Ctrl Pts',(100.225283873052,4.92438342235262,134.088132502492));
#182020=CARTESIAN_POINT('Ctrl Pts',(100.232683955567,4.8335977133866,134.216729839623));
#182021=CARTESIAN_POINT('Ctrl Pts',(100.240092175233,4.74271217620058,134.345468582747));
#182022=CARTESIAN_POINT('Ctrl Pts',(100.2475003949,4.6467393180703,134.470489590093));
#182023=CARTESIAN_POINT('Ctrl Pts',(100.254908614566,4.54603064494879,134.59138265839));
#182024=CARTESIAN_POINT('Ctrl Pts',(100.262321393868,4.4452599873193,134.712350134353));
#182025=CARTESIAN_POINT('Ctrl Pts',(100.269734173171,4.33974795618001,134.829184332247));
#182026=CARTESIAN_POINT('Ctrl Pts',(100.277146952473,4.22988319189158,134.941511659703));
#182027=CARTESIAN_POINT('Ctrl Pts',(100.284570323501,4.11986144767587,135.053999485712));
#182028=CARTESIAN_POINT('Ctrl Pts',(100.29199369453,4.00547481954478,135.161967324346));
#182029=CARTESIAN_POINT('Ctrl Pts',(100.299417065559,3.88714591821438,135.265081094463));
#182030=CARTESIAN_POINT('Ctrl Pts',(100.303353115,3.82440509546536,135.319754489561));
#182031=CARTESIAN_POINT('Ctrl Pts',(100.30728916444,3.76055646896729,135.373063937694));
#182032=CARTESIAN_POINT('Ctrl Pts',(100.311225213881,3.69566626063343,135.424964631385));
#182033=CARTESIAN_POINT('Ctrl Pts',(100.318648480287,3.57328535287096,135.522847719918));
#182034=CARTESIAN_POINT('Ctrl Pts',(100.326071746692,3.44682792085274,135.616013405926));
#182035=CARTESIAN_POINT('Ctrl Pts',(100.333495013098,3.3166935622925,135.704102894089));
#182036=CARTESIAN_POINT('Ctrl Pts',(100.340909505819,3.18671301173692,135.792088267793));
#182037=CARTESIAN_POINT('Ctrl Pts',(100.34832399854,3.05306449113602,135.875009178764));
#182038=CARTESIAN_POINT('Ctrl Pts',(100.355738491261,2.9161812393335,135.95254646715));
#182039=CARTESIAN_POINT('Ctrl Pts',(100.363145837614,2.77942992076272,136.030009022179));
#182040=CARTESIAN_POINT('Ctrl Pts',(100.370553183968,2.63945040045551,136.102098102025));
#182041=CARTESIAN_POINT('Ctrl Pts',(100.377960530322,2.49670542644565,136.16853740213));
#182042=CARTESIAN_POINT('Ctrl Pts',(100.385362351997,2.35406691702286,136.234927149299));
#182043=CARTESIAN_POINT('Ctrl Pts',(100.392764173673,2.20866739775046,136.295675350166));
#182044=CARTESIAN_POINT('Ctrl Pts',(100.400165995348,2.06099468475453,136.350551334798));
#182045=CARTESIAN_POINT('Ctrl Pts',(100.40756390966,1.9133999270344,136.405398350826));
#182046=CARTESIAN_POINT('Ctrl Pts',(100.414961823971,1.76353471448369,136.45437919451));
#182047=CARTESIAN_POINT('Ctrl Pts',(100.422359738282,1.6119072283005,136.49731113991));
#182048=CARTESIAN_POINT('Ctrl Pts',(100.429756423194,1.4603049398546,136.540235950799));
#182049=CARTESIAN_POINT('Ctrl Pts',(100.437153108107,1.30694131783884,136.577113756863));
#182050=CARTESIAN_POINT('Ctrl Pts',(100.444549793019,1.15234022045967,136.60781153739));
#182051=CARTESIAN_POINT('Ctrl Pts',(100.451946149954,0.997745978255167,
136.638507956746));
#182052=CARTESIAN_POINT('Ctrl Pts',(100.45934250689,0.841914735938592,136.663024822723));
#182053=CARTESIAN_POINT('Ctrl Pts',(100.466738863825,0.685380808968709,
136.681280194113));
#182054=CARTESIAN_POINT('Ctrl Pts',(100.474136353162,0.528822916254995,
136.699538360446));
#182055=CARTESIAN_POINT('Ctrl Pts',(100.481533842498,0.371562495485032,
136.711533080147));
#182056=CARTESIAN_POINT('Ctrl Pts',(100.488931331835,0.21413910303813,136.717234285001));
#182057=CARTESIAN_POINT('Ctrl Pts',(100.49633141435,0.0566605260651548,
136.722937488404));
#182058=CARTESIAN_POINT('Ctrl Pts',(100.503731496865,-0.10098076350849,
136.722342770967));
#182059=CARTESIAN_POINT('Ctrl Pts',(100.51113157938,-0.258245238563375,
136.715472184713));
#182060=CARTESIAN_POINT('Ctrl Pts',(100.518539799047,-0.415682642075875,
136.708594043543));
#182061=CARTESIAN_POINT('Ctrl Pts',(100.525948018713,-0.572742030421845,
136.695426268184));
#182062=CARTESIAN_POINT('Ctrl Pts',(100.533356238379,-0.728888290417765,
136.676042865661));
#182063=CARTESIAN_POINT('Ctrl Pts',(100.540769017682,-0.885130655831496,
136.656647532977));
#182064=CARTESIAN_POINT('Ctrl Pts',(100.548181796984,-1.04045840554142,
136.631029010719));
#182065=CARTESIAN_POINT('Ctrl Pts',(100.555594576286,-1.19434715609937,
136.599312337228));
#182066=CARTESIAN_POINT('Ctrl Pts',(100.563017947314,-1.34845579012067,
136.567550345468));
#182067=CARTESIAN_POINT('Ctrl Pts',(100.570441318343,-1.50112095712515,
136.529672889666));
#182068=CARTESIAN_POINT('Ctrl Pts',(100.577864689372,-1.651833153772,136.48585494517));
#182069=CARTESIAN_POINT('Ctrl Pts',(100.581800738813,-1.73174437672379,
136.462621619602));
#182070=CARTESIAN_POINT('Ctrl Pts',(100.585736788254,-1.81110686745139,
136.437719020714));
#182071=CARTESIAN_POINT('Ctrl Pts',(100.589672837694,-1.88984713359227,
136.411178643341));
#182072=CARTESIAN_POINT('Ctrl Pts',(100.5970961041,-2.0383488181342,136.361124319913));
#182073=CARTESIAN_POINT('Ctrl Pts',(100.604519370505,-2.18508507926232,
136.305090429881));
#182074=CARTESIAN_POINT('Ctrl Pts',(100.611942636911,-2.32953805998807,
136.243219228485));
#182075=CARTESIAN_POINT('Ctrl Pts',(100.619357129632,-2.47382030928688,
136.181421153711));
#182076=CARTESIAN_POINT('Ctrl Pts',(100.626771622353,-2.61582431006067,
136.113799646043));
#182077=CARTESIAN_POINT('Ctrl Pts',(100.634186115074,-2.75504736790875,
136.040546687892));
#182078=CARTESIAN_POINT('Ctrl Pts',(100.641593461428,-2.89413623733203,
135.967364333701));
#182079=CARTESIAN_POINT('Ctrl Pts',(100.649000807781,-3.0304491717913,135.888561507371));
#182080=CARTESIAN_POINT('Ctrl Pts',(100.656408154135,-3.16350358182101,
135.804378182566));
#182081=CARTESIAN_POINT('Ctrl Pts',(100.663809975811,-3.29645875485178,
135.72025764486));
#182082=CARTESIAN_POINT('Ctrl Pts',(100.671211797486,-3.42615992846691,
135.630764797794));
#182083=CARTESIAN_POINT('Ctrl Pts',(100.678613619161,-3.55214935698775,
135.536185372156));
#182084=CARTESIAN_POINT('Ctrl Pts',(100.686011533473,-3.67807227667005,
135.441655874261));
#182085=CARTESIAN_POINT('Ctrl Pts',(100.693409447784,-3.80028705571648,
135.342045368973));
#182086=CARTESIAN_POINT('Ctrl Pts',(100.700807362095,-3.91836527726643,
135.237682635693));
#182087=CARTESIAN_POINT('Ctrl Pts',(100.708204047008,-4.03642387635795,
135.133337245606));
#182088=CARTESIAN_POINT('Ctrl Pts',(100.71560073192,-4.15034700284785,135.024241441889));
#182089=CARTESIAN_POINT('Ctrl Pts',(100.722997416832,-4.2597395844868,134.910764060344));
#182090=CARTESIAN_POINT('Ctrl Pts',(100.730393773767,-4.36912731554406,
134.797291710504));
#182091=CARTESIAN_POINT('Ctrl Pts',(100.737790130703,-4.47398464210597,
134.679438437891));
#182092=CARTESIAN_POINT('Ctrl Pts',(100.745186487638,-4.57395381415604,
134.557609486009));
#182093=CARTESIAN_POINT('Ctrl Pts',(100.752583976975,-4.6739382917417,134.435761881803));
#182094=CARTESIAN_POINT('Ctrl Pts',(100.759981466312,-4.76903288785948,
134.309937674948));
#182095=CARTESIAN_POINT('Ctrl Pts',(100.767378955648,-4.85892066186766,
134.180574556903));
#182096=CARTESIAN_POINT('Ctrl Pts',(100.774779038163,-4.94883994589581,
134.051166090818));
#182097=CARTESIAN_POINT('Ctrl Pts',(100.782179120678,-5.03354856088985,
133.918216549965));
#182098=CARTESIAN_POINT('Ctrl Pts',(100.789579203193,-5.11277343225509,
133.782191773445));
#182099=CARTESIAN_POINT('Ctrl Pts',(100.79698742286,-5.19208541951074,133.646017423701));
#182100=CARTESIAN_POINT('Ctrl Pts',(100.804395642526,-5.26590143296005,
133.50676140791));
#182101=CARTESIAN_POINT('Ctrl Pts',(100.811803862193,-5.33399449506292,
133.364913934554));
#182102=CARTESIAN_POINT('Ctrl Pts',(100.819216641495,-5.40212946730932,
133.222979156445));
#182103=CARTESIAN_POINT('Ctrl Pts',(100.826629420797,-5.46453432178863,
133.078450084456));
#182104=CARTESIAN_POINT('Ctrl Pts',(100.834042200099,-5.52103081473653,
132.931835483511));
#182105=CARTESIAN_POINT('Ctrl Pts',(100.841465571127,-5.57760803252298,
132.78501139275));
#182106=CARTESIAN_POINT('Ctrl Pts',(100.848888942156,-5.62825990803157,
132.636096173978));
#182107=CARTESIAN_POINT('Ctrl Pts',(100.856312313185,-5.67285825397636,
132.485613065235));
#182108=CARTESIAN_POINT('Ctrl Pts',(100.860248362626,-5.69650536711889,
132.405823310187));
#182109=CARTESIAN_POINT('Ctrl Pts',(100.864184412066,-5.71845147017101,
132.325592936097));
#182110=CARTESIAN_POINT('Ctrl Pts',(100.868120461507,-5.73868333621174,
132.245000797898));
#182111=CARTESIAN_POINT('Ctrl Pts',(100.877925013815,-5.78908015969434,
132.044248788432));
#182112=CARTESIAN_POINT('Ctrl Pts',(100.887729566123,-5.82896187484381,
131.840759098584));
#182113=CARTESIAN_POINT('Ctrl Pts',(100.897534118431,-5.85808598425451,
131.635479841012));
#182114=CARTESIAN_POINT('Ctrl Pts',(100.907119184766,-5.88655811759235,
131.434795991399));
#182115=CARTESIAN_POINT('Ctrl Pts',(100.9167042511,-5.90474895845509,131.232401516521));
#182116=CARTESIAN_POINT('Ctrl Pts',(100.926289317435,-5.91247627987531,
131.029204568812));
#182117=CARTESIAN_POINT('Ctrl Pts',(100.929734473082,-5.91525370718769,
130.956169590497));
#182118=CARTESIAN_POINT('Ctrl Pts',(100.933179628729,-5.91667977690174,
130.883031174209));
#182119=CARTESIAN_POINT('Ctrl Pts',(100.936624784376,-5.91674746993127,
130.809832323138));
#182120=CARTESIAN_POINT('',(102.686624807795,-5.90708923804999,130.803354028443));
#182121=CARTESIAN_POINT('Ctrl Pts',(100.936624807795,-5.91594690676652,
130.809831085281));
#182122=CARTESIAN_POINT('Ctrl Pts',(101.006605900304,-5.90234915318238,
129.323137679429));
#182123=CARTESIAN_POINT('Ctrl Pts',(101.169402867416,-4.57985391044984,
125.843090929061));
#182124=CARTESIAN_POINT('Ctrl Pts',(101.425015709134,1.27163152452042,123.922463074289));
#182125=CARTESIAN_POINT('Ctrl Pts',(101.703463332946,6.47728320895777,128.154386511786));
#182126=CARTESIAN_POINT('Ctrl Pts',(101.981910956759,5.73062805723803,134.821506694067));
#182127=CARTESIAN_POINT('Ctrl Pts',(102.260358580572,-0.282194322339087,
137.797065880537));
#182128=CARTESIAN_POINT('Ctrl Pts',(102.495263197585,-5.13597471230578,
134.886235526842));
#182129=CARTESIAN_POINT('Ctrl Pts',(102.637351939992,-5.90549920155596,
131.854077402682));
#182130=CARTESIAN_POINT('Ctrl Pts',(102.686624807795,-5.90708923804999,
130.803354028443));
#182131=CARTESIAN_POINT('',(104.436623928268,-5.91867361597261,130.799254319557));
#182132=CARTESIAN_POINT('Ctrl Pts',(102.686624807795,-5.90708923804999,
130.803354028443));
#182133=CARTESIAN_POINT('Ctrl Pts',(102.730167814596,-5.90849437180735,
129.874817552491));
#182134=CARTESIAN_POINT('Ctrl Pts',(102.866526696002,-5.26416868365254,
126.968865704744));
#182135=CARTESIAN_POINT('Ctrl Pts',(103.09570145201,-0.712954253829686,
123.842374064699));
#182136=CARTESIAN_POINT('Ctrl Pts',(103.374149075824,5.47194727155702,126.441408224103));
#182137=CARTESIAN_POINT('Ctrl Pts',(103.652596699636,6.62839657387416,133.049782491025));
#182138=CARTESIAN_POINT('Ctrl Pts',(103.931044323449,1.69367323997139,137.594723751195));
#182139=CARTESIAN_POINT('Ctrl Pts',(104.192386583952,-4.39869557774552,
136.00378319751));
#182140=CARTESIAN_POINT('Ctrl Pts',(104.36091296985,-5.90497045334534,132.405092580601));
#182141=CARTESIAN_POINT('Ctrl Pts',(104.436623481144,-5.91965264882207,
130.799262955289));
#182142=CARTESIAN_POINT('',(106.186626238041,-5.92089107076249,130.807736560839));
#182143=CARTESIAN_POINT('Ctrl Pts',(104.436624807795,-5.91674778188568,
130.799237332397));
#182144=CARTESIAN_POINT('Ctrl Pts',(104.447754512545,-5.9165434785673,130.563292783946));
#182145=CARTESIAN_POINT('Ctrl Pts',(104.458884217295,-5.90222283262232,
130.32793572196));
#182146=CARTESIAN_POINT('Ctrl Pts',(104.470013922045,-5.87401388310876,
130.094507489415));
#182147=CARTESIAN_POINT('Ctrl Pts',(104.475989138389,-5.85886931459173,
129.969186627684));
#182148=CARTESIAN_POINT('Ctrl Pts',(104.481964354732,-5.83972243368569,
129.844421012513));
#182149=CARTESIAN_POINT('Ctrl Pts',(104.487939571075,-5.81661343588987,
129.720414724117));
#182150=CARTESIAN_POINT('Ctrl Pts',(104.49536283748,-5.78790414117255,129.566356416966));
#182151=CARTESIAN_POINT('Ctrl Pts',(104.502786103886,-5.7530266451983,129.413206531442));
#182152=CARTESIAN_POINT('Ctrl Pts',(104.510209370291,-5.71204908842056,
129.261497767545));
#182153=CARTESIAN_POINT('Ctrl Pts',(104.517623863012,-5.67111996371195,
129.109968310809));
#182154=CARTESIAN_POINT('Ctrl Pts',(104.525038355733,-5.62410522566874,
128.959876942165));
#182155=CARTESIAN_POINT('Ctrl Pts',(104.532452848454,-5.57112437816934,
128.811748330776));
#182156=CARTESIAN_POINT('Ctrl Pts',(104.539860194807,-5.51819459560541,
128.663762491319));
#182157=CARTESIAN_POINT('Ctrl Pts',(104.547267541161,-5.45931027629513,
128.517735992088));
#182158=CARTESIAN_POINT('Ctrl Pts',(104.554674887515,-5.39464126270649,
128.374180334294));
#182159=CARTESIAN_POINT('Ctrl Pts',(104.56207670919,-5.330020481708,128.230731745725));
#182160=CARTESIAN_POINT('Ctrl Pts',(104.569478530866,-5.2596237497342,128.089750668129));
#182161=CARTESIAN_POINT('Ctrl Pts',(104.576880352541,-5.18366970116864,
127.951730429181));
#182162=CARTESIAN_POINT('Ctrl Pts',(104.584278266852,-5.10775574815394,
127.813783050043));
#182163=CARTESIAN_POINT('Ctrl Pts',(104.591676181164,-5.02629050060196,
127.678793722975));
#182164=CARTESIAN_POINT('Ctrl Pts',(104.599074095475,-4.93953933280967,
127.547232781247));
#182165=CARTESIAN_POINT('Ctrl Pts',(104.606470780387,-4.85280258148795,
127.41569370256));
#182166=CARTESIAN_POINT('Ctrl Pts',(104.613867465299,-4.76078185863432,
127.287582189795));
#182167=CARTESIAN_POINT('Ctrl Pts',(104.621264150212,-4.66378687969518,
127.163341185692));
#182168=CARTESIAN_POINT('Ctrl Pts',(104.628660507147,-4.56679620161498,
127.039105690566));
#182169=CARTESIAN_POINT('Ctrl Pts',(104.636056864082,-4.46483193572243,
126.918740657105));
#182170=CARTESIAN_POINT('Ctrl Pts',(104.643453221018,-4.35824508450094,
126.802657187035));
#182171=CARTESIAN_POINT('Ctrl Pts',(104.650850710355,-4.25164191456034,
126.686555944289));
#182172=CARTESIAN_POINT('Ctrl Pts',(104.658248199691,-4.14041500259756,
126.574737845144));
#182173=CARTESIAN_POINT('Ctrl Pts',(104.665645689028,-4.02495320719324,
126.467578141766));
#182174=CARTESIAN_POINT('Ctrl Pts',(104.673045771543,-3.90945093683552,
126.36038087372));
#182175=CARTESIAN_POINT('Ctrl Pts',(104.680445854058,-3.78971110078864,
126.257845506502));
#182176=CARTESIAN_POINT('Ctrl Pts',(104.687845936573,-3.66615658516074,
126.160307812571));
#182177=CARTESIAN_POINT('Ctrl Pts',(104.695254156239,-3.54246620864119,
126.062662865918));
#182178=CARTESIAN_POINT('Ctrl Pts',(104.702662375906,-3.41495306876543,
125.970026798783));
#182179=CARTESIAN_POINT('Ctrl Pts',(104.710070595572,-3.28407065155395,
125.882693164547));
#182180=CARTESIAN_POINT('Ctrl Pts',(104.717483374874,-3.15310767839848,
125.795305777918));
#182181=CARTESIAN_POINT('Ctrl Pts',(104.724896154176,-3.01877161353898,
125.713227521416));
#182182=CARTESIAN_POINT('Ctrl Pts',(104.732308933478,-2.88154115773741,
125.636706302621));
#182183=CARTESIAN_POINT('Ctrl Pts',(104.739732304507,-2.74411462062511,
125.560075746721));
#182184=CARTESIAN_POINT('Ctrl Pts',(104.747155675536,-2.60378576492046,
125.489018254992));
#182185=CARTESIAN_POINT('Ctrl Pts',(104.754579046565,-2.46105464894796,
125.423734206321));
#182186=CARTESIAN_POINT('Ctrl Pts',(104.758515096006,-2.38537518646285,
125.389119037241));
#182187=CARTESIAN_POINT('Ctrl Pts',(104.762451145447,-2.30902065175045,
125.356126168367));
#182188=CARTESIAN_POINT('Ctrl Pts',(104.766387194889,-2.23206726167876,
125.324779766639));
#182189=CARTESIAN_POINT('Ctrl Pts',(104.773810461294,-2.08693556965547,
125.265661431276));
#182190=CARTESIAN_POINT('Ctrl Pts',(104.7812337277,-1.939234095028,125.212223602401));
#182191=CARTESIAN_POINT('Ctrl Pts',(104.788656994105,-1.78944784497462,
125.164696888884));
#182192=CARTESIAN_POINT('Ctrl Pts',(104.796071486826,-1.63983862982983,
125.117226347995));
#182193=CARTESIAN_POINT('Ctrl Pts',(104.803485979547,-1.48814989626871,
125.0756531277));
#182194=CARTESIAN_POINT('Ctrl Pts',(104.810900472268,-1.33488765808264,
125.040160282498));
#182195=CARTESIAN_POINT('Ctrl Pts',(104.818307818622,-1.18177313981183,
125.004701646637));
#182196=CARTESIAN_POINT('Ctrl Pts',(104.825715164976,-1.02708849740593,
124.975311802433));
#182197=CARTESIAN_POINT('Ctrl Pts',(104.83312251133,-0.871355875321791,
124.952124335507));
#182198=CARTESIAN_POINT('Ctrl Pts',(104.840524333005,-0.715739404502658,
124.928954162669));
#182199=CARTESIAN_POINT('Ctrl Pts',(104.84792615468,-0.559076877960228,
124.911977210923));
#182200=CARTESIAN_POINT('Ctrl Pts',(104.855327976356,-0.401901523465638,
124.901276192629));
#182201=CARTESIAN_POINT('Ctrl Pts',(104.862725890667,-0.244809140617348,
124.890580823319));
#182202=CARTESIAN_POINT('Ctrl Pts',(104.870123804979,-0.0872048404574969,
124.886154814723));
#182203=CARTESIAN_POINT('Ctrl Pts',(104.87752171929,0.0703722310258373,
124.888029126549));
#182204=CARTESIAN_POINT('Ctrl Pts',(104.884918404202,0.22792311605863,124.889903126898));
#182205=CARTESIAN_POINT('Ctrl Pts',(104.892315089114,0.385446408489498,
124.89807536525));
#182206=CARTESIAN_POINT('Ctrl Pts',(104.899711774026,0.542402039280793,
124.9125246906));
#182207=CARTESIAN_POINT('Ctrl Pts',(104.907108130962,0.69935071049494,124.926973375252));
#182208=CARTESIAN_POINT('Ctrl Pts',(104.914504487897,0.855731398391698,
124.947698559261));
#182209=CARTESIAN_POINT('Ctrl Pts',(104.921900844833,1.01100850603132,124.974627144822));
#182210=CARTESIAN_POINT('Ctrl Pts',(104.929298334169,1.16630938699253,125.001559853218));
#182211=CARTESIAN_POINT('Ctrl Pts',(104.936695823506,1.32050598344136,125.034697790466));
#182212=CARTESIAN_POINT('Ctrl Pts',(104.944093312842,1.47307239754155,125.073916631791));
#182213=CARTESIAN_POINT('Ctrl Pts',(104.951493395357,1.62569229356169,125.113149221221));
#182214=CARTESIAN_POINT('Ctrl Pts',(104.958893477872,1.77668050814672,125.15846686595));
#182215=CARTESIAN_POINT('Ctrl Pts',(104.966293560387,1.92552596614671,125.209695273133));
#182216=CARTESIAN_POINT('Ctrl Pts',(104.973701780054,2.07453509502946,125.260980011217));
#182217=CARTESIAN_POINT('Ctrl Pts',(104.98110999972,2.22139640868509,125.318188370107));
#182218=CARTESIAN_POINT('Ctrl Pts',(104.988518219387,2.36561781206822,125.381097491945));
#182219=CARTESIAN_POINT('Ctrl Pts',(104.995930998689,2.50992798131898,125.444045333297));
#182220=CARTESIAN_POINT('Ctrl Pts',(105.003343777991,2.65159466748911,125.512700766747));
#182221=CARTESIAN_POINT('Ctrl Pts',(105.010756557293,2.79015054945589,125.58679504789));
#182222=CARTESIAN_POINT('Ctrl Pts',(105.018179928322,2.92890440656424,125.660995198416));
#182223=CARTESIAN_POINT('Ctrl Pts',(105.02560329935,3.06453826104044,125.740649529086));
#182224=CARTESIAN_POINT('Ctrl Pts',(105.033026670379,3.19661323471266,125.825445636352));
#182225=CARTESIAN_POINT('Ctrl Pts',(105.03696271982,3.2666425548477,125.870406567078));
#182226=CARTESIAN_POINT('Ctrl Pts',(105.04089876926,3.3356718809024,125.916812348075));
#182227=CARTESIAN_POINT('Ctrl Pts',(105.044834818701,3.40363968346692,125.964611918756));
#182228=CARTESIAN_POINT('Ctrl Pts',(105.052258085107,3.53182483790369,126.054760417289));
#182229=CARTESIAN_POINT('Ctrl Pts',(105.059681351512,3.65661985161943,126.150141399217));
#182230=CARTESIAN_POINT('Ctrl Pts',(105.067104617917,3.77756854861396,126.250471463994));
#182231=CARTESIAN_POINT('Ctrl Pts',(105.074519110638,3.89837429429289,126.350682946966));
#182232=CARTESIAN_POINT('Ctrl Pts',(105.081933603359,4.0153424876353,126.455831633507));
#182233=CARTESIAN_POINT('Ctrl Pts',(105.08934809608,4.128045606891,126.565590745312));
#182234=CARTESIAN_POINT('Ctrl Pts',(105.096755442434,4.24064009863725,126.675244067153));
#182235=CARTESIAN_POINT('Ctrl Pts',(105.104162788788,4.34897743453195,126.789498709027));
#182236=CARTESIAN_POINT('Ctrl Pts',(105.111570135142,4.45266299337704,126.907987582305));
#182237=CARTESIAN_POINT('Ctrl Pts',(105.118971956817,4.55627121962051,127.02638808211));
#182238=CARTESIAN_POINT('Ctrl Pts',(105.126373778493,4.65523433222816,127.1490162455));
#182239=CARTESIAN_POINT('Ctrl Pts',(105.133775600168,4.74919452031331,127.275468160898));
#182240=CARTESIAN_POINT('Ctrl Pts',(105.141173514479,4.84310510754649,127.401853323315));
#182241=CARTESIAN_POINT('Ctrl Pts',(105.148571428791,4.93201780786472,127.532057918868));
#182242=CARTESIAN_POINT('Ctrl Pts',(105.155969343102,5.01561515241312,127.665645083246));
#182243=CARTESIAN_POINT('Ctrl Pts',(105.163366028014,5.09919860459946,127.79921004786));
#182244=CARTESIAN_POINT('Ctrl Pts',(105.170762712927,5.17746825630318,127.936156149521));
#182245=CARTESIAN_POINT('Ctrl Pts',(105.178159397839,5.25014998195715,128.076017580216));
#182246=CARTESIAN_POINT('Ctrl Pts',(105.185555754774,5.32282848482725,128.215872809309));
#182247=CARTESIAN_POINT('Ctrl Pts',(105.19295211171,5.38991938217132,128.358642779165));
#182248=CARTESIAN_POINT('Ctrl Pts',(105.200348468645,5.45119467001556,128.503837365761));
#182249=CARTESIAN_POINT('Ctrl Pts',(105.207745957982,5.51247933926285,128.649054182019));
#182250=CARTESIAN_POINT('Ctrl Pts',(105.215143447318,5.56794648098274,128.796696010208));
#182251=CARTESIAN_POINT('Ctrl Pts',(105.222540936655,5.61741643250335,128.946253197006));
#182252=CARTESIAN_POINT('Ctrl Pts',(105.22994101917,5.66690372563873,129.095862810843));
#182253=CARTESIAN_POINT('Ctrl Pts',(105.237341101685,5.71038952574151,129.247388765903));
#182254=CARTESIAN_POINT('Ctrl Pts',(105.2447411842,5.74774422171534,129.400306870647));
#182255=CARTESIAN_POINT('Ctrl Pts',(105.252149403867,5.78513999301754,129.553393124567));
#182256=CARTESIAN_POINT('Ctrl Pts',(105.259557623533,5.81639110777643,129.707874222446));
#182257=CARTESIAN_POINT('Ctrl Pts',(105.2669658432,5.84141907322822,129.863215690668));
#182258=CARTESIAN_POINT('Ctrl Pts',(105.274378622502,5.86646244297514,130.018652768972));
#182259=CARTESIAN_POINT('Ctrl Pts',(105.281791401804,5.88527498666656,130.174950903038));
#182260=CARTESIAN_POINT('Ctrl Pts',(105.289204181106,5.89783020810086,130.331571659454));
#182261=CARTESIAN_POINT('Ctrl Pts',(105.296627552135,5.91040336902432,130.488416202951));
#182262=CARTESIAN_POINT('Ctrl Pts',(105.304050923163,5.91670133608945,130.645583917464));
#182263=CARTESIAN_POINT('Ctrl Pts',(105.311474294192,5.91674971887665,130.802536700609));
#182264=CARTESIAN_POINT('Ctrl Pts',(105.315410343633,5.91677537259135,130.885756832263));
#182265=CARTESIAN_POINT('Ctrl Pts',(105.319346393074,5.91504491162565,130.96891661744));
#182266=CARTESIAN_POINT('Ctrl Pts',(105.323282442514,5.91156803654956,131.051936690209));
#182267=CARTESIAN_POINT('Ctrl Pts',(105.33070570892,5.90501075866559,131.208509956486));
#182268=CARTESIAN_POINT('Ctrl Pts',(105.338128975325,5.89221879044042,131.365059286446));
#182269=CARTESIAN_POINT('Ctrl Pts',(105.345552241731,5.87318399051068,131.521047701382));
#182270=CARTESIAN_POINT('Ctrl Pts',(105.352966734452,5.85417168813369,131.676851750967));
#182271=CARTESIAN_POINT('Ctrl Pts',(105.360381227173,5.82893128578972,131.832095838212));
#182272=CARTESIAN_POINT('Ctrl Pts',(105.367795719894,5.79750662537259,131.986243645306));
#182273=CARTESIAN_POINT('Ctrl Pts',(105.375203066248,5.76611225322631,132.140242878941));
#182274=CARTESIAN_POINT('Ctrl Pts',(105.382610412601,5.72854556349577,132.293147572659));
#182275=CARTESIAN_POINT('Ctrl Pts',(105.390017758955,5.68490209584444,132.444427300102));
#182276=CARTESIAN_POINT('Ctrl Pts',(105.397419580631,5.64129117913782,132.595594197416));
#182277=CARTESIAN_POINT('Ctrl Pts',(105.404821402306,5.59161261194114,132.745138184505));
#182278=CARTESIAN_POINT('Ctrl Pts',(105.412223223981,5.53601281097703,132.892539900865));
#182279=CARTESIAN_POINT('Ctrl Pts',(105.419621138293,5.4804423607151,133.039863805006));
#182280=CARTESIAN_POINT('Ctrl Pts',(105.427019052604,5.41895703322618,133.185047342242));
#182281=CARTESIAN_POINT('Ctrl Pts',(105.434416966915,5.35175277515702,133.327587281205));
#182282=CARTESIAN_POINT('Ctrl Pts',(105.441813651828,5.28455968521634,133.470103532616));
#182283=CARTESIAN_POINT('Ctrl Pts',(105.44921033674,5.21164970996226,133.609976720348));
#182284=CARTESIAN_POINT('Ctrl Pts',(105.456607021652,5.13326657530261,133.74672443419));
#182285=CARTESIAN_POINT('Ctrl Pts',(105.464003378588,5.05488691623329,133.883466084496));
#182286=CARTESIAN_POINT('Ctrl Pts',(105.471399735523,4.97103476593801,134.017082212602));
#182287=CARTESIAN_POINT('Ctrl Pts',(105.478796092458,4.88199923792222,134.147116068302));
#182288=CARTESIAN_POINT('Ctrl Pts',(105.486193581795,4.7929500783398,134.277169832517));
#182289=CARTESIAN_POINT('Ctrl Pts',(105.493591071132,4.69871617181061,134.403639924246));
#182290=CARTESIAN_POINT('Ctrl Pts',(105.500988560468,4.59962919204559,134.526099708123));
#182291=CARTESIAN_POINT('Ctrl Pts',(105.508388642983,4.50050747749342,134.648602420088));
#182292=CARTESIAN_POINT('Ctrl Pts',(105.515788725498,4.39652953721887,134.767091735234));
#182293=CARTESIAN_POINT('Ctrl Pts',(105.523188808013,4.28806633044486,134.881175269743));
#182294=CARTESIAN_POINT('Ctrl Pts',(105.53059702768,4.17948385722472,134.995384250827));
#182295=CARTESIAN_POINT('Ctrl Pts',(105.538005247346,4.06640652532517,135.105177505565));
#182296=CARTESIAN_POINT('Ctrl Pts',(105.545413467012,3.94924157527939,135.210200099729));
#182297=CARTESIAN_POINT('Ctrl Pts',(105.552826246315,3.83200451216169,135.315287333547));
#182298=CARTESIAN_POINT('Ctrl Pts',(105.560239025617,3.71067510476582,135.415597818611));
#182299=CARTESIAN_POINT('Ctrl Pts',(105.567651804919,3.58569203052612,135.510818226503));
#182300=CARTESIAN_POINT('Ctrl Pts',(105.575075175947,3.46053037460892,135.60617468978));
#182301=CARTESIAN_POINT('Ctrl Pts',(105.582498546976,3.33170493020274,135.696426336569));
#182302=CARTESIAN_POINT('Ctrl Pts',(105.589921918005,3.19968226068691,135.781303855453));
#182303=CARTESIAN_POINT('Ctrl Pts',(105.593857967446,3.12968067347,135.826307952573));
#182304=CARTESIAN_POINT('Ctrl Pts',(105.597794016886,3.05878063457298,135.869801961931));
#182305=CARTESIAN_POINT('Ctrl Pts',(105.601730066327,2.98705416019581,135.911751145669));
#182306=CARTESIAN_POINT('Ctrl Pts',(105.609153332733,2.85178026802552,135.99086599701));
#182307=CARTESIAN_POINT('Ctrl Pts',(105.616576599138,2.71315651173587,136.064722488628));
#182308=CARTESIAN_POINT('Ctrl Pts',(105.623999865543,2.57163026611553,136.133023520856));
#182309=CARTESIAN_POINT('Ctrl Pts',(105.631414358264,2.43027129276448,136.201243826935));
#182310=CARTESIAN_POINT('Ctrl Pts',(105.638828850985,2.28601699142607,136.263921582802));
#182311=CARTESIAN_POINT('Ctrl Pts',(105.646243343706,2.1393422790795,136.320803781004));
#182312=CARTESIAN_POINT('Ctrl Pts',(105.65365069006,1.9928089373428,136.377631154002));
#182313=CARTESIAN_POINT('Ctrl Pts',(105.661058036414,1.84386017461458,136.428673955848));
#182314=CARTESIAN_POINT('Ctrl Pts',(105.668465382768,1.69299389513649,136.473725858361));
#182315=CARTESIAN_POINT('Ctrl Pts',(105.675867204443,1.54224013742148,136.518744159465));
#182316=CARTESIAN_POINT('Ctrl Pts',(105.683269026118,1.38957206674136,136.557780351749));
#182317=CARTESIAN_POINT('Ctrl Pts',(105.690670847794,1.23550577761279,136.590676892709));
#182318=CARTESIAN_POINT('Ctrl Pts',(105.698068762105,1.08152081887889,136.623556067841));
#182319=CARTESIAN_POINT('Ctrl Pts',(105.705466676416,0.926139475819769,
136.650301968651));
#182320=CARTESIAN_POINT('Ctrl Pts',(105.712864590728,0.769891045187945,
136.670807441755));
#182321=CARTESIAN_POINT('Ctrl Pts',(105.72026127564,0.61366858021088,136.691309507221));
#182322=CARTESIAN_POINT('Ctrl Pts',(105.727657960552,0.456579683407301,
136.705573154684));
#182323=CARTESIAN_POINT('Ctrl Pts',(105.735054645464,0.299161959957347,
136.71354268315));
#182324=CARTESIAN_POINT('Ctrl Pts',(105.7424510024,0.141751216574213,136.721511858238));
#182325=CARTESIAN_POINT('Ctrl Pts',(105.749847359335,-0.0159879516442059,
136.723187450375));
#182326=CARTESIAN_POINT('Ctrl Pts',(105.757243716271,-0.17351499490074,
136.718565814297));
#182327=CARTESIAN_POINT('Ctrl Pts',(105.764641205607,-0.331066155949856,
136.713943470636));
#182328=CARTESIAN_POINT('Ctrl Pts',(105.772038694944,-0.488404754209991,
136.703021990012));
#182329=CARTESIAN_POINT('Ctrl Pts',(105.77943618428,-0.644992571524573,
136.685849812079));
#182330=CARTESIAN_POINT('Ctrl Pts',(105.786836266795,-0.801635280455549,
136.668671614466));
#182331=CARTESIAN_POINT('Ctrl Pts',(105.79423634931,-0.957526313599619,
136.645238397603));
#182332=CARTESIAN_POINT('Ctrl Pts',(105.801636431825,-1.11213503481809,
136.615650166954));
#182333=CARTESIAN_POINT('Ctrl Pts',(105.809044651492,-1.26691376421993,
136.586029401004));
#182334=CARTESIAN_POINT('Ctrl Pts',(105.816452871158,-1.42040699889691,
136.550240175196));
#182335=CARTESIAN_POINT('Ctrl Pts',(105.823861090825,-1.57209599917411,
136.508433261904));
#182336=CARTESIAN_POINT('Ctrl Pts',(105.831273870127,-1.7238783614999,136.466600617154));
#182337=CARTESIAN_POINT('Ctrl Pts',(105.838686649429,-1.87385392185703,
136.418743017881));
#182338=CARTESIAN_POINT('Ctrl Pts',(105.846099428731,-2.02152195230672,
136.365060174172));
#182339=CARTESIAN_POINT('Ctrl Pts',(105.853522799759,-2.16940097776336,
136.311300625899));
#182340=CARTESIAN_POINT('Ctrl Pts',(105.860946170788,-2.31496554370426,
136.251699350603));
#182341=CARTESIAN_POINT('Ctrl Pts',(105.868369541817,-2.45773688190387,
136.186503311868));
#182342=CARTESIAN_POINT('Ctrl Pts',(105.872305591258,-2.53343767116798,
136.151934807774));
#182343=CARTESIAN_POINT('Ctrl Pts',(105.876241640698,-2.6083536159097,136.115794171515));
#182344=CARTESIAN_POINT('Ctrl Pts',(105.880177690139,-2.68241656366872,
136.078123215698));
#182345=CARTESIAN_POINT('Ctrl Pts',(105.887600956545,-2.82209697171773,
136.007076968697));
#182346=CARTESIAN_POINT('Ctrl Pts',(105.89502422295,-2.95916405618854,135.930370114267));
#182347=CARTESIAN_POINT('Ctrl Pts',(105.902447489356,-3.09312604171576,
135.848218451859));
#182348=CARTESIAN_POINT('Ctrl Pts',(105.909861982077,-3.22692969530103,
135.766163885894));
#182349=CARTESIAN_POINT('Ctrl Pts',(105.917276474798,-3.35763523991832,
135.678677514719));
#182350=CARTESIAN_POINT('Ctrl Pts',(105.924690967519,-3.48477310900594,
135.586022142732));
#182351=CARTESIAN_POINT('Ctrl Pts',(105.932098313872,-3.6117884378286,135.49345607548));
#182352=CARTESIAN_POINT('Ctrl Pts',(105.939505660226,-3.7352426371587,135.395731144136));
#182353=CARTESIAN_POINT('Ctrl Pts',(105.94691300658,-3.85469298785055,135.293154724218));
#182354=CARTESIAN_POINT('Ctrl Pts',(105.954314828255,-3.97405424796441,
135.190654809664));
#182355=CARTESIAN_POINT('Ctrl Pts',(105.961716649931,-4.08941732342291,
135.083310853458));
#182356=CARTESIAN_POINT('Ctrl Pts',(105.969118471606,-4.20037070756353,
134.971471904962));
#182357=CARTESIAN_POINT('Ctrl Pts',(105.976516385917,-4.311265520276,134.859691995376));
#182358=CARTESIAN_POINT('Ctrl Pts',(105.983914300229,-4.41775501543425,
134.743422083526));
#182359=CARTESIAN_POINT('Ctrl Pts',(105.99131221454,-4.51946294403796,134.623049562737));
#182360=CARTESIAN_POINT('Ctrl Pts',(105.998708899452,-4.62115397062931,
134.502697045676));
#182361=CARTESIAN_POINT('Ctrl Pts',(106.006105584365,-4.7180647670393,134.378243557669));
#182362=CARTESIAN_POINT('Ctrl Pts',(106.013502269277,-4.80985788171252,
134.250111293432));
#182363=CARTESIAN_POINT('Ctrl Pts',(106.020898626212,-4.90164692618279,
134.121984710713));
#182364=CARTESIAN_POINT('Ctrl Pts',(106.028294983148,-4.98831852271849,
133.990179979564));
#182365=CARTESIAN_POINT('Ctrl Pts',(106.035691340083,-5.06957742408703,
133.855149909485));
#182366=CARTESIAN_POINT('Ctrl Pts',(106.04308882942,-5.15084876640076,133.720099165958));
#182367=CARTESIAN_POINT('Ctrl Pts',(106.050486318756,-5.22670557100859,
133.581822420132));
#182368=CARTESIAN_POINT('Ctrl Pts',(106.057883808093,-5.29689767150079,
133.440798673002));
#182369=CARTESIAN_POINT('Ctrl Pts',(106.065283890608,-5.3671143777252,133.299725490215));
#182370=CARTESIAN_POINT('Ctrl Pts',(106.072683973123,-5.43166225998016,
133.155903722865));
#182371=CARTESIAN_POINT('Ctrl Pts',(106.080084055638,-5.49033863389968,
133.009833865558));
#182372=CARTESIAN_POINT('Ctrl Pts',(106.087492275304,-5.54907952852431,
132.863603389427));
#182373=CARTESIAN_POINT('Ctrl Pts',(106.094900494971,-5.60193588187207,
132.71512023319));
#182374=CARTESIAN_POINT('Ctrl Pts',(106.102308714637,-5.64875415154569,
132.564902323376));
#182375=CARTESIAN_POINT('Ctrl Pts',(106.10972149394,-5.69560123708312,132.414591956945));
#182376=CARTESIAN_POINT('Ctrl Pts',(106.117134273242,-5.73640273714705,
132.262545069094));
#182377=CARTESIAN_POINT('Ctrl Pts',(106.124547052544,-5.77105601780815,
132.1092908846));
#182378=CARTESIAN_POINT('Ctrl Pts',(106.131970423572,-5.80575881270173,
131.95581772334));
#182379=CARTESIAN_POINT('Ctrl Pts',(106.139393794601,-5.83429577530219,
131.801134186271));
#182380=CARTESIAN_POINT('Ctrl Pts',(106.14681716563,-5.85661589714791,131.645776564512));
#182381=CARTESIAN_POINT('Ctrl Pts',(106.150753215071,-5.86845056131456,
131.563402225699));
#182382=CARTESIAN_POINT('Ctrl Pts',(106.154689264512,-5.87853831853057,
131.480838422975));
#182383=CARTESIAN_POINT('Ctrl Pts',(106.158625313952,-5.88687750885685,
131.398165095669));
#182384=CARTESIAN_POINT('Ctrl Pts',(106.167958478567,-5.90665140581494,
131.202130014161));
#182385=CARTESIAN_POINT('Ctrl Pts',(106.177291643181,-5.91663550124626,
131.005090988402));
#182386=CARTESIAN_POINT('Ctrl Pts',(106.186624807795,-5.91674902090619,
130.807764454462));
#182387=CARTESIAN_POINT('',(107.936623643011,-5.91240499895973,130.80786427171));
#182388=CARTESIAN_POINT('Ctrl Pts',(106.186627341394,-5.92408642895685,
130.80771504248));
#182389=CARTESIAN_POINT('Ctrl Pts',(106.270109206851,-5.91195890497154,
129.040502122754));
#182390=CARTESIAN_POINT('Ctrl Pts',(106.446406946912,-4.13303796844123,
125.287351149234));
#182391=CARTESIAN_POINT('Ctrl Pts',(106.715520561579,2.25550656452963,124.17938886912));
#182392=CARTESIAN_POINT('Ctrl Pts',(106.993968185391,6.79293275285633,129.121023115604));
#182393=CARTESIAN_POINT('Ctrl Pts',(107.272415809204,5.0879855945222,135.609562290782));
#182394=CARTESIAN_POINT('Ctrl Pts',(107.550863433017,-1.29257176326585,
137.682355875427));
#182395=CARTESIAN_POINT('Ctrl Pts',(107.772265740639,-5.42148536177523,
134.304840178653));
#182396=CARTESIAN_POINT('Ctrl Pts',(107.900852173658,-5.9130646159241,131.570055323628));
#182397=CARTESIAN_POINT('Ctrl Pts',(107.936622732073,-5.90900772285622,
130.807881682323));
#182398=CARTESIAN_POINT('',(109.686626001159,-5.91357378928978,130.799653518455));
#182399=CARTESIAN_POINT('Ctrl Pts',(107.936624807795,-5.91674897578147,
130.807842009375));
#182400=CARTESIAN_POINT('Ctrl Pts',(107.94409446103,-5.91684274612946,130.648475973948));
#182401=CARTESIAN_POINT('Ctrl Pts',(107.951564114265,-5.91049345477139,
130.489096138341));
#182402=CARTESIAN_POINT('Ctrl Pts',(107.9590337675,-5.89772439811517,130.330253576512));
#182403=CARTESIAN_POINT('Ctrl Pts',(107.966504510164,-5.88495347912462,
130.1713878479));
#182404=CARTESIAN_POINT('Ctrl Pts',(107.973975252829,-5.86576095780414,
130.013059911091));
#182405=CARTESIAN_POINT('Ctrl Pts',(107.981445995494,-5.84022206841509,
129.855816072435));
#182406=CARTESIAN_POINT('Ctrl Pts',(107.98891919135,-5.81467479273977,129.69852059912));
#182407=CARTESIAN_POINT('Ctrl Pts',(107.996392387206,-5.7827770550703,129.542310291412));
#182408=CARTESIAN_POINT('Ctrl Pts',(108.003865583063,-5.74465529499681,
129.38772160068));
#182409=CARTESIAN_POINT('Ctrl Pts',(108.011342597095,-5.70651405790379,
129.233053928102));
#182410=CARTESIAN_POINT('Ctrl Pts',(108.018819611127,-5.6621425497145,129.080009875145));
#182411=CARTESIAN_POINT('Ctrl Pts',(108.026296625159,-5.61171717273773,
128.929111051321));
#182412=CARTESIAN_POINT('Ctrl Pts',(108.033783535364,-5.5612250554452,128.778012505934));
#182413=CARTESIAN_POINT('Ctrl Pts',(108.04127044557,-5.50466317855855,128.629065205899));
#182414=CARTESIAN_POINT('Ctrl Pts',(108.048757355775,-5.44225660651554,
128.482772025387));
#182415=CARTESIAN_POINT('Ctrl Pts',(108.056249706816,-5.37980468279946,
128.336372531704));
#182416=CARTESIAN_POINT('Ctrl Pts',(108.063742057857,-5.31149975231297,
128.192631329411));
#182417=CARTESIAN_POINT('Ctrl Pts',(108.071234408898,-5.23761287276468,
128.052026706582));
#182418=CARTESIAN_POINT('Ctrl Pts',(108.078738864129,-5.16360662604355,
127.911194931432));
#182419=CARTESIAN_POINT('Ctrl Pts',(108.086243319359,-5.08400059452109,
127.773510173305));
#182420=CARTESIAN_POINT('Ctrl Pts',(108.093747774589,-4.99910978103279,
127.639422709852));
#182421=CARTESIAN_POINT('Ctrl Pts',(108.098418076607,-4.94627906576286,
127.55597508682));
#182422=CARTESIAN_POINT('Ctrl Pts',(108.103088378625,-4.89140236815802,
127.473920090637));
#182423=CARTESIAN_POINT('Ctrl Pts',(108.107758680642,-4.83456333426392,
127.39335960181));
#182424=CARTESIAN_POINT('Ctrl Pts',(108.115181947048,-4.74421986413769,
127.265311786478));
#182425=CARTESIAN_POINT('Ctrl Pts',(108.122605213453,-4.64864907589165,
127.14066207089));
#182426=CARTESIAN_POINT('Ctrl Pts',(108.130028479859,-4.54813506396797,
127.019866199231));
#182427=CARTESIAN_POINT('Ctrl Pts',(108.13744297258,-4.44773985125906,126.899213098261));
#182428=CARTESIAN_POINT('Ctrl Pts',(108.144857465301,-4.34241328079953,
126.782405058767));
#182429=CARTESIAN_POINT('Ctrl Pts',(108.152271958022,-4.23248278113099,
126.669869104704));
#182430=CARTESIAN_POINT('Ctrl Pts',(108.159679304375,-4.122658236617,126.55744161703));
#182431=CARTESIAN_POINT('Ctrl Pts',(108.167086650729,-4.00823885606507,
126.449278282703));
#182432=CARTESIAN_POINT('Ctrl Pts',(108.174493997083,-3.88959232822549,
126.345773163819));
#182433=CARTESIAN_POINT('Ctrl Pts',(108.181895818758,-3.77103429144233,
126.242345242957));
#182434=CARTESIAN_POINT('Ctrl Pts',(108.189297640434,-3.64825566504315,
126.143568864137));
#182435=CARTESIAN_POINT('Ctrl Pts',(108.196699462109,-3.52166090466189,
126.049801223145));
#182436=CARTESIAN_POINT('Ctrl Pts',(108.204097376421,-3.39513297266975,
125.956083081362));
#182437=CARTESIAN_POINT('Ctrl Pts',(108.211495290732,-3.26479321789758,
125.867368633233));
#182438=CARTESIAN_POINT('Ctrl Pts',(108.218893205043,-3.13107898728395,
125.783974682412));
#182439=CARTESIAN_POINT('Ctrl Pts',(108.226289889956,-2.99738697754934,
125.700594590154));
#182440=CARTESIAN_POINT('Ctrl Pts',(108.233686574868,-2.86032192138361,
125.622533437739));
#182441=CARTESIAN_POINT('Ctrl Pts',(108.24108325978,-2.72035004343166,125.550064641538));
#182442=CARTESIAN_POINT('Ctrl Pts',(108.248479616715,-2.58038437197945,
125.47759905868));
#182443=CARTESIAN_POINT('Ctrl Pts',(108.255875973651,-2.43751246652316,
125.410725510616));
#182444=CARTESIAN_POINT('Ctrl Pts',(108.263272330586,-2.29222479750266,
125.349671255172));
#182445=CARTESIAN_POINT('Ctrl Pts',(108.270669819923,-2.14691488456913,
125.288607652166));
#182446=CARTESIAN_POINT('Ctrl Pts',(108.27806730926,-1.99918881579962,125.233365260405));
#182447=CARTESIAN_POINT('Ctrl Pts',(108.285464798596,-1.84955651734156,
125.184122966749));
#182448=CARTESIAN_POINT('Ctrl Pts',(108.292864881111,-1.69987176551313,
125.134863411283));
#182449=CARTESIAN_POINT('Ctrl Pts',(108.300264963626,-1.5482798079326,125.091608258246));
#182450=CARTESIAN_POINT('Ctrl Pts',(108.307665046141,-1.39530503277655,
125.054486320852));
#182451=CARTESIAN_POINT('Ctrl Pts',(108.315073265808,-1.24216204612914,
125.017323564072));
#182452=CARTESIAN_POINT('Ctrl Pts',(108.322481485474,-1.08763356825991,
124.986307579436));
#182453=CARTESIAN_POINT('Ctrl Pts',(108.329889705141,-0.932254191617432,
124.961516046237));
#182454=CARTESIAN_POINT('Ctrl Pts',(108.337302484443,-0.776779181561499,
124.936709254263));
#182455=CARTESIAN_POINT('Ctrl Pts',(108.344715263745,-0.620452598997422,
124.91813459151));
#182456=CARTESIAN_POINT('Ctrl Pts',(108.352128043047,-0.463812917036198,
124.905817734744));
#182457=CARTESIAN_POINT('Ctrl Pts',(108.359551414076,-0.306949420951381,
124.893483279076));
#182458=CARTESIAN_POINT('Ctrl Pts',(108.366974785105,-0.149772304001651,
124.88742450181));
#182459=CARTESIAN_POINT('Ctrl Pts',(108.374398156133,0.00718037102544568,
124.887614974497));
#182460=CARTESIAN_POINT('Ctrl Pts',(108.378334205574,0.0904004453502009,
124.887715967686));
#182461=CARTESIAN_POINT('Ctrl Pts',(108.382270255015,0.173557500760324,
124.889572981685));
#182462=CARTESIAN_POINT('Ctrl Pts',(108.386206304455,0.256572186180075,
124.893176195153));
#182463=CARTESIAN_POINT('Ctrl Pts',(108.393629570861,0.41313529208642,124.899971743302));
#182464=CARTESIAN_POINT('Ctrl Pts',(108.401052837266,0.56966497356679,124.913001938145));
#182465=CARTESIAN_POINT('Ctrl Pts',(108.408476103672,0.725624240145992,
124.932274103846));
#182466=CARTESIAN_POINT('Ctrl Pts',(108.415890596393,0.881399175823931,
124.951523491448));
#182467=CARTESIAN_POINT('Ctrl Pts',(108.423305089114,1.03660467170355,124.977000119638));
#182468=CARTESIAN_POINT('Ctrl Pts',(108.430719581835,1.19070447731366,125.008659330387));
#182469=CARTESIAN_POINT('Ctrl Pts',(108.438126928189,1.34465575572914,125.040288026798));
#182470=CARTESIAN_POINT('Ctrl Pts',(108.445534274542,1.49750310227977,125.078087367941));
#182471=CARTESIAN_POINT('Ctrl Pts',(108.452941620896,1.64871623661404,125.121961007047));
#182472=CARTESIAN_POINT('Ctrl Pts',(108.460343442572,1.79981659048746,125.165801923537));
#182473=CARTESIAN_POINT('Ctrl Pts',(108.467745264247,1.94928480208421,125.215708013698));
#182474=CARTESIAN_POINT('Ctrl Pts',(108.475147085922,2.09660173432233,125.271532070599));
#182475=CARTESIAN_POINT('Ctrl Pts',(108.482545000234,2.24384089909842,125.327326658414));
#182476=CARTESIAN_POINT('Ctrl Pts',(108.489942914545,2.38893069801256,125.389032859332));
#182477=CARTESIAN_POINT('Ctrl Pts',(108.497340828856,2.53136819847509,125.456453961102));
#182478=CARTESIAN_POINT('Ctrl Pts',(108.504737513769,2.67378202840953,125.523863858708));
#182479=CARTESIAN_POINT('Ctrl Pts',(108.512134198681,2.81354409759998,125.596986612715));
#182480=CARTESIAN_POINT('Ctrl Pts',(108.519530883593,2.95017236730276,125.67557776335));
#182481=CARTESIAN_POINT('Ctrl Pts',(108.526927240528,3.08679457876498,125.754165429171));
#182482=CARTESIAN_POINT('Ctrl Pts',(108.534323597464,3.22028294344749,125.838220823368));
#182483=CARTESIAN_POINT('Ctrl Pts',(108.541719954399,3.35018115165315,125.927454137674));
#182484=CARTESIAN_POINT('Ctrl Pts',(108.549117443736,3.480099247606,126.016701113829));
#182485=CARTESIAN_POINT('Ctrl Pts',(108.556514933072,3.60642578491945,126.111127377187));
#182486=CARTESIAN_POINT('Ctrl Pts',(108.563912422409,3.72873463347499,126.210400605156));
#182487=CARTESIAN_POINT('Ctrl Pts',(108.571312504924,3.85108635720804,126.309708633201));
#182488=CARTESIAN_POINT('Ctrl Pts',(108.578712587439,3.96941729841992,126.413866773637));
#182489=CARTESIAN_POINT('Ctrl Pts',(108.586112669954,4.0833356382855,126.522503470532));
#182490=CARTESIAN_POINT('Ctrl Pts',(108.59352088962,4.19737924307678,126.631259624643));
#182491=CARTESIAN_POINT('Ctrl Pts',(108.600929109287,4.30700028622644,126.744503912244));
#182492=CARTESIAN_POINT('Ctrl Pts',(108.608337328953,4.41184445366697,126.861828553125));
#182493=CARTESIAN_POINT('Ctrl Pts',(108.615750108256,4.51675315094359,126.979225405365));
#182494=CARTESIAN_POINT('Ctrl Pts',(108.623162887558,4.61687887714527,127.100707327746));
#182495=CARTESIAN_POINT('Ctrl Pts',(108.63057566686,4.71190897181134,127.225835166509));
#182496=CARTESIAN_POINT('Ctrl Pts',(108.637999037888,4.80707484993294,127.351141793796));
#182497=CARTESIAN_POINT('Ctrl Pts',(108.645422408917,4.8971303418157,127.480104436667));
#182498=CARTESIAN_POINT('Ctrl Pts',(108.652845779946,4.98180684638433,127.612256122438));
#182499=CARTESIAN_POINT('Ctrl Pts',(108.656781829387,5.02670436089111,127.682326117169));
#182500=CARTESIAN_POINT('Ctrl Pts',(108.660717878828,5.07009042209485,127.753292264444));
#182501=CARTESIAN_POINT('Ctrl Pts',(108.664653928268,5.11193040177253,127.82508249528));
#182502=CARTESIAN_POINT('Ctrl Pts',(108.672077194674,5.19083929766396,127.960476630141));
#182503=CARTESIAN_POINT('Ctrl Pts',(108.679500461079,5.26448474199825,128.099212622914));
#182504=CARTESIAN_POINT('Ctrl Pts',(108.686923727485,5.33257031628044,128.240842647193));
#182505=CARTESIAN_POINT('Ctrl Pts',(108.694338220206,5.40057541906814,128.382305276546));
#182506=CARTESIAN_POINT('Ctrl Pts',(108.701752712927,5.46303357186457,128.526654795715));
#182507=CARTESIAN_POINT('Ctrl Pts',(108.709167205648,5.51969249025468,128.673415903237));
#182508=CARTESIAN_POINT('Ctrl Pts',(108.716574552001,5.57629679864595,128.820035556878));
#182509=CARTESIAN_POINT('Ctrl Pts',(108.723981898355,5.62711286672333,128.969061825581));
#182510=CARTESIAN_POINT('Ctrl Pts',(108.731389244709,5.67193512427151,129.119996491685));
#182511=CARTESIAN_POINT('Ctrl Pts',(108.738791066384,5.71672395168899,129.27081858502));
#182512=CARTESIAN_POINT('Ctrl Pts',(108.74619288806,5.75552776395484,129.423545885352));
#182513=CARTESIAN_POINT('Ctrl Pts',(108.753594709735,5.78818980415609,129.57766205901));
#182514=CARTESIAN_POINT('Ctrl Pts',(108.760992624046,5.82083460232035,129.731696875938));
#182515=CARTESIAN_POINT('Ctrl Pts',(108.768390538358,5.8473440082055,129.887118741775));
#182516=CARTESIAN_POINT('Ctrl Pts',(108.775788452669,5.86761167405109,130.043398197312));
#182517=CARTESIAN_POINT('Ctrl Pts',(108.783185137581,5.88787597177845,130.199651682039));
#182518=CARTESIAN_POINT('Ctrl Pts',(108.790581822493,5.90190054016471,130.35676210378));
#182519=CARTESIAN_POINT('Ctrl Pts',(108.797978507406,5.90963049642396,130.514191773208));
#182520=CARTESIAN_POINT('Ctrl Pts',(108.805374864341,5.91736010992885,130.67161446204));
#182521=CARTESIAN_POINT('Ctrl Pts',(108.812771221277,5.91879564796385,130.829355997565));
#182522=CARTESIAN_POINT('Ctrl Pts',(108.820167578212,5.91393428789429,130.986875825065));
#182523=CARTESIAN_POINT('Ctrl Pts',(108.827565067549,5.90907218353808,131.144419769252));
#182524=CARTESIAN_POINT('Ctrl Pts',(108.834962556885,5.89791127299929,131.301741564682));
#182525=CARTESIAN_POINT('Ctrl Pts',(108.842360046222,5.88050081494962,131.458303067539));
#182526=CARTESIAN_POINT('Ctrl Pts',(108.849760128737,5.86308425369089,131.614919452788));
#182527=CARTESIAN_POINT('Ctrl Pts',(108.857160211252,5.83941382434853,131.770774644046));
#182528=CARTESIAN_POINT('Ctrl Pts',(108.864560293767,5.80959033980777,131.92533815798));
#182529=CARTESIAN_POINT('Ctrl Pts',(108.871968513433,5.77973406127979,132.080071630387));
#182530=CARTESIAN_POINT('Ctrl Pts',(108.8793767331,5.74371128634123,132.233510222212));
#182531=CARTESIAN_POINT('Ctrl Pts',(108.886784952766,5.7016735766245,132.385135423831));
#182532=CARTESIAN_POINT('Ctrl Pts',(108.894197732068,5.65960999339889,132.536853948231));
#182533=CARTESIAN_POINT('Ctrl Pts',(108.90161051137,5.61152421227203,132.6867565038));
#182534=CARTESIAN_POINT('Ctrl Pts',(108.909023290672,5.55761670512263,132.834342667103));
#182535=CARTESIAN_POINT('Ctrl Pts',(108.916446661701,5.50363217239908,132.982139708437));
#182536=CARTESIAN_POINT('Ctrl Pts',(108.92387003273,5.44380944163022,133.127613402821));
#182537=CARTESIAN_POINT('Ctrl Pts',(108.931293403759,5.3783962047193,133.270285358421));
#182538=CARTESIAN_POINT('Ctrl Pts',(108.9352294532,5.34371253693922,133.345933452649));
#182539=CARTESIAN_POINT('Ctrl Pts',(108.939165502641,5.30745793321449,133.420794310745));
#182540=CARTESIAN_POINT('Ctrl Pts',(108.943101552081,5.2696743098201,133.49479984396));
#182541=CARTESIAN_POINT('Ctrl Pts',(108.950524818487,5.19841557528643,133.634371969968));
#182542=CARTESIAN_POINT('Ctrl Pts',(108.957948084892,5.12150021691154,133.771322160943));
#182543=CARTESIAN_POINT('Ctrl Pts',(108.965371351298,5.03914478229674,133.905158970499));
#182544=CARTESIAN_POINT('Ctrl Pts',(108.972785844019,4.95688668496634,134.038837596061));
#182545=CARTESIAN_POINT('Ctrl Pts',(108.98020033674,4.86920150351011,134.169409849959));
#182546=CARTESIAN_POINT('Ctrl Pts',(108.987614829461,4.77635275662183,134.29640656612));
#182547=CARTESIAN_POINT('Ctrl Pts',(108.995022175815,4.68359350085161,134.423280878064));
#182548=CARTESIAN_POINT('Ctrl Pts',(109.002429522168,4.58568080639566,134.546586213726));
#182549=CARTESIAN_POINT('Ctrl Pts',(109.009836868522,4.48292272216005,134.665880322247));
#182550=CARTESIAN_POINT('Ctrl Pts',(109.017238690197,4.3802412787808,134.785085456721));
#182551=CARTESIAN_POINT('Ctrl Pts',(109.024640511873,4.27272188391508,134.900285039362));
#182552=CARTESIAN_POINT('Ctrl Pts',(109.032042333548,4.16071421276395,135.011068095179));
#182553=CARTESIAN_POINT('Ctrl Pts',(109.03944024786,4.04876566958952,135.121792669484));
#182554=CARTESIAN_POINT('Ctrl Pts',(109.046838162171,3.93233383349262,135.228105098317));
#182555=CARTESIAN_POINT('Ctrl Pts',(109.054236076482,3.81180666993848,135.329629722659));
#182556=CARTESIAN_POINT('Ctrl Pts',(109.061632761395,3.69129953581284,135.431137475451));
#182557=CARTESIAN_POINT('Ctrl Pts',(109.069029446307,3.56669871018576,135.527858762617));
#182558=CARTESIAN_POINT('Ctrl Pts',(109.076426131219,3.43842690082814,135.619456775501));
#182559=CARTESIAN_POINT('Ctrl Pts',(109.083822488154,3.31016077917751,135.711050726833));
#182560=CARTESIAN_POINT('Ctrl Pts',(109.09121884509,3.17822430124098,135.797521638641));
#182561=CARTESIAN_POINT('Ctrl Pts',(109.098615202025,3.04307072530972,135.878574953132));
#182562=CARTESIAN_POINT('Ctrl Pts',(109.106012691362,2.90789645702027,135.959640677093));
#182563=CARTESIAN_POINT('Ctrl Pts',(109.113410180699,2.76950443017307,136.035286960192));
#182564=CARTESIAN_POINT('Ctrl Pts',(109.120807670035,2.62837402591716,136.105264365266));
#182565=CARTESIAN_POINT('Ctrl Pts',(109.12820775255,2.48719414861702,136.175266300812));
#182566=CARTESIAN_POINT('Ctrl Pts',(109.135607835065,2.34327431692121,136.239595236074));
#182567=CARTESIAN_POINT('Ctrl Pts',(109.14300791758,2.19711533330873,136.29804924859));
#182568=CARTESIAN_POINT('Ctrl Pts',(109.150416137247,2.05079563286817,136.356567537302));
#182569=CARTESIAN_POINT('Ctrl Pts',(109.157824356913,1.9022322101993,136.409197863355));
#182570=CARTESIAN_POINT('Ctrl Pts',(109.16523257658,1.75194322489847,136.455787472727));
#182571=CARTESIAN_POINT('Ctrl Pts',(109.172645355882,1.60156173923575,136.502405757225));
#182572=CARTESIAN_POINT('Ctrl Pts',(109.180058135184,1.44945293451599,136.542975820561));
#182573=CARTESIAN_POINT('Ctrl Pts',(109.187470914486,1.29614619109431,136.577395834314));
#182574=CARTESIAN_POINT('Ctrl Pts',(109.194894285514,1.14262039580749,136.611865028997));
#182575=CARTESIAN_POINT('Ctrl Pts',(109.202317656543,0.987893609460659,
136.64016655654));
#182576=CARTESIAN_POINT('Ctrl Pts',(109.209741027572,0.832502200176965,
136.662250224686));
#182577=CARTESIAN_POINT('Ctrl Pts',(109.213677077013,0.750109946408958,
136.673959515427));
#182578=CARTESIAN_POINT('Ctrl Pts',(109.217613126454,0.667530887443442,
136.683921612908));
#182579=CARTESIAN_POINT('Ctrl Pts',(109.221549175894,0.584844965044413,
136.692134978847));
#182580=CARTESIAN_POINT('Ctrl Pts',(109.2289724423,0.428901895939548,136.707625130678));
#182581=CARTESIAN_POINT('Ctrl Pts',(109.236395708705,0.272107191678051,
136.716938984737));
#182582=CARTESIAN_POINT('Ctrl Pts',(109.243818975111,0.114991369290807,
136.719993089879));
#182583=CARTESIAN_POINT('Ctrl Pts',(109.251233467832,-0.0419387552421442,
136.723043585323));
#182584=CARTESIAN_POINT('Ctrl Pts',(109.258647960553,-0.199188872851643,
136.719849051427));
#182585=CARTESIAN_POINT('Ctrl Pts',(109.266062453274,-0.356221822541083,
136.710377598209));
#182586=CARTESIAN_POINT('Ctrl Pts',(109.273469799627,-0.513103417961313,
136.700915273934));
#182587=CARTESIAN_POINT('Ctrl Pts',(109.280877145981,-0.669767892046414,
136.685188096883));
#182588=CARTESIAN_POINT('Ctrl Pts',(109.288284492335,-0.825676658664553,
136.663216189931));
#182589=CARTESIAN_POINT('Ctrl Pts',(109.29568631401,-0.981469142642558,
136.641260670457));
#182590=CARTESIAN_POINT('Ctrl Pts',(109.303088135686,-1.1365066733729,136.613069746773));
#182591=CARTESIAN_POINT('Ctrl Pts',(109.310489957361,-1.29025447796769,
136.578715468507));
#182592=CARTESIAN_POINT('Ctrl Pts',(109.317887871672,-1.44392112029299,
136.544379325597));
#182593=CARTESIAN_POINT('Ctrl Pts',(109.325285785984,-1.59629902900928,
136.503886388978));
#182594=CARTESIAN_POINT('Ctrl Pts',(109.332683700295,-1.74686244673501,
136.457360012108));
#182595=CARTESIAN_POINT('Ctrl Pts',(109.340080385207,-1.89740084355233,
136.410841367077));
#182596=CARTESIAN_POINT('Ctrl Pts',(109.34747707012,-2.04612499152957,136.358291381861));
#182597=CARTESIAN_POINT('Ctrl Pts',(109.354873755032,-2.19252304013005,
136.299883639172));
#182598=CARTESIAN_POINT('Ctrl Pts',(109.362270111967,-2.33891459728753,
136.241478486343));
#182599=CARTESIAN_POINT('Ctrl Pts',(109.369666468903,-2.48297991342709,
136.177216230822));
#182600=CARTESIAN_POINT('Ctrl Pts',(109.377062825838,-2.6242261715584,136.107318995963));
#182601=CARTESIAN_POINT('Ctrl Pts',(109.384460315175,-2.76549405485232,
136.037411059659));
#182602=CARTESIAN_POINT('Ctrl Pts',(109.391857804511,-2.90394168616086,
135.961866591785));
#182603=CARTESIAN_POINT('Ctrl Pts',(109.399255293848,-3.03910008971452,
135.8809540824));
#182604=CARTESIAN_POINT('Ctrl Pts',(109.406655376363,-3.17430587283665,
135.800013209261));
#182605=CARTESIAN_POINT('Ctrl Pts',(109.414055458878,-3.30621981243113,
135.713700739666));
#182606=CARTESIAN_POINT('Ctrl Pts',(109.421455541392,-3.43440132943781,
135.622328868899));
#182607=CARTESIAN_POINT('Ctrl Pts',(109.428863761059,-3.56272379520065,
135.530856525367));
#182608=CARTESIAN_POINT('Ctrl Pts',(109.436271980725,-3.68730533789365,
135.434313887141));
#182609=CARTESIAN_POINT('Ctrl Pts',(109.443680200392,-3.80773736331207,
135.333054329282));
#182610=CARTESIAN_POINT('Ctrl Pts',(109.451092979694,-3.92824351263296,
135.231732447855));
#182611=CARTESIAN_POINT('Ctrl Pts',(109.458505758996,-4.04459478033752,
135.125688112711));
#182612=CARTESIAN_POINT('Ctrl Pts',(109.465918538298,-4.15641935227887,
135.015311665786));
#182613=CARTESIAN_POINT('Ctrl Pts',(109.473341909327,-4.26840370441258,
134.904777507817));
#182614=CARTESIAN_POINT('Ctrl Pts',(109.480765280356,-4.37584818850849,
134.789899147314));
#182615=CARTESIAN_POINT('Ctrl Pts',(109.488188651384,-4.47842065632573,
134.671100715826));
#182616=CARTESIAN_POINT('Ctrl Pts',(109.492124700825,-4.53280703995719,
134.60811093692));
#182617=CARTESIAN_POINT('Ctrl Pts',(109.496060750266,-4.58582443318841,
134.544019592876));
#182618=CARTESIAN_POINT('Ctrl Pts',(109.499996799707,-4.63742833134212,
134.478893109485));
#182619=CARTESIAN_POINT('Ctrl Pts',(109.507772966711,-4.73937840491298,
134.350227446411));
#182620=CARTESIAN_POINT('Ctrl Pts',(109.515549133715,-4.83613835824615,
134.217102726659));
#182621=CARTESIAN_POINT('Ctrl Pts',(109.523325300718,-4.92729617052023,
134.079980102561));
#182622=CARTESIAN_POINT('Ctrl Pts',(109.530729946761,-5.01409874736348,
133.949408768976));
#182623=CARTESIAN_POINT('Ctrl Pts',(109.538134592803,-5.09582174505376,
133.815213002727));
#182624=CARTESIAN_POINT('Ctrl Pts',(109.545539238845,-5.17214874724491,
133.677826799527));
#182625=CARTESIAN_POINT('Ctrl Pts',(109.552936918627,-5.24840394130658,
133.540569848701));
#182626=CARTESIAN_POINT('Ctrl Pts',(109.560334598409,-5.31927306273739,
133.400128758789));
#182627=CARTESIAN_POINT('Ctrl Pts',(109.567732278191,-5.38448260220117,
133.256966918849));
#182628=CARTESIAN_POINT('Ctrl Pts',(109.575124465065,-5.44964372243038,
133.113911379103));
#182629=CARTESIAN_POINT('Ctrl Pts',(109.582516651939,-5.50915347148947,
132.968139449289));
#182630=CARTESIAN_POINT('Ctrl Pts',(109.589908838812,-5.56278404411905,
132.820139435044));
#182631=CARTESIAN_POINT('Ctrl Pts',(109.597297002377,-5.616385427498,132.672219972047));
#182632=CARTESIAN_POINT('Ctrl Pts',(109.604685165941,-5.6641138786913,132.522075189744));
#182633=CARTESIAN_POINT('Ctrl Pts',(109.612073329506,-5.70578961301687,
132.370213565479));
#182634=CARTESIAN_POINT('Ctrl Pts',(109.619459567761,-5.74745448690789,
132.2183915154));
#182635=CARTESIAN_POINT('Ctrl Pts',(109.626845806016,-5.78306968274208,
132.064853873456));
#182636=CARTESIAN_POINT('Ctrl Pts',(109.634232044272,-5.8125052155614,131.910124462865));
#182637=CARTESIAN_POINT('Ctrl Pts',(109.641617182809,-5.84193636580126,
131.755418089532));
#182638=CARTESIAN_POINT('Ctrl Pts',(109.649002321347,-5.86518961886955,
131.599520668681));
#182639=CARTESIAN_POINT('Ctrl Pts',(109.656387459885,-5.88218612271177,
131.442966114158));
#182640=CARTESIAN_POINT('Ctrl Pts',(109.663774300717,-5.8991865442944,131.286375473383));
#182641=CARTESIAN_POINT('Ctrl Pts',(109.671161141549,-5.90992729760968,
131.129127768272));
#182642=CARTESIAN_POINT('Ctrl Pts',(109.678547982381,-5.91438139765927,
130.971762067745));
#182643=CARTESIAN_POINT('Ctrl Pts',(109.681240257519,-5.9160047794402,130.914407134462));
#182644=CARTESIAN_POINT('Ctrl Pts',(109.683932532657,-5.91679355703985,
130.857036545142));
#182645=CARTESIAN_POINT('Ctrl Pts',(109.686624807795,-5.91674814578703,
130.79967640731));
#182646=CARTESIAN_POINT('',(111.436624807795,-5.92599054836748,130.802728473828));
#182647=CARTESIAN_POINT('Ctrl Pts',(109.686626838718,-5.9113458756003,130.799637453972));
#182648=CARTESIAN_POINT('Ctrl Pts',(109.717232700319,-5.91613812751391,
130.148157013076));
#182649=CARTESIAN_POINT('Ctrl Pts',(109.840654436524,-5.5159435970196,127.526716476239));
#182650=CARTESIAN_POINT('Ctrl Pts',(110.056892047334,-1.67299786539814,
124.008873977688));
#182651=CARTESIAN_POINT('Ctrl Pts',(110.335339671146,4.81293915681766,125.723693613804));
#182652=CARTESIAN_POINT('Ctrl Pts',(110.613787294959,6.87602021906624,132.107398021992));
#182653=CARTESIAN_POINT('Ctrl Pts',(110.892234918771,2.62037461225579,137.293674712428));
#182654=CARTESIAN_POINT('Ctrl Pts',(111.166514089717,-3.94351033188604,
136.528222003439));
#182655=CARTESIAN_POINT('Ctrl Pts',(111.347977386058,-5.9191353605258,132.677693844969));
#182656=CARTESIAN_POINT('Ctrl Pts',(111.436624807795,-5.92599054836748,
130.802728473828));
#182657=CARTESIAN_POINT('',(113.186624807795,-5.9163106462342,130.809833344935));
#182658=CARTESIAN_POINT('Ctrl Pts',(111.436624807795,-5.92599054836748,
130.802728473828));
#182659=CARTESIAN_POINT('Ctrl Pts',(111.440793260663,-5.92631289871739,
130.714562291163));
#182660=CARTESIAN_POINT('Ctrl Pts',(111.44496171353,-5.92451638237235,130.626409536429));
#182661=CARTESIAN_POINT('Ctrl Pts',(111.541946041002,-5.83246842234974,
128.577681904707));
#182662=CARTESIAN_POINT('Ctrl Pts',(111.72757779021,-3.51471719713118,124.752557286777));
#182663=CARTESIAN_POINT('Ctrl Pts',(112.006025414023,3.19176304137608,124.57618197385));
#182664=CARTESIAN_POINT('Ctrl Pts',(112.284473037836,6.96516897115486,130.123198571052));
#182665=CARTESIAN_POINT('Ctrl Pts',(112.562920661649,4.33792488386143,136.296169812387));
#182666=CARTESIAN_POINT('Ctrl Pts',(112.841368285462,-2.27566025228867,
137.422436693472));
#182667=CARTESIAN_POINT('Ctrl Pts',(113.049269667511,-5.65225878233849,
133.722498405386));
#182668=CARTESIAN_POINT('Ctrl Pts',(113.164355174955,-5.92066294021549,
131.282860026435));
#182669=CARTESIAN_POINT('Ctrl Pts',(113.186624807795,-5.9163106462342,130.809833344935));
#182670=CARTESIAN_POINT('',(114.936624807795,-5.90703435793375,130.803551001656));
#182671=CARTESIAN_POINT('Ctrl Pts',(113.186624807795,-5.9163106462342,130.809833344935));
#182672=CARTESIAN_POINT('Ctrl Pts',(113.257171049559,-5.90252335186627,
129.311368827196));
#182673=CARTESIAN_POINT('Ctrl Pts',(113.420533165929,-4.56253139760311,
125.819471574505));
#182674=CARTESIAN_POINT('Ctrl Pts',(113.676711156899,1.31350002779897,123.93033136193));
#182675=CARTESIAN_POINT('Ctrl Pts',(113.955158780714,6.49329434443499,128.193864671035));
#182676=CARTESIAN_POINT('Ctrl Pts',(114.233606404526,5.70606837360377,134.856316225183));
#182677=CARTESIAN_POINT('Ctrl Pts',(114.512054028339,-0.324755675635378,
137.795218524968));
#182678=CARTESIAN_POINT('Ctrl Pts',(114.746393496096,-5.14909238192378,
134.861969788687));
#182679=CARTESIAN_POINT('Ctrl Pts',(114.887917089248,-5.90577078422116,
131.842246860606));
#182680=CARTESIAN_POINT('Ctrl Pts',(114.936624807795,-5.90703435793375,
130.803551001656));
#182681=CARTESIAN_POINT('',(116.686624005233,-5.91849301305788,130.799182298099));
#182682=CARTESIAN_POINT('Ctrl Pts',(114.936624807795,-5.90703435793375,
130.803551001656));
#182683=CARTESIAN_POINT('Ctrl Pts',(114.980732963852,-5.9081786099777,129.86294116798));
#182684=CARTESIAN_POINT('Ctrl Pts',(115.117656994514,-5.25199350988407,
126.944533803055));
#182685=CARTESIAN_POINT('Ctrl Pts',(115.347396899778,-0.670561456245021,
123.838163099281));
#182686=CARTESIAN_POINT('Ctrl Pts',(115.625844523592,5.49840441862291,126.474798355674));
#182687=CARTESIAN_POINT('Ctrl Pts',(115.904292147403,6.61460524476664,133.09008981987));
#182688=CARTESIAN_POINT('Ctrl Pts',(116.182739771217,1.65230699240024,137.604907811225));
#182689=CARTESIAN_POINT('Ctrl Pts',(116.443516934764,-4.41711217639929,
135.980430952529));
#182690=CARTESIAN_POINT('Ctrl Pts',(116.611478223709,-5.90462326373388,
132.393283988731));
#182691=CARTESIAN_POINT('Ctrl Pts',(116.686623638048,-5.91929151057414,
130.799189386355));
#182692=CARTESIAN_POINT('',(118.436626221702,-5.92102170304425,130.807562845889));
#182693=CARTESIAN_POINT('Ctrl Pts',(116.686624807795,-5.91674772039611,
130.79916680515));
#182694=CARTESIAN_POINT('Ctrl Pts',(116.697559326435,-5.91654419251059,
130.567309538048));
#182695=CARTESIAN_POINT('Ctrl Pts',(116.708493845074,-5.9027089717455,130.336026612641));
#182696=CARTESIAN_POINT('Ctrl Pts',(116.719428363714,-5.87546247901726,
130.10659903926));
#182697=CARTESIAN_POINT('Ctrl Pts',(116.726163915423,-5.85867891800975,
129.965273999261));
#182698=CARTESIAN_POINT('Ctrl Pts',(116.732899467133,-5.8368073903389,129.824652131221));
#182699=CARTESIAN_POINT('Ctrl Pts',(116.739635018842,-5.80990738120078,
129.685027430187));
#182700=CARTESIAN_POINT('Ctrl Pts',(116.747058285247,-5.78026082175766,
129.531146739006));
#182701=CARTESIAN_POINT('Ctrl Pts',(116.754481551653,-5.74445170516041,
129.378212000212));
#182702=CARTESIAN_POINT('Ctrl Pts',(116.761904818058,-5.70255141329609,
129.226755489147));
#182703=CARTESIAN_POINT('Ctrl Pts',(116.769319310779,-5.66070064409708,
129.0754779871));
#182704=CARTESIAN_POINT('Ctrl Pts',(116.7767338035,-5.6127731283662,128.925675591356));
#182705=CARTESIAN_POINT('Ctrl Pts',(116.784148296221,-5.55889156157783,
128.777872233904));
#182706=CARTESIAN_POINT('Ctrl Pts',(116.791555642575,-5.50506192787217,
128.630211334891));
#182707=CARTESIAN_POINT('Ctrl Pts',(116.798962988928,-5.44528979480404,
128.484545986759));
#182708=CARTESIAN_POINT('Ctrl Pts',(116.806370335282,-5.37974811534769,
128.34138664736));
#182709=CARTESIAN_POINT('Ctrl Pts',(116.813772156957,-5.31425531934863,
128.198334081597));
#182710=CARTESIAN_POINT('Ctrl Pts',(116.821173978633,-5.24300169982891,
128.057784140942));
#182711=CARTESIAN_POINT('Ctrl Pts',(116.828575800308,-5.16620889014691,
127.920228813042));
#182712=CARTESIAN_POINT('Ctrl Pts',(116.835973714619,-5.08945661879133,
127.782746099529));
#182713=CARTESIAN_POINT('Ctrl Pts',(116.843371628931,-5.00717116225369,
127.648255175586));
#182714=CARTESIAN_POINT('Ctrl Pts',(116.850769543242,-4.91962075296629,
127.517224750358));
#182715=CARTESIAN_POINT('Ctrl Pts',(116.858166228154,-4.83208489296877,
127.386216100011));
#182716=CARTESIAN_POINT('Ctrl Pts',(116.865562913066,-4.73928602390572,
127.258667117113));
#182717=CARTESIAN_POINT('Ctrl Pts',(116.872959597979,-4.64153655180344,
127.135018850876));
#182718=CARTESIAN_POINT('Ctrl Pts',(116.880355954914,-4.54379141401512,
127.011376067333));
#182719=CARTESIAN_POINT('Ctrl Pts',(116.887752311849,-4.44109634116225,
126.891633949385));
#182720=CARTESIAN_POINT('Ctrl Pts',(116.895148668785,-4.33380483171786,
126.776201454489));
#182721=CARTESIAN_POINT('Ctrl Pts',(116.902546158121,-4.22649689566947,
126.660751286584));
#182722=CARTESIAN_POINT('Ctrl Pts',(116.909943647458,-4.11459137597694,
126.549612328952));
#182723=CARTESIAN_POINT('Ctrl Pts',(116.917341136794,-3.99847940828271,
126.443157459716));
#182724=CARTESIAN_POINT('Ctrl Pts',(116.924741219309,-3.88232673771803,
126.336665272891));
#182725=CARTESIAN_POINT('Ctrl Pts',(116.932141301824,-3.76196495829002,
126.234860695784));
#182726=CARTESIAN_POINT('Ctrl Pts',(116.939541384339,-3.63781899221396,
126.138076920405));
#182727=CARTESIAN_POINT('Ctrl Pts',(116.946949604006,-3.51353651488587,
126.041186721316));
#182728=CARTESIAN_POINT('Ctrl Pts',(116.954357823672,-3.38546183549985,
125.949328579188));
#182729=CARTESIAN_POINT('Ctrl Pts',(116.961766043339,-3.25405021861709,
125.862793281465));
#182730=CARTESIAN_POINT('Ctrl Pts',(116.969178822641,-3.12255772007668,
125.776204722711));
#182731=CARTESIAN_POINT('Ctrl Pts',(116.976591601943,-2.98772451050982,
125.694945728685));
#182732=CARTESIAN_POINT('Ctrl Pts',(116.984004381245,-2.85003079089306,
125.619261288386));
#182733=CARTESIAN_POINT('Ctrl Pts',(116.991427752274,-2.71214032803271,
125.54346870661));
#182734=CARTESIAN_POINT('Ctrl Pts',(116.998851123302,-2.57138152517667,
125.473266752986));
#182735=CARTESIAN_POINT('Ctrl Pts',(117.006274494331,-2.42825565114771,
125.408852758692));
#182736=CARTESIAN_POINT('Ctrl Pts',(117.010210543773,-2.35236687846472,
125.374698913318));
#182737=CARTESIAN_POINT('Ctrl Pts',(117.014146593214,-2.2758129214637,125.342171447449));
#182738=CARTESIAN_POINT('Ctrl Pts',(117.018082642656,-2.19867014271157,
125.311294063623));
#182739=CARTESIAN_POINT('Ctrl Pts',(117.025505909061,-2.05318126955525,
125.253060281388));
#182740=CARTESIAN_POINT('Ctrl Pts',(117.032929175466,-1.90515724026218,
125.20052254339));
#182741=CARTESIAN_POINT('Ctrl Pts',(117.040352441872,-1.75508445680622,
125.153908501852));
#182742=CARTESIAN_POINT('Ctrl Pts',(117.047766934593,-1.60518904691754,
125.10734955424));
#182743=CARTESIAN_POINT('Ctrl Pts',(117.055181427314,-1.4532500558055,125.066700476575));
#182744=CARTESIAN_POINT('Ctrl Pts',(117.062595920035,-1.29977460219091,
125.032141239718));
#182745=CARTESIAN_POINT('Ctrl Pts',(117.070003266389,-1.14644707399665,
124.997615312355));
#182746=CARTESIAN_POINT('Ctrl Pts',(117.077410612743,-0.991586393215401,
124.969167622001));
#182747=CARTESIAN_POINT('Ctrl Pts',(117.084817959096,-0.835715507803487,
124.946928573358));
#182748=CARTESIAN_POINT('Ctrl Pts',(117.092219780772,-0.679960876778697,
124.924706111436));
#182749=CARTESIAN_POINT('Ctrl Pts',(117.099621602447,-0.523197909306233,
124.908683123499));
#182750=CARTESIAN_POINT('Ctrl Pts',(117.107023424123,-0.365960326771369,
124.898939074464));
#182751=CARTESIAN_POINT('Ctrl Pts',(117.114421338434,-0.20880574873239,
124.889200169237));
#182752=CARTESIAN_POINT('Ctrl Pts',(117.121819252745,-0.0511774262446159,
124.885733624754));
#182753=CARTESIAN_POINT('Ctrl Pts',(117.129217167057,0.106385316232477,
124.888567118213));
#182754=CARTESIAN_POINT('Ctrl Pts',(117.136613851969,0.263921874640249,
124.891400140796));
#182755=CARTESIAN_POINT('Ctrl Pts',(117.144010536881,0.421392501794947,
124.900531116727));
#182756=CARTESIAN_POINT('Ctrl Pts',(117.151407221793,0.578257267417322,
124.915935607839));
#182757=CARTESIAN_POINT('Ctrl Pts',(117.158803578729,0.735115077491607,
124.931339415899));
#182758=CARTESIAN_POINT('Ctrl Pts',(117.166199935664,0.891366707938846,
124.953016149552));
#182759=CARTESIAN_POINT('Ctrl Pts',(117.1735962926,1.04647701670976,124.980889452015));
#182760=CARTESIAN_POINT('Ctrl Pts',(117.180993781936,1.20161107326492,125.008767021953));
#182761=CARTESIAN_POINT('Ctrl Pts',(117.188391271273,1.35560309277827,125.04284298368));
#182762=CARTESIAN_POINT('Ctrl Pts',(117.195788760609,1.50792794395739,125.082989813438));
#182763=CARTESIAN_POINT('Ctrl Pts',(117.203188843124,1.66030619237707,125.123150716604));
#182764=CARTESIAN_POINT('Ctrl Pts',(117.210588925639,1.81101574813416,125.169386629819));
#182765=CARTESIAN_POINT('Ctrl Pts',(117.217989008154,1.95954660651778,125.22152015241));
#182766=CARTESIAN_POINT('Ctrl Pts',(117.225397227821,2.10824078984943,125.273711001168));
#182767=CARTESIAN_POINT('Ctrl Pts',(117.232805447487,2.25475113898685,125.33181228662));
#182768=CARTESIAN_POINT('Ctrl Pts',(117.240213667154,2.39858692460105,125.395598159514));
#182769=CARTESIAN_POINT('Ctrl Pts',(117.247626446456,2.54251123874147,125.459423291549));
#182770=CARTESIAN_POINT('Ctrl Pts',(117.255039225758,2.68375737504578,125.528939818301));
#182771=CARTESIAN_POINT('Ctrl Pts',(117.26245200506,2.82185965697311,125.603876155629));
#182772=CARTESIAN_POINT('Ctrl Pts',(117.269875376089,2.96015926591721,125.67891956551));
#182773=CARTESIAN_POINT('Ctrl Pts',(117.277298747117,3.09530572889295,125.759398062139));
#182774=CARTESIAN_POINT('Ctrl Pts',(117.284722118146,3.22686207754897,125.844996576182));
#182775=CARTESIAN_POINT('Ctrl Pts',(117.288658167587,3.29661641025614,125.890382962234));
#182776=CARTESIAN_POINT('Ctrl Pts',(117.292594217028,3.36536197219685,125.937208084541));
#182777=CARTESIAN_POINT('Ctrl Pts',(117.296530266468,3.43303754592154,125.985420508912));
#182778=CARTESIAN_POINT('Ctrl Pts',(117.303953532874,3.56067156588671,126.07634763662));
#182779=CARTESIAN_POINT('Ctrl Pts',(117.311376799279,3.68488365633071,126.17248651403));
#182780=CARTESIAN_POINT('Ctrl Pts',(117.318800065685,3.80521937484481,126.273550968971));
#182781=CARTESIAN_POINT('Ctrl Pts',(117.326214558406,3.92541286653305,126.374495974119));
#182782=CARTESIAN_POINT('Ctrl Pts',(117.333629051127,4.04173882282624,126.480354731091));
#182783=CARTESIAN_POINT('Ctrl Pts',(117.341043543848,4.15377171908746,126.59079786519));
#182784=CARTESIAN_POINT('Ctrl Pts',(117.348450890201,4.2656966338253,126.701134550039));
#182785=CARTESIAN_POINT('Ctrl Pts',(117.355858236555,4.37333646204576,126.816046555153));
#182786=CARTESIAN_POINT('Ctrl Pts',(117.363265582909,4.47629882443489,126.935164396532));
#182787=CARTESIAN_POINT('Ctrl Pts',(117.370667404584,4.5791843936096,127.054193395332));
#182788=CARTESIAN_POINT('Ctrl Pts',(117.37806922626,4.67739920022347,127.177421703261));
#182789=CARTESIAN_POINT('Ctrl Pts',(117.385471047935,4.77058789874365,127.304443238133));
#182790=CARTESIAN_POINT('Ctrl Pts',(117.392868962247,4.86372740367526,127.431397719325));
#182791=CARTESIAN_POINT('Ctrl Pts',(117.400266876558,4.95184586431757,127.562141139332));
#182792=CARTESIAN_POINT('Ctrl Pts',(117.407664790869,5.03462847701474,127.696234709413));
#182793=CARTESIAN_POINT('Ctrl Pts',(117.415061475782,5.11739733274345,127.830305995576));
#182794=CARTESIAN_POINT('Ctrl Pts',(117.422458160694,5.19483190450104,127.967726009528));
#182795=CARTESIAN_POINT('Ctrl Pts',(117.429854845606,5.2666609073049,128.108027283209));
#182796=CARTESIAN_POINT('Ctrl Pts',(117.437251202542,5.33848672513551,128.248322335784));
#182797=CARTESIAN_POINT('Ctrl Pts',(117.444647559477,5.40470729811113,128.391498061778));
#182798=CARTESIAN_POINT('Ctrl Pts',(117.452043916412,5.46509761000641,128.537062958324));
#182799=CARTESIAN_POINT('Ctrl Pts',(117.459441405749,5.52549716781264,128.682650141228));
#182800=CARTESIAN_POINT('Ctrl Pts',(117.466838895086,5.58006454414085,128.830626878191));
#182801=CARTESIAN_POINT('Ctrl Pts',(117.474236384422,5.6286231820523,128.980482431677));
#182802=CARTESIAN_POINT('Ctrl Pts',(117.481636466937,5.677198842119,129.130390516794));
#182803=CARTESIAN_POINT('Ctrl Pts',(117.489036549452,5.71976145503388,129.282178374837));
#182804=CARTESIAN_POINT('Ctrl Pts',(117.496436631967,5.75618460300468,129.435321035));
#182805=CARTESIAN_POINT('Ctrl Pts',(117.503844851634,5.79264780197107,129.588632091261));
#182806=CARTESIAN_POINT('Ctrl Pts',(117.5112530713,5.82295796742928,129.743300561369));
#182807=CARTESIAN_POINT('Ctrl Pts',(117.518661290967,5.84703986156242,129.898791503804));
#182808=CARTESIAN_POINT('Ctrl Pts',(117.526074070269,5.87113657769958,130.054378148319));
#182809=CARTESIAN_POINT('Ctrl Pts',(117.533486849571,5.88899734173318,130.210787903836));
#182810=CARTESIAN_POINT('Ctrl Pts',(117.540899628873,5.90059893554949,130.367482185628));
#182811=CARTESIAN_POINT('Ctrl Pts',(117.548322999902,5.91221710626711,130.524400359559));
#182812=CARTESIAN_POINT('Ctrl Pts',(117.555746370931,5.91755823215747,130.681603499632));
#182813=CARTESIAN_POINT('Ctrl Pts',(117.563169741959,5.91665119790844,130.838553669326));
#182814=CARTESIAN_POINT('Ctrl Pts',(117.5671057914,5.91617026658563,130.921772415262));
#182815=CARTESIAN_POINT('Ctrl Pts',(117.571041840841,5.91393362046543,131.00492012587));
#182816=CARTESIAN_POINT('Ctrl Pts',(117.574977890281,5.90995144306108,131.087917495741));
#182817=CARTESIAN_POINT('Ctrl Pts',(117.582401156687,5.90244118075565,131.244447945065));
#182818=CARTESIAN_POINT('Ctrl Pts',(117.589824423092,5.88869648933059,131.400916506187));
#182819=CARTESIAN_POINT('Ctrl Pts',(117.597247689498,5.86871249631517,131.556786160789));
#182820=CARTESIAN_POINT('Ctrl Pts',(117.604662182219,5.84875212271991,131.712471590403));
#182821=CARTESIAN_POINT('Ctrl Pts',(117.61207667494,5.82256717319967,131.867559155842));
#182822=CARTESIAN_POINT('Ctrl Pts',(117.619491167661,5.79020475355474,132.021512816107));
#182823=CARTESIAN_POINT('Ctrl Pts',(117.626898514014,5.75787352602829,132.175318090037));
#182824=CARTESIAN_POINT('Ctrl Pts',(117.634305860368,5.7193767580515,132.327991271683));
#182825=CARTESIAN_POINT('Ctrl Pts',(117.641713206722,5.6748132163735,132.479002526086));
#182826=CARTESIAN_POINT('Ctrl Pts',(117.649115028397,5.63028291186618,132.629901150599));
#182827=CARTESIAN_POINT('Ctrl Pts',(117.656516850073,5.57969494840352,132.779139959445));
#182828=CARTESIAN_POINT('Ctrl Pts',(117.663918671748,5.5231989014902,132.926200493023));
#182829=CARTESIAN_POINT('Ctrl Pts',(117.671316586059,5.46673267840028,133.073183394489));
#182830=CARTESIAN_POINT('Ctrl Pts',(117.678714500371,5.40436471669324,133.217989963171));
#182831=CARTESIAN_POINT('Ctrl Pts',(117.686112414682,5.33629402269755,133.360118169804));
#182832=CARTESIAN_POINT('Ctrl Pts',(117.693509099594,5.26823464081633,133.502222757308));
#182833=CARTESIAN_POINT('Ctrl Pts',(117.700905784506,5.19447456862119,133.6416495298));
#182834=CARTESIAN_POINT('Ctrl Pts',(117.708302469419,5.11526046407216,133.777917569635));
#182835=CARTESIAN_POINT('Ctrl Pts',(117.715698826354,5.03604987195955,133.914179567203));
#182836=CARTESIAN_POINT('Ctrl Pts',(117.72309518329,4.95138591595434,134.047282787873));
#182837=CARTESIAN_POINT('Ctrl Pts',(117.730491540225,4.86156048457356,134.176772249816));
#182838=CARTESIAN_POINT('Ctrl Pts',(117.737889029561,4.77172130068986,134.306281536926));
#182839=CARTESIAN_POINT('Ctrl Pts',(117.745286518898,4.67671928075236,134.43217565692));
#182840=CARTESIAN_POINT('Ctrl Pts',(117.752684008235,4.57688868937742,134.554030001332));
#182841=CARTESIAN_POINT('Ctrl Pts',(117.76008409075,4.4770231025435,134.675927061594));
#182842=CARTESIAN_POINT('Ctrl Pts',(117.767484173265,4.37232581064742,134.793781238172));
#182843=CARTESIAN_POINT('Ctrl Pts',(117.77488425578,4.26317015459075,134.907202412652));
#182844=CARTESIAN_POINT('Ctrl Pts',(117.782292475446,4.1538944706687,135.020748305374));
#182845=CARTESIAN_POINT('Ctrl Pts',(117.789700695112,4.04015089112619,135.129851192083));
#182846=CARTESIAN_POINT('Ctrl Pts',(117.797108914779,3.92234880953655,135.234158624115));
#182847=CARTESIAN_POINT('Ctrl Pts',(117.804521694081,3.80447422273125,135.338530255631));
#182848=CARTESIAN_POINT('Ctrl Pts',(117.811934473383,3.68253644489493,135.438100315633));
#182849=CARTESIAN_POINT('Ctrl Pts',(117.819347252685,3.55697605265327,135.532558151865));
#182850=CARTESIAN_POINT('Ctrl Pts',(117.826770623714,3.43123625383499,135.627150953883));
#182851=CARTESIAN_POINT('Ctrl Pts',(117.834193994743,3.30186380887613,135.716616731473));
#182852=CARTESIAN_POINT('Ctrl Pts',(117.841617365771,3.16932691188674,135.800689018311));
#182853=CARTESIAN_POINT('Ctrl Pts',(117.845553415212,3.09905266891977,135.845266162082));
#182854=CARTESIAN_POINT('Ctrl Pts',(117.849489464653,3.02788918325162,135.88832777694));
#182855=CARTESIAN_POINT('Ctrl Pts',(117.853425514094,2.95590868120716,135.929839564051));
#182856=CARTESIAN_POINT('Ctrl Pts',(117.8608487805,2.82015570079294,136.008129499001));
#182857=CARTESIAN_POINT('Ctrl Pts',(117.868272046905,2.68108492745272,136.081140780079));
#182858=CARTESIAN_POINT('Ctrl Pts',(117.875695313311,2.53914553621633,136.148579036419));
#182859=CARTESIAN_POINT('Ctrl Pts',(117.883109806032,2.39737390555306,136.215937586342));
#182860=CARTESIAN_POINT('Ctrl Pts',(117.890524298753,2.25274073962245,136.277736064058));
#182861=CARTESIAN_POINT('Ctrl Pts',(117.897938791474,2.10572248673276,136.33372435776));
#182862=CARTESIAN_POINT('Ctrl Pts',(117.905346137827,1.95884593557024,136.389658687836));
#182863=CARTESIAN_POINT('Ctrl Pts',(117.912753484181,1.80958922049484,136.439793850581));
#182864=CARTESIAN_POINT('Ctrl Pts',(117.920160830535,1.65845149250135,136.483926552523));
#182865=CARTESIAN_POINT('Ctrl Pts',(117.927562652211,1.50742648872749,136.52802633863));
#182866=CARTESIAN_POINT('Ctrl Pts',(117.934964473886,1.35452362225062,136.566132473785));
#182867=CARTESIAN_POINT('Ctrl Pts',(117.942366295561,1.2002599370313,136.598090560017));
#182868=CARTESIAN_POINT('Ctrl Pts',(117.949764209873,1.04607768641041,136.630031775825));
#182869=CARTESIAN_POINT('Ctrl Pts',(117.957162124184,0.890536412317678,
136.655831330758));
#182870=CARTESIAN_POINT('Ctrl Pts',(117.964560038495,0.734166053972068,
136.675385295397));
#182871=CARTESIAN_POINT('Ctrl Pts',(117.971956723408,0.577821681543391,
136.694936010521));
#182872=CARTESIAN_POINT('Ctrl Pts',(117.97935340832,0.420648868362236,136.70824314901));
#182873=CARTESIAN_POINT('Ctrl Pts',(117.986750093232,0.263185548715929,
136.715254283455));
#182874=CARTESIAN_POINT('Ctrl Pts',(117.994146450168,0.105729211158112,
136.722265107019));
#182875=CARTESIAN_POINT('Ctrl Pts',(118.001542807103,-0.0520172343242812,
136.722980465023));
#182876=CARTESIAN_POINT('Ctrl Pts',(118.008939164039,-0.209513225759455,
136.71740000275));
#182877=CARTESIAN_POINT('Ctrl Pts',(118.016336653375,-0.367033330232874,
136.711818686093));
#182878=CARTESIAN_POINT('Ctrl Pts',(118.023734142712,-0.524302531221012,
136.699939643114));
#182879=CARTESIAN_POINT('Ctrl Pts',(118.031131632048,-0.680782915405135,
136.681814588853));
#182880=CARTESIAN_POINT('Ctrl Pts',(118.038531714563,-0.837318153545358,
136.663683180882));
#182881=CARTESIAN_POINT('Ctrl Pts',(118.045931797078,-0.993063653747919,
136.639301445216));
#182882=CARTESIAN_POINT('Ctrl Pts',(118.053331879593,-1.14748939846722,
136.608772615599));
#182883=CARTESIAN_POINT('Ctrl Pts',(118.06074009926,-1.3020849501683,136.578210216395));
#182884=CARTESIAN_POINT('Ctrl Pts',(118.068148318926,-1.45535748179579,
136.541487296792));
#182885=CARTESIAN_POINT('Ctrl Pts',(118.075556538593,-1.60678918108002,
136.498757784085));
#182886=CARTESIAN_POINT('Ctrl Pts',(118.082969317895,-1.75831408404838,
136.456001972077));
#182887=CARTESIAN_POINT('Ctrl Pts',(118.090382097197,-1.90799554291565,
136.40723231569));
#182888=CARTESIAN_POINT('Ctrl Pts',(118.097794876499,-2.05533405471236,
136.352651569385));
#182889=CARTESIAN_POINT('Ctrl Pts',(118.105218247528,-2.20288309068433,
136.297992835551));
#182890=CARTESIAN_POINT('Ctrl Pts',(118.112641618557,-2.34808214977163,
136.237506571698));
#182891=CARTESIAN_POINT('Ctrl Pts',(118.120064989585,-2.49045397595665,
136.171442651236));
#182892=CARTESIAN_POINT('Ctrl Pts',(118.124001039026,-2.56594293436141,
136.136413975426));
#182893=CARTESIAN_POINT('Ctrl Pts',(118.127937088467,-2.64063749277048,
136.099817974152));
#182894=CARTESIAN_POINT('Ctrl Pts',(118.131873137907,-2.71446975451147,
136.061696874107));
#182895=CARTESIAN_POINT('Ctrl Pts',(118.139296404313,-2.85371509593537,
135.989801669139));
#182896=CARTESIAN_POINT('Ctrl Pts',(118.146719670718,-2.99031270447579,
135.912261869661));
#182897=CARTESIAN_POINT('Ctrl Pts',(118.154142937123,-3.12377212751132,
135.829296264705));
#182898=CARTESIAN_POINT('Ctrl Pts',(118.161557429844,-3.25707381259186,
135.746428718203));
#182899=CARTESIAN_POINT('Ctrl Pts',(118.168971922565,-3.38724438116514,
135.658148326199));
#182900=CARTESIAN_POINT('Ctrl Pts',(118.176386415286,-3.51381587513444,
135.564720746606));
#182901=CARTESIAN_POINT('Ctrl Pts',(118.18379376164,-3.6402653747327,135.471383216031));
#182902=CARTESIAN_POINT('Ctrl Pts',(118.191201107994,-3.76312240734789,
135.372908594552));
#182903=CARTESIAN_POINT('Ctrl Pts',(118.198608454348,-3.88194613311887,
135.269606946948));
#182904=CARTESIAN_POINT('Ctrl Pts',(118.206010276023,-4.00068123567213,
135.166382345611));
#182905=CARTESIAN_POINT('Ctrl Pts',(118.213412097698,-4.11538874059069,
135.058338130456));
#182906=CARTESIAN_POINT('Ctrl Pts',(118.220813919374,-4.22565927359882,
134.945825849335));
#182907=CARTESIAN_POINT('Ctrl Pts',(118.228211833685,-4.33587159565062,
134.833372962571));
#182908=CARTESIAN_POINT('Ctrl Pts',(118.235609747996,-4.44165134985032,
134.71645697315));
#182909=CARTESIAN_POINT('Ctrl Pts',(118.243007662308,-4.54262465234175,
134.595467557556));
#182910=CARTESIAN_POINT('Ctrl Pts',(118.25040434722,-4.64358117490245,134.474498248207));
#182911=CARTESIAN_POINT('Ctrl Pts',(118.257801032132,-4.73973259207421,
134.34945714251));
#182912=CARTESIAN_POINT('Ctrl Pts',(118.265197717044,-4.83074402857291,
134.220768481523));
#182913=CARTESIAN_POINT('Ctrl Pts',(118.27259407398,-4.92175142952915,134.092085526726));
#182914=CARTESIAN_POINT('Ctrl Pts',(118.279990430915,-5.0076190874318,133.959755643005));
#182915=CARTESIAN_POINT('Ctrl Pts',(118.287386787851,-5.08805451689844,
133.824233428724));
#182916=CARTESIAN_POINT('Ctrl Pts',(118.294784277187,-5.16850226123474,
133.688690465645));
#182917=CARTESIAN_POINT('Ctrl Pts',(118.302181766524,-5.24351593059231,
133.549954519867));
#182918=CARTESIAN_POINT('Ctrl Pts',(118.30957925586,-5.31284827901142,133.408506106341));
#182919=CARTESIAN_POINT('Ctrl Pts',(118.316979338375,-5.38220493177775,
133.267008108293));
#182920=CARTESIAN_POINT('Ctrl Pts',(118.32437942089,-5.44587613419044,133.122796084346));
#182921=CARTESIAN_POINT('Ctrl Pts',(118.331779503405,-5.50366225229148,
132.976371753634));
#182922=CARTESIAN_POINT('Ctrl Pts',(118.339187723072,-5.56151191216997,
132.829786414316));
#182923=CARTESIAN_POINT('Ctrl Pts',(118.346595942738,-5.61346342709531,
132.680984257502));
#182924=CARTESIAN_POINT('Ctrl Pts',(118.354004162405,-5.65936641028078,
132.530484134782));
#182925=CARTESIAN_POINT('Ctrl Pts',(118.361416941707,-5.70529764598653,
132.379891381747));
#182926=CARTESIAN_POINT('Ctrl Pts',(118.368829721009,-5.7451728375307,132.227598940661));
#182927=CARTESIAN_POINT('Ctrl Pts',(118.376242500311,-5.77889257442692,
132.074136651256));
#182928=CARTESIAN_POINT('Ctrl Pts',(118.38366587134,-5.81266049166447,131.920455087736));
#182929=CARTESIAN_POINT('Ctrl Pts',(118.391089242369,-5.84025532294638,
131.765600704004));
#182930=CARTESIAN_POINT('Ctrl Pts',(118.398512613398,-5.86162932531237,
131.610110091744));
#182931=CARTESIAN_POINT('Ctrl Pts',(118.402448662838,-5.87296233422877,
131.527665238179));
#182932=CARTESIAN_POINT('Ctrl Pts',(118.406384712279,-5.88254731524014,
131.445041558131));
#182933=CARTESIAN_POINT('Ctrl Pts',(118.41032076172,-5.89038309505153,131.362318999554));
#182934=CARTESIAN_POINT('Ctrl Pts',(118.419088777078,-5.90783822074711,
131.178044722765));
#182935=CARTESIAN_POINT('Ctrl Pts',(118.427856792437,-5.91664794092523,
130.992938687461));
#182936=CARTESIAN_POINT('Ctrl Pts',(118.436624807795,-5.91674911845536,
130.807590440738));
#182937=CARTESIAN_POINT('',(120.186623619739,-5.91251430151314,130.808017835056));
#182938=CARTESIAN_POINT('Ctrl Pts',(118.436627322331,-5.92434761776706,
130.807541365187));
#182939=CARTESIAN_POINT('Ctrl Pts',(118.520674343399,-5.91263932333013,
129.028571282425));
#182940=CARTESIAN_POINT('Ctrl Pts',(118.69753723907,-4.11280805307987,125.264539470063));
#182941=CARTESIAN_POINT('Ctrl Pts',(118.967216009345,2.29579285864173,124.193241523149));
#182942=CARTESIAN_POINT('Ctrl Pts',(119.245663633159,6.80305384870884,129.162404813681));
#182943=CARTESIAN_POINT('Ctrl Pts',(119.524111256971,5.05864069946902,135.640445273981));
#182944=CARTESIAN_POINT('Ctrl Pts',(119.802558880784,-1.33441612424553,
137.674360190906));
#182945=CARTESIAN_POINT('Ctrl Pts',(120.023396027555,-5.4322063654912,134.280458789483));
#182946=CARTESIAN_POINT('Ctrl Pts',(120.151417299721,-5.91340439953517,
131.558097539106));
#182947=CARTESIAN_POINT('Ctrl Pts',(120.186622697283,-5.90922639532864,
130.808035468526));
#182948=CARTESIAN_POINT('',(121.936626022957,-5.91342861064485,130.799761379028));
#182949=CARTESIAN_POINT('Ctrl Pts',(120.186624807795,-5.91674888370799,
130.807995124438));
#182950=CARTESIAN_POINT('Ctrl Pts',(120.194083991,-5.9168466282442,130.648873159404));
#182951=CARTESIAN_POINT('Ctrl Pts',(120.201543174204,-5.91052102208661,
130.489729998654));
#182952=CARTESIAN_POINT('Ctrl Pts',(120.209002357409,-5.89779360542141,
130.331115279131));
#182953=CARTESIAN_POINT('Ctrl Pts',(120.216462331572,-5.88506483916271,
130.172483740374));
#182954=CARTESIAN_POINT('Ctrl Pts',(120.223922305736,-5.86593293838123,
130.014381117835));
#182955=CARTESIAN_POINT('Ctrl Pts',(120.231382279899,-5.84047139694184,
129.857352473987));
#182956=CARTESIAN_POINT('Ctrl Pts',(120.238844423679,-5.81500245041472,
129.700278160835));
#182957=CARTESIAN_POINT('Ctrl Pts',(120.246306567458,-5.78320025401866,
129.544278808323));
#182958=CARTESIAN_POINT('Ctrl Pts',(120.253768711238,-5.74518954052248,
129.389889795678));
#182959=CARTESIAN_POINT('Ctrl Pts',(120.261234404323,-5.70716074755135,
129.235427349203));
#182960=CARTESIAN_POINT('Ctrl Pts',(120.268700097408,-5.66291764158275,
129.082577121966));
#182961=CARTESIAN_POINT('Ctrl Pts',(120.276165790493,-5.61263496516564,
128.931859800397));
#182962=CARTESIAN_POINT('Ctrl Pts',(120.28364116073,-5.56228711153645,128.780947116616));
#182963=CARTESIAN_POINT('Ctrl Pts',(120.291116530966,-5.50588416412254,
128.63217320733));
#182964=CARTESIAN_POINT('Ctrl Pts',(120.298591901202,-5.44364958479852,
128.486040156451));
#182965=CARTESIAN_POINT('Ctrl Pts',(120.306072502209,-5.38137145782292,
128.339804851307));
#182966=CARTESIAN_POINT('Ctrl Pts',(120.313553103216,-5.3132537206381,128.196214416576));
#182967=CARTESIAN_POINT('Ctrl Pts',(120.321033704224,-5.23956589460368,
128.05574645792));
#182968=CARTESIAN_POINT('Ctrl Pts',(120.32852648743,-5.16575806754871,127.915049746439));
#182969=CARTESIAN_POINT('Ctrl Pts',(120.336019270636,-5.08636220911963,
127.777485986279));
#182970=CARTESIAN_POINT('Ctrl Pts',(120.343512053842,-5.00169188693494,
127.64350490579));
#182971=CARTESIAN_POINT('Ctrl Pts',(120.348826078698,-4.94164207843157,
127.548482966356));
#182972=CARTESIAN_POINT('Ctrl Pts',(120.354140103554,-4.87894016049074,
127.455262458878));
#182973=CARTESIAN_POINT('Ctrl Pts',(120.359454128411,-4.81371002966179,
127.363993440529));
#182974=CARTESIAN_POINT('Ctrl Pts',(120.366877394816,-4.72258876999511,
127.236497943973));
#182975=CARTESIAN_POINT('Ctrl Pts',(120.374300661221,-4.6262609742564,127.11243230437));
#182976=CARTESIAN_POINT('Ctrl Pts',(120.381723927627,-4.52501350586842,
126.9922505281));
#182977=CARTESIAN_POINT('Ctrl Pts',(120.389138420348,-4.42388570358,126.872210796709));
#182978=CARTESIAN_POINT('Ctrl Pts',(120.396552913069,-4.3178500408882,126.756046074127));
#182979=CARTESIAN_POINT('Ctrl Pts',(120.40396740579,-4.20723653968417,126.644181383249));
#182980=CARTESIAN_POINT('Ctrl Pts',(120.411374752144,-4.09672965193697,
126.53242451177));
#182981=CARTESIAN_POINT('Ctrl Pts',(120.418782098497,-3.98165397039524,
126.424959684706));
#182982=CARTESIAN_POINT('Ctrl Pts',(120.426189444851,-3.8623795757647,126.322178718623));
#182983=CARTESIAN_POINT('Ctrl Pts',(120.433591266527,-3.7431941404779,126.219474410462));
#182984=CARTESIAN_POINT('Ctrl Pts',(120.440993088202,-3.61981650902956,
126.121447250087));
#182985=CARTESIAN_POINT('Ctrl Pts',(120.448394909877,-3.49265330391212,
126.028451964632));
#182986=CARTESIAN_POINT('Ctrl Pts',(120.455792824189,-3.36555722726127,
125.935505770664));
#182987=CARTESIAN_POINT('Ctrl Pts',(120.4631907385,-3.23467985735817,125.847586381291));
#182988=CARTESIAN_POINT('Ctrl Pts',(120.470588652811,-3.10046046151212,
125.765007932042));
#182989=CARTESIAN_POINT('Ctrl Pts',(120.477985337723,-2.96626337049419,
125.682443205833));
#182990=CARTESIAN_POINT('Ctrl Pts',(120.485382022635,-2.82872567343642,
125.605217853611));
#182991=CARTESIAN_POINT('Ctrl Pts',(120.492778707548,-2.68831525070869,
125.533602448639));
#182992=CARTESIAN_POINT('Ctrl Pts',(120.500175064483,-2.54791105392604,
125.461990219169));
#182993=CARTESIAN_POINT('Ctrl Pts',(120.507571421418,-2.40463471728811,
125.395987611958));
#182994=CARTESIAN_POINT('Ctrl Pts',(120.514967778354,-2.25897808553035,
125.335818894986));
#182995=CARTESIAN_POINT('Ctrl Pts',(120.52236526769,-2.11329915337054,125.275640966031));
#182996=CARTESIAN_POINT('Ctrl Pts',(120.529762757027,-1.96523954550562,
125.221298848294));
#182997=CARTESIAN_POINT('Ctrl Pts',(120.537160246363,-1.81531026757037,
125.172968321255));
#182998=CARTESIAN_POINT('Ctrl Pts',(120.544560328878,-1.66532843215927,
125.124620852024));
#182999=CARTESIAN_POINT('Ctrl Pts',(120.551960411393,-1.513475976834,125.082289283677));
#183000=CARTESIAN_POINT('Ctrl Pts',(120.559360493908,-1.36027806417806,
125.046099234942));
#183001=CARTESIAN_POINT('Ctrl Pts',(120.566768713574,-1.20691169466769,
125.009869391529));
#183002=CARTESIAN_POINT('Ctrl Pts',(120.574176933241,-1.05219727675213,
124.979794640251));
#183003=CARTESIAN_POINT('Ctrl Pts',(120.581585152907,-0.896669865831108,
124.955949404748));
#183004=CARTESIAN_POINT('Ctrl Pts',(120.588997932209,-0.74104673038411,
124.932089492902));
#183005=CARTESIAN_POINT('Ctrl Pts',(120.596410711511,-0.584609974946085,
124.914466778572));
#183006=CARTESIAN_POINT('Ctrl Pts',(120.603823490813,-0.427898218953112,
124.903103660212));
#183007=CARTESIAN_POINT('Ctrl Pts',(120.611246861842,-0.270962545854011,
124.891724305696));
#183008=CARTESIAN_POINT('Ctrl Pts',(120.618670232871,-0.113751459536328,
124.886622422408));
#183009=CARTESIAN_POINT('Ctrl Pts',(120.626093603899,0.0431971480589227,
124.887768307046));
#183010=CARTESIAN_POINT('Ctrl Pts',(120.630029653341,0.126415065745407,
124.888375882577));
#183011=CARTESIAN_POINT('Ctrl Pts',(120.633965702782,0.209559276287754,
124.890739062768));
#183012=CARTESIAN_POINT('Ctrl Pts',(120.637901752223,0.292550489865668,
124.89484754343));
#183013=CARTESIAN_POINT('Ctrl Pts',(120.645325018628,0.449069328589629,
124.902596009737));
#183014=CARTESIAN_POINT('Ctrl Pts',(120.652748285034,0.605516791442864,
124.91657880376));
#183015=CARTESIAN_POINT('Ctrl Pts',(120.660171551439,0.761355853315115,
124.936799980715));
#183016=CARTESIAN_POINT('Ctrl Pts',(120.66758604416,0.917010726358304,124.956997257918));
#183017=CARTESIAN_POINT('Ctrl Pts',(120.675000536881,1.07205826317264,124.983418193991));
#183018=CARTESIAN_POINT('Ctrl Pts',(120.682415029602,1.22596249506846,125.016014867424));
#183019=CARTESIAN_POINT('Ctrl Pts',(120.689822375956,1.37971838827108,125.048580122956));
#183020=CARTESIAN_POINT('Ctrl Pts',(120.69722972231,1.53233280759622,125.087309188948));
#183021=CARTESIAN_POINT('Ctrl Pts',(120.704637068663,1.68327606900739,125.132102492444));
#183022=CARTESIAN_POINT('Ctrl Pts',(120.712038890339,1.83410675123923,125.176862387406));
#183023=CARTESIAN_POINT('Ctrl Pts',(120.719440712014,1.98326840100057,125.227677408351));
#183024=CARTESIAN_POINT('Ctrl Pts',(120.72684253369,2.13024278691824,125.284397190941));
#183025=CARTESIAN_POINT('Ctrl Pts',(120.734240448001,2.27713958620143,125.341087031599));
#183026=CARTESIAN_POINT('Ctrl Pts',(120.741638362312,2.42185107377855,125.403675292032));
#183027=CARTESIAN_POINT('Ctrl Pts',(120.749036276624,2.56387552382144,125.471962202139));
#183028=CARTESIAN_POINT('Ctrl Pts',(120.756432961536,2.70587637197733,125.5402377642));
#183029=CARTESIAN_POINT('Ctrl Pts',(120.763829646448,2.84519073274181,125.614209934796));
#183030=CARTESIAN_POINT('Ctrl Pts',(120.77122633136,2.98133806439828,125.693631324376));
#183031=CARTESIAN_POINT('Ctrl Pts',(120.778622688295,3.11747935913958,125.773049192329));
#183032=CARTESIAN_POINT('Ctrl Pts',(120.786019045231,3.25045358154954,125.857915610738));
#183033=CARTESIAN_POINT('Ctrl Pts',(120.793415402166,3.37980619453057,125.947937999021));
#183034=CARTESIAN_POINT('Ctrl Pts',(120.800812891503,3.5091786117264,126.037974169961));
#183035=CARTESIAN_POINT('Ctrl Pts',(120.808210380839,3.63492800903486,126.133167669307));
#183036=CARTESIAN_POINT('Ctrl Pts',(120.815607870176,3.75663028717459,126.233183586649));
#183037=CARTESIAN_POINT('Ctrl Pts',(120.823007952691,3.87837522785968,126.333234564416));
#183038=CARTESIAN_POINT('Ctrl Pts',(120.830408035206,3.99606993650866,126.438111089069));
#183039=CARTESIAN_POINT('Ctrl Pts',(120.837808117721,4.10932486332231,126.547439226445));
#183040=CARTESIAN_POINT('Ctrl Pts',(120.845216337387,4.22270432557088,126.656887581348));
#183041=CARTESIAN_POINT('Ctrl Pts',(120.852624557054,4.33163398757523,126.770797065199));
#183042=CARTESIAN_POINT('Ctrl Pts',(120.86003277672,4.43576202410635,126.888757748531));
#183043=CARTESIAN_POINT('Ctrl Pts',(120.867445556022,4.53995414970641,127.006791034695));
#183044=CARTESIAN_POINT('Ctrl Pts',(120.874858335325,4.63933852586753,127.128880200011));
#183045=CARTESIAN_POINT('Ctrl Pts',(120.882271114627,4.73360517117553,127.254584195604));
#183046=CARTESIAN_POINT('Ctrl Pts',(120.889694485655,4.82800650908714,127.38046780296));
#183047=CARTESIAN_POINT('Ctrl Pts',(120.897117856684,4.917275300239,127.509976249791));
#183048=CARTESIAN_POINT('Ctrl Pts',(120.904541227713,5.00114579112764,127.642640937015));
#183049=CARTESIAN_POINT('Ctrl Pts',(120.908477277154,5.04561593784276,127.712982937428));
#183050=CARTESIAN_POINT('Ctrl Pts',(120.912413326595,5.08856920412359,127.784211873135));
#183051=CARTESIAN_POINT('Ctrl Pts',(120.916349376036,5.12997140109303,127.856255465699));
#183052=CARTESIAN_POINT('Ctrl Pts',(120.923772642441,5.20805465245714,127.992127432866));
#183053=CARTESIAN_POINT('Ctrl Pts',(120.931195908846,5.28085420694602,128.131309155906));
#183054=CARTESIAN_POINT('Ctrl Pts',(120.938619175252,5.34807637760309,128.273351012325));
#183055=CARTESIAN_POINT('Ctrl Pts',(120.946033667973,5.41521909723699,128.415224987065));
#183056=CARTESIAN_POINT('Ctrl Pts',(120.953448160694,5.47679739633404,128.559952032276));
#183057=CARTESIAN_POINT('Ctrl Pts',(120.960862653415,5.53256188844834,128.707055319573));
#183058=CARTESIAN_POINT('Ctrl Pts',(120.968269999769,5.58827263264549,128.854016823183));
#183059=CARTESIAN_POINT('Ctrl Pts',(120.975677346123,5.63818059402247,129.003349662604));
#183060=CARTESIAN_POINT('Ctrl Pts',(120.983084692476,5.68208323896502,129.154554378042));
#183061=CARTESIAN_POINT('Ctrl Pts',(120.990486514152,5.72595313965853,129.305646319298));
#183062=CARTESIAN_POINT('Ctrl Pts',(120.997888335827,5.76382653855316,129.458606999766));
#183063=CARTESIAN_POINT('Ctrl Pts',(121.005290157503,5.79554982470989,129.612919141116));
#183064=CARTESIAN_POINT('Ctrl Pts',(121.012688071814,5.82725636439077,129.767149822288));
#183065=CARTESIAN_POINT('Ctrl Pts',(121.020085986125,5.85281918210673,129.922730178796));
#183066=CARTESIAN_POINT('Ctrl Pts',(121.027483900437,5.87213515503615,130.079130113872));
#183067=CARTESIAN_POINT('Ctrl Pts',(121.034880585349,5.89144791800142,130.235504058116));
#183068=CARTESIAN_POINT('Ctrl Pts',(121.042277270261,5.90451585081448,130.392696940494));
#183069=CARTESIAN_POINT('Ctrl Pts',(121.049673955173,5.91128734477379,130.550170747553));
#183070=CARTESIAN_POINT('Ctrl Pts',(121.057070312109,5.91805853847797,130.707637572059));
#183071=CARTESIAN_POINT('Ctrl Pts',(121.064466669044,5.91853383241655,130.865384923527));
#183072=CARTESIAN_POINT('Ctrl Pts',(121.07186302598,5.91271369451713,131.022872240071));
#183073=CARTESIAN_POINT('Ctrl Pts',(121.079260515317,5.90689266553974,131.180383668325));
#183074=CARTESIAN_POINT('Ctrl Pts',(121.086658004653,5.89477429936458,131.337634609316));
#183075=CARTESIAN_POINT('Ctrl Pts',(121.09405549399,5.87641112958486,131.494087229051));
#183076=CARTESIAN_POINT('Ctrl Pts',(121.101455576505,5.8580415226243,131.650594693011));
#183077=CARTESIAN_POINT('Ctrl Pts',(121.10885565902,5.83342279705357,131.806302908013));
#183078=CARTESIAN_POINT('Ctrl Pts',(121.116255741535,5.80265899309267,131.960682014229));
#183079=CARTESIAN_POINT('Ctrl Pts',(121.123663961202,5.77186136116694,132.115230876142));
#183080=CARTESIAN_POINT('Ctrl Pts',(121.131072180868,5.73490522938715,132.26844734425));
#183081=CARTESIAN_POINT('Ctrl Pts',(121.138480400535,5.69194531289289,132.419813841134));
#183082=CARTESIAN_POINT('Ctrl Pts',(121.145893179837,5.64895895528682,132.571273501572));
#183083=CARTESIAN_POINT('Ctrl Pts',(121.153305959139,5.59996156567458,132.720880567995));
#183084=CARTESIAN_POINT('Ctrl Pts',(121.160718738441,5.54515665844007,132.868135846572));
#183085=CARTESIAN_POINT('Ctrl Pts',(121.16814210947,5.49027344338409,133.015601530396));
#183086=CARTESIAN_POINT('Ctrl Pts',(121.175565480498,5.42956628132339,133.160708371548));
#183087=CARTESIAN_POINT('Ctrl Pts',(121.182988851527,5.36328577167897,133.302979494827));
#183088=CARTESIAN_POINT('Ctrl Pts',(121.186924900968,5.32814225508741,133.378415058137));
#183089=CARTESIAN_POINT('Ctrl Pts',(121.190860950409,5.29143262378694,133.453053837168));
#183090=CARTESIAN_POINT('Ctrl Pts',(121.194796999849,5.25319920775148,133.526827999589));
#183091=CARTESIAN_POINT('Ctrl Pts',(121.202220266255,5.18109217833081,133.665963767506));
#183092=CARTESIAN_POINT('Ctrl Pts',(121.20964353266,5.10334459033582,133.802443215493));
#183093=CARTESIAN_POINT('Ctrl Pts',(121.217066799066,5.0201759789293,133.935776224457));
#183094=CARTESIAN_POINT('Ctrl Pts',(121.224481291787,4.93710566591456,134.068951644878));
#183095=CARTESIAN_POINT('Ctrl Pts',(121.231895784508,4.84862727869129,134.198987714987));
#183096=CARTESIAN_POINT('Ctrl Pts',(121.239310277229,4.75500718701793,134.325416881517));
#183097=CARTESIAN_POINT('Ctrl Pts',(121.246717623582,4.66147732991412,134.451724190855));
#183098=CARTESIAN_POINT('Ctrl Pts',(121.254124969936,4.56281585497749,134.574431219593));
#183099=CARTESIAN_POINT('Ctrl Pts',(121.26153231629,4.45933349751323,134.693097600245));
#183100=CARTESIAN_POINT('Ctrl Pts',(121.268934137965,4.35592832109475,134.811675475034));
#183101=CARTESIAN_POINT('Ctrl Pts',(121.276335959641,4.2477096657567,134.92621842222));
#183102=CARTESIAN_POINT('Ctrl Pts',(121.283737781316,4.13502970194288,135.036317602998));
#183103=CARTESIAN_POINT('Ctrl Pts',(121.291135695627,4.02240922100567,135.146358663275));
#183104=CARTESIAN_POINT('Ctrl Pts',(121.298533609938,3.9053323881929,135.25196036875));
#183105=CARTESIAN_POINT('Ctrl Pts',(121.30593152425,3.78418944852479,135.352749429022));
#183106=CARTESIAN_POINT('Ctrl Pts',(121.313328209162,3.66306664061498,135.45352173998));
#183107=CARTESIAN_POINT('Ctrl Pts',(121.320724894074,3.53787935362518,135.549482754533));
#183108=CARTESIAN_POINT('Ctrl Pts',(121.328121578986,3.40905233774438,135.640298243406));
#183109=CARTESIAN_POINT('Ctrl Pts',(121.335517935922,3.28023103418856,135.731109705426));
#183110=CARTESIAN_POINT('Ctrl Pts',(121.342914292857,3.1477706277457,135.816775880339));
#183111=CARTESIAN_POINT('Ctrl Pts',(121.350310649792,3.01212616136603,135.897004974922));
#183112=CARTESIAN_POINT('Ctrl Pts',(121.357708139129,2.87646092747217,135.977246352785));
#183113=CARTESIAN_POINT('Ctrl Pts',(121.365105628466,2.73761098431293,136.052048802786));
#183114=CARTESIAN_POINT('Ctrl Pts',(121.372503117802,2.59605722255035,136.121165810513));
#183115=CARTESIAN_POINT('Ctrl Pts',(121.379903200317,2.4544538393353,136.1903070471));
#183116=CARTESIAN_POINT('Ctrl Pts',(121.387303282832,2.31014508565248,136.253758709631));
#183117=CARTESIAN_POINT('Ctrl Pts',(121.394703365347,2.16363298386153,136.311321927912));
#183118=CARTESIAN_POINT('Ctrl Pts',(121.402111585013,2.0169597769537,136.368948442868));
#183119=CARTESIAN_POINT('Ctrl Pts',(121.40951980468,1.86807873108844,136.420673446083));
#183120=CARTESIAN_POINT('Ctrl Pts',(121.416928024346,1.71750892611891,136.466347340546));
#183121=CARTESIAN_POINT('Ctrl Pts',(121.424340803648,1.5668464479467,136.512049346529));
#183122=CARTESIAN_POINT('Ctrl Pts',(121.43175358295,1.41449349995957,136.551692728728));
#183123=CARTESIAN_POINT('Ctrl Pts',(121.439166362252,1.26098007256295,136.585178883097));
#183124=CARTESIAN_POINT('Ctrl Pts',(121.446589733281,1.10724729798208,136.618712884054));
#183125=CARTESIAN_POINT('Ctrl Pts',(121.45401310431,0.952351098933248,136.64607202137));
#183126=CARTESIAN_POINT('Ctrl Pts',(121.461436475339,0.796828139136472,
136.667209368743));
#183127=CARTESIAN_POINT('Ctrl Pts',(121.465372524779,0.714366134128753,
136.678416897504));
#183128=CARTESIAN_POINT('Ctrl Pts',(121.46930857422,0.631727963045877,136.687876128241));
#183129=CARTESIAN_POINT('Ctrl Pts',(121.473244623661,0.54899357553466,136.695586009326));
#183130=CARTESIAN_POINT('Ctrl Pts',(121.480667890067,0.392959102742847,
136.710126604437));
#183131=CARTESIAN_POINT('Ctrl Pts',(121.488091156472,0.236110607450815,
136.718485832063));
#183132=CARTESIAN_POINT('Ctrl Pts',(121.495514422877,0.078979104850994,
136.720583472014));
#183133=CARTESIAN_POINT('Ctrl Pts',(121.502928915598,-0.0779666813618246,
136.722678632729));
#183134=CARTESIAN_POINT('Ctrl Pts',(121.510343408319,-0.23519443945632,
136.718526931922));
#183135=CARTESIAN_POINT('Ctrl Pts',(121.51775790104,-0.392166824264851,
136.708099750052));
#183136=CARTESIAN_POINT('Ctrl Pts',(121.525165247394,-0.548987913178997,
136.697682618292));
#183137=CARTESIAN_POINT('Ctrl Pts',(121.532572593748,-0.705553748843742,
136.681002071509));
#183138=CARTESIAN_POINT('Ctrl Pts',(121.539979940102,-0.861325877599658,
136.658081510731));
#183139=CARTESIAN_POINT('Ctrl Pts',(121.547381761777,-1.01698182562545,
136.635178044972));
#183140=CARTESIAN_POINT('Ctrl Pts',(121.554783583453,-1.17184487771584,
136.606043886146));
#183141=CARTESIAN_POINT('Ctrl Pts',(121.562185405128,-1.32538070947762,
136.57075433786));
#183142=CARTESIAN_POINT('Ctrl Pts',(121.569583319439,-1.47883549086751,
136.535483418652));
#183143=CARTESIAN_POINT('Ctrl Pts',(121.576981233751,-1.63096408437483,
136.494063664693));
#183144=CARTESIAN_POINT('Ctrl Pts',(121.584379148062,-1.78124149324664,
136.44662162759));
#183145=CARTESIAN_POINT('Ctrl Pts',(121.591775832974,-1.93149392874036,
136.399187474493));
#183146=CARTESIAN_POINT('Ctrl Pts',(121.599172517886,-2.07989543452824,
136.345733136804));
#183147=CARTESIAN_POINT('Ctrl Pts',(121.606569202799,-2.2259352262042,136.286435309801));
#183148=CARTESIAN_POINT('Ctrl Pts',(121.613965559734,-2.37196854232265,
136.227140112126));
#183149=CARTESIAN_POINT('Ctrl Pts',(121.621361916669,-2.5156400066765,136.162002080765));
#183150=CARTESIAN_POINT('Ctrl Pts',(121.628758273605,-2.6564581635341,136.091246334876));
#183151=CARTESIAN_POINT('Ctrl Pts',(121.636155762941,-2.7972978800106,136.020479756102));
#183152=CARTESIAN_POINT('Ctrl Pts',(121.643553252278,-2.93528308558697,
135.944093917864));
#183153=CARTESIAN_POINT('Ctrl Pts',(121.650950741615,-3.06994644755794,
135.862360160036));
#183154=CARTESIAN_POINT('Ctrl Pts',(121.65835082413,-3.20465701556178,135.780597750566));
#183155=CARTESIAN_POINT('Ctrl Pts',(121.665750906645,-3.33604310259594,
135.693483882548));
#183156=CARTESIAN_POINT('Ctrl Pts',(121.67315098916,-3.46366603818448,135.601333427415));
#183157=CARTESIAN_POINT('Ctrl Pts',(121.680559208826,-3.59142930831138,
135.509081643382));
#183158=CARTESIAN_POINT('Ctrl Pts',(121.687967428493,-3.71542086035615,
135.411782430656));
#183159=CARTESIAN_POINT('Ctrl Pts',(121.695375648159,-3.83523425877866,
135.309791644981));
#183160=CARTESIAN_POINT('Ctrl Pts',(121.702788427461,-3.95512140034852,
135.207738085679));
#183161=CARTESIAN_POINT('Ctrl Pts',(121.710201206763,-4.07082499036623,
135.1009874521));
#183162=CARTESIAN_POINT('Ctrl Pts',(121.717613986065,-4.18197559769595,
134.989932342286));
#183163=CARTESIAN_POINT('Ctrl Pts',(121.725037357094,-4.29328502222603,
134.878718551723));
#183164=CARTESIAN_POINT('Ctrl Pts',(121.732460728123,-4.4000282184377,134.763188274579));
#183165=CARTESIAN_POINT('Ctrl Pts',(121.739884099152,-4.50187562605314,
134.643767656426));
#183166=CARTESIAN_POINT('Ctrl Pts',(121.743820148593,-4.5558775653682,134.58044797922));
#183167=CARTESIAN_POINT('Ctrl Pts',(121.747756198034,-4.60850383410758,
134.51603509072));
#183168=CARTESIAN_POINT('Ctrl Pts',(121.751692247475,-4.65971033277122,
134.450595686396));
#183169=CARTESIAN_POINT('Ctrl Pts',(121.759397770821,-4.75995624605906,
134.322486305309));
#183170=CARTESIAN_POINT('Ctrl Pts',(121.767103294168,-4.855078114618,134.190031390031));
#183171=CARTESIAN_POINT('Ctrl Pts',(121.774808817515,-4.94467841284417,
134.05368146292));
#183172=CARTESIAN_POINT('Ctrl Pts',(121.782221809932,-5.03087714347355,
133.92250789686));
#183173=CARTESIAN_POINT('Ctrl Pts',(121.789634802349,-5.11196556567067,
133.787729956513));
#183174=CARTESIAN_POINT('Ctrl Pts',(121.797047794766,-5.18762905297334,
133.649784201366));
#183175=CARTESIAN_POINT('Ctrl Pts',(121.804453731265,-5.26322052139986,
133.511969747308));
#183176=CARTESIAN_POINT('Ctrl Pts',(121.811859667764,-5.33339715386406,
133.370993803931));
#183177=CARTESIAN_POINT('Ctrl Pts',(121.819265604263,-5.39788738894737,
133.22732209038));
#183178=CARTESIAN_POINT('Ctrl Pts',(121.826665950708,-5.46232894634043,
133.083758821266));
#183179=CARTESIAN_POINT('Ctrl Pts',(121.834066297153,-5.52109249856701,
132.937504171086));
#183180=CARTESIAN_POINT('Ctrl Pts',(121.841466643598,-5.5739523158509,132.789048538404));
#183181=CARTESIAN_POINT('Ctrl Pts',(121.848862862064,-5.62678264746364,
132.64067571558));
#183182=CARTESIAN_POINT('Ctrl Pts',(121.856259080531,-5.67371567677217,
132.490104705223));
#183183=CARTESIAN_POINT('Ctrl Pts',(121.863655298998,-5.71457379272419,
132.337845840843));
#183184=CARTESIAN_POINT('Ctrl Pts',(121.871049372158,-5.75542005759352,
132.185631139841));
#183185=CARTESIAN_POINT('Ctrl Pts',(121.878443445317,-5.79019481915347,
132.031729918762));
#183186=CARTESIAN_POINT('Ctrl Pts',(121.885837518477,-5.81877034216444,
131.876667601432));
#183187=CARTESIAN_POINT('Ctrl Pts',(121.893230393674,-5.84734123546433,
131.721630406781));
#183188=CARTESIAN_POINT('Ctrl Pts',(121.90062326887,-5.86971482614708,131.565432857629));
#183189=CARTESIAN_POINT('Ctrl Pts',(121.908016144067,-5.8858145526158,131.408610247037));
#183190=CARTESIAN_POINT('Ctrl Pts',(121.915410427234,-5.9019173452718,131.251757769634));
#183191=CARTESIAN_POINT('Ctrl Pts',(121.922804710401,-5.91174385098551,
131.094280364091));
#183192=CARTESIAN_POINT('Ctrl Pts',(121.930198993569,-5.91526939587632,
130.93671822675));
#183193=CARTESIAN_POINT('Ctrl Pts',(121.932340931644,-5.916290657663,130.891076433814));
#183194=CARTESIAN_POINT('Ctrl Pts',(121.93448286972,-5.91678353011378,130.845427540589));
#183195=CARTESIAN_POINT('Ctrl Pts',(121.936624807795,-5.91674823051506,
130.799784680839));
#183196=CARTESIAN_POINT('',(123.686624807795,-5.92584126535119,130.802516799045));
#183197=CARTESIAN_POINT('Ctrl Pts',(121.936626891659,-5.91105546203302,
130.799744720898));
#183198=CARTESIAN_POINT('Ctrl Pts',(121.967797884869,-5.91580744003664,
130.136152748363));
#183199=CARTESIAN_POINT('Ctrl Pts',(122.091784752684,-5.50598867124265,
127.502332575195));
#183200=CARTESIAN_POINT('Ctrl Pts',(122.308587495099,-1.63160081265663,
123.998815869465));
#183201=CARTESIAN_POINT('Ctrl Pts',(122.587035118914,4.84377744631919,125.753085473515));
#183202=CARTESIAN_POINT('Ctrl Pts',(122.865482742726,6.86796086381084,132.14923016645));
#183203=CARTESIAN_POINT('Ctrl Pts',(123.143930366539,2.58082376599965,137.309505444483));
#183204=CARTESIAN_POINT('Ctrl Pts',(123.417644388228,-3.96476507443635,
136.505770194011));
#183205=CARTESIAN_POINT('Ctrl Pts',(123.598542535314,-5.91824650158347,
132.665654016414));
#183206=CARTESIAN_POINT('Ctrl Pts',(123.686624807795,-5.92584126535119,
130.802516799045));
#183207=CARTESIAN_POINT('',(125.436624807795,-5.91667608508364,130.809827719978));
#183208=CARTESIAN_POINT('Ctrl Pts',(123.686624807795,-5.92584126535119,
130.802516799045));
#183209=CARTESIAN_POINT('Ctrl Pts',(123.691358409918,-5.92624941319846,
130.702390518927));
#183210=CARTESIAN_POINT('Ctrl Pts',(123.696092012042,-5.92393242245176,
130.602283526104));
#183211=CARTESIAN_POINT('Ctrl Pts',(123.793641488769,-5.81880593488637,
128.542219269167));
#183212=CARTESIAN_POINT('Ctrl Pts',(123.979273237977,-3.47781303298138,
124.731274331503));
#183213=CARTESIAN_POINT('Ctrl Pts',(124.257720861791,3.22961659657427,124.595726535137));
#183214=CARTESIAN_POINT('Ctrl Pts',(124.536168485603,6.96918634942095,130.16561015189));
#183215=CARTESIAN_POINT('Ctrl Pts',(124.814616109416,4.30441431082963,136.322474241898));
#183216=CARTESIAN_POINT('Ctrl Pts',(125.093063733229,-2.31590419708269,
137.408461485986));
#183217=CARTESIAN_POINT('Ctrl Pts',(125.300399966022,-5.66080020113054,
133.698150859813));
#183218=CARTESIAN_POINT('Ctrl Pts',(125.414920324211,-5.92093715202594,
131.270777417702));
#183219=CARTESIAN_POINT('Ctrl Pts',(125.436624807795,-5.91667608508364,
130.809827719978));
#183220=CARTESIAN_POINT('',(127.186624807795,-5.90699143088146,130.803749018818));
#183221=CARTESIAN_POINT('Ctrl Pts',(125.436624807795,-5.91667608508364,
130.809827719978));
#183222=CARTESIAN_POINT('Ctrl Pts',(125.507736198815,-5.90271535681672,
129.299597169321));
#183223=CARTESIAN_POINT('Ctrl Pts',(125.671663464439,-4.54509055714801,
125.795879117947));
#183224=CARTESIAN_POINT('Ctrl Pts',(125.928406604669,1.35531985884536,123.938454369257));
#183225=CARTESIAN_POINT('Ctrl Pts',(126.206854228481,6.50906486850591,128.23343956317));
#183226=CARTESIAN_POINT('Ctrl Pts',(126.485301852293,5.68129724950531,134.890975609601));
#183227=CARTESIAN_POINT('Ctrl Pts',(126.763749476106,-0.367304994988542,
137.793112120586));
#183228=CARTESIAN_POINT('Ctrl Pts',(126.997523794607,-5.16210537323063,
134.837695341821));
#183229=CARTESIAN_POINT('Ctrl Pts',(127.138482238503,-5.90604835788347,
131.830411623805));
#183230=CARTESIAN_POINT('Ctrl Pts',(127.186624807795,-5.90699143088146,
130.803749018818));
#183231=CARTESIAN_POINT('',(128.936624084929,-5.91831124264779,130.799118091926));
#183232=CARTESIAN_POINT('Ctrl Pts',(127.186624807795,-5.90699143088146,
130.803749018818));
#183233=CARTESIAN_POINT('Ctrl Pts',(127.231298113108,-5.90786654387585,
129.851070076254));
#183234=CARTESIAN_POINT('Ctrl Pts',(127.368787293024,-5.23971675382112,
126.920207720007));
#183235=CARTESIAN_POINT('Ctrl Pts',(127.599092347546,-0.628143810757646,
123.834210268875));
#183236=CARTESIAN_POINT('Ctrl Pts',(127.877539971358,5.52465782028921,126.508348920764));
#183237=CARTESIAN_POINT('Ctrl Pts',(128.155987595171,6.60056880902916,133.130312450174));
#183238=CARTESIAN_POINT('Ctrl Pts',(128.434435218984,1.61087951798409,137.614839874481));
#183239=CARTESIAN_POINT('Ctrl Pts',(128.694647287185,-4.43540799159065,
135.957047019246));
#183240=CARTESIAN_POINT('Ctrl Pts',(128.862043480784,-5.90429634502181,
132.381480787606));
#183241=CARTESIAN_POINT('Ctrl Pts',(128.936623799777,-5.9189280327544,130.799123593926));
#183242=CARTESIAN_POINT('',(130.686626174971,-5.92114659639425,130.807384154776));
#183243=CARTESIAN_POINT('Ctrl Pts',(128.936624807795,-5.91674766505958,
130.799104144226));
#183244=CARTESIAN_POINT('Ctrl Pts',(128.947379588894,-5.91654502312587,
130.571008021481));
#183245=CARTESIAN_POINT('Ctrl Pts',(128.958134369993,-5.90314918816152,
130.343473921271));
#183246=CARTESIAN_POINT('Ctrl Pts',(128.968889151092,-5.87677360007643,
130.117729263822));
#183247=CARTESIAN_POINT('Ctrl Pts',(128.976369589598,-5.85842818114997,
129.960713606087));
#183248=CARTESIAN_POINT('Ctrl Pts',(128.983850028104,-5.8338043041974,129.804562724547));
#183249=CARTESIAN_POINT('Ctrl Pts',(128.99133046661,-5.80298603825706,129.649681613559));
#183250=CARTESIAN_POINT('Ctrl Pts',(128.998753733015,-5.77240331265216,
129.495984240453));
#183251=CARTESIAN_POINT('Ctrl Pts',(129.006176999421,-5.73566390235169,
129.343270315442));
#183252=CARTESIAN_POINT('Ctrl Pts',(129.013600265826,-5.69284242803125,
129.192071669484));
#183253=CARTESIAN_POINT('Ctrl Pts',(129.021014758547,-5.65007156513736,
129.04105172777));
#183254=CARTESIAN_POINT('Ctrl Pts',(129.028429251268,-5.60123304769037,
128.891543855909));
#183255=CARTESIAN_POINT('Ctrl Pts',(129.035843743989,-5.54645275821413,
128.744071229301));
#183256=CARTESIAN_POINT('Ctrl Pts',(129.043251090343,-5.49172526804333,
128.596740742362));
#183257=CARTESIAN_POINT('Ctrl Pts',(129.050658436697,-5.43106753609541,
128.45144194301));
#183258=CARTESIAN_POINT('Ctrl Pts',(129.05806578305,-5.36465561944204,128.308684226828));
#183259=CARTESIAN_POINT('Ctrl Pts',(129.065467604726,-5.29829323530168,
128.166032984736));
#183260=CARTESIAN_POINT('Ctrl Pts',(129.072869426401,-5.22618536856474,
128.025919389152));
#183261=CARTESIAN_POINT('Ctrl Pts',(129.080271248076,-5.14855664335168,
127.888834069462));
#183262=CARTESIAN_POINT('Ctrl Pts',(129.087669162388,-5.07096889773812,
127.751821116045));
#183263=CARTESIAN_POINT('Ctrl Pts',(129.095067076699,-4.98786628133185,
127.617833578836));
#183264=CARTESIAN_POINT('Ctrl Pts',(129.10246499101,-4.89951987476105,127.48733852549));
#183265=CARTESIAN_POINT('Ctrl Pts',(129.109861675922,-4.81118814976063,
127.356865158054));
#183266=CARTESIAN_POINT('Ctrl Pts',(129.117258360835,-4.71761457318377,
127.2298834314));
#183267=CARTESIAN_POINT('Ctrl Pts',(129.124655045747,-4.61911423006035,
127.10683248486));
#183268=CARTESIAN_POINT('Ctrl Pts',(129.132051402682,-4.52061825454543,
126.983786994528));
#183269=CARTESIAN_POINT('Ctrl Pts',(129.139447759617,-4.41719618013541,
126.864672229181));
#183270=CARTESIAN_POINT('Ctrl Pts',(129.146844116553,-4.30920398819393,
126.749894986853));
#183271=CARTESIAN_POINT('Ctrl Pts',(129.154241605889,-4.20119526237202,
126.635100171836));
#183272=CARTESIAN_POINT('Ctrl Pts',(129.161639095226,-4.08861528164914,
126.524644474013));
#183273=CARTESIAN_POINT('Ctrl Pts',(129.169036584562,-3.97185744423585,
126.418898383643));
#183274=CARTESIAN_POINT('Ctrl Pts',(129.176436667077,-3.8550586775434,126.313115224144));
#183275=CARTESIAN_POINT('Ctrl Pts',(129.183836749592,-3.7340794147835,126.212045209555));
#183276=CARTESIAN_POINT('Ctrl Pts',(129.191236832107,-3.60934659853295,
126.116018939087));
#183277=CARTESIAN_POINT('Ctrl Pts',(129.198645051773,-3.48447662572835,
126.019887077865));
#183278=CARTESIAN_POINT('Ctrl Pts',(129.20605327144,-3.35584515268553,125.92881026458));
#183279=CARTESIAN_POINT('Ctrl Pts',(129.213461491106,-3.22390920563638,
125.843076509967));
#183280=CARTESIAN_POINT('Ctrl Pts',(129.220874270408,-3.0918920542133,125.757289987659));
#183281=CARTESIAN_POINT('Ctrl Pts',(129.22828704971,-2.95656669623262,125.676853267191));
#183282=CARTESIAN_POINT('Ctrl Pts',(129.235699829012,-2.81841481509146,
125.602008409903));
#183283=CARTESIAN_POINT('Ctrl Pts',(129.243123200041,-2.68006553606374,
125.527056610774));
#183284=CARTESIAN_POINT('Ctrl Pts',(129.250546571069,-2.5388820019244,125.457712796615));
#183285=CARTESIAN_POINT('Ctrl Pts',(129.257969942098,-2.39536667341973,
125.394171243582));
#183286=CARTESIAN_POINT('Ctrl Pts',(129.261905991539,-2.31927140263232,
125.3604799875));
#183287=CARTESIAN_POINT('Ctrl Pts',(129.265842040981,-2.24252086008494,
125.328419129956));
#183288=CARTESIAN_POINT('Ctrl Pts',(129.269778090422,-2.16519155121374,
125.298011908208));
#183289=CARTESIAN_POINT('Ctrl Pts',(129.277201356828,-2.01935088806817,
125.240664836975));
#183290=CARTESIAN_POINT('Ctrl Pts',(129.284624623233,-1.87100978919444,
125.189029136661));
#183291=CARTESIAN_POINT('Ctrl Pts',(129.292047889638,-1.72065603333818,
125.143329494402));
#183292=CARTESIAN_POINT('Ctrl Pts',(129.299462382359,-1.57047998313492,
125.097683865324));
#183293=CARTESIAN_POINT('Ctrl Pts',(129.30687687508,-1.41829636462693,125.057960436557));
#183294=CARTESIAN_POINT('Ctrl Pts',(129.314291367801,-1.26461338267296,
125.024336088651));
#183295=CARTESIAN_POINT('Ctrl Pts',(129.321698714155,-1.11107852616328,
124.990744149157));
#183296=CARTESIAN_POINT('Ctrl Pts',(129.329106060509,-0.956047545426268,
124.963239666791));
#183297=CARTESIAN_POINT('Ctrl Pts',(129.336513406863,-0.800044172539664,
124.941949860507));
#183298=CARTESIAN_POINT('Ctrl Pts',(129.343915228538,-0.644157152854006,
124.920675932963));
#183299=CARTESIAN_POINT('Ctrl Pts',(129.351317050214,-0.487299553360572,
124.905607502572));
#183300=CARTESIAN_POINT('Ctrl Pts',(129.358718871889,-0.330005569281536,
124.896820783867));
#183301=CARTESIAN_POINT('Ctrl Pts',(129.3661167862,-0.172794619472546,124.888038703602));
#183302=CARTESIAN_POINT('Ctrl Pts',(129.373514700512,-0.0151481156323031,
124.885531751684));
#183303=CARTESIAN_POINT('Ctrl Pts',(129.380912614823,0.142394459293183,
124.88932432178));
#183304=CARTESIAN_POINT('Ctrl Pts',(129.388309299735,0.29991085350083,124.89311626162));
#183305=CARTESIAN_POINT('Ctrl Pts',(129.395705984648,0.457322980247357,
124.903205636778));
#183306=CARTESIAN_POINT('Ctrl Pts',(129.40310266956,0.614091068019229,124.919564722832));
#183307=CARTESIAN_POINT('Ctrl Pts',(129.410499026495,0.770852204529808,
124.935923083507));
#183308=CARTESIAN_POINT('Ctrl Pts',(129.417895383431,0.926968987565892,
124.958550563564));
#183309=CARTESIAN_POINT('Ctrl Pts',(129.425291740366,1.08190674979855,124.987367550075));
#183310=CARTESIAN_POINT('Ctrl Pts',(129.432689229703,1.23686823339825,125.01618894854));
#183311=CARTESIAN_POINT('Ctrl Pts',(129.44008671904,1.39064996974529,125.05120167205));
#183312=CARTESIAN_POINT('Ctrl Pts',(129.447484208376,1.54272761355005,125.092275002583));
#183313=CARTESIAN_POINT('Ctrl Pts',(129.454884290891,1.6948585679371,125.13336273131));
#183314=CARTESIAN_POINT('Ctrl Pts',(129.462284373406,1.84528388026811,125.180515199723));
#183315=CARTESIAN_POINT('Ctrl Pts',(129.469684455921,1.99349463516965,125.233551905893));
#183316=CARTESIAN_POINT('Ctrl Pts',(129.477092675588,2.14186836303254,125.286646931374));
#183317=CARTESIAN_POINT('Ctrl Pts',(129.484500895254,2.28802231865685,125.345638990424));
#183318=CARTESIAN_POINT('Ctrl Pts',(129.491909114921,2.43146715661416,125.410299250766));
#183319=CARTESIAN_POINT('Ctrl Pts',(129.499321894223,2.57500028247584,125.474999308419));
#183320=CARTESIAN_POINT('Ctrl Pts',(129.506734673525,2.71582063498677,125.545374352514));
#183321=CARTESIAN_POINT('Ctrl Pts',(129.514147452827,2.85346419944377,125.621149969233));
#183322=CARTESIAN_POINT('Ctrl Pts',(129.521570823856,2.9913044354806,125.697033857707));
#183323=CARTESIAN_POINT('Ctrl Pts',(129.528994194885,3.12595849905387,125.778333538135));
#183324=CARTESIAN_POINT('Ctrl Pts',(129.536417565913,3.25699134782469,125.86473128707));
#183325=CARTESIAN_POINT('Ctrl Pts',(129.540353615354,3.32646810833134,125.91054144664));
#183326=CARTESIAN_POINT('Ctrl Pts',(129.544289664795,3.39492735876577,125.957784175133));
#183327=CARTESIAN_POINT('Ctrl Pts',(129.548225714235,3.46230819590717,126.006407666666));
#183328=CARTESIAN_POINT('Ctrl Pts',(129.555648980641,3.5893863518749,126.098110054211));
#183329=CARTESIAN_POINT('Ctrl Pts',(129.563072247046,3.7130109163222,126.19500326464));
#183330=CARTESIAN_POINT('Ctrl Pts',(129.570495513452,3.83272919727131,126.296798364764));
#183331=CARTESIAN_POINT('Ctrl Pts',(129.577910006173,3.95230598115442,126.398473151534));
#183332=CARTESIAN_POINT('Ctrl Pts',(129.585324498894,4.06798538989691,126.505038056301));
#183333=CARTESIAN_POINT('Ctrl Pts',(129.592738991615,4.17934391174314,126.616161120183));
#183334=CARTESIAN_POINT('Ctrl Pts',(129.600146337969,4.29059510205344,126.727177079473));
#183335=CARTESIAN_POINT('Ctrl Pts',(129.607553684322,4.39753343396602,126.842742189719));
#183336=CARTESIAN_POINT('Ctrl Pts',(129.614961030676,4.49976878459078,126.962484585245));
#183337=CARTESIAN_POINT('Ctrl Pts',(129.622362852352,4.601927884234,127.082137672375));
#183338=CARTESIAN_POINT('Ctrl Pts',(129.629764674027,4.69939074546822,127.205961558573));
#183339=CARTESIAN_POINT('Ctrl Pts',(129.637166495702,4.79180450128185,127.333548006088));
#183340=CARTESIAN_POINT('Ctrl Pts',(129.644564410014,4.88416947259307,127.46106710171));
#183341=CARTESIAN_POINT('Ctrl Pts',(129.651962324325,4.97149042829734,127.592344501425));
#183342=CARTESIAN_POINT('Ctrl Pts',(129.659360238637,5.053455241603,127.726939508323));
#183343=CARTESIAN_POINT('Ctrl Pts',(129.666756923549,5.13540643384361,127.861512147972));
#183344=CARTESIAN_POINT('Ctrl Pts',(129.674153608461,5.21200305628852,127.999400982067));
#183345=CARTESIAN_POINT('Ctrl Pts',(129.681550293373,5.28297667459216,128.140136899817));
#183346=CARTESIAN_POINT('Ctrl Pts',(129.688946650309,5.35394714585119,128.280866577189));
#183347=CARTESIAN_POINT('Ctrl Pts',(129.696343007244,5.41929494063072,128.424442753893));
#183348=CARTESIAN_POINT('Ctrl Pts',(129.703739364179,5.47879803879187,128.570372566427));
#183349=CARTESIAN_POINT('Ctrl Pts',(129.711136853516,5.53831024702926,128.716324721189));
#183350=CARTESIAN_POINT('Ctrl Pts',(129.718534342853,5.59197583595167,128.864630883593));
#183351=CARTESIAN_POINT('Ctrl Pts',(129.725931832189,5.6396213608959,129.014779250814));
#183352=CARTESIAN_POINT('Ctrl Pts',(129.733331914704,5.68728358790507,129.164980252312));
#183353=CARTESIAN_POINT('Ctrl Pts',(129.740731997219,5.72892143645894,129.317024388783));
#183354=CARTESIAN_POINT('Ctrl Pts',(129.748132079734,5.76441168675377,129.470385929607));
#183355=CARTESIAN_POINT('Ctrl Pts',(129.755540299401,5.79994096222729,129.62391610721));
#183356=CARTESIAN_POINT('Ctrl Pts',(129.762948519067,5.82930905523075,129.77876621825));
#183357=CARTESIAN_POINT('Ctrl Pts',(129.770356738734,5.85244398568209,129.934400873122));
#183358=CARTESIAN_POINT('Ctrl Pts',(129.777769518036,5.87559315529713,130.090131318527));
#183359=CARTESIAN_POINT('Ctrl Pts',(129.785182297338,5.89250147783606,130.246646899673));
#183360=CARTESIAN_POINT('Ctrl Pts',(129.79259507664,5.90314901413344,130.403408900479));
#183361=CARTESIAN_POINT('Ctrl Pts',(129.800018447669,5.91381176413,130.560394890182));
#183362=CARTESIAN_POINT('Ctrl Pts',(129.807441818697,5.91819585092863,130.717627630594));
#183363=CARTESIAN_POINT('Ctrl Pts',(129.814865189726,5.91633343325431,130.874569370989));
#183364=CARTESIAN_POINT('Ctrl Pts',(129.818801239167,5.9153459347153,130.957783647511));
#183365=CARTESIAN_POINT('Ctrl Pts',(129.822737288608,5.91260318632033,131.040916202488));
#183366=CARTESIAN_POINT('Ctrl Pts',(129.826673338048,5.90811585414848,131.123887793968));
#183367=CARTESIAN_POINT('Ctrl Pts',(129.834096604454,5.8996528857171,131.280369626048));
#183368=CARTESIAN_POINT('Ctrl Pts',(129.841519870859,5.88495598040664,131.436751620332));
#183369=CARTESIAN_POINT('Ctrl Pts',(129.848943137265,5.86402353481957,131.592496738793));
#183370=CARTESIAN_POINT('Ctrl Pts',(129.856357629986,5.84311582964484,131.748057779458));
#183371=CARTESIAN_POINT('Ctrl Pts',(129.863772122707,5.81598730324102,131.902983076263));
#183372=CARTESIAN_POINT('Ctrl Pts',(129.871186615428,5.78268832356932,132.056736884889));
#183373=CARTESIAN_POINT('Ctrl Pts',(129.878593961781,5.74942143870794,132.210342499806));
#183374=CARTESIAN_POINT('Ctrl Pts',(129.886001308135,5.70999601899646,132.362778512018));
#183375=CARTESIAN_POINT('Ctrl Pts',(129.893408654489,5.66451405460985,132.513515697606));
#183376=CARTESIAN_POINT('Ctrl Pts',(129.900810476164,5.61906601238819,132.664140457715));
#183377=CARTESIAN_POINT('Ctrl Pts',(129.90821229784,5.56757052721464,132.813068558219));
#183378=CARTESIAN_POINT('Ctrl Pts',(129.915614119515,5.51018032783333,132.959782459633));
#183379=CARTESIAN_POINT('Ctrl Pts',(129.923012033827,5.45282042429159,133.10641891192));
#183380=CARTESIAN_POINT('Ctrl Pts',(129.930409948138,5.38957213943364,133.250843146186));
#183381=CARTESIAN_POINT('Ctrl Pts',(129.937807862449,5.32063753189545,133.392554353878));
#183382=CARTESIAN_POINT('Ctrl Pts',(129.945204547361,5.25171438003843,133.534242011739));
#183383=CARTESIAN_POINT('Ctrl Pts',(129.952601232274,5.1771069441081,133.673217202481));
#183384=CARTESIAN_POINT('Ctrl Pts',(129.959997917186,5.09706480497668,133.809000518847));
#183385=CARTESIAN_POINT('Ctrl Pts',(129.967394274121,5.01702621499759,133.944777814438));
#183386=CARTESIAN_POINT('Ctrl Pts',(129.974790631057,4.93155359053565,134.077363195483));
#183387=CARTESIAN_POINT('Ctrl Pts',(129.982186987992,4.84094158430336,134.20630346539));
#183388=CARTESIAN_POINT('Ctrl Pts',(129.989584477329,4.75031570514154,134.335263476382));
#183389=CARTESIAN_POINT('Ctrl Pts',(129.996981966665,4.65454909212963,134.46057695959));
#183390=CARTESIAN_POINT('Ctrl Pts',(130.004379456002,4.55397858840311,134.581821349177));
#183391=CARTESIAN_POINT('Ctrl Pts',(130.011779538517,4.45337282984241,134.703108240798));
#183392=CARTESIAN_POINT('Ctrl Pts',(130.019179621032,4.34796006592033,134.820322911678));
#183393=CARTESIAN_POINT('Ctrl Pts',(130.026579703547,4.23811600538281,134.933077523267));
#183394=CARTESIAN_POINT('Ctrl Pts',(130.033987923213,4.12815116000849,135.045956120142));
#183395=CARTESIAN_POINT('Ctrl Pts',(130.04139614288,4.01374554763212,135.154364595974));
#183396=CARTESIAN_POINT('Ctrl Pts',(130.048804362546,3.89531069969698,135.257953000724));
#183397=CARTESIAN_POINT('Ctrl Pts',(130.056217141848,3.77680295708913,135.361605162409));
#183398=CARTESIAN_POINT('Ctrl Pts',(130.063629921151,3.65426132726043,135.460431107745));
#183399=CARTESIAN_POINT('Ctrl Pts',(130.071042700453,3.52812826970216,135.554122872146));
#183400=CARTESIAN_POINT('Ctrl Pts',(130.078466071481,3.4018149873162,135.647948507733));
#183401=CARTESIAN_POINT('Ctrl Pts',(130.08588944251,3.2719003357471,135.736625100936));
#183402=CARTESIAN_POINT('Ctrl Pts',(130.093312813539,3.13885412248647,135.819889040399));
#183403=CARTESIAN_POINT('Ctrl Pts',(130.09724886298,3.06830982781482,135.864037578994));
#183404=CARTESIAN_POINT('Ctrl Pts',(130.101184912421,2.99688553237233,135.906665203682));
#183405=CARTESIAN_POINT('Ctrl Pts',(130.105120961861,2.92465366993242,135.947738055928));
#183406=CARTESIAN_POINT('Ctrl Pts',(130.112544228267,2.78842663165143,136.025200173423));
#183407=CARTESIAN_POINT('Ctrl Pts',(130.119967494672,2.64891399457985,136.097363538501));
#183408=CARTESIAN_POINT('Ctrl Pts',(130.127390761078,2.50656671734434,136.163936520005));
#183409=CARTESIAN_POINT('Ctrl Pts',(130.134805253799,2.36438768276912,136.230430817773));
#183410=CARTESIAN_POINT('Ctrl Pts',(130.14221974652,2.21938101168184,136.291347727374));
#183411=CARTESIAN_POINT('Ctrl Pts',(130.149634239241,2.07202466606484,136.346440041908));
#183412=CARTESIAN_POINT('Ctrl Pts',(130.157041585595,1.92481034804172,136.401479256396));
#183413=CARTESIAN_POINT('Ctrl Pts',(130.164448931948,1.77525121138219,136.450704922263));
#183414=CARTESIAN_POINT('Ctrl Pts',(130.171856278302,1.62384763533801,136.49391678828));
#183415=CARTESIAN_POINT('Ctrl Pts',(130.179258099978,1.47255698179307,136.537096425256));
#183416=CARTESIAN_POINT('Ctrl Pts',(130.186659921653,1.31942498539211,136.574271091245));
#183417=CARTESIAN_POINT('Ctrl Pts',(130.194061743328,1.16496962038035,136.605289538531));
#183418=CARTESIAN_POINT('Ctrl Pts',(130.20145965764,1.01059579115362,136.63629161142));
#183419=CARTESIAN_POINT('Ctrl Pts',(130.208857571951,0.854900349667567,
136.661143864464));
#183420=CARTESIAN_POINT('Ctrl Pts',(130.216255486262,0.698413857970478,
136.679745596058));
#183421=CARTESIAN_POINT('Ctrl Pts',(130.223652171175,0.541953371489244,
136.698344236383));
#183422=CARTESIAN_POINT('Ctrl Pts',(130.231048856087,0.384702466027742,
136.710694372796));
#183423=CARTESIAN_POINT('Ctrl Pts',(130.238445540999,0.227199385047126,
136.716746853422));
#183424=CARTESIAN_POINT('Ctrl Pts',(130.245841897934,0.0697032879180588,
136.722799065674));
#183425=CARTESIAN_POINT('Ctrl Pts',(130.25323825487,-0.0880445894748271,
136.722554163036));
#183426=CARTESIAN_POINT('Ctrl Pts',(130.260634611805,-0.245503693015841,
136.716015081353));
#183427=CARTESIAN_POINT('Ctrl Pts',(130.268032101142,-0.40298690394747,
136.709474998521));
#183428=CARTESIAN_POINT('Ctrl Pts',(130.275429590478,-0.56018087999485,
136.696638833368));
#183429=CARTESIAN_POINT('Ctrl Pts',(130.282827079815,-0.716548032609668,
136.677561574409));
#183430=CARTESIAN_POINT('Ctrl Pts',(130.29022716233,-0.872969999487436,
136.658477627947));
#183431=CARTESIAN_POINT('Ctrl Pts',(130.297627244845,-1.02856419554083,
136.633148276953));
#183432=CARTESIAN_POINT('Ctrl Pts',(130.30502732736,-1.18280124145736,136.601679979625));
#183433=CARTESIAN_POINT('Ctrl Pts',(130.312435547026,-1.33720788686194,
136.57017707967));
#183434=CARTESIAN_POINT('Ctrl Pts',(130.319843766693,-1.4902540358692,136.532521827054));
#183435=CARTESIAN_POINT('Ctrl Pts',(130.327251986359,-1.64142282280249,
136.488871298292));
#183436=CARTESIAN_POINT('Ctrl Pts',(130.334664765661,-1.79268465160185,
136.445193903357));
#183437=CARTESIAN_POINT('Ctrl Pts',(130.342077544964,-1.9420664624772,136.395513997035));
#183438=CARTESIAN_POINT('Ctrl Pts',(130.349490324266,-2.0890699959377,136.340037370644));
#183439=CARTESIAN_POINT('Ctrl Pts',(130.356913695294,-2.23628357494058,
136.284481476649));
#183440=CARTESIAN_POINT('Ctrl Pts',(130.364337066323,-2.38111174676919,
136.223112465582));
#183441=CARTESIAN_POINT('Ctrl Pts',(130.371760437352,-2.52307878529869,
136.156183111416));
#183442=CARTESIAN_POINT('Ctrl Pts',(130.375696486793,-2.59835311557997,
136.120695561889));
#183443=CARTESIAN_POINT('Ctrl Pts',(130.379632536234,-2.67282351982889,
136.083645551673));
#183444=CARTESIAN_POINT('Ctrl Pts',(130.383568585674,-2.74642235967692,
136.045075719989));
#183445=CARTESIAN_POINT('Ctrl Pts',(130.39099185208,-2.88522747468796,135.972334221157));
#183446=CARTESIAN_POINT('Ctrl Pts',(130.398415118485,-3.02135054562298,
135.893964349898));
#183447=CARTESIAN_POINT('Ctrl Pts',(130.405838384891,-3.15430246077847,
135.810187876714));
#183448=CARTESIAN_POINT('Ctrl Pts',(130.413252877612,-3.28709723781139,
135.726510420364));
#183449=CARTESIAN_POINT('Ctrl Pts',(130.420667370333,-3.41672800682248,
135.637439278793));
#183450=CARTESIAN_POINT('Ctrl Pts',(130.428081863054,-3.5427284355203,135.543242953587));
#183451=CARTESIAN_POINT('Ctrl Pts',(130.435489209407,-3.66860742026092,
135.449137418347));
#183452=CARTESIAN_POINT('Ctrl Pts',(130.442896555761,-3.79086273364817,
135.349916755745));
#183453=CARTESIAN_POINT('Ctrl Pts',(130.450303902115,-3.90905543144098,
135.245893708338));
#183454=CARTESIAN_POINT('Ctrl Pts',(130.45770572379,-4.0271599766607,135.141948245244));
#183455=CARTESIAN_POINT('Ctrl Pts',(130.465107545466,-4.1412076605105,135.033207774757));
#183456=CARTESIAN_POINT('Ctrl Pts',(130.472509367141,-4.25079125627099,
134.920026330195));
#183457=CARTESIAN_POINT('Ctrl Pts',(130.479907281453,-4.36031700370395,
134.806904633237));
#183458=CARTESIAN_POINT('Ctrl Pts',(130.487305195764,-4.4653830972374,134.689346898611));
#183459=CARTESIAN_POINT('Ctrl Pts',(130.494703110075,-4.56561803201373,
134.567745071518));
#183460=CARTESIAN_POINT('Ctrl Pts',(130.502099794987,-4.66583630956262,
134.446163452443));
#183461=CARTESIAN_POINT('Ctrl Pts',(130.5094964799,-4.76122478456999,134.320539362502));
#183462=CARTESIAN_POINT('Ctrl Pts',(130.516893164812,-4.8514511704319,134.191299073372));
#183463=CARTESIAN_POINT('Ctrl Pts',(130.524289521747,-4.94167355556137,
134.062064514891));
#183464=CARTESIAN_POINT('Ctrl Pts',(130.531685878683,-5.02673409297332,
133.929214382131));
#183465=CARTESIAN_POINT('Ctrl Pts',(130.539082235618,-5.10634306997367,
133.793205045473));
#183466=CARTESIAN_POINT('Ctrl Pts',(130.546479724955,-5.18596423531163,
133.657174885439));
#183467=CARTESIAN_POINT('Ctrl Pts',(130.553877214291,-5.26013198975974,
133.517984880619));
#183468=CARTESIAN_POINT('Ctrl Pts',(130.561274703628,-5.32860201697006,
133.376117042122));
#183469=CARTESIAN_POINT('Ctrl Pts',(130.568674786143,-5.39709604624213,
133.234199472073));
#183470=CARTESIAN_POINT('Ctrl Pts',(130.576074868658,-5.45988820945286,
133.089602535361));
#183471=CARTESIAN_POINT('Ctrl Pts',(130.583474951173,-5.51678193044974,
132.94282915705));
#183472=CARTESIAN_POINT('Ctrl Pts',(130.590883170839,-5.5737382119418,132.795894386321));
#183473=CARTESIAN_POINT('Ctrl Pts',(130.598291390506,-5.62478296336238,
132.646778742849));
#183474=CARTESIAN_POINT('Ctrl Pts',(130.605699610172,-5.66976895910799,
132.496001984061));
#183475=CARTESIAN_POINT('Ctrl Pts',(130.613112389474,-5.71478264298338,
132.345132424692));
#183476=CARTESIAN_POINT('Ctrl Pts',(130.620525168776,-5.75373004841809,
132.192600073624));
#183477=CARTESIAN_POINT('Ctrl Pts',(130.627937948079,-5.78651499205246,
132.038935365911));
#183478=CARTESIAN_POINT('Ctrl Pts',(130.635361319107,-5.81934678035175,
131.885051094858));
#183479=CARTESIAN_POINT('Ctrl Pts',(130.642784690136,-5.8459984577789,131.730031602649));
#183480=CARTESIAN_POINT('Ctrl Pts',(130.650208061165,-5.86642554864406,
131.574413761652));
#183481=CARTESIAN_POINT('Ctrl Pts',(130.654144110606,-5.87725648236231,
131.491901448354));
#183482=CARTESIAN_POINT('Ctrl Pts',(130.658080160047,-5.88633833199474,
131.409220952629));
#183483=CARTESIAN_POINT('Ctrl Pts',(130.662016209487,-5.89367041093406,
131.326452228091));
#183484=CARTESIAN_POINT('Ctrl Pts',(130.67021907559,-5.9089507224997,131.153959281779));
#183485=CARTESIAN_POINT('Ctrl Pts',(130.678421941693,-5.91665983543796,
130.980785795447));
#183486=CARTESIAN_POINT('Ctrl Pts',(130.686624807795,-5.91674921377853,
130.807410822667));
#183487=CARTESIAN_POINT('',(132.436623601775,-5.91262847433545,130.80816648937));
#183488=CARTESIAN_POINT('Ctrl Pts',(130.686627247827,-5.92459733177465,
130.807363227819));
#183489=CARTESIAN_POINT('Ctrl Pts',(130.771239442985,-5.91334481668904,
129.016629511582));
#183490=CARTESIAN_POINT('Ctrl Pts',(130.948667512746,-4.09245350856522,
125.241769634098));
#183491=CARTESIAN_POINT('Ctrl Pts',(131.218911457113,2.33599408130523,124.207339154629));
#183492=CARTESIAN_POINT('Ctrl Pts',(131.497359080925,6.81292285489911,129.203847355033));
#183493=CARTESIAN_POINT('Ctrl Pts',(131.775806704738,5.02910835462435,135.671149054285));
#183494=CARTESIAN_POINT('Ctrl Pts',(132.054254328551,-1.37621103794747,
137.666109936025));
#183495=CARTESIAN_POINT('Ctrl Pts',(132.274526317919,-5.44283188373582,
134.256076213049));
#183496=CARTESIAN_POINT('Ctrl Pts',(132.401982432682,-5.91374388142558,
131.546133979802));
#183497=CARTESIAN_POINT('Ctrl Pts',(132.43662267284,-5.90945480774847,130.808184249578));
#183498=CARTESIAN_POINT('',(134.186626039157,-5.9132873379319,130.799875516716));
#183499=CARTESIAN_POINT('Ctrl Pts',(132.436624807795,-5.91674879074801,
130.8081434316));
#183500=CARTESIAN_POINT('Ctrl Pts',(132.44407390138,-5.91685037237187,130.649258288229));
#183501=CARTESIAN_POINT('Ctrl Pts',(132.451522994964,-5.91054770060562,
130.490344618787));
#183502=CARTESIAN_POINT('Ctrl Pts',(132.458972088549,-5.89786057853249,
130.331950669859));
#183503=CARTESIAN_POINT('Ctrl Pts',(132.466421684772,-5.88517260037755,
130.173546033072));
#183504=CARTESIAN_POINT('Ctrl Pts',(132.473871280995,-5.86609934203964,
130.015661551399));
#183505=CARTESIAN_POINT('Ctrl Pts',(132.481320877217,-5.84071257509522,
129.858841089674));
#183506=CARTESIAN_POINT('Ctrl Pts',(132.488772368481,-5.81531935022228,
129.701980735697));
#183507=CARTESIAN_POINT('Ctrl Pts',(132.496223859745,-5.78360947568675,
129.546185301953));
#183508=CARTESIAN_POINT('Ctrl Pts',(132.503675351009,-5.74570599473036,
129.391989142132));
#183509=CARTESIAN_POINT('Ctrl Pts',(132.511130130572,-5.70778578719094,
129.237724936454));
#183510=CARTESIAN_POINT('Ctrl Pts',(132.518584910135,-5.66366661589122,
129.085061765474));
#183511=CARTESIAN_POINT('Ctrl Pts',(132.526039689697,-5.61352158044227,
128.934519440244));
#183512=CARTESIAN_POINT('Ctrl Pts',(132.53350393347,-5.56331288340478,128.783785994129));
#183513=CARTESIAN_POINT('Ctrl Pts',(132.540968177242,-5.50706315523841,
128.635179119972));
#183514=CARTESIAN_POINT('Ctrl Pts',(132.548432421014,-5.44499427198543,
128.489200160806));
#183515=CARTESIAN_POINT('Ctrl Pts',(132.555901690165,-5.38288360022045,
128.343122919809));
#183516=CARTESIAN_POINT('Ctrl Pts',(132.563370959316,-5.31494612024657,
128.199677450412));
#183517=CARTESIAN_POINT('Ctrl Pts',(132.570840228467,-5.24144983426337,
128.059340727401));
#183518=CARTESIAN_POINT('Ctrl Pts',(132.578321762038,-5.16783286855118,
127.91877357373));
#183519=CARTESIAN_POINT('Ctrl Pts',(132.58580329561,-5.08863904046948,127.781325683021));
#183520=CARTESIAN_POINT('Ctrl Pts',(132.593284829182,-5.00418050062325,
127.647446288719));
#183521=CARTESIAN_POINT('Ctrl Pts',(132.599239744847,-4.93695584979939,
127.54088518133));
#183522=CARTESIAN_POINT('Ctrl Pts',(132.605194660512,-4.86639670527273,
127.436584300791));
#183523=CARTESIAN_POINT('Ctrl Pts',(132.611149576177,-4.79267835126431,
127.334754763319));
#183524=CARTESIAN_POINT('Ctrl Pts',(132.618572842582,-4.7007826785881,127.20781630993));
#183525=CARTESIAN_POINT('Ctrl Pts',(132.625996108988,-4.60370144481768,
127.08433934361));
#183526=CARTESIAN_POINT('Ctrl Pts',(132.633419375393,-4.50172427172658,
126.964776116107));
#183527=CARTESIAN_POINT('Ctrl Pts',(132.640833868114,-4.39986762718525,
126.845354202409));
#183528=CARTESIAN_POINT('Ctrl Pts',(132.648248360835,-4.29312680145029,
126.729837101266));
#183529=CARTESIAN_POINT('Ctrl Pts',(132.655662853556,-4.18183439753327,
126.618647818758));
#183530=CARTESIAN_POINT('Ctrl Pts',(132.66307019991,-4.07064926142554,126.507565704667));
#183531=CARTESIAN_POINT('Ctrl Pts',(132.670477546264,-3.95492154306506,
126.400803367012));
#183532=CARTESIAN_POINT('Ctrl Pts',(132.677884892618,-3.83502370139943,
126.298750362317));
#183533=CARTESIAN_POINT('Ctrl Pts',(132.685286714293,-3.71521528406725,
126.196773472603));
#183534=CARTESIAN_POINT('Ctrl Pts',(132.692688535969,-3.59124321937131,
126.099499163105));
#183535=CARTESIAN_POINT('Ctrl Pts',(132.700090357644,-3.463516281595,126.007279679159));
#183536=CARTESIAN_POINT('Ctrl Pts',(132.707488271955,-3.335856769874,125.91510887716));
#183537=CARTESIAN_POINT('Ctrl Pts',(132.714886186267,-3.20444663454561,
125.827987804427));
#183538=CARTESIAN_POINT('Ctrl Pts',(132.722284100578,-3.06972704701265,
125.746227916723));
#183539=CARTESIAN_POINT('Ctrl Pts',(132.72968078549,-2.93502984743204,125.66448161603));
#183540=CARTESIAN_POINT('Ctrl Pts',(132.737077470403,-2.79702460599024,
125.588094925615));
#183541=CARTESIAN_POINT('Ctrl Pts',(132.744474155315,-2.65618084144462,
125.517335565607));
#183542=CARTESIAN_POINT('Ctrl Pts',(132.75187051225,-2.51534332205942,125.446579343143));
#183543=CARTESIAN_POINT('Ctrl Pts',(132.759266869186,-2.37166786339592,
125.381450122535));
#183544=CARTESIAN_POINT('Ctrl Pts',(132.766663226121,-2.22564766625974,
125.322169173611));
#183545=CARTESIAN_POINT('Ctrl Pts',(132.774060715458,-2.07960511305829,
125.262879148622));
#183546=CARTESIAN_POINT('Ctrl Pts',(132.781458204794,-1.93121745249945,
125.209439318576));
#183547=CARTESIAN_POINT('Ctrl Pts',(132.788855694131,-1.7809967507698,125.16202234906));
#183548=CARTESIAN_POINT('Ctrl Pts',(132.796255776646,-1.63072338940593,
125.114588757598));
#183549=CARTESIAN_POINT('Ctrl Pts',(132.803655859161,-1.47861606328235,
125.073182342554));
#183550=CARTESIAN_POINT('Ctrl Pts',(132.811055941676,-1.32520068992937,
125.037925523514));
#183551=CARTESIAN_POINT('Ctrl Pts',(132.818464161342,-1.17161662060201,
125.002629935978));
#183552=CARTESIAN_POINT('Ctrl Pts',(132.825872381009,-1.01672199563854,
124.973497532491));
#183553=CARTESIAN_POINT('Ctrl Pts',(132.833280600675,-0.861052313563191,
124.950599478281));
#183554=CARTESIAN_POINT('Ctrl Pts',(132.840693379978,-0.705286819396123,
124.9276873307));
#183555=CARTESIAN_POINT('Ctrl Pts',(132.84810615928,-0.548745687904146,
124.911017217811));
#183556=CARTESIAN_POINT('Ctrl Pts',(132.855518938582,-0.391967664889735,
124.900608258923));
#183557=CARTESIAN_POINT('Ctrl Pts',(132.86294230961,-0.234965630083658,
124.890184427226));
#183558=CARTESIAN_POINT('Ctrl Pts',(132.870365680639,-0.0777263999109395,
124.88603962697));
#183559=CARTESIAN_POINT('Ctrl Pts',(132.877789051668,0.0792123244657625,
124.8881408811));
#183560=CARTESIAN_POINT('Ctrl Pts',(132.881725101109,0.162425001823287,
124.889255016459));
#183561=CARTESIAN_POINT('Ctrl Pts',(132.88566115055,0.245553286538442,124.892124275274));
#183562=CARTESIAN_POINT('Ctrl Pts',(132.88959719999,0.328517952984534,124.896737870888));
#183563=CARTESIAN_POINT('Ctrl Pts',(132.897020466396,0.484986724663619,
124.90543896823));
#183564=CARTESIAN_POINT('Ctrl Pts',(132.904443732801,0.641346171672067,
124.920373843296));
#183565=CARTESIAN_POINT('Ctrl Pts',(132.911866999207,0.79705925416422,124.941543282201));
#183566=CARTESIAN_POINT('Ctrl Pts',(132.919281491928,0.952588296724034,
124.962687700588));
#183567=CARTESIAN_POINT('Ctrl Pts',(132.926695984649,1.10747212912949,124.990051965506));
#183568=CARTESIAN_POINT('Ctrl Pts',(132.93411047737,1.26117508433303,125.023584893742));
#183569=CARTESIAN_POINT('Ctrl Pts',(132.941517823724,1.41472989484175,125.057085501678));
#183570=CARTESIAN_POINT('Ctrl Pts',(132.948925170077,1.5671057317581,125.096742857397));
#183571=CARTESIAN_POINT('Ctrl Pts',(132.956332516431,1.71777352698821,125.142454165453));
#183572=CARTESIAN_POINT('Ctrl Pts',(132.963734338107,1.86832894849248,125.188131380291));
#183573=CARTESIAN_POINT('Ctrl Pts',(132.971136159782,2.01717850917903,125.239853449051));
#183574=CARTESIAN_POINT('Ctrl Pts',(132.978537981457,2.16380490258672,125.297466855558));
#183575=CARTESIAN_POINT('Ctrl Pts',(132.985935895769,2.31035389306298,125.355049848397));
#183576=CARTESIAN_POINT('Ctrl Pts',(132.99333381008,2.45468170696657,125.418517849114));
#183577=CARTESIAN_POINT('Ctrl Pts',(133.000731724392,2.59628784382242,125.487668037162));
#183578=CARTESIAN_POINT('Ctrl Pts',(133.008128409304,2.73787044830651,125.556806733703));
#183579=CARTESIAN_POINT('Ctrl Pts',(133.015525094216,2.87673193830053,125.631625579822));
#183580=CARTESIAN_POINT('Ctrl Pts',(133.022921779128,3.0123932869216,125.711874265359));
#183581=CARTESIAN_POINT('Ctrl Pts',(133.030318136064,3.1480486201766,125.792119392586));
#183582=CARTESIAN_POINT('Ctrl Pts',(133.037714492999,3.28050377290562,125.877793690452));
#183583=CARTESIAN_POINT('Ctrl Pts',(133.045110849935,3.40930599745367,125.968601816899));
#183584=CARTESIAN_POINT('Ctrl Pts',(133.052508339271,3.53812794195056,126.059423846302));
#183585=CARTESIAN_POINT('Ctrl Pts',(133.059905828608,3.66329553956439,126.155381054207));
#183586=CARTESIAN_POINT('Ctrl Pts',(133.067303317944,3.7843867375661,126.256135954796));
#183587=CARTESIAN_POINT('Ctrl Pts',(133.074703400459,3.90552038390059,126.35692617486));
#183588=CARTESIAN_POINT('Ctrl Pts',(133.082103482974,4.02257449876675,126.462517197492));
#183589=CARTESIAN_POINT('Ctrl Pts',(133.089503565489,4.13516181582623,126.572532724157));
#183590=CARTESIAN_POINT('Ctrl Pts',(133.096911785156,4.24787293421459,126.682669224204));
#183591=CARTESIAN_POINT('Ctrl Pts',(133.104320004822,4.35610717864507,126.797239683346));
#183592=CARTESIAN_POINT('Ctrl Pts',(133.111728224489,4.45951522576416,126.915832038055));
#183593=CARTESIAN_POINT('Ctrl Pts',(133.119141003791,4.56298691881095,127.034497384378));
#183594=CARTESIAN_POINT('Ctrl Pts',(133.126553783093,4.66162626220762,127.157189268572));
#183595=CARTESIAN_POINT('Ctrl Pts',(133.133966562395,4.75512596507289,127.283464762987));
#183596=CARTESIAN_POINT('Ctrl Pts',(133.141389933424,4.84875926469812,127.40992068575));
#183597=CARTESIAN_POINT('Ctrl Pts',(133.148813304453,4.93723804723103,127.53997013756));
#183598=CARTESIAN_POINT('Ctrl Pts',(133.156236675481,5.0202994165876,127.673142910298));
#183599=CARTESIAN_POINT('Ctrl Pts',(133.160172724922,5.06434054764887,127.743754309837));
#183600=CARTESIAN_POINT('Ctrl Pts',(133.164108774363,5.10685942735345,127.815243394556));
#183601=CARTESIAN_POINT('Ctrl Pts',(133.168044823803,5.14782230743705,127.887537679238));
#183602=CARTESIAN_POINT('Ctrl Pts',(133.175468090209,5.22507702087024,128.023882443928));
#183603=CARTESIAN_POINT('Ctrl Pts',(133.182891356614,5.29702798789942,128.163504739803));
#183604=CARTESIAN_POINT('Ctrl Pts',(133.19031462302,5.3633842639891,128.305953164949));
#183605=CARTESIAN_POINT('Ctrl Pts',(133.197729115741,5.42966211247099,128.448233227885));
#183606=CARTESIAN_POINT('Ctrl Pts',(133.205143608462,5.4903582760621,128.593332436224));
#183607=CARTESIAN_POINT('Ctrl Pts',(133.212558101183,5.5452262755268,128.740772452329));
#183608=CARTESIAN_POINT('Ctrl Pts',(133.219965447537,5.60004139114794,128.888070360196));
#183609=CARTESIAN_POINT('Ctrl Pts',(133.22737279389,5.64903939646685,129.037704236752));
#183610=CARTESIAN_POINT('Ctrl Pts',(133.234780140244,5.69202080197526,129.189173398578));
#183611=CARTESIAN_POINT('Ctrl Pts',(133.24218196192,5.73497015032987,129.340529588989));
#183612=CARTESIAN_POINT('Ctrl Pts',(133.249583783595,5.77191173244081,129.49371798158));
#183613=CARTESIAN_POINT('Ctrl Pts',(133.256985605271,5.80269508903512,129.648220372532));
#183614=CARTESIAN_POINT('Ctrl Pts',(133.264383519582,5.83346219533502,129.802641202874));
#183615=CARTESIAN_POINT('Ctrl Pts',(133.271781433893,5.858077477642,129.958374284966));
#183616=CARTESIAN_POINT('Ctrl Pts',(133.279179348205,5.87644104189458,130.114888904124));
#183617=CARTESIAN_POINT('Ctrl Pts',(133.286576033117,5.89480155445593,130.271377513391));
#183618=CARTESIAN_POINT('Ctrl Pts',(133.293972718029,5.90691236745847,130.428647031564));
#183619=CARTESIAN_POINT('Ctrl Pts',(133.301369402941,5.91272514819743,130.586159141004));
#183620=CARTESIAN_POINT('Ctrl Pts',(133.308765759877,5.91853767119159,130.743664266192));
#183621=CARTESIAN_POINT('Ctrl Pts',(133.316162116812,5.91805270342139,130.901411588216));
#183622=CARTESIAN_POINT('Ctrl Pts',(133.323558473748,5.91127400335937,131.058860558053));
#183623=CARTESIAN_POINT('Ctrl Pts',(133.330955963084,5.90449426546107,131.216333633729));
#183624=CARTESIAN_POINT('Ctrl Pts',(133.338353452421,5.89141889269998,131.37350789329));
#183625=CARTESIAN_POINT('Ctrl Pts',(133.345750941757,5.87210369164419,131.529845832494));
#183626=CARTESIAN_POINT('Ctrl Pts',(133.353151024272,5.85278171967458,131.68623857572));
#183627=CARTESIAN_POINT('Ctrl Pts',(133.360551106787,5.82721561013181,131.841794044638));
#183628=CARTESIAN_POINT('Ctrl Pts',(133.367951189302,5.79551262671546,131.995983022559));
#183629=CARTESIAN_POINT('Ctrl Pts',(133.375359408969,5.7637747826097,132.150341547113));
#183630=CARTESIAN_POINT('Ctrl Pts',(133.382767628635,5.72588666341188,132.303330214011));
#183631=CARTESIAN_POINT('Ctrl Pts',(133.390175848302,5.68200613203574,132.454432397219));
#183632=CARTESIAN_POINT('Ctrl Pts',(133.397588627604,5.63809859292471,132.6056275813));
#183633=CARTESIAN_POINT('Ctrl Pts',(133.405001406906,5.58819141044362,132.754933614834));
#183634=CARTESIAN_POINT('Ctrl Pts',(133.412414186208,5.53249113394025,132.901852552085));
#183635=CARTESIAN_POINT('Ctrl Pts',(133.419837557237,5.47671127026969,133.048981414004));
#183636=CARTESIAN_POINT('Ctrl Pts',(133.427260928266,5.41512192644351,133.193716024936));
#183637=CARTESIAN_POINT('Ctrl Pts',(133.434684299295,5.34797660011437,133.335581043987));
#183638=CARTESIAN_POINT('Ctrl Pts',(133.438620348735,5.31237453696658,133.410801281088));
#183639=CARTESIAN_POINT('Ctrl Pts',(133.442556398176,5.27521123837849,133.485215215288));
#183640=CARTESIAN_POINT('Ctrl Pts',(133.446492447616,5.2365294464544,133.558755273187));
#183641=CARTESIAN_POINT('Ctrl Pts',(133.453915714022,5.1635767940994,133.697449527286));
#183642=CARTESIAN_POINT('Ctrl Pts',(133.461338980427,5.08499985744994,133.833453174989));
#183643=CARTESIAN_POINT('Ctrl Pts',(133.468762246833,5.00102115109538,133.966277442657));
#183644=CARTESIAN_POINT('Ctrl Pts',(133.476176739554,4.91714170059768,134.098944723072));
#183645=CARTESIAN_POINT('Ctrl Pts',(133.483591232275,4.82787338620697,134.228439790858));
#183646=CARTESIAN_POINT('Ctrl Pts',(133.491005724996,4.73348541887591,134.354296722877));
#183647=CARTESIAN_POINT('Ctrl Pts',(133.498413071349,4.63918842622115,134.480032349247));
#183648=CARTESIAN_POINT('Ctrl Pts',(133.505820417703,4.53978182674042,134.602136524107));
#183649=CARTESIAN_POINT('Ctrl Pts',(133.513227764057,4.43557903062356,134.720170779664));
#183650=CARTESIAN_POINT('Ctrl Pts',(133.520629585732,4.33145395288362,134.838117000821));
#183651=CARTESIAN_POINT('Ctrl Pts',(133.528031407408,4.22254004715631,134.95199906812));
#183652=CARTESIAN_POINT('Ctrl Pts',(133.535433229083,4.1091919660784,135.061410294093));
#183653=CARTESIAN_POINT('Ctrl Pts',(133.542831143395,3.99590372056947,135.170763762732));
#183654=CARTESIAN_POINT('Ctrl Pts',(133.550229057706,3.8781862293635,135.275650831741));
#183655=CARTESIAN_POINT('Ctrl Pts',(133.557626972017,3.75643200257498,135.375700593167));
#183656=CARTESIAN_POINT('Ctrl Pts',(133.56502365693,3.63469800913089,135.475733728138));
#183657=CARTESIAN_POINT('Ctrl Pts',(133.572420341842,3.50892889963901,135.570930914207));
#183658=CARTESIAN_POINT('Ctrl Pts',(133.579817026754,3.37955145096719,135.660960513869));
#183659=CARTESIAN_POINT('Ctrl Pts',(133.587213383689,3.25017973902701,135.750986121523));
#183660=CARTESIAN_POINT('Ctrl Pts',(133.594609740625,3.11720031244699,135.83584438515));
#183661=CARTESIAN_POINT('Ctrl Pts',(133.60200609756,2.98106998197459,135.915246286906));
#183662=CARTESIAN_POINT('Ctrl Pts',(133.609403586897,2.84491880960145,135.994660345297));
#183663=CARTESIAN_POINT('Ctrl Pts',(133.616801076233,2.70561609526588,136.068616190367));
#183664=CARTESIAN_POINT('Ctrl Pts',(133.62419856557,2.56364422132333,136.13687023959));
#183665=CARTESIAN_POINT('Ctrl Pts',(133.631598648085,2.42162257935944,136.205148215164));
#183666=CARTESIAN_POINT('Ctrl Pts',(133.6389987306,2.2769302511042,136.26772025374));
#183667=CARTESIAN_POINT('Ctrl Pts',(133.646398813115,2.13007046019527,136.324390544759));
#183668=CARTESIAN_POINT('Ctrl Pts',(133.653807032781,1.98304918184942,136.381123150588));
#183669=CARTESIAN_POINT('Ctrl Pts',(133.661215252448,1.83385602962931,136.431940914274));
#183670=CARTESIAN_POINT('Ctrl Pts',(133.668623472114,1.68301098441021,136.476697401366));
#183671=CARTESIAN_POINT('Ctrl Pts',(133.676036251416,1.53207309658211,136.52148143533));
#183672=CARTESIAN_POINT('Ctrl Pts',(133.683449030718,1.3794816508222,136.560196667391));
#183673=CARTESIAN_POINT('Ctrl Pts',(133.69086181002,1.22576722794721,136.592747721535));
#183674=CARTESIAN_POINT('Ctrl Pts',(133.698285181049,1.07183317069698,136.62534528615));
#183675=CARTESIAN_POINT('Ctrl Pts',(133.705708552078,0.916773298681986,
136.651761019437));
#183676=CARTESIAN_POINT('Ctrl Pts',(133.713131923107,0.761124551332805,
136.671951262785));
#183677=CARTESIAN_POINT('Ctrl Pts',(133.717067972547,0.678595850746283,
136.682656614266));
#183678=CARTESIAN_POINT('Ctrl Pts',(133.721004021988,0.595901629734843,
136.691612627742));
#183679=CARTESIAN_POINT('Ctrl Pts',(133.724940071429,0.513121842865592,
136.698818738282));
#183680=CARTESIAN_POINT('Ctrl Pts',(133.732363337835,0.357001748301379,
136.712409237865));
#183681=CARTESIAN_POINT('Ctrl Pts',(133.73978660424,0.200105274057244,136.719813529305));
#183682=CARTESIAN_POINT('Ctrl Pts',(133.747209870645,0.0429639138102346,
136.720954626336));
#183683=CARTESIAN_POINT('Ctrl Pts',(133.754624363366,-0.113991718398853,
136.722094374685));
#183684=CARTESIAN_POINT('Ctrl Pts',(133.762038856087,-0.271191290846173,
136.716985660809));
#183685=CARTESIAN_POINT('Ctrl Pts',(133.769453348808,-0.428097294104577,
136.70560313667));
#183686=CARTESIAN_POINT('Ctrl Pts',(133.776860695162,-0.584852065449522,
136.694231583436));
#183687=CARTESIAN_POINT('Ctrl Pts',(133.784268041516,-0.741313461089294,
136.676598285024));
#183688=CARTESIAN_POINT('Ctrl Pts',(133.79167538787,-0.896943179789474,
136.65272991975));
#183689=CARTESIAN_POINT('Ctrl Pts',(133.799077209545,-1.05245682397432,
136.628879356404));
#183690=CARTESIAN_POINT('Ctrl Pts',(133.80647903122,-1.20713965891711,136.598803042012));
#183691=CARTESIAN_POINT('Ctrl Pts',(133.813880852896,-1.36045782851884,
136.562579531373));
#183692=CARTESIAN_POINT('Ctrl Pts',(133.821278767207,-1.5136950626515,136.526375142843));
#183693=CARTESIAN_POINT('Ctrl Pts',(133.828676681518,-1.66556870377039,
136.484030106367));
#183694=CARTESIAN_POINT('Ctrl Pts',(133.83607459583,-1.81555453520508,136.435674167014));
#183695=CARTESIAN_POINT('Ctrl Pts',(133.843471280742,-1.96551544171603,
136.38732626354));
#183696=CARTESIAN_POINT('Ctrl Pts',(133.850867965654,-2.11358880624222,
136.332969554149));
#183697=CARTESIAN_POINT('Ctrl Pts',(133.858264650566,-2.25926492943554,
136.272783840134));
#183698=CARTESIAN_POINT('Ctrl Pts',(133.865661007502,-2.40493459319669,
136.212600794817));
#183699=CARTESIAN_POINT('Ctrl Pts',(133.873057364437,-2.54820688196584,
136.14658940133));
#183700=CARTESIAN_POINT('Ctrl Pts',(133.880453721372,-2.68859171948106,
136.074977766291));
#183701=CARTESIAN_POINT('Ctrl Pts',(133.887851210709,-2.8289980502734,136.003355167328));
#183702=CARTESIAN_POINT('Ctrl Pts',(133.895248700046,-2.96651571702576,
135.926130789232));
#183703=CARTESIAN_POINT('Ctrl Pts',(133.902646189382,-3.10067904741429,
135.843578811634));
#183704=CARTESIAN_POINT('Ctrl Pts',(133.910046271897,-3.23488940854992,
135.760997895569));
#183705=CARTESIAN_POINT('Ctrl Pts',(133.917446354412,-3.36574277446368,
135.673085857166));
#183706=CARTESIAN_POINT('Ctrl Pts',(133.924846436927,-3.49280239951895,
135.580160232334));
#183707=CARTESIAN_POINT('Ctrl Pts',(133.932254656593,-3.62000173969448,
135.487132426224));
#183708=CARTESIAN_POINT('Ctrl Pts',(133.93966287626,-3.74339870653799,135.389080244456));
#183709=CARTESIAN_POINT('Ctrl Pts',(133.947071095926,-3.86258903823458,
135.286362010271));
#183710=CARTESIAN_POINT('Ctrl Pts',(133.954483875228,-3.98185272959161,
135.183580554726));
#183711=CARTESIAN_POINT('Ctrl Pts',(133.96189665453,-4.09690435448368,135.076127578396));
#183712=CARTESIAN_POINT('Ctrl Pts',(133.969309433832,-4.20737687847538,
134.964397920881));
#183713=CARTESIAN_POINT('Ctrl Pts',(133.976732804861,-4.31800725079001,
134.852508618791));
#183714=CARTESIAN_POINT('Ctrl Pts',(133.98415617589,-4.42404520370888,134.736330706023));
#183715=CARTESIAN_POINT('Ctrl Pts',(133.991579546919,-4.52516377712922,
134.616292326379));
#183716=CARTESIAN_POINT('Ctrl Pts',(133.99551559636,-4.57877927106441,134.55264509721));
#183717=CARTESIAN_POINT('Ctrl Pts',(133.9994516458,-4.63101246522455,134.487913051098));
#183718=CARTESIAN_POINT('Ctrl Pts',(134.003387695241,-4.68181966692091,
134.422163150725));
#183719=CARTESIAN_POINT('Ctrl Pts',(134.011022574931,-4.7803720042715,134.294625987765));
#183720=CARTESIAN_POINT('Ctrl Pts',(134.018657454621,-4.87386670141188,
134.162855095918));
#183721=CARTESIAN_POINT('Ctrl Pts',(134.02629233431,-4.96192037701707,134.027290454631));
#183722=CARTESIAN_POINT('Ctrl Pts',(134.033714027795,-5.04751535913498,
133.895511139718));
#183723=CARTESIAN_POINT('Ctrl Pts',(134.041135721279,-5.12796884959424,
133.760147423981));
#183724=CARTESIAN_POINT('Ctrl Pts',(134.048557414764,-5.20296800714661,
133.62163846668));
#183725=CARTESIAN_POINT('Ctrl Pts',(134.05597195836,-5.27789491224383,133.483262945708));
#183726=CARTESIAN_POINT('Ctrl Pts',(134.063386501956,-5.34737776716814,
133.341748538514));
#183727=CARTESIAN_POINT('Ctrl Pts',(134.070801045553,-5.41114695277371,
133.197563328994));
#183728=CARTESIAN_POINT('Ctrl Pts',(134.078209897014,-5.47486718285919,
133.053488810271));
#183729=CARTESIAN_POINT('Ctrl Pts',(134.085618748475,-5.53288232615693,
132.906747909422));
#183730=CARTESIAN_POINT('Ctrl Pts',(134.093027599936,-5.58496872146775,
132.757833151984));
#183731=CARTESIAN_POINT('Ctrl Pts',(134.100432213184,-5.63702532090011,
132.609003580822));
#183732=CARTESIAN_POINT('Ctrl Pts',(134.107836826432,-5.68315980345566,
132.458002979346));
#183733=CARTESIAN_POINT('Ctrl Pts',(134.11524143968,-5.72319672339956,132.305343571423));
#183734=CARTESIAN_POINT('Ctrl Pts',(134.12264368252,-5.7632208264932,132.152733033712));
#183735=CARTESIAN_POINT('Ctrl Pts',(134.130045925361,-5.79715115857646,
131.998465105857));
#183736=CARTESIAN_POINT('Ctrl Pts',(134.137448168201,-5.82486222414745,
131.843066847546));
#183737=CARTESIAN_POINT('Ctrl Pts',(134.144849108908,-5.85256841504679,
131.687695925445));
#183738=CARTESIAN_POINT('Ctrl Pts',(134.152250049615,-5.87405745611901,
131.531195435284));
#183739=CARTESIAN_POINT('Ctrl Pts',(134.159650990322,-5.88925506503365,
131.374102086546));
#183740=CARTESIAN_POINT('Ctrl Pts',(134.167053047952,-5.90445496751447,
131.216985029869));
#183741=CARTESIAN_POINT('Ctrl Pts',(134.174455105581,-5.91336150741497,
131.0592753061));
#183742=CARTESIAN_POINT('Ctrl Pts',(134.18185716321,-5.91595230949239,130.901514280964));
#183743=CARTESIAN_POINT('Ctrl Pts',(134.183446378072,-5.91650855227934,
130.867643136172));
#183744=CARTESIAN_POINT('Ctrl Pts',(134.185035592933,-5.91677385779731,
130.833769631019));
#183745=CARTESIAN_POINT('Ctrl Pts',(134.186624807795,-5.91674831791726,
130.799899124178));
#183746=CARTESIAN_POINT('',(135.936624807795,-5.92567594249246,130.802308620648));
#183747=CARTESIAN_POINT('Ctrl Pts',(134.186626933769,-5.91077285849561,
130.799858365367));
#183748=CARTESIAN_POINT('Ctrl Pts',(134.218363062198,-5.91547483959939,
130.124154099521));
#183749=CARTESIAN_POINT('Ctrl Pts',(134.342915065229,-5.49594096797783,
127.477948136323));
#183750=CARTESIAN_POINT('Ctrl Pts',(134.560282942868,-1.5901433003448,123.989009943189));
#183751=CARTESIAN_POINT('Ctrl Pts',(134.83873056668,4.87443624786771,125.782664510092));
#183752=CARTESIAN_POINT('Ctrl Pts',(135.117178190494,6.8596470137397,132.19101247627));
#183753=CARTESIAN_POINT('Ctrl Pts',(135.395625814306,2.54117728637125,137.325095126005));
#183754=CARTESIAN_POINT('Ctrl Pts',(135.66877468674,-3.98589310494111,136.483271655578));
#183755=CARTESIAN_POINT('Ctrl Pts',(135.84910768457,-5.91738414547342,132.653629227728));
#183756=CARTESIAN_POINT('Ctrl Pts',(135.936624807795,-5.92567594249246,
130.802308620648));
#183757=CARTESIAN_POINT('',(137.686624807795,-5.91704275648427,130.809814173709));
#183758=CARTESIAN_POINT('Ctrl Pts',(135.936624807795,-5.92567594249246,
130.802308620648));
#183759=CARTESIAN_POINT('Ctrl Pts',(135.941923559174,-5.92617797191561,
130.690219840098));
#183760=CARTESIAN_POINT('Ctrl Pts',(135.947222310553,-5.92327425135077,
130.578157588943));
#183761=CARTESIAN_POINT('Ctrl Pts',(136.045336936536,-5.80492782942922,
128.506840458106));
#183762=CARTESIAN_POINT('Ctrl Pts',(136.230968685746,-3.44077999718933,
124.710216416672));
#183763=CARTESIAN_POINT('Ctrl Pts',(136.509416309557,3.26735047713948,124.615501159646));
#183764=CARTESIAN_POINT('Ctrl Pts',(136.787863933371,6.97294548192195,130.208045401854));
#183765=CARTESIAN_POINT('Ctrl Pts',(137.066311557183,4.27074423614178,136.348574195687));
#183766=CARTESIAN_POINT('Ctrl Pts',(137.344759180996,-2.35606232519568,
137.394241561112));
#183767=CARTESIAN_POINT('Ctrl Pts',(137.551530264534,-5.66925498345734,
133.67380708407));
#183768=CARTESIAN_POINT('Ctrl Pts',(137.665485473467,-5.92120632191818,
131.258690372421));
#183769=CARTESIAN_POINT('Ctrl Pts',(137.686624807795,-5.91704275648427,
130.809814173709));
#183770=CARTESIAN_POINT('',(139.436624807833,-5.91674998555252,130.803947139341));
#183771=CARTESIAN_POINT('Ctrl Pts',(137.686624807795,-5.91674748693855,
130.809813901568));
#183772=CARTESIAN_POINT('Ctrl Pts',(137.69393408468,-5.91689052743576,130.654616684241));
#183773=CARTESIAN_POINT('Ctrl Pts',(137.701243361564,-5.91092312658041,
130.499242156393));
#183774=CARTESIAN_POINT('Ctrl Pts',(137.708552638449,-5.89883028694207,
130.344217369919));
#183775=CARTESIAN_POINT('Ctrl Pts',(137.715856751963,-5.8867459898465,130.189302095017));
#183776=CARTESIAN_POINT('Ctrl Pts',(137.723160865477,-5.86854489581824,
130.034736451036));
#183777=CARTESIAN_POINT('Ctrl Pts',(137.730464978992,-5.84426407875375,
129.881047052038));
#183778=CARTESIAN_POINT('Ctrl Pts',(137.737766293394,-5.81999256668224,
129.727416550513));
#183779=CARTESIAN_POINT('Ctrl Pts',(137.745067607796,-5.78964602436644,
129.574662004816));
#183780=CARTESIAN_POINT('Ctrl Pts',(137.752368922199,-5.7533133206347,129.423304356182));
#183781=CARTESIAN_POINT('Ctrl Pts',(137.759668915328,-5.71698719180307,
129.271974097787));
#183782=CARTESIAN_POINT('Ctrl Pts',(137.766968908458,-5.67467714561526,
129.122040606972));
#183783=CARTESIAN_POINT('Ctrl Pts',(137.774268901587,-5.62652299648003,
128.974013783608));
#183784=CARTESIAN_POINT('Ctrl Pts',(137.781569104416,-5.57836746407182,
128.825982708035));
#183785=CARTESIAN_POINT('Ctrl Pts',(137.788869307244,-5.52436761338954,
128.679858774188));
#183786=CARTESIAN_POINT('Ctrl Pts',(137.796169510073,-5.46471278755805,
128.536135604037));
#183787=CARTESIAN_POINT('Ctrl Pts',(137.80347145356,-5.40504373764388,128.392378164567));
#183788=CARTESIAN_POINT('Ctrl Pts',(137.810773397047,-5.33971717708414,
128.251022982321));
#183789=CARTESIAN_POINT('Ctrl Pts',(137.818075340535,-5.26897000914988,
128.112542346364));
#183790=CARTESIAN_POINT('Ctrl Pts',(137.825384779612,-5.19815021783941,
127.973919557277));
#183791=CARTESIAN_POINT('Ctrl Pts',(137.83269421869,-5.12189888135447,127.838177549932));
#183792=CARTESIAN_POINT('Ctrl Pts',(137.840003657768,-5.04049846765269,
127.705763231636));
#183793=CARTESIAN_POINT('Ctrl Pts',(137.847317023562,-4.95905432468774,
127.573277778806));
#183794=CARTESIAN_POINT('Ctrl Pts',(137.854630389357,-4.87245580897648,
127.444123893767));
#183795=CARTESIAN_POINT('Ctrl Pts',(137.861943755151,-4.78102743035337,
127.318717596155));
#183796=CARTESIAN_POINT('Ctrl Pts',(137.869268052795,-4.68946238671831,
127.19312384413));
#183797=CARTESIAN_POINT('Ctrl Pts',(137.876592350438,-4.59305329741779,
127.07128916947));
#183798=CARTESIAN_POINT('Ctrl Pts',(137.883916648082,-4.49216403964663,
126.95359539447));
#183799=CARTESIAN_POINT('Ctrl Pts',(137.889829241595,-4.4107204391639,126.858586223006));
#183800=CARTESIAN_POINT('Ctrl Pts',(137.895741835109,-4.3263580580978,126.766274891852));
#183801=CARTESIAN_POINT('Ctrl Pts',(137.901654428623,-4.23928440043606,
126.676843405643));
#183802=CARTESIAN_POINT('Ctrl Pts',(137.909077695028,-4.12996334593991,
126.564562095313));
#183803=CARTESIAN_POINT('Ctrl Pts',(137.916500961434,-4.01601309505411,
126.456457204189));
#183804=CARTESIAN_POINT('Ctrl Pts',(137.923924227839,-3.89778575089131,
126.352934239129));
#183805=CARTESIAN_POINT('Ctrl Pts',(137.93133872056,-3.77969814163099,126.249533629616));
#183806=CARTESIAN_POINT('Ctrl Pts',(137.938753213281,-3.65734377954116,
126.150704410188));
#183807=CARTESIAN_POINT('Ctrl Pts',(137.946167706002,-3.53111305708877,
126.056816922079));
#183808=CARTESIAN_POINT('Ctrl Pts',(137.953575052356,-3.40500400055936,
125.963019926266));
#183809=CARTESIAN_POINT('Ctrl Pts',(137.96098239871,-3.27502631919018,125.874155400811));
#183810=CARTESIAN_POINT('Ctrl Pts',(137.968389745063,-3.14160499327923,
125.790554814715));
#183811=CARTESIAN_POINT('Ctrl Pts',(137.975791566739,-3.00828317802684,
125.70701658109));
#183812=CARTESIAN_POINT('Ctrl Pts',(137.983193388414,-2.87152314723186,
125.628734666894));
#183813=CARTESIAN_POINT('Ctrl Pts',(137.990595210089,-2.73178040618521,
125.55599836112));
#183814=CARTESIAN_POINT('Ctrl Pts',(137.997993124401,-2.5921114342442,125.483300452276));
#183815=CARTESIAN_POINT('Ctrl Pts',(138.005391038712,-2.44946321813233,
125.416142493546));
#183816=CARTESIAN_POINT('Ctrl Pts',(138.012788953023,-2.30431740720409,
125.354768720061));
#183817=CARTESIAN_POINT('Ctrl Pts',(138.020185637936,-2.15919571687599,
125.293405145783));
#183818=CARTESIAN_POINT('Ctrl Pts',(138.027582322848,-2.01157759898021,
125.237823994241));
#183819=CARTESIAN_POINT('Ctrl Pts',(138.03497900776,-1.86196641298671,125.188222118614));
#183820=CARTESIAN_POINT('Ctrl Pts',(138.042375364695,-1.71236186091009,
125.138622442387));
#183821=CARTESIAN_POINT('Ctrl Pts',(138.049771721631,-1.56076477078605,
125.095001632386));
#183822=CARTESIAN_POINT('Ctrl Pts',(138.057168078566,-1.40769520274225,
125.057507149913));
#183823=CARTESIAN_POINT('Ctrl Pts',(138.064565567903,-1.25460219935681,
125.020006926938));
#183824=CARTESIAN_POINT('Ctrl Pts',(138.071963057239,-1.10003663177245,
124.988634987906));
#183825=CARTESIAN_POINT('Ctrl Pts',(138.079360546576,-0.944530182811315,
124.963487969043));
#183826=CARTESIAN_POINT('Ctrl Pts',(138.086760629091,-0.788969221304679,
124.938332134932));
#183827=CARTESIAN_POINT('Ctrl Pts',(138.094160711606,-0.632467090023876,
124.919405625163));
#183828=CARTESIAN_POINT('Ctrl Pts',(138.101560794121,-0.475561895459883,
124.906753353083));
#183829=CARTESIAN_POINT('Ctrl Pts',(138.108969013787,-0.31848416750478,
124.894087168528));
#183830=CARTESIAN_POINT('Ctrl Pts',(138.116377233454,-0.161002863466468,
124.887709029779));
#183831=CARTESIAN_POINT('Ctrl Pts',(138.12378545312,-0.00365814210466802,
124.887611748424));
#183832=CARTESIAN_POINT('Ctrl Pts',(138.131198232422,0.153783422307805,
124.887514407193));
#183833=CARTESIAN_POINT('Ctrl Pts',(138.138611011724,0.311087864390723,
124.893705611727));
#183834=CARTESIAN_POINT('Ctrl Pts',(138.146023791026,0.4677193546816,124.906126206511));
#183835=CARTESIAN_POINT('Ctrl Pts',(138.153447162055,0.624574647391092,
124.918564548423));
#183836=CARTESIAN_POINT('Ctrl Pts',(138.160870533084,0.780754698214678,
124.937250013342));
#183837=CARTESIAN_POINT('Ctrl Pts',(138.168293904113,0.935732260909257,
124.962072050712));
#183838=CARTESIAN_POINT('Ctrl Pts',(138.172229953553,1.01790508328725,124.975233290522));
#183839=CARTESIAN_POINT('Ctrl Pts',(138.176166002994,1.09974005804813,124.990118896725));
#183840=CARTESIAN_POINT('Ctrl Pts',(138.180102052435,1.18116035903808,125.006706715449));
#183841=CARTESIAN_POINT('Ctrl Pts',(138.187525318841,1.33471650566103,125.037990823872));
#183842=CARTESIAN_POINT('Ctrl Pts',(138.194948585246,1.48726110624673,125.07542706292));
#183843=CARTESIAN_POINT('Ctrl Pts',(138.202371851651,1.63826267605801,125.118938384632));
#183844=CARTESIAN_POINT('Ctrl Pts',(138.209786344373,1.7890857745541,125.162398279576));
#183845=CARTESIAN_POINT('Ctrl Pts',(138.217200837094,1.93836911722859,125.211918862519));
#183846=CARTESIAN_POINT('Ctrl Pts',(138.224615329815,2.08559010884906,125.267371863706));
#183847=CARTESIAN_POINT('Ctrl Pts',(138.232022676168,2.23266920333493,125.322771417202));
#183848=CARTESIAN_POINT('Ctrl Pts',(138.239430022522,2.37768955703574,125.384091875053));
#183849=CARTESIAN_POINT('Ctrl Pts',(138.246837368876,2.52014258346241,125.451154856387));
#183850=CARTESIAN_POINT('Ctrl Pts',(138.254239190551,2.66248936304763,125.51816781962));
#183851=CARTESIAN_POINT('Ctrl Pts',(138.261641012227,2.80227229171358,125.590914620009));
#183852=CARTESIAN_POINT('Ctrl Pts',(138.269042833902,2.93900177070275,125.669168395818));
#183853=CARTESIAN_POINT('Ctrl Pts',(138.276440748213,3.07565907126367,125.747380862067));
#183854=CARTESIAN_POINT('Ctrl Pts',(138.283838662525,3.20926580914066,125.831094329171));
#183855=CARTESIAN_POINT('Ctrl Pts',(138.291236576836,3.33935615915975,125.920035586942));
#183856=CARTESIAN_POINT('Ctrl Pts',(138.298633261748,3.46942489052312,126.008962064289));
#183857=CARTESIAN_POINT('Ctrl Pts',(138.306029946661,3.59597808595126,126.103114397584));
#183858=CARTESIAN_POINT('Ctrl Pts',(138.313426631573,3.71857804920002,126.2021755002));
#183859=CARTESIAN_POINT('Ctrl Pts',(138.320822988508,3.84117257623801,126.301232210343));
#183860=CARTESIAN_POINT('Ctrl Pts',(138.328219345444,3.95981392927376,126.405197022414));
#183861=CARTESIAN_POINT('Ctrl Pts',(138.335615702379,4.07409693973764,126.513712101535));
#183862=CARTESIAN_POINT('Ctrl Pts',(138.343013191716,4.18839744722169,126.62224379459));
#183863=CARTESIAN_POINT('Ctrl Pts',(138.350410681052,4.29833801278211,126.735326884774));
#183864=CARTESIAN_POINT('Ctrl Pts',(138.357808170389,4.4035499460711,126.852566286511));
#183865=CARTESIAN_POINT('Ctrl Pts',(138.365208252904,4.50879876124089,126.96984678634));
#183866=CARTESIAN_POINT('Ctrl Pts',(138.372608335419,4.60931539467053,127.091286220921));
#183867=CARTESIAN_POINT('Ctrl Pts',(138.380008417934,4.70477119978698,127.216456142785));
#183868=CARTESIAN_POINT('Ctrl Pts',(138.3874166376,4.80033196837398,127.341763701845));
#183869=CARTESIAN_POINT('Ctrl Pts',(138.394824857267,4.89082056866922,127.470809643247));
#183870=CARTESIAN_POINT('Ctrl Pts',(138.402233076933,4.97595107948322,127.603135630613));
#183871=CARTESIAN_POINT('Ctrl Pts',(138.409645856235,5.06113398670645,127.735543062418));
#183872=CARTESIAN_POINT('Ctrl Pts',(138.417058635538,5.14095204430903,127.871234241915));
#183873=CARTESIAN_POINT('Ctrl Pts',(138.42447141484,5.21516539258678,128.009726385602));
#183874=CARTESIAN_POINT('Ctrl Pts',(138.431894785868,5.28948478037655,128.148416413358));
#183875=CARTESIAN_POINT('Ctrl Pts',(138.439318156897,5.35818330192005,128.289915063571));
#183876=CARTESIAN_POINT('Ctrl Pts',(138.446741527926,5.4210689770581,128.433718993769));
#183877=CARTESIAN_POINT('Ctrl Pts',(138.450677577367,5.45441247093785,128.509967288089));
#183878=CARTESIAN_POINT('Ctrl Pts',(138.454613626808,5.48612259164549,128.586863403795));
#183879=CARTESIAN_POINT('Ctrl Pts',(138.458549676248,5.51617645144817,128.664330730161));
#183880=CARTESIAN_POINT('Ctrl Pts',(138.465972942654,5.57285709308646,128.810431690011));
#183881=CARTESIAN_POINT('Ctrl Pts',(138.473396209059,5.62381500765201,128.959006984408));
#183882=CARTESIAN_POINT('Ctrl Pts',(138.480819475465,5.66882773729218,129.109567813886));
#183883=CARTESIAN_POINT('Ctrl Pts',(138.488233968186,5.71378726562398,129.259950692966));
#183884=CARTESIAN_POINT('Ctrl Pts',(138.495648460907,5.75281548986186,129.412314081771));
#183885=CARTESIAN_POINT('Ctrl Pts',(138.503062953628,5.78573785149633,129.566148973192));
#183886=CARTESIAN_POINT('Ctrl Pts',(138.510470299982,5.81862848131925,129.719835592754));
#183887=CARTESIAN_POINT('Ctrl Pts',(138.517877646335,5.84542488693863,129.874990528817));
#183888=CARTESIAN_POINT('Ctrl Pts',(138.525284992689,5.86600224181193,130.031089473945));
#183889=CARTESIAN_POINT('Ctrl Pts',(138.532686814365,5.88656424931753,130.18707199459));
#183890=CARTESIAN_POINT('Ctrl Pts',(138.54008863604,5.90091639318574,130.343996753884));
#183891=CARTESIAN_POINT('Ctrl Pts',(138.547490457715,5.90898489853239,130.501329214216));
#183892=CARTESIAN_POINT('Ctrl Pts',(138.554888372027,5.91704914457791,130.658578619969));
#183893=CARTESIAN_POINT('Ctrl Pts',(138.562286286338,5.91883633916288,130.81623492627));
#183894=CARTESIAN_POINT('Ctrl Pts',(138.569684200649,5.91432455187191,130.973758544428));
#183895=CARTESIAN_POINT('Ctrl Pts',(138.577080885562,5.90981351435814,131.131255985018));
#183896=CARTESIAN_POINT('Ctrl Pts',(138.584477570474,5.89900558318721,131.288620408449));
#183897=CARTESIAN_POINT('Ctrl Pts',(138.591874255386,5.8819309468065,131.445312175408));
#183898=CARTESIAN_POINT('Ctrl Pts',(138.599270612322,5.86485706753306,131.601996994489));
#183899=CARTESIAN_POINT('Ctrl Pts',(138.606666969257,5.84151707599249,131.758008845303));
#183900=CARTESIAN_POINT('Ctrl Pts',(138.614063326192,5.81199302529507,131.912813429562));
#183901=CARTESIAN_POINT('Ctrl Pts',(138.621460815529,5.7824644543901,132.067641714798));
#183902=CARTESIAN_POINT('Ctrl Pts',(138.628858304866,5.74675000907169,132.221261998736));
#183903=CARTESIAN_POINT('Ctrl Pts',(138.636255794202,5.70498279988453,132.37315053834));
#183904=CARTESIAN_POINT('Ctrl Pts',(138.643655876717,5.66320094926714,132.525092322235));
#183905=CARTESIAN_POINT('Ctrl Pts',(138.651055959232,5.61536220923463,132.675300793432));
#183906=CARTESIAN_POINT('Ctrl Pts',(138.658456041747,5.56164940327724,132.823267865937));
#183907=CARTESIAN_POINT('Ctrl Pts',(138.665864261414,5.50787753456762,132.971397643451));
#183908=CARTESIAN_POINT('Ctrl Pts',(138.67327248108,5.44821882806217,133.1172807491));
#183909=CARTESIAN_POINT('Ctrl Pts',(138.680680700747,5.38290434774678,133.260428887283));
#183910=CARTESIAN_POINT('Ctrl Pts',(138.688093480049,5.31754966745868,133.403665130756));
#183911=CARTESIAN_POINT('Ctrl Pts',(138.695506259351,5.24653244497277,133.544162720141));
#183912=CARTESIAN_POINT('Ctrl Pts',(138.702919038653,5.17012920969352,133.681458898399));
#183913=CARTESIAN_POINT('Ctrl Pts',(138.710342409682,5.09361680588854,133.818951251876));
#183914=CARTESIAN_POINT('Ctrl Pts',(138.71776578071,5.01170321296263,133.953232740431));
#183915=CARTESIAN_POINT('Ctrl Pts',(138.725189151739,4.92470813722807,134.083869776818));
#183916=CARTESIAN_POINT('Ctrl Pts',(138.72912520118,4.87858126065594,134.153136668103));
#183917=CARTESIAN_POINT('Ctrl Pts',(138.733061250621,4.83102647550725,134.221379519561));
#183918=CARTESIAN_POINT('Ctrl Pts',(138.736997300061,4.78209586517842,134.288537665126));
#183919=CARTESIAN_POINT('Ctrl Pts',(138.744420566467,4.6898142611695,134.415195831729));
#183920=CARTESIAN_POINT('Ctrl Pts',(138.751843832872,4.59235765566148,134.53837674423));
#183921=CARTESIAN_POINT('Ctrl Pts',(138.759267099278,4.49001704558511,134.657629034489));
#183922=CARTESIAN_POINT('Ctrl Pts',(138.766681591999,4.38779739361071,134.776740378444));
#183923=CARTESIAN_POINT('Ctrl Pts',(138.77409608472,4.28070546797207,134.891932062163));
#183924=CARTESIAN_POINT('Ctrl Pts',(138.781510577441,4.16907515762518,135.002782093856));
#183925=CARTESIAN_POINT('Ctrl Pts',(138.788917923794,4.05755244077452,135.113525284114));
#183926=CARTESIAN_POINT('Ctrl Pts',(138.796325270148,3.94150031062554,135.219934891887));
#183927=CARTESIAN_POINT('Ctrl Pts',(138.803732616502,3.82129241007672,135.321622496093));
#183928=CARTESIAN_POINT('Ctrl Pts',(138.811134438177,3.70117416511497,135.423234257847));
#183929=CARTESIAN_POINT('Ctrl Pts',(138.818536259853,3.57690660511175,135.520130788457));
#183930=CARTESIAN_POINT('Ctrl Pts',(138.825938081528,3.44889957457064,135.611961088386));
#183931=CARTESIAN_POINT('Ctrl Pts',(138.83333599584,3.32096011794519,135.703742911814));
#183932=CARTESIAN_POINT('Ctrl Pts',(138.840733910151,3.18928542472388,135.790463613759));
#183933=CARTESIAN_POINT('Ctrl Pts',(138.848131824462,3.05431761223031,135.871813082673));
#183934=CARTESIAN_POINT('Ctrl Pts',(138.855528509374,2.91937222893831,135.953149032781));
#183935=CARTESIAN_POINT('Ctrl Pts',(138.862925194287,2.78113513191781,136.029115328895));
#183936=CARTESIAN_POINT('Ctrl Pts',(138.870321879199,2.64007665259938,136.099445681179));
#183937=CARTESIAN_POINT('Ctrl Pts',(138.877718236134,2.49902442796164,136.169772914942));
#183938=CARTESIAN_POINT('Ctrl Pts',(138.88511459307,2.35515140384878,136.234464535202));
#183939=CARTESIAN_POINT('Ctrl Pts',(138.892510950005,2.20895145225117,136.29330077429));
#183940=CARTESIAN_POINT('Ctrl Pts',(138.899908439342,2.06272911706785,136.352146021356));
#183941=CARTESIAN_POINT('Ctrl Pts',(138.907305928678,1.91417949137052,136.405133962877));
#183942=CARTESIAN_POINT('Ctrl Pts',(138.914703418015,1.7638151645086,136.452093492619));
#183943=CARTESIAN_POINT('Ctrl Pts',(138.92210350053,1.61339812766402,136.499069483951));
#183944=CARTESIAN_POINT('Ctrl Pts',(138.929503583045,1.46116547920626,136.540012744826));
#183945=CARTESIAN_POINT('Ctrl Pts',(138.93690366556,1.30764350683274,136.574802456935));
#183946=CARTESIAN_POINT('Ctrl Pts',(138.944311885226,1.15395272126881,136.609630423908));
#183947=CARTESIAN_POINT('Ctrl Pts',(138.951720104893,0.998970144751367,
136.638291246499));
#183948=CARTESIAN_POINT('Ctrl Pts',(138.959128324559,0.843231489926721,
136.660715389683));
#183949=CARTESIAN_POINT('Ctrl Pts',(138.966541103861,0.687396980558781,
136.683153334553));
#183950=CARTESIAN_POINT('Ctrl Pts',(138.973953883163,0.530805836065061,
136.69934691287));
#183951=CARTESIAN_POINT('Ctrl Pts',(138.981366662465,0.373996857945198,
136.709278645172));
#183952=CARTESIAN_POINT('Ctrl Pts',(138.988790033494,0.216963823803561,
136.719224568399));
#183953=CARTESIAN_POINT('Ctrl Pts',(138.996213404523,0.0597127066057581,
136.722890767328));
#183954=CARTESIAN_POINT('Ctrl Pts',(139.003636775552,-0.0972188953469484,
136.720311855439));
#183955=CARTESIAN_POINT('Ctrl Pts',(139.007572824993,-0.180427796224534,
136.718944454475));
#183956=CARTESIAN_POINT('Ctrl Pts',(139.011508874433,-0.263546962858581,
136.715822195045));
#183957=CARTESIAN_POINT('Ctrl Pts',(139.015444923874,-0.346497202820251,
136.710956104895));
#183958=CARTESIAN_POINT('Ctrl Pts',(139.022868190279,-0.502938766598866,
136.701778810738));
#183959=CARTESIAN_POINT('Ctrl Pts',(139.030291456685,-0.659252032738175,
136.686368100478));
#183960=CARTESIAN_POINT('Ctrl Pts',(139.03771472309,-0.814899961487367,
136.664724822568));
#183961=CARTESIAN_POINT('Ctrl Pts',(139.045129215811,-0.970363927311087,
136.643107125215));
#183962=CARTESIAN_POINT('Ctrl Pts',(139.052543708532,-1.12516375489571,
136.615271573938));
#183963=CARTESIAN_POINT('Ctrl Pts',(139.059958201253,-1.27876393545895,
136.581270982101));
#183964=CARTESIAN_POINT('Ctrl Pts',(139.067365547607,-1.43221607038478,
136.547303161314));
#183965=CARTESIAN_POINT('Ctrl Pts',(139.074772893961,-1.58447049815674,
136.507182209653));
#183966=CARTESIAN_POINT('Ctrl Pts',(139.082180240315,-1.73499846600558,
136.461012532388));
#183967=CARTESIAN_POINT('Ctrl Pts',(139.08958206199,-1.8854141644169,136.41487729021));
#183968=CARTESIAN_POINT('Ctrl Pts',(139.096983883665,-2.03410561145598,
136.362702414163));
#183969=CARTESIAN_POINT('Ctrl Pts',(139.104385705341,-2.18055597030818,
136.304642994213));
#183970=CARTESIAN_POINT('Ctrl Pts',(139.111783619652,-2.32692901915716,
136.246614223378));
#183971=CARTESIAN_POINT('Ctrl Pts',(139.119181533963,-2.47106298978218,
136.182707232422));
#183972=CARTESIAN_POINT('Ctrl Pts',(139.126579448275,-2.61245800134243,
136.113126364302));
#183973=CARTESIAN_POINT('Ctrl Pts',(139.133976133187,-2.75382951561592,
136.043557059261));
#183974=CARTESIAN_POINT('Ctrl Pts',(139.141372818099,-2.89246263958192,
135.968315913089));
#183975=CARTESIAN_POINT('Ctrl Pts',(139.148769503011,-3.02787911043441,
135.887654692779));
#183976=CARTESIAN_POINT('Ctrl Pts',(139.156165859947,-3.16328957677839,
135.806997049072));
#183977=CARTESIAN_POINT('Ctrl Pts',(139.163562216882,-3.29548335289159,
135.720920000121));
#183978=CARTESIAN_POINT('Ctrl Pts',(139.170958573817,-3.42400859213571,
135.629720264627));
#183979=CARTESIAN_POINT('Ctrl Pts',(139.178356063154,-3.55255350892234,
135.538506566219));
#183980=CARTESIAN_POINT('Ctrl Pts',(139.185753552491,-3.67742846603564,
135.44216883567));
#183981=CARTESIAN_POINT('Ctrl Pts',(139.193151041827,-3.79821243989223,
135.341045841818));
#183982=CARTESIAN_POINT('Ctrl Pts',(139.200551124342,-3.91903875438439,
135.239887399457));
#183983=CARTESIAN_POINT('Ctrl Pts',(139.207951206857,-4.03577094431272,
135.133940593454));
#183984=CARTESIAN_POINT('Ctrl Pts',(139.215351289372,-4.14802289045598,
135.023582899309));
#183985=CARTESIAN_POINT('Ctrl Pts',(139.222759509039,-4.26039826915299,
134.913103855534));
#183986=CARTESIAN_POINT('Ctrl Pts',(139.230167728705,-4.36828329918245,
134.798204499265));
#183987=CARTESIAN_POINT('Ctrl Pts',(139.237575948372,-4.47132991298856,
134.679297955345));
#183988=CARTESIAN_POINT('Ctrl Pts',(139.244988727674,-4.57443995026648,
134.56031822643));
#183989=CARTESIAN_POINT('Ctrl Pts',(139.252401506976,-4.6727054048812,134.437326686306));
#183990=CARTESIAN_POINT('Ctrl Pts',(139.259814286278,-4.7658203354942,134.310767195858));
#183991=CARTESIAN_POINT('Ctrl Pts',(139.267237657306,-4.85906831308645,
134.184026871275));
#183992=CARTESIAN_POINT('Ctrl Pts',(139.274661028335,-4.94715085999547,
134.053708722867));
#183993=CARTESIAN_POINT('Ctrl Pts',(139.282084399364,-5.02980651250673,
133.920283756741));
#183994=CARTESIAN_POINT('Ctrl Pts',(139.286020448805,-5.0736325227633,133.849538638213));
#183995=CARTESIAN_POINT('Ctrl Pts',(139.289956498246,-5.11593361734224,
133.77792047178));
#183996=CARTESIAN_POINT('Ctrl Pts',(139.293892547686,-5.15667626875567,
133.70550184504));
#183997=CARTESIAN_POINT('Ctrl Pts',(139.301655844179,-5.23703534137144,
133.562666426064));
#183998=CARTESIAN_POINT('Ctrl Pts',(139.309419140672,-5.31155351039293,
133.416316834427));
#183999=CARTESIAN_POINT('Ctrl Pts',(139.317182437165,-5.37992469322463,
133.26694886121));
#184000=CARTESIAN_POINT('Ctrl Pts',(139.324933467789,-5.44818785081589,
133.117816886707));
#184001=CARTESIAN_POINT('Ctrl Pts',(139.332684498413,-5.5103232440121,132.965676328053));
#184002=CARTESIAN_POINT('Ctrl Pts',(139.340435529037,-5.56606974513515,
132.81104897274));
#184003=CARTESIAN_POINT('Ctrl Pts',(139.348451302267,-5.62372031227101,
132.65114019732));
#184004=CARTESIAN_POINT('Ctrl Pts',(139.356467075497,-5.67453761797106,
132.488572011555));
#184005=CARTESIAN_POINT('Ctrl Pts',(139.364482848727,-5.71828491622516,
132.323948778671));
#184006=CARTESIAN_POINT('Ctrl Pts',(139.37220791147,-5.76044561790614,132.165295986652));
#184007=CARTESIAN_POINT('Ctrl Pts',(139.379932974214,-5.79603998975774,
132.004734941028));
#184008=CARTESIAN_POINT('Ctrl Pts',(139.387658036958,-5.82490506791931,
131.842826559342));
#184009=CARTESIAN_POINT('Ctrl Pts',(139.395374508062,-5.85373804299438,
131.681098248492));
#184010=CARTESIAN_POINT('Ctrl Pts',(139.403090979166,-5.87585658124932,
131.518025905713));
#184011=CARTESIAN_POINT('Ctrl Pts',(139.41080745027,-5.89114804590412,131.354183556102));
#184012=CARTESIAN_POINT('Ctrl Pts',(139.418513889541,-5.90641963082197,
131.190554210469));
#184013=CARTESIAN_POINT('Ctrl Pts',(139.426220328812,-5.91488181128325,
131.026157176566));
#184014=CARTESIAN_POINT('Ctrl Pts',(139.433926768083,-5.91647336974226,
130.861574493773));
#184015=CARTESIAN_POINT('Ctrl Pts',(139.434826114654,-5.91665910566928,
130.84236758561));
#184016=CARTESIAN_POINT('Ctrl Pts',(139.435725461224,-5.9167513280669,130.82315815739));
#184017=CARTESIAN_POINT('Ctrl Pts',(139.436624807795,-5.91674998555258,
130.80394714016));
#184018=CARTESIAN_POINT('',(141.186624807795,-5.91699976706494,130.799049164418));
#184019=CARTESIAN_POINT('Ctrl Pts',(139.436624807833,-5.91674998555252,
130.803947139341));
#184020=CARTESIAN_POINT('Ctrl Pts',(139.444414740142,-5.9167383569805,130.637545744475));
#184021=CARTESIAN_POINT('Ctrl Pts',(139.452204672452,-5.90970268366904,
130.471295336118));
#184022=CARTESIAN_POINT('Ctrl Pts',(139.459994604761,-5.8957067789312,130.30579052283));
#184023=CARTESIAN_POINT('Ctrl Pts',(139.467795773126,-5.8816906867568,130.140046988432));
#184024=CARTESIAN_POINT('Ctrl Pts',(139.475596941491,-5.86069434653312,
129.975051505079));
#184025=CARTESIAN_POINT('Ctrl Pts',(139.483398109855,-5.83283296513644,
129.811390243729));
#184026=CARTESIAN_POINT('Ctrl Pts',(139.491218767466,-5.80490197912712,
129.647320116124));
#184027=CARTESIAN_POINT('Ctrl Pts',(139.499039425076,-5.77007170382882,
129.484591184027));
#184028=CARTESIAN_POINT('Ctrl Pts',(139.506860082686,-5.72850826458461,
129.323778426303));
#184029=CARTESIAN_POINT('Ctrl Pts',(139.514690882978,-5.68689092134039,
129.162757109059));
#184030=CARTESIAN_POINT('Ctrl Pts',(139.52252168327,-5.63852307109696,129.003657224133));
#184031=CARTESIAN_POINT('Ctrl Pts',(139.530352483562,-5.58361987152639,
128.847035991247));
#184032=CARTESIAN_POINT('Ctrl Pts',(139.538201730399,-5.5285873397904,128.690045815141));
#184033=CARTESIAN_POINT('Ctrl Pts',(139.546050977236,-5.46698878344372,
128.535546258075));
#184034=CARTESIAN_POINT('Ctrl Pts',(139.553900224074,-5.39908734484855,
128.384074187162));
#184035=CARTESIAN_POINT('Ctrl Pts',(139.560046873215,-5.34591455923882,
128.265458262093));
#184036=CARTESIAN_POINT('Ctrl Pts',(139.566193522357,-5.28887763188302,
128.148698427508));
#184037=CARTESIAN_POINT('Ctrl Pts',(139.572340171499,-5.22812176134569,
128.034040525764));
#184038=CARTESIAN_POINT('Ctrl Pts',(139.579763437905,-5.15474730930144,
127.895568956866));
#184039=CARTESIAN_POINT('Ctrl Pts',(139.58718670431,-5.07575678829435,127.759805100288));
#184040=CARTESIAN_POINT('Ctrl Pts',(139.594609970715,-4.99137419954193,
127.627237050147));
#184041=CARTESIAN_POINT('Ctrl Pts',(139.602024463436,-4.90709134400182,
127.494825684433));
#184042=CARTESIAN_POINT('Ctrl Pts',(139.609438956157,-4.81742930465359,
127.365602918501));
#184043=CARTESIAN_POINT('Ctrl Pts',(139.616853448878,-4.72265870931268,
127.240033853947));
#184044=CARTESIAN_POINT('Ctrl Pts',(139.624260795232,-4.62797945743952,
127.114585817584));
#184045=CARTESIAN_POINT('Ctrl Pts',(139.631668141586,-4.52820167529697,
126.992784767797));
#184046=CARTESIAN_POINT('Ctrl Pts',(139.63907548794,-4.42364010616832,126.875068216433));
#184047=CARTESIAN_POINT('Ctrl Pts',(139.646477309615,-4.3191565230031,126.757439462515));
#184048=CARTESIAN_POINT('Ctrl Pts',(139.653879131291,-4.20989650391839,
126.643889419174));
#184049=CARTESIAN_POINT('Ctrl Pts',(139.661280952966,-4.09621593772498,
126.534823692556));
#184050=CARTESIAN_POINT('Ctrl Pts',(139.668678867277,-3.98259538261721,
126.425815540885));
#184051=CARTESIAN_POINT('Ctrl Pts',(139.676076781589,-3.8645591965125,126.321287249256));
#184052=CARTESIAN_POINT('Ctrl Pts',(139.6834746959,-3.74250101662348,126.221608529238));
#184053=CARTESIAN_POINT('Ctrl Pts',(139.690871380812,-3.62046312058982,
126.121946374016));
#184054=CARTESIAN_POINT('Ctrl Pts',(139.698268065725,-3.49440484616371,
126.0271324268));
#184055=CARTESIAN_POINT('Ctrl Pts',(139.705664750637,-3.36475397762668,
125.937497024599));
#184056=CARTESIAN_POINT('Ctrl Pts',(139.713061107572,-3.23510885794502,
125.847865596926));
#184057=CARTESIAN_POINT('Ctrl Pts',(139.720457464508,-3.10187176795193,
125.763412469989));
#184058=CARTESIAN_POINT('Ctrl Pts',(139.727853821443,-2.96550039594985,
125.684425269915));
#184059=CARTESIAN_POINT('Ctrl Pts',(139.73525131078,-2.82910814514249,125.6054259767));
#184060=CARTESIAN_POINT('Ctrl Pts',(139.742648800116,-2.68958097989421,
125.531894463733));
#184061=CARTESIAN_POINT('Ctrl Pts',(139.750046289453,-2.5474020217075,125.464072844206));
#184062=CARTESIAN_POINT('Ctrl Pts',(139.757446371968,-2.40517322290756,
125.396227449915));
#184063=CARTESIAN_POINT('Ctrl Pts',(139.764846454483,-2.26029111709618,
125.334096094844));
#184064=CARTESIAN_POINT('Ctrl Pts',(139.772246536998,-2.11325952156014,
125.277873057005));
#184065=CARTESIAN_POINT('Ctrl Pts',(139.779654756665,-1.96606624966948,
125.221588196156));
#184066=CARTESIAN_POINT('Ctrl Pts',(139.787062976331,-1.81671911670941,
125.171224760489));
#184067=CARTESIAN_POINT('Ctrl Pts',(139.794471195998,-1.66573854684275,
125.126927601135));
#184068=CARTESIAN_POINT('Ctrl Pts',(139.8018839753,-1.51466505095442,125.082603177618));
#184069=CARTESIAN_POINT('Ctrl Pts',(139.809296754602,-1.36195647613885,
125.044352560755));
#184070=CARTESIAN_POINT('Ctrl Pts',(139.816709533904,-1.20814369104697,
125.012269511214));
#184071=CARTESIAN_POINT('Ctrl Pts',(139.824132904933,-1.05411113103469,
124.980140619907));
#184072=CARTESIAN_POINT('Ctrl Pts',(139.831556275961,-0.898971576840442,
124.954196957889));
#184073=CARTESIAN_POINT('Ctrl Pts',(139.83897964699,-0.743262098289538,
124.934480549307));
#184074=CARTESIAN_POINT('Ctrl Pts',(139.842915696431,-0.660701196564727,
124.924026436388));
#184075=CARTESIAN_POINT('Ctrl Pts',(139.846851745872,-0.577980099564831,
124.915322157159));
#184076=CARTESIAN_POINT('Ctrl Pts',(139.850787795312,-0.495178763206054,
124.908368033194));
#184077=CARTESIAN_POINT('Ctrl Pts',(139.858211061718,-0.339018026973734,
124.895252772426));
#184078=CARTESIAN_POINT('Ctrl Pts',(139.865634328123,-0.182099743347254,
124.88832605418));
#184079=CARTESIAN_POINT('Ctrl Pts',(139.873057594529,-0.0249556378615223,
124.887663246681));
#184080=CARTESIAN_POINT('Ctrl Pts',(139.88047208725,0.132002736341643,124.887001222565));
#184081=CARTESIAN_POINT('Ctrl Pts',(139.887886579971,0.289186031483495,
124.892588374202));
#184082=CARTESIAN_POINT('Ctrl Pts',(139.895301072692,0.446056663475881,
124.904448413518));
#184083=CARTESIAN_POINT('Ctrl Pts',(139.902708419046,0.60277609764719,124.916297021683));
#184084=CARTESIAN_POINT('Ctrl Pts',(139.910115765399,0.759183098873836,
124.934406453087));
#184085=CARTESIAN_POINT('Ctrl Pts',(139.917523111753,0.914739449614415,
124.958748391133));
#184086=CARTESIAN_POINT('Ctrl Pts',(139.924924933429,1.07017978055975,124.983072174044));
#184087=CARTESIAN_POINT('Ctrl Pts',(139.932326755104,1.22477035706669,125.013619150465));
#184088=CARTESIAN_POINT('Ctrl Pts',(139.939728576779,1.37797756460276,125.050309141089));
#184089=CARTESIAN_POINT('Ctrl Pts',(139.947126491091,1.53110389524665,125.086979763352));
#184090=CARTESIAN_POINT('Ctrl Pts',(139.954524405402,1.68284794917277,125.129786854809));
#184091=CARTESIAN_POINT('Ctrl Pts',(139.961922319713,1.83268590703819,125.17859907546));
#184092=CARTESIAN_POINT('Ctrl Pts',(139.969319004626,1.98249896455313,125.227403184404));
#184093=CARTESIAN_POINT('Ctrl Pts',(139.976715689538,2.13040620008801,125.282210326405));
#184094=CARTESIAN_POINT('Ctrl Pts',(139.98411237445,2.27589846390889,125.342839149653));
#184095=CARTESIAN_POINT('Ctrl Pts',(139.991508731385,2.42138427645033,125.403465284555));
#184096=CARTESIAN_POINT('Ctrl Pts',(139.998905088321,2.56445498561727,125.469912443845));
#184097=CARTESIAN_POINT('Ctrl Pts',(140.006301445256,2.70462121169588,125.541951030338));
#184098=CARTESIAN_POINT('Ctrl Pts',(140.013698934593,2.84480889758158,125.614000646124));
#184099=CARTESIAN_POINT('Ctrl Pts',(140.021096423929,2.98209088291864,125.691643222996));
#184100=CARTESIAN_POINT('Ctrl Pts',(140.028493913266,3.11600233204865,125.774603165246));
#184101=CARTESIAN_POINT('Ctrl Pts',(140.035893995781,3.24996072362956,125.857592188976));
#184102=CARTESIAN_POINT('Ctrl Pts',(140.043294078296,3.38054590943538,125.94590209281));
#184103=CARTESIAN_POINT('Ctrl Pts',(140.050694160811,3.50732211232254,126.03921401301));
#184104=CARTESIAN_POINT('Ctrl Pts',(140.058102380477,3.63423771867769,126.132628539258));
#184105=CARTESIAN_POINT('Ctrl Pts',(140.065510600144,3.75733567684197,126.231055844775));
#184106=CARTESIAN_POINT('Ctrl Pts',(140.07291881981,3.87621281748567,126.334136377546));
#184107=CARTESIAN_POINT('Ctrl Pts',(140.080331599112,3.99516312502599,126.437280354666));
#184108=CARTESIAN_POINT('Ctrl Pts',(140.087744378415,4.10988716710901,126.545083010852));
#184109=CARTESIAN_POINT('Ctrl Pts',(140.095157157717,4.22001911275532,126.657148391205));
#184110=CARTESIAN_POINT('Ctrl Pts',(140.102580528745,4.33030842009029,126.769373895829));
#184111=CARTESIAN_POINT('Ctrl Pts',(140.110003899774,4.43599227624557,126.885874013523));
#184112=CARTESIAN_POINT('Ctrl Pts',(140.117427270803,4.53674502575533,127.006219607311));
#184113=CARTESIAN_POINT('Ctrl Pts',(140.121363320244,4.59016655107471,127.07002972879));
#184114=CARTESIAN_POINT('Ctrl Pts',(140.125299369685,4.64220248121217,127.134920454943));
#184115=CARTESIAN_POINT('Ctrl Pts',(140.129235419125,4.69280932749273,127.200824690411));
#184116=CARTESIAN_POINT('Ctrl Pts',(140.136658685531,4.78825226019181,127.325118021702));
#184117=CARTESIAN_POINT('Ctrl Pts',(140.144081951936,4.87889806966939,127.453393757467));
#184118=CARTESIAN_POINT('Ctrl Pts',(140.151505218342,4.96439593586349,127.585245280322));
#184119=CARTESIAN_POINT('Ctrl Pts',(140.158919711063,5.04979275068001,127.716940965626));
#184120=CARTESIAN_POINT('Ctrl Pts',(140.166334203784,5.1300535322111,127.852203715424));
#184121=CARTESIAN_POINT('Ctrl Pts',(140.173748696505,5.20486775361052,127.990594061875));
#184122=CARTESIAN_POINT('Ctrl Pts',(140.181156042858,5.27960986624664,128.128851022499));
#184123=CARTESIAN_POINT('Ctrl Pts',(140.188563389212,5.348915693337,128.270229252329));
#184124=CARTESIAN_POINT('Ctrl Pts',(140.195970735566,5.41251813870924,128.414260627891));
#184125=CARTESIAN_POINT('Ctrl Pts',(140.203372557241,5.47607314697814,128.558184579419));
#184126=CARTESIAN_POINT('Ctrl Pts',(140.210774378917,5.5339330932668,128.704757396574));
#184127=CARTESIAN_POINT('Ctrl Pts',(140.218176200592,5.58587700300791,128.853486795463));
#184128=CARTESIAN_POINT('Ctrl Pts',(140.225574114904,5.63779349196338,129.00213768126));
#184129=CARTESIAN_POINT('Ctrl Pts',(140.232972029215,5.68380004126205,129.152942529997));
#184130=CARTESIAN_POINT('Ctrl Pts',(140.240369943526,5.72372401381683,129.305389645146));
#184131=CARTESIAN_POINT('Ctrl Pts',(140.247766628439,5.76364135173166,129.457811426351));
#184132=CARTESIAN_POINT('Ctrl Pts',(140.255163313351,5.79747802458901,129.611874571548));
#184133=CARTESIAN_POINT('Ctrl Pts',(140.262559998263,5.82511140093468,129.767052693562));
#184134=CARTESIAN_POINT('Ctrl Pts',(140.269956355198,5.85274355198747,129.922223934816));
#184135=CARTESIAN_POINT('Ctrl Pts',(140.277352712134,5.87417288799663,130.07850968707));
#184136=CARTESIAN_POINT('Ctrl Pts',(140.284749069069,5.88932805388643,130.235374118424));
#184137=CARTESIAN_POINT('Ctrl Pts',(140.292146558406,5.90448554007083,130.392262566123));
#184138=CARTESIAN_POINT('Ctrl Pts',(140.299544047743,5.91336690756985,130.54972949774));
#184139=CARTESIAN_POINT('Ctrl Pts',(140.306941537079,5.91595276783079,130.707234867658));
#184140=CARTESIAN_POINT('Ctrl Pts',(140.314341619594,5.91853953456102,130.864795450839));
#184141=CARTESIAN_POINT('Ctrl Pts',(140.321741702109,5.91482639404668,131.022394126134));
#184142=CARTESIAN_POINT('Ctrl Pts',(140.329141784624,5.90484606719343,131.17949190825));
#184143=CARTESIAN_POINT('Ctrl Pts',(140.336550004291,5.89485476594481,131.336762435527));
#184144=CARTESIAN_POINT('Ctrl Pts',(140.343958223957,5.87858253942994,131.493530596899));
#184145=CARTESIAN_POINT('Ctrl Pts',(140.351366443624,5.85611396607032,131.649262847943));
#184146=CARTESIAN_POINT('Ctrl Pts',(140.358779222926,5.83363156367869,131.805090949589));
#184147=CARTESIAN_POINT('Ctrl Pts',(140.366192002228,5.80494528293594,131.959881504242));
#184148=CARTESIAN_POINT('Ctrl Pts',(140.37360478153,5.77019051133239,132.113112704643));
#184149=CARTESIAN_POINT('Ctrl Pts',(140.381028152559,5.73538608048134,132.26656284897));
#184150=CARTESIAN_POINT('Ctrl Pts',(140.388451523587,5.69449593773427,132.418448829562));
#184151=CARTESIAN_POINT('Ctrl Pts',(140.395874894616,5.64770510344878,132.568264704238));
#184152=CARTESIAN_POINT('Ctrl Pts',(140.399810944057,5.62289548038023,132.647700675773));
#184153=CARTESIAN_POINT('Ctrl Pts',(140.403746993498,5.59642776595489,132.72655500006));
#184154=CARTESIAN_POINT('Ctrl Pts',(140.407683042938,5.56833490270679,132.804754822166));
#184155=CARTESIAN_POINT('Ctrl Pts',(140.415106309344,5.5153526393686,132.952237246126));
#184156=CARTESIAN_POINT('Ctrl Pts',(140.422529575749,5.45642690408131,133.097836301353));
#184157=CARTESIAN_POINT('Ctrl Pts',(140.429952842155,5.39171016875434,133.241037046362));
#184158=CARTESIAN_POINT('Ctrl Pts',(140.437367334876,5.32706992323409,133.384068539983));
#184159=CARTESIAN_POINT('Ctrl Pts',(140.444781827597,5.25665245388446,133.524707028831));
#184160=CARTESIAN_POINT('Ctrl Pts',(140.452196320318,5.18065965010269,133.662453714772));
#184161=CARTESIAN_POINT('Ctrl Pts',(140.459603666671,5.10474009104626,133.800067635271));
#184162=CARTESIAN_POINT('Ctrl Pts',(140.467011013025,5.02325607468222,133.934794977023));
#184163=CARTESIAN_POINT('Ctrl Pts',(140.474418359379,4.93645707454128,134.066157992283));
#184164=CARTESIAN_POINT('Ctrl Pts',(140.481820181054,4.84972281236938,134.19742303205));
#184165=CARTESIAN_POINT('Ctrl Pts',(140.48922200273,4.757681664416,134.325328431454));
#184166=CARTESIAN_POINT('Ctrl Pts',(140.496623824405,4.66062836091113,134.449422186864));
#184167=CARTESIAN_POINT('Ctrl Pts',(140.504021738717,4.56362629108983,134.573450434146));
#184168=CARTESIAN_POINT('Ctrl Pts',(140.511419653028,4.4616175645007,134.6936707514));
#184169=CARTESIAN_POINT('Ctrl Pts',(140.518817567339,4.35493937136174,134.809661309682));
#184170=CARTESIAN_POINT('Ctrl Pts',(140.526214252251,4.2482789062031,134.925632592438));
#184171=CARTESIAN_POINT('Ctrl Pts',(140.533610937164,4.13695076704041,135.037375236797));
#184172=CARTESIAN_POINT('Ctrl Pts',(140.541007622076,4.02133153301469,135.14450154432));
#184173=CARTESIAN_POINT('Ctrl Pts',(140.548403979011,3.90571742566694,135.251623101749));
#184174=CARTESIAN_POINT('Ctrl Pts',(140.555800335947,3.78581287560716,135.354128475629));
#184175=CARTESIAN_POINT('Ctrl Pts',(140.563196692882,3.66203012422643,135.451668002682));
#184176=CARTESIAN_POINT('Ctrl Pts',(140.570594182219,3.53822842139034,135.549222463287));
#184177=CARTESIAN_POINT('Ctrl Pts',(140.577991671555,3.41054762819856,135.641809332179));
#184178=CARTESIAN_POINT('Ctrl Pts',(140.585389160892,3.27943162033682,135.729120389376));
#184179=CARTESIAN_POINT('Ctrl Pts',(140.592789243407,3.14826964996188,135.816462053328));
#184180=CARTESIAN_POINT('Ctrl Pts',(140.600189325922,3.01367037786306,135.89852401661));
#184181=CARTESIAN_POINT('Ctrl Pts',(140.607589408437,2.87610495408147,135.975042473531));
#184182=CARTESIAN_POINT('Ctrl Pts',(140.614997628103,2.73838826297432,136.051645070362));
#184183=CARTESIAN_POINT('Ctrl Pts',(140.62240584777,2.59769923300498,136.122691805838));
#184184=CARTESIAN_POINT('Ctrl Pts',(140.629814067436,2.45453246690868,136.187965444389));
#184185=CARTESIAN_POINT('Ctrl Pts',(140.637226846738,2.31127758405667,136.253279257775));
#184186=CARTESIAN_POINT('Ctrl Pts',(140.644639626041,2.16554227108809,136.312812753108));
#184187=CARTESIAN_POINT('Ctrl Pts',(140.652052405343,2.01783871947345,136.366397786149));
#184188=CARTESIAN_POINT('Ctrl Pts',(140.659475776371,1.8699241220977,136.420059383997));
#184189=CARTESIAN_POINT('Ctrl Pts',(140.6668991474,1.72003602403849,136.467755431367));
#184190=CARTESIAN_POINT('Ctrl Pts',(140.674322518429,1.56870009680697,136.509368117016));
#184191=CARTESIAN_POINT('Ctrl Pts',(140.67825856787,1.48845815693258,136.53143216143));
#184192=CARTESIAN_POINT('Ctrl Pts',(140.682194617311,1.40780933448111,136.55178681208));
#184193=CARTESIAN_POINT('Ctrl Pts',(140.686130666751,1.32683273061614,136.570420404584));
#184194=CARTESIAN_POINT('Ctrl Pts',(140.693553933157,1.17411338292093,136.605562778511));
#184195=CARTESIAN_POINT('Ctrl Pts',(140.700977199562,1.01976597491551,136.634686734355));
#184196=CARTESIAN_POINT('Ctrl Pts',(140.708400465968,0.864306156244563,
136.657642212601));
#184197=CARTESIAN_POINT('Ctrl Pts',(140.715814958689,0.7090300781691,136.680570559379));
#184198=CARTESIAN_POINT('Ctrl Pts',(140.72322945141,0.552644572186405,136.697344886597));
#184199=CARTESIAN_POINT('Ctrl Pts',(140.730643944131,0.395678417444024,
136.707865436948));
#184200=CARTESIAN_POINT('Ctrl Pts',(140.738051290484,0.238863552591311,
136.718375847197));
#184201=CARTESIAN_POINT('Ctrl Pts',(140.745458636838,0.081469523095977,
136.722644455598));
#184202=CARTESIAN_POINT('Ctrl Pts',(140.752865983192,-0.0759668817954667,
136.720622916972));
#184203=CARTESIAN_POINT('Ctrl Pts',(140.760267804867,-0.233285864676519,
136.718602886085));
#184204=CARTESIAN_POINT('Ctrl Pts',(140.767669626543,-0.390646788362894,
136.710302054212));
#184205=CARTESIAN_POINT('Ctrl Pts',(140.775071448218,-0.547510060510293,
136.695724067239));
#184206=CARTESIAN_POINT('Ctrl Pts',(140.78246936253,-0.704290525757123,
136.681153775871));
#184207=CARTESIAN_POINT('Ctrl Pts',(140.789867276841,-0.860573491901972,
136.660312963175));
#184208=CARTESIAN_POINT('Ctrl Pts',(140.797265191152,-1.01582180275943,
136.633257307982));
#184209=CARTESIAN_POINT('Ctrl Pts',(140.804661876065,-1.17104431416416,
136.606206148948));
#184210=CARTESIAN_POINT('Ctrl Pts',(140.812058560977,-1.32523214413837,
136.572942261236));
#184211=CARTESIAN_POINT('Ctrl Pts',(140.819455245889,-1.47785556077945,
136.533572911064));
#184212=CARTESIAN_POINT('Ctrl Pts',(140.826851602824,-1.63047220993841,
136.494205306571));
#184213=CARTESIAN_POINT('Ctrl Pts',(140.83424795976,-1.78152422222521,136.448732871148));
#184214=CARTESIAN_POINT('Ctrl Pts',(140.841644316695,-1.93049458948127,
136.397313433609));
#184215=CARTESIAN_POINT('Ctrl Pts',(140.849041806032,-2.07948776448096,
136.345886123623));
#184216=CARTESIAN_POINT('Ctrl Pts',(140.856439295368,-2.22639830697387,
136.2885101204));
#184217=CARTESIAN_POINT('Ctrl Pts',(140.863836784705,-2.37072697710647,
136.225392268693));
#184218=CARTESIAN_POINT('Ctrl Pts',(140.87123686722,-2.51510624143075,136.162252291121));
#184219=CARTESIAN_POINT('Ctrl Pts',(140.878636949735,-2.65690148959547,
136.093366607084));
#184220=CARTESIAN_POINT('Ctrl Pts',(140.88603703225,-2.79563610629492,136.018989015034));
#184221=CARTESIAN_POINT('Ctrl Pts',(140.893445251916,-2.9345232759676,135.944529637176));
#184222=CARTESIAN_POINT('Ctrl Pts',(140.900853471583,-3.07034276389088,
135.86456646768));
#184223=CARTESIAN_POINT('Ctrl Pts',(140.908261691249,-3.2026444587668,135.779398208703));
#184224=CARTESIAN_POINT('Ctrl Pts',(140.915674470551,-3.33502758312833,
135.694177530085));
#184225=CARTESIAN_POINT('Ctrl Pts',(140.923087249853,-3.46388829527051,
135.603745592259));
#184226=CARTESIAN_POINT('Ctrl Pts',(140.930500029155,-3.58880827868209,
135.50844243035));
#184227=CARTESIAN_POINT('Ctrl Pts',(140.937923400184,-3.71390675362418,
135.413003094813));
#184228=CARTESIAN_POINT('Ctrl Pts',(140.945346771213,-3.83505296731995,
135.312678871508));
#184229=CARTESIAN_POINT('Ctrl Pts',(140.952770142242,-3.95186366354295,
135.207848342912));
#184230=CARTESIAN_POINT('Ctrl Pts',(140.956706191682,-4.01379949751447,
135.152264681276));
#184231=CARTESIAN_POINT('Ctrl Pts',(140.960642241123,-4.0745171000723,135.095414728721));
#184232=CARTESIAN_POINT('Ctrl Pts',(140.964578290564,-4.13396390152835,
135.037358730412));
#184233=CARTESIAN_POINT('Ctrl Pts',(140.971895211055,-4.24447255398932,
134.929435511951));
#184234=CARTESIAN_POINT('Ctrl Pts',(140.979212131547,-4.35094241740044,
134.816995737345));
#184235=CARTESIAN_POINT('Ctrl Pts',(140.986529052038,-4.45297372612522,
134.70037852781));
#184236=CARTESIAN_POINT('Ctrl Pts',(140.993837183181,-4.55488247116387,
134.58390140307));
#184237=CARTESIAN_POINT('Ctrl Pts',(141.001145314324,-4.65236301871726,
134.463257114099));
#184238=CARTESIAN_POINT('Ctrl Pts',(141.008453445466,-4.74505034526125,
134.338823488136));
#184239=CARTESIAN_POINT('Ctrl Pts',(141.01587725223,-4.83920475878625,134.212420283812));
#184240=CARTESIAN_POINT('Ctrl Pts',(141.023301058994,-4.92841261661277,
134.082107020091));
#184241=CARTESIAN_POINT('Ctrl Pts',(141.030724865757,-5.01233110107955,
133.948317916203));
#184242=CARTESIAN_POINT('Ctrl Pts',(141.038020045489,-5.09479558950856,
133.81684688119));
#184243=CARTESIAN_POINT('Ctrl Pts',(141.04531522522,-5.17215228161119,133.682019809762));
#184244=CARTESIAN_POINT('Ctrl Pts',(141.052610404951,-5.24411756057458,
133.544280611539));
#184245=CARTESIAN_POINT('Ctrl Pts',(141.05990249636,-5.31605237394326,133.406599723472));
#184246=CARTESIAN_POINT('Ctrl Pts',(141.067194587769,-5.38260013705376,
133.266009501727));
#184247=CARTESIAN_POINT('Ctrl Pts',(141.074486679178,-5.4435222173952,133.122980127366));
#184248=CARTESIAN_POINT('Ctrl Pts',(141.081777219704,-5.50443134082765,
132.979981172494));
#184249=CARTESIAN_POINT('Ctrl Pts',(141.089067760231,-5.55971701232054,
132.834544451499));
#184250=CARTESIAN_POINT('Ctrl Pts',(141.096358300758,-5.60918809127039,
132.687161594635));
#184251=CARTESIAN_POINT('Ctrl Pts',(141.103880509677,-5.6602311915705,132.535095415664));
#184252=CARTESIAN_POINT('Ctrl Pts',(141.111402718597,-5.70508387488403,
132.380957767139));
#184253=CARTESIAN_POINT('Ctrl Pts',(141.118924927517,-5.74359140978907,
132.225306879709));
#184254=CARTESIAN_POINT('Ctrl Pts',(141.126219416928,-5.78093320773838,
132.074368004931));
#184255=CARTESIAN_POINT('Ctrl Pts',(141.133513906339,-5.81230840630384,
131.922006577658));
#184256=CARTESIAN_POINT('Ctrl Pts',(141.14080839575,-5.83762777962395,131.768742527943));
#184257=CARTESIAN_POINT('Ctrl Pts',(141.148444464425,-5.86413278395792,
131.608301578218));
#184258=CARTESIAN_POINT('Ctrl Pts',(141.156080533099,-5.88400104460627,
131.44687190088));
#184259=CARTESIAN_POINT('Ctrl Pts',(141.163716601773,-5.89719109893007,
131.285055640632));
#184260=CARTESIAN_POINT('Ctrl Pts',(141.171352670447,-5.91038115325386,
131.123239380383));
#184261=CARTESIAN_POINT('Ctrl Pts',(141.178988739121,-5.91689302595348,
130.961037018775));
#184262=CARTESIAN_POINT('Ctrl Pts',(141.186624807795,-5.91674761616294,
130.799049390764));
#184263=CARTESIAN_POINT('',(142.936624807795,-5.92483523511467,130.807229770117));
#184264=CARTESIAN_POINT('Ctrl Pts',(141.186624807795,-5.91856290585919,
130.799047761251));
#184265=CARTESIAN_POINT('Ctrl Pts',(141.205425176656,-5.92226342242035,
130.400100415301));
#184266=CARTESIAN_POINT('Ctrl Pts',(141.317041420117,-5.70333307753058,
128.03562168117));
#184267=CARTESIAN_POINT('Ctrl Pts',(141.521473538194,-2.52131864300096,
124.275921843184));
#184268=CARTESIAN_POINT('Ctrl Pts',(141.799921162,4.12972612270149,125.154323212222));
#184269=CARTESIAN_POINT('Ctrl Pts',(142.078368785816,6.98575432998188,131.22483293709));
#184270=CARTESIAN_POINT('Ctrl Pts',(142.356816409628,3.42221558107838,136.908949141534));
#184271=CARTESIAN_POINT('Ctrl Pts',(142.635264033442,-3.28617210231038,
136.983246718178));
#184272=CARTESIAN_POINT('Ctrl Pts',(142.828533499497,-5.84638522401492,
133.093672015244));
#184273=CARTESIAN_POINT('Ctrl Pts',(142.928987090948,-5.92579859098698,
130.968857383612));
#184274=CARTESIAN_POINT('Ctrl Pts',(142.936624807795,-5.92483523511467,
130.807229770117));
#184275=CARTESIAN_POINT('',(144.686624807795,-5.90969244644754,130.808282040953));
#184276=CARTESIAN_POINT('Ctrl Pts',(142.936624807795,-5.92483523511467,
130.807229770117));
#184277=CARTESIAN_POINT('Ctrl Pts',(143.021802965552,-5.91409159534479,
129.004709116883));
#184278=CARTESIAN_POINT('Ctrl Pts',(143.199796997915,-4.07199242933219,
125.219045149632));
#184279=CARTESIAN_POINT('Ctrl Pts',(143.47060690488,2.37610874285143,124.221681241164));
#184280=CARTESIAN_POINT('Ctrl Pts',(143.749054528693,6.82253940572497,129.245349203993));
#184281=CARTESIAN_POINT('Ctrl Pts',(144.027502152506,4.99938965432202,135.701672493953));
#184282=CARTESIAN_POINT('Ctrl Pts',(144.305949776318,-1.41795495564429,
137.6576054165));
#184283=CARTESIAN_POINT('Ctrl Pts',(144.525657328082,-5.45337545441397,
134.231681535502));
#184284=CARTESIAN_POINT('Ctrl Pts',(144.652549005241,-5.91408802850884,
131.534134200586));
#184285=CARTESIAN_POINT('Ctrl Pts',(144.686624807795,-5.90969244644754,
130.808282040953));
#184286=CARTESIAN_POINT('',(146.436624824885,-5.9136271076536,130.800021490431));
#184287=CARTESIAN_POINT('Ctrl Pts',(144.686624807795,-5.90969244644754,
130.808282040953));
#184288=CARTESIAN_POINT('Ctrl Pts',(144.745364879845,-5.90211531582624,
129.557053751139));
#184289=CARTESIAN_POINT('Ctrl Pts',(144.8969208265,-4.90031956675752,126.317657450322));
#184290=CARTESIAN_POINT('Ctrl Pts',(145.141292647757,0.431102961529391,
123.819254264266));
#184291=CARTESIAN_POINT('Ctrl Pts',(145.419740271571,6.10978948450507,127.391439143905));
#184292=CARTESIAN_POINT('Ctrl Pts',(145.698187895383,6.17387795102984,134.099932127357));
#184293=CARTESIAN_POINT('Ctrl Pts',(145.976635519196,0.564474191264713,
137.779955890925));
#184294=CARTESIAN_POINT('Ctrl Pts',(146.222781156667,-4.85274554974043,
135.366472664822));
#184295=CARTESIAN_POINT('Ctrl Pts',(146.376110919533,-5.90179167691209,
132.088595634264));
#184296=CARTESIAN_POINT('Ctrl Pts',(146.436624807795,-5.91049805840725,
130.800024150482));
#184297=CARTESIAN_POINT('',(148.186624807795,-5.92111847692839,130.802105950051));
#184298=CARTESIAN_POINT('Ctrl Pts',(146.436624841933,-5.916748406975,130.800018836969));
#184299=CARTESIAN_POINT('Ctrl Pts',(146.445134157759,-5.91661530346575,
130.618632431374));
#184300=CARTESIAN_POINT('Ctrl Pts',(146.453643473586,-5.90813728831268,
130.437583582325));
#184301=CARTESIAN_POINT('Ctrl Pts',(146.462152789412,-5.89143102435819,
130.257578167473));
#184302=CARTESIAN_POINT('Ctrl Pts',(146.47070354915,-5.87464339393995,130.076696051277));
#184303=CARTESIAN_POINT('Ctrl Pts',(146.479254308889,-5.84954727551356,
129.896867686644));
#184304=CARTESIAN_POINT('Ctrl Pts',(146.487805068627,-5.81631051165087,
129.718790447305));
#184305=CARTESIAN_POINT('Ctrl Pts',(146.496410202756,-5.78286239478047,
129.539580812518));
#184306=CARTESIAN_POINT('Ctrl Pts',(146.505015336886,-5.74116985229078,
129.362144772545));
#184307=CARTESIAN_POINT('Ctrl Pts',(146.513620471015,-5.6914525224521,129.187172085831));
#184308=CARTESIAN_POINT('Ctrl Pts',(146.520257236284,-5.65310771073977,
129.052223271231));
#184309=CARTESIAN_POINT('Ctrl Pts',(146.526894001554,-5.60999045453091,
128.918739338434));
#184310=CARTESIAN_POINT('Ctrl Pts',(146.533530766823,-5.56222059870605,
128.787027582633));
#184311=CARTESIAN_POINT('Ctrl Pts',(146.540954033228,-5.50878969501127,
128.639707101586));
#184312=CARTESIAN_POINT('Ctrl Pts',(146.548377299634,-5.44942107922372,
128.494288070434));
#184313=CARTESIAN_POINT('Ctrl Pts',(146.555800566039,-5.38426878985133,
128.351284964201));
#184314=CARTESIAN_POINT('Ctrl Pts',(146.56321505876,-5.31919350507435,128.208450875764));
#184315=CARTESIAN_POINT('Ctrl Pts',(146.570629551481,-5.24834830671106,
128.068027364898));
#184316=CARTESIAN_POINT('Ctrl Pts',(146.578044044202,-5.17193660139352,
127.930512612945));
#184317=CARTESIAN_POINT('Ctrl Pts',(146.585451390556,-5.09559854455438,
127.793130402887));
#184318=CARTESIAN_POINT('Ctrl Pts',(146.59285873691,-5.01370484193458,127.658651694499));
#184319=CARTESIAN_POINT('Ctrl Pts',(146.600266083264,-4.92650642000909,
127.527553474002));
#184320=CARTESIAN_POINT('Ctrl Pts',(146.607667904939,-4.83937303395645,
127.396553031505));
#184321=CARTESIAN_POINT('Ctrl Pts',(146.615069726615,-4.74694301229305,
127.268928366144));
#184322=CARTESIAN_POINT('Ctrl Pts',(146.62247154829,-4.64951245962729,127.145130582399));
#184323=CARTESIAN_POINT('Ctrl Pts',(146.629869462601,-4.55213333979178,
127.02139815054));
#184324=CARTESIAN_POINT('Ctrl Pts',(146.637267376913,-4.44975917640805,
126.901488869612));
#184325=CARTESIAN_POINT('Ctrl Pts',(146.644665291224,-4.34272844203446,
126.785823540315));
#184326=CARTESIAN_POINT('Ctrl Pts',(146.652061976136,-4.23571549422752,
126.670177432496));
#184327=CARTESIAN_POINT('Ctrl Pts',(146.659458661048,-4.12404776455757,
126.558774150282));
#184328=CARTESIAN_POINT('Ctrl Pts',(146.666855345961,-4.00810301044205,
126.452000244138));
#184329=CARTESIAN_POINT('Ctrl Pts',(146.674251702896,-3.8921633974384,126.345231072461));
#184330=CARTESIAN_POINT('Ctrl Pts',(146.681648059831,-3.77194741167059,
126.243091121585));
#184331=CARTESIAN_POINT('Ctrl Pts',(146.689044416767,-3.64786835687497,
126.145928798444));
#184332=CARTESIAN_POINT('Ctrl Pts',(146.696441906103,-3.52377030525935,
126.048751599503));
#184333=CARTESIAN_POINT('Ctrl Pts',(146.70383939544,-3.39580830089613,125.956553775881));
#184334=CARTESIAN_POINT('Ctrl Pts',(146.711236884776,-3.26442715553067,
125.86964219513));
#184335=CARTESIAN_POINT('Ctrl Pts',(146.718636967291,-3.13299995470803,
125.782700147658));
#184336=CARTESIAN_POINT('Ctrl Pts',(146.726037049806,-2.99815153767556,
125.701048238365));
#184337=CARTESIAN_POINT('Ctrl Pts',(146.733437132321,-2.86035385522582,
125.624948837702));
#184338=CARTESIAN_POINT('Ctrl Pts',(146.740845351987,-2.72240465005856,
125.548765757924));
#184339=CARTESIAN_POINT('Ctrl Pts',(146.748253571654,-2.58150002992763,
125.478147560544));
#184340=CARTESIAN_POINT('Ctrl Pts',(146.75566179132,-2.43813525646765,125.413309974726));
#184341=CARTESIAN_POINT('Ctrl Pts',(146.763074570622,-2.29468224438167,
125.348432482455));
#184342=CARTESIAN_POINT('Ctrl Pts',(146.770487349924,-2.14876640696812,
125.289342831039));
#184343=CARTESIAN_POINT('Ctrl Pts',(146.777900129226,-2.0009004450983,125.236207605004));
#184344=CARTESIAN_POINT('Ctrl Pts',(146.785323500255,-1.85282320540788,
125.182996456866));
#184345=CARTESIAN_POINT('Ctrl Pts',(146.792746871284,-1.70279063125872,
125.135756838232));
#184346=CARTESIAN_POINT('Ctrl Pts',(146.800170242312,-1.551328750304,125.094604959836));
#184347=CARTESIAN_POINT('Ctrl Pts',(146.804106291753,-1.47102002674315,
125.072785246484));
#184348=CARTESIAN_POINT('Ctrl Pts',(146.808042341194,-1.39030962529649,
125.052676157388));
#184349=CARTESIAN_POINT('Ctrl Pts',(146.811978390635,-1.30927668226356,
125.034289116122));
#184350=CARTESIAN_POINT('Ctrl Pts',(146.81940165704,-1.1564510806562,124.999611730133));
#184351=CARTESIAN_POINT('Ctrl Pts',(146.826824923445,-1.00201574427408,
124.970957689606));
#184352=CARTESIAN_POINT('Ctrl Pts',(146.834248189851,-0.846486777102989,
124.9484754839));
#184353=CARTESIAN_POINT('Ctrl Pts',(146.841662682572,-0.691141632255162,
124.926019850294));
#184354=CARTESIAN_POINT('Ctrl Pts',(146.849077175293,-0.534705795357542,
124.909721584459));
#184355=CARTESIAN_POINT('Ctrl Pts',(146.856491668014,-0.37770834673534,
124.89967883382));
#184356=CARTESIAN_POINT('Ctrl Pts',(146.863899014368,-0.22086221816497,
124.889645762761));
#184357=CARTESIAN_POINT('Ctrl Pts',(146.871306360721,-0.0634559255323632,
124.885856227417));
#184358=CARTESIAN_POINT('Ctrl Pts',(146.878713707075,0.0939735972562396,
124.88835693894));
#184359=CARTESIAN_POINT('Ctrl Pts',(146.88611552875,0.251285703167327,124.890855785338));
#184360=CARTESIAN_POINT('Ctrl Pts',(146.893517350426,0.40862063309177,124.899635531284));
#184361=CARTESIAN_POINT('Ctrl Pts',(146.900919172101,0.565438808281448,
124.914690888575));
#184362=CARTESIAN_POINT('Ctrl Pts',(146.908317086413,0.722174200377338,
124.92973829826));
#184363=CARTESIAN_POINT('Ctrl Pts',(146.915715000724,0.878393010365668,
124.951054686014));
#184364=CARTESIAN_POINT('Ctrl Pts',(146.923112915035,1.0335582540163,124.978582738342));
#184365=CARTESIAN_POINT('Ctrl Pts',(146.930509599948,1.18869771201809,125.006106216007));
#184366=CARTESIAN_POINT('Ctrl Pts',(146.93790628486,1.34278358397292,125.03983924436));
#184367=CARTESIAN_POINT('Ctrl Pts',(146.945302969772,1.49528646691333,125.079672945355));
#184368=CARTESIAN_POINT('Ctrl Pts',(146.952699326707,1.64778258771611,125.119504880082));
#184369=CARTESIAN_POINT('Ctrl Pts',(146.960095683643,1.79869549788864,125.165436855246));
#184370=CARTESIAN_POINT('Ctrl Pts',(146.967492040578,1.9475086720437,125.217309469168));
#184371=CARTESIAN_POINT('Ctrl Pts',(146.974889529915,2.09634462987568,125.269190024919));
#184372=CARTESIAN_POINT('Ctrl Pts',(146.982287019251,2.24307985907154,125.327012907538));
#184373=CARTESIAN_POINT('Ctrl Pts',(146.989684508588,2.38721575165447,125.390569753712));
#184374=CARTESIAN_POINT('Ctrl Pts',(146.997084591103,2.53140217085101,125.45414887964));
#184375=CARTESIAN_POINT('Ctrl Pts',(147.004484673618,2.67298709790295,125.523465820563));
#184376=CARTESIAN_POINT('Ctrl Pts',(147.011884756133,2.8114946921874,125.598265328551));
#184377=CARTESIAN_POINT('Ctrl Pts',(147.0192929758,2.9501545898108,125.673147086288));
#184378=CARTESIAN_POINT('Ctrl Pts',(147.026701195466,3.08573006824559,125.753523273201));
#184379=CARTESIAN_POINT('Ctrl Pts',(147.034109415132,3.21777192742527,125.839093818534));
#184380=CARTESIAN_POINT('Ctrl Pts',(147.041522194435,3.34989505616613,125.924717031109));
#184381=CARTESIAN_POINT('Ctrl Pts',(147.048934973737,3.47847992772278,126.015540757741));
#184382=CARTESIAN_POINT('Ctrl Pts',(147.056347753039,3.60310926247154,126.111223691672));
#184383=CARTESIAN_POINT('Ctrl Pts',(147.063771124068,3.72791667345833,126.207043341866));
#184384=CARTESIAN_POINT('Ctrl Pts',(147.071194495096,3.84875697358736,126.307735827878));
#184385=CARTESIAN_POINT('Ctrl Pts',(147.078617866125,3.96524806068224,126.412921402484));
#184386=CARTESIAN_POINT('Ctrl Pts',(147.082553915566,4.02701443022521,126.468693318034));
#184387=CARTESIAN_POINT('Ctrl Pts',(147.086489965007,4.0875587198433,126.52572781076));
#184388=CARTESIAN_POINT('Ctrl Pts',(147.090426014447,4.14682854345745,126.583964475772));
#184389=CARTESIAN_POINT('Ctrl Pts',(147.097849280853,4.25860958104587,126.693797008481));
#184390=CARTESIAN_POINT('Ctrl Pts',(147.105272547258,4.36619310847296,126.808239621997));
#184391=CARTESIAN_POINT('Ctrl Pts',(147.112695813664,4.4691752306249,126.926938365545));
#184392=CARTESIAN_POINT('Ctrl Pts',(147.120110306385,4.5720356364607,127.045496817035));
#184393=CARTESIAN_POINT('Ctrl Pts',(147.127524799106,4.67030522009927,127.168301106319));
#184394=CARTESIAN_POINT('Ctrl Pts',(147.134939291827,4.76361542649413,127.294959154215));
#184395=CARTESIAN_POINT('Ctrl Pts',(147.142346638181,4.85683569699896,127.421495124316));
#184396=CARTESIAN_POINT('Ctrl Pts',(147.149753984534,4.94510588643994,127.551877159868));
#184397=CARTESIAN_POINT('Ctrl Pts',(147.157161330888,5.02809646950872,127.685678771687));
#184398=CARTESIAN_POINT('Ctrl Pts',(147.164563152564,5.11102515506961,127.819380589217));
#184399=CARTESIAN_POINT('Ctrl Pts',(147.171964974239,5.18868187889322,127.95649658886));
#184400=CARTESIAN_POINT('Ctrl Pts',(147.179366795914,5.2607794346013,128.096569949332));
#184401=CARTESIAN_POINT('Ctrl Pts',(147.186764710226,5.33283893057094,128.236569366167));
#184402=CARTESIAN_POINT('Ctrl Pts',(147.194162624537,5.39934493249765,128.379522703619));
#184403=CARTESIAN_POINT('Ctrl Pts',(147.201560538848,5.46005540675389,128.524947202304));
#184404=CARTESIAN_POINT('Ctrl Pts',(147.208957223761,5.52075579203069,128.670347534075));
#184405=CARTESIAN_POINT('Ctrl Pts',(147.216353908673,5.57566241745714,128.818217867889));
#184406=CARTESIAN_POINT('Ctrl Pts',(147.223750593585,5.62458072998013,128.968053950793));
#184407=CARTESIAN_POINT('Ctrl Pts',(147.23114695052,5.67349687341389,129.117883389808));
#184408=CARTESIAN_POINT('Ctrl Pts',(147.238543307456,5.71642511604805,129.269678049739));
#184409=CARTESIAN_POINT('Ctrl Pts',(147.245939664391,5.75322037244169,129.422917202647));
#184410=CARTESIAN_POINT('Ctrl Pts',(147.253337153728,5.79002126228304,129.576179816861));
#184411=CARTESIAN_POINT('Ctrl Pts',(147.260734643065,5.82068720909482,129.730887001399));
#184412=CARTESIAN_POINT('Ctrl Pts',(147.268132132401,5.84512400504113,129.886506637789));
#184413=CARTESIAN_POINT('Ctrl Pts',(147.275532214916,5.86956936726836,130.042180826402));
#184414=CARTESIAN_POINT('Ctrl Pts',(147.282932297431,5.88778117318749,130.198767735153));
#184415=CARTESIAN_POINT('Ctrl Pts',(147.290332379946,5.89971696663163,130.355729058111));
#184416=CARTESIAN_POINT('Ctrl Pts',(147.297740599613,5.9116658847077,130.51286297618));
#184417=CARTESIAN_POINT('Ctrl Pts',(147.305148819279,5.91732497999493,130.670371758208));
#184418=CARTESIAN_POINT('Ctrl Pts',(147.312557038945,5.91670390691144,130.827715283885));
#184419=CARTESIAN_POINT('Ctrl Pts',(147.319969818248,5.91608245156783,130.985155651876));
#184420=CARTESIAN_POINT('Ctrl Pts',(147.32738259755,5.90917314202703,131.142430188767));
#184421=CARTESIAN_POINT('Ctrl Pts',(147.334795376852,5.89603757950191,131.299003340752));
#184422=CARTESIAN_POINT('Ctrl Pts',(147.34221874788,5.88288324826905,131.4558002118));
#184423=CARTESIAN_POINT('Ctrl Pts',(147.349642118909,5.86348494193607,131.611893326914));
#184424=CARTESIAN_POINT('Ctrl Pts',(147.357065489938,5.83795561703674,131.766755950062));
#184425=CARTESIAN_POINT('Ctrl Pts',(147.361001539379,5.82441935640741,131.848867828732));
#184426=CARTESIAN_POINT('Ctrl Pts',(147.36493758882,5.80916028979156,131.930633990754));
#184427=CARTESIAN_POINT('Ctrl Pts',(147.36887363826,5.79220092157807,132.011977711918));
#184428=CARTESIAN_POINT('Ctrl Pts',(147.376296904666,5.7602160824111,132.165389431382));
#184429=CARTESIAN_POINT('Ctrl Pts',(147.383720171071,5.72208379492518,132.317761527952));
#184430=CARTESIAN_POINT('Ctrl Pts',(147.391143437477,5.67788353275672,132.468562874189));
#184431=CARTESIAN_POINT('Ctrl Pts',(147.398557930198,5.63373551162751,132.619185985759));
#184432=CARTESIAN_POINT('Ctrl Pts',(147.405972422919,5.58353389537917,132.768241687633));
#184433=CARTESIAN_POINT('Ctrl Pts',(147.41338691564,5.52740933832674,132.915207975638));
#184434=CARTESIAN_POINT('Ctrl Pts',(147.420794261993,5.47133887623547,133.062032612001));
#184435=CARTESIAN_POINT('Ctrl Pts',(147.428201608347,5.40935697062705,133.206771497293));
#184436=CARTESIAN_POINT('Ctrl Pts',(147.435608954701,5.34164432245116,133.348916864719));
#184437=CARTESIAN_POINT('Ctrl Pts',(147.443010776376,5.27398217692291,133.490956214767));
#184438=CARTESIAN_POINT('Ctrl Pts',(147.450412598052,5.20059795919364,133.630405562924));
#184439=CARTESIAN_POINT('Ctrl Pts',(147.457814419727,5.12172076388581,133.766776351267));
#184440=CARTESIAN_POINT('Ctrl Pts',(147.465212334039,5.04288520723543,133.903075150533));
#184441=CARTESIAN_POINT('Ctrl Pts',(147.47261024835,4.95856263432894,134.036298304224));
#184442=CARTESIAN_POINT('Ctrl Pts',(147.480008162661,4.86902837922111,134.165981239355));
#184443=CARTESIAN_POINT('Ctrl Pts',(147.487404847574,4.77950900308215,134.295642623536));
#184444=CARTESIAN_POINT('Ctrl Pts',(147.494801532486,4.68477987555104,134.421764649904));
#184445=CARTESIAN_POINT('Ctrl Pts',(147.502198217398,4.58516007824034,134.543911074427));
#184446=CARTESIAN_POINT('Ctrl Pts',(147.509594574333,4.48554469817586,134.66605208285));
#184447=CARTESIAN_POINT('Ctrl Pts',(147.516990931269,4.38103931545204,134.784217550653));
#184448=CARTESIAN_POINT('Ctrl Pts',(147.524387288204,4.27200361100666,134.898003947174));
#184449=CARTESIAN_POINT('Ctrl Pts',(147.531784777541,4.16295121291654,135.011807764683));
#184450=CARTESIAN_POINT('Ctrl Pts',(147.539182266877,4.04936737033896,135.121230906417));
#184451=CARTESIAN_POINT('Ctrl Pts',(147.546579756214,3.93164884797777,135.225906489622));
#184452=CARTESIAN_POINT('Ctrl Pts',(147.553979838729,3.81388905957093,135.330618766691));
#184453=CARTESIAN_POINT('Ctrl Pts',(147.561379921244,3.69199198441348,135.430579923824));
#184454=CARTESIAN_POINT('Ctrl Pts',(147.568780003759,3.56638756593778,135.52546327394));
#184455=CARTESIAN_POINT('Ctrl Pts',(147.576188223426,3.44064503249161,135.620450958054));
#184456=CARTESIAN_POINT('Ctrl Pts',(147.583596443092,3.31118731252439,135.710349459245));
#184457=CARTESIAN_POINT('Ctrl Pts',(147.591004662759,3.17847404300024,135.794874951828));
#184458=CARTESIAN_POINT('Ctrl Pts',(147.598417442061,3.04567909067309,135.879452468441));
#184459=CARTESIAN_POINT('Ctrl Pts',(147.605830221363,2.90962491796424,135.958650199476));
#184460=CARTESIAN_POINT('Ctrl Pts',(147.613243000665,2.77079539841787,136.032230491865));
#184461=CARTESIAN_POINT('Ctrl Pts',(147.620666371694,2.6317675127435,136.105915919227));
#184462=CARTESIAN_POINT('Ctrl Pts',(147.628089742722,2.48995669580852,136.173967716226));
#184463=CARTESIAN_POINT('Ctrl Pts',(147.635513113751,2.34586716132055,136.236196202701));
#184464=CARTESIAN_POINT('Ctrl Pts',(147.639449163192,2.2694674327546,136.269191239382));
#184465=CARTESIAN_POINT('Ctrl Pts',(147.643385212633,2.19242734667834,136.300549962301));
#184466=CARTESIAN_POINT('Ctrl Pts',(147.647321262073,2.11482361751463,136.330249833729));
#184467=CARTESIAN_POINT('Ctrl Pts',(147.654744528479,1.96846540624065,136.38626286434));
#184468=CARTESIAN_POINT('Ctrl Pts',(147.662167794884,1.81965901317569,136.436541931007));
#184469=CARTESIAN_POINT('Ctrl Pts',(147.66959106129,1.66889424831701,136.480866809797));
#184470=CARTESIAN_POINT('Ctrl Pts',(147.677005554011,1.51830767489006,136.525139300261));
#184471=CARTESIAN_POINT('Ctrl Pts',(147.684420046732,1.365767691602,136.563471506478));
#184472=CARTESIAN_POINT('Ctrl Pts',(147.691834539453,1.21178409719669,136.595691195618));
#184473=CARTESIAN_POINT('Ctrl Pts',(147.699241885806,1.05794891797699,136.627879830208));
#184474=CARTESIAN_POINT('Ctrl Pts',(147.70664923216,0.90267326058903,136.653967600545));
#184475=CARTESIAN_POINT('Ctrl Pts',(147.714056578514,0.746481996895511,
136.6738320751));
#184476=CARTESIAN_POINT('Ctrl Pts',(147.721458400189,0.590407226539157,
136.693681733981));
#184477=CARTESIAN_POINT('Ctrl Pts',(147.728860221865,0.433418578332028,
136.707317292175));
#184478=CARTESIAN_POINT('Ctrl Pts',(147.73626204354,0.276050921131112,136.714667415985));
#184479=CARTESIAN_POINT('Ctrl Pts',(147.743659957852,0.118766337091485,
136.722013659723));
#184480=CARTESIAN_POINT('Ctrl Pts',(147.751057872163,-0.0388964855337151,
136.723081059724));
#184481=CARTESIAN_POINT('Ctrl Pts',(147.758455786474,-0.196397863552939,
136.71785014928));
#184482=CARTESIAN_POINT('Ctrl Pts',(147.765852471386,-0.353873067700333,
136.712620108119));
#184483=CARTESIAN_POINT('Ctrl Pts',(147.773249156299,-0.51118650776281,
136.701093846212));
#184484=CARTESIAN_POINT('Ctrl Pts',(147.780645841211,-0.667798687876059,
136.683304015403));
#184485=CARTESIAN_POINT('Ctrl Pts',(147.788042198146,-0.824403923641123,
136.665514973413));
#184486=CARTESIAN_POINT('Ctrl Pts',(147.795438555082,-0.980307590371243,
136.641462956881));
#184487=CARTESIAN_POINT('Ctrl Pts',(147.802834912017,-1.13497576996038,
136.611232457387));
#184488=CARTESIAN_POINT('Ctrl Pts',(147.810232401354,-1.2896676296426,136.580997329526));
#184489=CARTESIAN_POINT('Ctrl Pts',(147.81762989069,-1.44312325915959,136.544581906819));
#184490=CARTESIAN_POINT('Ctrl Pts',(147.825027380027,-1.59481952864751,
136.502121689561));
#184491=CARTESIAN_POINT('Ctrl Pts',(147.832427462542,-1.74656897502743,
136.45964658794));
#184492=CARTESIAN_POINT('Ctrl Pts',(147.839827545057,-1.89655747419436,
136.411122573423));
#184493=CARTESIAN_POINT('Ctrl Pts',(147.847227627572,-2.04427778012711,
136.35673478725));
#184494=CARTESIAN_POINT('Ctrl Pts',(147.854635847238,-2.19216051972247,
136.302287196115));
#184495=CARTESIAN_POINT('Ctrl Pts',(147.862044066905,-2.33776973465519,
136.241963085661));
#184496=CARTESIAN_POINT('Ctrl Pts',(147.869452286571,-2.48061818933069,
136.175995746767));
#184497=CARTESIAN_POINT('Ctrl Pts',(147.876865065873,-2.62355456484653,
136.109987806076));
#184498=CARTESIAN_POINT('Ctrl Pts',(147.884277845175,-2.76372646261958,
136.038329885458));
#184499=CARTESIAN_POINT('Ctrl Pts',(147.891690624477,-2.90067239292292,
135.961300624143));
#184500=CARTESIAN_POINT('Ctrl Pts',(147.899113995506,-3.03781399799365,
135.884161299807));
#184501=CARTESIAN_POINT('Ctrl Pts',(147.906537366535,-3.17172011261075,
135.801635501764));
#184502=CARTESIAN_POINT('Ctrl Pts',(147.913960737564,-3.30195861365784,
135.714044912527));
#184503=CARTESIAN_POINT('Ctrl Pts',(147.917896787004,-3.37101419194558,
135.667602280405));
#184504=CARTESIAN_POINT('Ctrl Pts',(147.921832836445,-3.43903922199857,
135.619736429816));
#184505=CARTESIAN_POINT('Ctrl Pts',(147.925768885886,-3.50597327616687,
135.570499720583));
#184506=CARTESIAN_POINT('Ctrl Pts',(147.933123905128,-3.63104824377164,
135.478494538933));
#184507=CARTESIAN_POINT('Ctrl Pts',(147.940478924369,-3.75270524870596,
135.381410785428));
#184508=CARTESIAN_POINT('Ctrl Pts',(147.947833943611,-3.8704987908315,135.279533203363));
#184509=CARTESIAN_POINT('Ctrl Pts',(147.955180237663,-3.98815259559593,
135.177776477707));
#184510=CARTESIAN_POINT('Ctrl Pts',(147.962526531715,-4.10195177232589,
135.071237486037));
#184511=CARTESIAN_POINT('Ctrl Pts',(147.969872825766,-4.21148001421642,
134.960243995665));
#184512=CARTESIAN_POINT('Ctrl Pts',(147.97721208139,-4.3209033179346,134.849356847308));
#184513=CARTESIAN_POINT('Ctrl Pts',(147.984551337014,-4.42606356485535,
134.734023963175));
#184514=CARTESIAN_POINT('Ctrl Pts',(147.991890592638,-4.52657792759927,
134.614612948826));
#184515=CARTESIAN_POINT('Ctrl Pts',(147.999224490157,-4.62701890873292,
134.495289111794));
#184516=CARTESIAN_POINT('Ctrl Pts',(148.006558387677,-4.72282051299202,
134.37189336114));
#184517=CARTESIAN_POINT('Ctrl Pts',(148.013892285197,-4.81363732265844,
134.244829522877));
#184518=CARTESIAN_POINT('Ctrl Pts',(148.021223039868,-4.90441521392979,
134.117820136214));
#184519=CARTESIAN_POINT('Ctrl Pts',(148.028553794539,-4.99021233941579,
133.987146098375));
#184520=CARTESIAN_POINT('Ctrl Pts',(148.035884549209,-5.07072415600133,
133.853243543532));
#184521=CARTESIAN_POINT('Ctrl Pts',(148.043213762271,-5.15121904148193,
133.719369147514));
#184522=CARTESIAN_POINT('Ctrl Pts',(148.050542975332,-5.22643063297417,
133.582267911324));
#184523=CARTESIAN_POINT('Ctrl Pts',(148.057872188393,-5.29609838416044,
133.442403920431));
#184524=CARTESIAN_POINT('Ctrl Pts',(148.065201372892,-5.36576586384708,
133.302540474598));
#184525=CARTESIAN_POINT('Ctrl Pts',(148.072530557391,-5.42988937632489,
133.159914636398));
#184526=CARTESIAN_POINT('Ctrl Pts',(148.07985974189,-5.48825502631292,133.015013762827));
#184527=CARTESIAN_POINT('Ctrl Pts',(148.087190410633,-5.54663249601668,
132.870083545161));
#184528=CARTESIAN_POINT('Ctrl Pts',(148.094521079376,-5.59924964074774,
132.72287772861));
#184529=CARTESIAN_POINT('Ctrl Pts',(148.101851748119,-5.64594135944282,
132.573902006806));
#184530=CARTESIAN_POINT('Ctrl Pts',(148.109189520302,-5.69267832254938,
132.424781927093));
#184531=CARTESIAN_POINT('Ctrl Pts',(148.116527292484,-5.73347827712869,
132.273888880453));
#184532=CARTESIAN_POINT('Ctrl Pts',(148.123865064667,-5.76822634556614,
132.1217426384));
#184533=CARTESIAN_POINT('Ctrl Pts',(148.13120651168,-5.80299181618652,131.969520199975));
#184534=CARTESIAN_POINT('Ctrl Pts',(148.138547958692,-5.83169929265059,
131.816043689774));
#184535=CARTESIAN_POINT('Ctrl Pts',(148.145889405705,-5.85428548751921,
131.661840642477));
#184536=CARTESIAN_POINT('Ctrl Pts',(148.153241485596,-5.87690439477602,
131.50741425743));
#184537=CARTESIAN_POINT('Ctrl Pts',(148.160593565487,-5.89338426854782,
131.352259611532));
#184538=CARTESIAN_POINT('Ctrl Pts',(148.167945645379,-5.90371385336624,
131.196907812272));
#184539=CARTESIAN_POINT('Ctrl Pts',(148.174172032851,-5.91246185372226,
131.065342253818));
#184540=CARTESIAN_POINT('Ctrl Pts',(148.180398420323,-5.91679965474399,
130.93363543647));
#184541=CARTESIAN_POINT('Ctrl Pts',(148.186624807795,-5.91674957104603,
130.802107613661));
#184542=CARTESIAN_POINT('',(149.936624807795,-5.91741018499184,130.809792679456));
#184543=CARTESIAN_POINT('Ctrl Pts',(148.186624807795,-5.92549522901829,
130.802104283454));
#184544=CARTESIAN_POINT('Ctrl Pts',(148.19248870843,-5.9260986124455,130.678050383426));
#184545=CARTESIAN_POINT('Ctrl Pts',(148.198352609065,-5.92254184562957,
130.554031734584));
#184546=CARTESIAN_POINT('Ctrl Pts',(148.297032384304,-5.79083462023666,
128.4715467825));
#184547=CARTESIAN_POINT('Ctrl Pts',(148.482664133512,-3.40361946202966,
124.689384322596));
#184548=CARTESIAN_POINT('Ctrl Pts',(148.761111757326,3.30496328483161,124.635505114617));
#184549=CARTESIAN_POINT('Ctrl Pts',(149.039559381138,6.97644622936501,130.250502748502));
#184550=CARTESIAN_POINT('Ctrl Pts',(149.31800700495,4.23691590745723,136.374468706597));
#184551=CARTESIAN_POINT('Ctrl Pts',(149.596454628764,-2.39613314855434,
137.379777445777));
#184552=CARTESIAN_POINT('Ctrl Pts',(149.802660563045,-5.67762348943452,
133.649467228661));
#184553=CARTESIAN_POINT('Ctrl Pts',(149.916050622722,-5.92147029572398,
131.246598976015));
#184554=CARTESIAN_POINT('Ctrl Pts',(149.936624807795,-5.91741018499184,
130.809792679456));
#184555=CARTESIAN_POINT('',(151.686624807835,-5.91674999613679,130.804146806335));
#184556=CARTESIAN_POINT('Ctrl Pts',(149.936624807795,-5.91674750701871,
130.809792071131));
#184557=CARTESIAN_POINT('Ctrl Pts',(149.943932106311,-5.91688990486533,
130.654671145612));
#184558=CARTESIAN_POINT('Ctrl Pts',(149.951239404828,-5.91092786845665,
130.499368082824));
#184559=CARTESIAN_POINT('Ctrl Pts',(149.958546703344,-5.89884527149,130.344409505468));
#184560=CARTESIAN_POINT('Ctrl Pts',(149.965848675255,-5.88677148205011,
130.189563884111));
#184561=CARTESIAN_POINT('Ctrl Pts',(149.973150647166,-5.86858604119047,
130.035062629882));
#184562=CARTESIAN_POINT('Ctrl Pts',(149.980452619077,-5.84432489231685,
129.881432063698));
#184563=CARTESIAN_POINT('Ctrl Pts',(149.987751576981,-5.82007375762373,
129.727864911008));
#184564=CARTESIAN_POINT('Ctrl Pts',(149.995050534885,-5.78975196218206,
129.575168110421));
#184565=CARTESIAN_POINT('Ctrl Pts',(150.002349492789,-5.75344725503109,
129.423862429927));
#184566=CARTESIAN_POINT('Ctrl Pts',(150.009646984945,-5.7171498384515,129.272587134056));
#184567=CARTESIAN_POINT('Ctrl Pts',(150.016944477101,-5.67487198927059,
129.122702776197));
#184568=CARTESIAN_POINT('Ctrl Pts',(150.024241969256,-5.62675242818888,
128.974719211615));
#184569=CARTESIAN_POINT('Ctrl Pts',(150.031539528218,-5.57863242658976,
128.826734292296));
#184570=CARTESIAN_POINT('Ctrl Pts',(150.038837087179,-5.52467072538557,
128.680650566464));
#184571=CARTESIAN_POINT('Ctrl Pts',(150.046134646141,-5.46505561347183,
128.536961732464));
#184572=CARTESIAN_POINT('Ctrl Pts',(150.053433804352,-5.40542743699231,
128.393241409264));
#184573=CARTESIAN_POINT('Ctrl Pts',(150.060732962563,-5.34014353216303,
128.251917377002));
#184574=CARTESIAN_POINT('Ctrl Pts',(150.068032120774,-5.26943979956252,
128.113462113109));
#184575=CARTESIAN_POINT('Ctrl Pts',(150.075338692602,-5.1986642545184,127.974866222825));
#184576=CARTESIAN_POINT('Ctrl Pts',(150.082645264429,-5.12245806211543,
127.839145263181));
#184577=CARTESIAN_POINT('Ctrl Pts',(150.089951836257,-5.0411027552245,127.706746443114));
#184578=CARTESIAN_POINT('Ctrl Pts',(150.097262210755,-4.95970510735594,
127.574278716719));
#184579=CARTESIAN_POINT('Ctrl Pts',(150.104572585253,-4.87315322139015,
127.445136892233));
#184580=CARTESIAN_POINT('Ctrl Pts',(150.111882959752,-4.78177074702681,
127.319737383215));
#184581=CARTESIAN_POINT('Ctrl Pts',(150.119204413597,-4.69024977658409,
127.19414782309));
#184582=CARTESIAN_POINT('Ctrl Pts',(150.126525867443,-4.59388383081696,
127.072312209756));
#184583=CARTESIAN_POINT('Ctrl Pts',(150.133847321289,-4.49303604899263,
126.95461288233));
#184584=CARTESIAN_POINT('Ctrl Pts',(150.140348172989,-4.40349147386482,
126.850105514131));
#184585=CARTESIAN_POINT('Ctrl Pts',(150.146849024689,-4.31041409756609,
126.748858792964));
#184586=CARTESIAN_POINT('Ctrl Pts',(150.153349876389,-4.21408048751599,
126.651114151579));
#184587=CARTESIAN_POINT('Ctrl Pts',(150.160773142795,-4.10407797028059,
126.539500389849));
#184588=CARTESIAN_POINT('Ctrl Pts',(150.1681964092,-3.98947176547295,126.432091149178));
#184589=CARTESIAN_POINT('Ctrl Pts',(150.175619675606,-3.87061643811742,
126.32928978556));
#184590=CARTESIAN_POINT('Ctrl Pts',(150.183034168327,-3.75190158788854,
126.226609924616));
#184591=CARTESIAN_POINT('Ctrl Pts',(150.190448661048,-3.62894789123219,
126.128527341995));
#184592=CARTESIAN_POINT('Ctrl Pts',(150.197863153769,-3.50214798775444,
126.03540999564));
#184593=CARTESIAN_POINT('Ctrl Pts',(150.205270500122,-3.37547029879769,
125.942382399289));
#184594=CARTESIAN_POINT('Ctrl Pts',(150.212677846476,-3.2449540820249,125.854310731327));
#184595=CARTESIAN_POINT('Ctrl Pts',(150.22008519283,-3.11102632760607,125.771523867636));
#184596=CARTESIAN_POINT('Ctrl Pts',(150.227487014505,-2.97719846155896,
125.688798749512));
#184597=CARTESIAN_POINT('Ctrl Pts',(150.234888836181,-2.83996444037969,
125.611350782824));
#184598=CARTESIAN_POINT('Ctrl Pts',(150.242290657856,-2.69978152190396,
125.539466478413));
#184599=CARTESIAN_POINT('Ctrl Pts',(150.249688572167,-2.55967260489901,
125.467620121167));
#184600=CARTESIAN_POINT('Ctrl Pts',(150.257086486479,-2.41661822217042,
125.401331746898));
#184601=CARTESIAN_POINT('Ctrl Pts',(150.26448440079,-2.27110150087739,125.340842654274));
#184602=CARTESIAN_POINT('Ctrl Pts',(150.271881085702,-2.12560896182449,
125.280363613841));
#184603=CARTESIAN_POINT('Ctrl Pts',(150.279277770615,-1.97765524070537,
125.225682085472));
#184604=CARTESIAN_POINT('Ctrl Pts',(150.286674455527,-1.82774488596508,
125.176991854607));
#184605=CARTESIAN_POINT('Ctrl Pts',(150.294070812462,-1.67784117840697,
125.128303782718));
#184606=CARTESIAN_POINT('Ctrl Pts',(150.301467169398,-1.52598136477429,
125.085606595426));
#184607=CARTESIAN_POINT('Ctrl Pts',(150.308863526333,-1.37268639319796,
125.049044585546));
#184608=CARTESIAN_POINT('Ctrl Pts',(150.31626101567,-1.21936795177014,125.012476977928));
#184609=CARTESIAN_POINT('Ctrl Pts',(150.323658505006,-1.06461427803038,
124.982046504626));
#184610=CARTESIAN_POINT('Ctrl Pts',(150.331055994343,-0.908957633202125,
124.957846563573));
#184611=CARTESIAN_POINT('Ctrl Pts',(150.338456076858,-0.753246423178655,
124.933638139267));
#184612=CARTESIAN_POINT('Ctrl Pts',(150.345856159373,-0.596631980484085,
124.915664653056));
#184613=CARTESIAN_POINT('Ctrl Pts',(150.353256241888,-0.439652675039819,
124.903967741847));
#184614=CARTESIAN_POINT('Ctrl Pts',(150.360664461554,-0.282500754710905,
124.892257968682));
#184615=CARTESIAN_POINT('Ctrl Pts',(150.368072681221,-0.124983542895683,
124.886838581501));
#184616=CARTESIAN_POINT('Ctrl Pts',(150.375480900887,0.0323588554119081,
124.887699103927));
#184617=CARTESIAN_POINT('Ctrl Pts',(150.382893680189,0.189798095340595,
124.88856015599));
#184618=CARTESIAN_POINT('Ctrl Pts',(150.390306459491,0.347061935317314,
124.895708802602));
#184619=CARTESIAN_POINT('Ctrl Pts',(150.397719238793,0.503614915903667,
124.9090826276));
#184620=CARTESIAN_POINT('Ctrl Pts',(150.405142609822,0.660391586730009,
124.922475561746));
#184621=CARTESIAN_POINT('Ctrl Pts',(150.412565980851,0.816455000170236,
124.942111392765));
#184622=CARTESIAN_POINT('Ctrl Pts',(150.41998935188,0.9712785927025,124.967876362652));
#184623=CARTESIAN_POINT('Ctrl Pts',(150.423925401321,1.05336977640659,124.981537567908));
#184624=CARTESIAN_POINT('Ctrl Pts',(150.427861450762,1.1351126220454,124.996921051034));
#184625=CARTESIAN_POINT('Ctrl Pts',(150.431797500202,1.21643043974548,125.014004190906));
#184626=CARTESIAN_POINT('Ctrl Pts',(150.439220766608,1.36979330608149,125.046222459557));
#184627=CARTESIAN_POINT('Ctrl Pts',(150.446644033013,1.52210719535654,125.084586587279));
#184628=CARTESIAN_POINT('Ctrl Pts',(150.454067299419,1.67284110169347,125.129016292242));
#184629=CARTESIAN_POINT('Ctrl Pts',(150.46148179214,1.82339685307062,125.173393484984));
#184630=CARTESIAN_POINT('Ctrl Pts',(150.468896284861,1.9723759840262,125.223821880504));
#184631=CARTESIAN_POINT('Ctrl Pts',(150.476310777582,2.11925668982468,125.280170030237));
#184632=CARTESIAN_POINT('Ctrl Pts',(150.483718123936,2.26599582646911,125.336463869502));
#184633=CARTESIAN_POINT('Ctrl Pts',(150.491125470289,2.41064021824683,125.398665971281));
#184634=CARTESIAN_POINT('Ctrl Pts',(150.498532816643,2.55268237394668,125.466594862098));
#184635=CARTESIAN_POINT('Ctrl Pts',(150.505934638318,2.6946185892478,125.534473088986));
#184636=CARTESIAN_POINT('Ctrl Pts',(150.513336459994,2.83395609763766,125.608069439907));
#184637=CARTESIAN_POINT('Ctrl Pts',(150.520738281669,2.97020669040165,125.687154077002));
#184638=CARTESIAN_POINT('Ctrl Pts',(150.528136195981,3.10638535753878,125.766196965932));
#184639=CARTESIAN_POINT('Ctrl Pts',(150.535534110292,3.23948003235821,125.850722184156));
#184640=CARTESIAN_POINT('Ctrl Pts',(150.542932024603,3.36902656142461,125.940453690936));
#184641=CARTESIAN_POINT('Ctrl Pts',(150.550328709516,3.49855156220764,126.030170285968));
#184642=CARTESIAN_POINT('Ctrl Pts',(150.557725394428,3.62452928092174,126.125091240058));
#184643=CARTESIAN_POINT('Ctrl Pts',(150.56512207934,3.74652395962857,126.224896808076));
#184644=CARTESIAN_POINT('Ctrl Pts',(150.572518436275,3.86851322896337,126.32469795061));
#184645=CARTESIAN_POINT('Ctrl Pts',(150.579914793211,3.98651952052958,126.429383040045));
#184646=CARTESIAN_POINT('Ctrl Pts',(150.587311150146,4.10013985150687,126.538591781754));
#184647=CARTESIAN_POINT('Ctrl Pts',(150.594708639483,4.21377757804723,126.647817243601));
#184648=CARTESIAN_POINT('Ctrl Pts',(150.602106128819,4.32302773779736,126.761567478045));
#184649=CARTESIAN_POINT('Ctrl Pts',(150.609503618156,4.42752405223851,126.879445162508));
#184650=CARTESIAN_POINT('Ctrl Pts',(150.616903700671,4.5320569977008,126.997364168812));
#184651=CARTESIAN_POINT('Ctrl Pts',(150.624303783186,4.63183253248303,127.119413226679));
#184652=CARTESIAN_POINT('Ctrl Pts',(150.631703865701,4.72652462418257,127.245161896014));
#184653=CARTESIAN_POINT('Ctrl Pts',(150.639112085368,4.82132083957137,127.371048838938));
#184654=CARTESIAN_POINT('Ctrl Pts',(150.646520305034,4.91102222404954,127.500643219211));
#184655=CARTESIAN_POINT('Ctrl Pts',(150.653928524701,4.99534565174867,127.633484968466));
#184656=CARTESIAN_POINT('Ctrl Pts',(150.661341304003,5.07972097911038,127.766408479601));
#184657=CARTESIAN_POINT('Ctrl Pts',(150.668754083305,5.15871156714548,127.902583020226));
#184658=CARTESIAN_POINT('Ctrl Pts',(150.676166862607,5.23208049943405,128.041524355689));
#184659=CARTESIAN_POINT('Ctrl Pts',(150.683590233635,5.30555426469391,128.180664217048));
#184660=CARTESIAN_POINT('Ctrl Pts',(150.691013604664,5.37339017096703,128.322578433019));
#184661=CARTESIAN_POINT('Ctrl Pts',(150.698436975693,5.43539930563968,128.466762501817));
#184662=CARTESIAN_POINT('Ctrl Pts',(150.702373025134,5.46827803673185,128.543212354743));
#184663=CARTESIAN_POINT('Ctrl Pts',(150.706309074575,5.49951948144194,128.620300074247));
#184664=CARTESIAN_POINT('Ctrl Pts',(150.710245124015,5.52910121881237,128.697948911696));
#184665=CARTESIAN_POINT('Ctrl Pts',(150.717668390421,5.58489145227859,128.844392195787));
#184666=CARTESIAN_POINT('Ctrl Pts',(150.725091656826,5.63494400272429,128.993274932717));
#184667=CARTESIAN_POINT('Ctrl Pts',(150.732514923232,5.6790393918795,129.144106977913));
#184668=CARTESIAN_POINT('Ctrl Pts',(150.739929415953,5.72308266394661,129.294760752157));
#184669=CARTESIAN_POINT('Ctrl Pts',(150.747343908674,5.76118268588832,129.447358893899));
#184670=CARTESIAN_POINT('Ctrl Pts',(150.754758401395,5.79316800090004,129.601391342876));
#184671=CARTESIAN_POINT('Ctrl Pts',(150.762165747748,5.82512248726093,129.75527532958));
#184672=CARTESIAN_POINT('Ctrl Pts',(150.769573094102,5.85097392427088,129.910590508307));
#184673=CARTESIAN_POINT('Ctrl Pts',(150.776980440456,5.87060067930828,130.066811821482));
#184674=CARTESIAN_POINT('Ctrl Pts',(150.784382262131,5.89021279597131,130.222916618908));
#184675=CARTESIAN_POINT('Ctrl Pts',(150.791784083807,5.90360942837723,130.379925836323));
#184676=CARTESIAN_POINT('Ctrl Pts',(150.799185905482,5.91072005689088,130.537304496932));
#184677=CARTESIAN_POINT('Ctrl Pts',(150.806583819794,5.91782693175914,130.694600078573));
#184678=CARTESIAN_POINT('Ctrl Pts',(150.813981734105,5.91865439454688,130.852264343029));
#184679=CARTESIAN_POINT('Ctrl Pts',(150.821379648416,5.91318379987458,131.00975757811));
#184680=CARTESIAN_POINT('Ctrl Pts',(150.828776333329,5.9077141143159,131.167224640672));
#184681=CARTESIAN_POINT('Ctrl Pts',(150.836173018241,5.89594846148009,131.32452035756));
#184682=CARTESIAN_POINT('Ctrl Pts',(150.843569703153,5.87792031419289,131.481105283225));
#184683=CARTESIAN_POINT('Ctrl Pts',(150.850966060088,5.85989296629269,131.637683265751));
#184684=CARTESIAN_POINT('Ctrl Pts',(150.858362417024,5.8356037187708,131.793550148872));
#184685=CARTESIAN_POINT('Ctrl Pts',(150.865758773959,5.80513787564255,131.948172143684));
#184686=CARTESIAN_POINT('Ctrl Pts',(150.873156263296,5.77466736811589,132.102817811518));
#184687=CARTESIAN_POINT('Ctrl Pts',(150.880553752633,5.7380184542325,132.256217845262));
#184688=CARTESIAN_POINT('Ctrl Pts',(150.887951241969,5.69532743024335,132.407849321866));
#184689=CARTESIAN_POINT('Ctrl Pts',(150.895351324484,5.65262144098211,132.559533952648));
#184690=CARTESIAN_POINT('Ctrl Pts',(150.902751406999,5.60386922569224,132.709448432841));
#184691=CARTESIAN_POINT('Ctrl Pts',(150.910151489514,5.54925669734036,132.857085798764));
#184692=CARTESIAN_POINT('Ctrl Pts',(150.917559709181,5.49458411689897,133.004885507149));
#184693=CARTESIAN_POINT('Ctrl Pts',(150.924967928847,5.43403848386057,133.150402750441));
#184694=CARTESIAN_POINT('Ctrl Pts',(150.932376148513,5.36785383032385,133.293150648641));
#184695=CARTESIAN_POINT('Ctrl Pts',(150.939788927816,5.30162844123736,133.43598640579));
#184696=CARTESIAN_POINT('Ctrl Pts',(150.947201707118,5.22975728583163,133.576049090089));
#184697=CARTESIAN_POINT('Ctrl Pts',(150.95461448642,5.15251970532112,133.712877636388));
#184698=CARTESIAN_POINT('Ctrl Pts',(150.962037857448,5.0751717641333,133.849901689731));
#184699=CARTESIAN_POINT('Ctrl Pts',(150.969461228477,4.99244227934222,133.983682059071));
#184700=CARTESIAN_POINT('Ctrl Pts',(150.976884599506,4.90465359070537,134.113787111338));
#184701=CARTESIAN_POINT('Ctrl Pts',(150.980820648947,4.85810592152945,134.182771931878));
#184702=CARTESIAN_POINT('Ctrl Pts',(150.984756698388,4.81013660385384,134.25072403948));
#184703=CARTESIAN_POINT('Ctrl Pts',(150.988692747828,4.76079808940158,134.317583086248));
#184704=CARTESIAN_POINT('Ctrl Pts',(150.996116014234,4.66774719094704,134.443677161852));
#184705=CARTESIAN_POINT('Ctrl Pts',(151.003539280639,4.56954255390688,134.566262546077));
#184706=CARTESIAN_POINT('Ctrl Pts',(151.010962547045,4.46647791742634,134.684889650526));
#184707=CARTESIAN_POINT('Ctrl Pts',(151.018377039766,4.36353509478691,134.803376547588));
#184708=CARTESIAN_POINT('Ctrl Pts',(151.025791532487,4.25574394883958,134.917914198125));
#184709=CARTESIAN_POINT('Ctrl Pts',(151.033206025208,4.14344093113797,135.02808265064));
#184710=CARTESIAN_POINT('Ctrl Pts',(151.040613371561,4.03124615531315,135.138144918652));
#184711=CARTESIAN_POINT('Ctrl Pts',(151.048020717915,3.91454842985615,135.243846112645));
#184712=CARTESIAN_POINT('Ctrl Pts',(151.055428064269,3.79372375517209,135.344800093205));
#184713=CARTESIAN_POINT('Ctrl Pts',(151.062829885944,3.67298919608848,135.445678778479));
#184714=CARTESIAN_POINT('Ctrl Pts',(151.07023170762,3.54813410179089,135.541817061911));
#184715=CARTESIAN_POINT('Ctrl Pts',(151.077633529295,3.41957044582327,135.632866445309));
#184716=CARTESIAN_POINT('Ctrl Pts',(151.085031443607,3.29107465760982,135.723867764447));
#184717=CARTESIAN_POINT('Ctrl Pts',(151.092429357918,3.15887451048879,135.809785318427));
#184718=CARTESIAN_POINT('Ctrl Pts',(151.099827272229,3.02341400132938,135.89031169274));
#184719=CARTESIAN_POINT('Ctrl Pts',(151.107223957141,2.88797600324841,135.970824685032));
#184720=CARTESIAN_POINT('Ctrl Pts',(151.114620642054,2.74927903903473,136.04594808522));
#184721=CARTESIAN_POINT('Ctrl Pts',(151.122017326966,2.60779505238653,136.115418471445));
#184722=CARTESIAN_POINT('Ctrl Pts',(151.129413683901,2.46631733928662,136.18488577728));
#184723=CARTESIAN_POINT('Ctrl Pts',(151.136810040837,2.32205318455341,136.24870040302));
#184724=CARTESIAN_POINT('Ctrl Pts',(151.144206397772,2.1754977888152,136.306645591407));
#184725=CARTESIAN_POINT('Ctrl Pts',(151.151603887109,2.02891995507124,136.364599651351));
#184726=CARTESIAN_POINT('Ctrl Pts',(151.159001376445,1.88005052901395,136.416682347392));
#184727=CARTESIAN_POINT('Ctrl Pts',(151.166398865782,1.7294031320678,136.462725696747));
#184728=CARTESIAN_POINT('Ctrl Pts',(151.173798948297,1.57870292591083,136.508785186526));
#184729=CARTESIAN_POINT('Ctrl Pts',(151.181199030812,1.42622386472237,136.548801005477));
#184730=CARTESIAN_POINT('Ctrl Pts',(151.188599113327,1.27249296190427,136.582655541192));
#184731=CARTESIAN_POINT('Ctrl Pts',(151.196007332993,1.11859301615438,136.61654730345));
#184732=CARTESIAN_POINT('Ctrl Pts',(151.20341555266,0.963438844543162,136.644264172089));
#184733=CARTESIAN_POINT('Ctrl Pts',(151.210823772326,0.807566573070859,
136.66573987441));
#184734=CARTESIAN_POINT('Ctrl Pts',(151.218236551628,0.6515983648165,136.687228794667));
#184735=CARTESIAN_POINT('Ctrl Pts',(151.225649330931,0.494911546686642,
136.702468858212));
#184736=CARTESIAN_POINT('Ctrl Pts',(151.233062110233,0.338045016600596,
136.711445865745));
#184737=CARTESIAN_POINT('Ctrl Pts',(151.240485481261,0.180954348259829,
136.720435700046));
#184738=CARTESIAN_POINT('Ctrl Pts',(151.24790885229,0.0236838273676483,
136.723144598866));
#184739=CARTESIAN_POINT('Ctrl Pts',(151.255332223319,-0.133229168437175,
136.719610447554));
#184740=CARTESIAN_POINT('Ctrl Pts',(151.25926827276,-0.21642820388921,136.717736555728));
#184741=CARTESIAN_POINT('Ctrl Pts',(151.2632043222,-0.299526824438706,136.714108384187));
#184742=CARTESIAN_POINT('Ctrl Pts',(151.267140371641,-0.382445906253092,
136.70873744254));
#184743=CARTESIAN_POINT('Ctrl Pts',(151.274563638047,-0.538828706737724,
136.698608014215));
#184744=CARTESIAN_POINT('Ctrl Pts',(151.281986904452,-0.695045267387024,
136.682246066261));
#184745=CARTESIAN_POINT('Ctrl Pts',(151.289410170858,-0.850558563565077,
136.659655716231));
#184746=CARTESIAN_POINT('Ctrl Pts',(151.296824663579,-1.00588805594146,
136.637092066118));
#184747=CARTESIAN_POINT('Ctrl Pts',(151.3042391563,-1.16051557254203,136.608314720081));
#184748=CARTESIAN_POINT('Ctrl Pts',(151.311653649021,-1.31390593599615,
136.5733797503));
#184749=CARTESIAN_POINT('Ctrl Pts',(151.319060995374,-1.46714845604283,
136.538478452159));
#184750=CARTESIAN_POINT('Ctrl Pts',(151.326468341728,-1.61915583527227,
136.497431427929));
#184751=CARTESIAN_POINT('Ctrl Pts',(151.333875688082,-1.76939996625633,
136.450346299616));
#184752=CARTESIAN_POINT('Ctrl Pts',(151.341277509757,-1.91953203949932,
136.403296289168));
#184753=CARTESIAN_POINT('Ctrl Pts',(151.348679331433,-2.06790312835083,
136.350217252759));
#184754=CARTESIAN_POINT('Ctrl Pts',(151.356081153108,-2.21399734964868,
136.291267423613));
#184755=CARTESIAN_POINT('Ctrl Pts',(151.363479067419,-2.36001444894535,
136.232348713624));
#184756=CARTESIAN_POINT('Ctrl Pts',(151.370876981731,-2.50375672910866,
136.167565522326));
#184757=CARTESIAN_POINT('Ctrl Pts',(151.378274896042,-2.64472556245306,
136.097125231811));
#184758=CARTESIAN_POINT('Ctrl Pts',(151.385671580954,-2.78567096933374,
136.026696647195));
#184759=CARTESIAN_POINT('Ctrl Pts',(151.393068265867,-2.92384351053614,
135.950612995893));
#184760=CARTESIAN_POINT('Ctrl Pts',(151.400464950779,-3.0587664646925,135.869128951555));
#184761=CARTESIAN_POINT('Ctrl Pts',(151.407861307714,-3.19368343622383,
135.787648520304));
#184762=CARTESIAN_POINT('Ctrl Pts',(151.41525766465,-3.32535078766426,135.700768365125));
#184763=CARTESIAN_POINT('Ctrl Pts',(151.422654021585,-3.4533184869581,135.608787949739));
#184764=CARTESIAN_POINT('Ctrl Pts',(151.430051510922,-3.58130577843335,
135.516793451917));
#184765=CARTESIAN_POINT('Ctrl Pts',(151.437449000258,-3.7055919867931,135.419697356975));
#184766=CARTESIAN_POINT('Ctrl Pts',(151.444846489595,-3.82575815843665,
135.317840990367));
#184767=CARTESIAN_POINT('Ctrl Pts',(151.45224657211,-3.94596645414534,135.215948918166));
#184768=CARTESIAN_POINT('Ctrl Pts',(151.459646654625,-4.06205155301634,
135.109293493141));
#184769=CARTESIAN_POINT('Ctrl Pts',(151.46704673714,-4.17362964078278,134.998254534212));
#184770=CARTESIAN_POINT('Ctrl Pts',(151.474454956806,-4.28533042012754,
134.887093476532));
#184771=CARTESIAN_POINT('Ctrl Pts',(151.481863176473,-4.3925140263037,134.771539522283));
#184772=CARTESIAN_POINT('Ctrl Pts',(151.489271396139,-4.49483491301252,
134.652007907439));
#184773=CARTESIAN_POINT('Ctrl Pts',(151.496684175441,-4.59721877651929,
134.532402722881));
#184774=CARTESIAN_POINT('Ctrl Pts',(151.504096954743,-4.69473372608831,
134.408815291793));
#184775=CARTESIAN_POINT('Ctrl Pts',(151.511509734045,-4.78707652795662,
134.281691329188));
#184776=CARTESIAN_POINT('Ctrl Pts',(151.518933105074,-4.87955127355102,
134.154385725903));
#184777=CARTESIAN_POINT('Ctrl Pts',(151.526356476103,-4.96683890493653,
134.023533808525));
#184778=CARTESIAN_POINT('Ctrl Pts',(151.533779847131,-5.04868083039081,
133.889608166037));
#184779=CARTESIAN_POINT('Ctrl Pts',(151.537715896572,-5.09207538303798,
133.818597576886));
#184780=CARTESIAN_POINT('Ctrl Pts',(151.541651946013,-5.13393973377019,
133.7467232386));
#184781=CARTESIAN_POINT('Ctrl Pts',(151.545587995454,-5.17424079758205,
133.674057941525));
#184782=CARTESIAN_POINT('Ctrl Pts',(151.553371571041,-5.25393653848299,
133.53036161839));
#184783=CARTESIAN_POINT('Ctrl Pts',(151.561155146628,-5.32773786595042,
133.38317140476));
#184784=CARTESIAN_POINT('Ctrl Pts',(151.568938722215,-5.39534067565741,
133.23298771041));
#184785=CARTESIAN_POINT('Ctrl Pts',(151.576709743611,-5.46283444825421,
133.083046248537));
#184786=CARTESIAN_POINT('Ctrl Pts',(151.584480765007,-5.52414949831497,
132.930121219899));
#184787=CARTESIAN_POINT('Ctrl Pts',(151.592251786403,-5.57902686897509,
132.774738692392));
#184788=CARTESIAN_POINT('Ctrl Pts',(151.600116204852,-5.63456379060807,
132.617488679326));
#184789=CARTESIAN_POINT('Ctrl Pts',(151.607980623302,-5.6835070853738,132.457721980328));
#184790=CARTESIAN_POINT('Ctrl Pts',(151.615845041751,-5.72563672666113,
132.296008912845));
#184791=CARTESIAN_POINT('Ctrl Pts',(151.623589367304,-5.76712303104186,
132.136765270247));
#184792=CARTESIAN_POINT('Ctrl Pts',(151.631333692857,-5.80200216877751,
131.97563459611));
#184793=CARTESIAN_POINT('Ctrl Pts',(151.63907801841,-5.83011250681481,131.8131810775));
#184794=CARTESIAN_POINT('Ctrl Pts',(151.647002483308,-5.85887671429841,
131.646948757222));
#184795=CARTESIAN_POINT('Ctrl Pts',(151.654926948205,-5.8805532369963,131.479331604281));
#184796=CARTESIAN_POINT('Ctrl Pts',(151.662851413103,-5.89502310973353,
131.310950291965));
#184797=CARTESIAN_POINT('Ctrl Pts',(151.670775878,-5.90949298247077,131.142568979649));
#184798=CARTESIAN_POINT('Ctrl Pts',(151.678700342898,-5.91675611320991,
130.973423862282));
#184799=CARTESIAN_POINT('Ctrl Pts',(151.686624807795,-5.91674999613682,
130.804146807182));
#184800=CARTESIAN_POINT('',(153.436624807795,-5.91686882972502,130.799002464883));
#184801=CARTESIAN_POINT('Ctrl Pts',(151.686624807835,-5.91674999613679,
130.804146806335));
#184802=CARTESIAN_POINT('Ctrl Pts',(151.694394241467,-5.91674399871208,
130.638181424187));
#184803=CARTESIAN_POINT('Ctrl Pts',(151.702163675099,-5.90975068576896,
130.472358873233));
#184804=CARTESIAN_POINT('Ctrl Pts',(151.709933108731,-5.89583178258735,
130.307270933572));
#184805=CARTESIAN_POINT('Ctrl Pts',(151.717713027261,-5.88189409576128,
130.141960206734));
#184806=CARTESIAN_POINT('Ctrl Pts',(151.725492945791,-5.86101218853056,
129.977386382935));
#184807=CARTESIAN_POINT('Ctrl Pts',(151.733272864321,-5.83329921270253,
129.814132937896));
#184808=CARTESIAN_POINT('Ctrl Pts',(151.741071519732,-5.8055194939216,129.650486319022));
#184809=CARTESIAN_POINT('Ctrl Pts',(151.748870175143,-5.77087585845673,
129.488166749331));
#184810=CARTESIAN_POINT('Ctrl Pts',(151.756668830555,-5.72953240368024,
129.327746586183));
#184811=CARTESIAN_POINT('Ctrl Pts',(151.764477142575,-5.68813775577232,
129.167127784325));
#184812=CARTESIAN_POINT('Ctrl Pts',(151.772285454596,-5.64002681891617,
129.008413384443));
#184813=CARTESIAN_POINT('Ctrl Pts',(151.780093766616,-5.58541276505045,
128.852158064932));
#184814=CARTESIAN_POINT('Ctrl Pts',(151.787920366743,-5.53067079780044,
128.695536774662));
#184815=CARTESIAN_POINT('Ctrl Pts',(151.79574696687,-5.46939536664615,128.541386377018));
#184816=CARTESIAN_POINT('Ctrl Pts',(151.803573566996,-5.40184768559138,
128.390241286594));
#184817=CARTESIAN_POINT('Ctrl Pts',(151.810394251087,-5.34298158970802,
128.25852216247));
#184818=CARTESIAN_POINT('Ctrl Pts',(151.817214935177,-5.27935270885023,
128.129085204907));
#184819=CARTESIAN_POINT('Ctrl Pts',(151.824035619267,-5.21116117164875,
128.002266792299));
#184820=CARTESIAN_POINT('Ctrl Pts',(151.831458885672,-5.13694516332012,
127.864244440074));
#184821=CARTESIAN_POINT('Ctrl Pts',(151.838882152078,-5.05712967269481,
127.728963936607));
#184822=CARTESIAN_POINT('Ctrl Pts',(151.846305418483,-4.97194166800753,
127.596912003413));
#184823=CARTESIAN_POINT('Ctrl Pts',(151.853719911204,-4.88685434846738,
127.465016144638));
#184824=CARTESIAN_POINT('Ctrl Pts',(151.861134403925,-4.79640735469481,
127.336341571188));
#184825=CARTESIAN_POINT('Ctrl Pts',(151.868548896646,-4.70087414069661,
127.21135172865));
#184826=CARTESIAN_POINT('Ctrl Pts',(151.875956243,-4.60543300520682,127.086482356028));
#184827=CARTESIAN_POINT('Ctrl Pts',(151.883363589354,-4.50491563415403,
126.965290938613));
#184828=CARTESIAN_POINT('Ctrl Pts',(151.890770935708,-4.39963942824886,
126.848213064213));
#184829=CARTESIAN_POINT('Ctrl Pts',(151.898172757383,-4.29444174130989,
126.73122251091));
#184830=CARTESIAN_POINT('Ctrl Pts',(151.905574579058,-4.18449253521667,
126.618339668136));
#184831=CARTESIAN_POINT('Ctrl Pts',(151.912976400734,-4.07015016122592,
126.509967968125));
#184832=CARTESIAN_POINT('Ctrl Pts',(151.920374315045,-3.95586814768432,
126.401653476691));
#184833=CARTESIAN_POINT('Ctrl Pts',(151.927772229356,-3.83719785513682,
126.297845641497));
#184834=CARTESIAN_POINT('Ctrl Pts',(151.935170143668,-3.71453516404212,
126.198911771081));
#184835=CARTESIAN_POINT('Ctrl Pts',(151.94256682858,-3.59189285726126,126.099994341679));
#184836=CARTESIAN_POINT('Ctrl Pts',(151.949963513492,-3.46525975899447,
126.005949503642));
#184837=CARTESIAN_POINT('Ctrl Pts',(151.957360198404,-3.33506565645255,
125.917104983813));
#184838=CARTESIAN_POINT('Ctrl Pts',(151.96475655534,-3.20487732685367,125.828264403444));
#184839=CARTESIAN_POINT('Ctrl Pts',(151.972152912275,-3.0711286152806,125.744623893211));
#184840=CARTESIAN_POINT('Ctrl Pts',(151.979549269211,-2.93427895241776,
125.666468287836));
#184841=CARTESIAN_POINT('Ctrl Pts',(151.986946758547,-2.79740833752209,
125.588300716638));
#184842=CARTESIAN_POINT('Ctrl Pts',(151.994344247884,-2.65743615019851,
125.515619907497));
#184843=CARTESIAN_POINT('Ctrl Pts',(152.001741737221,-2.51484697681013,
125.448665028221));
#184844=CARTESIAN_POINT('Ctrl Pts',(152.009141819736,-2.37220781900786,
125.381686678016));
#184845=CARTESIAN_POINT('Ctrl Pts',(152.016541902251,-2.22695018633235,
125.320438412596));
#184846=CARTESIAN_POINT('Ctrl Pts',(152.023941984766,-2.07957906936119,
125.265111439494));
#184847=CARTESIAN_POINT('Ctrl Pts',(152.031350204432,-1.93204590269703,
125.209723628697));
#184848=CARTESIAN_POINT('Ctrl Pts',(152.038758424098,-1.78239496026529,
125.160270244536));
#184849=CARTESIAN_POINT('Ctrl Pts',(152.046166643765,-1.6311475383365,125.116892967488));
#184850=CARTESIAN_POINT('Ctrl Pts',(152.053579423067,-1.47980702614295,
125.07348899245));
#184851=CARTESIAN_POINT('Ctrl Pts',(152.060992202369,-1.32686843830145,
125.036168664721));
#184852=CARTESIAN_POINT('Ctrl Pts',(152.068404981671,-1.17286320437495,
125.005022511685));
#184853=CARTESIAN_POINT('Ctrl Pts',(152.0758283527,-1.01863792054824,124.973831855565));
#184854=CARTESIAN_POINT('Ctrl Pts',(152.083251723729,-0.86334331429587,
124.948833052723));
#184855=CARTESIAN_POINT('Ctrl Pts',(152.090675094757,-0.707516701305408,
124.930064857232));
#184856=CARTESIAN_POINT('Ctrl Pts',(152.094611144198,-0.624893692094613,
124.920113509647));
#184857=CARTESIAN_POINT('Ctrl Pts',(152.098547193639,-0.542121142311129,
124.911912938485));
#184858=CARTESIAN_POINT('Ctrl Pts',(152.102483243079,-0.459279008347264,
124.905462978601));
#184859=CARTESIAN_POINT('Ctrl Pts',(152.109906509485,-0.303041329096324,
124.893298555553));
#184860=CARTESIAN_POINT('Ctrl Pts',(152.11732977589,-0.146083787901677,
124.887327171775));
#184861=CARTESIAN_POINT('Ctrl Pts',(152.124753042296,0.0110614407656326,
124.887620957328));
#184862=CARTESIAN_POINT('Ctrl Pts',(152.132167535017,0.168020936822925,
124.887914395652));
#184863=CARTESIAN_POINT('Ctrl Pts',(152.139582027738,0.325167309145095,
124.894458263104));
#184864=CARTESIAN_POINT('Ctrl Pts',(152.146996520459,0.481962839262947,
124.907272998744));
#184865=CARTESIAN_POINT('Ctrl Pts',(152.154403866812,0.638607243945569,
124.920075383059));
#184866=CARTESIAN_POINT('Ctrl Pts',(152.161811213166,0.794901110064077,
124.939136572747));
#184867=CARTESIAN_POINT('Ctrl Pts',(152.16921855952,0.950306402420161,124.964424975453));
#184868=CARTESIAN_POINT('Ctrl Pts',(152.176620381195,1.1055957876461,124.989694517115));
#184869=CARTESIAN_POINT('Ctrl Pts',(152.184022202871,1.25999755183236,125.021181964288));
#184870=CARTESIAN_POINT('Ctrl Pts',(152.191424024546,1.41297857840731,125.058803890889));
#184871=CARTESIAN_POINT('Ctrl Pts',(152.198821938858,1.56587884748914,125.096405957168));
#184872=CARTESIAN_POINT('Ctrl Pts',(152.206219853169,1.71735951103385,125.140135964636));
#184873=CARTESIAN_POINT('Ctrl Pts',(152.21361776748,1.86689755890752,125.189859387087));
#184874=CARTESIAN_POINT('Ctrl Pts',(152.221014452393,2.01641075627049,125.239574546408));
#184875=CARTESIAN_POINT('Ctrl Pts',(152.228411137305,2.16398162479775,125.295281026284));
#184876=CARTESIAN_POINT('Ctrl Pts',(152.235807822217,2.30910212812869,125.356794378926));
#184877=CARTESIAN_POINT('Ctrl Pts',(152.243204179153,2.45421619666444,125.418305004001));
#184878=CARTESIAN_POINT('Ctrl Pts',(152.250600536088,2.59687977234429,125.485621844194));
#184879=CARTESIAN_POINT('Ctrl Pts',(152.257996893024,2.7366048821447,125.558512327583));
#184880=CARTESIAN_POINT('Ctrl Pts',(152.26539438236,2.87635138421607,125.63141397069));
#184881=CARTESIAN_POINT('Ctrl Pts',(152.272791871697,3.01315819363307,125.709890783435));
#184882=CARTESIAN_POINT('Ctrl Pts',(152.280189361033,3.14656216097893,125.79366434563));
#184883=CARTESIAN_POINT('Ctrl Pts',(152.287589443548,3.28001289287883,125.877467274517));
#184884=CARTESIAN_POINT('Ctrl Pts',(152.294989526063,3.41005809179386,125.966570451265));
#184885=CARTESIAN_POINT('Ctrl Pts',(152.302389608579,3.53626392966847,126.060652365341));
#184886=CARTESIAN_POINT('Ctrl Pts',(152.309797828245,3.66260854383611,126.154837732154));
#184887=CARTESIAN_POINT('Ctrl Pts',(152.317206047912,3.78510506633482,126.254012546252));
#184888=CARTESIAN_POINT('Ctrl Pts',(152.324614267578,3.90335252399985,126.357814808077));
#184889=CARTESIAN_POINT('Ctrl Pts',(152.33202704688,4.02167276100213,126.461680958462));
#184890=CARTESIAN_POINT('Ctrl Pts',(152.339439826182,4.13573845214823,126.570179975122));
#184891=CARTESIAN_POINT('Ctrl Pts',(152.346852605484,4.24518618352658,126.682913683576));
#184892=CARTESIAN_POINT('Ctrl Pts',(152.354275976513,4.35479029895607,126.795808471239));
#184893=CARTESIAN_POINT('Ctrl Pts',(152.361699347542,4.45976302775116,126.912949758086));
#184894=CARTESIAN_POINT('Ctrl Pts',(152.369122718571,4.55978133275822,127.033906432732));
#184895=CARTESIAN_POINT('Ctrl Pts',(152.373058768011,4.61281343797622,127.098040563942));
#184896=CARTESIAN_POINT('Ctrl Pts',(152.376994817452,4.66445339573696,127.163246845292));
#184897=CARTESIAN_POINT('Ctrl Pts',(152.380930866892,4.71465812659974,127.229457917941));
#184898=CARTESIAN_POINT('Ctrl Pts',(152.388354133298,4.80934268217594,127.354329934586));
#184899=CARTESIAN_POINT('Ctrl Pts',(152.395777399703,4.89920596138387,127.483155080469));
#184900=CARTESIAN_POINT('Ctrl Pts',(152.403200666109,4.98389962585687,127.615524610198));
#184901=CARTESIAN_POINT('Ctrl Pts',(152.41061515883,5.06849318945193,127.747737690136));
#184902=CARTESIAN_POINT('Ctrl Pts',(152.418029651551,5.14792910118636,127.883486503988));
#184903=CARTESIAN_POINT('Ctrl Pts',(152.425444144272,5.22189951513272,128.022329701786));
#184904=CARTESIAN_POINT('Ctrl Pts',(152.432851490626,5.29579863360919,128.161039077283));
#184905=CARTESIAN_POINT('Ctrl Pts',(152.440258836979,5.36424256721013,128.302836571942));
#184906=CARTESIAN_POINT('Ctrl Pts',(152.447666183333,5.42696707431228,128.447252445074));
#184907=CARTESIAN_POINT('Ctrl Pts',(152.455068005008,5.48964479911058,128.591560607398));
#184908=CARTESIAN_POINT('Ctrl Pts',(152.462469826684,5.54661144304806,128.738482918814));
#184909=CARTESIAN_POINT('Ctrl Pts',(152.469871648359,5.59764903232333,128.887525759413));
#184910=CARTESIAN_POINT('Ctrl Pts',(152.477269562671,5.6486596792525,129.036489921457));
#184911=CARTESIAN_POINT('Ctrl Pts',(152.484667476982,5.69374738423859,129.187572031053));
#184912=CARTESIAN_POINT('Ctrl Pts',(152.492065391293,5.73274262823508,129.340259350264));
#184913=CARTESIAN_POINT('Ctrl Pts',(152.499462076206,5.77173139192943,129.492921295612));
#184914=CARTESIAN_POINT('Ctrl Pts',(152.506858761118,5.80462961177846,129.647187559806));
#184915=CARTESIAN_POINT('Ctrl Pts',(152.51425544603,5.83131786286819,129.802531018934));
#184916=CARTESIAN_POINT('Ctrl Pts',(152.521651802965,5.8580049305729,129.957867589971));
#184917=CARTESIAN_POINT('Ctrl Pts',(152.529048159901,5.87848251381301,130.114280893062));
#184918=CARTESIAN_POINT('Ctrl Pts',(152.536444516836,5.89268252059566,130.271234671877));
#184919=CARTESIAN_POINT('Ctrl Pts',(152.543842006173,5.90688470143562,130.428212480717));
#184920=CARTESIAN_POINT('Ctrl Pts',(152.551239495509,5.91480735847635,130.585730558241));
#184921=CARTESIAN_POINT('Ctrl Pts',(152.558636984846,5.91643439093532,130.743248750815));
#184922=CARTESIAN_POINT('Ctrl Pts',(152.566037067361,5.918061993748,130.900822161147));
#184923=CARTESIAN_POINT('Ctrl Pts',(152.573437149876,5.91338957416129,131.058395313563));
#184924=CARTESIAN_POINT('Ctrl Pts',(152.580837232391,5.90245313343109,131.215429431938));
#184925=CARTESIAN_POINT('Ctrl Pts',(152.588245452057,5.89150466696001,131.37263622547));
#184926=CARTESIAN_POINT('Ctrl Pts',(152.595653671724,5.87427844963756,131.529302428629));
#184927=CARTESIAN_POINT('Ctrl Pts',(152.60306189139,5.85086230615452,131.684895021732));
#184928=CARTESIAN_POINT('Ctrl Pts',(152.610474670692,5.82743175042586,131.84058337948));
#184929=CARTESIAN_POINT('Ctrl Pts',(152.617887449994,5.79780374713262,131.995196444689));
#184930=CARTESIAN_POINT('Ctrl Pts',(152.625300229297,5.76211685764562,132.148213243912));
#184931=CARTESIAN_POINT('Ctrl Pts',(152.632723600325,5.72637897705737,132.301448680713));
#184932=CARTESIAN_POINT('Ctrl Pts',(152.640146971354,5.68456501883588,132.453082937305));
#184933=CARTESIAN_POINT('Ctrl Pts',(152.647570342383,5.63686307972441,132.60261120715));
#184934=CARTESIAN_POINT('Ctrl Pts',(152.651506391824,5.61157036701482,132.681894683705));
#184935=CARTESIAN_POINT('Ctrl Pts',(152.655442441264,5.58462313432085,132.760586430516));
#184936=CARTESIAN_POINT('Ctrl Pts',(152.659378490705,5.55605476705483,132.83861379453));
#184937=CARTESIAN_POINT('Ctrl Pts',(152.666801757111,5.50217571798014,132.985770967907));
#184938=CARTESIAN_POINT('Ctrl Pts',(152.674225023516,5.44236477167517,133.131008627844));
#184939=CARTESIAN_POINT('Ctrl Pts',(152.681648289922,5.37677753181936,133.273812770539));
#184940=CARTESIAN_POINT('Ctrl Pts',(152.689062782643,5.31126781063433,133.416448130596));
#184941=CARTESIAN_POINT('Ctrl Pts',(152.696477275364,5.23999553955777,133.556655362616));
#184942=CARTESIAN_POINT('Ctrl Pts',(152.703891768085,5.16316564057221,133.693936906664));
#184943=CARTESIAN_POINT('Ctrl Pts',(152.711299114438,5.08640979313591,133.83108613359));
#184944=CARTESIAN_POINT('Ctrl Pts',(152.718706460792,5.00410716291266,133.965314962822));
#184945=CARTESIAN_POINT('Ctrl Pts',(152.726113807146,4.91651012699712,134.096147174078));
#184946=CARTESIAN_POINT('Ctrl Pts',(152.733515628821,4.82897842425573,134.226881805736));
#184947=CARTESIAN_POINT('Ctrl Pts',(152.740917450497,4.73616038514163,134.354224554757));
#184948=CARTESIAN_POINT('Ctrl Pts',(152.748319272172,4.63835348589855,134.477725219992));
#184949=CARTESIAN_POINT('Ctrl Pts',(152.755717186483,4.54059821815634,134.601160690186));
#184950=CARTESIAN_POINT('Ctrl Pts',(152.763115100795,4.43785956635898,134.720757823964));
#184951=CARTESIAN_POINT('Ctrl Pts',(152.770513015106,4.33047728226959,134.836096852769));
#184952=CARTESIAN_POINT('Ctrl Pts',(152.777909700018,4.22311284316767,134.95141671432));
#184953=CARTESIAN_POINT('Ctrl Pts',(152.785306384931,4.11110655746502,135.062479602365));
#184954=CARTESIAN_POINT('Ctrl Pts',(152.792703069843,3.99483735735602,135.168900117991));
#184955=CARTESIAN_POINT('Ctrl Pts',(152.800099426778,3.87857331274518,135.27531591482));
#184956=CARTESIAN_POINT('Ctrl Pts',(152.807495783714,3.7580470049338,135.377089496483));
#184957=CARTESIAN_POINT('Ctrl Pts',(152.814892140649,3.63367279617466,135.473873715614));
#184958=CARTESIAN_POINT('Ctrl Pts',(152.822289629986,3.50927954540669,135.570672752655));
#184959=CARTESIAN_POINT('Ctrl Pts',(152.829687119322,3.38103751529433,135.662480676899));
#184960=CARTESIAN_POINT('Ctrl Pts',(152.837084608659,3.24939244952186,135.748991976069));
#184961=CARTESIAN_POINT('Ctrl Pts',(152.844484691174,3.11770123577574,135.83553360164));
#184962=CARTESIAN_POINT('Ctrl Pts',(152.851884773689,2.98260492302754,135.916774700531));
#184963=CARTESIAN_POINT('Ctrl Pts',(152.859284856204,2.84457625844915,135.992454339962));
#184964=CARTESIAN_POINT('Ctrl Pts',(152.86669307587,2.70639581716417,136.068217196937));
#184965=CARTESIAN_POINT('Ctrl Pts',(152.874101295537,2.56527691219257,136.138406202024));
#184966=CARTESIAN_POINT('Ctrl Pts',(152.881509515203,2.42171545948031,136.202807134465));
#184967=CARTESIAN_POINT('Ctrl Pts',(152.888922294505,2.27806564708916,136.267247704605));
#184968=CARTESIAN_POINT('Ctrl Pts',(152.896335073807,2.13197063697471,136.325892964705));
#184969=CARTESIAN_POINT('Ctrl Pts',(152.903747853109,1.98394363465944,136.378577891497));
#184970=CARTESIAN_POINT('Ctrl Pts',(152.911171224138,1.83570512442169,136.431338096984));
#184971=CARTESIAN_POINT('Ctrl Pts',(152.918594595167,1.68552946406388,136.47812084926));
#184972=CARTESIAN_POINT('Ctrl Pts',(152.926017966196,1.53394303250813,136.518811539179));
#184973=CARTESIAN_POINT('Ctrl Pts',(152.929954015637,1.45356826922851,136.540386719334));
#184974=CARTESIAN_POINT('Ctrl Pts',(152.933890065077,1.3727970364754,136.560250060588));
#184975=CARTESIAN_POINT('Ctrl Pts',(152.937826114518,1.29170850495124,136.578390380283));
#184976=CARTESIAN_POINT('Ctrl Pts',(152.945249380924,1.1387780651872,136.612602457086));
#184977=CARTESIAN_POINT('Ctrl Pts',(152.952672647329,0.984256231096225,
136.640786316849));
#184978=CARTESIAN_POINT('Ctrl Pts',(152.960095913735,0.828659556224084,
136.662795041743));
#184979=CARTESIAN_POINT('Ctrl Pts',(152.967510406456,0.673246783700032,
136.684777754151));
#184980=CARTESIAN_POINT('Ctrl Pts',(152.974924899177,0.516762065087655,
136.700599807618));
#184981=CARTESIAN_POINT('Ctrl Pts',(152.982339391898,0.35973477698849,136.710164665511));
#184982=CARTESIAN_POINT('Ctrl Pts',(152.989746738251,0.202858837701513,
136.719720304435));
#184983=CARTESIAN_POINT('Ctrl Pts',(152.997154084605,0.0454417401219702,
136.723030731617));
#184984=CARTESIAN_POINT('Ctrl Pts',(153.004561430959,-0.11197944215825,
136.720050870363));
#184985=CARTESIAN_POINT('Ctrl Pts',(153.011963252634,-0.269283213781397,
136.717073231602));
#184986=CARTESIAN_POINT('Ctrl Pts',(153.01936507431,-0.426590692414489,
136.707814652917));
#184987=CARTESIAN_POINT('Ctrl Pts',(153.026766895985,-0.583362317904174,
136.692282064779));
#184988=CARTESIAN_POINT('Ctrl Pts',(153.034164810297,-0.740051184873071,
136.676757676173));
#184989=CARTESIAN_POINT('Ctrl Pts',(153.041562724608,-0.896204391514378,
136.654965910835));
#184990=CARTESIAN_POINT('Ctrl Pts',(153.048960638919,-1.0512851305278,136.626965716388));
#184991=CARTESIAN_POINT('Ctrl Pts',(153.056357323832,-1.2063400979359,136.598970175065));
#184992=CARTESIAN_POINT('Ctrl Pts',(153.063754008744,-1.36032258444087,
136.564768318571));
#184993=CARTESIAN_POINT('Ctrl Pts',(153.071150693656,-1.51270352091475,
136.524470635766));
#184994=CARTESIAN_POINT('Ctrl Pts',(153.078547050591,-1.66507770065822,
136.484174739802));
#184995=CARTESIAN_POINT('Ctrl Pts',(153.085943407527,-1.81585011068001,
136.437783650405));
#184996=CARTESIAN_POINT('Ctrl Pts',(153.093339764462,-1.96450471314927,
136.385458340641));
#184997=CARTESIAN_POINT('Ctrl Pts',(153.100737253799,-2.11318207501793,
136.333125019739));
#184998=CARTESIAN_POINT('Ctrl Pts',(153.108134743135,-2.25974063158198,
136.274855793389));
#184999=CARTESIAN_POINT('Ctrl Pts',(153.115532232472,-2.40368241136039,
136.210860541529));
#185000=CARTESIAN_POINT('Ctrl Pts',(153.122932314987,-2.5476746497063,136.146842856234));
#185001=CARTESIAN_POINT('Ctrl Pts',(153.130332397502,-2.68904794402243,
136.077095300567));
#185002=CARTESIAN_POINT('Ctrl Pts',(153.137732480017,-2.82732723277683,
136.001874569572));
#185003=CARTESIAN_POINT('Ctrl Pts',(153.145140699683,-2.96575857382483,
135.926571125651));
#185004=CARTESIAN_POINT('Ctrl Pts',(153.15254891935,-3.10108878681862,135.845782665914));
#185005=CARTESIAN_POINT('Ctrl Pts',(153.159957139016,-3.23286958708453,
135.75981062694));
#185006=CARTESIAN_POINT('Ctrl Pts',(153.167369918318,-3.36473149623409,
135.67378567361));
#185007=CARTESIAN_POINT('Ctrl Pts',(153.174782697621,-3.4930393360125,135.582570999549));
#185008=CARTESIAN_POINT('Ctrl Pts',(153.182195476923,-3.61737686754928,
135.486509179991));
#185009=CARTESIAN_POINT('Ctrl Pts',(153.189618847951,-3.74189205838202,
135.3903101028));
#185010=CARTESIAN_POINT('Ctrl Pts',(153.19704221898,-3.86242532549634,135.289250286883));
#185011=CARTESIAN_POINT('Ctrl Pts',(153.204465590009,-3.97859572430564,
135.18371064069));
#185012=CARTESIAN_POINT('Ctrl Pts',(153.20840163945,-4.04019205722495,135.12775098789));
#185013=CARTESIAN_POINT('Ctrl Pts',(153.21233768889,-4.10056247302935,135.070532483352));
#185014=CARTESIAN_POINT('Ctrl Pts',(153.216273738331,-4.15965476973412,
135.012115691133));
#185015=CARTESIAN_POINT('Ctrl Pts',(153.223592420534,-4.26953086420184,
134.90349562831));
#185016=CARTESIAN_POINT('Ctrl Pts',(153.230911102736,-4.37533843268223,
134.790381873428));
#185017=CARTESIAN_POINT('Ctrl Pts',(153.238229784938,-4.47667967794884,
134.673116182801));
#185018=CARTESIAN_POINT('Ctrl Pts',(153.245539663129,-4.57789901472265,
134.555991556986));
#185019=CARTESIAN_POINT('Ctrl Pts',(153.252849541319,-4.67466246908713,
134.434725220875));
#185020=CARTESIAN_POINT('Ctrl Pts',(153.26015941951,-4.76660722913028,134.309697418175));
#185021=CARTESIAN_POINT('Ctrl Pts',(153.267512144022,-4.85909091672224,
134.183936774069));
#185022=CARTESIAN_POINT('Ctrl Pts',(153.274864868534,-4.94669893677471,
134.054370679206));
#185023=CARTESIAN_POINT('Ctrl Pts',(153.282217593045,-5.02910073848491,
133.921422747949));
#185024=CARTESIAN_POINT('Ctrl Pts',(153.289514502521,-5.11087702246753,
133.789484033556));
#185025=CARTESIAN_POINT('Ctrl Pts',(153.296811411997,-5.18752564005307,
133.654214974863));
#185026=CARTESIAN_POINT('Ctrl Pts',(153.304108321473,-5.25876516238274,
133.516061104237));
#185027=CARTESIAN_POINT('Ctrl Pts',(153.311402106787,-5.32997418361129,
133.377966383996));
#185028=CARTESIAN_POINT('Ctrl Pts',(153.318695892102,-5.39577854117277,
133.236989650387));
#185029=CARTESIAN_POINT('Ctrl Pts',(153.325989677416,-5.45594192358712,
133.093602476554));
#185030=CARTESIAN_POINT('Ctrl Pts',(153.333281875092,-5.51609221023646,
132.950246513812));
#185031=CARTESIAN_POINT('Ctrl Pts',(153.340574072768,-5.57060381713691,
132.804481509788));
#185032=CARTESIAN_POINT('Ctrl Pts',(153.347866270444,-5.61928803196595,
132.656800245814));
#185033=CARTESIAN_POINT('Ctrl Pts',(153.355262815223,-5.66866888956578,
132.507005748932));
#185034=CARTESIAN_POINT('Ctrl Pts',(153.362659360003,-5.71205414157252,
132.355240103339));
#185035=CARTESIAN_POINT('Ctrl Pts',(153.370055904782,-5.74929893923802,
132.202034495757));
#185036=CARTESIAN_POINT('Ctrl Pts',(153.377351841901,-5.78603713388111,
132.050912787906));
#185037=CARTESIAN_POINT('Ctrl Pts',(153.38464777902,-5.81680082570675,131.898390434799));
#185038=CARTESIAN_POINT('Ctrl Pts',(153.391943716139,-5.84150245883854,
131.744987847601));
#185039=CARTESIAN_POINT('Ctrl Pts',(153.399390564749,-5.86671502842724,
131.58841223237));
#185040=CARTESIAN_POINT('Ctrl Pts',(153.406837413358,-5.8856119489608,131.430919987324));
#185041=CARTESIAN_POINT('Ctrl Pts',(153.414284261967,-5.89815585201501,
131.273069597468));
#185042=CARTESIAN_POINT('Ctrl Pts',(153.421731110576,-5.91069975506921,
131.115219207613));
#185043=CARTESIAN_POINT('Ctrl Pts',(153.429177959186,-5.91689066209841,
130.957011097166));
#185044=CARTESIAN_POINT('Ctrl Pts',(153.436624807795,-5.91674757395282,
130.799002574689));
#185045=CARTESIAN_POINT('',(155.186624807795,-5.92506007442198,130.807039561929));
#185046=CARTESIAN_POINT('Ctrl Pts',(153.436624807795,-5.91819628231606,
130.799001262779));
#185047=CARTESIAN_POINT('Ctrl Pts',(153.455990325912,-5.92201671705791,
130.387995942853));
#185048=CARTESIAN_POINT('Ctrl Pts',(153.568171718631,-5.69523304119842,
128.011295060988));
#185049=CARTESIAN_POINT('Ctrl Pts',(153.773168985959,-2.48153146899543,
124.260694817819));
#185050=CARTESIAN_POINT('Ctrl Pts',(154.05161660977,4.16404298980398,125.179566709394));
#185051=CARTESIAN_POINT('Ctrl Pts',(154.330064233584,6.98306536577905,131.267349416113));
#185052=CARTESIAN_POINT('Ctrl Pts',(154.608511857395,3.38499181231609,136.92966803523));
#185053=CARTESIAN_POINT('Ctrl Pts',(154.886959481209,-3.32372385062522,
136.963128375415));
#185054=CARTESIAN_POINT('Ctrl Pts',(155.079663798008,-5.85279551419678,
133.069460061617));
#185055=CARTESIAN_POINT('Ctrl Pts',(155.179552240204,-5.92590251216317,
130.956692591981));
#185056=CARTESIAN_POINT('Ctrl Pts',(155.186624807795,-5.92506007442198,
130.807039561929));
#185057=CARTESIAN_POINT('',(156.936624807795,-5.90993960677025,130.808420119559));
#185058=CARTESIAN_POINT('Ctrl Pts',(155.186624807795,-5.92506007442198,
130.807039561929));
#185059=CARTESIAN_POINT('Ctrl Pts',(155.272368114808,-5.91484689555162,
128.992741496091));
#185060=CARTESIAN_POINT('Ctrl Pts',(155.450927296425,-4.05138645339299,
125.196360691353));
#185061=CARTESIAN_POINT('Ctrl Pts',(155.722302352647,2.41613535680962,124.236267251306));
#185062=CARTESIAN_POINT('Ctrl Pts',(156.00074997646,6.83190314484835,129.286908822695));
#185063=CARTESIAN_POINT('Ctrl Pts',(156.279197600274,4.96948569979414,135.732014461931));
#185064=CARTESIAN_POINT('Ctrl Pts',(156.557645224086,-1.45964633049555,
137.648846947465));
#185065=CARTESIAN_POINT('Ctrl Pts',(156.776787626594,-5.46381109745409,
134.20729724922));
#185066=CARTESIAN_POINT('Ctrl Pts',(156.903114154496,-5.9144261227287,131.522159083227));
#185067=CARTESIAN_POINT('Ctrl Pts',(156.936624807795,-5.90993960677025,
130.808420119559));
#185068=CARTESIAN_POINT('',(158.686624841308,-5.91340240352139,130.800147492464));
#185069=CARTESIAN_POINT('Ctrl Pts',(156.936624807795,-5.90993960677025,
130.808420119559));
#185070=CARTESIAN_POINT('Ctrl Pts',(156.995930029101,-5.90199962961032,
129.545286070295));
#185071=CARTESIAN_POINT('Ctrl Pts',(157.148051125009,-4.88528165776799,
126.293613740952));
#185072=CARTESIAN_POINT('Ctrl Pts',(157.392988095525,0.473615299172821,
123.822007928195));
#185073=CARTESIAN_POINT('Ctrl Pts',(157.671435719337,6.13045170597051,127.428694400194));
#185074=CARTESIAN_POINT('Ctrl Pts',(157.94988334315,6.15370248419541,134.13745321549));
#185075=CARTESIAN_POINT('Ctrl Pts',(158.228330966963,0.522001304524755,
137.783262763922));
#185076=CARTESIAN_POINT('Ctrl Pts',(158.473911455178,-4.86802256101213,
135.342465056774));
#185077=CARTESIAN_POINT('Ctrl Pts',(158.626676068789,-5.90188209181897,
132.076832144556));
#185078=CARTESIAN_POINT('Ctrl Pts',(158.686624807795,-5.91023198214956,
130.800150465391));
#185079=CARTESIAN_POINT('',(160.436624807795,-5.92111242539784,130.80190585319));
#185080=CARTESIAN_POINT('Ctrl Pts',(158.686624876677,-5.91674849775012,
130.800144354807));
#185081=CARTESIAN_POINT('Ctrl Pts',(158.695090859125,-5.91661988002312,
130.619653055616));
#185082=CARTESIAN_POINT('Ctrl Pts',(158.703556841572,-5.90822844586705,
130.43949138511));
#185083=CARTESIAN_POINT('Ctrl Pts',(158.712022824019,-5.89168835379828,
130.260357948255));
#185084=CARTESIAN_POINT('Ctrl Pts',(158.720527460507,-5.87507274286249,
130.080406622712));
#185085=CARTESIAN_POINT('Ctrl Pts',(158.729032096996,-5.85023399995928,
129.901493083318));
#185086=CARTESIAN_POINT('Ctrl Pts',(158.737536733484,-5.81733743584099,
129.724307044791));
#185087=CARTESIAN_POINT('Ctrl Pts',(158.746093572354,-5.78423894904418,
129.546033419143));
#185088=CARTESIAN_POINT('Ctrl Pts',(158.754650411224,-5.74298350254313,
129.369508707574));
#185089=CARTESIAN_POINT('Ctrl Pts',(158.763207250093,-5.69378812398778,
129.195414576943));
#185090=CARTESIAN_POINT('Ctrl Pts',(158.770546904925,-5.65159063687621,
129.04608480148));
#185091=CARTESIAN_POINT('Ctrl Pts',(158.777886559757,-5.60355225430021,
128.898543003698));
#185092=CARTESIAN_POINT('Ctrl Pts',(158.785226214589,-5.54983746486989,
128.753206143611));
#185093=CARTESIAN_POINT('Ctrl Pts',(158.792649480994,-5.49551076954329,
128.606213641147));
#185094=CARTESIAN_POINT('Ctrl Pts',(158.8000727474,-5.43525804680119,128.461158697887));
#185095=CARTESIAN_POINT('Ctrl Pts',(158.807496013805,-5.36923646405302,
128.318554841649));
#185096=CARTESIAN_POINT('Ctrl Pts',(158.814910506526,-5.30329291333286,
128.176119531326));
#185097=CARTESIAN_POINT('Ctrl Pts',(158.822324999247,-5.23159422979941,
128.036129877013));
#185098=CARTESIAN_POINT('Ctrl Pts',(158.829739491968,-5.15434684888729,
127.899082812628));
#185099=CARTESIAN_POINT('Ctrl Pts',(158.837146838322,-5.07717392190918,
127.762167839363));
#185100=CARTESIAN_POINT('Ctrl Pts',(158.844554184676,-4.99446312652244,
127.628190132767));
#185101=CARTESIAN_POINT('Ctrl Pts',(158.85196153103,-4.90646828810346,127.497625142761));
#185102=CARTESIAN_POINT('Ctrl Pts',(158.859363352705,-4.81853907955477,
127.36715753305));
#185103=CARTESIAN_POINT('Ctrl Pts',(158.866765174381,-4.7253338828433,127.240097880055));
#185104=CARTESIAN_POINT('Ctrl Pts',(158.874166996056,-4.62715154309232,
127.116895477425));
#185105=CARTESIAN_POINT('Ctrl Pts',(158.881564910367,-4.5290210330342,126.993758112383));
#185106=CARTESIAN_POINT('Ctrl Pts',(158.888962824679,-4.42591884457932,
126.874474233687));
#185107=CARTESIAN_POINT('Ctrl Pts',(158.89636073899,-4.31818600554819,126.759462573859));
#185108=CARTESIAN_POINT('Ctrl Pts',(158.903757423902,-4.21047106976063,
126.644470026882));
#185109=CARTESIAN_POINT('Ctrl Pts',(158.911154108815,-4.09812726563609,
126.533748561878));
#185110=CARTESIAN_POINT('Ctrl Pts',(158.918550793727,-3.98153469663544,
126.427682422635));
#185111=CARTESIAN_POINT('Ctrl Pts',(158.925947150662,-3.86494729747148,
126.321620986475));
#185112=CARTESIAN_POINT('Ctrl Pts',(158.933343507598,-3.74411178415559,
126.220214716842));
#185113=CARTESIAN_POINT('Ctrl Pts',(158.940739864533,-3.61944357361845,
126.123809498318));
#185114=CARTESIAN_POINT('Ctrl Pts',(158.94813735387,-3.49475627605998,126.027389519909));
#185115=CARTESIAN_POINT('Ctrl Pts',(158.955534843206,-3.36623540821487,
125.935972345539));
#185116=CARTESIAN_POINT('Ctrl Pts',(158.962932332543,-3.23432764157704,
125.849862129381));
#185117=CARTESIAN_POINT('Ctrl Pts',(158.970332415058,-3.10237363487604,
125.763721727419));
#185118=CARTESIAN_POINT('Ctrl Pts',(158.977732497573,-2.96703067792505,
125.682892191536));
#185119=CARTESIAN_POINT('Ctrl Pts',(158.985132580088,-2.82877230989586,
125.607633014423));
#185120=CARTESIAN_POINT('Ctrl Pts',(158.992540799755,-2.69036191257786,
125.532291082108));
#185121=CARTESIAN_POINT('Ctrl Pts',(158.999949019421,-2.54903003007183,
125.462531919536));
#185122=CARTESIAN_POINT('Ctrl Pts',(159.007357239088,-2.40527322804099,
125.398568237075));
#185123=CARTESIAN_POINT('Ctrl Pts',(159.01477001839,-2.26142794609707,125.334565186036));
#185124=CARTESIAN_POINT('Ctrl Pts',(159.022182797692,-2.11515511668609,
125.276364860532));
#185125=CARTESIAN_POINT('Ctrl Pts',(159.029595576994,-1.96696844522749,
125.224130721049));
#185126=CARTESIAN_POINT('Ctrl Pts',(159.037018948023,-1.81857003770349,
125.171821946978));
#185127=CARTESIAN_POINT('Ctrl Pts',(159.044442319051,-1.6682526823436,125.125496494448));
#185128=CARTESIAN_POINT('Ctrl Pts',(159.05186569008,-1.5165431044626,125.08526736996));
#185129=CARTESIAN_POINT('Ctrl Pts',(159.055801739521,-1.43610304604864,
125.063936922872));
#185130=CARTESIAN_POINT('Ctrl Pts',(159.059737788962,-1.35527173024639,
125.044319513473));
#185131=CARTESIAN_POINT('Ctrl Pts',(159.063673838402,-1.27412836142776,
125.0264260834));
#185132=CARTESIAN_POINT('Ctrl Pts',(159.071097104808,-1.12109450023375,
124.992679632717));
#185133=CARTESIAN_POINT('Ctrl Pts',(159.078520371213,-0.966487599903085,
124.96496621481));
#185134=CARTESIAN_POINT('Ctrl Pts',(159.085943637619,-0.810824658756232,
124.943431174615));
#185135=CARTESIAN_POINT('Ctrl Pts',(159.09335813034,-0.655345698278701,
124.921921587048));
#185136=CARTESIAN_POINT('Ctrl Pts',(159.100772623061,-0.498813547604672,
124.906575892524));
#185137=CARTESIAN_POINT('Ctrl Pts',(159.108187115782,-0.341757874707942,
124.897489015984));
#185138=CARTESIAN_POINT('Ctrl Pts',(159.115594462136,-0.184853577981791,
124.888410897718));
#185139=CARTESIAN_POINT('Ctrl Pts',(159.123001808489,-0.0274271337459625,
124.885579609365));
#185140=CARTESIAN_POINT('Ctrl Pts',(159.130409154843,0.129984249697388,
124.889038592745));
#185141=CARTESIAN_POINT('Ctrl Pts',(159.137810976519,0.287278229792342,
124.892494996285));
#185142=CARTESIAN_POINT('Ctrl Pts',(159.145212798194,0.444556799859494,
124.902232321938));
#185143=CARTESIAN_POINT('Ctrl Pts',(159.152614619869,0.601280423338662,
124.918241997031));
#185144=CARTESIAN_POINT('Ctrl Pts',(159.160012534181,0.757921313636707,
124.934243220741));
#185145=CARTESIAN_POINT('Ctrl Pts',(159.167410448492,0.914007470349413,
124.956510161788));
#185146=CARTESIAN_POINT('Ctrl Pts',(159.174808362803,1.06900226807922,124.984982238964));
#185147=CARTESIAN_POINT('Ctrl Pts',(159.182205047716,1.22397130848554,125.013449584598));
#185148=CARTESIAN_POINT('Ctrl Pts',(159.189601732628,1.37784898306789,125.048119952392));
#185149=CARTESIAN_POINT('Ctrl Pts',(159.19699841754,1.53010656143899,125.088881243695));
#185150=CARTESIAN_POINT('Ctrl Pts',(159.204394774475,1.68235738854946,125.1296407276));
#185151=CARTESIAN_POINT('Ctrl Pts',(159.211791131411,1.83298790168538,125.17649050147));
#185152=CARTESIAN_POINT('Ctrl Pts',(159.219187488346,1.9814825553528,125.229268022341));
#185153=CARTESIAN_POINT('Ctrl Pts',(159.226584977683,2.12999994393089,125.282053623586));
#185154=CARTESIAN_POINT('Ctrl Pts',(159.233982467019,2.27638047016422,125.340768653868));
#185155=CARTESIAN_POINT('Ctrl Pts',(159.241379956356,2.42012680368066,125.40520171857));
#185156=CARTESIAN_POINT('Ctrl Pts',(159.248780038871,2.56392352725143,125.469657370183));
#185157=CARTESIAN_POINT('Ctrl Pts',(159.256180121386,2.70508387916875,125.539834894461));
#185158=CARTESIAN_POINT('Ctrl Pts',(159.263580203901,2.84313358139258,125.615476151628));
#185159=CARTESIAN_POINT('Ctrl Pts',(159.270988423567,2.98133508345591,125.691200584132));
#185160=CARTESIAN_POINT('Ctrl Pts',(159.278396643234,3.11641877732786,125.772400568279));
#185161=CARTESIAN_POINT('Ctrl Pts',(159.2858048629,3.24793729788046,125.858773304462));
#185162=CARTESIAN_POINT('Ctrl Pts',(159.293217642202,3.379536765888,125.945199201623));
#185163=CARTESIAN_POINT('Ctrl Pts',(159.300630421504,3.5075663852619,126.036803978112));
#185164=CARTESIAN_POINT('Ctrl Pts',(159.308043200806,3.6316109617408,126.133243793394));
#185165=CARTESIAN_POINT('Ctrl Pts',(159.315466571835,3.75583277892774,126.229821406407));
#185166=CARTESIAN_POINT('Ctrl Pts',(159.322889942864,3.8760578964236,126.331247616026));
#185167=CARTESIAN_POINT('Ctrl Pts',(159.330313313893,3.99190653076059,126.437140356099));
#185168=CARTESIAN_POINT('Ctrl Pts',(159.334249363333,4.05333225643613,126.493287227747));
#185169=CARTESIAN_POINT('Ctrl Pts',(159.338185412774,4.11352823916345,126.550689214031));
#185170=CARTESIAN_POINT('Ctrl Pts',(159.342121462215,4.1724424615358,126.609285592293));
#185171=CARTESIAN_POINT('Ctrl Pts',(159.34954472862,4.28355284627977,126.719796532962));
#185172=CARTESIAN_POINT('Ctrl Pts',(159.356967995026,4.39043773576217,126.834891917589));
#185173=CARTESIAN_POINT('Ctrl Pts',(159.364391261431,4.49269539695125,126.954215343331));
#185174=CARTESIAN_POINT('Ctrl Pts',(159.371805754152,4.59483219807689,127.073397738694));
#185175=CARTESIAN_POINT('Ctrl Pts',(159.379220246873,4.69235241644284,127.196797947547));
#185176=CARTESIAN_POINT('Ctrl Pts',(159.386634739594,4.78488989052833,127.324021654474));
#185177=CARTESIAN_POINT('Ctrl Pts',(159.394042085948,4.87733817351233,127.451122738402));
#185178=CARTESIAN_POINT('Ctrl Pts',(159.401449432302,4.96481305505397,127.582039683973));
#185179=CARTESIAN_POINT('Ctrl Pts',(159.408856778656,5.04698761211093,127.716344003994));
#185180=CARTESIAN_POINT('Ctrl Pts',(159.416258600331,5.12910088028297,127.850548154785));
#185181=CARTESIAN_POINT('Ctrl Pts',(159.423660422006,5.20592150129936,127.988134332506));
#185182=CARTESIAN_POINT('Ctrl Pts',(159.431062243682,5.27716505490398,128.128643976029));
#185183=CARTESIAN_POINT('Ctrl Pts',(159.438460157993,5.3483709995912,128.269079445604));
#185184=CARTESIAN_POINT('Ctrl Pts',(159.445858072304,5.41400557177566,128.412434975372));
#185185=CARTESIAN_POINT('Ctrl Pts',(159.453255986616,5.47382968100753,128.558226341566));
#185186=CARTESIAN_POINT('Ctrl Pts',(159.460652671528,5.53364384855771,128.70399347988));
#185187=CARTESIAN_POINT('Ctrl Pts',(159.46804935644,5.587649327999,128.852195306212));
#185188=CARTESIAN_POINT('Ctrl Pts',(159.475446041352,5.63565463941373,129.002326392654));
#185189=CARTESIAN_POINT('Ctrl Pts',(159.482842398288,5.68365782222265,129.152450822126));
#185190=CARTESIAN_POINT('Ctrl Pts',(159.490238755223,5.72566125231639,129.304503986051));
#185191=CARTESIAN_POINT('Ctrl Pts',(159.497635112159,5.7615230167609,129.457964282962));
#185192=CARTESIAN_POINT('Ctrl Pts',(159.505032601495,5.79739027173312,129.611448075037));
#185193=CARTESIAN_POINT('Ctrl Pts',(159.512430090832,5.82711390383247,129.766339065531));
#185194=CARTESIAN_POINT('Ctrl Pts',(159.519827580168,5.85060294612467,129.922104572363));
#185195=CARTESIAN_POINT('Ctrl Pts',(159.527227662683,5.87410022246421,130.077924682551));
#185196=CARTESIAN_POINT('Ctrl Pts',(159.534627745198,5.89135850200246,130.234619550542));
#185197=CARTESIAN_POINT('Ctrl Pts',(159.542027827713,5.90233860618015,130.391650621933));
#185198=CARTESIAN_POINT('Ctrl Pts',(159.54943604738,5.91333078411117,130.54885436513));
#185199=CARTESIAN_POINT('Ctrl Pts',(159.556844267046,5.91803097388586,130.706394677405));
#185200=CARTESIAN_POINT('Ctrl Pts',(159.564252486713,5.91645211760912,130.863731507222));
#185201=CARTESIAN_POINT('Ctrl Pts',(159.571665266015,5.91487228957268,131.021165175233));
#185202=CARTESIAN_POINT('Ctrl Pts',(159.579078045317,5.90700573329939,131.178394739263));
#185203=CARTESIAN_POINT('Ctrl Pts',(159.586490824619,5.89291730892882,131.334885030413));
#185204=CARTESIAN_POINT('Ctrl Pts',(159.593914195648,5.87880875435682,131.491598922231));
#185205=CARTESIAN_POINT('Ctrl Pts',(159.601337566676,5.85846062433322,131.647571062304));
#185206=CARTESIAN_POINT('Ctrl Pts',(159.608760937705,5.83198907969069,131.802275411959));
#185207=CARTESIAN_POINT('Ctrl Pts',(159.612696987146,5.81795323154548,131.884303370225));
#185208=CARTESIAN_POINT('Ctrl Pts',(159.616633036587,5.80219671380875,131.965975131038));
#185209=CARTESIAN_POINT('Ctrl Pts',(159.620569086027,5.78474249749451,132.047214108602));
#185210=CARTESIAN_POINT('Ctrl Pts',(159.627992352433,5.75182439025273,132.200428284909));
#185211=CARTESIAN_POINT('Ctrl Pts',(159.635415618838,5.71276527706964,132.352565436319));
#185212=CARTESIAN_POINT('Ctrl Pts',(159.642838885244,5.66764786323264,132.503094929015));
#185213=CARTESIAN_POINT('Ctrl Pts',(159.650253377965,5.62258377443199,132.653446508352));
#185214=CARTESIAN_POINT('Ctrl Pts',(159.657667870686,5.57147574393903,132.802193857082));
#185215=CARTESIAN_POINT('Ctrl Pts',(159.665082363407,5.51445760123563,132.948815776033));
#185216=CARTESIAN_POINT('Ctrl Pts',(159.67248970976,5.45749441476486,133.095296375258));
#185217=CARTESIAN_POINT('Ctrl Pts',(159.679897056114,5.39463259086107,133.239655277422));
#185218=CARTESIAN_POINT('Ctrl Pts',(159.687304402468,5.3260559180466,133.381385825115));
#185219=CARTESIAN_POINT('Ctrl Pts',(159.694706224143,5.25753039230196,133.523010664818));
#185220=CARTESIAN_POINT('Ctrl Pts',(159.702108045819,5.18329866644969,133.662010718739));
#185221=CARTESIAN_POINT('Ctrl Pts',(159.709509867494,5.1035928048584,133.797898832571));
#185222=CARTESIAN_POINT('Ctrl Pts',(159.716907781805,5.02392901937096,133.933715212126));
#185223=CARTESIAN_POINT('Ctrl Pts',(159.724305696117,4.93879704161671,134.066422602066));
#185224=CARTESIAN_POINT('Ctrl Pts',(159.731703610428,4.8484750285367,134.19555811405));
#185225=CARTESIAN_POINT('Ctrl Pts',(159.73910029534,4.75816802533676,134.324672166054));
#185226=CARTESIAN_POINT('Ctrl Pts',(159.746496980253,4.66267291234489,134.450215212586));
#185227=CARTESIAN_POINT('Ctrl Pts',(159.753893665165,4.56231142080306,134.571752960037));
#185228=CARTESIAN_POINT('Ctrl Pts',(159.7612900221,4.46195437939494,134.693285318378));
#185229=CARTESIAN_POINT('Ctrl Pts',(159.768686379036,4.35673162617207,134.810812442921));
#185230=CARTESIAN_POINT('Ctrl Pts',(159.776082735971,4.24700529181384,134.923932999963));
#185231=CARTESIAN_POINT('Ctrl Pts',(159.783480225308,4.13726215807369,135.037070876051));
#185232=CARTESIAN_POINT('Ctrl Pts',(159.790877714644,4.02301433022011,135.145800573338));
#185233=CARTESIAN_POINT('Ctrl Pts',(159.798275203981,3.90466079892524,135.249757631089));
#185234=CARTESIAN_POINT('Ctrl Pts',(159.805675286496,3.78626577898337,135.353751130825));
#185235=CARTESIAN_POINT('Ctrl Pts',(159.813075369011,3.6637624703608,135.452968413815));
#185236=CARTESIAN_POINT('Ctrl Pts',(159.820475451526,3.53758279716106,135.547085416216));
#185237=CARTESIAN_POINT('Ctrl Pts',(159.827883671192,3.41126437643905,135.641305909937));
#185238=CARTESIAN_POINT('Ctrl Pts',(159.835291890859,3.28126181733074,135.730414699631));
#185239=CARTESIAN_POINT('Ctrl Pts',(159.842700110525,3.14803647601173,135.814130762812));
#185240=CARTESIAN_POINT('Ctrl Pts',(159.850112889827,3.01472913671803,135.897898351833));
#185241=CARTESIAN_POINT('Ctrl Pts',(159.857525669129,2.87819538571021,135.976266415152));
#185242=CARTESIAN_POINT('Ctrl Pts',(159.864938448432,2.73892053422907,136.049000249579));
#185243=CARTESIAN_POINT('Ctrl Pts',(159.87236181946,2.59944668030884,136.121838009519));
#185244=CARTESIAN_POINT('Ctrl Pts',(159.879785190489,2.45722424019631,136.189025302982));
#185245=CARTESIAN_POINT('Ctrl Pts',(159.887208561518,2.31275857289416,136.250375522614));
#185246=CARTESIAN_POINT('Ctrl Pts',(159.891144610959,2.23615940968312,136.282904881142));
#185247=CARTESIAN_POINT('Ctrl Pts',(159.8950806604,2.1589298615324,136.313794058186));
#185248=CARTESIAN_POINT('Ctrl Pts',(159.89901670984,2.08114677863706,136.343020983419));
#185249=CARTESIAN_POINT('Ctrl Pts',(159.906439976246,1.93445031182582,136.398142052265));
#185250=CARTESIAN_POINT('Ctrl Pts',(159.913863242651,1.78534061284876,136.447514360626));
#185251=CARTESIAN_POINT('Ctrl Pts',(159.921286509057,1.63430882319367,136.490920670263));
#185252=CARTESIAN_POINT('Ctrl Pts',(159.928701001778,1.48345554057138,136.534275677247));
#185253=CARTESIAN_POINT('Ctrl Pts',(159.936115494499,1.33068504447641,136.571678619083));
#185254=CARTESIAN_POINT('Ctrl Pts',(159.94352998722,1.17650817263736,136.602960369421));
#185255=CARTESIAN_POINT('Ctrl Pts',(159.950937333574,1.02247990227215,136.634211969231));
#185256=CARTESIAN_POINT('Ctrl Pts',(159.958344679927,0.86704831811973,136.659354049223));
#185257=CARTESIAN_POINT('Ctrl Pts',(159.965752026281,0.710739027593632,
136.678267375181));
#185258=CARTESIAN_POINT('Ctrl Pts',(159.973153847957,0.554546318433565,
136.697166594867));
#185259=CARTESIAN_POINT('Ctrl Pts',(159.980555669632,0.397477575349415,
136.709846265965));
#185260=CARTESIAN_POINT('Ctrl Pts',(159.987957491307,0.240068091516747,
136.716238311999));
#185261=CARTESIAN_POINT('Ctrl Pts',(159.995355405619,0.0827417029254899,
136.722626983722));
#185262=CARTESIAN_POINT('Ctrl Pts',(160.00275331993,-0.0749246961394813,
136.722734625595));
#185263=CARTESIAN_POINT('Ctrl Pts',(160.010151234241,-0.232391313986322,
136.716545056476));
#185264=CARTESIAN_POINT('Ctrl Pts',(160.017547919154,-0.389831763738124,
136.71035651595));
#185265=CARTESIAN_POINT('Ctrl Pts',(160.024944604066,-0.547072125519367,
136.697872856038));
#185266=CARTESIAN_POINT('Ctrl Pts',(160.032341288978,-0.703573112222377,
136.679130012041));
#185267=CARTESIAN_POINT('Ctrl Pts',(160.039737645913,-0.860067159507634,
136.660387999121));
#185268=CARTESIAN_POINT('Ctrl Pts',(160.047134002849,-1.01582152625271,
136.635387398346));
#185269=CARTESIAN_POINT('Ctrl Pts',(160.054530359784,-1.17030281856806,
136.604215949844));
#185270=CARTESIAN_POINT('Ctrl Pts',(160.061927849121,-1.3248077623638,136.573039728913));
#185271=CARTESIAN_POINT('Ctrl Pts',(160.069325338457,-1.47803887768987,
136.535690852927));
#185272=CARTESIAN_POINT('Ctrl Pts',(160.076722827794,-1.62947386920359,
136.492308004109));
#185273=CARTESIAN_POINT('Ctrl Pts',(160.084122910309,-1.7809619460186,136.448909947501));
#185274=CARTESIAN_POINT('Ctrl Pts',(160.091522992824,-1.93065228679722,
136.399473809455));
#185275=CARTESIAN_POINT('Ctrl Pts',(160.098923075339,-2.0780387819236,136.344187815532));
#185276=CARTESIAN_POINT('Ctrl Pts',(160.106331295005,-2.22558734365329,
136.288841028974));
#185277=CARTESIAN_POINT('Ctrl Pts',(160.113739514672,-2.37082665080243,
136.227631671566));
#185278=CARTESIAN_POINT('Ctrl Pts',(160.121147734338,-2.51327089691157,
136.160795995804));
#185279=CARTESIAN_POINT('Ctrl Pts',(160.12856051364,-2.65580281507737,136.093919183799));
#185280=CARTESIAN_POINT('Ctrl Pts',(160.135973292943,-2.79553591368827,
136.021409324709));
#185281=CARTESIAN_POINT('Ctrl Pts',(160.143386072245,-2.93201040772376,
135.94354786182));
#185282=CARTESIAN_POINT('Ctrl Pts',(160.150809443273,-3.06867990291634,
135.865575146821));
#185283=CARTESIAN_POINT('Ctrl Pts',(160.158232814302,-3.20208117860711,
135.782235753263));
#185284=CARTESIAN_POINT('Ctrl Pts',(160.165656185331,-3.33178407785868,
135.693853988154));
#185285=CARTESIAN_POINT('Ctrl Pts',(160.169592234772,-3.40055566722048,
135.646991855602));
#185286=CARTESIAN_POINT('Ctrl Pts',(160.173528284212,-3.4682880639065,135.598712804192));
#185287=CARTESIAN_POINT('Ctrl Pts',(160.177464333653,-3.5349211601155,135.549069560617));
#185288=CARTESIAN_POINT('Ctrl Pts',(160.184814521984,-3.65935196658665,
135.456365646416));
#185289=CARTESIAN_POINT('Ctrl Pts',(160.192164710316,-3.78033979812036,
135.358609719615));
#185290=CARTESIAN_POINT('Ctrl Pts',(160.199514898647,-3.89744121542264,
135.256088656746));
#185291=CARTESIAN_POINT('Ctrl Pts',(160.206856366003,-4.01440369225802,
135.1536892348));
#185292=CARTESIAN_POINT('Ctrl Pts',(160.214197833358,-4.12748864631828,
135.046536175349));
#185293=CARTESIAN_POINT('Ctrl Pts',(160.221539300714,-4.23628206835796,
134.93495921823));
#185294=CARTESIAN_POINT('Ctrl Pts',(160.228873737485,-4.3449713039615,134.82348911321));
#185295=CARTESIAN_POINT('Ctrl Pts',(160.236208174257,-4.44937692219924,
134.70760381301));
#185296=CARTESIAN_POINT('Ctrl Pts',(160.243542611028,-4.54911861775299,
134.587672706743));
#185297=CARTESIAN_POINT('Ctrl Pts',(160.250871701082,-4.64878760279232,
134.467829028831));
#185298=CARTESIAN_POINT('Ctrl Pts',(160.258200791136,-4.74379918996974,
134.343945707568));
#185299=CARTESIAN_POINT('Ctrl Pts',(160.26552988119,-4.83381069254079,134.216428136121));
#185300=CARTESIAN_POINT('Ctrl Pts',(160.272855833505,-4.9237836592839,134.088965157643));
#185301=CARTESIAN_POINT('Ctrl Pts',(160.280181785821,-5.00876058062966,
133.957871335271));
#185302=CARTESIAN_POINT('Ctrl Pts',(160.287507738136,-5.08843983619722,
133.823584126335));
#185303=CARTESIAN_POINT('Ctrl Pts',(160.294832163464,-5.16810248378662,
133.689324907607));
#185304=CARTESIAN_POINT('Ctrl Pts',(160.302156588792,-5.24246946773354,
133.551873954233));
#185305=CARTESIAN_POINT('Ctrl Pts',(160.309481014119,-5.31128333298679,
133.411696407072));
#185306=CARTESIAN_POINT('Ctrl Pts',(160.316805428625,-5.38009709656539,
133.271519067027));
#185307=CARTESIAN_POINT('Ctrl Pts',(160.32412984313,-5.4433575896976,133.1286154836));
#185308=CARTESIAN_POINT('Ctrl Pts',(160.331454257636,-5.5008541512746,132.983473778672));
#185309=CARTESIAN_POINT('Ctrl Pts',(160.338780177261,-5.55836252802465,
132.838302248058));
#185310=CARTESIAN_POINT('Ctrl Pts',(160.346106096887,-5.6101044760651,132.690892035358));
#185311=CARTESIAN_POINT('Ctrl Pts',(160.353432016512,-5.65591824276781,
132.541749288424));
#185312=CARTESIAN_POINT('Ctrl Pts',(160.360764971615,-5.70177600690807,
132.392463311645));
#185313=CARTESIAN_POINT('Ctrl Pts',(160.368097926717,-5.74169410699057,
132.24144184254));
#185314=CARTESIAN_POINT('Ctrl Pts',(160.375430881819,-5.77556110624976,
132.08920476005));
#185315=CARTESIAN_POINT('Ctrl Pts',(160.382767538779,-5.8094452024113,131.936890824499));
#185316=CARTESIAN_POINT('Ctrl Pts',(160.39010419574,-5.83727204445423,131.783360427865));
#185317=CARTESIAN_POINT('Ctrl Pts',(160.3974408527,-5.85898183122031,131.62914086947));
#185318=CARTESIAN_POINT('Ctrl Pts',(160.404787910665,-5.88072239543675,
131.47470267766));
#185319=CARTESIAN_POINT('Ctrl Pts',(160.412134968629,-5.89632854334946,
131.319573751473));
#185320=CARTESIAN_POINT('Ctrl Pts',(160.419482026594,-5.90579252285111,
131.16428455333));
#185321=CARTESIAN_POINT('Ctrl Pts',(160.425196286995,-5.91315324377544,
131.04350656032));
#185322=CARTESIAN_POINT('Ctrl Pts',(160.430910547395,-5.91679954108405,
130.922631689549));
#185323=CARTESIAN_POINT('Ctrl Pts',(160.436624807795,-5.91674949152901,
130.801907661968));
#185324=CARTESIAN_POINT('',(162.186624807795,-5.91777788669619,130.809763220789));
#185325=CARTESIAN_POINT('Ctrl Pts',(160.436624807795,-5.92529977099551,
130.801904117208));
#185326=CARTESIAN_POINT('Ctrl Pts',(160.443053857686,-5.92601137657551,
130.665882277054));
#185327=CARTESIAN_POINT('Ctrl Pts',(160.449482907576,-5.9217351792167,130.529905972966));
#185328=CARTESIAN_POINT('Ctrl Pts',(160.548727832071,-5.77652682953759,
128.436339550169));
#185329=CARTESIAN_POINT('Ctrl Pts',(160.734359581279,-3.3663328045,124.668778821217));
#185330=CARTESIAN_POINT('Ctrl Pts',(161.012807205092,3.34245362589332,124.655737658797));
#185331=CARTESIAN_POINT('Ctrl Pts',(161.291254828905,6.97968846202762,130.292980618556));
#185332=CARTESIAN_POINT('Ctrl Pts',(161.569702452718,4.20293057829504,136.400156815103));
#185333=CARTESIAN_POINT('Ctrl Pts',(161.848150076531,-2.43611518231675,
137.365069675955));
#185334=CARTESIAN_POINT('Ctrl Pts',(162.053790861556,-5.68590607778289,
133.625131439863));
#185335=CARTESIAN_POINT('Ctrl Pts',(162.166615771978,-5.92172892300598,
131.234503316265));
#185336=CARTESIAN_POINT('Ctrl Pts',(162.186624807795,-5.91777788669619,
130.809763220789));
#185337=CARTESIAN_POINT('',(163.936624807795,-5.90693473238044,130.804346773966));
#185338=CARTESIAN_POINT('Ctrl Pts',(162.186624807795,-5.91777788669619,
130.809763220789));
#185339=CARTESIAN_POINT('Ctrl Pts',(162.259431646582,-5.90340125874275,
129.264262281094));
#185340=CARTESIAN_POINT('Ctrl Pts',(162.425054359975,-4.4920549294218,125.725268843379));
#185341=CARTESIAN_POINT('Ctrl Pts',(162.683492947968,1.48047183150485,123.96434865219));
#185342=CARTESIAN_POINT('Ctrl Pts',(162.961940571783,6.5549269731353,128.352729954683));
#185343=CARTESIAN_POINT('Ctrl Pts',(163.240388195595,5.60572445244513,134.994040067549));
#185344=CARTESIAN_POINT('Ctrl Pts',(163.518835819408,-0.49486498518204,
137.785239443099));
#185345=CARTESIAN_POINT('Ctrl Pts',(163.750914690142,-5.20052006496424,
134.764823450537));
#185346=CARTESIAN_POINT('Ctrl Pts',(163.89017768627,-5.90691414848796,131.794876866286));
#185347=CARTESIAN_POINT('Ctrl Pts',(163.936624807795,-5.90693473238044,
130.804346773966));
#185348=CARTESIAN_POINT('',(165.686624807795,-5.9178288693344,130.79896272858));
#185349=CARTESIAN_POINT('Ctrl Pts',(163.936624807795,-5.90693473238044,
130.804346773966));
#185350=CARTESIAN_POINT('Ctrl Pts',(163.982993560875,-5.90695528154252,
129.815487965044));
#185351=CARTESIAN_POINT('Ctrl Pts',(164.122178188557,-5.20227317339492,
126.847267783513));
#185352=CARTESIAN_POINT('Ctrl Pts',(164.354178690849,-0.500757509154189,
123.823902004597));
#185353=CARTESIAN_POINT('Ctrl Pts',(164.632626314658,5.60218586257347,126.609950755435));
#185354=CARTESIAN_POINT('Ctrl Pts',(164.911073938473,6.55699410858763,133.250457261255));
#185355=CARTESIAN_POINT('Ctrl Pts',(165.189521562285,1.48624509578439,137.643120449992));
#185356=CARTESIAN_POINT('Ctrl Pts',(165.448038518726,-4.48957751367164,
135.886709966933));
#185357=CARTESIAN_POINT('Ctrl Pts',(165.613739600563,-5.90343703981052,
132.346093050683));
#185358=CARTESIAN_POINT('Ctrl Pts',(165.686624807795,-5.9178288693344,130.79896272858));
#185359=CARTESIAN_POINT('',(167.436624807795,-5.92148368288513,130.806842939611));
#185360=CARTESIAN_POINT('Ctrl Pts',(165.686624807795,-5.9178288693344,130.79896272858));
#185361=CARTESIAN_POINT('Ctrl Pts',(165.706555475167,-5.92176435608143,
130.375895538377));
#185362=CARTESIAN_POINT('Ctrl Pts',(165.819302017143,-5.6870478495866,127.986964075457));
#185363=CARTESIAN_POINT('Ctrl Pts',(166.024864433725,-2.44165234092735,
124.245710270396));
#185364=CARTESIAN_POINT('Ctrl Pts',(166.303312057537,4.19820555675649,125.205018635372));
#185365=CARTESIAN_POINT('Ctrl Pts',(166.581759681351,6.98011764152404,131.309848738916));
#185366=CARTESIAN_POINT('Ctrl Pts',(166.860207305163,3.34764261143406,136.950159953411));
#185367=CARTESIAN_POINT('Ctrl Pts',(167.138654928975,-3.36115243712761,
136.942781817248));
#185368=CARTESIAN_POINT('Ctrl Pts',(167.33079409652,-5.85912794910789,133.045254473615));
#185369=CARTESIAN_POINT('Ctrl Pts',(167.43011738946,-5.92599866040667,130.944526178327));
#185370=CARTESIAN_POINT('Ctrl Pts',(167.436624807795,-5.92527153925886,
130.806844527503));
#185371=CARTESIAN_POINT('',(169.186624778302,-5.9129989234673,130.808555423824));
#185372=CARTESIAN_POINT('Ctrl Pts',(167.436624807795,-5.91674948011374,
130.806840955004));
#185373=CARTESIAN_POINT('Ctrl Pts',(167.443972012379,-5.91681455163261,
130.651615351601));
#185374=CARTESIAN_POINT('Ctrl Pts',(167.451319216962,-5.91076692399308,
130.496140163611));
#185375=CARTESIAN_POINT('Ctrl Pts',(167.458666421546,-5.89857393061799,
130.34094272027));
#185376=CARTESIAN_POINT('Ctrl Pts',(167.466005334366,-5.88639469777177,
130.185920426611));
#185377=CARTESIAN_POINT('Ctrl Pts',(167.473344247186,-5.86808392919402,
130.031175630505));
#185378=CARTESIAN_POINT('Ctrl Pts',(167.480683160006,-5.84366093305929,
129.877237399252));
#185379=CARTESIAN_POINT('Ctrl Pts',(167.488015470109,-5.81925990995148,
129.723437664066));
#185380=CARTESIAN_POINT('Ctrl Pts',(167.495347780212,-5.78875766286815,
129.570443423924));
#185381=CARTESIAN_POINT('Ctrl Pts',(167.502680090315,-5.75222542074246,
129.418780135795));
#185382=CARTESIAN_POINT('Ctrl Pts',(167.510007480636,-5.71571769076565,
129.267218609641));
#185383=CARTESIAN_POINT('Ctrl Pts',(167.517334870957,-5.67318810855586,
129.116986627315));
#185384=CARTESIAN_POINT('Ctrl Pts',(167.524662261277,-5.62475920940763,
128.96860072077));
#185385=CARTESIAN_POINT('Ctrl Pts',(167.531987158873,-5.57634678541911,
128.820265294032));
#185386=CARTESIAN_POINT('Ctrl Pts',(167.539312056469,-5.5220391529434,128.673775056407));
#185387=CARTESIAN_POINT('Ctrl Pts',(167.546636954065,-5.46200904102642,
128.529632546291));
#185388=CARTESIAN_POINT('Ctrl Pts',(167.553960722033,-5.40198818680619,
128.38551226548));
#185389=CARTESIAN_POINT('Ctrl Pts',(167.561284490001,-5.33624675509488,
128.243739344073));
#185390=CARTESIAN_POINT('Ctrl Pts',(167.568608257969,-5.26500596497368,
128.104797180399));
#185391=CARTESIAN_POINT('Ctrl Pts',(167.575932412763,-5.19376141206259,
127.965847678088));
#185392=CARTESIAN_POINT('Ctrl Pts',(167.583256567557,-5.117017096654,127.829729570625));
#185393=CARTESIAN_POINT('Ctrl Pts',(167.590580722352,-5.03504049750885,
127.696902210613));
#185394=CARTESIAN_POINT('Ctrl Pts',(167.597906780482,-4.95304259501328,
127.564040332606));
#185395=CARTESIAN_POINT('Ctrl Pts',(167.605232838613,-4.86580990330667,
127.434471228328));
#185396=CARTESIAN_POINT('Ctrl Pts',(167.612558896743,-4.77365342222497,
127.308625563678));
#185397=CARTESIAN_POINT('Ctrl Pts',(167.619892590845,-4.68140088617454,
127.182648729726));
#185398=CARTESIAN_POINT('Ctrl Pts',(167.627226284948,-4.5842145368701,127.060403394326));
#185399=CARTESIAN_POINT('Ctrl Pts',(167.63455997905,-4.48244629727542,126.942287889802));
#185400=CARTESIAN_POINT('Ctrl Pts',(167.641897718933,-4.38062191517208,
126.824107224469));
#185401=CARTESIAN_POINT('Ctrl Pts',(167.649235458816,-4.27421086771408,
126.710061206532));
#185402=CARTESIAN_POINT('Ctrl Pts',(167.656573198699,-4.16360166614498,
126.600510985601));
#185403=CARTESIAN_POINT('Ctrl Pts',(167.663921850295,-4.0528279812466,126.490797856116));
#185404=CARTESIAN_POINT('Ctrl Pts',(167.671270501891,-3.93784395315123,
126.385594134857));
#185405=CARTESIAN_POINT('Ctrl Pts',(167.678619153487,-3.81907152118827,
126.285220956242));
#185406=CARTESIAN_POINT('Ctrl Pts',(167.684262827859,-3.72785574894204,
126.208135585093));
#185407=CARTESIAN_POINT('Ctrl Pts',(167.68990650223,-3.63440624112913,126.133898470931));
#185408=CARTESIAN_POINT('Ctrl Pts',(167.695550176602,-3.53892500501756,
126.062637262987));
#185409=CARTESIAN_POINT('Ctrl Pts',(167.702973443007,-3.41333614114691,
125.968905609436));
#185410=CARTESIAN_POINT('Ctrl Pts',(167.710396709413,-3.28383094794813,
125.880025172351));
#185411=CARTESIAN_POINT('Ctrl Pts',(167.717819975818,-3.15082080951499,
125.796341169837));
#185412=CARTESIAN_POINT('Ctrl Pts',(167.725234468539,-3.01796787801939,
125.712756074865));
#185413=CARTESIAN_POINT('Ctrl Pts',(167.73264896126,-2.88161855994549,125.634355386119));
#185414=CARTESIAN_POINT('Ctrl Pts',(167.740063453981,-2.74221653490598,
125.561443582347));
#185415=CARTESIAN_POINT('Ctrl Pts',(167.747470800335,-2.60294887078684,
125.488602053717));
#185416=CARTESIAN_POINT('Ctrl Pts',(167.754878146689,-2.46063468583382,
125.421239049779));
#185417=CARTESIAN_POINT('Ctrl Pts',(167.762285493042,-2.3157457177737,125.359615230212));
#185418=CARTESIAN_POINT('Ctrl Pts',(167.769687314718,-2.17096481337226,
125.298037372015));
#185419=CARTESIAN_POINT('Ctrl Pts',(167.777089136393,-2.02361329162015,
125.242190320611));
#185420=CARTESIAN_POINT('Ctrl Pts',(167.784490958069,-1.8741864167139,125.192288287499));
#185421=CARTESIAN_POINT('Ctrl Pts',(167.79188887238,-1.72483842309231,125.142412597282));
#185422=CARTESIAN_POINT('Ctrl Pts',(167.799286786691,-1.57341761136135,
125.098475793171));
#185423=CARTESIAN_POINT('Ctrl Pts',(167.806684701002,-1.42043799449899,
125.060643487842));
#185424=CARTESIAN_POINT('Ctrl Pts',(167.814081385915,-1.26748380007303,
125.022817469556));
#185425=CARTESIAN_POINT('Ctrl Pts',(167.821478070827,-1.11297167666974,
124.991094026185));
#185426=CARTESIAN_POINT('Ctrl Pts',(167.828874755739,-0.957429641656374,
124.965588568258));
#185427=CARTESIAN_POINT('Ctrl Pts',(167.836271112675,-0.801894503539834,
124.940084241271));
#185428=CARTESIAN_POINT('Ctrl Pts',(167.84366746961,-0.645329912993157,
124.920797411925));
#185429=CARTESIAN_POINT('Ctrl Pts',(167.851063826545,-0.488272628939536,
124.907792089826));
#185430=CARTESIAN_POINT('Ctrl Pts',(167.858461315882,-0.331191299014834,
124.89478477658));
#185431=CARTESIAN_POINT('Ctrl Pts',(167.865858805218,-0.1736174974353,124.888060916291));
#185432=CARTESIAN_POINT('Ctrl Pts',(167.873256294555,-0.0160914847102347,
124.887632499204));
#185433=CARTESIAN_POINT('Ctrl Pts',(167.88065637707,0.14148974851462,124.887203931936));
#185434=CARTESIAN_POINT('Ctrl Pts',(167.888056459585,0.29902278646763,124.893075202722));
#185435=CARTESIAN_POINT('Ctrl Pts',(167.8954565421,0.45596914255646,124.90520621176));
#185436=CARTESIAN_POINT('Ctrl Pts',(167.902864761766,0.613088077298231,
124.91735056009));
#185437=CARTESIAN_POINT('Ctrl Pts',(167.910272981433,0.769618669418635,
124.935768364139));
#185438=CARTESIAN_POINT('Ctrl Pts',(167.917681201099,0.925028582930064,
124.96036774597));
#185439=CARTESIAN_POINT('Ctrl Pts',(167.925093980401,1.08053414865005,124.984982268311));
#185440=CARTESIAN_POINT('Ctrl Pts',(167.932506759704,1.23491729609663,125.015785876818));
#185441=CARTESIAN_POINT('Ctrl Pts',(167.939919539006,1.38765812122744,125.052636050004));
#185442=CARTESIAN_POINT('Ctrl Pts',(167.947342910034,1.5406171896123,125.089538876447));
#185443=CARTESIAN_POINT('Ctrl Pts',(167.954766281063,1.69192889079118,125.132505421117));
#185444=CARTESIAN_POINT('Ctrl Pts',(167.962189652092,1.84108986408209,125.181343751606));
#185445=CARTESIAN_POINT('Ctrl Pts',(167.966125701533,1.92017859118967,125.20723900629));
#185446=CARTESIAN_POINT('Ctrl Pts',(167.970061750973,1.99866301631166,125.234784230544));
#185447=CARTESIAN_POINT('Ctrl Pts',(167.973997800414,2.07647074253002,125.263945487098));
#185448=CARTESIAN_POINT('Ctrl Pts',(167.98142106682,2.22321368588102,125.318942706867));
#185449=CARTESIAN_POINT('Ctrl Pts',(167.988844333225,2.36799203508985,125.379857046413));
#185450=CARTESIAN_POINT('Ctrl Pts',(167.996267599631,2.51029298523497,125.446528995465));
#185451=CARTESIAN_POINT('Ctrl Pts',(168.003682092352,2.65242574747452,125.513122143811));
#185452=CARTESIAN_POINT('Ctrl Pts',(168.011096585073,2.79208660427583,125.585459199409));
#185453=CARTESIAN_POINT('Ctrl Pts',(168.018511077794,2.92877956937595,125.663331460237));
#185454=CARTESIAN_POINT('Ctrl Pts',(168.025918424147,3.06534078464996,125.741128664848));
#185455=CARTESIAN_POINT('Ctrl Pts',(168.033325770501,3.19893948086716,125.824450270135));
#185456=CARTESIAN_POINT('Ctrl Pts',(168.040733116855,3.32910137189247,125.913040282711));
#185457=CARTESIAN_POINT('Ctrl Pts',(168.04813493853,3.45916618326872,126.001564221514));
#185458=CARTESIAN_POINT('Ctrl Pts',(168.055536760206,3.58579898605364,126.095348534552));
#185459=CARTESIAN_POINT('Ctrl Pts',(168.062938581881,3.70855185565093,126.194092328578));
#185460=CARTESIAN_POINT('Ctrl Pts',(168.070336496192,3.83123992496291,126.292783996523));
#185461=CARTESIAN_POINT('Ctrl Pts',(168.077734410504,3.95005185001548,126.396429698054));
#185462=CARTESIAN_POINT('Ctrl Pts',(168.085132324815,4.06457045960395,126.504686497192));
#185463=CARTESIAN_POINT('Ctrl Pts',(168.092529009727,4.17907003827798,126.612925306015));
#185464=CARTESIAN_POINT('Ctrl Pts',(168.09992569464,4.28927744650871,126.725773435414));
#185465=CARTESIAN_POINT('Ctrl Pts',(168.107322379552,4.3948101798645,126.842849031636));
#185466=CARTESIAN_POINT('Ctrl Pts',(168.114718736487,4.50033823378823,126.959919436603));
#185467=CARTESIAN_POINT('Ctrl Pts',(168.122115093423,4.60119177504133,127.081216658401));
#185468=CARTESIAN_POINT('Ctrl Pts',(168.129511450358,4.69702681922106,127.206323705301));
#185469=CARTESIAN_POINT('Ctrl Pts',(168.136908939695,4.79287653599075,127.331449906411));
#185470=CARTESIAN_POINT('Ctrl Pts',(168.144306429031,4.88370599878966,127.460386797676));
#185471=CARTESIAN_POINT('Ctrl Pts',(168.151703918368,4.96921309588313,127.59268632365));
#185472=CARTESIAN_POINT('Ctrl Pts',(168.159104000883,5.05475016735696,127.725032227017));
#185473=CARTESIAN_POINT('Ctrl Pts',(168.166504083398,5.13496095593303,127.860742798688));
#185474=CARTESIAN_POINT('Ctrl Pts',(168.173904165913,5.20958813355524,127.999343319719));
#185475=CARTESIAN_POINT('Ctrl Pts',(168.181312385579,5.28429737143119,128.138096246271));
#185476=CARTESIAN_POINT('Ctrl Pts',(168.188720605246,5.35341055977898,128.279745139567));
#185477=CARTESIAN_POINT('Ctrl Pts',(168.196128824912,5.41671725750466,128.423792467995));
#185478=CARTESIAN_POINT('Ctrl Pts',(168.203541604214,5.48006291944636,128.56792845515));
#185479=CARTESIAN_POINT('Ctrl Pts',(168.210954383516,5.53759483341865,128.714465472273));
#185480=CARTESIAN_POINT('Ctrl Pts',(168.218367162819,5.58915188595099,128.862889073023));
#185481=CARTESIAN_POINT('Ctrl Pts',(168.225790533847,5.64078260561777,129.011524748374));
#185482=CARTESIAN_POINT('Ctrl Pts',(168.233213904876,5.68642130519154,129.162052034856));
#185483=CARTESIAN_POINT('Ctrl Pts',(168.240637275905,5.72595738410117,129.313943696716));
#185484=CARTESIAN_POINT('Ctrl Pts',(168.244573325346,5.74692036179461,129.394480300425));
#185485=CARTESIAN_POINT('Ctrl Pts',(168.248509374786,5.76616853337601,129.475400336614));
#185486=CARTESIAN_POINT('Ctrl Pts',(168.252445424227,5.78369131892802,129.556624551783));
#185487=CARTESIAN_POINT('Ctrl Pts',(168.259868690633,5.81673874561114,129.709810886667));
#185488=CARTESIAN_POINT('Ctrl Pts',(168.267291957038,5.8437460207227,129.864542700632));
#185489=CARTESIAN_POINT('Ctrl Pts',(168.274715223444,5.86457016118434,130.020302337177));
#185490=CARTESIAN_POINT('Ctrl Pts',(168.282129716165,5.88536968924135,130.175877878767));
#185491=CARTESIAN_POINT('Ctrl Pts',(168.289544208886,5.90000058018201,130.332478458477));
#185492=CARTESIAN_POINT('Ctrl Pts',(168.296958701607,5.90837032823849,130.489573980475));
#185493=CARTESIAN_POINT('Ctrl Pts',(168.30436604796,5.91673200921669,130.646518087894));
#185494=CARTESIAN_POINT('Ctrl Pts',(168.311773394314,5.91884454153348,130.803955817635));
#185495=CARTESIAN_POINT('Ctrl Pts',(168.319180740668,5.91466693643344,130.961349768659));
#185496=CARTESIAN_POINT('Ctrl Pts',(168.326582562343,5.91049244714892,131.118626329337));
#185497=CARTESIAN_POINT('Ctrl Pts',(168.333984384019,5.90003717156359,131.275858804753));
#185498=CARTESIAN_POINT('Ctrl Pts',(168.341386205694,5.88331214550307,131.432507703109));
#185499=CARTESIAN_POINT('Ctrl Pts',(168.348784120006,5.86659594845354,131.589073907731));
#185500=CARTESIAN_POINT('Ctrl Pts',(168.356182034317,5.84361663198994,131.745056778573));
#185501=CARTESIAN_POINT('Ctrl Pts',(168.363579948628,5.81443722663803,131.89991997241));
#185502=CARTESIAN_POINT('Ctrl Pts',(168.370976633541,5.78526267037401,132.054757430793));
#185503=CARTESIAN_POINT('Ctrl Pts',(168.378373318453,5.74989013919929,132.208475214983));
#185504=CARTESIAN_POINT('Ctrl Pts',(168.385770003365,5.70843414450413,132.360545111885));
#185505=CARTESIAN_POINT('Ctrl Pts',(168.3931663603,5.66697998801119,132.512608265849));
#185506=CARTESIAN_POINT('Ctrl Pts',(168.400562717236,5.61944300252852,132.663023317657));
#185507=CARTESIAN_POINT('Ctrl Pts',(168.407959074171,5.56598808303539,132.811275469274));
#185508=CARTESIAN_POINT('Ctrl Pts',(168.415356563508,5.51252497945723,132.959550318676));
#185509=CARTESIAN_POINT('Ctrl Pts',(168.422754052845,5.4531422644287,133.105661257341));
#185510=CARTESIAN_POINT('Ctrl Pts',(168.430151542181,5.38805360091495,133.249111925198));
#185511=CARTESIAN_POINT('Ctrl Pts',(168.437551624696,5.32294212067166,133.392612879463));
#185512=CARTESIAN_POINT('Ctrl Pts',(168.444951707211,5.25212086368438,133.533451366482));
#185513=CARTESIAN_POINT('Ctrl Pts',(168.452351789726,5.17585013234562,133.67115429169));
#185514=CARTESIAN_POINT('Ctrl Pts',(168.459760009393,5.09949553349667,133.809008635421));
#185515=CARTESIAN_POINT('Ctrl Pts',(168.467168229059,5.01767967434691,133.943720204958));
#185516=CARTESIAN_POINT('Ctrl Pts',(168.474576448726,4.9307073937808,134.07484302226));
#185517=CARTESIAN_POINT('Ctrl Pts',(168.481989228028,4.84368158322695,134.206046543469));
#185518=CARTESIAN_POINT('Ctrl Pts',(168.48940200733,4.75149324537416,134.333656609204));
#185519=CARTESIAN_POINT('Ctrl Pts',(168.496814786632,4.6544881127323,134.457259599325));
#185520=CARTESIAN_POINT('Ctrl Pts',(168.504238157661,4.5573443746082,134.581039199194));
#185521=CARTESIAN_POINT('Ctrl Pts',(168.511661528689,4.45537033724308,134.700800004877));
#185522=CARTESIAN_POINT('Ctrl Pts',(168.519084899718,4.34894979669837,134.816163981179));
#185523=CARTESIAN_POINT('Ctrl Pts',(168.523020949159,4.2925230725765,134.877332729534));
#185524=CARTESIAN_POINT('Ctrl Pts',(168.5269569986,4.23484686126025,134.937266017562));
#185525=CARTESIAN_POINT('Ctrl Pts',(168.53089304804,4.17598212226016,134.995912105627));
#185526=CARTESIAN_POINT('Ctrl Pts',(168.538316314446,4.06496506161014,135.106516797436));
#185527=CARTESIAN_POINT('Ctrl Pts',(168.545739580851,3.94938289617561,135.212875107856));
#185528=CARTESIAN_POINT('Ctrl Pts',(168.553162847257,3.82959385918532,135.31458693519));
#185529=CARTESIAN_POINT('Ctrl Pts',(168.560577339978,3.70994640288897,135.416178547591));
#185530=CARTESIAN_POINT('Ctrl Pts',(168.567991832699,3.58610225395346,135.513134369022));
#185531=CARTESIAN_POINT('Ctrl Pts',(168.57540632542,3.45845739538752,135.605090042017));
#185532=CARTESIAN_POINT('Ctrl Pts',(168.582813671773,3.33093556574234,135.696957084672));
#185533=CARTESIAN_POINT('Ctrl Pts',(168.590221018127,3.19962062016315,135.783833356494));
#185534=CARTESIAN_POINT('Ctrl Pts',(168.597628364481,3.064942533938,135.865393894097));
#185535=CARTESIAN_POINT('Ctrl Pts',(168.605030186156,2.93036489571015,135.946893600775));
#185536=CARTESIAN_POINT('Ctrl Pts',(168.612432007832,2.79242942924893,136.023085274895));
#185537=CARTESIAN_POINT('Ctrl Pts',(168.619833829507,2.65159598941728,136.093686592717));
#185538=CARTESIAN_POINT('Ctrl Pts',(168.627231743819,2.51083689446027,136.164250640653));
#185539=CARTESIAN_POINT('Ctrl Pts',(168.63462965813,2.36718320570566,136.229230042688));
#185540=CARTESIAN_POINT('Ctrl Pts',(168.642027572441,2.22112023343574,136.288387921576));
#185541=CARTESIAN_POINT('Ctrl Pts',(168.649424257354,2.07508153418408,136.347535969496));
#185542=CARTESIAN_POINT('Ctrl Pts',(168.656820942266,1.92663469170935,136.400864274336));
#185543=CARTESIAN_POINT('Ctrl Pts',(168.664217627178,1.77628600285024,136.448183665694));
#185544=CARTESIAN_POINT('Ctrl Pts',(168.671613984114,1.62594398060959,136.49550095886));
#185545=CARTESIAN_POINT('Ctrl Pts',(168.679010341049,1.47370063573898,136.53680975625));
#185546=CARTESIAN_POINT('Ctrl Pts',(168.686406697984,1.32007821216927,136.571970527768));
#185547=CARTESIAN_POINT('Ctrl Pts',(168.693804187321,1.16643226861439,136.607136682489));
#185548=CARTESIAN_POINT('Ctrl Pts',(168.701201676658,1.01140718986344,136.636152853836));
#185549=CARTESIAN_POINT('Ctrl Pts',(168.708599165994,0.855536067754428,
136.658930507769));
#185550=CARTESIAN_POINT('Ctrl Pts',(168.715999248509,0.699610305265305,
136.681716146373));
#185551=CARTESIAN_POINT('Ctrl Pts',(168.723399331024,0.542838278075566,
136.698258859513));
#185552=CARTESIAN_POINT('Ctrl Pts',(168.730799413539,0.385758713844092,
136.708521927794));
#185553=CARTESIAN_POINT('Ctrl Pts',(168.738207633206,0.228506424483239,
136.718796281374));
#185554=CARTESIAN_POINT('Ctrl Pts',(168.745615852872,0.0709462954679959,
136.722777175773));
#185555=CARTESIAN_POINT('Ctrl Pts',(168.753024072538,-0.0863816863814132,
136.720480018555));
#185556=CARTESIAN_POINT('Ctrl Pts',(168.760436851841,-0.243806500978941,
136.718181447475));
#185557=CARTESIAN_POINT('Ctrl Pts',(168.767849631143,-0.400998511820644,
136.709597145508));
#185558=CARTESIAN_POINT('Ctrl Pts',(168.775262410445,-0.55742285170284,
136.69479441542));
#185559=CARTESIAN_POINT('Ctrl Pts',(168.782685781474,-0.714070698017043,
136.679970534497));
#185560=CARTESIAN_POINT('Ctrl Pts',(168.790109152502,-0.869948313691009,
136.658910529599));
#185561=CARTESIAN_POINT('Ctrl Pts',(168.797532523531,-1.02453019586171,
136.631732961965));
#185562=CARTESIAN_POINT('Ctrl Pts',(168.801468572972,-1.1064932189296,136.617322763489));
#185563=CARTESIAN_POINT('Ctrl Pts',(168.805404622413,-1.18809219258352,
136.601193539564));
#185564=CARTESIAN_POINT('Ctrl Pts',(168.809340671853,-1.26925063669719,
136.583368610617));
#185565=CARTESIAN_POINT('Ctrl Pts',(168.816763938259,-1.42231292942813,
136.549751350918));
#185566=CARTESIAN_POINT('Ctrl Pts',(168.824187204664,-1.57427017187731,
136.509998066409));
#185567=CARTESIAN_POINT('Ctrl Pts',(168.83161047107,-1.72459211334545,136.464193884111));
#185568=CARTESIAN_POINT('Ctrl Pts',(168.839024963791,-1.87473638676212,
136.418443838552));
#185569=CARTESIAN_POINT('Ctrl Pts',(168.846439456512,-2.02324885282527,
136.366657238365));
#185570=CARTESIAN_POINT('Ctrl Pts',(168.853853949233,-2.16960892878973,
136.308970291159));
#185571=CARTESIAN_POINT('Ctrl Pts',(168.861261295586,-2.31582793740229,
136.251338944805));
#185572=CARTESIAN_POINT('Ctrl Pts',(168.86866864194,-2.45989834098218,136.187818709047));
#185573=CARTESIAN_POINT('Ctrl Pts',(168.876075988294,-2.60131432648213,
136.118595683626));
#185574=CARTESIAN_POINT('Ctrl Pts',(168.883477809969,-2.74262483860503,
136.049424287348));
#185575=CARTESIAN_POINT('Ctrl Pts',(168.890879631645,-2.88128454078637,
135.974558733826));
#185576=CARTESIAN_POINT('Ctrl Pts',(168.89828145332,-3.01680734327979,135.894233309101));
#185577=CARTESIAN_POINT('Ctrl Pts',(168.905679367632,-3.15225860434103,
135.813950287542));
#185578=CARTESIAN_POINT('Ctrl Pts',(168.913077281943,-3.28457594329207,
135.72821332472));
#185579=CARTESIAN_POINT('Ctrl Pts',(168.920475196254,-3.41329774653486,
135.637302687982));
#185580=CARTESIAN_POINT('Ctrl Pts',(168.927871881166,-3.54199815854864,
135.546407158943));
#185581=CARTESIAN_POINT('Ctrl Pts',(168.935268566079,-3.66710391612022,
135.450339877519));
#185582=CARTESIAN_POINT('Ctrl Pts',(168.942665250991,-3.78818219902325,
135.349424554355));
#185583=CARTESIAN_POINT('Ctrl Pts',(168.950061607926,-3.90925511318838,
135.248513705883));
#185584=CARTESIAN_POINT('Ctrl Pts',(168.957457964862,-4.02630062101159,
135.1427554821));
#185585=CARTESIAN_POINT('Ctrl Pts',(168.964854321797,-4.1389190462698,135.032513842193));
#185586=CARTESIAN_POINT('Ctrl Pts',(168.972251811134,-4.25155471369718,
134.922255324009));
#185587=CARTESIAN_POINT('Ctrl Pts',(168.97964930047,-4.35976168219568,134.807512284089));
#185588=CARTESIAN_POINT('Ctrl Pts',(168.987046789807,-4.4631773164106,134.688685372884));
#185589=CARTESIAN_POINT('Ctrl Pts',(168.994446872322,-4.56662920281481,
134.569816807091));
#185590=CARTESIAN_POINT('Ctrl Pts',(169.001846954837,-4.66528616595876,
134.446861801133));
#185591=CARTESIAN_POINT('Ctrl Pts',(169.009247037352,-4.7588261173174,134.320253754116));
#185592=CARTESIAN_POINT('Ctrl Pts',(169.016655257018,-4.85246892546906,
134.193506488535));
#185593=CARTESIAN_POINT('Ctrl Pts',(169.024063476685,-4.94098326302515,
134.063098460322));
#185594=CARTESIAN_POINT('Ctrl Pts',(169.031471696351,-5.02409021673763,
133.929492303844));
#185595=CARTESIAN_POINT('Ctrl Pts',(169.038884475653,-5.10724832139393,
133.795803915006));
#185596=CARTESIAN_POINT('Ctrl Pts',(169.046297254955,-5.18499222651813,
133.658913799479));
#185597=CARTESIAN_POINT('Ctrl Pts',(169.053710034257,-5.25708944704321,
133.519308334979));
#185598=CARTESIAN_POINT('Ctrl Pts',(169.061133405286,-5.32928968345753,
133.379503395645));
#185599=CARTESIAN_POINT('Ctrl Pts',(169.068556776315,-5.39582696368089,
133.236975695829));
#185600=CARTESIAN_POINT('Ctrl Pts',(169.075980147344,-5.45651698950754,
133.092231441217));
#185601=CARTESIAN_POINT('Ctrl Pts',(169.079916196784,-5.48869629743827,
133.015484564331));
#185602=CARTESIAN_POINT('Ctrl Pts',(169.083852246225,-5.51923256297325,
132.938114797283));
#185603=CARTESIAN_POINT('Ctrl Pts',(169.087788295666,-5.54810406687026,
132.860199090228));
#185604=CARTESIAN_POINT('Ctrl Pts',(169.096337488275,-5.61081365713913,
132.690964329118));
#185605=CARTESIAN_POINT('Ctrl Pts',(169.104886680883,-5.66582349201742,
132.518730504111));
#185606=CARTESIAN_POINT('Ctrl Pts',(169.113435873491,-5.71287611630099,
132.344158345288));
#185607=CARTESIAN_POINT('Ctrl Pts',(169.1219544283,-5.75976011777493,132.170211801898));
#185608=CARTESIAN_POINT('Ctrl Pts',(169.130472983109,-5.79874374486091,
131.993943781956));
#185609=CARTESIAN_POINT('Ctrl Pts',(169.138991537918,-5.82961881215657,
131.816030063309));
#185610=CARTESIAN_POINT('Ctrl Pts',(169.147449767728,-5.86027523457195,
131.639376258474));
#185611=CARTESIAN_POINT('Ctrl Pts',(169.155907997538,-5.88293745840983,
131.461100123086));
#185612=CARTESIAN_POINT('Ctrl Pts',(169.164366227348,-5.89744884930004,
131.281883006978));
#185613=CARTESIAN_POINT('Ctrl Pts',(169.171785731182,-5.91017814641917,
131.124674925614));
#185614=CARTESIAN_POINT('Ctrl Pts',(169.179205235017,-5.91663626882271,
130.966743136856));
#185615=CARTESIAN_POINT('Ctrl Pts',(169.186624738851,-5.91674851051812,
130.808558924556));
#185616=CARTESIAN_POINT('',(170.936624807795,-5.90997459655701,130.800282389652));
#185617=CARTESIAN_POINT('Ctrl Pts',(169.186624807795,-5.91019576558979,
130.808552806709));
#185618=CARTESIAN_POINT('Ctrl Pts',(169.246495178356,-5.90189558337006,
129.533520458627));
#185619=CARTESIAN_POINT('Ctrl Pts',(169.399181423523,-4.87013215197593,
126.269586643864));
#185620=CARTESIAN_POINT('Ctrl Pts',(169.64468354329,0.516110086827318,123.825020325773));
#185621=CARTESIAN_POINT('Ctrl Pts',(169.923131167105,6.15088676129293,127.466074743035));
#185622=CARTESIAN_POINT('Ctrl Pts',(170.201578790917,6.13329898965285,134.174850794656));
#185623=CARTESIAN_POINT('Ctrl Pts',(170.48002641473,0.479509074835291,137.786311031131));
#185624=CARTESIAN_POINT('Ctrl Pts',(170.72504175369,-4.88318756993693,135.318440300322));
#185625=CARTESIAN_POINT('Ctrl Pts',(170.877241218044,-5.9019844995111,132.065066804779));
#185626=CARTESIAN_POINT('Ctrl Pts',(170.936624807795,-5.90997459655701,
130.800282389652));
#185627=CARTESIAN_POINT('',(172.686624807795,-5.92509021110593,130.801708436727));
#185628=CARTESIAN_POINT('Ctrl Pts',(170.936624807795,-5.90997459655701,
130.800282389652));
#185629=CARTESIAN_POINT('Ctrl Pts',(170.970057092649,-5.91447293021401,
130.088223165501));
#185630=CARTESIAN_POINT('Ctrl Pts',(171.096305252108,-5.46525073119121,
127.404805355658));
#185631=CARTESIAN_POINT('Ctrl Pts',(171.315369286168,-1.46542337909948,
123.961108842987));
#185632=CARTESIAN_POINT('Ctrl Pts',(171.593816909983,4.96532439755938,125.872513685901));
#185633=CARTESIAN_POINT('Ctrl Pts',(171.872264533795,6.83318162244277,132.316044924908));
#185634=CARTESIAN_POINT('Ctrl Pts',(172.150712157608,2.4216787557808,137.370412135345));
#185635=CARTESIAN_POINT('Ctrl Pts',(172.422165582275,-4.04851912677806,
136.415502720852));
#185636=CARTESIAN_POINT('Ctrl Pts',(172.600803132337,-5.91495363718931,
132.617640293932));
#185637=CARTESIAN_POINT('Ctrl Pts',(172.686624807795,-5.92509021110593,
130.801708436727));
#185638=CARTESIAN_POINT('',(174.436624807795,-5.9179196420516,130.809725587076));
#185639=CARTESIAN_POINT('Ctrl Pts',(172.686624807795,-5.92509021110593,
130.801708436727));
#185640=CARTESIAN_POINT('Ctrl Pts',(172.693619006941,-5.92591631029654,
130.653715648455));
#185641=CARTESIAN_POINT('Ctrl Pts',(172.793429080688,-5.85367826635182,
128.542618109344));
#185642=CARTESIAN_POINT('Ctrl Pts',(172.986055029049,-3.32892140626788,
124.648400676076));
#185643=CARTESIAN_POINT('Ctrl Pts',(173.264502652858,3.37982011111009,124.676198042461));
#185644=CARTESIAN_POINT('Ctrl Pts',(173.542950276673,6.9826720597651,130.335477437983));
#185645=CARTESIAN_POINT('Ctrl Pts',(173.821397900485,4.16878950799601,136.425637569324));
#185646=CARTESIAN_POINT('Ctrl Pts',(174.099845524299,-2.47600694493612,
137.350118796645));
#185647=CARTESIAN_POINT('Ctrl Pts',(174.304921160068,-5.69410310579832,
133.600799859742));
#185648=CARTESIAN_POINT('Ctrl Pts',(174.417180921234,-5.92198205708473,
131.22240348325));
#185649=CARTESIAN_POINT('Ctrl Pts',(174.436624807795,-5.91814536937201,
130.809725791712));
#185650=CARTESIAN_POINT('',(176.18662480776,-5.91674999707342,130.804546713429));
#185651=CARTESIAN_POINT('Ctrl Pts',(174.436624807795,-5.91674756863957,
130.809724524517));
#185652=CARTESIAN_POINT('Ctrl Pts',(174.443929001547,-5.9168880736424,130.654738123466));
#185653=CARTESIAN_POINT('Ctrl Pts',(174.451233195298,-5.91093472951897,
130.49956034794));
#185654=CARTESIAN_POINT('Ctrl Pts',(174.45853738905,-5.8988692447101,130.344717064023));
#185655=CARTESIAN_POINT('Ctrl Pts',(174.46583594041,-5.88681308032585,130.18999339446));
#185656=CARTESIAN_POINT('Ctrl Pts',(174.47313449177,-5.86865420127859,130.035604084019));
#185657=CARTESIAN_POINT('Ctrl Pts',(174.48043304313,-5.84442638127245,129.882074958789));
#185658=CARTESIAN_POINT('Ctrl Pts',(174.487779198497,-5.82004053794948,
129.727544456563));
#185659=CARTESIAN_POINT('Ctrl Pts',(174.495125353863,-5.78950629686442,
129.57388579532));
#185660=CARTESIAN_POINT('Ctrl Pts',(174.502471509229,-5.75291125004384,
129.421630451692));
#185661=CARTESIAN_POINT('Ctrl Pts',(174.509764874657,-5.71657917755128,
129.270469224622));
#185662=CARTESIAN_POINT('Ctrl Pts',(174.517058240085,-5.67427322768761,
129.120691588368));
#185663=CARTESIAN_POINT('Ctrl Pts',(174.524351605513,-5.62613037306831,
128.972807291086));
#185664=CARTESIAN_POINT('Ctrl Pts',(174.531644770911,-5.57798883883177,
128.824927049732));
#185665=CARTESIAN_POINT('Ctrl Pts',(174.538937936308,-5.52401083722427,
128.678940410037));
#185666=CARTESIAN_POINT('Ctrl Pts',(174.546231101706,-5.46438297325061,
128.535341163231));
#185667=CARTESIAN_POINT('Ctrl Pts',(174.553525601954,-5.40474419573206,
128.391715633801));
#185668=CARTESIAN_POINT('Ctrl Pts',(174.560820102202,-5.33945364616344,
128.25047872192));
#185669=CARTESIAN_POINT('Ctrl Pts',(174.56811460245,-5.26874562569991,128.112103182964));
#185670=CARTESIAN_POINT('Ctrl Pts',(174.575500116573,-5.1971553774347,127.972001124914));
#185671=CARTESIAN_POINT('Ctrl Pts',(174.582885630696,-5.12001174020782,
127.83483268724));
#185672=CARTESIAN_POINT('Ctrl Pts',(174.590271144818,-5.0376047641483,127.701060953864));
#185673=CARTESIAN_POINT('Ctrl Pts',(174.59757652405,-4.95609192679949,127.568740681165));
#185674=CARTESIAN_POINT('Ctrl Pts',(174.604881903281,-4.86942966911613,
127.439744052297));
#185675=CARTESIAN_POINT('Ctrl Pts',(174.612187282513,-4.77794074362902,
127.314487724054));
#185676=CARTESIAN_POINT('Ctrl Pts',(174.619612864081,-4.68494646403069,
127.187170434578));
#185677=CARTESIAN_POINT('Ctrl Pts',(174.62703844565,-4.58696555586886,127.063717931935));
#185678=CARTESIAN_POINT('Ctrl Pts',(174.634464027218,-4.48437712179394,
126.944530000553));
#185679=CARTESIAN_POINT('Ctrl Pts',(174.641889608787,-4.38178868771901,
126.825342069171));
#185680=CARTESIAN_POINT('Ctrl Pts',(174.649315190355,-4.27459305631298,
126.710418962902));
#185681=CARTESIAN_POINT('Ctrl Pts',(174.656740771924,-4.16320513849686,
126.60011829138));
#185682=CARTESIAN_POINT('Ctrl Pts',(174.664164038329,-4.05185194943482,
126.489852009629));
#185683=CARTESIAN_POINT('Ctrl Pts',(174.671587304735,-3.93594660125779,
126.383845984206));
#185684=CARTESIAN_POINT('Ctrl Pts',(174.67901057114,-3.81584854330713,126.282499224617));
#185685=CARTESIAN_POINT('Ctrl Pts',(174.686425063861,-3.69589243128723,
126.181272248482));
#185686=CARTESIAN_POINT('Ctrl Pts',(174.693839556582,-3.57175375582001,
126.084693815132));
#185687=CARTESIAN_POINT('Ctrl Pts',(174.701254049303,-3.44382960705885,
125.993127075111));
#185688=CARTESIAN_POINT('Ctrl Pts',(174.708661395657,-3.3160287564088,125.901648590562));
#185689=CARTESIAN_POINT('Ctrl Pts',(174.716068742011,-3.18444999758383,
125.815172398668));
#185690=CARTESIAN_POINT('Ctrl Pts',(174.723476088364,-3.04952429295717,
125.734022152615));
#185691=CARTESIAN_POINT('Ctrl Pts',(174.73087791004,-2.91469922101105,125.652932431477));
#185692=CARTESIAN_POINT('Ctrl Pts',(174.738279731715,-2.77653249221001,
125.577160938383));
#185693=CARTESIAN_POINT('Ctrl Pts',(174.745681553391,-2.63548481858331,
125.506988596128));
#185694=CARTESIAN_POINT('Ctrl Pts',(174.753079467702,-2.49451160292591,
125.436853297306));
#185695=CARTESIAN_POINT('Ctrl Pts',(174.760477382013,-2.35066080461964,
125.372311428666));
#185696=CARTESIAN_POINT('Ctrl Pts',(174.767875296325,-2.20441845267172,
125.313598389239));
#185697=CARTESIAN_POINT('Ctrl Pts',(174.775271981237,-2.05820040354942,
125.254895106854));
#185698=CARTESIAN_POINT('Ctrl Pts',(174.782668666149,-1.90959193565443,
125.202018870151));
#185699=CARTESIAN_POINT('Ctrl Pts',(174.790065351061,-1.75909991924992,
125.155157307665));
#185700=CARTESIAN_POINT('Ctrl Pts',(174.797461707997,-1.6086145758194,125.10829782307));
#185701=CARTESIAN_POINT('Ctrl Pts',(174.804858064932,-1.45624620636001,
125.067452593391));
#185702=CARTESIAN_POINT('Ctrl Pts',(174.812254421867,-1.30251747706525,
125.03275955855));
#185703=CARTESIAN_POINT('Ctrl Pts',(174.819651911204,-1.14876521150936,
124.998061212116));
#185704=CARTESIAN_POINT('Ctrl Pts',(174.827049400541,-0.993652535579348,
124.969517018183));
#185705=CARTESIAN_POINT('Ctrl Pts',(174.834446889877,-0.837712808111135,
124.947213887833));
#185706=CARTESIAN_POINT('Ctrl Pts',(174.841846972392,-0.681718416213029,
124.924902939155));
#185707=CARTESIAN_POINT('Ctrl Pts',(174.849247054907,-0.524896764851784,
124.908837462763));
#185708=CARTESIAN_POINT('Ctrl Pts',(174.856647137422,-0.367786690952134,
124.89905253818));
#185709=CARTESIAN_POINT('Ctrl Pts',(174.864055357088,-0.210503858375036,
124.889256854067));
#185710=CARTESIAN_POINT('Ctrl Pts',(174.871463576755,-0.0529323426943236,
124.885755536941));
#185711=CARTESIAN_POINT('Ctrl Pts',(174.878871796421,0.104387918666272,
124.888531535777));
#185712=CARTESIAN_POINT('Ctrl Pts',(174.886284575723,0.261805008023041,
124.891309243195));
#185713=CARTESIAN_POINT('Ctrl Pts',(174.893697355026,0.418970163099699,
124.900371943808));
#185714=CARTESIAN_POINT('Ctrl Pts',(174.901110134328,0.575348724016495,
124.915650707214));
#185715=CARTESIAN_POINT('Ctrl Pts',(174.908533505356,0.73195072595411,124.930951301634));
#185716=CARTESIAN_POINT('Ctrl Pts',(174.915956876385,0.887763520202904,
124.952485646826));
#185717=CARTESIAN_POINT('Ctrl Pts',(174.923380247414,1.04226196719356,124.98013358265));
#185718=CARTESIAN_POINT('Ctrl Pts',(174.927316296855,1.12418075092763,124.994793181628));
#185719=CARTESIAN_POINT('Ctrl Pts',(174.931252346295,1.20573025481183,125.01117069005));
#185720=CARTESIAN_POINT('Ctrl Pts',(174.935188395736,1.28683407005348,125.02924255482));
#185721=CARTESIAN_POINT('Ctrl Pts',(174.942611662142,1.43979333443543,125.063325527774));
#185722=CARTESIAN_POINT('Ctrl Pts',(174.950034928547,1.59162887770532,125.103541133724));
#185723=CARTESIAN_POINT('Ctrl Pts',(174.957458194952,1.74181071071733,125.149802632141));
#185724=CARTESIAN_POINT('Ctrl Pts',(174.964872687674,1.89181504127466,125.19600945331));
#185725=CARTESIAN_POINT('Ctrl Pts',(174.972287180395,2.04016919884106,125.248247834485));
#185726=CARTESIAN_POINT('Ctrl Pts',(174.979701673116,2.18635301765181,125.306379984215));
#185727=CARTESIAN_POINT('Ctrl Pts',(174.987109019469,2.33239593899437,125.36445610399));
#185728=CARTESIAN_POINT('Ctrl Pts',(174.994516365823,2.47627234150279,125.428414546277));
#185729=CARTESIAN_POINT('Ctrl Pts',(175.001923712177,2.61747698089627,125.498067672677));
#185730=CARTESIAN_POINT('Ctrl Pts',(175.009325533852,2.75857630454238,125.567668849148));
#185731=CARTESIAN_POINT('Ctrl Pts',(175.016727355528,2.89700749946936,125.642956088335));
#185732=CARTESIAN_POINT('Ctrl Pts',(175.024129177203,3.03228519126849,125.723693625791));
#185733=CARTESIAN_POINT('Ctrl Pts',(175.031527091514,3.16749147102659,125.804388542529));
#185734=CARTESIAN_POINT('Ctrl Pts',(175.038925005826,3.29954724326952,125.890527836688));
#185735=CARTESIAN_POINT('Ctrl Pts',(175.046322920137,3.42799174957475,125.981829837224));
#185736=CARTESIAN_POINT('Ctrl Pts',(175.053719605049,3.55641491073356,126.073116665024));
#185737=CARTESIAN_POINT('Ctrl Pts',(175.061116289962,3.6812276930651,126.169564280363));
#185738=CARTESIAN_POINT('Ctrl Pts',(175.068512974874,3.80199826361165,126.270847656738));
#185739=CARTESIAN_POINT('Ctrl Pts',(175.075909331809,3.92276347906459,126.372126542102));
#185740=CARTESIAN_POINT('Ctrl Pts',(175.083305688745,4.03948655308724,126.478240522284));
#185741=CARTESIAN_POINT('Ctrl Pts',(175.09070204568,4.15176891907437,126.588824423307));
#185742=CARTESIAN_POINT('Ctrl Pts',(175.098099535017,4.26406847577848,126.699425255008));
#185743=CARTESIAN_POINT('Ctrl Pts',(175.105497024353,4.37192570472563,126.814497108236));
#185744=CARTESIAN_POINT('Ctrl Pts',(175.11289451369,4.47497919168296,126.933638230659));
#185745=CARTESIAN_POINT('Ctrl Pts',(175.120294596205,4.57806880388083,127.052821117818));
#185746=CARTESIAN_POINT('Ctrl Pts',(175.12769467872,4.6763510773099,127.176075832118));
#185747=CARTESIAN_POINT('Ctrl Pts',(175.135094761235,4.76950524405483,127.302967996132));
#185748=CARTESIAN_POINT('Ctrl Pts',(175.142502980902,4.86276184338219,127.429999691124));
#185749=CARTESIAN_POINT('Ctrl Pts',(175.149911200568,4.95087885376649,127.560676522493));
#185750=CARTESIAN_POINT('Ctrl Pts',(175.157319420235,5.03357877135145,127.694535009095));
#185751=CARTESIAN_POINT('Ctrl Pts',(175.164732199537,5.11632958935577,127.828475883363));
#185752=CARTESIAN_POINT('Ctrl Pts',(175.172144978839,5.19365648795154,127.965601990528));
#185753=CARTESIAN_POINT('Ctrl Pts',(175.179557758141,5.26532846351507,128.105426247523));
#185754=CARTESIAN_POINT('Ctrl Pts',(175.18698112917,5.33710284735834,128.245450291974));
#185755=CARTESIAN_POINT('Ctrl Pts',(175.194404500198,5.40320601409473,128.388179848205));
#185756=CARTESIAN_POINT('Ctrl Pts',(175.201827871227,5.46345520708816,128.533108151934));
#185757=CARTESIAN_POINT('Ctrl Pts',(175.205763920668,5.49540077487273,128.609952616077));
#185758=CARTESIAN_POINT('Ctrl Pts',(175.209699970109,5.52570141200866,128.687414966641));
#185759=CARTESIAN_POINT('Ctrl Pts',(175.213636019549,5.55433563356411,128.765418187722));
#185760=CARTESIAN_POINT('Ctrl Pts',(175.221059285955,5.60833888177444,128.912529828282));
#185761=CARTESIAN_POINT('Ctrl Pts',(175.22848255236,5.6565751734508,129.062010888378));
#185762=CARTESIAN_POINT('Ctrl Pts',(175.235905818766,5.6988310137765,129.213368587756));
#185763=CARTESIAN_POINT('Ctrl Pts',(175.243320311487,5.74103691120799,129.364547394903));
#185764=CARTESIAN_POINT('Ctrl Pts',(175.250734804208,5.77727632757357,129.51759807029));
#185765=CARTESIAN_POINT('Ctrl Pts',(175.258149296929,5.80738402842343,129.672008504082));
#185766=CARTESIAN_POINT('Ctrl Pts',(175.265556643283,5.8374627103377,129.826270111284));
#185767=CARTESIAN_POINT('Ctrl Pts',(175.272963989636,5.86142137137703,129.981888503833));
#185768=CARTESIAN_POINT('Ctrl Pts',(175.28037133599,5.87914478016453,130.138337182269));
#185769=CARTESIAN_POINT('Ctrl Pts',(175.287773157665,5.89685497016506,130.294669175379));
#185770=CARTESIAN_POINT('Ctrl Pts',(175.295174979341,5.90833912582,130.451829852019));
#185771=CARTESIAN_POINT('Ctrl Pts',(175.302576801016,5.91353324571094,130.609283416511));
#185772=CARTESIAN_POINT('Ctrl Pts',(175.309974715328,5.91872462366646,130.766653862494));
#185773=CARTESIAN_POINT('Ctrl Pts',(175.317372629639,5.9176325664383,130.924316516258));
#185774=CARTESIAN_POINT('Ctrl Pts',(175.32477054395,5.91024500066961,131.081731478616));
#185775=CARTESIAN_POINT('Ctrl Pts',(175.332167228863,5.90285866258037,131.239120281463));
#185776=CARTESIAN_POINT('Ctrl Pts',(175.339563913775,5.88917890982933,131.396261102075));
#185777=CARTESIAN_POINT('Ctrl Pts',(175.346960598687,5.86924578015624,131.55261494239));
#185778=CARTESIAN_POINT('Ctrl Pts',(175.354356955622,5.84931353433896,131.708961849813));
#185779=CARTESIAN_POINT('Ctrl Pts',(175.361753312558,5.82312851013706,131.864521476024));
#185780=CARTESIAN_POINT('Ctrl Pts',(175.369149669493,5.79078250377275,132.018761110196));
#185781=CARTESIAN_POINT('Ctrl Pts',(175.37654715883,5.75843154515223,132.17302435885));
#185782=CARTESIAN_POINT('Ctrl Pts',(175.383944648166,5.71991780283251,132.325966847695));
#185783=CARTESIAN_POINT('Ctrl Pts',(175.391342137503,5.67538392920773,132.477067351752));
#185784=CARTESIAN_POINT('Ctrl Pts',(175.398742220018,5.63083444430259,132.628220823857));
#185785=CARTESIAN_POINT('Ctrl Pts',(175.406142302533,5.58026073187371,132.777530667734));
#185786=CARTESIAN_POINT('Ctrl Pts',(175.413542385048,5.52385486305895,132.924492220642));
#185787=CARTESIAN_POINT('Ctrl Pts',(175.420950604715,5.46738697019292,133.071615372885));
#185788=CARTESIAN_POINT('Ctrl Pts',(175.428358824381,5.40507424749297,133.216384728638));
#185789=CARTESIAN_POINT('Ctrl Pts',(175.435767044047,5.33715663715738,133.358316293169));
#185790=CARTESIAN_POINT('Ctrl Pts',(175.44317982335,5.26919722466591,133.500335214211));
#185791=CARTESIAN_POINT('Ctrl Pts',(175.450592602652,5.19562622460076,133.639512534424));
#185792=CARTESIAN_POINT('Ctrl Pts',(175.458005381954,5.11672857063927,133.775390623625));
#185793=CARTESIAN_POINT('Ctrl Pts',(175.465428752982,5.03771818400969,133.911462861812));
#185794=CARTESIAN_POINT('Ctrl Pts',(175.472852124011,4.95336614232203,134.044226139633));
#185795=CARTESIAN_POINT('Ctrl Pts',(175.48027549504,4.86400001629385,134.17325278028));
#185796=CARTESIAN_POINT('Ctrl Pts',(175.484211544481,4.81661595196297,134.241665801102));
#185797=CARTESIAN_POINT('Ctrl Pts',(175.488147593921,4.76782291709144,134.309028877887));
#185798=CARTESIAN_POINT('Ctrl Pts',(175.492083643362,4.71767409421103,134.375282305773));
#185799=CARTESIAN_POINT('Ctrl Pts',(175.499506909768,4.62309497934961,134.500234203069));
#185800=CARTESIAN_POINT('Ctrl Pts',(175.506930176173,4.52340522385552,134.621614925639));
#185801=CARTESIAN_POINT('Ctrl Pts',(175.514353442579,4.41890401854798,134.738978494484));
#185802=CARTESIAN_POINT('Ctrl Pts',(175.5217679353,4.31452632498669,134.856203349337));
#185803=CARTESIAN_POINT('Ctrl Pts',(175.529182428021,4.20534874690522,134.969420225197));
#185804=CARTESIAN_POINT('Ctrl Pts',(175.536596920742,4.09171282355591,135.078213297765));
#185805=CARTESIAN_POINT('Ctrl Pts',(175.544004267095,3.97818642678798,135.186901511475));
#185806=CARTESIAN_POINT('Ctrl Pts',(175.551411613449,3.8602105073087,135.291174153915));
#185807=CARTESIAN_POINT('Ctrl Pts',(175.558818959803,3.73816573865111,135.390649691848));
#185808=CARTESIAN_POINT('Ctrl Pts',(175.566220781478,3.6162119955864,135.490051037171));
#185809=CARTESIAN_POINT('Ctrl Pts',(175.573622603154,3.49019573395453,135.584662167159));
#185810=CARTESIAN_POINT('Ctrl Pts',(175.581024424829,3.36053313950423,135.674139624954));
#185811=CARTESIAN_POINT('Ctrl Pts',(175.588422339141,3.2309389929287,135.763569848295));
#185812=CARTESIAN_POINT('Ctrl Pts',(175.595820253452,3.097702653472,135.847871585104));
#185813=CARTESIAN_POINT('Ctrl Pts',(175.603218167763,2.96127182766808,135.926742849024));
#185814=CARTESIAN_POINT('Ctrl Pts',(175.610614852676,2.82486367419191,136.005601005972));
#185815=CARTESIAN_POINT('Ctrl Pts',(175.618011537588,2.68526241084319,136.07903029447));
#185816=CARTESIAN_POINT('Ctrl Pts',(175.6254082225,2.54294315333224,136.146773057786));
#185817=CARTESIAN_POINT('Ctrl Pts',(175.632804579435,2.4006302064062,136.214512817317));
#185818=CARTESIAN_POINT('Ctrl Pts',(175.640200936371,2.25559984201149,136.27656639258));
#185819=CARTESIAN_POINT('Ctrl Pts',(175.647597293306,2.108349862954,136.332723071121));
#185820=CARTESIAN_POINT('Ctrl Pts',(175.654994782643,1.96107733954886,136.388888347394));
#185821=CARTESIAN_POINT('Ctrl Pts',(175.66239227198,1.81158487365314,136.439154796263));
#185822=CARTESIAN_POINT('Ctrl Pts',(175.669789761316,1.66038809370673,136.483360700395));
#185823=CARTESIAN_POINT('Ctrl Pts',(175.677189843831,1.50913831196425,136.527582100839));
#185824=CARTESIAN_POINT('Ctrl Pts',(175.684589926346,1.35618338473752,136.565738621961));
#185825=CARTESIAN_POINT('Ctrl Pts',(175.691990008861,1.20205171822511,136.597719076112));
#185826=CARTESIAN_POINT('Ctrl Pts',(175.699398228528,1.04775056809937,136.629734696061));
#185827=CARTESIAN_POINT('Ctrl Pts',(175.706806448194,0.89227046033038,136.655560610638));
#185828=CARTESIAN_POINT('Ctrl Pts',(175.71421466786,0.736148288012586,136.675137079037));
#185829=CARTESIAN_POINT('Ctrl Pts',(175.721627447163,0.579930025102714,
136.694725596425));
#185830=CARTESIAN_POINT('Ctrl Pts',(175.729040226465,0.423069281292891,
136.708056971602));
#185831=CARTESIAN_POINT('Ctrl Pts',(175.736453005767,0.266105087431851,
136.715123567046));
#185832=CARTESIAN_POINT('Ctrl Pts',(175.743876376796,0.108916615769398,
136.722200259573));
#185833=CARTESIAN_POINT('Ctrl Pts',(175.751299747824,-0.0483752288583152,
136.722994292513));
#185834=CARTESIAN_POINT('Ctrl Pts',(175.758723118853,-0.205233569866812,
136.717550090625));
#185835=CARTESIAN_POINT('Ctrl Pts',(175.762659168294,-0.288403626033039,
136.714663444153));
#185836=CARTESIAN_POINT('Ctrl Pts',(175.766595217735,-0.371451917537092,
136.710023870462));
#185837=CARTESIAN_POINT('Ctrl Pts',(175.770531267175,-0.454299466532195,
136.703643841586));
#185838=CARTESIAN_POINT('Ctrl Pts',(175.777954533581,-0.610547358354118,
136.691611306242));
#185839=CARTESIAN_POINT('Ctrl Pts',(175.785377799986,-0.766553145834642,
136.673348737022));
#185840=CARTESIAN_POINT('Ctrl Pts',(175.792801066392,-0.921779894265251,
136.648866789094));
#185841=CARTESIAN_POINT('Ctrl Pts',(175.800215559113,-1.07682317756969,
136.624413776796));
#185842=CARTESIAN_POINT('Ctrl Pts',(175.807630051834,-1.2310888894619,136.593756075164));
#185843=CARTESIAN_POINT('Ctrl Pts',(175.815044544555,-1.38404257487515,
136.556956267656));
#185844=CARTESIAN_POINT('Ctrl Pts',(175.822451890908,-1.53684883776815,
136.520191929188));
#185845=CARTESIAN_POINT('Ctrl Pts',(175.829859237262,-1.68834523120841,
136.477297357118));
#185846=CARTESIAN_POINT('Ctrl Pts',(175.837266583616,-1.83800499713292,
136.428386594837));
#185847=CARTESIAN_POINT('Ctrl Pts',(175.844668405291,-1.98755314115846,
136.379512312047));
#185848=CARTESIAN_POINT('Ctrl Pts',(175.852070226967,-2.13526703187452,
136.324630888933));
#185849=CARTESIAN_POINT('Ctrl Pts',(175.859472048642,-2.2806327507365,136.263906827533));
#185850=CARTESIAN_POINT('Ctrl Pts',(175.866869962954,-2.42592173216508,
136.203214821893));
#185851=CARTESIAN_POINT('Ctrl Pts',(175.874267877265,-2.56886466684566,
136.136686463989));
#185852=CARTESIAN_POINT('Ctrl Pts',(175.881665791576,-2.70896548878649,
136.064535191006));
#185853=CARTESIAN_POINT('Ctrl Pts',(175.889062476488,-2.84904302851353,
135.992395908255));
#185854=CARTESIAN_POINT('Ctrl Pts',(175.896459161401,-2.98627906134308,
135.91463573573));
#185855=CARTESIAN_POINT('Ctrl Pts',(175.903855846313,-3.12020000172131,
135.831515131977));
#185856=CARTESIAN_POINT('Ctrl Pts',(175.911252203248,-3.25411500390483,
135.748398213878));
#185857=CARTESIAN_POINT('Ctrl Pts',(175.918648560184,-3.38471488874059,
135.659921534012));
#185858=CARTESIAN_POINT('Ctrl Pts',(175.926044917119,-3.51155330329859,
135.56639001275));
#185859=CARTESIAN_POINT('Ctrl Pts',(175.933442406456,-3.63841113714163,
135.472844171573));
#185860=CARTESIAN_POINT('Ctrl Pts',(175.940839895792,-3.76150605356803,
135.374242169608));
#185861=CARTESIAN_POINT('Ctrl Pts',(175.948237385129,-3.88042328543855,
135.270930407497));
#185862=CARTESIAN_POINT('Ctrl Pts',(175.955637467644,-3.99938220356058,
135.167582429608));
#185863=CARTESIAN_POINT('Ctrl Pts',(175.963037550159,-4.11416023972835,
135.059521649114));
#185864=CARTESIAN_POINT('Ctrl Pts',(175.970437632674,-4.224378232165,134.947132529476));
#185865=CARTESIAN_POINT('Ctrl Pts',(175.97784585234,-4.33471742061488,134.834619826447));
#185866=CARTESIAN_POINT('Ctrl Pts',(175.985254072007,-4.44048629003844,
134.717769546018));
#185867=CARTESIAN_POINT('Ctrl Pts',(175.992662291673,-4.5413443749702,134.597001100188));
#185868=CARTESIAN_POINT('Ctrl Pts',(176.000075070975,-4.64226453636987,
134.476158323397));
#185869=CARTESIAN_POINT('Ctrl Pts',(176.007487850277,-4.73826766343565,
134.351392871023));
#185870=CARTESIAN_POINT('Ctrl Pts',(176.014900629579,-4.82905597116431,
134.223154116721));
#185871=CARTESIAN_POINT('Ctrl Pts',(176.022324000608,-4.9199740014849,134.094732128872));
#185872=CARTESIAN_POINT('Ctrl Pts',(176.029747371637,-5.00566212797293,
133.96282723945));
#185873=CARTESIAN_POINT('Ctrl Pts',(176.037170742666,-5.08586753153024,
133.827915150599));
#185874=CARTESIAN_POINT('Ctrl Pts',(176.041106792106,-5.12839436099982,
133.756381523917));
#185875=CARTESIAN_POINT('Ctrl Pts',(176.045042841547,-5.16938058638033,
133.684002841315));
#185876=CARTESIAN_POINT('Ctrl Pts',(176.048978890988,-5.20879401129288,
133.610852290531));
#185877=CARTESIAN_POINT('Ctrl Pts',(176.056804946312,-5.28715980636309,
133.465406897628));
#185878=CARTESIAN_POINT('Ctrl Pts',(176.064631001636,-5.35952100433335,
133.316508050305));
#185879=CARTESIAN_POINT('Ctrl Pts',(176.07245705696,-5.42557744025171,133.164665683089));
#185880=CARTESIAN_POINT('Ctrl Pts',(176.080269925152,-5.49152256914748,
133.013079174693));
#185881=CARTESIAN_POINT('Ctrl Pts',(176.088082793345,-5.55118398804998,
132.858559319343));
#185882=CARTESIAN_POINT('Ctrl Pts',(176.095895661537,-5.60430706077633,
132.701641021469));
#185883=CARTESIAN_POINT('Ctrl Pts',(176.103690540573,-5.65730781744522,
132.545084028514));
#185884=CARTESIAN_POINT('Ctrl Pts',(176.11148541961,-5.70380015565364,132.386139904117));
#185885=CARTESIAN_POINT('Ctrl Pts',(176.119280298646,-5.74357746203557,
132.225363256584));
#185886=CARTESIAN_POINT('Ctrl Pts',(176.127064591086,-5.78330074496215,
132.064804967479));
#185887=CARTESIAN_POINT('Ctrl Pts',(176.134848883526,-5.81632709643767,
131.902419418109));
#185888=CARTESIAN_POINT('Ctrl Pts',(176.142633175966,-5.84249900201333,
131.738778069229));
#185889=CARTESIAN_POINT('Ctrl Pts',(176.150402849986,-5.86862175837175,
131.575444028665));
#185890=CARTESIAN_POINT('Ctrl Pts',(176.158172524007,-5.88791569417547,
131.410859201104));
#185891=CARTESIAN_POINT('Ctrl Pts',(176.165942198028,-5.9002739477779,131.245606471567));
#185892=CARTESIAN_POINT('Ctrl Pts',(176.172836401272,-5.91123969895993,
131.098974077335));
#185893=CARTESIAN_POINT('Ctrl Pts',(176.179730604516,-5.91674536509889,
130.951816162445));
#185894=CARTESIAN_POINT('Ctrl Pts',(176.18662480776,-5.91674999707342,130.804546713429));
#185895=CARTESIAN_POINT('',(177.936624807795,-5.91674751037323,130.798932819469));
#185896=CARTESIAN_POINT('Ctrl Pts',(176.186624807795,-5.91674999707345,
130.804546712692));
#185897=CARTESIAN_POINT('Ctrl Pts',(176.194355043842,-5.91675519072865,
130.639418479146));
#185898=CARTESIAN_POINT('Ctrl Pts',(176.202085279889,-5.90984332064331,
130.474416800835));
#185899=CARTESIAN_POINT('Ctrl Pts',(176.209815515936,-5.89607197714202,
130.310128078309));
#185900=CARTESIAN_POINT('Ctrl Pts',(176.217554849163,-5.88228442709847,
130.145646015741));
#185901=CARTESIAN_POINT('Ctrl Pts',(176.225294182391,-5.86162132030127,
129.981878903413));
#185902=CARTESIAN_POINT('Ctrl Pts',(176.233033515618,-5.8341917385858,129.819405126228));
#185903=CARTESIAN_POINT('Ctrl Pts',(176.240899598884,-5.80631293205789,
129.654270453487));
#185904=CARTESIAN_POINT('Ctrl Pts',(176.248765682149,-5.77144417701273,
129.490472187952));
#185905=CARTESIAN_POINT('Ctrl Pts',(176.256631765414,-5.72975279112999,
129.328601993997));
#185906=CARTESIAN_POINT('Ctrl Pts',(176.264397304788,-5.68859430250429,
129.168800816951));
#185907=CARTESIAN_POINT('Ctrl Pts',(176.272162844161,-5.64078673126599,
129.010878994164));
#185908=CARTESIAN_POINT('Ctrl Pts',(176.279928383534,-5.5865400071046,128.855386191998));
#185909=CARTESIAN_POINT('Ctrl Pts',(176.287844738745,-5.53123974824816,
128.696873538136));
#185910=CARTESIAN_POINT('Ctrl Pts',(176.295761093957,-5.46924781901711,
128.540885545812));
#185911=CARTESIAN_POINT('Ctrl Pts',(176.303677449168,-5.40083612746166,
128.387979089991));
#185912=CARTESIAN_POINT('Ctrl Pts',(176.311593804379,-5.3324244359062,128.23507263417));
#185913=CARTESIAN_POINT('Ctrl Pts',(176.31951015959,-5.25759319491068,128.085247996554));
#185914=CARTESIAN_POINT('Ctrl Pts',(176.327426514802,-5.17666132341062,
127.939031996761));
#185915=CARTESIAN_POINT('Ctrl Pts',(176.334849781207,-5.10077048390061,
127.801923404455));
#185916=CARTESIAN_POINT('Ctrl Pts',(176.342273047613,-5.01931395727661,
127.667624627721));
#185917=CARTESIAN_POINT('Ctrl Pts',(176.349696314018,-4.93252462046695,
127.536619588814));
#185918=CARTESIAN_POINT('Ctrl Pts',(176.357110806739,-4.84583786144609,
127.405769386985));
#185919=CARTESIAN_POINT('Ctrl Pts',(176.36452529946,-4.75383104242812,127.278205482258));
#185920=CARTESIAN_POINT('Ctrl Pts',(176.371939792181,-4.65678323929925,
127.154387956753));
#185921=CARTESIAN_POINT('Ctrl Pts',(176.379347138535,-4.55982897449686,
127.030689771241));
#185922=CARTESIAN_POINT('Ctrl Pts',(176.386754484889,-4.45784362701647,
126.91073106819));
#185923=CARTESIAN_POINT('Ctrl Pts',(176.394161831242,-4.35114987704113,
126.794943538984));
#185924=CARTESIAN_POINT('Ctrl Pts',(176.401563652918,-4.24453570328974,
126.679242368485));
#185925=CARTESIAN_POINT('Ctrl Pts',(176.408965474593,-4.13322037119265,
126.567706450713));
#185926=CARTESIAN_POINT('Ctrl Pts',(176.416367296269,-4.01756711697121,
126.460734825312));
#185927=CARTESIAN_POINT('Ctrl Pts',(176.42376521058,-3.90197491520212,126.353819669399));
#185928=CARTESIAN_POINT('Ctrl Pts',(176.431163124891,-3.78204962521748,
126.251464260148));
#185929=CARTESIAN_POINT('Ctrl Pts',(176.438561039203,-3.65819156987707,
126.154031059289));
#185930=CARTESIAN_POINT('Ctrl Pts',(176.445957724115,-3.53435409749872,
126.056614050062));
#185931=CARTESIAN_POINT('Ctrl Pts',(176.453354409027,-3.40658544998641,
125.964117856352));
#185932=CARTESIAN_POINT('Ctrl Pts',(176.460751093939,-3.27531937255807,
125.87686494834));
#185933=CARTESIAN_POINT('Ctrl Pts',(176.468147450875,-3.1440591156053,125.789615909212));
#185934=CARTESIAN_POINT('Ctrl Pts',(176.47554380781,-3.00930204797122,125.707609900153));
#185935=CARTESIAN_POINT('Ctrl Pts',(176.482940164745,-2.87151103396717,
125.631126141505));
#185936=CARTESIAN_POINT('Ctrl Pts',(176.490337654082,-2.73369892380657,
125.554630672999));
#185937=CARTESIAN_POINT('Ctrl Pts',(176.497735143419,-2.59285226879406,
125.483659319529));
#185938=CARTESIAN_POINT('Ctrl Pts',(176.505132632755,-2.44945853109072,
125.418445331659));
#185939=CARTESIAN_POINT('Ctrl Pts',(176.51253271527,-2.30601452693502,125.353208483127));
#185940=CARTESIAN_POINT('Ctrl Pts',(176.519932797785,-2.16002200197382,
125.293733172932));
#185941=CARTESIAN_POINT('Ctrl Pts',(176.5273328803,-2.01198823718576,125.240204446508));
#185942=CARTESIAN_POINT('Ctrl Pts',(176.534741099967,-1.86379169405521,
125.186616859746));
#185943=CARTESIAN_POINT('Ctrl Pts',(176.542149319633,-1.71354977984559,
125.138989042347));
#185944=CARTESIAN_POINT('Ctrl Pts',(176.549557539299,-1.56178547706073,
125.097456317848));
#185945=CARTESIAN_POINT('Ctrl Pts',(176.556970318601,-1.4099277658798,125.055898030649));
#185946=CARTESIAN_POINT('Ctrl Pts',(176.564383097904,-1.25654616188793,
125.02044239542));
#185947=CARTESIAN_POINT('Ctrl Pts',(176.571795877206,-1.10217315737517,
124.99117346303));
#185948=CARTESIAN_POINT('Ctrl Pts',(176.579219248234,-0.947579577474068,
124.961862709817));
#185949=CARTESIAN_POINT('Ctrl Pts',(176.586642619263,-0.791992136134873,
124.9387563693));
#185950=CARTESIAN_POINT('Ctrl Pts',(176.594065990292,-0.635948581030021,
124.921886651216));
#185951=CARTESIAN_POINT('Ctrl Pts',(176.598002039733,-0.553210543900006,
124.912941921905));
#185952=CARTESIAN_POINT('Ctrl Pts',(176.601938089173,-0.470344291830868,
124.905749659825));
#185953=CARTESIAN_POINT('Ctrl Pts',(176.605874138614,-0.387429773278801,
124.900308726426));
#185954=CARTESIAN_POINT('Ctrl Pts',(176.61329740502,-0.231055578962694,
124.890047295841));
#185955=CARTESIAN_POINT('Ctrl Pts',(176.620720671425,-0.0740369722305812,
124.885987209403));
#185956=CARTESIAN_POINT('Ctrl Pts',(176.62814393783,0.0830930337498934,
124.888194112958));
#185957=CARTESIAN_POINT('Ctrl Pts',(176.635558430551,0.240037325112162,
124.890398408136));
#185958=CARTESIAN_POINT('Ctrl Pts',(176.642972923272,0.397092384027427,
124.898854944318));
#185959=CARTESIAN_POINT('Ctrl Pts',(176.650387415993,0.553720283044722,
124.913577612681));
#185960=CARTESIAN_POINT('Ctrl Pts',(176.657794762347,0.710197218196119,
124.928286090781));
#185961=CARTESIAN_POINT('Ctrl Pts',(176.665202108701,0.866247443924086,
124.949248642838));
#185962=CARTESIAN_POINT('Ctrl Pts',(176.672609455055,1.02133334952026,124.976427128613));
#185963=CARTESIAN_POINT('Ctrl Pts',(176.68001127673,1.17630358619691,125.003585343648));
#185964=CARTESIAN_POINT('Ctrl Pts',(176.687413098406,1.33031056870666,125.036950197183));
#185965=CARTESIAN_POINT('Ctrl Pts',(176.694814920081,1.4828222356449,125.076431778974));
#185966=CARTESIAN_POINT('Ctrl Pts',(176.702212834392,1.63525339286118,125.115892518745));
#185967=CARTESIAN_POINT('Ctrl Pts',(176.709610748704,1.78619044609497,125.161463462799));
#185968=CARTESIAN_POINT('Ctrl Pts',(176.717008663015,1.93511206174074,125.213003727597));
#185969=CARTESIAN_POINT('Ctrl Pts',(176.724405347927,2.08400892931559,125.264535427338));
#185970=CARTESIAN_POINT('Ctrl Pts',(176.73180203284,2.23089067161478,125.322034357041));
#185971=CARTESIAN_POINT('Ctrl Pts',(176.739198717752,2.37525153545877,125.385309897578));
#185972=CARTESIAN_POINT('Ctrl Pts',(176.746595074687,2.51960599819104,125.448582632412));
#185973=CARTESIAN_POINT('Ctrl Pts',(176.753991431623,2.66143946282441,125.517631318926));
#185974=CARTESIAN_POINT('Ctrl Pts',(176.761387788558,2.8002668239092,125.592217461683));
#185975=CARTESIAN_POINT('Ctrl Pts',(176.768785277895,2.93911543981793,125.66681502377));
#185976=CARTESIAN_POINT('Ctrl Pts',(176.776182767231,3.0749567069106,125.746951553495));
#185977=CARTESIAN_POINT('Ctrl Pts',(176.783580256568,3.20733089967709,125.832343012762));
#185978=CARTESIAN_POINT('Ctrl Pts',(176.790980339083,3.33975149601111,125.917764405874));
#185979=CARTESIAN_POINT('Ctrl Pts',(176.798380421598,3.4687022847138,126.008444193921));
#185980=CARTESIAN_POINT('Ctrl Pts',(176.805780504113,3.59375338405989,126.104055608627));
#185981=CARTESIAN_POINT('Ctrl Pts',(176.81318872378,3.71894198994533,126.199772157913));
#185982=CARTESIAN_POINT('Ctrl Pts',(176.820596943446,3.84022204610599,126.300430936731));
#185983=CARTESIAN_POINT('Ctrl Pts',(176.828005163113,3.95719701619971,126.405665090767));
#185984=CARTESIAN_POINT('Ctrl Pts',(176.835417942415,4.07424398243563,126.510964014669));
#185985=CARTESIAN_POINT('Ctrl Pts',(176.842830721717,4.18698031602106,126.620843665207));
#185986=CARTESIAN_POINT('Ctrl Pts',(176.850243501019,4.29504747748942,126.734901473084));
#185987=CARTESIAN_POINT('Ctrl Pts',(176.857666872048,4.4032690503861,126.849122252105));
#185988=CARTESIAN_POINT('Ctrl Pts',(176.865090243076,4.50680788154691,126.967532831516));
#185989=CARTESIAN_POINT('Ctrl Pts',(176.872513614105,4.60534620625596,127.089698199119));
#185990=CARTESIAN_POINT('Ctrl Pts',(176.876449663546,4.65759359041109,127.154473208339));
#185991=CARTESIAN_POINT('Ctrl Pts',(176.880385712987,4.70843587755835,127.220303339764));
#185992=CARTESIAN_POINT('Ctrl Pts',(176.884321762427,4.75783081149922,127.287120715079));
#185993=CARTESIAN_POINT('Ctrl Pts',(176.891745028833,4.850988115349,127.413136199624));
#185994=CARTESIAN_POINT('Ctrl Pts',(176.899168295238,4.93927637338779,127.543045824573));
#185995=CARTESIAN_POINT('Ctrl Pts',(176.906591561644,5.02235224927055,127.676436634035));
#185996=CARTESIAN_POINT('Ctrl Pts',(176.914006054365,5.10532993636708,127.809669786638));
#185997=CARTESIAN_POINT('Ctrl Pts',(176.921420547086,5.18310730860256,127.946375620103));
#185998=CARTESIAN_POINT('Ctrl Pts',(176.928835039807,5.25538191600952,128.08610906935));
#185999=CARTESIAN_POINT('Ctrl Pts',(176.936242386161,5.32758686242861,128.225707838237));
#186000=CARTESIAN_POINT('Ctrl Pts',(176.943649732514,5.39429943243706,128.368328084139));
#186001=CARTESIAN_POINT('Ctrl Pts',(176.951057078868,5.45526112277846,128.513496884211));
#186002=CARTESIAN_POINT('Ctrl Pts',(176.958458900543,5.51617734559132,128.658557411914));
#186003=CARTESIAN_POINT('Ctrl Pts',(176.965860722219,5.57135108524651,128.806162366322));
#186004=CARTESIAN_POINT('Ctrl Pts',(176.973262543894,5.62057039359431,128.955815510421));
#186005=CARTESIAN_POINT('Ctrl Pts',(176.980660458206,5.66976371945242,129.10538965379));
#186006=CARTESIAN_POINT('Ctrl Pts',(176.988058372517,5.7130087576989,129.257009479828));
#186007=CARTESIAN_POINT('Ctrl Pts',(176.995456286828,5.75014224409737,129.410160224815));
#186008=CARTESIAN_POINT('Ctrl Pts',(177.002852971741,5.78726955958403,129.563285518926));
#186009=CARTESIAN_POINT('Ctrl Pts',(177.010249656653,5.81828725106939,129.717940864624));
#186010=CARTESIAN_POINT('Ctrl Pts',(177.017646341565,5.84308231987691,129.873597723139));
#186011=CARTESIAN_POINT('Ctrl Pts',(177.0250426985,5.86787628924509,130.029247679666));
#186012=CARTESIAN_POINT('Ctrl Pts',(177.032439055436,5.88644812582946,130.185898692064));
#186013=CARTESIAN_POINT('Ctrl Pts',(177.039835412371,5.89873627125152,130.343013714768));
#186014=CARTESIAN_POINT('Ctrl Pts',(177.047232901708,5.91102629802002,130.500152792183));
#186015=CARTESIAN_POINT('Ctrl Pts',(177.054630391044,5.91703068894933,130.657755649171));
#186016=CARTESIAN_POINT('Ctrl Pts',(177.062027880381,5.91673992046528,130.815281976114));
#186017=CARTESIAN_POINT('Ctrl Pts',(177.069427962896,5.91644905005278,130.972863523666));
#186018=CARTESIAN_POINT('Ctrl Pts',(177.076828045411,5.90985862727574,131.130368114695));
#186019=CARTESIAN_POINT('Ctrl Pts',(177.084228127926,5.89701120996687,131.287257451295));
#186020=CARTESIAN_POINT('Ctrl Pts',(177.091636347592,5.88414966560198,131.444319303847));
#186021=CARTESIAN_POINT('Ctrl Pts',(177.099044567259,5.86501741696226,131.600764178604));
#186022=CARTESIAN_POINT('Ctrl Pts',(177.106452786925,5.83970877139378,131.75606016459));
#186023=CARTESIAN_POINT('Ctrl Pts',(177.113865566227,5.81438454877628,131.911451732665));
#186024=CARTESIAN_POINT('Ctrl Pts',(177.121278345529,5.78287642886657,132.065692638045));
#186025=CARTESIAN_POINT('Ctrl Pts',(177.128691124831,5.74532930527565,132.218263632783));
#186026=CARTESIAN_POINT('Ctrl Pts',(177.13611449586,5.70772853259378,132.371052628114));
#186027=CARTESIAN_POINT('Ctrl Pts',(177.143537866889,5.66407162589269,132.522166589652));
#186028=CARTESIAN_POINT('Ctrl Pts',(177.150961237918,5.61455281366331,132.671103038224));
#186029=CARTESIAN_POINT('Ctrl Pts',(177.154897287358,5.58829675123149,132.750072716939));
#186030=CARTESIAN_POINT('Ctrl Pts',(177.158833336799,5.5603934953522,132.828430567071));
#186031=CARTESIAN_POINT('Ctrl Pts',(177.16276938624,5.53087731346671,132.906104347396));
#186032=CARTESIAN_POINT('Ctrl Pts',(177.170192652645,5.47521071559956,133.052594672972));
#186033=CARTESIAN_POINT('Ctrl Pts',(177.177615919051,5.4136360289286,133.197093410418));
#186034=CARTESIAN_POINT('Ctrl Pts',(177.185039185456,5.34631510325961,133.339088488395));
#186035=CARTESIAN_POINT('Ctrl Pts',(177.192453678177,5.27907374533417,133.480915739982));
#186036=CARTESIAN_POINT('Ctrl Pts',(177.199868170898,5.20609982544146,133.620244888226));
#186037=CARTESIAN_POINT('Ctrl Pts',(177.207282663619,5.12760430784209,133.756580904858));
#186038=CARTESIAN_POINT('Ctrl Pts',(177.214690009973,5.04918444717779,133.892785515704));
#186039=CARTESIAN_POINT('Ctrl Pts',(177.222097356327,4.96525376871951,134.026002416854));
#186040=CARTESIAN_POINT('Ctrl Pts',(177.22950470268,4.8760704285268,134.155758495847));
#186041=CARTESIAN_POINT('Ctrl Pts',(177.236906524356,4.78695360463412,134.28541779786));
#186042=CARTESIAN_POINT('Ctrl Pts',(177.244308346031,4.69259213007899,134.411621110942));
#186043=CARTESIAN_POINT('Ctrl Pts',(177.251710167707,4.59328893996197,134.533921888885));
#186044=CARTESIAN_POINT('Ctrl Pts',(177.259108082018,4.49403817122483,134.656158105201));
#186045=CARTESIAN_POINT('Ctrl Pts',(177.266505996329,4.38985111697191,134.774495600136));
#186046=CARTESIAN_POINT('Ctrl Pts',(177.273903910641,4.28107261419333,134.888518772499));
#186047=CARTESIAN_POINT('Ctrl Pts',(177.281300595553,4.17231218842958,135.002522996278));
#186048=CARTESIAN_POINT('Ctrl Pts',(177.288697280465,4.05896208592436,135.112214050608));
#186049=CARTESIAN_POINT('Ctrl Pts',(177.296093965377,3.94140590276758,135.217211178386));
#186050=CARTESIAN_POINT('Ctrl Pts',(177.303490322313,3.82385493217522,135.322203650482));
#186051=CARTESIAN_POINT('Ctrl Pts',(177.310886679248,3.70209853017439,135.422502361196));
#186052=CARTESIAN_POINT('Ctrl Pts',(177.318283036184,3.57655525460029,135.517765233477));
#186053=CARTESIAN_POINT('Ctrl Pts',(177.32568052552,3.4509927580304,135.613042690747));
#186054=CARTESIAN_POINT('Ctrl Pts',(177.333078014857,3.32164253086402,135.703282548755));
#186055=CARTESIAN_POINT('Ctrl Pts',(177.340475504193,3.18895400316233,135.788184744501));
#186056=CARTESIAN_POINT('Ctrl Pts',(177.347875586708,3.05621896170209,135.87311670258));
#186057=CARTESIAN_POINT('Ctrl Pts',(177.355275669223,2.92014360401691,135.952707071962));
#186058=CARTESIAN_POINT('Ctrl Pts',(177.362675751738,2.78120381892832,136.026700694589));
#186059=CARTESIAN_POINT('Ctrl Pts',(177.370083971405,2.64211125526319,136.10077568081));
#186060=CARTESIAN_POINT('Ctrl Pts',(177.377492191071,2.50014830366085,136.169241454361));
#186061=CARTESIAN_POINT('Ctrl Pts',(177.384900410737,2.35581345131169,136.231889847807));
#186062=CARTESIAN_POINT('Ctrl Pts',(177.39231319004,2.21138976326912,136.294576800294));
#186063=CARTESIAN_POINT('Ctrl Pts',(177.399725969342,2.06459161280398,136.351439103559));
#186064=CARTESIAN_POINT('Ctrl Pts',(177.407138748644,1.91593417645481,136.402317994502));
#186065=CARTESIAN_POINT('Ctrl Pts',(177.414562119672,1.76706433138938,136.45326958359));
#186066=CARTESIAN_POINT('Ctrl Pts',(177.421985490701,1.61633025132645,136.49822057893));
#186067=CARTESIAN_POINT('Ctrl Pts',(177.42940886173,1.46425967146917,136.537062788184));
#186068=CARTESIAN_POINT('Ctrl Pts',(177.433344911171,1.38362820114492,136.557657859537));
#186069=CARTESIAN_POINT('Ctrl Pts',(177.437280960611,1.30262113124199,136.576536392097));
#186070=CARTESIAN_POINT('Ctrl Pts',(177.441217010052,1.22131776273696,136.593688167889));
#186071=CARTESIAN_POINT('Ctrl Pts',(177.448640276458,1.06798214712807,136.626035881742));
#186072=CARTESIAN_POINT('Ctrl Pts',(177.456063542863,0.913128644707063,
136.652336451127));
#186073=CARTESIAN_POINT('Ctrl Pts',(177.463486809269,0.757275559365821,
136.672449257804));
#186074=CARTESIAN_POINT('Ctrl Pts',(177.47090130199,0.601606679428604,136.692538292813));
#186075=CARTESIAN_POINT('Ctrl Pts',(177.478315794711,0.444940934814573,
136.706454075208));
#186076=CARTESIAN_POINT('Ctrl Pts',(177.485730287432,0.287808838163108,
136.714106520325));
#186077=CARTESIAN_POINT('Ctrl Pts',(177.493137633785,0.130828191341923,
136.721751589727));
#186078=CARTESIAN_POINT('Ctrl Pts',(177.500544980139,-0.0266175423223238,
136.723145321975));
#186079=CARTESIAN_POINT('Ctrl Pts',(177.507952326493,-0.18399078026119,
136.718249182231));
#186080=CARTESIAN_POINT('Ctrl Pts',(177.515354148168,-0.341246643301121,
136.713356694213));
#186081=CARTESIAN_POINT('Ctrl Pts',(177.522755969844,-0.498429746764934,
136.702183686622));
#186082=CARTESIAN_POINT('Ctrl Pts',(177.530157791519,-0.655000654859997,
136.684743658205));
#186083=CARTESIAN_POINT('Ctrl Pts',(177.537555705831,-0.811488910392845,
136.667312836243));
#186084=CARTESIAN_POINT('Ctrl Pts',(177.544953620142,-0.96736524410747,
136.643621623335));
#186085=CARTESIAN_POINT('Ctrl Pts',(177.552351534454,-1.12209360613494,
136.613735498013));
#186086=CARTESIAN_POINT('Ctrl Pts',(177.559748219366,-1.27679625511462,
136.583854339223));
#186087=CARTESIAN_POINT('Ctrl Pts',(177.567144904278,-1.4303509448687,136.547780381962));
#186088=CARTESIAN_POINT('Ctrl Pts',(177.57454158919,-1.58222999060772,136.505630547969));
#186089=CARTESIAN_POINT('Ctrl Pts',(177.581937946126,-1.73410230187086,
136.463482582945));
#186090=CARTESIAN_POINT('Ctrl Pts',(177.589334303061,-1.88429875714948,
136.415259376694));
#186091=CARTESIAN_POINT('Ctrl Pts',(177.596730659997,-2.03230531659756,
136.361128172776));
#186092=CARTESIAN_POINT('Ctrl Pts',(177.604128149333,-2.18033453622717,
136.306988681232));
#186093=CARTESIAN_POINT('Ctrl Pts',(177.61152563867,-2.32617284183337,136.246939519212));
#186094=CARTESIAN_POINT('Ctrl Pts',(177.618923128006,-2.46932485398994,
136.181196613574));
#186095=CARTESIAN_POINT('Ctrl Pts',(177.626323210521,-2.61252704786361,
136.115430661862));
#186096=CARTESIAN_POINT('Ctrl Pts',(177.633723293036,-2.75304073439541,
136.04396714834));
#186097=CARTESIAN_POINT('Ctrl Pts',(177.641123375552,-2.89039401235355,
135.96706853259));
#186098=CARTESIAN_POINT('Ctrl Pts',(177.648531595218,-3.02789832436052,
135.890085358907));
#186099=CARTESIAN_POINT('Ctrl Pts',(177.655939814885,-3.16223496167907,
135.807655330097));
#186100=CARTESIAN_POINT('Ctrl Pts',(177.663348034551,-3.29295934264992,
135.720085317969));
#186101=CARTESIAN_POINT('Ctrl Pts',(177.670760813853,-3.42376418229605,
135.63246140796));
#186102=CARTESIAN_POINT('Ctrl Pts',(177.678173593155,-3.55095203452769,
135.539691430287));
#186103=CARTESIAN_POINT('Ctrl Pts',(177.685586372457,-3.67411086194991,
135.44212300223));
#186104=CARTESIAN_POINT('Ctrl Pts',(177.693009743486,-3.79744566448051,
135.344415163826));
#186105=CARTESIAN_POINT('Ctrl Pts',(177.700433114515,-3.91673966209711,
135.241895424228));
#186106=CARTESIAN_POINT('Ctrl Pts',(177.707856485544,-4.03161657575471,
135.134949301406));
#186107=CARTESIAN_POINT('Ctrl Pts',(177.711792534984,-4.09252707180661,
135.078243900951));
#186108=CARTESIAN_POINT('Ctrl Pts',(177.715728584425,-4.15219641590479,
135.020294666788));
#186109=CARTESIAN_POINT('Ctrl Pts',(177.719664633866,-4.21057314726077,
134.961162794007));
#186110=CARTESIAN_POINT('Ctrl Pts',(177.726987714394,-4.31918395389978,
134.851147035132));
#186111=CARTESIAN_POINT('Ctrl Pts',(177.734310794923,-4.42366599101378,
134.736683004449));
#186112=CARTESIAN_POINT('Ctrl Pts',(177.741633875452,-4.52362539881567,
134.61811779569));
#186113=CARTESIAN_POINT('Ctrl Pts',(177.748948118279,-4.62346417276795,
134.499695674788));
#186114=CARTESIAN_POINT('Ctrl Pts',(177.756262361106,-4.71879093201483,
134.377182514416));
#186115=CARTESIAN_POINT('Ctrl Pts',(177.763576603933,-4.80924728733108,
134.250963451053));
#186116=CARTESIAN_POINT('Ctrl Pts',(177.770882500434,-4.89960042235674,
134.124888417022));
#186117=CARTESIAN_POINT('Ctrl Pts',(177.778188396935,-4.985093998768,133.995116211621));
#186118=CARTESIAN_POINT('Ctrl Pts',(177.785494293436,-5.06540902935797,
133.862065954546));
#186119=CARTESIAN_POINT('Ctrl Pts',(177.792795471415,-5.14567218839746,
133.729101628126));
#186120=CARTESIAN_POINT('Ctrl Pts',(177.800096649395,-5.22076325672502,
133.592863788803));
#186121=CARTESIAN_POINT('Ctrl Pts',(177.807397827374,-5.29040573463265,
133.453801638888));
#186122=CARTESIAN_POINT('Ctrl Pts',(177.814695823601,-5.36001786330739,
133.314800090344));
#186123=CARTESIAN_POINT('Ctrl Pts',(177.821993819828,-5.42418595412213,
133.172977022927));
#186124=CARTESIAN_POINT('Ctrl Pts',(177.829291816054,-5.48267892226044,
133.028807155));
#186125=CARTESIAN_POINT('Ctrl Pts',(177.836588164671,-5.54115868490669,
132.884669835157));
#186126=CARTESIAN_POINT('Ctrl Pts',(177.843884513287,-5.59396573107036,
132.738187125347));
#186127=CARTESIAN_POINT('Ctrl Pts',(177.851180861903,-5.64091681357705,
132.589854404955));
#186128=CARTESIAN_POINT('Ctrl Pts',(177.85847957844,-5.68788313335843,132.441473545386));
#186129=CARTESIAN_POINT('Ctrl Pts',(177.865778294978,-5.72898957039591,
132.291241840484));
#186130=CARTESIAN_POINT('Ctrl Pts',(177.873077011515,-5.76410247697536,
132.139670767841));
#186131=CARTESIAN_POINT('Ctrl Pts',(177.88037674119,-5.79922025759192,131.988078655554));
#186132=CARTESIAN_POINT('Ctrl Pts',(177.887676470866,-5.82834277242975,
131.835147181732));
#186133=CARTESIAN_POINT('Ctrl Pts',(177.894976200541,-5.85138751742267,
131.681398064572));
#186134=CARTESIAN_POINT('Ctrl Pts',(177.902282487808,-5.87445296428058,
131.527510829438));
#186135=CARTESIAN_POINT('Ctrl Pts',(177.909588775074,-5.89142968455054,
131.372804865184));
#186136=CARTESIAN_POINT('Ctrl Pts',(177.916895062341,-5.90228702617907,
131.217807619125));
#186137=CARTESIAN_POINT('Ctrl Pts',(177.923471644159,-5.91206000566133,
131.078290511037));
#186138=CARTESIAN_POINT('Ctrl Pts',(177.930048225977,-5.91687557850981,
130.938537649031));
#186139=CARTESIAN_POINT('Ctrl Pts',(177.936624807795,-5.91674751037323,
130.798932819469));
#186140=CARTESIAN_POINT('',(179.686624807795,-5.92158244890185,130.806643466513));
#186141=CARTESIAN_POINT('Ctrl Pts',(177.936624807795,-5.91746116842021,
130.798932164786));
#186142=CARTESIAN_POINT('Ctrl Pts',(177.957120624423,-5.9215064818599,130.363799294495));
#186143=CARTESIAN_POINT('Ctrl Pts',(178.070432315656,-5.6787771470729,127.962628861881));
#186144=CARTESIAN_POINT('Ctrl Pts',(178.276559881491,-2.40168273653391,
124.230968756176));
#186145=CARTESIAN_POINT('Ctrl Pts',(178.555007505305,4.23221255766007,125.230678047027));
#186146=CARTESIAN_POINT('Ctrl Pts',(178.833455129117,6.97691126644166,131.352329330672));
#186147=CARTESIAN_POINT('Ctrl Pts',(179.11190275293,3.31016936242742,136.970424136732));
#186148=CARTESIAN_POINT('Ctrl Pts',(179.390350376743,-3.39845647489431,
136.922207797627));
#186149=CARTESIAN_POINT('Ctrl Pts',(179.581924395032,-5.86538284120287,
133.021055300245));
#186150=CARTESIAN_POINT('Ctrl Pts',(179.680682538715,-5.92608698495012,
130.932358269279));
#186151=CARTESIAN_POINT('Ctrl Pts',(179.686624807795,-5.92546899106887,
130.806644964827));
#186152=CARTESIAN_POINT('',(181.436624793272,-5.91313131605275,130.808682171932));
#186153=CARTESIAN_POINT('Ctrl Pts',(179.686624807795,-5.9167495603248,130.80664160337));
#186154=CARTESIAN_POINT('Ctrl Pts',(179.693977154138,-5.91680943647244,
130.651326226339));
#186155=CARTESIAN_POINT('Ctrl Pts',(179.701329500482,-5.91074953815374,
130.495761078002));
#186156=CARTESIAN_POINT('Ctrl Pts',(179.708681846825,-5.89853708827506,
130.340474014242));
#186157=CARTESIAN_POINT('Ctrl Pts',(179.716025830516,-5.88633852899205,
130.185363575961));
#186158=CARTESIAN_POINT('Ctrl Pts',(179.723369814208,-5.86800137290794,
130.030530968938));
#186159=CARTESIAN_POINT('Ctrl Pts',(179.730713797899,-5.84354481501677,
129.876505802743));
#186160=CARTESIAN_POINT('Ctrl Pts',(179.738051104691,-5.81911049219403,
129.722620670976));
#186161=CARTESIAN_POINT('Ctrl Pts',(179.745388411482,-5.78856789958858,
129.569541892852));
#186162=CARTESIAN_POINT('Ctrl Pts',(179.752725718274,-5.75198815284064,
129.417795490325));
#186163=CARTESIAN_POINT('Ctrl Pts',(179.760058027822,-5.71543331957921,
129.266152438212));
#186164=CARTESIAN_POINT('Ctrl Pts',(179.767390337371,-5.6728496059675,129.11584032425));
#186165=CARTESIAN_POINT('Ctrl Pts',(179.774722646919,-5.62435943793095,
128.96737627483));
#186166=CARTESIAN_POINT('Ctrl Pts',(179.782052360326,-5.57588643874756,
128.818964791891));
#186167=CARTESIAN_POINT('Ctrl Pts',(179.789382073733,-5.52151126173289,
128.672400433808));
#186168=CARTESIAN_POINT('Ctrl Pts',(179.796711787139,-5.46140653421223,
128.528186364447));
#186169=CARTESIAN_POINT('Ctrl Pts',(179.804040294966,-5.40131169262705,
128.383996015199));
#186170=CARTESIAN_POINT('Ctrl Pts',(179.811368802792,-5.33548932152652,
128.24215553726));
#186171=CARTESIAN_POINT('Ctrl Pts',(179.818697310619,-5.26416055459471,
128.103148997209));
#186172=CARTESIAN_POINT('Ctrl Pts',(179.826026126248,-5.19282879179809,
127.964136618774));
#186173=CARTESIAN_POINT('Ctrl Pts',(179.833354941878,-5.11599034668846,
127.827958754184));
#186174=CARTESIAN_POINT('Ctrl Pts',(179.840683757508,-5.03391263741617,
127.695075471208));
#186175=CARTESIAN_POINT('Ctrl Pts',(179.848014394317,-4.95181453217909,
127.562159167297));
#186176=CARTESIAN_POINT('Ctrl Pts',(179.855345031126,-4.86447477205808,
127.432539398244));
#186177=CARTESIAN_POINT('Ctrl Pts',(179.862675667936,-4.77220433056239,
127.306647594766));
#186178=CARTESIAN_POINT('Ctrl Pts',(179.870013917591,-4.67983806647012,
127.180625053001));
#186179=CARTESIAN_POINT('Ctrl Pts',(179.877352167246,-4.58253111937658,
127.058338516905));
#186180=CARTESIAN_POINT('Ctrl Pts',(179.884690416902,-4.48063543929967,
126.940187145452));
#186181=CARTESIAN_POINT('Ctrl Pts',(179.892032632595,-4.37868468856922,
126.821971917776));
#186182=CARTESIAN_POINT('Ctrl Pts',(179.899374848289,-4.27214052426441,
126.707896584654));
#186183=CARTESIAN_POINT('Ctrl Pts',(179.906717063983,-4.16139154293925,
126.598323172553));
#186184=CARTESIAN_POINT('Ctrl Pts',(179.914070345708,-4.05047564310977,
126.48858461374));
#186185=CARTESIAN_POINT('Ctrl Pts',(179.921423627433,-3.93534254692211,
126.383361787399));
#186186=CARTESIAN_POINT('Ctrl Pts',(179.928776909158,-3.81641438967868,
126.282976784186));
#186187=CARTESIAN_POINT('Ctrl Pts',(179.934933147562,-3.71684658903447,
126.198933490997));
#186188=CARTESIAN_POINT('Ctrl Pts',(179.941089385965,-3.61461941093371,
126.118280447087));
#186189=CARTESIAN_POINT('Ctrl Pts',(179.947245624368,-3.50999522101216,
126.041182675165));
#186190=CARTESIAN_POINT('Ctrl Pts',(179.954668890774,-3.38383811283284,
125.948217253306));
#186191=CARTESIAN_POINT('Ctrl Pts',(179.962092157179,-3.25379427861745,
125.860126797838));
#186192=CARTESIAN_POINT('Ctrl Pts',(179.969515423585,-3.12027719627839,
125.777254016261));
#186193=CARTESIAN_POINT('Ctrl Pts',(179.976929916306,-2.98691792004263,
125.694479183429));
#186194=CARTESIAN_POINT('Ctrl Pts',(179.984344409027,-2.85009388096072,
125.616909944266));
#186195=CARTESIAN_POINT('Ctrl Pts',(179.991758901748,-2.71025060387357,
125.544848071074));
#186196=CARTESIAN_POINT('Ctrl Pts',(179.999166248101,-2.5705421130023,125.47285565383));
#186197=CARTESIAN_POINT('Ctrl Pts',(180.006573594455,-2.42782050707694,
125.406360204809));
#186198=CARTESIAN_POINT('Ctrl Pts',(180.013980940809,-2.28255910179349,
125.345619507262));
#186199=CARTESIAN_POINT('Ctrl Pts',(180.021382762484,-2.13740603794629,
125.284924112419));
#186200=CARTESIAN_POINT('Ctrl Pts',(180.02878458416,-1.98971728942356,125.229975066268));
#186201=CARTESIAN_POINT('Ctrl Pts',(180.036186405835,-1.83998941521192,
125.180983561525));
#186202=CARTESIAN_POINT('Ctrl Pts',(180.043584320146,-1.69034058117979,
125.132017919016));
#186203=CARTESIAN_POINT('Ctrl Pts',(180.050982234458,-1.53865511912818,
125.089003670412));
#186204=CARTESIAN_POINT('Ctrl Pts',(180.058380148769,-1.38544804064297,
125.052103296376));
#186205=CARTESIAN_POINT('Ctrl Pts',(180.065776833681,-1.23226642239424,
125.015209054514));
#186206=CARTESIAN_POINT('Ctrl Pts',(180.073173518594,-1.07756405213862,
124.984426758055));
#186207=CARTESIAN_POINT('Ctrl Pts',(180.080570203506,-0.921869639997064,
124.959868601201));
#186208=CARTESIAN_POINT('Ctrl Pts',(180.087966560441,-0.76618213150912,
124.935311533282));
#186209=CARTESIAN_POINT('Ctrl Pts',(180.095362917377,-0.609503037337292,
124.916978114377));
#186210=CARTESIAN_POINT('Ctrl Pts',(180.102759274312,-0.452369496104509,
124.904929085503));
#186211=CARTESIAN_POINT('Ctrl Pts',(180.110156763649,-0.295211897325392,
124.892878211893));
#186212=CARTESIAN_POINT('Ctrl Pts',(180.117554252985,-0.137600085177405,
124.887113672636));
#186213=CARTESIAN_POINT('Ctrl Pts',(180.124951742322,0.0199256168518951,
124.887644169037));
#186214=CARTESIAN_POINT('Ctrl Pts',(180.132351824837,0.177506539271902,
124.888174851403));
#186215=CARTESIAN_POINT('Ctrl Pts',(180.139751907352,0.335000918410661,
124.895004961724));
#186216=CARTESIAN_POINT('Ctrl Pts',(180.147151989867,0.491870521751642,
124.908091123018));
#186217=CARTESIAN_POINT('Ctrl Pts',(180.154560209533,0.648912619348167,
124.921191673893));
#186218=CARTESIAN_POINT('Ctrl Pts',(180.1619684292,0.805328196918372,124.940561982845));
#186219=CARTESIAN_POINT('Ctrl Pts',(180.169376648866,0.960585487624677,
124.966106933161));
#186220=CARTESIAN_POINT('Ctrl Pts',(180.176789428168,1.115938336603,124.991667605968));
#186221=CARTESIAN_POINT('Ctrl Pts',(180.184202207471,1.27013111337955,125.023410417793));
#186222=CARTESIAN_POINT('Ctrl Pts',(180.191614986773,1.42264479111333,125.061189684987));
#186223=CARTESIAN_POINT('Ctrl Pts',(180.199038357801,1.57537638754186,125.09902293297));
#186224=CARTESIAN_POINT('Ctrl Pts',(180.20646172883,1.72642373571236,125.142909758842));
#186225=CARTESIAN_POINT('Ctrl Pts',(180.213885099859,1.87528465261602,125.192655169651));
#186226=CARTESIAN_POINT('Ctrl Pts',(180.2178211493,1.95421428262784,125.219031380086));
#186227=CARTESIAN_POINT('Ctrl Pts',(180.221757198741,2.03252957801731,125.247053850963));
#186228=CARTESIAN_POINT('Ctrl Pts',(180.225693248181,2.11015834979351,125.276688204941));
#186229=CARTESIAN_POINT('Ctrl Pts',(180.233116514587,2.25656379065098,125.332577671686));
#186230=CARTESIAN_POINT('Ctrl Pts',(180.240539780992,2.40096865457811,125.394372189534));
#186231=CARTESIAN_POINT('Ctrl Pts',(180.247963047398,2.5428611171387,125.461909129584));
#186232=CARTESIAN_POINT('Ctrl Pts',(180.255377540119,2.68458587459203,125.529366246579));
#186233=CARTESIAN_POINT('Ctrl Pts',(180.26279203284,2.82380380761203,125.602552117214));
#186234=CARTESIAN_POINT('Ctrl Pts',(180.270206525561,2.9600202095537,125.681255024126));
#186235=CARTESIAN_POINT('Ctrl Pts',(180.277613871915,3.09610532099887,125.759882074213));
#186236=CARTESIAN_POINT('Ctrl Pts',(180.285021218268,3.22919433968091,125.844015388928));
#186237=CARTESIAN_POINT('Ctrl Pts',(180.292428564622,3.35881454655656,125.933396092511));
#186238=CARTESIAN_POINT('Ctrl Pts',(180.299830386298,3.48833807779142,126.022710132594));
#186239=CARTESIAN_POINT('Ctrl Pts',(180.307232207973,3.61439764263109,126.11726355784));
#186240=CARTESIAN_POINT('Ctrl Pts',(180.314634029648,3.73654715640086,126.21675275393));
#186241=CARTESIAN_POINT('Ctrl Pts',(180.32203194396,3.8586321883935,126.316189430449));
#186242=CARTESIAN_POINT('Ctrl Pts',(180.329429858271,3.97681099133407,126.420556453577));
#186243=CARTESIAN_POINT('Ctrl Pts',(180.336827772583,4.09066848929571,126.529508354249));
#186244=CARTESIAN_POINT('Ctrl Pts',(180.344224457495,4.20450706620659,126.638442149092));
#186245=CARTESIAN_POINT('Ctrl Pts',(180.351621142407,4.31402549395549,126.751959051452));
#186246=CARTESIAN_POINT('Ctrl Pts',(180.359017827319,4.4188435996499,126.869674886236));
#186247=CARTESIAN_POINT('Ctrl Pts',(180.366414184255,4.52365705759943,126.987385501376));
#186248=CARTESIAN_POINT('Ctrl Pts',(180.37381054119,4.62377035965245,127.109294399949));
#186249=CARTESIAN_POINT('Ctrl Pts',(180.381206898125,4.71884206612648,127.234982504021));
#186250=CARTESIAN_POINT('Ctrl Pts',(180.388604387462,4.81392832832141,127.360689851263));
#186251=CARTESIAN_POINT('Ctrl Pts',(180.396001876799,4.90397123280667,127.490177258346));
#186252=CARTESIAN_POINT('Ctrl Pts',(180.403399366135,4.98867140088571,127.622994839086));
#186253=CARTESIAN_POINT('Ctrl Pts',(180.41079944865,5.07340126047743,127.755858978823));
#186254=CARTESIAN_POINT('Ctrl Pts',(180.418199531165,5.15278445416412,127.892055301928));
#186255=CARTESIAN_POINT('Ctrl Pts',(180.42559961368,5.22656654840633,128.031107531824));
#186256=CARTESIAN_POINT('Ctrl Pts',(180.433007833347,5.30042977364622,128.170312663941));
#186257=CARTESIAN_POINT('Ctrl Pts',(180.440416053013,5.36867942446826,128.312379644405));
#186258=CARTESIAN_POINT('Ctrl Pts',(180.44782427268,5.43110809229362,128.456809669807));
#186259=CARTESIAN_POINT('Ctrl Pts',(180.455237051982,5.49357518392232,128.60132858948));
#186260=CARTESIAN_POINT('Ctrl Pts',(180.462649831284,5.55021401954599,128.748213104701));
#186261=CARTESIAN_POINT('Ctrl Pts',(180.470062610586,5.60086662026004,128.896947797918));
#186262=CARTESIAN_POINT('Ctrl Pts',(180.477485981615,5.65159159578549,129.04589501024));
#186263=CARTESIAN_POINT('Ctrl Pts',(180.484909352643,5.69631314746229,129.196697323519));
#186264=CARTESIAN_POINT('Ctrl Pts',(180.492332723672,5.73492388620217,129.348826838512));
#186265=CARTESIAN_POINT('Ctrl Pts',(180.496268773113,5.75539622633393,129.429489557658));
#186266=CARTESIAN_POINT('Ctrl Pts',(180.500204822554,5.77415145806278,129.510525263669));
#186267=CARTESIAN_POINT('Ctrl Pts',(180.504140871994,5.79117948410592,129.591854640108));
#186268=CARTESIAN_POINT('Ctrl Pts',(180.5115641384,5.82329380979685,129.745239305871));
#186269=CARTESIAN_POINT('Ctrl Pts',(180.518987404805,5.84935868805641,129.900132653963));
#186270=CARTESIAN_POINT('Ctrl Pts',(180.526410671211,5.86923428957744,130.056016167097));
#186271=CARTESIAN_POINT('Ctrl Pts',(180.533825163932,5.88908639978802,130.211715438863));
#186272=CARTESIAN_POINT('Ctrl Pts',(180.541239656653,5.90276374747488,130.368402179512));
#186273=CARTESIAN_POINT('Ctrl Pts',(180.548654149374,5.91017705542789,130.525545739925));
#186274=CARTESIAN_POINT('Ctrl Pts',(180.556061495727,5.91758321815559,130.682537839459));
#186275=CARTESIAN_POINT('Ctrl Pts',(180.563468842081,5.91873734318499,130.839985511826));
#186276=CARTESIAN_POINT('Ctrl Pts',(180.570876188435,5.91360171383272,130.997351116438));
#186277=CARTESIAN_POINT('Ctrl Pts',(180.57827801011,5.90846991482658,131.154599351844));
#186278=CARTESIAN_POINT('Ctrl Pts',(180.585679831786,5.89705771424754,131.311765269877));
#186279=CARTESIAN_POINT('Ctrl Pts',(180.593081653461,5.87937943175644,131.468309455911));
#186280=CARTESIAN_POINT('Ctrl Pts',(180.600479567773,5.86171048149293,131.624771003489));
#186281=CARTESIAN_POINT('Ctrl Pts',(180.607877482084,5.83778207877467,131.780611102708));
#186282=CARTESIAN_POINT('Ctrl Pts',(180.615275396395,5.80766051783306,131.935293803967));
#186283=CARTESIAN_POINT('Ctrl Pts',(180.622672081308,5.77754396254863,132.089950799766));
#186284=CARTESIAN_POINT('Ctrl Pts',(180.63006876622,5.74123636296223,132.243450413284));
#186285=CARTESIAN_POINT('Ctrl Pts',(180.637465451132,5.69885544372551,132.395265138277));
#186286=CARTESIAN_POINT('Ctrl Pts',(180.644861808067,5.65647640370319,132.547073131647));
#186287=CARTESIAN_POINT('Ctrl Pts',(180.652258165003,5.60802467985748,132.697196025489));
#186288=CARTESIAN_POINT('Ctrl Pts',(180.659654521938,5.55366829783429,132.84512003507));
#186289=CARTESIAN_POINT('Ctrl Pts',(180.667052011275,5.49930359371009,132.993066692195));
#186290=CARTESIAN_POINT('Ctrl Pts',(180.674449500611,5.4390325601511,133.138813444321));
#186291=CARTESIAN_POINT('Ctrl Pts',(180.681846989948,5.37307187764845,133.281865241199));
#186292=CARTESIAN_POINT('Ctrl Pts',(180.689247072463,5.30708807273077,133.424967184663));
#186293=CARTESIAN_POINT('Ctrl Pts',(180.696647154978,5.23541080405183,133.56537195318));
#186294=CARTESIAN_POINT('Ctrl Pts',(180.704047237493,5.15830324904222,133.702608045482));
#186295=CARTESIAN_POINT('Ctrl Pts',(180.71145545716,5.08111090634927,133.839995042975));
#186296=CARTESIAN_POINT('Ctrl Pts',(180.718863676826,4.99847653549861,133.974206080262));
#186297=CARTESIAN_POINT('Ctrl Pts',(180.726271896493,4.91070768452162,134.104797043204));
#186298=CARTESIAN_POINT('Ctrl Pts',(180.733684675795,4.82288481328128,134.235468382706));
#186299=CARTESIAN_POINT('Ctrl Pts',(180.741097455097,4.72992138477512,134.362514907542));
#186300=CARTESIAN_POINT('Ctrl Pts',(180.748510234399,4.6321656429306,134.485525109809));
#186301=CARTESIAN_POINT('Ctrl Pts',(180.755933605427,4.53427022309773,134.608711074823));
#186302=CARTESIAN_POINT('Ctrl Pts',(180.763356976456,4.43156905705897,134.727848916707));
#186303=CARTESIAN_POINT('Ctrl Pts',(180.770780347485,4.32444823497244,134.842562943545));
#186304=CARTESIAN_POINT('Ctrl Pts',(180.774716396926,4.26765020477355,134.9033870731));
#186305=CARTESIAN_POINT('Ctrl Pts',(180.778652446367,4.20961023112803,134.962968159235));
#186306=CARTESIAN_POINT('Ctrl Pts',(180.782588495807,4.15038958737084,135.02125483435));
#186307=CARTESIAN_POINT('Ctrl Pts',(180.790011762213,4.03870130145738,135.131181684552));
#186308=CARTESIAN_POINT('Ctrl Pts',(180.797435028618,3.92247384426901,135.236834442952));
#186309=CARTESIAN_POINT('Ctrl Pts',(180.804858295024,3.80206787792984,135.337815195933));
#186310=CARTESIAN_POINT('Ctrl Pts',(180.812272787745,3.68180422144385,135.43867659805));
#186311=CARTESIAN_POINT('Ctrl Pts',(180.819687280466,3.5573721694491,135.534876748629));
#186312=CARTESIAN_POINT('Ctrl Pts',(180.827101773187,3.42916991556503,135.626053707414));
#186313=CARTESIAN_POINT('Ctrl Pts',(180.83450911954,3.30109122784012,135.717142786413));
#186314=CARTESIAN_POINT('Ctrl Pts',(180.841916465894,3.16924987469744,135.803218097274));
#186315=CARTESIAN_POINT('Ctrl Pts',(180.849323812248,3.03407780160299,135.883957300012));
#186316=CARTESIAN_POINT('Ctrl Pts',(180.856725633923,2.89900654493989,135.964636284407));
#186317=CARTESIAN_POINT('Ctrl Pts',(180.864127455599,2.76060983375698,136.039986894538));
#186318=CARTESIAN_POINT('Ctrl Pts',(180.871529277274,2.61934923298189,136.109729611159));
#186319=CARTESIAN_POINT('Ctrl Pts',(180.878927191586,2.47816320257805,136.179435511143));
#186320=CARTESIAN_POINT('Ctrl Pts',(180.886325105897,2.33411662733151,136.243539248482));
#186321=CARTESIAN_POINT('Ctrl Pts',(180.893723020208,2.18769625047188,136.301806904541));
#186322=CARTESIAN_POINT('Ctrl Pts',(180.901119705121,2.04130020602305,136.360064877571));
#186323=CARTESIAN_POINT('Ctrl Pts',(180.908516390033,1.8925314893964,136.412488556298));
#186324=CARTESIAN_POINT('Ctrl Pts',(180.915913074945,1.74189753958409,136.458891855794));
#186325=CARTESIAN_POINT('Ctrl Pts',(180.92330943188,1.59127026903901,136.505293097718));
#186326=CARTESIAN_POINT('Ctrl Pts',(180.930705788816,1.43877828651029,136.5456743813));
#186327=CARTESIAN_POINT('Ctrl Pts',(180.938102145751,1.28494467561209,136.579899358075));
#186328=CARTESIAN_POINT('Ctrl Pts',(180.945499635088,1.13108751239619,136.61412957478));
#186329=CARTESIAN_POINT('Ctrl Pts',(180.952897124424,0.97588867623078,136.642201526869));
#186330=CARTESIAN_POINT('Ctrl Pts',(180.960294613761,0.819881788008743,
136.664029927023));
#186331=CARTESIAN_POINT('Ctrl Pts',(180.967694696276,0.663820211813073,
136.685865979089));
#186332=CARTESIAN_POINT('Ctrl Pts',(180.975094778791,0.50695038905536,136.701454069904));
#186333=CARTESIAN_POINT('Ctrl Pts',(180.982494861306,0.34981126093449,136.710760760142));
#186334=CARTESIAN_POINT('Ctrl Pts',(180.989903080972,0.192499342187787,
136.720077684043));
#186335=CARTESIAN_POINT('Ctrl Pts',(180.997311300639,0.0349178995625732,
136.72309939146));
#186336=CARTESIAN_POINT('Ctrl Pts',(181.004719520305,-0.122393183915837,
136.719844576722));
#186337=CARTESIAN_POINT('Ctrl Pts',(181.012132299607,-0.279801089741335,
136.7165877587));
#186338=CARTESIAN_POINT('Ctrl Pts',(181.01954507891,-0.436937933096332,
136.707046743394));
#186339=CARTESIAN_POINT('Ctrl Pts',(181.026957858212,-0.593269266378005,
136.691292088211));
#186340=CARTESIAN_POINT('Ctrl Pts',(181.03438122924,-0.749823973199911,
136.675514922038));
#186341=CARTESIAN_POINT('Ctrl Pts',(181.041804600269,-0.905570502595506,
136.653506436043));
#186342=CARTESIAN_POINT('Ctrl Pts',(181.049227971298,-1.05998408315404,
136.625388388154));
#186343=CARTESIAN_POINT('Ctrl Pts',(181.053164020739,-1.14185786866959,
136.61047952448));
#186344=CARTESIAN_POINT('Ctrl Pts',(181.05710007018,-1.22335714732034,136.59385388328));
#186345=CARTESIAN_POINT('Ctrl Pts',(181.06103611962,-1.30440558235503,136.575535250101));
#186346=CARTESIAN_POINT('Ctrl Pts',(181.068459386026,-1.45726040139478,
136.540986879633));
#186347=CARTESIAN_POINT('Ctrl Pts',(181.075882652431,-1.60897283890215,
136.500309324795));
#186348=CARTESIAN_POINT('Ctrl Pts',(181.083305918837,-1.75901317219453,
136.453590938817));
#186349=CARTESIAN_POINT('Ctrl Pts',(181.090720411558,-1.90887617027225,
136.406927770093));
#186350=CARTESIAN_POINT('Ctrl Pts',(181.098134904279,-2.05707064500866,
136.354238091858));
#186351=CARTESIAN_POINT('Ctrl Pts',(181.105549397,-2.20307685243817,136.295661278134));
#186352=CARTESIAN_POINT('Ctrl Pts',(181.112956743353,-2.34894233358859,
136.237140922947));
#186353=CARTESIAN_POINT('Ctrl Pts',(181.120364089707,-2.49262340217373,
136.172744866634));
#186354=CARTESIAN_POINT('Ctrl Pts',(181.127771436061,-2.6336153873598,136.102662284512));
#186355=CARTESIAN_POINT('Ctrl Pts',(181.135173257736,-2.77450221540357,
136.032631972624));
#186356=CARTESIAN_POINT('Ctrl Pts',(181.142575079412,-2.91270362066783,
135.956923745224));
#186357=CARTESIAN_POINT('Ctrl Pts',(181.149976901087,-3.04773494857795,
135.875774842979));
#186358=CARTESIAN_POINT('Ctrl Pts',(181.157374815399,-3.1826949945026,135.794668778606));
#186359=CARTESIAN_POINT('Ctrl Pts',(181.16477272971,-3.31448797669285,135.708127951092));
#186360=CARTESIAN_POINT('Ctrl Pts',(181.172170644021,-3.44265399617015,
135.616435432566));
#186361=CARTESIAN_POINT('Ctrl Pts',(181.179567328934,-3.57079871677919,
135.524758151673));
#186362=CARTESIAN_POINT('Ctrl Pts',(181.186964013846,-3.69531736762194,
135.427931095897));
#186363=CARTESIAN_POINT('Ctrl Pts',(181.194360698758,-3.81577910700978,
135.326280604586));
#186364=CARTESIAN_POINT('Ctrl Pts',(181.201757055694,-3.93623550499821,
135.224634620564));
#186365=CARTESIAN_POINT('Ctrl Pts',(181.209153412629,-4.0526350639138,135.118165867008));
#186366=CARTESIAN_POINT('Ctrl Pts',(181.216549769564,-4.16458033046145,
135.007240729303));
#186367=CARTESIAN_POINT('Ctrl Pts',(181.223947258901,-4.27654273611478,
134.896298608676));
#186368=CARTESIAN_POINT('Ctrl Pts',(181.231344748238,-4.38404922633616,
134.78089900815));
#186369=CARTESIAN_POINT('Ctrl Pts',(181.238742237574,-4.48673961136266,
134.661444778215));
#186370=CARTESIAN_POINT('Ctrl Pts',(181.246142320089,-4.58946599434432,
134.541948673785));
#186371=CARTESIAN_POINT('Ctrl Pts',(181.253542402604,-4.68737266758336,
134.418395392961));
#186372=CARTESIAN_POINT('Ctrl Pts',(181.260942485119,-4.78014018674565,
134.291220287464));
#186373=CARTESIAN_POINT('Ctrl Pts',(181.268350704786,-4.87300971333234,
134.163905339864));
#186374=CARTESIAN_POINT('Ctrl Pts',(181.275758924452,-4.96072858024092,
134.032960915913));
#186375=CARTESIAN_POINT('Ctrl Pts',(181.283167144119,-5.04302069557768,
133.898851339232));
#186376=CARTESIAN_POINT('Ctrl Pts',(181.290579923421,-5.12536346033855,
133.764659220344));
#186377=CARTESIAN_POINT('Ctrl Pts',(181.297992702723,-5.20227263606082,
133.627298391857));
#186378=CARTESIAN_POINT('Ctrl Pts',(181.305405482025,-5.27351870270403,
133.487256637678));
#186379=CARTESIAN_POINT('Ctrl Pts',(181.312828853054,-5.34486656906833,
133.347014785273));
#186380=CARTESIAN_POINT('Ctrl Pts',(181.320252224083,-5.4105350099472,133.204084694854));
#186381=CARTESIAN_POINT('Ctrl Pts',(181.327675595111,-5.47034281196722,
133.058973684604));
#186382=CARTESIAN_POINT('Ctrl Pts',(181.331611644552,-5.50205434366603,
132.982032345081));
#186383=CARTESIAN_POINT('Ctrl Pts',(181.335547693993,-5.53211907170173,
132.904478128601));
#186384=CARTESIAN_POINT('Ctrl Pts',(181.339483743433,-5.56051574565194,
132.826388116107));
#186385=CARTESIAN_POINT('Ctrl Pts',(181.348080014218,-5.622533640077,132.655840742883));
#186386=CARTESIAN_POINT('Ctrl Pts',(181.356676285003,-5.67674712583689,
132.482312359138));
#186387=CARTESIAN_POINT('Ctrl Pts',(181.365272555788,-5.7229002646624,132.306473503879));
#186388=CARTESIAN_POINT('Ctrl Pts',(181.373836240798,-5.76887845136683,
132.13130119875));
#186389=CARTESIAN_POINT('Ctrl Pts',(181.382399925807,-5.8068571937891,131.953836020863));
#186390=CARTESIAN_POINT('Ctrl Pts',(181.390963610817,-5.83663002103799,
131.774762884679));
#186391=CARTESIAN_POINT('Ctrl Pts',(181.399463586485,-5.86618135400975,
131.597021959055));
#186392=CARTESIAN_POINT('Ctrl Pts',(181.407963562153,-5.88764834009424,
131.417697041437));
#186393=CARTESIAN_POINT('Ctrl Pts',(181.416463537821,-5.90087621830845,
131.237477713398));
#186394=CARTESIAN_POINT('Ctrl Pts',(181.423183949748,-5.91133469418984,
131.094989291209));
#186395=CARTESIAN_POINT('Ctrl Pts',(181.429904361675,-5.91664371146173,
130.95194217167));
#186396=CARTESIAN_POINT('Ctrl Pts',(181.436624773602,-5.91674841954496,
130.808685234569));
#186397=CARTESIAN_POINT('',(183.186624807795,-5.9097261727316,130.800419732287));
#186398=CARTESIAN_POINT('Ctrl Pts',(181.436624807795,-5.91046065331948,
130.808679910655));
#186399=CARTESIAN_POINT('Ctrl Pts',(181.497060327612,-5.90180348691877,
129.521756724088));
#186400=CARTESIAN_POINT('Ctrl Pts',(181.650311722033,-4.85487069311502,
126.24557662955));
#186401=CARTESIAN_POINT('Ctrl Pts',(181.89637899106,0.558585749835051,123.828291345372));
#186402=CARTESIAN_POINT('Ctrl Pts',(182.174826614872,6.17109389324245,127.503578787286));
#186403=CARTESIAN_POINT('Ctrl Pts',(182.453274238685,6.11266822346165,134.212123479067));
#186404=CARTESIAN_POINT('Ctrl Pts',(182.731721862497,0.436999076760051,
137.789100579601));
#186405=CARTESIAN_POINT('Ctrl Pts',(182.976172052201,-4.89824093256168,
135.294398866638));
#186406=CARTESIAN_POINT('Ctrl Pts',(183.1278063673,-5.90209859011289,132.053299422131));
#186407=CARTESIAN_POINT('Ctrl Pts',(183.186624807795,-5.9097261727316,130.800419732287));
#186408=CARTESIAN_POINT('',(184.936624807795,-5.92486718842363,130.801517542038));
#186409=CARTESIAN_POINT('Ctrl Pts',(183.186624807795,-5.9097261727316,130.800419732287));
#186410=CARTESIAN_POINT('Ctrl Pts',(183.220622241905,-5.91413496418055,
130.076247273033));
#186411=CARTESIAN_POINT('Ctrl Pts',(183.347435550617,-5.4548282023846,127.380421002293));
#186412=CARTESIAN_POINT('Ctrl Pts',(183.567064733937,-1.42373941229825,
123.952315184543));
#186413=CARTESIAN_POINT('Ctrl Pts',(183.845512357749,4.99525395369783,125.90283040054));
#186414=CARTESIAN_POINT('Ctrl Pts',(184.123959981563,6.82385296796736,132.357612432922));
#186415=CARTESIAN_POINT('Ctrl Pts',(184.402407605375,2.38166446842562,137.385031927559));
#186416=CARTESIAN_POINT('Ctrl Pts',(184.673295880787,-4.06914253102304,
136.392824298985));
#186417=CARTESIAN_POINT('Ctrl Pts',(184.851368281593,-5.91419482002716,
132.605670887374));
#186418=CARTESIAN_POINT('Ctrl Pts',(184.936624807795,-5.92486718842363,
130.801517542038));
#186419=CARTESIAN_POINT('',(186.686624807795,-5.91810304431807,130.809680029163));
#186420=CARTESIAN_POINT('Ctrl Pts',(184.936624807795,-5.92486718842363,
130.801517542038));
#186421=CARTESIAN_POINT('Ctrl Pts',(184.944184156197,-5.92581346379487,
130.641550624367));
#186422=CARTESIAN_POINT('Ctrl Pts',(185.044559379204,-5.84727879099301,
128.518407035367));
#186423=CARTESIAN_POINT('Ctrl Pts',(185.237750476814,-3.29138665363019,
124.628250642296));
#186424=CARTESIAN_POINT('Ctrl Pts',(185.516198100626,3.4170613558443,124.696885507443));
#186425=CARTESIAN_POINT('Ctrl Pts',(185.794645724439,6.98539691202545,130.377991632052));
#186426=CARTESIAN_POINT('Ctrl Pts',(186.073093348252,4.13449396166582,136.450910025061));
#186427=CARTESIAN_POINT('Ctrl Pts',(186.351540972065,-2.5158069582057,137.334925361857));
#186428=CARTESIAN_POINT('Ctrl Pts',(186.55605145858,-5.7022149293107,133.576472626177));
#186429=CARTESIAN_POINT('Ctrl Pts',(186.667746070489,-5.92222955506447,
131.210299569289));
#186430=CARTESIAN_POINT('Ctrl Pts',(186.686624807795,-5.91851213263273,
130.809680396867));
#186431=CARTESIAN_POINT('',(188.436624807759,-5.91674998742092,130.804746434304));
#186432=CARTESIAN_POINT('Ctrl Pts',(186.686624807795,-5.91674760990531,
130.809678810848));
#186433=CARTESIAN_POINT('Ctrl Pts',(186.693927872074,-5.91688686513407,
130.654750624113));
#186434=CARTESIAN_POINT('Ctrl Pts',(186.701230936354,-5.91093684901184,
130.499626658566));
#186435=CARTESIAN_POINT('Ctrl Pts',(186.708534000633,-5.89887823475046,
130.344832452937));
#186436=CARTESIAN_POINT('Ctrl Pts',(186.71583126983,-5.88682918916652,130.190161078655));
#186437=CARTESIAN_POINT('Ctrl Pts',(186.723128539027,-5.86868122137412,
130.035819325382));
#186438=CARTESIAN_POINT('Ctrl Pts',(186.730425808224,-5.84446706708341,
129.882332817401));
#186439=CARTESIAN_POINT('Ctrl Pts',(186.737842908702,-5.81985528279573,
129.726325848082));
#186440=CARTESIAN_POINT('Ctrl Pts',(186.745260009179,-5.78897632400346,
129.57120286325));
#186441=CARTESIAN_POINT('Ctrl Pts',(186.752677109657,-5.75191958714079,
129.417511085149));
#186442=CARTESIAN_POINT('Ctrl Pts',(186.759968840886,-5.71548921030546,
129.266417117715));
#186443=CARTESIAN_POINT('Ctrl Pts',(186.767260572116,-5.67308835349849,
129.116706741788));
#186444=CARTESIAN_POINT('Ctrl Pts',(186.774552303345,-5.62485348468246,
128.968889604895));
#186445=CARTESIAN_POINT('Ctrl Pts',(186.781843715033,-5.57662072963386,
128.821078945703));
#186446=CARTESIAN_POINT('Ctrl Pts',(186.789135126721,-5.52255459037707,
128.675161726577));
#186447=CARTESIAN_POINT('Ctrl Pts',(186.796426538409,-5.46284118724312,
128.531631701602));
#186448=CARTESIAN_POINT('Ctrl Pts',(186.803719166403,-5.40311782310642,
128.388077733878));
#186449=CARTESIAN_POINT('Ctrl Pts',(186.811011794397,-5.33774546886925,
128.246912107963));
#186450=CARTESIAN_POINT('Ctrl Pts',(186.818304422391,-5.26695796755661,
128.108607600227));
#186451=CARTESIAN_POINT('Ctrl Pts',(186.8258154055,-5.19405095418979,127.966161993203));
#186452=CARTESIAN_POINT('Ctrl Pts',(186.833326388608,-5.11539964036747,
127.826751909787));
#186453=CARTESIAN_POINT('Ctrl Pts',(186.840837371716,-5.03130930734334,
127.690864637748));
#186454=CARTESIAN_POINT('Ctrl Pts',(186.84814077682,-4.949542944875,127.558732827339));
#186455=CARTESIAN_POINT('Ctrl Pts',(186.855444181923,-4.86263449198645,
127.429931967507));
#186456=CARTESIAN_POINT('Ctrl Pts',(186.862747587026,-4.77090702822886,
127.30487827149));
#186457=CARTESIAN_POINT('Ctrl Pts',(186.870362359137,-4.6752689357269,127.174493145188));
#186458=CARTESIAN_POINT('Ctrl Pts',(186.877977131248,-4.57439219292684,
127.048182094909));
#186459=CARTESIAN_POINT('Ctrl Pts',(186.885591903359,-4.46868683856503,
126.926375509119));
#186460=CARTESIAN_POINT('Ctrl Pts',(186.89320667547,-4.3629814842032,126.80456892333));
#186461=CARTESIAN_POINT('Ctrl Pts',(186.900821447581,-4.25244789244555,
126.687267089292));
#186462=CARTESIAN_POINT('Ctrl Pts',(186.908436219692,-4.13753558760197,
126.574853574916));
#186463=CARTESIAN_POINT('Ctrl Pts',(186.915859486097,-4.02551323950221,
126.465267174611));
#186464=CARTESIAN_POINT('Ctrl Pts',(186.923282752503,-3.9089647500179,126.359968661986));
#186465=CARTESIAN_POINT('Ctrl Pts',(186.930706018908,-3.78825199071475,
126.259354851085));
#186466=CARTESIAN_POINT('Ctrl Pts',(186.938120511629,-3.66768190386831,
126.158859957352));
#186467=CARTESIAN_POINT('Ctrl Pts',(186.94553500435,-3.54295762806711,126.063038980729));
#186468=CARTESIAN_POINT('Ctrl Pts',(186.952949497071,-3.4144784567078,125.972252647831));
#186469=CARTESIAN_POINT('Ctrl Pts',(186.960356843425,-3.28612311841112,
125.881553818218));
#186470=CARTESIAN_POINT('Ctrl Pts',(186.967764189779,-3.15402039231062,
125.795880185779));
#186471=CARTESIAN_POINT('Ctrl Pts',(186.975171536132,-3.01860320296358,
125.715552774313));
#186472=CARTESIAN_POINT('Ctrl Pts',(186.982573357808,-2.88328701286552,
125.63528527406));
#186473=CARTESIAN_POINT('Ctrl Pts',(186.989975179483,-2.74466160138934,
125.560356244931));
#186474=CARTESIAN_POINT('Ctrl Pts',(186.997377001159,-2.60318938208514,
125.491043800031));
#186475=CARTESIAN_POINT('Ctrl Pts',(187.00477491547,-2.46179184486368,125.421767944631));
#186476=CARTESIAN_POINT('Ctrl Pts',(187.012172829781,-2.3175508271054,125.358102932441));
#186477=CARTESIAN_POINT('Ctrl Pts',(187.019570744093,-2.17095378175324,
125.300281199535));
#186478=CARTESIAN_POINT('Ctrl Pts',(187.026967429005,-2.02438109817091,
125.242469075553));
#186479=CARTESIAN_POINT('Ctrl Pts',(187.034364113917,-1.87545351098578,
125.190498440448));
#186480=CARTESIAN_POINT('Ctrl Pts',(187.041760798829,-1.72467902321808,
125.144553833817));
#186481=CARTESIAN_POINT('Ctrl Pts',(187.049157155765,-1.573911220949,125.098611264417));
#186482=CARTESIAN_POINT('Ctrl Pts',(187.0565535127,-1.42129703801589,125.058694301019));
#186483=CARTESIAN_POINT('Ctrl Pts',(187.063949869636,-1.2673599706079,125.024937699367));
#186484=CARTESIAN_POINT('Ctrl Pts',(187.071347358972,-1.11339933504184,
124.991175929494));
#186485=CARTESIAN_POINT('Ctrl Pts',(187.078744848309,-0.958115776379954,
124.963576479304));
#186486=CARTESIAN_POINT('Ctrl Pts',(187.086142337645,-0.802043172628662,
124.942223011561));
#186487=CARTESIAN_POINT('Ctrl Pts',(187.09354242016,-0.645915857868791,
124.920862058393));
#186488=CARTESIAN_POINT('Ctrl Pts',(187.100942502675,-0.488999316935465,
124.905751497561));
#186489=CARTESIAN_POINT('Ctrl Pts',(187.10834258519,-0.331832590309043,
124.896923127883));
#186490=CARTESIAN_POINT('Ctrl Pts',(187.115750804857,-0.174493042708975,
124.888085050506));
#186491=CARTESIAN_POINT('Ctrl Pts',(187.123159024523,-0.016903132952331,
124.885542980791));
#186492=CARTESIAN_POINT('Ctrl Pts',(187.13056724419,0.140397315335382,124.889276581278));
#186493=CARTESIAN_POINT('Ctrl Pts',(187.137980023492,0.297794579424681,
124.893012479734));
#186494=CARTESIAN_POINT('Ctrl Pts',(187.145392802794,0.454901655364147,
124.903031721345));
#186495=CARTESIAN_POINT('Ctrl Pts',(187.152805582096,0.611184312778971,
124.919262122357));
#186496=CARTESIAN_POINT('Ctrl Pts',(187.160228953124,0.767690274183362,
124.935515714127));
#186497=CARTESIAN_POINT('Ctrl Pts',(187.167652324153,0.923369095910833,
124.957998137041));
#186498=CARTESIAN_POINT('Ctrl Pts',(187.175075695182,1.07769637957054,124.986586036512));
#186499=CARTESIAN_POINT('Ctrl Pts',(187.179011744623,1.15952440839869,125.001744026769));
#186500=CARTESIAN_POINT('Ctrl Pts',(187.182947794064,1.24097270681647,125.01861764673));
#186501=CARTESIAN_POINT('Ctrl Pts',(187.186883843504,1.32196501082129,125.037182878614));
#186502=CARTESIAN_POINT('Ctrl Pts',(187.19430710991,1.47471396849223,125.072196326546));
#186503=CARTESIAN_POINT('Ctrl Pts',(187.201730376315,1.62630189479336,125.113335453442));
#186504=CARTESIAN_POINT('Ctrl Pts',(187.209153642721,1.77619933841254,125.160510294185));
#186505=CARTESIAN_POINT('Ctrl Pts',(187.216568135442,1.92591961570148,125.207629378185));
#186506=CARTESIAN_POINT('Ctrl Pts',(187.223982628163,2.07395303475566,125.260769865369));
#186507=CARTESIAN_POINT('Ctrl Pts',(187.231397120884,2.21978027822349,125.319790800442));
#186508=CARTESIAN_POINT('Ctrl Pts',(187.238804467237,2.36546696790406,125.378754848915));
#186509=CARTESIAN_POINT('Ctrl Pts',(187.246211813591,2.50895137152433,125.443587922699));
#186510=CARTESIAN_POINT('Ctrl Pts',(187.253619159945,2.64972939637269,125.514099311307));
#186511=CARTESIAN_POINT('Ctrl Pts',(187.26102098162,2.79040242365833,125.584558109861));
#186512=CARTESIAN_POINT('Ctrl Pts',(187.268422803296,2.92837275898145,125.660686624124));
#186513=CARTESIAN_POINT('Ctrl Pts',(187.275824624971,3.0631564720913,125.742246139407));
#186514=CARTESIAN_POINT('Ctrl Pts',(187.283222539282,3.19786903392806,125.823762600057));
#186515=CARTESIAN_POINT('Ctrl Pts',(187.290620453594,3.3293980051506,125.910704159221));
#186516=CARTESIAN_POINT('Ctrl Pts',(187.298018367905,3.45728435048477,126.002786346309));
#186517=CARTESIAN_POINT('Ctrl Pts',(187.305415052817,3.58514944342875,126.094853231009));
#186518=CARTESIAN_POINT('Ctrl Pts',(187.31281173773,3.70937280925888,126.192058830229));
#186519=CARTESIAN_POINT('Ctrl Pts',(187.320208422642,3.82952460154685,126.2940754948));
#186520=CARTESIAN_POINT('Ctrl Pts',(187.327604779577,3.94967106617857,126.396087635844));
#186521=CARTESIAN_POINT('Ctrl Pts',(187.335001136513,4.06574603167699,126.502910176461));
#186522=CARTESIAN_POINT('Ctrl Pts',(187.342397493448,4.17735316173905,126.614175523252));
#186523=CARTESIAN_POINT('Ctrl Pts',(187.349794982785,4.28897737913757,126.725457905052));
#186524=CARTESIAN_POINT('Ctrl Pts',(187.357192472121,4.39613213470813,126.841184183831));
#186525=CARTESIAN_POINT('Ctrl Pts',(187.364589961458,4.4984584664945,126.96095041467));
#186526=CARTESIAN_POINT('Ctrl Pts',(187.371990043973,4.6008206686173,127.080758629375));
#186527=CARTESIAN_POINT('Ctrl Pts',(187.379390126488,4.69835083467273,127.204609332144));
#186528=CARTESIAN_POINT('Ctrl Pts',(187.386790209003,4.79073084686722,127.332066200991));
#186529=CARTESIAN_POINT('Ctrl Pts',(187.394198428669,4.88321244038255,127.45966322177));
#186530=CARTESIAN_POINT('Ctrl Pts',(187.401606648336,4.97053235119977,127.590874025252));
#186531=CARTESIAN_POINT('Ctrl Pts',(187.409014868002,5.05241590194538,127.725233449638));
#186532=CARTESIAN_POINT('Ctrl Pts',(187.416427647304,5.13434985065019,127.859675570009));
#186533=CARTESIAN_POINT('Ctrl Pts',(187.423840426606,5.21084059102242,127.997269847324));
#186534=CARTESIAN_POINT('Ctrl Pts',(187.431253205909,5.28166008873117,128.137527801358));
#186535=CARTESIAN_POINT('Ctrl Pts',(187.438676576937,5.35258077665936,128.277986162534));
#186536=CARTESIAN_POINT('Ctrl Pts',(187.446099947966,5.41781388333707,128.421115463055));
#186537=CARTESIAN_POINT('Ctrl Pts',(187.453523318995,5.47717974033229,128.566407835537));
#186538=CARTESIAN_POINT('Ctrl Pts',(187.457459368436,5.50865694217581,128.64344533767));
#186539=CARTESIAN_POINT('Ctrl Pts',(187.461395417877,5.53848548259736,128.721090701616));
#186540=CARTESIAN_POINT('Ctrl Pts',(187.465331467317,5.56664434588085,128.799266782113));
#186541=CARTESIAN_POINT('Ctrl Pts',(187.472754733723,5.61975108322465,128.946704430135));
#186542=CARTESIAN_POINT('Ctrl Pts',(187.480178000128,5.66707654755361,129.096476348691));
#186543=CARTESIAN_POINT('Ctrl Pts',(187.487601266534,5.70841024769987,129.248088467055));
#186544=CARTESIAN_POINT('Ctrl Pts',(187.495015759255,5.74969509484514,129.399521392486));
#186545=CARTESIAN_POINT('Ctrl Pts',(187.502430251976,5.78500217687627,129.552789831813));
#186546=CARTESIAN_POINT('Ctrl Pts',(187.509844744697,5.81416937976279,129.707380678858));
#186547=CARTESIAN_POINT('Ctrl Pts',(187.517252091051,5.84330847020106,129.861822525424));
#186548=CARTESIAN_POINT('Ctrl Pts',(187.524659437404,5.86631939401667,130.017583877895));
#186549=CARTESIAN_POINT('Ctrl Pts',(187.532066783758,5.88309012691937,130.17413754512));
#186550=CARTESIAN_POINT('Ctrl Pts',(187.539468605433,5.89984835157674,130.330574448713));
#186551=CARTESIAN_POINT('Ctrl Pts',(187.546870427109,5.91037561281063,130.487802120845));
#186552=CARTESIAN_POINT('Ctrl Pts',(187.554272248784,5.91461117192879,130.64528438617));
#186553=CARTESIAN_POINT('Ctrl Pts',(187.561670163096,5.91884449512825,130.802683517833));
#186554=CARTESIAN_POINT('Ctrl Pts',(187.569068077407,5.91679272080989,130.960336602811));
#186555=CARTESIAN_POINT('Ctrl Pts',(187.576465991718,5.90844706236015,131.117703678424));
#186556=CARTESIAN_POINT('Ctrl Pts',(187.583862676631,5.90010279080743,131.275044602484));
#186557=CARTESIAN_POINT('Ctrl Pts',(187.591259361543,5.88546673073356,131.432099239102));
#186558=CARTESIAN_POINT('Ctrl Pts',(187.598656046455,5.86458220017064,131.588328843926));
#186559=CARTESIAN_POINT('Ctrl Pts',(187.60605240339,5.84369859564966,131.744551521365));
#186560=CARTESIAN_POINT('Ctrl Pts',(187.613448760326,5.81656712099775,131.899948869742));
#186561=CARTESIAN_POINT('Ctrl Pts',(187.620845117261,5.78328281349836,132.053988746889));
#186562=CARTESIAN_POINT('Ctrl Pts',(187.628242606598,5.74999341008647,132.208052207934));
#186563=CARTESIAN_POINT('Ctrl Pts',(187.635640095934,5.71054937699733,132.360757419028));
#186564=CARTESIAN_POINT('Ctrl Pts',(187.643037585271,5.66509653682644,132.511584033214));
#186565=CARTESIAN_POINT('Ctrl Pts',(187.650437667786,5.61962776323287,132.662463519436));
#186566=CARTESIAN_POINT('Ctrl Pts',(187.657837750301,5.56814609641887,132.811462740405));
#186567=CARTESIAN_POINT('Ctrl Pts',(187.665237832816,5.51084667598898,132.958078211923));
#186568=CARTESIAN_POINT('Ctrl Pts',(187.672646052482,5.45348424895594,133.104854902223));
#186569=CARTESIAN_POINT('Ctrl Pts',(187.680054272149,5.39029142860743,133.249242260506));
#186570=CARTESIAN_POINT('Ctrl Pts',(187.687462491815,5.3215110989095,133.390757761603));
#186571=CARTESIAN_POINT('Ctrl Pts',(187.694875271117,5.2526884360661,133.53236036313));
#186572=CARTESIAN_POINT('Ctrl Pts',(187.702288050419,5.17827158724947,133.671087257152));
#186573=CARTESIAN_POINT('Ctrl Pts',(187.709700829722,5.09854826658263,133.806482556433));
#186574=CARTESIAN_POINT('Ctrl Pts',(187.71712420075,5.01871103349667,133.942071314867));
#186575=CARTESIAN_POINT('Ctrl Pts',(187.724547571779,4.93355238690208,134.074318658072));
#186576=CARTESIAN_POINT('Ctrl Pts',(187.731970942808,4.84340249483737,134.20279891118));
#186577=CARTESIAN_POINT('Ctrl Pts',(187.735906992249,4.79560285894802,134.270922224219));
#186578=CARTESIAN_POINT('Ctrl Pts',(187.739843041689,4.74640066993037,134.337987035869));
#186579=CARTESIAN_POINT('Ctrl Pts',(187.74377909113,4.69584947277127,134.403933966114));
#186580=CARTESIAN_POINT('Ctrl Pts',(187.751202357536,4.6005114925774,134.528307818423));
#186581=CARTESIAN_POINT('Ctrl Pts',(187.758625623941,4.50008470519337,134.649079452252));
#186582=CARTESIAN_POINT('Ctrl Pts',(187.766048890346,4.39487101069584,134.765804718124));
#186583=CARTESIAN_POINT('Ctrl Pts',(187.773463383067,4.28978167004782,134.882392024425));
#186584=CARTESIAN_POINT('Ctrl Pts',(187.780877875788,4.17991693151612,134.994942207732));
#186585=CARTESIAN_POINT('Ctrl Pts',(187.788292368509,4.06562085926568,135.103041530498));
#186586=CARTESIAN_POINT('Ctrl Pts',(187.795699714863,3.95143494987295,135.211036663066));
#186587=CARTESIAN_POINT('Ctrl Pts',(187.803107061217,3.83282647904385,135.314589220668));
#186588=CARTESIAN_POINT('Ctrl Pts',(187.810514407571,3.71017843575953,135.413319994402));
#186589=CARTESIAN_POINT('Ctrl Pts',(187.817916229246,3.58762186801298,135.511977131));
#186590=CARTESIAN_POINT('Ctrl Pts',(187.825318050921,3.4610320163687,135.60581941131));
#186591=CARTESIAN_POINT('Ctrl Pts',(187.832719872597,3.33082714958386,135.69450591828));
#186592=CARTESIAN_POINT('Ctrl Pts',(187.840117786908,3.20069101693379,135.783145608334));
#186593=CARTESIAN_POINT('Ctrl Pts',(187.847515701219,3.06694397743706,135.866634735812));
#186594=CARTESIAN_POINT('Ctrl Pts',(187.854913615531,2.93003556760929,135.944674045271));
#186595=CARTESIAN_POINT('Ctrl Pts',(187.862310300443,2.79314990947657,136.022700386012));
#186596=CARTESIAN_POINT('Ctrl Pts',(187.869706985355,2.65310424769539,136.095278521522));
#186597=CARTESIAN_POINT('Ctrl Pts',(187.877103670267,2.51037525760295,136.162153692006));
#186598=CARTESIAN_POINT('Ctrl Pts',(187.884500027203,2.36765259626331,136.229025897175));
#186599=CARTESIAN_POINT('Ctrl Pts',(187.891896384138,2.22224718122004,136.290195481735));
#186600=CARTESIAN_POINT('Ctrl Pts',(187.899292741074,2.0746580887224,136.345454767407));
#186601=CARTESIAN_POINT('Ctrl Pts',(187.90669023041,1.92704639995784,136.400722513416));
#186602=CARTESIAN_POINT('Ctrl Pts',(187.914087719747,1.77725071766979,136.450078027893));
#186603=CARTESIAN_POINT('Ctrl Pts',(187.921485209083,1.62578764516406,136.493362735278));
#186604=CARTESIAN_POINT('Ctrl Pts',(187.928885291598,1.47427147751353,136.53666261605));
#186605=CARTESIAN_POINT('Ctrl Pts',(187.936285374113,1.32108711461301,136.573887350165));
#186606=CARTESIAN_POINT('Ctrl Pts',(187.943685456628,1.16676362970169,136.60492896859));
#186607=CARTESIAN_POINT('Ctrl Pts',(187.951093676295,1.01227045025355,136.636004720467));
#186608=CARTESIAN_POINT('Ctrl Pts',(187.958501895961,0.856636013498965,
136.660883705003));
#186609=CARTESIAN_POINT('Ctrl Pts',(187.965910115627,0.700397566244245,
136.679509450719));
#186610=CARTESIAN_POINT('Ctrl Pts',(187.973322894929,0.544062956832329,
136.698146660271));
#186611=CARTESIAN_POINT('Ctrl Pts',(187.980735674231,0.387123967424787,
136.710522932578));
#186612=CARTESIAN_POINT('Ctrl Pts',(187.988148453534,0.23011966537511,136.716633911495));
#186613=CARTESIAN_POINT('Ctrl Pts',(187.995571824562,0.072891028215697,
136.722753622065));
#186614=CARTESIAN_POINT('Ctrl Pts',(188.002995195591,-0.0844027356615752,
136.72259016019));
#186615=CARTESIAN_POINT('Ctrl Pts',(188.01041856662,-0.241225030045429,
136.716191217928));
#186616=CARTESIAN_POINT('Ctrl Pts',(188.014354616061,-0.324375973428068,
136.7127983452));
#186617=CARTESIAN_POINT('Ctrl Pts',(188.018290665501,-0.407394483839031,
136.707653318947));
#186618=CARTESIAN_POINT('Ctrl Pts',(188.022226714942,-0.490201660815617,
136.700769091733));
#186619=CARTESIAN_POINT('Ctrl Pts',(188.029649981348,-0.646373412268205,
136.687785654058));
#186620=CARTESIAN_POINT('Ctrl Pts',(188.037073247753,-0.80226513988054,
136.668573771693));
#186621=CARTESIAN_POINT('Ctrl Pts',(188.044496514159,-0.957339983753277,
136.643147368083));
#186622=CARTESIAN_POINT('Ctrl Pts',(188.051911006879,-1.11223154203839,
136.61775101637));
#186623=CARTESIAN_POINT('Ctrl Pts',(188.0593254996,-1.26630777361279,136.58615482358));
#186624=CARTESIAN_POINT('Ctrl Pts',(188.066739992321,-1.41903461427524,
136.548424625391));
#186625=CARTESIAN_POINT('Ctrl Pts',(188.074147338675,-1.57161425105952,
136.510730792987));
#186626=CARTESIAN_POINT('Ctrl Pts',(188.081554685029,-1.72284672618799,
136.466914814107));
#186627=CARTESIAN_POINT('Ctrl Pts',(188.088962031383,-1.87220598557174,
136.417093936555));
#186628=CARTESIAN_POINT('Ctrl Pts',(188.096363853058,-2.02145384718316,
136.367310217293));
#186629=CARTESIAN_POINT('Ctrl Pts',(188.103765674734,-2.16883092230147,
136.311530634628));
#186630=CARTESIAN_POINT('Ctrl Pts',(188.111167496409,-2.31382430327432,
136.249922815914));
#186631=CARTESIAN_POINT('Ctrl Pts',(188.11856541072,-2.45874114337115,136.188347519488));
#186632=CARTESIAN_POINT('Ctrl Pts',(188.125963325032,-2.60127645265397,
136.120950259984));
#186633=CARTESIAN_POINT('Ctrl Pts',(188.133361239343,-2.7409354735747,136.047947490328));
#186634=CARTESIAN_POINT('Ctrl Pts',(188.140757924255,-2.88057128569987,
135.974956852407));
#186635=CARTESIAN_POINT('Ctrl Pts',(188.148154609167,-3.01733142762264,
135.896362725914));
#186636=CARTESIAN_POINT('Ctrl Pts',(188.15555129408,-3.1507439080487,135.812428447418));
#186637=CARTESIAN_POINT('Ctrl Pts',(188.162947651015,-3.28415047282601,
135.728497890655));
#186638=CARTESIAN_POINT('Ctrl Pts',(188.170344007951,-3.41420935528581,
135.639227851488));
#186639=CARTESIAN_POINT('Ctrl Pts',(188.177740364886,-3.54047606690486,
135.544925961718));
#186640=CARTESIAN_POINT('Ctrl Pts',(188.185137854223,-3.66676211027926,
135.450609634088));
#186641=CARTESIAN_POINT('Ctrl Pts',(188.192535343559,-3.78925452766934,
135.351260145295));
#186642=CARTESIAN_POINT('Ctrl Pts',(188.199932832896,-3.90754066825958,
135.247226414368));
#186643=CARTESIAN_POINT('Ctrl Pts',(188.207332915411,-4.02586827387267,
135.143156214579));
#186644=CARTESIAN_POINT('Ctrl Pts',(188.214732997926,-4.13998638682651,
135.034398749718));
#186645=CARTESIAN_POINT('Ctrl Pts',(188.222133080441,-4.24951819270741,
134.921340784187));
#186646=CARTESIAN_POINT('Ctrl Pts',(188.229541300107,-4.35917044006939,
134.808158499799));
#186647=CARTESIAN_POINT('Ctrl Pts',(188.236949519774,-4.4642260490177,134.690666539206));
#186648=CARTESIAN_POINT('Ctrl Pts',(188.24435773944,-4.56434711347478,134.569286379147));
#186649=CARTESIAN_POINT('Ctrl Pts',(188.251770518742,-4.66452980077634,
134.447831511624));
#186650=CARTESIAN_POINT('Ctrl Pts',(188.259183298044,-4.75977166640558,
134.322483972582));
#186651=CARTESIAN_POINT('Ctrl Pts',(188.266596077347,-4.84977766634151,
134.193694940048));
#186652=CARTESIAN_POINT('Ctrl Pts',(188.274019448375,-4.93991227107106,
134.064721887705));
#186653=CARTESIAN_POINT('Ctrl Pts',(188.281442819404,-5.02479586745561,
133.932297834228));
#186654=CARTESIAN_POINT('Ctrl Pts',(188.288866190433,-5.10417853681512,
133.796900011929));
#186655=CARTESIAN_POINT('Ctrl Pts',(188.292802239874,-5.14626913287155,
133.725108837719));
#186656=CARTESIAN_POINT('Ctrl Pts',(188.296738289315,-5.18681400928749,
133.652482001339));
#186657=CARTESIAN_POINT('Ctrl Pts',(188.300674338755,-5.22578141579513,
133.579092885161));
#186658=CARTESIAN_POINT('Ctrl Pts',(188.308522635262,-5.30348058216972,
133.432758457005));
#186659=CARTESIAN_POINT('Ctrl Pts',(188.316370931769,-5.37511838685106,
133.282990724991));
#186660=CARTESIAN_POINT('Ctrl Pts',(188.324219228275,-5.44039662476336,
133.130304539453));
#186661=CARTESIAN_POINT('Ctrl Pts',(188.332053990155,-5.50556228836188,
132.977881665902));
#186662=CARTESIAN_POINT('Ctrl Pts',(188.339888752035,-5.56439012663925,
132.822550655319));
#186663=CARTESIAN_POINT('Ctrl Pts',(188.347723513915,-5.61662765213832,
132.664850977588));
#186664=CARTESIAN_POINT('Ctrl Pts',(188.355539641514,-5.6687409353559,132.507526374433));
#186665=CARTESIAN_POINT('Ctrl Pts',(188.363355769114,-5.71429507358988,
132.347844634376));
#186666=CARTESIAN_POINT('Ctrl Pts',(188.371171896713,-5.75308575484795,
132.1863645466));
#186667=CARTESIAN_POINT('Ctrl Pts',(188.378976980979,-5.7918216291147,132.025112612533));
#186668=CARTESIAN_POINT('Ctrl Pts',(188.386782065244,-5.82381301965768,
131.862067694374));
#186669=CARTESIAN_POINT('Ctrl Pts',(188.39458714951,-5.8489048080885,131.697805136503));
#186670=CARTESIAN_POINT('Ctrl Pts',(188.402376866656,-5.87394719429565,
131.533865988645));
#186671=CARTESIAN_POINT('Ctrl Pts',(188.410166583802,-5.89211702687552,
131.368714288067));
#186672=CARTESIAN_POINT('Ctrl Pts',(188.417956300948,-5.90330990566078,
131.20293648265));
#186673=CARTESIAN_POINT('Ctrl Pts',(188.424179136552,-5.91225136570458,
131.070504455847));
#186674=CARTESIAN_POINT('Ctrl Pts',(188.430401972156,-5.91674131959235,
130.937673208914));
#186675=CARTESIAN_POINT('Ctrl Pts',(188.436624807759,-5.91674998742092,
130.804746434304));
#186676=CARTESIAN_POINT('',(190.186624807795,-5.9167474892903,130.798909885783));
#186677=CARTESIAN_POINT('Ctrl Pts',(188.436624807795,-5.91674998742097,
130.80474643354));
#186678=CARTESIAN_POINT('Ctrl Pts',(188.444336312247,-5.91676072880488,
130.640020016287));
#186679=CARTESIAN_POINT('Ctrl Pts',(188.452047816698,-5.9098880006331,130.475412038668));
#186680=CARTESIAN_POINT('Ctrl Pts',(188.45975932115,-5.89618734660479,130.311506342716));
#186681=CARTESIAN_POINT('Ctrl Pts',(188.467479281045,-5.88247167020258,
130.147420928874));
#186682=CARTESIAN_POINT('Ctrl Pts',(188.47519924094,-5.86191315565751,129.984039656638));
#186683=CARTESIAN_POINT('Ctrl Pts',(188.482919200835,-5.83461887000143,
129.821938506494));
#186684=CARTESIAN_POINT('Ctrl Pts',(188.490936097646,-5.80627474974523,
129.65360237375));
#186685=CARTESIAN_POINT('Ctrl Pts',(188.498952994457,-5.77066650315088,
129.486647185334));
#186686=CARTESIAN_POINT('Ctrl Pts',(188.506969891268,-5.72797103557548,
129.321701392353));
#186687=CARTESIAN_POINT('Ctrl Pts',(188.514715160958,-5.6867221685032,129.162344264416));
#186688=CARTESIAN_POINT('Ctrl Pts',(188.522460430647,-5.63885863849107,
129.004862872487));
#186689=CARTESIAN_POINT('Ctrl Pts',(188.530205700337,-5.5845895056426,128.849804244379));
#186690=CARTESIAN_POINT('Ctrl Pts',(188.538358410709,-5.52746553966337,
128.686588741718));
#186691=CARTESIAN_POINT('Ctrl Pts',(188.546511121081,-5.46324405110737,
128.526058178221));
#186692=CARTESIAN_POINT('Ctrl Pts',(188.554663831453,-5.39222426567471,
128.368822067026));
#186693=CARTESIAN_POINT('Ctrl Pts',(188.562816541824,-5.32120448024206,
128.21158595583));
#186694=CARTESIAN_POINT('Ctrl Pts',(188.570969252196,-5.24338665044448,
128.057644630733));
#186695=CARTESIAN_POINT('Ctrl Pts',(188.579121962568,-5.15912334327355,
127.907573277876));
#186696=CARTESIAN_POINT('Ctrl Pts',(188.586545228974,-5.08239929092767,
127.770929194955));
#186697=CARTESIAN_POINT('Ctrl Pts',(188.593968495379,-5.00012675873199,
127.637128755464));
#186698=CARTESIAN_POINT('Ctrl Pts',(188.601391761784,-4.91254156507233,
127.506654455104));
#186699=CARTESIAN_POINT('Ctrl Pts',(188.608806254505,-4.82505988983811,
127.376334364533));
#186700=CARTESIAN_POINT('Ctrl Pts',(188.616220747226,-4.73227825779838,
127.249332894892));
#186701=CARTESIAN_POINT('Ctrl Pts',(188.623635239947,-4.6344785403192,127.126108420962));
#186702=CARTESIAN_POINT('Ctrl Pts',(188.631042586301,-4.53677308588965,
127.00300271542));
#186703=CARTESIAN_POINT('Ctrl Pts',(188.638449932655,-4.43405940528752,
126.883667048682));
#186704=CARTESIAN_POINT('Ctrl Pts',(188.645857279009,-4.32666280054533,
126.76853113989));
#186705=CARTESIAN_POINT('Ctrl Pts',(188.653259100684,-4.21934629624284,
126.653481103803));
#186706=CARTESIAN_POINT('Ctrl Pts',(188.66066092236,-4.10735407577181,126.542624860554));
#186707=CARTESIAN_POINT('Ctrl Pts',(188.668062744035,-3.99105179769123,
126.436359231274));
#186708=CARTESIAN_POINT('Ctrl Pts',(188.675460658346,-3.87481091467824,
126.330149698793));
#186709=CARTESIAN_POINT('Ctrl Pts',(188.682858572658,-3.75426478020397,
126.22852620523));
#186710=CARTESIAN_POINT('Ctrl Pts',(188.690256486969,-3.62981591611858,
126.131848768722));
#186711=CARTESIAN_POINT('Ctrl Pts',(188.697653171881,-3.50538773317637,
126.035187398249));
#186712=CARTESIAN_POINT('Ctrl Pts',(188.705049856793,-3.3770584023365,125.943470682302));
#186713=CARTESIAN_POINT('Ctrl Pts',(188.712446541706,-3.24526362374814,
125.857018444755));
#186714=CARTESIAN_POINT('Ctrl Pts',(188.719842898641,-3.11347468907845,
125.77057004059));
#186715=CARTESIAN_POINT('Ctrl Pts',(188.727239255577,-2.97822092432744,
125.689385855431));
#186716=CARTESIAN_POINT('Ctrl Pts',(188.734635612512,-2.83996688492409,
125.613742286863));
#186717=CARTESIAN_POINT('Ctrl Pts',(188.742033101849,-2.70169167847449,
125.53808713707));
#186718=CARTESIAN_POINT('Ctrl Pts',(188.749430591185,-2.56041561025224,
125.467974472102));
#186719=CARTESIAN_POINT('Ctrl Pts',(188.756828080522,-2.41662755324927,
125.403634570878));
#186720=CARTESIAN_POINT('Ctrl Pts',(188.764228163037,-2.27278909156605,
125.339272115401));
#186721=CARTESIAN_POINT('Ctrl Pts',(188.771628245552,-2.1264372284147,125.280686605083));
#186722=CARTESIAN_POINT('Ctrl Pts',(188.779028328067,-1.97808036179923,
125.228059993966));
#186723=CARTESIAN_POINT('Ctrl Pts',(188.786436547733,-1.82956036155703,
125.175375514479));
#186724=CARTESIAN_POINT('Ctrl Pts',(188.7938447674,-1.67903130693944,125.128663144689));
#186725=CARTESIAN_POINT('Ctrl Pts',(188.801252987066,-1.52701699451342,
125.088055022082));
#186726=CARTESIAN_POINT('Ctrl Pts',(188.808665766368,-1.37490911981405,
125.047421905852));
#186727=CARTESIAN_POINT('Ctrl Pts',(188.81607854567,-1.22131452911263,125.012900604892));
#186728=CARTESIAN_POINT('Ctrl Pts',(188.823491324972,-1.06676621647483,
124.984571927082));
#186729=CARTESIAN_POINT('Ctrl Pts',(188.830914696001,-0.911997077960795,
124.956202771929));
#186730=CARTESIAN_POINT('Ctrl Pts',(188.83833806703,-0.75627186444372,124.934043964435));
#186731=CARTESIAN_POINT('Ctrl Pts',(188.845761438059,-0.600128509702636,
124.918124440318));
#186732=CARTESIAN_POINT('Ctrl Pts',(188.8496974875,-0.517337556408728,124.909683526647));
#186733=CARTESIAN_POINT('Ctrl Pts',(188.853633536941,-0.434429058316661,
124.90299582822));
#186734=CARTESIAN_POINT('Ctrl Pts',(188.857569586381,-0.3514829554707,124.898059719837));
#186735=CARTESIAN_POINT('Ctrl Pts',(188.864992852787,-0.195049194165717,
124.888750373478));
#186736=CARTESIAN_POINT('Ctrl Pts',(188.872416119192,-0.0380087817261698,
124.885646179091));
#186737=CARTESIAN_POINT('Ctrl Pts',(188.879839385598,0.1191048789509,124.888809536702));
#186738=CARTESIAN_POINT('Ctrl Pts',(188.887253878319,0.276032844328527,
124.891969155487));
#186739=CARTESIAN_POINT('Ctrl Pts',(188.89466837104,0.433033516041292,124.90138157371));
#186740=CARTESIAN_POINT('Ctrl Pts',(188.902082863761,0.589568892045253,
124.917057407774));
#186741=CARTESIAN_POINT('Ctrl Pts',(188.909490210115,0.745953393360701,
124.932718132878));
#186742=CARTESIAN_POINT('Ctrl Pts',(188.916897556468,0.901873122835364,
124.954630218564));
#186743=CARTESIAN_POINT('Ctrl Pts',(188.924304902822,1.05679071189202,124.98275225271));
#186744=CARTESIAN_POINT('Ctrl Pts',(188.931706724498,1.21159275756575,125.010853312383));
#186745=CARTESIAN_POINT('Ctrl Pts',(188.939108546173,1.36539378534926,125.045155031959));
#186746=CARTESIAN_POINT('Ctrl Pts',(188.946510367848,1.51766229100495,125.085564264052));
#186747=CARTESIAN_POINT('Ctrl Pts',(188.95390828216,1.66985041530155,125.125952164426));
#186748=CARTESIAN_POINT('Ctrl Pts',(188.961306196471,1.8205072687502,125.17244106084));
#186749=CARTESIAN_POINT('Ctrl Pts',(188.968704110782,1.96911238500255,125.22488689886));
#186750=CARTESIAN_POINT('Ctrl Pts',(188.976100795695,2.11769280578066,125.277324021333));
#186751=CARTESIAN_POINT('Ctrl Pts',(188.983497480607,2.26422181439622,125.33571599657));
#186752=CARTESIAN_POINT('Ctrl Pts',(188.990894165519,2.40819482739287,125.39986913031));
#186753=CARTESIAN_POINT('Ctrl Pts',(188.998290522454,2.55216145647515,125.464019419434));
#186754=CARTESIAN_POINT('Ctrl Pts',(189.00568687939,2.69357197430951,125.533930207192));
#186755=CARTESIAN_POINT('Ctrl Pts',(189.013083236325,2.83194273622357,125.609360049592));
#186756=CARTESIAN_POINT('Ctrl Pts',(189.020480725662,2.97033468305507,125.684801440493));
#186757=CARTESIAN_POINT('Ctrl Pts',(189.027878214998,3.10568561952156,125.765763389823));
#186758=CARTESIAN_POINT('Ctrl Pts',(189.035275704335,3.23753755765109,125.851959066268));
#186759=CARTESIAN_POINT('Ctrl Pts',(189.04267578685,3.36943571627262,125.938184958474));
#186760=CARTESIAN_POINT('Ctrl Pts',(189.050075869365,3.49783212220785,126.029648026486));
#186761=CARTESIAN_POINT('Ctrl Pts',(189.05747595188,3.62229889082746,126.126018891269));
#186762=CARTESIAN_POINT('Ctrl Pts',(189.064884171547,3.74690252345494,126.222495725726));
#186763=CARTESIAN_POINT('Ctrl Pts',(189.072292391213,3.86756759402008,126.323890905695));
#186764=CARTESIAN_POINT('Ctrl Pts',(189.079700610879,3.98389980667395,126.429835169831));
#186765=CARTESIAN_POINT('Ctrl Pts',(189.087113390182,4.10030361986379,126.535844640893));
#186766=CARTESIAN_POINT('Ctrl Pts',(189.094526169484,4.21236899608596,126.646408513676));
#186767=CARTESIAN_POINT('Ctrl Pts',(189.101938948786,4.31973985307035,126.761122043812));
#186768=CARTESIAN_POINT('Ctrl Pts',(189.109362319814,4.42726412657015,126.875999482018));
#186769=CARTESIAN_POINT('Ctrl Pts',(189.116785690843,4.53008024059027,126.995038137808));
#186770=CARTESIAN_POINT('Ctrl Pts',(189.124209061872,4.627873084345,127.11780107272));
#186771=CARTESIAN_POINT('Ctrl Pts',(189.128145111313,4.6797251966109,127.182892926467));
#186772=CARTESIAN_POINT('Ctrl Pts',(189.132081160754,4.73016581507376,127.249031329645));
#186773=CARTESIAN_POINT('Ctrl Pts',(189.136017210194,4.77915309751256,127.316148147971));
#186774=CARTESIAN_POINT('Ctrl Pts',(189.1434404766,4.87154158335144,127.442728372691));
#186775=CARTESIAN_POINT('Ctrl Pts',(189.150863743005,4.95903740885353,127.573173026402));
#186776=CARTESIAN_POINT('Ctrl Pts',(189.158287009411,5.04129975781475,127.707067070878));
#186777=CARTESIAN_POINT('Ctrl Pts',(189.165701502132,5.12346487951111,127.840802863713));
#186778=CARTESIAN_POINT('Ctrl Pts',(189.173115994853,5.20040864350211,127.977979617276));
#186779=CARTESIAN_POINT('Ctrl Pts',(189.180530487574,5.27183131466145,128.118150433635));
#186780=CARTESIAN_POINT('Ctrl Pts',(189.187937833927,5.34318514596105,128.258186148084));
#186781=CARTESIAN_POINT('Ctrl Pts',(189.195345180281,5.40902831002284,128.401209849912));
#186782=CARTESIAN_POINT('Ctrl Pts',(189.202752526635,5.46910518719545,128.546747051454));
#186783=CARTESIAN_POINT('Ctrl Pts',(189.21015434831,5.52913725676648,128.692175705861));
#186784=CARTESIAN_POINT('Ctrl Pts',(189.217556169986,5.58341146092722,128.840113783703));
#186785=CARTESIAN_POINT('Ctrl Pts',(189.224957991661,5.6317188761904,128.990063766976));
#186786=CARTESIAN_POINT('Ctrl Pts',(189.232355905972,5.68000079034474,129.139934592819));
#186787=CARTESIAN_POINT('Ctrl Pts',(189.239753820284,5.72232207444452,129.291814854514));
#186788=CARTESIAN_POINT('Ctrl Pts',(189.247151734595,5.75852260079111,129.445188804042));
#186789=CARTESIAN_POINT('Ctrl Pts',(189.254548419507,5.79471711126733,129.598537265604));
#186790=CARTESIAN_POINT('Ctrl Pts',(189.26194510442,5.82479279708112,129.753378559388));
#186791=CARTESIAN_POINT('Ctrl Pts',(189.269341789332,5.84863987901503,129.909183468564));
#186792=CARTESIAN_POINT('Ctrl Pts',(189.276738146267,5.8724859035443,130.064981469187));
#186793=CARTESIAN_POINT('Ctrl Pts',(189.284134503203,5.89010381686027,130.221742631245));
#186794=CARTESIAN_POINT('Ctrl Pts',(189.291530860138,5.90143533087373,130.3789295444));
#186795=CARTESIAN_POINT('Ctrl Pts',(189.298928349475,5.91276857977092,130.536140523273));
#186796=CARTESIAN_POINT('Ctrl Pts',(189.306325838811,5.9178134861293,130.693777010678));
#186797=CARTESIAN_POINT('Ctrl Pts',(189.313723328148,5.91656381556915,130.851298649032));
#186798=CARTESIAN_POINT('Ctrl Pts',(189.321123410663,5.91531370693891,131.008875506353));
#186799=CARTESIAN_POINT('Ctrl Pts',(189.328523493178,5.90776463111646,131.166337061412));
#186800=CARTESIAN_POINT('Ctrl Pts',(189.335923575693,5.89396242191814,131.323145285339));
#186801=CARTESIAN_POINT('Ctrl Pts',(189.343331795359,5.88014503577195,131.480125936029));
#186802=CARTESIAN_POINT('Ctrl Pts',(189.350740015026,5.86006081725151,131.636451448796));
#186803=CARTESIAN_POINT('Ctrl Pts',(189.358148234692,5.83380730984865,131.791590496599));
#186804=CARTESIAN_POINT('Ctrl Pts',(189.365561013994,5.80753764385015,131.946825029897));
#186805=CARTESIAN_POINT('Ctrl Pts',(189.372973793296,5.77509119954317,132.100871278681));
#186806=CARTESIAN_POINT('Ctrl Pts',(189.380386572599,5.7366160286638,132.253210886634));
#186807=CARTESIAN_POINT('Ctrl Pts',(189.387809943627,5.69808588265588,132.405768164563));
#186808=CARTESIAN_POINT('Ctrl Pts',(189.395233314656,5.65350991124101,132.556613574327));
#186809=CARTESIAN_POINT('Ctrl Pts',(189.402656685685,5.60308539804483,132.705245828387));
#186810=CARTESIAN_POINT('Ctrl Pts',(189.406592735126,5.57634911122828,132.784054215872));
#186811=CARTESIAN_POINT('Ctrl Pts',(189.410528784567,5.54796938585717,132.862240759177));
#186812=CARTESIAN_POINT('Ctrl Pts',(189.414464834007,5.51798092849068,132.93973342701));
#186813=CARTESIAN_POINT('Ctrl Pts',(189.421888100413,5.46142363380593,133.085882180079));
#186814=CARTESIAN_POINT('Ctrl Pts',(189.429311366818,5.39897048314281,133.230003417703));
#186815=CARTESIAN_POINT('Ctrl Pts',(189.436734633224,5.33078644043194,133.371586063258));
#186816=CARTESIAN_POINT('Ctrl Pts',(189.444149125945,5.26268298559709,133.513001369884));
#186817=CARTESIAN_POINT('Ctrl Pts',(189.451563618666,5.18886228167012,133.651883723719));
#186818=CARTESIAN_POINT('Ctrl Pts',(189.458978111387,5.10953830238054,133.787739389865));
#186819=CARTESIAN_POINT('Ctrl Pts',(189.466385457741,5.03029077852894,133.923464113205));
#186820=CARTESIAN_POINT('Ctrl Pts',(189.473792804094,4.94555072602297,134.056167636292));
#186821=CARTESIAN_POINT('Ctrl Pts',(189.481200150448,4.85557917610903,134.1853784269));
#186822=CARTESIAN_POINT('Ctrl Pts',(189.488601972123,4.76567473037149,134.314492847226));
#186823=CARTESIAN_POINT('Ctrl Pts',(189.496003793799,4.67054676872829,134.440119416974));
#186824=CARTESIAN_POINT('Ctrl Pts',(189.503405615474,4.57050093892078,134.561813442263));
#186825=CARTESIAN_POINT('Ctrl Pts',(189.510803529786,4.470507922528,134.683443226223));
#186826=CARTESIAN_POINT('Ctrl Pts',(189.518201444097,4.36560244470111,134.801144312466));
#186827=CARTESIAN_POINT('Ctrl Pts',(189.525599358408,4.25613186592361,134.914503206622));
#186828=CARTESIAN_POINT('Ctrl Pts',(189.53299604332,4.1466794791702,135.027843262585));
#186829=CARTESIAN_POINT('Ctrl Pts',(189.540392728233,4.03266375619807,135.136842290347));
#186830=CARTESIAN_POINT('Ctrl Pts',(189.547789413145,3.9144706037665,135.241121874919));
#186831=CARTESIAN_POINT('Ctrl Pts',(189.55518577008,3.79628269214324,135.345396835624));
#186832=CARTESIAN_POINT('Ctrl Pts',(189.562582127016,3.67391799928616,135.444952522259));
#186833=CARTESIAN_POINT('Ctrl Pts',(189.569978483951,3.5477971575957,135.539449411987));
#186834=CARTESIAN_POINT('Ctrl Pts',(189.577375973288,3.42165700648274,135.633960769431));
#186835=CARTESIAN_POINT('Ctrl Pts',(189.584773462624,3.2917598602477,135.723411563957));
#186836=CARTESIAN_POINT('Ctrl Pts',(189.592170951961,3.15855696719353,135.807504473932));
#186837=CARTESIAN_POINT('Ctrl Pts',(189.599571034476,3.02530738007121,135.891626862547));
#186838=CARTESIAN_POINT('Ctrl Pts',(189.606971116991,2.88875005437881,135.970387427978));
#186839=CARTESIAN_POINT('Ctrl Pts',(189.614371199506,2.74936242334025,136.043533913767));
#186840=CARTESIAN_POINT('Ctrl Pts',(189.621779419172,2.6098215212719,136.116760831637));
#186841=CARTESIAN_POINT('Ctrl Pts',(189.629187638839,2.46744442931756,136.184361167894));
#186842=CARTESIAN_POINT('Ctrl Pts',(189.636595858505,2.3227308926061,136.246129793398));
#186843=CARTESIAN_POINT('Ctrl Pts',(189.644008637807,2.17792828712777,136.307936436459));
#186844=CARTESIAN_POINT('Ctrl Pts',(189.651421417109,2.03078671951321,136.363904084189));
#186845=CARTESIAN_POINT('Ctrl Pts',(189.658834196411,1.88182232319197,136.413877112455));
#186846=CARTESIAN_POINT('Ctrl Pts',(189.66625756744,1.73264507955527,136.463921544528));
#186847=CARTESIAN_POINT('Ctrl Pts',(189.673680938469,1.58164016277834,136.507954145901));
#186848=CARTESIAN_POINT('Ctrl Pts',(189.681104309498,1.42933595688406,136.545869938717));
#186849=CARTESIAN_POINT('Ctrl Pts',(189.685040358939,1.3485806124279,136.565973801845));
#186850=CARTESIAN_POINT('Ctrl Pts',(189.688976408379,1.26746012441086,136.584358871603));
#186851=CARTESIAN_POINT('Ctrl Pts',(189.69291245782,1.18605385454001,136.601015412931));
#186852=CARTESIAN_POINT('Ctrl Pts',(189.700335724226,1.03252417016951,136.632429130043));
#186853=CARTESIAN_POINT('Ctrl Pts',(189.707758990631,0.877513437794605,
136.657786574917));
#186854=CARTESIAN_POINT('Ctrl Pts',(189.715182257037,0.721540807687306,
136.676950286983));
#186855=CARTESIAN_POINT('Ctrl Pts',(189.722596749758,0.56575252427599,136.696091349132));
#186856=CARTESIAN_POINT('Ctrl Pts',(189.730011242479,0.409004972998288,
136.709053204846));
#186857=CARTESIAN_POINT('Ctrl Pts',(189.7374257352,0.251829205035335,136.715749000509));
#186858=CARTESIAN_POINT('Ctrl Pts',(189.744833081553,0.0948049289951359,
136.722438342512));
#186859=CARTESIAN_POINT('Ctrl Pts',(189.752240427907,-0.0626463716075346,
136.722873632068));
#186860=CARTESIAN_POINT('Ctrl Pts',(189.759647774261,-0.219986889591926,
136.717019607471));
#186861=CARTESIAN_POINT('Ctrl Pts',(189.767049595936,-0.377210057081186,
136.711169949027));
#186862=CARTESIAN_POINT('Ctrl Pts',(189.774451417612,-0.534322235037135,
136.699040330281));
#186863=CARTESIAN_POINT('Ctrl Pts',(189.781853239287,-0.690784079832339,
136.68064753343));
#186864=CARTESIAN_POINT('Ctrl Pts',(189.789251153599,-0.847163329639719,
136.662264445992));
#186865=CARTESIAN_POINT('Ctrl Pts',(189.79664906791,-1.00289256018978,136.637624808542));
#186866=CARTESIAN_POINT('Ctrl Pts',(189.804046982221,-1.15743613013174,
136.606797361484));
#186867=CARTESIAN_POINT('Ctrl Pts',(189.811443667134,-1.31195401773457,
136.575975037388));
#186868=CARTESIAN_POINT('Ctrl Pts',(189.818840352046,-1.4652862700588,136.538967017513));
#186869=CARTESIAN_POINT('Ctrl Pts',(189.826237036958,-1.61690592382758,
136.4958934336));
#186870=CARTESIAN_POINT('Ctrl Pts',(189.833633393893,-1.76851885462208,
136.452821759614));
#186871=CARTESIAN_POINT('Ctrl Pts',(189.841029750829,-1.91841897876412,
136.403685158374));
#186872=CARTESIAN_POINT('Ctrl Pts',(189.848426107764,-2.0660932839906,136.348653999445));
#186873=CARTESIAN_POINT('Ctrl Pts',(189.855823597101,-2.21379019853027,
136.293614415105));
#186874=CARTESIAN_POINT('Ctrl Pts',(189.863221086437,-2.35926026579751,
136.232678606497));
#186875=CARTESIAN_POINT('Ctrl Pts',(189.870618575774,-2.50200942995244,
136.166065511994));
#186876=CARTESIAN_POINT('Ctrl Pts',(189.878018658289,-2.64480863460694,
136.099429066372));
#186877=CARTESIAN_POINT('Ctrl Pts',(189.885418740804,-2.78488469905547,
136.027111530211));
#186878=CARTESIAN_POINT('Ctrl Pts',(189.892818823319,-2.92176732847544,
135.949378230826));
#186879=CARTESIAN_POINT('Ctrl Pts',(189.900227042986,-3.05880047441704,
135.871559455687));
#186880=CARTESIAN_POINT('Ctrl Pts',(189.907635262652,-3.19263284780672,
135.788313208874));
#186881=CARTESIAN_POINT('Ctrl Pts',(189.915043482319,-3.32282174323811,
135.699949062806));
#186882=CARTESIAN_POINT('Ctrl Pts',(189.922456261621,-3.45309076776235,
135.611530530079));
#186883=CARTESIAN_POINT('Ctrl Pts',(189.929869040923,-3.579711546312,135.517988042663));
#186884=CARTESIAN_POINT('Ctrl Pts',(189.937281820225,-3.70227416517129,
135.419671719583));
#186885=CARTESIAN_POINT('Ctrl Pts',(189.944705191254,-3.82501190724813,
135.321214917531));
#186886=CARTESIAN_POINT('Ctrl Pts',(189.952128562282,-3.94367962786938,
135.217970900963));
#186887=CARTESIAN_POINT('Ctrl Pts',(189.959551933311,-4.05790340171897,
135.110327471226));
#186888=CARTESIAN_POINT('Ctrl Pts',(189.963487982752,-4.1184675873743,135.053252341912));
#186889=CARTESIAN_POINT('Ctrl Pts',(189.967424032192,-4.17778307250271,
134.994940957179));
#186890=CARTESIAN_POINT('Ctrl Pts',(189.971360081633,-4.23579876978104,
134.935454824241));
#186891=CARTESIAN_POINT('Ctrl Pts',(189.97868580183,-4.34377677455446,134.824740065172));
#186892=CARTESIAN_POINT('Ctrl Pts',(189.986011522027,-4.44759549208393,
134.709599597571));
#186893=CARTESIAN_POINT('Ctrl Pts',(189.993337242224,-4.54686303201109,
134.590383217952));
#186894=CARTESIAN_POINT('Ctrl Pts',(190.000654105557,-4.6460105565541,134.471310972051));
#186895=CARTESIAN_POINT('Ctrl Pts',(190.00797096889,-4.74061760854022,134.348172911224));
#186896=CARTESIAN_POINT('Ctrl Pts',(190.015287832222,-4.83032801012746,
134.221356648743));
#186897=CARTESIAN_POINT('Ctrl Pts',(190.022596306275,-4.91993555265535,
134.094685789707));
#186898=CARTESIAN_POINT('Ctrl Pts',(190.029904780328,-5.00465740532908,
133.964345439033));
#186899=CARTESIAN_POINT('Ctrl Pts',(190.037213254381,-5.08417700870137,
133.830756941033));
#186900=CARTESIAN_POINT('Ctrl Pts',(190.044516984866,-5.16364499985177,
133.697255148686));
#186901=CARTESIAN_POINT('Ctrl Pts',(190.051820715352,-5.23791726272298,
133.560509731128));
#186902=CARTESIAN_POINT('Ctrl Pts',(190.059124445837,-5.30671991172705,
133.420971849862));
#186903=CARTESIAN_POINT('Ctrl Pts',(190.06642496806,-5.3754923382356,133.281495262502));
#186904=CARTESIAN_POINT('Ctrl Pts',(190.073725490283,-5.43879976191837,
133.139228995741));
#186905=CARTESIAN_POINT('Ctrl Pts',(190.081026012506,-5.49641386784294,
132.994649446895));
#186906=CARTESIAN_POINT('Ctrl Pts',(190.088324859137,-5.55401475037018,
132.850103081465));
#186907=CARTESIAN_POINT('Ctrl Pts',(190.095623705769,-5.60592477449524,
132.703244847386));
#186908=CARTESIAN_POINT('Ctrl Pts',(190.1029225524,-5.65196358703582,132.554571511522));
#186909=CARTESIAN_POINT('Ctrl Pts',(190.110223624323,-5.69801643600718,
132.405852847751));
#186910=CARTESIAN_POINT('Ctrl Pts',(190.117524696245,-5.73819437761977,
132.255318341899));
#186911=CARTESIAN_POINT('Ctrl Pts',(190.124825768168,-5.77236675875697,
132.103480536934));
#186912=CARTESIAN_POINT('Ctrl Pts',(190.132127831751,-5.80654378132449,
131.951622108746));
#186913=CARTESIAN_POINT('Ctrl Pts',(190.139429895335,-5.83471354286302,
131.79846040554));
#186914=CARTESIAN_POINT('Ctrl Pts',(190.146731958918,-5.85679658929349,
131.644517908875));
#186915=CARTESIAN_POINT('Ctrl Pts',(190.154040273153,-5.87889853906686,
131.490443635655));
#186916=CARTESIAN_POINT('Ctrl Pts',(190.161348587387,-5.89490331910291,
131.33558761541));
#186917=CARTESIAN_POINT('Ctrl Pts',(190.168656901621,-5.90478335808391,
131.180477695875));
#186918=CARTESIAN_POINT('Ctrl Pts',(190.174646203679,-5.91288023732375,
131.053362176412));
#186919=CARTESIAN_POINT('Ctrl Pts',(190.180635505737,-5.91686463980822,
130.926076303123));
#186920=CARTESIAN_POINT('Ctrl Pts',(190.186624807795,-5.9167474892903,130.798909885783));
#186921=CARTESIAN_POINT('',(191.936624807795,-5.92167388468568,130.806439789968));
#186922=CARTESIAN_POINT('Ctrl Pts',(190.186624807795,-5.91709367293974,
130.798909566865));
#186923=CARTESIAN_POINT('Ctrl Pts',(190.207685773679,-5.92124324054971,
130.351707301601));
#186924=CARTESIAN_POINT('Ctrl Pts',(190.321562614164,-5.67042057656234,
127.938289561738));
#186925=CARTESIAN_POINT('Ctrl Pts',(190.52825532926,-2.36162413690314,124.216470821409));
#186926=CARTESIAN_POINT('Ctrl Pts',(190.80670295307,4.26606273237082,125.256543993538));
#186927=CARTESIAN_POINT('Ctrl Pts',(191.085150576885,6.97344635934664,131.394789617243));
#186928=CARTESIAN_POINT('Ctrl Pts',(191.363598200697,3.27257345387652,136.990459834304));
#186929=CARTESIAN_POINT('Ctrl Pts',(191.64204582451,-3.43563458160472,136.901407078928));
#186930=CARTESIAN_POINT('Ctrl Pts',(191.833054693543,-5.87156050063434,
132.996862586964));
#186931=CARTESIAN_POINT('Ctrl Pts',(191.931247687971,-5.92616743922034,
130.920188992212));
#186932=CARTESIAN_POINT('Ctrl Pts',(191.936624807795,-5.92565178765728,
130.806441186659));
#186933=CARTESIAN_POINT('',(193.686624807763,-5.91674833022066,130.808805764476));
#186934=CARTESIAN_POINT('Ctrl Pts',(191.936624807795,-5.91674963529206,
130.806438061004));
#186935=CARTESIAN_POINT('Ctrl Pts',(191.943982571507,-5.91680420246894,
130.651025731606));
#186936=CARTESIAN_POINT('Ctrl Pts',(191.95134033522,-5.91073134974623,130.495363673782));
#186937=CARTESIAN_POINT('Ctrl Pts',(191.958698098932,-5.89849824070525,
130.3399803134));
#186938=CARTESIAN_POINT('Ctrl Pts',(191.966047433817,-5.88627914553708,
130.184774955408));
#186939=CARTESIAN_POINT('Ctrl Pts',(191.973396768702,-5.86791386650228,
130.029848035039));
#186940=CARTESIAN_POINT('Ctrl Pts',(191.980746103587,-5.84342153691622,
129.875729741274));
#186941=CARTESIAN_POINT('Ctrl Pts',(191.988088691781,-5.81895169129261,
129.721752928126));
#186942=CARTESIAN_POINT('Ctrl Pts',(191.995431279975,-5.7883660488743,129.568583637425));
#186943=CARTESIAN_POINT('Ctrl Pts',(192.00277386817,-5.7517356631725,129.416748487506));
#186944=CARTESIAN_POINT('Ctrl Pts',(192.010111385737,-5.71513057359504,
129.265018191543));
#186945=CARTESIAN_POINT('Ctrl Pts',(192.017448903304,-5.67248913923677,
129.114620570674));
#186946=CARTESIAN_POINT('Ctrl Pts',(192.024786420871,-5.62393372693014,
128.966073371895));
#186947=CARTESIAN_POINT('Ctrl Pts',(192.032121243465,-5.57539614838435,
128.817580732537));
#186948=CARTESIAN_POINT('Ctrl Pts',(192.03945606606,-5.52094902955856,128.670937524576));
#186949=CARTESIAN_POINT('Ctrl Pts',(192.046790888654,-5.46076494507694,
128.52664755901));
#186950=CARTESIAN_POINT('Ctrl Pts',(192.054124432835,-5.40059135029389,
128.382382742256));
#186951=CARTESIAN_POINT('Ctrl Pts',(192.061457977017,-5.33468292520694,
128.240470702987));
#186952=CARTESIAN_POINT('Ctrl Pts',(192.068791521199,-5.2632607654466,128.101396193566));
#186953=CARTESIAN_POINT('Ctrl Pts',(192.076125297015,-5.19183634977695,
127.962317291398));
#186954=CARTESIAN_POINT('Ctrl Pts',(192.083459072831,-5.11489802642811,
127.826076435999));
#186955=CARTESIAN_POINT('Ctrl Pts',(192.090792848647,-5.03271319836429,
127.693134424325));
#186956=CARTESIAN_POINT('Ctrl Pts',(192.098128366077,-4.95050885317121,
127.560160841782));
#186957=CARTESIAN_POINT('Ctrl Pts',(192.105463883507,-4.86305572373874,
127.43048798552));
#186958=CARTESIAN_POINT('Ctrl Pts',(192.112799400937,-4.77066480062535,
127.304548062218));
#186959=CARTESIAN_POINT('Ctrl Pts',(192.120142509709,-4.67817826447584,
127.178477806865));
#186960=CARTESIAN_POINT('Ctrl Pts',(192.12748561848,-4.58074395310877,127.056148507902));
#186961=CARTESIAN_POINT('Ctrl Pts',(192.134828727252,-4.47871388483845,
126.937960159743));
#186962=CARTESIAN_POINT('Ctrl Pts',(192.142175724157,-4.37662979224858,
126.81970923155));
#186963=CARTESIAN_POINT('Ctrl Pts',(192.149522721062,-4.26994535451669,
126.705603899663));
#186964=CARTESIAN_POINT('Ctrl Pts',(192.156869717967,-4.15904929270293,
126.596007074508));
#186965=CARTESIAN_POINT('Ctrl Pts',(192.164227936362,-4.04798385296286,
126.486242855825));
#186966=CARTESIAN_POINT('Ctrl Pts',(192.171586154757,-3.93269421798494,
126.381001158029));
#186967=CARTESIAN_POINT('Ctrl Pts',(192.178944373152,-3.81360275633488,
126.280605034052));
#186968=CARTESIAN_POINT('Ctrl Pts',(192.18560993948,-3.70572174572714,126.189659510622));
#186969=CARTESIAN_POINT('Ctrl Pts',(192.192275505808,-3.59472154676677,
126.102689823874));
#186970=CARTESIAN_POINT('Ctrl Pts',(192.198941072137,-3.48093537284348,
126.019904588655));
#186971=CARTESIAN_POINT('Ctrl Pts',(192.206364338542,-3.35421469515357,
125.927708843354));
#186972=CARTESIAN_POINT('Ctrl Pts',(192.213787604947,-3.22363703874374,
125.840411633728));
#186973=CARTESIAN_POINT('Ctrl Pts',(192.221210871353,-3.08961796002339,
125.758353143969));
#186974=CARTESIAN_POINT('Ctrl Pts',(192.228625364074,-2.95575728072412,
125.676391640529));
#186975=CARTESIAN_POINT('Ctrl Pts',(192.236039856795,-2.8184635906989,125.599656725305));
#186976=CARTESIAN_POINT('Ctrl Pts',(192.243454349516,-2.67818424350777,
125.528447452973));
#186977=CARTESIAN_POINT('Ctrl Pts',(192.25086169587,-2.53804010283326,125.457306814819));
#186978=CARTESIAN_POINT('Ctrl Pts',(192.258269042224,-2.39491636453648,
125.39168138473));
#186979=CARTESIAN_POINT('Ctrl Pts',(192.265676388577,-2.24928790474382,
125.331826059971));
#186980=CARTESIAN_POINT('Ctrl Pts',(192.273078210253,-2.10376806015,125.272015377571));
#186981=CARTESIAN_POINT('Ctrl Pts',(192.280480031928,-1.95574755751648,
125.21796637283));
#186982=CARTESIAN_POINT('Ctrl Pts',(192.287881853604,-1.80572423221982,
125.169887211854));
#186983=CARTESIAN_POINT('Ctrl Pts',(192.295279767915,-1.65578010306985,
125.121833431494));
#186984=CARTESIAN_POINT('Ctrl Pts',(192.302677682226,-1.5038356114583,125.079743332305));
#186985=CARTESIAN_POINT('Ctrl Pts',(192.310075596538,-1.35040674849502,
125.04377625692));
#186986=CARTESIAN_POINT('Ctrl Pts',(192.31747228145,-1.19700338262484,125.007815158611));
#186987=CARTESIAN_POINT('Ctrl Pts',(192.324868966362,-1.04211649807024,
124.977975149715));
#186988=CARTESIAN_POINT('Ctrl Pts',(192.332265651274,-0.886275478114352,
124.954365203944));
#186989=CARTESIAN_POINT('Ctrl Pts',(192.33966200821,-0.73044136831249,124.930756305064));
#186990=CARTESIAN_POINT('Ctrl Pts',(192.347058365145,-0.573653576316578,
124.913376975953));
#186991=CARTESIAN_POINT('Ctrl Pts',(192.354454722081,-0.416449600545396,
124.902284686785));
#186992=CARTESIAN_POINT('Ctrl Pts',(192.361852211417,-0.259221556444396,
124.891190699359));
#186993=CARTESIAN_POINT('Ctrl Pts',(192.369249700754,-0.10157757409154,
124.886385694742));
#186994=CARTESIAN_POINT('Ctrl Pts',(192.37664719009,0.0559419800692496,
124.887875084974));
#186995=CARTESIAN_POINT('Ctrl Pts',(192.384047272605,0.213516752465648,
124.88936499731));
#186996=CARTESIAN_POINT('Ctrl Pts',(192.39144735512,0.370966636778287,124.897153694073));
#186997=CARTESIAN_POINT('Ctrl Pts',(192.398847437635,0.527753674510833,
124.911194522712));
#186998=CARTESIAN_POINT('Ctrl Pts',(192.406255657302,0.684713115709465,
124.925250790685));
#186999=CARTESIAN_POINT('Ctrl Pts',(192.413663876968,0.841007882692738,
124.945572886768));
#187000=CARTESIAN_POINT('Ctrl Pts',(192.421072096635,0.996106797477932,
124.972062458991));
#187001=CARTESIAN_POINT('Ctrl Pts',(192.428484875937,1.15130117305738,124.998568335104));
#187002=CARTESIAN_POINT('Ctrl Pts',(192.435897655239,1.30529786549359,125.031249174006));
#187003=CARTESIAN_POINT('Ctrl Pts',(192.443310434541,1.45757874437968,125.069956135283));
#187004=CARTESIAN_POINT('Ctrl Pts',(192.45073380557,1.61007720932673,125.108718402881));
#187005=CARTESIAN_POINT('Ctrl Pts',(192.458157176598,1.76085460737413,125.153523883713));
#187006=CARTESIAN_POINT('Ctrl Pts',(192.465580547627,1.90940995179483,125.204174531507));
#187007=CARTESIAN_POINT('Ctrl Pts',(192.469516597068,1.9881775599421,125.231030720313));
#187008=CARTESIAN_POINT('Ctrl Pts',(192.473452646509,2.06632082359468,125.259529399429));
#187009=CARTESIAN_POINT('Ctrl Pts',(192.477388695949,2.14376776436376,125.289635752718));
#187010=CARTESIAN_POINT('Ctrl Pts',(192.484811962355,2.28983027762013,125.346415395433));
#187011=CARTESIAN_POINT('Ctrl Pts',(192.49223522876,2.43385630529008,125.409087801767));
#187012=CARTESIAN_POINT('Ctrl Pts',(192.499658495166,2.57533502238865,125.477487230207));
#187013=CARTESIAN_POINT('Ctrl Pts',(192.507072987887,2.71664652339273,125.545805816202));
#187014=CARTESIAN_POINT('Ctrl Pts',(192.514487480608,2.85541637385971,125.619837789946));
#187015=CARTESIAN_POINT('Ctrl Pts',(192.521901973329,2.99115116509402,125.699368426577));
#187016=CARTESIAN_POINT('Ctrl Pts',(192.529309319682,3.1267551300262,125.778822408586));
#187017=CARTESIAN_POINT('Ctrl Pts',(192.536716666036,3.25932953951027,125.863764315137));
#187018=CARTESIAN_POINT('Ctrl Pts',(192.54412401239,3.38840325911156,125.953932397693));
#187019=CARTESIAN_POINT('Ctrl Pts',(192.551525834065,3.51738071066331,126.044033229491));
#187020=CARTESIAN_POINT('Ctrl Pts',(192.558927655741,3.64286236637453,126.139352263232));
#187021=CARTESIAN_POINT('Ctrl Pts',(192.566329477416,3.76440399802195,126.239583174779));
#187022=CARTESIAN_POINT('Ctrl Pts',(192.573727391728,3.88588146878789,126.339761175208));
#187023=CARTESIAN_POINT('Ctrl Pts',(192.581125306039,4.00342277045593,126.444845652573));
#187024=CARTESIAN_POINT('Ctrl Pts',(192.58852322035,4.11661493775789,126.554488617525));
#187025=CARTESIAN_POINT('Ctrl Pts',(192.595919905262,4.22978829457512,126.664113361806));
#187026=CARTESIAN_POINT('Ctrl Pts',(192.603316590175,4.33861368359645,126.778294830715));
#187027=CARTESIAN_POINT('Ctrl Pts',(192.610713275087,4.44271327755592,126.896646542057));
#187028=CARTESIAN_POINT('Ctrl Pts',(192.618109632022,4.54680825563025,127.01499300556));
#187029=CARTESIAN_POINT('Ctrl Pts',(192.625505988958,4.64617760874819,127.137509063529));
#187030=CARTESIAN_POINT('Ctrl Pts',(192.632902345893,4.74048245459971,127.263773567354));
#187031=CARTESIAN_POINT('Ctrl Pts',(192.64029983523,4.83480173876412,127.390057402596));
#187032=CARTESIAN_POINT('Ctrl Pts',(192.647697324566,4.92405474836339,127.520090527295));
#187033=CARTESIAN_POINT('Ctrl Pts',(192.655094813903,5.00794484883268,127.653421241197));
#187034=CARTESIAN_POINT('Ctrl Pts',(192.662494896418,5.09186435684631,127.786798693974));
#187035=CARTESIAN_POINT('Ctrl Pts',(192.669894978933,5.1704170140703,127.923475721708));
#187036=CARTESIAN_POINT('Ctrl Pts',(192.677295061448,5.24335129090999,128.062974507837));
#187037=CARTESIAN_POINT('Ctrl Pts',(192.684703281114,5.31636576648502,128.202626687223));
#187038=CARTESIAN_POINT('Ctrl Pts',(192.692111500781,5.38374935076555,128.345106490511));
#187039=CARTESIAN_POINT('Ctrl Pts',(192.699519720447,5.4452976753735,128.48991386098));
#187040=CARTESIAN_POINT('Ctrl Pts',(192.706932499749,5.50688388194844,128.634810357969));
#187041=CARTESIAN_POINT('Ctrl Pts',(192.714345279052,5.56262754045087,128.782036928429));
#187042=CARTESIAN_POINT('Ctrl Pts',(192.721758058354,5.61237381239609,128.931077202695));
#187043=CARTESIAN_POINT('Ctrl Pts',(192.729181429382,5.66219116414747,129.080330432694));
#187044=CARTESIAN_POINT('Ctrl Pts',(192.736604800411,5.70599391075369,129.231402184733));
#187045=CARTESIAN_POINT('Ctrl Pts',(192.74402817144,5.74367787858866,129.383763915644));
#187046=CARTESIAN_POINT('Ctrl Pts',(192.747964220881,5.76365882254902,129.464549761242));
#187047=CARTESIAN_POINT('Ctrl Pts',(192.751900270321,5.7819204194436,129.545698134267));
#187048=CARTESIAN_POINT('Ctrl Pts',(192.755836319762,5.79845305499836,129.627129658289));
#187049=CARTESIAN_POINT('Ctrl Pts',(192.763259586168,5.82963308968896,129.780706971204));
#187050=CARTESIAN_POINT('Ctrl Pts',(192.770682852573,5.85475460525286,129.935756113794));
#187051=CARTESIAN_POINT('Ctrl Pts',(192.778106118978,5.87368093133555,130.091757727195));
#187052=CARTESIAN_POINT('Ctrl Pts',(192.785520611699,5.89258488807253,130.247574959644));
#187053=CARTESIAN_POINT('Ctrl Pts',(192.79293510442,5.90530818568646,130.404342055148));
#187054=CARTESIAN_POINT('Ctrl Pts',(192.800349597141,5.91176477883311,130.561527830965));
#187055=CARTESIAN_POINT('Ctrl Pts',(192.807756943495,5.91821514887222,130.718562105214));
#187056=CARTESIAN_POINT('Ctrl Pts',(192.815164289849,5.91841082384763,130.876013885927));
#187057=CARTESIAN_POINT('Ctrl Pts',(192.822571636203,5.91231736054565,131.033345312885));
#187058=CARTESIAN_POINT('Ctrl Pts',(192.829973457878,5.90622844197851,131.190559396129));
#187059=CARTESIAN_POINT('Ctrl Pts',(192.837375279553,5.89385973928897,131.347652932937));
#187060=CARTESIAN_POINT('Ctrl Pts',(192.844777101229,5.8752288554425,131.504086605847));
#187061=CARTESIAN_POINT('Ctrl Pts',(192.85217501554,5.8566078066946,131.660437698638));
#187062=CARTESIAN_POINT('Ctrl Pts',(192.859572929851,5.83173120439777,131.816129251521));
#187063=CARTESIAN_POINT('Ctrl Pts',(192.866970844163,5.80066860403245,131.970625728376));
#187064=CARTESIAN_POINT('Ctrl Pts',(192.874367529075,5.76961116570776,132.125096530719));
#187065=CARTESIAN_POINT('Ctrl Pts',(192.881764213987,5.73236984310127,132.278372285581));
#187066=CARTESIAN_POINT('Ctrl Pts',(192.889160898899,5.6890655697637,132.429926213114));
#187067=CARTESIAN_POINT('Ctrl Pts',(192.896557255835,5.64576321658296,132.581473420587));
#187068=CARTESIAN_POINT('Ctrl Pts',(192.90395361277,5.5963985497707,132.731298593605));
#187069=CARTESIAN_POINT('Ctrl Pts',(192.911349969705,5.54114271941322,132.878888979771));
#187070=CARTESIAN_POINT('Ctrl Pts',(192.918747459042,5.48587842924699,133.026501962402));
#187071=CARTESIAN_POINT('Ctrl Pts',(192.926144948379,5.42472131052274,133.17187912729));
#187072=CARTESIAN_POINT('Ctrl Pts',(192.933542437715,5.35789105322837,133.314526752354));
#187073=CARTESIAN_POINT('Ctrl Pts',(192.94094252023,5.29103736869093,133.457224382321));
#187074=CARTESIAN_POINT('Ctrl Pts',(192.948342602745,5.21850674434839,133.597190229583));
#187075=CARTESIAN_POINT('Ctrl Pts',(192.95574268526,5.14056522291733,133.733954403645));
#187076=CARTESIAN_POINT('Ctrl Pts',(192.963150904926,5.06253799677085,133.870868963976));
#187077=CARTESIAN_POINT('Ctrl Pts',(192.970559124593,4.97908817626604,134.004574495774));
#187078=CARTESIAN_POINT('Ctrl Pts',(192.977967344259,4.89052600718495,134.13462876526));
#187079=CARTESIAN_POINT('Ctrl Pts',(192.985380123561,4.80190932956638,134.26476308098));
#187080=CARTESIAN_POINT('Ctrl Pts',(192.992792902864,4.70817425520031,134.391241357163));
#187081=CARTESIAN_POINT('Ctrl Pts',(193.000205682166,4.60967152652743,134.51365421339));
#187082=CARTESIAN_POINT('Ctrl Pts',(193.007629053194,4.51102805253667,134.636241978846));
#187083=CARTESIAN_POINT('Ctrl Pts',(193.015052424223,4.40760356345385,134.754752442234));
#187084=CARTESIAN_POINT('Ctrl Pts',(193.022475795252,4.29978642922707,134.868812268839));
#187085=CARTESIAN_POINT('Ctrl Pts',(193.026411844693,4.24261919762311,134.929289525733));
#187086=CARTESIAN_POINT('Ctrl Pts',(193.030347894133,4.18421761234096,134.988516202176));
#187087=CARTESIAN_POINT('Ctrl Pts',(193.034283943574,4.12464325826948,135.046441304506));
#187088=CARTESIAN_POINT('Ctrl Pts',(193.04170720998,4.01228788574312,135.155686239721));
#187089=CARTESIAN_POINT('Ctrl Pts',(193.049130476385,3.89541944365211,135.260629531099));
#187090=CARTESIAN_POINT('Ctrl Pts',(193.05655374279,3.77440100965145,135.360875467848));
#187091=CARTESIAN_POINT('Ctrl Pts',(193.063968235512,3.65352560938941,135.461002922225));
#187092=CARTESIAN_POINT('Ctrl Pts',(193.071382728233,3.52851026521044,135.55644383722));
#187093=CARTESIAN_POINT('Ctrl Pts',(193.078797220954,3.39975536658942,135.6468387032));
#187094=CARTESIAN_POINT('Ctrl Pts',(193.086204567307,3.27112456678774,135.737146443204));
#187095=CARTESIAN_POINT('Ctrl Pts',(193.093611913661,3.13876169151149,135.822417603552));
#187096=CARTESIAN_POINT('Ctrl Pts',(193.101019260015,3.0031006403987,135.902332479605));
#187097=CARTESIAN_POINT('Ctrl Pts',(193.10842108169,2.86754077041626,135.982187752127));
#187098=CARTESIAN_POINT('Ctrl Pts',(193.115822903366,2.72868794285352,136.056694506122));
#187099=CARTESIAN_POINT('Ctrl Pts',(193.123224725041,2.58700541559937,136.125576037201));
#187100=CARTESIAN_POINT('Ctrl Pts',(193.130622639352,2.44539768144717,136.194421206256));
#187101=CARTESIAN_POINT('Ctrl Pts',(193.138020553664,2.30096355740562,136.257646903513));
#187102=CARTESIAN_POINT('Ctrl Pts',(193.145418467975,2.15419120161526,136.315022177613));
#187103=CARTESIAN_POINT('Ctrl Pts',(193.152815152887,2.00744323672871,136.372387916984));
#187104=CARTESIAN_POINT('Ctrl Pts',(193.1602118378,1.85835815862988,136.423905027017));
#187105=CARTESIAN_POINT('Ctrl Pts',(193.167608522712,1.70744452966099,136.46939051516));
#187106=CARTESIAN_POINT('Ctrl Pts',(193.175004879647,1.55653759236051,136.514873986428));
#187107=CARTESIAN_POINT('Ctrl Pts',(193.182401236583,1.40380262282025,136.554326259858));
#187108=CARTESIAN_POINT('Ctrl Pts',(193.189797593518,1.24976352495471,136.58761417367));
#187109=CARTESIAN_POINT('Ctrl Pts',(193.197195082855,1.09570084331009,136.620907183947));
#187110=CARTESIAN_POINT('Ctrl Pts',(193.204592572191,0.94033400067869,136.648033876561));
#187111=CARTESIAN_POINT('Ctrl Pts',(193.211990061528,0.78419712723474,136.668912214077));
#187112=CARTESIAN_POINT('Ctrl Pts',(193.219390144043,0.628005520252473,
136.689797870461));
#187113=CARTESIAN_POINT('Ctrl Pts',(193.226790226558,0.471043714796622,
136.704430761329));
#187114=CARTESIAN_POINT('Ctrl Pts',(193.234190309073,0.313850845635412,
136.712780728661));
#187115=CARTESIAN_POINT('Ctrl Pts',(193.241598528739,0.156485126754066,
136.721139877641));
#187116=CARTESIAN_POINT('Ctrl Pts',(193.249006748406,-0.00111179024260466,
136.723202286104));
#187117=CARTESIAN_POINT('Ctrl Pts',(193.256414968072,-0.15840014612975,
136.718989934455));
#187118=CARTESIAN_POINT('Ctrl Pts',(193.263827747375,-0.315785310375573,
136.714774990174));
#187119=CARTESIAN_POINT('Ctrl Pts',(193.271240526677,-0.472861163480505,
136.704277615075));
#187120=CARTESIAN_POINT('Ctrl Pts',(193.278653305979,-0.629093697246785,
136.687571618591));
#187121=CARTESIAN_POINT('Ctrl Pts',(193.286076677007,-0.785549463383723,
136.670841751796));
#187122=CARTESIAN_POINT('Ctrl Pts',(193.293500048036,-0.941159135255626,
136.647885600237));
#187123=CARTESIAN_POINT('Ctrl Pts',(193.300923419065,-1.09539869234955,
136.618828114018));
#187124=CARTESIAN_POINT('Ctrl Pts',(193.304859468506,-1.17718020644852,
136.6034211376));
#187125=CARTESIAN_POINT('Ctrl Pts',(193.308795517947,-1.25857677010934,
136.586299695192));
#187126=CARTESIAN_POINT('Ctrl Pts',(193.312731567387,-1.33951219278451,
136.567488036588));
#187127=CARTESIAN_POINT('Ctrl Pts',(193.320154833793,-1.49215387404138,
136.532009835551));
#187128=CARTESIAN_POINT('Ctrl Pts',(193.327578100198,-1.64361588484665,
136.490409517706));
#187129=CARTESIAN_POINT('Ctrl Pts',(193.335001366604,-1.79336905016339,
136.442778659217));
#187130=CARTESIAN_POINT('Ctrl Pts',(193.342415859325,-1.94294521967514,
136.395204096447));
#187131=CARTESIAN_POINT('Ctrl Pts',(193.349830352046,-2.0908162116855,136.3416132926));
#187132=CARTESIAN_POINT('Ctrl Pts',(193.357244844767,-2.23646314026778,
136.282148782941));
#187133=CARTESIAN_POINT('Ctrl Pts',(193.364652191121,-2.38196968885627,
136.222741587416));
#187134=CARTESIAN_POINT('Ctrl Pts',(193.372059537474,-2.52525609829113,
136.157472096766));
#187135=CARTESIAN_POINT('Ctrl Pts',(193.379466883828,-2.66581885865279,
136.08653255488));
#187136=CARTESIAN_POINT('Ctrl Pts',(193.386868705504,-2.80627678200372,
136.015645922381));
#187137=CARTESIAN_POINT('Ctrl Pts',(193.394270527179,-2.94401476924652,
135.9390978265));
#187138=CARTESIAN_POINT('Ctrl Pts',(193.401672348854,-3.07854961893739,
135.857128453737));
#187139=CARTESIAN_POINT('Ctrl Pts',(193.409070263166,-3.21301344872921,
135.775202351967));
#187140=CARTESIAN_POINT('Ctrl Pts',(193.416468177477,-3.34427719051927,
135.687860866565));
#187141=CARTESIAN_POINT('Ctrl Pts',(193.423866091788,-3.47188267699022,
135.595389863951));
#187142=CARTESIAN_POINT('Ctrl Pts',(193.4312627767,-3.59946695774474,135.502934228339));
#187143=CARTESIAN_POINT('Ctrl Pts',(193.438659461613,-3.72339388777422,
135.405350986174));
#187144=CARTESIAN_POINT('Ctrl Pts',(193.446056146525,-3.84323461989282,
135.302969093412));
#187145=CARTESIAN_POINT('Ctrl Pts',(193.45345250346,-3.96307003814781,135.200591740371));
#187146=CARTESIAN_POINT('Ctrl Pts',(193.460848860396,-4.07881933492679,
135.093416402282));
#187147=CARTESIAN_POINT('Ctrl Pts',(193.468245217331,-4.19008729459038,
134.981811877151));
#187148=CARTESIAN_POINT('Ctrl Pts',(193.475642706668,-4.30137228966243,
134.870190265084));
#187149=CARTESIAN_POINT('Ctrl Pts',(193.483040196004,-4.40817431791499,
134.754138380124));
#187150=CARTESIAN_POINT('Ctrl Pts',(193.490437685341,-4.51013564852389,
134.634061257879));
#187151=CARTESIAN_POINT('Ctrl Pts',(193.497837767856,-4.61213272151835,
134.513942042786));
#187152=CARTESIAN_POINT('Ctrl Pts',(193.505237850371,-4.70928547688403,
134.389795065409));
#187153=CARTESIAN_POINT('Ctrl Pts',(193.512637932886,-4.80127712631488,
134.262057613953));
#187154=CARTESIAN_POINT('Ctrl Pts',(193.520046152552,-4.89336993002218,
134.134179702037));
#187155=CARTESIAN_POINT('Ctrl Pts',(193.527454372219,-4.98029007582845,
134.002703734542));
#187156=CARTESIAN_POINT('Ctrl Pts',(193.534862591885,-5.06176430342499,
133.868095707138));
#187157=CARTESIAN_POINT('Ctrl Pts',(193.542275371188,-5.14328867704949,
133.733404830738));
#187158=CARTESIAN_POINT('Ctrl Pts',(193.54968815049,-5.21936027347246,133.595578379247));
#187159=CARTESIAN_POINT('Ctrl Pts',(193.557100929792,-5.28975254618504,
133.455105524687));
#187160=CARTESIAN_POINT('Ctrl Pts',(193.564524300821,-5.36024539867765,
133.314431955926));
#187161=CARTESIAN_POINT('Ctrl Pts',(193.571947671849,-5.42504256684365,
133.171104771232));
#187162=CARTESIAN_POINT('Ctrl Pts',(193.579371042878,-5.48396592885686,
133.025632382487));
#187163=CARTESIAN_POINT('Ctrl Pts',(193.583307092319,-5.51520850924322,
132.948499431412));
#187164=CARTESIAN_POINT('Ctrl Pts',(193.58724314176,-5.54480058572185,132.870763639298));
#187165=CARTESIAN_POINT('Ctrl Pts',(193.591179191201,-5.57272137747765,
132.792502215014));
#187166=CARTESIAN_POINT('Ctrl Pts',(193.59982438893,-5.63404702115283,132.62060765482));
#187167=CARTESIAN_POINT('Ctrl Pts',(193.60846958666,-5.6874596691831,132.445749915596));
#187168=CARTESIAN_POINT('Ctrl Pts',(193.61711478439,-5.7327048543804,132.268609781835));
#187169=CARTESIAN_POINT('Ctrl Pts',(193.625725250551,-5.77776826973561,
132.092181298032));
#187170=CARTESIAN_POINT('Ctrl Pts',(193.634335716713,-5.81472962923724,
131.913488824043));
#187171=CARTESIAN_POINT('Ctrl Pts',(193.642946182875,-5.84338413695381,
131.733226803029));
#187172=CARTESIAN_POINT('Ctrl Pts',(193.651489290023,-5.87181448266578,
131.554374957907));
#187173=CARTESIAN_POINT('Ctrl Pts',(193.660032397172,-5.89206736515099,
131.373978144609));
#187174=CARTESIAN_POINT('Ctrl Pts',(193.668575504321,-5.90398986112245,
131.192734512496));
#187175=CARTESIAN_POINT('Ctrl Pts',(193.674591938801,-5.91238621090631,
131.065094718366));
#187176=CARTESIAN_POINT('Ctrl Pts',(193.680608373282,-5.91665199363111,
130.937035352127));
#187177=CARTESIAN_POINT('Ctrl Pts',(193.686624807763,-5.91674833022066,
130.808805764476));
#187178=CARTESIAN_POINT('',(195.436626015881,-5.91264468443637,130.800534531502));
#187179=CARTESIAN_POINT('Ctrl Pts',(193.686624807795,-5.91674833022117,
130.808805763797));
#187180=CARTESIAN_POINT('Ctrl Pts',(193.694249891429,-5.91687042486749,
130.646290683926));
#187181=CARTESIAN_POINT('Ctrl Pts',(193.701874975063,-5.91029198571113,
130.483707620702));
#187182=CARTESIAN_POINT('Ctrl Pts',(193.709500058697,-5.89702633263468,
130.321648493507));
#187183=CARTESIAN_POINT('Ctrl Pts',(193.716903394445,-5.8841464629385,130.164302267934));
#187184=CARTESIAN_POINT('Ctrl Pts',(193.724306730192,-5.86496295699468,
130.007450318832));
#187185=CARTESIAN_POINT('Ctrl Pts',(193.731710065939,-5.839540805705,129.851630991173));
#187186=CARTESIAN_POINT('Ctrl Pts',(193.739114086533,-5.81411630273351,
129.695797249413));
#187187=CARTESIAN_POINT('Ctrl Pts',(193.746518107128,-5.78245206455313,
129.540996686389));
#187188=CARTESIAN_POINT('Ctrl Pts',(193.753922127722,-5.74466447835844,
129.387758840923));
#187189=CARTESIAN_POINT('Ctrl Pts',(193.761328280158,-5.70686601197486,
129.234476873648));
#187190=CARTESIAN_POINT('Ctrl Pts',(193.768734432594,-5.66294077563007,
129.082758880831));
#187191=CARTESIAN_POINT('Ctrl Pts',(193.776140585029,-5.61305539489754,
128.933120468277));
#187192=CARTESIAN_POINT('Ctrl Pts',(193.783931104195,-5.56058104765214,
128.775716076322));
#187193=CARTESIAN_POINT('Ctrl Pts',(193.79172162336,-5.50151156375219,128.620613319595));
#187194=CARTESIAN_POINT('Ctrl Pts',(193.799512142525,-5.43609843388967,
128.468388789919));
#187195=CARTESIAN_POINT('Ctrl Pts',(193.806931140232,-5.37380478565584,
128.32342368392));
#187196=CARTESIAN_POINT('Ctrl Pts',(193.814350137939,-5.3057587036248,128.181068965662));
#187197=CARTESIAN_POINT('Ctrl Pts',(193.821769135646,-5.23222448513309,
128.041797043696));
#187198=CARTESIAN_POINT('Ctrl Pts',(193.829193605055,-5.15863603325452,
127.902422405087));
#187199=CARTESIAN_POINT('Ctrl Pts',(193.836618074465,-5.07955156595895,
127.766135413061));
#187200=CARTESIAN_POINT('Ctrl Pts',(193.844042543874,-4.99527888296432,
127.633379784462));
#187201=CARTESIAN_POINT('Ctrl Pts',(193.851477405336,-4.91088824323663,
127.500438337403));
#187202=CARTESIAN_POINT('Ctrl Pts',(193.858912266798,-4.82129510231583,
127.371038424274));
#187203=CARTESIAN_POINT('Ctrl Pts',(193.86634712826,-4.72684806539047,127.245591458262));
#187204=CARTESIAN_POINT('Ctrl Pts',(193.867440357178,-4.71296048557474,
127.227145620151));
#187205=CARTESIAN_POINT('Ctrl Pts',(193.868533586096,-4.69896802508309,
127.20878518446));
#187206=CARTESIAN_POINT('Ctrl Pts',(193.869626815014,-4.68487185884326,
127.190511391503));
#187207=CARTESIAN_POINT('Ctrl Pts',(193.877050081419,-4.58915576902482,
127.066428291302));
#187208=CARTESIAN_POINT('Ctrl Pts',(193.884473347825,-4.48836185950119,
126.945962881474));
#187209=CARTESIAN_POINT('Ctrl Pts',(193.89189661423,-4.38279338078887,126.82955839056));
#187210=CARTESIAN_POINT('Ctrl Pts',(193.899311106951,-4.27734967525132,
126.713291480087));
#187211=CARTESIAN_POINT('Ctrl Pts',(193.906725599672,-4.16714288156309,
126.601076208577));
#187212=CARTESIAN_POINT('Ctrl Pts',(193.914140092393,-4.0525183215702,126.493325264447));
#187213=CARTESIAN_POINT('Ctrl Pts',(193.921547438747,-3.93800424104399,
126.385678174735));
#187214=CARTESIAN_POINT('Ctrl Pts',(193.928954785101,-3.81908114123644,
126.282487100167));
#187215=CARTESIAN_POINT('Ctrl Pts',(193.936362131454,-3.69613316353616,
126.184130082202));
#187216=CARTESIAN_POINT('Ctrl Pts',(193.94376395313,-3.57327688507596,126.085846422612));
#187217=CARTESIAN_POINT('Ctrl Pts',(193.951165774805,-3.44640199616621,
125.992389872936));
#187218=CARTESIAN_POINT('Ctrl Pts',(193.958567596481,-3.31592780126095,
125.904100075582));
#187219=CARTESIAN_POINT('Ctrl Pts',(193.965965510792,-3.18552248266734,
125.815856885725));
#187220=CARTESIAN_POINT('Ctrl Pts',(193.973363425103,-3.05152195049331,
125.732775224944));
#187221=CARTESIAN_POINT('Ctrl Pts',(193.980761339415,-2.91437665000294,
125.655152979063));
#187222=CARTESIAN_POINT('Ctrl Pts',(193.988158024327,-2.77725414057385,
125.577543632592));
#187223=CARTESIAN_POINT('Ctrl Pts',(193.995554709239,-2.63698822459584,
125.505392084079));
#187224=CARTESIAN_POINT('Ctrl Pts',(194.002951394151,-2.49405635059935,
125.438951641306));
#187225=CARTESIAN_POINT('Ctrl Pts',(194.010347751087,-2.35113081435208,
125.372514144571));
#187226=CARTESIAN_POINT('Ctrl Pts',(194.017744108022,-2.20553989364301,
125.31178740741));
#187227=CARTESIAN_POINT('Ctrl Pts',(194.025140464957,-2.057783294511,125.256977588125));
#187228=CARTESIAN_POINT('Ctrl Pts',(194.032537954294,-1.9100040734663,125.202159377317));
#187229=CARTESIAN_POINT('Ctrl Pts',(194.039935443631,-1.76005886381328,
125.15326001798));
#187230=CARTESIAN_POINT('Ctrl Pts',(194.047332932967,-1.60846474911433,
125.110436512579));
#187231=CARTESIAN_POINT('Ctrl Pts',(194.054733015482,-1.45681749333343,
125.067597995464));
#187232=CARTESIAN_POINT('Ctrl Pts',(194.062133097997,-1.30352054068615,
125.030839674279));
#187233=CARTESIAN_POINT('Ctrl Pts',(194.069533180512,-1.14910329058166,
125.000267907239));
#187234=CARTESIAN_POINT('Ctrl Pts',(194.076941400178,-0.994516242836139,
124.969662523398));
#187235=CARTESIAN_POINT('Ctrl Pts',(194.084349619845,-0.838806803898584,
124.945257351789));
#187236=CARTESIAN_POINT('Ctrl Pts',(194.091757839511,-0.68251238996658,
124.927107228436));
#187237=CARTESIAN_POINT('Ctrl Pts',(194.099170618813,-0.526121779430448,
124.908945933984));
#187238=CARTESIAN_POINT('Ctrl Pts',(194.106583398116,-0.369145847837443,
124.897047387302));
#187239=CARTESIAN_POINT('Ctrl Pts',(194.113996177418,-0.212123673302736,
124.891414303779));
#187240=CARTESIAN_POINT('Ctrl Pts',(194.121419548446,-0.0548771381217091,
124.885773171442));
#187241=CARTESIAN_POINT('Ctrl Pts',(194.128842919475,0.102415399659899,
124.886415380671));
#187242=CARTESIAN_POINT('Ctrl Pts',(194.136266290504,0.259217491474521,
124.893291606413));
#187243=CARTESIAN_POINT('Ctrl Pts',(194.140202339945,0.342357722969995,
124.896937546294));
#187244=CARTESIAN_POINT('Ctrl Pts',(194.144138389385,0.425360189154594,
124.902335228505));
#187245=CARTESIAN_POINT('Ctrl Pts',(194.148074438826,0.508146029354237,
124.909471460393));
#187246=CARTESIAN_POINT('Ctrl Pts',(194.155497705232,0.664277540311929,
124.922930171021));
#187247=CARTESIAN_POINT('Ctrl Pts',(194.162920971637,0.820110071483281,
124.942616445193));
#187248=CARTESIAN_POINT('Ctrl Pts',(194.170344238043,0.975106807833801,
124.968514725511));
#187249=CARTESIAN_POINT('Ctrl Pts',(194.177758730764,1.12992035091363,124.994382396213));
#187250=CARTESIAN_POINT('Ctrl Pts',(194.185173223485,1.28389970087569,125.0264473977));
#187251=CARTESIAN_POINT('Ctrl Pts',(194.192587716206,1.43651099637365,125.064642269093));
#187252=CARTESIAN_POINT('Ctrl Pts',(194.199995062559,1.58897519935966,125.102800326831));
#187253=CARTESIAN_POINT('Ctrl Pts',(194.207402408913,1.74007361322188,125.147076402391));
#187254=CARTESIAN_POINT('Ctrl Pts',(194.214809755267,1.88928054317001,125.197351647384));
#187255=CARTESIAN_POINT('Ctrl Pts',(194.222211576942,2.03837618896044,125.247589395203));
#187256=CARTESIAN_POINT('Ctrl Pts',(194.229613398618,2.18558280757734,125.303817284624));
#187257=CARTESIAN_POINT('Ctrl Pts',(194.237015220293,2.33038800394414,125.365866127951));
#187258=CARTESIAN_POINT('Ctrl Pts',(194.244413134605,2.47511675877508,125.427882216177));
#187259=CARTESIAN_POINT('Ctrl Pts',(194.251811048916,2.61744627377012,125.495712991953));
#187260=CARTESIAN_POINT('Ctrl Pts',(194.259208963227,2.75688245248113,125.569140497485));
#187261=CARTESIAN_POINT('Ctrl Pts',(194.26660564814,2.89629545942845,125.642555800698));
#187262=CARTESIAN_POINT('Ctrl Pts',(194.274002333052,3.03281575440156,125.721565813977));
#187263=CARTESIAN_POINT('Ctrl Pts',(194.281399017964,3.16597214979834,125.805905765394));
#187264=CARTESIAN_POINT('Ctrl Pts',(194.2887953749,3.29912264090107,125.89024197709));
#187265=CARTESIAN_POINT('Ctrl Pts',(194.296191731835,3.42890921364481,125.979907457263));
#187266=CARTESIAN_POINT('Ctrl Pts',(194.30358808877,3.55488831789053,126.07459322267));
#187267=CARTESIAN_POINT('Ctrl Pts',(194.310985578107,3.68088670985897,126.169293484709));
#187268=CARTESIAN_POINT('Ctrl Pts',(194.318383067444,3.80307617420363,126.269015338105));
#187269=CARTESIAN_POINT('Ctrl Pts',(194.32578055678,3.92104512400985,126.373408609478));
#187270=CARTESIAN_POINT('Ctrl Pts',(194.333180639295,4.03905542764841,126.477838475751));
#187271=CARTESIAN_POINT('Ctrl Pts',(194.34058072181,4.15284199170322,126.586942773136));
#187272=CARTESIAN_POINT('Ctrl Pts',(194.347980804325,4.26202918068377,126.700333592131));
#187273=CARTESIAN_POINT('Ctrl Pts',(194.355389023992,4.37133643220337,126.813849095989));
#187274=CARTESIAN_POINT('Ctrl Pts',(194.362797243658,4.47603394942869,126.931660265503));
#187275=CARTESIAN_POINT('Ctrl Pts',(194.370205463325,4.57578511067753,127.053344597419));
#187276=CARTESIAN_POINT('Ctrl Pts',(194.377618242627,4.67559766710175,127.17510382401));
#187277=CARTESIAN_POINT('Ctrl Pts',(194.385031021929,4.77045757678608,127.300740665929));
#187278=CARTESIAN_POINT('Ctrl Pts',(194.392443801231,4.86007117030686,127.429803049224));
#187279=CARTESIAN_POINT('Ctrl Pts',(194.39986717226,4.94981280793254,127.559049842905));
#187280=CARTESIAN_POINT('Ctrl Pts',(194.407290543289,5.03429295787514,127.691731639473));
#187281=CARTESIAN_POINT('Ctrl Pts',(194.414713914317,5.11326315514323,127.827370448158));
#187282=CARTESIAN_POINT('Ctrl Pts',(194.418649963758,5.15513504859709,127.899289399128));
#187283=CARTESIAN_POINT('Ctrl Pts',(194.422586013199,5.19545868610213,127.972039303758));
#187284=CARTESIAN_POINT('Ctrl Pts',(194.426522062639,5.23420254088829,128.04554668338));
#187285=CARTESIAN_POINT('Ctrl Pts',(194.433945329045,5.30727224186316,128.184179307264));
#187286=CARTESIAN_POINT('Ctrl Pts',(194.44136859545,5.37494091137785,128.325926541199));
#187287=CARTESIAN_POINT('Ctrl Pts',(194.448791861856,5.4369314766717,128.470328338338));
#187288=CARTESIAN_POINT('Ctrl Pts',(194.456206354577,5.49884877426541,128.614559464546));
#187289=CARTESIAN_POINT('Ctrl Pts',(194.463620847298,5.55510118019554,128.761438569126));
#187290=CARTESIAN_POINT('Ctrl Pts',(194.471035340019,5.60545688611216,128.910480035154));
#187291=CARTESIAN_POINT('Ctrl Pts',(194.478442686372,5.6557640573036,129.059377849406));
#187292=CARTESIAN_POINT('Ctrl Pts',(194.485850032726,5.70018572444837,129.21043352466));
#187293=CARTESIAN_POINT('Ctrl Pts',(194.49325737908,5.73853772718516,129.363140538545));
#187294=CARTESIAN_POINT('Ctrl Pts',(194.500659200755,5.77686112555123,129.515733657777));
#187295=CARTESIAN_POINT('Ctrl Pts',(194.508061022431,5.80912378280913,129.669975302801));
#187296=CARTESIAN_POINT('Ctrl Pts',(194.515462844106,5.83519107930323,129.825342931045));
#187297=CARTESIAN_POINT('Ctrl Pts',(194.522860758417,5.86124461507446,129.980628541928));
#187298=CARTESIAN_POINT('Ctrl Pts',(194.530258672729,5.88110924179336,130.13703858504));
#187299=CARTESIAN_POINT('Ctrl Pts',(194.53765658704,5.8947012623256,130.294039551533));
#187300=CARTESIAN_POINT('Ctrl Pts',(194.545053271952,5.90829102411064,130.451014427314));
#187301=CARTESIAN_POINT('Ctrl Pts',(194.552449956865,5.91561021638582,130.608579660035));
#187302=CARTESIAN_POINT('Ctrl Pts',(194.559846641777,5.91662691086489,130.766195710526));
#187303=CARTESIAN_POINT('Ctrl Pts',(194.567242998712,5.91764356026267,130.923804772156));
#187304=CARTESIAN_POINT('Ctrl Pts',(194.574639355648,5.91235826511605,131.081464273787));
#187305=CARTESIAN_POINT('Ctrl Pts',(194.582035712583,5.90079123209493,131.238634031134));
#187306=CARTESIAN_POINT('Ctrl Pts',(194.58943320192,5.88922242813151,131.395827851571));
#187307=CARTESIAN_POINT('Ctrl Pts',(194.596830691256,5.87136999872203,131.552531406112));
#187308=CARTESIAN_POINT('Ctrl Pts',(194.604228180593,5.84730608186697,131.708209137763));
#187309=CARTESIAN_POINT('Ctrl Pts',(194.611628263108,5.82323372944323,131.863941442));
#187310=CARTESIAN_POINT('Ctrl Pts',(194.619028345623,5.79294561132196,132.0186468387));
#187311=CARTESIAN_POINT('Ctrl Pts',(194.626428428138,5.75656504659628,132.171799620522));
#187312=CARTESIAN_POINT('Ctrl Pts',(194.633836647804,5.72014447769965,132.325120809573));
#187313=CARTESIAN_POINT('Ctrl Pts',(194.641244867471,5.67761816964086,132.476885610823));
#187314=CARTESIAN_POINT('Ctrl Pts',(194.648653087137,5.62915963413416,132.626582441586));
#187315=CARTESIAN_POINT('Ctrl Pts',(194.656065866439,5.58067127320736,132.776371408251));
#187316=CARTESIAN_POINT('Ctrl Pts',(194.663478645741,5.52624353814764,132.924089518748));
#187317=CARTESIAN_POINT('Ctrl Pts',(194.670891425043,5.46609803607665,133.069245343661));
#187318=CARTESIAN_POINT('Ctrl Pts',(194.678314796072,5.4058665952918,133.214608574024));
#187319=CARTESIAN_POINT('Ctrl Pts',(194.685738167101,5.33990122668302,133.35740186875));
#187320=CARTESIAN_POINT('Ctrl Pts',(194.69316153813,5.26846977602395,133.49715782152));
#187321=CARTESIAN_POINT('Ctrl Pts',(194.697097587571,5.23059510690934,133.571259781079));
#187322=CARTESIAN_POINT('Ctrl Pts',(194.701033637011,5.19118446278821,133.644508299809));
#187323=CARTESIAN_POINT('Ctrl Pts',(194.704969686452,5.15028262235604,133.716837136331));
#187324=CARTESIAN_POINT('Ctrl Pts',(194.712392952858,5.07314302780579,133.853247064702));
#187325=CARTESIAN_POINT('Ctrl Pts',(194.719816219263,4.99046363417835,133.986796475152));
#187326=CARTESIAN_POINT('Ctrl Pts',(194.727239485669,4.90248172731818,134.117003591961));
#187327=CARTESIAN_POINT('Ctrl Pts',(194.73465397839,4.81460380776549,134.247056814772));
#187328=CARTESIAN_POINT('Ctrl Pts',(194.742068471111,4.7214360566969,134.373775300779));
#187329=CARTESIAN_POINT('Ctrl Pts',(194.749482963832,4.62326173930799,134.496701535243));
#187330=CARTESIAN_POINT('Ctrl Pts',(194.756890310185,4.52518204602216,134.619509288774));
#187331=CARTESIAN_POINT('Ctrl Pts',(194.764297656539,4.4221056244628,134.738531777645));
#187332=CARTESIAN_POINT('Ctrl Pts',(194.771705002893,4.31435908307288,134.853340274814));
#187333=CARTESIAN_POINT('Ctrl Pts',(194.779106824568,4.2066929031187,134.968063143474));
#187334=CARTESIAN_POINT('Ctrl Pts',(194.786508646244,4.0943637931164,135.078578007448));
#187335=CARTESIAN_POINT('Ctrl Pts',(194.793910467919,3.97773861771825,135.184489160384));
#187336=CARTESIAN_POINT('Ctrl Pts',(194.801308382231,3.86117500784292,135.290344403647));
#187337=CARTESIAN_POINT('Ctrl Pts',(194.808706296542,3.74032012477287,135.39160052553));
#187338=CARTESIAN_POINT('Ctrl Pts',(194.816104210853,3.61557758426522,135.487898734701));
#187339=CARTESIAN_POINT('Ctrl Pts',(194.823500895765,3.49085577370419,135.584180940857));
#187340=CARTESIAN_POINT('Ctrl Pts',(194.830897580678,3.36224788314285,135.675506641639));
#187341=CARTESIAN_POINT('Ctrl Pts',(194.83829426559,3.23019058414608,135.761557340775));
#187342=CARTESIAN_POINT('Ctrl Pts',(194.845690622525,3.09813914070806,135.847604224333));
#187343=CARTESIAN_POINT('Ctrl Pts',(194.853086979461,2.96263890570939,135.928376367518));
#187344=CARTESIAN_POINT('Ctrl Pts',(194.860483336396,2.82415527368646,136.003598787972));
#187345=CARTESIAN_POINT('Ctrl Pts',(194.867880825733,2.68565043946621,136.078832725171));
#187346=CARTESIAN_POINT('Ctrl Pts',(194.875278315069,2.54416162679036,136.148515069628));
#187347=CARTESIAN_POINT('Ctrl Pts',(194.882675804406,2.40017840727624,136.212417031449));
#187348=CARTESIAN_POINT('Ctrl Pts',(194.890075886921,2.25614471466828,136.276341394004));
#187349=CARTESIAN_POINT('Ctrl Pts',(194.897475969436,2.10961521526799,136.33448118823));
#187350=CARTESIAN_POINT('Ctrl Pts',(194.904876051951,1.96109885853,136.386656008315));
#187351=CARTESIAN_POINT('Ctrl Pts',(194.912284271617,1.81241919278925,136.438888199978));
#187352=CARTESIAN_POINT('Ctrl Pts',(194.919692491284,1.66174865902651,136.485142194737));
#187353=CARTESIAN_POINT('Ctrl Pts',(194.92710071095,1.50961145356359,136.525287449974));
#187354=CARTESIAN_POINT('Ctrl Pts',(194.934513490252,1.35738061018877,136.565457413946));
#187355=CARTESIAN_POINT('Ctrl Pts',(194.941926269555,1.20368165996157,136.599511065906));
#187356=CARTESIAN_POINT('Ctrl Pts',(194.949339048857,1.04904784043026,136.627369220598));
#187357=CARTESIAN_POINT('Ctrl Pts',(194.956762419885,0.894193072846361,
136.655267180328));
#187358=CARTESIAN_POINT('Ctrl Pts',(194.964185790914,0.738401136849904,
136.676951911201));
#187359=CARTESIAN_POINT('Ctrl Pts',(194.971609161943,0.582210051798615,
136.692396114919));
#187360=CARTESIAN_POINT('Ctrl Pts',(194.975545211384,0.499393790750225,
136.700585002308));
#187361=CARTESIAN_POINT('Ctrl Pts',(194.979481260825,0.416465321632257,
136.70702032481));
#187362=CARTESIAN_POINT('Ctrl Pts',(194.983417310265,0.333504579172153,
136.711703950924));
#187363=CARTESIAN_POINT('Ctrl Pts',(194.990840576671,0.177043208009956,
136.720537123605));
#187364=CARTESIAN_POINT('Ctrl Pts',(194.998263843076,0.0199940748712888,
136.723163326617));
#187365=CARTESIAN_POINT('Ctrl Pts',(195.005687109482,-0.137109229893286,
136.71952178372));
#187366=CARTESIAN_POINT('Ctrl Pts',(195.013101602203,-0.294026851598554,
136.715884544824));
#187367=CARTESIAN_POINT('Ctrl Pts',(195.020516094924,-0.450998147931574,
136.70599431416));
#187368=CARTESIAN_POINT('Ctrl Pts',(195.027930587645,-0.607485087027711,
136.689842112868));
#187369=CARTESIAN_POINT('Ctrl Pts',(195.035337933998,-0.763821198120527,
136.673705479675));
#187370=CARTESIAN_POINT('Ctrl Pts',(195.042745280352,-0.919673512534122,
136.651318929462));
#187371=CARTESIAN_POINT('Ctrl Pts',(195.050152626706,-1.07450479022457,
136.622725509723));
#187372=CARTESIAN_POINT('Ctrl Pts',(195.057554448381,-1.22922058890767,
136.594153416035));
#187373=CARTESIAN_POINT('Ctrl Pts',(195.064956270057,-1.38291650166136,
136.559383737918));
#187374=CARTESIAN_POINT('Ctrl Pts',(195.072358091732,-1.53506131021855,
136.518511240044));
#187375=CARTESIAN_POINT('Ctrl Pts',(195.079756006044,-1.68712580271452,
136.477660318445));
#187376=CARTESIAN_POINT('Ctrl Pts',(195.087153920355,-1.83764046212198,
136.430713089725));
#187377=CARTESIAN_POINT('Ctrl Pts',(195.094551834666,-1.98608526295548,
136.377815191775));
#187378=CARTESIAN_POINT('Ctrl Pts',(195.101948519579,-2.13450539495601,
136.324926084496));
#187379=CARTESIAN_POINT('Ctrl Pts',(195.109345204491,-2.28085599977257,
136.266088395828));
#187380=CARTESIAN_POINT('Ctrl Pts',(195.116741889403,-2.42463308582467,
136.201497354913));
#187381=CARTESIAN_POINT('Ctrl Pts',(195.124138246339,-2.56840379665031,
136.136909178033));
#187382=CARTESIAN_POINT('Ctrl Pts',(195.131534603274,-2.70960087509142,
136.066568309123));
#187383=CARTESIAN_POINT('Ctrl Pts',(195.138930960209,-2.84774141358831,
135.990717663107));
#187384=CARTESIAN_POINT('Ctrl Pts',(195.146328449546,-2.98590310175456,
135.914855404164));
#187385=CARTESIAN_POINT('Ctrl Pts',(195.153725938883,-3.1210069909607,135.833481868153));
#187386=CARTESIAN_POINT('Ctrl Pts',(195.161123428219,-3.25259596837197,
135.746885279015));
#187387=CARTESIAN_POINT('Ctrl Pts',(195.168523510734,-3.38423107409569,
135.660258333577));
#187388=CARTESIAN_POINT('Ctrl Pts',(195.175923593249,-3.51234850319129,
135.568404894722));
#187389=CARTESIAN_POINT('Ctrl Pts',(195.183323675764,-3.63652137552785,
135.471655642292));
#187390=CARTESIAN_POINT('Ctrl Pts',(195.190731895431,-3.76083078870214,
135.374800004113));
#187391=CARTESIAN_POINT('Ctrl Pts',(195.198140115097,-3.88118668830531,
135.273038030831));
#187392=CARTESIAN_POINT('Ctrl Pts',(195.205548334764,-3.99719590421933,
135.166740182184));
#187393=CARTESIAN_POINT('Ctrl Pts',(195.212961114066,-4.11327652186949,
135.060376908984));
#187394=CARTESIAN_POINT('Ctrl Pts',(195.220373893368,-4.2250048606152,134.949472459869));
#187395=CARTESIAN_POINT('Ctrl Pts',(195.22778667267,-4.33202607173832,134.834432661125));
#187396=CARTESIAN_POINT('Ctrl Pts',(195.235210043698,-4.43920019978721,
134.719228488122));
#187397=CARTESIAN_POINT('Ctrl Pts',(195.242633414727,-4.54165352484936,
134.599877446827));
#187398=CARTESIAN_POINT('Ctrl Pts',(195.250056785756,-4.63907226748901,
134.476817432767));
#187399=CARTESIAN_POINT('Ctrl Pts',(195.253992835197,-4.6907260223665,134.411568060529));
#187400=CARTESIAN_POINT('Ctrl Pts',(195.257928884637,-4.7409651046425,134.345276439808));
#187401=CARTESIAN_POINT('Ctrl Pts',(195.261864934078,-4.78974787966705,
134.278010831926));
#187402=CARTESIAN_POINT('Ctrl Pts',(195.269344497194,-4.88244840344199,
134.150187905093));
#187403=CARTESIAN_POINT('Ctrl Pts',(195.27682406031,-4.97016722581075,134.018460598548));
#187404=CARTESIAN_POINT('Ctrl Pts',(195.284303623426,-5.05256043017122,
133.883250622416));
#187405=CARTESIAN_POINT('Ctrl Pts',(195.291774119838,-5.13485375774175,
133.748204547404));
#187406=CARTESIAN_POINT('Ctrl Pts',(195.29924461625,-5.21183412944589,133.609684515291));
#187407=CARTESIAN_POINT('Ctrl Pts',(195.306715112662,-5.28319868593022,
133.468144056114));
#187408=CARTESIAN_POINT('Ctrl Pts',(195.314177953125,-5.35449010624771,
133.326748651109));
#187409=CARTESIAN_POINT('Ctrl Pts',(195.321640793587,-5.42017700590164,
133.182339305798));
#187410=CARTESIAN_POINT('Ctrl Pts',(195.329103634049,-5.48000059220959,
133.03539716408));
#187411=CARTESIAN_POINT('Ctrl Pts',(195.336560224284,-5.53977407546993,
132.888578088357));
#187412=CARTESIAN_POINT('Ctrl Pts',(195.344016814518,-5.59369388645601,
132.739230777314));
#187413=CARTESIAN_POINT('Ctrl Pts',(195.351473404753,-5.64154786489769,
132.587859496334));
#187414=CARTESIAN_POINT('Ctrl Pts',(195.358924751708,-5.68936819367592,
132.436594655673));
#187415=CARTESIAN_POINT('Ctrl Pts',(195.366376098664,-5.73113107811833,
132.28330902832));
#187416=CARTESIAN_POINT('Ctrl Pts',(195.373827445619,-5.76667310995969,
132.128525186405));
#187417=CARTESIAN_POINT('Ctrl Pts',(195.381275645374,-5.80220013002815,
131.97380672004));
#187418=CARTESIAN_POINT('Ctrl Pts',(195.388723845128,-5.83151144890194,
131.817591655312));
#187419=CARTESIAN_POINT('Ctrl Pts',(195.396172044882,-5.85449396429676,
131.660416097376));
#187420=CARTESIAN_POINT('Ctrl Pts',(195.403619442704,-5.87747400521164,
131.503257462208));
#187421=CARTESIAN_POINT('Ctrl Pts',(195.411066840526,-5.89412654082032,
131.345138900639));
#187422=CARTESIAN_POINT('Ctrl Pts',(195.418514238348,-5.90438986155658,
131.186605205818));
#187423=CARTESIAN_POINT('Ctrl Pts',(195.424551094831,-5.91270930356792,
131.058097882038));
#187424=CARTESIAN_POINT('Ctrl Pts',(195.430587951313,-5.91683153852153,
130.929318034017));
#187425=CARTESIAN_POINT('Ctrl Pts',(195.436624807795,-5.91674877781543,
130.800557629312));
#187426=CARTESIAN_POINT('',(197.186623444831,-5.92116344383671,130.801362336707));
#187427=CARTESIAN_POINT('Ctrl Pts',(195.436626945312,-5.90948723714756,
130.800516761409));
#187428=CARTESIAN_POINT('Ctrl Pts',(195.471188816171,-5.9137909198465,130.064246680543));
#187429=CARTESIAN_POINT('Ctrl Pts',(195.598566561638,-5.44429779229546,
127.356026198653));
#187430=CARTESIAN_POINT('Ctrl Pts',(195.818760181701,-1.38200268831043,
123.943775431166));
#187431=CARTESIAN_POINT('Ctrl Pts',(196.097207805517,5.0249984088633,125.933328743181));
#187432=CARTESIAN_POINT('Ctrl Pts',(196.375655429329,6.81427145311116,132.39912238462));
#187433=CARTESIAN_POINT('Ctrl Pts',(196.654103053143,2.34156192761705,137.399407870579));
#187434=CARTESIAN_POINT('Ctrl Pts',(196.924425368086,-4.08962105397609,
136.370105731155));
#187435=CARTESIAN_POINT('Ctrl Pts',(197.101931808425,-5.91344458449586,
132.593748677927));
#187436=CARTESIAN_POINT('Ctrl Pts',(197.18662237416,-5.92463101698242,130.801383223244));
#187437=CARTESIAN_POINT('',(198.936625519421,-5.91828595945227,130.809611426597));
#187438=CARTESIAN_POINT('Ctrl Pts',(197.186624807795,-5.91674922678536,
130.801335748166));
#187439=CARTESIAN_POINT('Ctrl Pts',(197.194749305453,-5.91666143946249,
130.629620706627));
#187440=CARTESIAN_POINT('Ctrl Pts',(197.20287380311,-5.90909912685711,130.458101858393));
#187441=CARTESIAN_POINT('Ctrl Pts',(197.210998300767,-5.89410901923282,
130.287244158827));
#187442=CARTESIAN_POINT('Ctrl Pts',(197.218421567172,-5.88041271860844,
130.131133310534));
#187443=CARTESIAN_POINT('Ctrl Pts',(197.225844833577,-5.86048931664855,
129.975330918972));
#187444=CARTESIAN_POINT('Ctrl Pts',(197.233268099982,-5.83435518767231,
129.820373774879));
#187445=CARTESIAN_POINT('Ctrl Pts',(197.240682592703,-5.80825194706619,
129.665599777262));
#187446=CARTESIAN_POINT('Ctrl Pts',(197.248097085424,-5.77595265235115,
129.511669403079));
#187447=CARTESIAN_POINT('Ctrl Pts',(197.255511578145,-5.73752557677412,
129.359116410395));
#187448=CARTESIAN_POINT('Ctrl Pts',(197.262918924498,-5.69913553865926,
129.206710454028));
#187449=CARTESIAN_POINT('Ctrl Pts',(197.270326270852,-5.65462956830657,
129.055679595785));
#187450=CARTESIAN_POINT('Ctrl Pts',(197.277733617205,-5.60412731398305,
128.906549348981));
#187451=CARTESIAN_POINT('Ctrl Pts',(197.285135438881,-5.55366272614622,
128.757530329141));
#187452=CARTESIAN_POINT('Ctrl Pts',(197.292537260556,-5.49721087842226,
128.610409450263));
#187453=CARTESIAN_POINT('Ctrl Pts',(197.299939082232,-5.43494173808804,
128.465698849356));
#187454=CARTESIAN_POINT('Ctrl Pts',(197.307336996543,-5.37270546914825,
128.321064640048));
#187455=CARTESIAN_POINT('Ctrl Pts',(197.314734910855,-5.3046581706263,128.178838516762));
#187456=CARTESIAN_POINT('Ctrl Pts',(197.322132825166,-5.23101855199436,
128.03951424368));
#187457=CARTESIAN_POINT('Ctrl Pts',(197.329529510078,-5.15739117093109,
127.900213123764));
#187458=CARTESIAN_POINT('Ctrl Pts',(197.336926194991,-5.07817348849507,
127.76381322667));
#187459=CARTESIAN_POINT('Ctrl Pts',(197.344322879903,-4.9936309933754,127.630785336515));
#187460=CARTESIAN_POINT('Ctrl Pts',(197.351719236839,-4.90909224695859,
127.497763344956));
#187461=CARTESIAN_POINT('Ctrl Pts',(197.359115593775,-4.81922935754628,
127.368113378099));
#187462=CARTESIAN_POINT('Ctrl Pts',(197.36651195071,-4.72435198303289,127.242278515352));
#187463=CARTESIAN_POINT('Ctrl Pts',(197.373909440047,-4.62946008255125,
127.116424386966));
#187464=CARTESIAN_POINT('Ctrl Pts',(197.381306929384,-4.52955239306734,
126.9943868238));
#187465=CARTESIAN_POINT('Ctrl Pts',(197.388704418721,-4.42497971392021,
126.876576879388));
#187466=CARTESIAN_POINT('Ctrl Pts',(197.396104501236,-4.32037037698219,
126.758725636883));
#187467=CARTESIAN_POINT('Ctrl Pts',(197.403504583751,-4.21109304215689,
126.645105242758));
#187468=CARTESIAN_POINT('Ctrl Pts',(197.410904666267,-4.09753619015153,
126.536090741738));
#187469=CARTESIAN_POINT('Ctrl Pts',(197.418312885934,-3.9838544707137,126.426956368068));
#187470=CARTESIAN_POINT('Ctrl Pts',(197.4257211056,-3.86588410582371,126.322438260625));
#187471=CARTESIAN_POINT('Ctrl Pts',(197.433129325267,-3.74404811053006,
126.222872397726));
#187472=CARTESIAN_POINT('Ctrl Pts',(197.440542104569,-3.62213712721409,
126.123245253698));
#187473=CARTESIAN_POINT('Ctrl Pts',(197.447954883872,-3.49635607014594,
126.028576651746));
#187474=CARTESIAN_POINT('Ctrl Pts',(197.455367663174,-3.36715745966806,
125.939159572974));
#187475=CARTESIAN_POINT('Ctrl Pts',(197.462791034203,-3.23777424415678,
125.849614730886));
#187476=CARTESIAN_POINT('Ctrl Pts',(197.470214405232,-3.10496403682583,
125.765336597878));
#187477=CARTESIAN_POINT('Ctrl Pts',(197.477637776261,-2.96920520601125,
125.686572911233));
#187478=CARTESIAN_POINT('Ctrl Pts',(197.481573825702,-2.89722261642787,
125.644810514667));
#187479=CARTESIAN_POINT('Ctrl Pts',(197.485509875143,-2.82441143032903,
125.604597636826));
#187480=CARTESIAN_POINT('Ctrl Pts',(197.489445924583,-2.75084517427645,
125.565965692624));
#187481=CARTESIAN_POINT('Ctrl Pts',(197.496869190989,-2.61210151128014,
125.493107051516));
#187482=CARTESIAN_POINT('Ctrl Pts',(197.504292457394,-2.47025146129094,
125.425654175521));
#187483=CARTESIAN_POINT('Ctrl Pts',(197.5117157238,-2.32575549227818,125.363883436965));
#187484=CARTESIAN_POINT('Ctrl Pts',(197.519130216521,-2.18143030550119,
125.302185706292));
#187485=CARTESIAN_POINT('Ctrl Pts',(197.526544709242,-2.03446576441921,
125.246156890495));
#187486=CARTESIAN_POINT('Ctrl Pts',(197.533959201963,-1.88534783816607,
125.19602805863));
#187487=CARTESIAN_POINT('Ctrl Pts',(197.541366548317,-1.73637363738422,
125.14594754282));
#187488=CARTESIAN_POINT('Ctrl Pts',(197.548773894671,-1.58525053483429,
125.101755808138));
#187489=CARTESIAN_POINT('Ctrl Pts',(197.556181241024,-1.432485332562,125.063636243892));
#187490=CARTESIAN_POINT('Ctrl Pts',(197.5635830627,-1.27983406834118,125.025545110655));
#187491=CARTESIAN_POINT('Ctrl Pts',(197.570984884375,-1.12554350365379,
124.993517220284));
#187492=CARTESIAN_POINT('Ctrl Pts',(197.57838670605,-0.970136385334234,
124.967686397057));
#187493=CARTESIAN_POINT('Ctrl Pts',(197.585784620362,-0.814811305222937,
124.941869209721));
#187494=CARTESIAN_POINT('Ctrl Pts',(197.593182534673,-0.658371212651233,
124.922242635465));
#187495=CARTESIAN_POINT('Ctrl Pts',(197.600580448984,-0.501349743220964,
124.908889559417));
#187496=CARTESIAN_POINT('Ctrl Pts',(197.607977133896,-0.3443543679101,124.895538702408));
#187497=CARTESIAN_POINT('Ctrl Pts',(197.615373818808,-0.186778179082625,
124.88845930607));
#187498=CARTESIAN_POINT('Ctrl Pts',(197.622770503721,-0.0291607638722707,
124.887682477566));
#187499=CARTESIAN_POINT('Ctrl Pts',(197.630166860656,0.128449662416806,
124.886905683508));
#187500=CARTESIAN_POINT('Ctrl Pts',(197.637563217591,0.286100938161007,
124.892430903457));
#187501=CARTESIAN_POINT('Ctrl Pts',(197.644959574526,0.443252910452061,
124.9042371087));
#187502=CARTESIAN_POINT('Ctrl Pts',(197.652357063863,0.600428943111264,
124.916045121502));
#187503=CARTESIAN_POINT('Ctrl Pts',(197.659754553199,0.757105147833064,
124.934136006373));
#187504=CARTESIAN_POINT('Ctrl Pts',(197.667152042536,0.912746078026357,
124.958436810369));
#187505=CARTESIAN_POINT('Ctrl Pts',(197.674552125051,1.06844156790636,124.982746132975));
#187506=CARTESIAN_POINT('Ctrl Pts',(197.681952207565,1.2231006920997,125.013269651301));
#187507=CARTESIAN_POINT('Ctrl Pts',(197.68935229008,1.37619793154745,125.049883246362));
#187508=CARTESIAN_POINT('Ctrl Pts',(197.696760509747,1.52946351714884,125.086537101834));
#187509=CARTESIAN_POINT('Ctrl Pts',(197.704168729413,1.68116342485591,125.12929432084));
#187510=CARTESIAN_POINT('Ctrl Pts',(197.711576949079,1.83078633663098,125.177980613327));
#187511=CARTESIAN_POINT('Ctrl Pts',(197.718989728381,1.98050133881175,125.226696871413));
#187512=CARTESIAN_POINT('Ctrl Pts',(197.726402507683,2.12813644850627,125.281349345265));
#187513=CARTESIAN_POINT('Ctrl Pts',(197.733815286985,2.27320057411559,125.341715680144));
#187514=CARTESIAN_POINT('Ctrl Pts',(197.741238658014,2.41847197415036,125.402168269274));
#187515=CARTESIAN_POINT('Ctrl Pts',(197.748662029042,2.56116471546263,125.468350868582));
#187516=CARTESIAN_POINT('Ctrl Pts',(197.756085400071,2.7008117998894,125.539994921295));
#187517=CARTESIAN_POINT('Ctrl Pts',(197.760021449512,2.77485603483877,125.577982317118));
#187518=CARTESIAN_POINT('Ctrl Pts',(197.763957498952,2.84804449245546,125.617504387378));
#187519=CARTESIAN_POINT('Ctrl Pts',(197.767893548393,2.92031099958208,125.658516252623));
#187520=CARTESIAN_POINT('Ctrl Pts',(197.775316814799,3.05660337666153,125.735863350536));
#187521=CARTESIAN_POINT('Ctrl Pts',(197.782740081204,3.19002680850025,125.818745887891));
#187522=CARTESIAN_POINT('Ctrl Pts',(197.790163347609,3.32009988104743,125.906925845936));
#187523=CARTESIAN_POINT('Ctrl Pts',(197.79757784033,3.4500192180248,125.995001582594));
#187524=CARTESIAN_POINT('Ctrl Pts',(197.804992333051,3.57659577183659,126.08836206974));
#187525=CARTESIAN_POINT('Ctrl Pts',(197.812406825772,3.69937245935516,126.186723346248));
#187526=CARTESIAN_POINT('Ctrl Pts',(197.819814172126,3.82203081007992,126.284989818454));
#187527=CARTESIAN_POINT('Ctrl Pts',(197.82722151848,3.94089629635784,126.38824725262));
#187528=CARTESIAN_POINT('Ctrl Pts',(197.834628864833,4.05554068868584,126.49616838823));
#187529=CARTESIAN_POINT('Ctrl Pts',(197.842030686509,4.17009957490073,126.604009032185));
#187530=CARTESIAN_POINT('Ctrl Pts',(197.849432508184,4.28044336511714,126.716506196922));
#187531=CARTESIAN_POINT('Ctrl Pts',(197.85683432986,4.38617691174633,126.833292416016));
#187532=CARTESIAN_POINT('Ctrl Pts',(197.864232244171,4.49185464245934,126.950016984573));
#187533=CARTESIAN_POINT('Ctrl Pts',(197.871630158482,4.59292672653128,127.071025822277));
#187534=CARTESIAN_POINT('Ctrl Pts',(197.879028072794,4.68903498727919,127.195914767817));
#187535=CARTESIAN_POINT('Ctrl Pts',(197.886424757706,4.78512727657764,127.32078295908));
#187536=CARTESIAN_POINT('Ctrl Pts',(197.893821442618,4.87625715228911,127.449529682885));
#187537=CARTESIAN_POINT('Ctrl Pts',(197.90121812753,4.96210678305087,127.581717783478));
#187538=CARTESIAN_POINT('Ctrl Pts',(197.908614484466,5.04795260715005,127.713900022711));
#187539=CARTESIAN_POINT('Ctrl Pts',(197.916010841401,5.12851844851035,127.849523022255));
#187540=CARTESIAN_POINT('Ctrl Pts',(197.923407198337,5.20353003334438,127.988120969634));
#187541=CARTESIAN_POINT('Ctrl Pts',(197.930804687674,5.27855310264355,128.126740136713));
#187542=CARTESIAN_POINT('Ctrl Pts',(197.93820217701,5.34802004452218,128.268334830214));
#187543=CARTESIAN_POINT('Ctrl Pts',(197.945599666347,5.41170281439631,128.412415130906));
#187544=CARTESIAN_POINT('Ctrl Pts',(197.952999748862,5.47540790816671,128.556545938723));
#187545=CARTESIAN_POINT('Ctrl Pts',(197.960399831377,5.5333246421133,128.703163747315));
#187546=CARTESIAN_POINT('Ctrl Pts',(197.967799913892,5.58527338516755,128.851759333269));
#187547=CARTESIAN_POINT('Ctrl Pts',(197.975208133559,5.63727925120526,129.000518315345));
#187548=CARTESIAN_POINT('Ctrl Pts',(197.982616353225,5.68330389749944,129.15125906534));
#187549=CARTESIAN_POINT('Ctrl Pts',(197.990024572892,5.72321757932056,129.303457188875));
#187550=CARTESIAN_POINT('Ctrl Pts',(197.997437352194,5.76315582734688,129.455748987816));
#187551=CARTESIAN_POINT('Ctrl Pts',(198.004850131496,5.79697553623499,129.609499583923));
#187552=CARTESIAN_POINT('Ctrl Pts',(198.012262910798,5.82459833231772,129.76417561976));
#187553=CARTESIAN_POINT('Ctrl Pts',(198.019686281827,5.85226059714686,129.91907266397));
#187554=CARTESIAN_POINT('Ctrl Pts',(198.027109652855,5.87370821410285,130.074897420031));
#187555=CARTESIAN_POINT('Ctrl Pts',(198.034533023884,5.88891470369336,130.231111827664));
#187556=CARTESIAN_POINT('Ctrl Pts',(198.038469073325,5.89697754934896,130.313940454904));
#187557=CARTESIAN_POINT('Ctrl Pts',(198.042405122766,5.90328666138535,130.396878621457));
#187558=CARTESIAN_POINT('Ctrl Pts',(198.046341172207,5.90784402994841,130.479846395531));
#187559=CARTESIAN_POINT('Ctrl Pts',(198.053764438612,5.91643908482775,130.636321028099));
#187560=CARTESIAN_POINT('Ctrl Pts',(198.061187705018,5.9188262827532,130.793373976012));
#187561=CARTESIAN_POINT('Ctrl Pts',(198.068610971423,5.91494565958679,130.950471557045));
#187562=CARTESIAN_POINT('Ctrl Pts',(198.076025464144,5.91106962299469,131.107383461784));
#187563=CARTESIAN_POINT('Ctrl Pts',(198.083439956865,5.90094052019157,131.264339525099));
#187564=CARTESIAN_POINT('Ctrl Pts',(198.090854449586,5.88455019112052,131.420801702085));
#187565=CARTESIAN_POINT('Ctrl Pts',(198.09826179594,5.86817565966571,131.577113074935));
#187566=CARTESIAN_POINT('Ctrl Pts',(198.105669142294,5.84555195468406,131.732931140355));
#187567=CARTESIAN_POINT('Ctrl Pts',(198.113076488647,5.81672294120831,131.887718724436));
#187568=CARTESIAN_POINT('Ctrl Pts',(198.120478310323,5.78791542949845,132.042390862097));
#187569=CARTESIAN_POINT('Ctrl Pts',(198.127880131998,5.75291189262878,132.196033683341));
#187570=CARTESIAN_POINT('Ctrl Pts',(198.135281953674,5.71180790358625,132.348116114732));
#187571=CARTESIAN_POINT('Ctrl Pts',(198.142679867985,5.67072561301959,132.500118262991));
#187572=CARTESIAN_POINT('Ctrl Pts',(198.150077782296,5.6235493809752,132.650561302415));
#187573=CARTESIAN_POINT('Ctrl Pts',(198.157475696608,5.57042563656271,132.798925429756));
#187574=CARTESIAN_POINT('Ctrl Pts',(198.16487238152,5.5173107203528,132.94726490167));
#187575=CARTESIAN_POINT('Ctrl Pts',(198.172269066432,5.45825037911139,133.093525796069));
#187576=CARTESIAN_POINT('Ctrl Pts',(198.179665751344,5.39344060874215,133.237204419061));
#187577=CARTESIAN_POINT('Ctrl Pts',(198.18706210828,5.32863371210605,133.380876671192));
#187578=CARTESIAN_POINT('Ctrl Pts',(198.194458465215,5.25807804673258,133.5219665393));
#187579=CARTESIAN_POINT('Ctrl Pts',(198.20185482215,5.18201726216687,133.659991486062));
#187580=CARTESIAN_POINT('Ctrl Pts',(198.209252311487,5.1059448325008,133.798037564794));
#187581=CARTESIAN_POINT('Ctrl Pts',(198.216649800824,5.02436578559861,133.933017460883));
#187582=CARTESIAN_POINT('Ctrl Pts',(198.22404729016,4.93756904071554,134.064474500649));
#187583=CARTESIAN_POINT('Ctrl Pts',(198.231447372675,4.85074186936809,134.195977622476));
#187584=CARTESIAN_POINT('Ctrl Pts',(198.23884745519,4.75869356396067,134.323955117915));
#187585=CARTESIAN_POINT('Ctrl Pts',(198.246247537705,4.66175545359166,134.447980610569));
#187586=CARTESIAN_POINT('Ctrl Pts',(198.253655757372,4.56471074980486,134.572142482001));
#187587=CARTESIAN_POINT('Ctrl Pts',(198.261063977038,4.4627657331708,134.692343377834));
#187588=CARTESIAN_POINT('Ctrl Pts',(198.268472196704,4.35629146133617,134.808190692181));
#187589=CARTESIAN_POINT('Ctrl Pts',(198.275884976006,4.24975165636372,134.924109308617));
#187590=CARTESIAN_POINT('Ctrl Pts',(198.283297755308,4.13867730416189,135.035668740291));
#187591=CARTESIAN_POINT('Ctrl Pts',(198.290710534611,4.0234747705666,135.142514756496));
#187592=CARTESIAN_POINT('Ctrl Pts',(198.298133905639,3.9081076301889,135.249513439299));
#187593=CARTESIAN_POINT('Ctrl Pts',(198.305557276668,3.7886008105804,135.351785013754));
#187594=CARTESIAN_POINT('Ctrl Pts',(198.312980647697,3.6653926842793,135.449016367192));
#187595=CARTESIAN_POINT('Ctrl Pts',(198.316916697138,3.60006477937584,135.500570763819));
#187596=CARTESIAN_POINT('Ctrl Pts',(198.320852746578,3.53369678008804,135.550708903358));
#187597=CARTESIAN_POINT('Ctrl Pts',(198.324788796019,3.4663570110182,135.599389255089));
#187598=CARTESIAN_POINT('Ctrl Pts',(198.332212062425,3.33935630815509,135.691198879192));
#187599=CARTESIAN_POINT('Ctrl Pts',(198.33963532883,3.2085135538949,135.778098250994));
#187600=CARTESIAN_POINT('Ctrl Pts',(198.347058595235,3.07424533812585,135.859748452689));
#187601=CARTESIAN_POINT('Ctrl Pts',(198.354473087956,2.94013581623739,135.941302150627));
#187602=CARTESIAN_POINT('Ctrl Pts',(198.361887580677,2.80260920746114,136.017618835655));
#187603=CARTESIAN_POINT('Ctrl Pts',(198.369302073398,2.66211377350456,136.088400816071));
#187604=CARTESIAN_POINT('Ctrl Pts',(198.376709419752,2.52175375433678,136.15911457415));
#187605=CARTESIAN_POINT('Ctrl Pts',(198.384116766106,2.37843093774423,136.22430408084));
#187606=CARTESIAN_POINT('Ctrl Pts',(198.39152411246,2.23262097347329,136.283715885415));
#187607=CARTESIAN_POINT('Ctrl Pts',(198.398925934135,2.08691975977482,136.343083378425));
#187608=CARTESIAN_POINT('Ctrl Pts',(198.406327755811,1.93873543618441,136.396681609322));
#187609=CARTESIAN_POINT('Ctrl Pts',(198.413729577486,1.7885664693587,136.444303928202));
#187610=CARTESIAN_POINT('Ctrl Pts',(198.421127491797,1.63847677556185,136.49190110763));
#187611=CARTESIAN_POINT('Ctrl Pts',(198.428525406109,1.48640487996303,136.533528545095));
#187612=CARTESIAN_POINT('Ctrl Pts',(198.43592332042,1.33286725626621,136.569028469201));
#187613=CARTESIAN_POINT('Ctrl Pts',(198.443320005332,1.17935514773689,136.604522493864));
#187614=CARTESIAN_POINT('Ctrl Pts',(198.450716690245,1.02437815788533,136.633890942145));
#187615=CARTESIAN_POINT('Ctrl Pts',(198.458113375157,0.868465999221073,
136.657026452098));
#187616=CARTESIAN_POINT('Ctrl Pts',(198.465509732092,0.712560753865369,
136.680160936198));
#187617=CARTESIAN_POINT('Ctrl Pts',(198.472906089028,0.555720791400502,
136.697062976703));
#187618=CARTESIAN_POINT('Ctrl Pts',(198.480302445963,0.398483782675044,
136.707676739666));
#187619=CARTESIAN_POINT('Ctrl Pts',(198.4876999353,0.241222700562017,136.718292127623));
#187620=CARTESIAN_POINT('Ctrl Pts',(198.495097424636,0.0835648236240816,
136.722617295928));
#187621=CARTESIAN_POINT('Ctrl Pts',(198.502494913973,-0.0739494677253907,
136.720648477257));
#187622=CARTESIAN_POINT('Ctrl Pts',(198.509894996488,-0.231518975465559,
136.718678968419));
#187623=CARTESIAN_POINT('Ctrl Pts',(198.517295079003,-0.388944424367331,
136.710411084445));
#187624=CARTESIAN_POINT('Ctrl Pts',(198.524695161518,-0.545688000420484,
136.695893115032));
#187625=CARTESIAN_POINT('Ctrl Pts',(198.532103381184,-0.702603932149111,
136.681359181619));
#187626=CARTESIAN_POINT('Ctrl Pts',(198.539511600851,-0.858836121715699,
136.660561472159));
#187627=CARTESIAN_POINT('Ctrl Pts',(198.546919820517,-1.01385369294746,
136.633599954889));
#187628=CARTESIAN_POINT('Ctrl Pts',(198.55433259982,-1.16896667490789,136.606621843255));
#187629=CARTESIAN_POINT('Ctrl Pts',(198.561745379122,-1.32286318481004,
136.573472442769));
#187630=CARTESIAN_POINT('Ctrl Pts',(198.569158158424,-1.47502554766598,
136.534302170168));
#187631=CARTESIAN_POINT('Ctrl Pts',(198.576581529452,-1.62740532724162,
136.495075929244));
#187632=CARTESIAN_POINT('Ctrl Pts',(198.584004900481,-1.77804565442718,
136.449811741413));
#187633=CARTESIAN_POINT('Ctrl Pts',(198.59142827151,-1.92644614760085,136.398709176862));
#187634=CARTESIAN_POINT('Ctrl Pts',(198.595364320951,-2.00513164990258,
136.371613370947));
#187635=CARTESIAN_POINT('Ctrl Pts',(198.599300370392,-2.083187811426,136.34287698262));
#187636=CARTESIAN_POINT('Ctrl Pts',(198.603236419832,-2.16054276008407,
136.312535046934));
#187637=CARTESIAN_POINT('Ctrl Pts',(198.610659686238,-2.30643177908773,
136.255311103171));
#187638=CARTESIAN_POINT('Ctrl Pts',(198.618082952643,-2.4502663863924,136.192200621447));
#187639=CARTESIAN_POINT('Ctrl Pts',(198.625506219049,-2.59153626383937,
136.12337089728));
#187640=CARTESIAN_POINT('Ctrl Pts',(198.63292071177,-2.73263917202303,136.054622524132));
#187641=CARTESIAN_POINT('Ctrl Pts',(198.640335204491,-2.87118305185535,
135.980168525608));
#187642=CARTESIAN_POINT('Ctrl Pts',(198.647749697212,-3.00667515047484,
135.900225127344));
#187643=CARTESIAN_POINT('Ctrl Pts',(198.655157043566,-3.14203665670858,
135.820358781537));
#187644=CARTESIAN_POINT('Ctrl Pts',(198.662564389919,-3.27435191817235,
135.735013757533));
#187645=CARTESIAN_POINT('Ctrl Pts',(198.669971736273,-3.40315059928627,
135.644453236626));
#187646=CARTESIAN_POINT('Ctrl Pts',(198.677373557949,-3.53185321748438,
135.553960259172));
#187647=CARTESIAN_POINT('Ctrl Pts',(198.684775379624,-3.65704417362253,
135.458259743947));
#187648=CARTESIAN_POINT('Ctrl Pts',(198.692177201299,-3.77828017388039,
135.357659365744));
#187649=CARTESIAN_POINT('Ctrl Pts',(198.699575115611,-3.89945217459736,
135.257112093699));
#187650=CARTESIAN_POINT('Ctrl Pts',(198.706973029922,-4.01667309082048,
135.151670347788));
#187651=CARTESIAN_POINT('Ctrl Pts',(198.714370944233,-4.12953101835425,
135.041683372673));
#187652=CARTESIAN_POINT('Ctrl Pts',(198.721767629146,-4.24237019094798,
134.931714675399));
#187653=CARTESIAN_POINT('Ctrl Pts',(198.729164314058,-4.35084754678297,
134.81720250832));
#187654=CARTESIAN_POINT('Ctrl Pts',(198.73656099897,-4.45458643666219,134.69853450182));
#187655=CARTESIAN_POINT('Ctrl Pts',(198.743957355906,-4.55832072665023,
134.579871757183));
#187656=CARTESIAN_POINT('Ctrl Pts',(198.751353712841,-4.65731672275938,
134.457053820572));
#187657=CARTESIAN_POINT('Ctrl Pts',(198.758750069776,-4.75123682608077,
134.330502870084));
#187658=CARTESIAN_POINT('Ctrl Pts',(198.766147559113,-4.84517130880985,
134.203932544323));
#187659=CARTESIAN_POINT('Ctrl Pts',(198.77354504845,-4.93402812889303,134.073628366469));
#187660=CARTESIAN_POINT('Ctrl Pts',(198.780942537786,-5.01751202795966,
133.940042937537));
#187661=CARTESIAN_POINT('Ctrl Pts',(198.788342620301,-5.10102519217775,
133.80641068044));
#187662=CARTESIAN_POINT('Ctrl Pts',(198.795742702816,-5.17916148769389,
133.669495198516));
#187663=CARTESIAN_POINT('Ctrl Pts',(198.803142785331,-5.25167084038773,
133.529775071685));
#187664=CARTESIAN_POINT('Ctrl Pts',(198.810551004998,-5.32425992456896,
133.389901308211));
#187665=CARTESIAN_POINT('Ctrl Pts',(198.817959224664,-5.39120953722308,
133.247217072428));
#187666=CARTESIAN_POINT('Ctrl Pts',(198.825367444331,-5.45231683291927,
133.102223040768));
#187667=CARTESIAN_POINT('Ctrl Pts',(198.832780223633,-5.51346173913636,
132.957139767702));
#187668=CARTESIAN_POINT('Ctrl Pts',(198.840193002935,-5.56875703240109,
132.809744214664));
#187669=CARTESIAN_POINT('Ctrl Pts',(198.847605782237,-5.61804944659764,
132.660553220203));
#187670=CARTESIAN_POINT('Ctrl Pts',(198.855029153265,-5.66741229210717,
132.511149054653));
#187671=CARTESIAN_POINT('Ctrl Pts',(198.862452524294,-5.71075502537524,
132.359944681874));
#187672=CARTESIAN_POINT('Ctrl Pts',(198.869875895323,-5.74797508196189,
132.207468959657));
#187673=CARTESIAN_POINT('Ctrl Pts',(198.873811944764,-5.76771004904698,
132.126622673133));
#187674=CARTESIAN_POINT('Ctrl Pts',(198.877747994205,-5.78572457362142,
132.045419093963));
#187675=CARTESIAN_POINT('Ctrl Pts',(198.881684043645,-5.80200928305024,
131.96393762747));
#187676=CARTESIAN_POINT('Ctrl Pts',(198.892415019576,-5.84640680080297,
131.741792131358));
#187677=CARTESIAN_POINT('Ctrl Pts',(198.903145995507,-5.87805736973165,
131.517021225439));
#187678=CARTESIAN_POINT('Ctrl Pts',(198.913876971438,-5.89671799543621,
131.290824845232));
#187679=CARTESIAN_POINT('Ctrl Pts',(198.921459583557,-5.90990377532492,
131.130992279687));
#187680=CARTESIAN_POINT('Ctrl Pts',(198.929042195676,-5.91660456247561,
130.970448251875));
#187681=CARTESIAN_POINT('Ctrl Pts',(198.936624807795,-5.91674765788855,
130.809625156515));
#187682=CARTESIAN_POINT('',(200.686624807795,-5.90698642445631,130.80494468951));
#187683=CARTESIAN_POINT('Ctrl Pts',(198.936625793059,-5.9188774747153,130.809606147102));
#187684=CARTESIAN_POINT('Ctrl Pts',(199.011127751193,-5.90425259497605,
129.228876773919));
#187685=CARTESIAN_POINT('Ctrl Pts',(199.178445583929,-4.43793552679426,
125.654919300417));
#187686=CARTESIAN_POINT('Ctrl Pts',(199.438579291272,1.60513008150291,123.992524011201));
#187687=CARTESIAN_POINT('Ctrl Pts',(199.717026915084,6.59860307470548,128.472837940681));
#187688=CARTESIAN_POINT('Ctrl Pts',(199.995474538897,5.52828220193623,135.095707309003));
#187689=CARTESIAN_POINT('Ctrl Pts',(200.27392216271,-0.622259942815148,
137.775038711833));
#187690=CARTESIAN_POINT('Ctrl Pts',(200.504305585676,-5.2380063121806,134.691886300211));
#187691=CARTESIAN_POINT('Ctrl Pts',(200.641873134038,-5.90782357734734,
131.759296891607));
#187692=CARTESIAN_POINT('Ctrl Pts',(200.686624807795,-5.90698642445631,
130.80494468951));
#187693=CARTESIAN_POINT('',(202.436624807795,-5.91672686803579,130.798894919773));
#187694=CARTESIAN_POINT('Ctrl Pts',(200.686624807795,-5.90698642445631,
130.80494468951));
#187695=CARTESIAN_POINT('Ctrl Pts',(200.734689008642,-5.90608730535493,
129.77995116259));
#187696=CARTESIAN_POINT('Ctrl Pts',(200.875569084094,-5.16390162333142,
126.774392662908));
#187697=CARTESIAN_POINT('Ctrl Pts',(201.109265034148,-0.373204209884669,
123.815921653964));
#187698=CARTESIAN_POINT('Ctrl Pts',(201.387712657962,5.67784563147399,126.712951384136));
#187699=CARTESIAN_POINT('Ctrl Pts',(201.666160281774,6.5112327157493,133.369786323417));
#187700=CARTESIAN_POINT('Ctrl Pts',(201.944607905587,1.36111502553663,137.669120366955));
#187701=CARTESIAN_POINT('Ctrl Pts',(202.201429414261,-4.54266270085758,
135.816111494225));
#187702=CARTESIAN_POINT('Ctrl Pts',(202.36543504833,-5.90274340491685,132.310756663458));
#187703=CARTESIAN_POINT('Ctrl Pts',(202.436624807795,-5.91672686803579,
130.798894919773));
#187704=CARTESIAN_POINT('',(204.186624807795,-5.92581928566479,130.806233519117));
#187705=CARTESIAN_POINT('Ctrl Pts',(202.436624807795,-5.91672686803579,
130.798894919773));
#187706=CARTESIAN_POINT('Ctrl Pts',(202.458250922934,-5.9209747821421,130.339619647749));
#187707=CARTESIAN_POINT('Ctrl Pts',(202.572692912681,-5.66197777958727,
127.913946320691));
#187708=CARTESIAN_POINT('Ctrl Pts',(202.779950777024,-2.32147802600033,
124.202217003606));
#187709=CARTESIAN_POINT('Ctrl Pts',(203.058398400839,4.2997548257633,125.28261551589));
#187710=CARTESIAN_POINT('Ctrl Pts',(203.336846024651,6.96972305013295,131.437228026285));
#187711=CARTESIAN_POINT('Ctrl Pts',(203.615293648464,3.23485627607878,137.010266301744));
#187712=CARTESIAN_POINT('Ctrl Pts',(203.893741272277,-3.4726853742618,136.880380435614));
#187713=CARTESIAN_POINT('Ctrl Pts',(204.084184992054,-5.87766124044895,
132.972676372107));
#187714=CARTESIAN_POINT('Ctrl Pts',(204.181812837227,-5.92623998325372,
130.908018473525));
#187715=CARTESIAN_POINT('Ctrl Pts',(204.186624807795,-5.92581928566479,
130.806233519117));
#187716=CARTESIAN_POINT('',(205.936623590202,-5.91340924895264,130.808944439334));
#187717=CARTESIAN_POINT('Ctrl Pts',(204.186624807795,-5.92581928566479,
130.806233519117));
#187718=CARTESIAN_POINT('Ctrl Pts',(204.274628711831,-5.91812534204668,
128.944735566654));
#187719=CARTESIAN_POINT('Ctrl Pts',(204.455448490471,-3.96770241261772,
125.106068119418));
#187720=CARTESIAN_POINT('Ctrl Pts',(204.729084143717,2.57533168687046,124.297039558175));
#187721=CARTESIAN_POINT('Ctrl Pts',(205.007531767529,6.86682325353852,129.453694210665));
#187722=CARTESIAN_POINT('Ctrl Pts',(205.285979391342,4.84803947518153,135.851545143624));
#187723=CARTESIAN_POINT('Ctrl Pts',(205.564427015155,-1.62585529160082,
137.611280375001));
#187724=CARTESIAN_POINT('Ctrl Pts',(205.781308123836,-5.50460122239126,
134.109769780245));
#187725=CARTESIAN_POINT('Ctrl Pts',(205.905373357914,-5.91576144076024,
131.474232650613));
#187726=CARTESIAN_POINT('Ctrl Pts',(205.936622717388,-5.911015738934,130.80896117583));
#187727=CARTESIAN_POINT('',(207.686626030528,-5.91241378256136,130.800689035563));
#187728=CARTESIAN_POINT('Ctrl Pts',(205.936624807795,-5.91674824245351,
130.808921091594));
#187729=CARTESIAN_POINT('Ctrl Pts',(205.944320535086,-5.91687464410253,
130.644927890423));
#187730=CARTESIAN_POINT('Ctrl Pts',(205.952016262377,-5.91017796225583,
130.480857837863));
#187731=CARTESIAN_POINT('Ctrl Pts',(205.959711989668,-5.89667042808694,
130.31732014181));
#187732=CARTESIAN_POINT('Ctrl Pts',(205.967107144318,-5.8836904587688,130.160169750732));
#187733=CARTESIAN_POINT('Ctrl Pts',(205.974502298968,-5.86442165241146,
130.003511317041));
#187734=CARTESIAN_POINT('Ctrl Pts',(205.981897453618,-5.83892794642443,
129.847882181341));
#187735=CARTESIAN_POINT('Ctrl Pts',(205.989293079306,-5.81343261660182,
129.692243132757));
#187736=CARTESIAN_POINT('Ctrl Pts',(205.996688704995,-5.78171165733105,
129.53763388078));
#187737=CARTESIAN_POINT('Ctrl Pts',(206.004084330683,-5.74388042102671,
129.384583074623));
#187738=CARTESIAN_POINT('Ctrl Pts',(206.011481882822,-5.70603933025007,
129.231492401015));
#187739=CARTESIAN_POINT('Ctrl Pts',(206.01887943496,-5.66208488256809,129.079961343446));
#187740=CARTESIAN_POINT('Ctrl Pts',(206.026276987099,-5.61218269697228,
128.930504716408));
#187741=CARTESIAN_POINT('Ctrl Pts',(206.033677921977,-5.56225769219368,
128.780979746109));
#187742=CARTESIAN_POINT('Ctrl Pts',(206.041078856855,-5.50637965184727,
128.633531448377));
#187743=CARTESIAN_POINT('Ctrl Pts',(206.048479791733,-5.44476278582211,
128.488655807227));
#187744=CARTESIAN_POINT('Ctrl Pts',(206.055889603669,-5.38307201339005,
128.343606394855));
#187745=CARTESIAN_POINT('Ctrl Pts',(206.063299415605,-5.31562881696656,
128.201136143459));
#187746=CARTESIAN_POINT('Ctrl Pts',(206.070709227541,-5.24269425134762,
128.06171817835));
#187747=CARTESIAN_POINT('Ctrl Pts',(206.078124284764,-5.16970805651977,
127.922201521501));
#187748=CARTESIAN_POINT('Ctrl Pts',(206.085539341988,-5.09122293266157,
127.785741777807));
#187749=CARTESIAN_POINT('Ctrl Pts',(206.092954399211,-5.00754363174057,
127.652783656945));
#187750=CARTESIAN_POINT('Ctrl Pts',(206.100380033849,-4.92374496414771,
127.519635874265));
#187751=CARTESIAN_POINT('Ctrl Pts',(206.107805668488,-4.83473753693092,
127.389999992524));
#187752=CARTESIAN_POINT('Ctrl Pts',(206.115231303126,-4.74086717656672,
127.264288728938));
#187753=CARTESIAN_POINT('Ctrl Pts',(206.117261623011,-4.71520110645441,
127.229916706794));
#187754=CARTESIAN_POINT('Ctrl Pts',(206.119291942896,-4.68917170648531,
127.195837875561));
#187755=CARTESIAN_POINT('Ctrl Pts',(206.121322262781,-4.66278652276695,
127.162060189869));
#187756=CARTESIAN_POINT('Ctrl Pts',(206.128745542087,-4.56631670550191,
127.038561820438));
#187757=CARTESIAN_POINT('Ctrl Pts',(206.136168821393,-4.46479117026267,
126.918712002184));
#187758=CARTESIAN_POINT('Ctrl Pts',(206.1435921007,-4.35851586193957,126.802952110088));
#187759=CARTESIAN_POINT('Ctrl Pts',(206.151006606373,-4.25236616125308,
126.687329035533));
#187760=CARTESIAN_POINT('Ctrl Pts',(206.158421112046,-4.14147811176257,
126.575786537499));
#187761=CARTESIAN_POINT('Ctrl Pts',(206.165835617719,-4.02619954292322,
126.4687351952));
#187762=CARTESIAN_POINT('Ctrl Pts',(206.173242977064,-3.9110320831151,126.361787032278));
#187763=CARTESIAN_POINT('Ctrl Pts',(206.180650336408,-3.79148280018012,
126.259321659787));
#187764=CARTESIAN_POINT('Ctrl Pts',(206.188057695753,-3.66793813141363,
126.161714774232));
#187765=CARTESIAN_POINT('Ctrl Pts',(206.195459530445,-3.54448560632645,
126.064180687105));
#187766=CARTESIAN_POINT('Ctrl Pts',(206.202861365137,-3.41704392042245,
125.971498102217));
#187767=CARTESIAN_POINT('Ctrl Pts',(206.210263199829,-3.28603443959317,
125.884004103622));
#187768=CARTESIAN_POINT('Ctrl Pts',(206.217661127171,-3.15509411728722,
125.796556292186));
#187769=CARTESIAN_POINT('Ctrl Pts',(206.225059054513,-3.02059006058692,
125.714291818989));
#187770=CARTESIAN_POINT('Ctrl Pts',(206.232456981854,-2.88297452136991,
125.637505822661));
#187771=CARTESIAN_POINT('Ctrl Pts',(206.239853679775,-2.74538185171612,
125.560732586972));
#187772=CARTESIAN_POINT('Ctrl Pts',(206.247250377697,-2.60467905146201,
125.489436202917));
#187773=CARTESIAN_POINT('Ctrl Pts',(206.254647075618,-2.4613451038374,125.423867067499));
#187774=CARTESIAN_POINT('Ctrl Pts',(206.262043445548,-2.3180175120597,125.358300839608));
#187775=CARTESIAN_POINT('Ctrl Pts',(206.269439815478,-2.1720593443594,125.298461510681));
#187776=CARTESIAN_POINT('Ctrl Pts',(206.276836185407,-2.02397155401354,
125.244552193614));
#187777=CARTESIAN_POINT('Ctrl Pts',(206.284233687713,-1.87586109160203,
125.190634623095));
#187778=CARTESIAN_POINT('Ctrl Pts',(206.291631190018,-1.72562070814953,
125.142648999845));
#187779=CARTESIAN_POINT('Ctrl Pts',(206.299028692324,-1.57376843488975,
125.100749176045));
#187780=CARTESIAN_POINT('Ctrl Pts',(206.306428787771,-1.42186293089913,
125.058834664561));
#187781=CARTESIAN_POINT('Ctrl Pts',(206.313828883218,-1.26834477174244,
125.023010299208));
#187782=CARTESIAN_POINT('Ctrl Pts',(206.321228978665,-1.1137439959854,124.993379213887));
#187783=CARTESIAN_POINT('Ctrl Pts',(206.328637211142,-0.958973223613178,
124.963715546683));
#187784=CARTESIAN_POINT('Ctrl Pts',(206.336045443619,-0.803117824125187,
124.940258829909));
#187785=CARTESIAN_POINT('Ctrl Pts',(206.343453676096,-0.646715539100822,
124.923060627429));
#187786=CARTESIAN_POINT('Ctrl Pts',(206.35086646816,-0.490216992290331,
124.905851839875));
#187787=CARTESIAN_POINT('Ctrl Pts',(206.358279260223,-0.333171260766503,
124.894909268023));
#187788=CARTESIAN_POINT('Ctrl Pts',(206.365692052287,-0.176117430763197,
124.890232345954));
#187789=CARTESIAN_POINT('Ctrl Pts',(206.373115435889,-0.0188391992448544,
124.885548741409));
#187790=CARTESIAN_POINT('Ctrl Pts',(206.380538819491,0.13844678157505,124.887148662973));
#187791=CARTESIAN_POINT('Ctrl Pts',(206.387962203094,0.295204371712296,
124.894979521256));
#187792=CARTESIAN_POINT('Ctrl Pts',(206.391898097594,0.378317594721756,
124.899131459738));
#187793=CARTESIAN_POINT('Ctrl Pts',(206.395833992093,0.461282402246363,
124.905034131635));
#187794=CARTESIAN_POINT('Ctrl Pts',(206.399769886593,0.544020024813092,
124.912673866295));
#187795=CARTESIAN_POINT('Ctrl Pts',(206.407193124759,0.700066147897168,
124.927082679821));
#187796=CARTESIAN_POINT('Ctrl Pts',(206.414616362924,0.855775400938864,
124.947717077111));
#187797=CARTESIAN_POINT('Ctrl Pts',(206.42203960109,1.0106110768226,124.974558235503));
#187798=CARTESIAN_POINT('Ctrl Pts',(206.429454065568,1.1652637490334,125.001367669744));
#187799=CARTESIAN_POINT('Ctrl Pts',(206.436868530046,1.31904453505951,125.034369199787));
#187800=CARTESIAN_POINT('Ctrl Pts',(206.444282994524,1.47141999714576,125.07349211842));
#187801=CARTESIAN_POINT('Ctrl Pts',(206.451690312658,1.62364859393998,125.11257732889));
#187802=CARTESIAN_POINT('Ctrl Pts',(206.459097630792,1.77447420420068,125.157772089943));
#187803=CARTESIAN_POINT('Ctrl Pts',(206.466504948926,1.92337186920565,125.208954357494));
#187804=CARTESIAN_POINT('Ctrl Pts',(206.47390674243,2.07215848127999,125.260098451574));
#187805=CARTESIAN_POINT('Ctrl Pts',(206.481308535935,2.21901965969763,125.317221039542));
#187806=CARTESIAN_POINT('Ctrl Pts',(206.48871032944,2.36344405149433,125.380149819859));
#187807=CARTESIAN_POINT('Ctrl Pts',(206.496108215656,2.50779220395472,125.443045381076));
#187808=CARTESIAN_POINT('Ctrl Pts',(206.503506101871,2.64970579024399,125.511740881817));
#187809=CARTESIAN_POINT('Ctrl Pts',(206.510903988087,2.78869205246822,125.586015362698));
#187810=CARTESIAN_POINT('Ctrl Pts',(206.518300645105,2.92765522138042,125.660277502477));
#187811=CARTESIAN_POINT('Ctrl Pts',(206.525697302122,3.06369170265306,125.740116606851));
#187812=CARTESIAN_POINT('Ctrl Pts',(206.533093959139,3.19633193171053,125.825265042582));
#187813=CARTESIAN_POINT('Ctrl Pts',(206.540490288307,3.32896628161558,125.910409704189));
#187814=CARTESIAN_POINT('Ctrl Pts',(206.547886617474,3.45820436447894,126.000863027573));
#187815=CARTESIAN_POINT('Ctrl Pts',(206.555282946642,3.58360452178626,126.096313337224));
#187816=CARTESIAN_POINT('Ctrl Pts',(206.562680408361,3.70902388080001,126.191778262557));
#187817=CARTESIAN_POINT('Ctrl Pts',(206.57007787008,3.83060384705553,126.292241471571));
#187818=CARTESIAN_POINT('Ctrl Pts',(206.577475331799,3.94793497542389,126.397350293965));
#187819=CARTESIAN_POINT('Ctrl Pts',(206.584875386871,4.06530723695059,126.502495964703));
#187820=CARTESIAN_POINT('Ctrl Pts',(206.592275441942,4.17842741707443,126.612290242479));
#187821=CARTESIAN_POINT('Ctrl Pts',(206.599675497014,4.28692225118017,126.726342940454));
#187822=CARTESIAN_POINT('Ctrl Pts',(206.607083689639,4.39553639284793,126.840521057759));
#187823=CARTESIAN_POINT('Ctrl Pts',(206.614491882264,4.49951477334651,126.958966676524));
#187824=CARTESIAN_POINT('Ctrl Pts',(206.621900074889,4.59852335176967,127.081255254334));
#187825=CARTESIAN_POINT('Ctrl Pts',(206.629312827337,4.69759287104336,127.203619102085));
#187826=CARTESIAN_POINT('Ctrl Pts',(206.636725579785,4.79168627026316,127.329830323613));
#187827=CARTESIAN_POINT('Ctrl Pts',(206.644138332232,4.88051264007905,127.459435067942));
#187828=CARTESIAN_POINT('Ctrl Pts',(206.651561676931,4.96946593591552,127.589225007439));
#187829=CARTESIAN_POINT('Ctrl Pts',(206.658985021629,5.05313697283413,127.722417839174));
#187830=CARTESIAN_POINT('Ctrl Pts',(206.666408366327,5.13128020290801,127.85853407112));
#187831=CARTESIAN_POINT('Ctrl Pts',(206.670344747687,5.17271725948344,127.930712505499));
#187832=CARTESIAN_POINT('Ctrl Pts',(206.674281129047,5.21260076983565,128.003712593246));
#187833=CARTESIAN_POINT('Ctrl Pts',(206.678217510406,5.25089964747057,128.077460646043));
#187834=CARTESIAN_POINT('Ctrl Pts',(206.685640788461,5.32312415823054,128.216535662379));
#187835=CARTESIAN_POINT('Ctrl Pts',(206.693064066516,5.38992876580882,128.358692359875));
#187836=CARTESIAN_POINT('Ctrl Pts',(206.70048734457,5.45103920233565,128.503469012753));
#187837=CARTESIAN_POINT('Ctrl Pts',(206.707901848764,5.51207741006388,128.648074548481));
#187838=CARTESIAN_POINT('Ctrl Pts',(206.715316352958,5.56743469941649,128.795293535183));
#187839=CARTESIAN_POINT('Ctrl Pts',(206.722730857152,5.61688222173231,128.944638952992));
#187840=CARTESIAN_POINT('Ctrl Pts',(206.730138214794,5.66628208350656,129.093840422567));
#187841=CARTESIAN_POINT('Ctrl Pts',(206.737545572436,5.70978340170099,129.245163890933));
#187842=CARTESIAN_POINT('Ctrl Pts',(206.744952930079,5.74720510199896,129.398101723174));
#187843=CARTESIAN_POINT('Ctrl Pts',(206.752354762849,5.78459889084789,129.550925484796));
#187844=CARTESIAN_POINT('Ctrl Pts',(206.75975659562,5.81592200238041,129.705360851741));
#187845=CARTESIAN_POINT('Ctrl Pts',(206.76715842839,5.84104299956862,129.860884470708));
#187846=CARTESIAN_POINT('Ctrl Pts',(206.774556353595,5.86615073491324,130.016325985852));
#187847=CARTESIAN_POINT('Ctrl Pts',(206.7819542788,5.88506281728915,130.172854241269));
#187848=CARTESIAN_POINT('Ctrl Pts',(206.789352204005,5.89769879798555,130.3299352275));
#187849=CARTESIAN_POINT('Ctrl Pts',(206.796748899477,5.91033267824449,130.486990102675));
#187850=CARTESIAN_POINT('Ctrl Pts',(206.804145594949,5.916692497478,130.644597154582));
#187851=CARTESIAN_POINT('Ctrl Pts',(206.811542290421,5.91674961156377,130.802216658626));
#187852=CARTESIAN_POINT('Ctrl Pts',(206.818938657709,5.91680672311545,130.959829169243));
#187853=CARTESIAN_POINT('Ctrl Pts',(206.826335024996,5.91056168541346,131.117453757603));
#187854=CARTESIAN_POINT('Ctrl Pts',(206.833731392284,5.89803799224905,131.274550371269));
#187855=CARTESIAN_POINT('Ctrl Pts',(206.841128891757,5.88551238204311,131.431671032212));
#187856=CARTESIAN_POINT('Ctrl Pts',(206.84852639123,5.86670623237614,131.588263185401));
#187857=CARTESIAN_POINT('Ctrl Pts',(206.855923890704,5.84169493924943,131.743791721611));
#187858=CARTESIAN_POINT('Ctrl Pts',(206.863323983131,5.81667487922173,131.899374773326));
#187859=CARTESIAN_POINT('Ctrl Pts',(206.870724075559,5.78544540453325,132.053893097456));
#187860=CARTESIAN_POINT('Ctrl Pts',(206.878124167987,5.74813303139715,132.206821745677));
#187861=CARTESIAN_POINT('Ctrl Pts',(206.885532397177,5.71077963148513,132.359918546412));
#187862=CARTESIAN_POINT('Ctrl Pts',(206.892940626368,5.66733006440155,132.511421817633));
#187863=CARTESIAN_POINT('Ctrl Pts',(206.900348855559,5.61796095210065,132.660821040837));
#187864=CARTESIAN_POINT('Ctrl Pts',(206.907761644179,5.56856145534386,132.810312212507));
#187865=CARTESIAN_POINT('Ctrl Pts',(206.9151744328,5.51323528469942,132.957696407142));
#187866=CARTESIAN_POINT('Ctrl Pts',(206.922587221421,5.4522070340239,133.102483551754));
#187867=CARTESIAN_POINT('Ctrl Pts',(206.930010601367,5.39109158672778,133.247477566947));
#187868=CARTESIAN_POINT('Ctrl Pts',(206.937433981314,5.32425794604404,133.389866784103));
#187869=CARTESIAN_POINT('Ctrl Pts',(206.944857361261,5.25197679745634,133.529185434225));
#187870=CARTESIAN_POINT('Ctrl Pts',(206.948793285581,5.21365286245805,133.603053088456));
#187871=CARTESIAN_POINT('Ctrl Pts',(206.9527292099,5.17379827248528,133.67605802251));
#187872=CARTESIAN_POINT('Ctrl Pts',(206.956665134219,5.13245820404137,133.748134275011));
#187873=CARTESIAN_POINT('Ctrl Pts',(206.964088477532,5.05448883884311,133.884073567444));
#187874=CARTESIAN_POINT('Ctrl Pts',(206.971511820845,4.97099709000868,134.017118578131));
#187875=CARTESIAN_POINT('Ctrl Pts',(206.978935164159,4.8822231829641,134.146788979435));
#187876=CARTESIAN_POINT('Ctrl Pts',(206.986349734158,4.79355419377888,134.276306129166));
#187877=CARTESIAN_POINT('Ctrl Pts',(206.993764304158,4.69961568142008,134.402456303235));
#187878=CARTESIAN_POINT('Ctrl Pts',(207.001178874158,4.60069370173865,134.524783715183));
#187879=CARTESIAN_POINT('Ctrl Pts',(207.008586298086,4.50186706186089,134.646993229456));
#187880=CARTESIAN_POINT('Ctrl Pts',(207.015993722013,4.39806674964955,134.76538702808));
#187881=CARTESIAN_POINT('Ctrl Pts',(207.02340114594,4.2896219877561,134.879538376224));
#187882=CARTESIAN_POINT('Ctrl Pts',(207.030803045408,4.18125810400504,134.993604590251));
#187883=CARTESIAN_POINT('Ctrl Pts',(207.038204944876,4.06825692352974,135.103434384324));
#187884=CARTESIAN_POINT('Ctrl Pts',(207.045606844344,3.9509877230448,135.208634289223));
#187885=CARTESIAN_POINT('Ctrl Pts',(207.053004836591,3.8337804251313,135.313778662536));
#187886=CARTESIAN_POINT('Ctrl Pts',(207.060402828839,3.71230987122733,135.414297765317));
#187887=CARTESIAN_POINT('Ctrl Pts',(207.067800821086,3.58698186339951,135.509835266753));
#187888=CARTESIAN_POINT('Ctrl Pts',(207.0751975839,3.46167468317873,135.605356891311));
#187889=CARTESIAN_POINT('Ctrl Pts',(207.082594346714,3.33251161790928,135.695898331514));
#187890=CARTESIAN_POINT('Ctrl Pts',(207.089991109528,3.19993127924519,135.781143752344));
#187891=CARTESIAN_POINT('Ctrl Pts',(207.097387544336,3.06735681979036,135.866385393008));
#187892=CARTESIAN_POINT('Ctrl Pts',(207.104783979144,2.93136570223466,135.946331279376));
#187893=CARTESIAN_POINT('Ctrl Pts',(207.112180413952,2.79242499555474,136.020709264532));
#187894=CARTESIAN_POINT('Ctrl Pts',(207.119577981065,2.65346301872775,136.095098636061));
#187895=CARTESIAN_POINT('Ctrl Pts',(207.126975548178,2.51155088280885,136.163918232992));
#187896=CARTESIAN_POINT('Ctrl Pts',(207.134373115291,2.36717955207727,136.226942247263));
#187897=CARTESIAN_POINT('Ctrl Pts',(207.141773275419,2.22275761591827,136.289988352881));
#187898=CARTESIAN_POINT('Ctrl Pts',(207.149173435547,2.07587511060173,136.347234681915));
#187899=CARTESIAN_POINT('Ctrl Pts',(207.156573595675,1.92704208331791,136.398503927459));
#187900=CARTESIAN_POINT('Ctrl Pts',(207.163981892314,1.7780454134245,136.449829543778));
#187901=CARTESIAN_POINT('Ctrl Pts',(207.171390188953,1.62709429179282,136.495164830576));
#187902=CARTESIAN_POINT('Ctrl Pts',(207.178798485592,1.47471370865867,136.534382436023));
#187903=CARTESIAN_POINT('Ctrl Pts',(207.186211341619,1.32223934388331,136.573624177691));
#187904=CARTESIAN_POINT('Ctrl Pts',(207.193624197646,1.16833412867738,136.606740657254));
#187905=CARTESIAN_POINT('Ctrl Pts',(207.201037053673,1.01353178190939,136.633655934288));
#187906=CARTESIAN_POINT('Ctrl Pts',(207.208460500376,0.858508270520578,
136.660609664919));
#187907=CARTESIAN_POINT('Ctrl Pts',(207.215883947078,0.702585436732427,
136.681344449338));
#187908=CARTESIAN_POINT('Ctrl Pts',(207.223307393781,0.546301465452972,
136.695836262202));
#187909=CARTESIAN_POINT('Ctrl Pts',(207.227242515198,0.463456336076836,
136.703518279122));
#187910=CARTESIAN_POINT('Ctrl Pts',(207.231177636615,0.38050972967095,136.709446907009));
#187911=CARTESIAN_POINT('Ctrl Pts',(207.235112758032,0.297541510646655,
136.713624498283));
#187912=CARTESIAN_POINT('Ctrl Pts',(207.242535825934,0.141033322402311,
136.72150495238));
#187913=CARTESIAN_POINT('Ctrl Pts',(207.249958893836,-0.0160248826544751,
136.723175299195));
#187914=CARTESIAN_POINT('Ctrl Pts',(207.257381961737,-0.17309917929533,
136.71857799915));
#187915=CARTESIAN_POINT('Ctrl Pts',(207.264796255826,-0.329987819465992,
136.713986132956));
#187916=CARTESIAN_POINT('Ctrl Pts',(207.272210549914,-0.486892143847507,
136.703141376656));
#187917=CARTESIAN_POINT('Ctrl Pts',(207.279624844002,-0.643274099441511,
136.68603801398));
#187918=CARTESIAN_POINT('Ctrl Pts',(207.28703199178,-0.799505325385146,
136.668951136479));
#187919=CARTESIAN_POINT('Ctrl Pts',(207.294439139558,-0.955214816271548,
136.645617702214));
#187920=CARTESIAN_POINT('Ctrl Pts',(207.301846287336,-1.10986562624154,
136.616084015508));
#187921=CARTESIAN_POINT('Ctrl Pts',(207.309247910677,-1.26440109375863,
136.586572355766));
#187922=CARTESIAN_POINT('Ctrl Pts',(207.316649534019,-1.41787908742527,
136.550869720914));
#187923=CARTESIAN_POINT('Ctrl Pts',(207.32405115736,-1.56976899679204,136.509074094964));
#187924=CARTESIAN_POINT('Ctrl Pts',(207.331448873763,-1.72157873124577,
136.467300530788));
#187925=CARTESIAN_POINT('Ctrl Pts',(207.338846590166,-1.87180169182007,
136.419440479476));
#187926=CARTESIAN_POINT('Ctrl Pts',(207.34624430657,-2.01991876954609,136.365642729358));
#187927=CARTESIAN_POINT('Ctrl Pts',(207.353640794833,-2.16801125746096,
136.311853910529));
#187928=CARTESIAN_POINT('Ctrl Pts',(207.361037283097,-2.31399820584744,
136.252129476629));
#187929=CARTESIAN_POINT('Ctrl Pts',(207.36843377136,-2.4573768406137,136.186667708927));
#187930=CARTESIAN_POINT('Ctrl Pts',(207.375829932446,-2.60074913313828,
136.121208836875));
#187931=CARTESIAN_POINT('Ctrl Pts',(207.383226093531,-2.7415130018506,136.050013290682));
#187932=CARTESIAN_POINT('Ctrl Pts',(207.390622254617,-2.87918704637743,
135.973326908274));
#187933=CARTESIAN_POINT('Ctrl Pts',(207.398019549068,-3.01688218766657,
135.896628774672));
#187934=CARTESIAN_POINT('Ctrl Pts',(207.40541684352,-3.15148623585924,135.814438311193));
#187935=CARTESIAN_POINT('Ctrl Pts',(207.412814137971,-3.28254386071344,
135.727046506894));
#187936=CARTESIAN_POINT('Ctrl Pts',(207.420214026732,-3.41364744886641,
135.639624053363));
#187937=CARTESIAN_POINT('Ctrl Pts',(207.427613915493,-3.5412018269446,135.546996834099));
#187938=CARTESIAN_POINT('Ctrl Pts',(207.435013804254,-3.66478215559698,
135.449498109021));
#187939=CARTESIAN_POINT('Ctrl Pts',(207.442421832859,-3.78849842204456,
135.351892135792));
#187940=CARTESIAN_POINT('Ctrl Pts',(207.449829861464,-3.90823161575698,
135.249404186581));
#187941=CARTESIAN_POINT('Ctrl Pts',(207.457237890069,-4.02359084921884,
135.142407095024));
#187942=CARTESIAN_POINT('Ctrl Pts',(207.464650479546,-4.13902110546382,
135.035344128971));
#187943=CARTESIAN_POINT('Ctrl Pts',(207.472063069024,-4.25007177278625,
134.923766752786));
#187944=CARTESIAN_POINT('Ctrl Pts',(207.479475658502,-4.35639050034371,
134.80808293199));
#187945=CARTESIAN_POINT('Ctrl Pts',(207.486898843278,-4.4628611961998,134.692233756756));
#187946=CARTESIAN_POINT('Ctrl Pts',(207.494322028054,-4.56458620292865,
134.572266697968));
#187947=CARTESIAN_POINT('Ctrl Pts',(207.501745212829,-4.66125443395861,
134.448621539125));
#187948=CARTESIAN_POINT('Ctrl Pts',(207.505683602501,-4.71254201121785,
134.383021283805));
#187949=CARTESIAN_POINT('Ctrl Pts',(207.509621992173,-4.76240691754465,
134.316386173422));
#187950=CARTESIAN_POINT('Ctrl Pts',(207.513560381845,-4.81080786236673,
134.248784847229));
#187951=CARTESIAN_POINT('Ctrl Pts',(207.521051269147,-4.90286732147384,
134.120205920782));
#187952=CARTESIAN_POINT('Ctrl Pts',(207.528542156449,-4.98990483109686,
133.987743324545));
#187953=CARTESIAN_POINT('Ctrl Pts',(207.53603304375,-5.07157846591888,133.851822254163));
#187954=CARTESIAN_POINT('Ctrl Pts',(207.54351476451,-5.15315215733145,133.716067509366));
#187955=CARTESIAN_POINT('Ctrl Pts',(207.55099648527,-5.22937485457269,133.576863024161));
#187956=CARTESIAN_POINT('Ctrl Pts',(207.558478206029,-5.29994590927854,
133.43466552788));
#187957=CARTESIAN_POINT('Ctrl Pts',(207.565952157474,-5.37044368021443,
133.292615695094));
#187958=CARTESIAN_POINT('Ctrl Pts',(207.57342610892,-5.43530133283299,133.14757936331));
#187959=CARTESIAN_POINT('Ctrl Pts',(207.580900060365,-5.49426246614916,
133.000040584129));
#187960=CARTESIAN_POINT('Ctrl Pts',(207.588367634612,-5.55317329048832,
132.852627693386));
#187961=CARTESIAN_POINT('Ctrl Pts',(207.595835208858,-5.60619748008959,
132.702716943955));
#187962=CARTESIAN_POINT('Ctrl Pts',(207.603302783105,-5.65312540941891,
132.550815216999));
#187963=CARTESIAN_POINT('Ctrl Pts',(207.610764849886,-5.70001872858317,
132.399025520213));
#187964=CARTESIAN_POINT('Ctrl Pts',(207.618226916666,-5.74082463923422,
132.245248118835));
#187965=CARTESIAN_POINT('Ctrl Pts',(207.625688983447,-5.7753823822878,132.090007886789));
#187966=CARTESIAN_POINT('Ctrl Pts',(207.633147775048,-5.80992495758146,
131.934835791327));
#187967=CARTESIAN_POINT('Ctrl Pts',(207.640606566648,-5.83822474834227,
131.77820249896));
#187968=CARTESIAN_POINT('Ctrl Pts',(207.648065358248,-5.86017137152786,
131.620646142873));
#187969=CARTESIAN_POINT('Ctrl Pts',(207.655522975005,-5.88211453787134,
131.463114603699));
#187970=CARTESIAN_POINT('Ctrl Pts',(207.662980591761,-5.89770647524173,
131.304660650403));
#187971=CARTESIAN_POINT('Ctrl Pts',(207.670438208517,-5.9068882401741,131.145830792827));
#187972=CARTESIAN_POINT('Ctrl Pts',(207.67583374161,-5.9135311823046,131.030918511774));
#187973=CARTESIAN_POINT('Ctrl Pts',(207.681229274702,-5.91681984302548,
130.91580966449));
#187974=CARTESIAN_POINT('Ctrl Pts',(207.686624807795,-5.91674887527788,
130.800712412811));
#187975=CARTESIAN_POINT('Ctrl Pts',(207.686626923708,-5.90924709096476,
130.800671958988));
#187976=CARTESIAN_POINT('Ctrl Pts',(207.721753951025,-5.91343857842015,
130.052291188706));
#187977=CARTESIAN_POINT('Ctrl Pts',(207.849696852946,-5.433669738664,127.331654299026));
#187978=CARTESIAN_POINT('Ctrl Pts',(208.070455629472,-1.34028874287017,
123.935438990336));
#187979=CARTESIAN_POINT('Ctrl Pts',(208.348903253284,5.054696368039,125.964103710928));
#187980=CARTESIAN_POINT('Ctrl Pts',(208.627350877096,6.80417363260146,132.440391727885));
#187981=CARTESIAN_POINT('Ctrl Pts',(208.90579850091,2.30187076695336,137.413882217603));
#187982=CARTESIAN_POINT('Ctrl Pts',(209.175555710051,-4.11089059224102,
136.346724719354));
#187983=CARTESIAN_POINT('Ctrl Pts',(209.352497044589,-5.91202822503604,
132.582291201825));
#187984=CARTESIAN_POINT('Ctrl Pts',(209.436622504522,-5.92383576977198,
130.80157570118));
#187985=CARTESIAN_POINT('Origin',(213.235140564004,0.,130.804360617566));
#187986=CARTESIAN_POINT('',(-258.389859436029,-4.91824857376509,130.800615065845));
#187987=CARTESIAN_POINT('Ctrl Pts',(-258.319801180436,-4.76405452823419,
129.582490119309));
#187988=CARTESIAN_POINT('Ctrl Pts',(-258.327575080909,-4.79806489326847,
129.715096016398));
#187989=CARTESIAN_POINT('Ctrl Pts',(-258.335348981381,-4.82649184728085,
129.8489564752));
#187990=CARTESIAN_POINT('Ctrl Pts',(-258.343122881853,-4.84927537315292,
129.983561362064));
#187991=CARTESIAN_POINT('Ctrl Pts',(-258.34504967233,-4.85492235574935,
130.016923689642));
#187992=CARTESIAN_POINT('Ctrl Pts',(-258.346976462806,-4.86022290448851,
130.050331736036));
#187993=CARTESIAN_POINT('Ctrl Pts',(-258.348903253283,-4.86517660022172,
130.08377772077));
#187994=CARTESIAN_POINT('Ctrl Pts',(-258.362555314187,-4.90027546368103,
130.320755547965));
#187995=CARTESIAN_POINT('Ctrl Pts',(-258.376207375092,-4.91806560196264,
130.560356557379));
#187996=CARTESIAN_POINT('Ctrl Pts',(-258.389859435997,-4.91824857376465,
130.800615065277));
#187997=CARTESIAN_POINT('',(-259.999992532581,-4.31287516290238,128.44040399958));
#187998=CARTESIAN_POINT('Ctrl Pts',(-258.389859436029,-4.91824857376509,
130.800615065845));
#187999=CARTESIAN_POINT('Ctrl Pts',(-258.397511447859,-4.91835112986932,
130.935280517276));
#188000=CARTESIAN_POINT('Ctrl Pts',(-258.40516345969,-4.91291866327918,
131.070155068034));
#188001=CARTESIAN_POINT('Ctrl Pts',(-258.41281547152,-4.90192624921011,
131.204738076728));
#188002=CARTESIAN_POINT('Ctrl Pts',(-258.420459778954,-4.89094490280721,
131.339185581082));
#188003=CARTESIAN_POINT('Ctrl Pts',(-258.428104086388,-4.87441477518558,
131.473341728033));
#188004=CARTESIAN_POINT('Ctrl Pts',(-258.435748393821,-4.85236297429289,
131.606705074898));
#188005=CARTESIAN_POINT('Ctrl Pts',(-258.443731830625,-4.82933287505326,
131.745984906426));
#188006=CARTESIAN_POINT('Ctrl Pts',(-258.451715267428,-4.80027990481861,
131.884399532785));
#188007=CARTESIAN_POINT('Ctrl Pts',(-258.459698704231,-4.76529553161854,
132.02138221098));
#188008=CARTESIAN_POINT('Ctrl Pts',(-258.467334088494,-4.73183636620147,
132.152392878594));
#188009=CARTESIAN_POINT('Ctrl Pts',(-258.474969472757,-4.69295217675676,
132.282093385481));
#188010=CARTESIAN_POINT('Ctrl Pts',(-258.48260485702,-4.64877526646828,
132.409998056209));
#188011=CARTESIAN_POINT('Ctrl Pts',(-258.490238971884,-4.60460570069148,
132.537881462495));
#188012=CARTESIAN_POINT('Ctrl Pts',(-258.497873086747,-4.55514529512487,
132.663969245013));
#188013=CARTESIAN_POINT('Ctrl Pts',(-258.50550720161,-4.50057593422793,
132.787791816965));
#188014=CARTESIAN_POINT('Ctrl Pts',(-258.513141812779,-4.44600302568972,
132.91162243882));
#188015=CARTESIAN_POINT('Ctrl Pts',(-258.520776423949,-4.3863206644437,
133.033187188249));
#188016=CARTESIAN_POINT('Ctrl Pts',(-258.528411035118,-4.32175826677667,
133.152037883727));
#188017=CARTESIAN_POINT('Ctrl Pts',(-258.536047908509,-4.25717673853753,
133.270923796016));
#188018=CARTESIAN_POINT('Ctrl Pts',(-258.543684781901,-4.18771249147707,
133.387093701195));
#188019=CARTESIAN_POINT('Ctrl Pts',(-258.551321655292,-4.11363984045046,
133.50012587544));
#188020=CARTESIAN_POINT('Ctrl Pts',(-258.558966652433,-4.03948839439416,
133.613278288037));
#188021=CARTESIAN_POINT('Ctrl Pts',(-258.566611649574,-3.96071898158943,
133.723285970572));
#188022=CARTESIAN_POINT('Ctrl Pts',(-258.574256646714,-3.87764815134681,
133.829757761224));
#188023=CARTESIAN_POINT('Ctrl Pts',(-258.581906426395,-3.79452535384532,
133.936296158255));
#188024=CARTESIAN_POINT('Ctrl Pts',(-258.589556206076,-3.70709604330389,
134.039293954262));
#188025=CARTESIAN_POINT('Ctrl Pts',(-258.597205985756,-3.61571472858466,
134.13839571996));
#188026=CARTESIAN_POINT('Ctrl Pts',(-258.604866500394,-3.52420517820673,
134.237636555448));
#188027=CARTESIAN_POINT('Ctrl Pts',(-258.612527015032,-3.42873284137469,
134.332970167501));
#188028=CARTESIAN_POINT('Ctrl Pts',(-258.62018752967,-3.32968663806097,
134.424080213725));
#188029=CARTESIAN_POINT('Ctrl Pts',(-258.622575312145,-3.2988139356827,
134.452479215874));
#188030=CARTESIAN_POINT('Ctrl Pts',(-258.624963094621,-3.26759422865444,
134.48046818036));
#188031=CARTESIAN_POINT('Ctrl Pts',(-258.627350877096,-3.23603986999501,
134.508038387338));
#188032=CARTESIAN_POINT('Ctrl Pts',(-258.635127709651,-3.13326963599956,
134.597832531249));
#188033=CARTESIAN_POINT('Ctrl Pts',(-258.642904542206,-3.02659721906916,
134.683487383169));
#188034=CARTESIAN_POINT('Ctrl Pts',(-258.650681374762,-2.91639018574448,
134.764644868348));
#188035=CARTESIAN_POINT('Ctrl Pts',(-258.658448646073,-2.80631864669946,
134.845702574279));
#188036=CARTESIAN_POINT('Ctrl Pts',(-258.666215917384,-2.69272144950787,
134.922273685838));
#188037=CARTESIAN_POINT('Ctrl Pts',(-258.673983188696,-2.57600128484593,
134.994038462338));
#188038=CARTESIAN_POINT('Ctrl Pts',(-258.681742765027,-2.45939675401745,
135.065732141986));
#188039=CARTESIAN_POINT('Ctrl Pts',(-258.689502341359,-2.33967574347888,
135.132628759213));
#188040=CARTESIAN_POINT('Ctrl Pts',(-258.69726191769,-2.21727186503747,
135.194450427469));
#188041=CARTESIAN_POINT('Ctrl Pts',(-258.705015658649,-2.09496003701437,
135.256225604465));
#188042=CARTESIAN_POINT('Ctrl Pts',(-258.712769399607,-1.96996970432977,
135.312933253643));
#188043=CARTESIAN_POINT('Ctrl Pts',(-258.720523140566,-1.84276084284099,
135.36434039149));
#188044=CARTESIAN_POINT('Ctrl Pts',(-258.728273599587,-1.71560582524482,
135.415725770157));
#188045=CARTESIAN_POINT('Ctrl Pts',(-258.736024058607,-1.58623450800852,
135.461814953734));
#188046=CARTESIAN_POINT('Ctrl Pts',(-258.743774517628,-1.45512850411597,
135.502422356093));
#188047=CARTESIAN_POINT('Ctrl Pts',(-258.751523363193,-1.32404979326963,
135.543021304989));
#188048=CARTESIAN_POINT('Ctrl Pts',(-258.759272208759,-1.19123748701413,
135.578140627048));
#188049=CARTESIAN_POINT('Ctrl Pts',(-258.767021054325,-1.05718970734705,
135.60764418042));
#188050=CARTESIAN_POINT('Ctrl Pts',(-258.774769961837,-0.923140856050142,
135.637147969654));
#188051=CARTESIAN_POINT('Ctrl Pts',(-258.78251886935,-0.7878568931795,135.661035816665));
#188052=CARTESIAN_POINT('Ctrl Pts',(-258.790267776863,-0.651847129970203,
135.679222500907));
#188053=CARTESIAN_POINT('Ctrl Pts',(-258.79801842141,-0.515806878143327,
135.697413261966));
#188054=CARTESIAN_POINT('Ctrl Pts',(-258.805769065956,-0.379040889373938,
135.709900265377));
#188055=CARTESIAN_POINT('Ctrl Pts',(-258.813519710502,-0.24206421517884,
135.716650101934));
#188056=CARTESIAN_POINT('Ctrl Pts',(-258.821278578715,-0.104942204614877,
135.72340710027));
#188057=CARTESIAN_POINT('Ctrl Pts',(-258.829037446928,0.032390547106922,
135.724414752418));
#188058=CARTESIAN_POINT('Ctrl Pts',(-258.836796315141,0.169417802337889,
135.719691803839));
#188059=CARTESIAN_POINT('Ctrl Pts',(-258.844559321162,0.306518134269045,
135.71496633651));
#188060=CARTESIAN_POINT('Ctrl Pts',(-258.852322327183,0.443312255718664,
135.704504208516));
#188061=CARTESIAN_POINT('Ctrl Pts',(-258.860085333204,0.579289416653436,
135.688376059214));
#188062=CARTESIAN_POINT('Ctrl Pts',(-258.867860767497,0.715484271752939,
135.67222208937));
#188063=CARTESIAN_POINT('Ctrl Pts',(-258.87563620179,0.85085916677422,135.650384033521));
#188064=CARTESIAN_POINT('Ctrl Pts',(-258.883411636083,0.984913016375688,
135.622983803983));
#188065=CARTESIAN_POINT('Ctrl Pts',(-258.890873924358,1.11356801266962,
135.596687084864));
#188066=CARTESIAN_POINT('Ctrl Pts',(-258.898336212633,1.24100602086473,
135.565267616871));
#188067=CARTESIAN_POINT('Ctrl Pts',(-258.905798500908,1.36679936031642,
135.528875679574));
#188068=CARTESIAN_POINT('Ctrl Pts',(-258.913563209033,1.49769065382591,
135.49100890724));
#188069=CARTESIAN_POINT('Ctrl Pts',(-258.921327917158,1.6272174403873,135.447637701225));
#188070=CARTESIAN_POINT('Ctrl Pts',(-258.929092625283,1.75488088859039,
135.398876492972));
#188071=CARTESIAN_POINT('Ctrl Pts',(-258.936847736376,1.88238654720433,
135.350175552643));
#188072=CARTESIAN_POINT('Ctrl Pts',(-258.94460284747,2.00803308696774,135.296098003159));
#188073=CARTESIAN_POINT('Ctrl Pts',(-258.952357958563,2.13133483328165,
135.236808574501));
#188074=CARTESIAN_POINT('Ctrl Pts',(-258.960105351597,2.25451386693592,
135.177578152011));
#188075=CARTESIAN_POINT('Ctrl Pts',(-258.96785274463,2.37535239987729,135.1131463409));
#188076=CARTESIAN_POINT('Ctrl Pts',(-258.975600137663,2.49338316794614,
135.043726541888));
#188077=CARTESIAN_POINT('Ctrl Pts',(-258.983341684822,2.61132487469468,
134.974359124294));
#188078=CARTESIAN_POINT('Ctrl Pts',(-258.991083231981,2.72646269683481,
134.900011407841));
#188079=CARTESIAN_POINT('Ctrl Pts',(-258.99882477914,2.83835282906841,134.820943279509));
#188080=CARTESIAN_POINT('Ctrl Pts',(-259.006563070912,2.95019591054144,
134.741908400003));
#188081=CARTESIAN_POINT('Ctrl Pts',(-259.014301362683,3.05879369856792,
134.658157281911));
#188082=CARTESIAN_POINT('Ctrl Pts',(-259.022039654455,3.16373051564571,
134.569993670171));
#188083=CARTESIAN_POINT('Ctrl Pts',(-259.029776350361,3.26864569163368,
134.481848240388));
#188084=CARTESIAN_POINT('Ctrl Pts',(-259.037513046267,3.36990109832788,
134.389292378848));
#188085=CARTESIAN_POINT('Ctrl Pts',(-259.045249742173,3.46711370159911,
134.292670472307));
#188086=CARTESIAN_POINT('Ctrl Pts',(-259.052986528804,3.56432744483308,
134.19604743273));
#188087=CARTESIAN_POINT('Ctrl Pts',(-259.060723315434,3.65749801206921,
134.095358529446));
#188088=CARTESIAN_POINT('Ctrl Pts',(-259.068460102065,3.74627914665232,
133.99098510405));
#188089=CARTESIAN_POINT('Ctrl Pts',(-259.076198665721,3.83508067295352,
133.886587705616));
#188090=CARTESIAN_POINT('Ctrl Pts',(-259.083937229377,3.91949050655106,
133.778504399685));
#188091=CARTESIAN_POINT('Ctrl Pts',(-259.091675793033,3.99920287563806,
133.667149366669));
#188092=CARTESIAN_POINT('Ctrl Pts',(-259.099422711592,4.07900130579743,
133.555674109731));
#188093=CARTESIAN_POINT('Ctrl Pts',(-259.107169630151,4.1540919119548,133.440920388912));
#188094=CARTESIAN_POINT('Ctrl Pts',(-259.11491654871,4.22421216047996,133.323331575269));
#188095=CARTESIAN_POINT('Ctrl Pts',(-259.122667657237,4.29437033396256,
133.205679163011));
#188096=CARTESIAN_POINT('Ctrl Pts',(-259.130418765763,4.35955260727491,
133.085188947405));
#188097=CARTESIAN_POINT('Ctrl Pts',(-259.138169874289,4.41954308950522,
132.96232770316));
#188098=CARTESIAN_POINT('Ctrl Pts',(-259.145933621294,4.47963138850846,
132.839266128962));
#188099=CARTESIAN_POINT('Ctrl Pts',(-259.153697368299,4.53451082282979,
132.713826159953));
#188100=CARTESIAN_POINT('Ctrl Pts',(-259.161461115304,4.58401387421637,
132.586494132063));
#188101=CARTESIAN_POINT('Ctrl Pts',(-259.169056118443,4.63244098427488,
132.461929646523));
#188102=CARTESIAN_POINT('Ctrl Pts',(-259.176651121582,4.67572299195017,
132.33555485375));
#188103=CARTESIAN_POINT('Ctrl Pts',(-259.184246124721,4.71375015242697,
132.207835791196));
#188104=CARTESIAN_POINT('Ctrl Pts',(-259.192031309133,4.75272952499007,
132.076918603052));
#188105=CARTESIAN_POINT('Ctrl Pts',(-259.199816493545,4.78631181980715,
131.944171146245));
#188106=CARTESIAN_POINT('Ctrl Pts',(-259.207601677957,4.81432412344634,
131.810077425073));
#188107=CARTESIAN_POINT('Ctrl Pts',(-259.215377243051,4.84230181528276,
131.676149389148));
#188108=CARTESIAN_POINT('Ctrl Pts',(-259.223152808144,4.86472313132261,
131.540878776735));
#188109=CARTESIAN_POINT('Ctrl Pts',(-259.230928373238,4.88146463124323,
131.404765577923));
#188110=CARTESIAN_POINT('Ctrl Pts',(-259.238696177382,4.89818942113344,
131.268788236454));
#188111=CARTESIAN_POINT('Ctrl Pts',(-259.246463981527,4.90924563005071,
131.131970366726));
#188112=CARTESIAN_POINT('Ctrl Pts',(-259.254231785671,4.91456074023952,
130.994822668895));
#188113=CARTESIAN_POINT('Ctrl Pts',(-259.26199368058,4.91987180704147,130.857779304028));
#188114=CARTESIAN_POINT('Ctrl Pts',(-259.269755575489,4.91945045365875,
130.720406998459));
#188115=CARTESIAN_POINT('Ctrl Pts',(-259.277517470398,4.9132759609789,130.583221761263));
#188116=CARTESIAN_POINT('Ctrl Pts',(-259.285275943259,4.90710419049708,
130.446097006021));
#188117=CARTESIAN_POINT('Ctrl Pts',(-259.293034416119,4.89518434386338,
130.309159543684));
#188118=CARTESIAN_POINT('Ctrl Pts',(-259.300792888979,4.87754780323644,
130.172925355925));
#188119=CARTESIAN_POINT('Ctrl Pts',(-259.308549661931,4.8599151268374,130.036721017555));
#188120=CARTESIAN_POINT('Ctrl Pts',(-259.316306434883,4.83656829808708,
129.901220033568));
#188121=CARTESIAN_POINT('Ctrl Pts',(-259.324063207834,4.80759053215213,
129.766932866992));
#188122=CARTESIAN_POINT('Ctrl Pts',(-259.331819949055,4.77861288475751,
129.632646249749));
#188123=CARTESIAN_POINT('Ctrl Pts',(-259.339576690276,4.74400442807287,
129.499573821107));
#188124=CARTESIAN_POINT('Ctrl Pts',(-259.347333431497,4.7038993472714,129.368215084119));
#188125=CARTESIAN_POINT('Ctrl Pts',(-259.355091808782,4.66378580744186,
129.236828640735));
#188126=CARTESIAN_POINT('Ctrl Pts',(-259.362850186067,4.61817345026256,
129.107156981035));
#188127=CARTESIAN_POINT('Ctrl Pts',(-259.370608563352,4.56724598277686,
128.979683332316));
#188128=CARTESIAN_POINT('Ctrl Pts',(-259.378374961998,4.51626586154739,
128.852077889003));
#188129=CARTESIAN_POINT('Ctrl Pts',(-259.386141360644,4.45995979725993,
128.726675358917));
#188130=CARTESIAN_POINT('Ctrl Pts',(-259.393907759291,4.39855943860582,
128.603938401819));
#188131=CARTESIAN_POINT('Ctrl Pts',(-259.401678197314,4.33712714504929,
128.481137608079));
#188132=CARTESIAN_POINT('Ctrl Pts',(-259.409448635337,4.27059546581696,
128.361005491011));
#188133=CARTESIAN_POINT('Ctrl Pts',(-259.41721907336,4.19924100054342,128.243978208266));
#188134=CARTESIAN_POINT('Ctrl Pts',(-259.425001697521,4.12777463226247,
128.126767395242));
#188135=CARTESIAN_POINT('Ctrl Pts',(-259.432784321682,4.05147058038222,
128.012671471211));
#188136=CARTESIAN_POINT('Ctrl Pts',(-259.440566945844,3.97064809108426,
127.902096535979));
#188137=CARTESIAN_POINT('Ctrl Pts',(-259.447942546741,3.8940525351133,127.797304556493));
#188138=CARTESIAN_POINT('Ctrl Pts',(-259.455318147638,3.81339932404087,
127.695674852864));
#188139=CARTESIAN_POINT('Ctrl Pts',(-259.462693748534,3.72899119397172,
127.597522963773));
#188140=CARTESIAN_POINT('Ctrl Pts',(-259.470480941117,3.639872710803,127.493893758047));
#188141=CARTESIAN_POINT('Ctrl Pts',(-259.4782681337,3.54629431034451,127.393823152026));
#188142=CARTESIAN_POINT('Ctrl Pts',(-259.486055326282,3.44857082400634,
127.297718016115));
#188143=CARTESIAN_POINT('Ctrl Pts',(-259.493833075873,3.35096584020889,
127.201729420282));
#188144=CARTESIAN_POINT('Ctrl Pts',(-259.501610825463,3.24922604762373,
127.109696996534));
#188145=CARTESIAN_POINT('Ctrl Pts',(-259.509388575054,3.14370639443858,
127.021994536914));
#188146=CARTESIAN_POINT('Ctrl Pts',(-259.517158735265,3.03828970530945,
126.934377655674));
#188147=CARTESIAN_POINT('Ctrl Pts',(-259.524928895477,2.92910079372457,
126.851082577125));
#188148=CARTESIAN_POINT('Ctrl Pts',(-259.532699055688,2.81653106311716,
126.772445956639));
#188149=CARTESIAN_POINT('Ctrl Pts',(-259.540463473649,2.70404452301452,
126.693867449646));
#188150=CARTESIAN_POINT('Ctrl Pts',(-259.548227891611,2.58818245534753,
126.619940769906));
#188151=CARTESIAN_POINT('Ctrl Pts',(-259.555992309572,2.46936864366422,
126.550961792604));
#188152=CARTESIAN_POINT('Ctrl Pts',(-259.563753547399,2.35060349549515,
126.482011067568));
#188153=CARTESIAN_POINT('Ctrl Pts',(-259.571514785227,2.2288893440266,126.418004209507));
#188154=CARTESIAN_POINT('Ctrl Pts',(-259.579276023054,2.10467803831177,
126.359193194673));
#188155=CARTESIAN_POINT('Ctrl Pts',(-259.587035707387,1.98049159479754,
126.300393951483));
#188156=CARTESIAN_POINT('Ctrl Pts',(-259.594795391721,1.85380934306757,
126.246788649275));
#188157=CARTESIAN_POINT('Ctrl Pts',(-259.602555076055,1.72510641635312,
126.198582625222));
#188158=CARTESIAN_POINT('Ctrl Pts',(-259.610314871376,1.59640164878467,
126.150375911673));
#188159=CARTESIAN_POINT('Ctrl Pts',(-259.618074666698,1.46567651331978,
126.107568766764));
#188160=CARTESIAN_POINT('Ctrl Pts',(-259.625834462019,1.33342438310065,
126.070317686091));
#188161=CARTESIAN_POINT('Ctrl Pts',(-259.63359603252,1.20114199805461,126.033058083626));
#188162=CARTESIAN_POINT('Ctrl Pts',(-259.641357603021,1.06733229784172,
126.001357180389));
#188163=CARTESIAN_POINT('Ctrl Pts',(-259.649119173522,0.932501642178328,
125.975320987387));
#188164=CARTESIAN_POINT('Ctrl Pts',(-259.656888964626,0.797528181744626,
125.949257218368));
#188165=CARTESIAN_POINT('Ctrl Pts',(-259.66465875573,0.661531988718544,
125.92887021873));
#188166=CARTESIAN_POINT('Ctrl Pts',(-259.672428546834,0.525027960616441,
125.914214535589));
#188167=CARTESIAN_POINT('Ctrl Pts',(-259.680202491048,0.388450968345654,
125.899551018689));
#188168=CARTESIAN_POINT('Ctrl Pts',(-259.687976435263,0.251365988490296,
125.890624948406));
#188169=CARTESIAN_POINT('Ctrl Pts',(-259.695750379478,0.114289834376831,
125.887438725136));
#188170=CARTESIAN_POINT('Ctrl Pts',(-259.703536666297,-0.0230039540221484,
125.884247443135));
#188171=CARTESIAN_POINT('Ctrl Pts',(-259.711322953117,-0.160288499093245,
125.8868142119));
#188172=CARTESIAN_POINT('Ctrl Pts',(-259.719109239936,-0.297049294226065,
125.895089309184));
#188173=CARTESIAN_POINT('Ctrl Pts',(-259.726453284073,-0.426042399538032,
125.902894400508));
#188174=CARTESIAN_POINT('Ctrl Pts',(-259.73379732821,-0.554569337392523,
125.915777299511));
#188175=CARTESIAN_POINT('Ctrl Pts',(-259.741141372348,-0.682206894920373,
125.933654630235));
#188176=CARTESIAN_POINT('Ctrl Pts',(-259.748774629122,-0.814870892104533,
125.952235980417));
#188177=CARTESIAN_POINT('Ctrl Pts',(-259.756407885897,-0.947026750298924,
125.976276897283));
#188178=CARTESIAN_POINT('Ctrl Pts',(-259.764041142672,-1.07817805427494,
126.005744656085));
#188179=CARTESIAN_POINT('Ctrl Pts',(-259.771664808356,-1.209164568287,126.035175389019));
#188180=CARTESIAN_POINT('Ctrl Pts',(-259.77928847404,-1.33914864612342,
126.070019318878));
#188181=CARTESIAN_POINT('Ctrl Pts',(-259.786912139724,-1.46763882087358,
126.110191963378));
#188182=CARTESIAN_POINT('Ctrl Pts',(-259.794528200188,-1.5960008163482,
126.150324532435));
#188183=CARTESIAN_POINT('Ctrl Pts',(-259.802144260653,-1.72287148776318,
126.195775124874));
#188184=CARTESIAN_POINT('Ctrl Pts',(-259.809760321117,-1.8477699479343,
126.246408305177));
#188185=CARTESIAN_POINT('Ctrl Pts',(-259.817686663262,-1.97775682674349,
126.299104303693));
#188186=CARTESIAN_POINT('Ctrl Pts',(-259.825613005406,-2.10560695858319,
126.357414024714));
#188187=CARTESIAN_POINT('Ctrl Pts',(-259.83353934755,-2.23079566345197,
126.42112736226));
#188188=CARTESIAN_POINT('Ctrl Pts',(-259.841146810408,-2.35094798656864,
126.482277491799));
#188189=CARTESIAN_POINT('Ctrl Pts',(-259.848754273265,-2.46864846641231,
126.548404698225));
#188190=CARTESIAN_POINT('Ctrl Pts',(-259.856361736122,-2.58345457280964,
126.619274533299));
#188191=CARTESIAN_POINT('Ctrl Pts',(-259.863968055281,-2.69824341935702,
126.690133713862));
#188192=CARTESIAN_POINT('Ctrl Pts',(-259.871574374439,-2.81013841209187,
126.765733892621));
#188193=CARTESIAN_POINT('Ctrl Pts',(-259.879180693597,-2.91872362369027,
126.845795792909));
#188194=CARTESIAN_POINT('Ctrl Pts',(-259.886787647209,-3.0273178925455,
126.925864371281));
#188195=CARTESIAN_POINT('Ctrl Pts',(-259.894394600822,-3.13260150486788,
127.010395169864));
#188196=CARTESIAN_POINT('Ctrl Pts',(-259.902001554435,-3.2341898996486,
127.099067274859));
#188197=CARTESIAN_POINT('Ctrl Pts',(-259.9096109211,-3.33581051996215,127.187767508124));
#188198=CARTESIAN_POINT('Ctrl Pts',(-259.917220287765,-3.43373328697769,
127.280611392494));
#188199=CARTESIAN_POINT('Ctrl Pts',(-259.92482965443,-3.52760937784773,
127.377240085717));
#188200=CARTESIAN_POINT('Ctrl Pts',(-259.932447357799,-3.62158831789155,
127.473974643821));
#188201=CARTESIAN_POINT('Ctrl Pts',(-259.940065061167,-3.71151145141156,
127.574501994588));
#188202=CARTESIAN_POINT('Ctrl Pts',(-259.947682764535,-3.79706912348943,
127.678428895032));
#188203=CARTESIAN_POINT('Ctrl Pts',(-259.955305402399,-3.88268221700061,
127.782423115889));
#188204=CARTESIAN_POINT('Ctrl Pts',(-259.962928040264,-3.96392397811463,
127.889820945947));
#188205=CARTESIAN_POINT('Ctrl Pts',(-259.970550678129,-4.04052803945671,
128.000200097042));
#188206=CARTESIAN_POINT('Ctrl Pts',(-259.978184189506,-4.1172413746782,
128.110736701382));
#188207=CARTESIAN_POINT('Ctrl Pts',(-259.985817700883,-4.18930359531733,
128.224262770745));
#188208=CARTESIAN_POINT('Ctrl Pts',(-259.99345121226,-4.25649411764769,
128.340331216579));
#188209=CARTESIAN_POINT('Ctrl Pts',(-259.995631652367,-4.27568645292739,
128.373485067011));
#188210=CARTESIAN_POINT('Ctrl Pts',(-259.997812092474,-4.29448160516882,
128.406846227114));
#188211=CARTESIAN_POINT('Ctrl Pts',(-259.999992532581,-4.31287516290238,
128.44040399958));
#188212=CARTESIAN_POINT('',(-260.,0.837162017623962,125.957883255734));
#188213=CARTESIAN_POINT('Origin',(-260.,0.,130.804360617566));
#188214=CARTESIAN_POINT('',(-258.735140563986,-4.91824979995562,130.802957857252));
#188215=CARTESIAN_POINT('Ctrl Pts',(-258.735140564015,-4.91824979995577,
130.802957857762));
#188216=CARTESIAN_POINT('Ctrl Pts',(-258.743125920418,-4.91829022612684,
130.944697025984));
#188217=CARTESIAN_POINT('Ctrl Pts',(-258.751111276821,-4.91219912563647,
131.086370582116));
#188218=CARTESIAN_POINT('Ctrl Pts',(-258.759096633224,-4.9000197173338,
131.227432517176));
#188219=CARTESIAN_POINT('Ctrl Pts',(-258.767087865585,-4.88783134691572,
131.368598251478));
#188220=CARTESIAN_POINT('Ctrl Pts',(-258.775079097945,-4.86954576746095,
131.509151113065));
#188221=CARTESIAN_POINT('Ctrl Pts',(-258.783070330306,-4.84525785291376,
131.64855218426));
#188222=CARTESIAN_POINT('Ctrl Pts',(-258.791068654905,-4.82094838278348,
131.788076974244));
#188223=CARTESIAN_POINT('Ctrl Pts',(-258.799066979503,-4.79062601762179,
131.926447585823));
#188224=CARTESIAN_POINT('Ctrl Pts',(-258.807065304102,-4.75443630802797,
132.06313718845));
#188225=CARTESIAN_POINT('Ctrl Pts',(-258.815077527633,-4.71818371047263,
132.200064320765));
#188226=CARTESIAN_POINT('Ctrl Pts',(-258.823089751164,-4.67604348840026,
132.335304263536));
#188227=CARTESIAN_POINT('Ctrl Pts',(-258.831101974695,-4.62821082354395,
132.468346084849));
#188228=CARTESIAN_POINT('Ctrl Pts',(-258.83912215898,-4.58033063329716,
132.601520093331));
#188229=CARTESIAN_POINT('Ctrl Pts',(-258.847142343264,-4.52674685385319,
132.732491295973));
#188230=CARTESIAN_POINT('Ctrl Pts',(-258.855162527549,-4.46770190836591,
132.860770771325));
#188231=CARTESIAN_POINT('Ctrl Pts',(-258.863196907718,-4.40855245215567,
132.989277303889));
#188232=CARTESIAN_POINT('Ctrl Pts',(-258.871231287888,-4.34392267902974,
133.115082274356));
#188233=CARTESIAN_POINT('Ctrl Pts',(-258.879265668057,-4.27410033019235,
133.237722372413));
#188234=CARTESIAN_POINT('Ctrl Pts',(-258.881580280287,-4.25398531706869,
133.273053569701));
#188235=CARTESIAN_POINT('Ctrl Pts',(-258.883894892518,-4.23343961435544,
133.30812229263));
#188236=CARTESIAN_POINT('Ctrl Pts',(-258.886209504748,-4.2124707400616,
133.342917949325));
#188237=CARTESIAN_POINT('Ctrl Pts',(-258.89399669733,-4.14192386389677,
133.459983121708));
#188238=CARTESIAN_POINT('Ctrl Pts',(-258.901783889913,-4.06638508417377,
133.574285072608));
#188239=CARTESIAN_POINT('Ctrl Pts',(-258.909571082495,-3.98609680935438,
133.685370039445));
#188240=CARTESIAN_POINT('Ctrl Pts',(-258.917348832086,-3.90590589459564,
133.796320301194));
#188241=CARTESIAN_POINT('Ctrl Pts',(-258.925126581676,-3.82097717117305,
133.904061028655));
#188242=CARTESIAN_POINT('Ctrl Pts',(-258.932904331267,-3.73159812815367,
134.008164368182));
#188243=CARTESIAN_POINT('Ctrl Pts',(-258.940674491478,-3.64230629949165,
134.112166125665));
#188244=CARTESIAN_POINT('Ctrl Pts',(-258.94844465169,-3.54857304588502,
134.212537265401));
#188245=CARTESIAN_POINT('Ctrl Pts',(-258.956214811901,-3.45072800518379,
134.308880455823));
#188246=CARTESIAN_POINT('Ctrl Pts',(-258.963979229863,-3.35295527324923,
134.405152447366));
#188247=CARTESIAN_POINT('Ctrl Pts',(-258.971743647824,-3.25107707939238,
134.497402142855));
#188248=CARTESIAN_POINT('Ctrl Pts',(-258.979508065785,-3.14546180132275,
134.585267006108));
#188249=CARTESIAN_POINT('Ctrl Pts',(-258.987269303613,-3.03988978093909,
134.673095881854));
#188250=CARTESIAN_POINT('Ctrl Pts',(-258.99503054144,-2.93058401949167,
134.756543248864));
#188251=CARTESIAN_POINT('Ctrl Pts',(-259.002791779267,-2.8179479018152,
134.835285162277));
#188252=CARTESIAN_POINT('Ctrl Pts',(-259.010551463601,-2.70533432944358,
134.914011314667));
#188253=CARTESIAN_POINT('Ctrl Pts',(-259.018311147935,-2.58939204584363,
134.988033664008));
#188254=CARTESIAN_POINT('Ctrl Pts',(-259.026070832268,-2.47055518681673,
135.057070357413));
#188255=CARTESIAN_POINT('Ctrl Pts',(-259.03383062759,-2.35171662805145,
135.12610803826));
#188256=CARTESIAN_POINT('Ctrl Pts',(-259.041590422911,-2.22998374808351,
135.190159725453));
#188257=CARTESIAN_POINT('Ctrl Pts',(-259.049350218233,-2.1058168284298,
135.248988672601));
#188258=CARTESIAN_POINT('Ctrl Pts',(-259.057111788734,-1.98162150357265,
135.307831077827));
#188259=CARTESIAN_POINT('Ctrl Pts',(-259.064873359235,-1.85499138276835,
135.361448198621));
#188260=CARTESIAN_POINT('Ctrl Pts',(-259.072634929736,-1.72640798836747,
135.409650892913));
#188261=CARTESIAN_POINT('Ctrl Pts',(-259.08040472084,-1.59768840593121,
135.457904640688));
#188262=CARTESIAN_POINT('Ctrl Pts',(-259.088174511943,-1.46701178244654,
135.500732369397));
#188263=CARTESIAN_POINT('Ctrl Pts',(-259.095944303047,-1.33487665854731,
135.537994250302));
#188264=CARTESIAN_POINT('Ctrl Pts',(-259.103718247262,-1.20267090574684,
135.575276048436));
#188265=CARTESIAN_POINT('Ctrl Pts',(-259.111492191477,-1.06900547771351,
135.60698598034));
#188266=CARTESIAN_POINT('Ctrl Pts',(-259.119266135692,-0.934389518613181,
135.633035310482));
#188267=CARTESIAN_POINT('Ctrl Pts',(-259.127052422511,-0.79955983125197,
135.659125998855));
#188268=CARTESIAN_POINT('Ctrl Pts',(-259.134838709331,-0.6637769823593,
135.679538067927));
#188269=CARTESIAN_POINT('Ctrl Pts',(-259.14262499615,-0.527556552464962,
135.694234557296));
#188270=CARTESIAN_POINT('Ctrl Pts',(-259.149969040287,-0.399073120923145,
135.708096320816));
#188271=CARTESIAN_POINT('Ctrl Pts',(-259.157313084425,-0.270200707173242,
135.716873781456));
#188272=CARTESIAN_POINT('Ctrl Pts',(-259.164657128562,-0.141370506025531,
135.72057841609));
#188273=CARTESIAN_POINT('Ctrl Pts',(-259.172363388608,-0.00618626512051576,
135.724465767165));
#188274=CARTESIAN_POINT('Ctrl Pts',(-259.180069648654,0.129394565249223,
135.722779750212));
#188275=CARTESIAN_POINT('Ctrl Pts',(-259.187775908701,0.264868809592343,
135.715473279296));
#188276=CARTESIAN_POINT('Ctrl Pts',(-259.195472507276,0.400173207544053,
135.708175968628));
#188277=CARTESIAN_POINT('Ctrl Pts',(-259.203169105852,0.535370891849149,
135.695272240219));
#188278=CARTESIAN_POINT('Ctrl Pts',(-259.210865704427,0.669955370441971,
135.676766887995));
#188279=CARTESIAN_POINT('Ctrl Pts',(-259.218554573727,0.804404693166619,
135.65828011969));
#188280=CARTESIAN_POINT('Ctrl Pts',(-259.226243443028,0.938241643463367,
135.634202972054));
#188281=CARTESIAN_POINT('Ctrl Pts',(-259.233932312328,1.07096199527409,
135.604592223143));
#188282=CARTESIAN_POINT('Ctrl Pts',(-259.241615376899,1.20358214954474,
135.575003828936));
#188283=CARTESIAN_POINT('Ctrl Pts',(-259.249298441469,1.33508699557577,
135.539890232041));
#188284=CARTESIAN_POINT('Ctrl Pts',(-259.256981506039,1.4649801353849,135.499359687367));
#188285=CARTESIAN_POINT('Ctrl Pts',(-259.264736641303,1.59609173282675,
135.458448947467));
#188286=CARTESIAN_POINT('Ctrl Pts',(-259.272491776567,1.72556082352701,
135.412019167305));
#188287=CARTESIAN_POINT('Ctrl Pts',(-259.280246911831,1.85288991576312,
135.360233972101));
#188288=CARTESIAN_POINT('Ctrl Pts',(-259.287925523627,1.97896259357931,
135.308959765116));
#188289=CARTESIAN_POINT('Ctrl Pts',(-259.295604135422,2.10293694822109,
135.252435530452));
#188290=CARTESIAN_POINT('Ctrl Pts',(-259.303282747218,2.22434846112939,
135.190869136419));
#188291=CARTESIAN_POINT('Ctrl Pts',(-259.310961664611,2.34576480604577,
135.12930029213));
#188292=CARTESIAN_POINT('Ctrl Pts',(-259.318640582005,2.46461775081044,
135.06268906903));
#188293=CARTESIAN_POINT('Ctrl Pts',(-259.326319499398,2.58046650838747,
134.991289762129));
#188294=CARTESIAN_POINT('Ctrl Pts',(-259.334000455379,2.69634602131912,
134.919871500247));
#188295=CARTESIAN_POINT('Ctrl Pts',(-259.34168141136,2.80921942148387,134.843662834839));
#188296=CARTESIAN_POINT('Ctrl Pts',(-259.349362367341,2.91867451310751,
134.762961651901));
#188297=CARTESIAN_POINT('Ctrl Pts',(-259.35717423276,3.02999508926459,134.680885048172));
#188298=CARTESIAN_POINT('Ctrl Pts',(-259.36498609818,3.13777942900704,134.594161648671));
#188299=CARTESIAN_POINT('Ctrl Pts',(-259.372797963599,3.24162963026778,
134.503146959418));
#188300=CARTESIAN_POINT('Ctrl Pts',(-259.380492559669,3.34392086386956,
134.413498555019));
#188301=CARTESIAN_POINT('Ctrl Pts',(-259.388187155739,3.44239501607596,
134.319687131659));
#188302=CARTESIAN_POINT('Ctrl Pts',(-259.395881751809,3.53671030809215,
134.222088409409));
#188303=CARTESIAN_POINT('Ctrl Pts',(-259.403752251903,3.63318171581071,
134.122258509869));
#188304=CARTESIAN_POINT('Ctrl Pts',(-259.411622751998,3.72530153017333,
134.01846640365));
#188305=CARTESIAN_POINT('Ctrl Pts',(-259.419493252092,3.8127493250714,133.911147647066));
#188306=CARTESIAN_POINT('Ctrl Pts',(-259.427363752186,3.90019711996948,
133.803828890482));
#188307=CARTESIAN_POINT('Ctrl Pts',(-259.43523425228,3.98297269501011,133.69298387897));
#188308=CARTESIAN_POINT('Ctrl Pts',(-259.443104752374,4.06080482670846,
133.579076318657));
#188309=CARTESIAN_POINT('Ctrl Pts',(-259.450996306946,4.13884516815917,
133.464864042741));
#188310=CARTESIAN_POINT('Ctrl Pts',(-259.458887861518,4.21217532934342,
133.347193335508));
#188311=CARTESIAN_POINT('Ctrl Pts',(-259.46677941609,4.28047914998072,133.226483923486));
#188312=CARTESIAN_POINT('Ctrl Pts',(-259.474660674075,4.3486938505123,133.105932008299));
#188313=CARTESIAN_POINT('Ctrl Pts',(-259.482541932061,4.41189508226405,
132.98234960711));
#188314=CARTESIAN_POINT('Ctrl Pts',(-259.490423190047,4.46980916533012,
132.856186411348));
#188315=CARTESIAN_POINT('Ctrl Pts',(-259.498295871439,4.52766022475709,
132.730160509718));
#188316=CARTESIAN_POINT('Ctrl Pts',(-259.506168552831,4.58023543508844,
132.601559746475));
#188317=CARTESIAN_POINT('Ctrl Pts',(-259.514041234222,4.62730647137447,
132.470859307177));
#188318=CARTESIAN_POINT('Ctrl Pts',(-259.52190705186,4.67433646903304,132.340272818348));
#188319=CARTESIAN_POINT('Ctrl Pts',(-259.529772869497,4.71587172181415,
132.207590652673));
#188320=CARTESIAN_POINT('Ctrl Pts',(-259.537638687135,4.75173165413759,
132.073308744783));
#188321=CARTESIAN_POINT('Ctrl Pts',(-259.545499205399,4.78756742684223,
131.939117305544));
#188322=CARTESIAN_POINT('Ctrl Pts',(-259.553359723664,4.8177353988466,131.803328634847));
#188323=CARTESIAN_POINT('Ctrl Pts',(-259.561220241928,4.84210463919843,
131.666454420788));
#188324=CARTESIAN_POINT('Ctrl Pts',(-259.569077860488,4.8664648898651,131.529630698909));
#188325=CARTESIAN_POINT('Ctrl Pts',(-259.576935479049,4.88503060150653,
131.391722602004));
#188326=CARTESIAN_POINT('Ctrl Pts',(-259.584793097609,4.89772182492112,
131.253252573599));
#188327=CARTESIAN_POINT('Ctrl Pts',(-259.592649357877,4.91041085449106,
131.114806481558));
#188328=CARTESIAN_POINT('Ctrl Pts',(-259.600505618145,4.91722738378753,
130.97579902716));
#188329=CARTESIAN_POINT('Ctrl Pts',(-259.608361878413,4.9181432943351,130.836758131155));
#188330=CARTESIAN_POINT('Ctrl Pts',(-259.616218320535,4.91905922608383,
130.69771401668));
#188331=CARTESIAN_POINT('Ctrl Pts',(-259.624074762657,4.91407426562755,
130.558636836429));
#188332=CARTESIAN_POINT('Ctrl Pts',(-259.631931204778,4.90321241491024,
130.420054649918));
#188333=CARTESIAN_POINT('Ctrl Pts',(-259.639792798094,4.89234344245782,
130.28138159992));
#188334=CARTESIAN_POINT('Ctrl Pts',(-259.64765439141,4.87558990925817,130.143204568982));
#188335=CARTESIAN_POINT('Ctrl Pts',(-259.655515984725,4.85302777544528,
130.006047099419));
#188336=CARTESIAN_POINT('Ctrl Pts',(-259.66338015352,4.83045825021641,129.868844696698));
#188337=CARTESIAN_POINT('Ctrl Pts',(-259.671244322315,4.80207640315996,
129.732662891872));
#188338=CARTESIAN_POINT('Ctrl Pts',(-259.67910849111,4.76800926284416,129.598014592608));
#188339=CARTESIAN_POINT('Ctrl Pts',(-259.68698147486,4.73390393663589,129.463215365927));
#188340=CARTESIAN_POINT('Ctrl Pts',(-259.69485445861,4.69410068626818,129.32995344318));
#188341=CARTESIAN_POINT('Ctrl Pts',(-259.70272744236,4.64877652418144,129.198726820363));
#188342=CARTESIAN_POINT('Ctrl Pts',(-259.709002420302,4.61265195865421,
129.094135703471));
#188343=CARTESIAN_POINT('Ctrl Pts',(-259.715277398245,4.57302122015438,
128.990837253891));
#188344=CARTESIAN_POINT('Ctrl Pts',(-259.721552376188,4.52999553129857,
128.88907381165));
#188345=CARTESIAN_POINT('Ctrl Pts',(-259.729340865402,4.47659213822368,
128.762765244579));
#188346=CARTESIAN_POINT('Ctrl Pts',(-259.737129354617,4.41784166832893,
128.63854916123));
#188347=CARTESIAN_POINT('Ctrl Pts',(-259.744917843832,4.35393345271473,
128.51690645369));
#188348=CARTESIAN_POINT('Ctrl Pts',(-259.752699932249,4.29007775865146,
128.395363715515));
#188349=CARTESIAN_POINT('Ctrl Pts',(-259.760482020667,4.2210729339634,128.276390486525));
#188350=CARTESIAN_POINT('Ctrl Pts',(-259.768264109084,4.14715602421871,
128.160446857005));
#188351=CARTESIAN_POINT('Ctrl Pts',(-259.776041625002,4.07328254561895,
128.044571352147));
#188352=CARTESIAN_POINT('Ctrl Pts',(-259.78381914092,3.99450293455686,127.931722230335));
#188353=CARTESIAN_POINT('Ctrl Pts',(-259.791596656838,3.91109954323073,
127.822333886391));
#188354=CARTESIAN_POINT('Ctrl Pts',(-259.799371306898,3.82772688437878,
127.712985849855));
#188355=CARTESIAN_POINT('Ctrl Pts',(-259.807145956958,3.73973407267837,
127.607096360549));
#188356=CARTESIAN_POINT('Ctrl Pts',(-259.814920607018,3.64744583509542,
127.505069490287));
#188357=CARTESIAN_POINT('Ctrl Pts',(-259.822696039392,3.55514831113214,
127.403032353707));
#188358=CARTESIAN_POINT('Ctrl Pts',(-259.830471471765,3.45855475148024,
127.304858906876));
#188359=CARTESIAN_POINT('Ctrl Pts',(-259.838246904139,3.35802912226606,
127.210918886229));
#188360=CARTESIAN_POINT('Ctrl Pts',(-259.845756665457,3.26093825380846,
127.120188609196));
#188361=CARTESIAN_POINT('Ctrl Pts',(-259.853266426776,3.16017986615663,
127.03340743426));
#188362=CARTESIAN_POINT('Ctrl Pts',(-259.860776188094,3.05611296324695,
126.950874323523));
#188363=CARTESIAN_POINT('Ctrl Pts',(-259.86984693344,2.93041464406388,126.851185825005));
#188364=CARTESIAN_POINT('Ctrl Pts',(-259.878917678785,2.79997527753095,
126.757761425072));
#188365=CARTESIAN_POINT('Ctrl Pts',(-259.887988424131,2.66539424307775,
126.670977428039));
#188366=CARTESIAN_POINT('Ctrl Pts',(-259.89732272212,2.52690292495375,126.58167190152));
#188367=CARTESIAN_POINT('Ctrl Pts',(-259.906657020109,2.38402579214265,
126.499398505981));
#188368=CARTESIAN_POINT('Ctrl Pts',(-259.915991318098,2.2374405325973,126.424515537476));
#188369=CARTESIAN_POINT('Ctrl Pts',(-259.925109869169,2.09424334979852,
126.351363365404));
#188370=CARTESIAN_POINT('Ctrl Pts',(-259.93422842024,1.9475076731623,126.285263762748));
#188371=CARTESIAN_POINT('Ctrl Pts',(-259.943346971312,1.79788636277355,
126.226502200243));
#188372=CARTESIAN_POINT('Ctrl Pts',(-259.95278914276,1.64295494286366,126.165655170556));
#188373=CARTESIAN_POINT('Ctrl Pts',(-259.962231314208,1.48492941989842,
126.112676642776));
#188374=CARTESIAN_POINT('Ctrl Pts',(-259.971673485656,1.32455638043327,
126.067828821246));
#188375=CARTESIAN_POINT('Ctrl Pts',(-259.981115657104,1.16418334096776,
126.022980999715));
#188376=CARTESIAN_POINT('Ctrl Pts',(-259.990557828552,1.00146289783601,
125.986263963227));
#188377=CARTESIAN_POINT('Ctrl Pts',(-260.,0.837162017624996,125.957883255734));
#188378=CARTESIAN_POINT('Ctrl Pts',(-258.665423831404,-4.76405452823398,
129.582490119308));
#188379=CARTESIAN_POINT('Ctrl Pts',(-258.673755749879,-4.80055740878989,
129.724814296587));
#188380=CARTESIAN_POINT('Ctrl Pts',(-258.682087668354,-4.83071962826672,
129.868936410275));
#188381=CARTESIAN_POINT('Ctrl Pts',(-258.690419586829,-4.8543766360945,
130.014290660258));
#188382=CARTESIAN_POINT('Ctrl Pts',(-258.698727113262,-4.87796438703723,
130.159219379564));
#188383=CARTESIAN_POINT('Ctrl Pts',(-258.707034639695,-4.89508485697752,
130.305372751092));
#188384=CARTESIAN_POINT('Ctrl Pts',(-258.715342166129,-4.90562406003518,
130.452173672743));
#188385=CARTESIAN_POINT('Ctrl Pts',(-258.721941632081,-4.9139963610206,
130.568791740947));
#188386=CARTESIAN_POINT('Ctrl Pts',(-258.728541098034,-4.91821638989561,
130.685818086956));
#188387=CARTESIAN_POINT('Ctrl Pts',(-258.735140563986,-4.91824979995562,
130.802957857252));
#188388=CARTESIAN_POINT('Origin',(212.,0.,130.804360617566));
#188389=CARTESIAN_POINT('',(212.,-9.,130.804360617566));
#188390=CARTESIAN_POINT('Origin',(212.,0.,130.804360617566));
#188391=CARTESIAN_POINT('',(212.,-7.,130.804360617566));
#188392=CARTESIAN_POINT('Origin',(212.,0.,130.804360617566));
#188393=CARTESIAN_POINT('Origin',(210.,0.,130.804360617566));
#188394=CARTESIAN_POINT('',(210.,-9.,130.804360617566));
#188395=CARTESIAN_POINT('',(210.,-9.,130.804360617566));
#188396=CARTESIAN_POINT('Origin',(210.,0.,130.804360617566));
#188397=CARTESIAN_POINT('Origin',(210.,0.,130.804360617566));
#188398=CARTESIAN_POINT('Ctrl Pts',(210.,-2.8641783061622,134.81100053397));
#188399=CARTESIAN_POINT('Ctrl Pts',(210.,-2.96502472716555,134.75378484428));
#188400=CARTESIAN_POINT('Ctrl Pts',(210.,-3.06346128541938,134.692924280852));
#188401=CARTESIAN_POINT('Ctrl Pts',(210.,-3.15926168328819,134.628476370697));
#188402=CARTESIAN_POINT('Ctrl Pts',(210.,-3.27563203468335,134.550190412411));
#188403=CARTESIAN_POINT('Ctrl Pts',(210.,-3.38811397812997,134.466613066522));
#188404=CARTESIAN_POINT('Ctrl Pts',(210.,-3.49662687492886,134.378182862155));
#188405=CARTESIAN_POINT('Ctrl Pts',(210.,-3.60844752995494,134.287057072797));
#188406=CARTESIAN_POINT('Ctrl Pts',(210.,-3.7160539550275,134.190777777457));
#188407=CARTESIAN_POINT('Ctrl Pts',(210.,-3.81933617822931,134.089772607624));
#188408=CARTESIAN_POINT('Ctrl Pts',(210.,-3.92261840143113,133.988767437792));
#188409=CARTESIAN_POINT('Ctrl Pts',(210.,-4.02157682130595,133.883035820798));
#188410=CARTESIAN_POINT('Ctrl Pts',(210.,-4.11607356234994,133.772960819414));
#188411=CARTESIAN_POINT('Ctrl Pts',(210.,-4.169132731693,133.711154580655));
#188412=CARTESIAN_POINT('Ctrl Pts',(210.,-4.22078471769379,133.647978234656));
#188413=CARTESIAN_POINT('Ctrl Pts',(210.,-4.27100052841727,133.583494472577));
#188414=CARTESIAN_POINT('Ctrl Pts',(210.,-4.28346862121088,133.567483787542));
#188415=CARTESIAN_POINT('Ctrl Pts',(210.,-4.29584950541028,133.551390713183));
#188416=CARTESIAN_POINT('Ctrl Pts',(210.,-4.30813839293311,133.535221857428));
#188417=CARTESIAN_POINT('Ctrl Pts',(210.,-4.40009216432484,133.414235538449));
#188418=CARTESIAN_POINT('Ctrl Pts',(210.,-4.48665891050019,133.289326577391));
#188419=CARTESIAN_POINT('Ctrl Pts',(210.,-4.56773849979461,133.160993194298));
#188420=CARTESIAN_POINT('Ctrl Pts',(210.,-4.64849084265369,133.03317777932));
#188421=CARTESIAN_POINT('Ctrl Pts',(210.,-4.72380062867781,132.901964837969));
#188422=CARTESIAN_POINT('Ctrl Pts',(210.,-4.79353962578297,132.767799500622));
#188423=CARTESIAN_POINT('Ctrl Pts',(210.,-4.86402484104165,132.632198573225));
#188424=CARTESIAN_POINT('Ctrl Pts',(210.,-4.928819916136,132.493581111616));
#188425=CARTESIAN_POINT('Ctrl Pts',(210.,-4.98775557446357,132.352368204748));
#188426=CARTESIAN_POINT('Ctrl Pts',(210.,-5.04615226330057,132.21244669685));
#188427=CARTESIAN_POINT('Ctrl Pts',(210.,-5.09879659579809,132.069976268777));
#188428=CARTESIAN_POINT('Ctrl Pts',(210.,-5.14548145371836,131.925339242337));
#188429=CARTESIAN_POINT('Ctrl Pts',(210.,-5.15890833504517,131.88374065393));
#188430=CARTESIAN_POINT('Ctrl Pts',(210.,-5.17184197206715,131.84196271352));
#188431=CARTESIAN_POINT('Ctrl Pts',(210.,-5.18427670924701,131.800014223967));
#188432=CARTESIAN_POINT('Ctrl Pts',(210.,-5.19020423391478,131.780017765416));
#188433=CARTESIAN_POINT('Ctrl Pts',(210.,-5.19601887800011,131.75998081631));
#188434=CARTESIAN_POINT('Ctrl Pts',(210.,-5.20171845467757,131.739909779336));
#188435=CARTESIAN_POINT('Ctrl Pts',(210.,-5.244666117862,131.588669751436));
#188436=CARTESIAN_POINT('Ctrl Pts',(210.,-5.28095619241888,131.4359495813));
#188437=CARTESIAN_POINT('Ctrl Pts',(210.,-5.31045568168286,131.282214375908));
#188438=CARTESIAN_POINT('Ctrl Pts',(210.,-5.34002140650602,131.128133987004));
#188439=CARTESIAN_POINT('Ctrl Pts',(210.,-5.36276647177015,130.973033269566));
#188440=CARTESIAN_POINT('Ctrl Pts',(210.,-5.37851503032129,130.817349238262));
#188441=CARTESIAN_POINT('Ctrl Pts',(210.,-5.39406434679863,130.663634835425));
#188442=CARTESIAN_POINT('Ctrl Pts',(210.,-5.40279340123895,130.509351025403));
#188443=CARTESIAN_POINT('Ctrl Pts',(210.,-5.40448640685994,130.354899211369));
#188444=CARTESIAN_POINT('Ctrl Pts',(210.,-5.40520651984511,130.289203766836));
#188445=CARTESIAN_POINT('Ctrl Pts',(210.,-5.40465306852236,130.223477753562));
#188446=CARTESIAN_POINT('Ctrl Pts',(210.,-5.40280661787305,130.157751497854));
#188447=CARTESIAN_POINT('Ctrl Pts',(210.,-5.39955346179212,130.041952156823));
#188448=CARTESIAN_POINT('Ctrl Pts',(210.,-5.39228769078652,129.926152028858));
#188449=CARTESIAN_POINT('Ctrl Pts',(210.,-5.38110695373693,129.810516944227));
#188450=CARTESIAN_POINT('Ctrl Pts',(210.,-5.37798956653967,129.778275837868));
#188451=CARTESIAN_POINT('Ctrl Pts',(210.,-5.37456773065206,129.746047563338));
#188452=CARTESIAN_POINT('Ctrl Pts',(210.,-5.37084332865221,129.713835726721));
#188453=CARTESIAN_POINT('Ctrl Pts',(210.,-5.36786151250135,129.688046412175));
#188454=CARTESIAN_POINT('Ctrl Pts',(210.,-5.36468519189614,129.662263949371));
#188455=CARTESIAN_POINT('Ctrl Pts',(210.,-5.36131905158111,129.636517152514));
#188456=CARTESIAN_POINT('Ctrl Pts',(210.,-5.34132632447221,129.483597596195));
#188457=CARTESIAN_POINT('Ctrl Pts',(210.,-5.31462277703016,129.331755121105));
#188458=CARTESIAN_POINT('Ctrl Pts',(210.,-5.28154289170897,129.181379978409));
#188459=CARTESIAN_POINT('Ctrl Pts',(210.,-5.24788597458129,129.028381754061));
#188460=CARTESIAN_POINT('Ctrl Pts',(210.,-5.20762823228242,128.876901854454));
#188461=CARTESIAN_POINT('Ctrl Pts',(210.,-5.16106759031274,128.727341113289));
#188462=CARTESIAN_POINT('Ctrl Pts',(210.,-5.1136565897567,128.575048874982));
#188463=CARTESIAN_POINT('Ctrl Pts',(210.,-5.05971025362034,128.424745789725));
#188464=CARTESIAN_POINT('Ctrl Pts',(210.,-4.99948878343386,128.276855218127));
#188465=CARTESIAN_POINT('Ctrl Pts',(210.,-4.94601440467812,128.145534006347));
#188466=CARTESIAN_POINT('Ctrl Pts',(210.,-4.88759133985197,128.01611464299));
#188467=CARTESIAN_POINT('Ctrl Pts',(210.,-4.82436816053947,127.88890102204));
#188468=CARTESIAN_POINT('Ctrl Pts',(210.,-4.79249149405723,127.824760841));
#188469=CARTESIAN_POINT('Ctrl Pts',(210.,-4.75939410526878,127.761181537784));
#188470=CARTESIAN_POINT('Ctrl Pts',(210.,-4.7250921856227,127.698203303454));
#188471=CARTESIAN_POINT('Ctrl Pts',(210.,-4.71478448273727,127.679278388044));
#188472=CARTESIAN_POINT('Ctrl Pts',(210.,-4.70436799826693,127.660407756002));
#188473=CARTESIAN_POINT('Ctrl Pts',(210.,-4.69384313927245,127.641592516773));
#188474=CARTESIAN_POINT('Ctrl Pts',(210.,-4.68242422337511,127.621178976367));
#188475=CARTESIAN_POINT('Ctrl Pts',(210.,-4.67088203968081,127.60083836979));
#188476=CARTESIAN_POINT('Ctrl Pts',(210.,-4.65921993791005,127.580576301963));
#188477=CARTESIAN_POINT('Ctrl Pts',(210.,-4.64586056367047,127.5573653446));
#188478=CARTESIAN_POINT('Ctrl Pts',(210.,-4.63234280926635,127.534255628605));
#188479=CARTESIAN_POINT('Ctrl Pts',(210.,-4.61866803274399,127.511249065334));
#188480=CARTESIAN_POINT('Ctrl Pts',(210.,-4.53526957206909,127.370938767826));
#188481=CARTESIAN_POINT('Ctrl Pts',(210.,-4.44603502941789,127.234464045224));
#188482=CARTESIAN_POINT('Ctrl Pts',(210.,-4.35129440682451,127.102081779137));
#188483=CARTESIAN_POINT('Ctrl Pts',(210.,-4.25655378423112,126.969699513049));
#188484=CARTESIAN_POINT('Ctrl Pts',(210.,-4.15630670922515,126.841409133477));
#188485=CARTESIAN_POINT('Ctrl Pts',(210.,-4.05083428316753,126.71748608273));
#188486=CARTESIAN_POINT('Ctrl Pts',(210.,-3.99881145153813,126.656362732817));
#188487=CARTESIAN_POINT('Ctrl Pts',(210.,-3.94551667042523,126.596302213789));
#188488=CARTESIAN_POINT('Ctrl Pts',(210.,-3.8909797140714,126.537339895932));
#188489=CARTESIAN_POINT('Ctrl Pts',(210.,-3.86497510378344,126.509225160529));
#188490=CARTESIAN_POINT('Ctrl Pts',(210.,-3.8386880328713,126.481360140095));
#188491=CARTESIAN_POINT('Ctrl Pts',(210.,-3.81212153503869,126.453748815486));
#188492=CARTESIAN_POINT('Ctrl Pts',(210.,-3.79363314055594,126.43453329582));
#188493=CARTESIAN_POINT('Ctrl Pts',(210.,-3.77500857133956,126.41543988829));
#188494=CARTESIAN_POINT('Ctrl Pts',(210.,-3.75626121342458,126.396482227117));
#188495=CARTESIAN_POINT('Ctrl Pts',(210.,-3.6393612358576,126.278270894304));
#188496=CARTESIAN_POINT('Ctrl Pts',(210.,-3.51758395568067,126.165223350996));
#188497=CARTESIAN_POINT('Ctrl Pts',(210.,-3.39124299655272,126.057613808602));
#188498=CARTESIAN_POINT('Ctrl Pts',(210.,-3.26529717903502,125.950340823791));
#188499=CARTESIAN_POINT('Ctrl Pts',(210.,-3.13481576057488,125.848471304097));
#188500=CARTESIAN_POINT('Ctrl Pts',(210.,-3.00006601075642,125.752304395756));
#188501=CARTESIAN_POINT('Ctrl Pts',(210.,-2.86552956545396,125.656289716534));
#188502=CARTESIAN_POINT('Ctrl Pts',(210.,-2.72673788371416,125.565959020801));
#188503=CARTESIAN_POINT('Ctrl Pts',(210.,-2.58391981636417,125.481646183644));
#188504=CARTESIAN_POINT('Ctrl Pts',(210.,2.59168471337878,125.476247689738));
#188505=CARTESIAN_POINT('Ctrl Pts',(210.,2.71111266644001,125.545959660002));
#188506=CARTESIAN_POINT('Ctrl Pts',(210.,2.82764132334605,125.619975219606));
#188507=CARTESIAN_POINT('Ctrl Pts',(210.,2.94101107271424,125.698291576074));
#188508=CARTESIAN_POINT('Ctrl Pts',(210.,3.07489319746795,125.790777978005));
#188509=CARTESIAN_POINT('Ctrl Pts',(210.,3.20437111666488,125.889261565323));
#188510=CARTESIAN_POINT('Ctrl Pts',(210.,3.32928169753943,125.993299430327));
#188511=CARTESIAN_POINT('Ctrl Pts',(210.,3.45638475582413,126.099163406996));
#188512=CARTESIAN_POINT('Ctrl Pts',(210.,3.57875916616007,126.210779035122));
#188513=CARTESIAN_POINT('Ctrl Pts',(210.,3.69619194875321,126.327715160383));
#188514=CARTESIAN_POINT('Ctrl Pts',(210.,3.81326715672415,126.444295223309));
#188515=CARTESIAN_POINT('Ctrl Pts',(210.,3.9254310827064,126.566164219876));
#188516=CARTESIAN_POINT('Ctrl Pts',(210.,4.03242689161515,126.692918634597));
#188517=CARTESIAN_POINT('Ctrl Pts',(210.,4.08855183263102,126.759408005744));
#188518=CARTESIAN_POINT('Ctrl Pts',(210.,4.14325394828036,126.827241949012));
#188519=CARTESIAN_POINT('Ctrl Pts',(210.,4.19649068322839,126.896363740591));
#188520=CARTESIAN_POINT('Ctrl Pts',(210.,4.213627944191,126.918614507503));
#188521=CARTESIAN_POINT('Ctrl Pts',(210.,4.23061332624127,126.940998731528));
#188522=CARTESIAN_POINT('Ctrl Pts',(210.,4.24744532208237,126.963514532833));
#188523=CARTESIAN_POINT('Ctrl Pts',(210.,4.25948801745557,126.979623789201));
#188524=CARTESIAN_POINT('Ctrl Pts',(210.,4.2714501552323,126.995797726654));
#188525=CARTESIAN_POINT('Ctrl Pts',(210.,4.28332546167438,127.012027509189));
#188526=CARTESIAN_POINT('Ctrl Pts',(210.,4.37956101060926,127.143551023039));
#188527=CARTESIAN_POINT('Ctrl Pts',(210.,4.47021273499132,127.278892841946));
#188528=CARTESIAN_POINT('Ctrl Pts',(210.,4.55510872905159,127.417626057086));
#188529=CARTESIAN_POINT('Ctrl Pts',(210.,4.64006233451871,127.556453418196));
#188530=CARTESIAN_POINT('Ctrl Pts',(210.,4.71925268848836,127.69867755979));
#188531=CARTESIAN_POINT('Ctrl Pts',(210.,4.79246067878325,127.843893787959));
#188532=CARTESIAN_POINT('Ctrl Pts',(210.,4.86453983676611,127.986870851115));
#188533=CARTESIAN_POINT('Ctrl Pts',(210.,4.93081984635459,128.1327491888));
#188534=CARTESIAN_POINT('Ctrl Pts',(210.,4.99104310450031,128.281153501978));
#188535=CARTESIAN_POINT('Ctrl Pts',(210.,5.05072900641638,128.428233642658));
#188536=CARTESIAN_POINT('Ctrl Pts',(210.,5.10446594616894,128.577795554527));
#188537=CARTESIAN_POINT('Ctrl Pts',(210.,5.15195263203104,128.729474268576));
#188538=CARTESIAN_POINT('Ctrl Pts',(210.,5.16621208753242,128.775020843036));
#188539=CARTESIAN_POINT('Ctrl Pts',(210.,5.17990759903754,128.820758254765));
#188540=CARTESIAN_POINT('Ctrl Pts',(210.,5.1930300689057,128.866676489988));
#188541=CARTESIAN_POINT('Ctrl Pts',(210.,5.19914764870326,128.888083166548));
#188542=CARTESIAN_POINT('Ctrl Pts',(210.,5.2051406806358,128.90952914099));
#188543=CARTESIAN_POINT('Ctrl Pts',(210.,5.21100820960353,128.931013391454));
#188544=CARTESIAN_POINT('Ctrl Pts',(210.,5.21620337908719,128.950035764076));
#188545=CARTESIAN_POINT('Ctrl Pts',(210.,5.22129750196036,128.96907841561));
#188546=CARTESIAN_POINT('Ctrl Pts',(210.,5.22629012191461,128.988140212046));
#188547=CARTESIAN_POINT('Ctrl Pts',(210.,5.26614820913265,129.140318177088));
#188548=CARTESIAN_POINT('Ctrl Pts',(210.,5.29954350738592,129.293724156363));
#188549=CARTESIAN_POINT('Ctrl Pts',(210.,5.32627173644381,129.447991892391));
#188550=CARTESIAN_POINT('Ctrl Pts',(210.,5.35267492411837,129.600383582004));
#188551=CARTESIAN_POINT('Ctrl Pts',(210.,5.37257233544242,129.753616870713));
#188552=CARTESIAN_POINT('Ctrl Pts',(210.,5.38571671980561,129.907341042028));
#188553=CARTESIAN_POINT('Ctrl Pts',(210.,5.39854800023754,130.057403448666));
#188554=CARTESIAN_POINT('Ctrl Pts',(210.,5.40494414667608,130.207934192936));
#188555=CARTESIAN_POINT('Ctrl Pts',(210.,5.40462612405376,130.358600246709));
#188556=CARTESIAN_POINT('Ctrl Pts',(210.,5.4044980822189,130.41926120798));
#188557=CARTESIAN_POINT('Ctrl Pts',(210.,5.40328109662435,130.479943979233));
#188558=CARTESIAN_POINT('Ctrl Pts',(210.,5.40095462579041,130.540626197016));
#188559=CARTESIAN_POINT('Ctrl Pts',(210.,5.39555663845411,130.681423940254));
#188560=CARTESIAN_POINT('Ctrl Pts',(210.,5.38418746158711,130.82222005765));
#188561=CARTESIAN_POINT('Ctrl Pts',(210.,5.36695826250822,130.962655854025));
#188562=CARTESIAN_POINT('Ctrl Pts',(210.,5.36453283903126,130.982425564501));
#188563=CARTESIAN_POINT('Ctrl Pts',(210.,5.36199124033403,131.002188101967));
#188564=CARTESIAN_POINT('Ctrl Pts',(210.,5.35933373296221,131.021942432198));
#188565=CARTESIAN_POINT('Ctrl Pts',(210.,5.35674292549998,131.041200954947));
#188566=CARTESIAN_POINT('Ctrl Pts',(210.,5.35404312369154,131.060442922715));
#188567=CARTESIAN_POINT('Ctrl Pts',(210.,5.35123522163466,131.079665129237));
#188568=CARTESIAN_POINT('Ctrl Pts',(210.,5.32917189754803,131.23070521666));
#188569=CARTESIAN_POINT('Ctrl Pts',(210.,5.30043229141883,131.380573392734));
#188570=CARTESIAN_POINT('Ctrl Pts',(210.,5.26526672076462,131.52884789957));
#188571=CARTESIAN_POINT('Ctrl Pts',(210.,5.22989628612353,131.677986208872));
#188572=CARTESIAN_POINT('Ctrl Pts',(210.,5.18802438233364,131.825513008037));
#188573=CARTESIAN_POINT('Ctrl Pts',(210.,5.13985568266502,131.970981511079));
#188574=CARTESIAN_POINT('Ctrl Pts',(210.,5.09214210403352,132.115075557753));
#188575=CARTESIAN_POINT('Ctrl Pts',(210.,5.03824965696429,132.257150705429));
#188576=CARTESIAN_POINT('Ctrl Pts',(210.,4.97833532758118,132.396744612767));
#188577=CARTESIAN_POINT('Ctrl Pts',(210.,4.92981628697671,132.509788729726));
#188578=CARTESIAN_POINT('Ctrl Pts',(210.,4.87734729734596,132.621205309558));
#188579=CARTESIAN_POINT('Ctrl Pts',(210.,4.82099454674417,132.730730504221));
#188580=CARTESIAN_POINT('Ctrl Pts',(210.,4.79165588826149,132.787752073659));
#188581=CARTESIAN_POINT('Ctrl Pts',(210.,4.76126429707162,132.844260685062));
#188582=CARTESIAN_POINT('Ctrl Pts',(210.,4.72982767878697,132.900216977775));
#188583=CARTESIAN_POINT('Ctrl Pts',(210.,4.71933699539195,132.91889009794));
#188584=CARTESIAN_POINT('Ctrl Pts',(210.,4.70872882129724,132.937503608749));
#188585=CARTESIAN_POINT('Ctrl Pts',(210.,4.69800701316631,132.956049819302));
#188586=CARTESIAN_POINT('Ctrl Pts',(210.,4.67896109085937,132.988994792853));
#188587=CARTESIAN_POINT('Ctrl Pts',(210.,4.65956569768156,133.021711868397));
#188588=CARTESIAN_POINT('Ctrl Pts',(210.,4.63982391216924,133.054194020027));
#188589=CARTESIAN_POINT('Ctrl Pts',(210.,4.56178429176233,133.182596528585));
#188590=CARTESIAN_POINT('Ctrl Pts',(210.,4.47833472600848,133.30733089509));
#188591=CARTESIAN_POINT('Ctrl Pts',(210.,4.3897187404882,133.4281029892));
#188592=CARTESIAN_POINT('Ctrl Pts',(210.,4.30158605741235,133.548216404765));
#188593=CARTESIAN_POINT('Ctrl Pts',(210.,4.20834258956795,133.66441109461));
#188594=CARTESIAN_POINT('Ctrl Pts',(210.,4.11019598182694,133.776357668134));
#188595=CARTESIAN_POINT('Ctrl Pts',(210.,4.06527327633945,133.827596759005));
#188596=CARTESIAN_POINT('Ctrl Pts',(210.,4.01932297958479,133.877945279926));
#188597=CARTESIAN_POINT('Ctrl Pts',(210.,3.9723632412024,133.927368436226));
#188598=CARTESIAN_POINT('Ctrl Pts',(210.,3.95145209377834,133.949376542386));
#188599=CARTESIAN_POINT('Ctrl Pts',(210.,3.93034076955951,133.971201128248));
#188600=CARTESIAN_POINT('Ctrl Pts',(210.,3.90903081243557,133.992838982041));
#188601=CARTESIAN_POINT('Ctrl Pts',(210.,3.89187183158307,134.010261988421));
#188602=CARTESIAN_POINT('Ctrl Pts',(210.,3.87458340886331,134.027564474838));
#188603=CARTESIAN_POINT('Ctrl Pts',(210.,3.85717820998098,134.044733292105));
#188604=CARTESIAN_POINT('Ctrl Pts',(210.,3.75307497292274,134.147422693473));
#188605=CARTESIAN_POINT('Ctrl Pts',(210.,3.64469941185318,134.245433426635));
#188606=CARTESIAN_POINT('Ctrl Pts',(210.,3.5322642813685,134.338467234451));
#188607=CARTESIAN_POINT('Ctrl Pts',(210.000000000001,3.42170402111848,134.429949691579));
#188608=CARTESIAN_POINT('Ctrl Pts',(210.000000000001,3.30721789468442,134.516620114227));
#188609=CARTESIAN_POINT('Ctrl Pts',(210.000000000001,3.18898565748847,134.598150619545));
#188610=CARTESIAN_POINT('Ctrl Pts',(210.000000000001,3.0814058769606,134.672335411075));
#188611=CARTESIAN_POINT('Ctrl Pts',(210.000000000001,2.97072408738642,134.742264450146));
#188612=CARTESIAN_POINT('Ctrl Pts',(210.000000000001,2.85706463458494,134.807654853105));
#188613=CARTESIAN_POINT('Origin',(236.,4.44872159004524,125.399836936956));
#188614=CARTESIAN_POINT('',(236.,4.44872159004524,125.399836936956));
#188615=CARTESIAN_POINT('',(236.,4.44872159004524,136.208884298175));
#188616=CARTESIAN_POINT('',(236.,4.44872159004524,128.102098777261));
#188617=CARTESIAN_POINT('',(224.,4.44872159004524,125.399836936956));
#188618=CARTESIAN_POINT('',(210.,4.44872159004524,125.399836936956));
#188619=CARTESIAN_POINT('',(224.,4.44872159004524,136.208884298175));
#188620=CARTESIAN_POINT('',(224.,4.44872159004524,143.664891345585));
#188621=CARTESIAN_POINT('',(210.,4.44872159004524,136.208884298175));
#188622=CARTESIAN_POINT('Origin',(224.,5.72436079502262,130.804360617566));
#188623=CARTESIAN_POINT('Origin',(224.,0.,130.804360617566));
#188624=CARTESIAN_POINT('Origin',(236.,-4.44872159004524,136.208884298175));
#188625=CARTESIAN_POINT('',(236.,-4.44872159004524,136.208884298175));
#188626=CARTESIAN_POINT('',(236.,-4.44872159004524,125.399836936956));
#188627=CARTESIAN_POINT('',(236.,-4.44872159004524,133.50662245787));
#188628=CARTESIAN_POINT('',(224.,-4.44872159004524,136.208884298175));
#188629=CARTESIAN_POINT('',(210.,-4.44872159004524,136.208884298175));
#188630=CARTESIAN_POINT('',(224.,-4.44872159004524,125.399836936956));
#188631=CARTESIAN_POINT('',(224.,-4.44872159004524,117.943829889547));
#188632=CARTESIAN_POINT('',(210.,-4.44872159004524,125.399836936956));
#188633=CARTESIAN_POINT('Origin',(224.,-5.72436079502262,130.804360617566));
#188634=CARTESIAN_POINT('',(224.,-7.,130.804360617566));
#188635=CARTESIAN_POINT('Origin',(224.,0.,130.804360617566));
#188636=CARTESIAN_POINT('Origin',(224.,0.,130.804360617566));
#188637=CARTESIAN_POINT('Origin',(210.,0.,130.804360617566));
#188638=CARTESIAN_POINT('',(210.,-7.,130.804360617566));
#188639=CARTESIAN_POINT('Origin',(236.,0.,130.804360617566));
#188640=CARTESIAN_POINT('Origin',(236.,0.,130.804360617566));
#188641=CARTESIAN_POINT('Origin',(236.,0.,130.804360617566));
#188642=CARTESIAN_POINT('Ctrl Pts',(210.579426101437,-2.14555810197798,
126.384433368448));
#188643=CARTESIAN_POINT('Ctrl Pts',(210.533016425084,-2.88204635455982,
126.741945114569));
#188644=CARTESIAN_POINT('Ctrl Pts',(210.440198811428,-4.16073755837059,
127.832228156677));
#188645=CARTESIAN_POINT('Ctrl Pts',(210.254565323169,-5.41774734084591,
130.983824311839));
#188646=CARTESIAN_POINT('Ctrl Pts',(210.022525636658,-3.70466367662459,
135.280954889074));
#188647=CARTESIAN_POINT('Ctrl Pts',(209.744078012845,1.77278938863763,136.341871604603));
#188648=CARTESIAN_POINT('Ctrl Pts',(209.465630389032,5.61248518735455,132.305536381355));
#188649=CARTESIAN_POINT('Ctrl Pts',(209.187182765219,4.2990952821384,126.894094626803));
#188650=CARTESIAN_POINT('Ctrl Pts',(208.908735141406,-0.967335548355457,
125.073681250508));
#188651=CARTESIAN_POINT('Ctrl Pts',(208.630287517594,-5.34357155608916,
128.520706403956));
#188652=CARTESIAN_POINT('Ctrl Pts',(208.351839893781,-4.80999390579215,
134.065650134797));
#188653=CARTESIAN_POINT('Ctrl Pts',(208.073392269968,0.144086686833323,
136.613971320579));
#188654=CARTESIAN_POINT('Ctrl Pts',(207.794944646155,4.96557142732685,133.823362329787));
#188655=CARTESIAN_POINT('Ctrl Pts',(207.516497022342,5.22403776314189,128.258534510045));
#188656=CARTESIAN_POINT('Ctrl Pts',(207.238049398529,0.681816090004523,
125.033145533949));
#188657=CARTESIAN_POINT('Ctrl Pts',(206.959601774716,-4.48693345015888,
127.111248278652));
#188658=CARTESIAN_POINT('Ctrl Pts',(206.681154150904,-5.53242507739068,
132.583126545744));
#188659=CARTESIAN_POINT('Ctrl Pts',(206.40270652709,-1.49388053201802,136.420413394932));
#188660=CARTESIAN_POINT('Ctrl Pts',(206.124258903278,3.91746311099657,135.0968180907));
#188661=CARTESIAN_POINT('Ctrl Pts',(205.845811279465,5.72885172159717,129.828666190814));
#188662=CARTESIAN_POINT('Ctrl Pts',(205.567363655652,2.27570431130586,125.457128678938));
#188663=CARTESIAN_POINT('Ctrl Pts',(205.288916031839,-3.26870357308214,
125.999436687584));
#188664=CARTESIAN_POINT('Ctrl Pts',(205.010468408026,-5.80933288384994,
130.9572347388));
#188665=CARTESIAN_POINT('Ctrl Pts',(204.732020784213,-3.01146890392974,
135.774549108008));
#188666=CARTESIAN_POINT('Ctrl Pts',(204.4535731604,2.5537877891123,136.024502973214));
#188667=CARTESIAN_POINT('Ctrl Pts',(204.175125536587,5.77223831170541,131.477401078575));
#188668=CARTESIAN_POINT('Ctrl Pts',(203.896677912775,3.6862837897924,126.311807855303));
#188669=CARTESIAN_POINT('Ctrl Pts',(203.618230288961,-1.78718543642468,
125.274651160291));
#188670=CARTESIAN_POINT('Ctrl Pts',(203.339782665149,-5.61831856260093,
129.319027308227));
#188671=CARTESIAN_POINT('Ctrl Pts',(203.061335041336,-4.28649139606962,
134.728352208566));
#188672=CARTESIAN_POINT('Ctrl Pts',(202.782887417523,0.984411954691954,
136.531720532469));
#188673=CARTESIAN_POINT('Ctrl Pts',(202.50443979371,5.3506888113544,133.071924892697));
#188674=CARTESIAN_POINT('Ctrl Pts',(202.225992169897,4.79994404549834,127.528348460205));
#188675=CARTESIAN_POINT('Ctrl Pts',(201.947544546084,-0.161714807569177,
124.995267158526));
#188676=CARTESIAN_POINT('Ctrl Pts',(201.669096922271,-4.97476565284641,
127.800458955558));
#188677=CARTESIAN_POINT('Ctrl Pts',(201.390649298458,-5.21624989388704,
133.366089631302));
#188678=CARTESIAN_POINT('Ctrl Pts',(201.112201674645,-0.664255310463968,
136.577616490799));
#188679=CARTESIAN_POINT('Ctrl Pts',(200.833754050833,4.49815745262305,134.483803242045));
#188680=CARTESIAN_POINT('Ctrl Pts',(200.55530642702,5.52698326394509,129.008761972148));
#188681=CARTESIAN_POINT('Ctrl Pts',(200.276858803207,1.47678146385132,125.183788137525));
#188682=CARTESIAN_POINT('Ctrl Pts',(199.998411179394,-3.93051035674001,
126.523845831826));
#188683=CARTESIAN_POINT('Ctrl Pts',(199.719963555581,-5.7258551755912,131.79748749945));
#188684=CARTESIAN_POINT('Ctrl Pts',(199.441515931768,-2.25941881165118,
136.158494079568));
#188685=CARTESIAN_POINT('Ctrl Pts',(199.163068307955,3.28331306145151,135.599313572066));
#188686=CARTESIAN_POINT('Ctrl Pts',(198.884620684142,5.80884062984016,130.633805545853));
#188687=CARTESIAN_POINT('Ctrl Pts',(198.606173060329,2.99632743704681,125.825029298466));
#188688=CARTESIAN_POINT('Ctrl Pts',(198.327725436517,-2.56966429165962,
125.592015279473));
#188689=CARTESIAN_POINT('Ctrl Pts',(198.049277812704,-5.77426007141042,
130.148891988961));
#188690=CARTESIAN_POINT('Ctrl Pts',(197.770830188891,-3.6725929338218,135.308112346714));
#188691=CARTESIAN_POINT('Ctrl Pts',(197.492382565078,1.80400769380988,136.328604885883));
#188692=CARTESIAN_POINT('Ctrl Pts',(197.213934941265,5.62281338150559,132.272586816804));
#188693=CARTESIAN_POINT('Ctrl Pts',(196.935487317452,4.27452826130232,126.867340597462));
#188694=CARTESIAN_POINT('Ctrl Pts',(196.657039693639,-1.00183950872307,
125.080023442474));
#188695=CARTESIAN_POINT('Ctrl Pts',(196.378592069827,-5.35756571281285,
128.553092501978));
#188696=CARTESIAN_POINT('Ctrl Pts',(196.100144446013,-4.78995075846325,
134.094966979145));
#188697=CARTESIAN_POINT('Ctrl Pts',(195.821696822201,0.179394940810534,
136.612934965078));
#188698=CARTESIAN_POINT('Ctrl Pts',(195.543249198387,4.98388545340951,133.79310689028));
#188699=CARTESIAN_POINT('Ctrl Pts',(195.264801574575,5.20842871066526,128.22676699923));
#188700=CARTESIAN_POINT('Ctrl Pts',(194.986353950762,0.64668042870769,125.029109720981));
#188701=CARTESIAN_POINT('Ctrl Pts',(194.70790632695,-4.50933557513701,127.138625880003));
#188702=CARTESIAN_POINT('Ctrl Pts',(194.429458703136,-5.52149247872048,
132.616773181746));
#188703=CARTESIAN_POINT('Ctrl Pts',(194.151011079324,-1.4596675342632,136.429401878284));
#188704=CARTESIAN_POINT('Ctrl Pts',(193.87256345551,3.9435205654586,135.072892454764));
#188705=CARTESIAN_POINT('Ctrl Pts',(193.594115831698,5.72280591721378,129.793810802232));
#188706=CARTESIAN_POINT('Ctrl Pts',(193.315668207884,2.24311220566103,125.443375061888));
#188707=CARTESIAN_POINT('Ctrl Pts',(193.037220584072,-3.29789204077089,
126.019423148508));
#188708=CARTESIAN_POINT('Ctrl Pts',(192.758772960259,-5.80829461271728,
130.992595012001));
#188709=CARTESIAN_POINT('Ctrl Pts',(192.480325336446,-2.98115818654302,
135.792788662769));
#188710=CARTESIAN_POINT('Ctrl Pts',(192.201877712633,2.58551697539033,136.008860638253));
#188711=CARTESIAN_POINT('Ctrl Pts',(191.92343008882,5.77622834646622,131.442251348686));
#188712=CARTESIAN_POINT('Ctrl Pts',(191.644982465007,3.658868051582,126.289451639914));
#188713=CARTESIAN_POINT('Ctrl Pts',(191.366534841194,-1.82081323706467,
125.285632716038));
#188714=CARTESIAN_POINT('Ctrl Pts',(191.088087217381,-5.6272561125207,129.35325512882));
#188715=CARTESIAN_POINT('Ctrl Pts',(190.809639593569,-4.26252552731426,
134.754372595315));
#188716=CARTESIAN_POINT('Ctrl Pts',(190.531191969755,1.01925778154541,136.525622023071));
#188717=CARTESIAN_POINT('Ctrl Pts',(190.252744345943,5.36439298267566,133.039311718326));
#188718=CARTESIAN_POINT('Ctrl Pts',(189.974296722129,4.77991309789331,127.499190535413));
#188719=CARTESIAN_POINT('Ctrl Pts',(189.695849098317,-0.197073412116412,
124.996359191464));
#188720=CARTESIAN_POINT('Ctrl Pts',(189.417401474504,-4.99295908396257,
127.830797421458));
#188721=CARTESIAN_POINT('Ctrl Pts',(189.138953850692,-5.20055927725872,
133.397794962038));
#188722=CARTESIAN_POINT('Ctrl Pts',(188.860506226878,-0.629099556198964,
136.581553036358));
#188723=CARTESIAN_POINT('Ctrl Pts',(188.582058603065,4.52047192378579,134.456353509349));
#188724=CARTESIAN_POINT('Ctrl Pts',(188.303610979253,5.51595054314194,128.975150924561));
#188725=CARTESIAN_POINT('Ctrl Pts',(188.02516335544,1.44254008251539,125.174902685784));
#188726=CARTESIAN_POINT('Ctrl Pts',(187.746715731627,-3.95649424194195,
126.547851272005));
#188727=CARTESIAN_POINT('Ctrl Pts',(187.468268107814,-5.71970364354381,
131.832324004755));
#188728=CARTESIAN_POINT('Ctrl Pts',(187.189820484001,-2.22678481978599,
136.172148603481));
#188729=CARTESIAN_POINT('Ctrl Pts',(186.911372860188,3.312440468869,135.579238274173));
#188730=CARTESIAN_POINT('Ctrl Pts',(186.632925236375,5.80769478834652,130.598448644184));
#188731=CARTESIAN_POINT('Ctrl Pts',(186.354477612562,2.96596131899707,125.806882058373));
#188732=CARTESIAN_POINT('Ctrl Pts',(186.076029988749,-2.60134570724499,
125.607754128061));
#188733=CARTESIAN_POINT('Ctrl Pts',(185.797582364937,-5.7781431113317,130.184053693262));
#188734=CARTESIAN_POINT('Ctrl Pts',(185.519134741124,-3.64510927408837,
135.33038501822));
#188735=CARTESIAN_POINT('Ctrl Pts',(185.240687117311,1.83760191255446,136.317521027561));
#188736=CARTESIAN_POINT('Ctrl Pts',(184.962239493498,5.63164671340385,132.238331952975));
#188737=CARTESIAN_POINT('Ctrl Pts',(184.683791869685,4.25048330587202,126.841393274542));
#188738=CARTESIAN_POINT('Ctrl Pts',(184.405344245872,-1.03666661210287,
125.086227982629));
#188739=CARTESIAN_POINT('Ctrl Pts',(184.126896622059,-5.37117055753467,
128.585747235914));
#188740=CARTESIAN_POINT('Ctrl Pts',(183.848448998247,-4.7698311568614,134.124063801647));
#188741=CARTESIAN_POINT('Ctrl Pts',(183.570001374433,0.214750057761129,
136.611735317726));
#188742=CARTESIAN_POINT('Ctrl Pts',(183.291553750621,5.00198646042476,133.762713190383));
#188743=CARTESIAN_POINT('Ctrl Pts',(183.013106126807,5.19264166658148,128.195109572179));
#188744=CARTESIAN_POINT('Ctrl Pts',(182.734658502995,0.611512855797894,
125.025280195685));
#188745=CARTESIAN_POINT('Ctrl Pts',(182.456210879182,-4.53156639540017,
127.166143403126));
#188746=CARTESIAN_POINT('Ctrl Pts',(182.177763255369,-5.5103575085511,132.650350493844));
#188747=CARTESIAN_POINT('Ctrl Pts',(181.899315631556,-1.42539926727337,
136.438183069882));
#188748=CARTESIAN_POINT('Ctrl Pts',(181.620868007743,3.96943126600311,135.048808039769));
#188749=CARTESIAN_POINT('Ctrl Pts',(181.34242038393,5.71654838332065,129.758993181434));
#188750=CARTESIAN_POINT('Ctrl Pts',(181.063972760118,2.21043680528058,125.429819927867));
#188751=CARTESIAN_POINT('Ctrl Pts',(180.785525136304,-3.32695821097111,
126.039587007222));
#188752=CARTESIAN_POINT('Ctrl Pts',(180.507077512492,-5.80704116228462,
131.027948262352));
#188753=CARTESIAN_POINT('Ctrl Pts',(180.228629888679,-2.95073697519064,
135.810843394787));
#188754=CARTESIAN_POINT('Ctrl Pts',(179.950182264866,2.61715034058839,135.993025435236));
#188755=CARTESIAN_POINT('Ctrl Pts',(179.671734641053,5.78000434826875,131.407077988614));
#188756=CARTESIAN_POINT('Ctrl Pts',(179.39328701724,3.63131672880039,126.26726272238));
#188757=CARTESIAN_POINT('Ctrl Pts',(179.114839393428,-1.8543735647511,125.296818772266));
#188758=CARTESIAN_POINT('Ctrl Pts',(178.836391769614,-5.63598514348121,
129.387536719606));
#188759=CARTESIAN_POINT('Ctrl Pts',(178.557944145802,-4.23840170853308,
134.780246613475));
#188760=CARTESIAN_POINT('Ctrl Pts',(178.279496521988,1.05406583912245,136.519311509933));
#188761=CARTESIAN_POINT('Ctrl Pts',(178.001048898175,5.3778983746034,133.006615727177));
#188762=CARTESIAN_POINT('Ctrl Pts',(177.722601274363,4.75970502876524,127.470155084831));
#188763=CARTESIAN_POINT('Ctrl Pts',(177.44415365055,-0.232424713990654,
124.997666442073));
#188764=CARTESIAN_POINT('Ctrl Pts',(177.165706026737,-5.01096749916768,
127.861246073811));
#188765=CARTESIAN_POINT('Ctrl Pts',(176.887258402924,-5.18467595198119,
133.429404192122));
#188766=CARTESIAN_POINT('Ctrl Pts',(176.608810779111,-0.593920490425269,
136.585275505922));
#188767=CARTESIAN_POINT('Ctrl Pts',(176.330363155298,4.54261888720253,134.428768450716));
#188768=CARTESIAN_POINT('Ctrl Pts',(176.051915531486,5.50471342676105,128.941607659011));
#188769=CARTESIAN_POINT('Ctrl Pts',(175.773467907672,1.40824524732727,125.166225835676));
#188770=CARTESIAN_POINT('Ctrl Pts',(175.49502028386,-3.98233151779528,126.572014438702));
#188771=CARTESIAN_POINT('Ctrl Pts',(175.216572660047,-5.7133401657742,131.867122418498));
#188772=CARTESIAN_POINT('Ctrl Pts',(174.938125036234,-2.19406831359054,
136.185604222037));
#188773=CARTESIAN_POINT('Ctrl Pts',(174.659677412421,3.34144513258691,135.558986041432));
#188774=CARTESIAN_POINT('Ctrl Pts',(174.381229788608,5.80633374058666,130.563099372659));
#188775=CARTESIAN_POINT('Ctrl Pts',(174.102782164795,2.93548529615992,125.788920001687));
#188776=CARTESIAN_POINT('Ctrl Pts',(173.824334540982,-2.63293072900865,
125.623685538813));
#188777=CARTESIAN_POINT('Ctrl Pts',(173.54588691717,-5.7818120400351,130.219238383264));
#188778=CARTESIAN_POINT('Ctrl Pts',(173.267439293356,-3.61749054349026,
135.352489976228));
#188779=CARTESIAN_POINT('Ctrl Pts',(172.988991669544,1.87112803828436,136.306232877052));
#188780=CARTESIAN_POINT('Ctrl Pts',(172.71054404573,5.64027136256211,132.204023952811));
#188781=CARTESIAN_POINT('Ctrl Pts',(172.432096421918,4.22628084721974,126.815592800833));
#188782=CARTESIAN_POINT('Ctrl Pts',(172.153648798105,-1.07145530142008,
125.092644410292));
#188783=CARTESIAN_POINT('Ctrl Pts',(171.875201174292,-5.38457637155629,
128.618484181386));
#188784=CARTESIAN_POINT('Ctrl Pts',(171.596753550479,-4.74953480741189,
134.153037611328));
#188785=CARTESIAN_POINT('Ctrl Pts',(171.318305926666,0.25009721706947,136.610320475968));
#188786=CARTESIAN_POINT('Ctrl Pts',(171.039858302853,5.01990211699227,133.732209867644));
#188787=CARTESIAN_POINT('Ctrl Pts',(170.76141067904,5.1766622072511,128.163548831885));
#188788=CARTESIAN_POINT('Ctrl Pts',(170.482963055228,0.576322623054293,
125.021664816339));
#188789=CARTESIAN_POINT('Ctrl Pts',(170.204515431414,-4.55362929680409,
127.193795741725));
#188790=CARTESIAN_POINT('Ctrl Pts',(169.926067807602,-5.4990183500578,132.683859402108));
#188791=CARTESIAN_POINT('Ctrl Pts',(169.647620183788,-1.39107818158956,
136.446755498118));
#188792=CARTESIAN_POINT('Ctrl Pts',(169.369172559976,3.99519487781229,135.024566345214));
#188793=CARTESIAN_POINT('Ctrl Pts',(169.090724936163,5.71007902062496,129.724214297113));
#188794=CARTESIAN_POINT('Ctrl Pts',(168.81227731235,2.17767949635139,125.416463949427));
#188795=CARTESIAN_POINT('Ctrl Pts',(168.533829688537,-3.35590109951139,
126.059927426375));
#188796=CARTESIAN_POINT('Ctrl Pts',(168.255382064725,-5.80557252980615,
131.063293227581));
#188797=CARTESIAN_POINT('Ctrl Pts',(167.976934440911,-2.92020642319446,
135.828712609743));
#188798=CARTESIAN_POINT('Ctrl Pts',(167.698486817099,2.64868672631821,135.976997964335));
#188799=CARTESIAN_POINT('Ctrl Pts',(167.420039193286,5.78356616988455,131.371882294628));
#188800=CARTESIAN_POINT('Ctrl Pts',(167.141591569473,3.60363084624196,126.245241928676));
#188801=CARTESIAN_POINT('Ctrl Pts',(166.86314394566,-1.88786517794308,125.308208912483));
#188802=CARTESIAN_POINT('Ctrl Pts',(166.584696321847,-5.64450533093961,
129.421870811324));
#188803=CARTESIAN_POINT('Ctrl Pts',(166.306248698034,-4.21412083421794,
134.805973303719));
#188804=CARTESIAN_POINT('Ctrl Pts',(166.027801074221,1.08883483790225,136.512789227187));
#188805=CARTESIAN_POINT('Ctrl Pts',(165.749353450409,5.3912044865292,132.973838130654));
#188806=CARTESIAN_POINT('Ctrl Pts',(165.470905826595,4.73932058701693,127.441243184462));
#188807=CARTESIAN_POINT('Ctrl Pts',(165.192458202783,-0.267767403281747,
124.999188861871));
#188808=CARTESIAN_POINT('Ctrl Pts',(164.914010578969,-5.02879023112935,
127.891803784357));
#188809=CARTESIAN_POINT('Ctrl Pts',(164.635562955157,-5.16860050662956,
133.46091615025));
#188810=CARTESIAN_POINT('Ctrl Pts',(164.357115331344,-0.55871941670932,
136.588783761558));
#188811=CARTESIAN_POINT('Ctrl Pts',(164.078667707531,4.56459752220588,134.401049088318));
#188812=CARTESIAN_POINT('Ctrl Pts',(163.800220083718,5.49327233119978,128.908133418456));
#188813=CARTESIAN_POINT('Ctrl Pts',(163.521772459905,1.37389822909362,125.157757908727));
#188814=CARTESIAN_POINT('Ctrl Pts',(163.243324836092,-4.00802122688977,
126.596334436543));
#188815=CARTESIAN_POINT('Ctrl Pts',(162.964877212279,-5.70676497808368,
131.901881451211));
#188816=CARTESIAN_POINT('Ctrl Pts',(162.686429588467,-2.16127050538683,
136.198860436632));
#188817=CARTESIAN_POINT('Ctrl Pts',(162.407981964654,3.37032597782655,135.538557624299));
#188818=CARTESIAN_POINT('Ctrl Pts',(162.129534340841,5.80475753699479,130.527759041158));
#188819=CARTESIAN_POINT('Ctrl Pts',(161.851086717028,2.90490049783562,125.771143793998));
#188820=CARTESIAN_POINT('Ctrl Pts',(161.572639093215,-2.66441818655578,
125.639808921385));
#188821=CARTESIAN_POINT('Ctrl Pts',(161.294191469402,-5.7852667215671,130.254444755185));
#188822=CARTESIAN_POINT('Ctrl Pts',(161.015743845589,-3.58973776544978,
135.37442640163));
#188823=CARTESIAN_POINT('Ctrl Pts',(160.737296221776,1.90458482867669,136.294740852644));
#188824=CARTESIAN_POINT('Ctrl Pts',(160.458848597964,5.64868700939082,132.169664087608));
#188825=CARTESIAN_POINT('Ctrl Pts',(160.18040097415,4.20192178217643,126.789940132385));
#188826=CARTESIAN_POINT('Ctrl Pts',(159.901953350338,-1.10620428756715,
125.099272487699));
#188827=CARTESIAN_POINT('Ctrl Pts',(159.623505726525,-5.39778265812024,
128.651302125312));
#188828=CARTESIAN_POINT('Ctrl Pts',(159.345058102712,-4.72906246220349,
134.18188733455));
#188829=CARTESIAN_POINT('Ctrl Pts',(159.066610478899,0.285435108933367,
136.608690492233));
#188830=CARTESIAN_POINT('Ctrl Pts',(158.788162855086,5.03763175924073,133.701598052375));
#188831=CARTESIAN_POINT('Ctrl Pts',(158.509715231273,5.16049092479898,128.132085947844));
#188832=CARTESIAN_POINT('Ctrl Pts',(158.23126760746,0.541111034464008,125.018263716911));
#188833=CARTESIAN_POINT('Ctrl Pts',(157.952819983648,-4.57552346179978,
127.221581871133));
#188834=CARTESIAN_POINT('Ctrl Pts',(157.674372359834,-5.48747542341729,
132.717298664853));
#188835=CARTESIAN_POINT('Ctrl Pts',(157.395924736022,-1.35670554899215,
136.455118845335));
#188836=CARTESIAN_POINT('Ctrl Pts',(157.117477112209,4.02081044620608,135.000168269382));
#188837=CARTESIAN_POINT('Ctrl Pts',(156.839029488396,5.70339806885126,129.68947543801));
#188838=CARTESIAN_POINT('Ctrl Pts',(156.560581864583,2.1448414927076,125.403307621479));
#188839=CARTESIAN_POINT('Ctrl Pts',(156.28213424077,-3.38471963390224,126.080443652244));
#188840=CARTESIAN_POINT('Ctrl Pts',(156.003686616957,-5.8038887697026,131.098628597966));
#188841=CARTESIAN_POINT('Ctrl Pts',(155.725238993144,-2.88956766187541,
135.846395645489));
#188842=CARTESIAN_POINT('Ctrl Pts',(155.446791369331,2.68012496398725,135.960778819456));
#188843=CARTESIAN_POINT('Ctrl Pts',(155.168343745519,5.78691367932904,131.336665570917));
#188844=CARTESIAN_POINT('Ctrl Pts',(154.889896121706,3.57581142981733,126.223390074792));
#188845=CARTESIAN_POINT('Ctrl Pts',(154.611448497893,-1.92128683559663,
125.319802714623));
#188846=CARTESIAN_POINT('Ctrl Pts',(154.33300087408,-5.65281635917722,129.456256131708));
#188847=CARTESIAN_POINT('Ctrl Pts',(154.054553250267,-4.18968380410554,
134.831551712731));
#188848=CARTESIAN_POINT('Ctrl Pts',(153.776105626454,1.12356348950664,136.50605541652));
#188849=CARTESIAN_POINT('Ctrl Pts',(153.497658002641,5.40431082539012,132.940980143345));
#188850=CARTESIAN_POINT('Ctrl Pts',(153.219210378828,4.71876052800142,127.412455905645));
#188851=CARTESIAN_POINT('Ctrl Pts',(152.940762755016,-0.303100170353132,
125.000926394444));
#188852=CARTESIAN_POINT('Ctrl Pts',(152.662315131202,-5.04642661941966,
127.922469420767));
#188853=CARTESIAN_POINT('Ctrl Pts',(152.38386750739,-5.15233353688545,133.492329668737));
#188854=CARTESIAN_POINT('Ctrl Pts',(152.105419883576,-0.523497639439988,
136.592077673268));
#188855=CARTESIAN_POINT('Ctrl Pts',(151.826972259764,4.58640701436939,134.373196449306));
#188856=CARTESIAN_POINT('Ctrl Pts',(151.548524635951,5.48162768041213,128.874729443297));
#188857=CARTESIAN_POINT('Ctrl Pts',(151.270077012138,1.33950030055583,125.149499218718));
#188858=CARTESIAN_POINT('Ctrl Pts',(150.991629388325,-4.03356241728369,
126.620810364342));
#188859=CARTESIAN_POINT('Ctrl Pts',(150.713181764512,-5.69997832411825,
131.936599814887));
#188860=CARTESIAN_POINT('Ctrl Pts',(150.434734140699,-2.1283926105098,136.211916756054));
#188861=CARTESIAN_POINT('Ctrl Pts',(150.156286516886,3.39908193439765,135.517953779753));
#188862=CARTESIAN_POINT('Ctrl Pts',(149.877838893074,5.8029662359777,130.49242895923));
#188863=CARTESIAN_POINT('Ctrl Pts',(149.599391269261,2.87420805735513,125.753554094008));
#188864=CARTESIAN_POINT('Ctrl Pts',(149.320943645448,-2.69580691310719,
125.65612367832));
#188865=CARTESIAN_POINT('Ctrl Pts',(149.042496021635,-5.7885070279132,130.289671504441));
#188866=CARTESIAN_POINT('Ctrl Pts',(148.764048397822,-3.56185196835627,
135.396193481562));
#188867=CARTESIAN_POINT('Ctrl Pts',(148.485600774009,1.93797104397778,136.283045380177));
#188868=CARTESIAN_POINT('Ctrl Pts',(148.207153150196,5.6568933420451,132.135253630582));
#188869=CARTESIAN_POINT('Ctrl Pts',(147.928705526383,4.17740701337624,126.764436219762));
#188870=CARTESIAN_POINT('Ctrl Pts',(147.65025790257,-1.14091228290746,125.106111969245));
#188871=CARTESIAN_POINT('Ctrl Pts',(147.371810278758,-5.41078892786276,
128.684199851613));
#188872=CARTESIAN_POINT('Ctrl Pts',(147.093362654945,-4.70841487984645,
134.210611902278));
#188873=CARTESIAN_POINT('Ctrl Pts',(146.814915031132,0.320762423894332,
136.60684542692));
#188874=CARTESIAN_POINT('Ctrl Pts',(146.536467407319,5.05517473019176,133.670878878906));
#188875=CARTESIAN_POINT('Ctrl Pts',(146.258019783506,5.14412841845787,128.100722085923));
#188876=CARTESIAN_POINT('Ctrl Pts',(145.979572159693,0.505879394805349,
125.015077023433));
#188877=CARTESIAN_POINT('Ctrl Pts',(145.70112453588,-4.59724807909095,127.249500761725));
#188878=CARTESIAN_POINT('Ctrl Pts',(145.422676912067,-5.47572915635697,
132.750667042976));
#188879=CARTESIAN_POINT('Ctrl Pts',(145.144229288255,-1.32228264317164,
136.463272801628));
#188880=CARTESIAN_POINT('Ctrl Pts',(144.865781664442,4.0462770219901,134.975614716357));
#188881=CARTESIAN_POINT('Ctrl Pts',(144.587334040629,5.69650577556471,129.654777891387));
#188882=CARTESIAN_POINT('Ctrl Pts',(144.308886416816,2.11192401117359,125.390351431538));
#188883=CARTESIAN_POINT('Ctrl Pts',(144.030438793003,-3.41341274626234,
126.101134924595));
#188884=CARTESIAN_POINT('Ctrl Pts',(143.75199116919,-5.80198994436631,131.133953064144));
#188885=CARTESIAN_POINT('Ctrl Pts',(143.473543545377,-2.85882182656403,
135.863891846773));
#188886=CARTESIAN_POINT('Ctrl Pts',(143.195095921564,2.71146388864014,135.944368601604));
#188887=CARTESIAN_POINT('Ctrl Pts',(142.916648297751,5.790046752559,131.301429122451));
#188888=CARTESIAN_POINT('Ctrl Pts',(142.638200673938,3.54785951038517,126.201707970457));
#188889=CARTESIAN_POINT('Ctrl Pts',(142.359753050125,-1.95463729925998,
125.331599749072));
#188890=CARTESIAN_POINT('Ctrl Pts',(142.081305426313,-5.66091792022584,
129.490691406602));
#188891=CARTESIAN_POINT('Ctrl Pts',(141.8028578025,-4.16509152371897,134.856980892698));
#188892=CARTESIAN_POINT('Ctrl Pts',(141.524410178687,1.15825050705268,136.499110327454));
#188893=CARTESIAN_POINT('Ctrl Pts',(141.245962554874,5.41721690552589,132.908042982814));
#188894=CARTESIAN_POINT('Ctrl Pts',(140.967514931061,4.69802561357932,127.383794315106));
#188895=CARTESIAN_POINT('Ctrl Pts',(140.689067307248,-0.338421705936203,
125.002878975406));
#188896=CARTESIAN_POINT('Ctrl Pts',(140.410619683435,-5.06387601051571,
127.953241846716));
#188897=CARTESIAN_POINT('Ctrl Pts',(140.132172059623,-5.13587564552739,
133.523643583541));
#188898=CARTESIAN_POINT('Ctrl Pts',(139.85372443581,-0.48825646377323,136.595157118993));
#188899=CARTESIAN_POINT('Ctrl Pts',(139.575276811997,4.60804655553434,134.34521156577));
#188900=CARTESIAN_POINT('Ctrl Pts',(139.296829188184,5.46977990589493,128.841396971331));
#188901=CARTESIAN_POINT('Ctrl Pts',(139.018381564371,1.30505273634171,125.141450071677));
#188902=CARTESIAN_POINT('Ctrl Pts',(138.739933940558,-4.05895414253892,
126.645441315135));
#188903=CARTESIAN_POINT('Ctrl Pts',(138.461486316745,-5.69298045535984,
131.971276223022));
#188904=CARTESIAN_POINT('Ctrl Pts',(138.183038692932,-2.09543584726193,
136.224772696493));
#188905=CARTESIAN_POINT('Ctrl Pts',(137.904591069119,3.42771193673771,135.49717527128));
#188906=CARTESIAN_POINT('Ctrl Pts',(137.626143445306,5.80095990391266,130.457110436044));
#188907=CARTESIAN_POINT('Ctrl Pts',(137.347695821494,2.84340911203807,125.736151553513));
#188908=CARTESIAN_POINT('Ctrl Pts',(137.069248197681,-2.727095745542,125.672629205068));
#188909=CARTESIAN_POINT('Ctrl Pts',(136.790800573868,-5.7915328390027,130.324917325691));
#188910=CARTESIAN_POINT('Ctrl Pts',(136.512352950055,-3.53383418552815,
135.417790409441));
#188911=CARTESIAN_POINT('Ctrl Pts',(136.233905326242,1.97128544704926,136.271146893031));
#188912=CARTESIAN_POINT('Ctrl Pts',(135.955457702429,5.66489005643625,132.100793856825));
#188913=CARTESIAN_POINT('Ctrl Pts',(135.677010078616,4.15273744922295,126.739082008025));
#188914=CARTESIAN_POINT('Ctrl Pts',(135.398562454803,-1.17557800132362,
125.113162601491));
#188915=CARTESIAN_POINT('Ctrl Pts',(135.12011483099,-5.42359469883174,128.717176141249));
#188916=CARTESIAN_POINT('Ctrl Pts',(134.841667207177,-4.68759282544451,
134.239210250113));
#188917=CARTESIAN_POINT('Ctrl Pts',(134.563219583365,0.356077852885664,
136.604785348398));
#188918=CARTESIAN_POINT('Ctrl Pts',(134.284771959552,5.0725303797842,133.640053485549));
#188919=CARTESIAN_POINT('Ctrl Pts',(134.006324335739,5.12757529454644,128.069458408322));
#188920=CARTESIAN_POINT('Ctrl Pts',(133.727876711926,0.470629009599695,
125.012104853988));
#188921=CARTESIAN_POINT('Ctrl Pts',(133.449429088113,-4.61880234366392,
127.277551378957));
#188922=CARTESIAN_POINT('Ctrl Pts',(133.1709814643,-5.46377998413907,132.783963299997));
#188923=CARTESIAN_POINT('Ctrl Pts',(132.892533840487,-1.28781073968153,
136.47121706485));
#188924=CARTESIAN_POINT('Ctrl Pts',(132.614086216674,4.07159366149105,134.950906595976));
#188925=CARTESIAN_POINT('Ctrl Pts',(132.335638592862,5.68940239616175,129.620122942976));
#188926=CARTESIAN_POINT('Ctrl Pts',(132.057190969048,2.07892827151876,125.377595859696));
#188927=CARTESIAN_POINT('Ctrl Pts',(131.778743345236,-3.44197937335791,
126.122000476702));
#188928=CARTESIAN_POINT('Ctrl Pts',(131.500295721423,-5.79987612415893,
131.169265317152));
#188929=CARTESIAN_POINT('Ctrl Pts',(131.22184809761,-2.82797005655853,135.881200565267));
#188930=CARTESIAN_POINT('Ctrl Pts',(130.943400473797,2.74270233900145,135.927767918864));
#188931=CARTESIAN_POINT('Ctrl Pts',(130.664952849984,5.79296527347731,131.26617425493));
#188932=CARTESIAN_POINT('Ctrl Pts',(130.386505226171,3.51977612371406,126.180196419108));
#188933=CARTESIAN_POINT('Ctrl Pts',(130.108057602358,-1.98791533311939,
125.343599578688));
#188934=CARTESIAN_POINT('Ctrl Pts',(129.829609978546,-5.66880971387908,
129.52517535999));
#188935=CARTESIAN_POINT('Ctrl Pts',(129.551162354732,-4.14034490433441,
134.882259901329));
#188936=CARTESIAN_POINT('Ctrl Pts',(129.27271473092,1.19289460520041,136.491954217345));
#188937=CARTESIAN_POINT('Ctrl Pts',(128.994267107107,5.42992224869717,132.875027869557));
#188938=CARTESIAN_POINT('Ctrl Pts',(128.715819483294,4.67711661209022,127.355259474909));
#188939=CARTESIAN_POINT('Ctrl Pts',(128.437371859481,-0.373730701178542,
125.005046532403));
#188940=CARTESIAN_POINT('Ctrl Pts',(128.158924235668,-5.0811377578241,127.984119921918));
#188941=CARTESIAN_POINT('Ctrl Pts',(127.880476611855,-5.11922744240848,
133.554856734316));
#188942=CARTESIAN_POINT('Ctrl Pts',(127.602028988042,-0.452997195583419,
136.598021984625));
#188943=CARTESIAN_POINT('Ctrl Pts',(127.323581364229,4.62951534383955,134.3170954747));
#188944=CARTESIAN_POINT('Ctrl Pts',(127.045133740417,5.45772944667181,128.808137237705));
#188945=CARTESIAN_POINT('Ctrl Pts',(126.766686116604,1.2705568129186,125.133610765869));
#188946=CARTESIAN_POINT('Ctrl Pts',(126.488238492791,-4.08419546175569,
126.67022637621));
#188947=CARTESIAN_POINT('Ctrl Pts',(126.209790868978,-5.68577163111709,
132.005909390672));
#188948=CARTESIAN_POINT('Ctrl Pts',(125.931343245165,-2.06240143686808,
136.237427781569));
#188949=CARTESIAN_POINT('Ctrl Pts',(125.652895621352,3.45621492395137,135.476222868834));
#188950=CARTESIAN_POINT('Ctrl Pts',(125.374447997539,5.79873861514512,130.421804780342));
#188951=CARTESIAN_POINT('Ctrl Pts',(125.096000373726,2.8125048031507,125.718936817367));
#188952=CARTESIAN_POINT('Ctrl Pts',(124.817552749914,-2.75828352444112,
125.68932489001));
#188953=CARTESIAN_POINT('Ctrl Pts',(124.5391051261,-5.79434404271298,130.36018091289));
#188954=CARTESIAN_POINT('Ctrl Pts',(124.260657502288,-3.50568545517477,
135.439216384981));
#188955=CARTESIAN_POINT('Ctrl Pts',(123.982209878475,2.00452680341345,136.25904583211));
#188956=CARTESIAN_POINT('Ctrl Pts',(123.703762254662,5.67267685624313,132.066286043259));
#188957=CARTESIAN_POINT('Ctrl Pts',(123.425314630849,4.12791400385628,126.71387843668));
#188958=CARTESIAN_POINT('Ctrl Pts',(123.146867007036,-1.21020015826455,
125.120424123171));
#188959=CARTESIAN_POINT('Ctrl Pts',(122.868419383223,-5.43619949650465,
128.750229772276));
#188960=CARTESIAN_POINT('Ctrl Pts',(122.58997175941,-4.66659707056658,134.267681318331));
#188961=CARTESIAN_POINT('Ctrl Pts',(122.311524135597,0.391380087281262,
136.602510333005));
#188962=CARTESIAN_POINT('Ctrl Pts',(122.033076511785,5.08969806489794,133.609123014551));
#188963=CARTESIAN_POINT('Ctrl Pts',(121.754628887972,5.11083216644683,128.038296073528));
#188964=CARTESIAN_POINT('Ctrl Pts',(121.476181264159,0.435361185062875,
125.00934731871));
#188965=CARTESIAN_POINT('Ctrl Pts',(121.197733640346,-4.64018545681751,
127.305732683402));
#188966=CARTESIAN_POINT('Ctrl Pts',(120.919286016533,-5.45162834954452,
132.817186202114));
#188967=CARTESIAN_POINT('Ctrl Pts',(120.64083839272,-1.25329111589093,136.478951340622));
#188968=CARTESIAN_POINT('Ctrl Pts',(120.362390768907,4.09675942659154,134.92604482381));
#188969=CARTESIAN_POINT('Ctrl Pts',(120.083943145094,5.68208819386074,129.585511876926));
#188970=CARTESIAN_POINT('Ctrl Pts',(119.805495521281,2.04585549641223,125.36504137862));
#188971=CARTESIAN_POINT('Ctrl Pts',(119.527047897469,-3.47041845664194,
126.143039535386));
#188972=CARTESIAN_POINT('Ctrl Pts',(119.248600273655,-5.79754738740892,
131.204564048482));
#188973=CARTESIAN_POINT('Ctrl Pts',(118.970152649843,-2.7970134950826,135.898321159589));
#188974=CARTESIAN_POINT('Ctrl Pts',(118.69170502603,2.77383915751901,135.910977386384));
#188975=CARTESIAN_POINT('Ctrl Pts',(118.413257402217,5.795669133937,131.230902274733));
#188976=CARTESIAN_POINT('Ctrl Pts',(118.134809778404,3.49156231044436,126.158856217863));
#188977=CARTESIAN_POINT('Ctrl Pts',(117.856362154591,-2.02111970404504,
125.355801758813));
#188978=CARTESIAN_POINT('Ctrl Pts',(117.577914530778,-5.67649144770371,
129.559706714059));
#188979=CARTESIAN_POINT('Ctrl Pts',(117.299466906965,-4.11544486294674,
134.907387801903));
#188980=CARTESIAN_POINT('Ctrl Pts',(117.021019283153,1.22749450019975,136.484587351363));
#188981=CARTESIAN_POINT('Ctrl Pts',(116.74257165934,5.44242638410263,132.841936026965));
#188982=CARTESIAN_POINT('Ctrl Pts',(116.464124035527,4.65603429832517,127.326852442422));
#188983=CARTESIAN_POINT('Ctrl Pts',(116.185676411714,-0.409025847692317,
125.007428985116));
#188984=CARTESIAN_POINT('Ctrl Pts',(115.907228787901,-5.09821122170419,
128.015102502178));
#188985=CARTESIAN_POINT('Ctrl Pts',(115.628781164088,-5.10238954443416,
133.585967964446));
#188986=CARTESIAN_POINT('Ctrl Pts',(115.350333540275,-0.417721141415912,
136.600672164005));
#188987=CARTESIAN_POINT('Ctrl Pts',(115.071885916462,4.65081258375125,134.288849217947));
#188988=CARTESIAN_POINT('Ctrl Pts',(114.793438292649,5.44547674927697,128.77495147487));
#188989=CARTESIAN_POINT('Ctrl Pts',(114.514990668836,1.23601380854556,125.125981591782));
#188990=CARTESIAN_POINT('Ctrl Pts',(114.236543045024,-4.10928543960769,
126.695164629152));
#188991=CARTESIAN_POINT('Ctrl Pts',(113.958095421211,-5.67835211851559,
132.040498034489));
#188992=CARTESIAN_POINT('Ctrl Pts',(113.679647797398,-2.02929060343055,
136.249881542344));
#188993=CARTESIAN_POINT('Ctrl Pts',(113.401200173585,3.48458983985001,135.455097348814));
#188994=CARTESIAN_POINT('Ctrl Pts',(113.122752549772,5.79630245198571,130.386513300387));
#188995=CARTESIAN_POINT('Ctrl Pts',(112.844304925959,2.78149627586357,125.701910523471));
#188996=CARTESIAN_POINT('Ctrl Pts',(112.565857302146,-2.78936909412988,
125.706210114483));
#188997=CARTESIAN_POINT('Ctrl Pts',(112.287409678333,-5.7969405348739,130.395460959329));
#188998=CARTESIAN_POINT('Ctrl Pts',(112.008962054521,-3.47740682035766,
135.460470614237));
#188999=CARTESIAN_POINT('Ctrl Pts',(111.730514430707,2.03769388129978,136.246742645822));
#189000=CARTESIAN_POINT('Ctrl Pts',(111.452066806895,5.68025345292297,132.031731468582));
#189001=CARTESIAN_POINT('Ctrl Pts',(111.173619183082,4.10293759711819,126.688826439658));
#189002=CARTESIAN_POINT('Ctrl Pts',(110.895171559269,-1.24477747079359,
125.127896265209));
#189003=CARTESIAN_POINT('Ctrl Pts',(110.616723935456,-5.44860285380605,
128.783359519875));
#189004=CARTESIAN_POINT('Ctrl Pts',(110.338276311643,-4.64542839321807,
134.296024051927));
#189005=CARTESIAN_POINT('Ctrl Pts',(110.05982868783,0.426667818943798,136.600020465042));
#189006=CARTESIAN_POINT('Ctrl Pts',(109.781381064017,5.10667714937814,133.57808861205));
#189007=CARTESIAN_POINT('Ctrl Pts',(109.502933440204,5.0938996545818,128.007236236273));
#189008=CARTESIAN_POINT('Ctrl Pts',(109.224485816392,0.400077228057368,
125.006804519781));
#189009=CARTESIAN_POINT('Ctrl Pts',(108.946038192578,-4.66139662619255,
127.334043630792));
#189010=CARTESIAN_POINT('Ctrl Pts',(108.667590568766,-5.43927470285667,
132.850334518237));
#189011=CARTESIAN_POINT('Ctrl Pts',(108.389142944953,-1.21872505093712,
136.486475342347));
#189012=CARTESIAN_POINT('Ctrl Pts',(108.11069532114,4.1217733847649,134.901030321119));
#189013=CARTESIAN_POINT('Ctrl Pts',(107.832247697327,5.67456343969215,129.550945975765));
#189014=CARTESIAN_POINT('Ctrl Pts',(107.553800073514,2.01270691137792,125.352688453517));
#189015=CARTESIAN_POINT('Ctrl Pts',(107.275352449701,-3.49872894229381,
126.164251321038));
#189016=CARTESIAN_POINT('Ctrl Pts',(106.996904825888,-5.7950038204084,131.239847950126));
#189017=CARTESIAN_POINT('Ctrl Pts',(106.718457202076,-2.76595328924301,
135.91525299533));
#189018=CARTESIAN_POINT('Ctrl Pts',(106.440009578262,2.80487319040651,135.893997626342));
#189019=CARTESIAN_POINT('Ctrl Pts',(106.16156195445,5.7981582337456,131.195614488879));
#189020=CARTESIAN_POINT('Ctrl Pts',(105.883114330637,3.46321911604922,126.137688157493));
#189021=CARTESIAN_POINT('Ctrl Pts',(105.604666706824,-2.05424918163679,
125.36820583729));
#189022=CARTESIAN_POINT('Ctrl Pts',(105.326219083011,-5.68396283705021,
129.594284189235));
#189023=CARTESIAN_POINT('Ctrl Pts',(105.047771459198,-4.09039232223623,
134.932363663296));
#189024=CARTESIAN_POINT('Ctrl Pts',(104.769323835385,1.26204890993897,136.47701000249));
#189025=CARTESIAN_POINT('Ctrl Pts',(104.490876211572,5.45472884839698,132.808768681268));
#189026=CARTESIAN_POINT('Ctrl Pts',(104.21242858776,4.63477945349693,127.29857427028));
#189027=CARTESIAN_POINT('Ctrl Pts',(103.933980963947,-0.444305837602887,
125.010026245263));
#189028=CARTESIAN_POINT('Ctrl Pts',(103.655533340134,-5.1150957694926,128.046188439421));
#189029=CARTESIAN_POINT('Ctrl Pts',(103.377085716321,-5.08536257553889,
133.616976121092));
#189030=CARTESIAN_POINT('Ctrl Pts',(103.098638092508,-0.38242960843803,
136.603107558928));
#189031=CARTESIAN_POINT('Ctrl Pts',(102.820190468695,4.6719374860923,134.260473842188));
#189032=CARTESIAN_POINT('Ctrl Pts',(102.541742844882,5.4330222677386,128.741840912539));
#189033=CARTESIAN_POINT('Ctrl Pts',(102.263295221069,1.2014250032263,125.118562832119));
#189034=CARTESIAN_POINT('Ctrl Pts',(101.984847597256,-4.13422314637653,
126.720255149861));
#189035=CARTESIAN_POINT('Ctrl Pts',(101.706399973443,-5.67072219248816,
132.07504087278));
#189036=CARTESIAN_POINT('Ctrl Pts',(101.427952349631,-1.99610457388343,
136.262133517338));
#189037=CARTESIAN_POINT('Ctrl Pts',(101.149504725818,3.51283563299066,135.433799494034));
#189038=CARTESIAN_POINT('Ctrl Pts',(100.871057102005,5.7936515047074,130.351237303918));
#189039=CARTESIAN_POINT('Ctrl Pts',(100.592609478192,2.75038467920892,125.685073302739));
#189040=CARTESIAN_POINT('Ctrl Pts',(100.314161854379,-2.82035130272114,
125.723284252797));
#189041=CARTESIAN_POINT('Ctrl Pts',(100.035714230566,-5.79932221927147,
130.430756157697));
#189042=CARTESIAN_POINT('Ctrl Pts',(99.7572666067534,-3.44899932895201,
135.481552309624));
#189043=CARTESIAN_POINT('Ctrl Pts',(99.4788189829407,2.07078545168999,136.234237790066));
#189044=CARTESIAN_POINT('Ctrl Pts',(99.2003713591278,5.6876195657222,131.997131413226));
#189045=CARTESIAN_POINT('Ctrl Pts',(98.9219237353147,4.07780915451857,126.663926945268));
#189046=CARTESIAN_POINT('Ctrl Pts',(98.6434761115021,-1.27930865763567,
125.13557875072));
#189047=CARTESIAN_POINT('Ctrl Pts',(98.3650284876889,-5.460804311125,128.816564156414));
#189048=CARTESIAN_POINT('Ctrl Pts',(98.0865808638763,-4.62408757781209,
134.324237400649));
#189049=CARTESIAN_POINT('Ctrl Pts',(97.8081332400632,0.461939740273397,
136.597315836771));
#189050=CARTESIAN_POINT('Ctrl Pts',(97.5296856162504,5.12346700405862,133.546951428038));
#189051=CARTESIAN_POINT('Ctrl Pts',(97.2512379924375,5.07677838639178,127.97628004749));
#189052=CARTESIAN_POINT('Ctrl Pts',(96.9727903686245,0.364778446043045,
125.004476551425));
#189053=CARTESIAN_POINT('Ctrl Pts',(96.6943427448119,-4.68243506580139,
127.362483172053));
#189054=CARTESIAN_POINT('Ctrl Pts',(96.4158951209985,-5.42671950184442,
132.883407020047));
#189055=CARTESIAN_POINT('Ctrl Pts',(96.1374474971861,-1.18411382567837,
136.493788791223));
#189056=CARTESIAN_POINT('Ctrl Pts',(95.8589998733729,4.14663460910971,134.875864014826));
#189057=CARTESIAN_POINT('Ctrl Pts',(95.5805522495601,5.66682841248846,129.516426520346));
#189058=CARTESIAN_POINT('Ctrl Pts',(95.3021046257473,1.97948374474885,125.340537542131));
#189059=CARTESIAN_POINT('Ctrl Pts',(95.0236570019342,-3.52690978125809,
126.185635047646));
#189060=CARTESIAN_POINT('Ctrl Pts',(94.7452093781216,-5.79224551741027,
131.275115714627));
#189061=CARTESIAN_POINT('Ctrl Pts',(94.4667617543085,-2.73479058998699,
135.931995445075));
#189062=CARTESIAN_POINT('Ctrl Pts',(94.1883141304955,2.8358032876865,135.876829267928));
#189063=CARTESIAN_POINT('Ctrl Pts',(93.909866506683,5.80043248066857,131.160312204968));
#189064=CARTESIAN_POINT('Ctrl Pts',(93.6314188828698,3.43474759079615,126.116693022386));
#189065=CARTESIAN_POINT('Ctrl Pts',(93.352971259057,-2.08730253826965,125.380811354481));
#189066=CARTESIAN_POINT('Ctrl Pts',(93.0745236352441,-5.69122360506351,
129.628906504239));
#189067=CARTESIAN_POINT('Ctrl Pts',(92.7960760114314,-4.06518821053398,
134.957186560018));
#189068=CARTESIAN_POINT('Ctrl Pts',(92.5176283876181,1.29655655399172,136.469222451509));
#189069=CARTESIAN_POINT('Ctrl Pts',(92.2391807638055,5.46682918570788,132.775527061492));
#189070=CARTESIAN_POINT('Ctrl Pts',(91.9607331399925,4.61335286521161,127.270426006341));
#189071=CARTESIAN_POINT('Ctrl Pts',(91.6822855161797,-0.479569363597252,
125.012838216602));
#189072=CARTESIAN_POINT('Ctrl Pts',(91.4038378923669,-5.13179077552621,
128.077376581749));
#189073=CARTESIAN_POINT('Ctrl Pts',(91.1253902685539,-5.06814716666323,
133.647880055237));
#189074=CARTESIAN_POINT('Ctrl Pts',(90.846942644741,-0.347123904390365,
136.605328079151));
#189075=CARTESIAN_POINT('Ctrl Pts',(90.5684950209282,4.69288926807169,134.231970398883));
#189076=CARTESIAN_POINT('Ctrl Pts',(90.2900473971151,5.42036646356212,128.708806777632));
#189077=CARTESIAN_POINT('Ctrl Pts',(90.0115997733025,1.16679167866171,125.111354761782));
#189078=CARTESIAN_POINT('Ctrl Pts',(89.7331521494893,-4.15900765798632,
126.7454970086));
#189079=CARTESIAN_POINT('Ctrl Pts',(89.4547045256766,-5.66288213576447,
132.109536625546));
#189080=CARTESIAN_POINT('Ctrl Pts',(89.1762569018636,-1.96284457794726,
136.274183252551));
#189081=CARTESIAN_POINT('Ctrl Pts',(88.8978092780507,3.5409512567151,135.412330093694));
#189082=CARTESIAN_POINT('Ctrl Pts',(88.619361654238,5.79078587154194,130.3159780981));
#189083=CARTESIAN_POINT('Ctrl Pts',(88.3409140304249,2.71917116603865,125.668425779081));
#189084=CARTESIAN_POINT('Ctrl Pts',(88.0624664066122,-2.85122900215762,
125.740546672265));
#189085=CARTESIAN_POINT('Ctrl Pts',(87.7840187827991,-5.80148900765152,
130.466065200115));
#189086=CARTESIAN_POINT('Ctrl Pts',(87.5055711589863,-3.42046403360785,
135.502460689953));
#189087=CARTESIAN_POINT('Ctrl Pts',(87.2271235351733,2.10380028836375,136.221531728214));
#189088=CARTESIAN_POINT('Ctrl Pts',(86.9486759113605,5.69477492168681,131.962487159311));
#189089=CARTESIAN_POINT('Ctrl Pts',(86.6702282875477,4.05252960720113,126.63918087617));
#189090=CARTESIAN_POINT('Ctrl Pts',(86.3917806637346,-1.31379243922498,
125.14347129503));
#189091=CARTESIAN_POINT('Ctrl Pts',(86.113333039922,-5.47280341633199,128.849842451481));
#189092=CARTESIAN_POINT('Ctrl Pts',(85.8348854161089,-4.6025754151404,134.352320319043));
#189093=CARTESIAN_POINT('Ctrl Pts',(85.5564377922961,0.497194544256039,
136.594396548415));
#189094=CARTESIAN_POINT('Ctrl Pts',(85.2779901684829,5.1400670067851,133.515712616316));
#189095=CARTESIAN_POINT('Ctrl Pts',(84.9995425446705,5.05946899631168,127.945428654274));
#189096=CARTESIAN_POINT('Ctrl Pts',(84.7210949208572,0.329466147029263,
125.002363499906));
#189097=CARTESIAN_POINT('Ctrl Pts',(84.4426472970446,-4.70329999605691,
127.391050253351));
#189098=CARTESIAN_POINT('Ctrl Pts',(84.1641996732315,-5.41396321174535,
132.916402482027));
#189099=CARTESIAN_POINT('Ctrl Pts',(83.8857520494189,-1.14945872264635,
136.500891416245));
#189100=CARTESIAN_POINT('Ctrl Pts',(83.6073044256056,4.17134217838416,134.850546837477));
#189101=CARTESIAN_POINT('Ctrl Pts',(83.328856801793,5.65888339887398,129.481954789796));
#189102=CARTESIAN_POINT('Ctrl Pts',(83.05040917798,1.94618722762166,125.328589094719));
#189103=CARTESIAN_POINT('Ctrl Pts',(82.7719615541671,-3.5549599292834,126.207189922827));
#189104=CARTESIAN_POINT('Ctrl Pts',(82.4935139303543,-5.78927258062435,
131.310366035126));
#189105=CARTESIAN_POINT('Ctrl Pts',(82.2150663065413,-2.70352655206008,
135.948547888425));
#189106=CARTESIAN_POINT('Ctrl Pts',(81.9366186827285,2.86662830323276,135.859472947324));
#189107=CARTESIAN_POINT('Ctrl Pts',(81.6581710589156,5.80249179043285,131.124996731141));
#189108=CARTESIAN_POINT('Ctrl Pts',(81.3797234351026,3.40614878970799,126.095871590527));
#189109=CARTESIAN_POINT('Ctrl Pts',(81.1012758112897,-2.12027854913937,
125.393617843285));
#189110=CARTESIAN_POINT('Ctrl Pts',(80.822828187477,-5.6982734826932,129.663572376127));
#189111=CARTESIAN_POINT('Ctrl Pts',(80.5443805636639,-4.03983346178761,
134.981855572247));
#189112=CARTESIAN_POINT('Ctrl Pts',(80.2659329398512,1.33101615366455,136.461224986989));
#189113=CARTESIAN_POINT('Ctrl Pts',(79.9874853160382,5.47872694765296,132.742212399419));
#189114=CARTESIAN_POINT('Ctrl Pts',(79.7090376922254,4.59175532743923,127.242408693648));
#189115=CARTESIAN_POINT('Ctrl Pts',(79.4305900684125,-0.514815118972584,
125.015864794932));
#189116=CARTESIAN_POINT('Ctrl Pts',(79.1521424445996,-5.1482956211654,128.108665773475));
#189117=CARTESIAN_POINT('Ctrl Pts',(78.8736948207867,-5.05074395573051,
133.678678621723));
#189118=CARTESIAN_POINT('Ctrl Pts',(78.5952471969738,-0.31180533753877,
136.607333642391));
#189119=CARTESIAN_POINT('Ctrl Pts',(78.3167995731609,4.71366715331346,134.203339944237));
#189120=CARTESIAN_POINT('Ctrl Pts',(78.0383519493481,5.407509805713,128.675850294243));
#189121=CARTESIAN_POINT('Ctrl Pts',(77.7599043255351,1.1321151182024,125.104357647873));
#189122=CARTESIAN_POINT('Ctrl Pts',(77.4814567017223,-4.18363805603787,
126.770889270024));
#189123=CARTESIAN_POINT('Ctrl Pts',(77.2030090779094,-5.65483223886072,
132.143984014535));
#189124=CARTESIAN_POINT('Ctrl Pts',(76.9245614540965,-1.92951184808342,
136.286030301474));
#189125=CARTESIAN_POINT('Ctrl Pts',(76.6461138302835,3.56893566918854,135.390689943351));
#189126=CARTESIAN_POINT('Ctrl Pts',(76.3676662064707,5.78770565867644,130.280736989476));
#189127=CARTESIAN_POINT('Ctrl Pts',(76.0892185826578,2.68785689298084,125.651968569378));
#189128=CARTESIAN_POINT('Ctrl Pts',(75.8107709588449,-2.8820010482549,125.75799673322));
#189129=CARTESIAN_POINT('Ctrl Pts',(75.532323335032,-5.8034408197229,130.501386778194));
#189130=CARTESIAN_POINT('Ctrl Pts',(75.2538757112192,-3.39180199171105,
135.523194980456));
#189131=CARTESIAN_POINT('Ctrl Pts',(74.9754280874062,2.13673716794415,136.208624931095));
#189132=CARTESIAN_POINT('Ctrl Pts',(74.6969804635933,5.70171925567246,131.92779999059));
#189133=CARTESIAN_POINT('Ctrl Pts',(74.4185328397805,4.02709989190878,126.61458914934));
#189134=CARTESIAN_POINT('Ctrl Pts',(74.1400852159675,-1.34822753775231,
125.151573605674));
#189135=CARTESIAN_POINT('Ctrl Pts',(73.8616375921548,-5.48459972479585,
128.883193171938));
#189136=CARTESIAN_POINT('Ctrl Pts',(73.5831899683417,-4.58089270234404,
134.380271766487));
#189137=CARTESIAN_POINT('Ctrl Pts',(73.3047423445289,0.532430924512096,
136.591262708148));
#189138=CARTESIAN_POINT('Ctrl Pts',(73.026294720716,5.15647654243839,133.484373334449));
#189139=CARTESIAN_POINT('Ctrl Pts',(72.7478470969032,5.04197212574731,127.914683199832));
#189140=CARTESIAN_POINT('Ctrl Pts',(72.46939947309,0.294141639526237,125.000465443524));
#189141=CARTESIAN_POINT('Ctrl Pts',(72.1909518492774,-4.72399064380143,
127.419743816117));
#189142=CARTESIAN_POINT('Ctrl Pts',(71.9125042254643,-5.40100630524849,
132.949319681519));
#189143=CARTESIAN_POINT('Ctrl Pts',(71.6340566016516,-1.11476102599866,
136.507782954223));
#189144=CARTESIAN_POINT('Ctrl Pts',(71.3556089778387,4.19589517704018,134.82507972721));
#189145=CARTESIAN_POINT('Ctrl Pts',(71.0771613540258,5.65072869325411,129.447532061481));
#189146=CARTESIAN_POINT('Ctrl Pts',(70.7987137302128,1.91281859381102,125.316843554035));
#189147=CARTESIAN_POINT('Ctrl Pts',(70.5202661064001,-3.58287834696108,
126.22891514786));
#189148=CARTESIAN_POINT('Ctrl Pts',(70.241818482587,-5.78608512021397,131.345597605407));
#189149=CARTESIAN_POINT('Ctrl Pts',(69.9633708587742,-2.67216233396265,
135.964909712024));
#189150=CARTESIAN_POINT('Ctrl Pts',(69.6849232349613,2.89734709481291,135.841929307673));
#189151=CARTESIAN_POINT('Ctrl Pts',(69.4064756111484,5.80433608672999,131.089669376025));
#189152=CARTESIAN_POINT('Ctrl Pts',(69.1280279873355,3.37742377252397,126.07522463346));
#189153=CARTESIAN_POINT('Ctrl Pts',(68.8495803635227,-2.15317599230747,
125.406624829152));
#189154=CARTESIAN_POINT('Ctrl Pts',(68.5711327397097,-5.70511220870344,
129.698280520343));
#189155=CARTESIAN_POINT('Ctrl Pts',(68.2926851158969,-4.01432901552682,
135.006369785865));
#189156=CARTESIAN_POINT('Ctrl Pts',(68.014237492084,1.36542643204398,136.45301790528));
#189157=CARTESIAN_POINT('Ctrl Pts',(67.735789868271,5.49042169335597,132.708825929535));
#189158=CARTESIAN_POINT('Ctrl Pts',(67.4573422444582,4.56998764048497,127.214523370394));
#189159=CARTESIAN_POINT('Ctrl Pts',(67.1788946206453,-0.550041797684044,
125.019105868103));
#189160=CARTESIAN_POINT('Ctrl Pts',(66.9004469968323,-5.164609694817,128.140054855163));
#189161=CARTESIAN_POINT('Ctrl Pts',(66.6219993730196,-5.03315358762317,
133.709370679297));
#189162=CARTESIAN_POINT('Ctrl Pts',(66.3435517492066,-0.2764752166261,136.609124174332));
#189163=CARTESIAN_POINT('Ctrl Pts',(66.0651041253938,4.73427037188528,134.174583539162));
#189164=CARTESIAN_POINT('Ctrl Pts',(65.7866565015808,5.39445277059944,128.642972683589));
#189165=CARTESIAN_POINT('Ctrl Pts',(65.508208877768,1.0973966068015,125.097571749668));
#189166=CARTESIAN_POINT('Ctrl Pts',(65.2297612539551,-4.20811342784249,
126.796430993211));
#189167=CARTESIAN_POINT('Ctrl Pts',(64.9513136301422,-5.64657280006891,
132.178381763287));
#189168=CARTESIAN_POINT('Ctrl Pts',(64.6728660063292,-1.89610761944867,
136.297674225111));
#189169=CARTESIAN_POINT('Ctrl Pts',(64.3944183825164,3.59678783343796,135.368879844889));
#189170=CARTESIAN_POINT('Ctrl Pts',(64.1159707587035,5.78441098024938,130.245515283918));
#189171=CARTESIAN_POINT('Ctrl Pts',(63.8375231348906,2.65644302039782,125.635702283457));
#189172=CARTESIAN_POINT('Ctrl Pts',(63.5590755110777,-2.91266630074331,
125.775633789045));
#189173=CARTESIAN_POINT('Ctrl Pts',(63.2806278872649,-5.80517758316048,
130.53671958308));
#189174=CARTESIAN_POINT('Ctrl Pts',(63.0021802634519,-3.36301426534433,
135.543754412816));
#189175=CARTESIAN_POINT('Ctrl Pts',(62.723732639639,2.16959486994269,136.195517876976));
#189176=CARTESIAN_POINT('Ctrl Pts',(62.4452850158262,5.70845231035428,131.893071192411));
#189177=CARTESIAN_POINT('Ctrl Pts',(62.1668373920132,4.00152095094907,126.590152676031));
#189178=CARTESIAN_POINT('Ctrl Pts',(61.8883897682004,-1.38261267721222,
125.159885382419));
#189179=CARTESIAN_POINT('Ctrl Pts',(61.6099421443874,-5.49619279939966,
128.916615081961));
#189180=CARTESIAN_POINT('Ctrl Pts',(61.3314945205747,-4.55904024288434,
134.408090707227));
#189181=CARTESIAN_POINT('Ctrl Pts',(61.0530468967616,0.567647575344072,
136.587914432096));
#189182=CARTESIAN_POINT('Ctrl Pts',(60.7745992729488,5.17269500295686,133.452934743723));
#189183=CARTESIAN_POINT('Ctrl Pts',(60.496151649136,5.02428842305186,127.884044823451));
#189184=CARTESIAN_POINT('Ctrl Pts',(60.2177040253229,0.258806232497024,
124.998782452612));
#189185=CARTESIAN_POINT('Ctrl Pts',(59.9392564015102,-4.74450624233532,
127.448562797104));
#189186=CARTESIAN_POINT('Ctrl Pts',(59.6608087776971,-5.38784926247686,
132.982157398764));
#189187=CARTESIAN_POINT('Ctrl Pts',(59.3823611538844,-1.08002202147149,
136.514463149789));
#189188=CARTESIAN_POINT('Ctrl Pts',(59.1039135300714,4.22029269525717,134.799463627718));
#189189=CARTESIAN_POINT('Ctrl Pts',(58.8254659062585,5.64236459780459,129.413159610949));
#189190=CARTESIAN_POINT('Ctrl Pts',(58.5470182824457,1.8793790798041,125.305301355313));
#189191=CARTESIAN_POINT('Ctrl Pts',(58.2685706586328,-3.61066399976409,
126.250809917708));
#189192=CARTESIAN_POINT('Ctrl Pts',(57.9901230348199,-5.78268325429153,
131.380809119953));
#189193=CARTESIAN_POINT('Ctrl Pts',(57.711675411007,-2.64069909790739,135.981080309579));
#189194=CARTESIAN_POINT('Ctrl Pts',(57.4332277871941,2.92795852413098,135.824198999061));
#189195=CARTESIAN_POINT('Ctrl Pts',(57.1547801633813,5.80596530121877,131.054331448687));
#189196=CARTESIAN_POINT('Ctrl Pts',(56.8763325395683,3.34857360366007,126.054752916266));
#189197=CARTESIAN_POINT('Ctrl Pts',(56.5978849157555,-2.18599364874745,
125.419831830104));
#189198=CARTESIAN_POINT('Ctrl Pts',(56.3194372919424,-5.71173952968275,
129.733029650764));
#189199=CARTESIAN_POINT('Ctrl Pts',(56.0409896681298,-3.98867581682796,
135.030728292487));
#189200=CARTESIAN_POINT('Ctrl Pts',(55.7625420443167,1.39978611404518,136.444601510497));
#189201=CARTESIAN_POINT('Ctrl Pts',(55.4840944205039,5.50191298946419,132.675368888989));
#189202=CARTESIAN_POINT('Ctrl Pts',(55.2056467966909,4.54805061095778,127.186771069878));
#189203=CARTESIAN_POINT('Ctrl Pts',(54.9271991728781,-0.585248094394635,
125.022561316018));
#189204=CARTESIAN_POINT('Ctrl Pts',(54.6487515490652,-5.18073239195715,
128.171542663682));
#189205=CARTESIAN_POINT('Ctrl Pts',(54.3703039252523,-5.01537671415865,
133.739955090657));
#189206=CARTESIAN_POINT('Ctrl Pts',(54.0918563014394,-0.241134850822232,
136.610699608625));
#189207=CARTESIAN_POINT('Ctrl Pts',(53.8134086776265,4.75469816032759,134.145702249237));
#189208=CARTESIAN_POINT('Ctrl Pts',(53.5349610538137,5.38119584205463,128.610175163959));
#189209=CARTESIAN_POINT('Ctrl Pts',(53.2565134300007,1.06263743096531,125.090997318624));
#189210=CARTESIAN_POINT('Ctrl Pts',(52.9780658061879,-4.23243286645675,
126.822121231705));
#189211=CARTESIAN_POINT('Ctrl Pts',(52.6996181823749,-5.63810412544538,
132.21272859718));
#189212=CARTESIAN_POINT('Ctrl Pts',(52.4211705585621,-1.86263312984859,
136.309114591992));
#189213=CARTESIAN_POINT('Ctrl Pts',(52.1427229347491,3.62450671739182,135.346900606486));
#189214=CARTESIAN_POINT('Ctrl Pts',(51.8642753109363,5.7809019583462,130.210314286579));
#189215=CARTESIAN_POINT('Ctrl Pts',(51.5858276871234,2.62493071234137,125.619627524071));
#189216=CARTESIAN_POINT('Ctrl Pts',(51.3073800633105,-2.94322362331098,
125.793457186192));
#189217=CARTESIAN_POINT('Ctrl Pts',(51.0289324394976,-5.80669923360788,
130.572062305503));
#189218=CARTESIAN_POINT('Ctrl Pts',(50.7504848156848,-3.33410192124705,
135.564138225197));
#189219=CARTESIAN_POINT('Ctrl Pts',(50.4720371918718,2.20237217680579,136.182211051539));
#189220=CARTESIAN_POINT('Ctrl Pts',(50.193589568059,5.71497383623647,131.858302051661));
#189221=CARTESIAN_POINT('Ctrl Pts',(49.915141944246,3.97579373215887,126.565872361749));
#189222=CARTESIAN_POINT('Ctrl Pts',(49.6366943204332,-1.41694658345112,
125.168406317271));
#189223=CARTESIAN_POINT('Ctrl Pts',(49.3582466966203,-5.50758221055828,
128.950106943089));
#189224=CARTESIAN_POINT('Ctrl Pts',(49.0797990728074,-4.53701884651156,
134.435776110423));
#189225=CARTESIAN_POINT('Ctrl Pts',(48.8013514489945,0.602843191786665,
136.584351844331));
#189226=CARTESIAN_POINT('Ctrl Pts',(48.5229038251815,5.18872178735999,133.421398009111));
#189227=CARTESIAN_POINT('Ctrl Pts',(48.2444562013688,5.006418543501,127.853514660444));
#189228=CARTESIAN_POINT('Ctrl Pts',(47.9660085775558,0.223461235307256,
124.997314589534));
#189229=CARTESIAN_POINT('Ctrl Pts',(47.6875609537429,-4.7648460314457,127.477506128414));
#189230=CARTESIAN_POINT('Ctrl Pts',(47.40911332993,-5.37449257096935,133.014914416948));
#189231=CARTESIAN_POINT('Ctrl Pts',(47.1306657061172,-1.04524299633083,
136.520931755405));
#189232=CARTESIAN_POINT('Ctrl Pts',(46.8522180823042,4.24453382897653,134.773699488214));
#189233=CARTESIAN_POINT('Ctrl Pts',(46.5737704584914,5.6337914224598,129.378838711881));
#189234=CARTESIAN_POINT('Ctrl Pts',(46.2953228346785,1.84586992471411,125.293962926255));
#189235=CARTESIAN_POINT('Ctrl Pts',(46.0168752108656,-3.63831585808481,
126.272873421051));
#189236=CARTESIAN_POINT('Ctrl Pts',(45.7384275870526,-5.77906710891461,
131.415999273987));
#189237=CARTESIAN_POINT('Ctrl Pts',(45.4599799632399,-2.60913800977569,
135.997059081882));
#189238=CARTESIAN_POINT('Ctrl Pts',(45.1815323394269,2.95846145686929,135.806282678493));
#189239=CARTESIAN_POINT('Ctrl Pts',(44.903084715614,5.80737937352832,131.018984258588));
#189240=CARTESIAN_POINT('Ctrl Pts',(44.6246370918012,3.31959935216964,126.034457197533));
#189241=CARTESIAN_POINT('Ctrl Pts',(44.3461894679882,-2.21873030238901,
125.43323835675));
#189242=CARTESIAN_POINT('Ctrl Pts',(44.0677418441753,-5.7181552000533,129.767818479747));
#189243=CARTESIAN_POINT('Ctrl Pts',(43.7892942203624,-3.96287481627985,
135.054930189501));
#189244=CARTESIAN_POINT('Ctrl Pts',(43.5108465965496,1.43409392645716,136.435976114513));
#189245=CARTESIAN_POINT('Ctrl Pts',(43.2323989727367,5.51320041016325,132.641842517543));
#189246=CARTESIAN_POINT('Ctrl Pts',(42.9539513489238,4.52594505174265,127.159152820475));
#189247=CARTESIAN_POINT('Ctrl Pts',(42.6755037251109,-0.620432704521861,
125.026231010632));
#189248=CARTESIAN_POINT('Ctrl Pts',(42.397056101298,-5.19666311515333,128.203128032237));
#189249=CARTESIAN_POINT('Ctrl Pts',(42.1186084774851,-4.99741399406557,
133.770430722483));
#189250=CARTESIAN_POINT('Ctrl Pts',(41.8401608536722,-0.205785549677785,
136.612059886891));
#189251=CARTESIAN_POINT('Ctrl Pts',(41.5617132298594,4.77494976168102,134.11669714467));
#189252=CARTESIAN_POINT('Ctrl Pts',(41.2832656060464,5.36773951131901,128.577458950676));
#189253=CARTESIAN_POINT('Ctrl Pts',(41.0048179822336,1.02783887870806,125.084634598359));
#189254=CARTESIAN_POINT('Ctrl Pts',(40.7263703584206,-4.25659547071474,
126.847959033542));
#189255=CARTESIAN_POINT('Ctrl Pts',(40.4479227346078,-5.62942652880005,
132.24702324348));
#189256=CARTESIAN_POINT('Ctrl Pts',(40.1694751107948,-1.82908961969292,
136.320350978189));
#189257=CARTESIAN_POINT('Ctrl Pts',(39.891027486982,3.65209129391637,135.324753042595));
#189258=CARTESIAN_POINT('Ctrl Pts',(39.6125798631691,5.77717872299504,130.175135301845));
#189259=CARTESIAN_POINT('Ctrl Pts',(39.3341322393562,2.59332113651206,125.603744886877));
#189260=CARTESIAN_POINT('Ctrl Pts',(39.0556846155433,-2.97367188364494,
125.811466264208));
#189261=CARTESIAN_POINT('Ctrl Pts',(38.7772369917304,-5.80800571467979,
130.607413635826));
#189262=CARTESIAN_POINT('Ctrl Pts',(38.4987893679175,-3.30506603077697,
135.584345662267));
#189263=CARTESIAN_POINT('Ctrl Pts',(38.2203417441046,2.23506787395795,136.16870494788));
#189264=CARTESIAN_POINT('Ctrl Pts',(37.9418941202917,5.72128359166147,131.823493856722));
#189265=CARTESIAN_POINT('Ctrl Pts',(37.6634464964789,3.94991918886983,126.541749106207));
#189266=CARTESIAN_POINT('Ctrl Pts',(37.3849988726659,-1.45122798421329,
125.177136094481));
#189267=CARTESIAN_POINT('Ctrl Pts',(37.1065512488531,-5.51876753623267,
128.983667514269));
#189268=CARTESIAN_POINT('Ctrl Pts',(36.8281036250402,-4.51482932923697,
134.463326950183));
#189269=CARTESIAN_POINT('Ctrl Pts',(36.5496560012273,0.6380164696531,136.580575076865));
#189270=CARTESIAN_POINT('Ctrl Pts',(36.2712083774144,5.20455630176915,133.389764299214));
#189271=CARTESIAN_POINT('Ctrl Pts',(35.9927607536015,4.9883631492699,127.82309384212));
#189272=CARTESIAN_POINT('Ctrl Pts',(35.7143131297886,0.188107957679239,
124.996061908681));
#189273=CARTESIAN_POINT('Ctrl Pts',(35.4358655059757,-4.78500925743413,
127.50657273754));
#189274=CARTESIAN_POINT('Ctrl Pts',(35.1574178821628,-5.36093672566315,
133.047589522248));
#189275=CARTESIAN_POINT('Ctrl Pts',(34.87897025835,-1.01042523932657,136.527188531377));
#189276=CARTESIAN_POINT('Ctrl Pts',(34.6005226345371,4.26861767993396,134.747788263399));
#189277=CARTESIAN_POINT('Ctrl Pts',(34.3220750107242,5.62500948490202,129.34457063605));
#189278=CARTESIAN_POINT('Ctrl Pts',(34.0436273869112,1.81229237023524,125.282828687009));
#189279=CARTESIAN_POINT('Ctrl Pts',(33.7651797630984,-3.66583289727342,
126.295104840318));
#189280=CARTESIAN_POINT('Ctrl Pts',(33.4867321392855,-5.77523681808073,
131.451166763527));
#189281=CARTESIAN_POINT('Ctrl Pts',(33.2082845154725,-2.57748023907555,
136.012845436834));
#189282=CARTESIAN_POINT('Ctrl Pts',(32.9298368916598,2.98885476273036,135.788181009863));
#189283=CARTESIAN_POINT('Ctrl Pts',(32.6513892678468,5.80857825125962,130.983629115531));
#189284=CARTESIAN_POINT('Ctrl Pts',(32.3729416440339,3.29050209170421,126.014338229324));
#189285=CARTESIAN_POINT('Ctrl Pts',(32.094494020221,-2.25138474016344,125.446843912307));
#189286=CARTESIAN_POINT('Ctrl Pts',(31.8160463964081,-5.72435898208005,
129.802645718181));
#189287=CARTESIAN_POINT('Ctrl Pts',(31.5375987725953,-3.93692696994811,
135.078974580096));
#189288=CARTESIAN_POINT('Ctrl Pts',(31.2591511487823,1.46834859799131,136.427142036947));
#189289=CARTESIAN_POINT('Ctrl Pts',(30.9807035249695,5.52428353719365,132.608248057529));
#189290=CARTESIAN_POINT('Ctrl Pts',(30.7022559011566,4.50367178196922,127.131669645585));
#189291=CARTESIAN_POINT('Ctrl Pts',(30.4238082773436,-0.655594324287056,
125.030114815962));
#189292=CARTESIAN_POINT('Ctrl Pts',(30.1453606535308,-5.21240127408669,
128.234809790423));
#189293=CARTESIAN_POINT('Ctrl Pts',(29.8669130297179,-4.97926609295916,
133.80079644549));
#189294=CARTESIAN_POINT('Ctrl Pts',(29.588465405905,-0.170428623074124,
136.613204958723));
#189295=CARTESIAN_POINT('Ctrl Pts',(29.3100177820921,4.79502442551506,134.087569300254));
#189296=CARTESIAN_POINT('Ctrl Pts',(29.0315701582792,5.35408427702179,128.544825256054));
#189297=CARTESIAN_POINT('Ctrl Pts',(28.7531225344664,0.99300223950345,125.078483824645));
#189298=CARTESIAN_POINT('Ctrl Pts',(28.4746749106534,-4.28060034526213,
126.873943441297));
#189299=CARTESIAN_POINT('Ctrl Pts',(28.1962272868406,-5.6205403316845,132.281264431386));
#189300=CARTESIAN_POINT('Ctrl Pts',(27.9177796630277,-1.79547833194873,
136.331382967337));
#189301=CARTESIAN_POINT('Ctrl Pts',(27.6393320392148,3.67954054085496,135.3024379739));
#189302=CARTESIAN_POINT('Ctrl Pts',(27.3608844154018,5.77324141216173,130.139979633288));
#189303=CARTESIAN_POINT('Ctrl Pts',(27.082436791589,2.56161546421434,125.58805496041));
#189304=CARTESIAN_POINT('Ctrl Pts',(26.8039891677761,-3.00400995347367,
125.82966035576));
#189305=CARTESIAN_POINT('Ctrl Pts',(26.5255415439632,-5.80909697796402,
130.642772264091));
#189306=CARTESIAN_POINT('Ctrl Pts',(26.2470939201503,-3.27590766986969,
135.604375975235));
#189307=CARTESIAN_POINT('Ctrl Pts',(25.9686462963375,2.2676807498481,136.155000066467));
#189308=CARTESIAN_POINT('Ctrl Pts',(25.6901986725246,5.727381342819,131.788647897428));
#189309=CARTESIAN_POINT('Ctrl Pts',(25.4117510487116,3.92389827987267,126.517783803302));
#189310=CARTESIAN_POINT('Ctrl Pts',(25.1333034248988,-1.48545560918882,
125.186074390566));
#189311=CARTESIAN_POINT('Ctrl Pts',(24.8548558010858,-5.5297483619465,129.017295551901));
#189312=CARTESIAN_POINT('Ctrl Pts',(24.576408177273,-4.49247251330123,134.490742205601));
#189313=CARTESIAN_POINT('Ctrl Pts',(24.2979605534601,0.673166105584617,
136.576584269648));
#189314=CARTESIAN_POINT('Ctrl Pts',(24.0195129296472,5.22019795943058,133.358034786234));
#189315=CARTESIAN_POINT('Ctrl Pts',(23.7410653058343,4.97012290940784,127.792783495733));
#189316=CARTESIAN_POINT('Ctrl Pts',(23.4626176820214,0.152747709641667,
124.995024456474));
#189317=CARTESIAN_POINT('Ctrl Pts',(23.1841700582085,-4.80499517314482,
127.53576154741));
#189318=CARTESIAN_POINT('Ctrl Pts',(22.9057224343956,-5.34718222887511,
133.080181503877));
#189319=CARTESIAN_POINT('Ctrl Pts',(22.6272748105827,-0.975570040643468,
136.533233245855));
#189320=CARTESIAN_POINT('Ctrl Pts',(22.3488271867698,4.29254335569345,134.721730913422));
#189321=CARTESIAN_POINT('Ctrl Pts',(22.070379562957,5.61601911054919,129.310356653276));
#189322=CARTESIAN_POINT('Ctrl Pts',(21.791931939144,1.77864766059611,125.27189905016));
#189323=CARTESIAN_POINT('Ctrl Pts',(21.5134843153312,-3.69321409767591,
126.317503351717));
#189324=CARTESIAN_POINT('Ctrl Pts',(21.2350366915183,-5.77119252372273,
131.486310285425));
#189325=CARTESIAN_POINT('Ctrl Pts',(20.9565890677054,-2.54572695889727,
136.028438789465));
#189326=CARTESIAN_POINT('Ctrl Pts',(20.6781414438925,3.01913731547902,135.769894663934));
#189327=CARTESIAN_POINT('Ctrl Pts',(20.3996938200796,5.80956188998761,130.948267329615));
#189328=CARTESIAN_POINT('Ctrl Pts',(20.1212461962667,3.26128290047392,125.994396757156));
#189329=CARTESIAN_POINT('Ctrl Pts',(19.8427985724538,-2.28395575204823,
125.460647992615));
#189330=CARTESIAN_POINT('Ctrl Pts',(19.5643509486409,-5.7303506458796,129.837510075529));
#189331=CARTESIAN_POINT('Ctrl Pts',(19.285903324828,-3.91083323933969,135.102860573299));
#189332=CARTESIAN_POINT('Ctrl Pts',(19.0074557010152,1.50254885932817,136.418099605148));
#189333=CARTESIAN_POINT('Ctrl Pts',(18.7290080772022,5.53516195986603,132.574586753804));
#189334=CARTESIAN_POINT('Ctrl Pts',(18.4505604533894,4.48123162698169,127.104322563612));
#189335=CARTESIAN_POINT('Ctrl Pts',(18.1721128295765,-0.690731650763477,
125.034212588094));
#189336=CARTESIAN_POINT('Ctrl Pts',(17.8936652057636,-5.22794628557398,
128.26658676426));
#189337=CARTESIAN_POINT('Ctrl Pts',(17.6152175819507,-4.96093368331654,
133.831051134467));
#189338=CARTESIAN_POINT('Ctrl Pts',(17.3367699581378,-0.135065381175154,
136.614134781694));
#189339=CARTESIAN_POINT('Ctrl Pts',(17.0583223343249,4.81492140795562,134.058319795333));
#189340=CARTESIAN_POINT('Ctrl Pts',(16.779874710512,5.34023064516271,128.512275289347));
#189341=CARTESIAN_POINT('Ctrl Pts',(16.5014270866992,0.958128804235671,
125.0725452254));
#189342=CARTESIAN_POINT('Ctrl Pts',(16.2229794628862,-4.30444660058956,
126.900073492105));
#189343=CARTESIAN_POINT('Ctrl Pts',(15.9445318390734,-5.61144586338,132.315450892077));
#189344=CARTESIAN_POINT('Ctrl Pts',(15.6660842152604,-1.76180051209467,
136.342210150638));
#189345=CARTESIAN_POINT('Ctrl Pts',(15.3876365914476,3.70685344106567,135.279956227294));
#189346=CARTESIAN_POINT('Ctrl Pts',(15.1091889676347,5.76909017174479,130.104848583611));
#189347=CARTESIAN_POINT('Ctrl Pts',(14.8307413438218,2.52981487031356,125.572558326068));
#189348=CARTESIAN_POINT('Ctrl Pts',(14.5522937200089,-3.03423670860886,
125.848038786661));
#189349=CARTESIAN_POINT('Ctrl Pts',(14.273846096196,-5.80997298302346,130.678136880072));
#189350=CARTESIAN_POINT('Ctrl Pts',(13.9953984723831,-3.24662791899898,
135.624228421867));
#189351=CARTESIAN_POINT('Ctrl Pts',(13.7169508485702,2.30020959599411,136.141096915141));
#189352=CARTESIAN_POINT('Ctrl Pts',(13.4385032247574,5.73326686375462,131.753765465006));
#189353=CARTESIAN_POINT('Ctrl Pts',(13.1600556009444,3.89773196938174,126.493977341077));
#189354=CARTESIAN_POINT('Ctrl Pts',(12.8816079771316,-1.51962819006047,
125.195220874312));
#189355=CARTESIAN_POINT('Ctrl Pts',(12.6031603533186,-5.54052428080121,
129.050989809886));
#189356=CARTESIAN_POINT('Ctrl Pts',(12.3247127295058,-4.46994922714442,
134.518020860792));
#189357=CARTESIAN_POINT('Ctrl Pts',(12.0462651056929,0.708290797098533,
136.572379570561));
#189358=CARTESIAN_POINT('Ctrl Pts',(11.76781748188,5.23564618073708,133.326210645918));
#189359=CARTESIAN_POINT('Ctrl Pts',(11.4893698580671,4.95169849981347,127.762584744442));
#189360=CARTESIAN_POINT('Ctrl Pts',(11.2109222342542,0.117381801481337,
124.994202271355));
#189361=CARTESIAN_POINT('Ctrl Pts',(10.9324746104413,-4.82480303799234,
127.565071476419));
#189362=CARTESIAN_POINT('Ctrl Pts',(10.6540269866284,-5.33322959028317,
133.112689154126));
#189363=CARTESIAN_POINT('Ctrl Pts',(10.3755793628155,-0.940678691853753,
136.539065674851));
#189364=CARTESIAN_POINT('Ctrl Pts',(10.0971317390026,4.31630996968034,134.695528403849));
#189365=CARTESIAN_POINT('Ctrl Pts',(9.81868411518972,5.60682063254294,129.276198031366));
#189366=CARTESIAN_POINT('Ctrl Pts',(9.54023649137686,1.74493704251384,125.261174420708));
#189367=CARTESIAN_POINT('Ctrl Pts',(9.26178886756394,-3.72045844467185,
126.340068125262));
#189368=CARTESIAN_POINT('Ctrl Pts',(8.98334124375105,-5.76693437570339,
131.52142853743));
#189369=CARTESIAN_POINT('Ctrl Pts',(8.70489361993813,-2.51387934587036,
136.043838561958));
#189370=CARTESIAN_POINT('Ctrl Pts',(8.42644599612531,3.0493079929842,135.751424318317));
#189371=CARTESIAN_POINT('Ctrl Pts',(8.14799837231237,5.81033025326331,130.912900211183));
#189372=CARTESIAN_POINT('Ctrl Pts',(7.86955074849947,3.23194286120641,125.974633519968));
#189373=CARTESIAN_POINT('Ctrl Pts',(7.59110312468663,-2.3164421311127,125.47465008616));
#189374=CARTESIAN_POINT('Ctrl Pts',(7.31265550087371,-5.73612996942864,
129.872410259879));
#189375=CARTESIAN_POINT('Ctrl Pts',(7.0342078770608,-3.88459459136738,135.126587284006));
#189376=CARTESIAN_POINT('Ctrl Pts',(6.75576025324794,1.53669344316449,136.408849154185));
#189377=CARTESIAN_POINT('Ctrl Pts',(6.47731262943506,5.54583527507644,132.540859853697));
#189378=CARTESIAN_POINT('Ctrl Pts',(6.19886500562214,4.45862541830825,127.077112587908));
#189379=CARTESIAN_POINT('Ctrl Pts',(5.92041738180924,-0.725843381924555,
125.038524175185));
#189380=CARTESIAN_POINT('Ctrl Pts',(5.64196975799638,-5.24329757358911,
128.29845777624));
#189381=CARTESIAN_POINT('Ctrl Pts',(5.36352213418349,-4.94241744445191,
133.861193668313));
#189382=CARTESIAN_POINT('Ctrl Pts',(5.08507451037056,-0.0996971343788212,
136.614849321347));
#189383=CARTESIAN_POINT('Ctrl Pts',(4.80662688655771,4.83463997171276,134.028949713759));
#189384=CARTESIAN_POINT('Ctrl Pts',(4.5281792627448,5.32617912909322,128.479810256704));
#189385=CARTESIAN_POINT('Ctrl Pts',(4.24973163893191,0.923219865152705,
125.066819020683));
#189386=CARTESIAN_POINT('Ctrl Pts',(3.97128401511898,-4.32813335306523,
126.926348217707));
#189387=CARTESIAN_POINT('Ctrl Pts',(3.69283639130614,-5.60214346088543,
132.349581358763));
#189388=CARTESIAN_POINT('Ctrl Pts',(3.41438876749324,-1.72805740807474,
136.352832126888));
#189389=CARTESIAN_POINT('Ctrl Pts',(3.13594114368033,3.73402898245891,135.257308635848));
#189390=CARTESIAN_POINT('Ctrl Pts',(2.85749351986744,5.76472515556999,130.06974345461));
#189391=CARTESIAN_POINT('Ctrl Pts',(2.5790458960546,2.49792053319242,125.557255558086));
#189392=CARTESIAN_POINT('Ctrl Pts',(2.30059827224166,-3.06435102898697,
125.866600875889));
#189393=CARTESIAN_POINT('Ctrl Pts',(2.02215064842876,-5.81063369739741,
130.713506173321));
#189394=CARTESIAN_POINT('Ctrl Pts',(1.74370302461591,-3.21722786313679,
135.643902266527));
#189395=CARTESIAN_POINT('Ctrl Pts',(1.46525540080302,2.33265320702766,136.12699600909));
#189396=CARTESIAN_POINT('Ctrl Pts',(1.18680777699008,5.73893993637821,131.718847852038));
#189397=CARTESIAN_POINT('Ctrl Pts',(0.908360153177235,3.87142122699929,
126.47033060169));
#189398=CARTESIAN_POINT('Ctrl Pts',(0.629912529364331,-1.55374446055069,
125.204575206795));
#189399=CARTESIAN_POINT('Ctrl Pts',(0.351464905551429,-5.55109489349118,
129.084749039672));
#189400=CARTESIAN_POINT('Ctrl Pts',(0.0730172817385382,-4.44726030537518,
134.545161904937));
#189401=CARTESIAN_POINT('Ctrl Pts',(-0.205430342074321,0.743389242636492,
136.56796113541));
#189402=CARTESIAN_POINT('Ctrl Pts',(-0.48387796588724,5.25090039324876,
133.294293057522));
#189403=CARTESIAN_POINT('Ctrl Pts',(-0.762325589700153,4.93309060321035,
127.732498707276));
#189404=CARTESIAN_POINT('Ctrl Pts',(-1.040773213513,0.0820115436953976,
124.993595383789));
#189405=CARTESIAN_POINT('Ctrl Pts',(-1.3192208373259,-4.84443211798899,
127.594501438479));
#189406=CARTESIAN_POINT('Ctrl Pts',(-1.5976684611388,-5.31907932690746,
133.145111268411));
#189407=CARTESIAN_POINT('Ctrl Pts',(-1.8761160849517,-0.905752485869179,
136.544685602242));
#189408=CARTESIAN_POINT('Ctrl Pts',(-2.15456370876455,4.33991664121397,
134.669181705622));
#189409=CARTESIAN_POINT('Ctrl Pts',(-2.43301133257747,5.59741439173625,
129.242096036083));
#189410=CARTESIAN_POINT('Ctrl Pts',(-2.71145895639038,1.71116176514775,
125.250655196059));
#189411=CARTESIAN_POINT('Ctrl Pts',(-2.98990658020324,-3.74756492871192,
126.362798324807));
#189412=CARTESIAN_POINT('Ctrl Pts',(-3.26835420401613,-5.76246253181,131.556520218218));
#189413=CARTESIAN_POINT('Ctrl Pts',(-3.54680182782904,-2.48193858011979,
136.059044183669));
#189414=CARTESIAN_POINT('Ctrl Pts',(-3.82524945164193,3.0793656772603,135.732770657435));
#189415=CARTESIAN_POINT('Ctrl Pts',(-4.1036970754548,5.81088331261472,130.877529070775));
#189416=CARTESIAN_POINT('Ctrl Pts',(-4.38214469926771,3.20248306110764,
125.955049250094));
#189417=CARTESIAN_POINT('Ctrl Pts',(-4.66059232308062,-2.34884267356213,
125.488849674089));
#189418=CARTESIAN_POINT('Ctrl Pts',(-4.93903994689347,-5.7416967385722,
129.907344977992));
#189419=CARTESIAN_POINT('Ctrl Pts',(-5.21748757070636,-3.85821199831392,
135.150153833014));
#189420=CARTESIAN_POINT('Ctrl Pts',(-5.49593519451928,1.57078108426016,
136.399391026839));
#189421=CARTESIAN_POINT('Ctrl Pts',(-5.77438281833216,5.55630308732125,
132.507068606974));
#189422=CARTESIAN_POINT('Ctrl Pts',(-6.05283044214503,4.43585399363028,
127.050040726751));
#189423=CARTESIAN_POINT('Ctrl Pts',(-6.33127806595794,-0.76092821669219,
125.043049417465));
#189424=CARTESIAN_POINT('Ctrl Pts',(-6.60972568977086,-5.25845456928442,
128.330421645371));
#189425=CARTESIAN_POINT('Ctrl Pts',(-6.88817331358369,-4.92371806249131,
133.891222930087));
#189426=CARTESIAN_POINT('Ctrl Pts',(-7.16662093739661,-0.0643251932685087,
136.615348551203));
#189427=CARTESIAN_POINT('Ctrl Pts',(-7.44506856120951,4.8541793861078,133.999460143849));
#189428=CARTESIAN_POINT('Ctrl Pts',(-7.72351618502242,5.3119302494974,128.44743136113));
#189429=CARTESIAN_POINT('Ctrl Pts',(-8.00196380883526,0.888276715818123,
125.06130542268));
#189430=CARTESIAN_POINT('Ctrl Pts',(-8.28041143264819,-4.35165972496785,
126.952766644486));
#189431=CARTESIAN_POINT('Ctrl Pts',(-8.55885905646108,-5.59263346890473,
132.383654566726));
#189432=CARTESIAN_POINT('Ctrl Pts',(-8.83730668027396,-1.69425027025207,
136.363248502487));
#189433=CARTESIAN_POINT('Ctrl Pts',(-9.11575430408684,3.76106615803527,
135.234496038775));
#189434=CARTESIAN_POINT('Ctrl Pts',(-9.39420192789976,5.7601465253845,130.034665547118));
#189435=CARTESIAN_POINT('Ctrl Pts',(-9.67264955171265,2.4659336347071,125.542147223509));
#189436=CARTESIAN_POINT('Ctrl Pts',(-9.95109717552551,-3.09435179871079,
125.885345935621));
#189437=CARTESIAN_POINT('Ctrl Pts',(-10.2295447993384,-5.81107909660284,
130.748878833214));
#189438=CARTESIAN_POINT('Ctrl Pts',(-10.5079924231513,-3.18770859171301,
135.663396780189));
#189439=CARTESIAN_POINT('Ctrl Pts',(-10.7864400469642,2.36501038073878,
136.112697870828));
#189440=CARTESIAN_POINT('Ctrl Pts',(-11.0648876707771,5.74440035047196,
131.683896352409));
#189441=CARTESIAN_POINT('Ctrl Pts',(-11.34333529459,3.84496702767957,126.446844461378));
#189442=CARTESIAN_POINT('Ctrl Pts',(-11.6217829184029,-1.58780315646856,
125.214137041385));
#189443=CARTESIAN_POINT('Ctrl Pts',(-11.9002305422157,-5.56145980831845,
129.118571990297));
#189444=CARTESIAN_POINT('Ctrl Pts',(-12.1786781660286,-4.42440658873985,
134.572164332316));
#189445=CARTESIAN_POINT('Ctrl Pts',(-12.4571257898416,0.778460141612691,
136.563329127923));
#189446=CARTESIAN_POINT('Ctrl Pts',(-12.7355734136544,5.26596003171537,
133.262283203764));
#189447=CARTESIAN_POINT('Ctrl Pts',(-13.0140210374673,4.91429990912079,
127.702526499083));
#189448=CARTESIAN_POINT('Ctrl Pts',(-13.2924686612802,0.0466382469415425,
124.993203816266));
#189449=CARTESIAN_POINT('Ctrl Pts',(-13.5709162850931,-4.86388168577195,
127.624050343051));
#189450=CARTESIAN_POINT('Ctrl Pts',(-13.849363908906,-5.30473196309121,
133.177446645321));
#189451=CARTESIAN_POINT('Ctrl Pts',(-14.1278115327188,-0.87079271689315,
136.550092819781));
#189452=CARTESIAN_POINT('Ctrl Pts',(-14.4062591565318,4.36336249554048,
134.642691795028));
#189453=CARTESIAN_POINT('Ctrl Pts',(-14.6847067803446,5.58780073668082,
129.20805193109));
#189454=CARTESIAN_POINT('Ctrl Pts',(-14.9631544041576,1.67732308005318,
125.240341766008));
#189455=CARTESIAN_POINT('Ctrl Pts',(-15.2416020279704,-3.77453254535539,
126.385693108075));
#189456=CARTESIAN_POINT('Ctrl Pts',(-15.5200496517834,-5.75777715774833,
131.591584027456));
#189457=CARTESIAN_POINT('Ctrl Pts',(-15.7984972755962,-2.44990584522241,
136.074055091149));
#189458=CARTESIAN_POINT('Ctrl Pts',(-16.0769448994091,3.1093092545088,135.713934372506));
#189459=CARTESIAN_POINT('Ctrl Pts',(-16.355392523222,5.81122104754806,130.842155219084));
#189460=CARTESIAN_POINT('Ctrl Pts',(-16.6338401470349,3.17290459182133,
125.935644673236));
#189461=CARTESIAN_POINT('Ctrl Pts',(-16.9122877708478,-2.38115617878252,
125.50324623023));
#189462=CARTESIAN_POINT('Ctrl Pts',(-17.1907353946607,-5.74705074703162,
129.94231293535));
#189463=CARTESIAN_POINT('Ctrl Pts',(-17.4691830184736,-3.83168643779603,
135.173559347056));
#189464=CARTESIAN_POINT('Ctrl Pts',(-17.7476306422864,1.6048105194851,136.389725573584));
#189465=CARTESIAN_POINT('Ctrl Pts',(-18.0260782660994,5.56656500871184,
132.473214265779));
#189466=CARTESIAN_POINT('Ctrl Pts',(-18.3045258899123,4.4129181967513,127.023107983299));
#189467=CARTESIAN_POINT('Ctrl Pts',(-18.5829735137251,-0.795984854984928,
125.047788147249));
#189468=CARTESIAN_POINT('Ctrl Pts',(-18.861421137538,-5.27341671101187,
128.362477187221));
#189469=CARTESIAN_POINT('Ctrl Pts',(-19.1398687613509,-4.90483623034722,
133.921137807042));
#189470=CARTESIAN_POINT('Ctrl Pts',(-19.4183163851638,-0.0289508685644962,
136.615632452765));
#189471=CARTESIAN_POINT('Ctrl Pts',(-19.6967640089767,4.87353892710056,
133.969852178351));
#189472=CARTESIAN_POINT('Ctrl Pts',(-19.9752116327896,5.29748453437273,
128.415139802436));
#189473=CARTESIAN_POINT('Ctrl Pts',(-20.2536592566025,0.853300651063172,
125.056004635698));
#189474=CARTESIAN_POINT('Ctrl Pts',(-20.5321068804154,-4.37502484451904,
126.979327793496));
#189475=CARTESIAN_POINT('Ctrl Pts',(-20.8105545042282,-5.58291623983416,
132.417669253371));
#189476=CARTESIAN_POINT('Ctrl Pts',(-21.0890021280412,-1.66038035136256,
136.37345889145));
#189477=CARTESIAN_POINT('Ctrl Pts',(-21.367449751854,3.78796396592178,135.211519281404));
#189478=CARTESIAN_POINT('Ctrl Pts',(-21.6458973756669,5.75535445085128,
129.999616160961));
#189479=CARTESIAN_POINT('Ctrl Pts',(-21.9243449994798,2.43385536014432,
125.527233882186));
#189480=CARTESIAN_POINT('Ctrl Pts',(-22.2027926232928,-3.12423790609075,
125.904273271251));
#189481=CARTESIAN_POINT('Ctrl Pts',(-22.4812402471056,-5.81130916413533,
130.784253549004));
#189482=CARTESIAN_POINT('Ctrl Pts',(-22.7596878709185,-3.15807119857507,
135.682711240481));
#189483=CARTESIAN_POINT('Ctrl Pts',(-23.0381354947314,2.39727991812053,
136.098203030175));
#189484=CARTESIAN_POINT('Ctrl Pts',(-23.3165831185443,5.74964790369824,
131.648912261261));
#189485=CARTESIAN_POINT('Ctrl Pts',(-23.5950307423572,3.81837035169266,
126.423519790431));
#189486=CARTESIAN_POINT('Ctrl Pts',(-23.8734783661701,-1.62180301575654,
125.223906023766));
#189487=CARTESIAN_POINT('Ctrl Pts',(-24.151925989983,-5.57161864120731,
129.15245740844));
#189488=CARTESIAN_POINT('Ctrl Pts',(-24.4303736137958,-4.4013889240913,
134.599027142342));
#189489=CARTESIAN_POINT('Ctrl Pts',(-24.7088212376087,0.813502194462058,
136.558483719739));
#189490=CARTESIAN_POINT('Ctrl Pts',(-24.9872688614217,5.28082453809644,
133.230182270781));
#189491=CARTESIAN_POINT('Ctrl Pts',(-25.2657164852345,4.89532711384086,
127.672669230493));
#189492=CARTESIAN_POINT('Ctrl Pts',(-25.5441641090475,0.0112632219902977,
124.993027583295));
#189493=CARTESIAN_POINT('Ctrl Pts',(-25.8226117328602,-4.88315102063038,
127.65371709519));
#189494=CARTESIAN_POINT('Ctrl Pts',(-26.1010593566733,-5.29018803048126,
133.209694086655));
#189495=CARTESIAN_POINT('Ctrl Pts',(-26.3795069804861,-0.835800680372761,
136.555287127099));
#189496=CARTESIAN_POINT('Ctrl Pts',(-26.6579546042989,4.38664666386508,
134.616059653661));
#189497=CARTESIAN_POINT('Ctrl Pts',(-26.9364022281119,5.57798002361419,
129.174066977901));
#189498=CARTESIAN_POINT('Ctrl Pts',(-27.2148498519247,1.64342224113504,
125.23023451272));
#189499=CARTESIAN_POINT('Ctrl Pts',(-27.4932974757377,-3.80136029530733,
126.408751626694));
#189500=CARTESIAN_POINT('Ctrl Pts',(-27.7717450995505,-5.75287842713667,
131.626618665841));
#189501=CARTESIAN_POINT('Ctrl Pts',(-28.0501927233634,-2.41778232816299,
136.088870728161));
#189502=CARTESIAN_POINT('Ctrl Pts',(-28.3286403471763,3.13913761515943,
135.694916161515));
#189503=CARTESIAN_POINT('Ctrl Pts',(-28.6070879709892,5.8113434455484,130.8067799669));
#189504=CARTESIAN_POINT('Ctrl Pts',(-28.8855355948021,3.14320854938853,
125.916420508438));
#189505=CARTESIAN_POINT('Ctrl Pts',(-29.163983218615,-2.41338144938502,
125.517839221114));
#189506=CARTESIAN_POINT('Ctrl Pts',(-29.4424308424279,-5.75219179641212,
129.977312836202));
#189507=CARTESIAN_POINT('Ctrl Pts',(-29.7208784662408,-3.80501889272807,
135.196802958832));
#189508=CARTESIAN_POINT('Ctrl Pts',(-29.9993260900537,1.6387804878663,136.379853152576));
#189509=CARTESIAN_POINT('Ctrl Pts',(-30.2777737138665,5.576620658989,132.439298084597));
#189510=CARTESIAN_POINT('Ctrl Pts',(-30.5562213376795,4.38981887756547,
126.996315355552));
#189511=CARTESIAN_POINT('Ctrl Pts',(-30.8346689614924,-0.831011997766135,
125.052740188944));
#189512=CARTESIAN_POINT('Ctrl Pts',(-31.1131165853052,-5.2881834443438,
128.394623213959));
#189513=CARTESIAN_POINT('Ctrl Pts',(-31.3915642091181,-4.88577264769286,
133.950937190672));
#189514=CARTESIAN_POINT('Ctrl Pts',(-31.670011832931,0.00642452892459172,
136.615701015511));
#189515=CARTESIAN_POINT('Ctrl Pts',(-31.9484594567439,4.89271787731614,
133.940126914399));
#189516=CARTESIAN_POINT('Ctrl Pts',(-32.2269070805568,5.28284251901049,
128.382936777197));
#189517=CARTESIAN_POINT('Ctrl Pts',(-32.5053547043697,0.818292966938792,
125.050916856162));
#189518=CARTESIAN_POINT('Ctrl Pts',(-32.7838023281826,-4.3982278459157,
127.006030680504));
#189519=CARTESIAN_POINT('Ctrl Pts',(-33.0622499519955,-5.57299213374921,
132.451624158271));
#189520=CARTESIAN_POINT('Ctrl Pts',(-33.3406975758084,-1.62644890646854,
136.383462915428));
#189521=CARTESIAN_POINT('Ctrl Pts',(-33.6191451996212,3.81472140941051,
135.188379215148));
#189522=CARTESIAN_POINT('Ctrl Pts',(-33.8975928234342,5.75034910954236,
129.964596594906));
#189523=CARTESIAN_POINT('Ctrl Pts',(-34.176040447247,2.40168689817613,125.512516086734));
#189524=CARTESIAN_POINT('Ctrl Pts',(-34.4544880710599,-3.15400824368619,
125.923382181419));
#189525=CARTESIAN_POINT('Ctrl Pts',(-34.7329356948729,-5.81132389146964,
130.81962900987));
#189526=CARTESIAN_POINT('Ctrl Pts',(-35.0113833186857,-3.1283167819475,
135.701844931696));
#189527=CARTESIAN_POINT('Ctrl Pts',(-35.2898309424986,2.42946062341331,
136.083512024245));
#189528=CARTESIAN_POINT('Ctrl Pts',(-35.5682785663115,5.75468240160701,
131.613896874941));
#189529=CARTESIAN_POINT('Ctrl Pts',(-35.8467261901244,3.79163218458816,
126.400357453152));
#189530=CARTESIAN_POINT('Ctrl Pts',(-36.1251738139373,-1.65574277853735,
125.233881791944));
#189531=CARTESIAN_POINT('Ctrl Pts',(-36.4036214377501,-5.58157101571846,
129.186404038463));
#189532=CARTESIAN_POINT('Ctrl Pts',(-36.6820690615631,-4.37820816435757,
134.625749339604));
#189533=CARTESIAN_POINT('Ctrl Pts',(-36.960516685376,0.848514102688449,
136.553425090409));
#189534=CARTESIAN_POINT('Ctrl Pts',(-37.2389643091888,5.29549336158222,
133.197991448084));
#189535=CARTESIAN_POINT('Ctrl Pts',(-37.5174119330018,4.87617292041449,
127.64292800788));
#189536=CARTESIAN_POINT('Ctrl Pts',(-37.7958595568146,-0.0241122203237842,
124.993066691407));
#189537=CARTESIAN_POINT('Ctrl Pts',(-38.0743071806275,-4.90223940853195,
127.683500595584));
#189538=CARTESIAN_POINT('Ctrl Pts',(-38.3527548044404,-5.27544806800837,
133.241852397473));
#189539=CARTESIAN_POINT('Ctrl Pts',(-38.6312024282533,-0.800777672950798,
136.560268331721));
#189540=CARTESIAN_POINT('Ctrl Pts',(-38.9096500520661,4.40976828338437,
134.589286268384));
#189541=CARTESIAN_POINT('Ctrl Pts',(-39.1880976758791,5.56795261644649,
129.140142435842));
#189542=CARTESIAN_POINT('Ctrl Pts',(-39.4665452996919,1.6094605046014,125.220333810727));
#189543=CARTESIAN_POINT('Ctrl Pts',(-39.7449929235049,-3.82804718445556,
126.43197302622));
#189544=CARTESIAN_POINT('Ctrl Pts',(-40.0234405473177,-5.74776652149929,
131.661622835152));
#189545=CARTESIAN_POINT('Ctrl Pts',(-40.3018881711306,-2.38556921929025,
136.103490545709));
#189546=CARTESIAN_POINT('Ctrl Pts',(-40.5803357949436,3.16884965391132,
135.675716729192));
#189547=CARTESIAN_POINT('Ctrl Pts',(-40.8587834187564,5.81125050208024,
130.771404625066));
#189548=CARTESIAN_POINT('Ctrl Pts',(-41.1372310425694,3.11339603420704,
125.897377468058));
#189549=CARTESIAN_POINT('Ctrl Pts',(-41.4156786663821,-2.4455172912504,
125.532628105994));
#189550=CARTESIAN_POINT('Ctrl Pts',(-41.6941262901951,-5.75711969621025,
130.012343383614));
#189551=CARTESIAN_POINT('Ctrl Pts',(-41.9725739140079,-3.77821035128576,
135.219883807042));
#189552=CARTESIAN_POINT('Ctrl Pts',(-42.2510215378209,1.67268973063362,
136.369774129642));
#189553=CARTESIAN_POINT('Ctrl Pts',(-42.5294691616338,5.58646966553678,
132.405321320208));
#189554=CARTESIAN_POINT('Ctrl Pts',(-42.8079167854466,4.366556892027,126.969663836325));
#189555=CARTESIAN_POINT('Ctrl Pts',(-43.0863644092596,-0.866008347092154,
125.057905359049));
#189556=CARTESIAN_POINT('Ctrl Pts',(-43.3648120330724,-5.3027542220935,
128.426858534403));
#189557=CARTESIAN_POINT('Ctrl Pts',(-43.6432596568854,-4.86652802093628,
133.98061997675));
#189558=CARTESIAN_POINT('Ctrl Pts',(-43.9217072806982,0.0417996883503892,
136.615554236903));
#189559=CARTESIAN_POINT('Ctrl Pts',(-44.2001549045111,4.9117155260715,133.910285453475));
#189560=CARTESIAN_POINT('Ctrl Pts',(-44.478602528324,5.26800474597596,128.350823478709));
#189561=CARTESIAN_POINT('Ctrl Pts',(-44.7570501521369,0.783254960667603,
125.046042272601));
#189562=CARTESIAN_POINT('Ctrl Pts',(-45.0354977759497,-4.42126786936209,
127.032874316024));
#189563=CARTESIAN_POINT('Ctrl Pts',(-45.3139453997627,-5.56286151839129,
132.485518023215));
#189564=CARTESIAN_POINT('Ctrl Pts',(-45.5923930235756,-1.59245719291215,
136.393260203719));
#189565=CARTESIAN_POINT('Ctrl Pts',(-45.8708406473885,3.84133749699455,
135.165076697471));
#189566=CARTESIAN_POINT('Ctrl Pts',(-46.1492882712014,5.74513068693249,
129.929608146614));
#189567=CARTESIAN_POINT('Ctrl Pts',(-46.4277358950142,2.3694294408167,125.497994382526));
#189568=CARTESIAN_POINT('Ctrl Pts',(-46.7061835188271,-3.18366170834627,
125.942671958037));
#189569=CARTESIAN_POINT('Ctrl Pts',(-46.98463114264,-5.81112327806003,130.85500390496));
#189570=CARTESIAN_POINT('Ctrl Pts',(-47.263078766453,-3.09844644439114,
135.720797144829));
#189571=CARTESIAN_POINT('Ctrl Pts',(-47.5415263902657,2.46155130414924,
136.068625397419));
#189572=CARTESIAN_POINT('Ctrl Pts',(-47.8199740140787,5.75950365764311,
131.578851490957));
#189573=CARTESIAN_POINT('Ctrl Pts',(-48.0984216378915,3.76475351715869,
126.377358307829));
#189574=CARTESIAN_POINT('Ctrl Pts',(-48.3768692617045,-1.6896211871606,
125.244063976264));
#189575=CARTESIAN_POINT('Ctrl Pts',(-48.6553168855173,-5.59131656306301,
129.220410622463));
#189576=CARTESIAN_POINT('Ctrl Pts',(-48.9337645093303,-4.35486516851022,
134.652329933902));
#189577=CARTESIAN_POINT('Ctrl Pts',(-49.2122121331431,0.883494568912716,
136.548153427379));
#189578=CARTESIAN_POINT('Ctrl Pts',(-49.4906597569561,5.3099659586141,133.165711928516));
#189579=CARTESIAN_POINT('Ctrl Pts',(-49.7691073807689,4.85683803860733,
127.613303933314));
#189580=CARTESIAN_POINT('Ctrl Pts',(-50.0475550045819,-0.0594867691506708,
124.993321139153));
#189581=CARTESIAN_POINT('Ctrl Pts',(-50.3260026283946,-4.92114614214944,
127.713399740592));
#189582=CARTESIAN_POINT('Ctrl Pts',(-50.6044502522077,-5.26051262186729,
133.273920386136));
#189583=CARTESIAN_POINT('Ctrl Pts',(-50.8828978760204,-0.765724992417492,
136.565036249065));
#189584=CARTESIAN_POINT('Ctrl Pts',(-51.1613454998334,4.4327264973184,134.562372631296));
#189585=CARTESIAN_POINT('Ctrl Pts',(-51.4397931236463,5.55771888674681,
129.106279562002));
#189586=CARTESIAN_POINT('Ctrl Pts',(-51.7182407474591,1.57543912891688,
125.210640026899));
#189587=CARTESIAN_POINT('Ctrl Pts',(-51.9966883712721,-3.85459222390762,
126.455356446176));
#189588=CARTESIAN_POINT('Ctrl Pts',(-52.2751359950849,-5.7424416302597,
131.696595238295));
#189589=CARTESIAN_POINT('Ctrl Pts',(-52.5535836188979,-2.35326771227282,
136.117914002047));
#189590=CARTESIAN_POINT('Ctrl Pts',(-52.8320312427106,3.19844426977395,
135.656336786975));
#189591=CARTESIAN_POINT('Ctrl Pts',(-53.1104788665238,5.81094222058764,
130.736030504428));
#189592=CARTESIAN_POINT('Ctrl Pts',(-53.3889264903363,3.08346815099054,
125.878516257743));
#189593=CARTESIAN_POINT('Ctrl Pts',(-53.6673741141495,-2.47756251357323,
125.547612336859));
#189594=CARTESIAN_POINT('Ctrl Pts',(-53.9458217379622,-5.76183426382087,
130.047403279515));
#189595=CARTESIAN_POINT('Ctrl Pts',(-54.2242693617753,-3.75126180686946,
135.242801036416));
#189596=CARTESIAN_POINT('Ctrl Pts',(-54.502716985588,1.70653699126786,136.359488878264));
#189597=CARTESIAN_POINT('Ctrl Pts',(-54.7811646094011,5.59611166339667,
132.371285231631));
#189598=CARTESIAN_POINT('Ctrl Pts',(-55.0596122332138,4.3431331021171,126.943154413196));
#189599=CARTESIAN_POINT('Ctrl Pts',(-55.3380598570268,-0.900972606160421,
125.063283466166));
#189600=CARTESIAN_POINT('Ctrl Pts',(-55.6165074808396,-5.31712850433539,
128.459181954061));
#189601=CARTESIAN_POINT('Ctrl Pts',(-55.8949551046525,-4.84710306319425,
134.01018506537));
#189602=CARTESIAN_POINT('Ctrl Pts',(-56.1734027284654,0.0771732988733811,
136.615192122377));
#189603=CARTESIAN_POINT('Ctrl Pts',(-56.4518503522783,4.93053116940174,
133.880328901363));
#189604=CARTESIAN_POINT('Ctrl Pts',(-56.7302979760911,5.25297176508825,
128.318801096944));
#189605=CARTESIAN_POINT('Ctrl Pts',(-57.0087455999042,0.748187930595796,
125.041381065643));
#189606=CARTESIAN_POINT('Ctrl Pts',(-57.2871932237169,-4.44414406110167,
127.059857705357));
#189607=CARTESIAN_POINT('Ctrl Pts',(-57.5656408475299,-5.55252476915405,
132.519349592253));
#189608=CARTESIAN_POINT('Ctrl Pts',(-57.8440884713427,-1.55840647026886,
136.402850393281));
#189609=CARTESIAN_POINT('Ctrl Pts',(-58.1225360951557,3.867811242405,135.141612591857));
#189610=CARTESIAN_POINT('Ctrl Pts',(-58.4009837189685,5.73969937639226,
129.894652112598));
#189611=CARTESIAN_POINT('Ctrl Pts',(-58.6794313427815,2.33708418337799,
125.483669307672));
#189612=CARTESIAN_POINT('Ctrl Pts',(-58.9578789665944,-3.21319720125095,
125.962141886319));
#189613=CARTESIAN_POINT('Ctrl Pts',(-59.2363265904072,-5.81070733134035,
130.890376923444));
#189614=CARTESIAN_POINT('Ctrl Pts',(-59.5147742142201,-3.06846129276222,
135.739567177598));
#189615=CARTESIAN_POINT('Ctrl Pts',(-59.793221838033,2.49355077119662,136.053543701326));
#189616=CARTESIAN_POINT('Ctrl Pts',(-60.071669461846,5.76411149315304,131.543777407928));
#189617=CARTESIAN_POINT('Ctrl Pts',(-60.3501170856587,3.73773534540316,
126.354523206705));
#189618=CARTESIAN_POINT('Ctrl Pts',(-60.6285647094717,-1.72343698624942,
125.254452199421));
#189619=CARTESIAN_POINT('Ctrl Pts',(-60.9070123332846,-5.6008549221161,
129.254475900312));
#189620=CARTESIAN_POINT('Ctrl Pts',(-61.1854599570975,-4.33136080153256,
134.678767940282));
#189621=CARTESIAN_POINT('Ctrl Pts',(-61.4639075809103,0.918442296920838,
136.542668925995));
#189622=CARTESIAN_POINT('Ctrl Pts',(-61.7423552047232,5.32424179290464,
133.133344908207));
#189623=CARTESIAN_POINT('Ctrl Pts',(-62.0208028285362,4.83732318488056,
127.583798104527));
#189624=CARTESIAN_POINT('Ctrl Pts',(-62.299250452349,-0.0948591136734494,
124.993790917104));
#189625=CARTESIAN_POINT('Ctrl Pts',(-62.5776980761619,-4.93987052088691,
127.743413422294));
#189626=CARTESIAN_POINT('Ctrl Pts',(-62.8561456999749,-5.24538224549645,
133.305896864355));
#189627=CARTESIAN_POINT('Ctrl Pts',(-63.1345933237877,-0.730643937663188,
136.569590702456));
#189628=CARTESIAN_POINT('Ctrl Pts',(-63.4130409476006,4.45552045494177,
134.53531973969));
#189629=CARTESIAN_POINT('Ctrl Pts',(-63.6914885714135,5.5472792137301,129.072479611178));
#189630=CARTESIAN_POINT('Ctrl Pts',(-63.9699361952264,1.54135937475606,
125.201153520444));
#189631=CARTESIAN_POINT('Ctrl Pts',(-64.2483838190392,-3.88099443002729,
126.478901020081));
#189632=CARTESIAN_POINT('Ctrl Pts',(-64.5268314428522,-5.73690395073373,
131.731534579357));
#189633=CARTESIAN_POINT('Ctrl Pts',(-64.805279066665,-2.32087900405488,
136.132140562712));
#189634=CARTESIAN_POINT('Ctrl Pts',(-65.083726690478,3.22792036610792,135.636777052998));
#189635=CARTESIAN_POINT('Ctrl Pts',(-65.3621743142908,5.81041861249411,
130.700658915789));
#189636=CARTESIAN_POINT('Ctrl Pts',(-65.6406219381037,3.05342600872776,
125.859837576403));
#189637=CARTESIAN_POINT('Ctrl Pts',(-65.9190695619166,-2.50951592890599,
125.562791358466));
#189638=CARTESIAN_POINT('Ctrl Pts',(-66.1975171857295,-5.76633532454392,
130.082491224748));
#189639=CARTESIAN_POINT('Ctrl Pts',(-66.4759648095424,-3.72417425806736,
135.26555379775));
#189640=CARTESIAN_POINT('Ctrl Pts',(-66.7544124333553,1.74032101554631,
136.348997779564));
#189641=CARTESIAN_POINT('Ctrl Pts',(-67.0328600571681,5.60554629528092,
132.337191080086));
#189642=CARTESIAN_POINT('Ctrl Pts',(-67.3113076809811,4.31954837581292,
126.916788068483));
#189643=CARTESIAN_POINT('Ctrl Pts',(-67.5897553047939,-0.935903479357421,
125.068874311009));
#189644=CARTESIAN_POINT('Ctrl Pts',(-67.8682029286069,-5.33130575842519,
128.491592275178));
#189645=CARTESIAN_POINT('Ctrl Pts',(-68.1466505524197,-4.82749849426569,
134.039631360986));
#189646=CARTESIAN_POINT('Ctrl Pts',(-68.4250981762326,0.112544049711387,
136.614614685353));
#189647=CARTESIAN_POINT('Ctrl Pts',(-68.7035458000455,4.94916411008632,
133.850258368115));
#189648=CARTESIAN_POINT('Ctrl Pts',(-68.9819934238584,5.23774413340002,
128.286870818499));
#189649=CARTESIAN_POINT('Ctrl Pts',(-69.2604410476712,0.713093176145084,
125.036933408012));
#189650=CARTESIAN_POINT('Ctrl Pts',(-69.5388886714842,-4.46685557344872,
127.086979848621));
#189651=CARTESIAN_POINT('Ctrl Pts',(-69.8173362952971,-5.54198226906957,
132.553117611744));
#189652=CARTESIAN_POINT('Ctrl Pts',(-70.09578391911,-1.52429800030071,136.412233128746));
#189653=CARTESIAN_POINT('Ctrl Pts',(-70.3742315429229,3.89414166464747,
135.117987767775));
#189654=CARTESIAN_POINT('Ctrl Pts',(-70.6526791667357,5.73405537918087,
129.859729788164));
#189655=CARTESIAN_POINT('Ctrl Pts',(-70.9311267905487,2.3046523244254,125.469541392991));
#189656=CARTESIAN_POINT('Ctrl Pts',(-71.2095744143614,-3.24261362795168,
125.981791244794));
#189657=CARTESIAN_POINT('Ctrl Pts',(-71.4880220381746,-5.81007606672361,
130.925746754563));
#189658=CARTESIAN_POINT('Ctrl Pts',(-71.7664696619872,-3.03836243817177,
135.758154334473));
#189659=CARTESIAN_POINT('Ctrl Pts',(-72.0449172858002,2.52545783880292,
136.038267494822));
#189660=CARTESIAN_POINT('Ctrl Pts',(-72.3233649096131,5.76850573739207,
131.508675925537));
#189661=CARTESIAN_POINT('Ctrl Pts',(-72.601812533426,3.71057867048956,126.331852995942));
#189662=CARTESIAN_POINT('Ctrl Pts',(-72.8802601572389,-1.75718892274731,
125.265046076474));
#189663=CARTESIAN_POINT('Ctrl Pts',(-73.1587077810518,-5.61018573943046,
129.28859860971));
#189664=CARTESIAN_POINT('Ctrl Pts',(-73.4371554048648,-4.30769593438731,
134.705062379074));
#189665=CARTESIAN_POINT('Ctrl Pts',(-73.7156030286775,0.953355991712339,
136.536971789486));
#189666=CARTESIAN_POINT('Ctrl Pts',(-73.9940506524905,5.33832033545752,
133.100891586529));
#189667=CARTESIAN_POINT('Ctrl Pts',(-74.2724982763033,4.81762908236426,
127.554411614868));
#189668=CARTESIAN_POINT('Ctrl Pts',(-74.5509459001162,-0.130227943157576,
124.994476007852));
#189669=CARTESIAN_POINT('Ctrl Pts',(-74.8293935239292,-4.95841185090586,
127.77354052852));
#189670=CARTESIAN_POINT('Ctrl Pts',(-75.107841147742,-5.23005749955717,
133.337780647228));
#189671=CARTESIAN_POINT('Ctrl Pts',(-75.3862887715549,-0.695535808628632,
136.573931523126));
#189672=CARTESIAN_POINT('Ctrl Pts',(-75.6647363953679,4.4781493116164,134.508128596022));
#189673=CARTESIAN_POINT('Ctrl Pts',(-75.9431840191806,5.53663398424198,
129.038743835842));
#189674=CARTESIAN_POINT('Ctrl Pts',(-76.2216316429937,1.50722250495638,
125.191874642891));
#189675=CARTESIAN_POINT('Ctrl Pts',(-76.5000792668064,-3.90725282447187,
126.502605875483));
#189676=CARTESIAN_POINT('Ctrl Pts',(-76.7785268906195,-5.73115368812196,
131.766439563647));
#189677=CARTESIAN_POINT('Ctrl Pts',(-77.0569745144322,-2.28840429481114,
136.146169700531));
#189678=CARTESIAN_POINT('Ctrl Pts',(-77.3354221382452,3.25727685066645,
135.617038252052));
#189679=CARTESIAN_POINT('Ctrl Pts',(-77.613869762058,5.80967969720196,130.665291169852));
#189680=CARTESIAN_POINT('Ctrl Pts',(-77.8923173858709,3.0232707206408,125.841342116181));
#189681=CARTESIAN_POINT('Ctrl Pts',(-78.1707650096839,-2.54137635320382,
125.57816460835));
#189682=CARTESIAN_POINT('Ctrl Pts',(-78.4492126334967,-5.77062271159095,
130.117605919119));
#189683=CARTESIAN_POINT('Ctrl Pts',(-78.7276602573096,-3.69694870861804,
135.288141247929));
#189684=CARTESIAN_POINT('Ctrl Pts',(-79.0061078811224,1.77404055158998,
136.338301222296));
#189685=CARTESIAN_POINT('Ctrl Pts',(-79.2845555049354,5.61477321158579,
132.303040128944));
#189686=CARTESIAN_POINT('Ctrl Pts',(-79.5630031287483,4.29580358705489,
126.8905657792));
#189687=CARTESIAN_POINT('Ctrl Pts',(-79.8414507525611,-0.970799672307275,
125.074677686406));
#189688=CARTESIAN_POINT('Ctrl Pts',(-80.1198983763742,-5.34528545901998,
128.524088296775));
#189689=CARTESIAN_POINT('Ctrl Pts',(-80.3983460001869,-4.80771504060458,
134.068957772455));
#189690=CARTESIAN_POINT('Ctrl Pts',(-80.6767936239998,0.147910630189091,
136.613821947228));
#189691=CARTESIAN_POINT('Ctrl Pts',(-80.9552412478128,4.96761365767528,
133.820074968005));
#189692=CARTESIAN_POINT('Ctrl Pts',(-81.2336888716256,5.22232241517632,
128.255033826564));
#189693=CARTESIAN_POINT('Ctrl Pts',(-81.5121364954386,0.6779719977639,125.032699464516));
#189694=CARTESIAN_POINT('Ctrl Pts',(-81.7905841192513,-4.48940156482041,
127.114239740797));
#189695=CARTESIAN_POINT('Ctrl Pts',(-82.0690317430644,-5.53123440879372,
132.586820830401));
#189696=CARTESIAN_POINT('Ctrl Pts',(-82.3474793668772,-1.490133046909,136.421408062431));
#189697=CARTESIAN_POINT('Ctrl Pts',(-82.62592699069,3.92032778803891,135.094203100652));
#189698=CARTESIAN_POINT('Ctrl Pts',(-82.9043746145031,5.72819890443852,
129.824842467372));
#189699=CARTESIAN_POINT('Ctrl Pts',(-83.1828222383158,2.27213506573304,
125.455611161998));
#189700=CARTESIAN_POINT('Ctrl Pts',(-83.4612698621288,-3.27190989841242,
126.001619305352));
#189701=CARTESIAN_POINT('Ctrl Pts',(-83.7397174859417,-5.80922950760163,
130.961112087674));
#189702=CARTESIAN_POINT('Ctrl Pts',(-84.0181651097544,-3.00815099594316,
135.776557926701));
#189703=CARTESIAN_POINT('Ctrl Pts',(-84.2966127335676,2.55727132464077,
136.022797343974));
#189704=CARTESIAN_POINT('Ctrl Pts',(-84.5750603573801,5.77268622752965,
131.473548344486));
#189705=CARTESIAN_POINT('Ctrl Pts',(-84.8535079811934,3.68328449871872,
126.309348515594));
#189706=CARTESIAN_POINT('Ctrl Pts',(-85.131955605006,-1.79087574596318,
125.275845214866));
#189707=CARTESIAN_POINT('Ctrl Pts',(-85.4104032288191,-5.61930866924928,
129.322777486226));
#189708=CARTESIAN_POINT('Ctrl Pts',(-85.6888508526319,-4.28387144398495,
134.731212275928));
#189709=CARTESIAN_POINT('Ctrl Pts',(-85.9672984764448,0.98823435954663,
136.531062228962));
#189710=CARTESIAN_POINT('Ctrl Pts',(-86.2457461002577,5.35220106458756,
133.068353166051));
#189711=CARTESIAN_POINT('Ctrl Pts',(-86.5241937240705,4.79775646083024,
127.525145553266));
#189712=CARTESIAN_POINT('Ctrl Pts',(-86.8026413478836,-0.165591946996939,
124.995376386011));
#189713=CARTESIAN_POINT('Ctrl Pts',(-87.0810889716963,-4.97676944515001,
127.803779942897));
#189714=CARTESIAN_POINT('Ctrl Pts',(-87.3595365955093,-5.21453895191432,
133.36957055329));
#189715=CARTESIAN_POINT('Ctrl Pts',(-87.6379842193221,-0.660401906259044,
136.578058550223));
#189716=CARTESIAN_POINT('Ctrl Pts',(-87.916431843135,4.50061222882128,134.480800207869));
#189717=CARTESIAN_POINT('Ctrl Pts',(-88.1948794669479,5.52578359274576,
129.005073486085));
#189718=CARTESIAN_POINT('Ctrl Pts',(-88.4733270907608,1.47302978447255,
125.182803738068));
#189719=CARTESIAN_POINT('Ctrl Pts',(-88.7517747145737,-3.93336643422502,
126.526470133988));
#189720=CARTESIAN_POINT('Ctrl Pts',(-89.0302223383866,-5.7251910555031,
131.801308897747));
#189721=CARTESIAN_POINT('Ctrl Pts',(-89.3086699621995,-2.25584478790559,
136.16000089565));
#189722=CARTESIAN_POINT('Ctrl Pts',(-89.5871175860123,3.28651263563227,
135.597121115567));
#189723=CARTESIAN_POINT('Ctrl Pts',(-89.8655652098253,5.80872550209253,
130.629928577187));
#189724=CARTESIAN_POINT('Ctrl Pts',(-90.1440128336381,2.99300340414587,
125.823030562435));
#189725=CARTESIAN_POINT('Ctrl Pts',(-90.4224604574511,-2.57314260586573,
125.593731516848));
#189726=CARTESIAN_POINT('Ctrl Pts',(-90.7009080812639,-5.77469626609129,
130.152746061436));
#189727=CARTESIAN_POINT('Ctrl Pts',(-90.9793557050769,-3.66958616737523,
135.310562549967));
#189728=CARTESIAN_POINT('Ctrl Pts',(-91.2578033288896,1.80769434990835,
136.327399602824));
#189729=CARTESIAN_POINT('Ctrl Pts',(-91.5362509527026,5.62379207040447,
132.268833643682));
#189730=CARTESIAN_POINT('Ctrl Pts',(-91.8146985765155,4.27189961571542,
126.864488517025));
#189731=CARTESIAN_POINT('Ctrl Pts',(-92.0931462003284,-1.00565989191805,
125.080693377311));
#189732=CARTESIAN_POINT('Ctrl Pts',(-92.3715938241412,-5.3590670880956,
128.556668814702));
#189733=CARTESIAN_POINT('Ctrl Pts',(-92.6500414479542,-4.78775343529548,
134.098163213075));
#189734=CARTESIAN_POINT('Ctrl Pts',(-92.928489071767,0.183271729783054,
136.612813937377));
#189735=CARTESIAN_POINT('Ctrl Pts',(-93.2069366955801,4.98587912851244,
133.789779819492));
#189736=CARTESIAN_POINT('Ctrl Pts',(-93.4853843193926,5.2067071818758,128.223291300872));
#189737=CARTESIAN_POINT('Ctrl Pts',(-93.7638319432059,0.642825696881324,
125.028679392048));
#189738=CARTESIAN_POINT('Ctrl Pts',(-94.0422795670186,-4.51178119976554,
127.14163637176));
#189739=CARTESIAN_POINT('Ctrl Pts',(-94.3207271908314,-5.52028158659305,
132.62045799934));
#189740=CARTESIAN_POINT('Ctrl Pts',(-94.5991748146444,-1.45591287608963,
136.430374854359));
#189741=CARTESIAN_POINT('Ctrl Pts',(-94.8776224384574,3.94636864224209,
135.07025947184));
#189742=CARTESIAN_POINT('Ctrl Pts',(-95.1560700622702,5.7221301691794,129.789991442987));
#189743=CARTESIAN_POINT('Ctrl Pts',(-95.4345176860831,2.23953361224044,
125.441879130882));
#189744=CARTESIAN_POINT('Ctrl Pts',(-95.7129653098959,-3.30108492704829,
126.021625333256));
#189745=CARTESIAN_POINT('Ctrl Pts',(-95.9914129337089,-5.80816768534362,
130.996471612301));
#189746=CARTESIAN_POINT('Ctrl Pts',(-96.2698605575217,-2.97782808557417,
135.794777272329));
#189747=CARTESIAN_POINT('Ctrl Pts',(-96.5483081813347,2.58899004984866,
136.007133822036));
#189748=CARTESIAN_POINT('Ctrl Pts',(-96.8267558051475,5.77665280865574,
131.438395966436));
#189749=CARTESIAN_POINT('Ctrl Pts',(-97.1052034289604,3.65585384148698,
126.287010599573));
#189750=CARTESIAN_POINT('Ctrl Pts',(-97.3836510527732,-1.82449620761995,
125.286849214428));
#189751=CARTESIAN_POINT('Ctrl Pts',(-97.6620986765863,-5.62822337351841,
129.35701126335));
#189752=CARTESIAN_POINT('Ctrl Pts',(-97.9405463003989,-4.25988821315111,
134.757216661848));
#189753=CARTESIAN_POINT('Ctrl Pts',(-98.2189939242121,1.02307610799351,
136.524940463405));
#189754=CARTESIAN_POINT('Ctrl Pts',(-98.4974415480248,5.36588346593846,
133.035730852497));
#189755=CARTESIAN_POINT('Ctrl Pts',(-98.7758891718378,4.77770605666655,
127.496001004183));
#189756=CARTESIAN_POINT('Ctrl Pts',(-99.0543367956506,-0.200949814765295,
124.996492018215));
#189757=CARTESIAN_POINT('Ctrl Pts',(-99.3327844194636,-4.99494262337204,
127.834130544897));
#189758=CARTESIAN_POINT('Ctrl Pts',(-99.6112320432764,-5.19882717761281,
133.401265404553));
#189759=CARTESIAN_POINT('Ctrl Pts',(-99.8896796670892,-0.625243532454567,
136.581971630822));
#189760=CARTESIAN_POINT('Ctrl Pts',(-100.168127290903,4.5229083741848,134.453335587896));
#189761=CARTESIAN_POINT('Ctrl Pts',(-100.446574914715,5.51472844130613,
128.971469809575));
#189762=CARTESIAN_POINT('Ctrl Pts',(-100.725022538528,1.43878248032906,
125.173941142103));
#189763=CARTESIAN_POINT('Ctrl Pts',(-101.003470162341,-3.95933429163924,
126.550492911299));
#189764=CARTESIAN_POINT('Ctrl Pts',(-101.281917786154,-5.71901627382367,
131.836141289563));
#189765=CARTESIAN_POINT('Ctrl Pts',(-101.560365409967,-2.22320168984167,
136.17363363555));
#189766=CARTESIAN_POINT('Ctrl Pts',(-101.83881303378,3.31562663766449,135.577026381578));
#189767=CARTESIAN_POINT('Ctrl Pts',(-102.117260657593,5.80755606252295,
130.594572448163));
#189768=CARTESIAN_POINT('Ctrl Pts',(-102.395708281405,2.96262518080941,
125.804903593708));
#189769=CARTESIAN_POINT('Ctrl Pts',(-102.674155905219,-2.60481350978186,
125.609491507123));
#189770=CARTESIAN_POINT('Ctrl Pts',(-102.952603529031,-5.77855583709781,
130.187910349571));
#189771=CARTESIAN_POINT('Ctrl Pts',(-103.231051152844,-3.64208764826766,
135.332816873036));
#189772=CARTESIAN_POINT('Ctrl Pts',(-103.509498776657,1.84128116344741,
136.316293325111));
#189773=CARTESIAN_POINT('Ctrl Pts',(-103.78794640047,5.63260253753978,132.234572891835));
#189774=CARTESIAN_POINT('Ctrl Pts',(-104.066394024283,4.24783734756473,
126.838557248259));
#189775=CARTESIAN_POINT('Ctrl Pts',(-104.344841648096,-1.04048284643121,
125.086921160811));
#189776=CARTESIAN_POINT('Ctrl Pts',(-104.623289271909,-5.3726501349701,
128.589332621676));
#189777=CARTESIAN_POINT('Ctrl Pts',(-104.901736895722,-4.76761441802147,
134.12724660063));
#189778=CARTESIAN_POINT('Ctrl Pts',(-105.180184519534,0.218626038175886,
136.611590693152));
#189779=CARTESIAN_POINT('Ctrl Pts',(-105.458632143348,5.00395984576562,
133.759374045173));
#189780=CARTESIAN_POINT('Ctrl Pts',(-105.73707976716,5.1908990121252,128.191644417652));
#189781=CARTESIAN_POINT('Ctrl Pts',(-106.015527390973,0.607655575856702,
125.024873339572));
#189782=CARTESIAN_POINT('Ctrl Pts',(-106.293975014786,-4.53399364899913,
127.169168726316));
#189783=CARTESIAN_POINT('Ctrl Pts',(-106.572422638599,-5.50912420832816,
132.654027872123));
#189784=CARTESIAN_POINT('Ctrl Pts',(-106.850870262412,-1.42163875588365,
136.43913317226));
#189785=CARTESIAN_POINT('Ctrl Pts',(-107.129317886225,3.97226326230387,
135.046157768576));
#189786=CARTESIAN_POINT('Ctrl Pts',(-107.407765510038,5.71584939828273,
129.755178006424));
#189787=CARTESIAN_POINT('Ctrl Pts',(-107.686213133851,2.20684917200607,
125.428345808491));
#189788=CARTESIAN_POINT('Ctrl Pts',(-107.964660757664,-3.3301376327682,
126.041808587174));
#189789=CARTESIAN_POINT('Ctrl Pts',(-108.243108381476,-5.80689063929651,
131.031824018185));
#189790=CARTESIAN_POINT('Ctrl Pts',(-108.521556005289,-2.94739483068967,
135.812811696231));
#189791=CARTESIAN_POINT('Ctrl Pts',(-108.800003629102,2.62061283907833,
135.991277509423));
#189792=CARTESIAN_POINT('Ctrl Pts',(-109.078451252915,5.7804053337882,131.403220093974));
#189793=CARTESIAN_POINT('Ctrl Pts',(-109.356898876728,3.62828771524594,
126.264840075618));
#189794=CARTESIAN_POINT('Ctrl Pts',(-109.635346500541,-1.85804906189805,
125.298057667405));
#189795=CARTESIAN_POINT('Ctrl Pts',(-109.913794124354,-5.636929521901,129.391298672536));
#189796=CARTESIAN_POINT('Ctrl Pts',(-110.192241748167,-4.2357471305931,
134.783074573235));
#189797=CARTESIAN_POINT('Ctrl Pts',(-110.470689371979,1.05787994597834,
136.518606719657));
#189798=CARTESIAN_POINT('Ctrl Pts',(-110.749136995792,5.37936703250445,
133.003025854698));
#189799=CARTESIAN_POINT('Ctrl Pts',(-111.027584619605,4.75747861284798,
127.466979047582));
#189800=CARTESIAN_POINT('Ctrl Pts',(-111.306032243418,-0.23630023626489,
124.997822863128));
#189801=CARTESIAN_POINT('Ctrl Pts',(-111.584479867231,-5.01293071215839,
127.864591209862));
#189802=CARTESIAN_POINT('Ctrl Pts',(-111.862927491044,-5.18292275885852,
133.432864026556));
#189803=CARTESIAN_POINT('Ctrl Pts',(-112.141375114857,-0.590061990020461,
136.585670619917));
#189804=CARTESIAN_POINT('Ctrl Pts',(-112.41982273867,4.54503692151536,134.425735753813));
#189805=CARTESIAN_POINT('Ctrl Pts',(-112.698270362483,5.50346893957634,
128.937934051507));
#189806=CARTESIAN_POINT('Ctrl Pts',(-112.976717986295,1.40448186157095,
125.165287183403));
#189807=CARTESIAN_POINT('Ctrl Pts',(-113.255165610108,-3.98515543446448,
126.574673317241));
#189808=CARTESIAN_POINT('Ctrl Pts',(-113.533613233921,-5.71262957189362,
131.870935448366));
#189809=CARTESIAN_POINT('Ctrl Pts',(-113.812060857734,-2.19047621022174,
136.187067415062));
#189810=CARTESIAN_POINT('Ctrl Pts',(-114.090508481547,3.34461777793161,
135.556754794705));
#189811=CARTESIAN_POINT('Ctrl Pts',(-114.36895610536,5.80617142182825,130.559224092919));
#189812=CARTESIAN_POINT('Ctrl Pts',(-114.647403729173,2.9321371763071,125.786961881698));
#189813=CARTESIAN_POINT('Ctrl Pts',(-114.925851352986,-2.63638789137572,
125.625443995184));
#189814=CARTESIAN_POINT('Ctrl Pts',(-115.204298976799,-5.78220128159277,
130.223097480497));
#189815=CARTESIAN_POINT('Ctrl Pts',(-115.482746600612,-3.61445417026275,
135.354903392492));
#189816=CARTESIAN_POINT('Ctrl Pts',(-115.761194224424,1.87479974763623,
136.304982800703));
#189817=CARTESIAN_POINT('Ctrl Pts',(-116.039641848237,5.64120428651674,
132.200259142944));
#189818=CARTESIAN_POINT('Ctrl Pts',(-116.31808947205,4.22361767423897,126.812772933795));
#189819=CARTESIAN_POINT('Ctrl Pts',(-116.596537095863,-1.07526724547036,
125.093360806132));
#189820=CARTESIAN_POINT('Ctrl Pts',(-116.874984719676,-5.38603409631742,
128.622078507325));
#189821=CARTESIAN_POINT('Ctrl Pts',(-117.153432343489,-4.7472987350426,
134.156206857421));
#189822=CARTESIAN_POINT('Ctrl Pts',(-117.431879967302,0.253972245300257,
136.610152259881));
#189823=CARTESIAN_POINT('Ctrl Pts',(-117.710327591115,5.02185513944583,
133.728858771743));
#189824=CARTESIAN_POINT('Ctrl Pts',(-117.988775214928,5.17489849170343,
128.160094349593));
#189825=CARTESIAN_POINT('Ctrl Pts',(-118.26722283874,0.572462937930709,
125.021281448121));
#189826=CARTESIAN_POINT('Ctrl Pts',(-118.545670462553,-4.55603808943068,
127.196835784245));
#189827=CARTESIAN_POINT('Ctrl Pts',(-118.824118086366,-5.49776268743969,
132.687529204804));
#189828=CARTESIAN_POINT('Ctrl Pts',(-119.102565710179,-1.38731195633035,
136.447682691592));
#189829=CARTESIAN_POINT('Ctrl Pts',(-119.381013333992,3.99801068868978,
135.021898883958));
#189830=CARTESIAN_POINT('Ctrl Pts',(-119.659460957805,5.70935682448427,
129.720403447709));
#189831=CARTESIAN_POINT('Ctrl Pts',(-119.937908581618,2.17408295616475,
125.415011696306));
#189832=CARTESIAN_POINT('Ctrl Pts',(-120.216356205431,-3.3590669390133,
126.062168319208));
#189833=CARTESIAN_POINT('Ctrl Pts',(-120.494803829244,-5.80539841678086,
131.067167995328));
#189834=CARTESIAN_POINT('Ctrl Pts',(-120.773251453056,-2.91685235900652,
135.830660530138));
#189835=CARTESIAN_POINT('Ctrl Pts',(-121.051699076869,2.65213852053535,
135.975228993696));
#189836=CARTESIAN_POINT('Ctrl Pts',(-121.330146700682,5.78394366387473,
131.368022030553));
#189837=CARTESIAN_POINT('Ctrl Pts',(-121.608594324495,3.60058714147007,
126.242837765265));
#189838=CARTESIAN_POINT('Ctrl Pts',(-121.887041948308,-1.89153306548558,
125.309470158462));
#189839=CARTESIAN_POINT('Ctrl Pts',(-122.165489572121,-5.64542679178685,
129.425638443252));
#189840=CARTESIAN_POINT('Ctrl Pts',(-122.443937195934,-4.21144909086733,
134.808785051914));
#189841=CARTESIAN_POINT('Ctrl Pts',(-122.722384819747,1.09264458383337,
136.512061232418));
#189842=CARTESIAN_POINT('Ctrl Pts',(-123.00083244356,5.39265126464657,132.97023938455));
#189843=CARTESIAN_POINT('Ctrl Pts',(-123.279280067372,4.73707487890982,
127.438080758883));
#189844=CARTESIAN_POINT('Ctrl Pts',(-123.557727691185,-0.27164190157181,
124.999368871432));
#189845=CARTESIAN_POINT('Ctrl Pts',(-123.836175314998,-5.03073304495359,
127.895160809065));
#189846=CARTESIAN_POINT('Ctrl Pts',(-124.114622938811,-5.16682628499523,
133.464365248398));
#189847=CARTESIAN_POINT('Ctrl Pts',(-124.393070562624,-0.554858582622917,
136.589155380447));
#189848=CARTESIAN_POINT('Ctrl Pts',(-124.671518186437,4.56699705083122,
134.398001728342));
#189849=CARTESIAN_POINT('Ctrl Pts',(-124.94996581025,5.49200550478084,128.904467454562));
#189850=CARTESIAN_POINT('Ctrl Pts',(-125.228413434063,1.37012919922165,
125.156842182641));
#189851=CARTESIAN_POINT('Ctrl Pts',(-125.506861057876,-4.0108289058903,
126.599010455801));
#189852=CARTESIAN_POINT('Ctrl Pts',(-125.785308681688,-5.70603118637341,
131.905690084846));
#189853=CARTESIAN_POINT('Ctrl Pts',(-126.063756305501,-2.1576695617001,
136.200301736396));
#189854=CARTESIAN_POINT('Ctrl Pts',(-126.342203929314,3.37348498215772,
135.536307106118));
#189855=CARTESIAN_POINT('Ctrl Pts',(-126.620651553127,5.8045716313158,130.523884821299));
#189856=CARTESIAN_POINT('Ctrl Pts',(-126.89909917694,2.90154052038371,125.769206091244));
#189857=CARTESIAN_POINT('Ctrl Pts',(-127.177546800753,-2.66786458064647,
125.641588389905));
#189858=CARTESIAN_POINT('Ctrl Pts',(-127.455994424566,-5.7856324644928,
130.258306150342));
#189859=CARTESIAN_POINT('Ctrl Pts',(-127.734442048379,-3.5866867573295,
135.376821289913));
#189860=CARTESIAN_POINT('Ctrl Pts',(-128.012889672192,1.90824886043053,
136.293468448719));
#189861=CARTESIAN_POINT('Ctrl Pts',(-128.291337296005,5.64959699859458,
132.16589366852));
#189862=CARTESIAN_POINT('Ctrl Pts',(-128.569784919818,4.19924149320669,
126.787136529081));
#189863=CARTESIAN_POINT('Ctrl Pts',(-128.84823254363,-1.11001180008614,
125.100012074652));
#189864=CARTESIAN_POINT('Ctrl Pts',(-129.126680167443,-5.39921847619124,
128.654905258242));
#189865=CARTESIAN_POINT('Ctrl Pts',(-129.405127791256,-4.72680713916258,
134.185042910317));
#189866=CARTESIAN_POINT('Ctrl Pts',(-129.683575415069,0.289309041389885,
136.608498690867));
#189867=CARTESIAN_POINT('Ctrl Pts',(-129.962023038882,5.03956434643776,
133.69823512996));
#189868=CARTESIAN_POINT('Ctrl Pts',(-130.240470662695,5.15870621351431,
128.128642265792));
#189869=CARTESIAN_POINT('Ctrl Pts',(-130.518918286508,0.537249087180579,
125.017903850796));
#189870=CARTESIAN_POINT('Ctrl Pts',(-130.79736591032,-4.57791370419536,
127.224636520332));
#189871=CARTESIAN_POINT('Ctrl Pts',(-131.075813534134,-5.4861974449331,
132.720960755981));
#189872=CARTESIAN_POINT('Ctrl Pts',(-131.354261157946,-1.35293374942274,
136.456023095549));
#189873=CARTESIAN_POINT('Ctrl Pts',(-131.632708781759,4.02360996731925,
134.99748371691));
#189874=CARTESIAN_POINT('Ctrl Pts',(-131.911156405572,5.7026526883694,129.685669055425));
#189875=CARTESIAN_POINT('Ctrl Pts',(-132.189604029385,2.1412361788793,125.401877288427));
#189876=CARTESIAN_POINT('Ctrl Pts',(-132.468051653198,-3.38787177379785,
126.082703774923));
#189877=CARTESIAN_POINT('Ctrl Pts',(-132.746499277011,-5.80369107309236,
131.102502234048));
#189878=CARTESIAN_POINT('Ctrl Pts',(-133.024946900823,-2.88620180228584,
135.848323112653));
#189879=CARTESIAN_POINT('Ctrl Pts',(-133.303394524637,2.68356592602436,
135.95898886954));
#189880=CARTESIAN_POINT('Ctrl Pts',(-133.581842148449,5.78726766780228,
131.332803080451));
#189881=CARTESIAN_POINT('Ctrl Pts',(-133.860289772262,3.57275314661281,
126.221004483821));
#189882=CARTESIAN_POINT('Ctrl Pts',(-134.138737396075,-1.92494697761906,
125.321086264707));
#189883=CARTESIAN_POINT('Ctrl Pts',(-134.417185019888,-5.65371486830715,
129.460029303025));
#189884=CARTESIAN_POINT('Ctrl Pts',(-134.695632643701,-4.1869949943469,
134.834347145171));
#189885=CARTESIAN_POINT('Ctrl Pts',(-134.974080267514,1.1273687333409,136.505304244234));
#189886=CARTESIAN_POINT('Ctrl Pts',(-135.252527891327,5.40573567011315,
132.937372656969));
#189887=CARTESIAN_POINT('Ctrl Pts',(-135.53097551514,4.71649561092,127.409307208922));
#189888=CARTESIAN_POINT('Ctrl Pts',(-135.809423138953,-0.306973501088704,
125.001129985841));
#189889=CARTESIAN_POINT('Ctrl Pts',(-136.087870762765,-5.04834896208586,
127.925838209736));
#189890=CARTESIAN_POINT('Ctrl Pts',(-136.366318386578,-5.15053835248403,
133.49576790279));
#189891=CARTESIAN_POINT('Ctrl Pts',(-136.644766010391,-0.519634614735935,
136.592425783278));
#189892=CARTESIAN_POINT('Ctrl Pts',(-136.923213634204,4.58878794839197,
134.37013453918));
#189893=CARTESIAN_POINT('Ctrl Pts',(-137.201661258017,5.48033856170195,
128.871071258858));
#189894=CARTESIAN_POINT('Ctrl Pts',(-137.48010888183,1.33572576623031,125.148606452753));
#189895=CARTESIAN_POINT('Ctrl Pts',(-137.758556505643,-4.03635375457527,
126.623503425159));
#189896=CARTESIAN_POINT('Ctrl Pts',(-138.037004129456,-5.69922136176977,
131.940403911158));
#189897=CARTESIAN_POINT('Ctrl Pts',(-138.315451753269,-2.12478295993955,
136.213336109146));
#189898=CARTESIAN_POINT('Ctrl Pts',(-138.593899377082,3.40222718065648,
135.515684073514));
#189899=CARTESIAN_POINT('Ctrl Pts',(-138.872347000894,5.80275675026745,
130.488555942812));
#189900=CARTESIAN_POINT('Ctrl Pts',(-139.150794624707,2.870836346809,125.751636880291));
#189901=CARTESIAN_POINT('Ctrl Pts',(-139.42924224852,-2.69924241121433,
125.65792409305));
#189902=CARTESIAN_POINT('Ctrl Pts',(-139.707689872333,-5.78884925865424,
130.293535054436));
#189903=CARTESIAN_POINT('Ctrl Pts',(-139.986137496146,-3.55878643839929,
135.398569753122));
#189904=CARTESIAN_POINT('Ctrl Pts',(-140.264585119959,1.94162726236197,
136.281750695826));
#189905=CARTESIAN_POINT('Ctrl Pts',(-140.543032743772,5.65778036277742,
132.131477741989));
#189906=CARTESIAN_POINT('Ctrl Pts',(-140.821480367585,4.17470970773734,
126.761648984083));
#189907=CARTESIAN_POINT('Ctrl Pts',(-141.099927991397,-1.14471522280625,
125.106874719905));
#189908=CARTESIAN_POINT('Ctrl Pts',(-141.37837561521,-5.41220278603824,
128.687811658017));
#189909=CARTESIAN_POINT('Ctrl Pts',(-141.656823239023,-4.70614038970644,
134.213753690789));
#189910=CARTESIAN_POINT('Ctrl Pts',(-141.935270862836,0.324635117026387,
136.60663004738));
#189911=CARTESIAN_POINT('Ctrl Pts',(-142.213718486649,5.05708681051884,
133.667504254592));
#189912=CARTESIAN_POINT('Ctrl Pts',(-142.492166110462,5.14232277757003,
128.097289331719));
#189913=CARTESIAN_POINT('Ctrl Pts',(-142.770613734275,0.502015328467386,
125.014740672754));
#189914=CARTESIAN_POINT('Ctrl Pts',(-143.049061358088,-4.59961968268416,
127.252569904414));
#189915=CARTESIAN_POINT('Ctrl Pts',(-143.327508981901,-5.4744289093626,
132.754321286837));
#189916=CARTESIAN_POINT('Ctrl Pts',(-143.605956605714,-1.31850540905707,
136.464154075075));
#189917=CARTESIAN_POINT('Ctrl Pts',(-143.884404229526,4.04906014960179,
134.972913172143));
#189918=CARTESIAN_POINT('Ctrl Pts',(-144.162851853339,5.69573723836169,
129.650976116669));
#189919=CARTESIAN_POINT('Ctrl Pts',(-144.441299477152,2.10831005730047,
125.388943071553));
#189920=CARTESIAN_POINT('Ctrl Pts',(-144.719747100965,-3.41655106974776,
126.103414193369));
#189921=CARTESIAN_POINT('Ctrl Pts',(-144.998194724778,-5.80176867149642,
131.13782542502));
#189922=CARTESIAN_POINT('Ctrl Pts',(-145.276642348591,-2.85544429629671,
135.865798789283));
#189923=CARTESIAN_POINT('Ctrl Pts',(-145.555089972404,2.71489389099137,
135.942557738738));
#189924=CARTESIAN_POINT('Ctrl Pts',(-145.833537596217,5.79037722239768,
131.29756454872));
#189925=CARTESIAN_POINT('Ctrl Pts',(-146.111985220029,3.54478676207412,
126.199341040322));
#189926=CARTESIAN_POINT('Ctrl Pts',(-146.390432843843,-1.95828956013508,
125.332905555698));
#189927=CARTESIAN_POINT('Ctrl Pts',(-146.668880467655,-5.66179344434354,
129.49446997749));
#189928=CARTESIAN_POINT('Ctrl Pts',(-146.947328091469,-4.16238574718705,
134.859759905796));
#189929=CARTESIAN_POINT('Ctrl Pts',(-147.225775715281,1.16205110778606,
136.498336005488));
#189930=CARTESIAN_POINT('Ctrl Pts',(-147.504223339094,5.41861976405632,
132.904426889841));
#189931=CARTESIAN_POINT('Ctrl Pts',(-147.782670962907,4.6957415714508,127.380659463914));
#189932=CARTESIAN_POINT('Ctrl Pts',(-148.06111858672,-0.342293725589094,
125.003106141093));
#189933=CARTESIAN_POINT('Ctrl Pts',(-148.339566210533,-5.06577781079073,
127.956622275114));
#189934=CARTESIAN_POINT('Ctrl Pts',(-148.618013834346,-5.1340595648799,
133.527070826096));
#189935=CARTESIAN_POINT('Ctrl Pts',(-148.896461458158,-0.48439139159784,
136.595481707227));
#189936=CARTESIAN_POINT('Ctrl Pts',(-149.174909081971,4.61040880672808,
134.342135218952));
#189937=CARTESIAN_POINT('Ctrl Pts',(-149.453356705784,5.4684685426618,128.837746701901));
#189938=CARTESIAN_POINT('Ctrl Pts',(-149.731804329597,1.30127283742975,
125.140580298914));
#189939=CARTESIAN_POINT('Ctrl Pts',(-150.01025195341,-4.06172903468827,
126.648151317718));
#189940=CARTESIAN_POINT('Ctrl Pts',(-150.288699577223,-5.69220035042211,
131.975075640969));
#189941=CARTESIAN_POINT('Ctrl Pts',(-150.567147201036,-2.09181762356486,
136.226170050321));
#189942=CARTESIAN_POINT('Ctrl Pts',(-150.845594824849,3.43084330837664,
135.494886461086));
#189943=CARTESIAN_POINT('Ctrl Pts',(-151.124042448661,5.80072684593324,
130.453238766583));
#189944=CARTESIAN_POINT('Ctrl Pts',(-151.402490072475,2.84002579333802,
125.734254899877));
#189945=CARTESIAN_POINT('Ctrl Pts',(-151.680937696287,-2.73052022036177,
125.674450499292));
#189946=CARTESIAN_POINT('Ctrl Pts',(-151.9593853201,-5.79185154487752,130.32878288736));
#189947=CARTESIAN_POINT('Ctrl Pts',(-152.237832943913,-3.53075424732904,
135.420147976222));
#189948=CARTESIAN_POINT('Ctrl Pts',(-152.516280567726,1.97493371658077,
136.269829976228));
#189949=CARTESIAN_POINT('Ctrl Pts',(-152.794728191539,5.66575407582884,
132.097012638644));
#189950=CARTESIAN_POINT('Ctrl Pts',(-153.073175815352,4.15002322686382,
126.736311243251));
#189951=CARTESIAN_POINT('Ctrl Pts',(-153.351623439165,-1.17937622768304,
125.113948487592));
#189952=CARTESIAN_POINT('Ctrl Pts',(-153.630071062978,-5.42498654472129,
128.720796487292));
#189953=CARTESIAN_POINT('Ctrl Pts',(-153.90851868679,-4.6852992524868,134.242338134946));
#189954=CARTESIAN_POINT('Ctrl Pts',(-154.186966310604,0.359949163189457,
136.604546398667));
#189955=CARTESIAN_POINT('Ctrl Pts',(-154.465413934416,5.0744218823891,133.636667284384));
#189956=CARTESIAN_POINT('Ctrl Pts',(-154.743861558229,5.12574879096345,
128.066036709167));
#189957=CARTESIAN_POINT('Ctrl Pts',(-155.022309182042,0.466762967392146,
125.011792031209));
#189958=CARTESIAN_POINT('Ctrl Pts',(-155.300756805855,-4.62115522057418,
127.280634901405));
#189959=CARTESIAN_POINT('Ctrl Pts',(-155.579204429668,-5.46245751681569,
132.787609561181));
#189960=CARTESIAN_POINT('Ctrl Pts',(-155.857652053481,-1.28402821098903,
136.472075328871));
#189961=CARTESIAN_POINT('Ctrl Pts',(-156.136099677293,4.07436029247137,
134.948188160129));
#189962=CARTESIAN_POINT('Ctrl Pts',(-156.414547301107,5.68861073071636,
129.616325916999));
#189963=CARTESIAN_POINT('Ctrl Pts',(-156.692994924919,2.07530581151645,
125.376209524969));
#189964=CARTESIAN_POINT('Ctrl Pts',(-156.971442548732,-3.44510376414151,
126.124298807112));
#189965=CARTESIAN_POINT('Ctrl Pts',(-157.249890172545,-5.79963128322921,
131.173136259331));
#189966=CARTESIAN_POINT('Ctrl Pts',(-157.528337796358,-2.82458098076833,
135.883086912459));
#189967=CARTESIAN_POINT('Ctrl Pts',(-157.806785420171,2.74612125456611,
135.925936210153));
#189968=CARTESIAN_POINT('Ctrl Pts',(-158.085233043984,5.79327221243612,
131.262307741136));
#189969=CARTESIAN_POINT('Ctrl Pts',(-158.363680667797,3.51668902415852,
126.177848237519));
#189970=CARTESIAN_POINT('Ctrl Pts',(-158.64212829161,-1.9915595775106,125.344927593469));
#189971=CARTESIAN_POINT('Ctrl Pts',(-158.920575915422,-5.66966222054205,
129.528959190434));
#189972=CARTESIAN_POINT('Ctrl Pts',(-159.199023539236,-4.13762226129274,
134.885022392109));
#189973=CARTESIAN_POINT('Ctrl Pts',(-159.477471163048,1.19669042199943,
136.491156774389));
#189974=CARTESIAN_POINT('Ctrl Pts',(-159.755918786861,5.43130306905165,
132.871403303985));
#189975=CARTESIAN_POINT('Ctrl Pts',(-160.034366410674,4.67481352955083,
127.352138585409));
#189976=CARTESIAN_POINT('Ctrl Pts',(-160.312814034487,-0.377601266270116,
125.005297263965));
#189977=CARTESIAN_POINT('Ctrl Pts',(-160.5912616583,-5.08301894523598,127.987511864483));
#189978=CARTESIAN_POINT('Ctrl Pts',(-160.869709282113,-5.1173905328107,
133.558272858373));
#189979=CARTESIAN_POINT('Ctrl Pts',(-161.148156905926,-0.449130219157962,
136.598323039052));
#189980=CARTESIAN_POINT('Ctrl Pts',(-161.426604529739,4.63185882466967,
134.314004805186));
#189981=CARTESIAN_POINT('Ctrl Pts',(-161.705052153551,5.45639588750942,
128.804495018547));
#189982=CARTESIAN_POINT('Ctrl Pts',(-161.983499777364,1.26677168948586,
125.13276401854));
#189983=CARTESIAN_POINT('Ctrl Pts',(-162.261947401177,-4.08695380593746,
126.67295322014));
#189984=CARTESIAN_POINT('Ctrl Pts',(-162.54039502499,-5.68496841249774,
132.009703989503));
#189985=CARTESIAN_POINT('Ctrl Pts',(-162.818842648803,-2.05877477411906,
136.238803084352));
#189986=CARTESIAN_POINT('Ctrl Pts',(-163.097290272616,3.45933230493559,
135.473915039499));
#189987=CARTESIAN_POINT('Ctrl Pts',(-163.375737896429,5.79848199353304,
130.417934601304));
#189988=CARTESIAN_POINT('Ctrl Pts',(-163.654185520242,2.80911000166655,
125.717060794092));
#189989=CARTESIAN_POINT('Ctrl Pts',(-163.932633144055,-2.76169684907854,
125.691166996241));
#189990=CARTESIAN_POINT('Ctrl Pts',(-164.211080767867,-5.79463921191188,
130.36404834299));
#189991=CARTESIAN_POINT('Ctrl Pts',(-164.489528391681,-3.50259122286156,
135.441555159625));
#189992=CARTESIAN_POINT('Ctrl Pts',(-164.767976015493,2.00816698890481,
136.257706731653));
#189993=CARTESIAN_POINT('Ctrl Pts',(-165.046423639306,5.67351784227885,
132.062499635604));
#189994=CARTESIAN_POINT('Ctrl Pts',(-165.324871263119,4.12518296535417,
126.711124245485));
#189995=CARTESIAN_POINT('Ctrl Pts',(-165.603318886932,-1.21399353033979,
125.121233115594));
#189996=CARTESIAN_POINT('Ctrl Pts',(-165.881766510745,-5.43756927853226,
128.753858523801));
#189997=CARTESIAN_POINT('Ctrl Pts',(-166.160214134558,-4.66428449978105,
134.270795183582));
#189998=CARTESIAN_POINT('Ctrl Pts',(-166.438661758371,0.395249871304121,
136.602247821935));
#189999=CARTESIAN_POINT('Ctrl Pts',(-166.717109382183,5.09156891968999,
133.60572536201));
#190000=CARTESIAN_POINT('Ctrl Pts',(-166.995557005996,5.10898486785074,
128.034885556215));
#190001=CARTESIAN_POINT('Ctrl Pts',(-167.274004629809,0.431493310242956,
125.009058035423));
#190002=CARTESIAN_POINT('Ctrl Pts',(-167.552452253622,-4.64251951985801,
127.30883047135));
#190003=CARTESIAN_POINT('Ctrl Pts',(-167.830899877435,-5.45028371089662,
132.820824345507));
#190004=CARTESIAN_POINT('Ctrl Pts',(-168.109347501248,-1.24950343278299,
136.479786563416));
#190005=CARTESIAN_POINT('Ctrl Pts',(-168.387795125061,4.09950945842204,
134.923309597059));
#190006=CARTESIAN_POINT('Ctrl Pts',(-168.666242748874,5.68127342950807,
129.581719740392));
#190007=CARTESIAN_POINT('Ctrl Pts',(-168.944690372687,2.04222466451309,
125.36367712052));
#190008=CARTESIAN_POINT('Ctrl Pts',(-169.223137996499,-3.47352879894819,
126.145356842267));
#190009=CARTESIAN_POINT('Ctrl Pts',(-169.501585620313,-5.79727898749155,
131.208433428525));
#190010=CARTESIAN_POINT('Ctrl Pts',(-169.780033244125,-2.79361299935373,
135.900186841566));
#190011=CARTESIAN_POINT('Ctrl Pts',(-170.058480867939,2.77724685960862,
135.909124899701));
#190012=CARTESIAN_POINT('Ctrl Pts',(-170.336928491751,5.79595253064181,
131.227033964152));
#190013=CARTESIAN_POINT('Ctrl Pts',(-170.615376115564,3.48846097403773,
126.156526871832));
#190014=CARTESIAN_POINT('Ctrl Pts',(-170.893823739377,-2.02475579691427,
125.357151932539));
#190015=CARTESIAN_POINT('Ctrl Pts',(-171.17227136319,-5.67732090532164,
129.563495663847));
#190016=CARTESIAN_POINT('Ctrl Pts',(-171.450718987003,-4.11270545428381,
134.910133667999));
#190017=CARTESIAN_POINT('Ctrl Pts',(-171.729166610815,1.23128539240979,
136.483766816968));
#190018=CARTESIAN_POINT('Ctrl Pts',(-172.007614234629,5.44378511511418,
132.838303123102));
#190019=CARTESIAN_POINT('Ctrl Pts',(-172.286061858441,4.65371226071637,
127.323745630264));
#190020=CARTESIAN_POINT('Ctrl Pts',(-172.564509482254,-0.412894814796852,
125.00770327326));
#190021=CARTESIAN_POINT('Ctrl Pts',(-172.842957106067,-5.10007172654484,
128.018505833219));
#190022=CARTESIAN_POINT('Ctrl Pts',(-173.12140472988,-5.10053187395325,
133.589372843419));
#190023=CARTESIAN_POINT('Ctrl Pts',(-173.399852353693,-0.413852404033268,
136.600949673471));
#190024=CARTESIAN_POINT('Ctrl Pts',(-173.678299977506,4.65313720737985,
134.285744340263));
#190025=CARTESIAN_POINT('Ctrl Pts',(-173.956747601319,5.44412104360021,
128.771317440947));
#190026=CARTESIAN_POINT('Ctrl Pts',(-174.235195225131,1.23222360085094,
125.125157901261));
#190027=CARTESIAN_POINT('Ctrl Pts',(-174.513642848945,-4.11202713361109,
126.697908213384));
#190028=CARTESIAN_POINT('Ctrl Pts',(-174.792090472757,-5.67752581597763,
132.044287673595));
#190029=CARTESIAN_POINT('Ctrl Pts',(-175.070538096571,-2.02565563601667,
136.251234743121));
#190030=CARTESIAN_POINT('Ctrl Pts',(-175.348985720383,3.48769311466452,
135.452770585855));
#190031=CARTESIAN_POINT('Ctrl Pts',(-175.627433344196,5.79602227624969,
130.382644755183));
#190032=CARTESIAN_POINT('Ctrl Pts',(-175.905880968009,2.77809011739122,
125.700055200075));
#190033=CARTESIAN_POINT('Ctrl Pts',(-176.184328591822,-2.79277114210269,
125.708072964459));
#190034=CARTESIAN_POINT('Ctrl Pts',(-176.462776215635,-5.79721215645926,
130.399330114555));
#190035=CARTESIAN_POINT('Ctrl Pts',(-176.741223839448,-3.47429840858841,
135.462790510077));
#190036=CARTESIAN_POINT('Ctrl Pts',(-177.019671463261,2.04132584786218,
136.245381411334));
#190037=CARTESIAN_POINT('Ctrl Pts',(-177.298119087073,5.68107137443935,
132.02794001176));
#190038=CARTESIAN_POINT('Ctrl Pts',(-177.576566710886,4.10018984367198,
126.686088924097));
#190039=CARTESIAN_POINT('Ctrl Pts',(-177.855014334699,-1.24856584802001,
125.128728333976));
#190040=CARTESIAN_POINT('Ctrl Pts',(-178.133461958512,-5.4499505212146,
128.786996542421));
#190041=CARTESIAN_POINT('Ctrl Pts',(-178.411909582325,-4.64309691029714,
134.29912378221));
#190042=CARTESIAN_POINT('Ctrl Pts',(-178.690357206138,0.430535933288815,
136.599734402363));
#190043=CARTESIAN_POINT('Ctrl Pts',(-178.968804829951,5.10852728703229,
133.574679634036));
#190044=CARTESIAN_POINT('Ctrl Pts',(-179.247252453763,5.09203162942501,
128.00383702718));
#190045=CARTESIAN_POINT('Ctrl Pts',(-179.525700077576,0.396207663951002,
125.006538786706));
#190046=CARTESIAN_POINT('Ctrl Pts',(-179.80414770139,-4.66371178887382,
127.337155569449));
#190047=CARTESIAN_POINT('Ctrl Pts',(-180.082595325202,-5.43790794271038,
132.853964409027));
#190048=CARTESIAN_POINT('Ctrl Pts',(-180.361042949015,-1.2149323537682,
136.487287492965));
#190049=CARTESIAN_POINT('Ctrl Pts',(-180.639490572828,4.12450671554208,
134.898278404822));
#190050=CARTESIAN_POINT('Ctrl Pts',(-180.917938196641,5.67372560662389,
129.547158869193));
#190051=CARTESIAN_POINT('Ctrl Pts',(-181.196385820454,2.00906784212309,
125.351346322599));
#190052=CARTESIAN_POINT('Ctrl Pts',(-181.474833444267,-3.50182512086801,
126.166587518521));
#190053=CARTESIAN_POINT('Ctrl Pts',(-181.75328106808,-5.79471187144949,
131.243715624654));
#190054=CARTESIAN_POINT('Ctrl Pts',(-182.031728691892,-2.76254149958135,
135.917097942958));
#190055=CARTESIAN_POINT('Ctrl Pts',(-182.310176315705,2.80826955274668,
135.892124430331));
#190056=CARTESIAN_POINT('Ctrl Pts',(-182.588623939518,5.79841807769547,
131.191744524852));
#190057=CARTESIAN_POINT('Ctrl Pts',(-182.867071563331,3.46010365771282,
126.135377733334));
#190058=CARTESIAN_POINT('Ctrl Pts',(-183.145519187144,-2.05787698824661,
125.369578119929));
#190059=CARTESIAN_POINT('Ctrl Pts',(-183.423966810957,-5.68476921488759,
129.598078117967));
#190060=CARTESIAN_POINT('Ctrl Pts',(-183.70241443477,-4.08763624946197,
134.93509280296));
#190061=CARTESIAN_POINT('Ctrl Pts',(-183.980862058583,1.26583473708647,
136.476166407061));
#190062=CARTESIAN_POINT('Ctrl Pts',(-184.259309682396,5.45606543971754,
132.805127573733));
#190063=CARTESIAN_POINT('Ctrl Pts',(-184.537757306209,4.63243854686269,
127.295481650585));
#190064=CARTESIAN_POINT('Ctrl Pts',(-184.816204930021,-0.448173063354899,
125.010324079826));
#190065=CARTESIAN_POINT('Ctrl Pts',(-185.094652553834,-5.11693552282041,
128.049603032828));
#190066=CARTESIAN_POINT('Ctrl Pts',(-185.373100177647,-5.08348421301165,
133.620369628814));
#190067=CARTESIAN_POINT('Ctrl Pts',(-185.65154780146,-0.378559253454916,
136.60336151315));
#190068=CARTESIAN_POINT('Ctrl Pts',(-185.929995425273,4.67424316637891,
134.257354871388));
#190069=CARTESIAN_POINT('Ctrl Pts',(-186.208443049086,5.4316444657843,128.73821519851));
#190070=CARTESIAN_POINT('Ctrl Pts',(-186.486890672899,1.19762985171755,
125.117762228929));
#190071=CARTESIAN_POINT('Ctrl Pts',(-186.765338296712,-4.13694808860639,
126.72301537273));
#190072=CARTESIAN_POINT('Ctrl Pts',(-187.043785920525,-5.66987283665109,
132.078825411735));
#190073=CARTESIAN_POINT('Ctrl Pts',(-187.322233544337,-1.99246143649967,
136.263464565965));
#190074=CARTESIAN_POINT('Ctrl Pts',(-187.600681168151,3.51592468664221,
135.43145388367));
#190075=CARTESIAN_POINT('Ctrl Pts',(-187.879128791963,5.79334778522967,
130.347370535898));
#190076=CARTESIAN_POINT('Ctrl Pts',(-188.157576415776,2.74696728996466,
125.683238747971));
#190077=CARTESIAN_POINT('Ctrl Pts',(-188.436024039589,-2.82374194796541,
125.72516777749));
#190078=CARTESIAN_POINT('Ctrl Pts',(-188.714471663402,-5.79957028317828,
130.434626894674));
#190079=CARTESIAN_POINT('Ctrl Pts',(-188.992919287215,-3.44587685290989,
135.483853240698));
#190080=CARTESIAN_POINT('Ctrl Pts',(-189.271366911028,2.07440906473995,
136.232854471987));
#190081=CARTESIAN_POINT('Ctrl Pts',(-189.54981453484,5.68841439241029,131.993335047731));
#190082=CARTESIAN_POINT('Ctrl Pts',(-189.828262158654,4.07504478794802,
126.661206206783));
#190083=CARTESIAN_POINT('Ctrl Pts',(-190.106709782466,-1.28309189963338,
125.136433864998));
#190084=CARTESIAN_POINT('Ctrl Pts',(-190.385157406279,-5.46212981397553,
128.820209315208));
#190085=CARTESIAN_POINT('Ctrl Pts',(-190.663605030092,-4.62173726915045,
134.327322881104));
#190086=CARTESIAN_POINT('Ctrl Pts',(-190.942052653905,0.465806041606811,
136.597006233083));
#190087=CARTESIAN_POINT('Ctrl Pts',(-191.220500277718,5.12529635601715,
133.543531250871));
#190088=CARTESIAN_POINT('Ctrl Pts',(-191.49894790153,5.07488970389458,127.972892272577));
#190089=CARTESIAN_POINT('Ctrl Pts',(-191.777395525344,0.360907336037817,
125.004234378408));
#190090=CARTESIAN_POINT('Ctrl Pts',(-192.055843149156,-4.68473124233415,
127.365609146106));
#190091=CARTESIAN_POINT('Ctrl Pts',(-192.33429077297,-5.42533067084548,
132.887028523726));
#190092=CARTESIAN_POINT('Ctrl Pts',(-192.612738396782,-1.1803162549878,
136.494577839569));
#190093=CARTESIAN_POINT('Ctrl Pts',(-192.891186020595,4.14935113754904,
134.873095510955));
#190094=CARTESIAN_POINT('Ctrl Pts',(-193.169633644408,5.66596754175055,
129.512644584067));
#190095=CARTESIAN_POINT('Ctrl Pts',(-193.448081268221,1.97583657298603,
125.339217588127));
#190096=CARTESIAN_POINT('Ctrl Pts',(-193.726528892034,-3.52999168137001,
126.187990049162));
#190097=CARTESIAN_POINT('Ctrl Pts',(-194.004976515847,-5.79193003022761,
131.27898154032));
#190098=CARTESIAN_POINT('Ctrl Pts',(-194.28342413966,-2.73136763281852,
135.933819589987));
#190099=CARTESIAN_POINT('Ctrl Pts',(-194.561871763472,2.83918818442447,
135.874935432001));
#190100=CARTESIAN_POINT('Ctrl Pts',(-194.840319387286,5.80066876223446,
131.156440730899));
#190101=CARTESIAN_POINT('Ctrl Pts',(-195.118767011098,3.43161812597426,
126.114401605713));
#190102=CARTESIAN_POINT('Ctrl Pts',(-195.397214634911,-2.09092192419104,
125.382205695184));
#190103=CARTESIAN_POINT('Ctrl Pts',(-195.675662258724,-5.69200687323938,
129.63270527133));
#190104=CARTESIAN_POINT('Ctrl Pts',(-195.954109882537,-4.06241557577554,
134.95989887212));
#190105=CARTESIAN_POINT('Ctrl Pts',(-196.23255750635,1.30033717579212,136.468355826305));
#190106=CARTESIAN_POINT('Ctrl Pts',(-196.511005130163,5.46814358780935,
132.771877885207));
#190107=CARTESIAN_POINT('Ctrl Pts',(-196.789452753976,4.61099317629508,
127.267347693709));
#190108=CARTESIAN_POINT('Ctrl Pts',(-197.067900377789,-0.483434704694746,
125.013159586548));
#190109=CARTESIAN_POINT('Ctrl Pts',(-197.346348001602,-5.13360970916836,
128.080802310993));
#190110=CARTESIAN_POINT('Ctrl Pts',(-197.624795625414,-5.06624818169292,
133.651262065958));
#190111=CARTESIAN_POINT('Ctrl Pts',(-197.903243249227,-0.343252075224855,
136.605558468718));
#190112=CARTESIAN_POINT('Ctrl Pts',(-198.18169087304,4.69517591957924,134.228837450539));
#190113=CARTESIAN_POINT('Ctrl Pts',(-198.460138496853,5.41896661638458,
128.705189517851));
#190114=CARTESIAN_POINT('Ctrl Pts',(-198.738586120666,1.1629917239694,125.110577275591));
#190115=CARTESIAN_POINT('Ctrl Pts',(-199.017033744479,-4.16171574746965,
126.748273767825));
#190116=CARTESIAN_POINT('Ctrl Pts',(-199.295481368292,-5.6620097581009,
132.113315924113));
#190117=CARTESIAN_POINT('Ctrl Pts',(-199.573928992105,-1.95919340559182,
136.275492099704));
#190118=CARTESIAN_POINT('Ctrl Pts',(-199.852376615917,3.54402597473752,
135.409965722843));
#190119=CARTESIAN_POINT('Ctrl Pts',(-200.13082423973,5.79045861957696,130.312113250549));
#190120=CARTESIAN_POINT('Ctrl Pts',(-200.409271863544,2.71574267265526,
125.666612060922));
#190121=CARTESIAN_POINT('Ctrl Pts',(-200.687719487356,-2.85460811903155,
125.742450801881));
#190122=CARTESIAN_POINT('Ctrl Pts',(-200.966167111169,-5.80171350468764,
130.469937375411));
#190123=CARTESIAN_POINT('Ctrl Pts',(-201.244614734982,-3.41732760899753,
135.504742570997));
#190124=CARTESIAN_POINT('Ctrl Pts',(-201.523062358795,2.10741541362659,
136.220126377805));
#190125=CARTESIAN_POINT('Ctrl Pts',(-201.801509982608,5.69554662409457,
131.958686025817));
#190126=CARTESIAN_POINT('Ctrl Pts',(-202.079957606421,4.04974872994014,
126.636477015578));
#190127=CARTESIAN_POINT('Ctrl Pts',(-202.358405230234,-1.31757040580477,
125.144349423131));
#190128=CARTESIAN_POINT('Ctrl Pts',(-202.636852854047,-5.47410670550813,
128.853495611451));
#190129=CARTESIAN_POINT('Ctrl Pts',(-202.915300477859,-4.6002063678289,
134.355391435336));
#190130=CARTESIAN_POINT('Ctrl Pts',(-203.193748101672,0.501058889310003,
136.594063415189));
#190131=CARTESIAN_POINT('Ctrl Pts',(-203.472195725485,5.14187550526088,
133.512281366733));
#190132=CARTESIAN_POINT('Ctrl Pts',(-203.750643349298,5.05755972645996,
127.942052439074));
#190133=CARTESIAN_POINT('Ctrl Pts',(-204.029090973111,0.325593634571106,
125.002144895921));
#190134=CARTESIAN_POINT('Ctrl Pts',(-204.307538596924,-4.70557710135553,
127.394190146963));
#190135=CARTESIAN_POINT('Ctrl Pts',(-204.585986220737,-5.41255236135747,
132.920015464399));
#190136=CARTESIAN_POINT('Ctrl Pts',(-204.864433844549,-1.14565641915494,
136.50165733308));
#190137=CARTESIAN_POINT('Ctrl Pts',(-205.142881468362,4.17404180382362,
134.847761848621));
#190138=CARTESIAN_POINT('Ctrl Pts',(-205.421329092175,5.6579995223666,129.478178163952));
#190139=CARTESIAN_POINT('Ctrl Pts',(-205.699776715988,1.94253208849746,
125.327291366541));
#190140=CARTESIAN_POINT('Ctrl Pts',(-205.978224339801,-3.55802743673226,
126.209563641112));
#190141=CARTESIAN_POINT('Ctrl Pts',(-206.256671963614,-5.78893356690891,
131.314229868733));
#190142=CARTESIAN_POINT('Ctrl Pts',(-206.535119587427,-2.70009255422283,
135.950351163029));
#190143=CARTESIAN_POINT('Ctrl Pts',(-206.81356721124,2.87000160893922,135.857558541658));
#190144=CARTESIAN_POINT('Ctrl Pts',(-207.092014835053,5.80270450085972,
131.121123890489));
#190145=CARTESIAN_POINT('Ctrl Pts',(-207.370462458865,3.40300543436423,
126.09359926625));
#190146=CARTESIAN_POINT('Ctrl Pts',(-207.648910082679,-2.12388938025395,
125.395034190384));
#190147=CARTESIAN_POINT('Ctrl Pts',(-207.927357706491,-5.69903361218359,
129.667375840811));
#190148=CARTESIAN_POINT('Ctrl Pts',(-208.205805330304,-4.03704436778601,
134.984550956282));
#190149=CARTESIAN_POINT('Ctrl Pts',(-208.484252954117,1.33479143002538,
136.460335364123));
#190150=CARTESIAN_POINT('Ctrl Pts',(-208.76270057793,5.48001911182977,132.738555289606));
#190151=CARTESIAN_POINT('Ctrl Pts',(-209.041148201743,4.58937694367963,
127.239344802146));
#190152=CARTESIAN_POINT('Ctrl Pts',(-209.319595825556,-0.518678432184342,
125.016209688352));
#190153=CARTESIAN_POINT('Ctrl Pts',(-209.598043449369,-5.15009366772074,
128.112102511612));
#190154=CARTESIAN_POINT('Ctrl Pts',(-209.876491073182,-5.04882441868487,
133.682049010123));
#190155=CARTESIAN_POINT('Ctrl Pts',(-210.154938696994,-0.307932177662294,
136.607540458767));
#190156=CARTESIAN_POINT('Ctrl Pts',(-210.433386320807,4.71593469130848,
134.200193134443));
#190157=CARTESIAN_POINT('Ctrl Pts',(-210.71183394462,5.40608796518471,128.672241622749));
#190158=CARTESIAN_POINT('Ctrl Pts',(-210.990281568433,1.12831050113542,
125.103603307488));
#190159=CARTESIAN_POINT('Ctrl Pts',(-211.268729192246,-4.18632919242468,
126.773682462711));
#190160=CARTESIAN_POINT('Ctrl Pts',(-211.547176816059,-5.65393687169752,
132.14775793267));
#190161=CARTESIAN_POINT('Ctrl Pts',(-211.825624439872,-1.92585277605142,
136.287316898656));
#190162=CARTESIAN_POINT('Ctrl Pts',(-212.104072063685,3.57199593764717,
135.388306899624));
#190163=CARTESIAN_POINT('Ctrl Pts',(-212.382519687498,5.78735488635066,
130.276874205606));
#190164=CARTESIAN_POINT('Ctrl Pts',(-212.660967311311,2.68441742250212,
125.650175755035));
#190165=CARTESIAN_POINT('Ctrl Pts',(-212.939414935123,-2.88536851154432,
125.759921397201));
#190166=CARTESIAN_POINT('Ctrl Pts',(-213.217862558936,-5.80364174156953,
130.505260248325));
#190167=CARTESIAN_POINT('Ctrl Pts',(-213.496310182749,-3.38865173475374,
135.525457726916));
#190168=CARTESIAN_POINT('Ctrl Pts',(-213.774757806562,2.14034367146046,
136.20719760043));
#190169=CARTESIAN_POINT('Ctrl Pts',(-214.053205430375,5.7024678052036,131.923994229952));
#190170=CARTESIAN_POINT('Ctrl Pts',(-214.331653054188,4.02430260700449,
126.611902266833));
#190171=CARTESIAN_POINT('Ctrl Pts',(-214.610100678001,-1.35200008892003,
125.152474715061));
#190172=CARTESIAN_POINT('Ctrl Pts',(-214.888548301814,-5.48588075200302,
128.886854197714));
#190173=CARTESIAN_POINT('Ctrl Pts',(-215.166995925626,-4.5785050041694,
134.383328404815));
#190174=CARTESIAN_POINT('Ctrl Pts',(-215.445443549439,0.536293170092427,
136.59090605773));
#190175=CARTESIAN_POINT('Ctrl Pts',(-215.723891173253,5.15826412041666,
133.480931139593));
#190176=CARTESIAN_POINT('Ctrl Pts',(-216.002338797065,5.04004233928969,
127.911318669453));
#190177=CARTESIAN_POINT('Ctrl Pts',(-216.280786420879,0.290267868112,125.000270416672));
#190178=CARTESIAN_POINT('Ctrl Pts',(-216.559234044691,-4.72624859348692,
127.422897512942));
#190179=CARTESIAN_POINT('Ctrl Pts',(-216.837681668504,-5.39957348775117,
132.952924008705));
#190180=CARTESIAN_POINT('Ctrl Pts',(-217.116129292317,-1.11095413060172,
136.508525711168));
#190181=CARTESIAN_POINT('Ctrl Pts',(-217.39457691613,4.19857779944424,134.822278356567));
#190182=CARTESIAN_POINT('Ctrl Pts',(-217.673024539943,5.64982184372931,
129.443760886018));
#190183=CARTESIAN_POINT('Ctrl Pts',(-217.951472163756,1.90915562276867,
125.315568099769));
#190184=CARTESIAN_POINT('Ctrl Pts',(-218.229919787568,-3.58593134807924,
126.231307494954));
#190185=CARTESIAN_POINT('Ctrl Pts',(-218.508367411381,-5.78572259252759,
131.349459303753));
#190186=CARTESIAN_POINT('Ctrl Pts',(-218.786815035194,-2.66871742270537,
135.966692049498));
#190187=CARTESIAN_POINT('Ctrl Pts',(-219.065262659007,2.90070868448967,
135.839994403207));
#190188=CARTESIAN_POINT('Ctrl Pts',(-219.34371028282,5.80452521813531,131.085795312298));
#190189=CARTESIAN_POINT('Ctrl Pts',(-219.622157906633,3.37426664313623,
126.07297148578));
#190190=CARTESIAN_POINT('Ctrl Pts',(-219.900605530446,-2.15677813481551,
125.408063130162));
#190191=CARTESIAN_POINT('Ctrl Pts',(-220.179053154259,-5.70584917134113,
129.702088541682));
#190192=CARTESIAN_POINT('Ctrl Pts',(-220.457500778071,-4.01152356563293,
135.009048141953));
#190193=CARTESIAN_POINT('Ctrl Pts',(-220.735948401884,1.36919622307095,
136.452105317718));
#190194=CARTESIAN_POINT('Ctrl Pts',(-221.014396025697,5.49169157172664,
132.705161021709));
#190195=CARTESIAN_POINT('Ctrl Pts',(-221.29284364951,4.56759065001379,127.211474013555));
#190196=CARTESIAN_POINT('Ctrl Pts',(-221.571291273323,-0.553902939853376,
125.019474272218));
#190197=CARTESIAN_POINT('Ctrl Pts',(-221.849738897136,-5.16638678765824,
128.143502474846));
#190198=CARTESIAN_POINT('Ctrl Pts',(-222.128186520948,-5.03121356963114,
133.712729320486));
#190199=CARTESIAN_POINT('Ctrl Pts',(-222.406634144762,-0.272600869560251,
136.609307409853));
#190200=CARTESIAN_POINT('Ctrl Pts',(-222.685081768574,4.73651871234416,
134.171422984523));
#190201=CARTESIAN_POINT('Ctrl Pts',(-222.963529392388,5.39300898940659,
128.639372734101));
#190202=CARTESIAN_POINT('Ctrl Pts',(-223.2419770162,1.09358746834067,125.096840583045));
#190203=CARTESIAN_POINT('Ctrl Pts',(-223.520424640014,-4.21078751141269,
126.799240515859));
#190204=CARTESIAN_POINT('Ctrl Pts',(-223.798872263826,-5.64565447658353,
132.182150161146));
#190205=CARTESIAN_POINT('Ctrl Pts',(-224.077319887639,-1.89244078332859,
136.298938524645));
#190206=CARTESIAN_POINT('Ctrl Pts',(-224.355767511452,3.59983353893359,
135.366478216591));
#190207=CARTESIAN_POINT('Ctrl Pts',(-224.634215135265,5.78403670056078,
130.241654706868));
#190208=CARTESIAN_POINT('Ctrl Pts',(-224.912662759078,2.65299270027449,
125.633930439363));
#190209=CARTESIAN_POINT('Ctrl Pts',(-225.191110382891,-2.91602198566553,
125.77757891607));
#190210=CARTESIAN_POINT('Ctrl Pts',(-225.469558006704,-5.8053549223724,
130.540594204513));
#190211=CARTESIAN_POINT('Ctrl Pts',(-225.748005630516,-3.35985029277391,
135.545997940844));
#190212=CARTESIAN_POINT('Ctrl Pts',(-226.026453254329,2.17319261807209,
136.194068618944));
#190213=CARTESIAN_POINT('Ctrl Pts',(-226.304900878142,5.7091776792716,131.88926094565));
#190214=CARTESIAN_POINT('Ctrl Pts',(-226.583348501955,3.99870736205508,
126.587482871174));
#190215=CARTESIAN_POINT('Ctrl Pts',(-226.861796125768,-1.38637967317499,
125.160809439701));
#190216=CARTESIAN_POINT('Ctrl Pts',(-227.140243749581,-5.49745151716988,
128.920283837883));
#190217=CARTESIAN_POINT('Ctrl Pts',(-227.418691373394,-4.55663398232247,
134.411132754326));
#190218=CARTESIAN_POINT('Ctrl Pts',(-227.697138997207,0.571507578333558,
136.5875342777));
#190219=CARTESIAN_POINT('Ctrl Pts',(-227.97558662102,5.17446159419872,133.44948173115));
#190220=CARTESIAN_POINT('Ctrl Pts',(-228.254034244832,5.02233819149715,
127.880692102567));
#190221=CARTESIAN_POINT('Ctrl Pts',(-228.532481868645,0.254931345670833,
124.998611010119));
#190222=CARTESIAN_POINT('Ctrl Pts',(-228.810929492458,-4.74674495273865,
127.451730180279));
#190223=CARTESIAN_POINT('Ctrl Pts',(-229.089377116271,-5.38639453096373,
132.985752937203));
#190224=CARTESIAN_POINT('Ctrl Pts',(-229.367824740084,-1.07621067523457,
136.515182719319));
#190225=CARTESIAN_POINT('Ctrl Pts',(-229.646272363897,4.22295821522052,
134.796645979094));
#190226=CARTESIAN_POINT('Ctrl Pts',(-229.92471998771,5.64143480886619,129.409394025606));
#190227=CARTESIAN_POINT('Ctrl Pts',(-230.203167611523,1.87570841257552,
125.304048222223));
#190228=CARTESIAN_POINT('Ctrl Pts',(-230.481615235336,-3.61370238142155,
126.25322080496));
#190229=CARTESIAN_POINT('Ctrl Pts',(-230.760062859148,-5.78229722606833,
131.384668539942));
#190230=CARTESIAN_POINT('Ctrl Pts',(-231.038510482961,-2.63724340088164,
135.982841643878));
#190231=CARTESIAN_POINT('Ctrl Pts',(-231.316958106774,2.93130827321233,
135.822243667495));
#190232=CARTESIAN_POINT('Ctrl Pts',(-231.595405730587,5.80613084659478,
131.050456305442));
#190233=CARTESIAN_POINT('Ctrl Pts',(-231.8738533544,3.34540281721704,126.052519028673));
#190234=CARTESIAN_POINT('Ctrl Pts',(-232.152300978213,-2.18958696916944,
125.42129203173));
#190235=CARTESIAN_POINT('Ctrl Pts',(-232.430748602025,-5.71245329815966,
129.736842087648));
#190236=CARTESIAN_POINT('Ctrl Pts',(-232.709196225839,-3.98585411499877,
135.033389521383));
#190237=CARTESIAN_POINT('Ctrl Pts',(-232.987643849651,1.40355028004735,
136.443665992055));
#190238=CARTESIAN_POINT('Ctrl Pts',(-233.266091473464,5.50316053497282,
132.671696318956));
#190239=CARTESIAN_POINT('Ctrl Pts',(-233.544539097277,4.5456351025967,127.183736360699));
#190240=CARTESIAN_POINT('Ctrl Pts',(-233.82298672109,-0.589106922445798,
125.022953217175));
#190241=CARTESIAN_POINT('Ctrl Pts',(-234.101434344904,-5.18248846523346,
128.175001037157));
#190242=CARTESIAN_POINT('Ctrl Pts',(-234.379881968716,-5.01341628710851,
133.743301860178));
#190243=CARTESIAN_POINT('Ctrl Pts',(-234.658329592529,-0.237259460132118,
136.610859256499));
#190244=CARTESIAN_POINT('Ctrl Pts',(-234.936777216342,4.75692721993639,
134.14252806687));
#190245=CARTESIAN_POINT('Ctrl Pts',(-235.215224840155,5.37973017369771,
128.606584069875));
#190246=CARTESIAN_POINT('Ctrl Pts',(-235.493672463967,1.05882391226032,
125.090289352854));
#190247=CARTESIAN_POINT('Ctrl Pts',(-235.772120087781,-4.23508979812022,
126.824946980203));
#190248=CARTESIAN_POINT('Ctrl Pts',(-236.050567711593,-5.63716287966734,
132.216491335124));
#190249=CARTESIAN_POINT('Ctrl Pts',(-236.329015335406,-1.85895866551617,
136.310356547029));
#190250=CARTESIAN_POINT('Ctrl Pts',(-236.607462959219,3.62753774706455,
135.344480482612));
#190251=CARTESIAN_POINT('Ctrl Pts',(-236.885910583032,5.78050418516386,
130.206456059403));
#190252=CARTESIAN_POINT('Ctrl Pts',(-237.164358206845,2.62146967042642,
125.617876715884));
#190253=CARTESIAN_POINT('Ctrl Pts',(-237.442805830658,-2.94656740551997,
125.795422704185));
#190254=CARTESIAN_POINT('Ctrl Pts',(-237.72125345447,-5.80685298361372,
130.575937934662));
#190255=CARTESIAN_POINT('Ctrl Pts',(-237.999701078284,-3.33092435030571,
135.566362451659));
#190256=CARTESIAN_POINT('Ctrl Pts',(-238.278148702096,2.20596103623244,
136.180739919846));
#190257=CARTESIAN_POINT('Ctrl Pts',(-238.55659632591,5.7156759976606,131.854487459968));
#190258=CARTESIAN_POINT('Ctrl Pts',(-238.835043949722,3.97296394353457,
126.56321973347));
#190259=CARTESIAN_POINT('Ctrl Pts',(-239.113491573535,-1.42070788462113,
125.169353288205));
#190260=CARTESIAN_POINT('Ctrl Pts',(-239.391939197348,-5.50881857224844,
128.95378329321));
#190261=CARTESIAN_POINT('Ctrl Pts',(-239.670386821161,-4.53459411272838,
134.438803453569));
#190262=CARTESIAN_POINT('Ctrl Pts',(-239.948834444974,0.606700809151854,
136.583948200045));
#190263=CARTESIAN_POINT('Ctrl Pts',(-240.227282068787,5.1904673264033,133.417934306771));
#190264=CARTESIAN_POINT('Ctrl Pts',(-240.5057296926,5.00444793911587,127.850173873291));
#190265=CARTESIAN_POINT('Ctrl Pts',(-240.784177316413,0.21958537665436,
124.997166737753));
#190266=CARTESIAN_POINT('Ctrl Pts',(-241.062624940225,-4.76706541961049,
127.48068708057));
#190267=CARTESIAN_POINT('Ctrl Pts',(-241.341072564039,-5.37301597934592,
133.018501033406));
#190268=CARTESIAN_POINT('Ctrl Pts',(-241.619520187851,-1.04142734048567,
136.521628110858));
#190269=CARTESIAN_POINT('Ctrl Pts',(-241.897967811664,4.24718214772698,
134.770865666018));
#190270=CARTESIAN_POINT('Ctrl Pts',(-242.176415435477,5.63283872856131,
129.375078856195));
#190271=CARTESIAN_POINT('Ctrl Pts',(-242.45486305929,1.84219169731802,125.292732160775));
#190272=CARTESIAN_POINT('Ctrl Pts',(-242.733310683103,-3.64133950769301,
126.275302759127));
#190273=CARTESIAN_POINT('Ctrl Pts',(-243.011758306915,-5.77865759445851,
131.419856272607));
#190274=CARTESIAN_POINT('Ctrl Pts',(-243.290205930729,-2.60567165503458,
135.998799347738));
#190275=CARTESIAN_POINT('Ctrl Pts',(-243.568653554541,2.96179924122969,
135.80430699228));
#190276=CARTESIAN_POINT('Ctrl Pts',(-243.847101178355,5.80752132674009,
131.015108179419));
#190277=CARTESIAN_POINT('Ctrl Pts',(-244.125548802166,3.31641502616601,
126.032242652805));
#190278=CARTESIAN_POINT('Ctrl Pts',(-244.403996425981,-2.22231466757369,
125.434720404883));
#190279=CARTESIAN_POINT('Ctrl Pts',(-244.682444049792,-5.71884574792013,
129.771635190908));
#190280=CARTESIAN_POINT('Ctrl Pts',(-244.960891673606,-3.96003696707471,
135.05757419259));
#190281=CARTESIAN_POINT('Ctrl Pts',(-245.239339297418,1.43785232795156,
136.435017699859));
#190282=CARTESIAN_POINT('Ctrl Pts',(-245.517786921232,5.51442557658153,
132.638162421391));
#190283=CARTESIAN_POINT('Ctrl Pts',(-245.796234545044,4.52351111499922,
127.156132871406));
#190284=CARTESIAN_POINT('Ctrl Pts',(-246.074682168857,-0.624289075464052,
125.026646394309));
#190285=CARTESIAN_POINT('Ctrl Pts',(-246.353129792671,-5.19839810379266,
128.206597031353));
#190286=CARTESIAN_POINT('Ctrl Pts',(-246.631577416483,-4.99543323060155,
133.773765496319));
#190287=CARTESIAN_POINT('Ctrl Pts',(-246.910025040296,-0.201909258968066,
136.612195941205));
#190288=CARTESIAN_POINT('Ctrl Pts',(-247.188472664109,4.77715945784187,
134.113509452194));
#190289=CARTESIAN_POINT('Ctrl Pts',(-247.466920287922,5.36625201010822,
128.573876845067));
#190290=CARTESIAN_POINT('Ctrl Pts',(-247.745367911734,1.02402112107033,
125.083949859676));
#190291=CARTESIAN_POINT('Ctrl Pts',(-248.023815535548,-4.25923515201858,
126.850800903184));
#190292=CARTESIAN_POINT('Ctrl Pts',(-248.30226315936,-5.62846239560694,
132.250780182078));
#190293=CARTESIAN_POINT('Ctrl Pts',(-248.580710783174,-1.82540766330725,
136.32157054271));
#190294=CARTESIAN_POINT('Ctrl Pts',(-248.859158406986,3.65510753545023,
135.322314512822));
#190295=CARTESIAN_POINT('Ctrl Pts',(-249.137606030799,5.7767574710584,130.171279567513));
#190296=CARTESIAN_POINT('Ctrl Pts',(-249.416053654612,2.58984950105633,
125.602015179472));
#190297=CARTESIAN_POINT('Ctrl Pts',(-249.694501278425,-2.97700363923603,
125.813452100338));
#190298=CARTESIAN_POINT('Ctrl Pts',(-249.972948902238,-5.80813586978118,
130.611290129096));
#190299=CARTESIAN_POINT('Ctrl Pts',(-250.251396526051,-3.30187497921299,
135.586550504748));
#190300=CARTESIAN_POINT('Ctrl Pts',(-250.529844149864,2.23864771169993,
136.167211997028));
#190301=CARTESIAN_POINT('Ctrl Pts',(-250.808291773676,5.72196251956533,
131.819675061465));
#190302=CARTESIAN_POINT('Ctrl Pts',(-251.08673939749,3.94707330538994,126.539113752772));
#190303=CARTESIAN_POINT('Ctrl Pts',(-251.365187021302,-1.45498345124562,
125.178105944033));
#190304=CARTESIAN_POINT('Ctrl Pts',(-251.643634645115,-5.5199814959705,
128.987351322257));
#190305=CARTESIAN_POINT('Ctrl Pts',(-251.922082268928,-4.51238621219265,
134.466339477392));
#190306=CARTESIAN_POINT('Ctrl Pts',(-252.200529892741,0.641871558658502,
136.580147957277));
#190307=CARTESIAN_POINT('Ctrl Pts',(-252.478977516554,5.20628072353487,
133.386290036154));
#190308=CARTESIAN_POINT('Ctrl Pts',(-252.757425140367,4.98637224582674,
127.819765111179));
#190309=CARTESIAN_POINT('Ctrl Pts',(-253.035872764179,0.184231269403876,
124.995937655572));
#190310=CARTESIAN_POINT('Ctrl Pts',(-253.314320387993,-4.78720923844335,
127.509767136124));
#190311=CARTESIAN_POINT('Ctrl Pts',(-253.592768011806,-5.35943833369967,
133.051167092665));
#190312=CARTESIAN_POINT('Ctrl Pts',(-253.871215635618,-1.00660540571931,
136.527861630253));
#190313=CARTESIAN_POINT('Ctrl Pts',(-254.149663259431,4.27124868131666,
134.744938404161));
#190314=CARTESIAN_POINT('Ctrl Pts',(-254.428110883244,5.62403395537261,
129.340816589823));
#190315=CARTESIAN_POINT('Ctrl Pts',(-254.706558507057,1.80860665472018,
125.281620447135));
#190316=CARTESIAN_POINT('Ctrl Pts',(-254.98500613087,-3.66884158147516,
126.297552326988));
#190317=CARTESIAN_POINT('Ctrl Pts',(-255.263453754682,-5.77480406163408,
131.45502159855));
#190318=CARTESIAN_POINT('Ctrl Pts',(-255.541901378496,-2.57400292253984,
136.014563813166));
#190319=CARTESIAN_POINT('Ctrl Pts',(-255.820349002309,2.99217964199006,
135.78618647082));
#190320=CARTESIAN_POINT('Ctrl Pts',(-256.098796626121,5.80869814913581,
130.979749546569));
#190321=CARTESIAN_POINT('Ctrl Pts',(-256.377244249934,3.28730143236016,
126.01214820295));
#190322=CARTESIAN_POINT('Ctrl Pts',(-256.655691873747,-2.25495451926359,
125.448338134603));
#190323=CARTESIAN_POINT('Ctrl Pts',(-256.93413949756,-5.72503666514098,
129.806484721847));
#190324=CARTESIAN_POINT('Ctrl Pts',(-257.212587121373,-3.93405347634203,
135.081566970265));
#190325=CARTESIAN_POINT('Ctrl Pts',(-257.491034745186,1.47206408278265,
136.426225506557));
#190326=CARTESIAN_POINT('Ctrl Pts',(-257.769482368999,5.52555616721843,
132.604438319186));
#190327=CARTESIAN_POINT('Ctrl Pts',(-258.047929992812,4.50108754276566,
127.128895412351));
#190328=CARTESIAN_POINT('Ctrl Pts',(-258.326377616624,-0.659198908970111,
125.030117734768));
#190329=CARTESIAN_POINT('Ctrl Pts',(-258.604825240438,-5.21458571703409,
128.239112839452));
#190330=CARTESIAN_POINT('Ctrl Pts',(-258.883272864251,-4.97637574492231,
133.802560593787));
#190331=CARTESIAN_POINT('Ctrl Pts',(-259.161720488063,-0.168236736403017,
136.616288572087));
#190332=CARTESIAN_POINT('Ctrl Pts',(-259.440168111876,4.80044487344316,
134.078525892203));
#190333=CARTESIAN_POINT('Ctrl Pts',(-259.672207798387,5.25516631655033,
129.4749169549));
#190334=CARTESIAN_POINT('Ctrl Pts',(-259.857849473896,3.17366342871357,
126.795179433485));
#190335=CARTESIAN_POINT('Ctrl Pts',(-259.9506752748,1.64266665146648,126.102093112095));
#190336=CARTESIAN_POINT('Ctrl Pts',(-259.997093138402,0.835778587061721,
125.962806053044));
#190337=CARTESIAN_POINT('Ctrl Pts',(210.385579563201,-2.29217962691353,
126.082387726892));
#190338=CARTESIAN_POINT('Ctrl Pts',(210.339169886847,-3.0789974560272,126.464330840008));
#190339=CARTESIAN_POINT('Ctrl Pts',(210.246352273192,-4.44507089109247,
127.629120819077));
#190340=CARTESIAN_POINT('Ctrl Pts',(210.060718784933,-5.78798125627161,
130.996088365878));
#190341=CARTESIAN_POINT('Ctrl Pts',(209.828679098422,-3.95783017776954,
135.586872998689));
#190342=CARTESIAN_POINT('Ctrl Pts',(209.550231474609,1.89393692750204,136.720289837399));
#190343=CARTESIAN_POINT('Ctrl Pts',(209.271783850796,5.99602695027556,132.40812259401));
#190344=CARTESIAN_POINT('Ctrl Pts',(208.993336226983,4.59288360023261,126.626877830413));
#190345=CARTESIAN_POINT('Ctrl Pts',(208.71488860317,-1.03344059257722,124.682062423228));
#190346=CARTESIAN_POINT('Ctrl Pts',(208.436440979357,-5.70873650289865,
128.364647771496));
#190347=CARTESIAN_POINT('Ctrl Pts',(208.157993355544,-5.13869562717284,
134.288517668348));
#190348=CARTESIAN_POINT('Ctrl Pts',(207.879545731732,0.153933173725622,
137.010984097728));
#190349=CARTESIAN_POINT('Ctrl Pts',(207.601098107919,5.30490488755997,134.029672582798));
#190350=CARTESIAN_POINT('Ctrl Pts',(207.322650484106,5.58103410012833,128.084559773234));
#190351=CARTESIAN_POINT('Ctrl Pts',(207.044202860293,0.728409521696789,
124.638756607567));
#190352=CARTESIAN_POINT('Ctrl Pts',(206.76575523648,-4.79355811073501,126.858871164077));
#190353=CARTESIAN_POINT('Ctrl Pts',(206.487307612667,-5.91049575314416,
132.704682504842));
#190354=CARTESIAN_POINT('Ctrl Pts',(206.208859988854,-1.59596820864792,
136.804198957117));
#190355=CARTESIAN_POINT('Ctrl Pts',(205.930412365042,4.1851717387407,135.390152799229));
#190356=CARTESIAN_POINT('Ctrl Pts',(205.651964741228,6.12034565262566,129.76198992389));
#190357=CARTESIAN_POINT('Ctrl Pts',(205.373517117416,2.43121966936229,125.091713591677));
#190358=CARTESIAN_POINT('Ctrl Pts',(205.095069493603,-3.49207776276838,
125.671081434371));
#190359=CARTESIAN_POINT('Ctrl Pts',(204.81662186979,-6.20632667560231,130.96768173473));
#190360=CARTESIAN_POINT('Ctrl Pts',(204.538174245977,-3.21726438559061,
136.114198085604));
#190361=CARTESIAN_POINT('Ctrl Pts',(204.259726622164,2.72830660529182,136.381233108793));
#190362=CARTESIAN_POINT('Ctrl Pts',(203.981278998351,6.16669716267351,131.523394807979));
#190363=CARTESIAN_POINT('Ctrl Pts',(203.702831374538,3.9381942601484,126.004799186432));
#190364=CARTESIAN_POINT('Ctrl Pts',(203.424383750725,-1.909316761502,124.896766062528));
#190365=CARTESIAN_POINT('Ctrl Pts',(203.145936126912,-6.00225896230248,
129.217523725228));
#190366=CARTESIAN_POINT('Ctrl Pts',(202.867488503099,-4.57941839934143,
134.996506974633));
#190367=CARTESIAN_POINT('Ctrl Pts',(202.589040879287,1.05168395343957,136.923112517541));
#190368=CARTESIAN_POINT('Ctrl Pts',(202.310593255474,5.71634013176502,133.226883983125));
#190369=CARTESIAN_POINT('Ctrl Pts',(202.032145631661,5.12795898713612,127.30447482202));
#190370=CARTESIAN_POINT('Ctrl Pts',(201.753698007848,-0.172765951628197,
124.598289728405));
#190371=CARTESIAN_POINT('Ctrl Pts',(201.475250384035,-5.31472742110118,
127.595180598346));
#190372=CARTESIAN_POINT('Ctrl Pts',(201.196802760222,-5.57271402936141,
133.541151128878));
#190373=CARTESIAN_POINT('Ctrl Pts',(200.918355136409,-0.709648686901125,
136.972144879116));
#190374=CARTESIAN_POINT('Ctrl Pts',(200.639907512596,4.80554913058071,134.735246206027));
#190375=CARTESIAN_POINT('Ctrl Pts',(200.361459888783,5.90468206117194,128.886055711564));
#190376=CARTESIAN_POINT('Ctrl Pts',(200.083012264971,1.57770063730838,124.799693711321));
#190377=CARTESIAN_POINT('Ctrl Pts',(199.804564641158,-4.19911059728431,
126.231327253625));
#190378=CARTESIAN_POINT('Ctrl Pts',(199.526117017345,-6.11714433092778,
131.865355052293));
#190379=CARTESIAN_POINT('Ctrl Pts',(199.247669393532,-2.4138212635637,136.524380797905));
#190380=CARTESIAN_POINT('Ctrl Pts',(198.969221769719,3.50768562329156,135.926987436306));
#190381=CARTESIAN_POINT('Ctrl Pts',(198.690774145906,6.20580078231077,130.622150282517));
#190382=CARTESIAN_POINT('Ctrl Pts',(198.412326522093,3.20108819260905,125.484755525167));
#190383=CARTESIAN_POINT('Ctrl Pts',(198.13387889828,-2.74526806424844,125.235817970576));
#190384=CARTESIAN_POINT('Ctrl Pts',(197.855431274468,-6.16885708386238,
130.104099070135));
#190385=CARTESIAN_POINT('Ctrl Pts',(197.576983650655,-3.92356780882929,
135.615886322105));
#190386=CARTESIAN_POINT('Ctrl Pts',(197.298536026841,1.92728860557448,136.706116507701));
#190387=CARTESIAN_POINT('Ctrl Pts',(197.020088403029,6.00706094473797,132.372921347066));
#190388=CARTESIAN_POINT('Ctrl Pts',(196.741640779216,4.56663773692898,126.598295504472));
#190389=CARTESIAN_POINT('Ctrl Pts',(196.463193155403,-1.07030245846182,
124.688838023107));
#190390=CARTESIAN_POINT('Ctrl Pts',(196.184745531591,-5.72368698170812,
128.399247046161));
#190391=CARTESIAN_POINT('Ctrl Pts',(195.906297907777,-5.11728278641862,
134.319837945007));
#190392=CARTESIAN_POINT('Ctrl Pts',(195.627850283965,0.191654296427489,
137.009876920548));
#190393=CARTESIAN_POINT('Ctrl Pts',(195.349402660151,5.32447044368961,133.997349569974));
#190394=CARTESIAN_POINT('Ctrl Pts',(195.070955036339,5.56435836804288,128.050621358318));
#190395=CARTESIAN_POINT('Ctrl Pts',(194.792507412526,0.690872786183208,
124.634444998269));
#190396=CARTESIAN_POINT('Ctrl Pts',(194.514059788713,-4.81749113516689,
126.888119675218));
#190397=CARTESIAN_POINT('Ctrl Pts',(194.2356121649,-5.89881605082435,132.740628459178));
#190398=CARTESIAN_POINT('Ctrl Pts',(193.957164541087,-1.55941718895885,
136.81380168864));
#190399=CARTESIAN_POINT('Ctrl Pts',(193.678716917274,4.21300988779493,135.364592151301));
#190400=CARTESIAN_POINT('Ctrl Pts',(193.400269293461,6.11388669464029,129.724752614155));
#190401=CARTESIAN_POINT('Ctrl Pts',(193.121821669648,2.39640030908087,125.077020090361));
#190402=CARTESIAN_POINT('Ctrl Pts',(192.843374045836,-3.52326088986039,
125.692433714928));
#190403=CARTESIAN_POINT('Ctrl Pts',(192.564926422022,-6.20521745188322,
131.005458431507));
#190404=CARTESIAN_POINT('Ctrl Pts',(192.28647879821,-3.1848823173506,136.133684081248));
#190405=CARTESIAN_POINT('Ctrl Pts',(192.008031174397,2.76220407667619,136.36452181979));
#190406=CARTESIAN_POINT('Ctrl Pts',(191.729583550584,6.17095986540858,131.485843042463));
#190407=CARTESIAN_POINT('Ctrl Pts',(191.451135926771,3.90890500597959,125.980915208923));
#190408=CARTESIAN_POINT('Ctrl Pts',(191.172688302958,-1.94524259331895,
124.908498067517));
#190409=CARTESIAN_POINT('Ctrl Pts',(190.894240679145,-6.01180727974115,
129.254090580708));
#190410=CARTESIAN_POINT('Ctrl Pts',(190.615793055332,-4.5538147691942,135.024305522869));
#190411=CARTESIAN_POINT('Ctrl Pts',(190.337345431519,1.08891104802307,136.916597252826));
#190412=CARTESIAN_POINT('Ctrl Pts',(190.058897807707,5.73098080836918,133.192042114338));
#190413=CARTESIAN_POINT('Ctrl Pts',(189.780450183893,5.10655917980125,127.273324325042));
#190414=CARTESIAN_POINT('Ctrl Pts',(189.502002560081,-0.210540865719208,
124.599456387862));
#190415=CARTESIAN_POINT('Ctrl Pts',(189.223554936268,-5.33416414113684,
127.627592311355));
#190416=CARTESIAN_POINT('Ctrl Pts',(188.945107312455,-5.55595115925501,
133.575023114497));
#190417=CARTESIAN_POINT('Ctrl Pts',(188.666659688642,-0.672090485321342,
136.976350437346));
#190418=CARTESIAN_POINT('Ctrl Pts',(188.388212064829,4.82938851117716,134.705920634282));
#190419=CARTESIAN_POINT('Ctrl Pts',(188.109764441016,5.89289539464864,128.850147777659));
#190420=CARTESIAN_POINT('Ctrl Pts',(187.831316817203,1.54111929438253,124.790201052305));
#190421=CARTESIAN_POINT('Ctrl Pts',(187.552869193391,-4.22687014955807,
126.256973159398));
#190422=CARTESIAN_POINT('Ctrl Pts',(187.274421569578,-6.11057242014135,
131.902572188318));
#190423=CARTESIAN_POINT('Ctrl Pts',(186.995973945765,-2.37895715467313,
136.538968434335));
#190424=CARTESIAN_POINT('Ctrl Pts',(186.717526321952,3.53880351742172,135.905540247907));
#190425=CARTESIAN_POINT('Ctrl Pts',(186.439078698139,6.20457663716883,130.584377187674));
#190426=CARTESIAN_POINT('Ctrl Pts',(186.160631074326,3.16864693777749,125.465368152723));
#190427=CARTESIAN_POINT('Ctrl Pts',(185.882183450513,-2.77911450042273,
125.25263236868));
#190428=CARTESIAN_POINT('Ctrl Pts',(185.6037358267,-6.17300548002561,130.14166362836));
#190429=CARTESIAN_POINT('Ctrl Pts',(185.325288202887,-3.89420599156785,
135.639681046572));
#190430=CARTESIAN_POINT('Ctrl Pts',(185.046840579075,1.96317856060187,136.694275209062));
#190431=CARTESIAN_POINT('Ctrl Pts',(184.768392955261,6.0164979221829,132.336325600291));
#190432=CARTESIAN_POINT('Ctrl Pts',(184.489945331449,4.54094961554151,126.570575013045));
#190433=CARTESIAN_POINT('Ctrl Pts',(184.211497707636,-1.10750955006109,
124.695466564429));
#190434=CARTESIAN_POINT('Ctrl Pts',(183.933050083823,-5.73822154400692,
128.434133314579));
#190435=CARTESIAN_POINT('Ctrl Pts',(183.65460246001,-5.09578826671723,134.350923164133));
#190436=CARTESIAN_POINT('Ctrl Pts',(183.376154836197,0.229425484589131,
137.008595292604));
#190437=CARTESIAN_POINT('Ctrl Pts',(183.097707212384,5.34380842361613,133.964878848429));
#190438=CARTESIAN_POINT('Ctrl Pts',(182.819259588571,5.54749248089459,128.016800549989));
#190439=CARTESIAN_POINT('Ctrl Pts',(182.540811964758,0.653301958305029,
124.630353773773));
#190440=CARTESIAN_POINT('Ctrl Pts',(182.262364340946,-4.84124114839195,
126.917517669999));
#190441=CARTESIAN_POINT('Ctrl Pts',(181.983916717133,-5.88692014749505,
132.776500352206));
#190442=CARTESIAN_POINT('Ctrl Pts',(181.70546909332,-1.52280712308763,136.82318296266));
#190443=CARTESIAN_POINT('Ctrl Pts',(181.427021469507,4.24069125417353,135.33886187379));
#190444=CARTESIAN_POINT('Ctrl Pts',(181.148573845694,6.10720153813428,129.687555653153));
#190445=CARTESIAN_POINT('Ctrl Pts',(180.870126221881,2.36149196193127,125.062538635854));
#190446=CARTESIAN_POINT('Ctrl Pts',(180.591678598068,-3.55431336199069,
125.713975516152));
#190447=CARTESIAN_POINT('Ctrl Pts',(180.313230974255,-6.20387834410407,
131.04322762551));
#190448=CARTESIAN_POINT('Ctrl Pts',(180.034783350442,-3.15238220429199,
136.15297262387));
#190449=CARTESIAN_POINT('Ctrl Pts',(179.75633572663,2.79599917883219,136.347604482659));
#190450=CARTESIAN_POINT('Ctrl Pts',(179.477888102817,6.17499390876314,131.448266031944));
#190451=CARTESIAN_POINT('Ctrl Pts',(179.199440479004,3.8794709017638,125.957209961944));
#190452=CARTESIAN_POINT('Ctrl Pts',(178.920992855191,-1.98109634126673,
124.920448547985));
#190453=CARTESIAN_POINT('Ctrl Pts',(178.642545231378,-6.02113282860982,
129.290714880887));
#190454=CARTESIAN_POINT('Ctrl Pts',(178.364097607565,-4.52804239515191,
135.051947700091));
#190455=CARTESIAN_POINT('Ctrl Pts',(178.085649983752,1.12609779228193,136.909855496619));
#190456=CARTESIAN_POINT('Ctrl Pts',(177.807202359939,5.74540912154417,133.157111769304));
#190457=CARTESIAN_POINT('Ctrl Pts',(177.528754736127,5.08497014694685,127.242304671825));
#190458=CARTESIAN_POINT('Ctrl Pts',(177.250307112313,-0.248307978092709,
124.600852972375));
#190459=CARTESIAN_POINT('Ctrl Pts',(176.971859488501,-5.35340320178418,
127.660121740658));
#190460=CARTESIAN_POINT('Ctrl Pts',(176.693411864688,-5.53898241132168,
133.608792432211));
#190461=CARTESIAN_POINT('Ctrl Pts',(176.414964240875,-0.634507379188621,
136.980327290216));
#190462=CARTESIAN_POINT('Ctrl Pts',(176.136516617062,4.85304893701009,134.676450488799));
#190463=CARTESIAN_POINT('Ctrl Pts',(175.858068993249,5.88089036471739,128.814312257825));
#190464=CARTESIAN_POINT('Ctrl Pts',(175.579621369436,1.50448084471559,124.780931250186));
#190465=CARTESIAN_POINT('Ctrl Pts',(175.301173745623,-4.25447307360455,
126.282787570284));
#190466=CARTESIAN_POINT('Ctrl Pts',(175.02272612181,-6.10377407984646,131.939748629711));
#190467=CARTESIAN_POINT('Ctrl Pts',(174.744278497998,-2.34400489265046,
136.553343572764));
#190468=CARTESIAN_POINT('Ctrl Pts',(174.465830874185,3.56979027988629,135.883904033421));
#190469=CARTESIAN_POINT('Ctrl Pts',(174.187383250372,6.20312257915782,130.546612244398));
#190470=CARTESIAN_POINT('Ctrl Pts',(173.908935626559,3.13608826756835,125.446178618609));
#190471=CARTESIAN_POINT('Ctrl Pts',(173.630488002746,-2.81285795548731,
125.269652488117));
#190472=CARTESIAN_POINT('Ctrl Pts',(173.352040378933,-6.17692513320066,
130.179252743065));
#190473=CARTESIAN_POINT('Ctrl Pts',(173.07359275512,-3.86469987307124,135.663296596462));
#190474=CARTESIAN_POINT('Ctrl Pts',(172.795145131307,1.99899576932572,136.682215657471));
#190475=CARTESIAN_POINT('Ctrl Pts',(172.516697507494,6.02571195608475,132.29967308599));
#190476=CARTESIAN_POINT('Ctrl Pts',(172.238249883681,4.51509322759614,126.543011406101));
#190477=CARTESIAN_POINT('Ctrl Pts',(171.959802259869,-1.14467560248665,
124.702321473066));
#190478=CARTESIAN_POINT('Ctrl Pts',(171.681354636056,-5.75254347439624,
128.469107412642));
#190479=CARTESIAN_POINT('Ctrl Pts',(171.402907012243,-5.07410492070761,
134.38187696408));
#190480=CARTESIAN_POINT('Ctrl Pts',(171.12445938843,0.267188171305193,137.007083764462));
#190481=CARTESIAN_POINT('Ctrl Pts',(170.846011764617,5.36294838675633,133.932291012718));
#190482=CARTESIAN_POINT('Ctrl Pts',(170.567564140804,5.53042102937231,127.983083035723));
#190483=CARTESIAN_POINT('Ctrl Pts',(170.289116516991,0.615706922082464,
124.62649132937));
#190484=CARTESIAN_POINT('Ctrl Pts',(170.010668893178,-4.86481176764585,
126.947059693175));
#190485=CARTESIAN_POINT('Ctrl Pts',(169.732221269365,-5.87480610217478,
132.812299166869));
#190486=CARTESIAN_POINT('Ctrl Pts',(169.453773645553,-1.48614062903852,
136.832341207004));
#190487=CARTESIAN_POINT('Ctrl Pts',(169.17532602174,4.26821548017818,135.312963568669));
#190488=CARTESIAN_POINT('Ctrl Pts',(168.896878397927,6.10029007702938,129.650400075769));
#190489=CARTESIAN_POINT('Ctrl Pts',(168.618430774114,2.32649610882855,125.048269946673));
#190490=CARTESIAN_POINT('Ctrl Pts',(168.339983150301,-3.58523412773234,
125.735705943466));
#190491=CARTESIAN_POINT('Ctrl Pts',(168.061535526488,-6.2023093493314,131.08098796821));
#190492=CARTESIAN_POINT('Ctrl Pts',(167.783087902675,-3.11976527855146,
136.172062971709));
#190493=CARTESIAN_POINT('Ctrl Pts',(167.504640278862,2.82969067421049,136.330481738588));
#190494=CARTESIAN_POINT('Ctrl Pts',(167.22619265505,6.17879913544756,131.410665161273));
#190495=CARTESIAN_POINT('Ctrl Pts',(166.947745031236,3.84989304232704,125.933684327914));
#190496=CARTESIAN_POINT('Ctrl Pts',(166.669297407424,-2.01687667896098,
124.93261705898));
#190497=CARTESIAN_POINT('Ctrl Pts',(166.39084978361,-6.03023526218728,129.327395269766));
#190498=CARTESIAN_POINT('Ctrl Pts',(166.112402159798,-4.50210223283349,
135.079432481411));
#190499=CARTESIAN_POINT('Ctrl Pts',(165.833954535985,1.16324280857304,136.902887499053));
#190500=CARTESIAN_POINT('Ctrl Pts',(165.555506912173,5.75962453647134,133.122094242209));
#190501=CARTESIAN_POINT('Ctrl Pts',(165.277059288359,5.06319268865361,127.2114170119));
#190502=CARTESIAN_POINT('Ctrl Pts',(164.998611664547,-0.286065889322858,
124.602479430144));
#190503=CARTESIAN_POINT('Ctrl Pts',(164.720164040733,-5.37244389010723,
127.692767680889));
#190504=CARTESIAN_POINT('Ctrl Pts',(164.441716416921,-5.52180841435808,
133.642457830674));
#190505=CARTESIAN_POINT('Ctrl Pts',(164.163268793108,-0.596900761151562,
136.984075290369));
#190506=CARTESIAN_POINT('Ctrl Pts',(163.884821169295,4.87652953132996,134.646836861603));
#190507=CARTESIAN_POINT('Ctrl Pts',(163.606373545482,5.86866741623098,128.778550479967));
#190508=CARTESIAN_POINT('Ctrl Pts',(163.327925921669,1.46778664595768,124.771884648456));
#190509=CARTESIAN_POINT('Ctrl Pts',(163.049478297856,-4.28191834658676,
126.308769529723));
#190510=CARTESIAN_POINT('Ctrl Pts',(162.771030674043,-6.09674956195837,
131.976882998882));
#190511=CARTESIAN_POINT('Ctrl Pts',(162.49258305023,-2.30896577266445,136.567505680515));
#190512=CARTESIAN_POINT('Ctrl Pts',(162.214135426418,3.60064476245918,135.862079594585));
#190513=CARTESIAN_POINT('Ctrl Pts',(161.935687802605,6.20143866215845,130.508856852083));
#190514=CARTESIAN_POINT('Ctrl Pts',(161.657240178792,3.10341338845521,125.427187633898));
#190515=CARTESIAN_POINT('Ctrl Pts',(161.378792554979,-2.84649717906582,
125.2868776982));
#190516=CARTESIAN_POINT('Ctrl Pts',(161.100344931166,-6.18061589814333,
130.216865021372));
#190517=CARTESIAN_POINT('Ctrl Pts',(160.821897307353,-3.83505054669964,
135.686732096692));
#190518=CARTESIAN_POINT('Ctrl Pts',(160.54344968354,2.0347389045262,136.6699382998));
#190519=CARTESIAN_POINT('Ctrl Pts',(160.265002059727,6.03470270501411,132.262965162335));
#190520=CARTESIAN_POINT('Ctrl Pts',(159.986554435914,4.48906953121078,126.51560570502));
#190521=CARTESIAN_POINT('Ctrl Pts',(159.708106812101,-1.18179923853688,
124.709402495009));
#190522=CARTESIAN_POINT('Ctrl Pts',(159.429659188289,-5.76665224217155,
128.50416804437));
#190523=CARTESIAN_POINT('Ctrl Pts',(159.151211564475,-5.05223355187421,
134.412698197843));
#190524=CARTESIAN_POINT('Ctrl Pts',(158.872763940663,0.304940957265202,
137.005342392132));
#190525=CARTESIAN_POINT('Ctrl Pts',(158.59431631685,5.38188962387183,133.899587270395));
#190526=CARTESIAN_POINT('Ctrl Pts',(158.315868693037,5.51314464606502,127.949470064936));
#190527=CARTESIAN_POINT('Ctrl Pts',(158.037421069224,0.57808907061355,124.622857808186));
#190528=CARTESIAN_POINT('Ctrl Pts',(157.758973445411,-4.88820211951067,
126.976744650055));
#190529=CARTESIAN_POINT('Ctrl Pts',(157.480525821598,-5.86247436375394,
132.848023576631));
#190530=CARTESIAN_POINT('Ctrl Pts',(157.202078197785,-1.44941906550188,
136.841276082311));
#190531=CARTESIAN_POINT('Ctrl Pts',(156.923630573973,4.29558154588865,135.286898195607));
#190532=CARTESIAN_POINT('Ctrl Pts',(156.645182950159,6.09315256743229,129.613287258817));
#190533=CARTESIAN_POINT('Ctrl Pts',(156.366735326347,2.29141404655692,125.034214551549));
#190534=CARTESIAN_POINT('Ctrl Pts',(156.088287702534,-3.61602204130483,
125.757624191644));
#190535=CARTESIAN_POINT('Ctrl Pts',(155.809840078721,-6.2005105257049,131.11873806038));
#190536=CARTESIAN_POINT('Ctrl Pts',(155.531392454908,-3.08703274876129,
136.190954417361));
#190537=CARTESIAN_POINT('Ctrl Pts',(155.252944831095,2.86327731436015,136.313154222067));
#190538=CARTESIAN_POINT('Ctrl Pts',(154.974497207282,6.18237540445775,131.373041823765));
#190539=CARTESIAN_POINT('Ctrl Pts',(154.696049583469,3.82017252368788,125.910339178587));
#190540=CARTESIAN_POINT('Ctrl Pts',(154.417601959656,-2.05258228054818,
124.945003149591));
#190541=CARTESIAN_POINT('Ctrl Pts',(154.139154335844,-6.03911424317947,
129.364130388138));
#190542=CARTESIAN_POINT('Ctrl Pts',(153.860706712031,-4.47599524346119,
135.106758848372));
#190543=CARTESIAN_POINT('Ctrl Pts',(153.582259088218,1.20034472047403,136.895693518332));
#190544=CARTESIAN_POINT('Ctrl Pts',(153.303811464405,5.77362652639317,133.086990830643));
#190545=CARTESIAN_POINT('Ctrl Pts',(153.025363840592,5.04122761189337,127.180662489822));
#190546=CARTESIAN_POINT('Ctrl Pts',(152.746916216779,-0.323813200276178,
124.604335700902));
#190547=CARTESIAN_POINT('Ctrl Pts',(152.468468592966,-5.39128550054617,
127.725528922339));
#190548=CARTESIAN_POINT('Ctrl Pts',(152.190020969154,-5.5044298047531,133.6760180624));
#190549=CARTESIAN_POINT('Ctrl Pts',(151.91157334534,-0.55927202473736,136.987594298923));
#190550=CARTESIAN_POINT('Ctrl Pts',(151.633125721528,4.89982942405471,134.617080850036));
#190551=CARTESIAN_POINT('Ctrl Pts',(151.354678097715,5.85622700211526,128.742863769248));
#190552=CARTESIAN_POINT('Ctrl Pts',(151.076230473902,1.43103805782584,124.763061582343));
#190553=CARTESIAN_POINT('Ctrl Pts',(150.797782850089,-4.3092049515099,126.334918074943));
#190554=CARTESIAN_POINT('Ctrl Pts',(150.519335226276,-6.0894991267732,132.013973919806));
#190555=CARTESIAN_POINT('Ctrl Pts',(150.240887602463,-2.27384109310269,
136.581454232806));
#190556=CARTESIAN_POINT('Ctrl Pts',(149.96243997865,3.63136582181627,135.840067740113));
#190557=CARTESIAN_POINT('Ctrl Pts',(149.683992354837,6.19952494856889,130.471112409769));
#190558=CARTESIAN_POINT('Ctrl Pts',(149.405544731024,3.0706235112177,125.40839590231));
#190559=CARTESIAN_POINT('Ctrl Pts',(149.127097107212,-2.88003092464457,
125.30430736064));
#190560=CARTESIAN_POINT('Ctrl Pts',(148.848649483398,-6.18407763809098,
130.254499069545));
#190561=CARTESIAN_POINT('Ctrl Pts',(148.570201859586,-3.80525911111971,
135.709986678852));
#190562=CARTESIAN_POINT('Ctrl Pts',(148.291754235773,2.07040664172831,136.657443590992));
#190563=CARTESIAN_POINT('Ctrl Pts',(148.01330661196,6.04346983581547,132.226203189553));
#190564=CARTESIAN_POINT('Ctrl Pts',(147.734858988147,4.46287949070312,126.488358925329));
#190565=CARTESIAN_POINT('Ctrl Pts',(147.456411364334,-1.21887908258166,
124.716709367866));
#190566=CARTESIAN_POINT('Ctrl Pts',(147.177963740522,-5.78054732452736,
128.53931391058));
#190567=CARTESIAN_POINT('Ctrl Pts',(146.899516116708,-5.03017497066859,
134.44338572333));
#190568=CARTESIAN_POINT('Ctrl Pts',(146.621068492896,0.342682443525903,
137.003371240143));
#190569=CARTESIAN_POINT('Ctrl Pts',(146.342620869082,5.40063143308812,133.866768833311));
#190570=CARTESIAN_POINT('Ctrl Pts',(146.06417324527,5.49566397115542,127.915962883168));
#190571=CARTESIAN_POINT('Ctrl Pts',(145.785725621457,0.540449797841529,
124.619453344862));
#190572=CARTESIAN_POINT('Ctrl Pts',(145.507277997644,-4.91141133724831,
127.006571440652));
#190573=CARTESIAN_POINT('Ctrl Pts',(145.228830373831,-5.84992538918966,
132.883672257711));
#190574=CARTESIAN_POINT('Ctrl Pts',(144.950382750018,-1.41264379320865,
136.849987257496));
#190575=CARTESIAN_POINT('Ctrl Pts',(144.671935126205,4.32278843724517,135.260666720466));
#190576=CARTESIAN_POINT('Ctrl Pts',(144.393487502392,6.08578927382608,129.576218577526));
#190577=CARTESIAN_POINT('Ctrl Pts',(144.11503987858,2.25624707509518,125.020372971309));
#190578=CARTESIAN_POINT('Ctrl Pts',(143.836592254767,-3.64667596185081,
125.779729448496));
#190579=CARTESIAN_POINT('Ctrl Pts',(143.558144630954,-6.19848193988065,
131.156476503179));
#190580=CARTESIAN_POINT('Ctrl Pts',(143.279697007141,-3.05418582783736,
136.209646260801));
#190581=CARTESIAN_POINT('Ctrl Pts',(143.001249383328,2.89675785471595,136.295622575173));
#190582=CARTESIAN_POINT('Ctrl Pts',(142.722801759515,6.18572258327378,131.335397413564));
#190583=CARTESIAN_POINT('Ctrl Pts',(142.444354135702,3.79031044715096,125.887175379022));
#190584=CARTESIAN_POINT('Ctrl Pts',(142.165906511889,-2.0882118229442,124.957606360848));
#190585=CARTESIAN_POINT('Ctrl Pts',(141.887458888076,-6.04776944257254,
129.400918874772));
#190586=CARTESIAN_POINT('Ctrl Pts',(141.609011264264,-4.44972239443904,
135.133925788383));
#190587=CARTESIAN_POINT('Ctrl Pts',(141.33056364045,1.2374021531599,136.888273821029));
#190588=CARTESIAN_POINT('Ctrl Pts',(141.052116016638,5.78741457246075,133.051802835376));
#190589=CARTESIAN_POINT('Ctrl Pts',(140.773668392825,5.01907573059014,127.15004224521));
#190590=CARTESIAN_POINT('Ctrl Pts',(140.495220769012,-0.361548512212229,
124.606421715863));
#190591=CARTESIAN_POINT('Ctrl Pts',(140.216773145199,-5.4099273349182,127.758404251031));
#190592=CARTESIAN_POINT('Ctrl Pts',(139.938325521386,-5.48684722647749,
133.709471883804));
#190593=CARTESIAN_POINT('Ctrl Pts',(139.659877897573,-0.521622564292735,
136.990884185479));
#190594=CARTESIAN_POINT('Ctrl Pts',(139.38143027376,4.92294775179823,134.58718355672));
#190595=CARTESIAN_POINT('Ctrl Pts',(139.102982649947,5.84356958335437,128.707253448052));
#190596=CARTESIAN_POINT('Ctrl Pts',(138.824535026135,1.39423644205237,124.754462378786));
#190597=CARTESIAN_POINT('Ctrl Pts',(138.546087402322,-4.33633187725888,
126.361232236999));
#190598=CARTESIAN_POINT('Ctrl Pts',(138.267639778509,-6.08202304295846,
132.051020018064));
#190599=CARTESIAN_POINT('Ctrl Pts',(137.989192154696,-2.23863215552307,
136.595188712768));
#190600=CARTESIAN_POINT('Ctrl Pts',(137.710744530883,3.66195231957746,135.817869285661));
#190601=CARTESIAN_POINT('Ctrl Pts',(137.43229690707,6.19738150930245,130.433380316089));
#190602=CARTESIAN_POINT('Ctrl Pts',(137.153849283257,3.03771985089675,125.389804120178));
#190603=CARTESIAN_POINT('Ctrl Pts',(136.875401659444,-2.91345794961824,
125.321940829576));
#190604=CARTESIAN_POINT('Ctrl Pts',(136.596954035631,-6.1873102247676,130.29215349304));
#190605=CARTESIAN_POINT('Ctrl Pts',(136.318506411819,-3.77532667026395,
135.733059481234));
#190606=CARTESIAN_POINT('Ctrl Pts',(136.040058788006,2.10599765925102,136.644731994041));
#190607=CARTESIAN_POINT('Ctrl Pts',(135.761611164193,6.05201302361958,132.189388529871));
#190608=CARTESIAN_POINT('Ctrl Pts',(135.48316354038,4.4365240765547,126.461272076668));
#190609=CARTESIAN_POINT('Ctrl Pts',(135.204715916567,-1.25591376061384,
124.724241820878));
#190610=CARTESIAN_POINT('Ctrl Pts',(134.926268292754,-5.79422820657625,
128.574543708929));
#190611=CARTESIAN_POINT('Ctrl Pts',(134.647820668941,-5.00792999447956,
134.473938403405));
#190612=CARTESIAN_POINT('Ctrl Pts',(134.369373045128,0.380411231562576,
137.001170381535));
#190613=CARTESIAN_POINT('Ctrl Pts',(134.090925421316,5.41917311992063,133.833836917565));
#190614=CARTESIAN_POINT('Ctrl Pts',(133.812477797503,5.4779796523963,127.88256273204));
#190615=CARTESIAN_POINT('Ctrl Pts',(133.53403017369,0.502790498503515,124.616278065551));
#190616=CARTESIAN_POINT('Ctrl Pts',(133.255582549877,-4.93443856083268,
127.036538959725));
#190617=CARTESIAN_POINT('Ctrl Pts',(132.977134926064,-5.83715964348875,
132.919243889133));
#190618=CARTESIAN_POINT('Ctrl Pts',(132.698687302251,-1.37581617488021,
136.858474409763));
#190619=CARTESIAN_POINT('Ctrl Pts',(132.420239678438,4.34983514608645,135.234270115264));
#190620=CARTESIAN_POINT('Ctrl Pts',(132.141792054625,6.07820046906025,129.539195405491));
#190621=CARTESIAN_POINT('Ctrl Pts',(131.863344430812,2.22099649756843,125.006745718858));
#190622=CARTESIAN_POINT('Ctrl Pts',(131.584896806999,-3.67719475347803,
125.802020894903));
#190623=CARTESIAN_POINT('Ctrl Pts',(131.306449183186,-6.1962236670286,131.194201898194));
#190624=CARTESIAN_POINT('Ctrl Pts',(131.028001559374,-3.02122573293442,
136.228137809392));
#190625=CARTESIAN_POINT('Ctrl Pts',(130.749553935561,2.93013105464412,136.277887447547));
#190626=CARTESIAN_POINT('Ctrl Pts',(130.471106311748,6.18884054786473,131.2977333256));
#190627=CARTESIAN_POINT('Ctrl Pts',(130.192658687935,3.76030791926647,125.864193787566));
#190628=CARTESIAN_POINT('Ctrl Pts',(129.914211064122,-2.12376398588317,
124.970426225734));
#190629=CARTESIAN_POINT('Ctrl Pts',(129.635763440309,-6.05620053964477,
129.437759366456));
#190630=CARTESIAN_POINT('Ctrl Pts',(129.357315816496,-4.42328465931731,
135.160932294765));
#190631=CARTESIAN_POINT('Ctrl Pts',(129.078868192683,1.27441373345414,136.880628682086));
#190632=CARTESIAN_POINT('Ctrl Pts',(128.800420568871,5.80098816375315,133.01653156031));
#190633=CARTESIAN_POINT('Ctrl Pts',(128.521972945058,4.99673786558976,127.11955741271));
#190634=CARTESIAN_POINT('Ctrl Pts',(128.243525321245,-0.399270426835251,
124.608737397728));
#190635=CARTESIAN_POINT('Ctrl Pts',(127.965077697432,-5.42836870244348,
127.791392448756));
#190636=CARTESIAN_POINT('Ctrl Pts',(127.686630073619,-5.46906133106002,
133.742818055242));
#190637=CARTESIAN_POINT('Ctrl Pts',(127.408182449806,-0.483953774931917,
136.993944828129));
#190638=CARTESIAN_POINT('Ctrl Pts',(127.129734825993,4.9458836579024,134.557146089508));
#190639=CARTESIAN_POINT('Ctrl Pts',(126.85128720218,5.8306956289736,128.671720835934));
#190640=CARTESIAN_POINT('Ctrl Pts',(126.572839578367,1.35738316233494,124.746087356435));
#190641=CARTESIAN_POINT('Ctrl Pts',(126.294391954555,-4.36329811863544,
126.387711040812));
#190642=CARTESIAN_POINT('Ctrl Pts',(126.015944330741,-6.07432158754323,
132.088019920899));
#190643=CARTESIAN_POINT('Ctrl Pts',(125.737496706929,-2.20334026460562,
136.608708611466));
#190644=CARTESIAN_POINT('Ctrl Pts',(125.459049083116,3.69240312234872,135.795485053802));
#190645=CARTESIAN_POINT('Ctrl Pts',(125.180601459303,6.19500842378515,130.39566196922));
#190646=CARTESIAN_POINT('Ctrl Pts',(124.90215383549,3.00470362674961,125.371412976429));
#190647=CARTESIAN_POINT('Ctrl Pts',(124.623706211677,-2.9467770153362,125.339777451594));
#190648=CARTESIAN_POINT('Ctrl Pts',(124.345258587864,-6.19031353838844,
130.329826896558));
#190649=CARTESIAN_POINT('Ctrl Pts',(124.066810964051,-3.74525433329013,
135.755949648866));
#190650=CARTESIAN_POINT('Ctrl Pts',(123.788363340238,2.14151063825588,136.631803979981));
#190651=CARTESIAN_POINT('Ctrl Pts',(123.509915716426,6.0603319518555,132.152522547471));
#190652=CARTESIAN_POINT('Ctrl Pts',(123.231468092613,4.4100042653751,126.43434616275));
#190653=CARTESIAN_POINT('Ctrl Pts',(122.9530204688,-1.29290190029971,124.731999574929));
#190654=CARTESIAN_POINT('Ctrl Pts',(122.674572844987,-5.80769438136815,
128.609856133963));
#190655=CARTESIAN_POINT('Ctrl Pts',(122.396125221174,-4.98549944760296,
134.504355105923));
#190656=CARTESIAN_POINT('Ctrl Pts',(122.117677597361,0.418125923321227,
136.998739897863));
#190657=CARTESIAN_POINT('Ctrl Pts',(121.839229973548,5.43751399730024,133.80079274346));
#190658=CARTESIAN_POINT('Ctrl Pts',(121.560782349735,5.46009234508668,127.849270849208));
#190659=CARTESIAN_POINT('Ctrl Pts',(121.282334725922,0.465112568078527,
124.613332087916));
#190660=CARTESIAN_POINT('Ctrl Pts',(121.00388710211,-4.95728293698158,127.066646096814));
#190661=CARTESIAN_POINT('Ctrl Pts',(120.725439478297,-5.82417759969065,
132.954737152777));
#190662=CARTESIAN_POINT('Ctrl Pts',(120.446991854484,-1.33893757517749,
136.866737224615));
#190663=CARTESIAN_POINT('Ctrl Pts',(120.168544230671,4.37672067018674,135.207709358136));
#190664=CARTESIAN_POINT('Ctrl Pts',(119.890096606858,6.07038643434081,129.502219114618));
#190665=CARTESIAN_POINT('Ctrl Pts',(119.611648983045,2.18566362019961,124.993333299159));
#190666=CARTESIAN_POINT('Ctrl Pts',(119.333201359232,-3.7075772853013,125.82449770485));
#190667=CARTESIAN_POINT('Ctrl Pts',(119.054753735419,-6.19373579082994,
131.231912847497));
#190668=CARTESIAN_POINT('Ctrl Pts',(118.776306111606,-2.98815368540088,
136.246428377926));
#190669=CARTESIAN_POINT('Ctrl Pts',(118.497858487794,2.96339567748857,136.259949496373));
#190670=CARTESIAN_POINT('Ctrl Pts',(118.219410863981,6.1917291826932,131.26005095553));
#190671=CARTESIAN_POINT('Ctrl Pts',(117.940963240168,3.73016605178927,125.841395255808));
#190672=CARTESIAN_POINT('Ctrl Pts',(117.662515616355,-2.15923745196658,
124.983462269205));
#190673=CARTESIAN_POINT('Ctrl Pts',(117.384067992542,-6.06440722197891,
129.474650498052));
#190674=CARTESIAN_POINT('Ctrl Pts',(117.105620368729,-4.39668301775581,
135.187777366781));
#190675=CARTESIAN_POINT('Ctrl Pts',(116.827172744916,1.31137808987868,136.872758384795));
#190676=CARTESIAN_POINT('Ctrl Pts',(116.548725121103,5.81434679729579,132.981178312436));
#190677=CARTESIAN_POINT('Ctrl Pts',(116.27027749729,4.97421484463032,127.089209121948));
#190678=CARTESIAN_POINT('Ctrl Pts',(115.991829873478,-0.436977546345769,
124.611282660692));
#190679=CARTESIAN_POINT('Ctrl Pts',(115.713382249665,-5.44660891977013,
127.824492293124));
#190680=CARTESIAN_POINT('Ctrl Pts',(115.434934625852,-5.45107277756375,
133.776055341058));
#190681=CARTESIAN_POINT('Ctrl Pts',(115.156487002039,-0.446267052485976,
136.99677611346));
#190682=CARTESIAN_POINT('Ctrl Pts',(114.878039378226,4.9686362924688,134.526969561451));
#190683=CARTESIAN_POINT('Ctrl Pts',(114.599591754413,5.81760561602206,128.636267249567));
#190684=CARTESIAN_POINT('Ctrl Pts',(114.3211441306,1.32047958428524,124.737936825626));
#190685=CARTESIAN_POINT('Ctrl Pts',(114.042696506787,-4.39010267639563,
126.414353505198));
#190686=CARTESIAN_POINT('Ctrl Pts',(113.764248882975,-6.06639504590774,
132.124972257267));
#190687=CARTESIAN_POINT('Ctrl Pts',(113.485801259161,-2.16796672810439,
136.622013427915));
#190688=CARTESIAN_POINT('Ctrl Pts',(113.207353635349,3.72271710176439,135.772915873991));
#190689=CARTESIAN_POINT('Ctrl Pts',(112.928906011536,6.19240577995249,130.357958766832));
#190690=CARTESIAN_POINT('Ctrl Pts',(112.650458387723,2.97157606220462,125.353223152553));
#190691=CARTESIAN_POINT('Ctrl Pts',(112.37201076391,-2.9799868871482,125.357816565752));
#190692=CARTESIAN_POINT('Ctrl Pts',(112.093563140097,-6.19308746766462,
130.367517884098));
#190693=CARTESIAN_POINT('Ctrl Pts',(111.815115516284,-3.71504321453968,
135.778656333547));
#190694=CARTESIAN_POINT('Ctrl Pts',(111.536667892471,2.1769442627965,136.618660027865));
#190695=CARTESIAN_POINT('Ctrl Pts',(111.258220268658,6.06842631226225,132.115606608435));
#190696=CARTESIAN_POINT('Ctrl Pts',(110.979772644846,4.38332103986566,126.407582181323));
#190697=CARTESIAN_POINT('Ctrl Pts',(110.701325021032,-1.32984213103019,
124.739982342551));
#190698=CARTESIAN_POINT('Ctrl Pts',(110.42287739722,-5.82094534990898,128.645249877167));
#190699=CARTESIAN_POINT('Ctrl Pts',(110.144429773407,-4.96288416121089,
134.534634703787));
#190700=CARTESIAN_POINT('Ctrl Pts',(109.865982149594,0.455825121270016,
136.996079879188));
#190701=CARTESIAN_POINT('Ctrl Pts',(109.587534525781,5.45565338559904,133.767637535461));
#190702=CARTESIAN_POINT('Ctrl Pts',(109.309086901968,5.44200271204727,127.816088468313));
#190703=CARTESIAN_POINT('Ctrl Pts',(109.030639278155,0.427417402736423,
124.610615521118));
#190704=CARTESIAN_POINT('Ctrl Pts',(108.752191654342,-4.97994361918818,
127.096891736289));
#190705=CARTESIAN_POINT('Ctrl Pts',(108.473744030529,-5.81097973884976,
132.990150733429));
#190706=CARTESIAN_POINT('Ctrl Pts',(108.195296406717,-1.30200936065053,
136.874775395874));
#190707=CARTESIAN_POINT('Ctrl Pts',(107.916848782904,4.40344401329306,135.180985433302));
#190708=CARTESIAN_POINT('Ctrl Pts',(107.638401159091,6.06234745921968,129.465291075077));
#190709=CARTESIAN_POINT('Ctrl Pts',(107.359953535278,2.15024975226158,124.980136209215));
#190710=CARTESIAN_POINT('Ctrl Pts',(107.081505911465,-3.73782243148481,
125.847159045447));
#190711=CARTESIAN_POINT('Ctrl Pts',(106.803058287652,-6.19101840347381,
131.269607953695));
#190712=CARTESIAN_POINT('Ctrl Pts',(106.524610663839,-2.95497091073364,
136.264517288637));
#190713=CARTESIAN_POINT('Ctrl Pts',(106.246163040026,2.99655049061638,136.241809386346));
#190714=CARTESIAN_POINT('Ctrl Pts',(105.967715416213,6.1943883807198,131.222351699685));
#190715=CARTESIAN_POINT('Ctrl Pts',(105.689267792401,3.69988596163724,125.818780628557));
#190716=CARTESIAN_POINT('Ctrl Pts',(105.410820168588,-2.19463090671215,
124.996714008204));
#190717=CARTESIAN_POINT('Ctrl Pts',(105.132372544775,-6.07238918547325,
129.511590902545));
#190718=CARTESIAN_POINT('Ctrl Pts',(104.853924920962,-4.36991845548819,
135.214460009678));
#190719=CARTESIAN_POINT('Ctrl Pts',(104.575477297149,1.34829385270585,136.864663220793));
#190720=CARTESIAN_POINT('Ctrl Pts',(104.297029673336,5.82748997807964,132.945744401783));
#190721=CARTESIAN_POINT('Ctrl Pts',(104.018582049523,4.95150750231056,127.058998497491));
#190722=CARTESIAN_POINT('Ctrl Pts',(103.74013442571,-0.474668473492613,
124.614057410436));
#190723=CARTESIAN_POINT('Ctrl Pts',(103.461686801897,-5.46464731100027,
127.857702557609));
#190724=CARTESIAN_POINT('Ctrl Pts',(103.183239178085,-5.43288223256107,
133.809182509633));
#190725=CARTESIAN_POINT('Ctrl Pts',(102.904791554272,-0.408563793450433,
136.999377936557));
#190726=CARTESIAN_POINT('Ctrl Pts',(102.626343930459,4.99120481239017,134.496655090749));
#190727=CARTESIAN_POINT('Ctrl Pts',(102.347896306646,5.80430002955499,128.600894002697));
#190728=CARTESIAN_POINT('Ctrl Pts',(102.069448682833,1.28352707537895,124.730011088381));
#190729=CARTESIAN_POINT('Ctrl Pts',(101.79100105902,-4.41674455728669,126.441158642913));
#190730=CARTESIAN_POINT('Ctrl Pts',(101.512553435207,-6.05824371177293,
132.161875657885));
#190731=CARTESIAN_POINT('Ctrl Pts',(101.234105811394,-2.13251285679878,
136.635102669099));
#190732=CARTESIAN_POINT('Ctrl Pts',(100.955658187581,3.75289313452884,135.750162582539));
#190733=CARTESIAN_POINT('Ctrl Pts',(100.677210563769,6.18957367424645,130.320272106026));
#190734=CARTESIAN_POINT('Ctrl Pts',(100.398762939956,2.93833838481571,125.33523532258));
#190735=CARTESIAN_POINT('Ctrl Pts',(100.120315316143,-3.01308633445025,
125.376057503601));
#190736=CARTESIAN_POINT('Ctrl Pts',(99.8418676923298,-6.19563190980719,
130.405225059005));
#190737=CARTESIAN_POINT('Ctrl Pts',(99.5634200685172,-3.68469443349671,
135.801178693871));
#190738=CARTESIAN_POINT('Ctrl Pts',(99.2849724447041,2.2122972198669,136.605300624745));
#190739=CARTESIAN_POINT('Ctrl Pts',(99.0065248208913,6.07629580490035,132.078642080696));
#190740=CARTESIAN_POINT('Ctrl Pts',(98.7280771970783,4.35647538878314,126.380981124141));
#190741=CARTESIAN_POINT('Ctrl Pts',(98.4496295732656,-1.36673308397146,
124.748189827941));
#190742=CARTESIAN_POINT('Ctrl Pts',(98.1711819494526,-5.8339806211792,128.680723627015));
#190743=CARTESIAN_POINT('Ctrl Pts',(97.8927343256397,-4.94008497332115,
134.564776074971));
#190744=CARTESIAN_POINT('Ctrl Pts',(97.6142867018267,0.493507428451318,
136.993190424079));
#190745=CARTESIAN_POINT('Ctrl Pts',(97.3358390780141,5.47359061265531,133.734372522146));
#190746=CARTESIAN_POINT('Ctrl Pts',(97.0573914542009,5.42371142359607,127.783016818942));
#190747=CARTESIAN_POINT('Ctrl Pts',(96.7789438303882,0.389706399285272,
124.608128465823));
#190748=CARTESIAN_POINT('Ctrl Pts',(96.5004962065753,-5.0024197677526,127.127274757387));
#190749=CARTESIAN_POINT('Ctrl Pts',(96.2220485827623,-5.79756655001767,
133.025483318824));
#190750=CARTESIAN_POINT('Ctrl Pts',(95.9436009589496,-1.26503289968789,
136.882588625681));
#190751=CARTESIAN_POINT('Ctrl Pts',(95.6651533351365,4.4300041851621,135.154099331026));
#190752=CARTESIAN_POINT('Ctrl Pts',(95.3867057113237,6.05408384158403,129.428412655251));
#190753=CARTESIAN_POINT('Ctrl Pts',(95.1082580875108,2.11475620602821,124.967154938047));
#190754=CARTESIAN_POINT('Ctrl Pts',(94.8298104636979,-3.76792907128354,
125.870004076972));
#190755=CARTESIAN_POINT('Ctrl Pts',(94.5513628398851,-6.18807160565406,
131.307285819983));
#190756=CARTESIAN_POINT('Ctrl Pts',(94.2729152160721,-2.92167863853249,
136.282403871234));
#190757=CARTESIAN_POINT('Ctrl Pts',(93.9944675922592,3.02959426546386,136.223467789656));
#190758=CARTESIAN_POINT('Ctrl Pts',(93.7160199684464,6.19681804340696,131.184636955029));
#190759=CARTESIAN_POINT('Ctrl Pts',(93.4375723446334,3.66946877085029,125.796350743805));
#190760=CARTESIAN_POINT('Ctrl Pts',(93.1591247208205,-2.22994303860241,
125.010180951684));
#190761=CARTESIAN_POINT('Ctrl Pts',(92.8806770970077,-6.08014613435319,
129.548579211095));
#190762=CARTESIAN_POINT('Ctrl Pts',(92.6022294731947,-4.3429919642852,135.24097923472));
#190763=CARTESIAN_POINT('Ctrl Pts',(92.323781849382,1.38515965400848,136.856343490049));
#190764=CARTESIAN_POINT('Ctrl Pts',(92.045334225569,5.84041721907928,132.910231141365));
#190765=CARTESIAN_POINT('Ctrl Pts',(91.7668866017561,4.9286166800594,127.028926658805));
#190766=CARTESIAN_POINT('Ctrl Pts',(91.4884389779432,-0.512341811624615,
124.617061544141));
#190767=CARTESIAN_POINT('Ctrl Pts',(91.2099913541303,-5.48248320771468,
127.891022011592));
#190768=CARTESIAN_POINT('Ctrl Pts',(90.9315437303175,-5.41449037010934,
133.842198333429));
#190769=CARTESIAN_POINT('Ctrl Pts',(90.6530961065044,-0.370845394933272,
137.00175020101));
#190770=CARTESIAN_POINT('Ctrl Pts',(90.3746484826917,5.01358838138169,134.466203800718));
#190771=CARTESIAN_POINT('Ctrl Pts',(90.0962008588786,5.79077936261581,128.565602406094));
#190772=CARTESIAN_POINT('Ctrl Pts',(89.817753235066,1.24652700490487,124.722310438393));
#190773=CARTESIAN_POINT('Ctrl Pts',(89.5393056112528,-4.44322277408392,
126.468125460682));
#190774=CARTESIAN_POINT('Ctrl Pts',(89.2608579874402,-6.04986788718945,
132.198728755283));
#190775=CARTESIAN_POINT('Ctrl Pts',(88.9824103636271,-2.09697996444503,
136.647975849991));
#190776=CARTESIAN_POINT('Ctrl Pts',(88.7039627398144,3.78293010245805,135.727226022576));
#190777=CARTESIAN_POINT('Ctrl Pts',(88.4255151160013,6.18651221161165,130.282603383299));
#190778=CARTESIAN_POINT('Ctrl Pts',(88.1470674921886,2.9049918262175,125.317450153056));
#190779=CARTESIAN_POINT('Ctrl Pts',(87.8686198683756,-3.04607413073006,
125.394499589218));
#190780=CARTESIAN_POINT('Ctrl Pts',(87.5901722445627,-6.19794677053091,
130.442947024027));
#190781=CARTESIAN_POINT('Ctrl Pts',(87.3117246207499,-3.65420911474647,
135.823515895262));
#190782=CARTESIAN_POINT('Ctrl Pts',(87.033276996937,2.24756819945024,136.59172626566));
#190783=CARTESIAN_POINT('Ctrl Pts',(86.754829373124,6.08394013816284,132.041630333989));
#190784=CARTESIAN_POINT('Ctrl Pts',(86.4763817493112,4.32946830690299,126.35454397691));
#190785=CARTESIAN_POINT('Ctrl Pts',(86.1979341254982,-1.40357339211569,
124.756621726966));
#190786=CARTESIAN_POINT('Ctrl Pts',(85.9194865016854,-5.84679971215209,
128.716276069012));
#190787=CARTESIAN_POINT('Ctrl Pts',(85.6410388778725,-4.91710272876601,
134.594778102578));
#190788=CARTESIAN_POINT('Ctrl Pts',(85.3625912540596,0.531171448533366,
136.990071639606));
#190789=CARTESIAN_POINT('Ctrl Pts',(85.0841436302467,5.49132501379855,133.700998936161));
#190790=CARTESIAN_POINT('Ctrl Pts',(84.8056960064338,5.4052191575235,127.750057126576));
#190791=CARTESIAN_POINT('Ctrl Pts',(84.527248382621,0.351980955120191,124.60587101419));
#190792=CARTESIAN_POINT('Ctrl Pts',(84.2488007588079,-5.02471054981291,
127.157794034254));
#190793=CARTESIAN_POINT('Ctrl Pts',(83.9703531349953,-5.78393853022499,
133.0607335997));
#190794=CARTESIAN_POINT('Ctrl Pts',(83.6919055111822,-1.22800956246596,
136.890176624513));
#190795=CARTESIAN_POINT('Ctrl Pts',(83.4134578873695,4.45640020159694,135.127052047582));
#190796=CARTESIAN_POINT('Ctrl Pts',(83.1350102635564,6.04559588764522,129.391585221682));
#190797=CARTESIAN_POINT('Ctrl Pts',(82.8565626397436,2.07918429672594,124.954389966684));
#190798=CARTESIAN_POINT('Ctrl Pts',(82.5781150159307,-3.79789608908488,
125.893031952893));
#190799=CARTESIAN_POINT('Ctrl Pts',(82.2996673921181,-6.18489550656524,
131.344945050191));
#190800=CARTESIAN_POINT('Ctrl Pts',(82.0212197683047,-2.88827810245507,
136.300087462925));
#190801=CARTESIAN_POINT('Ctrl Pts',(81.7427721444922,3.06252577758164,136.204925385956));
#190802=CARTESIAN_POINT('Ctrl Pts',(81.464324520679,6.19901808072266,131.146908119091));
#190803=CARTESIAN_POINT('Ctrl Pts',(81.1858768968663,3.6389156065486,125.774106432701));
#190804=CARTESIAN_POINT('Ctrl Pts',(80.9074292730533,-2.26517253913331,
125.023862600622));
#190805=CARTESIAN_POINT('Ctrl Pts',(80.6289816492404,-6.08767778118217,
129.585614053086));
#190806=CARTESIAN_POINT('Ctrl Pts',(80.3505340254275,-4.31590454191782,
135.267334059228));
#190807=CARTESIAN_POINT('Ctrl Pts',(80.0720864016147,1.42197412771073,136.847799500855));
#190808=CARTESIAN_POINT('Ctrl Pts',(79.7936387778018,5.85312804127117,132.874639847142));
#190809=CARTESIAN_POINT('Ctrl Pts',(79.5151911539889,4.90554322610457,126.998994720211));
#190810=CARTESIAN_POINT('Ctrl Pts',(79.236743530176,-0.54999616474248,124.62029495049));
#190811=CARTESIAN_POINT('Ctrl Pts',(78.9582959063631,-5.50011594899764,
127.924449420408));
#190812=CARTESIAN_POINT('Ctrl Pts',(78.6798482825503,-5.39589787172579,
133.87510158903));
#190813=CARTESIAN_POINT('Ctrl Pts',(78.4014006587372,-0.333113254603616,
137.003892818912));
#190814=CARTESIAN_POINT('Ctrl Pts',(78.1229530349246,5.035786170012,134.435616819741));
#190815=CARTESIAN_POINT('Ctrl Pts',(77.8445054111114,5.77704411621779,128.530393767498));
#190816=CARTESIAN_POINT('Ctrl Pts',(77.5660577872988,1.20948074391421,124.71483516101));
#190817=CARTESIAN_POINT('Ctrl Pts',(77.2876101634857,-4.46953634562727,
126.49525295924));
#190818=CARTESIAN_POINT('Ctrl Pts',(77.009162539673,-6.04126788252658,132.235530183857));
#190819=CARTESIAN_POINT('Ctrl Pts',(76.73071491586,-2.06136936772754,136.660632493573));
#190820=CARTESIAN_POINT('Ctrl Pts',(76.4522672920471,3.81282689252116,135.704107044024));
#190821=CARTESIAN_POINT('Ctrl Pts',(76.1738196682342,6.18322150549176,130.244953994479));
#190822=CARTESIAN_POINT('Ctrl Pts',(75.8953720444213,2.87153762207887,125.299868303017));
#190823=CARTESIAN_POINT('Ctrl Pts',(75.6169244206085,-3.07894905361277,
125.413142139227));
#190824=CARTESIAN_POINT('Ctrl Pts',(75.3384767967955,-6.20003196405775,
130.480682381363));
#190825=CARTESIAN_POINT('Ctrl Pts',(75.0600291729826,-3.62358838793365,
135.84566711001));
#190826=CARTESIAN_POINT('Ctrl Pts',(74.7815815491698,2.28275589456742,136.577937453613));
#190827=CARTESIAN_POINT('Ctrl Pts',(74.5031339253568,6.09135902878616,132.004572739798));
#190828=CARTESIAN_POINT('Ctrl Pts',(74.224686301544,4.30230079498258,126.328271719272));
#190829=CARTESIAN_POINT('Ctrl Pts',(73.946238677731,-1.44036169033171,124.76527772718));
#190830=CARTESIAN_POINT('Ctrl Pts',(73.6677910539182,-5.85940214781156,
128.75190588575));
#190831=CARTESIAN_POINT('Ctrl Pts',(73.3893434301052,-4.89393827916089,
134.624639674871));
#190832=CARTESIAN_POINT('Ctrl Pts',(73.1108958062924,0.56881578586215,136.986723641335));
#190833=CARTESIAN_POINT('Ctrl Pts',(72.8324481824796,5.50885593187395,133.66751801418));
#190834=CARTESIAN_POINT('Ctrl Pts',(72.5540005586665,5.38652659906729,127.717210612549));
#190835=CARTESIAN_POINT('Ctrl Pts',(72.2755529348538,0.314242468171368,
124.603843249867));
#190836=CARTESIAN_POINT('Ctrl Pts',(71.9971053110409,-5.04681513937595,
127.188448435987));
#190837=CARTESIAN_POINT('Ctrl Pts',(71.7186576872279,-5.77009618446306,
133.095900269846));
#190838=CARTESIAN_POINT('Ctrl Pts',(71.4402100634152,-1.19094072089807,
136.897539111196));
#190839=CARTESIAN_POINT('Ctrl Pts',(71.1617624396021,4.48263108448347,135.099844585217));
#190840=CARTESIAN_POINT('Ctrl Pts',(70.8833148157894,6.03688391192757,129.354810139024));
#190841=CARTESIAN_POINT('Ctrl Pts',(70.6048671919763,2.04353534248492,124.941841768133));
#190842=CARTESIAN_POINT('Ctrl Pts',(70.3264195681636,-3.82772237444985,
125.916241819903));
#190843=CARTESIAN_POINT('Ctrl Pts',(70.0479719443506,-6.18149022389895,
131.382584248845));
#190844=CARTESIAN_POINT('Ctrl Pts',(69.7695243205378,-2.85477054017052,
136.317567408437));
#190845=CARTESIAN_POINT('Ctrl Pts',(69.4910766967249,3.09534380668036,136.186182862342));
#190846=CARTESIAN_POINT('Ctrl Pts',(69.2126290729119,6.20098841114368,131.109166589932));
#190847=CARTESIAN_POINT('Ctrl Pts',(68.934181449099,3.60822760089105,125.752048519516));
#190848=CARTESIAN_POINT('Ctrl Pts',(68.6557338252862,-2.30031810286251,
125.037758448041));
#190849=CARTESIAN_POINT('Ctrl Pts',(68.3772862014732,-6.09498384687224,
129.622694056181));
#190850=CARTESIAN_POINT('Ctrl Pts',(68.0988385776604,-4.28865719212064,
135.293523506613));
#190851=CARTESIAN_POINT('Ctrl Pts',(67.8203909538475,1.45873590963839,136.83903156981));
#190852=CARTESIAN_POINT('Ctrl Pts',(67.5419433300346,5.86562197365073,132.83897183796));
#190853=CARTESIAN_POINT('Ctrl Pts',(67.2634957062218,4.88228799544191,126.969203790852));
#190854=CARTESIAN_POINT('Ctrl Pts',(66.9850480824087,-0.587630137549865,
124.623757509667));
#190855=CARTESIAN_POINT('Ctrl Pts',(66.706600458596,-5.51754488146136,127.957983545393));
#190856=CARTESIAN_POINT('Ctrl Pts',(66.428152834783,-5.37710542636232,133.907891057196));
#190857=CARTESIAN_POINT('Ctrl Pts',(66.1497052109702,-0.295368770640213,
137.00580571087));
#190858=CARTESIAN_POINT('Ctrl Pts',(65.8712575871573,5.05779735573374,134.404895281231));
#190859=CARTESIAN_POINT('Ctrl Pts',(65.5928099633443,5.76309479932555,128.495269391582));
#190860=CARTESIAN_POINT('Ctrl Pts',(65.3143623395316,1.17238966517029,124.707585533234));
#190861=CARTESIAN_POINT('Ctrl Pts',(65.0359147157185,-4.49568429685739,
126.522540133366));
#190862=CARTESIAN_POINT('Ctrl Pts',(64.7574670919057,-6.03244401646077,
132.272278579917));
#190863=CARTESIAN_POINT('Ctrl Pts',(64.4790194680927,-2.02568238621027,
136.673072130848));
#190864=CARTESIAN_POINT('Ctrl Pts',(64.20057184428,3.84258239688126,135.680806503568));
#190865=CARTESIAN_POINT('Ctrl Pts',(63.922124220467,6.17970167782515,130.207325334677));
#190866=CARTESIAN_POINT('Ctrl Pts',(63.6436765966542,2.8379770120581,125.282490423967));
#190867=CARTESIAN_POINT('Ctrl Pts',(63.3652289728412,-3.11170988490585,
125.431984462817));
#190868=CARTESIAN_POINT('Ctrl Pts',(63.0867813490283,-6.20188741312008,
130.518429732716));
#190869=CARTESIAN_POINT('Ctrl Pts',(62.8083337252156,-3.59283338772076,
135.86763151729));
#190870=CARTESIAN_POINT('Ctrl Pts',(62.5298861014024,2.31785900132509,136.563934699553));
#190871=CARTESIAN_POINT('Ctrl Pts',(62.2514384775899,6.09855220186056,131.967470671305));
#190872=CARTESIAN_POINT('Ctrl Pts',(61.9729908537767,4.27497385972414,126.302165324755));
#190873=CARTESIAN_POINT('Ctrl Pts',(61.6945432299639,-1.47709661541541,
124.774157507831));
#190874=CARTESIAN_POINT('Ctrl Pts',(61.416095606151,-5.87178746116934,128.787611756953));
#190875=CARTESIAN_POINT('Ctrl Pts',(61.1376479823382,-4.8705924828735,134.65435968532));
#190876=CARTESIAN_POINT('Ctrl Pts',(60.8592003585251,0.606439045512412,
136.983146553331));
#190877=CARTESIAN_POINT('Ctrl Pts',(60.5807527347125,5.52618271726667,133.633930996847));
#190878=CARTESIAN_POINT('Ctrl Pts',(60.3023051108993,5.36763444088732,127.684478494003));
#190879=CARTESIAN_POINT('Ctrl Pts',(60.0238574870866,0.276492336852797,
124.602045247997));
#190880=CARTESIAN_POINT('Ctrl Pts',(59.7454098632736,-5.06873271734795,
127.219236826675));
#190881=CARTESIAN_POINT('Ctrl Pts',(59.4669622394608,-5.75604002566515,
133.130982026147));
#190882=CARTESIAN_POINT('Ctrl Pts',(59.1885146156479,-1.15382774858414,
136.904675812908));
#190883=CARTESIAN_POINT('Ctrl Pts',(58.9100669918351,4.50869586182645,135.072477952114));
#190884=CARTESIAN_POINT('Ctrl Pts',(58.6316193680221,6.02794823725661,129.318088769994));
#190885=CARTESIAN_POINT('Ctrl Pts',(58.3531717442092,2.00781066429043,124.929510807376));
#190886=CARTESIAN_POINT('Ctrl Pts',(58.0747241203963,-3.85740682215468,
125.939632817953));
#190887=CARTESIAN_POINT('Ctrl Pts',(57.7962764965834,-6.17785588383907,
131.42020202121));
#190888=CARTESIAN_POINT('Ctrl Pts',(57.5178288727705,-2.82115719331391,
136.334843060042));
#190889=CARTESIAN_POINT('Ctrl Pts',(57.2393812489577,3.12804713667602,136.167240913326));
#190890=CARTESIAN_POINT('Ctrl Pts',(56.9609336251447,6.20272896165862,131.071413766074));
#190891=CARTESIAN_POINT('Ctrl Pts',(56.6824860013319,3.57740589103289,125.730177821614));
#190892=CARTESIAN_POINT('Ctrl Pts',(56.404038377519,-2.33537842745856,125.051867979023));
#190893=CARTESIAN_POINT('Ctrl Pts',(56.125590753706,-6.10206406069443,129.659817846364));
#190894=CARTESIAN_POINT('Ctrl Pts',(55.8471431298932,-4.26125092455389,
135.319546606417));
#190895=CARTESIAN_POINT('Ctrl Pts',(55.5686955060803,1.49544363757083,136.830040021814));
#190896=CARTESIAN_POINT('Ctrl Pts',(55.2902478822675,5.87789855325116,132.80322843551));
#190897=CARTESIAN_POINT('Ctrl Pts',(55.0118002584545,4.85885184980179,126.939554974638));
#190898=CARTESIAN_POINT('Ctrl Pts',(54.7333526346416,-0.625242335506623,
124.627449093364));
#190899=CARTESIAN_POINT('Ctrl Pts',(54.4549050108287,-5.53476935927053,
127.991623143927));
#190900=CARTESIAN_POINT('Ctrl Pts',(54.1764573870159,-5.35811373037978,
133.9405655229));
#190901=CARTESIAN_POINT('Ctrl Pts',(53.8980097632029,-0.257613341678002,
137.007488805997));
#190902=CARTESIAN_POINT('Ctrl Pts',(53.61956213939,5.07962112291461,134.374040323585));
#190903=CARTESIAN_POINT('Ctrl Pts',(53.3411145155772,5.74893192883615,128.460230579889));
#190904=CARTESIAN_POINT('Ctrl Pts',(53.0626668917642,1.13525514309568,124.7005618237));
#190905=CARTESIAN_POINT('Ctrl Pts',(52.7842192679514,-4.52166565885288,
126.549985971924));
#190906=CARTESIAN_POINT('Ctrl Pts',(52.5057716441385,-6.0233966159634,132.308972581737));
#190907=CARTESIAN_POINT('Ctrl Pts',(52.2273240203255,-1.98992034228702,
136.685294300858));
#190908=CARTESIAN_POINT('Ctrl Pts',(51.9488763965128,3.87219551293788,135.657325264614));
#190909=CARTESIAN_POINT('Ctrl Pts',(51.6704287726998,6.17595285904027,130.169718798237));
#190910=CARTESIAN_POINT('Ctrl Pts',(51.391981148887,2.80431123975502,125.265317159845));
#190911=CARTESIAN_POINT('Ctrl Pts',(51.113533525074,-3.14435541064497,125.451025861782));
#190912=CARTESIAN_POINT('Ctrl Pts',(50.8350859012611,-6.20351304896362,
130.556187679343));
#190913=CARTESIAN_POINT('Ctrl Pts',(50.5566382774483,-3.5619452537452,135.889408303207));
#190914=CARTESIAN_POINT('Ctrl Pts',(50.2781906536353,2.35287621896542,136.549718522358));
#190915=CARTESIAN_POINT('Ctrl Pts',(49.9997430298226,6.10551939084041,131.930325503341));
#190916=CARTESIAN_POINT('Ctrl Pts',(49.7212954060095,4.2474885137371,126.27622576074));
#190917=CARTESIAN_POINT('Ctrl Pts',(49.4428477821967,-1.51377680614101,
124.783260739875));
#190918=CARTESIAN_POINT('Ctrl Pts',(49.1644001583838,-5.88395519328364,
128.823392359526));
#190919=CARTESIAN_POINT('Ctrl Pts',(48.8859525345709,-4.84706620499019,
134.683937032636));
#190920=CARTESIAN_POINT('Ctrl Pts',(48.607504910758,0.644039833341117,136.97934050814));
#190921=CARTESIAN_POINT('Ctrl Pts',(48.3290572869451,5.54330472792681,133.600239128744));
#190922=CARTESIAN_POINT('Ctrl Pts',(48.0506096631323,5.34854338303893,127.651861983834));
#190923=CARTESIAN_POINT('Ctrl Pts',(47.7721620393193,0.23873196000854,124.600477075203));
#190924=CARTESIAN_POINT('Ctrl Pts',(47.4937144155065,-5.09046247156518,
127.250158065443));
#190925=CARTESIAN_POINT('Ctrl Pts',(47.2152667916935,-5.74177057468722,
133.165977568637));
#190926=CARTESIAN_POINT('Ctrl Pts',(46.9368191678807,-1.11667202075834,
136.911586465198));
#190927=CARTESIAN_POINT('Ctrl Pts',(46.6583715440677,4.53459356778643,135.044953162355));
#190928=CARTESIAN_POINT('Ctrl Pts',(46.379923920255,6.01878919474683,129.281422475313));
#190929=CARTESIAN_POINT('Ctrl Pts',(46.101476296442,1.97201158593325,124.917397541337));
#190930=CARTESIAN_POINT('Ctrl Pts',(45.8230286726291,-3.88694833223118,
125.963204080281));
#190931=CARTESIAN_POINT('Ctrl Pts',(45.5445810488162,-6.17399262105761,
131.457796973343));
#190932=CARTESIAN_POINT('Ctrl Pts',(45.2661334250033,-2.78743930743976,
136.351913777587));
#190933=CARTESIAN_POINT('Ctrl Pts',(44.9876858011905,3.16063455573481,136.148100240809));
#190934=CARTESIAN_POINT('Ctrl Pts',(44.7092381773775,6.20423966777097,131.033651046464));
#190935=CARTESIAN_POINT('Ctrl Pts',(44.4307905535647,3.54645161908363,125.708495149421));
#190936=CARTESIAN_POINT('Ctrl Pts',(44.1523429297517,-2.37035221374829,
125.066190670735));
#190937=CARTESIAN_POINT('Ctrl Pts',(43.8738953059389,-6.10891816028884,
129.696984048001));
#190938=CARTESIAN_POINT('Ctrl Pts',(43.5954476821259,-4.23368675476706,
135.345402394343));
#190939=CARTESIAN_POINT('Ctrl Pts',(43.3170000583131,1.53209595128933,136.820825190051));
#190940=CARTESIAN_POINT('Ctrl Pts',(43.0385524345002,5.88995732515911,132.767410964279));
#190941=CARTESIAN_POINT('Ctrl Pts',(42.7601048106873,4.83523565761953,126.910049370218));
#190942=CARTESIAN_POINT('Ctrl Pts',(42.4816571868744,-0.662831364878718,
124.631369564788));
#190943=CARTESIAN_POINT('Ctrl Pts',(42.2032095630615,-5.55178874416567,
128.025366969483));
#190944=CARTESIAN_POINT('Ctrl Pts',(41.9247619392486,-5.33892348752252,
133.973123775378));
#190945=CARTESIAN_POINT('Ctrl Pts',(41.6463143154357,-0.219848366758665,
137.008942041929));
#190946=CARTESIAN_POINT('Ctrl Pts',(41.3678666916229,5.10125666286673,134.343053090145));
#190947=CARTESIAN_POINT('Ctrl Pts',(41.0894190678099,5.73455602955998,128.425278630796));
#190948=CARTESIAN_POINT('Ctrl Pts',(40.8109714439971,1.09807855372398,124.693764292674));
#190949=CARTESIAN_POINT('Ctrl Pts',(40.5325238201841,-4.5474794688646,126.5775894579));
#190950=CARTESIAN_POINT('Ctrl Pts',(40.2540761963713,-6.01412601628932,
132.345610829607));
#190951=CARTESIAN_POINT('Ctrl Pts',(39.9756285725584,-1.95408456113369,
136.697298550707));
#190952=CARTESIAN_POINT('Ctrl Pts',(39.6971809487455,3.90166514336576,135.633664197272));
#190953=CARTESIAN_POINT('Ctrl Pts',(39.4187333249326,6.171975188051,130.132135778682));
#190954=CARTESIAN_POINT('Ctrl Pts',(39.1402857011198,2.77054155266769,125.248349147017));
#190955=CARTESIAN_POINT('Ctrl Pts',(38.8618380773068,-3.17688442113803,
125.470265630536));
#190956=CARTESIAN_POINT('Ctrl Pts',(38.583390453494,-6.20490881134979,130.593954822108));
#190957=CARTESIAN_POINT('Ctrl Pts',(38.304942829681,-3.53092513057837,135.910996660811));
#190958=CARTESIAN_POINT('Ctrl Pts',(38.0264952058682,2.38780624991219,136.535289448812));
#190959=CARTESIAN_POINT('Ctrl Pts',(37.7480475820552,6.11226033755391,131.893138612335));
#190960=CARTESIAN_POINT('Ctrl Pts',(37.4695999582424,4.21984577550119,126.250453988427));
#190961=CARTESIAN_POINT('Ctrl Pts',(37.1911523344295,-1.55040090331038,
124.792587085991));
#190962=CARTESIAN_POINT('Ctrl Pts',(36.9127047106166,-5.89590489327443,
128.859246367608));
#190963=CARTESIAN_POINT('Ctrl Pts',(36.6342570868037,-4.82336031728617,
134.713370620821));
#190964=CARTESIAN_POINT('Ctrl Pts',(36.3558094629908,0.681616756036961,
136.975305646799));
#190965=CARTESIAN_POINT('Ctrl Pts',(36.0773618391779,5.56022132939171,133.566443658335));
#190966=CARTESIAN_POINT('Ctrl Pts',(35.798914215365,5.32925413294858,127.619362290662));
#190967=CARTESIAN_POINT('Ctrl Pts',(35.5204665915522,0.200962736863706,
124.599138789596));
#190968=CARTESIAN_POINT('Ctrl Pts',(35.2420189677392,-5.11200359682353,
127.281211006494));
#190969=CARTESIAN_POINT('Ctrl Pts',(34.9635713439263,-5.72728836028912,
133.200885600541));
#190970=CARTESIAN_POINT('Ctrl Pts',(34.6851237201134,-1.07947491424015,
136.918270811987));
#190971=CARTESIAN_POINT('Ctrl Pts',(34.4066760963006,4.56032324271418,135.017271235878));
#190972=CARTESIAN_POINT('Ctrl Pts',(34.1282284724876,6.00940712379002,129.244812613665));
#190973=CARTESIAN_POINT('Ctrl Pts',(33.8497808486748,1.93613943396156,124.905502418881));
#190974=CARTESIAN_POINT('Ctrl Pts',(33.5713332248619,-3.91634581000783,
125.986954733445));
#190975=CARTESIAN_POINT('Ctrl Pts',(33.292885601049,-6.16990057870911,131.495367712155));
#190976=CARTESIAN_POINT('Ctrl Pts',(33.0144379772361,-2.753618131977,136.368778928511));
#190977=CARTESIAN_POINT('Ctrl Pts',(32.7359903534233,3.19310485631782,136.128761554055));
#190978=CARTESIAN_POINT('Ctrl Pts',(32.4575427296103,6.20552047350092,130.995879830412));
#190979=CARTESIAN_POINT('Ctrl Pts',(32.1790951057975,3.51536593206519,125.687001306397));
#190980=CARTESIAN_POINT('Ctrl Pts',(31.9006474819845,-2.40523816576522,
125.080725992446));
#190981=CARTESIAN_POINT('Ctrl Pts',(31.6221998581717,-6.11554589167424,
129.734191283883));
#190982=CARTESIAN_POINT('Ctrl Pts',(31.3437522343588,-4.20596570416061,
135.371089912296));
#190983=CARTESIAN_POINT('Ctrl Pts',(31.0653046105458,1.56869149262894,136.811387415981));
#190984=CARTESIAN_POINT('Ctrl Pts',(30.786856986733,5.90179784253235,132.731520751495));
#190985=CARTESIAN_POINT('Ctrl Pts',(30.5084093629201,4.81144029400183,126.880688070935));
#190986=CARTESIAN_POINT('Ctrl Pts',(30.2299617391072,-0.700395832790832,
124.635518778667));
#190987=CARTESIAN_POINT('Ctrl Pts',(29.9515141152943,-5.56860240548724,
128.05921377167));
#190988=CARTESIAN_POINT('Ctrl Pts',(29.6730664914815,-5.31953540889204,
134.005564608172));
#190989=CARTESIAN_POINT('Ctrl Pts',(29.3946188676685,-0.182075245277261,
137.010165364815));
#190990=CARTESIAN_POINT('Ctrl Pts',(29.1161712438556,5.12270317387725,134.311934729152));
#190991=CARTESIAN_POINT('Ctrl Pts',(28.8377236200427,5.71996763420123,128.390414839463));
#190992=CARTESIAN_POINT('Ctrl Pts',(28.5592759962298,1.06086127464794,124.687193192043));
#190993=CARTESIAN_POINT('Ctrl Pts',(28.280828372417,-4.57312477035222,126.605349568435));
#190994=CARTESIAN_POINT('Ctrl Pts',(28.0023807486041,-6.00463256096402,
132.382191965885));
#190995=CARTESIAN_POINT('Ctrl Pts',(27.7239331247912,-1.91817637065835,
136.709084435575));
#190996=CARTESIAN_POINT('Ctrl Pts',(27.4454855009783,3.93099019615694,135.60982417831));
#190997=CARTESIAN_POINT('Ctrl Pts',(27.1670378771654,6.16776881225138,130.094577668667));
#190998=CARTESIAN_POINT('Ctrl Pts',(26.8885902533525,2.73666920214424,125.231587014236));
#190999=CARTESIAN_POINT('Ctrl Pts',(26.6101426295396,-3.20929571101057,
125.48970305614));
#191000=CARTESIAN_POINT('Ctrl Pts',(26.3316950057267,-6.2060746485581,130.631729761538));
#191001=CARTESIAN_POINT('Ctrl Pts',(26.0532473819138,-3.49977416768234,
135.932395790139));
#191002=CARTESIAN_POINT('Ctrl Pts',(25.774799758101,2.42264779982026,136.52064801359));
#191003=CARTESIAN_POINT('Ctrl Pts',(25.4963521342881,6.11877479221284,131.85591137626));
#191004=CARTESIAN_POINT('Ctrl Pts',(25.2179045104751,4.19204666932822,126.224850962798));
#191005=CARTESIAN_POINT('Ctrl Pts',(24.9394568866623,-1.58696754980412,
124.802136200585));
#191006=CARTESIAN_POINT('Ctrl Pts',(24.6610092628494,-5.90763611834117,
128.895172452612));
#191007=CARTESIAN_POINT('Ctrl Pts',(24.3825616390365,-4.79947569819179,
134.742659359205));
#191008=CARTESIAN_POINT('Ctrl Pts',(24.1041140152236,0.719168421173241,
136.97104211882));
#191009=CARTESIAN_POINT('Ctrl Pts',(23.8256663914108,5.57693189481048,133.532545837923));
#191010=CARTESIAN_POINT('Ctrl Pts',(23.5472187675978,5.3097674053865,127.586980618775));
#191011=CARTESIAN_POINT('Ctrl Pts',(23.2687711437849,0.163186066970757,
124.598030440764));
#191012=CARTESIAN_POINT('Ctrl Pts',(22.990323519972,-5.13335529490864,127.312394499151));
#191013=CARTESIAN_POINT('Ctrl Pts',(22.7118758961592,-5.71259391911463,
133.235704828331));
#191014=CARTESIAN_POINT('Ctrl Pts',(22.4334282723462,-1.04223780738205,
136.924728605587));
#191015=CARTESIAN_POINT('Ctrl Pts',(22.1549806485334,4.58588393318709,134.98943319845));
#191016=CARTESIAN_POINT('Ctrl Pts',(21.8765330247205,5.9998023720423,129.208260541641));
#191017=CARTESIAN_POINT('Ctrl Pts',(21.5980854009075,1.90019553763114,124.893825880784));
#191018=CARTESIAN_POINT('Ctrl Pts',(21.3196377770947,-3.94559816615024,
126.010883897355));
#191019=CARTESIAN_POINT('Ctrl Pts',(21.0411901532818,-6.16557990842568,
131.532912845442));
#191020=CARTESIAN_POINT('Ctrl Pts',(20.7627425294689,-2.71969492018171,
136.385437887866));
#191021=CARTESIAN_POINT('Ctrl Pts',(20.484294905656,3.22545683522612,136.109225569666));
#191022=CARTESIAN_POINT('Ctrl Pts',(20.2058472818431,6.20657133138755,130.958101517545));
#191023=CARTESIAN_POINT('Ctrl Pts',(19.9273996580302,3.48414998186958,125.665697089004));
#191024=CARTESIAN_POINT('Ctrl Pts',(19.6489520342174,-2.44003499079723,
125.095473405541));
#191025=CARTESIAN_POINT('Ctrl Pts',(19.3705044104044,-6.12194700925765,
129.771438175283));
#191026=CARTESIAN_POINT('Ctrl Pts',(19.0920567865916,-4.17808879994825,
135.396608208416));
#191027=CARTESIAN_POINT('Ctrl Pts',(18.8136091627787,1.60522890552839,136.801727049323));
#191028=CARTESIAN_POINT('Ctrl Pts',(18.5351615389658,5.91341966661616,132.695559127084));
#191029=CARTESIAN_POINT('Ctrl Pts',(18.2567139151529,4.78746664069464,126.85147216478));
#191030=CARTESIAN_POINT('Ctrl Pts',(17.97826629134,-0.737934347277788,124.63989658125));
#191031=CARTESIAN_POINT('Ctrl Pts',(17.6998186675271,-5.58520972019883,
128.093162296283));
#191032=CARTESIAN_POINT('Ctrl Pts',(17.4213710437142,-5.29995021292075,
134.037886819174));
#191033=CARTESIAN_POINT('Ctrl Pts',(17.1429234199013,-0.144295376930669,
137.011158729324));
#191034=CARTESIAN_POINT('Ctrl Pts',(16.8644757960885,5.14395986123776,134.280686393713));
#191035=CARTESIAN_POINT('Ctrl Pts',(16.5860281722755,5.70516728333829,128.355640497777));
#191036=CARTESIAN_POINT('Ctrl Pts',(16.3075805484627,1.02360468496723,124.6808487653));
#191037=CARTESIAN_POINT('Ctrl Pts',(16.0291329246498,-4.5986006130197,126.633265274869));
#191038=CARTESIAN_POINT('Ctrl Pts',(15.7506853008369,-5.99491660177097,
132.418714635041));
#191039=CARTESIAN_POINT('Ctrl Pts',(15.472237677024,-1.88219710145218,136.720651518731));
#191040=CARTESIAN_POINT('Ctrl Pts',(15.1937900532111,3.96016958466077,135.585806091128));
#191041=CARTESIAN_POINT('Ctrl Pts',(14.9153424293982,6.16333388751023,130.057045859918));
#191042=CARTESIAN_POINT('Ctrl Pts',(14.6368948055853,2.70269544333712,125.215031382631));
#191043=CARTESIAN_POINT('Ctrl Pts',(14.3584471817724,-3.24158807925031,
125.509337418335));
#191044=CARTESIAN_POINT('Ctrl Pts',(14.0799995579596,-6.20701051738803,
130.669511097867));
#191045=CARTESIAN_POINT('Ctrl Pts',(13.8015519341466,-3.46849351936748,
135.953604898237));
#191046=CARTESIAN_POINT('Ctrl Pts',(13.5231043103337,2.45739957762318,136.505794759238));
#191047=CARTESIAN_POINT('Ctrl Pts',(13.2446566865208,6.12506251342167,131.818645174584));
#191048=CARTESIAN_POINT('Ctrl Pts',(12.966209062708,4.16409222532429,126.199417632585));
#191049=CARTESIAN_POINT('Ctrl Pts',(12.687761438895,-1.62347539063169,124.811907729812));
#191050=CARTESIAN_POINT('Ctrl Pts',(12.4093138150822,-5.91914843377905,
128.931169283287));
#191051=CARTESIAN_POINT('Ctrl Pts',(12.1308661912693,-4.77541323276041,
134.771802162479));
#191052=CARTESIAN_POINT('Ctrl Pts',(11.8524185674564,0.756693437259193,
136.96655008219));
#191053=CARTESIAN_POINT('Ctrl Pts',(11.5739709436435,5.59343580496719,133.498546923603));
#191054=CARTESIAN_POINT('Ctrl Pts',(11.2955233198306,5.2900839224404,127.554718168085));
#191055=CARTESIAN_POINT('Ctrl Pts',(11.0170756960177,0.125403350157864,
124.597152069781));
#191056=CARTESIAN_POINT('Ctrl Pts',(10.7386280722048,-5.15451677462551,
127.343707387895));
#191057=CARTESIAN_POINT('Ctrl Pts',(10.460180448392,-5.69768779567166,133.270433961767));
#191058=CARTESIAN_POINT('Ctrl Pts',(10.1817328245791,-1.0049620800187,136.930959606699));
#191059=CARTESIAN_POINT('Ctrl Pts',(9.90328520076621,4.61127469204443,134.961440081617));
#191060=CARTESIAN_POINT('Ctrl Pts',(9.62483757695328,5.98997529541125,129.171767613693));
#191061=CARTESIAN_POINT('Ctrl Pts',(9.34638995314043,1.86418122885626,124.882368359726));
#191062=CARTESIAN_POINT('Ctrl Pts',(9.0679423293275,-3.97470431670162,126.034990685308));
#191063=CARTESIAN_POINT('Ctrl Pts',(8.78949470551463,-6.16103077031137,
131.57043098196));
#191064=CARTESIAN_POINT('Ctrl Pts',(8.5110470817017,-2.68567092909101,136.401890038352));
#191065=CARTESIAN_POINT('Ctrl Pts',(8.2325994578889,3.25768929364524,136.089493011555));
#191066=CARTESIAN_POINT('Ctrl Pts',(7.95415183407592,6.20739220249103,130.920317507753));
#191067=CARTESIAN_POINT('Ctrl Pts',(7.67570421026306,3.45280492521512,125.644583286679));
#191068=CARTESIAN_POINT('Ctrl Pts',(7.39725658645018,-2.47474139943534,
125.110432363552));
#191069=CARTESIAN_POINT('Ctrl Pts',(7.11880896263729,-6.1281212758433,129.808723342005));
#191070=CARTESIAN_POINT('Ctrl Pts',(6.84036133882437,-4.15005707511893,
135.421956337113));
#191071=CARTESIAN_POINT('Ctrl Pts',(6.56191371501151,1.64170683608044,136.791844448048));
#191072=CARTESIAN_POINT('Ctrl Pts',(6.28346609119863,5.92482236675955,132.659527423617));
#191073=CARTESIAN_POINT('Ctrl Pts',(6.00501846738572,4.76331558605049,126.822402734361));
#191074=CARTESIAN_POINT('Ctrl Pts',(5.72657084357281,-0.775445517336138,
124.644502810313));
#191075=CARTESIAN_POINT('Ctrl Pts',(5.44812321975995,-5.60161007291028,
128.127211285347));
#191076=CARTESIAN_POINT('Ctrl Pts',(5.16967559594705,-5.28016862534525,
134.070089210674));
#191077=CARTESIAN_POINT('Ctrl Pts',(4.89122797213414,-0.106510161665837,
137.011922098645));
#191078=CARTESIAN_POINT('Ctrl Pts',(4.6127803483213,5.16502593727395,134.249309241742));
#191079=CARTESIAN_POINT('Ctrl Pts',(4.33433272450837,5.69015552540359,128.320956894316));
#191080=CARTESIAN_POINT('Ctrl Pts',(4.05588510069549,0.986310165238503,
124.674731247541));
#191081=CARTESIAN_POINT('Ctrl Pts',(3.77743747688256,-4.62390605285035,
126.661335542776));
#191082=CARTESIAN_POINT('Ctrl Pts',(3.49898985306972,-5.98497849873861,
132.455177483715));
#191083=CARTESIAN_POINT('Ctrl Pts',(3.22054222925682,-1.84614808674025,
136.731999371551));
#191084=CARTESIAN_POINT('Ctrl Pts',(2.94209460544391,3.9892022276243,135.561610825727));
#191085=CARTESIAN_POINT('Ctrl Pts',(2.66364698163102,6.15867057816533,130.019541743194));
#191086=CARTESIAN_POINT('Ctrl Pts',(2.38519935781816,2.66862153515642,125.198682865676));
#191087=CARTESIAN_POINT('Ctrl Pts',(2.10675173400524,-3.27376032925169,
125.529167989562));
#191088=CARTESIAN_POINT('Ctrl Pts',(1.82830411019233,-6.20771638316062,
130.707297431096));
#191089=CARTESIAN_POINT('Ctrl Pts',(1.54985648637947,-3.43708434474973,
135.974623199195));
#191090=CARTESIAN_POINT('Ctrl Pts',(1.27140886256659,2.49206029558105,136.490730236146));
#191091=CARTESIAN_POINT('Ctrl Pts',(0.992961238753657,6.13112326818657,
131.78134138822));
#191092=CARTESIAN_POINT('Ctrl Pts',(0.714513614940807,4.13598347935162,
126.174154940227));
#191093=CARTESIAN_POINT('Ctrl Pts',(0.436065991127901,-1.65992307298164,
124.821901311585));
#191094=CARTESIAN_POINT('Ctrl Pts',(0.157618367314999,-5.93044141299494,
128.967235525755));
#191095=CARTESIAN_POINT('Ctrl Pts',(-0.120829256497892,-4.75117381263555,
134.800797950748));
#191096=CARTESIAN_POINT('Ctrl Pts',(-0.399276880310752,0.794190413791566,
136.961829703365));
#191097=CARTESIAN_POINT('Ctrl Pts',(-0.67772450412367,5.60973244830296,
133.464448175219));
#191098=CARTESIAN_POINT('Ctrl Pts',(-0.956172127936585,5.27020441348929,
127.522576134092));
#191099=CARTESIAN_POINT('Ctrl Pts',(-1.23461975174943,0.0876159864779326,
124.596503709192));
#191100=CARTESIAN_POINT('Ctrl Pts',(-1.51306737556233,-5.17548725182775,
127.375148512417));
#191101=CARTESIAN_POINT('Ctrl Pts',(-1.79151499937523,-5.6825705423121,
133.305071713949));
#191102=CARTESIAN_POINT('Ctrl Pts',(-2.06996262318813,-0.967649113415911,
136.936963584433));
#191103=CARTESIAN_POINT('Ctrl Pts',(-2.34841024700098,4.63649457842225,
134.933292922676));
#191104=CARTESIAN_POINT('Ctrl Pts',(-2.62685787081389,5.97992625804282,
129.13533518208));
#191105=CARTESIAN_POINT('Ctrl Pts',(-2.90530549462681,1.82809784216042,
124.871130280269));
#191106=CARTESIAN_POINT('Ctrl Pts',(-3.18375311843967,-4.00366318312286,
126.059274204017));
#191107=CARTESIAN_POINT('Ctrl Pts',(-3.46220074225256,-6.15625333293613,
131.607920731459));
#191108=CARTESIAN_POINT('Ctrl Pts',(-3.74064836606547,-2.65154741947636,
136.418134770325));
#191109=CARTESIAN_POINT('Ctrl Pts',(-4.01909598987837,3.28980103718956,
136.06956461092));
#191110=CARTESIAN_POINT('Ctrl Pts',(-4.29754361369122,6.20798305639367,
130.882529201136));
#191111=CARTESIAN_POINT('Ctrl Pts',(-4.57599123750414,3.42133192360438,
125.623660681799));
#191112=CARTESIAN_POINT('Ctrl Pts',(-4.85443886131705,-2.5093561056208,
125.125602312169));
#191113=CARTESIAN_POINT('Ctrl Pts',(-5.13288648512991,-6.13406846264146,
129.846045402432));
#191114=CARTESIAN_POINT('Ctrl Pts',(-5.41133410894279,-4.12187156839848,
135.447133359102));
#191115=CARTESIAN_POINT('Ctrl Pts',(-5.68978173275571,1.67812393258193,
136.781739978358));
#191116=CARTESIAN_POINT('Ctrl Pts',(-5.9682293565686,5.93600552043131,132.623426976261));
#191117=CARTESIAN_POINT('Ctrl Pts',(-6.24667698038146,4.73898802499559,
126.793480856855));
#191118=CARTESIAN_POINT('Ctrl Pts',(-6.52512460419438,-0.812927952975666,
124.649337295173));
#191119=CARTESIAN_POINT('Ctrl Pts',(-6.80357222800728,-5.61780285590049,
128.161359477164));
#191120=CARTESIAN_POINT('Ctrl Pts',(-7.08201985182013,-5.26019137917956,
134.1021705894));
#191121=CARTESIAN_POINT('Ctrl Pts',(-7.36046747563304,-0.0687209996277829,
137.012455444495));
#191122=CARTESIAN_POINT('Ctrl Pts',(-7.63891509944595,5.18590062137458,
134.217804435933));
#191123=CARTESIAN_POINT('Ctrl Pts',(-7.91736272325884,5.67493291666336,
128.286365314294));
#191124=CARTESIAN_POINT('Ctrl Pts',(-8.1958103470717,0.948979097423875,
124.668840865451));
#191125=CARTESIAN_POINT('Ctrl Pts',(-8.47425797088461,-4.64904015214177,
126.689559331999));
#191126=CARTESIAN_POINT('Ctrl Pts',(-8.75270559469752,-5.97481862012702,
132.491579160764));
#191127=CARTESIAN_POINT('Ctrl Pts',(-9.03115321851038,-1.81003066233205,
136.743127573537));
#191128=CARTESIAN_POINT('Ctrl Pts',(-9.30960084232328,4.0180870492325,135.537239278668));
#191129=CARTESIAN_POINT('Ctrl Pts',(-9.58804846613619,6.15377905701727,
129.982066708221));
#191130=CARTESIAN_POINT('Ctrl Pts',(-9.86649608994908,2.63444874022312,
125.182542069172));
#191131=CARTESIAN_POINT('Ctrl Pts',(-10.144943713762,-3.30581126886015,
125.549194034992));
#191132=CARTESIAN_POINT('Ctrl Pts',(-10.4233913375749,-6.20819221971975,
130.745087361036));
#191133=CARTESIAN_POINT('Ctrl Pts',(-10.7018389613878,-3.40554780770759,
135.995449914173));
#191134=CARTESIAN_POINT('Ctrl Pts',(-10.9802865852006,2.52662866932821,
136.475455002538));
#191135=CARTESIAN_POINT('Ctrl Pts',(-11.2587342090136,6.13695683192405,
131.744001399476));
#191136=CARTESIAN_POINT('Ctrl Pts',(-11.5371818328265,4.10772147299012,
126.149063821843));
#191137=CARTESIAN_POINT('Ctrl Pts',(-11.8156294566394,-1.69630924627168,
124.832116575588));
#191138=CARTESIAN_POINT('Ctrl Pts',(-12.0940770804522,-5.94151463752335,
129.003369843568));
#191139=CARTESIAN_POINT('Ctrl Pts',(-12.3725247042651,-4.72675833601782,
134.829645649562));
#191140=CARTESIAN_POINT('Ctrl Pts',(-12.6509723280781,0.83165796130609,
136.956881157257));
#191141=CARTESIAN_POINT('Ctrl Pts',(-12.9294199518909,5.62582122093989,
133.430250856313));
#191142=CARTESIAN_POINT('Ctrl Pts',(-13.2078675757038,5.25012961517551,
127.490555707831));
#191143=CARTESIAN_POINT('Ctrl Pts',(-13.4863151995167,0.0498253761554086,
124.596085383024));
#191144=CARTESIAN_POINT('Ctrl Pts',(-13.7647628233296,-5.19626594944658,
127.406716707655));
#191145=CARTESIAN_POINT('Ctrl Pts',(-14.0432104471424,-5.66724271921134,
133.339616801361));
#191146=CARTESIAN_POINT('Ctrl Pts',(-14.3216580709554,-0.930300290219375,
136.942740316309));
#191147=CARTESIAN_POINT('Ctrl Pts',(-14.6001056947683,4.6615426577884,134.904992764631));
#191148=CARTESIAN_POINT('Ctrl Pts',(-14.8785533185811,5.96965563230779,
129.098964596818));
#191149=CARTESIAN_POINT('Ctrl Pts',(-15.157000942394,1.79194671462675,124.860112058844));
#191150=CARTESIAN_POINT('Ctrl Pts',(-15.4354485662069,-4.03247369233249,
126.08373355365));
#191151=CARTESIAN_POINT('Ctrl Pts',(-15.7138961900198,-6.15124777332969,
131.645380704742));
#191152=CARTESIAN_POINT('Ctrl Pts',(-15.9923438138327,-2.61732565579698,
136.434171481834));
#191153=CARTESIAN_POINT('Ctrl Pts',(-16.2707914376456,3.32179087594663,
136.049441106215));
#191154=CARTESIAN_POINT('Ctrl Pts',(-16.5492390614585,6.2083438712012,130.844737997954));
#191155=CARTESIAN_POINT('Ctrl Pts',(-16.8276866852714,3.38973214328102,
125.602930049661));
#191156=CARTESIAN_POINT('Ctrl Pts',(-17.1061343090842,-2.54387782669295,
125.140982689263));
#191157=CARTESIAN_POINT('Ctrl Pts',(-17.3845819328972,-6.13978834927694,
129.883402973582));
#191158=CARTESIAN_POINT('Ctrl Pts',(-17.66302955671,-4.09353332421128,135.47213834144));
#191159=CARTESIAN_POINT('Ctrl Pts',(-17.9414771805229,1.71447884558397,
136.771414014676));
#191160=CARTESIAN_POINT('Ctrl Pts',(-18.2199248043358,5.94696871323555,
132.587259122732));
#191161=CARTESIAN_POINT('Ctrl Pts',(-18.4983724281487,4.71448485899666,
126.764707603974));
#191162=CARTESIAN_POINT('Ctrl Pts',(-18.7768200519616,-0.850380265270943,
124.654399856686));
#191163=CARTESIAN_POINT('Ctrl Pts',(-19.0552676757745,-5.63378746913994,
128.19560560636));
#191164=CARTESIAN_POINT('Ctrl Pts',(-19.3337152995874,-5.24001921468789,
134.134129766565));
#191165=CARTESIAN_POINT('Ctrl Pts',(-19.6121629234003,-0.0309292911078312,
137.012758747106));
#191166=CARTESIAN_POINT('Ctrl Pts',(-19.8906105472132,5.2065831400206,134.18617314371));
#191167=CARTESIAN_POINT('Ctrl Pts',(-20.1690581710261,5.65950002119693,
128.251867039513));
#191168=CARTESIAN_POINT('Ctrl Pts',(-20.447505794839,0.911612864839816,
124.663177837304));
#191169=CARTESIAN_POINT('Ctrl Pts',(-20.7259534186518,-4.67400197954067,
126.717935596697));
#191170=CARTESIAN_POINT('Ctrl Pts',(-21.0044010424647,-5.96443734241423,
132.527918317308));
#191171=CARTESIAN_POINT('Ctrl Pts',(-21.2828486662776,-1.77384616657202,
136.754035712331));
#191172=CARTESIAN_POINT('Ctrl Pts',(-21.5612962900905,4.0468229791472,135.512692353051));
#191173=CARTESIAN_POINT('Ctrl Pts',(-21.8397439139034,6.14865950532324,
129.944622143653));
#191174=CARTESIAN_POINT('Ctrl Pts',(-22.1181915377163,2.60017832482316,
125.166609591221));
#191175=CARTESIAN_POINT('Ctrl Pts',(-22.3966391615293,-3.33773971041633,
125.569414812551));
#191176=CARTESIAN_POINT('Ctrl Pts',(-22.6750867853421,-6.20843800943312,
130.782879487369));
#191177=CARTESIAN_POINT('Ctrl Pts',(-22.953534409155,-3.37388507683905,
136.016084271426));
#191178=CARTESIAN_POINT('Ctrl Pts',(-23.2319820329679,2.56110341792085,
136.45996962444));
#191179=CARTESIAN_POINT('Ctrl Pts',(-23.5104296567807,6.14256298846929,
131.706626591997));
#191180=CARTESIAN_POINT('Ctrl Pts',(-23.7888772805937,4.07930725349882,
126.124145207193));
#191181=CARTESIAN_POINT('Ctrl Pts',(-24.0673249044065,-1.73263256219878,
124.842553143289));
#191182=CARTESIAN_POINT('Ctrl Pts',(-24.3457725282195,-5.95236769704188,
129.039570897758));
#191183=CARTESIAN_POINT('Ctrl Pts',(-24.6242201520323,-4.70216770763169,
134.858344189959));
#191184=CARTESIAN_POINT('Ctrl Pts',(-24.9026677758452,0.86909469142902,
136.951704627238));
#191185=CARTESIAN_POINT('Ctrl Pts',(-25.1811153996581,5.64170152670257,
133.395956234079));
#191186=CARTESIAN_POINT('Ctrl Pts',(-25.459563023471,5.22986027137813,127.458658075828));
#191187=CARTESIAN_POINT('Ctrl Pts',(-25.7380106472839,0.0120329195352371,
124.595897106778));
#191188=CARTESIAN_POINT('Ctrl Pts',(-26.0164582710968,-5.21685209751974,
127.438410803838));
#191189=CARTESIAN_POINT('Ctrl Pts',(-26.2949058949097,-5.6517048943475,
133.374067943923));
#191190=CARTESIAN_POINT('Ctrl Pts',(-26.5733535187226,-0.892916994403456,
136.948289588268));
#191191=CARTESIAN_POINT('Ctrl Pts',(-26.8518011425354,4.68641800197708,
134.876540656153));
#191192=CARTESIAN_POINT('Ctrl Pts',(-27.1302487663484,5.95916379878798,
129.062657205632));
#191193=CARTESIAN_POINT('Ctrl Pts',(-27.4086963901612,1.75572918584856,
124.849314103734));
#191194=CARTESIAN_POINT('Ctrl Pts',(-27.6871440139742,-4.06113477674652,
126.108367827853));
#191195=CARTESIAN_POINT('Ctrl Pts',(-27.965591637787,-6.1460142769749,131.682809513716));
#191196=CARTESIAN_POINT('Ctrl Pts',(-28.2440392616,-2.5830069061529,136.449999578631));
#191197=CARTESIAN_POINT('Ctrl Pts',(-28.5224868854127,3.3536576245212,136.029123243122));
#191198=CARTESIAN_POINT('Ctrl Pts',(-28.8009345092257,6.20847463354345,
130.806945298572));
#191199=CARTESIAN_POINT('Ctrl Pts',(-29.0793821330386,3.35800675518651,
125.582392158445));
#191200=CARTESIAN_POINT('Ctrl Pts',(-29.3578297568515,-2.57830528343674,
125.156572924908));
#191201=CARTESIAN_POINT('Ctrl Pts',(-29.6362773806644,-6.14528072379723,
129.920794671155));
#191202=CARTESIAN_POINT('Ctrl Pts',(-29.9147250044772,-4.06504339264135,
135.496970357558));
#191203=CARTESIAN_POINT('Ctrl Pts',(-30.1931726282902,1.75077022794215,
136.760866939637));
#191204=CARTESIAN_POINT('Ctrl Pts',(-30.471620252103,5.95771153892721,132.551025203244));
#191205=CARTESIAN_POINT('Ctrl Pts',(-30.750067875916,4.68980699602731,126.736084041921));
#191206=CARTESIAN_POINT('Ctrl Pts',(-31.0285154997288,-0.887801066412759,
124.659690307256));
#191207=CARTESIAN_POINT('Ctrl Pts',(-31.3069631235417,-5.6495633203129,
128.229948403933));
#191208=CARTESIAN_POINT('Ctrl Pts',(-31.5854107473546,-5.21965287935721,
134.16596555791));
#191209=CARTESIAN_POINT('Ctrl Pts',(-31.8638583711675,0.00686356350839004,
137.012831995241));
#191210=CARTESIAN_POINT('Ctrl Pts',(-32.1423059949804,5.22707272681363,
134.154416537178));
#191211=CARTESIAN_POINT('Ctrl Pts',(-32.4207536187933,5.64385741087595,
128.217463348321));
#191212=CARTESIAN_POINT('Ctrl Pts',(-32.6992012426062,0.874212852105795,
124.657742372942));
#191213=CARTESIAN_POINT('Ctrl Pts',(-32.9776488664191,-4.69879061007736,
126.746463285377));
#191214=CARTESIAN_POINT('Ctrl Pts',(-33.2560964902319,-5.9538350502823,
132.564193606789));
#191215=CARTESIAN_POINT('Ctrl Pts',(-33.5345441140448,-1.73759594028995,
136.764723383724));
#191216=CARTESIAN_POINT('Ctrl Pts',(-33.8129917378578,4.07540895254819,
135.487970958469));
#191217=CARTESIAN_POINT('Ctrl Pts',(-34.0914393616706,6.14331211279008,
129.907209437008));
#191218=CARTESIAN_POINT('Ctrl Pts',(-34.3698869854835,2.56581155885918,
125.150886022208));
#191219=CARTESIAN_POINT('Ctrl Pts',(-34.6483346092964,-3.3695444708001,
125.589829572953));
#191220=CARTESIAN_POINT('Ctrl Pts',(-34.9267822331094,-6.2084537431929,
130.820672409693));
#191221=CARTESIAN_POINT('Ctrl Pts',(-35.2052298569221,-3.34209732541825,
136.036525506343));
#191222=CARTESIAN_POINT('Ctrl Pts',(-35.4836774807351,2.59548326388451,
136.444274675672));
#191223=CARTESIAN_POINT('Ctrl Pts',(-35.7621251045479,6.14794153008404,
131.66921835072));
#191224=CARTESIAN_POINT('Ctrl Pts',(-36.0405727283609,4.05074187377708,
126.099400019648));
#191225=CARTESIAN_POINT('Ctrl Pts',(-36.3190203521737,-1.76889167478912,
124.85321062796));
#191226=CARTESIAN_POINT('Ctrl Pts',(-36.5974679759867,-5.96300018938643,
129.075837346879));
#191227=CARTESIAN_POINT('Ctrl Pts',(-36.8759155997995,-4.67740283869194,
134.886892508504));
#191228=CARTESIAN_POINT('Ctrl Pts',(-37.1543632236125,0.906499216928551,
136.946300305126));
#191229=CARTESIAN_POINT('Ctrl Pts',(-37.4328108474252,5.65737277714046,
133.361565579315));
#191230=CARTESIAN_POINT('Ctrl Pts',(-37.7112584712383,5.2093971331851,127.426884420063));
#191231=CARTESIAN_POINT('Ctrl Pts',(-37.9897060950511,-0.0257599829691867,
124.595938887431));
#191232=CARTESIAN_POINT('Ctrl Pts',(-38.268153718864,-5.23724493321992,
127.470229626529));
#191233=CARTESIAN_POINT('Ctrl Pts',(-38.5466013426768,-5.63595764348039,
133.408423865036));
#191234=CARTESIAN_POINT('Ctrl Pts',(-38.8250489664898,-0.855500611219946,
136.953611194679));
#191235=CARTESIAN_POINT('Ctrl Pts',(-39.1034965903026,4.71111968922328,
134.847937651547));
#191236=CARTESIAN_POINT('Ctrl Pts',(-39.3819442141156,5.94845114626212,
129.026414353905));
#191237=CARTESIAN_POINT('Ctrl Pts',(-39.6603918379284,1.71944659787975,
124.838736815064));
#191238=CARTESIAN_POINT('Ctrl Pts',(-39.9388394617414,-4.08964537431793,
126.133176113797));
#191239=CARTESIAN_POINT('Ctrl Pts',(-40.2172870855541,-6.14055303780089,
131.720205771443));
#191240=CARTESIAN_POINT('Ctrl Pts',(-40.495734709367,-2.54859244223803,
136.465618474199));
#191241=CARTESIAN_POINT('Ctrl Pts',(-40.7741823331801,3.3854001020792,136.008611774531));
#191242=CARTESIAN_POINT('Ctrl Pts',(-41.0526299569928,6.20837533857501,
130.769152503414));
#191243=CARTESIAN_POINT('Ctrl Pts',(-41.3310775808058,3.3261569349168,125.562047769191));
#191244=CARTESIAN_POINT('Ctrl Pts',(-41.6095252046187,-2.61263720013008,
125.172372441404));
#191245=CARTESIAN_POINT('Ctrl Pts',(-41.8879728284316,-6.15054538268038,
129.958219109591));
#191246=CARTESIAN_POINT('Ctrl Pts',(-42.1664204522444,-4.03640282939359,
135.521628487296));
#191247=CARTESIAN_POINT('Ctrl Pts',(-42.4448680760573,1.78699673486542,
136.750099144066));
#191248=CARTESIAN_POINT('Ctrl Pts',(-42.7233156998703,5.96823359942677,
132.514726560457));
#191249=CARTESIAN_POINT('Ctrl Pts',(-43.0017633236831,4.66495535053527,
126.707611231352));
#191250=CARTESIAN_POINT('Ctrl Pts',(-43.2802109474961,-0.925188969759574,
124.665208450844));
#191251=CARTESIAN_POINT('Ctrl Pts',(-43.5586585713089,-5.6651298248394,
128.264386597296));
#191252=CARTESIAN_POINT('Ctrl Pts',(-43.8371061951219,-5.19909312786956,
134.197676783747));
#191253=CARTESIAN_POINT('Ctrl Pts',(-44.1155538189346,0.0446561637927345,
137.012675186187));
#191254=CARTESIAN_POINT('Ctrl Pts',(-44.3940014427476,5.24736862250453,
134.122535793092));
#191255=CARTESIAN_POINT('Ctrl Pts',(-44.6724490665605,5.62800566534308,
128.183155515557));
#191256=CARTESIAN_POINT('Ctrl Pts',(-44.9508966903734,0.836780445093053,
124.65253467378));
#191257=CARTESIAN_POINT('Ctrl Pts',(-45.2293443141862,-4.72340512520001,
126.775141340936));
#191258=CARTESIAN_POINT('Ctrl Pts',(-45.5077919379991,-5.94301213660306,
132.600403685011));
#191259=CARTESIAN_POINT('Ctrl Pts',(-45.7862395618121,-1.7012813267513,
136.775190191685));
#191260=CARTESIAN_POINT('Ctrl Pts',(-46.0646871856249,4.10384391017172,
135.463076010984));
#191261=CARTESIAN_POINT('Ctrl Pts',(-46.3431348094379,6.13773707756737,
129.869829974632));
#191262=CARTESIAN_POINT('Ctrl Pts',(-46.6215824332507,2.5313497158043,125.135371944775));
#191263=CARTESIAN_POINT('Ctrl Pts',(-46.9000300570636,-3.40122437147435,
125.610437559721));
#191264=CARTESIAN_POINT('Ctrl Pts',(-47.1784776808764,-6.20823942041608,
130.858464727578));
#191265=CARTESIAN_POINT('Ctrl Pts',(-47.4569253046894,-3.31018573135201,
136.056772861467));
#191266=CARTESIAN_POINT('Ctrl Pts',(-47.7353729285023,2.62976693326135,
136.428370737814));
#191267=CARTESIAN_POINT('Ctrl Pts',(-48.0138205523151,6.15309225746451,
131.631778061822));
#191268=CARTESIAN_POINT('Ctrl Pts',(-48.2922681761281,4.02202639232555,
126.074829176147));
#191269=CARTESIAN_POINT('Ctrl Pts',(-48.570715799941,-1.80508524044794,
124.864088634681));
#191270=CARTESIAN_POINT('Ctrl Pts',(-48.8491634237538,-5.97341172056607,
129.112167847066));
#191271=CARTESIAN_POINT('Ctrl Pts',(-49.1276110475668,-4.65246464686987,
134.915289547327));
#191272=CARTESIAN_POINT('Ctrl Pts',(-49.4060586713796,0.943870151766231,
136.940668391181));
#191273=CARTESIAN_POINT('Ctrl Pts',(-49.6845062951925,5.6728343915496,133.327080166382));
#191274=CARTESIAN_POINT('Ctrl Pts',(-49.9629539190054,5.18874095886556,
127.395235917922));
#191275=CARTESIAN_POINT('Ctrl Pts',(-50.2414015428183,-0.0635519309279763,
124.596210723434));
#191276=CARTESIAN_POINT('Ctrl Pts',(-50.5198491666312,-5.25744370088312,
127.50217199667));
#191277=CARTESIAN_POINT('Ctrl Pts',(-50.798296790444,-5.6200015501302,133.442683291627));
#191278=CARTESIAN_POINT('Ctrl Pts',(-51.076744414257,-0.818052527146474,
136.958704938348));
#191279=CARTESIAN_POINT('Ctrl Pts',(-51.3551920380699,4.73564680419706,
134.819184810706));
#191280=CARTESIAN_POINT('Ctrl Pts',(-51.6336396618827,5.93751807169133,
128.990237384633));
#191281=CARTESIAN_POINT('Ctrl Pts',(-51.9120872856956,1.68310029518491,
124.828380584778));
#191282=CARTESIAN_POINT('Ctrl Pts',(-52.1905349095086,-4.11800442857602,
126.1581574922));
#191283=CARTESIAN_POINT('Ctrl Pts',(-52.4689825333214,-6.13486425817587,
131.757568092191));
#191284=CARTESIAN_POINT('Ctrl Pts',(-52.7474301571343,-2.51408353929296,
136.481027589776));
#191285=CARTESIAN_POINT('Ctrl Pts',(-53.0258777809472,3.41701713239144,
135.987907460498));
#191286=CARTESIAN_POINT('Ctrl Pts',(-53.3043254047601,6.20804598997526,
130.731361012906));
#191287=CARTESIAN_POINT('Ctrl Pts',(-53.5827730285729,3.29418386267868,
125.541897635768));
#191288=CARTESIAN_POINT('Ctrl Pts',(-53.8612206523859,-2.64687230459117,
125.188380653292));
#191289=CARTESIAN_POINT('Ctrl Pts',(-54.1396682761987,-6.15558213084251,
129.995674902111));
#191290=CARTESIAN_POINT('Ctrl Pts',(-54.4181159000117,-4.0076126957546,
135.546111816938));
#191291=CARTESIAN_POINT('Ctrl Pts',(-54.6965635238244,1.82315702396754,
136.739111026966));
#191292=CARTESIAN_POINT('Ctrl Pts',(-54.9750111476374,5.97853450483549,
132.478364539431));
#191293=CARTESIAN_POINT('Ctrl Pts',(-55.2534587714502,4.63993084340721,
126.679290227339));
#191294=CARTESIAN_POINT('Ctrl Pts',(-55.5319063952633,-0.962542589888887,
124.670954082973));
#191295=CARTESIAN_POINT('Ctrl Pts',(-55.810354019076,-5.68048640589689,
128.298918910331));
#191296=CARTESIAN_POINT('Ctrl Pts',(-56.088801642889,-5.1783407220741,134.229262269005));
#191297=CARTESIAN_POINT('Ctrl Pts',(-56.3672492667019,0.0824471093265141,
137.012288325754));
#191298=CARTESIAN_POINT('Ctrl Pts',(-56.6456968905149,5.26747007502141,
134.090532092806));
#191299=CARTESIAN_POINT('Ctrl Pts',(-56.9241445143275,5.6119453719906,128.148944812513));
#191300=CARTESIAN_POINT('Ctrl Pts',(-57.2025921381407,0.799317030873196,
124.64755493279));
#191301=CARTESIAN_POINT('Ctrl Pts',(-57.4810397619534,-4.74784461280872,
126.803968700697));
#191302=CARTESIAN_POINT('Ctrl Pts',(-57.7594873857663,-5.93196900242356,
132.636547210196));
#191303=CARTESIAN_POINT('Ctrl Pts',(-58.0379350095792,-1.66490367160747,
136.785435748359));
#191304=CARTESIAN_POINT('Ctrl Pts',(-58.3163826333922,4.13212679834998,
135.438008433087));
#191305=CARTESIAN_POINT('Ctrl Pts',(-58.5948302572049,6.13193460624012,
129.832485141631));
#191306=CARTESIAN_POINT('Ctrl Pts',(-58.873277881018,2.49679407265481,125.120067933803));
#191307=CARTESIAN_POINT('Ctrl Pts',(-59.1517255048308,-3.43277823852872,
125.631238009216));
#191308=CARTESIAN_POINT('Ctrl Pts',(-59.4301731286437,-6.20779504904446,
130.896255040614));
#191309=CARTESIAN_POINT('Ctrl Pts',(-59.7086207524566,-3.27815147713605,
136.076825586523));
#191310=CARTESIAN_POINT('Ctrl Pts',(-59.9870683762695,2.66395315565763,
136.412258400192));
#191311=CARTESIAN_POINT('Ctrl Pts',(-60.2655160000824,6.15801497974849,
131.594307112665));
#191312=CARTESIAN_POINT('Ctrl Pts',(-60.5439636238952,3.99316187320697,
126.050433587173));
#191313=CARTESIAN_POINT('Ctrl Pts',(-60.8224112477081,-1.84121191800936,
124.875186760365));
#191314=CARTESIAN_POINT('Ctrl Pts',(-61.1008588715211,-5.98360190477769,
129.148561052078));
#191315=CARTESIAN_POINT('Ctrl Pts',(-61.3793064953339,-4.62735405625939,
134.943534254169));
#191316=CARTESIAN_POINT('Ctrl Pts',(-61.6577541191468,0.981206111148332,
136.934809094094));
#191317=CARTESIAN_POINT('Ctrl Pts',(-61.9362017429597,5.68808579699418,
133.292501273148));
#191318=CARTESIAN_POINT('Ctrl Pts',(-62.2146493667725,5.16789251384163,
127.36371374215));
#191319=CARTESIAN_POINT('Ctrl Pts',(-62.4930969905855,-0.10134152394658,
124.596712604715));
#191320=CARTESIAN_POINT('Ctrl Pts',(-62.7715446143984,-5.27744765203657,
127.534236730624));
#191321=CARTESIAN_POINT('Ctrl Pts',(-63.0499922382113,-5.60383720555579,
133.476844954201));
#191322=CARTESIAN_POINT('Ctrl Pts',(-63.3284398620242,-0.780574129835986,
136.963570630527));
#191323=CARTESIAN_POINT('Ctrl Pts',(-63.606887485837,4.75999843803683,134.790283199078));
#191324=CARTESIAN_POINT('Ctrl Pts',(-63.88533510965,5.92636498020503,128.954127638363));
#191325=CARTESIAN_POINT('Ctrl Pts',(-64.1637827334628,1.64669162458969,
124.818245796629));
#191326=CARTESIAN_POINT('Ctrl Pts',(-64.4422303572757,-4.14621088866563,
126.183311037368));
#191327=CARTESIAN_POINT('Ctrl Pts',(-64.7206779810887,-6.12894814889968,
131.794895091487));
#191328=CARTESIAN_POINT('Ctrl Pts',(-64.9991256049015,-2.47948147605779,
136.49622635437));
#191329=CARTESIAN_POINT('Ctrl Pts',(-65.2775732287142,3.44850754387722,
135.967011068231));
#191330=CARTESIAN_POINT('Ctrl Pts',(-65.5560208525274,6.20748659994837,
130.693572227424));
#191331=CARTESIAN_POINT('Ctrl Pts',(-65.83446847634,3.26208872324607,125.521942504845));
#191332=CARTESIAN_POINT('Ctrl Pts',(-66.1129161001531,-2.68100932822562,
125.204596967384));
#191333=CARTESIAN_POINT('Ctrl Pts',(-66.3913637239659,-6.1603907816451,
130.033160660777));
#191334=CARTESIAN_POINT('Ctrl Pts',(-66.6698113477789,-3.97867405855336,
135.570419439246));
#191335=CARTESIAN_POINT('Ctrl Pts',(-66.9482589715917,1.85924975531565,
136.727902995508));
#191336=CARTESIAN_POINT('Ctrl Pts',(-67.2267065954047,5.98861387344954,
132.441940487574));
#191337=CARTESIAN_POINT('Ctrl Pts',(-67.5051542192175,4.61473440193538,
126.651122079325));
#191338=CARTESIAN_POINT('Ctrl Pts',(-67.7836018430304,-0.999860542648545,
124.676926990737));
#191339=CARTESIAN_POINT('Ctrl Pts',(-68.0620494668433,-5.69563249444164,
128.33354406343));
#191340=CARTESIAN_POINT('Ctrl Pts',(-68.3404970906562,-5.15739643095884,
134.260720843274));
#191341=CARTESIAN_POINT('Ctrl Pts',(-68.618944714469,0.120234999752325,
137.011671428276));
#191342=CARTESIAN_POINT('Ctrl Pts',(-68.8973923382821,5.28737633949755,
134.058406622227));
#191343=CARTESIAN_POINT('Ctrl Pts',(-69.1758399620947,5.59567712593856,
128.114832506878));
#191344=CARTESIAN_POINT('Ctrl Pts',(-69.4542875859078,0.761823997666808,
124.642803334499));
#191345=CARTESIAN_POINT('Ctrl Pts',(-69.7327352097205,-4.77210816728929,
126.832944296451));
#191346=CARTESIAN_POINT('Ctrl Pts',(-70.0111828335336,-5.92070605695121,
132.672622843033));
#191347=CARTESIAN_POINT('Ctrl Pts',(-70.2896304573463,-1.62846432284579,
136.795459674095));
#191348=CARTESIAN_POINT('Ctrl Pts',(-70.5680780811594,4.16025656905012,
135.412769153666));
#191349=CARTESIAN_POINT('Ctrl Pts',(-70.8465257049722,6.12590491382102,
129.795176321834));
#191350=CARTESIAN_POINT('Ctrl Pts',(-71.1249733287852,2.46214590988275,
125.104974556385));
#191351=CARTESIAN_POINT('Ctrl Pts',(-71.4034209525978,-3.46420490272305,
125.652230150673));
#191352=CARTESIAN_POINT('Ctrl Pts',(-71.681868576411,-6.20712064554441,
130.93404194847));
#191353=CARTESIAN_POINT('Ctrl Pts',(-71.9603162002238,-3.24599574981168,
136.09668293845));
#191354=CARTESIAN_POINT('Ctrl Pts',(-72.2387638240367,2.69804066428979,
136.395938259856));
#191355=CARTESIAN_POINT('Ctrl Pts',(-72.5172114478495,6.16270951452303,
131.556806891751));
#191356=CARTESIAN_POINT('Ctrl Pts',(-72.7956590716624,3.96414938600637,
126.026214156713));
#191357=CARTESIAN_POINT('Ctrl Pts',(-73.0741066954753,-1.87727036878649,
124.886504593767));
#191358=CARTESIAN_POINT('Ctrl Pts',(-73.3525543192881,-5.99357036442037,
129.185015613353));
#191359=CARTESIAN_POINT('Ctrl Pts',(-73.6310019431012,-4.60207199734241,
134.971625582408));
#191360=CARTESIAN_POINT('Ctrl Pts',(-73.909449566914,1.01850571157763,136.928722630985));
#191361=CARTESIAN_POINT('Ctrl Pts',(-74.187897190727,5.70312642832773,133.257830180947));
#191362=CARTESIAN_POINT('Ctrl Pts',(-74.4663448145398,5.14685257066011,
127.332319060812));
#191363=CARTESIAN_POINT('Ctrl Pts',(-74.7447924383527,-0.139127361718492,
124.597444512675));
#191364=CARTESIAN_POINT('Ctrl Pts',(-75.0232400621657,-5.29725604542678,
127.566422640223));
#191365=CARTESIAN_POINT('Ctrl Pts',(-75.3016876859784,-5.58746520873256,
133.510907586884));
#191366=CARTESIAN_POINT('Ctrl Pts',(-75.5801353097915,-0.743066808063574,
136.968208090913));
#191367=CARTESIAN_POINT('Ctrl Pts',(-75.8585829336042,4.7841736883842,134.761233887624));
#191368=CARTESIAN_POINT('Ctrl Pts',(-76.1370305574171,5.91499228508486,
128.918086453158));
#191369=CARTESIAN_POINT('Ctrl Pts',(-76.41547818123,1.61022193523031,124.808332826166));
#191370=CARTESIAN_POINT('Ctrl Pts',(-76.693925805043,-4.17426370938676,
126.208635817229));
#191371=CARTESIAN_POINT('Ctrl Pts',(-76.9723734288558,-6.12280492919574,
131.832185386163));
#191372=CARTESIAN_POINT('Ctrl Pts',(-77.2508210526686,-2.44478753472383,
136.511214204787));
#191373=CARTESIAN_POINT('Ctrl Pts',(-77.5292686764817,3.47987016964863,
135.945923372052));
#191374=CARTESIAN_POINT('Ctrl Pts',(-77.8077163002943,6.20669718922256,
130.655787547247));
#191375=CARTESIAN_POINT('Ctrl Pts',(-78.0861639241075,3.22987270591563,
125.502183115868));
#191376=CARTESIAN_POINT('Ctrl Pts',(-78.3646115479203,-2.71504700607423,
125.221020782777));
#191377=CARTESIAN_POINT('Ctrl Pts',(-78.6430591717333,-6.16497115690175,
130.070674996542));
#191378=CARTESIAN_POINT('Ctrl Pts',(-78.921506795546,-3.94958799012119,
135.594550453492));
#191379=CARTESIAN_POINT('Ctrl Pts',(-79.199954419359,1.89527359148086,136.71647546501));
#191380=CARTESIAN_POINT('Ctrl Pts',(-79.4784020431719,5.9984713317742,132.405455754592));
#191381=CARTESIAN_POINT('Ctrl Pts',(-79.7568496669848,4.58936695978296,
126.623107831093));
#191382=CARTESIAN_POINT('Ctrl Pts',(-80.0352972907976,-1.0371414452086,
124.683126952807));
#191383=CARTESIAN_POINT('Ctrl Pts',(-80.3137449146107,-5.71056752923021,
128.368260773546));
#191384=CARTESIAN_POINT('Ctrl Pts',(-80.5921925384234,-5.13626103062165,
134.292051340844));
#191385=CARTESIAN_POINT('Ctrl Pts',(-80.8706401622364,0.158018434826916,
137.010824516613));
#191386=CARTESIAN_POINT('Ctrl Pts',(-81.1490877860493,5.30708667829958,
134.026160571776));
#191387=CARTESIAN_POINT('Ctrl Pts',(-81.4275354098621,5.57920153001237,
128.080819862696));
#191388=CARTESIAN_POINT('Ctrl Pts',(-81.705983033675,0.724302734791404,
124.63828005498));
#191389=CARTESIAN_POINT('Ctrl Pts',(-81.984430657488,-4.79619488954742,
126.862067054498));
#191390=CARTESIAN_POINT('Ctrl Pts',(-82.2628782813007,-5.90922371753823,
132.708629246728));
#191391=CARTESIAN_POINT('Ctrl Pts',(-82.5413259051138,-1.59196463073914,
136.805261597452));
#191392=CARTESIAN_POINT('Ctrl Pts',(-82.8197735289264,4.18823217991362,
135.387359107972));
#191393=CARTESIAN_POINT('Ctrl Pts',(-83.0982211527395,6.11964822374235,
129.757904897731));
#191394=CARTESIAN_POINT('Ctrl Pts',(-83.3766687765523,2.42740651138818,
125.090092371815));
#191395=CARTESIAN_POINT('Ctrl Pts',(-83.6551164003652,-3.49550319953123,
125.67341320622));
#191396=CARTESIAN_POINT('Ctrl Pts',(-83.9335640241781,-6.20621623490623,
130.971824050937));
#191397=CARTESIAN_POINT('Ctrl Pts',(-84.2120116479911,-3.21371974092037,
136.116344181428));
#191398=CARTESIAN_POINT('Ctrl Pts',(-84.4904592718038,2.73202819603347,
136.379410921554));
#191399=CARTESIAN_POINT('Ctrl Pts',(-84.7689068956169,6.16717568783019,
131.519278788663));
#191400=CARTESIAN_POINT('Ctrl Pts',(-85.0473545194296,3.9349900057924,126.002171782228));
#191401=CARTESIAN_POINT('Ctrl Pts',(-85.3258021432425,-1.91325925661942,
124.898041715501));
#191402=CARTESIAN_POINT('Ctrl Pts',(-85.6042497670555,-6.00331673010926,
129.221530180052));
#191403=CARTESIAN_POINT('Ctrl Pts',(-85.8826973908683,-4.57661940695503,
134.999562491112));
#191404=CARTESIAN_POINT('Ctrl Pts',(-86.1611450146813,1.05576757090286,
136.922409227389));
#191405=CARTESIAN_POINT('Ctrl Pts',(-86.4395926384942,5.71795572821454,
133.223068174528));
#191406=CARTESIAN_POINT('Ctrl Pts',(-86.718040262307,5.12562190896342,127.301053037252));
#191407=CARTESIAN_POINT('Ctrl Pts',(-86.9964878861199,-0.176908044074368,
124.598406420195));
#191408=CARTESIAN_POINT('Ctrl Pts',(-87.2749355099329,-5.31686814704595,
127.598728532803));
#191409=CARTESIAN_POINT('Ctrl Pts',(-87.5533831337457,-5.57088616633168,
133.544869927476));
#191410=CARTESIAN_POINT('Ctrl Pts',(-87.8318307575586,-0.70553195167748,
136.972617147663));
#191411=CARTESIAN_POINT('Ctrl Pts',(-88.1102783813713,4.80817165941601,
134.732037952774));
#191412=CARTESIAN_POINT('Ctrl Pts',(-88.3887260051845,5.90340040775061,
128.882115164534));
#191413=CARTESIAN_POINT('Ctrl Pts',(-88.6671736289971,1.57369257850503,
124.798642040718));
#191414=CARTESIAN_POINT('Ctrl Pts',(-88.9456212528103,-4.20216185122988,
126.234130893362));
#191415=CARTESIAN_POINT('Ctrl Pts',(-89.2240688766231,-6.11643482670397,
131.869437594414));
#191416=CARTESIAN_POINT('Ctrl Pts',(-89.5025165004358,-2.41000300088966,
136.525990585645));
#191417=CARTESIAN_POINT('Ctrl Pts',(-89.7809641242489,3.51110384754994,
135.924645153375));
#191418=CARTESIAN_POINT('Ctrl Pts',(-90.0594117480617,6.20567778705031,
130.618008372501));
#191419=CARTESIAN_POINT('Ctrl Pts',(-90.3378593718745,3.19753700446471,
125.482620201028));
#191420=CARTESIAN_POINT('Ctrl Pts',(-90.6163069956876,-2.74898407685696,
125.237651490881));
#191421=CARTESIAN_POINT('Ctrl Pts',(-90.8947546195002,-6.16932308688508,
130.108216519297));
#191422=CARTESIAN_POINT('Ctrl Pts',(-91.1732022433134,-3.92035556825405,
135.618503965492));
#191423=CARTESIAN_POINT('Ctrl Pts',(-91.4516498671261,1.93122719758584,
136.70482885892));
#191424=CARTESIAN_POINT('Ctrl Pts',(-91.7300974909391,6.00810651453776,
132.368911692441));
#191425=CARTESIAN_POINT('Ctrl Pts',(-92.0085451147519,4.56382945695037,
126.595248520721));
#191426=CARTESIAN_POINT('Ctrl Pts',(-92.2869927385648,-1.07438391611076,
124.689553739443));
#191427=CARTESIAN_POINT('Ctrl Pts',(-92.5654403623776,-5.72529095683809,
128.403067754236));
#191428=CARTESIAN_POINT('Ctrl Pts',(-92.8438879861907,-5.11493530424405,
134.323252600751));
#191429=CARTESIAN_POINT('Ctrl Pts',(-93.1223356100035,0.195796014469281,
137.009747622148));
#191430=CARTESIAN_POINT('Ctrl Pts',(-93.4007832338166,5.32660036105212,
133.993795136343));
#191431=CARTESIAN_POINT('Ctrl Pts',(-93.6792308576291,5.56251919472255,
128.046908140318));
#191432=CARTESIAN_POINT('Ctrl Pts',(-93.9576784814422,0.686754632612129,
124.633985261843));
#191433=CARTESIAN_POINT('Ctrl Pts',(-94.2361261052551,-4.82010388703947,
126.891335895681));
#191434=CARTESIAN_POINT('Ctrl Pts',(-94.5145737290679,-5.8975224096676,
132.744565087048));
#191435=CARTESIAN_POINT('Ctrl Pts',(-94.7930213528811,-1.55540594779807,
136.814841155217));
#191436=CARTESIAN_POINT('Ctrl Pts',(-95.0714689766937,4.21605259429308,
135.361779237583));
#191437=CARTESIAN_POINT('Ctrl Pts',(-95.3499166005066,6.11316476784841,
129.720672250431));
#191438=CARTESIAN_POINT('Ctrl Pts',(-95.6283642243196,2.39257716445285,
125.075421931555));
#191439=CARTESIAN_POINT('Ctrl Pts',(-95.9068118481323,-3.52667196918255,
125.694786390909));
#191440=CARTESIAN_POINT('Ctrl Pts',(-96.1852594719453,-6.20508185064282,
131.009599947983));
#191441=CARTESIAN_POINT('Ctrl Pts',(-96.4637070957582,-3.18132464646333,
136.135808586901));
#191442=CARTESIAN_POINT('Ctrl Pts',(-96.742154719571,2.76591449146702,136.362676997713));
#191443=CARTESIAN_POINT('Ctrl Pts',(-97.020602343384,6.17141333417382,131.481724194021));
#191444=CARTESIAN_POINT('Ctrl Pts',(-97.299049967197,3.90568481307747,125.978307354616));
#191445=CARTESIAN_POINT('Ctrl Pts',(-97.5774975910097,-1.94917724792726,
124.909797698053));
#191446=CARTESIAN_POINT('Ctrl Pts',(-97.8559452148228,-6.01284064068852,
129.258103399115));
#191447=CARTESIAN_POINT('Ctrl Pts',(-98.1343928386354,-4.55099722825276,
135.027343945068));
#191448=CARTESIAN_POINT('Ctrl Pts',(-98.4128404624484,1.09299030837272,
136.915869117251));
#191449=CARTESIAN_POINT('Ctrl Pts',(-98.6912880862614,5.73257314714861,
133.188216542011));
#191450=CARTESIAN_POINT('Ctrl Pts',(-98.9697357100741,5.10420131546234,
127.269916830042));
#191451=CARTESIAN_POINT('Ctrl Pts',(-99.2481833338871,-0.214682171037078,
124.599598291628));
#191452=CARTESIAN_POINT('Ctrl Pts',(-99.5266309576999,-5.33628323016052,
127.631153211259));
#191453=CARTESIAN_POINT('Ctrl Pts',(-99.8050785815131,-5.55410069269506,
133.578730717485));
#191454=CARTESIAN_POINT('Ctrl Pts',(-100.083526205326,-0.667970951546107,
136.976797637399));
#191455=CARTESIAN_POINT('Ctrl Pts',(-100.361973829139,4.83199146187865,
134.702696476397));
#191456=CARTESIAN_POINT('Ctrl Pts',(-100.640421452952,5.89158977774298,
128.846215105423));
#191457=CARTESIAN_POINT('Ctrl Pts',(-100.918869076765,1.53710490802326,
124.789173799381));
#191458=CARTESIAN_POINT('Ctrl Pts',(-101.197316700577,-4.22990428042106,
126.259795321038));
#191459=CARTESIAN_POINT('Ctrl Pts',(-101.47576432439,-6.10983807746976,
131.906650335846));
#191460=CARTESIAN_POINT('Ctrl Pts',(-101.754211948203,-2.37512916350784,
136.540554949401));
#191461=CARTESIAN_POINT('Ctrl Pts',(-102.032659572016,3.54220742020778,
135.903177200671));
#191462=CARTESIAN_POINT('Ctrl Pts',(-102.311107195829,6.20442843120499,
130.580236103105));
#191463=CARTESIAN_POINT('Ctrl Pts',(-102.589554819642,3.16508281710451,
125.463254485237));
#191464=CARTESIAN_POINT('Ctrl Pts',(-102.868002443455,-2.78281928302352,
125.254488475437));
#191465=CARTESIAN_POINT('Ctrl Pts',(-103.146450067268,-6.1734464103326,
130.145783837928));
#191466=CARTESIAN_POINT('Ctrl Pts',(-103.424897691081,-3.8909778761698,
135.642279087639));
#191467=CARTESIAN_POINT('Ctrl Pts',(-103.703345314893,1.96710924135641,
136.69296360881));
#191468=CARTESIAN_POINT('Ctrl Pts',(-103.981792938706,6.01751906470488,
132.332309655276));
#191469=CARTESIAN_POINT('Ctrl Pts',(-104.260240562519,4.53812283973896,
126.567545180546));
#191470=CARTESIAN_POINT('Ctrl Pts',(-104.538688186332,-1.11158657532129,
124.696207112496));
#191471=CARTESIAN_POINT('Ctrl Pts',(-104.817135810145,-5.73980223168479,
128.437963715717));
#191472=CARTESIAN_POINT('Ctrl Pts',(-105.095583433958,-5.093420042057,134.354323466822));
#191473=CARTESIAN_POINT('Ctrl Pts',(-105.374031057771,0.233566338818549,
137.008440784786));
#191474=CARTESIAN_POINT('Ctrl Pts',(-105.652478681584,5.34591666467016,
133.961311515241));
#191475=CARTESIAN_POINT('Ctrl Pts',(-105.930926305397,5.54563073823764,
128.013098596357));
#191476=CARTESIAN_POINT('Ctrl Pts',(-106.20937392921,0.649181082487974,
124.629919114234));
#191477=CARTESIAN_POINT('Ctrl Pts',(-106.487821553022,-4.84383427380942,
126.920749735436));
#191478=CARTESIAN_POINT('Ctrl Pts',(-106.766269176835,-5.88560256693534,
132.780429032376));
#191479=CARTESIAN_POINT('Ctrl Pts',(-107.044716800648,-1.51878962871805,
136.824197992414));
#191480=CARTESIAN_POINT('Ctrl Pts',(-107.323164424461,4.2437167812931,135.336030490371));
#191481=CARTESIAN_POINT('Ctrl Pts',(-107.601612048274,6.10645478638612,
129.683479759601));
#191482=CARTESIAN_POINT('Ctrl Pts',(-107.880059672087,2.35765915969063,
125.060963779225));
#191483=CARTESIAN_POINT('Ctrl Pts',(-108.1585072959,-3.55771005670707,125.716348912751));
#191484=CARTESIAN_POINT('Ctrl Pts',(-108.436954919713,-6.20371753478999,
131.04736823981));
#191485=CARTESIAN_POINT('Ctrl Pts',(-108.715402543526,-3.14881166685081,
136.155075433609));
#191486=CARTESIAN_POINT('Ctrl Pts',(-108.993850167338,2.79969829492213,
136.345737108415));
#191487=CARTESIAN_POINT('Ctrl Pts',(-109.272297791151,6.17542229652738,
131.444144499421));
#191488=CARTESIAN_POINT('Ctrl Pts',(-109.550745414964,3.87623489377466,
125.954621758183));
#191489=CARTESIAN_POINT('Ctrl Pts',(-109.829193038777,-1.98502301175461,
124.921772105802));
#191490=CARTESIAN_POINT('Ctrl Pts',(-110.10764066259,-6.02214174324697,
129.294733915307));
#191491=CARTESIAN_POINT('Ctrl Pts',(-110.386088286403,-4.52520641067474,
135.054968914823));
#191492=CARTESIAN_POINT('Ctrl Pts',(-110.664535910216,1.13017254468408,
136.909102542919));
#191493=CARTESIAN_POINT('Ctrl Pts',(-110.942983534029,5.74697814347679,
133.153276574838));
#191494=CARTESIAN_POINT('Ctrl Pts',(-111.221431157841,5.08259158390449,
127.238911592946));
#191495=CARTESIAN_POINT('Ctrl Pts',(-111.499878781655,-0.252448342873548,
124.601020082813));
#191496=CARTESIAN_POINT('Ctrl Pts',(-111.778326405467,-5.3555005753377,
127.663695474083));
#191497=CARTESIAN_POINT('Ctrl Pts',(-112.05677402928,-5.53710940981492,
133.612488702192));
#191498=CARTESIAN_POINT('Ctrl Pts',(-112.335221653093,-0.630385199504834,
136.980749405212));
#191499=CARTESIAN_POINT('Ctrl Pts',(-112.613669276906,4.85563221312083,
134.673210545752));
#191500=CARTESIAN_POINT('Ctrl Pts',(-112.892116900719,5.8795608327098,128.810387606114));
#191501=CARTESIAN_POINT('Ctrl Pts',(-113.170564524532,1.50046027955312,
124.779928453004));
#191502=CARTESIAN_POINT('Ctrl Pts',(-113.449012148345,-4.25748996895278,
126.285628149252));
#191503=CARTESIAN_POINT('Ctrl Pts',(-113.727459772158,-6.10301492593933,
131.943822231527));
#191504=CARTESIAN_POINT('Ctrl Pts',(-114.00590739597,-2.3401673148416,136.554906756366));
#191505=CARTESIAN_POINT('Ctrl Pts',(-114.284355019783,3.57317973506622,
135.881520309444));
#191506=CARTESIAN_POINT('Ctrl Pts',(-114.562802643596,6.202949167983,130.542472138726));
#191507=CARTESIAN_POINT('Ctrl Pts',(-114.841250267409,3.13251134643626,
125.444086686097));
#191508=CARTESIAN_POINT('Ctrl Pts',(-115.119697891222,-2.81655137079845,
125.271531112549));
#191509=CARTESIAN_POINT('Ctrl Pts',(-115.398145515035,-6.17734097445314,
130.183375560363));
#191510=CARTESIAN_POINT('Ctrl Pts',(-115.676593138848,-3.86145600246928,
135.665874938939));
#191511=CARTESIAN_POINT('Ctrl Pts',(-115.955040762661,2.00291839317105,
136.680880154352));
#191512=CARTESIAN_POINT('Ctrl Pts',(-116.233488386474,6.02670863349017,
132.295650999397));
#191513=CARTESIAN_POINT('Ctrl Pts',(-116.511936010287,4.51224806071678,
126.539998837124));
#191514=CARTESIAN_POINT('Ctrl Pts',(-116.790383634099,-1.14874804428301,
124.703086825424));
#191515=CARTESIAN_POINT('Ctrl Pts',(-117.068831257912,-5.75410081604829,
128.472947364906));
#191516=CARTESIAN_POINT('Ctrl Pts',(-117.347278881725,-5.07171604131793,
134.385262787713));
#191517=CARTESIAN_POINT('Ctrl Pts',(-117.625726505538,0.271328008281021,
137.006904052952));
#191518=CARTESIAN_POINT('Ctrl Pts',(-117.904174129351,5.3650348733795,133.928710912162));
#191519=CARTESIAN_POINT('Ctrl Pts',(-118.182621753164,5.52853678636705,
127.979392483636));
#191520=CARTESIAN_POINT('Ctrl Pts',(-118.461069376977,0.611583476719488,
124.626081762825));
#191521=CARTESIAN_POINT('Ctrl Pts',(-118.73951700079,-4.86738517051901,
126.95030748382));
#191522=CARTESIAN_POINT('Ctrl Pts',(-119.017964624603,-5.87346463103546,
132.816219753764));
#191523=CARTESIAN_POINT('Ctrl Pts',(-119.296412248415,-1.48211703032935,
136.833331762325));
#191524=CARTESIAN_POINT('Ctrl Pts',(-119.574859872228,4.27122371580729,
135.310113820466));
#191525=CARTESIAN_POINT('Ctrl Pts',(-119.853307496041,6.09951852799569,
129.646328803424));
#191526=CARTESIAN_POINT('Ctrl Pts',(-120.131755119854,2.32265379100196,
125.046718450578));
#191527=CARTESIAN_POINT('Ctrl Pts',(-120.410202743667,-3.58861631197691,
125.738099972737));
#191528=CARTESIAN_POINT('Ctrl Pts',(-120.68865036748,-6.20212333790203,
131.085127526901));
#191529=CARTESIAN_POINT('Ctrl Pts',(-120.967097991293,-3.11618200686478,
136.174144007612));
#191530=CARTESIAN_POINT('Ctrl Pts',(-121.245545615105,2.83337835452712,
136.328591881372));
#191531=CARTESIAN_POINT('Ctrl Pts',(-121.523993238919,6.17920242633619,
131.406541097396));
#191532=CARTESIAN_POINT('Ctrl Pts',(-121.802440862731,3.84664133916317,
125.931115870606));
#191533=CARTESIAN_POINT('Ctrl Pts',(-122.080888486544,-2.02079521982502,
124.933964495032));
#191534=CARTESIAN_POINT('Ctrl Pts',(-122.359336110357,-6.03121969312815,
129.331420371272));
#191535=CARTESIAN_POINT('Ctrl Pts',(-122.63778373417,-4.49924790990888,
135.082436376724));
#191536=CARTESIAN_POINT('Ctrl Pts',(-122.916231357983,1.16731290203685,
136.90210975513));
#191537=CARTESIAN_POINT('Ctrl Pts',(-123.194678981796,5.76117018341619,
133.118249567719));
#191538=CARTESIAN_POINT('Ctrl Pts',(-123.473126605609,5.06079351504635,
127.208038474877));
#191539=CARTESIAN_POINT('Ctrl Pts',(-123.751574229422,-0.290205160143283,
124.602671741062));
#191540=CARTESIAN_POINT('Ctrl Pts',(-124.030021853235,-5.37451947047147,
127.696354115408));
#191541=CARTESIAN_POINT('Ctrl Pts',(-124.308469477047,-5.51991294730918,
133.646142630679));
#191542=CARTESIAN_POINT('Ctrl Pts',(-124.58691710086,-0.592776088308802,
136.984472304668));
#191543=CARTESIAN_POINT('Ctrl Pts',(-124.865364724673,4.87909303712557,
134.64358125345));
#191544=CARTESIAN_POINT('Ctrl Pts',(-125.143812348486,5.86731401838748,
128.774633994209));
#191545=CARTESIAN_POINT('Ctrl Pts',(-125.422259972299,1.46376005097626,
124.770906344175));
#191546=CARTESIAN_POINT('Ctrl Pts',(-125.700707596112,-4.28491789462882,
126.311628420759));
#191547=CARTESIAN_POINT('Ctrl Pts',(-125.979155219925,-6.09596562494584,
131.980951904039));
#191548=CARTESIAN_POINT('Ctrl Pts',(-126.257602843738,-2.30511875041471,
136.569045474729));
#191549=CARTESIAN_POINT('Ctrl Pts',(-126.536050467551,3.60401964443632,
135.859675282198));
#191550=CARTESIAN_POINT('Ctrl Pts',(-126.814498091363,6.20124005219796,
130.50471787872));
#191551=CARTESIAN_POINT('Ctrl Pts',(-127.092945715177,3.09982379940838,
125.42511751388));
#191552=CARTESIAN_POINT('Ctrl Pts',(-127.371393338989,-2.85017909022625,
125.288778770691));
#191553=CARTESIAN_POINT('Ctrl Pts',(-127.649840962802,-6.18100663493216,
130.220990293627));
#191554=CARTESIAN_POINT('Ctrl Pts',(-127.928288586615,-3.83179104109667,
135.689290645038));
#191555=CARTESIAN_POINT('Ctrl Pts',(-128.206736210428,2.03865332610762,
136.6685789433));
#191556=CARTESIAN_POINT('Ctrl Pts',(-128.485183834241,6.03567488037103,
132.258937083203));
#191557=CARTESIAN_POINT('Ctrl Pts',(-128.763631458054,4.48620607868298,
126.512610511197));
#191558=CARTESIAN_POINT('Ctrl Pts',(-129.042079081867,-1.18586694596332,
124.710192623294));
#191559=CARTESIAN_POINT('Ctrl Pts',(-129.32052670568,-5.76818618009069,
128.508017405469));
#191560=CARTESIAN_POINT('Ctrl Pts',(-129.598974329492,-5.04982410627509,
134.416069416958));
#191561=CARTESIAN_POINT('Ctrl Pts',(-129.877421953305,0.30907962358457,
137.005137483589));
#191562=CARTESIAN_POINT('Ctrl Pts',(-130.155869577118,5.38395427874936,
133.895994535135));
#191563=CARTESIAN_POINT('Ctrl Pts',(-130.434317200931,5.51123797253198,
127.945791051148));
#191564=CARTESIAN_POINT('Ctrl Pts',(-130.712764824744,0.573963208500954,
124.622473349811));
#191565=CARTESIAN_POINT('Ctrl Pts',(-130.991212448557,-4.89075570448117,
126.980008045559));
#191566=CARTESIAN_POINT('Ctrl Pts',(-131.26966007237,-5.8611090517438,132.851935924971));
#191567=CARTESIAN_POINT('Ctrl Pts',(-131.548107696183,-1.44538951154951,
136.842242126491));
#191568=CARTESIAN_POINT('Ctrl Pts',(-131.826555319995,4.29857237855583,
135.28403018822));
#191569=CARTESIAN_POINT('Ctrl Pts',(-132.105002943808,6.09235624970348,
129.609220758541));
#191570=CARTESIAN_POINT('Ctrl Pts',(-132.383450567622,2.28756235552218,
125.032686473479));
#191571=CARTESIAN_POINT('Ctrl Pts',(-132.661898191434,-3.6193895897498,
125.760038764874));
#191572=CARTESIAN_POINT('Ctrl Pts',(-132.940345815247,-6.20029931905343,
131.122876410071));
#191573=CARTESIAN_POINT('Ctrl Pts',(-133.21879343906,-3.08343687560774,
136.193013602317));
#191574=CARTESIAN_POINT('Ctrl Pts',(-133.497241062873,2.86695342225543,
136.311241951909));
#191575=CARTESIAN_POINT('Ctrl Pts',(-133.775688686686,6.18275358352724,
131.368915381349));
#191576=CARTESIAN_POINT('Ctrl Pts',(-134.054136310499,3.81690524584148,
125.907790562906));
#191577=CARTESIAN_POINT('Ctrl Pts',(-134.332583934311,-2.05649254658467,
124.946374413949));
#191578=CARTESIAN_POINT('Ctrl Pts',(-134.611031558124,-6.04007415394596,
129.36816140758));
#191579=CARTESIAN_POINT('Ctrl Pts',(-134.889479181937,-4.47312268785726,
135.109745312956));
#191580=CARTESIAN_POINT('Ctrl Pts',(-135.16792680575,1.20441000418008,136.894891013003));
#191581=CARTESIAN_POINT('Ctrl Pts',(-135.446374429563,5.775148741076,133.083136818595));
#191582=CARTESIAN_POINT('Ctrl Pts',(-135.724822053376,5.03880791662344,
127.177298619846));
#191583=CARTESIAN_POINT('Ctrl Pts',(-136.003269677189,-0.327951223754644,
124.604553205172));
#191584=CARTESIAN_POINT('Ctrl Pts',(-136.281717301002,-5.39333921080989,
127.729127925058));
#191585=CARTESIAN_POINT('Ctrl Pts',(-136.560164924815,-5.50251194239939,
133.679691255889));
#191586=CARTESIAN_POINT('Ctrl Pts',(-136.838612548628,-0.555145011576188,
136.987966197812));
#191587=CARTESIAN_POINT('Ctrl Pts',(-137.117060172441,4.90237306454367,
134.613809697415));
#191588=CARTESIAN_POINT('Ctrl Pts',(-137.395507796253,5.8548497885868,128.73895559457));
#191589=CARTESIAN_POINT('Ctrl Pts',(-137.673955420066,1.42700558223168,
124.762107807213));
#191590=CARTESIAN_POINT('Ctrl Pts',(-137.952403043879,-4.3121870410957,
126.33779517211));
#191591=CARTESIAN_POINT('Ctrl Pts',(-138.230850667692,-6.08869043570493,
132.018037977528));
#191592=CARTESIAN_POINT('Ctrl Pts',(-138.509298291505,-2.26998476896503,
136.582970580575));
#191593=CARTESIAN_POINT('Ctrl Pts',(-138.787745915318,3.63472600553235,
135.837642928407));
#191594=CARTESIAN_POINT('Ctrl Pts',(-139.066193539131,6.1993011471828,130.466974722087));
#191595=CARTESIAN_POINT('Ctrl Pts',(-139.344641162943,3.06702138726935,
125.406347671494));
#191596=CARTESIAN_POINT('Ctrl Pts',(-139.623088786757,-2.88370119522,125.306230810748));
#191597=CARTESIAN_POINT('Ctrl Pts',(-139.901536410569,-6.18444325593727,
130.258626643894));
#191598=CARTESIAN_POINT('Ctrl Pts',(-140.179984034382,-3.80198409129777,
135.712525338258));
#191599=CARTESIAN_POINT('Ctrl Pts',(-140.458431658195,2.07431271599591,
136.656060431482));
#191600=CARTESIAN_POINT('Ctrl Pts',(-140.736879282008,6.04441747309895,
132.222169267145));
#191601=CARTESIAN_POINT('Ctrl Pts',(-141.015326905821,4.45999785863389,
126.485381217648));
#191602=CARTESIAN_POINT('Ctrl Pts',(-141.293774529634,-1.22294190490765,
124.717524242802));
#191603=CARTESIAN_POINT('Ctrl Pts',(-141.572222153447,-5.78205780187226,
128.543172537875));
#191604=CARTESIAN_POINT('Ctrl Pts',(-141.85066977726,-5.02774504814366,
134.446742213005));
#191605=CARTESIAN_POINT('Ctrl Pts',(-142.129117401072,0.346819785828787,
137.003141142159));
#191606=CARTESIAN_POINT('Ctrl Pts',(-142.407565024885,5.40267417971275,
133.863163596476));
#191607=CARTESIAN_POINT('Ctrl Pts',(-142.686012648698,5.49373493774783,
127.912295544006));
#191608=CARTESIAN_POINT('Ctrl Pts',(-142.964460272511,0.536321671864061,
124.619094008905));
#191609=CARTESIAN_POINT('Ctrl Pts',(-143.242907896324,-4.91394500969209,
127.00985032009));
#191610=CARTESIAN_POINT('Ctrl Pts',(-143.521355520137,-5.84853628690073,
132.887576222521));
#191611=CARTESIAN_POINT('Ctrl Pts',(-143.79980314395,-1.40860843332932,
136.850928754739));
#191612=CARTESIAN_POINT('Ctrl Pts',(-144.078250767763,4.32576175612421,
135.257780560169));
#191613=CARTESIAN_POINT('Ctrl Pts',(-144.356698391576,6.08496821690962,
129.572157000006));
#191614=CARTESIAN_POINT('Ctrl Pts',(-144.635146015388,2.2523861535788,125.018868367886));
#191615=CARTESIAN_POINT('Ctrl Pts',(-144.913593639201,-3.65002874971022,
125.782164476213));
#191616=CARTESIAN_POINT('Ctrl Pts',(-145.192041263014,-6.19824554583293,
131.160613490521));
#191617=CARTESIAN_POINT('Ctrl Pts',(-145.470488886827,-3.05057748646412,
136.211683518503));
#191618=CARTESIAN_POINT('Ctrl Pts',(-145.74893651064,2.90042225397064,136.293687962933));
#191619=CARTESIAN_POINT('Ctrl Pts',(-146.027384134453,6.18607563651005,
131.33126874552));
#191620=CARTESIAN_POINT('Ctrl Pts',(-146.305831758266,3.78702771569254,
125.884646699409));
#191621=CARTESIAN_POINT('Ctrl Pts',(-146.584279382079,-2.09211366925746,
124.959001402698));
#191622=CARTESIAN_POINT('Ctrl Pts',(-146.862727005891,-6.04870479759444,
129.404955662777));
#191623=CARTESIAN_POINT('Ctrl Pts',(-147.141174629705,-4.4468317125993,
135.136894711575));
#191624=CARTESIAN_POINT('Ctrl Pts',(-147.419622253517,1.24146247646836,
136.887446584034));
#191625=CARTESIAN_POINT('Ctrl Pts',(-147.69806987733,5.78891329847519,133.04793962858));
#191626=CARTESIAN_POINT('Ctrl Pts',(-147.976517501143,5.01663560332014,
127.146693166932));
#191627=CARTESIAN_POINT('Ctrl Pts',(-148.254965124956,-0.365685135012239,
124.606664405427));
#191628=CARTESIAN_POINT('Ctrl Pts',(-148.533412748769,-5.41195909898036,
127.762015688586));
#191629=CARTESIAN_POINT('Ctrl Pts',(-148.811860372582,-5.48490703988586,
133.713133334664));
#191630=CARTESIAN_POINT('Ctrl Pts',(-149.090307996395,-0.517493363741682,
136.991230955176));
#191631=CARTESIAN_POINT('Ctrl Pts',(-149.368755620208,4.92547143272535,
134.583896980843));
#191632=CARTESIAN_POINT('Ctrl Pts',(-149.647203244021,5.84216860517359,
128.703353729273));
#191633=CARTESIAN_POINT('Ctrl Pts',(-149.925650867833,1.39019823527075,
124.753533168151));
#191634=CARTESIAN_POINT('Ctrl Pts',(-150.204098491647,-4.33929639788676,
126.364127433687));
#191635=CARTESIAN_POINT('Ctrl Pts',(-150.482546115459,-6.08118962780021,
132.055079077756));
#191636=CARTESIAN_POINT('Ctrl Pts',(-150.760993739272,-2.23476667239474,
136.596681557904));
#191637=CARTESIAN_POINT('Ctrl Pts',(-151.039441363085,3.66529768052036,
135.81542406449));
#191638=CARTESIAN_POINT('Ctrl Pts',(-151.317888986898,6.19713252478332,
130.429244067412));
#191639=CARTESIAN_POINT('Ctrl Pts',(-151.596336610711,3.03410532552526,
125.387777854462));
#191640=CARTESIAN_POINT('Ctrl Pts',(-151.874784234524,-2.91711644360522,
125.323886586026));
#191641=CARTESIAN_POINT('Ctrl Pts',(-152.153231858337,-6.18765071012318,
130.296283216534));
#191642=CARTESIAN_POINT('Ctrl Pts',(-152.431679482149,-3.77203625758034,
135.735578157629));
#191643=CARTESIAN_POINT('Ctrl Pts',(-152.710127105962,2.10989524146327,
136.643325082775));
#191644=CARTESIAN_POINT('Ctrl Pts',(-152.988574729775,6.0529360877152,132.185348913665));
#191645=CARTESIAN_POINT('Ctrl Pts',(-153.267022353588,4.43362437172323,
126.458311965469));
#191646=CARTESIAN_POINT('Ctrl Pts',(-153.545469977401,-1.25997154729018,
124.725081412269));
#191647=CARTESIAN_POINT('Ctrl Pts',(-153.823917601214,-5.79571516737629,
128.578411459437));
#191648=CARTESIAN_POINT('Ctrl Pts',(-154.102365225027,-5.00547968506979,
134.477280039263));
#191649=CARTESIAN_POINT('Ctrl Pts',(-154.38081284884,0.38454709653853,137.000915102638));
#191650=CARTESIAN_POINT('Ctrl Pts',(-154.659260472653,5.4211938825983,133.830219312748));
#191651=CARTESIAN_POINT('Ctrl Pts',(-154.937708096465,5.47602833059452,
127.8789072034));
#191652=CARTESIAN_POINT('Ctrl Pts',(-155.216155720278,0.498660261630971,
124.615943865326));
#191653=CARTESIAN_POINT('Ctrl Pts',(-155.494603344091,-4.93695222686361,
127.039833201595));
#191654=CARTESIAN_POINT('Ctrl Pts',(-155.773050967904,-5.83574680239484,
132.923139325752));
#191655=CARTESIAN_POINT('Ctrl Pts',(-156.051498591717,-1.37177515860606,
136.85939132518));
#191656=CARTESIAN_POINT('Ctrl Pts',(-156.32994621553,4.3527908409998,135.231365909006));
#191657=CARTESIAN_POINT('Ctrl Pts',(-156.608393839343,6.0773547033811,129.535138901228));
#191658=CARTESIAN_POINT('Ctrl Pts',(-156.886841463156,2.21712648863745,
125.005264645838));
#191659=CARTESIAN_POINT('Ctrl Pts',(-157.165289086968,-3.68053265651321,
125.804476286877));
#191660=CARTESIAN_POINT('Ctrl Pts',(-157.443736710782,-6.19596209434481,
131.19833736989));
#191661=CARTESIAN_POINT('Ctrl Pts',(-157.722184334594,-3.0176050570491,
136.230153064351));
#191662=CARTESIAN_POINT('Ctrl Pts',(-158.000631958407,2.93378360947182,
136.275930564914));
#191663=CARTESIAN_POINT('Ctrl Pts',(-158.27907958222,6.18916846218569,131.293602584915));
#191664=CARTESIAN_POINT('Ctrl Pts',(-158.557527206033,3.7570098558391,125.861685137721));
#191665=CARTESIAN_POINT('Ctrl Pts',(-158.835974829846,-2.12765726788813,
124.971844993383));
#191666=CARTESIAN_POINT('Ctrl Pts',(-159.114422453659,-6.05711130426257,
129.44180177344));
#191667=CARTESIAN_POINT('Ctrl Pts',(-159.392870077472,-4.42037595835707,
135.163883566548));
#191668=CARTESIAN_POINT('Ctrl Pts',(-159.671317701285,1.27846894590735,
136.879776744077));
#191669=CARTESIAN_POINT('Ctrl Pts',(-159.949765325097,5.80246334556346,
133.01265930192));
#191670=CARTESIAN_POINT('Ctrl Pts',(-160.22821294891,4.9942773967397,127.116223250229));
#191671=CARTESIAN_POINT('Ctrl Pts',(-160.506660572723,-0.403405495673234,
124.609005263594));
#191672=CARTESIAN_POINT('Ctrl Pts',(-160.785108196536,-5.43037844501628,
127.795016187323));
#191673=CARTESIAN_POINT('Ctrl Pts',(-161.063555820349,-5.46709889212507,
133.746467627798));
#191674=CARTESIAN_POINT('Ctrl Pts',(-161.342003444162,-0.479822539999598,
136.994266455786));
#191675=CARTESIAN_POINT('Ctrl Pts',(-161.620451067975,4.94838728575097,
134.553844212161));
#191676=CARTESIAN_POINT('Ctrl Pts',(-161.898898691787,5.82927093805496,
128.66782971756));
#191677=CARTESIAN_POINT('Ctrl Pts',(-162.177346315601,1.35333937400316,
124.745182744726));
#191678=CARTESIAN_POINT('Ctrl Pts',(-162.455793939413,-4.36624496045326,
126.390624229737));
#191679=CARTESIAN_POINT('Ctrl Pts',(-162.734241563226,-6.07346347917808,
132.092073832152));
#191680=CARTESIAN_POINT('Ctrl Pts',(-163.012689187039,-2.19946576572379,
136.61017789865));
#191681=CARTESIAN_POINT('Ctrl Pts',(-163.291136810852,3.69573353655413,
135.793019513774));
#191682=CARTESIAN_POINT('Ctrl Pts',(-163.569584434665,6.19473426535967,
130.391527312818));
#191683=CARTESIAN_POINT('Ctrl Pts',(-163.848032058478,3.0010768338922,125.369408750896));
#191684=CARTESIAN_POINT('Ctrl Pts',(-164.126479682291,-2.95042359716811,
125.341745442286));
#191685=CARTESIAN_POINT('Ctrl Pts',(-164.404927306104,-6.19062887863655,
130.333958616169));
#191686=CARTESIAN_POINT('Ctrl Pts',(-164.683374929917,-3.74194864967208,
135.758448248921));
#191687=CARTESIAN_POINT('Ctrl Pts',(-164.961822553729,2.14539958398697,
136.630373369092));
#191688=CARTESIAN_POINT('Ctrl Pts',(-165.240270177542,6.06123040855813,
132.148477387157));
#191689=CARTESIAN_POINT('Ctrl Pts',(-165.518717801355,4.40708659523179,
126.431403757722));
#191690=CARTESIAN_POINT('Ctrl Pts',(-165.797165425168,-1.29695450096345,
124.732863851664));
#191691=CARTESIAN_POINT('Ctrl Pts',(-166.075613048981,-5.80915777052276,
128.613732864363));
#191692=CARTESIAN_POINT('Ctrl Pts',(-166.354060672794,-4.98302884210618,
134.50768176414));
#191693=CARTESIAN_POINT('Ctrl Pts',(-166.632508296607,0.422260157714416,
136.998459447511));
#191694=CARTESIAN_POINT('Ctrl Pts',(-166.91095592042,5.43951270115045,133.797162904712));
#191695=CARTESIAN_POINT('Ctrl Pts',(-167.189403544233,5.45811880719792,
127.845627266545));
#191696=CARTESIAN_POINT('Ctrl Pts',(-167.467851168046,0.460980373357943,
124.613023035806));
#191697=CARTESIAN_POINT('Ctrl Pts',(-167.746298791858,-4.95977650345479,
127.069955579048));
#191698=CARTESIAN_POINT('Ctrl Pts',(-168.024746415672,-5.822741072145,132.958623916859));
#191699=CARTESIAN_POINT('Ctrl Pts',(-168.303194039484,-1.33489105224939,
136.867629524233));
#191700=CARTESIAN_POINT('Ctrl Pts',(-168.581641663297,4.37965863161014,
135.204787213532));
#191701=CARTESIAN_POINT('Ctrl Pts',(-168.86008928711,6.06951599123876,129.498167833929));
#191702=CARTESIAN_POINT('Ctrl Pts',(-169.138536910923,2.18178466725943,
124.991875811423));
#191703=CARTESIAN_POINT('Ctrl Pts',(-169.416984534736,-3.71090017982492,
125.826973370093));
#191704=CARTESIAN_POINT('Ctrl Pts',(-169.695432158549,-6.19344904920226,
131.236046650305));
#191705=CARTESIAN_POINT('Ctrl Pts',(-169.973879782361,-2.98452080916978,
136.248421555465));
#191706=CARTESIAN_POINT('Ctrl Pts',(-170.252327406175,2.96703625254325,
136.257970415857));
#191707=CARTESIAN_POINT('Ctrl Pts',(-170.530775029987,6.19203194594742,
131.25591829527));
#191708=CARTESIAN_POINT('Ctrl Pts',(-170.8092226538,3.72685277860365,125.838906728691));
#191709=CARTESIAN_POINT('Ctrl Pts',(-171.087670277614,-2.16312202539704,
124.984904710079));
#191710=CARTESIAN_POINT('Ctrl Pts',(-171.366117901426,-6.06529336244348,
129.478698374222));
#191711=CARTESIAN_POINT('Ctrl Pts',(-171.644565525239,-4.39375640545797,
135.190710877796));
#191712=CARTESIAN_POINT('Ctrl Pts',(-171.923013149052,1.31542804121008,
136.871881777341));
#191713=CARTESIAN_POINT('Ctrl Pts',(-172.201460772865,5.81579838023838,
132.977297145939));
#191714=CARTESIAN_POINT('Ctrl Pts',(-172.479908396678,4.97173412537368,
127.085889998814));
#191715=CARTESIAN_POINT('Ctrl Pts',(-172.75835602049,-0.441110907994683,
124.611575692932));
#191716=CARTESIAN_POINT('Ctrl Pts',(-173.036803644304,-5.4485965663818,
127.828128198426));
#191717=CARTESIAN_POINT('Ctrl Pts',(-173.315251268116,-5.44908815900415,
133.779692900072));
#191718=CARTESIAN_POINT('Ctrl Pts',(-173.593698891929,-0.442133936257506,
136.997072587158));
#191719=CARTESIAN_POINT('Ctrl Pts',(-173.872146515742,4.97111977446672,
134.523652504987));
#191720=CARTESIAN_POINT('Ctrl Pts',(-174.150594139555,5.81615726515733,
128.632384875785));
#191721=CARTESIAN_POINT('Ctrl Pts',(-174.429041763368,1.31643036424716,
124.737056846366));
#191722=CARTESIAN_POINT('Ctrl Pts',(-174.707489387181,-4.39303173020782,
126.417284578411));
#191723=CARTESIAN_POINT('Ctrl Pts',(-174.985937010994,-6.06551227613263,
132.129020869861));
#191724=CARTESIAN_POINT('Ctrl Pts',(-175.264384634806,-2.16408335703982,
136.623459102702));
#191725=CARTESIAN_POINT('Ctrl Pts',(-175.542832258619,3.72603244582337,
135.770430106468));
#191726=CARTESIAN_POINT('Ctrl Pts',(-175.821279882432,6.19210645777918,
130.353825855915));
#191727=CARTESIAN_POINT('Ctrl Pts',(-176.099727506245,2.96793713625374,
125.351241041473));
#191728=CARTESIAN_POINT('Ctrl Pts',(-176.378175130058,-2.98362142169932,
125.359806717758));
#191729=CARTESIAN_POINT('Ctrl Pts',(-176.656622753871,-6.19337765112022,
130.371651446723));
#191730=CARTESIAN_POINT('Ctrl Pts',(-176.935070377684,-3.71172238248064,
135.781134764673));
#191731=CARTESIAN_POINT('Ctrl Pts',(-177.213518001496,2.18082442793968,
136.617205770365));
#191732=CARTESIAN_POINT('Ctrl Pts',(-177.49196562531,6.06930012827989,132.111556053907));
#191733=CARTESIAN_POINT('Ctrl Pts',(-177.770413249122,4.38038551252508,
126.404657591498));
#191734=CARTESIAN_POINT('Ctrl Pts',(-178.048860872936,-1.33388939551094,
124.740871272604));
#191735=CARTESIAN_POINT('Ctrl Pts',(-178.327308496748,-5.82238511319243,
128.649135443807));
#191736=CARTESIAN_POINT('Ctrl Pts',(-178.605756120561,-4.96039335117553,
134.537946261091));
#191737=CARTESIAN_POINT('Ctrl Pts',(-178.884203744374,0.459957571884186,
136.995774267775));
#191738=CARTESIAN_POINT('Ctrl Pts',(-179.162651368187,5.45762995655925,
133.763995597288));
#191739=CARTESIAN_POINT('Ctrl Pts',(-179.441098991999,5.44000703120181,
127.812456966643));
#191740=CARTESIAN_POINT('Ctrl Pts',(-179.719546615813,0.423283403288203,
124.610331628578));
#191741=CARTESIAN_POINT('Ctrl Pts',(-179.997994239625,-4.98241699370369,
127.100216336253));
#191742=CARTESIAN_POINT('Ctrl Pts',(-180.276441863438,-5.80951957808352,
132.994028680947));
#191743=CARTESIAN_POINT('Ctrl Pts',(-180.554889487251,-1.29795748101432,
136.875643046625));
#191744=CARTESIAN_POINT('Ctrl Pts',(-180.833337111064,4.40636413235919,
135.178045458633));
#191745=CARTESIAN_POINT('Ctrl Pts',(-181.111784734877,6.06145237094964,
129.461245168083));
#191746=CARTESIAN_POINT('Ctrl Pts',(-181.39023235869,2.14636199904753,124.97870236077));
#191747=CARTESIAN_POINT('Ctrl Pts',(-181.668679982503,-3.74113019436597,
125.849654892224));
#191748=CARTESIAN_POINT('Ctrl Pts',(-181.947127606316,-6.19070650352801,
131.273739934436));
#191749=CARTESIAN_POINT('Ctrl Pts',(-182.225575230128,-2.95132596877351,
136.266488314898));
#191750=CARTESIAN_POINT('Ctrl Pts',(-182.504022853942,3.00017895099442,
136.239808181284));
#191751=CARTESIAN_POINT('Ctrl Pts',(-182.782470477755,6.19466598168877,
131.218217272988));
#191752=CARTESIAN_POINT('Ctrl Pts',(-183.060918101567,3.6965576014681,125.81631231638));
#191753=CARTESIAN_POINT('Ctrl Pts',(-183.33936572538,-2.19850662762309,
124.998180068855));
#191754=CARTESIAN_POINT('Ctrl Pts',(-183.617813349193,-6.07325066894868,
129.515644097905));
#191755=CARTESIAN_POINT('Ctrl Pts',(-183.896260973006,-4.36697404029963,
135.217375651221));
#191756=CARTESIAN_POINT('Ctrl Pts',(-184.174708596819,1.35233839284232,
136.863761976378));
#191757=CARTESIAN_POINT('Ctrl Pts',(-184.453156220632,5.8289179083658,132.941854470998));
#191758=CARTESIAN_POINT('Ctrl Pts',(-184.731603844444,4.94900662457131,
127.055694536694));
#191759=CARTESIAN_POINT('Ctrl Pts',(-185.010051468258,-0.478799974789776,
124.614375598192));
#191760=CARTESIAN_POINT('Ctrl Pts',(-185.28849909207,-5.46661278799793,
127.861350494915));
#191761=CARTESIAN_POINT('Ctrl Pts',(-185.566946715884,-5.43087550791776,
133.812807920317));
#191762=CARTESIAN_POINT('Ctrl Pts',(-185.845394339696,-0.404428949079144,
136.999649245311));
#191763=CARTESIAN_POINT('Ctrl Pts',(-186.123841963509,4.99366805651034,
134.493322978084));
#191764=CARTESIAN_POINT('Ctrl Pts',(-186.402289587322,5.80282807241402,
128.59702051737));
#191765=CARTESIAN_POINT('Ctrl Pts',(-186.680737211135,1.27947257368013,
124.729155774178));
#191766=CARTESIAN_POINT('Ctrl Pts',(-186.959184834948,-4.41965571455532,
126.444107491802));
#191767=CARTESIAN_POINT('Ctrl Pts',(-187.237632458761,-6.0573363132998,
132.165918821797));
#191768=CARTESIAN_POINT('Ctrl Pts',(-187.516080082574,-2.12862075745111,
136.636524677919));
#191769=CARTESIAN_POINT('Ctrl Pts',(-187.794527706387,3.75619328558978,
135.74765667963));
#191770=CARTESIAN_POINT('Ctrl Pts',(-188.072975330199,6.18924919941703,
130.316141093742));
#191771=CARTESIAN_POINT('Ctrl Pts',(-188.351422954013,2.93468746061294,
125.333275399398));
#191772=CARTESIAN_POINT('Ctrl Pts',(-188.629870577825,-3.01670868704181,
125.378069743179));
#191773=CARTESIAN_POINT('Ctrl Pts',(-188.908318201638,-6.19589692571743,
130.409360311474));
#191774=CARTESIAN_POINT('Ctrl Pts',(-189.186765825451,-3.68135857605119,
135.80363686423));
#191775=CARTESIAN_POINT('Ctrl Pts',(-189.465213449264,2.21616846064164,
136.603822774524));
#191776=CARTESIAN_POINT('Ctrl Pts',(-189.743661073077,6.07714494785282,
132.07458628205));
#191777=CARTESIAN_POINT('Ctrl Pts',(-190.02210869689,4.35352211302309,126.378074457888));
#191778=CARTESIAN_POINT('Ctrl Pts',(-190.300556320702,-1.37077486229612,
124.749103378371));
#191779=CARTESIAN_POINT('Ctrl Pts',(-190.579003944516,-5.83539670523986,
128.684617885911));
#191780=CARTESIAN_POINT('Ctrl Pts',(-190.857451568328,-4.93757405104588,
134.568072408653));
#191781=CARTESIAN_POINT('Ctrl Pts',(-191.135899192141,0.497637942157669,
136.992859662928));
#191782=CARTESIAN_POINT('Ctrl Pts',(-191.414346815954,5.47554497748281,
133.730718619501));
#191783=CARTESIAN_POINT('Ctrl Pts',(-191.692794439767,5.42169367374449,
127.779397532831));
#191784=CARTESIAN_POINT('Ctrl Pts',(-191.97124206358,0.385570748295746,
124.60786974337));
#191785=CARTESIAN_POINT('Ctrl Pts',(-192.249689687393,-5.00487285865859,
127.130614351886));
#191786=CARTESIAN_POINT('Ctrl Pts',(-192.528137311206,-5.79608281013753,
133.029352306079));
#191787=CARTESIAN_POINT('Ctrl Pts',(-192.806584935019,-1.26097581348702,
136.883431595415));
#191788=CARTESIAN_POINT('Ctrl Pts',(-193.085032558831,4.43290635366497,
135.151141635234));
#191789=CARTESIAN_POINT('Ctrl Pts',(-193.363480182644,6.05316414131348,
129.424372271875));
#191790=CARTESIAN_POINT('Ctrl Pts',(-193.641927806457,2.11085979660312,
124.965744782026));
#191791=CARTESIAN_POINT('Ctrl Pts',(-193.92037543027,-3.77122157995168,
125.872520012798));
#191792=CARTESIAN_POINT('Ctrl Pts',(-194.198823054083,-6.1877345589472,
131.311415825543));
#191793=CARTESIAN_POINT('Ctrl Pts',(-194.477270677896,-2.91802176590892,
136.284352673182));
#191794=CARTESIAN_POINT('Ctrl Pts',(-194.755718301709,3.03321047671203,
136.221444534203));
#191795=CARTESIAN_POINT('Ctrl Pts',(-195.034165925522,6.19707047180361,
131.180500915096));
#191796=CARTESIAN_POINT('Ctrl Pts',(-195.312613549334,3.66612544703105,
125.793902738034));
#191797=CARTESIAN_POINT('Ctrl Pts',(-195.591061173148,-2.23380976337827,
125.011670577786));
#191798=CARTESIAN_POINT('Ctrl Pts',(-195.86950879696,-6.08098292891658,
129.552637575454));
#191799=CARTESIAN_POINT('Ctrl Pts',(-196.147956420774,-4.3400298553121,
135.243876898752));
#191800=CARTESIAN_POINT('Ctrl Pts',(-196.426404044586,1.38919863307876,
136.855417642068));
#191801=CARTESIAN_POINT('Ctrl Pts',(-196.704851668399,5.84182144379631,
132.906332590435));
#191802=CARTESIAN_POINT('Ctrl Pts',(-196.983299292212,4.92609573650846,
127.025637982775));
#191803=CARTESIAN_POINT('Ctrl Pts',(-197.261746916025,-0.516471299475173,
124.617404875624));
#191804=CARTESIAN_POINT('Ctrl Pts',(-197.540194539838,-5.48442644226676,
127.894681845726));
#191805=CARTESIAN_POINT('Ctrl Pts',(-197.81864216365,-5.41246161374207,
133.845811461438));
#191806=CARTESIAN_POINT('Ctrl Pts',(-198.097089787464,-0.36670897563802,
137.001996334766));
#191807=CARTESIAN_POINT('Ctrl Pts',(-198.375537411276,5.01603129634849,
134.462856755322));
#191808=CARTESIAN_POINT('Ctrl Pts',(-198.65398503509,5.78928385374183,128.561737952753));
#191809=CARTESIAN_POINT('Ctrl Pts',(-198.932432658902,1.24246737178614,
124.721479820939));
#191810=CARTESIAN_POINT('Ctrl Pts',(-199.210880282716,-4.44611592693577,
126.471091975977));
#191811=CARTESIAN_POINT('Ctrl Pts',(-199.489327906528,-6.04893589364168,
132.202766320694));
#191812=CARTESIAN_POINT('Ctrl Pts',(-199.767775530341,-2.09307928103787,
136.649374140152));
#191813=CARTESIAN_POINT('Ctrl Pts',(-200.046223154153,3.7862149382325,135.724700077139));
#191814=CARTESIAN_POINT('Ctrl Pts',(-200.324670777967,6.18616259614969,
130.278474422724));
#191815=CARTESIAN_POINT('Ctrl Pts',(-200.603118401779,2.90132903904936,
125.315512490399));
#191816=CARTESIAN_POINT('Ctrl Pts',(-200.881566025592,-3.04968416713424,
125.396533841802));
#191817=CARTESIAN_POINT('Ctrl Pts',(-201.160013649405,-6.1981866090755,
130.447083813107));
#191818=CARTESIAN_POINT('Ctrl Pts',(-201.438461273218,-3.65085835552605,
135.825953713766));
#191819=CARTESIAN_POINT('Ctrl Pts',(-201.716908897031,2.2514303724059,136.590224877478));
#191820=CARTESIAN_POINT('Ctrl Pts',(-201.995356520844,6.08476457658541,
132.037569441512));
#191821=CARTESIAN_POINT('Ctrl Pts',(-202.273804144657,4.32649739215744,
126.35165534194));
#191822=CARTESIAN_POINT('Ctrl Pts',(-202.55225176847,-1.40760953451491,
124.757559863922));
#191823=CARTESIAN_POINT('Ctrl Pts',(-202.830699392283,-5.84819206451709,
128.720178875862));
#191824=CARTESIAN_POINT('Ctrl Pts',(-203.109147016096,-4.91457178729319,
134.59805909049));
#191825=CARTESIAN_POINT('Ctrl Pts',(-203.387594639908,0.535299872273523,
136.989715740974));
#191826=CARTESIAN_POINT('Ctrl Pts',(-203.666042263721,5.49325710007376,
133.697333204442));
#191827=CARTESIAN_POINT('Ctrl Pts',(-203.944489887534,5.40317941343439,
127.746450190138));
#191828=CARTESIAN_POINT('Ctrl Pts',(-204.222937511347,0.347843805837959,
124.605637471411));
#191829=CARTESIAN_POINT('Ctrl Pts',(-204.50138513516,-5.0271432662092,127.161148499539));
#191830=CARTESIAN_POINT('Ctrl Pts',(-204.779832758973,-5.78243126621161,
133.064593483327));
#191831=CARTESIAN_POINT('Ctrl Pts',(-205.058280382786,-1.22394742003769,
136.890994881994));
#191832=CARTESIAN_POINT('Ctrl Pts',(-205.336728006599,4.45928431199552,
135.124076740266));
#191833=CARTESIAN_POINT('Ctrl Pts',(-205.615175630412,6.04465160945437,
129.387550511641));
#191834=CARTESIAN_POINT('Ctrl Pts',(-205.893623254225,2.07527937547198,
124.953003555339));
#191835=CARTESIAN_POINT('Ctrl Pts',(-206.172070878037,-3.80117322153507,
125.89556788454));
#191836=CARTESIAN_POINT('Ctrl Pts',(-206.45051850185,-6.18453332558722,
131.349072927534));
#191837=CARTESIAN_POINT('Ctrl Pts',(-206.728966125663,-2.8846094346739,
136.302013968343));
#191838=CARTESIAN_POINT('Ctrl Pts',(-207.007413749476,3.06612960569919,
136.202880155086));
#191839=CARTESIAN_POINT('Ctrl Pts',(-207.285861373289,6.19924532719362,
131.142770619188));
#191840=CARTESIAN_POINT('Ctrl Pts',(-207.564308997102,3.63555744296752,
125.771678824048));
#191841=CARTESIAN_POINT('Ctrl Pts',(-207.842756620915,-2.26903012449045,
125.025375736976));
#191842=CARTESIAN_POINT('Ctrl Pts',(-208.121204244728,-6.08848985582611,
129.58967743606));
#191843=CARTESIAN_POINT('Ctrl Pts',(-208.399651868541,-4.31292484892225,
135.270213638376));
#191844=CARTESIAN_POINT('Ctrl Pts',(-208.678099492353,1.42600739604885,
136.846849083615));
#191845=CARTESIAN_POINT('Ctrl Pts',(-208.956547116166,5.85450850838505,
132.870732820528));
#191846=CARTESIAN_POINT('Ctrl Pts',(-209.234994739979,4.90300231015654,
126.995721450812));
#191847=CARTESIAN_POINT('Ctrl Pts',(-209.513442363792,-0.554123486127181,
124.620663412976));
#191848=CARTESIAN_POINT('Ctrl Pts',(-209.791889987605,-5.50203686909699,
127.928121015754));
#191849=CARTESIAN_POINT('Ctrl Pts',(-210.070337611418,-5.393847158811,133.878702300482));
#191850=CARTESIAN_POINT('Ctrl Pts',(-210.348785235231,-0.328975413660277,
137.004113768549));
#191851=CARTESIAN_POINT('Ctrl Pts',(-210.627232859043,5.03820866530154,
134.432254965643));
#191852=CARTESIAN_POINT('Ctrl Pts',(-210.905680482857,5.77552511102812,
128.526538489345));
#191853=CARTESIAN_POINT('Ctrl Pts',(-211.184128106669,1.20541612980698,
124.714029271085));
#191854=CARTESIAN_POINT('Ctrl Pts',(-211.462575730482,-4.47241138685473,
126.498237031013));
#191855=CARTESIAN_POINT('Ctrl Pts',(-211.741023354295,-6.04031132844015,
132.239562001151));
#191856=CARTESIAN_POINT('Ctrl Pts',(-212.019470978108,-2.05746024480169,
136.66200701326));
#191857=CARTESIAN_POINT('Ctrl Pts',(-212.297918601921,3.81609629128846,
135.701561149659));
#191858=CARTESIAN_POINT('Ctrl Pts',(-212.576366225734,6.1828467623524,130.240827238612));
#191859=CARTESIAN_POINT('Ctrl Pts',(-212.854813849547,2.86786310767097,
125.297952972686));
#191860=CARTESIAN_POINT('Ctrl Pts',(-213.133261473359,-3.0825466400586,
125.415198329437));
#191861=CARTESIAN_POINT('Ctrl Pts',(-213.411709097173,-6.20024661634941,
130.484820553763));
#191862=CARTESIAN_POINT('Ctrl Pts',(-213.690156720985,-3.62022285110177,
135.848084486325));
#191863=CARTESIAN_POINT('Ctrl Pts',(-213.968604344798,2.28660885659016,
136.576412583105));
#191864=CARTESIAN_POINT('Ctrl Pts',(-214.247051968611,6.09215873212836,
132.00050690397));
#191865=CARTESIAN_POINT('Ctrl Pts',(-214.525499592424,4.29931235134063,
126.325401222624));
#191866=CARTESIAN_POINT('Ctrl Pts',(-214.803947216237,-1.44439204724454,
124.766240415898));
#191867=CARTESIAN_POINT('Ctrl Pts',(-215.08239484005,-5.86077071688603,
128.755817095934));
#191868=CARTESIAN_POINT('Ctrl Pts',(-215.360842463863,-4.89138741227638,
134.627905195436));
#191869=CARTESIAN_POINT('Ctrl Pts',(-215.639290087675,0.572941966656434,
136.986342618411));
#191870=CARTESIAN_POINT('Ctrl Pts',(-215.917737711489,5.51076566800256,
133.66384058922));
#191871=CARTESIAN_POINT('Ctrl Pts',(-216.196185335301,5.38446493632399,
127.713616159441));
#191872=CARTESIAN_POINT('Ctrl Pts',(-216.474632959115,0.310103973899474,
124.603634895418));
#191873=CARTESIAN_POINT('Ctrl Pts',(-216.753080582927,-5.04922739111732,
127.191817647757));
#191874=CARTESIAN_POINT('Ctrl Pts',(-217.031528206741,-5.76856545216855,
133.099750906814));
#191875=CARTESIAN_POINT('Ctrl Pts',(-217.309975830553,-1.18687367276612,
136.898332626102));
#191876=CARTESIAN_POINT('Ctrl Pts',(-217.588423454366,4.48549702990607,
135.096851776628));
#191877=CARTESIAN_POINT('Ctrl Pts',(-217.866871078179,6.03591509080661,
129.350781251827));
#191878=CARTESIAN_POINT('Ctrl Pts',(-218.145318701992,2.03962205410111,
124.94047915284));
#191879=CARTESIAN_POINT('Ctrl Pts',(-218.423766325804,-3.83098400924668,
125.9187976534));
#191880=CARTESIAN_POINT('Ctrl Pts',(-218.702213949618,-6.18110292207006,
131.386709845009));
#191881=CARTESIAN_POINT('Ctrl Pts',(-218.98066157343,-2.85109021317626,
136.319471545938));
#191882=CARTESIAN_POINT('Ctrl Pts',(-219.259109197243,3.09893511812703,
136.18411573184));
#191883=CARTESIAN_POINT('Ctrl Pts',(-219.537556821056,6.20119046726778,
131.105027783371));
#191884=CARTESIAN_POINT('Ctrl Pts',(-219.816004444869,3.6048547219858,125.749641397935));
#191885=CARTESIAN_POINT('Ctrl Pts',(-220.094452068682,-2.30416640585769,
125.039295038577));
#191886=CARTESIAN_POINT('Ctrl Pts',(-220.372899692494,-6.09577117150464,
129.626762307198));
#191887=CARTESIAN_POINT('Ctrl Pts',(-220.651347316308,-4.28566002551621,
135.296384894171));
#191888=CARTESIAN_POINT('Ctrl Pts',(-220.929794940121,1.46276331779004,
136.83805661853));
#191889=CARTESIAN_POINT('Ctrl Pts',(-221.208242563933,5.86697863200795,
132.835056480438));
#191890=CARTESIAN_POINT('Ctrl Pts',(-221.486690187747,4.87972720125093,
126.965946049375));
#191891=CARTESIAN_POINT('Ctrl Pts',(-221.765137811559,-0.591755139529082,
124.624151089502));
#191892=CARTESIAN_POINT('Ctrl Pts',(-222.043585435373,-5.51944341592756,
127.961666765899));
#191893=CARTESIAN_POINT('Ctrl Pts',(-222.322033059185,-5.37503283288975,
133.911479218663));
#191894=CARTESIAN_POINT('Ctrl Pts',(-222.600480682998,-0.29122966137826,
137.006001468201));
#191895=CARTESIAN_POINT('Ctrl Pts',(-222.878928306811,5.06019934158045,
134.401518743003));
#191896=CARTESIAN_POINT('Ctrl Pts',(-223.157375930624,5.7615523541068,128.491423431472));
#191897=CARTESIAN_POINT('Ctrl Pts',(-223.435823554437,1.16832022068962,
124.706804400699));
#191898=CARTESIAN_POINT('Ctrl Pts',(-223.71427117825,-4.49854111992577,
126.525541651043));
#191899=CARTESIAN_POINT('Ctrl Pts',(-223.992718802062,-6.03146293728042,
132.276304499695));
#191900=CARTESIAN_POINT('Ctrl Pts',(-224.271166425875,-2.02176496861996,
136.674422829126));
#191901=CARTESIAN_POINT('Ctrl Pts',(-224.549614049688,3.84583623749284,
135.678240754614));
#191902=CARTESIAN_POINT('Ctrl Pts',(-224.828061673501,6.1793018208946,130.203200936436));
#191903=CARTESIAN_POINT('Ctrl Pts',(-225.106509297314,2.83429090657077,
125.280597496933));
#191904=CARTESIAN_POINT('Ctrl Pts',(-225.384956921127,-3.11529488808334,
125.434062514461));
#191905=CARTESIAN_POINT('Ctrl Pts',(-225.66340454494,-6.20207687120481,
130.522569135094));
#191906=CARTESIAN_POINT('Ctrl Pts',(-225.941852168753,-3.5894531979886,
135.87002836184));
#191907=CARTESIAN_POINT('Ctrl Pts',(-226.220299792565,2.32170260964191,
136.562386403224));
#191908=CARTESIAN_POINT('Ctrl Pts',(-226.498747416378,6.09932714048972,
131.963400042786));
#191909=CARTESIAN_POINT('Ctrl Pts',(-226.777195040191,4.27196799792278,
126.299313072794));
#191910=CARTESIAN_POINT('Ctrl Pts',(-227.055642664004,-1.48112103749588,
124.775144712639));
#191911=CARTESIAN_POINT('Ctrl Pts',(-227.334090287817,-5.87313219624144,
128.79153122554));
#191912=CARTESIAN_POINT('Ctrl Pts',(-227.61253791163,-4.8680217850994,134.65760961753));
#191913=CARTESIAN_POINT('Ctrl Pts',(-227.890985535443,0.610562830463375,
136.982740420231));
#191914=CARTESIAN_POINT('Ctrl Pts',(-228.169433159256,5.52807003248314,
133.630242014917));
#191915=CARTESIAN_POINT('Ctrl Pts',(-228.447880783069,5.36555093588535,
127.680896657417));
#191916=CARTESIAN_POINT('Ctrl Pts',(-228.726328406882,0.272352650944771,
124.601862089598));
#191917=CARTESIAN_POINT('Ctrl Pts',(-229.004776030695,-5.07112441504767,
127.222620660081));
#191918=CARTESIAN_POINT('Ctrl Pts',(-229.283223654507,-5.75448588181141,
133.134823273769));
#191919=CARTESIAN_POINT('Ctrl Pts',(-229.561671278321,-1.14975594545406,
136.905444555836));
#191920=CARTESIAN_POINT('Ctrl Pts',(-229.840118902133,4.51154353607471,
135.069467753152));
#191921=CARTESIAN_POINT('Ctrl Pts',(-230.118566525947,6.0269549091058,129.314065854931));
#191922=CARTESIAN_POINT('Ctrl Pts',(-230.397014149759,2.00388915378425,
124.928172038625));
#191923=CARTESIAN_POINT('Ctrl Pts',(-230.675461773572,-3.86065283843716,
125.942208458593));
#191924=CARTESIAN_POINT('Ctrl Pts',(-230.953909397385,-6.17744347551146,
131.424325183319));
#191925=CARTESIAN_POINT('Ctrl Pts',(-231.232357021197,-2.81746534348149,
136.33672475907));
#191926=CARTESIAN_POINT('Ctrl Pts',(-231.510804645011,3.13162579837364,
136.165151959792));
#191927=CARTESIAN_POINT('Ctrl Pts',(-231.789252268823,6.20290581994918,
131.067273806224));
#191928=CARTESIAN_POINT('Ctrl Pts',(-232.067699892636,3.57401842178686,
125.727791276302));
#191929=CARTESIAN_POINT('Ctrl Pts',(-232.346147516449,-2.33921730549066,
125.053427966802));
#191930=CARTESIAN_POINT('Ctrl Pts',(-232.624595140262,-6.10282660614105,
129.663890814674));
#191931=CARTESIAN_POINT('Ctrl Pts',(-232.903042764075,-4.25823639540172,
135.322389696357));
#191932=CARTESIAN_POINT('Ctrl Pts',(-233.181490387888,1.499465036299,136.829040572621));
#191933=CARTESIAN_POINT('Ctrl Pts',(-233.459938011701,5.87923135258013,
132.799304892167));
#191934=CARTESIAN_POINT('Ctrl Pts',(-233.738385635514,4.85627127225937,
126.9363128818));
#191935=CARTESIAN_POINT('Ctrl Pts',(-234.016833259326,-0.629364865227224,
124.627867775965));
#191936=CARTESIAN_POINT('Ctrl Pts',(-234.29528088314,-5.53664543775268,
127.99531785311));
#191937=CARTESIAN_POINT('Ctrl Pts',(-234.573728506952,-5.35601933315035,
133.944141001422));
#191938=CARTESIAN_POINT('Ctrl Pts',(-234.852176130765,-0.253473117473377,
137.007659363768));
#191939=CARTESIAN_POINT('Ctrl Pts',(-235.130623754578,5.08200251031112,
134.370649226346));
#191940=CARTESIAN_POINT('Ctrl Pts',(-235.409071378391,5.74736610074488,
128.456394080338));
#191941=CARTESIAN_POINT('Ctrl Pts',(-235.687519002204,1.13118101903705,
124.699805477501));
#191942=CARTESIAN_POINT('Ctrl Pts',(-235.965966626017,-4.52450415790052,
126.553004824284));
#191943=CARTESIAN_POINT('Ctrl Pts',(-236.24441424983,-6.0223910480441,132.312992454817));
#191944=CARTESIAN_POINT('Ctrl Pts',(-236.522861873642,-1.98599477519336,
136.686621127679));
#191945=CARTESIAN_POINT('Ctrl Pts',(-236.801309497456,3.87543367482126,
135.654739756147));
#191946=CARTESIAN_POINT('Ctrl Pts',(-237.079757121268,6.1755279031354,130.165596910454));
#191947=CARTESIAN_POINT('Ctrl Pts',(-237.358204745081,2.80061367977841,
125.263446706254));
#191948=CARTESIAN_POINT('Ctrl Pts',(-237.636652368894,-3.14792769771062,
125.453125697856));
#191949=CARTESIAN_POINT('Ctrl Pts',(-237.915099992707,-6.20367730582095,
130.560328158313));
#191950=CARTESIAN_POINT('Ctrl Pts',(-238.19354761652,-3.55855053636696,
135.891784527174));
#191951=CARTESIAN_POINT('Ctrl Pts',(-238.471995240333,2.35671033115007,
136.54814685758));
#191952=CARTESIAN_POINT('Ctrl Pts',(-238.750442864146,6.10626953604027,
131.92625023297));
#191953=CARTESIAN_POINT('Ctrl Pts',(-239.028890487959,4.24446534516054,
126.273391859158));
#191954=CARTESIAN_POINT('Ctrl Pts',(-239.307338111771,-1.51779514426229,
124.784272424193));
#191955=CARTESIAN_POINT('Ctrl Pts',(-239.585785735585,-5.88527604452282,
128.827319941278));
#191956=CARTESIAN_POINT('Ctrl Pts',(-239.864233359397,-4.84447577158576,
134.687171256065));
#191957=CARTESIAN_POINT('Ctrl Pts',(-240.14268098321,0.648161069640796,
136.978909279916));
#191958=CARTESIAN_POINT('Ctrl Pts',(-240.421128607023,5.54516955229552,
133.596538726537));
#191959=CARTESIAN_POINT('Ctrl Pts',(-240.699576230836,5.34643811298351,
127.648292896498));
#191960=CARTESIAN_POINT('Ctrl Pts',(-240.978023854649,0.234591235861842,
124.600319119639));
#191961=CARTESIAN_POINT('Ctrl Pts',(-241.256471478461,-5.09283352659785,
127.253556395099));
#191962=CARTESIAN_POINT('Ctrl Pts',(-241.534919102275,-5.74019307686353,
133.169809284574));
#191963=CARTESIAN_POINT('Ctrl Pts',(-241.813366726087,-1.11259561351327,
136.912330407661));
#191964=CARTESIAN_POINT('Ctrl Pts',(-242.0918143499,4.53742286533832,135.041925684563));
#191965=CARTESIAN_POINT('Ctrl Pts',(-242.370261973713,6.01777139637409,
129.277405681456));
#191966=CARTESIAN_POINT('Ctrl Pts',(-242.648709597526,1.96808199861856,
124.916082668738));
#191967=CARTESIAN_POINT('Ctrl Pts',(-242.927157221339,-3.89017860971679,
125.965799432623));
#191968=CARTESIAN_POINT('Ctrl Pts',(-243.205604845152,-6.1735551215127,
131.461917548614));
#191969=CARTESIAN_POINT('Ctrl Pts',(-243.484052468965,-2.78373607157309,
136.353772968415));
#191970=CARTESIAN_POINT('Ctrl Pts',(-243.762500092778,3.16420043507544,
136.145989541648));
#191971=CARTESIAN_POINT('Ctrl Pts',(-244.040947716591,6.20439132167383,
131.029510086731));
#191972=CARTESIAN_POINT('Ctrl Pts',(-244.319395340403,3.54304968502077,
125.706129268813));
#191973=CARTESIAN_POINT('Ctrl Pts',(-244.597842964216,-2.37418152456686,
125.067773997952));
#191974=CARTESIAN_POINT('Ctrl Pts',(-244.876290588029,-6.10965589829292,
129.701061582678));
#191975=CARTESIAN_POINT('Ctrl Pts',(-245.154738211842,-4.23065497477177,
135.348227081313));
#191976=CARTESIAN_POINT('Ctrl Pts',(-245.433185835655,1.53611119157916,
136.819801279981));
#191977=CARTESIAN_POINT('Ctrl Pts',(-245.711633459468,5.89126621607239,
132.763479380503));
#191978=CARTESIAN_POINT('Ctrl Pts',(-245.990081083281,4.83263539234992,
126.906823046158));
#191979=CARTESIAN_POINT('Ctrl Pts',(-246.268528707094,-0.666951269578287,
124.631813334641));
#191980=CARTESIAN_POINT('Ctrl Pts',(-246.546976330906,-5.55364229714491,
128.029073030433));
#191981=CARTESIAN_POINT('Ctrl Pts',(-246.825423954719,-5.33680736414475,
133.976686438464));
#191982=CARTESIAN_POINT('Ctrl Pts',(-247.103871578532,-0.215707181029578,
137.009087393821));
#191983=CARTESIAN_POINT('Ctrl Pts',(-247.382319202345,5.10361736357064,
134.339647559554));
#191984=CARTESIAN_POINT('Ctrl Pts',(-247.660766826158,5.73296687661779,
128.421451733968));
#191985=CARTESIAN_POINT('Ctrl Pts',(-247.939214449971,1.09399990105564,
124.693032760838));
#191986=CARTESIAN_POINT('Ctrl Pts',(-248.217662073784,-4.55029953871062,
126.580625533077));
#191987=CARTESIAN_POINT('Ctrl Pts',(-248.496109697597,-6.01309599689209,
132.349624507031));
#191988=CARTESIAN_POINT('Ctrl Pts',(-248.77455732141,-1.95015099000055,
136.698601456905));
#191989=CARTESIAN_POINT('Ctrl Pts',(-249.053004945222,3.90488750652966,
135.631059025098));
#191990=CARTESIAN_POINT('Ctrl Pts',(-249.331452569036,6.17152514891849,
130.128016554096));
#191991=CARTESIAN_POINT('Ctrl Pts',(-249.609900192848,2.76683267521693,
125.246501236177));
#191992=CARTESIAN_POINT('Ctrl Pts',(-249.888347816661,-3.18044385971988,
125.472387173231));
#191993=CARTESIAN_POINT('Ctrl Pts',(-250.166795440474,-6.20504786089197,
130.598096224241));
#191994=CARTESIAN_POINT('Ctrl Pts',(-250.445243064287,-3.5275160113489,
135.913352176149));
#191995=CARTESIAN_POINT('Ctrl Pts',(-250.7236906881,2.39163072389511,136.533694473816));
#191996=CARTESIAN_POINT('Ctrl Pts',(-251.002138311913,6.11298566151878,
131.889058851139));
#191997=CARTESIAN_POINT('Ctrl Pts',(-251.280585935725,4.21680541219097,
126.247638542206));
#191998=CARTESIAN_POINT('Ctrl Pts',(-251.559033559539,-1.5544130086051,
124.793623212388));
#191999=CARTESIAN_POINT('Ctrl Pts',(-251.837481183351,-5.89720181167361,
128.863181916876));
#192000=CARTESIAN_POINT('Ctrl Pts',(-252.115928807165,-4.82075024435922,
134.716589015834));
#192001=CARTESIAN_POINT('Ctrl Pts',(-252.394376430977,0.685735291195708,
136.974849339035));
#192002=CARTESIAN_POINT('Ctrl Pts',(-252.67282405479,5.56206359338632,133.562731973716));
#192003=CARTESIAN_POINT('Ctrl Pts',(-252.951271678603,5.32712717665345,
127.615806083426));
#192004=CARTESIAN_POINT('Ctrl Pts',(-253.229719302416,0.196821126400439,
124.599006045371));
#192005=CARTESIAN_POINT('Ctrl Pts',(-253.508166926229,-5.11435391846912,
127.284623701469));
#192006=CARTESIAN_POINT('Ctrl Pts',(-253.786614550041,-5.72568757235024,
133.204707652256));
#192007=CARTESIAN_POINT('Ctrl Pts',(-254.065062173855,-1.07539404373626,
136.918989908584));
#192008=CARTESIAN_POINT('Ctrl Pts',(-254.343509797667,4.56313403947717,
135.014226625117));
#192009=CARTESIAN_POINT('Ctrl Pts',(-254.621957421481,6.00836492926231,
129.240802026269));
#192010=CARTESIAN_POINT('Ctrl Pts',(-254.900405045293,1.9322018468105,124.904211611225));
#192011=CARTESIAN_POINT('Ctrl Pts',(-255.178852669106,-3.91956009939235,
125.989569474605));
#192012=CARTESIAN_POINT('Ctrl Pts',(-255.457300292919,-6.16943824888009,
131.499485975975));
#192013=CARTESIAN_POINT('Ctrl Pts',(-255.735747916732,-2.74990318521692,
136.370614733943));
#192014=CARTESIAN_POINT('Ctrl Pts',(-256.014195540545,3.19665694865877,
136.126630713714));
#192015=CARTESIAN_POINT('Ctrl Pts',(-256.292643164358,6.20564856486739,
130.991735142402));
#192016=CARTESIAN_POINT('Ctrl Pts',(-256.571090788171,3.51194654848645,
125.68466161966));
#192017=CARTESIAN_POINT('Ctrl Pts',(-256.849538411983,-2.40905189372645,
125.082322325773));
#192018=CARTESIAN_POINT('Ctrl Pts',(-257.127986035797,-6.11626988572704,
129.738292634474));
#192019=CARTESIAN_POINT('Ctrl Pts',(-257.406433659609,-4.20289584392431,
135.373859459261));
#192020=CARTESIAN_POINT('Ctrl Pts',(-257.684881283423,1.57266088340656,
136.810408252432));
#192021=CARTESIAN_POINT('Ctrl Pts',(-257.963328907235,5.90315744058412,
132.727450666138));
#192022=CARTESIAN_POINT('Ctrl Pts',(-258.241776531048,4.80867945501638,
126.87772425425));
#192023=CARTESIAN_POINT('Ctrl Pts',(-258.520224154861,-0.704246744852541,
124.635521896935));
#192024=CARTESIAN_POINT('Ctrl Pts',(-258.798671778674,-5.5709361272427,
128.063810879205));
#192025=CARTESIAN_POINT('Ctrl Pts',(-259.077119402487,-5.31644754243966,
134.007449313497));
#192026=CARTESIAN_POINT('Ctrl Pts',(-259.355567026299,-0.179733571114533,
137.013459703814));
#192027=CARTESIAN_POINT('Ctrl Pts',(-259.634014650113,5.12849404027147,
134.30227331953));
#192028=CARTESIAN_POINT('Ctrl Pts',(-259.866054336623,5.61428989304695,
129.384066440553));
#192029=CARTESIAN_POINT('Ctrl Pts',(-260.051696012132,3.39054283699284,
126.521203045511));
#192030=CARTESIAN_POINT('Ctrl Pts',(-260.144521813036,1.754921961264,125.780753115897));
#192031=CARTESIAN_POINT('Ctrl Pts',(-260.190939676638,0.892893391295023,
125.631947563271));
#192032=CARTESIAN_POINT('Ctrl Pts',(210.191733024964,-2.43880115184907,
125.780342085335));
#192033=CARTESIAN_POINT('Ctrl Pts',(210.145323348611,-3.27594855749458,
126.186716565447));
#192034=CARTESIAN_POINT('Ctrl Pts',(210.052505734956,-4.72940422381435,
127.426013481475));
#192035=CARTESIAN_POINT('Ctrl Pts',(209.866872246696,-6.15821517169733,
131.008352419918));
#192036=CARTESIAN_POINT('Ctrl Pts',(209.634832560185,-4.21099667891447,
135.892791108304));
#192037=CARTESIAN_POINT('Ctrl Pts',(209.356384936373,2.01508446636645,137.098708070195));
#192038=CARTESIAN_POINT('Ctrl Pts',(209.07793731256,6.37956871319657,132.510708806665));
#192039=CARTESIAN_POINT('Ctrl Pts',(208.799489688747,4.8866719183268,126.359661034021));
#192040=CARTESIAN_POINT('Ctrl Pts',(208.521042064934,-1.09954563679898,
124.290443595948));
#192041=CARTESIAN_POINT('Ctrl Pts',(208.242594441121,-6.07390144970816,
128.208589139036));
#192042=CARTESIAN_POINT('Ctrl Pts',(207.964146817309,-5.46739734855352,
134.511385201899));
#192043=CARTESIAN_POINT('Ctrl Pts',(207.685699193495,0.163779660617915,
137.407996874876));
#192044=CARTESIAN_POINT('Ctrl Pts',(207.407251569682,5.6442383477931,134.235982835808));
#192045=CARTESIAN_POINT('Ctrl Pts',(207.128803945869,5.93803043711477,127.910585036422));
#192046=CARTESIAN_POINT('Ctrl Pts',(206.850356322057,0.775002953389061,
124.244367681185));
#192047=CARTESIAN_POINT('Ctrl Pts',(206.571908698243,-5.10018277131114,
126.606494049502));
#192048=CARTESIAN_POINT('Ctrl Pts',(206.293461074431,-6.28856642889766,
132.82623846394));
#192049=CARTESIAN_POINT('Ctrl Pts',(206.015013450618,-1.69805588527783,
137.187984519302));
#192050=CARTESIAN_POINT('Ctrl Pts',(205.736565826805,4.45288036648484,135.683487507757));
#192051=CARTESIAN_POINT('Ctrl Pts',(205.458118202992,6.51183958365415,129.695313656966));
#192052=CARTESIAN_POINT('Ctrl Pts',(205.179670579179,2.58673502741873,124.726298504418));
#192053=CARTESIAN_POINT('Ctrl Pts',(204.901222955366,-3.71545195245463,
125.342726181157));
#192054=CARTESIAN_POINT('Ctrl Pts',(204.622775331554,-6.60332046735468,
130.978128730661));
#192055=CARTESIAN_POINT('Ctrl Pts',(204.344327707741,-3.42305986725146,
136.4538470632));
#192056=CARTESIAN_POINT('Ctrl Pts',(204.065880083927,2.90282542147133,136.737963244372));
#192057=CARTESIAN_POINT('Ctrl Pts',(203.787432460115,6.56115601364161,131.569388537382));
#192058=CARTESIAN_POINT('Ctrl Pts',(203.508984836302,4.1901047305044,125.69779051756));
#192059=CARTESIAN_POINT('Ctrl Pts',(203.230537212489,-2.03144808657932,
124.518880964767));
#192060=CARTESIAN_POINT('Ctrl Pts',(202.952089588676,-6.38619936200403,
129.116020142231));
#192061=CARTESIAN_POINT('Ctrl Pts',(202.673641964863,-4.87234540261322,
135.2646617407));
#192062=CARTESIAN_POINT('Ctrl Pts',(202.39519434105,1.1189559521872,137.314504502614));
#192063=CARTESIAN_POINT('Ctrl Pts',(202.116746717238,6.08199145217563,133.381843073553));
#192064=CARTESIAN_POINT('Ctrl Pts',(201.838299093424,5.45597392877388,127.080601183836));
#192065=CARTESIAN_POINT('Ctrl Pts',(201.559851469612,-0.183817095687214,
124.201312298284));
#192066=CARTESIAN_POINT('Ctrl Pts',(201.281403845799,-5.65468918935595,
127.389902241135));
#192067=CARTESIAN_POINT('Ctrl Pts',(201.002956221986,-5.92917816483575,
133.716212626452));
#192068=CARTESIAN_POINT('Ctrl Pts',(200.724508598173,-0.755042063338292,
137.366673267433));
#192069=CARTESIAN_POINT('Ctrl Pts',(200.44606097436,5.11294080853837,134.986689170007));
#192070=CARTESIAN_POINT('Ctrl Pts',(200.167613350547,6.2823808583988,128.763349450982));
#192071=CARTESIAN_POINT('Ctrl Pts',(199.889165726734,1.67861981076543,124.415599285115));
#192072=CARTESIAN_POINT('Ctrl Pts',(199.610718102921,-4.46771083782862,
125.938808675424));
#192073=CARTESIAN_POINT('Ctrl Pts',(199.332270479108,-6.50843348626435,
131.933222605136));
#192074=CARTESIAN_POINT('Ctrl Pts',(199.053822855296,-2.56822371547623,
136.890267516244));
#192075=CARTESIAN_POINT('Ctrl Pts',(198.775375231483,3.73205818513161,136.254661300547));
#192076=CARTESIAN_POINT('Ctrl Pts',(198.49692760767,6.60276093478139,130.610495019181));
#192077=CARTESIAN_POINT('Ctrl Pts',(198.218479983857,3.4058489481713,125.14448175187));
#192078=CARTESIAN_POINT('Ctrl Pts',(197.940032360044,-2.92087183683725,
124.879620661678));
#192079=CARTESIAN_POINT('Ctrl Pts',(197.661584736231,-6.56345409631434,
130.05930615131));
#192080=CARTESIAN_POINT('Ctrl Pts',(197.383137112418,-4.1745426838368,135.923660297497));
#192081=CARTESIAN_POINT('Ctrl Pts',(197.104689488605,2.05056951733907,137.083628129519));
#192082=CARTESIAN_POINT('Ctrl Pts',(196.826241864792,6.39130850797037,132.473255877329));
#192083=CARTESIAN_POINT('Ctrl Pts',(196.54779424098,4.85874721255563,126.329250411482));
#192084=CARTESIAN_POINT('Ctrl Pts',(196.269346617166,-1.13876540820057,
124.297652603739));
#192085=CARTESIAN_POINT('Ctrl Pts',(195.990898993354,-6.0898082506034,128.245401590344));
#192086=CARTESIAN_POINT('Ctrl Pts',(195.712451369541,-5.44461481437399,
134.544708910868));
#192087=CARTESIAN_POINT('Ctrl Pts',(195.434003745728,0.203913652044436,
137.406818876019));
#192088=CARTESIAN_POINT('Ctrl Pts',(195.155556121915,5.66505543396973,134.201592249669));
#192089=CARTESIAN_POINT('Ctrl Pts',(194.877108498102,5.92028802542049,127.874475717408));
#192090=CARTESIAN_POINT('Ctrl Pts',(194.59866087429,0.735065143658737,124.239780275557));
#192091=CARTESIAN_POINT('Ctrl Pts',(194.320213250476,-5.1256466951968,126.637613470433));
#192092=CARTESIAN_POINT('Ctrl Pts',(194.041765626664,-6.2761396229282,132.86448373661));
#192093=CARTESIAN_POINT('Ctrl Pts',(193.763318002851,-1.6591668436545,137.198201498994));
#192094=CARTESIAN_POINT('Ctrl Pts',(193.484870379038,4.48249921013125,135.656291847837));
#192095=CARTESIAN_POINT('Ctrl Pts',(193.206422755225,6.50496747206681,129.655694426079));
#192096=CARTESIAN_POINT('Ctrl Pts',(192.927975131412,2.54968841250072,124.710665118833));
#192097=CARTESIAN_POINT('Ctrl Pts',(192.649527507599,-3.74862973894988,
125.365444281348));
#192098=CARTESIAN_POINT('Ctrl Pts',(192.371079883787,-6.60214029104917,
131.018321851013));
#192099=CARTESIAN_POINT('Ctrl Pts',(192.092632259973,-3.38860644815819,
136.474579499726));
#192100=CARTESIAN_POINT('Ctrl Pts',(191.814184636161,2.93889117796205,136.720183001327));
#192101=CARTESIAN_POINT('Ctrl Pts',(191.535737012347,6.56569138435095,131.529434736241));
#192102=CARTESIAN_POINT('Ctrl Pts',(191.257289388535,4.15894196037717,125.672378777932));
#192103=CARTESIAN_POINT('Ctrl Pts',(190.978841764722,-2.06967194957323,
124.531363418996));
#192104=CARTESIAN_POINT('Ctrl Pts',(190.700394140909,-6.3963584469616,129.154926032595));
#192105=CARTESIAN_POINT('Ctrl Pts',(190.421946517096,-4.84510401107414,
135.294238450423));
#192106=CARTESIAN_POINT('Ctrl Pts',(190.143498893283,1.15856431450073,137.307572482581));
#192107=CARTESIAN_POINT('Ctrl Pts',(189.86505126947,6.09756863406271,133.344772510351));
#192108=CARTESIAN_POINT('Ctrl Pts',(189.586603645657,5.4332052617092,127.047458114672));
#192109=CARTESIAN_POINT('Ctrl Pts',(189.308156021844,-0.224008319322015,
124.202553584261));
#192110=CARTESIAN_POINT('Ctrl Pts',(189.029708398032,-5.67536919831109,
127.424387201254));
#192111=CARTESIAN_POINT('Ctrl Pts',(188.751260774218,-5.91134304125131,
133.752251266956));
#192112=CARTESIAN_POINT('Ctrl Pts',(188.472813150406,-0.71508141444371,
137.371147838333));
#192113=CARTESIAN_POINT('Ctrl Pts',(188.194365526593,5.13830509856852,134.955487759214));
#192114=CARTESIAN_POINT('Ctrl Pts',(187.91591790278,6.26984024615536,128.725144630756));
#192115=CARTESIAN_POINT('Ctrl Pts',(187.637470278967,1.63969850624965,124.405499418827));
#192116=CARTESIAN_POINT('Ctrl Pts',(187.359022655154,-4.49724605717418,
125.966095046791));
#192117=CARTESIAN_POINT('Ctrl Pts',(187.080575031341,-6.5014411967389,131.972820371883));
#192118=CARTESIAN_POINT('Ctrl Pts',(186.802127407528,-2.53112948956026,
136.905788265189));
#192119=CARTESIAN_POINT('Ctrl Pts',(186.523679783716,3.76516656597443,136.231842221641));
#192120=CARTESIAN_POINT('Ctrl Pts',(186.245232159903,6.60145848599114,130.570305731164));
#192121=CARTESIAN_POINT('Ctrl Pts',(185.96678453609,3.3713325565579,125.123854247073));
#192122=CARTESIAN_POINT('Ctrl Pts',(185.688336912277,-2.95688329360047,
124.897510609301));
#192123=CARTESIAN_POINT('Ctrl Pts',(185.409889288464,-6.5678678487195,130.099273563458));
#192124=CARTESIAN_POINT('Ctrl Pts',(185.131441664651,-4.14330270904733,
135.948977074923));
#192125=CARTESIAN_POINT('Ctrl Pts',(184.852994040838,2.08875520864929,137.071029390563));
#192126=CARTESIAN_POINT('Ctrl Pts',(184.574546417025,6.40134913096194,132.434319247607));
#192127=CARTESIAN_POINT('Ctrl Pts',(184.296098793212,4.831415925211,126.299756751549));
#192128=CARTESIAN_POINT('Ctrl Pts',(184.017651169399,-1.17835248801931,
124.304705146227));
#192129=CARTESIAN_POINT('Ctrl Pts',(183.739203545587,-6.10527253047917,
128.282519393244));
#192130=CARTESIAN_POINT('Ctrl Pts',(183.460755921774,-5.42174537657308,
134.577782526619));
#192131=CARTESIAN_POINT('Ctrl Pts',(183.182308297961,0.244100911417136,
137.405455267482));
#192132=CARTESIAN_POINT('Ctrl Pts',(182.903860674148,5.68563038680749,134.167044506474));
#192133=CARTESIAN_POINT('Ctrl Pts',(182.625413050335,5.90234329520773,127.838491527799));
#192134=CARTESIAN_POINT('Ctrl Pts',(182.346965426522,0.695091060812155,
124.23542735186));
#192135=CARTESIAN_POINT('Ctrl Pts',(182.068517802709,-5.15091590138369,
126.668891936874));
#192136=CARTESIAN_POINT('Ctrl Pts',(181.790070178896,-6.263482786439,132.902650210566));
#192137=CARTESIAN_POINT('Ctrl Pts',(181.511622555083,-1.62021497890189,
137.208182855437));
#192138=CARTESIAN_POINT('Ctrl Pts',(181.233174931271,4.51195124234396,135.628915707812));
#192139=CARTESIAN_POINT('Ctrl Pts',(180.954727307458,6.49785469294791,129.61611812487));
#192140=CARTESIAN_POINT('Ctrl Pts',(180.676279683645,2.51254711858197,124.695257343842));
#192141=CARTESIAN_POINT('Ctrl Pts',(180.397832059832,-3.78166851301026,
125.388364025079));
#192142=CARTESIAN_POINT('Ctrl Pts',(180.119384436019,-6.60071552592353,
131.058506988669));
#192143=CARTESIAN_POINT('Ctrl Pts',(179.840936812206,-3.35402743339335,
136.495101852955));
#192144=CARTESIAN_POINT('Ctrl Pts',(179.562489188393,2.97484801707599,136.702183530083));
#192145=CARTESIAN_POINT('Ctrl Pts',(179.28404156458,6.56998346925752,131.489454075275));
#192146=CARTESIAN_POINT('Ctrl Pts',(179.005593940767,4.12762507472721,125.647157201507));
#192147=CARTESIAN_POINT('Ctrl Pts',(178.727146316955,-2.10781911778238,
124.544078323705));
#192148=CARTESIAN_POINT('Ctrl Pts',(178.448698693142,-6.40628051373842,
129.193893042167));
#192149=CARTESIAN_POINT('Ctrl Pts',(178.170251069329,-4.81768308177075,
135.323648786705));
#192150=CARTESIAN_POINT('Ctrl Pts',(177.891803445516,1.19812974544141,137.300399483306));
#192151=CARTESIAN_POINT('Ctrl Pts',(177.613355821703,6.11291986848493,133.307607811431));
#192152=CARTESIAN_POINT('Ctrl Pts',(177.33490819789,5.41023526512845,127.014454258818));
#192153=CARTESIAN_POINT('Ctrl Pts',(177.056460574078,-0.264191242194762,
124.204039502676));
#192154=CARTESIAN_POINT('Ctrl Pts',(176.778012950264,-5.69583890440069,
127.458997407505));
#192155=CARTESIAN_POINT('Ctrl Pts',(176.499565326452,-5.89328887066216,
133.788180672302));
#192156=CARTESIAN_POINT('Ctrl Pts',(176.221117702638,-0.675094267951971,
137.375379074508));
#192157=CARTESIAN_POINT('Ctrl Pts',(175.942670078826,5.16347898681764,134.924132526884));
#192158=CARTESIAN_POINT('Ctrl Pts',(175.664222455013,6.25706730267374,128.687016856641));
#192159=CARTESIAN_POINT('Ctrl Pts',(175.3857748312,1.60071644210391,124.395636664696));
#192160=CARTESIAN_POINT('Ctrl Pts',(175.107327207387,-4.5266146294138,125.993560701866));
#192161=CARTESIAN_POINT('Ctrl Pts',(174.828879583574,-6.49420799391872,
132.012374840923));
#192162=CARTESIAN_POINT('Ctrl Pts',(174.550431959762,-2.49394147171037,
136.92108292349));
#192163=CARTESIAN_POINT('Ctrl Pts',(174.271984335948,3.79813542718566,136.208822025409));
#192164=CARTESIAN_POINT('Ctrl Pts',(173.993536712136,6.59991141772898,130.530125116137));
#192165=CARTESIAN_POINT('Ctrl Pts',(173.715089088322,3.33669123897678,125.103437235529));
#192166=CARTESIAN_POINT('Ctrl Pts',(173.43664146451,-2.99278518196597,124.915619437422));
#192167=CARTESIAN_POINT('Ctrl Pts',(173.158193840697,-6.5720382263662,130.139267102866));
#192168=CARTESIAN_POINT('Ctrl Pts',(172.879746216884,-4.11190920265221,
135.974103216695));
#192169=CARTESIAN_POINT('Ctrl Pts',(172.601298593071,2.12686350036709,137.058198437889));
#192170=CARTESIAN_POINT('Ctrl Pts',(172.322850969258,6.41115254960738,132.395322219168));
#192171=CARTESIAN_POINT('Ctrl Pts',(172.044403345445,4.80390560797255,126.270430011369));
#192172=CARTESIAN_POINT('Ctrl Pts',(171.765955721632,-1.21789590355323,
124.31199853584));
#192173=CARTESIAN_POINT('Ctrl Pts',(171.487508097819,-6.12051057723618,
128.319730643897));
#192174=CARTESIAN_POINT('Ctrl Pts',(171.209060474007,-5.39867503400336,
134.610716316833));
#192175=CARTESIAN_POINT('Ctrl Pts',(170.930612850193,0.284279125540913,
137.403847052956));
#192176=CARTESIAN_POINT('Ctrl Pts',(170.652165226381,5.70599465652041,134.13237215779));
#192177=CARTESIAN_POINT('Ctrl Pts',(170.373717602568,5.88417985149351,127.802617239562));
#192178=CARTESIAN_POINT('Ctrl Pts',(170.095269978755,0.655091221110643,
124.231317842401));
#192179=CARTESIAN_POINT('Ctrl Pts',(169.816822354942,-5.17599423848763,
126.700323644626));
#192180=CARTESIAN_POINT('Ctrl Pts',(169.538374731129,-6.25059385429175,
132.940738931629));
#192181=CARTESIAN_POINT('Ctrl Pts',(169.259927107316,-1.58120307648749,
137.217926915891));
#192182=CARTESIAN_POINT('Ctrl Pts',(168.981479483503,4.54123608254409,135.601360792124));
#192183=CARTESIAN_POINT('Ctrl Pts',(168.703031859691,6.49050113343381,129.576585854424));
#192184=CARTESIAN_POINT('Ctrl Pts',(168.424584235878,2.47531272130571,124.680075943919));
#192185=CARTESIAN_POINT('Ctrl Pts',(168.146136612065,-3.81456715595326,
125.411484460556));
#192186=CARTESIAN_POINT('Ctrl Pts',(167.867688988252,-6.59904616885666,
131.098682708838));
#192187=CARTESIAN_POINT('Ctrl Pts',(167.589241364439,-3.31932413390846,
136.515413333674));
#192188=CARTESIAN_POINT('Ctrl Pts',(167.310793740626,3.01069462210276,136.683965512842));
#192189=CARTESIAN_POINT('Ctrl Pts',(167.032346116813,6.57403210101054,131.449448027918));
#192190=CARTESIAN_POINT('Ctrl Pts',(166.753898493,4.09615523841214,125.622126727152));
#192191=CARTESIAN_POINT('Ctrl Pts',(166.475450869187,-2.14588817997888,
124.557025205477));
#192192=CARTESIAN_POINT('Ctrl Pts',(166.197003245374,-6.41596519343492,
129.232919728208));
#192193=CARTESIAN_POINT('Ctrl Pts',(165.918555621562,-4.79008363144905,
135.352891659104));
#192194=CARTESIAN_POINT('Ctrl Pts',(165.640107997748,1.23765077924384,137.292985770921));
#192195=CARTESIAN_POINT('Ctrl Pts',(165.361660373936,6.12804458641347,133.270350353765));
#192196=CARTESIAN_POINT('Ctrl Pts',(165.083212750123,5.38706479029029,126.981590839339));
#192197=CARTESIAN_POINT('Ctrl Pts',(164.80476512631,-0.304364375363971,
124.205769998417));
#192198=CARTESIAN_POINT('Ctrl Pts',(164.526317502497,-5.71609754908509,
127.493731577419));
#192199=CARTESIAN_POINT('Ctrl Pts',(164.247869878684,-5.8750163220866,133.823999511097));
#192200=CARTESIAN_POINT('Ctrl Pts',(163.969422254871,-0.635082105593798,
137.37936681918));
#192201=CARTESIAN_POINT('Ctrl Pts',(163.690974631059,5.18846154045405,134.892624634889));
#192202=CARTESIAN_POINT('Ctrl Pts',(163.412527007245,6.24406250126218,128.648967541478));
#192203=CARTESIAN_POINT('Ctrl Pts',(163.134079383433,1.56167506282176,124.386011388187));
#192204=CARTESIAN_POINT('Ctrl Pts',(162.85563175962,-4.55581546628373,126.021204622902));
#192205=CARTESIAN_POINT('Ctrl Pts',(162.577184135807,-6.48673414583306,
132.051884546553));
#192206=CARTESIAN_POINT('Ctrl Pts',(162.298736511994,-2.45666103994207,
136.936150924396));
#192207=CARTESIAN_POINT('Ctrl Pts',(162.020288888181,3.83096354709181,136.185601564872));
#192208=CARTESIAN_POINT('Ctrl Pts',(161.741841264368,6.59811978732212,130.489954663008));
#192209=CARTESIAN_POINT('Ctrl Pts',(161.463393640556,3.30192627907479,125.083231473798));
#192210=CARTESIAN_POINT('Ctrl Pts',(161.184946016742,-3.02857617157586,
124.933946475014));
#192211=CARTESIAN_POINT('Ctrl Pts',(160.90649839293,-6.57596507471956,130.179285287561));
#192212=CARTESIAN_POINT('Ctrl Pts',(160.628050769116,-4.08036332794952,
135.999037791754));
#192213=CARTESIAN_POINT('Ctrl Pts',(160.349603145304,2.16489298037573,137.045135746957));
#192214=CARTESIAN_POINT('Ctrl Pts',(160.07115552149,6.42071840063739,132.356266237063));
#192215=CARTESIAN_POINT('Ctrl Pts',(159.792707897678,4.77621728024515,126.241271277656));
#192216=CARTESIAN_POINT('Ctrl Pts',(159.514260273865,-1.25739418950663,
124.319532502318));
#192217=CARTESIAN_POINT('Ctrl Pts',(159.235812650052,-6.13552182622286,
128.357033963427));
#192218=CARTESIAN_POINT('Ctrl Pts',(158.957365026239,-5.37540464154493,
134.643509061136));
#192219=CARTESIAN_POINT('Ctrl Pts',(158.678917402427,0.324446805597038,
137.401994292032));
#192220=CARTESIAN_POINT('Ctrl Pts',(158.400469778613,5.72614748850293,134.097576488416));
#192221=CARTESIAN_POINT('Ctrl Pts',(158.122022154801,5.86579836733105,127.766854182028));
#192222=CARTESIAN_POINT('Ctrl Pts',(157.843574530988,0.615067106763091,
124.22745189946));
#192223=CARTESIAN_POINT('Ctrl Pts',(157.565126907175,-5.20088077722156,
126.731907428977));
#192224=CARTESIAN_POINT('Ctrl Pts',(157.286679283362,-6.23747330409059,
132.978748488409));
#192225=CARTESIAN_POINT('Ctrl Pts',(157.008231659549,-1.54213258201158,
137.227433319288));
#192226=CARTESIAN_POINT('Ctrl Pts',(156.729784035736,4.5703526455712,135.57362812183));
#192227=CARTESIAN_POINT('Ctrl Pts',(156.451336411923,6.48290706601333,129.537099079623));
#192228=CARTESIAN_POINT('Ctrl Pts',(156.172888788111,2.43798660040623,124.665121481617));
#192229=CARTESIAN_POINT('Ctrl Pts',(155.894441164297,-3.84732444870741,
125.434804731043));
#192230=CARTESIAN_POINT('Ctrl Pts',(155.615993540485,-6.59713228170722,
131.138847522794));
#192231=CARTESIAN_POINT('Ctrl Pts',(155.337545916672,-3.28449783564716,
136.535513189234));
#192232=CARTESIAN_POINT('Ctrl Pts',(155.059098292859,3.04642966473303,136.665529624679));
#192233=CARTESIAN_POINT('Ctrl Pts',(154.780650669046,6.57783712958646,131.409418076611));
#192234=CARTESIAN_POINT('Ctrl Pts',(154.502203045233,4.06453361755842,125.597288282381));
#192235=CARTESIAN_POINT('Ctrl Pts',(154.22375542142,-2.18387772549973,124.57020358456));
#192236=CARTESIAN_POINT('Ctrl Pts',(153.945307797607,-6.42541212718171,
129.272004644569));
#192237=CARTESIAN_POINT('Ctrl Pts',(153.666860173794,-4.76230668281685,
135.381965984011));
#192238=CARTESIAN_POINT('Ctrl Pts',(153.388412549982,1.27712595144142,137.285331620145));
#192239=CARTESIAN_POINT('Ctrl Pts',(153.109964926169,6.14294222739622,133.233001517943));
#192240=CARTESIAN_POINT('Ctrl Pts',(152.831517302356,5.36369469578529,126.948869073999));
#192241=CARTESIAN_POINT('Ctrl Pts',(152.553069678543,-0.344526230199219,
124.207745007359));
#192242=CARTESIAN_POINT('Ctrl Pts',(152.27462205473,-5.73614438167267,127.528588423912));
#192243=CARTESIAN_POINT('Ctrl Pts',(151.996174430917,-5.85652607262075,
133.859706456064));
#192244=CARTESIAN_POINT('Ctrl Pts',(151.717726807104,-0.595046410034728,
137.383110924578));
#192245=CARTESIAN_POINT('Ctrl Pts',(151.439279183291,5.21325183374003,134.860965250768));
#192246=CARTESIAN_POINT('Ctrl Pts',(151.160831559478,6.23082632381839,128.610998095198));
#192247=CARTESIAN_POINT('Ctrl Pts',(150.882383935665,1.52257581509584,124.376623945969));
#192248=CARTESIAN_POINT('Ctrl Pts',(150.603936311853,-4.58484748573611,
126.049025785542));
#192249=CARTESIAN_POINT('Ctrl Pts',(150.32548868804,-6.47901992942814,132.091348024725));
#192250=CARTESIAN_POINT('Ctrl Pts',(150.047041064227,-2.41928957569559,
136.950991709558));
#192251=CARTESIAN_POINT('Ctrl Pts',(149.768593440414,3.8636497092349,136.162181700472));
#192252=CARTESIAN_POINT('Ctrl Pts',(149.490145816601,6.59608366116008,130.449795860306));
#192253=CARTESIAN_POINT('Ctrl Pts',(149.211698192788,3.26703896508027,125.06323771061));
#192254=CARTESIAN_POINT('Ctrl Pts',(148.933250568975,-3.06425493618196,
124.95249104296));
#192255=CARTESIAN_POINT('Ctrl Pts',(148.654802945162,-6.57964824826877,
130.219326634649));
#192256=CARTESIAN_POINT('Ctrl Pts',(148.376355321349,-4.04866625388314,
136.02377987614));
#192257=CARTESIAN_POINT('Ctrl Pts',(148.097907697537,2.20284223947883,137.031841801807));
#192258=CARTESIAN_POINT('Ctrl Pts',(147.819460073724,6.43004632958585,132.317152748525));
#192259=CARTESIAN_POINT('Ctrl Pts',(147.541012449911,4.74835196802999,126.212281630895));
#192260=CARTESIAN_POINT('Ctrl Pts',(147.262564826098,-1.29684588225586,
124.327306766486));
#192261=CARTESIAN_POINT('Ctrl Pts',(146.984117202285,-6.15030572119196,
128.394427969547));
#192262=CARTESIAN_POINT('Ctrl Pts',(146.705669578472,-5.35193506149072,
134.676159544383));
#192263=CARTESIAN_POINT('Ctrl Pts',(146.427221954659,0.364602463157475,
137.399897053366));
#192264=CARTESIAN_POINT('Ctrl Pts',(146.148774330846,5.74608813598446,134.062658787717));
#192265=CARTESIAN_POINT('Ctrl Pts',(145.870326707034,5.84719952385297,127.731203680413));
#192266=CARTESIAN_POINT('Ctrl Pts',(145.59187908322,0.575020200877703,124.22382966629));
#192267=CARTESIAN_POINT('Ctrl Pts',(145.313431459408,-5.22557459540567,
126.76364211958));
#192268=CARTESIAN_POINT('Ctrl Pts',(145.034983835595,-6.22412162202233,
133.016677472446));
#192269=CARTESIAN_POINT('Ctrl Pts',(144.756536211782,-1.50300494324566,
137.236701713364));
#192270=CARTESIAN_POINT('Ctrl Pts',(144.478088587969,4.59929985250025,135.545718724575));
#192271=CARTESIAN_POINT('Ctrl Pts',(144.199640964156,6.47507277208744,129.497659263665));
#192272=CARTESIAN_POINT('Ctrl Pts',(143.921193340343,2.40057013901678,124.65039451108));
#192273=CARTESIAN_POINT('Ctrl Pts',(143.64274571653,-3.87993917743928,125.458323972397));
#192274=CARTESIAN_POINT('Ctrl Pts',(143.364298092718,-6.594973935395,131.178999942215));
#192275=CARTESIAN_POINT('Ctrl Pts',(143.085850468904,-3.2495498291107,136.555400674828));
#192276=CARTESIAN_POINT('Ctrl Pts',(142.807402845092,3.08205182079176,136.646876548744));
#192277=CARTESIAN_POINT('Ctrl Pts',(142.528955221279,6.58139841398854,131.369365704677));
#192278=CARTESIAN_POINT('Ctrl Pts',(142.250507597466,4.03276138391676,125.572642787588));
#192279=CARTESIAN_POINT('Ctrl Pts',(141.972059973653,-2.2217863466284,124.583612972623));
#192280=CARTESIAN_POINT('Ctrl Pts',(141.69361234984,-6.43462096491922,129.311146342943));
#192281=CARTESIAN_POINT('Ctrl Pts',(141.415164726027,-4.7343532651591,135.410870684068));
#192282=CARTESIAN_POINT('Ctrl Pts',(141.136717102214,1.31655379926713,137.277437314604));
#192283=CARTESIAN_POINT('Ctrl Pts',(140.858269478402,6.15761223939561,133.195562687939));
#192284=CARTESIAN_POINT('Ctrl Pts',(140.579821854588,5.34012584760095,126.916290175316));
#192285=CARTESIAN_POINT('Ctrl Pts',(140.301374230776,-0.384675318488256,
124.20996445632));
#192286=CARTESIAN_POINT('Ctrl Pts',(140.022926606963,-5.75597865932068,
127.563566655346));
#192287=CARTESIAN_POINT('Ctrl Pts',(139.74447898315,-5.83781880742758,133.895300184066));
#192288=CARTESIAN_POINT('Ctrl Pts',(139.466031359337,-0.554988664812238,
137.386611251964));
#192289=CARTESIAN_POINT('Ctrl Pts',(139.187583735524,5.23784894806212,134.829155547671));
#192290=CARTESIAN_POINT('Ctrl Pts',(138.909136111711,6.21735926081381,128.573109924773));
#192291=CARTESIAN_POINT('Ctrl Pts',(138.630688487898,1.48342014776303,124.367474685896));
#192292=CARTESIAN_POINT('Ctrl Pts',(138.352240864086,-4.61370961197883,
126.077023158863));
#192293=CARTESIAN_POINT('Ctrl Pts',(138.073793240272,-6.47106563055709,
132.130763813104));
#192294=CARTESIAN_POINT('Ctrl Pts',(137.79534561646,-2.38182846378423,136.965604729043));
#192295=CARTESIAN_POINT('Ctrl Pts',(137.516897992647,3.89619270241722,136.138563300043));
#192296=CARTESIAN_POINT('Ctrl Pts',(137.238450368834,6.59380311469226,130.409650196134));
#192297=CARTESIAN_POINT('Ctrl Pts',(136.960002745021,3.23203058975544,125.043456686844));
#192298=CARTESIAN_POINT('Ctrl Pts',(136.681555121208,-3.09982015369448,
124.971252454085));
#192299=CARTESIAN_POINT('Ctrl Pts',(136.403107497395,-6.58308761053252,
130.259389660389));
#192300=CARTESIAN_POINT('Ctrl Pts',(136.124659873582,-4.01681915499975,
136.048328553027));
#192301=CARTESIAN_POINT('Ctrl Pts',(135.846212249769,2.24070987145278,137.018317095051));
#192302=CARTESIAN_POINT('Ctrl Pts',(135.567764625956,6.43913599080291,132.277983202917));
#192303=CARTESIAN_POINT('Ctrl Pts',(135.289317002144,4.72031070388647,126.183462145311));
#192304=CARTESIAN_POINT('Ctrl Pts',(135.010869378331,-1.33624951990408,
124.335321040266));
#192305=CARTESIAN_POINT('Ctrl Pts',(134.732421754518,-6.16486171432077,
128.431911276607));
#192306=CARTESIAN_POINT('Ctrl Pts',(134.453974130705,-5.32826716351462,
134.708666556695));
#192307=CARTESIAN_POINT('Ctrl Pts',(134.175526506892,0.404744610239488,
137.397555414672));
#192308=CARTESIAN_POINT('Ctrl Pts',(133.897078883079,5.76581586005707,134.027620349581));
#192309=CARTESIAN_POINT('Ctrl Pts',(133.618631259266,5.82838401024617,127.695667055759));
#192310=CARTESIAN_POINT('Ctrl Pts',(133.340183635453,0.534951987407334,
124.220451277114));
#192311=CARTESIAN_POINT('Ctrl Pts',(133.06173601164,-5.25007477800144,126.795526540492));
#192312=CARTESIAN_POINT('Ctrl Pts',(132.783288387828,-6.21053930283845,
133.054524478268));
#192313=CARTESIAN_POINT('Ctrl Pts',(132.504840764015,-1.46382161007886,
137.245731754674));
#192314=CARTESIAN_POINT('Ctrl Pts',(132.226393140202,4.62807663068185,135.517633634551));
#192315=CARTESIAN_POINT('Ctrl Pts',(131.947945516389,6.46699854195874,129.458267868007));
#192316=CARTESIAN_POINT('Ctrl Pts',(131.669497892576,2.3630647236181,124.635895578019));
#192317=CARTESIAN_POINT('Ctrl Pts',(131.391050268763,-3.91241013359816,
125.482041313105));
#192318=CARTESIAN_POINT('Ctrl Pts',(131.11260264495,-6.59257120989826,131.219138479237));
#192319=CARTESIAN_POINT('Ctrl Pts',(130.834155021138,-3.2144814093103,136.575075053519));
#192320=CARTESIAN_POINT('Ctrl Pts',(130.555707397324,3.1175597702868,136.628006976231));
#192321=CARTESIAN_POINT('Ctrl Pts',(130.277259773512,6.58471582225214,131.329292396271));
#192322=CARTESIAN_POINT('Ctrl Pts',(129.998812149698,4.0008397148189,125.548191156024));
#192323=CARTESIAN_POINT('Ctrl Pts',(129.720364525886,-2.25961263864694,
124.59725287278));
#192324=CARTESIAN_POINT('Ctrl Pts',(129.441916902073,-6.44359136541048,
129.350343372922));
#192325=CARTESIAN_POINT('Ctrl Pts',(129.16346927826,-4.70622441430021,135.439604688201));
#192326=CARTESIAN_POINT('Ctrl Pts',(128.885021654447,1.35593286170785,137.269303146827));
#192327=CARTESIAN_POINT('Ctrl Pts',(128.606574030634,6.17205407880915,133.158035251063));
#192328=CARTESIAN_POINT('Ctrl Pts',(128.328126406821,5.31635911908928,126.883855350513));
#192329=CARTESIAN_POINT('Ctrl Pts',(128.049678783009,-0.424810152491945,
124.212428263054));
#192330=CARTESIAN_POINT('Ctrl Pts',(127.771231159195,-5.77559964706288,
127.598664975593));
#192331=CARTESIAN_POINT('Ctrl Pts',(127.492783535383,-5.81889521971155,
133.930779376167));
#192332=CARTESIAN_POINT('Ctrl Pts',(127.21433591157,-0.514910354280421,
137.389867671632));
#192333=CARTESIAN_POINT('Ctrl Pts',(126.935888287757,5.26225197196523,134.797196704317));
#192334=CARTESIAN_POINT('Ctrl Pts',(126.657440663944,6.20366181127538,128.535304434163));
#192335=CARTESIAN_POINT('Ctrl Pts',(126.378993040131,1.44420951175126,124.358563947));
#192336=CARTESIAN_POINT('Ctrl Pts',(126.100545416318,-4.64240077551519,
126.105195705413));
#192337=CARTESIAN_POINT('Ctrl Pts',(125.822097792505,-6.46287154396936,
132.170130451126));
#192338=CARTESIAN_POINT('Ctrl Pts',(125.543650168692,-2.34427909234318,
136.979989441362));
#192339=CARTESIAN_POINT('Ctrl Pts',(125.26520254488,3.92859132074607,136.114747238771));
#192340=CARTESIAN_POINT('Ctrl Pts',(124.986754921067,6.59127823242518,130.369519158099));
#192341=CARTESIAN_POINT('Ctrl Pts',(124.708307297254,3.19690245034852,125.023889135492));
#192342=CARTESIAN_POINT('Ctrl Pts',(124.429859673441,-3.13527050623128,
124.990230013179));
#192343=CARTESIAN_POINT('Ctrl Pts',(124.151412049628,-6.58628303406391,
130.299472880227));
#192344=CARTESIAN_POINT('Ctrl Pts',(123.872964425815,-3.98482321140548,
136.072682912751));
#192345=CARTESIAN_POINT('Ctrl Pts',(123.594516802002,2.2784944730983,137.004562127853));
#192346=CARTESIAN_POINT('Ctrl Pts',(123.316069178189,6.44798704746787,132.238759051683));
#192347=CARTESIAN_POINT('Ctrl Pts',(123.037621554376,4.6920945268939,126.154813888819));
#192348=CARTESIAN_POINT('Ctrl Pts',(122.759173930564,-1.37560364233486,
124.343575026687));
#192349=CARTESIAN_POINT('Ctrl Pts',(122.480726306751,-6.17918926623166,
128.46948249565));
#192350=CARTESIAN_POINT('Ctrl Pts',(122.202278682938,-5.30440182463932,
134.741028893516));
#192351=CARTESIAN_POINT('Ctrl Pts',(121.923831059125,0.444871759361186,
137.394969462721));
#192352=CARTESIAN_POINT('Ctrl Pts',(121.645383435312,5.78532992970255,133.992462472369));
#192353=CARTESIAN_POINT('Ctrl Pts',(121.366935811499,5.80935252372653,127.660245624887));
#192354=CARTESIAN_POINT('Ctrl Pts',(121.088488187686,0.494863951094175,
124.21731685712));
#192355=CARTESIAN_POINT('Ctrl Pts',(120.810040563873,-5.27438041714564,
126.827559510225));
#192356=CARTESIAN_POINT('Ctrl Pts',(120.53159294006,-6.19672684983677,133.092288103441));
#192357=CARTESIAN_POINT('Ctrl Pts',(120.253145316248,-1.42458403446405,
137.254523108609));
#192358=CARTESIAN_POINT('Ctrl Pts',(119.974697692435,4.65668191378195,135.489373892464));
#192359=CARTESIAN_POINT('Ctrl Pts',(119.696250068622,6.45868467482089,129.418926352309));
#192360=CARTESIAN_POINT('Ctrl Pts',(119.417802444809,2.32547174398699,124.621625219699));
#192361=CARTESIAN_POINT('Ctrl Pts',(119.139354820996,-3.94473611396066,
125.505955874312));
#192362=CARTESIAN_POINT('Ctrl Pts',(118.860907197183,-6.58992419425096,
131.259261646514));
#192363=CARTESIAN_POINT('Ctrl Pts',(118.58245957337,-3.17929387571916,136.594535596262));
#192364=CARTESIAN_POINT('Ctrl Pts',(118.304011949557,3.15295219745811,136.608921606362));
#192365=CARTESIAN_POINT('Ctrl Pts',(118.025564325744,6.58778923144938,131.289199636326));
#192366=CARTESIAN_POINT('Ctrl Pts',(117.747116701932,3.96876979313418,125.523934293753));
#192367=CARTESIAN_POINT('Ctrl Pts',(117.468669078118,-2.29735519988813,
124.611122779595));
#192368=CARTESIAN_POINT('Ctrl Pts',(117.190221454306,-6.45232299625411,
129.389594282045));
#192369=CARTESIAN_POINT('Ctrl Pts',(116.911773830493,-4.67792117256487,
135.468166931659));
#192370=CARTESIAN_POINT('Ctrl Pts',(116.63332620668,1.39526167955762,137.260929418227));
#192371=CARTESIAN_POINT('Ctrl Pts',(116.354878582867,6.18626721048894,133.120420597908));
#192372=CARTESIAN_POINT('Ctrl Pts',(116.076430959054,5.29239539093549,126.851565801475));
#192373=CARTESIAN_POINT('Ctrl Pts',(115.797983335241,-0.464929244999223,
124.215136336267));
#192374=CARTESIAN_POINT('Ctrl Pts',(115.519535711428,-5.79500661783607,
127.633882084071));
#192375=CARTESIAN_POINT('Ctrl Pts',(115.241088087616,-5.79975601069334,
133.96614271767));
#192376=CARTESIAN_POINT('Ctrl Pts',(114.962640463802,-0.474812963556037,
137.392880062915));
#192377=CARTESIAN_POINT('Ctrl Pts',(114.68419283999,5.28646000118636,134.765089904953));
#192378=CARTESIAN_POINT('Ctrl Pts',(114.405745216177,6.18973448276714,128.497583024264));
#192379=CARTESIAN_POINT('Ctrl Pts',(114.127297592364,1.40494536002493,124.349892059469));
#192380=CARTESIAN_POINT('Ctrl Pts',(113.848849968551,-4.67091991318358,
126.133542381245));
#192381=CARTESIAN_POINT('Ctrl Pts',(113.570402344738,-6.45443797329988,
132.209446480045));
#192382=CARTESIAN_POINT('Ctrl Pts',(113.291954720925,-2.30664285277824,
136.994145313484));
#192383=CARTESIAN_POINT('Ctrl Pts',(113.013507097112,3.96084436367879,136.09073439917));
#192384=CARTESIAN_POINT('Ctrl Pts',(112.735059473299,6.58850910791926,130.329404233275));
#192385=CARTESIAN_POINT('Ctrl Pts',(112.456611849487,3.16165584854565,125.004535781636));
#192386=CARTESIAN_POINT('Ctrl Pts',(112.178164225674,-3.1706046801665,125.00942301702));
#192387=CARTESIAN_POINT('Ctrl Pts',(111.899716601861,-6.58923440045535,
130.339574808866));
#192388=CARTESIAN_POINT('Ctrl Pts',(111.621268978048,-3.9526796087217,136.096842052857));
#192389=CARTESIAN_POINT('Ctrl Pts',(111.342821354235,2.31619464429322,136.990577409908));
#192390=CARTESIAN_POINT('Ctrl Pts',(111.064373730422,6.45659917160154,132.199481748287));
#192391=CARTESIAN_POINT('Ctrl Pts',(110.785926106609,4.66370448261314,126.12633792299));
#192392=CARTESIAN_POINT('Ctrl Pts',(110.507478482796,-1.41490679126679,
124.352068419894));
#192393=CARTESIAN_POINT('Ctrl Pts',(110.229030858983,-6.19328784601188,
128.50714023446));
#192394=CARTESIAN_POINT('Ctrl Pts',(109.950583235171,-5.28033992920373,
134.773245355646));
#192395=CARTESIAN_POINT('Ctrl Pts',(109.672135611358,0.484982423596243,
137.392139293334));
#192396=CARTESIAN_POINT('Ctrl Pts',(109.393687987545,5.80462962181993,133.957186458871));
#192397=CARTESIAN_POINT('Ctrl Pts',(109.115240363732,5.79010576951274,127.624940700352));
#192398=CARTESIAN_POINT('Ctrl Pts',(108.836792739919,0.454757577415474,
124.214426522456));
#192399=CARTESIAN_POINT('Ctrl Pts',(108.558345116106,-5.29849061218381,
126.859739841786));
#192400=CARTESIAN_POINT('Ctrl Pts',(108.279897492293,-6.18268477484283,
133.12996694862));
#192401=CARTESIAN_POINT('Ctrl Pts',(108.00144986848,-1.38529367036394,137.2630754494));
#192402=CARTESIAN_POINT('Ctrl Pts',(107.723002244667,4.68511464182123,135.460940545486));
#192403=CARTESIAN_POINT('Ctrl Pts',(107.444554620855,6.45013147874722,129.379636174388));
#192404=CARTESIAN_POINT('Ctrl Pts',(107.166106997042,2.28779259314522,124.607583964913));
#192405=CARTESIAN_POINT('Ctrl Pts',(106.887659373229,-3.97691592067581,
125.530066769856));
#192406=CARTESIAN_POINT('Ctrl Pts',(106.609211749416,-6.58703298653922,
131.299367957265));
#192407=CARTESIAN_POINT('Ctrl Pts',(106.330764125603,-3.14398853222427,
136.613781581943));
#192408=CARTESIAN_POINT('Ctrl Pts',(106.05231650179,3.18822779082625,136.589621146351));
#192409=CARTESIAN_POINT('Ctrl Pts',(105.773868877977,6.59061852769399,131.249088910493));
#192410=CARTESIAN_POINT('Ctrl Pts',(105.495421254164,3.93655280722527,125.49987309962));
#192411=CARTESIAN_POINT('Ctrl Pts',(105.216973630351,-2.33501263178752,
124.625222179118));
#192412=CARTESIAN_POINT('Ctrl Pts',(104.938526006539,-6.46081553389627,
129.428897615854));
#192413=CARTESIAN_POINT('Ctrl Pts',(104.660078382726,-4.64944458874018,
135.49655635606));
#192414=CARTESIAN_POINT('Ctrl Pts',(104.381630758913,1.43453879547275,137.252316439095));
#192415=CARTESIAN_POINT('Ctrl Pts',(104.1031831351,6.20025110776228,133.082720122298));
#192416=CARTESIAN_POINT('Ctrl Pts',(103.824735511287,5.26823555112421,126.819422724701));
#192417=CARTESIAN_POINT('Ctrl Pts',(103.546287887474,-0.505031109382345,
124.218088575609));
#192418=CARTESIAN_POINT('Ctrl Pts',(103.267840263661,-5.81419885250792,
127.669216675797));
#192419=CARTESIAN_POINT('Ctrl Pts',(102.989392639848,-5.78040188958328,
134.001388898174));
#192420=CARTESIAN_POINT('Ctrl Pts',(102.710945016035,-0.434697978462825,
137.395648314187));
#192421=CARTESIAN_POINT('Ctrl Pts',(102.432497392222,5.31047213868803,134.732836339309));
#192422=CARTESIAN_POINT('Ctrl Pts',(102.15404976841,6.17557779137139,128.459947092858));
#192423=CARTESIAN_POINT('Ctrl Pts',(101.875602144597,1.3656291475316,124.341459344644));
#192424=CARTESIAN_POINT('Ctrl Pts',(101.597154520784,-4.69926596819684,
126.162062135967));
#192425=CARTESIAN_POINT('Ctrl Pts',(101.318706896971,-6.44576523105769,
132.248710442988));
#192426=CARTESIAN_POINT('Ctrl Pts',(101.040259273158,-2.26892113971413,
137.008071820859));
#192427=CARTESIAN_POINT('Ctrl Pts',(100.761811649345,3.99295063606701,136.066525671043));
#192428=CARTESIAN_POINT('Ctrl Pts',(100.483364025532,6.58549584378548,130.289306908136));
#192429=CARTESIAN_POINT('Ctrl Pts',(100.204916401719,3.12629209042249,124.985397342422));
#192430=CARTESIAN_POINT('Ctrl Pts',(99.9264687779064,-3.20582136617937,
125.028830754405));
#192431=CARTESIAN_POINT('Ctrl Pts',(99.6480211540935,-6.5919416003429,130.379693960313));
#192432=CARTESIAN_POINT('Ctrl Pts',(99.3695735302808,-3.92038953804142,
136.120805078117));
#192433=CARTESIAN_POINT('Ctrl Pts',(99.0911259064677,2.35380898804382,136.976363459425));
#192434=CARTESIAN_POINT('Ctrl Pts',(98.812678282655,6.46497204407849,132.160152748165));
#192435=CARTESIAN_POINT('Ctrl Pts',(98.5342306588419,4.63514162304771,126.098035303012));
#192436=CARTESIAN_POINT('Ctrl Pts',(98.2557830350292,-1.45415751030726,
124.36080090516));
#192437=CARTESIAN_POINT('Ctrl Pts',(97.9773354112161,-6.20715693123341,
128.544883097616));
#192438=CARTESIAN_POINT('Ctrl Pts',(97.6988877874034,-5.25608236883021,
134.805314749293));
#192439=CARTESIAN_POINT('Ctrl Pts',(97.4204401635904,0.525075116629235,
137.389065011387));
#192440=CARTESIAN_POINT('Ctrl Pts',(97.1419925397775,5.82371422125203,133.921793616252));
#192441=CARTESIAN_POINT('Ctrl Pts',(96.8635449159648,5.77064446080036,127.589753590393));
#192442=CARTESIAN_POINT('Ctrl Pts',(96.5850972921516,0.414634352527504,
124.211780380221));
#192443=CARTESIAN_POINT('Ctrl Pts',(96.306649668339,-5.32240446970382,126.89206634272));
#192444=CARTESIAN_POINT('Ctrl Pts',(96.0282020445258,-6.16841359819089,
133.1675596176));
#192445=CARTESIAN_POINT('Ctrl Pts',(95.7497544207132,-1.34595197369742,
137.271388460138));
#192446=CARTESIAN_POINT('Ctrl Pts',(95.4713067969001,4.7133737612145,135.432334647225));
#192447=CARTESIAN_POINT('Ctrl Pts',(95.1928591730874,6.44133927067958,129.340398790155));
#192448=CARTESIAN_POINT('Ctrl Pts',(94.9144115492744,2.25002866730758,124.593772333964));
#192449=CARTESIAN_POINT('Ctrl Pts',(94.6359639254615,-4.008948361309,125.554373106298));
#192450=CARTESIAN_POINT('Ctrl Pts',(94.3575163016487,-6.58389769389783,
131.339455925338));
#192451=CARTESIAN_POINT('Ctrl Pts',(94.0790686778357,-3.10856668707799,
136.632812297395));
#192452=CARTESIAN_POINT('Ctrl Pts',(93.8006210540229,3.22338524324122,136.570106311383));
#192453=CARTESIAN_POINT('Ctrl Pts',(93.52217343021,6.59320360614536,131.208961705089));
#192454=CARTESIAN_POINT('Ctrl Pts',(93.2437258063971,3.90418995090443,125.476008465224));
#192455=CARTESIAN_POINT('Ctrl Pts',(92.9652781825842,-2.37258353893516,
124.639550548886));
#192456=CARTESIAN_POINT('Ctrl Pts',(92.6868305587713,-6.46906866364288,
129.468251917951));
#192457=CARTESIAN_POINT('Ctrl Pts',(92.4083829349583,-4.62079571803641,
135.524771909422));
#192458=CARTESIAN_POINT('Ctrl Pts',(92.1299353111456,1.47376275402524,137.24346452859));
#192459=CARTESIAN_POINT('Ctrl Pts',(91.8514876873325,6.21400525245068,133.04493522124));
#192460=CARTESIAN_POINT('Ctrl Pts',(91.5730400635199,5.24388049490719,126.787427311268));
#192461=CARTESIAN_POINT('Ctrl Pts',(91.2945924397067,-0.545114259651984,
124.221284871682));
#192462=CARTESIAN_POINT('Ctrl Pts',(91.016144815894,-5.83317563990314,127.704667441434));
#192463=CARTESIAN_POINT('Ctrl Pts',(90.7376971920811,-5.76083357355547,
134.036516611621));
#192464=CARTESIAN_POINT('Ctrl Pts',(90.4592495682681,-0.394566885476172,
137.398172322869));
#192465=CARTESIAN_POINT('Ctrl Pts',(90.1808019444553,5.33428749469169,134.700437202553));
#192466=CARTESIAN_POINT('Ctrl Pts',(89.9023543206424,6.16119226166949,128.422398034556));
#192467=CARTESIAN_POINT('Ctrl Pts',(89.6239066968295,1.32626233114802,124.333266115003));
#192468=CARTESIAN_POINT('Ctrl Pts',(89.3454590730166,-4.72743789018152,
126.190753912764));
#192469=CARTESIAN_POINT('Ctrl Pts',(89.0670114492037,-6.43685363861442,
132.28792088502));
#192470=CARTESIAN_POINT('Ctrl Pts',(88.7885638253908,-2.23111535094281,
137.021768447433));
#192471=CARTESIAN_POINT('Ctrl Pts',(88.5101162015778,4.02490894820102,136.042121951457));
#192472=CARTESIAN_POINT('Ctrl Pts',(88.2316685777651,6.58223855168135,130.2492286685));
#192473=CARTESIAN_POINT('Ctrl Pts',(87.9532209539521,3.09081248639635,124.966474527032));
#192474=CARTESIAN_POINT('Ctrl Pts',(87.6747733301392,-3.2409192593025,125.048452506173));
#192475=CARTESIAN_POINT('Ctrl Pts',(87.3963257063264,-6.59440453341028,
130.41982884794));
#192476=CARTESIAN_POINT('Ctrl Pts',(87.1178780825135,-3.88795419588509,
136.144571100572));
#192477=CARTESIAN_POINT('Ctrl Pts',(86.8394304587006,2.39133611053674,136.961920803106));
#192478=CARTESIAN_POINT('Ctrl Pts',(86.5609828348878,6.47310535463887,132.120773508667));
#192479=CARTESIAN_POINT('Ctrl Pts',(86.2825352110747,4.60640700660486,126.06990707765));
#192480=CARTESIAN_POINT('Ctrl Pts',(86.004087587262,-1.49335434500641,124.369772158902));
#192481=CARTESIAN_POINT('Ctrl Pts',(85.725639963449,-6.22079600797217,128.582709686544));
#192482=CARTESIAN_POINT('Ctrl Pts',(85.4471923396362,-5.23163004239161,
134.837235886113));
#192483=CARTESIAN_POINT('Ctrl Pts',(85.1687447158232,0.565148352810691,
137.385746730796));
#192484=CARTESIAN_POINT('Ctrl Pts',(84.8902970920103,5.842583020812,133.886285256006));
#192485=CARTESIAN_POINT('Ctrl Pts',(84.6118494681974,5.75096931873532,127.554685598878));
#192486=CARTESIAN_POINT('Ctrl Pts',(84.3334018443846,0.374495763211118,
124.209378528473));
#192487=CARTESIAN_POINT('Ctrl Pts',(84.0549542205716,-5.34612110356891,
126.924537815158));
#192488=CARTESIAN_POINT('Ctrl Pts',(83.7765065967588,-6.15391384870464,
133.205064717373));
#192489=CARTESIAN_POINT('Ctrl Pts',(83.498058972946,-1.30656040228555,137.279461832782));
#192490=CARTESIAN_POINT('Ctrl Pts',(83.2196113491328,4.74145822480973,135.403557257686));
#192491=CARTESIAN_POINT('Ctrl Pts',(82.9411637253203,6.43230837641647,129.301215653567));
#192492=CARTESIAN_POINT('Ctrl Pts',(82.6627161015071,2.21218136583022,124.580190838648));
#192493=CARTESIAN_POINT('Ctrl Pts',(82.3842684776944,-4.04083224888638,
125.578873982957));
#192494=CARTESIAN_POINT('Ctrl Pts',(82.1058208538814,-6.58051843250612,
131.379524065257));
#192495=CARTESIAN_POINT('Ctrl Pts',(81.8273732300686,-3.07302965285007,
136.651627037425));
#192496=CARTESIAN_POINT('Ctrl Pts',(81.5489256062556,3.25842325193051,136.550377824588));
#192497=CARTESIAN_POINT('Ctrl Pts',(81.270477982443,6.59554437101248,131.168819507043));
#192498=CARTESIAN_POINT('Ctrl Pts',(80.9920303586297,3.87168242338918,125.452341274876));
#192499=CARTESIAN_POINT('Ctrl Pts',(80.713582734817,-2.41006652912724,124.654107357959));
#192500=CARTESIAN_POINT('Ctrl Pts',(80.435135111004,-6.47708207967116,129.507655730047));
#192501=CARTESIAN_POINT('Ctrl Pts',(80.1566874871913,-4.59197562204804,
135.552812546207));
#192502=CARTESIAN_POINT('Ctrl Pts',(79.8782398633782,1.51293210175691,137.234374014721));
#192503=CARTESIAN_POINT('Ctrl Pts',(79.5997922395654,6.22752913488936,133.007067294864));
#192504=CARTESIAN_POINT('Ctrl Pts',(79.3213446157525,5.2193311247699,126.755580746775));
#192505=CARTESIAN_POINT('Ctrl Pts',(79.0428969919396,-0.585177210512381,
124.224725106049));
#192506=CARTESIAN_POINT('Ctrl Pts',(78.7644493681267,-5.85193627682986,
127.740233067343));
#192507=CARTESIAN_POINT('Ctrl Pts',(78.4860017443139,-5.74105178772106,
134.071524556339));
#192508=CARTESIAN_POINT('Ctrl Pts',(78.2075541205009,-0.354421171668466,
137.400451995434));
#192509=CARTESIAN_POINT('Ctrl Pts',(77.9291064966881,5.35790518671055,134.667893695246));
#192510=CARTESIAN_POINT('Ctrl Pts',(77.6506588728751,6.14657842672258,128.384937240753));
#192511=CARTESIAN_POINT('Ctrl Pts',(77.3722112490624,1.28684636962602,124.325312674148));
#192512=CARTESIAN_POINT('Ctrl Pts',(77.0937636252493,-4.75543463521666,
126.219616648455));
#192513=CARTESIAN_POINT('Ctrl Pts',(76.8153160014366,-6.42770352619243,
132.327076353179));
#192514=CARTESIAN_POINT('Ctrl Pts',(76.5368683776235,-2.19322688737167,
137.035234685673));
#192515=CARTESIAN_POINT('Ctrl Pts',(76.2584207538107,4.05671811585379,136.017524144697));
#192516=CARTESIAN_POINT('Ctrl Pts',(75.9799731299978,6.57873735230709,130.209170999483));
#192517=CARTESIAN_POINT('Ctrl Pts',(75.7015255061849,3.05521835117689,124.947768036657));
#192518=CARTESIAN_POINT('Ctrl Pts',(75.423077882372,-3.27589705897064,125.068287545233));
#192519=CARTESIAN_POINT('Ctrl Pts',(75.1446302585591,-6.5966231083926,130.459977984534));
#192520=CARTESIAN_POINT('Ctrl Pts',(74.8661826347462,-3.85537478415624,
136.168139239563));
#192521=CARTESIAN_POINT('Ctrl Pts',(74.5877350109334,2.42877462119068,136.94724997613));
#192522=CARTESIAN_POINT('Ctrl Pts',(74.3092873871204,6.48099880189986,132.081345489005));
#192523=CARTESIAN_POINT('Ctrl Pts',(74.0308397633076,4.57750169805637,126.041954289206));
#192524=CARTESIAN_POINT('Ctrl Pts',(73.7523921394947,-1.53249584291112,
124.378981848686));
#192525=CARTESIAN_POINT('Ctrl Pts',(73.4739445156818,-6.23420457082727,
128.620618599563));
#192526=CARTESIAN_POINT('Ctrl Pts',(73.1954968918689,-5.20698385597775,
134.869007583256));
#192527=CARTESIAN_POINT('Ctrl Pts',(72.917049268056,0.605200647212208,137.382184574524));
#192528=CARTESIAN_POINT('Ctrl Pts',(72.6386016442432,5.86123532130951,133.850662693911));
#192529=CARTESIAN_POINT('Ctrl Pts',(72.3601540204302,5.73108107238729,127.519738025268));
#192530=CARTESIAN_POINT('Ctrl Pts',(72.0817063966174,0.334343296816498,
124.207221056211));
#192531=CARTESIAN_POINT('Ctrl Pts',(71.8032587728044,-5.36963963495047,
126.957153055855));
#192532=CARTESIAN_POINT('Ctrl Pts',(71.5248111489915,-6.13918606367764,
133.242480858172));
#192533=CARTESIAN_POINT('Ctrl Pts',(71.2463635251787,-1.26712041579749,
137.287295268168));
#192534=CARTESIAN_POINT('Ctrl Pts',(70.9679159013657,4.76936699192676,135.374609443224));
#192535=CARTESIAN_POINT('Ctrl Pts',(70.689468277553,6.423039130601,129.262088216567));
#192536=CARTESIAN_POINT('Ctrl Pts',(70.4110206537399,2.17425209115883,124.566839982233));
#192537=CARTESIAN_POINT('Ctrl Pts',(70.1325730299272,-4.07256640193864,
125.603568491945));
#192538=CARTESIAN_POINT('Ctrl Pts',(69.8541254061142,-6.57689532758393,
131.419570892283));
#192539=CARTESIAN_POINT('Ctrl Pts',(69.5756777823013,-3.03737874637841,
136.670225104848));
#192540=CARTESIAN_POINT('Ctrl Pts',(69.2972301584884,3.2933405185478,136.530436417012));
#192541=CARTESIAN_POINT('Ctrl Pts',(69.0187825346755,6.5976407355574,131.128663803839));
#192542=CARTESIAN_POINT('Ctrl Pts',(68.7403349108627,3.83903142925813,125.428872405572));
#192543=CARTESIAN_POINT('Ctrl Pts',(68.4618872870498,-2.44746021341752,
124.668892066929));
#192544=CARTESIAN_POINT('Ctrl Pts',(68.1834396632368,-6.48485548504104,
129.547107592018));
#192545=CARTESIAN_POINT('Ctrl Pts',(67.904992039424,-4.56298536871445,135.580677227361));
#192546=CARTESIAN_POINT('Ctrl Pts',(67.6265444156111,1.55204538723279,137.225045234339));
#192547=CARTESIAN_POINT('Ctrl Pts',(67.3480967917982,6.2408222539455,132.969117746385));
#192548=CARTESIAN_POINT('Ctrl Pts',(67.0696491679854,5.19458835039884,126.723884211309));
#192549=CARTESIAN_POINT('Ctrl Pts',(66.7912015441724,-0.625218477415679,
124.228409151229));
#192550=CARTESIAN_POINT('Ctrl Pts',(66.5127539203596,-5.87048006810572,
127.775912235624));
#192551=CARTESIAN_POINT('Ctrl Pts',(66.2343062965465,-5.72105726510147,
134.106411435094));
#192552=CARTESIAN_POINT('Ctrl Pts',(65.9558586727338,-0.314262324654327,
137.402487247406));
#192553=CARTESIAN_POINT('Ctrl Pts',(65.6774110489208,5.3813243395822,134.6352070233));
#192554=CARTESIAN_POINT('Ctrl Pts',(65.398963425108,6.13173682805169,128.347566099575));
#192555=CARTESIAN_POINT('Ctrl Pts',(65.120515801295,1.24738272353907,124.317599316798));
#192556=CARTESIAN_POINT('Ctrl Pts',(64.8420681774823,-4.78325516587229,
126.248649273519));
#192557=CARTESIAN_POINT('Ctrl Pts',(64.5636205536692,-6.41831523285262,
132.366175396547));
#192558=CARTESIAN_POINT('Ctrl Pts',(64.2851729298565,-2.15525715297185,
137.048470036584));
#192559=CARTESIAN_POINT('Ctrl Pts',(64.0067253060435,4.08837696032456,135.992733162246));
#192560=CARTESIAN_POINT('Ctrl Pts',(63.7282776822307,6.57499237540094,130.169135385437));
#192561=CARTESIAN_POINT('Ctrl Pts',(63.4498300584178,3.01951100371835,124.929278564476));
#192562=CARTESIAN_POINT('Ctrl Pts',(63.1713824346048,-3.31075346906837,
125.088335136589));
#192563=CARTESIAN_POINT('Ctrl Pts',(62.892934810792,-6.59859724307971,130.500139882352));
#192564=CARTESIAN_POINT('Ctrl Pts',(62.614487186979,-3.82265251009718,136.191508621766));
#192565=CARTESIAN_POINT('Ctrl Pts',(62.3360395631662,2.46612313270748,136.932351522132));
#192566=CARTESIAN_POINT('Ctrl Pts',(62.0575919393533,6.48865209336687,132.041870150199));
#192567=CARTESIAN_POINT('Ctrl Pts',(61.7791443155403,4.5484267684992,126.014177973478));
#192568=CARTESIAN_POINT('Ctrl Pts',(61.5006966917276,-1.57158055361859,
124.388429633243));
#192569=CARTESIAN_POINT('Ctrl Pts',(61.2222490679146,-6.24738212293903,
128.658608431946));
#192570=CARTESIAN_POINT('Ctrl Pts',(60.9438014441017,-5.18214472286266,
134.900628663412));
#192571=CARTESIAN_POINT('Ctrl Pts',(60.6653538202889,0.645230515680748,
137.378378674564));
#192572=CARTESIAN_POINT('Ctrl Pts',(60.3869061964759,5.87967043157647,133.814927249971));
#192573=CARTESIAN_POINT('Ctrl Pts',(60.108458572663,5.71098045872276,127.484912164554));
#192574=CARTESIAN_POINT('Ctrl Pts',(59.8300109488502,0.294178441208572,
124.205308043382));
#192575=CARTESIAN_POINT('Ctrl Pts',(59.5515633250373,-5.39295919236059,
126.989910856244));
#192576=CARTESIAN_POINT('Ctrl Pts',(59.2731157012244,-6.12423078885343,
133.27980665353));
#192577=CARTESIAN_POINT('Ctrl Pts',(58.9946680774115,-1.2276334756968,137.294888476026));
#192578=CARTESIAN_POINT('Ctrl Pts',(58.7162204535986,4.79709902839574,135.345492276511));
#192579=CARTESIAN_POINT('Ctrl Pts',(58.4377728297857,6.41353187670863,129.223017929039));
#192580=CARTESIAN_POINT('Ctrl Pts',(58.1593252059728,2.13624224877676,124.553720259438));
#192581=CARTESIAN_POINT('Ctrl Pts',(57.8808775821599,-4.10414964454526,
125.628455718198));
#192582=CARTESIAN_POINT('Ctrl Pts',(57.602429958347,-6.57302851338661,131.459594922466));
#192583=CARTESIAN_POINT('Ctrl Pts',(57.3239823345341,-3.00161528872044,
136.688605810505));
#192584=CARTESIAN_POINT('Ctrl Pts',(57.0455347107212,3.32813574922106,136.510282827592));
#192585=CARTESIAN_POINT('Ctrl Pts',(56.7670870869083,6.59949262209846,131.088496083461));
#192586=CARTESIAN_POINT('Ctrl Pts',(56.4886394630955,3.80623817840574,125.405602726962));
#192587=CARTESIAN_POINT('Ctrl Pts',(56.2101918392826,-2.48476320616966,
124.683904127941));
#192588=CARTESIAN_POINT('Ctrl Pts',(55.9317442154696,-6.49238859170611,
129.586606041964));
#192589=CARTESIAN_POINT('Ctrl Pts',(55.6532965916568,-4.53382603227983,
135.608364920346));
#192590=CARTESIAN_POINT('Ctrl Pts',(55.3748489678439,1.59110116109648,137.215478533129));
#192591=CARTESIAN_POINT('Ctrl Pts',(55.096401344031,6.25388411703813,132.931087982032));
#192592=CARTESIAN_POINT('Ctrl Pts',(54.8179537202181,5.1696530886458,126.692338879397));
#192593=CARTESIAN_POINT('Ctrl Pts',(54.5395060964052,-0.665236576618623,
124.23233687071));
#192594=CARTESIAN_POINT('Ctrl Pts',(54.2610584725923,-5.88880632658389,
127.811703624173));
#192595=CARTESIAN_POINT('Ctrl Pts',(53.9826108487795,-5.70085074660091,
134.141175955143));
#192596=CARTESIAN_POINT('Ctrl Pts',(53.7041632249665,-0.274091832533765,
137.40427800337));
#192597=CARTESIAN_POINT('Ctrl Pts',(53.4257156011537,5.40454408550164,134.602378397932));
#192598=CARTESIAN_POINT('Ctrl Pts',(53.1472679773408,6.11666801561766,128.310285995821));
#192599=CARTESIAN_POINT('Ctrl Pts',(52.8688203535278,1.20787285522606,124.310126328773));
#192600=CARTESIAN_POINT('Ctrl Pts',(52.590372729715,-4.81089845124901,126.277850712144));
#192601=CARTESIAN_POINT('Ctrl Pts',(52.3119251059021,-6.40868910648141,
132.405216566294));
#192602=CARTESIAN_POINT('Ctrl Pts',(52.0334774820892,-2.11720755472543,
137.061474009724));
#192603=CARTESIAN_POINT('Ctrl Pts',(51.7550298582764,4.11988430848393,135.967749922743));
#192604=CARTESIAN_POINT('Ctrl Pts',(51.4765822344634,6.57100375973434,130.129123309894));
#192605=CARTESIAN_POINT('Ctrl Pts',(51.1981346106506,2.98369176716867,124.91100679562));
#192606=CARTESIAN_POINT('Ctrl Pts',(50.9196869868376,-3.34548719797895,
125.108594537373));
#192607=CARTESIAN_POINT('Ctrl Pts',(50.6412393630248,-6.60032686431936,
130.540313053181));
#192608=CARTESIAN_POINT('Ctrl Pts',(50.3627917392119,-3.78978858624336,
136.214678381218));
#192609=CARTESIAN_POINT('Ctrl Pts',(50.0843441153989,2.50338026112505,136.917225993175));
#192610=CARTESIAN_POINT('Ctrl Pts',(49.8058964915862,6.49606494544435,132.002348955022));
#192611=CARTESIAN_POINT('Ctrl Pts',(49.5274488677731,4.51918329531533,125.986579159731));
#192612=CARTESIAN_POINT('Ctrl Pts',(49.2490012439603,-1.6106070288309,124.39811516248));
#192613=CARTESIAN_POINT('Ctrl Pts',(48.9705536201474,-6.26032817600901,
128.696677775965));
#192614=CARTESIAN_POINT('Ctrl Pts',(48.6921059963345,-5.15711356346882,
134.932097954848));
#192615=CARTESIAN_POINT('Ctrl Pts',(48.4136583725217,0.685236474895564,
137.374329171949));
#192616=CARTESIAN_POINT('Ctrl Pts',(48.1352107487087,5.89788766849362,133.779080248378));
#192617=CARTESIAN_POINT('Ctrl Pts',(47.8567631248959,5.69066822257687,127.450209307224));
#192618=CARTESIAN_POINT('Ctrl Pts',(47.578315501083,0.254002684709825,124.203639560873));
#192619=CARTESIAN_POINT('Ctrl Pts',(47.29986787727,-5.41607891168467,127.022810002472));
#192620=CARTESIAN_POINT('Ctrl Pts',(47.0214202534572,-6.10904857840509,
133.317040720324));
#192621=CARTESIAN_POINT('Ctrl Pts',(46.7429726296443,-1.18810104518584,
137.302241174989));
#192622=CARTESIAN_POINT('Ctrl Pts',(46.4645250058313,4.82465330659632,135.316206836494));
#192623=CARTESIAN_POINT('Ctrl Pts',(46.1860773820186,6.40378696703385,129.184006238746));
#192624=CARTESIAN_POINT('Ctrl Pts',(45.9076297582056,2.09815324715241,124.54083215642));
#192625=CARTESIAN_POINT('Ctrl Pts',(45.6291821343927,-4.13558080637756,
125.653534739511));
#192626=CARTESIAN_POINT('Ctrl Pts',(45.3507345105798,-6.56891813320061,
131.499594672701));
#192627=CARTESIAN_POINT('Ctrl Pts',(45.072286886767,-2.96574060510383,136.706768473292));
#192628=CARTESIAN_POINT('Ctrl Pts',(44.793839262954,3.36280765460034,136.489917803126));
#192629=CARTESIAN_POINT('Ctrl Pts',(44.5153916391412,6.60109996201359,131.048317834339));
#192630=CARTESIAN_POINT('Ctrl Pts',(44.2369440153282,3.77330388599763,125.38253310131));
#192631=CARTESIAN_POINT('Ctrl Pts',(43.9584963915154,-2.52197412510756,
124.699142984721));
#192632=CARTESIAN_POINT('Ctrl Pts',(43.6800487677024,-6.49968112052436,
129.626149616253));
#192633=CARTESIAN_POINT('Ctrl Pts',(43.4016011438896,-4.50449869325427,
135.635874599185));
#192634=CARTESIAN_POINT('Ctrl Pts',(43.1231535200766,1.6300979761215,137.205674265588));
#192635=CARTESIAN_POINT('Ctrl Pts',(42.8447058962639,6.26671424015497,132.892979411015));
#192636=CARTESIAN_POINT('Ctrl Pts',(42.5662582724509,5.14452626349642,126.660945919963));
#192637=CARTESIAN_POINT('Ctrl Pts',(42.287810648638,-0.705230025235587,
124.236508118946));
#192638=CARTESIAN_POINT('Ctrl Pts',(42.0093630248251,-5.90691437317801,
127.847605906729));
#192639=CARTESIAN_POINT('Ctrl Pts',(41.7309154010123,-5.68043298097947,
134.175816828272));
#192640=CARTESIAN_POINT('Ctrl Pts',(41.4524677771993,-0.233911183839542,
137.405824196969));
#192641=CARTESIAN_POINT('Ctrl Pts',(41.1740201533865,5.42756356405245,134.569409035618));
#192642=CARTESIAN_POINT('Ctrl Pts',(40.8955725295735,6.10137254780096,128.273098310918));
#192643=CARTESIAN_POINT('Ctrl Pts',(40.6171249057607,1.1683182287399,124.302893986988));
#192644=CARTESIAN_POINT('Ctrl Pts',(40.3386772819477,-4.83836346701448,
126.307219882257));
#192645=CARTESIAN_POINT('Ctrl Pts',(40.060229658135,-6.39882550377857,132.444198415735));
#192646=CARTESIAN_POINT('Ctrl Pts',(39.781782034322,-2.07907950257448,137.074246123225));
#192647=CARTESIAN_POINT('Ctrl Pts',(39.5033344105091,4.15123899281517,135.94257535195));
#192648=CARTESIAN_POINT('Ctrl Pts',(39.2248867866962,6.56677165310695,130.089136255519));
#192649=CARTESIAN_POINT('Ctrl Pts',(38.9464391628834,2.94776196882331,124.892953407157));
#192650=CARTESIAN_POINT('Ctrl Pts',(38.6679915390704,-3.38009695863112,
125.129064996863));
#192651=CARTESIAN_POINT('Ctrl Pts',(38.3895439152575,-6.6018119080198,130.58049600839));
#192652=CARTESIAN_POINT('Ctrl Pts',(38.1110962914447,-3.75678423037978,
136.237647659355));
#192653=CARTESIAN_POINT('Ctrl Pts',(37.8326486676317,2.54054462586645,136.901873949744));
#192654=CARTESIAN_POINT('Ctrl Pts',(37.5542010438189,6.50323708344635,131.962783367948));
#192655=CARTESIAN_POINT('Ctrl Pts',(37.275753420006,4.48977236213255,125.959158870647));
#192656=CARTESIAN_POINT('Ctrl Pts',(36.9973057961931,-1.64957382240749,
124.4080380775));
#192657=CARTESIAN_POINT('Ctrl Pts',(36.7188581723802,-6.27304225031618,
128.734825220947));
#192658=CARTESIAN_POINT('Ctrl Pts',(36.4404105485673,-5.13189130533538,
134.96341429146));
#192659=CARTESIAN_POINT('Ctrl Pts',(36.1619629247544,0.725217042420823,
137.370036216732));
#192660=CARTESIAN_POINT('Ctrl Pts',(35.8835153009416,5.91588635701427,133.743123017455));
#192661=CARTESIAN_POINT('Ctrl Pts',(35.6050676771286,5.67014511662727,127.415630739204));
#192662=CARTESIAN_POINT('Ctrl Pts',(35.3266200533158,0.213817516048174,
124.202215670509));
#192663=CARTESIAN_POINT('Ctrl Pts',(35.0481724295028,-5.43899793621292,
127.055849275448));
#192664=CARTESIAN_POINT('Ctrl Pts',(34.76972480569,-6.09363999491508,133.354181678833));
#192665=CARTESIAN_POINT('Ctrl Pts',(34.4912771818771,-1.14852458915375,
137.309353092597));
#192666=CARTESIAN_POINT('Ctrl Pts',(34.2128295580642,4.85202880549439,135.286754208357));
#192667=CARTESIAN_POINT('Ctrl Pts',(33.9343819342512,6.393804762678,129.145054591279));
#192668=CARTESIAN_POINT('Ctrl Pts',(33.6559343104384,2.05998649768791,124.528176150753));
#192669=CARTESIAN_POINT('Ctrl Pts',(33.3774866866255,-4.16685872274224,
125.678804626571));
#192670=CARTESIAN_POINT('Ctrl Pts',(33.0990390628127,-6.56456433933747,
131.539568660782));
#192671=CARTESIAN_POINT('Ctrl Pts',(32.8205914389997,-2.92975602487846,
136.724712420187));
#192672=CARTESIAN_POINT('Ctrl Pts',(32.5421438151868,3.39735494990529,136.469342098247));
#192673=CARTESIAN_POINT('Ctrl Pts',(32.263696191374,6.60246269574222,131.008130545292));
#192674=CARTESIAN_POINT('Ctrl Pts',(31.985248567561,3.74022977242616,125.359664383471));
#192675=CARTESIAN_POINT('Ctrl Pts',(31.7068009437482,-2.55909159136699,
124.714608072585));
#192676=CARTESIAN_POINT('Ctrl Pts',(31.4283533199352,-6.50673280126843,
129.665736849585));
#192677=CARTESIAN_POINT('Ctrl Pts',(31.1499056961224,-4.47500443837311,
135.663205244496));
#192678=CARTESIAN_POINT('Ctrl Pts',(30.8714580723094,1.66903438726656,137.195632795014));
#192679=CARTESIAN_POINT('Ctrl Pts',(30.5930104484966,6.27931214787105,132.854793445461));
#192680=CARTESIAN_POINT('Ctrl Pts',(30.3145628246837,5.11920880603445,126.629706496284));
#192681=CARTESIAN_POINT('Ctrl Pts',(30.0361152008708,-0.745197341294603,
124.240922741373));
#192682=CARTESIAN_POINT('Ctrl Pts',(29.7576675770579,-5.9248035368878,127.883617752917));
#192683=CARTESIAN_POINT('Ctrl Pts',(29.4792199532451,-5.65980472482494,
134.210332770852));
#192684=CARTESIAN_POINT('Ctrl Pts',(29.2007723294321,-0.193721867480399,
137.407125770907));
#192685=CARTESIAN_POINT('Ctrl Pts',(28.9223247056193,5.45038192223944,134.536300158051));
#192686=CARTESIAN_POINT('Ctrl Pts',(28.6438770818064,6.08585099138068,128.236004422871));
#192687=CARTESIAN_POINT('Ctrl Pts',(28.3654294579935,1.12872030979243,124.29590255944));
#192688=CARTESIAN_POINT('Ctrl Pts',(28.0869818341806,-4.86564919544231,
126.336755695574));
#192689=CARTESIAN_POINT('Ctrl Pts',(27.8085342103677,-6.38872479024353,
132.483119500384));
#192690=CARTESIAN_POINT('Ctrl Pts',(27.5300865865548,-2.04087440936798,
137.086785903815));
#192691=CARTESIAN_POINT('Ctrl Pts',(27.2516389627419,4.18243985145892,135.91721038272));
#192692=CARTESIAN_POINT('Ctrl Pts',(26.973191338929,6.56229621234102,130.049175704046));
#192693=CARTESIAN_POINT('Ctrl Pts',(26.6947437151162,2.91172294007416,124.875119068062));
#192694=CARTESIAN_POINT('Ctrl Pts',(26.4162960913032,-3.41458146854746,
125.149745756519));
#192695=CARTESIAN_POINT('Ctrl Pts',(26.1378484674903,-6.60305231915217,
130.620687258984));
#192696=CARTESIAN_POINT('Ctrl Pts',(25.8594008436774,-3.72364066549499,
136.260415605043));
#192697=CARTESIAN_POINT('Ctrl Pts',(25.5809532198646,2.57761484979243,136.886295960714));
#192698=CARTESIAN_POINT('Ctrl Pts',(25.3025055960517,6.51016824160669,131.92317485509));
#192699=CARTESIAN_POINT('Ctrl Pts',(25.0240579722387,4.46019505878377,125.931918122295));
#192700=CARTESIAN_POINT('Ctrl Pts',(24.7456103484259,-1.68847949041943,
124.418198010604));
#192701=CARTESIAN_POINT('Ctrl Pts',(24.467162724613,-6.28552387473587,128.773049353324));
#192702=CARTESIAN_POINT('Ctrl Pts',(24.1887151008001,-5.10647888308236,
134.994576512808));
#192703=CARTESIAN_POINT('Ctrl Pts',(23.9102674769872,0.765170736761864,
137.365499967992));
#192704=CARTESIAN_POINT('Ctrl Pts',(23.6318198531744,5.93366583019039,133.707056889611));
#192705=CARTESIAN_POINT('Ctrl Pts',(23.3533722293614,5.64941190136517,127.381177741815));
#192706=CARTESIAN_POINT('Ctrl Pts',(23.0749246055485,0.173624424299845,
124.201036425055));
#192707=CARTESIAN_POINT('Ctrl Pts',(22.7964769817356,-5.46171541667246,
127.08902745089));
#192708=CARTESIAN_POINT('Ctrl Pts',(22.5180293579228,-6.07800560935413,
133.391228152785));
#192709=CARTESIAN_POINT('Ctrl Pts',(22.2395817341099,-1.10890557412062,
137.316223965318));
#192710=CARTESIAN_POINT('Ctrl Pts',(21.9611341102969,4.87922451068073,135.257135483476));
#192711=CARTESIAN_POINT('Ctrl Pts',(21.6826864864842,6.38358563353538,129.106164430008));
#192712=CARTESIAN_POINT('Ctrl Pts',(21.4042388626712,2.02174341466617,124.515752711409));
#192713=CARTESIAN_POINT('Ctrl Pts',(21.1257912388583,-4.19798223462457,
125.704264442993));
#192714=CARTESIAN_POINT('Ctrl Pts',(20.8473436150454,-6.55996729312864,
131.579515405459));
#192715=CARTESIAN_POINT('Ctrl Pts',(20.5688959912325,-2.89366288146616,
136.742436986267));
#192716=CARTESIAN_POINT('Ctrl Pts',(20.2904483674196,3.43177635497322,136.448556475397));
#192717=CARTESIAN_POINT('Ctrl Pts',(20.0120007436067,6.60358077278748,130.967935705476));
#192718=CARTESIAN_POINT('Ctrl Pts',(19.7335531197938,3.70701706326526,125.336997420853));
#192719=CARTESIAN_POINT('Ctrl Pts',(19.455105495981,-2.59611422954622,124.730298818468));
#192720=CARTESIAN_POINT('Ctrl Pts',(19.176657872168,-6.51354337263571,129.705366275038));
#192721=CARTESIAN_POINT('Ctrl Pts',(18.8982102483552,-4.4453443605568,135.690355843533));
#192722=CARTESIAN_POINT('Ctrl Pts',(18.6197626245423,1.70790895172861,137.1853544935));
#192723=CARTESIAN_POINT('Ctrl Pts',(18.3413150007294,6.29167737336628,132.816531500364));
#192724=CARTESIAN_POINT('Ctrl Pts',(18.0628673769165,5.09370165440758,126.598621765949));
#192725=CARTESIAN_POINT('Ctrl Pts',(17.7844197531036,-0.785137043792105,
124.245580574404));
#192726=CARTESIAN_POINT('Ctrl Pts',(17.5059721292907,-5.94247315482366,
127.919737828307));
#192727=CARTESIAN_POINT('Ctrl Pts',(17.2275245054778,-5.63896674252494,
134.244722503881));
#192728=CARTESIAN_POINT('Ctrl Pts',(16.949076881665,-0.15352537268619,137.408182676953));
#192729=CARTESIAN_POINT('Ctrl Pts',(16.6706292578521,5.47299831451989,134.503052992091));
#192730=CARTESIAN_POINT('Ctrl Pts',(16.3921816340391,6.07010392151387,128.199005706208));
#192731=CARTESIAN_POINT('Ctrl Pts',(16.1137340102263,1.08908056569879,124.289152305198));
#192732=CARTESIAN_POINT('Ctrl Pts',(15.8352863864134,-4.89275462544986,
126.366457057635));
#192733=CARTESIAN_POINT('Ctrl Pts',(15.5568387626005,-6.37838734016194,
132.521978378005));
#192734=CARTESIAN_POINT('Ctrl Pts',(15.2783911387876,-2.00259369080969,
137.099092886824));
#192735=CARTESIAN_POINT('Ctrl Pts',(14.9999435149747,4.21348572825588,135.891655954962));
#192736=CARTESIAN_POINT('Ctrl Pts',(14.7214958911618,6.55757760327567,130.009243136227));
#192737=CARTESIAN_POINT('Ctrl Pts',(14.4430482673489,2.87557601636067,124.857504439193));
#192738=CARTESIAN_POINT('Ctrl Pts',(14.164600643536,-3.44893944989177,125.170636050008));
#192739=CARTESIAN_POINT('Ctrl Pts',(13.8861530197231,-6.60404805175259,
130.660885315664));
#192740=CARTESIAN_POINT('Ctrl Pts',(13.6077053959103,-3.69035911973598,
136.282981374608));
#192741=CARTESIAN_POINT('Ctrl Pts',(13.3292577720973,2.61458955925225,136.870492603333));
#192742=CARTESIAN_POINT('Ctrl Pts',(13.0508101482845,6.5168581630887,131.883524884162));
#192743=CARTESIAN_POINT('Ctrl Pts',(12.7723625244716,4.43045248126686,125.904857924092));
#192744=CARTESIAN_POINT('Ctrl Pts',(12.4939149006587,-1.72732259120293,
124.428594585312));
#192745=CARTESIAN_POINT('Ctrl Pts',(12.2154672768458,-6.29777258675688,
128.811348756686));
#192746=CARTESIAN_POINT('Ctrl Pts',(11.9370196530329,-5.08087723837641,
135.025583464166));
#192747=CARTESIAN_POINT('Ctrl Pts',(11.65857202922,0.805096077419857,137.36072059382));
#192748=CARTESIAN_POINT('Ctrl Pts',(11.3801244054071,5.95122542919731,133.670883201288));
#192749=CARTESIAN_POINT('Ctrl Pts',(11.1016767815943,5.62846934506734,127.346851591727));
#192750=CARTESIAN_POINT('Ctrl Pts',(10.8232291577813,0.13342489883439,124.200101868207));
#192751=CARTESIAN_POINT('Ctrl Pts',(10.5447815339684,-5.4842305112587,127.12234329937));
#192752=CARTESIAN_POINT('Ctrl Pts',(10.2663339101556,-6.06214600106014,
133.428178769409));
#192753=CARTESIAN_POINT('Ctrl Pts',(9.98788628634267,-1.06924546818365,
137.322853538546));
#192754=CARTESIAN_POINT('Ctrl Pts',(9.70943866252976,4.90623941440849,135.227351759386));
#192755=CARTESIAN_POINT('Ctrl Pts',(9.43099103871685,6.37312995827954,129.067337196021));
#192756=CARTESIAN_POINT('Ctrl Pts',(9.15254341490403,1.98342541519871,124.503562298745));
#192757=CARTESIAN_POINT('Ctrl Pts',(8.87409579109107,-4.22895018873139,
125.729913245354));
#192758=CARTESIAN_POINT('Ctrl Pts',(8.59564816727821,-6.55512716491932,
131.61943342649));
#192759=CARTESIAN_POINT('Ctrl Pts',(8.31720054346528,-2.85746251231165,
136.759941514744));
#192760=CARTESIAN_POINT('Ctrl Pts',(8.03875291965246,3.46607059430627,136.427561704794));
#192761=CARTESIAN_POINT('Ctrl Pts',(7.76030529583951,6.60445415171875,130.927734804324));
#192762=CARTESIAN_POINT('Ctrl Pts',(7.48185767202662,3.67366698922382,125.314533053388));
#192763=CARTESIAN_POINT('Ctrl Pts',(7.20341004821377,-2.63304066775796,
124.746214640945));
#192764=CARTESIAN_POINT('Ctrl Pts',(6.92496242440086,-6.52011258225796,
129.745036424131));
#192765=CARTESIAN_POINT('Ctrl Pts',(6.64651480058794,-4.41551955887045,
135.71732539022));
#192766=CARTESIAN_POINT('Ctrl Pts',(6.36806717677509,1.74672022899638,137.174839741911));
#192767=CARTESIAN_POINT('Ctrl Pts',(6.08961955296221,6.30380945844269,132.778194993536));
#192768=CARTESIAN_POINT('Ctrl Pts',(5.81117192914928,5.06800575379271,126.567692880813));
#192769=CARTESIAN_POINT('Ctrl Pts',(5.53272430533639,-0.825047652747706,
124.250481445441));
#192770=CARTESIAN_POINT('Ctrl Pts',(5.25427668152353,-5.95992257223146,
127.955964794454));
#192771=CARTESIAN_POINT('Ctrl Pts',(4.97582905771062,-5.61791980623858,
134.278984753035));
#192772=CARTESIAN_POINT('Ctrl Pts',(4.69738143389771,-0.113323188952861,
137.408994875945));
#192773=CARTESIAN_POINT('Ctrl Pts',(4.41893381008486,5.49541190283514,134.469668769726));
#192774=CARTESIAN_POINT('Ctrl Pts',(4.14048618627195,6.05413192171396,128.162103531929));
#192775=CARTESIAN_POINT('Ctrl Pts',(3.86203856245905,1.0494004653243,124.282643474398));
#192776=CARTESIAN_POINT('Ctrl Pts',(3.58359093864613,-4.91967875263547,
126.396322867843));
#192777=CARTESIAN_POINT('Ctrl Pts',(3.30514331483329,-6.36781353659179,
132.560773608667));
#192778=CARTESIAN_POINT('Ctrl Pts',(3.02669569102039,-1.96423876540577,
137.111166616214));
#192779=CARTESIAN_POINT('Ctrl Pts',(2.74824806720748,4.24437547278969,135.865913015604));
#192780=CARTESIAN_POINT('Ctrl Pts',(2.46980044339459,6.55261600076067,129.969340031779));
#192781=CARTESIAN_POINT('Ctrl Pts',(2.19135281958173,2.83932253712042,124.840110173268));
#192782=CARTESIAN_POINT('Ctrl Pts',(1.91290519576881,-3.48316962951642,
125.191735103234));
#192783=CARTESIAN_POINT('Ctrl Pts',(1.6344575719559,-6.60479906892382,130.701088688872));
#192784=CARTESIAN_POINT('Ctrl Pts',(1.35600994814304,-3.65694082636265,
136.305344131865));
#192785=CARTESIAN_POINT('Ctrl Pts',(1.07756232433016,2.65146738413444,136.854464463202));
#192786=CARTESIAN_POINT('Ctrl Pts',(0.799114700517227,6.52330659999492,
131.843834924404));
#192787=CARTESIAN_POINT('Ctrl Pts',(0.520667076704378,4.40054573170394,
125.877979278764));
#192788=CARTESIAN_POINT('Ctrl Pts',(0.242219452891471,-1.76610168541259,
124.439227416375));
#192789=CARTESIAN_POINT('Ctrl Pts',(-0.03622817092143,-6.30978793249869,
128.849722011837));
#192790=CARTESIAN_POINT('Ctrl Pts',(-0.314675794734322,-5.05508731989592,
135.056433996558));
#192791=CARTESIAN_POINT('Ctrl Pts',(-0.593123418547181,0.844991584946641,
137.355698271319));
#192792=CARTESIAN_POINT('Ctrl Pts',(-0.871571042360099,5.96856450335716,
133.634603292916));
#192793=CARTESIAN_POINT('Ctrl Pts',(-1.15001866617301,5.60731822376822,
127.312653560908));
#192794=CARTESIAN_POINT('Ctrl Pts',(-1.42846628998586,0.0932204292604712,
124.199412034595));
#192795=CARTESIAN_POINT('Ctrl Pts',(-1.70691391379876,-5.50654238566651,
127.155795586355));
#192796=CARTESIAN_POINT('Ctrl Pts',(-1.98536153761166,-6.04606175771675,
133.465032159487));
#192797=CARTESIAN_POINT('Ctrl Pts',(-2.26380916142456,-1.02954574096264,
137.329241566624));
#192798=CARTESIAN_POINT('Ctrl Pts',(-2.5422567852374,4.9330725156305,135.197404139731));
#192799=CARTESIAN_POINT('Ctrl Pts',(-2.82070440905033,6.36243812434939,
129.028574328076));
#192800=CARTESIAN_POINT('Ctrl Pts',(-3.09915203286324,1.94503391917308,
124.491605364478));
#192801=CARTESIAN_POINT('Ctrl Pts',(-3.3775996566761,-4.25976143753379,
125.755750083229));
#192802=CARTESIAN_POINT('Ctrl Pts',(-3.65604728048899,-6.55004413406227,
131.659321244699));
#192803=CARTESIAN_POINT('Ctrl Pts',(-3.9344949043019,-2.82115625883292,
136.777225356981));
#192804=CARTESIAN_POINT('Ctrl Pts',(-4.2129425281148,3.50023639711881,136.406358564405));
#192805=CARTESIAN_POINT('Ctrl Pts',(-4.49139015192765,6.60508280017262,
130.887529331496));
#192806=CARTESIAN_POINT('Ctrl Pts',(-4.76983777574057,3.64018078610111,
125.292272113504));
#192807=CARTESIAN_POINT('Ctrl Pts',(-5.04828539955349,-2.66986953767946,
124.762354950249));
#192808=CARTESIAN_POINT('Ctrl Pts',(-5.32673302336633,-6.52644018671072,
129.784745826872));
#192809=CARTESIAN_POINT('Ctrl Pts',(-5.60518064717923,-4.38553113848304,
135.74411288519));
#192810=CARTESIAN_POINT('Ctrl Pts',(-5.88362827099213,1.7854667809037,137.164088929876));
#192811=CARTESIAN_POINT('Ctrl Pts',(-6.16207589480503,6.31570795354138,
132.739785345549));
#192812=CARTESIAN_POINT('Ctrl Pts',(-6.44052351861788,5.04212205636089,
126.536920986959));
#192813=CARTESIAN_POINT('Ctrl Pts',(-6.71897114243081,-0.864927689259141,
124.255625172881));
#192814=CARTESIAN_POINT('Ctrl Pts',(-6.99741876624371,-5.97715114251656,
127.992297308957));
#192815=CARTESIAN_POINT('Ctrl Pts',(-7.27586639005655,-5.59666469586782,
134.313118248714));
#192816=CARTESIAN_POINT('Ctrl Pts',(-7.55431401386947,-0.0731168059870705,
137.409562337785));
#192817=CARTESIAN_POINT('Ctrl Pts',(-7.83276163768236,5.51762185664139,
134.436148728019));
#192818=CARTESIAN_POINT('Ctrl Pts',(-8.11120926149529,6.03793558382929,
128.125299267457));
#192819=CARTESIAN_POINT('Ctrl Pts',(-8.38965688530811,1.00968147902963,
124.276376308223));
#192820=CARTESIAN_POINT('Ctrl Pts',(-8.66810450912106,-4.94642057931569,
126.426352019512));
#192821=CARTESIAN_POINT('Ctrl Pts',(-8.94655213293394,-6.3570037713493,
132.599503754801));
#192822=CARTESIAN_POINT('Ctrl Pts',(-9.22499975674682,-1.92581105441205,
137.123006644589));
#192823=CARTESIAN_POINT('Ctrl Pts',(-9.50344738055969,4.27510794042973,
135.839982518561));
#192824=CARTESIAN_POINT('Ctrl Pts',(-9.78189500437264,6.54741158865002,
129.929467869325));
#192825=CARTESIAN_POINT('Ctrl Pts',(-10.0603426281855,2.80296384573913,
124.822936914835));
#192826=CARTESIAN_POINT('Ctrl Pts',(-10.3387902519984,-3.51727073900952,
125.213042134361));
#192827=CARTESIAN_POINT('Ctrl Pts',(-10.6172378758113,-6.60530534283666,
130.74129588886));
#192828=CARTESIAN_POINT('Ctrl Pts',(-10.8956854996242,-3.62338702370218,
136.327503048155));
#192829=CARTESIAN_POINT('Ctrl Pts',(-11.174133123437,2.68824695791763,136.838212134247));
#192830=CARTESIAN_POINT('Ctrl Pts',(-11.4525807472499,6.52951331337615,
131.804106446543));
#192831=CARTESIAN_POINT('Ctrl Pts',(-11.7310283710628,4.37047591830066,
125.851283182307));
#192832=CARTESIAN_POINT('Ctrl Pts',(-12.0094759948757,-1.80481533607482,
124.450096109789));
#192833=CARTESIAN_POINT('Ctrl Pts',(-12.2879236186886,-6.32156946672825,
128.88816769684));
#192834=CARTESIAN_POINT('Ctrl Pts',(-12.5663712425015,-5.02911008329581,
135.087126966809));
#192835=CARTESIAN_POINT('Ctrl Pts',(-12.8448188663144,0.884855780999501,
137.350433186591));
#192836=CARTESIAN_POINT('Ctrl Pts',(-13.1232664901273,5.98568241016441,
133.598218508862));
#192837=CARTESIAN_POINT('Ctrl Pts',(-13.4017141139402,5.58595932123025,
127.278584916578));
#192838=CARTESIAN_POINT('Ctrl Pts',(-13.6801617377531,0.0530125053692662,
124.198966949783));
#192839=CARTESIAN_POINT('Ctrl Pts',(-13.958609361566,-5.5286502131212,127.189383072259));
#192840=CARTESIAN_POINT('Ctrl Pts',(-14.2370569853788,-6.02975347533148,
133.501786957402));
#192841=CARTESIAN_POINT('Ctrl Pts',(-14.5155046091917,-0.989807863545592,
137.335387812837));
#192842=CARTESIAN_POINT('Ctrl Pts',(-14.7939522330047,4.95972282003631,
135.167293734234));
#192843=CARTESIAN_POINT('Ctrl Pts',(-15.0723998568175,6.35151052793477,
128.989877262545));
#192844=CARTESIAN_POINT('Ctrl Pts',(-15.3508474806304,1.9065703492003,124.479882351679));
#192845=CARTESIAN_POINT('Ctrl Pts',(-15.6292951044433,-4.29041483930959,
125.781773999224));
#192846=CARTESIAN_POINT('Ctrl Pts',(-15.9077427282562,-6.54471838891106,
131.699177382027));
#192847=CARTESIAN_POINT('Ctrl Pts',(-16.186190352069,-2.78474546637155,
136.794287872519));
#192848=CARTESIAN_POINT('Ctrl Pts',(-16.464637975882,3.53427249738445,136.384947839923));
#192849=CARTESIAN_POINT('Ctrl Pts',(-16.7430855996949,6.60546669485434,
130.847320776822));
#192850=CARTESIAN_POINT('Ctrl Pts',(-17.0215332235078,3.6065596947407,125.270215426085));
#192851=CARTESIAN_POINT('Ctrl Pts',(-17.2999808473206,-2.7065994746034,
124.778719148295));
#192852=CARTESIAN_POINT('Ctrl Pts',(-17.5784284711336,-6.53252595152224,
129.824493011814));
#192853=CARTESIAN_POINT('Ctrl Pts',(-17.8568760949464,-4.35538021062653,
135.770717335825));
#192854=CARTESIAN_POINT('Ctrl Pts',(-18.1353237187593,1.82414717168286,
137.153102455769));
#192855=CARTESIAN_POINT('Ctrl Pts',(-18.4137713425722,6.32737241775927,
132.701303979686));
#192856=CARTESIAN_POINT('Ctrl Pts',(-18.6922189663851,5.01605152124203,
126.506307224649));
#192857=CARTESIAN_POINT('Ctrl Pts',(-18.9706665901979,-0.904775675556959,
124.261011566121));
#192858=CARTESIAN_POINT('Ctrl Pts',(-19.2491142140109,-5.99415822726801,
128.028734025499));
#192859=CARTESIAN_POINT('Ctrl Pts',(-19.5275618378238,-5.57520219902858,
134.347121726088));
#192860=CARTESIAN_POINT('Ctrl Pts',(-19.8060094616367,-0.0329077136511566,
137.409885041447));
#192861=CARTESIAN_POINT('Ctrl Pts',(-20.0844570854496,5.53962735294063,
134.402494109067));
#192862=CARTESIAN_POINT('Ctrl Pts',(-20.3629047092624,6.02151550802112,
128.08859427659));
#192863=CARTESIAN_POINT('Ctrl Pts',(-20.6413523330754,0.969925078616457,
124.270351038909));
#192864=CARTESIAN_POINT('Ctrl Pts',(-20.9197999568882,-4.9729791145623,
126.456543399899));
#192865=CARTESIAN_POINT('Ctrl Pts',(-21.1982475807011,-6.34595844499429,
132.638167381246));
#192866=CARTESIAN_POINT('Ctrl Pts',(-21.476695204514,-1.88731198178147,
137.134612533211));
#192867=CARTESIAN_POINT('Ctrl Pts',(-21.7551428283269,4.30568199237261,
135.813865424697));
#192868=CARTESIAN_POINT('Ctrl Pts',(-22.0335904521398,6.54196455979519,
129.889628126344));
#192869=CARTESIAN_POINT('Ctrl Pts',(-22.3120380759527,2.766501289502,124.805985300257));
#192870=CARTESIAN_POINT('Ctrl Pts',(-22.5904856997656,-3.5512415147419,
125.234556353852));
#192871=CARTESIAN_POINT('Ctrl Pts',(-22.8689333235784,-6.60556685473091,
130.781505425734));
#192872=CARTESIAN_POINT('Ctrl Pts',(-23.1473809473914,-3.58969895510304,
136.349457302372));
#192873=CARTESIAN_POINT('Ctrl Pts',(-23.4258285712042,2.7249269177212,136.821736218705));
#192874=CARTESIAN_POINT('Ctrl Pts',(-23.7042761950172,6.53547807324032,
131.764340922733));
#192875=CARTESIAN_POINT('Ctrl Pts',(-23.98272381883,4.34024415530499,125.824770623956));
#192876=CARTESIAN_POINT('Ctrl Pts',(-24.2611714426429,-1.84346210864104,
124.461200262812));
#192877=CARTESIAN_POINT('Ctrl Pts',(-24.5396190664558,-6.33311675287646,
128.926684387076));
#192878=CARTESIAN_POINT('Ctrl Pts',(-24.8180666902687,-5.00294649117208,
135.117661237576));
#192879=CARTESIAN_POINT('Ctrl Pts',(-25.0965143140816,0.924687188395989,
137.344925534737));
#192880=CARTESIAN_POINT('Ctrl Pts',(-25.3749619378945,6.00257851530871,
133.561730197376));
#192881=CARTESIAN_POINT('Ctrl Pts',(-25.6534095617074,5.56439342891538,
127.244646921163));
#192882=CARTESIAN_POINT('Ctrl Pts',(-25.9318571855203,0.0128026170801758,
124.198766630261));
#192883=CARTESIAN_POINT('Ctrl Pts',(-26.2103048093331,-5.5505531744091,
127.223104512485));
#192884=CARTESIAN_POINT('Ctrl Pts',(-26.4887524331461,-6.01322175821376,
133.538441801192));
#192885=CARTESIAN_POINT('Ctrl Pts',(-26.7672000569589,-0.950033308434149,
137.341292049436));
#192886=CARTESIAN_POINT('Ctrl Pts',(-27.0456476807718,4.98618934008908,
135.137021658645));
#192887=CARTESIAN_POINT('Ctrl Pts',(-27.3240953045847,6.34034757396176,
128.951247433362));
#192888=CARTESIAN_POINT('Ctrl Pts',(-27.6025429283976,1.86803613056208,
124.468393694749));
#192889=CARTESIAN_POINT('Ctrl Pts',(-27.8809905522105,-4.32090925818572,
125.807984029013));
#192890=CARTESIAN_POINT('Ctrl Pts',(-28.1594381760234,-6.53915012681315,
131.739000361591));
#192891=CARTESIAN_POINT('Ctrl Pts',(-28.4378857998363,-2.74823148414282,
136.811128429099));
#192892=CARTESIAN_POINT('Ctrl Pts',(-28.7163334236492,3.56817763388296,
136.36333032473));
#192893=CARTESIAN_POINT('Ctrl Pts',(-28.994781047462,6.60560582153853,130.807110630244));
#192894=CARTESIAN_POINT('Ctrl Pts',(-29.273228671275,3.5728049609845,125.248363808452));
#192895=CARTESIAN_POINT('Ctrl Pts',(-29.5516762950878,-2.74322911748845,
124.795306628702));
#192896=CARTESIAN_POINT('Ctrl Pts',(-29.8301239189007,-6.53836965118233,
129.86427650611));
#192897=CARTESIAN_POINT('Ctrl Pts',(-30.1085715427137,-4.32506789255462,
135.797137756284));
#192898=CARTESIAN_POINT('Ctrl Pts',(-30.3870191665265,1.862759968018,137.141880726698));
#192899=CARTESIAN_POINT('Ctrl Pts',(-30.6654667903394,6.33880241886542,
132.662752321889));
#192900=CARTESIAN_POINT('Ctrl Pts',(-30.9439144141524,4.98979511448915,
126.475852728289));
#192901=CARTESIAN_POINT('Ctrl Pts',(-31.2223620379652,-0.944590135059391,
124.266640425567));
#192902=CARTESIAN_POINT('Ctrl Pts',(-31.5008096617781,-6.01094319628198,
128.065273593905));
#192903=CARTESIAN_POINT('Ctrl Pts',(-31.7792572855909,-5.55353311102158,
134.380993925146));
#192904=CARTESIAN_POINT('Ctrl Pts',(-32.0577049094039,0.00730259809219468,
137.409962974972));
#192905=CARTESIAN_POINT('Ctrl Pts',(-32.3361525332168,5.56142757631112,
134.368706159956));
#192906=CARTESIAN_POINT('Ctrl Pts',(-32.6146001570296,6.0048723027414,128.051989919443));
#192907=CARTESIAN_POINT('Ctrl Pts',(-32.8930477808425,0.930132737272799,
124.264567889721));
#192908=CARTESIAN_POINT('Ctrl Pts',(-33.1714954046555,-4.99935337423901,
126.486895890252));
#192909=CARTESIAN_POINT('Ctrl Pts',(-33.4499430284683,-6.33467796681538,
132.676763055306));
#192910=CARTESIAN_POINT('Ctrl Pts',(-33.7283906522812,-1.84874297411136,
137.145983852021));
#192911=CARTESIAN_POINT('Ctrl Pts',(-34.0068382760941,4.33609649568588,
135.787562701789));
#192912=CARTESIAN_POINT('Ctrl Pts',(-34.285285899907,6.53627511603778,129.849822279112));
#192913=CARTESIAN_POINT('Ctrl Pts',(-34.5637335237199,2.72993621954223,
124.789255957683));
#192914=CARTESIAN_POINT('Ctrl Pts',(-34.8421811475328,-3.58508069791401,
125.256276964487));
#192915=CARTESIAN_POINT('Ctrl Pts',(-35.1206287713457,-6.60558359491616,
130.821715809516));
#192916=CARTESIAN_POINT('Ctrl Pts',(-35.3990763951586,-3.55587786888901,
136.37120608099));
#192917=CARTESIAN_POINT('Ctrl Pts',(-35.6775240189714,2.76150590435573,
136.805037327097));
#192918=CARTESIAN_POINT('Ctrl Pts',(-35.9559716427844,6.54120065856107,
131.724539826499));
#192919=CARTESIAN_POINT('Ctrl Pts',(-36.2344192665972,4.30985156296601,
125.798442586144));
#192920=CARTESIAN_POINT('Ctrl Pts',(-36.5128668904101,-1.8820405710409,
124.472539463974));
#192921=CARTESIAN_POINT('Ctrl Pts',(-36.791314514223,-6.3444293630544,128.965270655295));
#192922=CARTESIAN_POINT('Ctrl Pts',(-37.0697621380359,-4.9765975130263,
135.148035677403));
#192923=CARTESIAN_POINT('Ctrl Pts',(-37.3482097618488,0.964484331168655,
137.339175519844));
#192924=CARTESIAN_POINT('Ctrl Pts',(-37.6266573856617,6.0192521926987,133.525139710547));
#192925=CARTESIAN_POINT('Ctrl Pts',(-37.9051050094746,5.54262134595571,
127.210840832248));
#192926=CARTESIAN_POINT('Ctrl Pts',(-38.1835526332875,-0.0274077456145885,
124.198811083455));
#192927=CARTESIAN_POINT('Ctrl Pts',(-38.4620002571004,-5.5722504579079,
127.256958657474));
#192928=CARTESIAN_POINT('Ctrl Pts',(-38.7404478809132,-5.99646721895241,
133.574995332598));
#192929=CARTESIAN_POINT('Ctrl Pts',(-39.0188955047262,-0.910223549489097,
137.346954057637));
#192930=CARTESIAN_POINT('Ctrl Pts',(-39.297343128539,5.0124710950622,135.106589034709));
#192931=CARTESIAN_POINT('Ctrl Pts',(-39.5757907523519,6.32894967607775,
128.912686271968));
#192932=CARTESIAN_POINT('Ctrl Pts',(-39.8542383761648,1.82943269115809,
124.457139819403));
#192933=CARTESIAN_POINT('Ctrl Pts',(-40.1326859999777,-4.35124356418029,
125.834379201373));
#192934=CARTESIAN_POINT('Ctrl Pts',(-40.4111336237906,-6.53333955410249,
131.778788707735));
#192935=CARTESIAN_POINT('Ctrl Pts',(-40.6895812476035,-2.7116156651858,
136.827746402689));
#192936=CARTESIAN_POINT('Ctrl Pts',(-40.9680288714165,3.60195055024708,
136.34150681987));
#192937=CARTESIAN_POINT('Ctrl Pts',(-41.2464764952292,6.60550017506977,
130.766900381762));
#192938=CARTESIAN_POINT('Ctrl Pts',(-41.5249241190422,3.53891783562657,
125.226718070324));
#192939=CARTESIAN_POINT('Ctrl Pts',(-41.803371742855,-2.77975710900975,
124.812116776814));
#192940=CARTESIAN_POINT('Ctrl Pts',(-42.081819366668,-6.5439710691505,129.904094835568));
#192941=CARTESIAN_POINT('Ctrl Pts',(-42.3602669904808,-4.2945953075014,
135.82337316755));
#192942=CARTESIAN_POINT('Ctrl Pts',(-42.6387146142937,1.90130373909722,
137.130424158489));
#192943=CARTESIAN_POINT('Ctrl Pts',(-42.9171622381066,6.34999753331677,
132.624131800705));
#192944=CARTESIAN_POINT('Ctrl Pts',(-43.1956098619195,4.96335380904355,
126.44555862638));
#192945=CARTESIAN_POINT('Ctrl Pts',(-43.4740574857324,-0.984369592426984,
124.272511542639));
#192946=CARTESIAN_POINT('Ctrl Pts',(-43.7525051095453,-6.02750542758532,
128.101914660188));
#192947=CARTESIAN_POINT('Ctrl Pts',(-44.0309527333582,-5.53165823480283,
134.414733590743));
#192948=CARTESIAN_POINT('Ctrl Pts',(-44.3094003571711,0.0475126392350714,
137.409796135472));
#192949=CARTESIAN_POINT('Ctrl Pts',(-44.5878479809839,5.58302171893757,
134.334786132711));
#192950=CARTESIAN_POINT('Ctrl Pts',(-44.8662956047969,5.98800658471021,
128.015487552405));
#192951=CARTESIAN_POINT('Ctrl Pts',(-45.1447432286098,0.890305929518511,
124.259027074959));
#192952=CARTESIAN_POINT('Ctrl Pts',(-45.4231908524226,-5.02554238103793,
126.517408365848));
#192953=CARTESIAN_POINT('Ctrl Pts',(-45.7016384762356,-6.32316275481482,
132.715289346806));
#192954=CARTESIAN_POINT('Ctrl Pts',(-45.9800861000484,-1.81010546059046,
137.15712017965));
#192955=CARTESIAN_POINT('Ctrl Pts',(-46.2585337238614,4.36635032334889,
135.761075324496));
#192956=CARTESIAN_POINT('Ctrl Pts',(-46.5369813476741,6.53034346820225,
129.810051802649));
#192957=CARTESIAN_POINT('Ctrl Pts',(-46.8154289714873,2.6932699907919,124.772749507024));
#192958=CARTESIAN_POINT('Ctrl Pts',(-47.0938765952999,-3.61878703460243,
125.278203161403));
#192959=CARTESIAN_POINT('Ctrl Pts',(-47.3723242191129,-6.60535556277213,
130.861925550195));
#192960=CARTESIAN_POINT('Ctrl Pts',(-47.6507718429257,-3.52192501831287,
136.392748578105));
#192961=CARTESIAN_POINT('Ctrl Pts',(-47.9292194667387,2.79798256237344,
136.788116078208));
#192962=CARTESIAN_POINT('Ctrl Pts',(-48.2076670905515,6.54668085728591,
131.684704632686));
#192963=CARTESIAN_POINT('Ctrl Pts',(-48.4861147143645,4.27929926749242,
125.772300044465));
#192964=CARTESIAN_POINT('Ctrl Pts',(-48.7645623381774,-1.92054929373528,
124.484113293097));
#192965=CARTESIAN_POINT('Ctrl Pts',(-49.0430099619902,-6.35550687806913,
129.003925071669));
#192966=CARTESIAN_POINT('Ctrl Pts',(-49.3214575858032,-4.95006412522954,
135.178249160753));
#192967=CARTESIAN_POINT('Ctrl Pts',(-49.5999052096159,1.00424573461974,
137.333183354982));
#192968=CARTESIAN_POINT('Ctrl Pts',(-49.878352833429,6.03570282448511,133.488448404247));
#192969=CARTESIAN_POINT('Ctrl Pts',(-50.1568004572417,5.52064387912377,
127.17716790253));
#192970=CARTESIAN_POINT('Ctrl Pts',(-50.4352480810547,-0.0676170927052693,
124.199100307716));
#192971=CARTESIAN_POINT('Ctrl Pts',(-50.7136957048675,-5.5937412596168,
127.290944252747));
#192972=CARTESIAN_POINT('Ctrl Pts',(-50.9921433286805,-5.97949047839309,
133.611446197116));
#192973=CARTESIAN_POINT('Ctrl Pts',(-51.2705909524933,-0.870380061875472,
137.352373627632));
#192974=CARTESIAN_POINT('Ctrl Pts',(-51.5490385763063,5.03856711107574,
135.075996990117));
#192975=CARTESIAN_POINT('Ctrl Pts',(-51.8274862001192,6.31731725663583,
128.874195207264));
#192976=CARTESIAN_POINT('Ctrl Pts',(-52.105933823932,1.79076146145295,124.446121142656));
#192977=CARTESIAN_POINT('Ctrl Pts',(-52.3843814477449,-4.38141663324442,
125.860958538224));
#192978=CARTESIAN_POINT('Ctrl Pts',(-52.6628290715579,-6.52728688609205,
131.818540946088));
#192979=CARTESIAN_POINT('Ctrl Pts',(-52.9412766953706,-2.67489936631311,
136.844141177504));
#192980=CARTESIAN_POINT('Ctrl Pts',(-53.2197243191836,3.63558999500893,
136.319478134021));
#192981=CARTESIAN_POINT('Ctrl Pts',(-53.4981719429964,6.60514975936288,
130.726691521383));
#192982=CARTESIAN_POINT('Ctrl Pts',(-53.7766195668094,3.50489957436681,
125.205279013792));
#192983=CARTESIAN_POINT('Ctrl Pts',(-54.0550671906223,-2.8161820956091,
124.829148969725));
#192984=CARTESIAN_POINT('Ctrl Pts',(-54.3335148144351,-6.54932999786417,
129.943946524707));
#192985=CARTESIAN_POINT('Ctrl Pts',(-54.6119624382481,-4.26396358463975,
135.849422597461));
#192986=CARTESIAN_POINT('Ctrl Pts',(-54.890410062061,1.93977705666721,137.11873317567));
#192987=CARTESIAN_POINT('Ctrl Pts',(-55.1688576858738,6.3609573462743,132.58544384723));
#192988=CARTESIAN_POINT('Ctrl Pts',(-55.4473053096868,4.93672858469731,
126.415426041482));
#192989=CARTESIAN_POINT('Ctrl Pts',(-55.7257529334997,-1.02411257361735,
124.278624699781));
#192990=CARTESIAN_POINT('Ctrl Pts',(-56.0042005573125,-6.0438443074584,
128.138655866601));
#192991=CARTESIAN_POINT('Ctrl Pts',(-56.2826481811254,-5.50957838095395,
134.448339472641));
#192992=CARTESIAN_POINT('Ctrl Pts',(-56.5610958049383,0.0877209197796484,
137.40938452913));
#192993=CARTESIAN_POINT('Ctrl Pts',(-56.8395434287512,5.60440898064107,
134.300735284249));
#192994=CARTESIAN_POINT('Ctrl Pts',(-57.117991052564,5.97091897889293,127.979088528083));
#192995=CARTESIAN_POINT('Ctrl Pts',(-57.396438676377,0.850446131150592,
124.253728799937));
#192996=CARTESIAN_POINT('Ctrl Pts',(-57.6748863001899,-5.05154516451579,
126.548079696037));
#192997=CARTESIAN_POINT('Ctrl Pts',(-57.9533339240027,-6.31141323569307,
132.753744828139));
#192998=CARTESIAN_POINT('Ctrl Pts',(-58.2317815478157,-1.77140087294607,
137.168021103437));
#192999=CARTESIAN_POINT('Ctrl Pts',(-58.5102291716285,4.39644235429495,
135.734404274317));
#193000=CARTESIAN_POINT('Ctrl Pts',(-58.7886767954414,6.52416983608798,
129.770318170665));
#193001=CARTESIAN_POINT('Ctrl Pts',(-59.0671244192543,2.65650396193163,
124.756466559932));
#193002=CARTESIAN_POINT('Ctrl Pts',(-59.3455720430672,-3.6523592758065,
125.300334132115));
#193003=CARTESIAN_POINT('Ctrl Pts',(-59.62401966688,-6.60488276674858,130.902133157784));
#193004=CARTESIAN_POINT('Ctrl Pts',(-59.902467290693,-3.48784166150989,
136.414083995446));
#193005=CARTESIAN_POINT('Ctrl Pts',(-60.1809149145059,2.83435554011865,
136.770973099059));
#193006=CARTESIAN_POINT('Ctrl Pts',(-60.4593625383188,6.55191846634393,
131.644836817403));
#193007=CARTESIAN_POINT('Ctrl Pts',(-60.7378101621316,4.24858840101079,
125.746343967642));
#193008=CARTESIAN_POINT('Ctrl Pts',(-61.0162577859445,-1.95898684976931,
124.49592132131));
#193009=CARTESIAN_POINT('Ctrl Pts',(-61.2947054097575,-6.36634888743926,
129.042646203845));
#193010=CARTESIAN_POINT('Ctrl Pts',(-61.5731530335703,-4.92334731098624,
135.208300568055));
#193011=CARTESIAN_POINT('Ctrl Pts',(-61.8516006573832,1.04396992537583,
137.326949262193));
#193012=CARTESIAN_POINT('Ctrl Pts',(-62.1300482811962,6.05192980108374,
133.451657638088));
#193013=CARTESIAN_POINT('Ctrl Pts',(-62.408495905009,5.49846184280268,127.143629379772));
#193014=CARTESIAN_POINT('Ctrl Pts',(-62.6869435288219,-0.107823934219708,
124.199634292325));
#193015=CARTESIAN_POINT('Ctrl Pts',(-62.9653911526347,-5.61502478318622,
127.325060038955));
#193016=CARTESIAN_POINT('Ctrl Pts',(-63.2438387764477,-5.96229216561512,
133.647793044045));
#193017=CARTESIAN_POINT('Ctrl Pts',(-63.5222864002605,-0.830504322008783,
137.357550558596));
#193018=CARTESIAN_POINT('Ctrl Pts',(-63.8007340240734,5.06447642113188,
135.045246658467));
#193019=CARTESIAN_POINT('Ctrl Pts',(-64.0791816478864,6.30545074667997,
128.835775665549));
#193020=CARTESIAN_POINT('Ctrl Pts',(-64.3576292716992,1.75202387442331,
124.435338072814));
#193021=CARTESIAN_POINT('Ctrl Pts',(-64.6360768955121,-4.41142734730395,
125.887721054655));
#193022=CARTESIAN_POINT('Ctrl Pts',(-64.914524519325,-6.52099234706562,
131.858255603616));
#193023=CARTESIAN_POINT('Ctrl Pts',(-65.1929721431379,-2.63808394806071,
136.860312146029));
#193024=CARTESIAN_POINT('Ctrl Pts',(-65.4714197669508,3.66909472164654,
136.297245083462));
#193025=CARTESIAN_POINT('Ctrl Pts',(-65.7498673907637,6.60455458740261,
130.686485539062));
#193026=CARTESIAN_POINT('Ctrl Pts',(-66.0283150145766,3.4707514377644,125.184047433287));
#193027=CARTESIAN_POINT('Ctrl Pts',(-66.3067626383895,-2.85250272754526,
124.846402576302));
#193028=CARTESIAN_POINT('Ctrl Pts',(-66.5852102622024,-6.55444623874626,
129.983830096806));
#193029=CARTESIAN_POINT('Ctrl Pts',(-66.8636578860152,-4.23317385903938,
135.875285080744));
#193030=CARTESIAN_POINT('Ctrl Pts',(-67.1421055098281,1.978178495085,137.106808211453));
#193031=CARTESIAN_POINT('Ctrl Pts',(-67.4205531336411,6.37168145161813,
132.546689895061));
#193032=CARTESIAN_POINT('Ctrl Pts',(-67.6990007574539,4.90992042805787,
126.385456090168));
#193033=CARTESIAN_POINT('Ctrl Pts',(-67.9774483812669,-1.06381760593968,
124.284979670466));
#193034=CARTESIAN_POINT('Ctrl Pts',(-68.2558960050797,-6.05995923045808,
128.175495851683));
#193035=CARTESIAN_POINT('Ctrl Pts',(-68.5343436288926,-5.48729436765201,
134.481810325563));
#193036=CARTESIAN_POINT('Ctrl Pts',(-68.8127912527054,0.12792594979327,
137.408728171199));
#193037=CARTESIAN_POINT('Ctrl Pts',(-69.0912388765185,5.62558856890878,
134.266554876337));
#193038=CARTESIAN_POINT('Ctrl Pts',(-69.3696865003312,5.9536101184771,127.942794195258));
#193039=CARTESIAN_POINT('Ctrl Pts',(-69.6481341241442,0.810554819188534,
124.248673260987));
#193040=CARTESIAN_POINT('Ctrl Pts',(-69.9265817479571,-5.07736076112986,
126.578908744281));
#193041=CARTESIAN_POINT('Ctrl Pts',(-70.2050293717699,-6.29942984483285,
132.792128074323));
#193042=CARTESIAN_POINT('Ctrl Pts',(-70.4834769955829,-1.73263064539088,
137.178686219444));
#193043=CARTESIAN_POINT('Ctrl Pts',(-70.7619246193956,4.42637147345276,
135.707550539556));
#193044=CARTESIAN_POINT('Ctrl Pts',(-71.0403722432087,6.51775444846118,
129.730622855503));
#193045=CARTESIAN_POINT('Ctrl Pts',(-71.3188198670216,2.6196394953401,124.740407719779));
#193046=CARTESIAN_POINT('Ctrl Pts',(-71.5972674908343,-3.68579617749442,
125.322669056552));
#193047=CARTESIAN_POINT('Ctrl Pts',(-71.8757151146474,-6.6041652243652,
130.942337142376));
#193048=CARTESIAN_POINT('Ctrl Pts',(-72.1541627384602,-3.45362906145158,
136.435211542427));
#193049=CARTESIAN_POINT('Ctrl Pts',(-72.4326103622731,2.87062348977667,
136.753609024891));
#193050=CARTESIAN_POINT('Ctrl Pts',(-72.711057986086,6.55691329165398,131.604937857965));
#193051=CARTESIAN_POINT('Ctrl Pts',(-72.9895056098989,4.21772010152317,
125.720575317484));
#193052=CARTESIAN_POINT('Ctrl Pts',(-73.2679532337117,-1.99735181482566,
124.50796311106));
#193053=CARTESIAN_POINT('Ctrl Pts',(-73.5464008575247,-6.37695498941029,
129.081432616995));
#193054=CARTESIAN_POINT('Ctrl Pts',(-73.8248484813376,-4.89644806029751,
135.238188785743));
#193055=CARTESIAN_POINT('Ctrl Pts',(-74.1032961051504,1.08365543144292,
137.320473472483));
#193056=CARTESIAN_POINT('Ctrl Pts',(-74.3817437289633,6.06793252119795,
133.414768775364));
#193057=CARTESIAN_POINT('Ctrl Pts',(-74.6601913527762,5.47607605895596,
127.110226506756));
#193058=CARTESIAN_POINT('Ctrl Pts',(-74.9386389765891,-0.148026780279403,
124.200413017498));
#193059=CARTESIAN_POINT('Ctrl Pts',(-75.217086600402,-5.63610023994771,
127.359304751927));
#193060=CARTESIAN_POINT('Ctrl Pts',(-75.4955342242149,-5.94487291790794,
133.684034526541));
#193061=CARTESIAN_POINT('Ctrl Pts',(-75.7739818480278,-0.790597807498519,
137.362484658699));
#193062=CARTESIAN_POINT('Ctrl Pts',(-76.0524294718406,5.09019806515201,
135.014339179226));
#193063=CARTESIAN_POINT('Ctrl Pts',(-76.3308770956536,6.29335058592772,
128.797429070474));
#193064=CARTESIAN_POINT('Ctrl Pts',(-76.6093247194664,1.71322136550425,
124.424791009442));
#193065=CARTESIAN_POINT('Ctrl Pts',(-76.8877723432794,-4.44127459430165,
125.914665758975));
#193066=CARTESIAN_POINT('Ctrl Pts',(-77.1662199670922,-6.51445617026952,
131.89793120868));
#193067=CARTESIAN_POINT('Ctrl Pts',(-77.4446675909052,-2.60117077463652,
136.876258709042));
#193068=CARTESIAN_POINT('Ctrl Pts',(-77.7231152147181,3.7024634886308,136.274808492052));
#193069=CARTESIAN_POINT('Ctrl Pts',(-78.0015628385308,6.60371468124315,
130.646283924643));
#193070=CARTESIAN_POINT('Ctrl Pts',(-78.2800104623438,3.43647469119047,
125.163024115555));
#193071=CARTESIAN_POINT('Ctrl Pts',(-78.5584580861567,-2.88871765894464,
124.863876957204));
#193072=CARTESIAN_POINT('Ctrl Pts',(-78.8369057099696,-6.55931960221255,
130.023744073965));
#193073=CARTESIAN_POINT('Ctrl Pts',(-79.1153533337825,-4.20222727162433,
135.900959659057));
#193074=CARTESIAN_POINT('Ctrl Pts',(-79.3938009575953,2.01650663137172,
137.094649707722));
#193075=CARTESIAN_POINT('Ctrl Pts',(-79.6722485814083,6.38216945196263,
132.507871380239));
#193076=CARTESIAN_POINT('Ctrl Pts',(-79.9506962052212,4.88293033251105,
126.355649882987));
#193077=CARTESIAN_POINT('Ctrl Pts',(-80.229143829034,-1.10348321810992,
124.29157621921));
#193078=CARTESIAN_POINT('Ctrl Pts',(-80.507591452847,-6.07584959944043,
128.212433250316));
#193079=CARTESIAN_POINT('Ctrl Pts',(-80.7860390766598,-5.46480702063872,
134.515144909234));
#193080=CARTESIAN_POINT('Ctrl Pts',(-81.0644867004727,0.168126239464741,
137.407827085998));
#193081=CARTESIAN_POINT('Ctrl Pts',(-81.3429343242857,5.64655969892388,
134.232246175545));
#193082=CARTESIAN_POINT('Ctrl Pts',(-81.6213819480984,5.93608064484842,
127.906605898828));
#193083=CARTESIAN_POINT('Ctrl Pts',(-81.8998295719115,0.770633471818905,
124.243860645443));
#193084=CARTESIAN_POINT('Ctrl Pts',(-82.1782771957242,-5.10298821427442,
126.609894368197));
#193085=CARTESIAN_POINT('Ctrl Pts',(-82.4567248195372,-6.28721302628274,
132.830437663053));
#193086=CARTESIAN_POINT('Ctrl Pts',(-82.7351724433501,-1.69379621456928,
137.189115132473));
#193087=CARTESIAN_POINT('Ctrl Pts',(-83.0136200671628,4.45613657178832,
135.680515115291));
#193088=CARTESIAN_POINT('Ctrl Pts',(-83.2920676909759,6.51109754304618,
129.690967328089));
#193089=CARTESIAN_POINT('Ctrl Pts',(-83.5705153147887,2.58267795704331,
124.724573581631));
#193090=CARTESIAN_POINT('Ctrl Pts',(-83.8489629386017,-3.71909650065006,
125.345207107088));
#193091=CARTESIAN_POINT('Ctrl Pts',(-84.1274105624144,-6.60320296221082,
130.982536014198));
#193092=CARTESIAN_POINT('Ctrl Pts',(-84.4058581862275,-3.41928848589759,
136.456130436155));
#193093=CARTESIAN_POINT('Ctrl Pts',(-84.6843058100402,2.90678506742617,
136.736024499134));
#193094=CARTESIAN_POINT('Ctrl Pts',(-84.9627534338533,6.56166514813073,
131.565009232842));
#193095=CARTESIAN_POINT('Ctrl Pts',(-85.241201057666,4.1866955128661,125.694995048862));
#193096=CARTESIAN_POINT('Ctrl Pts',(-85.519648681479,-2.03564276727566,
124.520238216135));
#193097=CARTESIAN_POINT('Ctrl Pts',(-85.7980963052919,-6.38732479096924,
129.120282873878));
#193098=CARTESIAN_POINT('Ctrl Pts',(-86.0765439291047,-4.8693673699251,
135.267912706297));
#193099=CARTESIAN_POINT('Ctrl Pts',(-86.3549915529177,1.12330078225909,
137.313756225814));
#193100=CARTESIAN_POINT('Ctrl Pts',(-86.6334391767305,6.08371039184151,
133.377783183006));
#193101=CARTESIAN_POINT('Ctrl Pts',(-86.9118868005434,5.45348735709659,
127.076960521238));
#193102=CARTESIAN_POINT('Ctrl Pts',(-87.1903344243564,-0.188224141151809,
124.201436454379));
#193103=CARTESIAN_POINT('Ctrl Pts',(-87.4687820481692,-5.65696684894189,
127.39367712271));
#193104=CARTESIAN_POINT('Ctrl Pts',(-87.7472296719821,-5.92723338074904,
133.720169301662));
#193105=CARTESIAN_POINT('Ctrl Pts',(-88.0256772957949,-0.750661997095914,
137.367175745102));
#193106=CARTESIAN_POINT('Ctrl Pts',(-88.3041249196079,5.11573109001074,
134.983275697681));
#193107=CARTESIAN_POINT('Ctrl Pts',(-88.5825725434208,6.28101722275544,
128.759156842984));
#193108=CARTESIAN_POINT('Ctrl Pts',(-88.8610201672337,1.67435537253749,
124.414480343369));
#193109=CARTESIAN_POINT('Ctrl Pts',(-89.1394677910466,-4.47095726823472,
125.941791652735));
#193110=CARTESIAN_POINT('Ctrl Pts',(-89.4179154148595,-6.50767859790483,
131.93756629108));
#193111=CARTESIAN_POINT('Ctrl Pts',(-89.6963630386723,-2.56416121387375,
136.891980275641));
#193112=CARTESIAN_POINT('Ctrl Pts',(-89.9748106624853,3.73569505946763,
136.252169191183));
#193113=CARTESIAN_POINT('Ctrl Pts',(-90.253258286298,6.60263007200808,130.606088167816));
#193114=CARTESIAN_POINT('Ctrl Pts',(-90.5317059101111,3.40207060478355,
125.142209839621));
#193115=CARTESIAN_POINT('Ctrl Pts',(-90.8101535339238,-2.9248255478482,
124.881571464914));
#193116=CARTESIAN_POINT('Ctrl Pts',(-91.0886011577368,-6.56394990767886,
130.063686977158));
#193117=CARTESIAN_POINT('Ctrl Pts',(-91.3670487815497,-4.17112496913288,
135.926445381018));
#193118=CARTESIAN_POINT('Ctrl Pts',(-91.6454964053626,2.05476004526333,
137.082258115016));
#193119=CARTESIAN_POINT('Ctrl Pts',(-91.9239440291755,6.39242095867105,
132.468989741201));
#193120=CARTESIAN_POINT('Ctrl Pts',(-92.2023916529884,4.85575929818535,
126.326008524418));
#193121=CARTESIAN_POINT('Ctrl Pts',(-92.4808392768012,-1.14310794030347,
124.298414101576));
#193122=CARTESIAN_POINT('Ctrl Pts',(-92.7592869006141,-6.09151482558059,
128.249466693771));
#193123=CARTESIAN_POINT('Ctrl Pts',(-93.0377345244271,-5.44211717319261,
134.548341988427));
#193124=CARTESIAN_POINT('Ctrl Pts',(-93.3161821482399,0.208320299155509,
137.406681306919));
#193125=CARTESIAN_POINT('Ctrl Pts',(-93.5946297720528,5.6673215935918,134.197810453193));
#193126=CARTESIAN_POINT('Ctrl Pts',(-93.8730773958657,5.91833120756931,
127.870524979765));
#193127=CARTESIAN_POINT('Ctrl Pts',(-94.1515250196785,0.730683568342929,
124.239291131637));
#193128=CARTESIAN_POINT('Ctrl Pts',(-94.4299726434915,-5.12842657431339,
126.641035419604));
#193129=CARTESIAN_POINT('Ctrl Pts',(-94.7084202673044,-6.27476323274215,
132.868672174754));
#193130=CARTESIAN_POINT('Ctrl Pts',(-94.9868678911172,-1.6548990195065,
137.199307456074));
#193131=CARTESIAN_POINT('Ctrl Pts',(-95.2653155149302,4.48573654634406,
135.653299003326));
#193132=CARTESIAN_POINT('Ctrl Pts',(-95.543763138743,6.50419936651746,129.651353057874));
#193133=CARTESIAN_POINT('Ctrl Pts',(-95.822210762556,2.54562071666526,124.708964732227));
#193134=CARTESIAN_POINT('Ctrl Pts',(-96.1006583863688,-3.75225901131679,
125.367947448562));
#193135=CARTESIAN_POINT('Ctrl Pts',(-96.3791060101818,-6.60199601594203,
131.022728283664));
#193136=CARTESIAN_POINT('Ctrl Pts',(-96.6575536339946,-3.38482120735248,
136.476839901474));
#193137=CARTESIAN_POINT('Ctrl Pts',(-96.9360012578075,2.94283893308538,
136.718220173391));
#193138=CARTESIAN_POINT('Ctrl Pts',(-97.2144488816204,6.5661738596919,131.525052421605));
#193139=CARTESIAN_POINT('Ctrl Pts',(-97.4928965054334,4.15551578466796,
125.669604109659));
#193140=CARTESIAN_POINT('Ctrl Pts',(-97.771344129246,-2.07385828823457,
124.532746181678));
#193141=CARTESIAN_POINT('Ctrl Pts',(-98.0497917530593,-6.39745790785863,
129.15919553488));
#193142=CARTESIAN_POINT('Ctrl Pts',(-98.3282393768718,-4.84210624335443,
135.297471228287));
#193143=CARTESIAN_POINT('Ctrl Pts',(-98.606687000685,1.16290450875192,137.306797771098));
#193144=CARTESIAN_POINT('Ctrl Pts',(-98.8851346244975,6.09926282835875,
133.340702231527));
#193145=CARTESIAN_POINT('Ctrl Pts',(-99.1635822483109,5.43069657425812,
127.043832655902));
#193146=CARTESIAN_POINT('Ctrl Pts',(-99.4420298721233,-0.228414527308866,
124.202704565042));
#193147=CARTESIAN_POINT('Ctrl Pts',(-99.7204774959365,-5.67762383694899,
127.428175877623));
#193148=CARTESIAN_POINT('Ctrl Pts',(-99.9989251197493,-5.90937420777732,
133.756196030418));
#193149=CARTESIAN_POINT('Ctrl Pts',(-100.277372743562,-0.710698370637635,
137.371623643978));
#193150=CARTESIAN_POINT('Ctrl Pts',(-100.555820367375,5.14107454957247,
134.9520573649));
#193151=CARTESIAN_POINT('Ctrl Pts',(-100.834267991188,6.26845111417983,
128.720960401273));
#193152=CARTESIAN_POINT('Ctrl Pts',(-101.112715615001,1.63542733571746,
124.404406456659));
#193153=CARTESIAN_POINT('Ctrl Pts',(-101.391163238814,-4.50047426920288,
125.969097730777));
#193154=CARTESIAN_POINT('Ctrl Pts',(-101.669610862627,-6.50065988111587,
131.977159382129));
#193155=CARTESIAN_POINT('Ctrl Pts',(-101.94805848644,-2.52705663717401,
136.907476263252));
#193156=CARTESIAN_POINT('Ctrl Pts',(-102.226506110253,3.76878820275105,
136.229328019765));
#193157=CARTESIAN_POINT('Ctrl Pts',(-102.504953734065,6.60130079988703,
130.565899758046));
#193158=CARTESIAN_POINT('Ctrl Pts',(-102.783401357878,3.36754045339959,
125.121605376767));
#193159=CARTESIAN_POINT('Ctrl Pts',(-103.061848981691,-2.96082505626518,
124.899485443752));
#193160=CARTESIAN_POINT('Ctrl Pts',(-103.340296605504,-6.56833698356739,
130.103657326284));
#193161=CARTESIAN_POINT('Ctrl Pts',(-103.618744229317,-4.13986810407194,
135.951741302244));
#193162=CARTESIAN_POINT('Ctrl Pts',(-103.89719185313,2.0929373192654,137.06963389251));
#193163=CARTESIAN_POINT('Ctrl Pts',(-104.175639476943,6.40243559186997,
132.430046418718));
#193164=CARTESIAN_POINT('Ctrl Pts',(-104.454087100755,4.82840833191319,
126.296533112833));
#193165=CARTESIAN_POINT('Ctrl Pts',(-104.732534724569,-1.18269030421136,
124.305493064181));
#193166=CARTESIAN_POINT('Ctrl Pts',(-105.010982348381,-6.10695432839948,
128.286594809759));
#193167=CARTESIAN_POINT('Ctrl Pts',(-105.289429972194,-5.41922566609253,
134.581400333014));
#193168=CARTESIAN_POINT('Ctrl Pts',(-105.567877596007,0.248506639461218,
137.40529087642));
#193169=CARTESIAN_POINT('Ctrl Pts',(-105.84632521982,5.68787348357469,134.163248985309));
#193170=CARTESIAN_POINT('Ctrl Pts',(-106.124772843633,5.90036246435008,
127.834552775061));
#193171=CARTESIAN_POINT('Ctrl Pts',(-106.403220467446,0.690706589119241,
124.234964888896));
#193172=CARTESIAN_POINT('Ctrl Pts',(-106.681668091259,-5.1536748986197,
126.672330744555));
#193173=CARTESIAN_POINT('Ctrl Pts',(-106.960115715072,-6.26208092554253,
132.906830192629));
#193174=CARTESIAN_POINT('Ctrl Pts',(-107.238563338885,-1.61594050155245,
137.209262812568));
#193175=CARTESIAN_POINT('Ctrl Pts',(-107.517010962697,4.51517030028232,
135.625903212168));
#193176=CARTESIAN_POINT('Ctrl Pts',(-107.79545858651,6.49706017448951,129.611781512777));
#193177=CARTESIAN_POINT('Ctrl Pts',(-108.073906210323,2.50846914737518,
124.69358174996));
#193178=CARTESIAN_POINT('Ctrl Pts',(-108.352353834136,-3.78528248064593,
125.390889238328));
#193179=CARTESIAN_POINT('Ctrl Pts',(-108.630801457949,-6.60054443028347,
131.062912461436));
#193180=CARTESIAN_POINT('Ctrl Pts',(-108.909249081762,-3.35022850301195,
136.497339170987));
#193181=CARTESIAN_POINT('Ctrl Pts',(-109.187696705575,2.97878375076591,
136.700196707408));
#193182=CARTESIAN_POINT('Ctrl Pts',(-109.466144329388,6.57043925926657,
131.485068904869));
#193183=CARTESIAN_POINT('Ctrl Pts',(-109.7445919532,4.12418207230337,125.644403440746));
#193184=CARTESIAN_POINT('Ctrl Pts',(-110.023039577014,-2.11199696161116,
124.5454865442));
#193185=CARTESIAN_POINT('Ctrl Pts',(-110.301487200826,-6.40735396459295,
129.198169158078));
#193186=CARTESIAN_POINT('Ctrl Pts',(-110.579934824639,-4.81466569075636,
135.326863256411));
#193187=CARTESIAN_POINT('Ctrl Pts',(-110.858382448452,1.20246514338981,
137.299598366182));
#193188=CARTESIAN_POINT('Ctrl Pts',(-111.136830072265,6.11458925444912,
133.303527294979));
#193189=CARTESIAN_POINT('Ctrl Pts',(-111.415277696078,5.407704554961,127.010844138312));
#193190=CARTESIAN_POINT('Ctrl Pts',(-111.693725319891,-0.268596449482207,
124.204217302498));
#193191=CARTESIAN_POINT('Ctrl Pts',(-111.972172943703,-5.69807043851701,
127.462799738304));
#193192=CARTESIAN_POINT('Ctrl Pts',(-112.250620567517,-5.89129606077132,
133.792113377828));
#193193=CARTESIAN_POINT('Ctrl Pts',(-112.529068191329,-0.670708408989202,
137.375828190507));
#193194=CARTESIAN_POINT('Ctrl Pts',(-112.807515815142,5.16622750472631,
134.920685337692));
#193195=CARTESIAN_POINT('Ctrl Pts',(-113.085963438955,6.25565272584325,
128.682841160722));
#193196=CARTESIAN_POINT('Ctrl Pts',(-113.364411062768,1.5964386975353,124.394569722605));
#193197=CARTESIAN_POINT('Ctrl Pts',(-113.642858686581,-4.52982450344111,
125.996582981263));
#193198=CARTESIAN_POINT('Ctrl Pts',(-113.921306310394,-6.49340027998504,
132.016709014688));
#193199=CARTESIAN_POINT('Ctrl Pts',(-114.199753934207,-2.48985841946147,
136.922746097669));
#193200=CARTESIAN_POINT('Ctrl Pts',(-114.47820155802,3.80174169220082,136.206285824184));
#193201=CARTESIAN_POINT('Ctrl Pts',(-114.756649181833,6.59972691413776,
130.525720184532));
#193202=CARTESIAN_POINT('Ctrl Pts',(-115.035096805645,3.3328855165654,125.101211490497));
#193203=CARTESIAN_POINT('Ctrl Pts',(-115.313544429458,-2.99671485022117,
124.917618229914));
#193204=CARTESIAN_POINT('Ctrl Pts',(-115.591992053271,-6.57248066731354,
130.143653640229));
#193205=CARTESIAN_POINT('Ctrl Pts',(-115.870439677084,-4.10845783467579,
135.976846485386));
#193206=CARTESIAN_POINT('Ctrl Pts',(-116.148887300897,2.13103703870585,
137.056777507999));
#193207=CARTESIAN_POINT('Ctrl Pts',(-116.42733492471,6.41221298046361,132.391042855849));
#193208=CARTESIAN_POINT('Ctrl Pts',(-116.705782548523,4.8008784471946,126.267224740454));
#193209=CARTESIAN_POINT('Ctrl Pts',(-116.984230172336,-1.22222884309565,
124.312812844714));
#193210=CARTESIAN_POINT('Ctrl Pts',(-117.262677796149,-6.12216753577917,
128.323816222486));
#193211=CARTESIAN_POINT('Ctrl Pts',(-117.541125419961,-5.39613334759327,
134.614318718005));
#193212=CARTESIAN_POINT('Ctrl Pts',(-117.819573043774,0.288683771261777,
137.403655846021));
#193213=CARTESIAN_POINT('Ctrl Pts',(-118.098020667587,5.70821460731317,
134.128563052582));
#193214=CARTESIAN_POINT('Ctrl Pts',(-118.3764682914,5.88217508103065,127.79869061768));
#193215=CARTESIAN_POINT('Ctrl Pts',(-118.654915915213,0.650704015508265,
124.230882077529));
#193216=CARTESIAN_POINT('Ctrl Pts',(-118.933363539026,-5.17873225160735,
126.703779183394));
#193217=CARTESIAN_POINT('Ctrl Pts',(-119.211811162839,-6.24916657463125,
132.944910302722));
#193218=CARTESIAN_POINT('Ctrl Pts',(-119.490258786652,-1.57692210432836,
137.218980833058));
#193219=CARTESIAN_POINT('Ctrl Pts',(-119.768706410464,4.54443674292479,
135.598328756974));
#193220=CARTESIAN_POINT('Ctrl Pts',(-120.047154034278,6.48968023150711,
129.572254159139));
#193221=CARTESIAN_POINT('Ctrl Pts',(-120.32560165809,2.47122462583917,124.67842520485));
#193222=CARTESIAN_POINT('Ctrl Pts',(-120.604049281903,-3.81816568494053,
125.414031626265));
#193223=CARTESIAN_POINT('Ctrl Pts',(-120.882496905716,-6.59884825902321,
131.103087058474));
#193224=CARTESIAN_POINT('Ctrl Pts',(-121.160944529529,-3.31551165472302,
136.517627485086));
#193225=CARTESIAN_POINT('Ctrl Pts',(-121.439392153342,3.0146181885189,136.68195476905));
#193226=CARTESIAN_POINT('Ctrl Pts',(-121.717839777155,6.57446118879764,
131.445060164237));
#193227=CARTESIAN_POINT('Ctrl Pts',(-121.996287400968,4.0926955368563,125.619393975946));
#193228=CARTESIAN_POINT('Ctrl Pts',(-122.274735024781,-2.15005737416446,
124.5584588316));
#193229=CARTESIAN_POINT('Ctrl Pts',(-122.553182648593,-6.41701259446945,
129.237202299292));
#193230=CARTESIAN_POINT('Ctrl Pts',(-122.831630272406,-4.7870467289504,
135.356087701536));
#193231=CARTESIAN_POINT('Ctrl Pts',(-123.110077896219,1.24198122024032,
137.292158277842));
#193232=CARTESIAN_POINT('Ctrl Pts',(-123.388525520032,6.1296891021858,133.266259750888));
#193233=CARTESIAN_POINT('Ctrl Pts',(-123.666973143845,5.38451215118288,
126.97799619087));
#193234=CARTESIAN_POINT('Ctrl Pts',(-123.945420767658,-0.30876841871475,
124.20597461069));
#193235=CARTESIAN_POINT('Ctrl Pts',(-124.223868391471,-5.71830589598935,
127.497547421752));
#193236=CARTESIAN_POINT('Ctrl Pts',(-124.502316015284,-5.87299960962311,
133.827920012961));
#193237=CARTESIAN_POINT('Ctrl Pts',(-124.780763639097,-0.630693593994696,
137.379789228888));
#193238=CARTESIAN_POINT('Ctrl Pts',(-125.059211262909,5.19118902341993,
134.889160778557));
#193239=CARTESIAN_POINT('Ctrl Pts',(-125.337658886723,6.24262253199412,
128.644800533857));
#193240=CARTESIAN_POINT('Ctrl Pts',(-125.616106510535,1.55739090273089,
124.384970505708));
#193241=CARTESIAN_POINT('Ctrl Pts',(-125.894554134348,-4.55900688336737,
126.024246385717));
#193242=CARTESIAN_POINT('Ctrl Pts',(-126.173001758161,-6.48590006351826,
132.056213723232));
#193243=CARTESIAN_POINT('Ctrl Pts',(-126.451449381974,-2.45256793912933,
136.937789213063));
#193244=CARTESIAN_POINT('Ctrl Pts',(-126.729897005787,3.83455430671493,
136.183043458277));
#193245=CARTESIAN_POINT('Ctrl Pts',(-127.0083446296,6.5979084730801,130.485550936142));
#193246=CARTESIAN_POINT('Ctrl Pts',(-127.286792253413,3.29810707843306,
125.081028936517));
#193247=CARTESIAN_POINT('Ctrl Pts',(-127.565239877225,-3.03249359980603,
124.935969151478));
#193248=CARTESIAN_POINT('Ctrl Pts',(-127.843687501038,-6.57638080537151,
130.183674436914));
#193249=CARTESIAN_POINT('Ctrl Pts',(-128.122135124851,-4.07689532486387,
136.001760000162));
#193250=CARTESIAN_POINT('Ctrl Pts',(-128.400582748664,2.1690577917847,137.043689437881));
#193251=CARTESIAN_POINT('Ctrl Pts',(-128.679030372477,6.42175276214748,
132.351980497887));
#193252=CARTESIAN_POINT('Ctrl Pts',(-128.95747799629,4.77317066415926,126.238084493312));
#193253=CARTESIAN_POINT('Ctrl Pts',(-129.235925620103,-1.26172209184052,
124.320373171937));
#193254=CARTESIAN_POINT('Ctrl Pts',(-129.514373243916,-6.13715388399014,
128.361129552696));
#193255=CARTESIAN_POINT('Ctrl Pts',(-129.792820867728,-5.37284107338758,
134.647095923599));
#193256=CARTESIAN_POINT('Ctrl Pts',(-130.071268491542,0.328850205779251,
137.401776276312));
#193257=CARTESIAN_POINT('Ctrl Pts',(-130.349716115354,5.72834421106097,
134.093753940311));
#193258=CARTESIAN_POINT('Ctrl Pts',(-130.628163739167,5.86376973154965,
127.762939836503));
#193259=CARTESIAN_POINT('Ctrl Pts',(-130.90661136298,0.610677329821333,
124.227042848828));
#193260=CARTESIAN_POINT('Ctrl Pts',(-131.185058986793,-5.20359770476699,
126.735379570785));
#193261=CARTESIAN_POINT('Ctrl Pts',(-131.463506610606,-6.23602065855449,
132.982911093959));
#193262=CARTESIAN_POINT('Ctrl Pts',(-131.741954234419,-1.53784527367628,
137.228461157434));
#193263=CARTESIAN_POINT('Ctrl Pts',(-132.020401858232,4.57353478979242,
135.57057665953));
#193264=CARTESIAN_POINT('Ctrl Pts',(-132.298849482045,6.48205981103755,
129.532772461657));
#193265=CARTESIAN_POINT('Ctrl Pts',(-132.577297105858,2.43388853216508,
124.66349565853));
#193266=CARTESIAN_POINT('Ctrl Pts',(-132.85574472967,-3.85090740570176,
125.437373754826));
#193267=CARTESIAN_POINT('Ctrl Pts',(-133.134192353483,-6.59690756501448,
131.143250586095));
#193268=CARTESIAN_POINT('Ctrl Pts',(-133.412639977296,-3.28067194892964,
136.53770409198));
#193269=CARTESIAN_POINT('Ctrl Pts',(-133.691087601109,3.0503409184865,136.663495034279));
#193270=CARTESIAN_POINT('Ctrl Pts',(-133.969535224922,6.5782394992522,131.405027682246));
#193271=CARTESIAN_POINT('Ctrl Pts',(-134.247982848735,4.06105734507014,
125.59457664199));
#193272=CARTESIAN_POINT('Ctrl Pts',(-134.526430472548,-2.18803811555026,
124.57166256319));
#193273=CARTESIAN_POINT('Ctrl Pts',(-134.804878096361,-6.42643343958478,
129.276293512134));
#193274=CARTESIAN_POINT('Ctrl Pts',(-135.083325720174,-4.75925038136761,
135.385143480741));
#193275=CARTESIAN_POINT('Ctrl Pts',(-135.361773343986,1.28145127501926,
137.284477781773));
#193276=CARTESIAN_POINT('Ctrl Pts',(-135.640220967799,6.14456181203885,
133.228900980221));
#193277=CARTESIAN_POINT('Ctrl Pts',(-135.918668591612,5.36112022232688,
126.945290030769));
#193278=CARTESIAN_POINT('Ctrl Pts',(-136.197116215425,-0.348928946420584,
124.207976424505));
#193279=CARTESIAN_POINT('Ctrl Pts',(-136.475563839238,-5.73832945953392,
127.53241764038));
#193280=CARTESIAN_POINT('Ctrl Pts',(-136.754011463051,-5.85448553231475,
133.863614608987));
#193281=CARTESIAN_POINT('Ctrl Pts',(-137.032459086864,-0.590655408416443,
137.383506612345));
#193282=CARTESIAN_POINT('Ctrl Pts',(-137.310906710677,5.21595818069537,
134.857484855651));
#193283=CARTESIAN_POINT('Ctrl Pts',(-137.58935433449,6.22936101547165,128.606839930282));
#193284=CARTESIAN_POINT('Ctrl Pts',(-137.867801958302,1.51828539823306,
124.375609161675));
#193285=CARTESIAN_POINT('Ctrl Pts',(-138.146249582115,-4.58802032761614,
126.052086919061));
#193286=CARTESIAN_POINT('Ctrl Pts',(-138.424697205928,-6.47815950964009,
132.095672043897));
#193287=CARTESIAN_POINT('Ctrl Pts',(-138.703144829741,-2.41518657799051,
136.952605052004));
#193288=CARTESIAN_POINT('Ctrl Pts',(-138.981592453554,3.86722483040823,
136.159601783301));
#193289=CARTESIAN_POINT('Ctrl Pts',(-139.260040077367,6.59584554409815,
130.445393501362));
#193290=CARTESIAN_POINT('Ctrl Pts',(-139.53848770118,3.26320642772972,125.061058462695));
#193291=CARTESIAN_POINT('Ctrl Pts',(-139.816935324993,-3.06815997922566,
124.954537528447));
#193292=CARTESIAN_POINT('Ctrl Pts',(-140.095382948806,-6.58003725322031,
130.223718233352));
#193293=CARTESIAN_POINT('Ctrl Pts',(-140.373830572619,-4.04518174419624,
136.026480923393));
#193294=CARTESIAN_POINT('Ctrl Pts',(-140.652278196431,2.20699816962987,
137.030370167137));
#193295=CARTESIAN_POINT('Ctrl Pts',(-140.930725820244,6.43105458342049,
132.312860792301));
#193296=CARTESIAN_POINT('Ctrl Pts',(-141.209173444057,4.74528600953044,
126.209113451214));
#193297=CARTESIAN_POINT('Ctrl Pts',(-141.48762106787,-1.30116858700904,
124.328173765698));
#193298=CARTESIAN_POINT('Ctrl Pts',(-141.766068691683,-6.15191281770628,
128.398533417733));
#193299=CARTESIAN_POINT('Ctrl Pts',(-142.044516315496,-5.34934970658085,
134.679730735221));
#193300=CARTESIAN_POINT('Ctrl Pts',(-142.322963939309,0.369004454631186,
137.399652236939));
#193301=CARTESIAN_POINT('Ctrl Pts',(-142.601411563122,5.74826154890666,
134.058822938361));
#193302=CARTESIAN_POINT('Ctrl Pts',(-142.879859186934,5.84514709792562,
127.727301756295));
#193303=CARTESIAN_POINT('Ctrl Pts',(-143.158306810748,0.570628015260733,
124.223447345055));
#193304=CARTESIAN_POINT('Ctrl Pts',(-143.43675443456,-5.22827033670001,
126.767130735766));
#193305=CARTESIAN_POINT('Ctrl Pts',(-143.715202058373,-6.22264366443886,
133.020831158207));
#193306=CARTESIAN_POINT('Ctrl Pts',(-143.993649682186,-1.49871145760156,
137.237703434405));
#193307=CARTESIAN_POINT('Ctrl Pts',(-144.272097305999,4.60246336264661,
135.542647948195));
#193308=CARTESIAN_POINT('Ctrl Pts',(-144.550544929812,6.47419919545755,
129.493337883343));
#193309=CARTESIAN_POINT('Ctrl Pts',(-144.828992553625,2.39646224985712,
124.648793664219));
#193310=CARTESIAN_POINT('Ctrl Pts',(-145.107440177438,-3.8835064296727,
125.460914759058));
#193311=CARTESIAN_POINT('Ctrl Pts',(-145.38588780125,-6.59472242016944,
131.183401556022));
#193312=CARTESIAN_POINT('Ctrl Pts',(-145.664335425064,-3.24571067663155,
136.557568247724));
#193313=CARTESIAN_POINT('Ctrl Pts',(-145.942783048876,3.08595061694992,
136.644818187128));
#193314=CARTESIAN_POINT('Ctrl Pts',(-146.221230672689,6.58177405062243,
131.364972942318));
#193315=CARTESIAN_POINT('Ctrl Pts',(-146.499678296502,4.02926866931097,
125.569952358496));
#193316=CARTESIAN_POINT('Ctrl Pts',(-146.778125920315,-2.22593777837984,
124.585097249699));
#193317=CARTESIAN_POINT('Ctrl Pts',(-147.056573544128,-6.43561615084533,
129.315441348065));
#193318=CARTESIAN_POINT('Ctrl Pts',(-147.335021167941,-4.73127767801157,
135.414029517352));
#193319=CARTESIAN_POINT('Ctrl Pts',(-147.613468791753,1.32087384515067,
137.276557162581));
#193320=CARTESIAN_POINT('Ctrl Pts',(-147.891916415567,6.15920683289404,
133.191452367319));
#193321=CARTESIAN_POINT('Ctrl Pts',(-148.170364039379,5.33752963518947,
126.91272686995));
#193322=CARTESIAN_POINT('Ctrl Pts',(-148.448811663193,-0.389076544435395,
124.210222669761));
#193323=CARTESIAN_POINT('Ctrl Pts',(-148.727259287005,-5.75814038716998,
127.567409102056));
#193324=CARTESIAN_POINT('Ctrl Pts',(-149.005706910818,-5.83575451489182,
133.899195843233));
#193325=CARTESIAN_POINT('Ctrl Pts',(-149.284154534631,-0.550595335885521,
137.386980203127));
#193326=CARTESIAN_POINT('Ctrl Pts',(-149.562602158444,5.24053405872261,
134.825658742734));
#193327=CARTESIAN_POINT('Ctrl Pts',(-149.841049782257,6.21586866768539,
128.568960756646));
#193328=CARTESIAN_POINT('Ctrl Pts',(-150.119497406069,1.47912363311174,
124.366486037389));
#193329=CARTESIAN_POINT('Ctrl Pts',(-150.397945029883,-4.61686376108527,
126.080103549656));
#193330=CARTESIAN_POINT('Ctrl Pts',(-150.676392653695,-6.4701789051783,
132.135082514543));
#193331=CARTESIAN_POINT('Ctrl Pts',(-150.954840277509,-2.37771572122463,
136.967193065487));
#193332=CARTESIAN_POINT('Ctrl Pts',(-151.233287901321,3.89975205266408,
136.135961667893));
#193333=CARTESIAN_POINT('Ctrl Pts',(-151.511735525134,6.59353820363339,
130.405249368239));
#193334=CARTESIAN_POINT('Ctrl Pts',(-151.790183148947,3.22818485771248,
125.041300809049));
#193335=CARTESIAN_POINT('Ctrl Pts',(-152.06863077276,-3.10371266684865,
124.97332267276));
#193336=CARTESIAN_POINT('Ctrl Pts',(-152.347078396573,-6.58344987536885,
130.263783545709));
#193337=CARTESIAN_POINT('Ctrl Pts',(-152.625526020386,-4.01331826783166,
136.051008339035));
#193338=CARTESIAN_POINT('Ctrl Pts',(-152.903973644199,2.24485676634579,
137.016820189321));
#193339=CARTESIAN_POINT('Ctrl Pts',(-153.182421268012,6.44011809960154,
132.273685188686));
#193340=CARTESIAN_POINT('Ctrl Pts',(-153.460868891824,4.71722551658265,
126.180312687687));
#193341=CARTESIAN_POINT('Ctrl Pts',(-153.739316515637,-1.34056686689732,
124.336214336947));
#193342=CARTESIAN_POINT('Ctrl Pts',(-154.01776413945,-6.16644379003131,
128.436026431582));
#193343=CARTESIAN_POINT('Ctrl Pts',(-154.296211763263,-5.32566011765276,
134.712221943579));
#193344=CARTESIAN_POINT('Ctrl Pts',(-154.574659387076,0.409145029887599,
137.397283806609));
#193345=CARTESIAN_POINT('Ctrl Pts',(-154.853107010889,5.7679658828075,134.023771341112));
#193346=CARTESIAN_POINT('Ctrl Pts',(-155.131554634702,5.82630787022557,
127.691777697632));
#193347=CARTESIAN_POINT('Ctrl Pts',(-155.410002258515,0.530557555869813,
124.220095699443));
#193348=CARTESIAN_POINT('Ctrl Pts',(-155.688449882327,-5.25274923315307,
126.799031501784));
#193349=CARTESIAN_POINT('Ctrl Pts',(-155.96689750614,-6.20903608797397,
133.058669090323));
#193350=CARTESIAN_POINT('Ctrl Pts',(-156.245345129953,-1.4595221062231,
137.246707321489));
#193351=CARTESIAN_POINT('Ctrl Pts',(-156.523792753766,4.63122138952822,
135.514543657883));
#193352=CARTESIAN_POINT('Ctrl Pts',(-156.802240377579,6.46609867604585,
129.453951885458));
#193353=CARTESIAN_POINT('Ctrl Pts',(-157.080688001392,2.35894716575843,
124.634319766706));
#193354=CARTESIAN_POINT('Ctrl Pts',(-157.359135625205,-3.9159615488849,
125.484653766641));
#193355=CARTESIAN_POINT('Ctrl Pts',(-157.637583249018,-6.59229290546042,
131.223538480449));
#193356=CARTESIAN_POINT('Ctrl Pts',(-157.916030872831,-3.21062913332988,
136.577219216243));
#193357=CARTESIAN_POINT('Ctrl Pts',(-158.194478496644,3.12144596437753,
136.625924919674));
#193358=CARTESIAN_POINT('Ctrl Pts',(-158.472926120456,6.58506471193526,
131.324897428694));
#193359=CARTESIAN_POINT('Ctrl Pts',(-158.751373744269,3.99733068751967,
125.545522037924));
#193360=CARTESIAN_POINT('Ctrl Pts',(-159.029821368082,-2.26375495826568,
124.598762393297));
#193361=CARTESIAN_POINT('Ctrl Pts',(-159.308268991895,-6.44456038798308,
129.354644356446));
#193362=CARTESIAN_POINT('Ctrl Pts',(-159.586716615708,-4.7031296554214,
135.442744740987));
#193363=CARTESIAN_POINT('Ctrl Pts',(-159.865164239521,1.36024746981527,
137.268396713766));
#193364=CARTESIAN_POINT('Ctrl Pts',(-160.143611863334,6.17362362207528,
133.153915299856));
#193365=CARTESIAN_POINT('Ctrl Pts',(-160.422059487147,5.31374126392856,
126.880307915048));
#193366=CARTESIAN_POINT('Ctrl Pts',(-160.70050711096,-0.429209725076344,
124.212713263223));
#193367=CARTESIAN_POINT('Ctrl Pts',(-160.978954734773,-5.77773794479658,
127.602520510164));
#193368=CARTESIAN_POINT('Ctrl Pts',(-161.257402358585,-5.81680725143943,
133.934662397221));
#193369=CARTESIAN_POINT('Ctrl Pts',(-161.535849982398,-0.51051486084124,
137.390209872519));
#193370=CARTESIAN_POINT('Ctrl Pts',(-161.814297606211,5.26491574683228,
134.793683619137));
#193371=CARTESIAN_POINT('Ctrl Pts',(-162.092745230024,6.20214598860049,
128.531164416574));
#193372=CARTESIAN_POINT('Ctrl Pts',(-162.371192853837,1.43990705852047,
124.357601470914));
#193373=CARTESIAN_POINT('Ctrl Pts',(-162.64964047765,-4.64553611496906,
126.108295239334));
#193374=CARTESIAN_POINT('Ctrl Pts',(-162.928088101462,-6.46195854585841,
132.1744436748));
#193375=CARTESIAN_POINT('Ctrl Pts',(-163.206535725276,-2.34015675732853,
136.981552712947));
#193376=CARTESIAN_POINT('Ctrl Pts',(-163.484983349088,3.93213476817268,
136.112123988049));
#193377=CARTESIAN_POINT('Ctrl Pts',(-163.763430972902,6.5909865371863,130.365120024332));
#193378=CARTESIAN_POINT('Ctrl Pts',(-164.041878596714,3.19304366611785,
125.021756707701));
#193379=CARTESIAN_POINT('Ctrl Pts',(-164.320326220527,-3.13915034525769,
124.99232388833));
#193380=CARTESIAN_POINT('Ctrl Pts',(-164.59877384434,-6.58661854536123,
130.303868889347));
#193381=CARTESIAN_POINT('Ctrl Pts',(-164.877221468153,-3.98130607648258,
136.075341338217));
#193382=CARTESIAN_POINT('Ctrl Pts',(-165.155669091966,2.28263217906914,
137.003040006531));
#193383=CARTESIAN_POINT('Ctrl Pts',(-165.434116715779,6.44894297483741,
132.23445513871));
#193384=CARTESIAN_POINT('Ctrl Pts',(-165.712564339591,4.6889902251094,126.151683269957));
#193385=CARTESIAN_POINT('Ctrl Pts',(-165.991011963405,-1.37991547158711,
124.344494587733));
#193386=CARTESIAN_POINT('Ctrl Pts',(-166.269459587217,-6.18074626251326,
128.473607204924));
#193387=CARTESIAN_POINT('Ctrl Pts',(-166.54790721103,-5.3017731844313,134.744568344699));
#193388=CARTESIAN_POINT('Ctrl Pts',(-166.826354834843,0.449270444124704,
137.394671073086));
#193389=CARTESIAN_POINT('Ctrl Pts',(-167.104802458656,5.78745648261092,
133.988600447415));
#193390=CARTESIAN_POINT('Ctrl Pts',(-167.383250082469,5.8072527465451,127.656368976875));
#193391=CARTESIAN_POINT('Ctrl Pts',(-167.661697706282,0.490467436472931,
124.216988036188));
#193392=CARTESIAN_POINT('Ctrl Pts',(-167.940145330095,-5.27703348705155,
126.831080686747));
#193393=CARTESIAN_POINT('Ctrl Pts',(-168.218592953908,-6.19519843339338,
133.096423488211));
#193394=CARTESIAN_POINT('Ctrl Pts',(-168.49704057772,-1.42027867171577,
137.255472485049));
#193395=CARTESIAN_POINT('Ctrl Pts',(-168.775488201534,4.65980780479824,
135.486264830004));
#193396=CARTESIAN_POINT('Ctrl Pts',(-169.053935825346,6.45775855296945,
129.414615927465));
#193397=CARTESIAN_POINT('Ctrl Pts',(-169.332383449159,2.32134467000579,
124.620074502325));
#193398=CARTESIAN_POINT('Ctrl Pts',(-169.610831072972,-3.94827156070164,
125.508589897919));
#193399=CARTESIAN_POINT('Ctrl Pts',(-169.889278696785,-6.58961911091297,
131.263659872085));
#193400=CARTESIAN_POINT('Ctrl Pts',(-170.167726320598,-3.17542861898582,
136.596656269364));
#193401=CARTESIAN_POINT('Ctrl Pts',(-170.446173944411,3.15682564547787,
136.606815932013));
#193402=CARTESIAN_POINT('Ctrl Pts',(-170.724621568223,6.58811136125304,
131.284802626386));
#193403=CARTESIAN_POINT('Ctrl Pts',(-171.003069192037,3.96524458316956,
125.521286585549));
#193404=CARTESIAN_POINT('Ctrl Pts',(-171.28151681585,-2.30148825387982,
124.612657487621));
#193405=CARTESIAN_POINT('Ctrl Pts',(-171.559964439662,-6.45326581956532,
129.393901084596));
#193406=CARTESIAN_POINT('Ctrl Pts',(-171.838412063475,-4.67480735663214,
135.471288087592));
#193407=CARTESIAN_POINT('Ctrl Pts',(-172.116859687288,1.39957069001038,
137.259996737715));
#193408=CARTESIAN_POINT('Ctrl Pts',(-172.395307311101,6.18781164536257,
133.116291168777));
#193409=CARTESIAN_POINT('Ctrl Pts',(-172.673754934914,5.289755990031,126.848034367363));
#193410=CARTESIAN_POINT('Ctrl Pts',(-172.952202558727,-0.469327001192524,
124.215448112602));
#193411=CARTESIAN_POINT('Ctrl Pts',(-173.23065018254,-5.79712140621875,
127.637750563632));
#193412=CARTESIAN_POINT('Ctrl Pts',(-173.509097806352,-5.79764444405506,
133.970012956726));
#193413=CARTESIAN_POINT('Ctrl Pts',(-173.787545430165,-0.470415468481743,
137.393195500846));
#193414=CARTESIAN_POINT('Ctrl Pts',(-174.065993053978,5.28910234155359,
134.76156066971));
#193415=CARTESIAN_POINT('Ctrl Pts',(-174.344440677791,6.18819348671444,
128.493452310623));
#193416=CARTESIAN_POINT('Ctrl Pts',(-174.622888301604,1.40063712764339,
124.34895579147));
#193417=CARTESIAN_POINT('Ctrl Pts',(-174.901335925417,-4.67403632680454,
126.13666094344));
#193418=CARTESIAN_POINT('Ctrl Pts',(-175.17978354923,-6.45349873628761,
132.213754066126));
#193419=CARTESIAN_POINT('Ctrl Pts',(-175.458231173043,-2.30251107806296,
136.995683462282));
#193420=CARTESIAN_POINT('Ctrl Pts',(-175.736678796856,3.96437177698222,
136.088089627079));
#193421=CARTESIAN_POINT('Ctrl Pts',(-176.015126420669,6.58819063930867,
130.325006956645));
#193422=CARTESIAN_POINT('Ctrl Pts',(-176.293574044481,3.15778415511627,
125.002426882869));
#193423=CARTESIAN_POINT('Ctrl Pts',(-176.572021668294,-3.17447170129595,
125.011540471058));
#193424=CARTESIAN_POINT('Ctrl Pts',(-176.850469292107,-6.58954314578118,
130.343972778891));
#193425=CARTESIAN_POINT('Ctrl Pts',(-177.12891691592,-3.94914635637289,
136.099479019269));
#193426=CARTESIAN_POINT('Ctrl Pts',(-177.407364539733,2.32032300801719,
136.989030129397));
#193427=CARTESIAN_POINT('Ctrl Pts',(-177.685812163546,6.45752888212044,
132.195172096054));
#193428=CARTESIAN_POINT('Ctrl Pts',(-177.964259787359,4.66058118137817,
126.123226258898));
#193429=CARTESIAN_POINT('Ctrl Pts',(-178.242707411172,-1.41921294300185,
124.353014211231));
#193430=CARTESIAN_POINT('Ctrl Pts',(-178.521155034985,-6.19481970517025,
128.511274345191));
#193431=CARTESIAN_POINT('Ctrl Pts',(-178.799602658797,-5.27768979205393,
134.776768739972));
#193432=CARTESIAN_POINT('Ctrl Pts',(-179.078050282611,0.489379210479558,
137.391814133187));
#193433=CARTESIAN_POINT('Ctrl Pts',(-179.356497906423,5.80673262608622,
133.95331156054));
#193434=CARTESIAN_POINT('Ctrl Pts',(-179.634945530236,5.7879824329786,127.621076906106));
#193435=CARTESIAN_POINT('Ctrl Pts',(-179.913393154049,0.450359142625426,
124.214124470449));
#193436=CARTESIAN_POINT('Ctrl Pts',(-180.191840777862,-5.30112219853358,
126.863277103057));
#193437=CARTESIAN_POINT('Ctrl Pts',(-180.470288401675,-6.18113121345664,
133.134092952866));
#193438=CARTESIAN_POINT('Ctrl Pts',(-180.748736025488,-1.38098260826046,
137.263998600285));
#193439=CARTESIAN_POINT('Ctrl Pts',(-181.0271836493,4.68822154917632,135.457812512445));
#193440=CARTESIAN_POINT('Ctrl Pts',(-181.305631273113,6.44917913527537,
129.375331466973));
#193441=CARTESIAN_POINT('Ctrl Pts',(-181.584078896926,2.28365615597197,
124.606058398942));
#193442=CARTESIAN_POINT('Ctrl Pts',(-181.862526520739,-3.98043526786393,
125.532722265928));
#193443=CARTESIAN_POINT('Ctrl Pts',(-182.140974144552,-6.58670113560653,
131.303764244219));
#193444=CARTESIAN_POINT('Ctrl Pts',(-182.419421768365,-3.14011043796568,
136.615878686839));
#193445=CARTESIAN_POINT('Ctrl Pts',(-182.697869392178,3.19208834924215,
136.587491932238));
#193446=CARTESIAN_POINT('Ctrl Pts',(-182.976317015991,6.59091388568205,
131.244690021124));
#193447=CARTESIAN_POINT('Ctrl Pts',(-183.254764639804,3.93301154522339,
125.497246899427));
#193448=CARTESIAN_POINT('Ctrl Pts',(-183.533212263617,-2.33913626699958,
124.626782017781));
#193449=CARTESIAN_POINT('Ctrl Pts',(-183.811659887429,-6.46173212300977,
129.433210077844));
#193450=CARTESIAN_POINT('Ctrl Pts',(-184.090107511242,-4.64631183113728,
135.499658499484));
#193451=CARTESIAN_POINT('Ctrl Pts',(-184.368555135055,1.43884204859816,
137.251357545694));
#193452=CARTESIAN_POINT('Ctrl Pts',(-184.647002758868,6.20177037701405,
133.078581368264));
#193453=CARTESIAN_POINT('Ctrl Pts',(-184.925450382681,5.26557470227994,
126.815907422802));
#193454=CARTESIAN_POINT('Ctrl Pts',(-185.203898006494,-0.50942688622466,
124.218427116558));
#193455=CARTESIAN_POINT('Ctrl Pts',(-185.482345630307,-5.81629005317544,
127.673097957001));
#193456=CARTESIAN_POINT('Ctrl Pts',(-185.76079325412,-5.77826680282389,
134.005246211819));
#193457=CARTESIAN_POINT('Ctrl Pts',(-186.039240877932,-0.430298644703365,
137.395936977472));
#193458=CARTESIAN_POINT('Ctrl Pts',(-186.317688501746,5.31309294664177,
134.729291084778));
#193459=CARTESIAN_POINT('Ctrl Pts',(-186.596136125558,6.17401167904375,
128.455825836229));
#193460=CARTESIAN_POINT('Ctrl Pts',(-186.874583749371,1.36131529564269,
124.340549319425));
#193461=CARTESIAN_POINT('Ctrl Pts',(-187.153031373184,-4.70236334050424,
126.165199610876));
#193462=CARTESIAN_POINT('Ctrl Pts',(-187.431478996997,-6.44479978994851,
132.253012231859));
#193463=CARTESIAN_POINT('Ctrl Pts',(-187.70992662081,-2.26478007840253,
137.009584789872));
#193464=CARTESIAN_POINT('Ctrl Pts',(-187.988374244623,3.99646188453734,
136.063859475589));
#193465=CARTESIAN_POINT('Ctrl Pts',(-188.266821868436,6.58515061360439,
130.284911651585));
#193466=CARTESIAN_POINT('Ctrl Pts',(-188.545269492249,3.12240763126122,
124.983312050825));
#193467=CARTESIAN_POINT('Ctrl Pts',(-188.823717116061,-3.20967542611822,
125.030971708867));
#193468=CARTESIAN_POINT('Ctrl Pts',(-189.102164739874,-6.59222356825658,
130.384093728275));
#193469=CARTESIAN_POINT('Ctrl Pts',(-189.380612363687,-3.91684029919248,
136.123420487763));
#193470=CARTESIAN_POINT('Ctrl Pts',(-189.6590599875,2.35792785654334,136.974791077059));
#193471=CARTESIAN_POINT('Ctrl Pts',(-189.937507611313,6.46587550329532,
132.155837516369));
#193472=CARTESIAN_POINT('Ctrl Pts',(-190.215955235126,4.63199943809816,
126.094942708994));
#193473=CARTESIAN_POINT('Ctrl Pts',(-190.494402858939,-1.45845782495887,
124.361772891742));
#193474=CARTESIAN_POINT('Ctrl Pts',(-190.772850482752,-6.2086635965042,
128.549026456613));
#193475=CARTESIAN_POINT('Ctrl Pts',(-191.051298106565,-5.25341083294129,
134.808821936201));
#193476=CARTESIAN_POINT('Ctrl Pts',(-191.329745730377,0.529469842708527,
137.388713092773));
#193477=CARTESIAN_POINT('Ctrl Pts',(-191.60819335419,5.82579359894846,133.91790598813));
#193478=CARTESIAN_POINT('Ctrl Pts',(-191.886640978003,5.76849764359442,
127.585902793086));
#193479=CARTESIAN_POINT('Ctrl Pts',(-192.165088601816,0.410234160553658,
124.211505108333));
#193480=CARTESIAN_POINT('Ctrl Pts',(-192.443536225629,-5.32501447498302,
126.895619557667));
#193481=CARTESIAN_POINT('Ctrl Pts',(-192.721983849442,-6.16683494942961,
133.171676088433));
#193482=CARTESIAN_POINT('Ctrl Pts',(-193.000431473255,-1.34163537198624,
137.272285351261));
#193483=CARTESIAN_POINT('Ctrl Pts',(-193.278879097068,4.71646156978089,
135.429187759513));
#193484=CARTESIAN_POINT('Ctrl Pts',(-193.557326720881,6.44036074087642,
129.336099959682));
#193485=CARTESIAN_POINT('Ctrl Pts',(-193.835774344694,2.24588302022023,
124.592271975924));
#193486=CARTESIAN_POINT('Ctrl Pts',(-194.114221968506,-4.01245147853337,
125.557049976435));
#193487=CARTESIAN_POINT('Ctrl Pts',(-194.392669592319,-6.58353908766677,
131.343850110767));
#193488=CARTESIAN_POINT('Ctrl Pts',(-194.671117216133,-3.10467589899933,
136.634885756375));
#193489=CARTESIAN_POINT('Ctrl Pts',(-194.949564839945,3.22723276899961,
136.567953636405));
#193490=CARTESIAN_POINT('Ctrl Pts',(-195.228012463758,6.59347218137276,
131.204561099293));
#193491=CARTESIAN_POINT('Ctrl Pts',(-195.506460087571,3.90063276808784,
125.473403870355));
#193492=CARTESIAN_POINT('Ctrl Pts',(-195.784907711384,-2.3766976025655,
124.641135460387));
#193493=CARTESIAN_POINT('Ctrl Pts',(-196.063355335197,-6.46995898459376,
129.472569879579));
#193494=CARTESIAN_POINT('Ctrl Pts',(-196.34180295901,-4.61764413484867,
135.527854925386));
#193495=CARTESIAN_POINT('Ctrl Pts',(-196.620250582823,1.47806009036541,
137.242479457832));
#193496=CARTESIAN_POINT('Ctrl Pts',(-196.898698206635,6.21549929978325,
133.040787295662));
#193497=CARTESIAN_POINT('Ctrl Pts',(-197.177145830448,5.24119829672186,
126.783928271841));
#193498=CARTESIAN_POINT('Ctrl Pts',(-197.455593454261,-0.5495078942556,
124.2216501647));
#193499=CARTESIAN_POINT('Ctrl Pts',(-197.734041078074,-5.83524317536515,
127.708561380459));
#193500=CARTESIAN_POINT('Ctrl Pts',(-198.012488701887,-5.75867504579123,
134.040360856918));
#193501=CARTESIAN_POINT('Ctrl Pts',(-198.2909363257,-0.390165876051177,
137.398434200813));
#193502=CARTESIAN_POINT('Ctrl Pts',(-198.569383949513,5.33688667311775,
134.696876060105));
#193503=CARTESIAN_POINT('Ctrl Pts',(-198.847831573325,6.15960109109908,
128.418286387655));
#193504=CARTESIAN_POINT('Ctrl Pts',(-199.126279197139,1.32194301960288,
124.332382366286));
#193505=CARTESIAN_POINT('Ctrl Pts',(-199.404726820951,-4.73051610640191,
126.193910184127));
#193506=CARTESIAN_POINT('Ctrl Pts',(-199.683174444764,-6.43586202918244,
132.292216717274));
#193507=CARTESIAN_POINT('Ctrl Pts',(-199.961622068577,-2.22696515648391,
137.023256180599));
#193508=CARTESIAN_POINT('Ctrl Pts',(-200.24006969239,4.02840390172748,136.039434431435));
#193509=CARTESIAN_POINT('Ctrl Pts',(-200.518517316203,6.58186657272242,
130.244835594899));
#193510=CARTESIAN_POINT('Ctrl Pts',(-200.796964940016,3.08691540544346,
124.964412919876));
#193511=CARTESIAN_POINT('Ctrl Pts',(-201.075412563829,-3.24476021523692,
125.050616881724));
#193512=CARTESIAN_POINT('Ctrl Pts',(-201.353860187642,-6.59465971346335,
130.424230250803));
#193513=CARTESIAN_POINT('Ctrl Pts',(-201.632307811455,-3.88438910205457,
136.147164856536));
#193514=CARTESIAN_POINT('Ctrl Pts',(-201.910755435267,2.39544533118521,
136.960323377152));
#193515=CARTESIAN_POINT('Ctrl Pts',(-202.18920305908,6.47398252907625,132.116452857208));
#193516=CARTESIAN_POINT('Ctrl Pts',(-202.467650682893,4.60324605437475,
126.066833668302));
#193517=CARTESIAN_POINT('Ctrl Pts',(-202.746098306706,-1.49764866322506,
124.370770304711));
#193518=CARTESIAN_POINT('Ctrl Pts',(-203.024545930519,-6.22227742352606,
128.586862140274));
#193519=CARTESIAN_POINT('Ctrl Pts',(-203.302993554332,-5.22893720675747,
134.840726745644));
#193520=CARTESIAN_POINT('Ctrl Pts',(-203.581441178145,0.569540855237039,
137.385368066758));
#193521=CARTESIAN_POINT('Ctrl Pts',(-203.859888801958,5.84463869488665,
133.882385042152));
#193522=CARTESIAN_POINT('Ctrl Pts',(-204.138336425771,5.7487991004088,127.550847941203));
#193523=CARTESIAN_POINT('Ctrl Pts',(-204.416784049583,0.370093977104817,
124.209130046901));
#193524=CARTESIAN_POINT('Ctrl Pts',(-204.695231673396,-5.34870943106288,
126.928106852114));
#193525=CARTESIAN_POINT('Ctrl Pts',(-204.973679297209,-6.15231017106575,
133.209171502253));
#193526=CARTESIAN_POINT('Ctrl Pts',(-205.252126921022,-1.30223842092043,
137.280332430907));
#193527=CARTESIAN_POINT('Ctrl Pts',(-205.530574544835,4.74452682016742,
135.400391631911));
#193528=CARTESIAN_POINT('Ctrl Pts',(-205.809022168648,6.43130369654214,
129.296922859329));
#193529=CARTESIAN_POINT('Ctrl Pts',(-206.087469792461,2.20802666244648,
124.578715744137));
#193530=CARTESIAN_POINT('Ctrl Pts',(-206.365917416273,-4.04431900633787,
125.581572127967));
#193531=CARTESIAN_POINT('Ctrl Pts',(-206.644365040087,-6.58013308426553,
131.383915986335));
#193532=CARTESIAN_POINT('Ctrl Pts',(-206.922812663899,-3.06912631512495,
136.653676773657));
#193533=CARTESIAN_POINT('Ctrl Pts',(-207.201260287713,3.26225760245914,
136.548201768512));
#193534=CARTESIAN_POINT('Ctrl Pts',(-207.479707911525,6.59578615352751,
131.164417347887));
#193535=CARTESIAN_POINT('Ctrl Pts',(-207.758155535338,3.86810945157081,
125.449758381845));
#193536=CARTESIAN_POINT('Ctrl Pts',(-208.036603159151,-2.41417086872696,
124.655717283569));
#193537=CARTESIAN_POINT('Ctrl Pts',(-208.315050782964,-6.47794609946865,
129.511979031309));
#193538=CARTESIAN_POINT('Ctrl Pts',(-208.593498406777,-4.58880533005852,
135.555876320469));
#193539=CARTESIAN_POINT('Ctrl Pts',(-208.87194603059,1.51722336207232,137.233362803106));
#193540=CARTESIAN_POINT('Ctrl Pts',(-209.150393654402,6.22899790494034,
133.00291035145));
#193541=CARTESIAN_POINT('Ctrl Pts',(-209.428841278216,5.21662767663345,
126.752098099478));
#193542=CARTESIAN_POINT('Ctrl Pts',(-209.707288902028,-0.589568540070009,
124.225117137599));
#193543=CARTESIAN_POINT('Ctrl Pts',(-209.985736525842,-5.85398007047323,
127.744139519898));
#193544=CARTESIAN_POINT('Ctrl Pts',(-210.264184149654,-5.73886989893714,
134.07535559084));
#193545=CARTESIAN_POINT('Ctrl Pts',(-210.542631773467,-0.350018649658268,
137.400687078332));
#193546=CARTESIAN_POINT('Ctrl Pts',(-210.82107939728,5.36048263929459,134.664316796842));
#193547=CARTESIAN_POINT('Ctrl Pts',(-211.099527021093,6.14496225687153,
128.38083535594));
#193548=CARTESIAN_POINT('Ctrl Pts',(-211.377974644906,1.28252175847855,
124.324455234681));
#193549=CARTESIAN_POINT('Ctrl Pts',(-211.656422268719,-4.75849358128477,
126.222791599316));
#193550=CARTESIAN_POINT('Ctrl Pts',(-211.934869892531,-6.4266857851828,
132.331366069634));
#193551=CARTESIAN_POINT('Ctrl Pts',(-212.213317516344,-2.18906771355195,
137.036697127864));
#193552=CARTESIAN_POINT('Ctrl Pts',(-212.491765140157,4.06019664492976,
136.014815399695));
#193553=CARTESIAN_POINT('Ctrl Pts',(-212.770212763971,6.57833863835413,
130.204780271616));
#193554=CARTESIAN_POINT('Ctrl Pts',(-213.048660387783,3.05130879283982,
124.945730190337));
#193555=CARTESIAN_POINT('Ctrl Pts',(-213.327108011596,-3.27972476857289,
125.070475261673));
#193556=CARTESIAN_POINT('Ctrl Pts',(-213.605555635409,-6.59685149112928,
130.464380859201));
#193557=CARTESIAN_POINT('Ctrl Pts',(-213.884003259222,-3.85179396744981,
136.170711245733));
#193558=CARTESIAN_POINT('Ctrl Pts',(-214.162450883035,2.43287404171984,
136.94562756578));
#193559=CARTESIAN_POINT('Ctrl Pts',(-214.440898506847,6.48184965905313,
132.077019577989));
#193560=CARTESIAN_POINT('Ctrl Pts',(-214.71934613066,4.57432209567675,126.038900178414));
#193561=CARTESIAN_POINT('Ctrl Pts',(-214.997793754473,-1.53678400556905,
124.380006116735));
#193562=CARTESIAN_POINT('Ctrl Pts',(-215.276241378286,-6.23566068176903,
128.624779994154));
#193563=CARTESIAN_POINT('Ctrl Pts',(-215.554689002099,-5.20426982038336,
134.872481986055));
#193564=CARTESIAN_POINT('Ctrl Pts',(-215.833136625912,0.609590763220439,
137.381779179092));
#193565=CARTESIAN_POINT('Ctrl Pts',(-216.111584249725,5.86326721558844,
133.846750038845));
#193566=CARTESIAN_POINT('Ctrl Pts',(-216.390031873537,5.72888753335829,
127.51591364943));
#193567=CARTESIAN_POINT('Ctrl Pts',(-216.668479497351,0.329940079686948,
124.206999374164));
#193568=CARTESIAN_POINT('Ctrl Pts',(-216.946927121163,-5.37220618874772,
126.960737782571));
#193569=CARTESIAN_POINT('Ctrl Pts',(-217.225374744977,-6.13755741658593,
133.246577804923));
#193570=CARTESIAN_POINT('Ctrl Pts',(-217.503822368789,-1.26279321493052,
137.288139541036));
#193571=CARTESIAN_POINT('Ctrl Pts',(-217.782269992602,4.77241626036792,
135.37142519669));
#193572=CARTESIAN_POINT('Ctrl Pts',(-218.060717616415,6.4220083378839,129.257801617636));
#193573=CARTESIAN_POINT('Ctrl Pts',(-218.339165240228,2.17008848543354,
124.565390205911));
#193574=CARTESIAN_POINT('Ctrl Pts',(-218.617612864041,-4.07603667041411,
125.606287811847));
#193575=CARTESIAN_POINT('Ctrl Pts',(-218.896060487854,-6.57648325161253,
131.423960386264));
#193576=CARTESIAN_POINT('Ctrl Pts',(-219.174508111666,-3.03346300364714,
136.672251042379));
#193577=CARTESIAN_POINT('Ctrl Pts',(-219.45295573548,3.29716155176439,136.528237060474));
#193578=CARTESIAN_POINT('Ctrl Pts',(-219.731403359293,6.59785571640026,
131.124260254445));
#193579=CARTESIAN_POINT('Ctrl Pts',(-220.009850983105,3.83544280083539,
125.426311310091));
#193580=CARTESIAN_POINT('Ctrl Pts',(-220.288298606918,-2.45155467689987,
124.67052694699));
#193581=CARTESIAN_POINT('Ctrl Pts',(-220.566746230731,-6.48569317166813,
129.551436072715));
#193582=CARTESIAN_POINT('Ctrl Pts',(-220.845193854544,-4.55979648539947,
135.58372164639));
#193583=CARTESIAN_POINT('Ctrl Pts',(-221.123641478357,1.55633041250914,
137.224007919343));
#193584=CARTESIAN_POINT('Ctrl Pts',(-221.40208910217,6.24226569228925,132.964951939167));
#193585=CARTESIAN_POINT('Ctrl Pts',(-221.680536725983,5.19186375248807,
126.720418085194));
#193586=CARTESIAN_POINT('Ctrl Pts',(-221.958984349796,-0.629607339204784,
124.228827906785));
#193587=CARTESIAN_POINT('Ctrl Pts',(-222.237431973609,-5.87250004419688,
127.779831056953));
#193588=CARTESIAN_POINT('Ctrl Pts',(-222.515879597421,-5.71885209614835,
134.110229116839));
#193589=CARTESIAN_POINT('Ctrl Pts',(-222.794327221234,-0.309858453196267,
137.402695526548));
#193590=CARTESIAN_POINT('Ctrl Pts',(-223.072774845047,5.38387997081673,
134.631614501482));
#193591=CARTESIAN_POINT('Ctrl Pts',(-223.35122246886,6.13009571880702,128.343474128844));
#193592=CARTESIAN_POINT('Ctrl Pts',(-223.629670092673,1.24305297303857,
124.316768218352));
#193593=CARTESIAN_POINT('Ctrl Pts',(-223.908117716486,-4.78629472843886,
126.25184278623));
#193594=CARTESIAN_POINT('Ctrl Pts',(-224.186565340298,-6.41727139797729,
132.370458838244));
#193595=CARTESIAN_POINT('Ctrl Pts',(-224.465012964112,-2.15108915391133,
137.049907133607));
#193596=CARTESIAN_POINT('Ctrl Pts',(-224.743460587925,4.09183893605206,
135.990003292637));
#193597=CARTESIAN_POINT('Ctrl Pts',(-225.021908211737,6.57456694122844,
130.164747166004));
#193598=CARTESIAN_POINT('Ctrl Pts',(-225.300355835551,3.01558911286705,
124.927264554503));
#193599=CARTESIAN_POINT('Ctrl Pts',(-225.578803459363,-3.31456779050113,
125.090546112851));
#193600=CARTESIAN_POINT('Ctrl Pts',(-225.857251083176,-6.5987988200372,
130.504544065675));
#193601=CARTESIAN_POINT('Ctrl Pts',(-226.135698706989,-3.8190561032033,
136.194058782834));
#193602=CARTESIAN_POINT('Ctrl Pts',(-226.414146330802,2.47021260121173,
136.930704187504));
#193603=CARTESIAN_POINT('Ctrl Pts',(-226.692593954615,6.48947660170784,
132.037539139922));
#193604=CARTESIAN_POINT('Ctrl Pts',(-226.971041578427,4.54522863379049,
126.011143274415));
#193605=CARTESIAN_POINT('Ctrl Pts',(-227.24948920224,-1.57586240181677,
124.389479985577));
#193606=CARTESIAN_POINT('Ctrl Pts',(-227.527936826054,-6.24881287531301,
128.662778613197));
#193607=CARTESIAN_POINT('Ctrl Pts',(-227.806384449866,-5.17940958787633,
134.904086480733));
#193608=CARTESIAN_POINT('Ctrl Pts',(-228.084832073679,0.649618082593193,
137.377946562762));
#193609=CARTESIAN_POINT('Ctrl Pts',(-228.363279697492,5.88167847076755,
133.811002298682));
#193610=CARTESIAN_POINT('Ctrl Pts',(-228.641727321305,5.70876368027354,
127.481101212267));
#193611=CARTESIAN_POINT('Ctrl Pts',(-228.920174945118,0.289773956218704,
124.205113169075));
#193612=CARTESIAN_POINT('Ctrl Pts',(-229.198622568931,-5.39550387735667,
126.993511139885));
#193613=CARTESIAN_POINT('Ctrl Pts',(-229.477070192744,-6.12257723265909,
133.283893610337));
#193614=CARTESIAN_POINT('Ctrl Pts',(-229.755517816557,-1.22330121567356,
137.295706392352));
#193615=CARTESIAN_POINT('Ctrl Pts',(-230.033965440369,4.80012885692891,
135.34228952721));
#193616=CARTESIAN_POINT('Ctrl Pts',(-230.312413064183,6.41247500934538,
129.218737684256));
#193617=CARTESIAN_POINT('Ctrl Pts',(-230.590860687995,2.13206989499296,
124.552295855027));
#193618=CARTESIAN_POINT('Ctrl Pts',(-230.869308311808,-4.10760329545278,
125.631196112227));
#193619=CARTESIAN_POINT('Ctrl Pts',(-231.147755935621,-6.5725897249546,
131.463981826697));
#193620=CARTESIAN_POINT('Ctrl Pts',(-231.426203559434,-2.99768728608136,
136.690607874263));
#193621=CARTESIAN_POINT('Ctrl Pts',(-231.704651183247,3.33194332353496,
136.508060252089));
#193622=CARTESIAN_POINT('Ctrl Pts',(-231.98309880706,6.59968079330357,131.084091307006));
#193623=CARTESIAN_POINT('Ctrl Pts',(-232.261546430872,3.80263402635669,
125.403063523931));
#193624=CARTESIAN_POINT('Ctrl Pts',(-232.539994054686,-2.48884764181187,
124.685563901874));
#193625=CARTESIAN_POINT('Ctrl Pts',(-232.818441678498,-6.49319991412244,
129.5909395417));
#193626=CARTESIAN_POINT('Ctrl Pts',(-233.096889302311,-4.53061867580467,
135.611389871331));
#193627=CARTESIAN_POINT('Ctrl Pts',(-233.375336926124,1.59537979255065,
137.214415153187));
#193628=CARTESIAN_POINT('Ctrl Pts',(-233.653784549937,6.25530217018742,
132.926913465378));
#193629=CARTESIAN_POINT('Ctrl Pts',(-233.93223217375,5.16690744192206,126.688889402902));
#193630=CARTESIAN_POINT('Ctrl Pts',(-234.210679797563,-0.669622808008655,
124.232782334755));
#193631=CARTESIAN_POINT('Ctrl Pts',(-234.489127421376,-5.89080241027189,
127.815634669064));
#193632=CARTESIAN_POINT('Ctrl Pts',(-234.767575045188,-5.69862237919218,
134.144980142666));
#193633=CARTESIAN_POINT('Ctrl Pts',(-235.046022669002,-0.269686774814632,
137.404459471037));
#193634=CARTESIAN_POINT('Ctrl Pts',(-235.324470292814,5.40707780068583,
134.598770385822));
#193635=CARTESIAN_POINT('Ctrl Pts',(-235.602917916627,6.11500202779203,
128.306204090801));
#193636=CARTESIAN_POINT('Ctrl Pts',(-235.88136554044,1.20353812581378,124.309321602146));
#193637=CARTESIAN_POINT('Ctrl Pts',(-236.159813164253,-4.81391851768082,
126.281062668365));
#193638=CARTESIAN_POINT('Ctrl Pts',(-236.438260788066,-6.40761921642086,
132.40949357451));
#193639=CARTESIAN_POINT('Ctrl Pts',(-236.716708411879,-2.11303088487057,
137.062885708328));
#193640=CARTESIAN_POINT('Ctrl Pts',(-236.995156035692,4.12332960257798,
135.964999029683));
#193641=CARTESIAN_POINT('Ctrl Pts',(-237.273603659505,6.57055162110693,
130.124737761504));
#193642=CARTESIAN_POINT('Ctrl Pts',(-237.552051283318,2.97975768913041,
124.909016696624));
#193643=CARTESIAN_POINT('Ctrl Pts',(-237.83049890713,-3.34928798990126,
125.110828691528));
#193644=CARTESIAN_POINT('Ctrl Pts',(-238.108946530943,-6.60050162802816,
130.544718381962));
#193645=CARTESIAN_POINT('Ctrl Pts',(-238.387394154756,-3.7861767224282,
136.217206602688));
#193646=CARTESIAN_POINT('Ctrl Pts',(-238.665841778569,2.5074596260677,136.915553795314));
#193647=CARTESIAN_POINT('Ctrl Pts',(-238.944289402382,6.49686307441993,
131.998013005973));
#193648=CARTESIAN_POINT('Ctrl Pts',(-239.222737026195,4.51596674678651,
125.983563984846));
#193649=CARTESIAN_POINT('Ctrl Pts',(-239.501184650008,-1.61488240390346,
124.399191560181));
#193650=CARTESIAN_POINT('Ctrl Pts',(-239.77963227382,-6.26173351679718,
128.700856589348));
#193651=CARTESIAN_POINT('Ctrl Pts',(-240.058079897633,-5.15435743044315,
134.935539058562));
#193652=CARTESIAN_POINT('Ctrl Pts',(-240.336527521446,0.689621330129741,
137.373870359787));
#193653=CARTESIAN_POINT('Ctrl Pts',(-240.614975145259,5.89987177818775,
133.775143146303));
#193654=CARTESIAN_POINT('Ctrl Pts',(-240.893422769072,5.68842828685113,
127.446411919705));
#193655=CARTESIAN_POINT('Ctrl Pts',(-241.171870392886,0.249597095069331,
124.203471501526));
#193656=CARTESIAN_POINT('Ctrl Pts',(-241.450318016698,-5.41860163358522,
127.026425709627));
#193657=CARTESIAN_POINT('Ctrl Pts',(-241.728765640511,-6.10737017438111,
133.321117535742));
#193658=CARTESIAN_POINT('Ctrl Pts',(-242.007213264324,-1.18376388654087,
137.303032704464));
#193659=CARTESIAN_POINT('Ctrl Pts',(-242.285660888137,4.82766358294966,
135.312985703106));
#193660=CARTESIAN_POINT('Ctrl Pts',(-242.56410851195,6.40270406418687,129.179732506718));
#193661=CARTESIAN_POINT('Ctrl Pts',(-242.842556135762,2.09397229991911,
124.539433176702));
#193662=CARTESIAN_POINT('Ctrl Pts',(-243.121003759575,-4.13901771174057,
125.65629610612));
#193663=CARTESIAN_POINT('Ctrl Pts',(-243.399451383388,-6.56845264856689,
131.503978824623));
#193664=CARTESIAN_POINT('Ctrl Pts',(-243.677899007202,-2.9618004881116,
136.70874658909));
#193665=CARTESIAN_POINT('Ctrl Pts',(-243.956346631013,3.36660162892119,
136.487672091016));
#193666=CARTESIAN_POINT('Ctrl Pts',(-244.234794254827,6.60126131660758,
131.043911994042));
#193667=CARTESIAN_POINT('Ctrl Pts',(-244.513241878639,3.76968434387551,
125.380015884821));
#193668=CARTESIAN_POINT('Ctrl Pts',(-244.791689502453,-2.52604838156001,
124.70082759102));
#193669=CARTESIAN_POINT('Ctrl Pts',(-245.070137126265,-6.50046604866569,
129.630487974449));
#193670=CARTESIAN_POINT('Ctrl Pts',(-245.348584750079,-4.50127298246883,
135.638879970036));
#193671=CARTESIAN_POINT('Ctrl Pts',(-245.627032373891,1.63437005520677,
137.204584860103));
#193672=CARTESIAN_POINT('Ctrl Pts',(-245.905479997704,6.26810685556324,
132.888796339615));
#193673=CARTESIAN_POINT('Ctrl Pts',(-246.183927621517,5.14175966970064,
126.65751322091));
#193674=CARTESIAN_POINT('Ctrl Pts',(-246.46237524533,-0.709613463692526,
124.236980274974));
#193675=CARTESIAN_POINT('Ctrl Pts',(-246.740822869143,-5.90888649049716,
127.851549029514));
#193676=CARTESIAN_POINT('Ctrl Pts',(-247.019270492956,-5.67818149768794,
134.179607380607));
#193677=CARTESIAN_POINT('Ctrl Pts',(-247.297718116769,-0.229505103091092,
137.405978846438));
#193678=CARTESIAN_POINT('Ctrl Pts',(-247.576165740581,5.43007526929941,
134.565785666913));
#193679=CARTESIAN_POINT('Ctrl Pts',(-247.854613364394,6.09968174312738,
128.269026622868));
#193680=CARTESIAN_POINT('Ctrl Pts',(-248.133060988207,1.16397868104094,
124.302115661998));
#193681=CARTESIAN_POINT('Ctrl Pts',(-248.41150861202,-4.84136392540264,
126.31045016297));
#193682=CARTESIAN_POINT('Ctrl Pts',(-248.689956235833,-6.39772959817725,
132.448468831983));
#193683=CARTESIAN_POINT('Ctrl Pts',(-248.968403859646,-2.07489431669385,
137.075632371099));
#193684=CARTESIAN_POINT('Ctrl Pts',(-249.246851483459,4.15466747760909,
135.939803537374));
#193685=CARTESIAN_POINT('Ctrl Pts',(-249.525299107272,6.56629282677857,
130.08475354068));
#193686=CARTESIAN_POINT('Ctrl Pts',(-249.803746731085,2.94381584937754,
124.890987292882));
#193687=CARTESIAN_POINT('Ctrl Pts',(-250.082194354898,-3.38388408020374,
125.131322246124));
#193688=CARTESIAN_POINT('Ctrl Pts',(-250.36064197871,-6.60195985200274,
130.584902319384));
#193689=CARTESIAN_POINT('Ctrl Pts',(-250.639089602524,-3.75315704348482,
136.240153847548));
#193690=CARTESIAN_POINT('Ctrl Pts',(-250.917537226336,2.54461373609029,
136.900176950603));
#193691=CARTESIAN_POINT('Ctrl Pts',(-251.19598485015,6.50400880347224,131.958442640812));
#193692=CARTESIAN_POINT('Ctrl Pts',(-251.474432473962,4.48653751899202,
125.956163331638));
#193693=CARTESIAN_POINT('Ctrl Pts',(-251.752880097775,-1.65384256596459,
124.409140480742));
#193694=CARTESIAN_POINT('Ctrl Pts',(-252.031327721588,-6.27442212737671,
128.739012511497));
#193695=CARTESIAN_POINT('Ctrl Pts',(-252.309775345401,-5.12911427652582,
134.966838554275));
#193696=CARTESIAN_POINT('Ctrl Pts',(-252.588222969213,0.729599023732927,
137.369550720794));
#193697=CARTESIAN_POINT('Ctrl Pts',(-252.866670593027,5.91784646323776,
133.739173911277));
#193698=CARTESIAN_POINT('Ctrl Pts',(-253.145118216839,5.66788210748017,
127.411847055674));
#193699=CARTESIAN_POINT('Ctrl Pts',(-253.423565840652,0.209410983396998,
124.20207443517));
#193700=CARTESIAN_POINT('Ctrl Pts',(-253.702013464465,-5.44149859849489,
127.059480266814));
#193701=CARTESIAN_POINT('Ctrl Pts',(-253.980461088278,-6.0919368110008,
133.358248211846));
#193702=CARTESIAN_POINT('Ctrl Pts',(-254.258908712091,-1.1441826817532,
137.310118186916));
#193703=CARTESIAN_POINT('Ctrl Pts',(-254.537356335904,4.85501939763767,
135.283514846073));
#193704=CARTESIAN_POINT('Ctrl Pts',(-254.815803959717,6.39269590315201,
129.140787462715));
#193705=CARTESIAN_POINT('Ctrl Pts',(-255.09425158353,2.05579703890082,124.526802775315));
#193706=CARTESIAN_POINT('Ctrl Pts',(-255.372699207342,-4.17027861730954,
125.681586622223));
#193707=CARTESIAN_POINT('Ctrl Pts',(-255.651146831155,-6.5640724361261,
131.5439503534));
#193708=CARTESIAN_POINT('Ctrl Pts',(-255.929594454968,-2.925803447894,136.726665654721));
#193709=CARTESIAN_POINT('Ctrl Pts',(-256.208042078781,3.40113425532747,
136.467074956607));
#193710=CARTESIAN_POINT('Ctrl Pts',(-256.486489702594,6.60259898059897,
131.003720738236));
#193711=CARTESIAN_POINT('Ctrl Pts',(-256.764937326407,3.73659166461274,
125.357175036369));
#193712=CARTESIAN_POINT('Ctrl Pts',(-257.04338495022,-2.56314926818932,
124.716306516944));
#193713=CARTESIAN_POINT('Ctrl Pts',(-257.321832574033,-6.5075031063131,
129.670100547101));
#193714=CARTESIAN_POINT('Ctrl Pts',(-257.600280197845,-4.47173821150659,
135.666151948257));
#193715=CARTESIAN_POINT('Ctrl Pts',(-257.878727821659,1.67325768403046,
137.194590998305));
#193716=CARTESIAN_POINT('Ctrl Pts',(-258.157175445471,6.28075871394982,
132.850463013089));
#193717=CARTESIAN_POINT('Ctrl Pts',(-258.435623069284,5.1162713672671,126.626553096149));
#193718=CARTESIAN_POINT('Ctrl Pts',(-258.714070693097,-0.749294580734974,
124.240926059104));
#193719=CARTESIAN_POINT('Ctrl Pts',(-258.99251831691,-5.92728653745133,
127.888508918958));
#193720=CARTESIAN_POINT('Ctrl Pts',(-259.270965940723,-5.656519339957,134.212338033208));
#193721=CARTESIAN_POINT('Ctrl Pts',(-259.549413564536,-0.191230405826049,
137.41063083554));
#193722=CARTESIAN_POINT('Ctrl Pts',(-259.827861188349,5.45654320709978,
134.526020746857));
#193723=CARTESIAN_POINT('Ctrl Pts',(-260.059900874859,5.97341346954355,
129.293215926205));
#193724=CARTESIAN_POINT('Ctrl Pts',(-260.245542550368,3.60742224527213,
126.247226657536));
#193725=CARTESIAN_POINT('Ctrl Pts',(-260.338368351272,1.86717727106152,
125.459413119698));
#193726=CARTESIAN_POINT('Ctrl Pts',(-260.384786214875,0.950008195528324,
125.301089073499));
#193727=CARTESIAN_POINT('Ctrl Pts',(209.997886486728,-2.58542267678463,
125.478296443779));
#193728=CARTESIAN_POINT('Ctrl Pts',(209.951476810375,-3.47289965896197,
125.909102290886));
#193729=CARTESIAN_POINT('Ctrl Pts',(209.85865919672,-5.01373755653622,127.222906143875));
#193730=CARTESIAN_POINT('Ctrl Pts',(209.67302570846,-6.52844908712303,131.020616473957));
#193731=CARTESIAN_POINT('Ctrl Pts',(209.440986021949,-4.4641631800594,136.198709217918));
#193732=CARTESIAN_POINT('Ctrl Pts',(209.162538398136,2.13623200523086,137.47712630299));
#193733=CARTESIAN_POINT('Ctrl Pts',(208.884090774324,6.76311047611758,132.61329501932));
#193734=CARTESIAN_POINT('Ctrl Pts',(208.60564315051,5.180460236421,126.09244423763));
#193735=CARTESIAN_POINT('Ctrl Pts',(208.327195526698,-1.16565068102074,
123.898824768668));
#193736=CARTESIAN_POINT('Ctrl Pts',(208.048747902884,-6.43906639651766,
128.052530506575));
#193737=CARTESIAN_POINT('Ctrl Pts',(207.770300279072,-5.79609906993421,
134.734252735451));
#193738=CARTESIAN_POINT('Ctrl Pts',(207.491852655259,0.173626147510206,
137.805009652024));
#193739=CARTESIAN_POINT('Ctrl Pts',(207.213405031446,5.98357180802623,134.442293088818));
#193740=CARTESIAN_POINT('Ctrl Pts',(206.934957407633,6.29502677410122,127.736610299611));
#193741=CARTESIAN_POINT('Ctrl Pts',(206.65650978382,0.821596385081328,123.849978754804));
#193742=CARTESIAN_POINT('Ctrl Pts',(206.378062160007,-5.40680743188727,
126.354116934927));
#193743=CARTESIAN_POINT('Ctrl Pts',(206.099614536195,-6.66663710465116,
132.947794423038));
#193744=CARTESIAN_POINT('Ctrl Pts',(205.821166912381,-1.80014356190772,
137.571770081489));
#193745=CARTESIAN_POINT('Ctrl Pts',(205.542719288569,4.72058899422897,135.976822216287));
#193746=CARTESIAN_POINT('Ctrl Pts',(205.264271664756,6.90333351468265,129.628637390042));
#193747=CARTESIAN_POINT('Ctrl Pts',(204.985824040943,2.74225038547515,124.360883417158));
#193748=CARTESIAN_POINT('Ctrl Pts',(204.70737641713,-3.93882614214087,125.014370927945));
#193749=CARTESIAN_POINT('Ctrl Pts',(204.428928793317,-7.00031425910704,
130.988575726592));
#193750=CARTESIAN_POINT('Ctrl Pts',(204.150481169504,-3.62885534891233,
136.793496040797));
#193751=CARTESIAN_POINT('Ctrl Pts',(203.872033545692,3.07734423765085,137.09469337995));
#193752=CARTESIAN_POINT('Ctrl Pts',(203.593585921878,6.95561486460971,131.615382266785));
#193753=CARTESIAN_POINT('Ctrl Pts',(203.315138298066,4.44201520086038,125.390781848689));
#193754=CARTESIAN_POINT('Ctrl Pts',(203.036690674253,-2.15357941165663,
124.140995867004));
#193755=CARTESIAN_POINT('Ctrl Pts',(202.75824305044,-6.77013976170558,129.014516559232));
#193756=CARTESIAN_POINT('Ctrl Pts',(202.479795426627,-5.16527240588502,
135.532816506767));
#193757=CARTESIAN_POINT('Ctrl Pts',(202.201347802814,1.18622795093483,137.705896487686));
#193758=CARTESIAN_POINT('Ctrl Pts',(201.922900179001,6.44764277258624,133.536802163981));
#193759=CARTESIAN_POINT('Ctrl Pts',(201.644452555188,5.78398887041165,126.856727545651));
#193760=CARTESIAN_POINT('Ctrl Pts',(201.366004931376,-0.194868239746226,
123.804334868162));
#193761=CARTESIAN_POINT('Ctrl Pts',(201.087557307562,-5.99465095761073,
127.184623883922));
#193762=CARTESIAN_POINT('Ctrl Pts',(200.80910968375,-6.2856423003101,133.891274124028));
#193763=CARTESIAN_POINT('Ctrl Pts',(200.530662059936,-0.80043543977546,
137.76120165575));
#193764=CARTESIAN_POINT('Ctrl Pts',(200.252214436124,5.42033248649604,135.238132133988));
#193765=CARTESIAN_POINT('Ctrl Pts',(199.973766812311,6.66007965562565,128.640643190398));
#193766=CARTESIAN_POINT('Ctrl Pts',(199.695319188498,1.77953898422249,124.031504858911));
#193767=CARTESIAN_POINT('Ctrl Pts',(199.416871564685,-4.73631107837294,
125.646290097223));
#193768=CARTESIAN_POINT('Ctrl Pts',(199.138423940872,-6.89972264160091,
132.00109015798));
#193769=CARTESIAN_POINT('Ctrl Pts',(198.859976317059,-2.72262616738874,
137.256154234582));
#193770=CARTESIAN_POINT('Ctrl Pts',(198.581528693247,3.95643074697165,136.582335164788));
#193771=CARTESIAN_POINT('Ctrl Pts',(198.303081069434,6.999721087252,130.598839755845));
#193772=CARTESIAN_POINT('Ctrl Pts',(198.024633445621,3.61060970373355,124.804207978572));
#193773=CARTESIAN_POINT('Ctrl Pts',(197.746185821808,-3.09647560942607,
124.523423352781));
#193774=CARTESIAN_POINT('Ctrl Pts',(197.467738197995,-6.9580511087663,130.014513232485));
#193775=CARTESIAN_POINT('Ctrl Pts',(197.189290574182,-4.4255175588443,136.231434272887));
#193776=CARTESIAN_POINT('Ctrl Pts',(196.910842950369,2.17385042910367,137.461139751337));
#193777=CARTESIAN_POINT('Ctrl Pts',(196.632395326556,6.77555607120273,132.573590407591));
#193778=CARTESIAN_POINT('Ctrl Pts',(196.353947702743,5.15085668818228,126.060205318492));
#193779=CARTESIAN_POINT('Ctrl Pts',(196.07550007893,-1.20722835793932,123.90646718437));
#193780=CARTESIAN_POINT('Ctrl Pts',(195.797052455118,-6.45592951949867,
128.091556134528));
#193781=CARTESIAN_POINT('Ctrl Pts',(195.518604831305,-5.77194684232935,
134.769579876729));
#193782=CARTESIAN_POINT('Ctrl Pts',(195.240157207492,0.216173007661386,
137.80376083149));
#193783=CARTESIAN_POINT('Ctrl Pts',(194.961709583679,6.00564042424985,134.405834929363));
#193784=CARTESIAN_POINT('Ctrl Pts',(194.683261959866,6.2762176827981,127.698330076496));
#193785=CARTESIAN_POINT('Ctrl Pts',(194.404814336053,0.779257501134259,
123.845115552844));
#193786=CARTESIAN_POINT('Ctrl Pts',(194.12636671224,-5.43380225522669,126.387107265649));
#193787=CARTESIAN_POINT('Ctrl Pts',(193.847919088427,-6.65346319503207,
132.988339014042));
#193788=CARTESIAN_POINT('Ctrl Pts',(193.569471464615,-1.75891649835014,
137.58260130935));
#193789=CARTESIAN_POINT('Ctrl Pts',(193.291023840801,4.75198853246758,135.947991544374));
#193790=CARTESIAN_POINT('Ctrl Pts',(193.012576216989,6.89604824949333,129.586636238002));
#193791=CARTESIAN_POINT('Ctrl Pts',(192.734128593176,2.70297651592057,124.344310147306));
#193792=CARTESIAN_POINT('Ctrl Pts',(192.455680969363,-3.97399858803937,
125.038454847768));
#193793=CARTESIAN_POINT('Ctrl Pts',(192.17723334555,-6.99906313021511,131.031185270517));
#193794=CARTESIAN_POINT('Ctrl Pts',(191.898785721737,-3.59233057896577,
136.815474918205));
#193795=CARTESIAN_POINT('Ctrl Pts',(191.620338097924,3.11557827924791,137.075844182864));
#193796=CARTESIAN_POINT('Ctrl Pts',(191.341890474111,6.96042290329331,131.573026430018));
#193797=CARTESIAN_POINT('Ctrl Pts',(191.063442850298,4.40897891477476,125.363842346942));
#193798=CARTESIAN_POINT('Ctrl Pts',(190.784995226486,-2.19410130582752,
124.154228770475));
#193799=CARTESIAN_POINT('Ctrl Pts',(190.506547602672,-6.78090961418206,
129.055761484483));
#193800=CARTESIAN_POINT('Ctrl Pts',(190.22809997886,-5.13639325295408,135.564171377977));
#193801=CARTESIAN_POINT('Ctrl Pts',(189.949652355047,1.22821758097839,137.698547712335));
#193802=CARTESIAN_POINT('Ctrl Pts',(189.671204731234,6.46415645975623,133.497502906364));
#193803=CARTESIAN_POINT('Ctrl Pts',(189.392757107421,5.75985134361714,126.821591904301));
#193804=CARTESIAN_POINT('Ctrl Pts',(189.114309483608,-0.237475772924818,
123.80565078066));
#193805=CARTESIAN_POINT('Ctrl Pts',(188.835861859795,-6.01657425548534,
127.221182091151));
#193806=CARTESIAN_POINT('Ctrl Pts',(188.557414235982,-6.2667349232476,133.929479419415));
#193807=CARTESIAN_POINT('Ctrl Pts',(188.278966612169,-0.758072343566082,
137.76594523932));
#193808=CARTESIAN_POINT('Ctrl Pts',(188.000518988357,5.44722168595988,135.205054884148));
#193809=CARTESIAN_POINT('Ctrl Pts',(187.722071364544,6.64678509766207,128.600141483854));
#193810=CARTESIAN_POINT('Ctrl Pts',(187.443623740731,1.73827771811677,124.02079778535));
#193811=CARTESIAN_POINT('Ctrl Pts',(187.165176116918,-4.76762196479028,
125.675216934184));
#193812=CARTESIAN_POINT('Ctrl Pts',(186.886728493105,-6.89230997333645,
132.043068555446));
#193813=CARTESIAN_POINT('Ctrl Pts',(186.608280869292,-2.68330182444739,
137.272608096043));
#193814=CARTESIAN_POINT('Ctrl Pts',(186.329833245479,3.99152961452714,136.558144195375));
#193815=CARTESIAN_POINT('Ctrl Pts',(186.051385621667,6.99834033481346,130.556234274655));
#193816=CARTESIAN_POINT('Ctrl Pts',(185.772937997853,3.5740181753383,124.782340341422));
#193817=CARTESIAN_POINT('Ctrl Pts',(185.494490374041,-3.13465208677821,
124.542388849921));
#193818=CARTESIAN_POINT('Ctrl Pts',(185.216042750227,-6.96273021741339,
130.056883498557));
#193819=CARTESIAN_POINT('Ctrl Pts',(184.937595126415,-4.39239942652681,
136.258273103275));
#193820=CARTESIAN_POINT('Ctrl Pts',(184.659147502602,2.21433185669671,137.447783572063));
#193821=CARTESIAN_POINT('Ctrl Pts',(184.380699878789,6.78620033974098,132.532312894923));
#193822=CARTESIAN_POINT('Ctrl Pts',(184.102252254976,5.12188223488049,126.028938490053));
#193823=CARTESIAN_POINT('Ctrl Pts',(183.823804631163,-1.24919542597752,
123.913943728027));
#193824=CARTESIAN_POINT('Ctrl Pts',(183.54535700735,-6.47232351695142,128.130905471908));
#193825=CARTESIAN_POINT('Ctrl Pts',(183.266909383538,-5.74770248642891,
134.804641889104));
#193826=CARTESIAN_POINT('Ctrl Pts',(182.988461759724,0.258776338245136,
137.80231524236));
#193827=CARTESIAN_POINT('Ctrl Pts',(182.710014135912,6.02745234999885,134.369210164519));
#193828=CARTESIAN_POINT('Ctrl Pts',(182.431566512099,6.25719410952084,127.66018250561));
#193829=CARTESIAN_POINT('Ctrl Pts',(182.153118888286,0.73688016331929,123.840500929948));
#193830=CARTESIAN_POINT('Ctrl Pts',(181.874671264473,-5.46059065437546,
126.420266203747));
#193831=CARTESIAN_POINT('Ctrl Pts',(181.59622364066,-6.64004542538295,133.028800068927));
#193832=CARTESIAN_POINT('Ctrl Pts',(181.317776016847,-1.71762283471616,
137.593182748215));
#193833=CARTESIAN_POINT('Ctrl Pts',(181.039328393035,4.78321123051439,135.918969541833));
#193834=CARTESIAN_POINT('Ctrl Pts',(180.760880769221,6.88850784776155,129.544680596588));
#193835=CARTESIAN_POINT('Ctrl Pts',(180.482433145409,2.66360227523266,124.32797605183));
#193836=CARTESIAN_POINT('Ctrl Pts',(180.203985521595,-4.00902366402984,
125.062752534008));
#193837=CARTESIAN_POINT('Ctrl Pts',(179.925537897783,-6.99755270774298,
131.073786351827));
#193838=CARTESIAN_POINT('Ctrl Pts',(179.64709027397,-3.5556726624947,136.837231082039));
#193839=CARTESIAN_POINT('Ctrl Pts',(179.368642650157,3.15369685531979,137.056762577506));
#193840=CARTESIAN_POINT('Ctrl Pts',(179.090195026344,6.96497302975191,131.530642118605));
#193841=CARTESIAN_POINT('Ctrl Pts',(178.811747402531,4.37577924769062,125.337104441072));
#193842=CARTESIAN_POINT('Ctrl Pts',(178.533299778718,-2.23454189429802,
124.167708099424));
#193843=CARTESIAN_POINT('Ctrl Pts',(178.254852154906,-6.79142819886702,
129.097071203448));
#193844=CARTESIAN_POINT('Ctrl Pts',(177.976404531092,-5.10732376838957,
135.595349873321));
#193845=CARTESIAN_POINT('Ctrl Pts',(177.69795690728,1.27016169860089,137.690943469992));
#193846=CARTESIAN_POINT('Ctrl Pts',(177.419509283467,6.48043061542571,133.458103853558));
#193847=CARTESIAN_POINT('Ctrl Pts',(177.141061659654,5.73550038331004,126.786603845811));
#193848=CARTESIAN_POINT('Ctrl Pts',(176.862614035841,-0.280074506296806,
123.807226032976));
#193849=CARTESIAN_POINT('Ctrl Pts',(176.584166412028,-6.0382746070172,127.257873074351));
#193850=CARTESIAN_POINT('Ctrl Pts',(176.305718788215,-6.24759533000263,
133.967568912391));
#193851=CARTESIAN_POINT('Ctrl Pts',(176.027271164402,-0.71568115671533,
137.770430858802));
#193852=CARTESIAN_POINT('Ctrl Pts',(175.748823540589,5.4739090366252,135.171814564968));
#193853=CARTESIAN_POINT('Ctrl Pts',(175.470375916777,6.63324424063007,128.559721455457));
#193854=CARTESIAN_POINT('Ctrl Pts',(175.191928292964,1.69695203949225,124.010342079205));
#193855=CARTESIAN_POINT('Ctrl Pts',(174.913480669151,-4.79875618522306,
125.704333833448));
#193856=CARTESIAN_POINT('Ctrl Pts',(174.635033045338,-6.88464190799096,
132.085001052137));
#193857=CARTESIAN_POINT('Ctrl Pts',(174.356585421525,-2.64387805077028,
137.288822274217));
#193858=CARTESIAN_POINT('Ctrl Pts',(174.078137797712,4.02648057448505,136.533740017397));
#193859=CARTESIAN_POINT('Ctrl Pts',(173.799690173899,6.99670025630013,130.513637987877));
#193860=CARTESIAN_POINT('Ctrl Pts',(173.521242550086,3.53729421038521,124.76069585245));
#193861=CARTESIAN_POINT('Ctrl Pts',(173.242794926273,-3.17271240844464,
124.561586386726));
#193862=CARTESIAN_POINT('Ctrl Pts',(172.96434730246,-6.96715131953175,130.099281462668));
#193863=CARTESIAN_POINT('Ctrl Pts',(172.685899678648,-4.35911853223319,
136.284909836929));
#193864=CARTESIAN_POINT('Ctrl Pts',(172.407452054835,2.25473123140845,137.434181218309));
#193865=CARTESIAN_POINT('Ctrl Pts',(172.129004431022,6.79659314313001,132.490971352347));
#193866=CARTESIAN_POINT('Ctrl Pts',(171.850556807209,5.09271798834896,125.997848616637));
#193867=CARTESIAN_POINT('Ctrl Pts',(171.572109183396,-1.29111620461978,
123.921675598615));
#193868=CARTESIAN_POINT('Ctrl Pts',(171.293661559583,-6.48847768007612,
128.170353875152));
#193869=CARTESIAN_POINT('Ctrl Pts',(171.01521393577,-5.72324514729908,134.839555669585));
#193870=CARTESIAN_POINT('Ctrl Pts',(170.736766311957,0.301370079776633,
137.800610341449));
#193871=CARTESIAN_POINT('Ctrl Pts',(170.458318688145,6.04904092628448,134.332453302864));
#193872=CARTESIAN_POINT('Ctrl Pts',(170.179871064331,6.23793867361471,127.6221514434));
#193873=CARTESIAN_POINT('Ctrl Pts',(169.901423440519,0.694475520138818,
123.836144355433));
#193874=CARTESIAN_POINT('Ctrl Pts',(169.622975816706,-5.4871767093294,126.453587596077));
#193875=CARTESIAN_POINT('Ctrl Pts',(169.344528192893,-6.62638160640872,
133.06917869639));
#193876=CARTESIAN_POINT('Ctrl Pts',(169.06608056908,-1.67626552393645,137.603512624779));
#193877=CARTESIAN_POINT('Ctrl Pts',(168.787632945267,4.81425668490999,135.88975801558));
#193878=CARTESIAN_POINT('Ctrl Pts',(168.509185321454,6.88071218983824,129.50277163308));
#193879=CARTESIAN_POINT('Ctrl Pts',(168.230737697641,2.62412933378287,124.311881941165));
#193880=CARTESIAN_POINT('Ctrl Pts',(167.952290073828,-4.0439001841742,125.087262977647));
#193881=CARTESIAN_POINT('Ctrl Pts',(167.673842450016,-6.99578298838191,
131.116377449467));
#193882=CARTESIAN_POINT('Ctrl Pts',(167.395394826203,-3.51888298926545,
136.858763695638));
#193883=CARTESIAN_POINT('Ctrl Pts',(167.11694720239,3.19169856999505,137.037449287095));
#193884=CARTESIAN_POINT('Ctrl Pts',(166.838499578577,6.96926506657354,131.488230894564));
#193885=CARTESIAN_POINT('Ctrl Pts',(166.560051954764,4.34241743449723,125.310569126392));
#193886=CARTESIAN_POINT('Ctrl Pts',(166.281604330951,-2.27489968099678,
124.181433351974));
#193887=CARTESIAN_POINT('Ctrl Pts',(166.003156707138,-6.80169512468258,
129.13844418665));
#193888=CARTESIAN_POINT('Ctrl Pts',(165.724709083325,-5.0780650300646,135.626350836796));
#193889=CARTESIAN_POINT('Ctrl Pts',(165.446261459512,1.31205874991464,137.683084042787));
#193890=CARTESIAN_POINT('Ctrl Pts',(165.1678138357,6.49646463635559,133.418606465321));
#193891=CARTESIAN_POINT('Ctrl Pts',(164.889366211887,5.71093689192698,126.751764666776));
#193892=CARTESIAN_POINT('Ctrl Pts',(164.610918588074,-0.322662861405092,
123.809060566689));
#193893=CARTESIAN_POINT('Ctrl Pts',(164.332470964261,-6.05975120806294,
127.29469547395));
#193894=CARTESIAN_POINT('Ctrl Pts',(164.054023340448,-6.22822422981513,
134.00554119152));
#193895=CARTESIAN_POINT('Ctrl Pts',(163.775575716635,-0.673263450036036,
137.774658347991));
#193896=CARTESIAN_POINT('Ctrl Pts',(163.497128092822,5.50039354957815,135.138412408175));
#193897=CARTESIAN_POINT('Ctrl Pts',(163.218680469009,6.61945758629338,128.51938460299));
#193898=CARTESIAN_POINT('Ctrl Pts',(162.940232845196,1.65556347968583,124.000138127916));
#193899=CARTESIAN_POINT('Ctrl Pts',(162.661785221384,-4.82971258598073,
125.733639716082));
#193900=CARTESIAN_POINT('Ctrl Pts',(162.383337597571,-6.87671872970774,
132.126886094224));
#193901=CARTESIAN_POINT('Ctrl Pts',(162.104889973758,-2.60435630721971,
137.304796168278));
#193902=CARTESIAN_POINT('Ctrl Pts',(161.826442349945,4.06128233172446,136.509123535159));
#193903=CARTESIAN_POINT('Ctrl Pts',(161.547994726132,6.99480091248578,130.471052473933));
#193904=CARTESIAN_POINT('Ctrl Pts',(161.269547102319,3.50043916969439,124.739275313697));
#193905=CARTESIAN_POINT('Ctrl Pts',(160.991099478506,-3.21065516408591,
124.581015251828));
#193906=CARTESIAN_POINT('Ctrl Pts',(160.712651854693,-6.97131425129578,
130.141705553748));
#193907=CARTESIAN_POINT('Ctrl Pts',(160.434204230881,-4.32567610919938,
136.311343486817));
#193908=CARTESIAN_POINT('Ctrl Pts',(160.155756607067,2.29504705622523,137.420333194114));
#193909=CARTESIAN_POINT('Ctrl Pts',(159.877308983254,6.80673409626067,132.449567311792));
#193910=CARTESIAN_POINT('Ctrl Pts',(159.598861359442,5.06336502927952,125.966936850291));
#193911=CARTESIAN_POINT('Ctrl Pts',(159.320413735629,-1.33298914047637,
123.929662509627));
#193912=CARTESIAN_POINT('Ctrl Pts',(159.041966111816,-6.50439141027418,
128.209899882485));
#193913=CARTESIAN_POINT('Ctrl Pts',(158.763518488003,-5.69857573121565,
134.874319924428));
#193914=CARTESIAN_POINT('Ctrl Pts',(158.48507086419,0.343952653928878,137.798646191931));
#193915=CARTESIAN_POINT('Ctrl Pts',(158.206623240377,6.07040535313402,134.295565706438));
#193916=CARTESIAN_POINT('Ctrl Pts',(157.928175616564,6.2184520885971,127.584238299121));
#193917=CARTESIAN_POINT('Ctrl Pts',(157.649727992752,0.652045142912632,
123.832045990734));
#193918=CARTESIAN_POINT('Ctrl Pts',(157.371280368939,-5.51355943493244,
126.487070207899));
#193919=CARTESIAN_POINT('Ctrl Pts',(157.092832745126,-6.61247224442723,
133.109473400187));
#193920=CARTESIAN_POINT('Ctrl Pts',(156.814385121313,-1.63484609852131,
137.613590556265));
#193921=CARTESIAN_POINT('Ctrl Pts',(156.5359374975,4.84512374525377,135.860358048054));
#193922=CARTESIAN_POINT('Ctrl Pts',(156.257489873687,6.87266156459436,129.46091090043));
#193923=CARTESIAN_POINT('Ctrl Pts',(155.979042249874,2.58455915425555,124.296028411687));
#193924=CARTESIAN_POINT('Ctrl Pts',(155.700594626061,-4.07862685611001,
125.111985270442));
#193925=CARTESIAN_POINT('Ctrl Pts',(155.422147002248,-6.99375403770952,
131.158956985208));
#193926=CARTESIAN_POINT('Ctrl Pts',(155.143699378435,-3.48196292253304,
136.880071961106));
#193927=CARTESIAN_POINT('Ctrl Pts',(154.865251754623,3.22958201510593,137.017905027291));
#193928=CARTESIAN_POINT('Ctrl Pts',(154.58680413081,6.97329885471516,131.445794329457));
#193929=CARTESIAN_POINT('Ctrl Pts',(154.308356506997,4.30889471142897,125.284237386175));
#193930=CARTESIAN_POINT('Ctrl Pts',(154.029908883184,-2.31517317045128,
124.195404019528));
#193931=CARTESIAN_POINT('Ctrl Pts',(153.751461259371,-6.81171001118396,
129.179878900999));
#193932=CARTESIAN_POINT('Ctrl Pts',(153.473013635558,-5.04861812217248,
135.65717311965));
#193933=CARTESIAN_POINT('Ctrl Pts',(153.194566011745,1.3539071824088,137.674969721956));
#193934=CARTESIAN_POINT('Ctrl Pts',(152.916118387933,6.51225792839928,133.379012205241));
#193935=CARTESIAN_POINT('Ctrl Pts',(152.637670764119,5.68616177967723,126.717075658174));
#193936=CARTESIAN_POINT('Ctrl Pts',(152.359223140307,-0.365239260122265,
123.811154313817));
#193937=CARTESIAN_POINT('Ctrl Pts',(152.080775516494,-6.08100326279917,
127.331647925483));
#193938=CARTESIAN_POINT('Ctrl Pts',(151.802327892681,-6.20862234048841,
134.043394849727));
#193939=CARTESIAN_POINT('Ctrl Pts',(151.523880268868,-0.630820795332096,
137.778627550233));
#193940=CARTESIAN_POINT('Ctrl Pts',(151.245432645055,5.52667424342534,135.104849651499));
#193941=CARTESIAN_POINT('Ctrl Pts',(150.966985021242,6.60542564552152,128.479132421149));
#193942=CARTESIAN_POINT('Ctrl Pts',(150.688537397429,1.61411357236584,123.990186309594));
#193943=CARTESIAN_POINT('Ctrl Pts',(150.410089773616,-4.86049001996232,
125.763133496143));
#193944=CARTESIAN_POINT('Ctrl Pts',(150.131642149803,-6.8685407320831,132.168722129643));
#193945=CARTESIAN_POINT('Ctrl Pts',(149.853194525991,-2.56473805828847,
137.32052918631));
#193946=CARTESIAN_POINT('Ctrl Pts',(149.574746902178,4.09593359665354,136.484295660832));
#193947=CARTESIAN_POINT('Ctrl Pts',(149.296299278365,6.99264237375128,130.428479310845));
#193948=CARTESIAN_POINT('Ctrl Pts',(149.017851654552,3.46345441894284,124.718079518912));
#193949=CARTESIAN_POINT('Ctrl Pts',(148.739404030739,-3.24847894771935,
124.600674725279));
#193950=CARTESIAN_POINT('Ctrl Pts',(148.460956406926,-6.97521885844655,
130.184154199754));
#193951=CARTESIAN_POINT('Ctrl Pts',(148.182508783113,-4.29207339664657,
136.337573073429));
#193952=CARTESIAN_POINT('Ctrl Pts',(147.9040611593,2.33527783722936,137.406240012622));
#193953=CARTESIAN_POINT('Ctrl Pts',(147.625613535487,6.81662282335624,132.408102307496));
#193954=CARTESIAN_POINT('Ctrl Pts',(147.347165911675,5.03382444535687,125.936204336462));
#193955=CARTESIAN_POINT('Ctrl Pts',(147.068718287862,-1.37481268193005,
123.937904165105));
#193956=CARTESIAN_POINT('Ctrl Pts',(146.790270664049,-6.52006411785656,
128.249542028514));
#193957=CARTESIAN_POINT('Ctrl Pts',(146.511823040236,-5.67369515231286,
134.908933365434));
#193958=CARTESIAN_POINT('Ctrl Pts',(146.233375416423,0.386522482789046,
137.796422866589));
#193959=CARTESIAN_POINT('Ctrl Pts',(145.95492779261,6.09154483888081,134.258548742122));
#193960=CARTESIAN_POINT('Ctrl Pts',(145.676480168797,6.19873507655051,127.546444477659));
#193961=CARTESIAN_POINT('Ctrl Pts',(145.398032544984,0.609590603913882,
123.828205987717));
#193962=CARTESIAN_POINT('Ctrl Pts',(145.119584921171,-5.53973785356302,
126.520712798507));
#193963=CARTESIAN_POINT('Ctrl Pts',(144.841137297358,-6.59831785485502,
133.149682687181));
#193964=CARTESIAN_POINT('Ctrl Pts',(144.562689673546,-1.59336609328267,
137.623416169231));
#193965=CARTESIAN_POINT('Ctrl Pts',(144.284242049733,4.87581126775532,135.830770728684));
#193966=CARTESIAN_POINT('Ctrl Pts',(144.00579442592,6.86435627034879,129.419099949804));
#193967=CARTESIAN_POINT('Ctrl Pts',(143.727346802107,2.54489320293839,124.280416050852));
#193968=CARTESIAN_POINT('Ctrl Pts',(143.448899178294,-4.11320239302776,
125.136918496298));
#193969=CARTESIAN_POINT('Ctrl Pts',(143.170451554481,-6.99146593090932,
131.201523381251));
#193970=CARTESIAN_POINT('Ctrl Pts',(142.892003930668,-3.44491383038404,
136.901155088855));
#193971=CARTESIAN_POINT('Ctrl Pts',(142.613556306855,3.26734578686757,136.998130522314));
#193972=CARTESIAN_POINT('Ctrl Pts',(142.335108683042,6.97707424470332,131.403333995789));
#193973=CARTESIAN_POINT('Ctrl Pts',(142.05666105923,4.27521232068256,125.258110196154));
#193974=CARTESIAN_POINT('Ctrl Pts',(141.778213435417,-2.35536087031262,
124.209619584399));
#193975=CARTESIAN_POINT('Ctrl Pts',(141.499765811604,-6.8214724872659,129.221373811115));
#193976=CARTESIAN_POINT('Ctrl Pts',(141.221318187791,-5.01898413587917,
135.687815579753));
#193977=CARTESIAN_POINT('Ctrl Pts',(140.942870563978,1.39570544537436,137.666600808179));
#193978=CARTESIAN_POINT('Ctrl Pts',(140.664422940165,6.52780990633047,133.339322540502));
#193979=CARTESIAN_POINT('Ctrl Pts',(140.385975316352,5.66117596461176,126.68253810542));
#193980=CARTESIAN_POINT('Ctrl Pts',(140.10752769254,-0.407802124764288,
123.813507196776));
#193981=CARTESIAN_POINT('Ctrl Pts',(139.829080068726,-6.10202998372316,
127.368729059661));
#193982=CARTESIAN_POINT('Ctrl Pts',(139.550632444914,-6.18879038837768,
134.081128484328));
#193983=CARTESIAN_POINT('Ctrl Pts',(139.272184821101,-0.588354765331746,
137.78233831845));
#193984=CARTESIAN_POINT('Ctrl Pts',(138.993737197288,5.55275014432601,135.071127538621));
#193985=CARTESIAN_POINT('Ctrl Pts',(138.715289573475,6.59114893827324,128.438966401494));
#193986=CARTESIAN_POINT('Ctrl Pts',(138.436841949662,1.57260385347371,123.980486993006));
#193987=CARTESIAN_POINT('Ctrl Pts',(138.158394325849,-4.8910873466988,125.792814080728));
#193988=CARTESIAN_POINT('Ctrl Pts',(137.879946702036,-6.86010821815569,
132.210507608145));
#193989=CARTESIAN_POINT('Ctrl Pts',(137.601499078223,-2.52502477204539,
137.336020745319));
#193990=CARTESIAN_POINT('Ctrl Pts',(137.32305145441,4.13043308525698,136.459257314423));
#193991=CARTESIAN_POINT('Ctrl Pts',(137.044603830598,6.99022472008204,130.385920076178));
#193992=CARTESIAN_POINT('Ctrl Pts',(136.766156206785,3.42634132861412,124.69710925351));
#193993=CARTESIAN_POINT('Ctrl Pts',(136.487708582972,-3.28618235777073,
124.620564078594));
#193994=CARTESIAN_POINT('Ctrl Pts',(136.209260959159,-6.97886499629743,
130.226625827737));
#193995=CARTESIAN_POINT('Ctrl Pts',(135.930813335346,-4.25831163973555,
136.363597624819));
#193996=CARTESIAN_POINT('Ctrl Pts',(135.652365711533,2.37542208365453,137.391902196061));
#193997=CARTESIAN_POINT('Ctrl Pts',(135.37391808772,6.82625895798624,132.366577875963));
#193998=CARTESIAN_POINT('Ctrl Pts',(135.095470463907,5.00409733121823,125.905652213954));
#193999=CARTESIAN_POINT('Ctrl Pts',(134.817022840094,-1.4165852791943,123.946400259653));
#194000=CARTESIAN_POINT('Ctrl Pts',(134.538575216282,-6.53549522206528,
128.289278844285));
#194001=CARTESIAN_POINT('Ctrl Pts',(134.260127592469,-5.64860433254967,
134.943394709987));
#194002=CARTESIAN_POINT('Ctrl Pts',(133.981679968656,0.429077988916399,
137.793940447809));
#194003=CARTESIAN_POINT('Ctrl Pts',(133.703232344843,6.1124586001935,134.221403781595));
#194004=CARTESIAN_POINT('Ctrl Pts',(133.42478472103,6.17878836809604,127.508771379477));
#194005=CARTESIAN_POINT('Ctrl Pts',(133.146337097217,0.567113476311158,
123.824624488677));
#194006=CARTESIAN_POINT('Ctrl Pts',(132.867889473404,-5.5657109951702,126.554514121259));
#194007=CARTESIAN_POINT('Ctrl Pts',(132.589441849591,-6.58391896218814,
133.189805067404));
#194008=CARTESIAN_POINT('Ctrl Pts',(132.310994225778,-1.55182704527753,
137.632989099587));
#194009=CARTESIAN_POINT('Ctrl Pts',(132.032546601965,4.90631811527725,135.800997153839));
#194010=CARTESIAN_POINT('Ctrl Pts',(131.754098978153,6.85579661485726,129.377340330521));
#194011=CARTESIAN_POINT('Ctrl Pts',(131.47565135434,2.50513294966777,124.265045437181));
#194012=CARTESIAN_POINT('Ctrl Pts',(131.197203730527,-4.14762551371829,
125.162061731307));
#194013=CARTESIAN_POINT('Ctrl Pts',(130.918756106714,-6.98891875276791,
131.244075060281));
#194014=CARTESIAN_POINT('Ctrl Pts',(130.640308482901,-3.4077370856862,136.922012297644));
#194015=CARTESIAN_POINT('Ctrl Pts',(130.361860859088,3.30498848592948,136.978126504915));
#194016=CARTESIAN_POINT('Ctrl Pts',(130.083413235275,6.98059109663955,131.360851466943));
#194017=CARTESIAN_POINT('Ctrl Pts',(129.804965611462,4.24137151037132,125.232188524482));
#194018=CARTESIAN_POINT('Ctrl Pts',(129.526517987649,-2.39546129141071,
124.224079519825));
#194019=CARTESIAN_POINT('Ctrl Pts',(129.248070363836,-6.83098219117618,
129.262927379388));
#194020=CARTESIAN_POINT('Ctrl Pts',(128.969622740024,-4.98916416928312,
135.718277081636));
#194021=CARTESIAN_POINT('Ctrl Pts',(128.691175116211,1.43745198996158,137.657977611568));
#194022=CARTESIAN_POINT('Ctrl Pts',(128.412727492398,6.54311999386511,133.299538941816));
#194023=CARTESIAN_POINT('Ctrl Pts',(128.134279868585,5.63598037258881,126.648153288314));
#194024=CARTESIAN_POINT('Ctrl Pts',(127.855832244772,-0.450349878148651,
123.81611912838));
#194025=CARTESIAN_POINT('Ctrl Pts',(127.577384620959,-6.12283059168226,
127.40593750243));
#194026=CARTESIAN_POINT('Ctrl Pts',(127.298936997146,-6.16872910836309,
134.118740697091));
#194027=CARTESIAN_POINT('Ctrl Pts',(127.020489373333,-0.545866933628919,
137.785790515136));
#194028=CARTESIAN_POINT('Ctrl Pts',(126.742041749521,5.57862028602806,135.037247319125));
#194029=CARTESIAN_POINT('Ctrl Pts',(126.463594125708,6.57662799357718,128.398888032392));
#194030=CARTESIAN_POINT('Ctrl Pts',(126.185146501895,1.53103586116759,123.971040537565));
#194031=CARTESIAN_POINT('Ctrl Pts',(125.906698878082,-4.92150343239493,
125.822680370014));
#194032=CARTESIAN_POINT('Ctrl Pts',(125.628251254269,-6.85142150039552,
132.252240981353));
#194033=CARTESIAN_POINT('Ctrl Pts',(125.349803630456,-2.48521792008072,
137.351270271259));
#194034=CARTESIAN_POINT('Ctrl Pts',(125.071356006643,4.16477951914341,136.434009423738));
#194035=CARTESIAN_POINT('Ctrl Pts',(124.79290838283,6.98754804106521,130.343376346978));
#194036=CARTESIAN_POINT('Ctrl Pts',(124.514460759018,3.38910127394743,124.676365294554));
#194037=CARTESIAN_POINT('Ctrl Pts',(124.236013135205,-3.32376399712637,
124.640682574762));
#194038=CARTESIAN_POINT('Ctrl Pts',(123.957565511392,-6.98225252973936,
130.269118863895));
#194039=CARTESIAN_POINT('Ctrl Pts',(123.679117887579,-4.22439208952083,
136.389416176637));
#194040=CARTESIAN_POINT('Ctrl Pts',(123.400670263766,2.41547830794073,137.377320275725));
#194041=CARTESIAN_POINT('Ctrl Pts',(123.122222639953,6.83564214308024,132.324995555895));
#194042=CARTESIAN_POINT('Ctrl Pts',(122.84377501614,4.97418478841272,125.875281614887));
#194043=CARTESIAN_POINT('Ctrl Pts',(122.565327392328,-1.45830538437,123.955150478444));
#194044=CARTESIAN_POINT('Ctrl Pts',(122.286879768514,-6.55068415109515,
128.329108857337));
#194045=CARTESIAN_POINT('Ctrl Pts',(122.008432144702,-5.62330420167569,
134.977702681109));
#194046=CARTESIAN_POINT('Ctrl Pts',(121.729984520888,0.471617595401148,
137.791199027578));
#194047=CARTESIAN_POINT('Ctrl Pts',(121.451536897076,6.13314586210485,134.184132201278));
#194048=CARTESIAN_POINT('Ctrl Pts',(121.173089273263,6.15861270236637,127.471220400567));
#194049=CARTESIAN_POINT('Ctrl Pts',(120.89464164945,0.52461533410983,123.821301626325));
#194050=CARTESIAN_POINT('Ctrl Pts',(120.616194025637,-5.5914778973097,126.588472923636));
#194051=CARTESIAN_POINT('Ctrl Pts',(120.337746401824,-6.56927609998288,
133.229839054105));
#194052=CARTESIAN_POINT('Ctrl Pts',(120.059298778011,-1.51023049375061,
137.642308992603));
#194053=CARTESIAN_POINT('Ctrl Pts',(119.780851154198,4.93664315737715,135.77103842679));
#194054=CARTESIAN_POINT('Ctrl Pts',(119.502403530385,6.84698291530094,129.33563359));
#194055=CARTESIAN_POINT('Ctrl Pts',(119.223955906573,2.46527986777437,124.249917140239));
#194056=CARTESIAN_POINT('Ctrl Pts',(118.94550828276,-4.18189494262004,125.187414043775));
#194057=CARTESIAN_POINT('Ctrl Pts',(118.667060658947,-6.98611259767199,
131.28661044553));
#194058=CARTESIAN_POINT('Ctrl Pts',(118.388613035134,-3.37043406603744,
136.942642814599));
#194059=CARTESIAN_POINT('Ctrl Pts',(118.110165411321,3.34250871742766,136.95789371635));
#194060=CARTESIAN_POINT('Ctrl Pts',(117.831717787508,6.98384928020556,131.318348317123));
#194061=CARTESIAN_POINT('Ctrl Pts',(117.553270163695,4.20737353447909,125.206473331696));
#194062=CARTESIAN_POINT('Ctrl Pts',(117.274822539882,-2.43547294780967,
124.238783289987));
#194063=CARTESIAN_POINT('Ctrl Pts',(116.99637491607,-6.84023877052931,129.304538066038));
#194064=CARTESIAN_POINT('Ctrl Pts',(116.717927292256,-4.95915932737393,
135.748556496538));
#194065=CARTESIAN_POINT('Ctrl Pts',(116.439479668444,1.47914526923655,137.649100451659));
#194066=CARTESIAN_POINT('Ctrl Pts',(116.161032044631,6.55818762368211,133.259662883379));
#194067=CARTESIAN_POINT('Ctrl Pts',(115.882584420818,5.61057593724064,126.613922481));
#194068=CARTESIAN_POINT('Ctrl Pts',(115.604136797005,-0.49288094365267,
123.818990011842));
#194069=CARTESIAN_POINT('Ctrl Pts',(115.325689173192,-6.14340431590201,
127.443271875017));
#194070=CARTESIAN_POINT('Ctrl Pts',(115.047241549379,-6.14843924382291,
134.156230094282));
#194071=CARTESIAN_POINT('Ctrl Pts',(114.768793925566,-0.5033588746261,137.78898401237));
#194072=CARTESIAN_POINT('Ctrl Pts',(114.490346301753,5.60428370990391,135.003210248456));
#194073=CARTESIAN_POINT('Ctrl Pts',(114.211898677941,6.56186334951224,128.358898798961));
#194074=CARTESIAN_POINT('Ctrl Pts',(113.933451054127,1.48941113576461,123.961847293312));
#194075=CARTESIAN_POINT('Ctrl Pts',(113.655003430315,-4.95173714997151,
125.852731257293));
#194076=CARTESIAN_POINT('Ctrl Pts',(113.376555806502,-6.84248090069202,
132.293920702821));
#194077=CARTESIAN_POINT('Ctrl Pts',(113.098108182689,-2.4453189774521,137.366277199056));
#194078=CARTESIAN_POINT('Ctrl Pts',(112.819660558876,4.19897162559319,136.408552924347));
#194079=CARTESIAN_POINT('Ctrl Pts',(112.541212935063,6.98461243588604,130.300849699721));
#194080=CARTESIAN_POINT('Ctrl Pts',(112.26276531125,3.35173563488669,124.655848410718));
#194081=CARTESIAN_POINT('Ctrl Pts',(111.984317687437,-3.3612224731848,124.661029468288));
#194082=CARTESIAN_POINT('Ctrl Pts',(111.705870063624,-6.98538133324609,
130.311631733633));
#194083=CARTESIAN_POINT('Ctrl Pts',(111.427422439812,-4.1903160029037,136.415027772168));
#194084=CARTESIAN_POINT('Ctrl Pts',(111.148974815999,2.45544502578993,137.362494791951));
#194085=CARTESIAN_POINT('Ctrl Pts',(110.870527192186,6.84477203094083,132.28335688814));
#194086=CARTESIAN_POINT('Ctrl Pts',(110.592079568373,4.94408792536061,125.845093664656));
#194087=CARTESIAN_POINT('Ctrl Pts',(110.31363194456,-1.49997145150339,123.964154497236));
#194088=CARTESIAN_POINT('Ctrl Pts',(110.035184320747,-6.56563034211481,
128.369030591753));
#194089=CARTESIAN_POINT('Ctrl Pts',(109.756736696934,-5.59779569719655,
135.011856007506));
#194090=CARTESIAN_POINT('Ctrl Pts',(109.478289073121,0.514139725922464,
137.788198707481));
#194091=CARTESIAN_POINT('Ctrl Pts',(109.199841449309,6.15360585804082,134.146735382281));
#194092=CARTESIAN_POINT('Ctrl Pts',(108.921393825496,6.13820882697821,127.433792932393));
#194093=CARTESIAN_POINT('Ctrl Pts',(108.642946201683,0.482097752094529,
123.818237523792));
#194094=CARTESIAN_POINT('Ctrl Pts',(108.36449857787,-5.61703760517944,126.622587947283));
#194095=CARTESIAN_POINT('Ctrl Pts',(108.086050954057,-6.5543898108359,133.26978316381));
#194096=CARTESIAN_POINT('Ctrl Pts',(107.807603330244,-1.46857798007734,
137.651375502926));
#194097=CARTESIAN_POINT('Ctrl Pts',(107.529155706431,4.96678527034939,135.740895657668));
#194098=CARTESIAN_POINT('Ctrl Pts',(107.250708082618,6.83791549827476,129.2939812737));
#194099=CARTESIAN_POINT('Ctrl Pts',(106.972260458805,2.42533543402888,124.23503172061));
#194100=CARTESIAN_POINT('Ctrl Pts',(106.693812834992,-4.21600940986681,
125.212974494265));
#194101=CARTESIAN_POINT('Ctrl Pts',(106.415365211179,-6.98304756960462,
131.329127960835));
#194102=CARTESIAN_POINT('Ctrl Pts',(106.136917587367,-3.33300615371489,
136.96304587525));
#194103=CARTESIAN_POINT('Ctrl Pts',(105.858469963554,3.37990509103613,136.937432906355));
#194104=CARTESIAN_POINT('Ctrl Pts',(105.580022339741,6.98684867466819,131.275826121299));
#194105=CARTESIAN_POINT('Ctrl Pts',(105.301574715928,4.1732196528133,125.180965570684));
#194106=CARTESIAN_POINT('Ctrl Pts',(105.023127092115,-2.4753943568629,124.253730350031));
#194107=CARTESIAN_POINT('Ctrl Pts',(104.744679468302,-6.84924188231931,
129.346204329164));
#194108=CARTESIAN_POINT('Ctrl Pts',(104.466231844489,-4.92897072199215,
135.778652702442));
#194109=CARTESIAN_POINT('Ctrl Pts',(104.187784220676,1.52078373823962,137.639969657397));
#194110=CARTESIAN_POINT('Ctrl Pts',(103.909336596864,6.57301223744494,133.219695842813));
#194111=CARTESIAN_POINT('Ctrl Pts',(103.63088897305,5.58496359993783,126.579846951912));
#194112=CARTESIAN_POINT('Ctrl Pts',(103.352441349238,-0.535393745272065,
123.82211974078));
#194113=CARTESIAN_POINT('Ctrl Pts',(103.073993725425,-6.1637503940156,127.480730793984));
#194114=CARTESIAN_POINT('Ctrl Pts',(102.795546101612,-6.12792154660547,
134.193595286717));
#194115=CARTESIAN_POINT('Ctrl Pts',(102.517098477799,-0.460832163475232,
137.791918691816));
#194116=CARTESIAN_POINT('Ctrl Pts',(102.238650853986,5.6297394649859,134.96901758787));
#194117=CARTESIAN_POINT('Ctrl Pts',(101.960203230173,6.54685555318778,128.319000183017));
#194118=CARTESIAN_POINT('Ctrl Pts',(101.68175560636,1.44773121968427,123.952907600908));
#194119=CARTESIAN_POINT('Ctrl Pts',(101.403307982548,-4.981787379107,125.882965629019));
#194120=CARTESIAN_POINT('Ctrl Pts',(101.124860358735,-6.83328675034245,
132.335545228093));
#194121=CARTESIAN_POINT('Ctrl Pts',(100.846412734922,-2.4053294226295,137.38104097262));
#194122=CARTESIAN_POINT('Ctrl Pts',(100.567965111109,4.23300813760519,136.382888759548));
#194123=CARTESIAN_POINT('Ctrl Pts',(100.289517487296,6.98141801332452,130.258341710245));
#194124=CARTESIAN_POINT('Ctrl Pts',(100.011069863483,3.31424579602927,124.635559362262));
#194125=CARTESIAN_POINT('Ctrl Pts',(99.7326222396699,-3.39855639790849,
124.681604005209));
#194126=CARTESIAN_POINT('Ctrl Pts',(99.4541746158571,-6.98825129087862,
130.354162861621));
#194127=CARTESIAN_POINT('Ctrl Pts',(99.1757269920442,-4.15608464258612,
136.440431462363));
#194128=CARTESIAN_POINT('Ctrl Pts',(98.8972793682313,2.49532075622072,137.347426294104));
#194129=CARTESIAN_POINT('Ctrl Pts',(98.6188317444184,6.85364828325664,132.241663415635));
#194130=CARTESIAN_POINT('Ctrl Pts',(98.3403841206056,4.91380785731226,125.815089481885));
#194131=CARTESIAN_POINT('Ctrl Pts',(98.0619364967926,-1.54158193664305,
123.97341198238));
#194132=CARTESIAN_POINT('Ctrl Pts',(97.7834888729798,-6.58033324128762,
128.409042568218));
#194133=CARTESIAN_POINT('Ctrl Pts',(97.5050412491668,-5.57207976433927,
135.045853423614));
#194134=CARTESIAN_POINT('Ctrl Pts',(97.226593625354,0.55664280480716,137.784939598694));
#194135=CARTESIAN_POINT('Ctrl Pts',(96.948146001541,6.17383782984873,134.109214710358));
#194136=CARTESIAN_POINT('Ctrl Pts',(96.6696983777281,6.11757749800464,127.396490361844));
#194137=CARTESIAN_POINT('Ctrl Pts',(96.3912507539153,0.43956230576973,123.815432294619));
#194138=CARTESIAN_POINT('Ctrl Pts',(96.1128031301024,-5.64238917165504,
126.656857928054));
#194139=CARTESIAN_POINT('Ctrl Pts',(95.8343555062895,-6.53926064636413,
133.309635916377));
#194140=CARTESIAN_POINT('Ctrl Pts',(95.5559078824767,-1.42687104770695,
137.660188294596));
#194141=CARTESIAN_POINT('Ctrl Pts',(95.2774602586637,4.99674333726689,135.710569963425));
#194142=CARTESIAN_POINT('Ctrl Pts',(94.9990126348508,6.82859469977515,129.252384925061));
#194143=CARTESIAN_POINT('Ctrl Pts',(94.720565011038,2.38530112858694,124.22038972988));
#194144=CARTESIAN_POINT('Ctrl Pts',(94.442117387225,-4.24996765133445,125.238742135624));
#194145=CARTESIAN_POINT('Ctrl Pts',(94.1636697634123,-6.97972378214161,
131.371626030693));
#194146=CARTESIAN_POINT('Ctrl Pts',(93.885222139599,-3.29545473562348,136.983220723554));
#194147=CARTESIAN_POINT('Ctrl Pts',(93.6067745157866,3.41717622101856,136.91674483311));
#194148=CARTESIAN_POINT('Ctrl Pts',(93.3283268919733,6.98958916888377,131.233286455149));
#194149=CARTESIAN_POINT('Ctrl Pts',(93.0498792681607,4.13891113095855,125.155666186642));
#194150=CARTESIAN_POINT('Ctrl Pts',(92.7714316443476,-2.51522403926791,
124.268920146089));
#194151=CARTESIAN_POINT('Ctrl Pts',(92.4929840205349,-6.85799119293255,
129.387924624807));
#194152=CARTESIAN_POINT('Ctrl Pts',(92.2145363967218,-4.89859947178764,
135.808564584124));
#194153=CARTESIAN_POINT('Ctrl Pts',(91.9360887729091,1.562365854042,137.63058556713));
#194154=CARTESIAN_POINT('Ctrl Pts',(91.6576411490961,6.58759328582208,133.179639301113));
#194155=CARTESIAN_POINT('Ctrl Pts',(91.3791935252832,5.55914430975498,126.545927963732));
#194156=CARTESIAN_POINT('Ctrl Pts',(91.1007459014705,-0.57788670767935,
123.825508199223));
#194157=CARTESIAN_POINT('Ctrl Pts',(90.8222982776573,-6.18386807209161,
127.518312871276));
#194158=CARTESIAN_POINT('Ctrl Pts',(90.5438506538447,-6.10717677700159,
134.230834889814));
#194159=CARTESIAN_POINT('Ctrl Pts',(90.2654030300316,-0.41828837601907,
137.794594444728));
#194160=CARTESIAN_POINT('Ctrl Pts',(89.9869554062187,5.65498660800168,134.934670604388));
#194161=CARTESIAN_POINT('Ctrl Pts',(89.708507782406,6.53160516072318,128.279193663018));
#194162=CARTESIAN_POINT('Ctrl Pts',(89.430060158593,1.40599765739116,123.944221791613));
#194163=CARTESIAN_POINT('Ctrl Pts',(89.1516125347801,-5.01165300627911,
125.913382364846));
#194164=CARTESIAN_POINT('Ctrl Pts',(88.8731649109673,-6.82383939003939,
132.377113014756));
#194165=CARTESIAN_POINT('Ctrl Pts',(88.5947172871542,-2.36525073744058,
137.395561044874));
#194166=CARTESIAN_POINT('Ctrl Pts',(88.3162696633415,4.26688779394398,136.357017880338));
#194167=CARTESIAN_POINT('Ctrl Pts',(88.0378220395285,6.97796489175107,130.2158539537));
#194168=CARTESIAN_POINT('Ctrl Pts',(87.7593744157156,3.2766331465752,124.615498901007));
#194169=CARTESIAN_POINT('Ctrl Pts',(87.4809267919028,-3.43576438787495,
124.702405423128));
#194170=CARTESIAN_POINT('Ctrl Pts',(87.2024791680898,-6.99086229628967,
130.396710671853));
#194171=CARTESIAN_POINT('Ctrl Pts',(86.924031544277,-4.1216992770237,136.465626305881));
#194172=CARTESIAN_POINT('Ctrl Pts',(86.6455839204641,2.53510402162323,137.332115340552));
#194173=CARTESIAN_POINT('Ctrl Pts',(86.3671362966513,6.8622705711149,132.199916683345));
#194174=CARTESIAN_POINT('Ctrl Pts',(86.0886886728382,4.88334570630671,125.785270178391));
#194175=CARTESIAN_POINT('Ctrl Pts',(85.8102410490255,-1.58313529789712,
123.982922590838));
#194176=CARTESIAN_POINT('Ctrl Pts',(85.5317934252125,-6.59479230379227,
128.449143304076));
#194177=CARTESIAN_POINT('Ctrl Pts',(85.2533458013996,-5.5461573560172,135.079693669646));
#194178=CARTESIAN_POINT('Ctrl Pts',(84.9748981775869,0.599125257088023,
137.781421821987));
#194179=CARTESIAN_POINT('Ctrl Pts',(84.6964505537737,6.19384102782544,134.071571575853));
#194180=CARTESIAN_POINT('Ctrl Pts',(84.418002929961,6.09671947994716,127.359314071181));
#194181=CARTESIAN_POINT('Ctrl Pts',(84.1395553061481,0.397010571302045,
123.812886042756));
#194182=CARTESIAN_POINT('Ctrl Pts',(83.8611076823352,-5.66753165732491,
126.691281596061));
#194183=CARTESIAN_POINT('Ctrl Pts',(83.5826600585222,-6.52388916718428,
133.349395835046));
#194184=CARTESIAN_POINT('Ctrl Pts',(83.3042124347095,-1.38511124210516,
137.66874704105));
#194185=CARTESIAN_POINT('Ctrl Pts',(83.0257648108964,5.02651624802251,135.68006246779));
#194186=CARTESIAN_POINT('Ctrl Pts',(82.7473171870836,6.81902086518772,129.210846085452));
#194187=CARTESIAN_POINT('Ctrl Pts',(82.4688695632707,2.34517843493451,124.205991710613));
#194188=CARTESIAN_POINT('Ctrl Pts',(82.1904219394578,-4.28376840868787,
125.264716013022));
#194189=CARTESIAN_POINT('Ctrl Pts',(81.9119743156449,-6.97614135844701,
131.414103080323));
#194190=CARTESIAN_POINT('Ctrl Pts',(81.6335266918322,-3.25778120324508,
137.003166611925));
#194191=CARTESIAN_POINT('Ctrl Pts',(81.355079068019,3.45432072627939,136.895830263219));
#194192=CARTESIAN_POINT('Ctrl Pts',(81.0766314442065,6.99207066130227,131.190730894994));
#194193=CARTESIAN_POINT('Ctrl Pts',(80.7981838203932,4.10444924022979,125.130576117049));
#194194=CARTESIAN_POINT('Ctrl Pts',(80.5197361965806,-2.55496051912119,
124.284352115297));
#194195=CARTESIAN_POINT('Ctrl Pts',(80.2412885727675,-6.86648637816013,
129.429697407007));
#194196=CARTESIAN_POINT('Ctrl Pts',(79.9628409489547,-4.86804670217826,
135.838291033188));
#194197=CARTESIAN_POINT('Ctrl Pts',(79.6843933251418,1.6038900758031,137.620948528586));
#194198=CARTESIAN_POINT('Ctrl Pts',(79.405945701329,6.60193022850756,133.139494742587));
#194199=CARTESIAN_POINT('Ctrl Pts',(79.1274980775159,5.53311902343524,126.512166773338));
#194200=CARTESIAN_POINT('Ctrl Pts',(78.8490504537032,-0.620358256282274,
123.829155261608));
#194201=CARTESIAN_POINT('Ctrl Pts',(78.5706028298902,-6.2037566046621,127.556016714277));
#194202=CARTESIAN_POINT('Ctrl Pts',(78.2921552060774,-6.08620570371632,
134.267947523646));
#194203=CARTESIAN_POINT('Ctrl Pts',(78.0137075822645,-0.375729088733312,
137.797011171955));
#194204=CARTESIAN_POINT('Ctrl Pts',(77.7352599584516,5.68002420340909,134.90017057075));
#194205=CARTESIAN_POINT('Ctrl Pts',(77.4568123346387,6.51611273722737,128.23948071401));
#194206=CARTESIAN_POINT('Ctrl Pts',(77.1783647108257,1.36421199533782,123.935790187287));
#194207=CARTESIAN_POINT('Ctrl Pts',(76.8999170870129,-5.04133292480603,
125.94398033767));
#194208=CARTESIAN_POINT('Ctrl Pts',(76.6214694632,-6.81413916985829,132.418622522501));
#194209=CARTESIAN_POINT('Ctrl Pts',(76.3430218393871,-2.32508440701577,
137.409836877774));
#194210=CARTESIAN_POINT('Ctrl Pts',(76.0645742155741,4.30060933918641,136.33094124537));
#194211=CARTESIAN_POINT('Ctrl Pts',(75.7861265917614,6.97425319912241,130.173388004487));
#194212=CARTESIAN_POINT('Ctrl Pts',(75.5076789679483,3.23889908027492,124.595667770297));
#194213=CARTESIAN_POINT('Ctrl Pts',(75.2292313441357,-3.47284506432852,
124.72343295124));
#194214=CARTESIAN_POINT('Ctrl Pts',(74.9507837203226,-6.99321425272744,
130.439273587703));
#194215=CARTESIAN_POINT('Ctrl Pts',(74.6723360965098,-4.08716118037883,
136.490611369118));
#194216=CARTESIAN_POINT('Ctrl Pts',(74.3938884726969,2.57479334781394,137.316562498648));
#194217=CARTESIAN_POINT('Ctrl Pts',(74.1154408488841,6.87063857501356,132.158118238212));
#194218=CARTESIAN_POINT('Ctrl Pts',(73.836993225071,4.85270260113016,125.755636859138));
#194219=CARTESIAN_POINT('Ctrl Pts',(73.5585456012583,-1.62462999549052,
123.992685970191));
#194220=CARTESIAN_POINT('Ctrl Pts',(73.2800979774453,-6.60900699384299,
128.489331313375));
#194221=CARTESIAN_POINT('Ctrl Pts',(73.0016503536324,-5.52002943279461,
135.113375491641));
#194222=CARTESIAN_POINT('Ctrl Pts',(72.7232027298196,0.641585508562261,
137.777645507711));
#194223=CARTESIAN_POINT('Ctrl Pts',(72.4447551060067,6.21361471074508,134.033807373642));
#194224=CARTESIAN_POINT('Ctrl Pts',(72.1663074821937,6.07563554570727,127.322265437984));
#194225=CARTESIAN_POINT('Ctrl Pts',(71.8878598583809,0.354444125461637,
123.810598862555));
#194226=CARTESIAN_POINT('Ctrl Pts',(71.609412234568,-5.69246413052499,126.725857675724));
#194227=CARTESIAN_POINT('Ctrl Pts',(71.330964610755,-6.5082759428922,133.3890614465));
#194228=CARTESIAN_POINT('Ctrl Pts',(71.0525169869423,-1.34330011069692,
137.677051425141));
#194229=CARTESIAN_POINT('Ctrl Pts',(70.7740693631292,5.05610289937005,135.649374301231));
#194230=CARTESIAN_POINT('Ctrl Pts',(70.4956217393166,6.80919434927445,129.16936629411));
#194231=CARTESIAN_POINT('Ctrl Pts',(70.2171741155033,2.30496883983272,124.191838196331));
#194232=CARTESIAN_POINT('Ctrl Pts',(69.9387264916908,-4.31741042942741,
125.290895163988));
#194233=CARTESIAN_POINT('Ctrl Pts',(69.6602788678776,-6.97230043126892,
131.456557535721));
#194234=CARTESIAN_POINT('Ctrl Pts',(69.3818312440649,-3.21998695258627,
137.02288280126));
#194235=CARTESIAN_POINT('Ctrl Pts',(69.1033836202519,3.49133723041524,136.874689971681));
#194236=CARTESIAN_POINT('Ctrl Pts',(68.8249359964391,6.9942930599711,131.148161017746));
#194237=CARTESIAN_POINT('Ctrl Pts',(68.5464883726262,4.0698352576252,125.105696291628));
#194238=CARTESIAN_POINT('Ctrl Pts',(68.2680407488133,-2.59460232397255,
124.300025685817));
#194239=CARTESIAN_POINT('Ctrl Pts',(67.9895931250004,-6.87472712320984,
129.471521127857));
#194240=CARTESIAN_POINT('Ctrl Pts',(67.7111455011875,-4.83731354530826,
135.867830948109));
#194241=CARTESIAN_POINT('Ctrl Pts',(67.4326978773747,1.64535486482719,137.61105889887));
#194242=CARTESIAN_POINT('Ctrl Pts',(67.1542502535617,6.61602253424027,133.099263654809));
#194243=CARTESIAN_POINT('Ctrl Pts',(66.8758026297489,5.50688870535577,126.478564631767));
#194244=CARTESIAN_POINT('Ctrl Pts',(66.5973550059358,-0.662806817281494,
123.833060792792));
#194245=CARTESIAN_POINT('Ctrl Pts',(66.3189073821232,-6.22341525475008,
127.593840925854));
#194246=CARTESIAN_POINT('Ctrl Pts',(66.0404597583101,-6.0650091038406,134.304931812993));
#194247=CARTESIAN_POINT('Ctrl Pts',(65.7620121344974,-0.333155878668442,
137.799168783944));
#194248=CARTESIAN_POINT('Ctrl Pts',(65.4835645106842,5.70485132343066,134.865518765369));
#194249=CARTESIAN_POINT('Ctrl Pts',(65.2051168868716,6.50037885677781,128.199862807569));
#194250=CARTESIAN_POINT('Ctrl Pts',(64.9266692630585,1.32237578190785,123.927613100363));
#194251=CARTESIAN_POINT('Ctrl Pts',(64.6482216392459,-5.07082603488719,
125.974758413674));
#194252=CARTESIAN_POINT('Ctrl Pts',(64.3697740154327,-6.80418644924447,
132.460072213177));
#194253=CARTESIAN_POINT('Ctrl Pts',(64.09132639162,-2.28483191973344,137.423867942321));
#194254=CARTESIAN_POINT('Ctrl Pts',(63.812878767807,4.33417152376786,136.304659820925));
#194255=CARTESIAN_POINT('Ctrl Pts',(63.5344311439942,6.97028307297671,130.130945436197));
#194256=CARTESIAN_POINT('Ctrl Pts',(63.2559835201813,3.20104499537862,124.576066704985));
#194257=CARTESIAN_POINT('Ctrl Pts',(62.9775358963684,-3.5097970532309,124.744685810362));
#194258=CARTESIAN_POINT('Ctrl Pts',(62.6990882725555,-6.9953070730393,130.481850031987));
#194259=CARTESIAN_POINT('Ctrl Pts',(62.4206406487427,-4.05247163247362,
136.51538572624));
#194260=CARTESIAN_POINT('Ctrl Pts',(62.1421930249296,2.61438726408988,137.300768344709));
#194261=CARTESIAN_POINT('Ctrl Pts',(61.8637454011169,6.87875198487314,132.116269629093));
#194262=CARTESIAN_POINT('Ctrl Pts',(61.5852977773038,4.82187967727427,125.726190622201));
#194263=CARTESIAN_POINT('Ctrl Pts',(61.3068501534911,-1.66606449182178,
124.002701758653));
#194264=CARTESIAN_POINT('Ctrl Pts',(61.0284025296781,-6.62297678470872,
128.529605106938));
#194265=CARTESIAN_POINT('Ctrl Pts',(60.7499549058653,-5.49369696285183,
135.146897641504));
#194266=CARTESIAN_POINT('Ctrl Pts',(60.4715072820523,0.684021985849089,
137.773610795799));
#194267=CARTESIAN_POINT('Ctrl Pts',(60.1930596582395,6.23315814588628,133.995923503096));
#194268=CARTESIAN_POINT('Ctrl Pts',(59.9146120344266,6.05432647655821,127.285345835106));
#194269=CARTESIAN_POINT('Ctrl Pts',(59.6361644106137,0.311864545564345,
123.808570838767));
#194270=CARTESIAN_POINT('Ctrl Pts',(59.3577167868007,-5.71718566737322,
126.760584885814));
#194271=CARTESIAN_POINT('Ctrl Pts',(59.0792691629879,-6.49242155204172,
133.428631280914));
#194272=CARTESIAN_POINT('Ctrl Pts',(58.800821539175,-1.30143920280946,137.685101139145));
#194273=CARTESIAN_POINT('Ctrl Pts',(58.5223739153621,5.08550219496502,135.618506600908));
#194274=CARTESIAN_POINT('Ctrl Pts',(58.2439262915492,6.79911551616065,129.127947088084));
#194275=CARTESIAN_POINT('Ctrl Pts',(57.9654786677363,2.26467383326308,124.1779297115));
#194276=CARTESIAN_POINT('Ctrl Pts',(57.6870310439234,-4.35089246693584,
125.317278618444));
#194277=CARTESIAN_POINT('Ctrl Pts',(57.4085834201106,-6.96820114293417,
131.498987823723));
#194278=CARTESIAN_POINT('Ctrl Pts',(57.1301357962976,-3.18207338412696,
137.042368560968));
#194279=CARTESIAN_POINT('Ctrl Pts',(56.8516881724848,3.52822436176609,136.853324741857));
#194280=CARTESIAN_POINT('Ctrl Pts',(56.5732405486719,6.9962562825383,131.105578400848));
#194281=CARTESIAN_POINT('Ctrl Pts',(56.294792924859,4.03507046577855,125.081027632309));
#194282=CARTESIAN_POINT('Ctrl Pts',(56.0163453010462,-2.63414798488075,
124.315940276861));
#194283=CARTESIAN_POINT('Ctrl Pts',(55.7378976772331,-6.8827131227178,129.513394237565));
#194284=CARTESIAN_POINT('Ctrl Pts',(55.4594500534204,-4.80640114000575,
135.897183234276));
#194285=CARTESIAN_POINT('Ctrl Pts',(55.1810024296073,1.68675868462211,137.600917044446));
#194286=CARTESIAN_POINT('Ctrl Pts',(54.9025548057946,6.62986968082513,133.058947528554));
#194287=CARTESIAN_POINT('Ctrl Pts',(54.6241071819816,5.4804543274898,126.445122784157));
#194288=CARTESIAN_POINT('Ctrl Pts',(54.3456595581689,-0.705230817730614,
123.837224648055));
#194289=CARTESIAN_POINT('Ctrl Pts',(54.0672119343557,-6.24284329389726,
127.63178410442));
#194290=CARTESIAN_POINT('Ctrl Pts',(53.7887643105431,-6.04358776282204,
134.341786387386));
#194291=CARTESIAN_POINT('Ctrl Pts',(53.51031668673,-0.290570323389535,137.801067200743));
#194292=CARTESIAN_POINT('Ctrl Pts',(53.2318690629172,5.72946704808866,134.830716472279));
#194293=CARTESIAN_POINT('Ctrl Pts',(52.9534214391043,6.48440410239917,128.160341411752));
#194294=CARTESIAN_POINT('Ctrl Pts',(52.6749738152913,1.28049056735643,123.919690833848));
#194295=CARTESIAN_POINT('Ctrl Pts',(52.3965261914786,-5.10013124364513,
126.005715452363));
#194296=CARTESIAN_POINT('Ctrl Pts',(52.1180785676656,-6.79398159699943,
132.501460550851));
#194297=CARTESIAN_POINT('Ctrl Pts',(51.8396309438527,-2.24449476716385,
137.43765371859));
#194298=CARTESIAN_POINT('Ctrl Pts',(51.5611833200399,4.36757310402998,136.278174580871));
#194299=CARTESIAN_POINT('Ctrl Pts',(51.2827356962269,6.96605466042841,130.088527821552));
#194300=CARTESIAN_POINT('Ctrl Pts',(51.0042880724141,3.16307229458231,124.556696431394));
#194301=CARTESIAN_POINT('Ctrl Pts',(50.7258404486012,-3.54661898531293,
124.766163212963));
#194302=CARTESIAN_POINT('Ctrl Pts',(50.4473928247883,-6.99714067967511,
130.52443842702));
#194303=CARTESIAN_POINT('Ctrl Pts',(50.1689452009753,-4.0176319187415,136.539948459229));
#194304=CARTESIAN_POINT('Ctrl Pts',(49.8904975771625,2.65388430328469,137.284733463992));
#194305=CARTESIAN_POINT('Ctrl Pts',(49.6120499533496,6.88661050004828,132.074372406703));
#194306=CARTESIAN_POINT('Ctrl Pts',(49.3336023295367,4.79087807689359,125.696932558722));
#194307=CARTESIAN_POINT('Ctrl Pts',(49.0551547057238,-1.7074372515208,124.012969585086));
#194308=CARTESIAN_POINT('Ctrl Pts',(48.776707081911,-6.63670115873435,128.569963192402));
#194309=CARTESIAN_POINT('Ctrl Pts',(48.498259458098,-5.46716092194746,135.180258877061));
#194310=CARTESIAN_POINT('Ctrl Pts',(48.2198118342852,0.72643311645002,137.769317835757));
#194311=CARTESIAN_POINT('Ctrl Pts',(47.9413642104722,6.25247060906043,133.957921368012));
#194312=CARTESIAN_POINT('Ctrl Pts',(47.6629165866595,6.03279306211481,127.248556630613));
#194313=CARTESIAN_POINT('Ctrl Pts',(47.3844689628464,0.269273409411107,
123.806802046542));
#194314=CARTESIAN_POINT('Ctrl Pts',(47.1060213390337,-5.74169535180415,
126.7954619395));
#194315=CARTESIAN_POINT('Ctrl Pts',(46.8275737152206,-6.47632658212296,
133.468103872012));
#194316=CARTESIAN_POINT('Ctrl Pts',(46.5491260914079,-1.25953006961336,
137.69289588478));
#194317=CARTESIAN_POINT('Ctrl Pts',(46.2706784675948,5.11471304540623,135.587460510634));
#194318=CARTESIAN_POINT('Ctrl Pts',(45.9922308437821,6.78878473932087,129.086590002178));
#194319=CARTESIAN_POINT('Ctrl Pts',(45.7137832199691,2.22429490837156,124.164266771503));
#194320=CARTESIAN_POINT('Ctrl Pts',(45.4353355961562,-4.38421328052394,
125.343865398741));
#194321=CARTESIAN_POINT('Ctrl Pts',(45.1568879723434,-6.96384364534361,
131.541392372057));
#194322=CARTESIAN_POINT('Ctrl Pts',(44.8784403485304,-3.1440419027679,137.061623168999));
#194323=CARTESIAN_POINT('Ctrl Pts',(44.5999927247176,3.56498075346585,136.831735365442));
#194324=CARTESIAN_POINT('Ctrl Pts',(44.3215451009046,6.99796025625624,131.062984622213));
#194325=CARTESIAN_POINT('Ctrl Pts',(44.0430974770918,4.00015615291162,125.056571053198));
#194326=CARTESIAN_POINT('Ctrl Pts',(43.7646498532789,-2.67359603646683,
124.332095298706));
#194327=CARTESIAN_POINT('Ctrl Pts',(43.486202229466,-6.8904440807599,129.555315184507));
#194328=CARTESIAN_POINT('Ctrl Pts',(43.2077546056531,-4.77531063174146,
135.926346804027));
#194329=CARTESIAN_POINT('Ctrl Pts',(42.9293069818402,1.72810000095366,137.590523341125));
#194330=CARTESIAN_POINT('Ctrl Pts',(42.6508593580274,6.64347115515083,133.018547857752));
#194331=CARTESIAN_POINT('Ctrl Pts',(42.3724117342144,5.4538168693733,126.411842469708));
#194332=CARTESIAN_POINT('Ctrl Pts',(42.0939641104015,-0.74762868559244,
123.841646673103));
#194333=CARTESIAN_POINT('Ctrl Pts',(41.8155164865887,-6.26204000219037,
127.669844843974));
#194334=CARTESIAN_POINT('Ctrl Pts',(41.5370688627757,-6.02194247443641,
134.378509881167));
#194335=CARTESIAN_POINT('Ctrl Pts',(41.2586212389629,-0.247974000920424,
137.802706352008));
#194336=CARTESIAN_POINT('Ctrl Pts',(40.9801736151499,5.75387046523817,134.795764981093));
#194337=CARTESIAN_POINT('Ctrl Pts',(40.7017259913371,6.46818906604193,128.120917991039));
#194338=CARTESIAN_POINT('Ctrl Pts',(40.4232783675241,1.23855790375582,123.912023681303));
#194339=CARTESIAN_POINT('Ctrl Pts',(40.1448307437113,-5.12924746516435,
126.036850306614));
#194340=CARTESIAN_POINT('Ctrl Pts',(39.8663831198984,-6.78352499126783,
132.542786001862));
#194341=CARTESIAN_POINT('Ctrl Pts',(39.5879354960856,-2.20407444401526,
137.451193695743));
#194342=CARTESIAN_POINT('Ctrl Pts',(39.3094878722726,4.40081284226458,136.251486506627));
#194343=CARTESIAN_POINT('Ctrl Pts',(39.0310402484598,6.96156811816289,130.046136732356));
#194344=CARTESIAN_POINT('Ctrl Pts',(38.7525926246468,3.12498238497894,124.537557667297));
#194345=CARTESIAN_POINT('Ctrl Pts',(38.474145000834,-3.58330949612422,124.78786436319));
#194346=CARTESIAN_POINT('Ctrl Pts',(38.195697377021,-6.9987150046898,130.567037194673));
#194347=CARTESIAN_POINT('Ctrl Pts',(37.9172497532082,-3.98264333018119,
136.564298657899));
#194348=CARTESIAN_POINT('Ctrl Pts',(37.6388021293952,2.69328300182069,137.268458450676));
#194349=CARTESIAN_POINT('Ctrl Pts',(37.3603545055824,6.89421382933879,132.032428123559));
#194350=CARTESIAN_POINT('Ctrl Pts',(37.0819068817695,4.7596989487639,125.667863752866));
#194351=CARTESIAN_POINT('Ctrl Pts',(36.8034592579566,-1.74874674150458,
124.02348906901));
#194352=CARTESIAN_POINT('Ctrl Pts',(36.5250116341437,-6.65017960735793,
128.610404074285));
#194353=CARTESIAN_POINT('Ctrl Pts',(36.2465640103308,-5.44042229338459,
135.213457962098));
#194354=CARTESIAN_POINT('Ctrl Pts',(35.968116386518,0.768817328804687,137.764766786667));
#194355=CARTESIAN_POINT('Ctrl Pts',(35.689668762705,6.27155138463682,133.919802376575));
#194356=CARTESIAN_POINT('Ctrl Pts',(35.4112211388921,6.01103610030595,127.211899187745));
#194357=CARTESIAN_POINT('Ctrl Pts',(35.1327735150793,0.226672295232647,
123.805292551423));
#194358=CARTESIAN_POINT('Ctrl Pts',(34.8543258912663,-5.76599227560232,
126.830487544402));
#194359=CARTESIAN_POINT('Ctrl Pts',(34.5758782674535,-6.45999162954105,
133.507477757125));
#194360=CARTESIAN_POINT('Ctrl Pts',(34.2974306436406,-1.21757426406734,
137.700435373207));
#194361=CARTESIAN_POINT('Ctrl Pts',(34.0189830198277,5.1437343682746,135.556237180835));
#194362=CARTESIAN_POINT('Ctrl Pts',(33.7405353960148,6.778202401566,129.045296568894));
#194363=CARTESIAN_POINT('Ctrl Pts',(33.4620877722019,2.18383356141425,124.150849882625));
#194364=CARTESIAN_POINT('Ctrl Pts',(33.1836401483891,-4.41737163547663,
125.370654519698));
#194365=CARTESIAN_POINT('Ctrl Pts',(32.9051925245761,-6.95922809996586,
131.58376960941));
#194366=CARTESIAN_POINT('Ctrl Pts',(32.6267449007632,-3.10589391777991,
137.080645911863));
#194367=CARTESIAN_POINT('Ctrl Pts',(32.3482972769504,3.60160504349277,136.80992264244));
#194368=CARTESIAN_POINT('Ctrl Pts',(32.0698496531375,6.99940491798352,131.020381260171));
#194369=CARTESIAN_POINT('Ctrl Pts',(31.7914020293246,3.96509361278713,125.032327460544));
#194370=CARTESIAN_POINT('Ctrl Pts',(31.5129544055117,-2.71294501696876,
124.348490152723));
#194371=CARTESIAN_POINT('Ctrl Pts',(31.2345067816988,-6.89791971086261,
129.597282415287));
#194372=CARTESIAN_POINT('Ctrl Pts',(30.9560591578859,-4.74404317258561,
135.955320576696));
#194373=CARTESIAN_POINT('Ctrl Pts',(30.677611534073,1.76937728190418,137.579878174048));
#194374=CARTESIAN_POINT('Ctrl Pts',(30.3991639102601,6.65682645320975,132.978066139427));
#194375=CARTESIAN_POINT('Ctrl Pts',(30.1207162864473,5.42697731806706,126.378724921634));
#194376=CARTESIAN_POINT('Ctrl Pts',(29.8422686626343,-0.789998849798377,
123.846326704078));
#194377=CARTESIAN_POINT('Ctrl Pts',(29.5638210388214,-6.28100466828836,
127.708021734164));
#194378=CARTESIAN_POINT('Ctrl Pts',(29.2853734150086,-6.00007404075783,
134.415100933532));
#194379=CARTESIAN_POINT('Ctrl Pts',(29.0069257911957,-0.205368489683527,
137.804086176998));
#194380=CARTESIAN_POINT('Ctrl Pts',(28.7284781673828,5.77806067060162,134.760665586949));
#194381=CARTESIAN_POINT('Ctrl Pts',(28.4500305435699,6.45173434856014,128.08159400628));
#194382=CARTESIAN_POINT('Ctrl Pts',(28.171582919757,1.19657934493693,123.904611926838));
#194383=CARTESIAN_POINT('Ctrl Pts',(27.8931352959441,-5.15817362053239,
126.068161822712));
#194384=CARTESIAN_POINT('Ctrl Pts',(27.6146876721312,-6.77281701952304,
132.584047034882));
#194385=CARTESIAN_POINT('Ctrl Pts',(27.3362400483183,-2.16357244807759,
137.464487372053));
#194386=CARTESIAN_POINT('Ctrl Pts',(27.0577924245054,4.4338895067609,136.22459658713));
#194387=CARTESIAN_POINT('Ctrl Pts',(26.7793448006925,6.95682361243065,130.003773739425));
#194388=CARTESIAN_POINT('Ctrl Pts',(26.5008971768797,3.08677667800406,124.518651121888));
#194389=CARTESIAN_POINT('Ctrl Pts',(26.2224495530668,-3.61986722608435,
124.809788456898));
#194390=CARTESIAN_POINT('Ctrl Pts',(25.9440019292538,-7.00002998974624,
130.609644756432));
#194391=CARTESIAN_POINT('Ctrl Pts',(25.665554305441,-3.94750716330764,136.588435419948));
#194392=CARTESIAN_POINT('Ctrl Pts',(25.3871066816281,2.7325818997646,137.251943907838));
#194393=CARTESIAN_POINT('Ctrl Pts',(25.1086590578152,6.90156169100052,131.990438333922));
#194394=CARTESIAN_POINT('Ctrl Pts',(24.8302114340022,4.72834344823931,125.638985281792));
#194395=CARTESIAN_POINT('Ctrl Pts',(24.5517638101894,-1.78999143103474,
124.034259820624));
#194396=CARTESIAN_POINT('Ctrl Pts',(24.2733161863765,-6.66341163113055,
128.650926254035));
#194397=CARTESIAN_POINT('Ctrl Pts',(23.9948685625636,-5.41348206797292,
135.246493666413));
#194398=CARTESIAN_POINT('Ctrl Pts',(23.7164209387507,0.811173052350488,
137.759957817164));
#194399=CARTESIAN_POINT('Ctrl Pts',(23.4379733149379,6.29039976557031,133.881567941299));
#194400=CARTESIAN_POINT('Ctrl Pts',(23.159525691125,5.98905639734383,127.175374864857));
#194401=CARTESIAN_POINT('Ctrl Pts',(22.8810780673121,0.184062781628937,
123.804042409345));
#194402=CARTESIAN_POINT('Ctrl Pts',(22.6026304434992,-5.79007553843628,
126.865660402631));
#194403=CARTESIAN_POINT('Ctrl Pts',(22.3241828196863,-6.44341729959363,
133.546751477239));
#194404=CARTESIAN_POINT('Ctrl Pts',(22.0457351958734,-1.17557334085921,
137.707719325048));
#194405=CARTESIAN_POINT('Ctrl Pts',(21.7672875720605,5.17256508817436,135.524837768503));
#194406=CARTESIAN_POINT('Ctrl Pts',(21.4888399482477,6.76736889502847,129.004068318375));
#194407=CARTESIAN_POINT('Ctrl Pts',(21.2103923244347,2.14329129170119,124.137679542035));
#194408=CARTESIAN_POINT('Ctrl Pts',(20.9319447006219,-4.45036630309889,
125.397644988631));
#194409=CARTESIAN_POINT('Ctrl Pts',(20.6534970768089,-6.95435467783159,
131.626117965476));
#194410=CARTESIAN_POINT('Ctrl Pts',(20.3750494529961,-3.06763084275059,
137.099436084669));
#194411=CARTESIAN_POINT('Ctrl Pts',(20.0966018291831,3.6380958747203,136.787887381128));
#194412=CARTESIAN_POINT('Ctrl Pts',(19.8181542053702,7.00059021418742,130.977769893405));
#194413=CARTESIAN_POINT('Ctrl Pts',(19.5397065815574,3.92988414466092,125.0082977527));
#194414=CARTESIAN_POINT('Ctrl Pts',(19.2612589577445,-2.75219346829522,
124.365124231394));
#194415=CARTESIAN_POINT('Ctrl Pts',(18.9828113339316,-6.90513973601376,
129.639294374793));
#194416=CARTESIAN_POINT('Ctrl Pts',(18.7043637101187,-4.71259992116536,
135.98410347865));
#194417=CARTESIAN_POINT('Ctrl Pts',(18.4259160863058,1.81058899792882,137.568981937677));
#194418=CARTESIAN_POINT('Ctrl Pts',(18.1474684624929,6.6699350801164,132.937503873645));
#194419=CARTESIAN_POINT('Ctrl Pts',(17.86902083868,5.39993666812053,126.345771367118));
#194420=CARTESIAN_POINT('Ctrl Pts',(17.5905732148672,-0.832339740306418,
123.851264567558));
#194421=CARTESIAN_POINT('Ctrl Pts',(17.3121255910542,-6.29973658944851,
127.746313360329));
#194422=CARTESIAN_POINT('Ctrl Pts',(17.0336779672413,-5.97798327212915,
134.451558188587));
#194423=CARTESIAN_POINT('Ctrl Pts',(16.7552303434285,-0.162755368441711,
137.805206624583));
#194424=CARTESIAN_POINT('Ctrl Pts',(16.4767827196156,5.80203676780203,134.72541959047));
#194425=CARTESIAN_POINT('Ctrl Pts',(16.1983350958026,6.43504055968944,128.042370914639));
#194426=CARTESIAN_POINT('Ctrl Pts',(15.9198874719898,1.15455644643036,123.897455845098));
#194427=CARTESIAN_POINT('Ctrl Pts',(15.6414398481769,-5.18690863788001,
126.0996488404));
#194428=CARTESIAN_POINT('Ctrl Pts',(15.362992224364,-6.7618580785529,132.625242120967));
#194429=CARTESIAN_POINT('Ctrl Pts',(15.0845446005511,-2.12299028016722,
137.477534254917));
#194430=CARTESIAN_POINT('Ctrl Pts',(14.8060969767383,4.466801871851,136.197505818795));
#194431=CARTESIAN_POINT('Ctrl Pts',(14.5276493529253,6.95182131904109,129.961440412534));
#194432=CARTESIAN_POINT('Ctrl Pts',(14.2492017291125,3.04845658938423,124.499977495755));
#194433=CARTESIAN_POINT('Ctrl Pts',(13.9707541052995,-3.65629082053323,
124.831934681683));
#194434=CARTESIAN_POINT('Ctrl Pts',(13.6923064814867,-7.00108558611715,
130.652259533458));
#194435=CARTESIAN_POINT('Ctrl Pts',(13.4138588576738,-3.91222472010448,
136.612357850978));
#194436=CARTESIAN_POINT('Ctrl Pts',(13.1354112338608,2.77177954088132,137.23519044743));
#194437=CARTESIAN_POINT('Ctrl Pts',(12.856963610048,6.90865381275575,131.94840459374));
#194438=CARTESIAN_POINT('Ctrl Pts',(12.5785159862351,4.6968127372094,125.6102982156));
#194439=CARTESIAN_POINT('Ctrl Pts',(12.3000683624222,-1.83116979177416,
124.045281440813));
#194440=CARTESIAN_POINT('Ctrl Pts',(12.0216207386093,-6.67639673973472,
128.691528230086));
#194441=CARTESIAN_POINT('Ctrl Pts',(11.7431731147965,-5.38634124399241,
135.279364765853));
#194442=CARTESIAN_POINT('Ctrl Pts',(11.4647254909835,0.853498717580522,
137.75489110545));
#194443=CARTESIAN_POINT('Ctrl Pts',(11.1862778671706,6.30901505342741,133.843219478972));
#194444=CARTESIAN_POINT('Ctrl Pts',(10.9078302433578,5.96685476769427,127.13898501537));
#194445=CARTESIAN_POINT('Ctrl Pts',(10.6293826195448,0.141446447510913,
123.803051666633));
#194446=CARTESIAN_POINT('Ctrl Pts',(10.350934995732,-5.81394424789186,126.900979210845));
#194447=CARTESIAN_POINT('Ctrl Pts',(10.0724873719191,-6.42660420644864,
133.585923577051));
#194448=CARTESIAN_POINT('Ctrl Pts',(9.79403974810624,-1.1335288563486,137.714747470394));
#194449=CARTESIAN_POINT('Ctrl Pts',(9.51559212429333,5.20120413677258,135.493263437154));
#194450=CARTESIAN_POINT('Ctrl Pts',(9.23714450048043,6.75628462114785,128.962906778349));
#194451=CARTESIAN_POINT('Ctrl Pts',(8.95869687666756,2.10266960154115,124.124756237763));
#194452=CARTESIAN_POINT('Ctrl Pts',(8.68024925285465,-4.48319606076117,
125.4248358054));
#194453=CARTESIAN_POINT('Ctrl Pts',(8.40180162904178,-6.94922355952728,
131.66843587102));
#194454=CARTESIAN_POINT('Ctrl Pts',(8.12335400522884,-3.0292540955323,137.117992991138));
#194455=CARTESIAN_POINT('Ctrl Pts',(7.84490638141603,3.67445189496732,136.765630398031));
#194456=CARTESIAN_POINT('Ctrl Pts',(7.56645875760307,7.00151610094645,130.935152100895));
#194457=CARTESIAN_POINT('Ctrl Pts',(7.2880111337902,3.89452905323253,124.984482820099));
#194458=CARTESIAN_POINT('Ctrl Pts',(7.00956350997733,-2.79133993608059,
124.381996918337));
#194459=CARTESIAN_POINT('Ctrl Pts',(6.73111588616443,-6.91210388867261,
129.681349506257));
#194460=CARTESIAN_POINT('Ctrl Pts',(6.45266826235151,-4.68098204262199,
136.012694443327));
#194461=CARTESIAN_POINT('Ctrl Pts',(6.17422063853866,1.85173362191231,137.557835035774));
#194462=CARTESIAN_POINT('Ctrl Pts',(5.89577301472578,6.68279655012581,132.896862563455));
#194463=CARTESIAN_POINT('Ctrl Pts',(5.61732539091285,5.37269592153495,126.312983027266));
#194464=CARTESIAN_POINT('Ctrl Pts',(5.33887776709996,-0.874649788159289,
123.856460080569));
#194465=CARTESIAN_POINT('Ctrl Pts',(5.06043014328709,-6.31823507155263,
127.784718303561));
#194466=CARTESIAN_POINT('Ctrl Pts',(4.7819825194742,-5.95567098713191,134.487880295395));
#194467=CARTESIAN_POINT('Ctrl Pts',(4.50353489566127,-0.120136216239877,
137.806067653244));
#194468=CARTESIAN_POINT('Ctrl Pts',(4.22508727184843,5.82579786839633,134.690028297709));
#194469=CARTESIAN_POINT('Ctrl Pts',(3.94663964803551,6.41810831802433,128.003250169541));
#194470=CARTESIAN_POINT('Ctrl Pts',(3.66819202422262,1.11249076541009,123.890555701254));
#194471=CARTESIAN_POINT('Ctrl Pts',(3.3897444004097,-5.21545145242058,126.131310192911));
#194472=CARTESIAN_POINT('Ctrl Pts',(3.11129677659686,-6.75064857444498,
132.666369733619));
#194473=CARTESIAN_POINT('Ctrl Pts',(2.83284915278395,-2.08232944407128,
137.490333860877));
#194474=CARTESIAN_POINT('Ctrl Pts',(2.55440152897106,4.49954871795507,136.170215205482));
#194475=CARTESIAN_POINT('Ctrl Pts',(2.27595390515816,6.94656142335602,129.919138320362));
#194476=CARTESIAN_POINT('Ctrl Pts',(1.9975062813453,3.01002353908442,124.481537480858));
#194477=CARTESIAN_POINT('Ctrl Pts',(1.71905865753238,-3.69257892978116,
124.854302216906));
#194478=CARTESIAN_POINT('Ctrl Pts',(1.44061103371947,-7.00188175468703,
130.694879946647));
#194479=CARTESIAN_POINT('Ctrl Pts',(1.16216340990662,-3.87679730797559,
136.636065064534));
#194480=CARTESIAN_POINT('Ctrl Pts',(0.883715786093727,2.81087447268782,
137.218198690258));
#194481=CARTESIAN_POINT('Ctrl Pts',(0.605268162280799,6.91548993180329,
131.906328460586));
#194482=CARTESIAN_POINT('Ctrl Pts',(0.326820538467947,4.66510798405627,
125.5818036173));
#194483=CARTESIAN_POINT('Ctrl Pts',(0.0483729146550416,-1.87228029784353,
124.056553521165));
#194484=CARTESIAN_POINT('Ctrl Pts',(-0.23007470915786,-6.68913445200245,
128.732208497919));
#194485=CARTESIAN_POINT('Ctrl Pts',(-0.508522332970751,-5.35900082715629,
135.312070042369));
#194486=CARTESIAN_POINT('Ctrl Pts',(-0.786969956783612,0.895792756101716,
137.749566839272));
#194487=CARTESIAN_POINT('Ctrl Pts',(-1.06541758059653,6.32739655841135,
133.804758410613));
#194488=CARTESIAN_POINT('Ctrl Pts',(-1.34386520440944,5.94443203404716,
127.102730987725));
#194489=CARTESIAN_POINT('Ctrl Pts',(-1.62231282822229,0.0988248720430084,
123.802320359999));
#194490=CARTESIAN_POINT('Ctrl Pts',(-1.90076045203519,-5.83759751950527,
126.936442660293));
#194491=CARTESIAN_POINT('Ctrl Pts',(-2.17920807584809,-6.40955297312139,
133.624992605024));
#194492=CARTESIAN_POINT('Ctrl Pts',(-2.45765569966099,-1.09144236850938,
137.721519548813));
#194493=CARTESIAN_POINT('Ctrl Pts',(-2.73610332347384,5.22965045283876,
135.461515356786));
#194494=CARTESIAN_POINT('Ctrl Pts',(-3.01455094728676,6.74494999065597,
128.921813474073));
#194495=CARTESIAN_POINT('Ctrl Pts',(-3.29299857109967,2.06196999618574,
124.112080448687));
#194496=CARTESIAN_POINT('Ctrl Pts',(-3.57144619491253,-4.51585969194472,
125.452225962441));
#194497=CARTESIAN_POINT('Ctrl Pts',(-3.84989381872542,-6.94383493518842,
131.710721757939));
#194498=CARTESIAN_POINT('Ctrl Pts',(-4.12834144253832,-2.99076509818949,
137.136315943637));
#194499=CARTESIAN_POINT('Ctrl Pts',(-4.40678906635123,3.71067175704807,
136.743152517891));
#194500=CARTESIAN_POINT('Ctrl Pts',(-4.68523669016409,7.00218254395157,
130.892529461858));
#194501=CARTESIAN_POINT('Ctrl Pts',(-4.963684313977,3.85902964859785,124.960883545208));
#194502=CARTESIAN_POINT('Ctrl Pts',(-5.24213193778992,-2.83038296973812,
124.399107588329));
#194503=CARTESIAN_POINT('Ctrl Pts',(-5.52057956160276,-6.91881191077996,
129.723446251312));
#194504=CARTESIAN_POINT('Ctrl Pts',(-5.79902718541567,-4.6491907085676,
136.041092411279));
#194505=CARTESIAN_POINT('Ctrl Pts',(-6.07747480922856,1.89280962922548,
137.546437881394));
#194506=CARTESIAN_POINT('Ctrl Pts',(-6.35592243304147,6.69541038665145,
132.856143714835));
#194507=CARTESIAN_POINT('Ctrl Pts',(-6.63437005685431,5.34525608772619,
126.280361117063));
#194508=CARTESIAN_POINT('Ctrl Pts',(-6.91281768066725,-0.916927425542613,
123.86191305059));
#194509=CARTESIAN_POINT('Ctrl Pts',(-7.19126530448013,-6.33649942913263,
127.823235140749));
#194510=CARTESIAN_POINT('Ctrl Pts',(-7.469712928293,-5.93313801255607,134.524065908027));
#194511=CARTESIAN_POINT('Ctrl Pts',(-7.74816055210589,-0.0775126123463511,
137.806669231077));
#194512=CARTESIAN_POINT('Ctrl Pts',(-8.02660817591882,5.84934309190818,
134.654493020103));
#194513=CARTESIAN_POINT('Ctrl Pts',(-8.3050557997317,6.40093825099524,127.964233220621));
#194514=CARTESIAN_POINT('Ctrl Pts',(-8.58350342354456,1.07038386063539,
123.883911750995));
#194515=CARTESIAN_POINT('Ctrl Pts',(-8.86195104735747,-5.2438010064896,
126.163144707024));
#194516=CARTESIAN_POINT('Ctrl Pts',(-9.14039867117038,-6.73918892257159,
132.707428348838));
#194517=CARTESIAN_POINT('Ctrl Pts',(-9.41884629498326,-2.04159144649203,
137.50288571564));
#194518=CARTESIAN_POINT('Ctrl Pts',(-9.69729391879612,4.53212883162697,
136.142725758454));
#194519=CARTESIAN_POINT('Ctrl Pts',(-9.97574154260907,6.94104412028278,
129.876869030427));
#194520=CARTESIAN_POINT('Ctrl Pts',(-10.254189166422,2.97147895125515,124.463331760497));
#194521=CARTESIAN_POINT('Ctrl Pts',(-10.5326367902348,-3.72873020915888,
124.876890233732));
#194522=CARTESIAN_POINT('Ctrl Pts',(-10.8110844140478,-7.00241846595355,
130.737504416682));
#194523=CARTESIAN_POINT('Ctrl Pts',(-11.0895320378606,-3.84122623969676,
136.659556182137));
#194524=CARTESIAN_POINT('Ctrl Pts',(-11.3679796616735,2.84986524650705,
137.200969265957));
#194525=CARTESIAN_POINT('Ctrl Pts',(-11.6464272854864,6.92206979482823,
131.864211493609));
#194526=CARTESIAN_POINT('Ctrl Pts',(-11.9248749092993,4.6332303636112,125.553502542771));
#194527=CARTESIAN_POINT('Ctrl Pts',(-12.2033225331122,-1.91332142587795,
124.068075643991));
#194528=CARTESIAN_POINT('Ctrl Pts',(-12.4817701569251,-6.70162429593314,
128.77296555011));
#194529=CARTESIAN_POINT('Ctrl Pts',(-12.760217780738,-5.33146183057377,
135.344608284054));
#194530=CARTESIAN_POINT('Ctrl Pts',(-13.0386654045509,0.938053600692905,
137.743985215925));
#194531=CARTESIAN_POINT('Ctrl Pts',(-13.3171130283637,6.34554359938892,
133.766186161411));
#194532=CARTESIAN_POINT('Ctrl Pts',(-13.5955606521767,5.92178902728497,
127.066614125326));
#194533=CARTESIAN_POINT('Ctrl Pts',(-13.8740082759896,0.0561996345831295,
123.801848516541));
#194534=CARTESIAN_POINT('Ctrl Pts',(-14.1524558998025,-5.86103447679583,
126.972049436864));
#194535=CARTESIAN_POINT('Ctrl Pts',(-14.4309035236153,-6.39226423145161,
133.663957113442));
#194536=CARTESIAN_POINT('Ctrl Pts',(-14.7093511474282,-1.04931543687181,
137.728035309365));
#194537=CARTESIAN_POINT('Ctrl Pts',(-14.9877987712411,5.25790298228423,
135.429594703837));
#194538=CARTESIAN_POINT('Ctrl Pts',(-15.266246395054,6.73336542356173,128.880789928272));
#194539=CARTESIAN_POINT('Ctrl Pts',(-15.5446940188669,2.02119398377386,
124.099652644515));
#194540=CARTESIAN_POINT('Ctrl Pts',(-15.8231416426798,-4.54835598628669,
125.479814444798));
#194541=CARTESIAN_POINT('Ctrl Pts',(-16.1015892664927,-6.93818900449243,
131.752974059312));
#194542=CARTESIAN_POINT('Ctrl Pts',(-16.3800368903055,-2.95216527694612,
137.154404263204));
#194543=CARTESIAN_POINT('Ctrl Pts',(-16.6584845141185,3.74675411882228,
136.720454573632));
#194544=CARTESIAN_POINT('Ctrl Pts',(-16.9369321379314,7.00258951850748,
130.849903555692));
#194545=CARTESIAN_POINT('Ctrl Pts',(-17.2153797617442,3.82338724620039,
124.93750080251));
#194546=CARTESIAN_POINT('Ctrl Pts',(-17.4938273855571,-2.86932112251383,
124.416455607327));
#194547=CARTESIAN_POINT('Ctrl Pts',(-17.77227500937,-6.92526355376757,129.765583050046));
#194548=CARTESIAN_POINT('Ctrl Pts',(-18.0507226331829,-4.61722709704176,
136.069296330209));
#194549=CARTESIAN_POINT('Ctrl Pts',(-18.3291702569958,1.93381549778173,
137.534790896862));
#194550=CARTESIAN_POINT('Ctrl Pts',(-18.6076178808087,6.70777612228299,
132.81534883664));
#194551=CARTESIAN_POINT('Ctrl Pts',(-18.8860655046216,5.31761818348739,
126.247906845325));
#194552=CARTESIAN_POINT('Ctrl Pts',(-19.1645131284344,-0.959171085842972,
123.867623275557));
#194553=CARTESIAN_POINT('Ctrl Pts',(-19.4429607522474,-6.35452898539608,
127.861862444637));
#194554=CARTESIAN_POINT('Ctrl Pts',(-19.7214083760603,-5.91038518336925,
134.560113685611));
#194555=CARTESIAN_POINT('Ctrl Pts',(-19.9998559998732,-0.0348861361944895,
137.807011335788));
#194556=CARTESIAN_POINT('Ctrl Pts',(-20.278303623686,5.87267156586067,134.618815074426));
#194557=CARTESIAN_POINT('Ctrl Pts',(-20.5567512474989,6.38353099484532,
127.925321513668));
#194558=CARTESIAN_POINT('Ctrl Pts',(-20.8351988713118,1.02823729239309,
123.877524240513));
#194559=CARTESIAN_POINT('Ctrl Pts',(-21.1136464951247,-5.27195624958391,
126.1951512031));
#194560=CARTESIAN_POINT('Ctrl Pts',(-21.3920941189376,-6.72747954757436,
132.748416445183));
#194561=CARTESIAN_POINT('Ctrl Pts',(-21.6705417427505,-2.00077779699093,
137.515189354092));
#194562=CARTESIAN_POINT('Ctrl Pts',(-21.9489893665634,4.56454100559805,
136.115038496344));
#194563=CARTESIAN_POINT('Ctrl Pts',(-22.2274369903762,6.93526961426714,
129.834634109035));
#194564=CARTESIAN_POINT('Ctrl Pts',(-22.5058846141892,2.93282425418085,
124.445361009293));
#194565=CARTESIAN_POINT('Ctrl Pts',(-22.784332238002,-3.76474331906749,
124.899697895151));
#194566=CARTESIAN_POINT('Ctrl Pts',(-23.062779861815,-7.0026957000287,130.780131364099));
#194567=CARTESIAN_POINT('Ctrl Pts',(-23.3412274856278,-3.80551283336702,
136.682830333316));
#194568=CARTESIAN_POINT('Ctrl Pts',(-23.6196751094408,2.88875041752152,
137.183502812971));
#194569=CARTESIAN_POINT('Ctrl Pts',(-23.8981227332536,6.92839315801137,
131.822055253468));
#194570=CARTESIAN_POINT('Ctrl Pts',(-24.1765703570665,4.60118105711114,
125.525396040718));
#194571=CARTESIAN_POINT('Ctrl Pts',(-24.4550179808794,-1.95429165508329,
124.079847382335));
#194572=CARTESIAN_POINT('Ctrl Pts',(-24.7334656046923,-6.71386580871103,
128.813797876394));
#194573=CARTESIAN_POINT('Ctrl Pts',(-25.0119132285052,-5.30372527471246,
135.376978285193));
#194574=CARTESIAN_POINT('Ctrl Pts',(-25.290360852318,0.980279685362951,
137.738146442235));
#194575=CARTESIAN_POINT('Ctrl Pts',(-25.568808476131,6.36345550391485,133.727504160674));
#194576=CARTESIAN_POINT('Ctrl Pts',(-25.8472560999438,5.89892658645264,
127.030635766497));
#194577=CARTESIAN_POINT('Ctrl Pts',(-26.1257037237567,0.0135723146251221,
123.801636153745));
#194578=CARTESIAN_POINT('Ctrl Pts',(-26.4041513475696,-5.88425425129846,
127.007798221134));
#194579=CARTESIAN_POINT('Ctrl Pts',(-26.6825989713826,-6.37473862207999,
133.70281565846));
#194580=CARTESIAN_POINT('Ctrl Pts',(-26.9610465951954,-1.00714962246484,
137.734294510605));
#194581=CARTESIAN_POINT('Ctrl Pts',(-27.2394942190083,5.28596067820108,
135.397502661138));
#194582=CARTESIAN_POINT('Ctrl Pts',(-27.5179418428212,6.72153134913555,
128.839837661092));
#194583=CARTESIAN_POINT('Ctrl Pts',(-27.7963894666341,1.98034307527561,
124.087473285763));
#194584=CARTESIAN_POINT('Ctrl Pts',(-28.0748370904469,-4.58068373962494,
125.507600230172));
#194585=CARTESIAN_POINT('Ctrl Pts',(-28.3532847142599,-6.93228597665136,
131.795191209466));
#194586=CARTESIAN_POINT('Ctrl Pts',(-28.6317323380727,-2.91345606213275,
137.172257279568));
#194587=CARTESIAN_POINT('Ctrl Pts',(-28.9101799618857,3.78269764324474,
136.697537406337));
#194588=CARTESIAN_POINT('Ctrl Pts',(-29.1886275856985,7.00273700953358,
130.807275961916));
#194589=CARTESIAN_POINT('Ctrl Pts',(-29.4670752095115,3.78760316678249,
124.914335458459));
#194590=CARTESIAN_POINT('Ctrl Pts',(-29.7455228333243,-2.90815295154017,
124.434040332496));
#194591=CARTESIAN_POINT('Ctrl Pts',(-30.0239704571372,-6.93145857856742,
129.807758341064));
#194592=CARTESIAN_POINT('Ctrl Pts',(-30.3024180809501,-4.5850923924679,
136.097305155009));
#194593=CARTESIAN_POINT('Ctrl Pts',(-30.580865704763,1.97474970809384,137.52289451376));
#194594=CARTESIAN_POINT('Ctrl Pts',(-30.8593133285759,6.71989329880362,
132.774479440534));
#194595=CARTESIAN_POINT('Ctrl Pts',(-31.1377609523888,5.28978323295099,
126.215621414657));
#194596=CARTESIAN_POINT('Ctrl Pts',(-31.4162085762017,-1.00137920370602,
123.873590543879));
#194597=CARTESIAN_POINT('Ctrl Pts',(-31.6946562000146,-6.37232307225107,
127.900598783877));
#194598=CARTESIAN_POINT('Ctrl Pts',(-31.9731038238274,-5.88741334268594,
134.596022292384));
#194599=CARTESIAN_POINT('Ctrl Pts',(-32.2515514476404,0.00774163267598956,
137.807093954702));
#194600=CARTESIAN_POINT('Ctrl Pts',(-32.5299990714533,5.89578242580862,
134.582995782735));
#194601=CARTESIAN_POINT('Ctrl Pts',(-32.8084466952661,6.36588719460685,
127.886516490566));
#194602=CARTESIAN_POINT('Ctrl Pts',(-33.086894319079,0.9860526224398,123.8713934065));
#194603=CARTESIAN_POINT('Ctrl Pts',(-33.365341942892,-5.29991613840065,
126.227328495126));
#194604=CARTESIAN_POINT('Ctrl Pts',(-33.6437895667048,-6.71552088334846,
132.789332503824));
#194605=CARTESIAN_POINT('Ctrl Pts',(-33.9222371905177,-1.95989000793276,
137.527244320318));
#194606=CARTESIAN_POINT('Ctrl Pts',(-34.2006848143306,4.59678403882356,
136.08715444511));
#194607=CARTESIAN_POINT('Ctrl Pts',(-34.4791324381435,6.9292381192855,129.792435121214));
#194608=CARTESIAN_POINT('Ctrl Pts',(-34.7575800619564,2.89406088022529,
124.427625893158));
#194609=CARTESIAN_POINT('Ctrl Pts',(-35.0360276857693,-3.80061692502793,
124.922724356021));
#194610=CARTESIAN_POINT('Ctrl Pts',(-35.3144753095821,-7.00271344663942,
130.822759209339));
#194611=CARTESIAN_POINT('Ctrl Pts',(-35.592922933395,-3.76965841235978,
136.705886655638));
#194612=CARTESIAN_POINT('Ctrl Pts',(-35.8713705572079,2.92752854482695,
137.165799978524));
#194613=CARTESIAN_POINT('Ctrl Pts',(-36.1498181810209,6.9344597870381,131.779861302279));
#194614=CARTESIAN_POINT('Ctrl Pts',(-36.4282658048337,4.56896125215494,
125.49748515264));
#194615=CARTESIAN_POINT('Ctrl Pts',(-36.7067134286466,-1.99518946729269,
124.091868299989));
#194616=CARTESIAN_POINT('Ctrl Pts',(-36.9851610524595,-6.72585853672236,
128.854703963711));
#194617=CARTESIAN_POINT('Ctrl Pts',(-37.2636086762724,-5.27579218736066,
135.409178846303));
#194618=CARTESIAN_POINT('Ctrl Pts',(-37.5420563000852,1.02246944540875,
137.732050734562));
#194619=CARTESIAN_POINT('Ctrl Pts',(-37.8205039238982,6.38113160825695,
133.688713841779));
#194620=CARTESIAN_POINT('Ctrl Pts',(-38.0989515477111,5.87584555872632,
126.994797244432));
#194621=CARTESIAN_POINT('Ctrl Pts',(-38.377399171524,-0.0290555082599903,
123.801683279478));
#194622=CARTESIAN_POINT('Ctrl Pts',(-38.6558467953367,-5.90725598259587,
127.04368768842));
#194623=CARTESIAN_POINT('Ctrl Pts',(-38.9342944191497,-6.35697679442443,
133.741566800161));
#194624=CARTESIAN_POINT('Ctrl Pts',(-39.2127420429625,-0.964946487758246,
137.740296920595));
#194625=CARTESIAN_POINT('Ctrl Pts',(-39.4911896667755,5.31382250090111,
135.365240417872));
#194626=CARTESIAN_POINT('Ctrl Pts',(-39.7696372905882,6.70944820589337,
128.798958190032));
#194627=CARTESIAN_POINT('Ctrl Pts',(-40.0480849144012,1.93941878443644,
124.07554282374));
#194628=CARTESIAN_POINT('Ctrl Pts',(-40.3265325382142,-4.61284175404266,
125.535582288951));
#194629=CARTESIAN_POINT('Ctrl Pts',(-40.604980162027,-6.9261260704041,131.837371644027));
#194630=CARTESIAN_POINT('Ctrl Pts',(-40.8834277858398,-2.87463888813357,
137.18987433118));
#194631=CARTESIAN_POINT('Ctrl Pts',(-41.1618754096529,3.81850099841496,
136.674401865208));
#194632=CARTESIAN_POINT('Ctrl Pts',(-41.4403230334656,7.00262501156454,
130.76464826011));
#194633=CARTESIAN_POINT('Ctrl Pts',(-41.7187706572786,3.75167873633635,
124.891388371457));
#194634=CARTESIAN_POINT('Ctrl Pts',(-41.9972182810916,-2.94687701788942,
124.451861112224));
#194635=CARTESIAN_POINT('Ctrl Pts',(-42.2756659049044,-6.93739675562063,
129.849970561546));
#194636=CARTESIAN_POINT('Ctrl Pts',(-42.5541135287174,-4.55278778560923,
136.125117847804));
#194637=CARTESIAN_POINT('Ctrl Pts',(-42.8325611525302,2.01561074332903,
137.510749172913));
#194638=CARTESIAN_POINT('Ctrl Pts',(-43.1110087763431,6.73176146720674,
132.733537040953));
#194639=CARTESIAN_POINT('Ctrl Pts',(-43.389456400156,5.26175226755184,126.183506021407));
#194640=CARTESIAN_POINT('Ctrl Pts',(-43.6679040239687,-1.0435502150944,
123.879814634434));
#194641=CARTESIAN_POINT('Ctrl Pts',(-43.9463516477818,-6.38988103033122,
127.93944272308));
#194642=CARTESIAN_POINT('Ctrl Pts',(-44.2247992715946,-5.86422334173611,
134.631790397739));
#194643=CARTESIAN_POINT('Ctrl Pts',(-44.5032468954075,0.050369114677416,
137.806917084757));
#194644=CARTESIAN_POINT('Ctrl Pts',(-44.7816945192204,5.91867481537061,
134.547036472328));
#194645=CARTESIAN_POINT('Ctrl Pts',(-45.0601421430334,6.34800750407734,
127.847819589252));
#194646=CARTESIAN_POINT('Ctrl Pts',(-45.3385897668461,0.943831413943965,
123.865519476137));
#194647=CARTESIAN_POINT('Ctrl Pts',(-45.6170373906592,-5.32767963687585,
126.25967539076));
#194648=CARTESIAN_POINT('Ctrl Pts',(-45.895485014472,-6.7033133730266,132.830175008601));
#194649=CARTESIAN_POINT('Ctrl Pts',(-46.1739326382849,-1.91892959442962,
137.539050167615));
#194650=CARTESIAN_POINT('Ctrl Pts',(-46.4523802620978,4.62885673652604,
136.059074638009));
#194651=CARTESIAN_POINT('Ctrl Pts',(-46.7308278859106,6.92294985883713,
129.750273630666));
#194652=CARTESIAN_POINT('Ctrl Pts',(-47.0092755097235,2.8551902657795,124.410127069272));
#194653=CARTESIAN_POINT('Ctrl Pts',(-47.2877231335364,-3.83634969773052,
124.945968763085));
#194654=CARTESIAN_POINT('Ctrl Pts',(-47.5661707573492,-7.00247170512816,
130.865386372813));
#194655=CARTESIAN_POINT('Ctrl Pts',(-47.8446183811622,-3.73366430527375,
136.728724294741));
#194656=CARTESIAN_POINT('Ctrl Pts',(-48.123066004975,2.96619819148554,137.147861418602));
#194657=CARTESIAN_POINT('Ctrl Pts',(-48.4015136287881,6.9402694571073,131.737631203552));
#194658=CARTESIAN_POINT('Ctrl Pts',(-48.6799612526008,4.53657214265928,
125.469770912784));
#194659=CARTESIAN_POINT('Ctrl Pts',(-48.9584088764139,-2.03601334702262,
124.104137951514));
#194660=CARTESIAN_POINT('Ctrl Pts',(-49.2368565002267,-6.7376020355722,
128.895682296272));
#194661=CARTESIAN_POINT('Ctrl Pts',(-49.5153041240395,-5.24766360358919,
135.441208774179));
#194662=CARTESIAN_POINT('Ctrl Pts',(-49.7937517478526,1.06462131747325,
137.725698318783));
#194663=CARTESIAN_POINT('Ctrl Pts',(-50.0721993716652,6.39857125742062,
133.649816642113));
#194664=CARTESIAN_POINT('Ctrl Pts',(-50.3506469954783,5.85254679938199,
126.959099887138));
#194665=CARTESIAN_POINT('Ctrl Pts',(-50.6290946192911,-0.0716822544825644,
123.801989891996));
#194666=CARTESIAN_POINT('Ctrl Pts',(-50.907542243104,-5.93003881835047,
127.079716508824));
#194667=CARTESIAN_POINT('Ctrl Pts',(-51.1859898669169,-6.33897940665598,
133.780209102606));
#194668=CARTESIAN_POINT('Ctrl Pts',(-51.4644374907297,-0.922707596604453,
137.746042316915));
#194669=CARTESIAN_POINT('Ctrl Pts',(-51.7428851145428,5.34148741795441,
135.332809169526));
#194670=CARTESIAN_POINT('Ctrl Pts',(-52.0213327383556,6.69711644158035,
128.758153029896));
#194671=CARTESIAN_POINT('Ctrl Pts',(-52.2997803621686,1.89842262772099,
124.063861700536));
#194672=CARTESIAN_POINT('Ctrl Pts',(-52.5782279859813,-4.64482883791282,
125.563759584248));
#194673=CARTESIAN_POINT('Ctrl Pts',(-52.8566756097944,-6.91970951400822,
131.879513799985));
#194674=CARTESIAN_POINT('Ctrl Pts',(-53.135123233607,-2.83571519333325,
137.207254765232));
#194675=CARTESIAN_POINT('Ctrl Pts',(-53.4135708574202,3.85416285762642,
136.651048807542));
#194676=CARTESIAN_POINT('Ctrl Pts',(-53.6920184812329,7.0022535287505,130.72202202986));
#194677=CARTESIAN_POINT('Ctrl Pts',(-53.9704661050458,3.71561528605495,
124.868660391816));
#194678=CARTESIAN_POINT('Ctrl Pts',(-54.2489137288587,-2.98549188662705,
124.469917286158));
#194679=CARTESIAN_POINT('Ctrl Pts',(-54.5273613526715,-6.94307786488582,
129.892218147303));
#194680=CARTESIAN_POINT('Ctrl Pts',(-54.8058089764845,-4.5203144735249,
136.152733377983));
#194681=CARTESIAN_POINT('Ctrl Pts',(-55.0842566002972,2.05639708936689,
137.498355324372));
#194682=CARTESIAN_POINT('Ctrl Pts',(-55.3627042241104,6.74338018771311,
132.69252315503));
#194683=CARTESIAN_POINT('Ctrl Pts',(-55.6411518479232,5.23352632598741,
126.151561855625));
#194684=CARTESIAN_POINT('Ctrl Pts',(-55.919599471736,-1.08568255734582,
123.886295316588));
#194685=CARTESIAN_POINT('Ctrl Pts',(-56.1980470955489,-6.40720220901991,
127.978392822871));
#194686=CARTESIAN_POINT('Ctrl Pts',(-56.4764947193619,-5.8408160398338,
134.667416676276));
#194687=CARTESIAN_POINT('Ctrl Pts',(-56.7549423431748,0.0929947302327828,
137.806480732508));
#194688=CARTESIAN_POINT('Ctrl Pts',(-57.0333899669875,5.94134788626073,
134.510938475691));
#194689=CARTESIAN_POINT('Ctrl Pts',(-57.3118375908005,6.32989258579528,
127.809232243652));
#194690=CARTESIAN_POINT('Ctrl Pts',(-57.5902852146133,0.901575231427987,
123.859902667085));
#194691=CARTESIAN_POINT('Ctrl Pts',(-57.8687328384263,-5.35524571622284,
126.292190691378));
#194692=CARTESIAN_POINT('Ctrl Pts',(-58.1471804622391,-6.69085746896258,
132.870942446081));
#194693=CARTESIAN_POINT('Ctrl Pts',(-58.4256280860521,-1.87789807428466,
137.550606458515));
#194694=CARTESIAN_POINT('Ctrl Pts',(-58.7040757098649,4.6607579102399,136.030800115547));
#194695=CARTESIAN_POINT('Ctrl Pts',(-58.9825233336777,6.91640506593584,
129.708151199698));
#194696=CARTESIAN_POINT('Ctrl Pts',(-59.2609709574908,2.81621385120844,
124.392865186062));
#194697=CARTESIAN_POINT('Ctrl Pts',(-59.5394185813036,-3.87194031308425,
124.969430255013));
#194698=CARTESIAN_POINT('Ctrl Pts',(-59.8178662051166,-7.00197048445272,
130.908011274954));
#194699=CARTESIAN_POINT('Ctrl Pts',(-60.0963138289294,-3.69753184588372,
136.751342404371));
#194700=CARTESIAN_POINT('Ctrl Pts',(-60.3747614527424,3.00475792457964,
137.129687797925));
#194701=CARTESIAN_POINT('Ctrl Pts',(-60.6532090765552,6.94582195293937,
131.695366522141));
#194702=CARTESIAN_POINT('Ctrl Pts',(-60.9316567003681,4.50401492881459,
125.442254348109));
#194703=CARTESIAN_POINT('Ctrl Pts',(-61.210104324181,-2.07676178152925,
124.116655882255));
#194704=CARTESIAN_POINT('Ctrl Pts',(-61.4885519479939,-6.74909587010084,
128.93673135561));
#194705=CARTESIAN_POINT('Ctrl Pts',(-61.7669995718066,-5.21934056571308,
135.473066881942));
#194706=CARTESIAN_POINT('Ctrl Pts',(-62.0454471956197,1.10673373960332,
137.719089430292));
#194707=CARTESIAN_POINT('Ctrl Pts',(-62.3238948194324,6.41577380517329,
133.610814003028));
#194708=CARTESIAN_POINT('Ctrl Pts',(-62.6023424432454,5.82903117176375,
126.923545017394));
#194709=CARTESIAN_POINT('Ctrl Pts',(-62.8807900670583,-0.114306344492842,
123.802555979936));
#194710=CARTESIAN_POINT('Ctrl Pts',(-63.1592376908712,-5.95260191433588,
127.115883347286));
#194711=CARTESIAN_POINT('Ctrl Pts',(-63.4376853146842,-6.32074712567447,
133.818741133891));
#194712=CARTESIAN_POINT('Ctrl Pts',(-63.716132938497,-0.880434514181572,
137.751530486667));
#194713=CARTESIAN_POINT('Ctrl Pts',(-63.99458056231,5.36895440422691,135.300210117855));
#194714=CARTESIAN_POINT('Ctrl Pts',(-64.2730281861228,6.6845365131549,128.717423692735));
#194715=CARTESIAN_POINT('Ctrl Pts',(-64.5514758099358,1.85735612425694,
124.052430348997));
#194716=CARTESIAN_POINT('Ctrl Pts',(-64.8299234337484,-4.67664380594228,
125.592131071942));
#194717=CARTESIAN_POINT('Ctrl Pts',(-65.1083710575615,-6.91303654523158,
131.921616115747));
#194718=CARTESIAN_POINT('Ctrl Pts',(-65.3868186813742,-2.79668642006362,
137.224397937687));
#194719=CARTESIAN_POINT('Ctrl Pts',(-65.6652663051872,3.88968189941585,
136.627479098696));
#194720=CARTESIAN_POINT('Ctrl Pts',(-65.9437139290001,7.00162257485687,
130.679398850698));
#194721=CARTESIAN_POINT('Ctrl Pts',(-66.2221615528129,3.67941415228271,
124.846152361731));
#194722=CARTESIAN_POINT('Ctrl Pts',(-66.500609176626,-3.02399612686491,
124.48820818522));
#194723=CARTESIAN_POINT('Ctrl Pts',(-66.7790568004388,-6.94850169584742,
129.934499532835));
#194724=CARTESIAN_POINT('Ctrl Pts',(-67.0575044242516,-4.48767365952541,
136.180150722241));
#194725=CARTESIAN_POINT('Ctrl Pts',(-67.3359520480646,2.09710723485436,
137.485713427398));
#194726=CARTESIAN_POINT('Ctrl Pts',(-67.6143996718775,6.75474902978674,
132.651439302549));
#194727=CARTESIAN_POINT('Ctrl Pts',(-67.8928472956903,5.20510645418034,
126.119790101011));
#194728=CARTESIAN_POINT('Ctrl Pts',(-68.1712949195033,-1.12777466923081,
123.893032350195));
#194729=CARTESIAN_POINT('Ctrl Pts',(-68.449742543316,-6.42428596647451,
128.017447639935));
#194730=CARTESIAN_POINT('Ctrl Pts',(-68.728190167129,-5.81719230434518,
134.702899807851));
#194731=CARTESIAN_POINT('Ctrl Pts',(-69.0066377909419,0.135616899834216,
137.805784914121));
#194732=CARTESIAN_POINT('Ctrl Pts',(-69.2850854147548,5.96380079832,134.474703130449));
#194733=CARTESIAN_POINT('Ctrl Pts',(-69.5635330385676,6.31154311101565,
127.770755883637));
#194734=CARTESIAN_POINT('Ctrl Pts',(-69.8419806623805,0.859285640710264,
123.854543187474));
#194735=CARTESIAN_POINT('Ctrl Pts',(-70.1204282861936,-5.38261335497044,
126.324873192109));
#194736=CARTESIAN_POINT('Ctrl Pts',(-70.3988759100064,-6.67815363271447,
132.911633305611));
#194737=CARTESIAN_POINT('Ctrl Pts',(-70.6773235338194,-1.83679696793597,
137.561912764793));
#194738=CARTESIAN_POINT('Ctrl Pts',(-70.9557711576322,4.69248637785542,
136.002331925448));
#194739=CARTESIAN_POINT('Ctrl Pts',(-71.2342187814451,6.90960398310133,
129.666069389173));
#194740=CARTESIAN_POINT('Ctrl Pts',(-71.5126664052579,2.77713308079745,
124.375840883174));
#194741=CARTESIAN_POINT('Ctrl Pts',(-71.7911140290708,-3.90738745226578,
124.993107962432));
#194742=CARTESIAN_POINT('Ctrl Pts',(-72.0695616528837,-7.00120980318599,
130.950632336283));
#194743=CARTESIAN_POINT('Ctrl Pts',(-72.3480092766965,-3.66126237309149,
136.773740146404));
#194744=CARTESIAN_POINT('Ctrl Pts',(-72.6264569005095,3.04320631526353,
137.111279789924));
#194745=CARTESIAN_POINT('Ctrl Pts',(-72.9049045243223,6.95111706878496,
131.653068824177));
#194746=CARTESIAN_POINT('Ctrl Pts',(-73.1833521481353,4.47129081703998,
125.414936478256));
#194747=CARTESIAN_POINT('Ctrl Pts',(-73.4617997719481,-2.11743326086482,
124.129421628353));
#194748=CARTESIAN_POINT('Ctrl Pts',(-73.7402473957612,-6.76033961440018,
128.977849620639));
#194749=CARTESIAN_POINT('Ctrl Pts',(-74.018695019574,-5.19082412325261,
135.504751989078));
#194750=CARTESIAN_POINT('Ctrl Pts',(-74.2971426433868,1.14880515130821,
137.712224313981));
#194751=CARTESIAN_POINT('Ctrl Pts',(-74.5755902671998,6.43273861406817,
133.571707369781));
#194752=CARTESIAN_POINT('Ctrl Pts',(-74.8540378910127,5.80529954725181,
126.8881339527));
#194753=CARTESIAN_POINT('Ctrl Pts',(-75.1324855148255,-0.156926198840311,
123.803381522322));
#194754=CARTESIAN_POINT('Ctrl Pts',(-75.4109331386384,-5.97494443446864,
127.15218686363));
#194755=CARTESIAN_POINT('Ctrl Pts',(-75.6893807624512,-6.30228062708332,
133.857161466198));
#194756=CARTESIAN_POINT('Ctrl Pts',(-75.9678283862644,-0.838128806933456,
137.756761226486));
#194757=CARTESIAN_POINT('Ctrl Pts',(-76.2462760100769,5.3962224419198,135.267444470826));
#194758=CARTESIAN_POINT('Ctrl Pts',(-76.52472363389,6.67170888677059,128.676771687789));
#194759=CARTESIAN_POINT('Ctrl Pts',(-76.8031712577027,1.81622079577817,
124.041249192718));
#194760=CARTESIAN_POINT('Ctrl Pts',(-77.0816188815158,-4.70828547921653,
125.620695700721));
#194761=CARTESIAN_POINT('Ctrl Pts',(-77.3600665053286,-6.90610741134329,
131.963677031195));
#194762=CARTESIAN_POINT('Ctrl Pts',(-77.6385141291417,-2.75755401454922,
137.241303213299));
#194763=CARTESIAN_POINT('Ctrl Pts',(-77.9169617529544,3.92505680761298,
136.603693612052));
#194764=CARTESIAN_POINT('Ctrl Pts',(-78.1954093767674,7.00073217326374,
130.636780302039));
#194765=CARTESIAN_POINT('Ctrl Pts',(-78.4738570005803,3.6430766764653,124.823865115242));
#194766=CARTESIAN_POINT('Ctrl Pts',(-78.7523046243931,-3.06238831181505,
124.506733131632));
#194767=CARTESIAN_POINT('Ctrl Pts',(-79.0307522482061,-6.95366804752337,
129.976813151389));
#194768=CARTESIAN_POINT('Ctrl Pts',(-79.3091998720188,-4.45486655312747,
136.207368864621));
#194769=CARTESIAN_POINT('Ctrl Pts',(-79.5876474958318,2.13773967126259,
137.472823950436));
#194770=CARTESIAN_POINT('Ctrl Pts',(-79.8660951196445,6.76586757215105,
132.610287005887));
#194771=CARTESIAN_POINT('Ctrl Pts',(-80.1445427434577,5.17649370523912,
126.08819193488));
#194772=CARTESIAN_POINT('Ctrl Pts',(-80.4229903672703,-1.16982499101125,
123.900025485612));
#194773=CARTESIAN_POINT('Ctrl Pts',(-80.7014379910835,-6.44113166965063,
128.056605727087));
#194774=CARTESIAN_POINT('Ctrl Pts',(-80.9798856148961,-5.7933530106558,
134.738238477622));
#194775=CARTESIAN_POINT('Ctrl Pts',(-81.2583332387092,0.17823404410257,
137.804829655383));
#194776=CARTESIAN_POINT('Ctrl Pts',(-81.5367808625219,5.98603271954817,
134.438331779315));
#194777=CARTESIAN_POINT('Ctrl Pts',(-81.815228486335,6.29295975968447,127.732391934959));
#194778=CARTESIAN_POINT('Ctrl Pts',(-82.0936761101477,0.816964208846405,
123.849441235906));
#194779=CARTESIAN_POINT('Ctrl Pts',(-82.3721237339607,-5.40978153900143,
126.357721681897));
#194780=CARTESIAN_POINT('Ctrl Pts',(-82.6505713577735,-6.66520233502723,
132.952246079378));
#194781=CARTESIAN_POINT('Ctrl Pts',(-82.9290189815866,-1.79562779839943,
137.572968667493));
#194782=CARTESIAN_POINT('Ctrl Pts',(-83.2074666053992,4.72404096366304,
135.97367112261));
#194783=CARTESIAN_POINT('Ctrl Pts',(-83.4859142292123,6.90254686235,129.624029758449));
#194784=CARTESIAN_POINT('Ctrl Pts',(-83.7643618530252,2.73794940269844,
124.359054791448));
#194785=CARTESIAN_POINT('Ctrl Pts',(-84.0428094768383,-3.94268980176888,
125.017001007954));
#194786=CARTESIAN_POINT('Ctrl Pts',(-84.3212571006508,-7.00018968951541,
130.99324797746));
#194787=CARTESIAN_POINT('Ctrl Pts',(-84.5997047244641,-3.62485723087481,
136.795916690882));
#194788=CARTESIAN_POINT('Ctrl Pts',(-84.8781523482765,3.08154193881888,
137.092638076712));
#194789=CARTESIAN_POINT('Ctrl Pts',(-85.1565999720898,6.95615460843127,
131.61073967702));
#194790=CARTESIAN_POINT('Ctrl Pts',(-85.4350475959023,4.4384010199398,125.387818315495));
#194791=CARTESIAN_POINT('Ctrl Pts',(-85.7134952197154,-2.1580262779319,
124.142434716771));
#194792=CARTESIAN_POINT('Ctrl Pts',(-85.9919428435283,-6.7713328518292,
129.019035567703));
#194793=CARTESIAN_POINT('Ctrl Pts',(-86.2703904673411,-5.16211533289519,
135.536262921482));
#194794=CARTESIAN_POINT('Ctrl Pts',(-86.5488380911541,1.19083399361533,
137.70510322424));
#194795=CARTESIAN_POINT('Ctrl Pts',(-86.827285714967,6.4494650554685,133.532498191482));
#194796=CARTESIAN_POINT('Ctrl Pts',(-87.1057333387799,5.78135280522977,
126.852868005224));
#194797=CARTESIAN_POINT('Ctrl Pts',(-87.3841809625928,-0.199540238229241,
123.804466488563));
#194798=CARTESIAN_POINT('Ctrl Pts',(-87.6626285864056,-5.99706555083783,
127.188625712615));
#194799=CARTESIAN_POINT('Ctrl Pts',(-87.9410762102187,-6.28358059516641,
133.895468675847));
#194800=CARTESIAN_POINT('Ctrl Pts',(-88.2195238340314,-0.795792042514341,
137.761734342542));
#194801=CARTESIAN_POINT('Ctrl Pts',(-88.4979714578443,5.42329052060546,
135.234513442586));
#194802=CARTESIAN_POINT('Ctrl Pts',(-88.7764190816572,6.65863403776028,
128.636198521433));
#194803=CARTESIAN_POINT('Ctrl Pts',(-89.0548667054699,1.77501816656995,
124.03031864602));
#194804=CARTESIAN_POINT('Ctrl Pts',(-89.3333143292831,-4.73975268523957,
125.649452412109));
#194805=CARTESIAN_POINT('Ctrl Pts',(-89.6117619530957,-6.8989223691057,
132.005694987746));
#194806=CARTESIAN_POINT('Ctrl Pts',(-89.8902095769088,-2.71831942685781,
137.257969965635));
#194807=CARTESIAN_POINT('Ctrl Pts',(-90.1686572007216,3.9602862713853,136.579693228991));
#194808=CARTESIAN_POINT('Ctrl Pts',(-90.4471048245344,6.99958235696585,
130.59416796313));
#194809=CARTESIAN_POINT('Ctrl Pts',(-90.7255524483476,3.60660420510239,
124.801799478213));
#194810=CARTESIAN_POINT('Ctrl Pts',(-91.0040000721602,-3.10066701883943,
124.525491438947));
#194811=CARTESIAN_POINT('Ctrl Pts',(-91.2824476959735,-6.95857672847263,
130.019157435019));
#194812=CARTESIAN_POINT('Ctrl Pts',(-91.560895319786,-4.4218943700117,136.234386796543));
#194813=CARTESIAN_POINT('Ctrl Pts',(-91.8393429435991,2.17829289294083,
137.459687371113));
#194814=CARTESIAN_POINT('Ctrl Pts',(-92.1177905674117,6.77673540280433,
132.56906778996));
#194815=CARTESIAN_POINT('Ctrl Pts',(-92.3962381912249,5.14768913942031,
126.056768528114));
#194816=CARTESIAN_POINT('Ctrl Pts',(-92.6746858150375,-1.21183196449619,
123.907274463707));
#194817=CARTESIAN_POINT('Ctrl Pts',(-92.9531334388505,-6.45773869432309,
128.095865633305));
#194818=CARTESIAN_POINT('Ctrl Pts',(-93.2315810626634,-5.76929904214118,
134.773431376103));
#194819=CARTESIAN_POINT('Ctrl Pts',(-93.5100286864763,0.220844583841736,
137.803614991691));
#194820=CARTESIAN_POINT('Ctrl Pts',(-93.7884763102892,6.00804282613147,
134.401825770043));
#194821=CARTESIAN_POINT('Ctrl Pts',(-94.0669239341021,6.27414322041607,
127.694141819211));
#194822=CARTESIAN_POINT('Ctrl Pts',(-94.3453715579151,0.774612504073732,
123.844597001431));
#194823=CARTESIAN_POINT('Ctrl Pts',(-94.6238191817278,-5.43674926158731,
126.390734943524));
#194824=CARTESIAN_POINT('Ctrl Pts',(-94.9022668055408,-6.65200405581671,
132.99277926246));
#194825=CARTESIAN_POINT('Ctrl Pts',(-95.1807144293538,-1.75439209121494,
137.583773756932));
#194826=CARTESIAN_POINT('Ctrl Pts',(-95.4591620531666,4.75542049839504,
135.94481876907));
#194827=CARTESIAN_POINT('Ctrl Pts',(-95.7376096769794,6.89523396518648,
129.582033865318));
#194828=CARTESIAN_POINT('Ctrl Pts',(-96.0160573007924,2.69866426887766,
124.342507532899));
#194829=CARTESIAN_POINT('Ctrl Pts',(-96.2945049246052,-3.97784605345104,
125.041108506217));
#194830=CARTESIAN_POINT('Ctrl Pts',(-96.5729525484182,-6.99891018124123,
131.035856619345));
#194831=CARTESIAN_POINT('Ctrl Pts',(-96.8514001722308,-3.58831776824163,
136.817871216047));
#194832=CARTESIAN_POINT('Ctrl Pts',(-97.129847796044,3.11976337470375,137.073763349068));
#194833=CARTESIAN_POINT('Ctrl Pts',(-97.4082954198568,6.96093438520996,
131.56838064919));
#194834=CARTESIAN_POINT('Ctrl Pts',(-97.6867430436697,4.40534675625846,
125.360900864701));
#194835=CARTESIAN_POINT('Ctrl Pts',(-97.9651906674826,-2.1985393285419,
124.155694665303));
#194836=CARTESIAN_POINT('Ctrl Pts',(-98.2436382912955,-6.78207517502872,
129.060287670645));
#194837=CARTESIAN_POINT('Ctrl Pts',(-98.5220859151084,-5.13321525845608,
135.567598511506));
#194838=CARTESIAN_POINT('Ctrl Pts',(-98.8005335389213,1.23281870913114,
137.697726424945));
#194839=CARTESIAN_POINT('Ctrl Pts',(-99.0789811627341,6.4659525095689,133.493187921042));
#194840=CARTESIAN_POINT('Ctrl Pts',(-99.3574287865471,5.7571918330539,126.817748481762));
#194841=CARTESIAN_POINT('Ctrl Pts',(-99.6358764103599,-0.242146883580649,
123.805810838454));
#194842=CARTESIAN_POINT('Ctrl Pts',(-99.9143240341728,-6.01896444373747,
127.225198543987));
#194843=CARTESIAN_POINT('Ctrl Pts',(-100.192771657986,-6.26464772285957,
133.93366134335));
#194844=CARTESIAN_POINT('Ctrl Pts',(-100.471219281798,-0.753425789729175,
137.766449650557));
#194845=CARTESIAN_POINT('Ctrl Pts',(-100.749666905611,5.45015763726631,
135.201418253402));
#194846=CARTESIAN_POINT('Ctrl Pts',(-101.028114529424,6.64531245061667,
128.595705697122));
#194847=CARTESIAN_POINT('Ctrl Pts',(-101.306562153237,1.73374976341167,
124.019639113937));
#194848=CARTESIAN_POINT('Ctrl Pts',(-101.58500977705,-4.77104425798471,
125.678400140516));
#194849=CARTESIAN_POINT('Ctrl Pts',(-101.863457400863,-6.89148168476197,
132.047668428412));
#194850=CARTESIAN_POINT('Ctrl Pts',(-102.141905024676,-2.67898411084018,
137.274397577103));
#194851=CARTESIAN_POINT('Ctrl Pts',(-102.420352648489,3.99536898529432,
136.555478838857));
#194852=CARTESIAN_POINT('Ctrl Pts',(-102.698800272302,6.99817316856906,
130.551563412989));
#194853=CARTESIAN_POINT('Ctrl Pts',(-102.977247896115,3.56999808969468,
124.779956268296));
#194854=CARTESIAN_POINT('Ctrl Pts',(-103.255695519928,-3.13883082950684,
124.544482412068));
#194855=CARTESIAN_POINT('Ctrl Pts',(-103.53414314374,-6.96322755680218,
130.061530814641));
#194856=CARTESIAN_POINT('Ctrl Pts',(-103.812590767553,-4.38875833197407,
136.261203516848));
#194857=CARTESIAN_POINT('Ctrl Pts',(-104.091038391366,2.21876539717438,
137.44630417621));
#194858=CARTESIAN_POINT('Ctrl Pts',(-104.369486015179,6.78735211903507,
132.52778318216));
#194859=CARTESIAN_POINT('Ctrl Pts',(-104.647933638992,5.11869382408742,
126.02552104512));
#194860=CARTESIAN_POINT('Ctrl Pts',(-104.926381262805,-1.25379403310144,
123.914779015865));
#194861=CARTESIAN_POINT('Ctrl Pts',(-105.204828886617,-6.47410642511416,
128.135225903801));
#194862=CARTESIAN_POINT('Ctrl Pts',(-105.483276510431,-5.74503129012806,
134.808477199207));
#194863=CARTESIAN_POINT('Ctrl Pts',(-105.761724134243,0.263446940103889,
137.802140968053));
#194864=CARTESIAN_POINT('Ctrl Pts',(-106.040171758056,6.02983030247923,
134.365186455377));
#194865=CARTESIAN_POINT('Ctrl Pts',(-106.318619381869,6.25509419046252,
127.656006953765));
#194866=CARTESIAN_POINT('Ctrl Pts',(-106.597067005682,0.732232095750508,
123.840010663559));
#194867=CARTESIAN_POINT('Ctrl Pts',(-106.875514629495,-5.46351552342998,
126.423911753675));
#194868=CARTESIAN_POINT('Ctrl Pts',(-107.153962253308,-6.63855928414971,
133.033231352883));
#194869=CARTESIAN_POINT('Ctrl Pts',(-107.432409877121,-1.71309137438684,
137.594327632723));
#194870=CARTESIAN_POINT('Ctrl Pts',(-107.710857500934,4.78662381927155,
135.915775933963));
#194871=CARTESIAN_POINT('Ctrl Pts',(-107.989305124746,6.8876655625929,129.540083265954));
#194872=CARTESIAN_POINT('Ctrl Pts',(-108.26775274856,2.65927913505975,124.326199720693));
#194873=CARTESIAN_POINT('Ctrl Pts',(-108.546200372372,-4.0128549045848,
125.065429563905));
#194874=CARTESIAN_POINT('Ctrl Pts',(-108.824647996185,-6.99737132577695,
131.078456683062));
#194875=CARTESIAN_POINT('Ctrl Pts',(-109.103095619998,-3.5516453391731,
136.839602908365));
#194876=CARTESIAN_POINT('Ctrl Pts',(-109.381543243811,3.1578692066097,137.054656306401));
#194877=CARTESIAN_POINT('Ctrl Pts',(-109.659990867624,6.96545622200577,
131.525993310316));
#194878=CARTESIAN_POINT('Ctrl Pts',(-109.938438491437,4.37212925083209,
125.334185123311));
#194879=CARTESIAN_POINT('Ctrl Pts',(-110.21688611525,-2.23897091146772,
124.169200982596));
#194880=CARTESIAN_POINT('Ctrl Pts',(-110.495333739063,-6.79256618593892,
129.10160440085));
#194881=CARTESIAN_POINT('Ctrl Pts',(-110.773781362875,-5.10412497083799,
135.598757597999));
#194882=CARTESIAN_POINT('Ctrl Pts',(-111.052228986688,1.27475774209554,
137.690094189444));
#194883=CARTESIAN_POINT('Ctrl Pts',(-111.330676610501,6.48220036542147,
133.453778015119));
#194884=CARTESIAN_POINT('Ctrl Pts',(-111.609124234314,5.73281752601749,
126.782776683677));
#194885=CARTESIAN_POINT('Ctrl Pts',(-111.887571858127,-0.284744556090853,
123.807414522182));
#194886=CARTESIAN_POINT('Ctrl Pts',(-112.16601948194,-6.04064030169634,
127.261904002525));
#194887=CARTESIAN_POINT('Ctrl Pts',(-112.444467105753,-6.24548271172772,
133.971738053464));
#194888=CARTESIAN_POINT('Ctrl Pts',(-112.722914729566,-0.71103161847358,
137.770906975801));
#194889=CARTESIAN_POINT('Ctrl Pts',(-113.001362353379,5.47682279633179,
135.16816012963));
#194890=CARTESIAN_POINT('Ctrl Pts',(-113.279809977192,6.63174461897671,
128.55529471533));
#194891=CARTESIAN_POINT('Ctrl Pts',(-113.558257601004,1.69241711551747,
124.009210992206));
#194892=CARTESIAN_POINT('Ctrl Pts',(-113.836705224817,-4.80215903792943,
125.707537813274));
#194893=CARTESIAN_POINT('Ctrl Pts',(-114.11515284863,-6.88378563403075,
132.089595797848));
#194894=CARTESIAN_POINT('Ctrl Pts',(-114.393600472443,-2.63954952408134,
137.290585438973));
#194895=CARTESIAN_POINT('Ctrl Pts',(-114.672048096256,4.03030364933543,
136.531051338922));
#194896=CARTESIAN_POINT('Ctrl Pts',(-114.950495720069,6.99650466029252,
130.508968230339));
#194897=CARTESIAN_POINT('Ctrl Pts',(-115.228943343882,3.53325968669456,
124.758336294896));
#194898=CARTESIAN_POINT('Ctrl Pts',(-115.507390967695,-3.17687832964389,
124.563705347279));
#194899=CARTESIAN_POINT('Ctrl Pts',(-115.785838591507,-6.96762036017394,
130.103931720095));
#194900=CARTESIAN_POINT('Ctrl Pts',(-116.06428621532,-4.35545966688232,
136.287818031834));
#194901=CARTESIAN_POINT('Ctrl Pts',(-116.342733839133,2.25915568424066,
137.432674861647));
#194902=CARTESIAN_POINT('Ctrl Pts',(-116.621181462946,6.79771732743703,
132.486434712303));
#194903=CARTESIAN_POINT('Ctrl Pts',(-116.899629086759,5.08950883367243,
125.994450643782));
#194904=CARTESIAN_POINT('Ctrl Pts',(-117.178076710572,-1.2957096419083,
123.922538864004));
#194905=CARTESIAN_POINT('Ctrl Pts',(-117.456524334385,-6.49023425551004,
128.174685080065));
#194906=CARTESIAN_POINT('Ctrl Pts',(-117.734971958198,-5.7205506538686,
134.843374648297));
#194907=CARTESIAN_POINT('Ctrl Pts',(-118.013419582011,0.306039534242538,
137.800407639092));
#194908=CARTESIAN_POINT('Ctrl Pts',(-118.291867205823,6.05139434124684,
134.328415193001));
#194909=CARTESIAN_POINT('Ctrl Pts',(-118.570314829636,6.23581337569426,
127.617988751722));
#194910=CARTESIAN_POINT('Ctrl Pts',(-118.848762453449,0.689824554297045,
123.835682392233));
#194911=CARTESIAN_POINT('Ctrl Pts',(-119.127210077262,-5.49007933269568,
126.457250882969));
#194912=CARTESIAN_POINT('Ctrl Pts',(-119.405657701075,-6.62486851822702,
133.073600851681));
#194913=CARTESIAN_POINT('Ctrl Pts',(-119.684105324888,-1.67172717832737,
137.60462990379));
#194914=CARTESIAN_POINT('Ctrl Pts',(-119.962552948701,4.81764977004229,
135.886543693482));
#194915=CARTESIAN_POINT('Ctrl Pts',(-120.241000572514,6.87984193501854,
129.498179514853));
#194916=CARTESIAN_POINT('Ctrl Pts',(-120.519448196327,2.61979546067638,
124.310131959122));
#194917=CARTESIAN_POINT('Ctrl Pts',(-120.79789582014,-4.04771505790416,
125.089963279793));
#194918=CARTESIAN_POINT('Ctrl Pts',(-121.076343443952,-6.9955731801444,
131.121046590047));
#194919=CARTESIAN_POINT('Ctrl Pts',(-121.354791067765,-3.51484130258126,
136.86111096256));
#194920=CARTESIAN_POINT('Ctrl Pts',(-121.633238691578,3.19585802251066,
137.035317656727));
#194921=CARTESIAN_POINT('Ctrl Pts',(-121.911686315391,6.96971995125911,
131.483579231079));
#194922=CARTESIAN_POINT('Ctrl Pts',(-122.190133939204,4.3387497345494,125.307672081285));
#194923=CARTESIAN_POINT('Ctrl Pts',(-122.468581563017,-2.2793195285039,
124.182953168171));
#194924=CARTESIAN_POINT('Ctrl Pts',(-122.74702918683,-6.80280549581075,
129.142984227312));
#194925=CARTESIAN_POINT('Ctrl Pts',(-123.025476810643,-5.07484554799192,
135.629739026348));
#194926=CARTESIAN_POINT('Ctrl Pts',(-123.303924434456,1.31664953844379,
137.682206800553));
#194927=CARTESIAN_POINT('Ctrl Pts',(-123.582372058268,6.49820802095541,
133.414269934058));
#194928=CARTESIAN_POINT('Ctrl Pts',(-123.860819682081,5.7082307873194,126.747953906865));
#194929=CARTESIAN_POINT('Ctrl Pts',(-124.139267305894,-0.327331677286216,
123.809277480321));
#194930=CARTESIAN_POINT('Ctrl Pts',(-124.417714929707,-6.06209232150722,
127.298740728095));
#194931=CARTESIAN_POINT('Ctrl Pts',(-124.69616255352,-6.22608627193705,
134.009697395242));
#194932=CARTESIAN_POINT('Ctrl Pts',(-124.974610177333,-0.668611099680587,
137.77510615311));
#194933=CARTESIAN_POINT('Ctrl Pts',(-125.253057801146,5.50328500971429,
135.134740303665));
#194934=CARTESIAN_POINT('Ctrl Pts',(-125.531505424959,6.61793104560076,
128.514967073503));
#194935=CARTESIAN_POINT('Ctrl Pts',(-125.809953048772,1.6510217544855,123.999034667242));
#194936=CARTESIAN_POINT('Ctrl Pts',(-126.088400672584,-4.8330958721059,
125.736864350674));
#194937=CARTESIAN_POINT('Ctrl Pts',(-126.366848296398,-6.87583450209069,
132.131475542423));
#194938=CARTESIAN_POINT('Ctrl Pts',(-126.64529592021,-2.60001712784396,
137.306532951397));
#194939=CARTESIAN_POINT('Ctrl Pts',(-126.923743544023,4.06508896899354,
136.506411634357));
#194940=CARTESIAN_POINT('Ctrl Pts',(-127.202191167836,6.99457689396224,
130.466383993564));
#194941=CARTESIAN_POINT('Ctrl Pts',(-127.480638791649,3.49639035745773,
124.736940359153));
#194942=CARTESIAN_POINT('Ctrl Pts',(-127.759086415462,-3.21480810938582,
124.583159532264));
#194943=CARTESIAN_POINT('Ctrl Pts',(-128.037534039275,-6.97175497581086,
130.146358580199));
#194944=CARTESIAN_POINT('Ctrl Pts',(-128.315981663087,-4.32199960863106,
136.314229355287));
#194945=CARTESIAN_POINT('Ctrl Pts',(-128.594429286901,2.29946225746178,
137.418799932461));
#194946=CARTESIAN_POINT('Ctrl Pts',(-128.872876910713,6.80783064392392,
132.44502391257));
#194947=CARTESIAN_POINT('Ctrl Pts',(-129.151324534526,5.06013524963555,
125.963558475429));
#194948=CARTESIAN_POINT('Ctrl Pts',(-129.429772158339,-1.33757723771771,
123.930553720578));
#194949=CARTESIAN_POINT('Ctrl Pts',(-129.708219782152,-6.50612158788957,
128.214241699924));
#194950=CARTESIAN_POINT('Ctrl Pts',(-129.986667405965,-5.69585804050008,
134.878122430239));
#194951=CARTESIAN_POINT('Ctrl Pts',(-130.265115029778,0.348620787973942,
137.798415069035));
#194952=CARTESIAN_POINT('Ctrl Pts',(-130.543562653591,6.07273414337257,
134.291513345486));
#194953=CARTESIAN_POINT('Ctrl Pts',(-130.822010277403,6.21630149056731,
127.58008862186));
#194954=CARTESIAN_POINT('Ctrl Pts',(-131.100457901217,0.647391451141708,
123.831612347843));
#194955=CARTESIAN_POINT('Ctrl Pts',(-131.378905525029,-5.5164397050528,
126.490751096011));
#194956=CARTESIAN_POINT('Ctrl Pts',(-131.657353148842,-6.61093226536518,
133.113886262947));
#194957=CARTESIAN_POINT('Ctrl Pts',(-131.935800772655,-1.63030103580305,
137.614680188378));
#194958=CARTESIAN_POINT('Ctrl Pts',(-132.214248396468,4.848497201029,135.857123130838));
#194959=CARTESIAN_POINT('Ctrl Pts',(-132.492696020281,6.87176337237162,
129.456324164773));
#194960=CARTESIAN_POINT('Ctrl Pts',(-132.771143644094,2.58021470880796,
124.294304843582));
#194961=CARTESIAN_POINT('Ctrl Pts',(-133.049591267907,-4.08242522165371,
125.114708744776));
#194962=CARTESIAN_POINT('Ctrl Pts',(-133.32803889172,-6.99351581097555,
131.163624762118));
#194963=CARTESIAN_POINT('Ctrl Pts',(-133.606486515532,-3.47790702225152,
136.882394581644));
#194964=CARTESIAN_POINT('Ctrl Pts',(-133.884934139345,3.23372841471757,
137.015748116649));
#194965=CARTESIAN_POINT('Ctrl Pts',(-134.163381763158,6.97372541497715,
131.441139983145));
#194966=CARTESIAN_POINT('Ctrl Pts',(-134.441829386971,4.30520944429882,
125.281362721075));
#194967=CARTESIAN_POINT('Ctrl Pts',(-134.720277010784,-2.31958368451587,
124.196950712432));
#194968=CARTESIAN_POINT('Ctrl Pts',(-134.998724634597,-6.81279272522359,
129.184425616688));
#194969=CARTESIAN_POINT('Ctrl Pts',(-135.27717225841,-5.04537807487797,
135.660541648527));
#194970=CARTESIAN_POINT('Ctrl Pts',(-135.555619882223,1.35849254585843,
137.674064550544));
#194971=CARTESIAN_POINT('Ctrl Pts',(-135.834067506036,6.51397488300169,
133.374665141848));
#194972=CARTESIAN_POINT('Ctrl Pts',(-136.112515129848,5.68343252803032,
126.713281441693));
#194973=CARTESIAN_POINT('Ctrl Pts',(-136.390962753662,-0.369906669086523,
123.811399643837));
#194974=CARTESIAN_POINT('Ctrl Pts',(-136.669410377474,-6.08331970825794,
127.335707355701));
#194975=CARTESIAN_POINT('Ctrl Pts',(-136.947858001288,-6.20645912223011,
134.047537962086));
#194976=CARTESIAN_POINT('Ctrl Pts',(-137.2263056251,-0.626165805256695,
137.779047026878));
#194977=CARTESIAN_POINT('Ctrl Pts',(-137.504753248913,5.52954329684707,
135.101160013885));
#194978=CARTESIAN_POINT('Ctrl Pts',(-137.783200872726,6.60387224235649,
128.474724265995));
#194979=CARTESIAN_POINT('Ctrl Pts',(-138.061648496539,1.60956521423443,
123.989110516135));
#194980=CARTESIAN_POINT('Ctrl Pts',(-138.340096120352,-4.86385361413656,
125.766378666012));
#194981=CARTESIAN_POINT('Ctrl Pts',(-138.618543744165,-6.86762858357524,
132.173306110266));
#194982=CARTESIAN_POINT('Ctrl Pts',(-138.896991367977,-2.56038838701599,
137.322239523433));
#194983=CARTESIAN_POINT('Ctrl Pts',(-139.17543899179,4.09972365528409,136.481560638194));
#194984=CARTESIAN_POINT('Ctrl Pts',(-139.453886615603,6.99238994101352,
130.423812280637));
#194985=CARTESIAN_POINT('Ctrl Pts',(-139.732334239416,3.45939146819007,
124.715769253897));
#194986=CARTESIAN_POINT('Ctrl Pts',(-140.010781863229,-3.25261876323132,
124.602844246145));
#194987=CARTESIAN_POINT('Ctrl Pts',(-140.289229487042,-6.97563125050334,
130.188809822811));
#194988=CARTESIAN_POINT('Ctrl Pts',(-140.567677110855,-4.28837939709471,
136.340436508528));
#194989=CARTESIAN_POINT('Ctrl Pts',(-140.846124734668,2.33968362326381,
137.404679902793));
#194990=CARTESIAN_POINT('Ctrl Pts',(-141.124572358481,6.81769169374202,
132.403552317457));
#194991=CARTESIAN_POINT('Ctrl Pts',(-141.403019982293,5.03057416042698,
125.932845684778));
#194992=CARTESIAN_POINT('Ctrl Pts',(-141.681467606106,-1.37939526911043,
123.938823288595));
#194993=CARTESIAN_POINT('Ctrl Pts',(-141.959915229919,-6.52176783354029,
128.253894297592));
#194994=CARTESIAN_POINT('Ctrl Pts',(-142.238362853732,-5.67095436501806,
134.912719257437));
#194995=CARTESIAN_POINT('Ctrl Pts',(-142.516810477545,0.39118912343359,
137.796163331718));
#194996=CARTESIAN_POINT('Ctrl Pts',(-142.795258101358,6.09384891810056,
134.254482280245));
#194997=CARTESIAN_POINT('Ctrl Pts',(-143.073705725171,6.19655925810344,
127.542307968582));
#194998=CARTESIAN_POINT('Ctrl Pts',(-143.352153348984,0.604934358657401,
123.827800681205));
#194999=CARTESIAN_POINT('Ctrl Pts',(-143.630600972796,-5.54259566370794,
126.524411151443));
#195000=CARTESIAN_POINT('Ctrl Pts',(-143.90904859661,-6.59675104197701,
133.154086093891));
#195001=CARTESIAN_POINT('Ctrl Pts',(-144.187496220422,-1.58881448187379,
137.624478114069));
#195002=CARTESIAN_POINT('Ctrl Pts',(-144.465943844235,4.87916496916901,
135.827515336221));
#195003=CARTESIAN_POINT('Ctrl Pts',(-144.744391468048,6.86343017400547,
129.41451876668));
#195004=CARTESIAN_POINT('Ctrl Pts',(-145.022839091861,2.54053834613545,
124.278718960552));
#195005=CARTESIAN_POINT('Ctrl Pts',(-145.301286715674,-4.11698410963516,
125.139665041902));
#195006=CARTESIAN_POINT('Ctrl Pts',(-145.579734339487,-6.99119929450595,
131.206189621523));
#195007=CARTESIAN_POINT('Ctrl Pts',(-145.8581819633,-3.44084386679896,136.903452976945));
#195008=CARTESIAN_POINT('Ctrl Pts',(-146.136629587113,3.27147897992919,
136.995948411323));
#195009=CARTESIAN_POINT('Ctrl Pts',(-146.415077210925,6.97747246473481,
131.398677139117));
#195010=CARTESIAN_POINT('Ctrl Pts',(-146.693524834738,4.27150962292939,
125.255258017582));
#195011=CARTESIAN_POINT('Ctrl Pts',(-146.971972458551,-2.35976188750221,
124.211193096699));
#195012=CARTESIAN_POINT('Ctrl Pts',(-147.250420082364,-6.82252750409623,
129.225927033352));
#195013=CARTESIAN_POINT('Ctrl Pts',(-147.528867706177,-5.01572364342383,
135.69116432313));
#195014=CARTESIAN_POINT('Ctrl Pts',(-147.80731532999,1.40028521383297,137.665667741127));
#195015=CARTESIAN_POINT('Ctrl Pts',(-148.085762953803,6.52950036731291,
133.334965106058));
#195016=CARTESIAN_POINT('Ctrl Pts',(-148.364210577616,5.65842366705879,
126.678760572968));
#195017=CARTESIAN_POINT('Ctrl Pts',(-148.642658201429,-0.412467953858535,
123.813780934094));
#195018=CARTESIAN_POINT('Ctrl Pts',(-148.921105825242,-6.10432167535963,
127.372802515528));
#195019=CARTESIAN_POINT('Ctrl Pts',(-149.199553449054,-6.18660198989778,
134.085258351801));
#195020=CARTESIAN_POINT('Ctrl Pts',(-149.478001072867,-0.583697308029368,
137.782729451077));
#195021=CARTESIAN_POINT('Ctrl Pts',(-149.75644869668,5.55559668471987,135.067420504625));
#195022=CARTESIAN_POINT('Ctrl Pts',(-150.034896320493,6.58956873019717,
128.434567784019));
#195023=CARTESIAN_POINT('Ctrl Pts',(-150.313343944306,1.56804903095274,
123.979438906626));
#195024=CARTESIAN_POINT('Ctrl Pts',(-150.591791568119,-4.89443112428377,
125.796079665625));
#195025=CARTESIAN_POINT('Ctrl Pts',(-150.870239191931,-6.85916818255639,
132.21508595133));
#195026=CARTESIAN_POINT('Ctrl Pts',(-151.148686815745,-2.52066477005453,
137.33770457307));
#195027=CARTESIAN_POINT('Ctrl Pts',(-151.427134439557,4.13420642480782,
136.456499271296));
#195028=CARTESIAN_POINT('Ctrl Pts',(-151.705582063371,6.98994388248347,
130.381254669068));
#195029=CARTESIAN_POINT('Ctrl Pts',(-151.984029687183,3.42226438989971,
124.694823763634));
#195030=CARTESIAN_POINT('Ctrl Pts',(-152.262477310996,-3.29030889009209,
124.622758759495));
#195031=CARTESIAN_POINT('Ctrl Pts',(-152.540924934809,-6.97924904061452,
130.231283874884));
#195032=CARTESIAN_POINT('Ctrl Pts',(-152.819372558622,-4.25460027808296,
136.366438520441));
#195033=CARTESIAN_POINT('Ctrl Pts',(-153.097820182435,2.37981829122829,
137.390315295868));
#195034=CARTESIAN_POINT('Ctrl Pts',(-153.376267806248,6.82730011148789,
132.362021463707));
#195035=CARTESIAN_POINT('Ctrl Pts',(-153.654715430061,5.00082666144207,
125.902313409905));
#195036=CARTESIAN_POINT('Ctrl Pts',(-153.933163053873,-1.42116218650446,
123.947347261623));
#195037=CARTESIAN_POINT('Ctrl Pts',(-154.211610677687,-6.53717241268631,
128.293641403726));
#195038=CARTESIAN_POINT('Ctrl Pts',(-154.490058301499,-5.64584055023574,
134.947163847896));
#195039=CARTESIAN_POINT('Ctrl Pts',(-154.768505925312,0.433742963236675,
137.79365251058));
#195040=CARTESIAN_POINT('Ctrl Pts',(-155.046953549125,6.11473788301669,
134.217323369476));
#195041=CARTESIAN_POINT('Ctrl Pts',(-155.325401172938,6.17658740985663,
127.504648191865));
#195042=CARTESIAN_POINT('Ctrl Pts',(-155.603848796751,0.562454850108638,
123.824247533559));
#195043=CARTESIAN_POINT('Ctrl Pts',(-155.882296420564,-5.5685462394425,
126.558229801974));
#195044=CARTESIAN_POINT('Ctrl Pts',(-156.160744044376,-6.5823253735531,
133.194198854895));
#195045=CARTESIAN_POINT('Ctrl Pts',(-156.43919166819,-1.54726905384013,
137.634023317798));
#195046=CARTESIAN_POINT('Ctrl Pts',(-156.717639292002,4.90965193805665,
135.79772140676));
#195047=CARTESIAN_POINT('Ctrl Pts',(-156.996086915816,6.8548426487106,129.372764869687));
#195048=CARTESIAN_POINT('Ctrl Pts',(-157.274534539628,2.50076784287941,
124.263374887574));
#195049=CARTESIAN_POINT('Ctrl Pts',(-157.552982163441,-4.15139044125659,
125.164831246407));
#195050=CARTESIAN_POINT('Ctrl Pts',(-157.831429787254,-6.98862371657603,
131.248739591007));
#195051=CARTESIAN_POINT('Ctrl Pts',(-158.109877411067,-3.40365320961064,
136.924285368134));
#195052=CARTESIAN_POINT('Ctrl Pts',(-158.38832503488,3.30910831928323,136.975919274434));
#195053=CARTESIAN_POINT('Ctrl Pts',(-158.666772658693,6.98096096168483,
131.356192272474));
#195054=CARTESIAN_POINT('Ctrl Pts',(-158.945220282506,4.23765151920024,
125.229358938127));
#195055=CARTESIAN_POINT('Ctrl Pts',(-159.223667906319,-2.39985264864321,
124.225679793212));
#195056=CARTESIAN_POINT('Ctrl Pts',(-159.502115530131,-6.8320094717036,
129.267486939452));
#195057=CARTESIAN_POINT('Ctrl Pts',(-159.780563153944,-4.98588335248574,
135.721605915426));
#195058=CARTESIAN_POINT('Ctrl Pts',(-160.059010777757,1.44202599372318,
137.657016683454));
#195059=CARTESIAN_POINT('Ctrl Pts',(-160.33745840157,6.54478389858708,133.295171297791));
#195060=CARTESIAN_POINT('Ctrl Pts',(-160.615906025383,5.63320513111742,
126.644392579866));
#195061=CARTESIAN_POINT('Ctrl Pts',(-160.894353649196,-0.455013954479453,
123.816421262852));
#195062=CARTESIAN_POINT('Ctrl Pts',(-161.172801273009,-6.12509744457689,
127.410024833003));
#195063=CARTESIAN_POINT('Ctrl Pts',(-161.451248896821,-6.16651561075379,
134.122857166646));
#195064=CARTESIAN_POINT('Ctrl Pts',(-161.729696520635,-0.541207181682879,
137.786153289251));
#195065=CARTESIAN_POINT('Ctrl Pts',(-162.008144144447,5.58144420791359,
135.033523026113));
#195066=CARTESIAN_POINT('Ctrl Pts',(-162.286591768261,6.57502103914602,
128.394499115588));
#195067=CARTESIAN_POINT('Ctrl Pts',(-162.565039392073,1.52647474303778,
123.970020197102));
#195068=CARTESIAN_POINT('Ctrl Pts',(-162.843487015886,-4.92482726948487,
125.825966248931));
#195069=CARTESIAN_POINT('Ctrl Pts',(-163.121934639699,-6.85045361253876,
132.256813517449));
#195070=CARTESIAN_POINT('Ctrl Pts',(-163.400382263512,-2.48084774893327,
137.352927527244));
#195071=CARTESIAN_POINT('Ctrl Pts',(-163.678829887325,4.16853599979124,
136.431228462323));
#195072=CARTESIAN_POINT('Ctrl Pts',(-163.957277511138,6.98723880901292,
130.338712735846));
#195073=CARTESIAN_POINT('Ctrl Pts',(-164.23572513495,3.3850104983435,124.674104664506));
#195074=CARTESIAN_POINT('Ctrl Pts',(-164.514172758764,-3.32787709334726,
124.642902334375));
#195075=CARTESIAN_POINT('Ctrl Pts',(-164.792620382576,-6.98260821208591,
130.273779162525));
#195076=CARTESIAN_POINT('Ctrl Pts',(-165.07106800639,-4.22066350329308,
136.392234427513));
#195077=CARTESIAN_POINT('Ctrl Pts',(-165.349515630202,2.4198647741513,137.37570664397));
#195078=CARTESIAN_POINT('Ctrl Pts',(-165.627963254015,6.83665554111671,
132.320432890263));
#195079=CARTESIAN_POINT('Ctrl Pts',(-165.906410877828,4.97089385498702,
125.871962782194));
#195080=CARTESIAN_POINT('Ctrl Pts',(-166.184858501641,-1.46287644221077,
123.956125323802));
#195081=CARTESIAN_POINT('Ctrl Pts',(-166.463306125454,-6.55233475450377,
128.333481545486));
#195082=CARTESIAN_POINT('Ctrl Pts',(-166.741753749267,-5.62051752675643,
134.981454925258));
#195083=CARTESIAN_POINT('Ctrl Pts',(-167.020201373079,0.476280730534997,
137.790882698662));
#195084=CARTESIAN_POINT('Ctrl Pts',(-167.298648996893,6.13540026407138,
134.180037990117));
#195085=CARTESIAN_POINT('Ctrl Pts',(-167.577096620705,6.15638668589229,
127.467110687205));
#195086=CARTESIAN_POINT('Ctrl Pts',(-167.855544244518,0.519954499587912,
123.820953036571));
#195087=CARTESIAN_POINT('Ctrl Pts',(-168.133991868331,-5.5942904706483,
126.592205794446));
#195088=CARTESIAN_POINT('Ctrl Pts',(-168.412439492144,-6.56765579464175,
133.234223059563));
#195089=CARTESIAN_POINT('Ctrl Pts',(-168.690887115956,-1.50566629118217,
137.643315445865));
#195090=CARTESIAN_POINT('Ctrl Pts',(-168.96933473977,4.93995697798634,135.767742446477));
#195091=CARTESIAN_POINT('Ctrl Pts',(-169.247782363582,6.84600111470013,
129.331064021001));
#195092=CARTESIAN_POINT('Ctrl Pts',(-169.526229987396,2.46090467275213,
124.248273193229));
#195093=CARTESIAN_POINT('Ctrl Pts',(-169.804677611208,-4.18564294157836,
125.190206425745));
#195094=CARTESIAN_POINT('Ctrl Pts',(-170.083125235021,-6.98578917262369,
131.291273093865));
#195095=CARTESIAN_POINT('Ctrl Pts',(-170.361572858834,-3.36633642880185,
136.944890983262));
#195096=CARTESIAN_POINT('Ctrl Pts',(-170.640020482647,3.34661503841248,
136.955661448171));
#195097=CARTESIAN_POINT('Ctrl Pts',(-170.91846810646,6.98419077655865,131.313686957504));
#195098=CARTESIAN_POINT('Ctrl Pts',(-171.196915730273,4.20363638773547,
125.203666442409));
#195099=CARTESIAN_POINT('Ctrl Pts',(-171.475363354086,-2.43985448236259,
124.240410265162));
#195100=CARTESIAN_POINT('Ctrl Pts',(-171.753810977898,-6.84123827668714,
129.309103794972));
#195101=CARTESIAN_POINT('Ctrl Pts',(-172.032258601712,-4.9558583078063,
135.751865297389));
#195102=CARTESIAN_POINT('Ctrl Pts',(-172.310706225524,1.48371333881067,
137.648111698089));
#195103=CARTESIAN_POINT('Ctrl Pts',(-172.589153849337,6.55982491048677,
133.255285191615));
#195104=CARTESIAN_POINT('Ctrl Pts',(-172.86760147315,5.60777785468832,126.610178735912));
#195105=CARTESIAN_POINT('Ctrl Pts',(-173.146049096963,-0.497543094390354,
123.819320532272));
#195106=CARTESIAN_POINT('Ctrl Pts',(-173.424496720776,-6.14564624605571,
127.447372928838));
#195107=CARTESIAN_POINT('Ctrl Pts',(-173.702944344589,-6.14620072910595,
134.160333013378));
#195108=CARTESIAN_POINT('Ctrl Pts',(-173.981391968402,-0.498697000705985,
137.789318414533));
#195109=CARTESIAN_POINT('Ctrl Pts',(-174.259839592215,5.60708490864046,
134.999468834432));
#195110=CARTESIAN_POINT('Ctrl Pts',(-174.538287216028,6.56022970827155,
128.354519745462));
#195111=CARTESIAN_POINT('Ctrl Pts',(-174.81673483984,1.48484389103961,123.960854736574));
#195112=CARTESIAN_POINT('Ctrl Pts',(-175.095182463654,-4.95504092340126,
125.85603730847));
#195113=CARTESIAN_POINT('Ctrl Pts',(-175.373630087466,-6.8414851964426,
132.298487262391));
#195114=CARTESIAN_POINT('Ctrl Pts',(-175.652077711279,-2.44093879908611,
137.367907821863));
#195115=CARTESIAN_POINT('Ctrl Pts',(-175.930525335092,4.20271110814107,
136.405749147692));
#195116=CARTESIAN_POINT('Ctrl Pts',(-176.208972958905,6.98427482083815,
130.296188057377));
#195117=CARTESIAN_POINT('Ctrl Pts',(-176.487420582718,3.3476311739788,124.653612724266));
#195118=CARTESIAN_POINT('Ctrl Pts',(-176.765868206531,-3.36532198089259,
124.663274224357));
#195119=CARTESIAN_POINT('Ctrl Pts',(-177.044315830343,-6.98570864044213,
130.316294111058));
#195120=CARTESIAN_POINT('Ctrl Pts',(-177.322763454156,-4.18657033026512,
136.417823273865));
#195121=CARTESIAN_POINT('Ctrl Pts',(-177.601211077969,2.4598215880947,137.360854488428));
#195122=CARTESIAN_POINT('Ctrl Pts',(-177.879658701782,6.84575763596098,
132.278788138201));
#195123=CARTESIAN_POINT('Ctrl Pts',(-178.158106325595,4.94077685023126,
125.841794926299));
#195124=CARTESIAN_POINT('Ctrl Pts',(-178.436553949408,-1.50453649049278,
123.965157149858));
#195125=CARTESIAN_POINT('Ctrl Pts',(-178.715001573221,-6.56725429714808,
128.373413246577));
#195126=CARTESIAN_POINT('Ctrl Pts',(-178.993449197033,-5.59498623293233,
135.015591218853));
#195127=CARTESIAN_POINT('Ctrl Pts',(-179.271896820847,0.518800849074927,
137.787853998597));
#195128=CARTESIAN_POINT('Ctrl Pts',(-179.550344444659,6.15583529561319,
134.142627523792));
#195129=CARTESIAN_POINT('Ctrl Pts',(-179.828792068472,6.13595783475539,
127.429696845569));
#195130=CARTESIAN_POINT('Ctrl Pts',(-180.107239692285,0.477434881962636,
123.81791731232));
#195131=CARTESIAN_POINT('Ctrl Pts',(-180.385687316098,-5.61982740336347,
126.626337869861));
#195132=CARTESIAN_POINT('Ctrl Pts',(-180.664134939911,-6.55274284882976,
133.274157224785));
#195133=CARTESIAN_POINT('Ctrl Pts',(-180.942582563724,-1.4640077355066,
137.652354153945));
#195134=CARTESIAN_POINT('Ctrl Pts',(-181.221030187537,4.97007896599344,
135.737579566256));
#195135=CARTESIAN_POINT('Ctrl Pts',(-181.499477811349,6.83690589960112,
129.289417765863));
#195136=CARTESIAN_POINT('Ctrl Pts',(-181.777925435163,2.42095031289641,
124.233414437113));
#195137=CARTESIAN_POINT('Ctrl Pts',(-182.056373058975,-4.21974034136189,
125.215789639631));
#195138=CARTESIAN_POINT('Ctrl Pts',(-182.334820682789,-6.98269576768506,
131.333788554001));
#195139=CARTESIAN_POINT('Ctrl Pts',(-182.613268306601,-3.32889490715784,
136.965269058779));
#195140=CARTESIAN_POINT('Ctrl Pts',(-182.891715930414,3.38399774748988,
136.935175683191));
#195141=CARTESIAN_POINT('Ctrl Pts',(-183.170163554227,6.98716178967534,
131.27116276926));
#195142=CARTESIAN_POINT('Ctrl Pts',(-183.44861117804,4.16946548897866,125.178181482475));
#195143=CARTESIAN_POINT('Ctrl Pts',(-183.727058801853,-2.47976590637605,
124.255383966707));
#195144=CARTESIAN_POINT('Ctrl Pts',(-184.005506425666,-6.85021357707087,
129.350776057783));
#195145=CARTESIAN_POINT('Ctrl Pts',(-184.283954049479,-4.92564962197493,
135.781941347746));
#195146=CARTESIAN_POINT('Ctrl Pts',(-184.562401673291,1.52534570435398,
137.63895311501));
#195147=CARTESIAN_POINT('Ctrl Pts',(-184.840849297105,6.5746228456623,133.215308265529));
#195148=CARTESIAN_POINT('Ctrl Pts',(-185.119296920917,5.58214277998856,
126.576120308909));
#195149=CARTESIAN_POINT('Ctrl Pts',(-185.39774454473,-0.540053797659538,
123.822478634922));
#195150=CARTESIAN_POINT('Ctrl Pts',(-185.676192168543,-6.16596731835295,
127.484845419088));
#195151=CARTESIAN_POINT('Ctrl Pts',(-185.954639792356,-6.12565809773001,
134.197684503321));
#195152=CARTESIAN_POINT('Ctrl Pts',(-186.233087416169,-0.456168340327589,
137.792224709632));
#195153=CARTESIAN_POINT('Ctrl Pts',(-186.511535039982,5.63251783677319,
134.965259191474));
#195154=CARTESIAN_POINT('Ctrl Pts',(-186.789982663795,6.54519528567348,
128.314631155089));
#195155=CARTESIAN_POINT('Ctrl Pts',(-187.068430287608,1.44315801760525,
123.951942864674));
#195156=CARTESIAN_POINT('Ctrl Pts',(-187.346877911421,-4.98507096645316,
125.886291729948));
#195157=CARTESIAN_POINT('Ctrl Pts',(-187.625325535233,-6.83226326659722,
132.340105641921));
#195158=CARTESIAN_POINT('Ctrl Pts',(-187.903773159046,-2.40093939935397,
137.382644901827));
#195159=CARTESIAN_POINT('Ctrl Pts',(-188.182220782859,4.23673048348491,
136.380062271549));
#195160=CARTESIAN_POINT('Ctrl Pts',(-188.460668406672,6.98105202779173,
130.25368220943));
#195161=CARTESIAN_POINT('Ctrl Pts',(-188.739116030485,3.31012780190951,
124.633348702251));
#195162=CARTESIAN_POINT('Ctrl Pts',(-189.017563654298,-3.40264216519462,
124.683873674555));
#195163=CARTESIAN_POINT('Ctrl Pts',(-189.296011278111,-6.98855021079573,
130.358827145076));
#195164=CARTESIAN_POINT('Ctrl Pts',(-189.574458901924,-4.15232202233378,
136.443204111294));
#195165=CARTESIAN_POINT('Ctrl Pts',(-189.852906525736,2.49968725244504,
137.345759379595));
#195166=CARTESIAN_POINT('Ctrl Pts',(-190.13135414955,6.85460605873784,132.237088750687));
#195167=CARTESIAN_POINT('Ctrl Pts',(-190.409801773362,4.91047676317321,
125.8118109601));
#195168=CARTESIAN_POINT('Ctrl Pts',(-190.688249397175,-1.5461407876216,
123.974442405114));
#195169=CARTESIAN_POINT('Ctrl Pts',(-190.966697020988,-6.58193048776853,
128.413435027317));
#195170=CARTESIAN_POINT('Ctrl Pts',(-191.245144644801,-5.56924761483672,
135.049571463749));
#195171=CARTESIAN_POINT('Ctrl Pts',(-191.523592268614,0.561301743259386,
137.784566522618));
#195172=CARTESIAN_POINT('Ctrl Pts',(-191.802039892427,6.17604222041412,
134.105093356759));
#195173=CARTESIAN_POINT('Ctrl Pts',(-192.08048751624,6.11530161344434,127.39240805334));
#195174=CARTESIAN_POINT('Ctrl Pts',(-192.358935140053,0.43489757281158,
123.815140473294));
#195175=CARTESIAN_POINT('Ctrl Pts',(-192.637382763865,-5.64515609130746,
126.660624763449));
#195176=CARTESIAN_POINT('Ctrl Pts',(-192.915830387678,-6.53758708872167,
133.313999870785));
#195177=CARTESIAN_POINT('Ctrl Pts',(-193.194278011491,-1.42229493048546,
137.661139107108));
#195178=CARTESIAN_POINT('Ctrl Pts',(-193.472725635304,5.00001678589681,
135.707233883791));
#195179=CARTESIAN_POINT('Ctrl Pts',(-193.751173259117,6.82755734043935,
129.247827647489));
#195180=CARTESIAN_POINT('Ctrl Pts',(-194.02962088293,2.38090624383734,124.218799169824));
#195181=CARTESIAN_POINT('Ctrl Pts',(-194.308068506743,-4.25368137711504,
125.241579940071));
#195182=CARTESIAN_POINT('Ctrl Pts',(-194.586516130556,-6.97934361638637,
131.376284395991));
#195183=CARTESIAN_POINT('Ctrl Pts',(-194.864963754369,-3.29133003208973,
136.985418839569));
#195184=CARTESIAN_POINT('Ctrl Pts',(-195.143411378181,3.42125506128717,
136.914462738605));
#195185=CARTESIAN_POINT('Ctrl Pts',(-195.421859001994,6.98987389094189,
131.22862128349));
#195186=CARTESIAN_POINT('Ctrl Pts',(-195.700306625807,4.13514008914463,
125.152905002676));
#195187=CARTESIAN_POINT('Ctrl Pts',(-195.97875424962,-2.51958544175274,
124.270600342989));
#195188=CARTESIAN_POINT('Ctrl Pts',(-196.257201873433,-6.85893504027095,
129.392502183704));
#195189=CARTESIAN_POINT('Ctrl Pts',(-196.535649497246,-4.89525841438522,
135.811832952018));
#195190=CARTESIAN_POINT('Ctrl Pts',(-196.814097121059,1.56692154765205,
137.629541273595));
#195191=CARTESIAN_POINT('Ctrl Pts',(-197.092544744872,6.58917715577019,
133.175242000891));
#195192=CARTESIAN_POINT('Ctrl Pts',(-197.370992368684,5.55630085693524,
126.542218560906));
#195193=CARTESIAN_POINT('Ctrl Pts',(-197.649439992498,-0.582544489036021,
123.825895453776));
#195194=CARTESIAN_POINT('Ctrl Pts',(-197.92788761631,-6.18605990846357,
127.522440915193));
#195195=CARTESIAN_POINT('Ctrl Pts',(-198.206335240123,-6.10488847784037,
134.234910252398));
#195196=CARTESIAN_POINT('Ctrl Pts',(-198.484782863936,-0.413622776464342,
137.79487206686));
#195197=CARTESIAN_POINT('Ctrl Pts',(-198.763230487749,5.657742049887,134.930895364888));
#195198=CARTESIAN_POINT('Ctrl Pts',(-199.041678111562,6.52991832845634,
128.274834822558));
#195199=CARTESIAN_POINT('Ctrl Pts',(-199.320125735375,1.40141866741961,
123.943284911633));
#195200=CARTESIAN_POINT('Ctrl Pts',(-199.598573359188,-5.01491628586802,
125.916728392279));
#195201=CARTESIAN_POINT('Ctrl Pts',(-199.877020983,-6.82278816472322,132.381667113854));
#195202=CARTESIAN_POINT('Ctrl Pts',(-200.155468606814,-2.36085103192995,
137.397138221046));
#195203=CARTESIAN_POINT('Ctrl Pts',(-200.433916230626,4.27059286522247,
136.354168785731));
#195204=CARTESIAN_POINT('Ctrl Pts',(-200.712363854439,6.97757054929515,
130.211196767073));
#195205=CARTESIAN_POINT('Ctrl Pts',(-200.990811478252,3.27250177183757,
124.613313349352));
#195206=CARTESIAN_POINT('Ctrl Pts',(-201.269259102065,-3.43983626333961,
124.704699921646));
#195207=CARTESIAN_POINT('Ctrl Pts',(-201.547706725878,-6.9911328178512,
130.401376688499));
#195208=CARTESIAN_POINT('Ctrl Pts',(-201.826154349691,-4.1179198485831,
136.468375999304));
#195209=CARTESIAN_POINT('Ctrl Pts',(-202.104601973504,2.53946028996452,
137.330421876826));
#195210=CARTESIAN_POINT('Ctrl Pts',(-202.383049597317,6.86320048156709,
132.195336272904));
#195211=CARTESIAN_POINT('Ctrl Pts',(-202.66149722113,4.87999471659204,125.782011994664));
#195212=CARTESIAN_POINT('Ctrl Pts',(-202.939944844942,-1.5876877919352,
123.983980745501));
#195213=CARTESIAN_POINT('Ctrl Pts',(-203.218392468755,-6.59636278253501,
128.453545404684));
#195214=CARTESIAN_POINT('Ctrl Pts',(-203.496840092568,-5.54330262622176,
135.083394400798));
#195215=CARTESIAN_POINT('Ctrl Pts',(-203.775287716381,0.603781838200554,
137.781020392543));
#195216=CARTESIAN_POINT('Ctrl Pts',(-204.053735340194,6.19602028969954,
134.067436879861));
#195217=CARTESIAN_POINT('Ctrl Pts',(-204.332182964007,6.09441878738321,
127.355245692268));
#195218=CARTESIAN_POINT('Ctrl Pts',(-204.61063058782,0.392344148371673,
123.812622622391));
#195219=CARTESIAN_POINT('Ctrl Pts',(-204.889078211633,-5.67027559591653,
126.69506520469));
#195220=CARTESIAN_POINT('Ctrl Pts',(-205.167525835445,-6.5221890759199,
133.353749521179));
#195221=CARTESIAN_POINT('Ctrl Pts',(-205.445973459259,-1.38052942180316,
137.66966997982));
#195222=CARTESIAN_POINT('Ctrl Pts',(-205.724421083071,5.02976932833932,
135.676706523556));
#195223=CARTESIAN_POINT('Ctrl Pts',(-206.002868706884,6.8179557836299,129.206295207017));
#195224=CARTESIAN_POINT('Ctrl Pts',(-206.281316330697,2.340773949421,124.204427932937));
#195225=CARTESIAN_POINT('Ctrl Pts',(-206.55976395451,-4.28746479114066,
125.267576371395));
#195226=CARTESIAN_POINT('Ctrl Pts',(-206.838211578323,-6.97573284294384,
131.418759045136));
#195227=CARTESIAN_POINT('Ctrl Pts',(-207.116659202136,-3.253643195576,137.005339578972));
#195228=CARTESIAN_POINT('Ctrl Pts',(-207.395106825949,3.4583855992191,136.893523381939));
#195229=CARTESIAN_POINT('Ctrl Pts',(-207.673554449762,6.99232697986142,
131.186064076586));
#195230=CARTESIAN_POINT('Ctrl Pts',(-207.952002073574,4.10066146017411,
125.127837939644));
#195231=CARTESIAN_POINT('Ctrl Pts',(-208.230449697387,-2.55931161296347,
124.286058830161));
#195232=CARTESIAN_POINT('Ctrl Pts',(-208.5088973212,-6.86740234311116,129.434280626559));
#195233=CARTESIAN_POINT('Ctrl Pts',(-208.787344945013,-4.86468581119477,
135.841539002563));
#195234=CARTESIAN_POINT('Ctrl Pts',(-209.065792568826,1.60843932809579,
137.619876522599));
#195235=CARTESIAN_POINT('Ctrl Pts',(-209.344240192639,6.60348730149562,
133.135087882371));
#195236=CARTESIAN_POINT('Ctrl Pts',(-209.622687816452,5.53025304311036,
126.508474748144));
#195237=CARTESIAN_POINT('Ctrl Pts',(-209.901135440264,-0.625013594012848,
123.829570862223));
#195238=CARTESIAN_POINT('Ctrl Pts',(-210.179583064078,-6.20592327184948,
127.56015802404));
#195239=CARTESIAN_POINT('Ctrl Pts',(-210.45803068789,-6.08389263906328,
134.272008881199));
#195240=CARTESIAN_POINT('Ctrl Pts',(-210.736478311703,-0.371061885656257,
137.797260388114));
#195241=CARTESIAN_POINT('Ctrl Pts',(-211.014925935516,5.68275661328764,
134.896378628042));
#195242=CARTESIAN_POINT('Ctrl Pts',(-211.293373559329,6.51439940271492,
128.235132222534));
#195243=CARTESIAN_POINT('Ctrl Pts',(-211.571821183142,1.35962738715011,
123.934881198276));
#195244=CARTESIAN_POINT('Ctrl Pts',(-211.850268806955,-5.04457577571481,
125.947346167619));
#195245=CARTESIAN_POINT('Ctrl Pts',(-212.128716430768,-6.81306024192543,
132.423170138115));
#195246=CARTESIAN_POINT('Ctrl Pts',(-212.40716405458,-2.32067518230222,
137.411387242468));
#195247=CARTESIAN_POINT('Ctrl Pts',(-212.685611678394,4.30429699857105,
136.32806964973));
#195248=CARTESIAN_POINT('Ctrl Pts',(-212.964059302206,6.97383051435588,
130.168733304621));
#195249=CARTESIAN_POINT('Ctrl Pts',(-213.24250692602,3.23475447800865,124.593507407987));
#195250=CARTESIAN_POINT('Ctrl Pts',(-213.520954549832,-3.47690289708716,
124.725752193909));
#195251=CARTESIAN_POINT('Ctrl Pts',(-213.799402173646,-6.99345636590915,
130.443941164641));
#195252=CARTESIAN_POINT('Ctrl Pts',(-214.077849797458,-4.08336508379785,
136.49333800514));
#195253=CARTESIAN_POINT('Ctrl Pts',(-214.356297421271,2.57913922684953,
137.314842548456));
#195254=CARTESIAN_POINT('Ctrl Pts',(-214.634745045084,6.87154058597789,
132.153532252007));
#195255=CARTESIAN_POINT('Ctrl Pts',(-214.913192668897,4.84933184001288,
125.752399134204));
#195256=CARTESIAN_POINT('Ctrl Pts',(-215.19164029271,-1.62917596389355,
123.993771817573));
#195257=CARTESIAN_POINT('Ctrl Pts',(-215.470087916522,-6.61055064665203,
128.493742892374));
#195258=CARTESIAN_POINT('Ctrl Pts',(-215.748535540335,-5.51715222849034,
135.117058776675));
#195259=CARTESIAN_POINT('Ctrl Pts',(-216.026983164148,0.646239559784443,
137.777215739773));
#195260=CARTESIAN_POINT('Ctrl Pts',(-216.305430787961,6.21576876317433,
134.029659488472));
#195261=CARTESIAN_POINT('Ctrl Pts',(-216.583878411774,6.0733101303926,127.318211139417));
#195262=CARTESIAN_POINT('Ctrl Pts',(-216.862326035587,0.349776185474419,
123.810363852911));
#195263=CARTESIAN_POINT('Ctrl Pts',(-217.1407736594,-5.69518498637811,126.729657917385));
#195264=CARTESIAN_POINT('Ctrl Pts',(-217.419221283213,-6.50654938100331,
133.393404703032));
#195265=CARTESIAN_POINT('Ctrl Pts',(-217.697668907026,-1.33871275709491,
137.67794645597));
#195266=CARTESIAN_POINT('Ctrl Pts',(-217.976116530838,5.05933549082977,
135.64599861675));
#195267=CARTESIAN_POINT('Ctrl Pts',(-218.254564154652,6.80810158496121,
129.164821983446));
#195268=CARTESIAN_POINT('Ctrl Pts',(-218.533011778464,2.30055491676597,
124.190301258982));
#195269=CARTESIAN_POINT('Ctrl Pts',(-218.811459402277,-4.32108933158155,
125.293777970294));
#195270=CARTESIAN_POINT('Ctrl Pts',(-219.08990702609,-6.97186358115499,
131.461210927519));
#195271=CARTESIAN_POINT('Ctrl Pts',(-219.368354649903,-3.21583579411804,
137.02503053882));
#195272=CARTESIAN_POINT('Ctrl Pts',(-219.646802273716,3.49538798540175,
136.872358389107));
#195273=CARTESIAN_POINT('Ctrl Pts',(-219.925249897529,6.99452096553273,
131.143492725519));
#195274=CARTESIAN_POINT('Ctrl Pts',(-220.203697521342,4.06603087968498,
125.102981222246));
#195275=CARTESIAN_POINT('Ctrl Pts',(-220.482145145155,-2.59894294794204,
124.301758855404));
#195276=CARTESIAN_POINT('Ctrl Pts',(-220.760592768967,-6.87561517183164,
129.476109838232));
#195277=CARTESIAN_POINT('Ctrl Pts',(-221.03904039278,-4.83393294528274,
135.87105839861));
#195278=CARTESIAN_POINT('Ctrl Pts',(-221.317488016593,1.64989750722823,
137.609959220154));
#195279=CARTESIAN_POINT('Ctrl Pts',(-221.595935640406,6.61755275257056,
133.094847397895));
#195280=CARTESIAN_POINT('Ctrl Pts',(-221.874383264219,5.5040003037252,126.474890121013));
#195281=CARTESIAN_POINT('Ctrl Pts',(-222.152830888031,-0.667459538880483,
123.83350472407));
#195282=CARTESIAN_POINT('Ctrl Pts',(-222.431278511845,-6.22555667246622,
127.597995348007));
#195283=CARTESIAN_POINT('Ctrl Pts',(-222.709726135657,-6.06267135940695,
134.308979015016));
#195284=CARTESIAN_POINT('Ctrl Pts',(-222.988173759471,-0.328487245014279,
137.799389584896));
#195285=CARTESIAN_POINT('Ctrl Pts',(-223.266621383283,5.70756060005303,
134.861710259961));
#195286=CARTESIAN_POINT('Ctrl Pts',(-223.545069007096,6.49863908350723,
128.195524826214));
#195287=CARTESIAN_POINT('Ctrl Pts',(-223.823516630909,1.31778572538753,
123.926732036005));
#195288=CARTESIAN_POINT('Ctrl Pts',(-224.101964254722,-5.07404833695195,
125.978143921416));
#195289=CARTESIAN_POINT('Ctrl Pts',(-224.380411878535,-6.80307985867417,
132.464613176793));
#195290=CARTESIAN_POINT('Ctrl Pts',(-224.658859502348,-2.28041333920269,
137.425391438088));
#195291=CARTESIAN_POINT('Ctrl Pts',(-224.937307126161,4.33784163461131,
136.30176583066));
#195292=CARTESIAN_POINT('Ctrl Pts',(-225.215754749974,6.96983206156226,
130.126293395573));
#195293=CARTESIAN_POINT('Ctrl Pts',(-225.494202373786,3.19688731916334,
124.573931612073));
#195294=CARTESIAN_POINT('Ctrl Pts',(-225.7726499976,-3.51384069291894,124.747029711241));
#195295=CARTESIAN_POINT('Ctrl Pts',(-226.051097621412,-6.9955207688696,
130.486518996257));
#195296=CARTESIAN_POINT('Ctrl Pts',(-226.329545245225,-4.04865900841799,
136.518089203828));
#195297=CARTESIAN_POINT('Ctrl Pts',(-226.607992869038,2.61872259278156,
137.299021971784));
#195298=CARTESIAN_POINT('Ctrl Pts',(-226.886440492851,6.87962606292594,
132.111678237058));
#195299=CARTESIAN_POINT('Ctrl Pts',(-227.164888116664,4.81848926965818,
125.722973476035));
#195300=CARTESIAN_POINT('Ctrl Pts',(-227.443335740477,-1.67060376613766,
124.003815258517));
#195301=CARTESIAN_POINT('Ctrl Pts',(-227.72178336429,-6.62449355438458,
128.534026000853));
#195302=CARTESIAN_POINT('Ctrl Pts',(-228.000230988102,-5.49079739065326,
135.150563343936));
#195303=CARTESIAN_POINT('Ctrl Pts',(-228.278678611916,0.688673334723007,
137.773152705292));
#195304=CARTESIAN_POINT('Ctrl Pts',(-228.557126235728,6.23528690905198,
133.991762582447));
#195305=CARTESIAN_POINT('Ctrl Pts',(-228.835573859542,6.05197642466173,
127.281305767118));
#195306=CARTESIAN_POINT('Ctrl Pts',(-229.114021483354,0.307195261492642,
123.808364248553));
#195307=CARTESIAN_POINT('Ctrl Pts',(-229.392469107167,-5.7198833396657,
126.764401619687));
#195308=CARTESIAN_POINT('Ctrl Pts',(-229.670916730979,-6.49066858350677,
133.432963946903));
#195309=CARTESIAN_POINT('Ctrl Pts',(-229.949364354793,-1.29684648589306,
137.685968228869));
#195310=CARTESIAN_POINT('Ctrl Pts',(-230.227811978605,5.0887141777831,135.615111301269));
#195311=CARTESIAN_POINT('Ctrl Pts',(-230.506259602419,6.79799510958498,
129.123409513582));
#195312=CARTESIAN_POINT('Ctrl Pts',(-230.784707226231,2.26025063620168,
124.176419671429));
#195313=CARTESIAN_POINT('Ctrl Pts',(-231.063154850045,-4.35455375246839,
125.32018376586));
#195314=CARTESIAN_POINT('Ctrl Pts',(-231.341602473857,-6.96773597439774,
131.503638470075));
#195315=CARTESIAN_POINT('Ctrl Pts',(-231.62005009767,-3.17790922868121,
137.044490989456));
#195316=CARTESIAN_POINT('Ctrl Pts',(-231.898497721483,3.53226084869627,
136.850968544386));
#195317=CARTESIAN_POINT('Ctrl Pts',(-232.176945345296,6.99645576665798,
131.100908807788));
#195318=CARTESIAN_POINT('Ctrl Pts',(-232.455392969109,4.03124963092651,
125.078335771559));
#195319=CARTESIAN_POINT('Ctrl Pts',(-232.733840592922,-2.63847797813309,
124.317699836946));
#195320=CARTESIAN_POINT('Ctrl Pts',(-233.012288216734,-6.88357322210384,
129.517988268725));
#195321=CARTESIAN_POINT('Ctrl Pts',(-233.290735840548,-4.80300095620762,
135.900390046307));
#195322=CARTESIAN_POINT('Ctrl Pts',(-233.56918346436,1.6912945488023,137.599789733751));
#195323=CARTESIAN_POINT('Ctrl Pts',(-233.847631088173,6.63137298779474,
133.05452203859));
#195324=CARTESIAN_POINT('Ctrl Pts',(-234.126078711986,5.47754361158473,
126.441465924004));
#195325=CARTESIAN_POINT('Ctrl Pts',(-234.404526335799,-0.709880750790079,
123.837696893545));
#195326=CARTESIAN_POINT('Ctrl Pts',(-234.682973959612,-6.24495938279112,
127.635951485018));
#195327=CARTESIAN_POINT('Ctrl Pts',(-234.961421583425,-6.04122542523402,
134.345819283911));
#195328=CARTESIAN_POINT('Ctrl Pts',(-235.239869207238,-0.285900432155891,
137.801259578306));
#195329=CARTESIAN_POINT('Ctrl Pts',(-235.518316831051,5.73215309106056,
134.826891545298));
#195330=CARTESIAN_POINT('Ctrl Pts',(-235.796764454864,6.48263795483918,
128.156014101264));
#195331=CARTESIAN_POINT('Ctrl Pts',(-236.075212078676,1.27589523259052,
123.918837726791));
#195332=CARTESIAN_POINT('Ctrl Pts',(-236.353659702489,-5.10333287746112,
126.009120512446));
#195333=CARTESIAN_POINT('Ctrl Pts',(-236.632107326302,-6.79284738479763,
132.505994694203));
#195334=CARTESIAN_POINT('Ctrl Pts',(-236.910554950115,-2.24006699454776,
137.439150288976));
#195335=CARTESIAN_POINT('Ctrl Pts',(-237.189002573928,4.3712255303347,136.275258303218));
#195336=CARTESIAN_POINT('Ctrl Pts',(-237.467450197741,6.96557533907847,
130.083878612554));
#195337=CARTESIAN_POINT('Ctrl Pts',(-237.745897821554,3.15890169848239,
124.554586686994));
#195338=CARTESIAN_POINT('Ctrl Pts',(-238.024345445366,-3.55064828209192,
124.768531685198));
#195339=CARTESIAN_POINT('Ctrl Pts',(-238.30279306918,-6.99732595023538,
130.529108605612));
#195340=CARTESIAN_POINT('Ctrl Pts',(-238.581240692992,-4.01380290848946,
136.542628678202));
#195341=CARTESIAN_POINT('Ctrl Pts',(-238.859688316805,2.65820892098533,
137.282960733047));
#195342=CARTESIAN_POINT('Ctrl Pts',(-239.138135940618,6.88745661279959,
132.069775778975));
#195343=CARTESIAN_POINT('Ctrl Pts',(-239.416583564431,4.78746814841248,
125.693736110535));
#195344=CARTESIAN_POINT('Ctrl Pts',(-239.695031188244,-1.71196966354462,
124.014110696169));
#195345=CARTESIAN_POINT('Ctrl Pts',(-239.973478812057,-6.63819098907155,
128.574393237416));
#195346=CARTESIAN_POINT('Ctrl Pts',(-240.25192643587,-5.46423908930053,
135.183906861057));
#195347=CARTESIAN_POINT('Ctrl Pts',(-240.530374059683,0.731081590618679,
137.768831439659));
#195348=CARTESIAN_POINT('Ctrl Pts',(-240.808821683496,6.25457400407998,
133.95374756607));
#195349=CARTESIAN_POINT('Ctrl Pts',(-241.087269307308,6.03041846071876,
127.244530942912));
#195350=CARTESIAN_POINT('Ctrl Pts',(-241.365716931122,0.264602954276818,
123.806623883412));
#195351=CARTESIAN_POINT('Ctrl Pts',(-241.644164554934,-5.74436974057257,
126.799295024156));
#195352=CARTESIAN_POINT('Ctrl Pts',(-241.922612178747,-6.47454727189872,
133.472425786911));
#195353=CARTESIAN_POINT('Ctrl Pts',(-242.20105980256,-1.25493215956847,
137.693735001267));
#195354=CARTESIAN_POINT('Ctrl Pts',(-242.479507426373,5.11790430056101,
135.584045721651));
#195355=CARTESIAN_POINT('Ctrl Pts',(-242.757955050186,6.78763673199965,
129.082059331979));
#195356=CARTESIAN_POINT('Ctrl Pts',(-243.036402673998,2.21986260121965,
124.162783684665));
#195357=CARTESIAN_POINT('Ctrl Pts',(-243.314850297812,-4.38785681376436,
125.346792779616));
#195358=CARTESIAN_POINT('Ctrl Pts',(-243.593297921624,-6.96335017562108,
131.54604010063));
#195359=CARTESIAN_POINT('Ctrl Pts',(-243.871745545438,-3.13986490465013,
137.063720209766));
#195360=CARTESIAN_POINT('Ctrl Pts',(-244.15019316925,3.56900282276695,136.829354640385));
#195361=CARTESIAN_POINT('Ctrl Pts',(-244.428640793064,6.99813131154132,
131.058313901354));
#195362=CARTESIAN_POINT('Ctrl Pts',(-244.707088416876,3.99631900273028,
125.053902500829));
#195363=CARTESIAN_POINT('Ctrl Pts',(-244.985536040689,-2.67791523855318,
124.333881184089));
#195364=CARTESIAN_POINT('Ctrl Pts',(-245.263983664501,-6.89127619903846,
129.559914366219));
#195365=CARTESIAN_POINT('Ctrl Pts',(-245.542431288315,-4.7718909901659,
135.929532858758));
#195366=CARTESIAN_POINT('Ctrl Pts',(-245.820878912128,1.73262891883438,
137.589368440225));
#195367=CARTESIAN_POINT('Ctrl Pts',(-246.09932653594,6.6449474950541,133.014113298726));
#195368=CARTESIAN_POINT('Ctrl Pts',(-246.377774159753,5.45088394705135,
126.408203395661));
#195369=CARTESIAN_POINT('Ctrl Pts',(-246.656221783566,-0.752275657806765,
123.842147215306));
#195370=CARTESIAN_POINT('Ctrl Pts',(-246.934669407379,-6.26413068384941,
127.674025028594));
#195371=CARTESIAN_POINT('Ctrl Pts',(-247.213117031192,-6.01955563123113,
134.382528322752));
#195372=CARTESIAN_POINT('Ctrl Pts',(-247.491564655005,-0.243303025152602,
137.802870299053));
#195373=CARTESIAN_POINT('Ctrl Pts',(-247.770012278818,5.75653317502817,
134.791923774272));
#195374=CARTESIAN_POINT('Ctrl Pts',(-248.048459902631,6.46639660963695,
128.116601511768));
#195375=CARTESIAN_POINT('Ctrl Pts',(-248.326907526444,1.23395746102625,
123.91119856316));
#195376=CARTESIAN_POINT('Ctrl Pts',(-248.605355150257,-5.13242831209467,
126.040274792862));
#195377=CARTESIAN_POINT('Ctrl Pts',(-248.883802774069,-6.78236319946242,
132.547313156937));
#195378=CARTESIAN_POINT('Ctrl Pts',(-249.162250397883,-2.19963764338714,
137.452663285294));
#195379=CARTESIAN_POINT('Ctrl Pts',(-249.440698021695,4.40444744868852,
136.24854804965));
#195380=CARTESIAN_POINT('Ctrl Pts',(-249.719145645508,6.96106050463867,
130.041490527264));
#195381=CARTESIAN_POINT('Ctrl Pts',(-249.997593269321,3.12079902353814,
124.535473349588));
#195382=CARTESIAN_POINT('Ctrl Pts',(-250.276040893134,-3.58732430068758,
124.790257319018));
#195383=CARTESIAN_POINT('Ctrl Pts',(-250.554488516946,-6.99887184311352,
130.571708414529));
#195384=CARTESIAN_POINT('Ctrl Pts',(-250.83293614076,-3.97879807562073,
136.566955518948));
#195385=CARTESIAN_POINT('Ctrl Pts',(-251.111383764572,2.69759674828547,
137.26665942739));
#195386=CARTESIAN_POINT('Ctrl Pts',(-251.389831388386,6.89503194542569,
132.027826430486));
#195387=CARTESIAN_POINT('Ctrl Pts',(-251.668279012198,4.75626962579305,
125.66468812107));
#195388=CARTESIAN_POINT('Ctrl Pts',(-251.946726636011,-1.75327212332407,
124.024657749096));
#195389=CARTESIAN_POINT('Ctrl Pts',(-252.225174259824,-6.65164244307981,
128.614843106116));
#195390=CARTESIAN_POINT('Ctrl Pts',(-252.503621883637,-5.43747830869239,
135.217088092717));
#195391=CARTESIAN_POINT('Ctrl Pts',(-252.78206950745,0.773462756270139,
137.764252102553));
#195392=CARTESIAN_POINT('Ctrl Pts',(-253.060517131263,6.2736293330892,133.91561584884));
#195393=CARTESIAN_POINT('Ctrl Pts',(-253.338964755075,6.00863703830687,
127.207888027921));
#195394=CARTESIAN_POINT('Ctrl Pts',(-253.617412378889,0.222000840393564,
123.805142824969));
#195395=CARTESIAN_POINT('Ctrl Pts',(-253.895860002702,-5.76864327852066,
126.83433683216));
#195396=CARTESIAN_POINT('Ctrl Pts',(-254.174307626514,-6.45818604965135,
133.511788771436));
#195397=CARTESIAN_POINT('Ctrl Pts',(-254.452755250327,-1.21297131977014,
137.701246465247));
#195398=CARTESIAN_POINT('Ctrl Pts',(-254.73120287414,5.14690475579816,135.55280306703));
#195399=CARTESIAN_POINT('Ctrl Pts',(-255.009650497953,6.7770268770417,129.040772899161));
#195400=CARTESIAN_POINT('Ctrl Pts',(-255.288098121766,2.17939223099114,
124.149393939406));
#195401=CARTESIAN_POINT('Ctrl Pts',(-255.566545745579,-4.42099713522674,
125.37360376984));
#195402=CARTESIAN_POINT('Ctrl Pts',(-255.844993369392,-6.95870662337211,
131.588414730824));
#195403=CARTESIAN_POINT('Ctrl Pts',(-256.123440993205,-3.10170371057109,
137.082716575498));
#195404=CARTESIAN_POINT('Ctrl Pts',(-256.401888617018,3.60561156199617,
136.807519199501));
#195405=CARTESIAN_POINT('Ctrl Pts',(-256.68033624083,6.99954939633056,131.01570633407));
#195406=CARTESIAN_POINT('Ctrl Pts',(-256.958783864643,3.96123678073902,
125.029688453078));
#195407=CARTESIAN_POINT('Ctrl Pts',(-257.237231488456,-2.71724664265218,
124.350290708114));
#195408=CARTESIAN_POINT('Ctrl Pts',(-257.515679112269,-6.89873632689917,
129.601908459729));
#195409=CARTESIAN_POINT('Ctrl Pts',(-257.794126736082,-4.74058057908887,
135.958444437253));
#195410=CARTESIAN_POINT('Ctrl Pts',(-258.072574359895,1.77385448465437,
137.578773744179));
#195411=CARTESIAN_POINT('Ctrl Pts',(-258.351021983707,6.6583599873155,132.973475360041));
#195412=CARTESIAN_POINT('Ctrl Pts',(-258.629469607521,5.42386327951784,
126.375381938049));
#195413=CARTESIAN_POINT('Ctrl Pts',(-258.907917231333,-0.794342416617398,
123.846330221273));
#195414=CARTESIAN_POINT('Ctrl Pts',(-259.186364855146,-6.28363694765996,
127.713206958712));
#195415=CARTESIAN_POINT('Ctrl Pts',(-259.464812478959,-5.99659113747434,
134.41722675292));
#195416=CARTESIAN_POINT('Ctrl Pts',(-259.743260102772,-0.202727240537578,
137.807801967267));
#195417=CARTESIAN_POINT('Ctrl Pts',(-260.021707726585,5.7845923739281,134.749768174183));
#195418=CARTESIAN_POINT('Ctrl Pts',(-260.253747413096,6.33253704604016,
129.202365411857));
#195419=CARTESIAN_POINT('Ctrl Pts',(-260.439389088604,3.82430165355141,
125.973250269562));
#195420=CARTESIAN_POINT('Ctrl Pts',(-260.532214889509,1.97943258085903,
125.138073123498));
#195421=CARTESIAN_POINT('Ctrl Pts',(-260.578632753112,1.00712299976162,
124.970230583726));
#195422=CARTESIAN_POINT('Ctrl Pts',(-260.,4.64727355878983,134.479645829435));
#195423=CARTESIAN_POINT('Ctrl Pts',(-260.,4.72445468230523,134.365238782885));
#195424=CARTESIAN_POINT('Ctrl Pts',(-260.,4.79717385008238,134.248223015737));
#195425=CARTESIAN_POINT('Ctrl Pts',(-260.,4.86519974457552,134.128712980314));
#195426=CARTESIAN_POINT('Ctrl Pts',(-260.,4.94591766572252,133.986905192449));
#195427=CARTESIAN_POINT('Ctrl Pts',(-260.,5.02002908188102,133.841585703171));
#195428=CARTESIAN_POINT('Ctrl Pts',(-260.,5.08757949274479,133.693228223168));
#195429=CARTESIAN_POINT('Ctrl Pts',(-260.,5.15592794008602,133.543118056849));
#195430=CARTESIAN_POINT('Ctrl Pts',(-260.,5.21755948895336,133.389896884846));
#195431=CARTESIAN_POINT('Ctrl Pts',(-260.,5.2724692973062,133.234041404611));
#195432=CARTESIAN_POINT('Ctrl Pts',(-260.,5.32751299525585,133.077805893413));
#195433=CARTESIAN_POINT('Ctrl Pts',(-260.,5.37580210608346,132.918922369593));
#195434=CARTESIAN_POINT('Ctrl Pts',(-260.,5.41727981065124,132.757869539038));
#195435=CARTESIAN_POINT('Ctrl Pts',(-260.,5.4388804792077,132.673996797064));
#195436=CARTESIAN_POINT('Ctrl Pts',(-260.,5.4586329773621,132.589535771846));
#195437=CARTESIAN_POINT('Ctrl Pts',(-260.,5.47652375629486,132.504555076365));
#195438=CARTESIAN_POINT('Ctrl Pts',(-260.,5.48230964795087,132.477072254138));
#195439=CARTESIAN_POINT('Ctrl Pts',(-260.,5.48790079663348,132.449535089018));
#195440=CARTESIAN_POINT('Ctrl Pts',(-260.,5.49329665994448,132.421945928666));
#195441=CARTESIAN_POINT('Ctrl Pts',(-260.,5.49715720698584,132.402206872054));
#195442=CARTESIAN_POINT('Ctrl Pts',(-260.,5.50091711018986,132.382444492444));
#195443=CARTESIAN_POINT('Ctrl Pts',(-260.,5.50457455091086,132.362669472875));
#195444=CARTESIAN_POINT('Ctrl Pts',(-260.,5.53421387188956,132.202415842791));
#195445=CARTESIAN_POINT('Ctrl Pts',(-260.,5.55716564037324,132.041144769358));
#195446=CARTESIAN_POINT('Ctrl Pts',(-260.,5.57346020341767,131.879315471242));
#195447=CARTESIAN_POINT('Ctrl Pts',(-260.,5.58976582436389,131.717376351679));
#195448=CARTESIAN_POINT('Ctrl Pts',(-260.,5.59940512720595,131.554877419695));
#195449=CARTESIAN_POINT('Ctrl Pts',(-260.,5.60235628880471,131.392278361123));
#195450=CARTESIAN_POINT('Ctrl Pts',(-260.,5.60526194489148,131.232186502907));
#195451=CARTESIAN_POINT('Ctrl Pts',(-260.,5.6016839329031,131.071996842801));
#195452=CARTESIAN_POINT('Ctrl Pts',(-260.,5.59155299666625,130.912159283332));
#195453=CARTESIAN_POINT('Ctrl Pts',(-260.,5.58151245621597,130.753747914057));
#195454=CARTESIAN_POINT('Ctrl Pts',(-260.,5.56503528598279,130.595681704101));
#195455=CARTESIAN_POINT('Ctrl Pts',(-260.,5.542008385626,130.438420204743));
#195456=CARTESIAN_POINT('Ctrl Pts',(-260.,5.53509379108037,130.391197196485));
#195457=CARTESIAN_POINT('Ctrl Pts',(-260.,5.52758829894611,130.344046935964));
#195458=CARTESIAN_POINT('Ctrl Pts',(-260.,5.51948805734336,130.296982392616));
#195459=CARTESIAN_POINT('Ctrl Pts',(-260.,5.51571179868533,130.275041332334));
#195460=CARTESIAN_POINT('Ctrl Pts',(-260.,5.51180627565152,130.253118905161));
#195461=CARTESIAN_POINT('Ctrl Pts',(-260.,5.50777107109651,130.23121644617));
#195462=CARTESIAN_POINT('Ctrl Pts',(-260.,5.50419825781951,130.211823774692));
#195463=CARTESIAN_POINT('Ctrl Pts',(-260.,5.50052560593342,130.192456675027));
#195464=CARTESIAN_POINT('Ctrl Pts',(-260.,5.49675319635138,130.173116366892));
#195465=CARTESIAN_POINT('Ctrl Pts',(-260.,5.4666002147623,130.018528710794));
#195466=CARTESIAN_POINT('Ctrl Pts',(-260.,5.43007631185038,129.865642846568));
#195467=CARTESIAN_POINT('Ctrl Pts',(-260.,5.38715622994236,129.714878921409));
#195468=CARTESIAN_POINT('Ctrl Pts',(-260.,5.34514940182371,129.567322952057));
#195469=CARTESIAN_POINT('Ctrl Pts',(-260.,5.29701544650841,129.421798967472));
#195470=CARTESIAN_POINT('Ctrl Pts',(-260.,5.24268558046692,129.278720038982));
#195471=CARTESIAN_POINT('Ctrl Pts',(-260.,5.18884719914122,129.136935446585));
#195472=CARTESIAN_POINT('Ctrl Pts',(-260.,5.12892436413587,128.997551287232));
#195473=CARTESIAN_POINT('Ctrl Pts',(-260.,5.06280805876399,128.860997446897));
#195474=CARTESIAN_POINT('Ctrl Pts',(-260.,5.03637289178243,128.806399363249));
#195475=CARTESIAN_POINT('Ctrl Pts',(-260.,5.00894715733214,128.752254104499));
#195476=CARTESIAN_POINT('Ctrl Pts',(-260.,4.98052205131543,128.698590732034));
#195477=CARTESIAN_POINT('Ctrl Pts',(-260.,4.92892839867658,128.601187774354));
#195478=CARTESIAN_POINT('Ctrl Pts',(-260.,4.87404261145725,128.505371761023));
#195479=CARTESIAN_POINT('Ctrl Pts',(-260.,4.81598802038452,128.411272751585));
#195480=CARTESIAN_POINT('Ctrl Pts',(-260.,4.79983018598994,128.385082984625));
#195481=CARTESIAN_POINT('Ctrl Pts',(-260.,4.78342684813515,128.359026287272));
#195482=CARTESIAN_POINT('Ctrl Pts',(-260.,4.76678058132004,128.333105619803));
#195483=CARTESIAN_POINT('Ctrl Pts',(-260.,4.75601759437824,128.316346077944));
#195484=CARTESIAN_POINT('Ctrl Pts',(-260.,4.74515304943485,128.299643405288));
#195485=CARTESIAN_POINT('Ctrl Pts',(-260.,4.73418763536694,128.282998417979));
#195486=CARTESIAN_POINT('Ctrl Pts',(-260.,4.72349743847076,128.266771197505));
#195487=CARTESIAN_POINT('Ctrl Pts',(-260.,4.71271622399387,128.250606183426));
#195488=CARTESIAN_POINT('Ctrl Pts',(-260.,4.70184618864053,128.23450587656));
#195489=CARTESIAN_POINT('Ctrl Pts',(-260.,4.61643398223665,128.107996376954));
#195490=CARTESIAN_POINT('Ctrl Pts',(-260.,4.52551512678615,127.985439463241));
#195491=CARTESIAN_POINT('Ctrl Pts',(-260.,4.42949814447551,127.867106517455));
#195492=CARTESIAN_POINT('Ctrl Pts',(-260.,4.3329217980936,127.748084201967));
#195493=CARTESIAN_POINT('Ctrl Pts',(-260.,4.23118703860946,127.633334688566));
#195494=CARTESIAN_POINT('Ctrl Pts',(-260.,4.12467212342404,127.523171713096));
#195495=CARTESIAN_POINT('Ctrl Pts',(-260.,4.01916361053234,127.414049608484));
#195496=CARTESIAN_POINT('Ctrl Pts',(-260.,3.90896409695521,127.309427379582));
#195497=CARTESIAN_POINT('Ctrl Pts',(-260.,3.79441562469337,127.209653467817));
#195498=CARTESIAN_POINT('Ctrl Pts',(-260.,3.70165347482906,127.128855859844));
#195499=CARTESIAN_POINT('Ctrl Pts',(-260.,3.60603870571396,127.051238430853));
#195500=CARTESIAN_POINT('Ctrl Pts',(-260.,3.50774543010271,126.977010181796));
#195501=CARTESIAN_POINT('Ctrl Pts',(-260.,3.45657148047279,126.938365089802));
#195502=CARTESIAN_POINT('Ctrl Pts',(-260.,3.40467143540377,126.900639007406));
#195503=CARTESIAN_POINT('Ctrl Pts',(-260.,3.35206949555686,126.863863967217));
#195504=CARTESIAN_POINT('Ctrl Pts',(-260.,3.33451576292437,126.851591811002));
#195505=CARTESIAN_POINT('Ctrl Pts',(-260.,3.31688203845638,126.839424338156));
#195506=CARTESIAN_POINT('Ctrl Pts',(-260.,3.2991751338089,126.82736680457));
#195507=CARTESIAN_POINT('Ctrl Pts',(-260.,3.26772105256822,126.805948117989));
#195508=CARTESIAN_POINT('Ctrl Pts',(-260.,3.2360509900514,126.78488639037));
#195509=CARTESIAN_POINT('Ctrl Pts',(-260.,3.20417076835762,126.764186616116));
#195510=CARTESIAN_POINT('Ctrl Pts',(-260.,3.07819216095848,126.682388918501));
#195511=CARTESIAN_POINT('Ctrl Pts',(-260.,2.94893322126365,126.606239408971));
#195512=CARTESIAN_POINT('Ctrl Pts',(-260.,2.81674061255645,126.535897250836));
#195513=CARTESIAN_POINT('Ctrl Pts',(-260.,2.6849707683341,126.465780053586));
#195514=CARTESIAN_POINT('Ctrl Pts',(-260.,2.55028528681488,126.401432946769));
#195515=CARTESIAN_POINT('Ctrl Pts',(-260.,2.41301606338223,126.343063828293));
#195516=CARTESIAN_POINT('Ctrl Pts',(-260.,2.35052041203885,126.316489655392));
#195517=CARTESIAN_POINT('Ctrl Pts',(-260.,2.28748911504771,126.291155293666));
#195518=CARTESIAN_POINT('Ctrl Pts',(-260.,2.22395330100519,126.267083981877));
#195519=CARTESIAN_POINT('Ctrl Pts',(-260.,2.19556404838833,126.256328370077));
#195520=CARTESIAN_POINT('Ctrl Pts',(-260.,2.16707406918085,126.245824957815));
#195521=CARTESIAN_POINT('Ctrl Pts',(-260.,2.13848614791516,126.235575968929));
#195522=CARTESIAN_POINT('Ctrl Pts',(-260.,2.1154668765457,126.227323383712));
#195523=CARTESIAN_POINT('Ctrl Pts',(-260.,2.09238327371483,126.219235546019));
#195524=CARTESIAN_POINT('Ctrl Pts',(-260.,2.06925245604652,126.211318807416));
#195525=CARTESIAN_POINT('Ctrl Pts',(-260.,1.93090341986312,126.163967556319));
#195526=CARTESIAN_POINT('Ctrl Pts',(-260.,1.79073515085027,126.122685331451));
#195527=CARTESIAN_POINT('Ctrl Pts',(-260.,1.64906874319027,126.087648542449));
#195528=CARTESIAN_POINT('Ctrl Pts',(-260.,1.50976463913972,126.053195995926));
#195529=CARTESIAN_POINT('Ctrl Pts',(-260.,1.36901131538522,126.024782312242));
#195530=CARTESIAN_POINT('Ctrl Pts',(-260.,1.22711298900573,126.002624910688));
#195531=CARTESIAN_POINT('Ctrl Pts',(-260.,1.09799938680752,125.982463841823));
#195532=CARTESIAN_POINT('Ctrl Pts',(-260.,0.967937472914146,125.967482984268));
#195533=CARTESIAN_POINT('Ctrl Pts',(-260.,0.837162017623963,125.957883255734));
#195534=CARTESIAN_POINT('Ctrl Pts',(210.578629502474,3.43871735229388,135.623751273273));
#195535=CARTESIAN_POINT('Ctrl Pts',(210.532211638871,4.24191310225744,135.050661598608));
#195536=CARTESIAN_POINT('Ctrl Pts',(210.439385837966,5.5417116830592,133.497735776206));
#195537=CARTESIAN_POINT('Ctrl Pts',(210.253744162458,6.40049231640402,129.500124813146));
#195538=CARTESIAN_POINT('Ctrl Pts',(210.021704475947,3.49988613106459,124.739836436729));
#195539=CARTESIAN_POINT('Ctrl Pts',(209.743256852134,-3.22132718841443,
124.582443963435));
#195540=CARTESIAN_POINT('Ctrl Pts',(209.464809228321,-6.97029916743427,
130.151104711613));
#195541=CARTESIAN_POINT('Ctrl Pts',(209.186361604508,-4.320155850937,136.315756482887));
#195542=CARTESIAN_POINT('Ctrl Pts',(208.907913980696,2.30329626696544,137.417975354914));
#195543=CARTESIAN_POINT('Ctrl Pts',(208.629466356883,6.80838731381026,132.441404887444));
#195544=CARTESIAN_POINT('Ctrl Pts',(208.35101873307,5.05782663488002,125.961106241921));
#195545=CARTESIAN_POINT('Ctrl Pts',(208.072571109257,-1.34111875541754,
123.931185212061));
#195546=CARTESIAN_POINT('Ctrl Pts',(207.794123485444,-6.50738248846785,
128.217554840719));
#195547=CARTESIAN_POINT('Ctrl Pts',(207.515675861631,-5.69381680528821,
134.880978212762));
#195548=CARTESIAN_POINT('Ctrl Pts',(207.237228237818,0.352161018465804,
137.798239159538));
#195549=CARTESIAN_POINT('Ctrl Pts',(206.958780614005,6.07448159193836,134.288440920842));
#195550=CARTESIAN_POINT('Ctrl Pts',(206.680332990192,6.21467071562046,127.576957111676));
#195551=CARTESIAN_POINT('Ctrl Pts',(206.40188536638,0.643870262773591,123.831292031177));
#195552=CARTESIAN_POINT('Ctrl Pts',(206.123437742567,-5.51860979104455,
126.493540260974));
#195553=CARTESIAN_POINT('Ctrl Pts',(205.844990118754,-6.60976007302988,
133.117219720399));
#195554=CARTESIAN_POINT('Ctrl Pts',(205.566542494941,-1.62686214948821,
137.615495756827));
#195555=CARTESIAN_POINT('Ctrl Pts',(205.288094871128,4.8510417637676,135.85467075854));
#195556=CARTESIAN_POINT('Ctrl Pts',(205.009647247315,6.87107573233629,129.452857771449));
#195557=CARTESIAN_POINT('Ctrl Pts',(204.731199623502,2.57692653546199,124.293009711503));
#195558=CARTESIAN_POINT('Ctrl Pts',(204.452751999689,-4.08529213152394,
125.116775123829));
#195559=CARTESIAN_POINT('Ctrl Pts',(204.174304375876,-6.9933269740478,131.167153704944));
#195560=CARTESIAN_POINT('Ctrl Pts',(203.895856752063,-3.47483593506387,
136.884143186524));
#195561=CARTESIAN_POINT('Ctrl Pts',(203.617409128251,3.23685955433703,137.014109488232));
#195562=CARTESIAN_POINT('Ctrl Pts',(203.338961504438,6.97403925260401,131.437619947721));
#195563=CARTESIAN_POINT('Ctrl Pts',(203.060513880625,4.30241757323156,125.27919601562));
#195564=CARTESIAN_POINT('Ctrl Pts',(202.782066256812,-2.32291566837452,
124.198128435325));
#195565=CARTESIAN_POINT('Ctrl Pts',(202.503618632999,-6.81360289295739,
129.18786549711));
#195566=CARTESIAN_POINT('Ctrl Pts',(202.225171009186,-5.0429219211382,135.663082604955));
#195567=CARTESIAN_POINT('Ctrl Pts',(201.946723385373,1.36195793536179,137.673371567868));
#195568=CARTESIAN_POINT('Ctrl Pts',(201.66827576156,6.51526498482727,133.371375037445));
#195569=CARTESIAN_POINT('Ctrl Pts',(201.389828137747,5.6813618015098,126.710417660699));
#195570=CARTESIAN_POINT('Ctrl Pts',(201.111380513935,-0.373435327379839,
123.811593861123));
#195571=CARTESIAN_POINT('Ctrl Pts',(200.832932890122,-6.08506363376988,
127.338781095048));
#195572=CARTESIAN_POINT('Ctrl Pts',(200.554485266309,-6.20481573259303,
134.050666607207));
#195573=CARTESIAN_POINT('Ctrl Pts',(200.276037642496,-0.622645295272457,
137.779355505743));
#195574=CARTESIAN_POINT('Ctrl Pts',(199.997590018683,5.53170575049466,135.098364849491));
#195575=CARTESIAN_POINT('Ctrl Pts',(199.71914239487,6.60268945040398,128.471394077867));
#195576=CARTESIAN_POINT('Ctrl Pts',(199.440694771057,1.60612410470526,123.988305584475));
#195577=CARTESIAN_POINT('Ctrl Pts',(199.162247147244,-4.86639082969376,
125.768838683693));
#195578=CARTESIAN_POINT('Ctrl Pts',(198.883799523432,-6.86693032801245,
132.176770441218));
#195579=CARTESIAN_POINT('Ctrl Pts',(198.605351899619,-2.5570963230842,137.323524616753));
#195580=CARTESIAN_POINT('Ctrl Pts',(198.326904275806,4.10258428165832,136.479485555902));
#195581=CARTESIAN_POINT('Ctrl Pts',(198.048456651993,6.99219035394115,130.420283921986));
#195582=CARTESIAN_POINT('Ctrl Pts',(197.77000902818,3.45631507844086,124.714030008118));
#195583=CARTESIAN_POINT('Ctrl Pts',(197.491561404367,-3.25574490376804,
124.604492395141));
#195584=CARTESIAN_POINT('Ctrl Pts',(197.213113780554,-6.97593437139489,
130.192330798173));
#195585=CARTESIAN_POINT('Ctrl Pts',(196.934666156741,-4.28558094504976,
136.342594705906));
#195586=CARTESIAN_POINT('Ctrl Pts',(196.656218532928,2.3430120075278,137.403492044232));
#195587=CARTESIAN_POINT('Ctrl Pts',(196.377770909115,6.81849138768721,132.400109986944));
#195588=CARTESIAN_POINT('Ctrl Pts',(196.099323285303,5.02811028438465,125.930312215887));
#195589=CARTESIAN_POINT('Ctrl Pts',(195.82087566149,-1.38285853342424,123.939526815472));
#195590=CARTESIAN_POINT('Ctrl Pts',(195.542428037677,-6.5230479154113,128.257188313404));
#195591=CARTESIAN_POINT('Ctrl Pts',(195.263980413864,-5.66887493174189,
134.915576722577));
#195592=CARTESIAN_POINT('Ctrl Pts',(194.985532790051,0.394717174261835,
137.795958375315));
#195593=CARTESIAN_POINT('Ctrl Pts',(194.707085166238,6.09558348012494,134.251403247221));
#195594=CARTESIAN_POINT('Ctrl Pts',(194.428637542425,6.19490635356113,127.539184339867));
#195595=CARTESIAN_POINT('Ctrl Pts',(194.150189918612,0.601412926074683,
123.827502918989));
#195596=CARTESIAN_POINT('Ctrl Pts',(193.871742294799,-5.54474959981957,
126.527212884656));
#195597=CARTESIAN_POINT('Ctrl Pts',(193.593294670987,-6.59555811955654,
133.157412666584));
#195598=CARTESIAN_POINT('Ctrl Pts',(193.314847047174,-1.58537093834796,
137.625272568447));
#195599=CARTESIAN_POINT('Ctrl Pts',(193.036399423361,4.88169468552635,135.825047607524));
#195600=CARTESIAN_POINT('Ctrl Pts',(192.757951799548,6.86272137744547,129.411056577024));
#195601=CARTESIAN_POINT('Ctrl Pts',(192.479504175735,2.53724238606986,124.277443893095));
#195602=CARTESIAN_POINT('Ctrl Pts',(192.201056551922,-4.11983840692253,
125.141748821346));
#195603=CARTESIAN_POINT('Ctrl Pts',(191.922608928109,-6.99098896924831,
131.209717356357));
#195604=CARTESIAN_POINT('Ctrl Pts',(191.644161304296,-3.43776219763276,
136.905182851196));
#195605=CARTESIAN_POINT('Ctrl Pts',(191.365713680483,3.27460008958736,136.994290755064));
#195606=CARTESIAN_POINT('Ctrl Pts',(191.08726605667,6.9777648675845,131.395155257469));
#195607=CARTESIAN_POINT('Ctrl Pts',(190.808818432858,4.26870461503614,125.253108347726));
#195608=CARTESIAN_POINT('Ctrl Pts',(190.530370809044,-2.36308664091672,
124.212391080215));
#195609=CARTESIAN_POINT('Ctrl Pts',(190.251923185232,-6.82331671706736,
129.229371781915));
#195610=CARTESIAN_POINT('Ctrl Pts',(189.973475561419,-5.01325206778612,
135.693690281095));
#195611=CARTESIAN_POINT('Ctrl Pts',(189.695027937606,1.40374632081163,137.664953676525));
#195612=CARTESIAN_POINT('Ctrl Pts',(189.416580313793,6.53077041740369,133.331667209374));
#195613=CARTESIAN_POINT('Ctrl Pts',(189.13813268998,5.65633554627347,126.675909450142));
#195614=CARTESIAN_POINT('Ctrl Pts',(188.859685066167,-0.41599536452862,
123.81399662772));
#195615=CARTESIAN_POINT('Ctrl Pts',(188.581237442354,-6.10604685783229,
127.375886813701));
#195616=CARTESIAN_POINT('Ctrl Pts',(188.302789818542,-6.18493958576042,
134.088376935175));
#195617=CARTESIAN_POINT('Ctrl Pts',(188.024342194729,-0.580174985471077,
137.783016493883));
#195618=CARTESIAN_POINT('Ctrl Pts',(187.745894570916,5.55774208334242,135.064612228548));
#195619=CARTESIAN_POINT('Ctrl Pts',(187.467446947103,6.58836568835925,128.431244857581));
#195620=CARTESIAN_POINT('Ctrl Pts',(187.18899932329,1.56460308533104,123.97865493689));
#195621=CARTESIAN_POINT('Ctrl Pts',(186.910551699478,-4.89695331800637,
125.798555082479));
#195622=CARTESIAN_POINT('Ctrl Pts',(186.632104075664,-6.85844885156509,
132.218545967617));
#195623=CARTESIAN_POINT('Ctrl Pts',(186.353656451852,-2.51736494438869,
137.338969602853));
#195624=CARTESIAN_POINT('Ctrl Pts',(186.075208828038,4.13705436656654,136.454406814005));
#195625=CARTESIAN_POINT('Ctrl Pts',(185.796761204226,6.98972282098866,130.377727590732));
#195626=CARTESIAN_POINT('Ctrl Pts',(185.518313580413,3.41917746986535,124.693103276936));
#195627=CARTESIAN_POINT('Ctrl Pts',(185.2398659566,-3.29342493995873,124.62442590766));
#195628=CARTESIAN_POINT('Ctrl Pts',(184.961418332787,-6.97953072271363,
130.234806630193));
#195629=CARTESIAN_POINT('Ctrl Pts',(184.682970708974,-4.25178874032612,
136.368579642862));
#195630=CARTESIAN_POINT('Ctrl Pts',(184.404523085161,2.38313938299372,137.389107198495));
#195631=CARTESIAN_POINT('Ctrl Pts',(184.126075461348,6.82807883617355,132.358574329007));
#195632=CARTESIAN_POINT('Ctrl Pts',(183.847627837535,4.99834740910532,125.899794986266));
#195633=CARTESIAN_POINT('Ctrl Pts',(183.569180213722,-1.42462110408482,
123.948071857337));
#195634=CARTESIAN_POINT('Ctrl Pts',(183.290732589909,-6.53843241923107,
128.296943150732));
#195635=CARTESIAN_POINT('Ctrl Pts',(183.012284966097,-5.64374376128527,
134.950008601993));
#195636=CARTESIAN_POINT('Ctrl Pts',(182.733837342284,0.437269701071178,
137.793426081729));
#195637=CARTESIAN_POINT('Ctrl Pts',(182.455389718471,6.11645366995566,134.214233834728));
#195638=CARTESIAN_POINT('Ctrl Pts',(182.176942094658,6.17491552152431,127.501534682722));
#195639=CARTESIAN_POINT('Ctrl Pts',(181.898494470845,0.558931670205695,
123.82397121282));
#195640=CARTESIAN_POINT('Ctrl Pts',(181.620046847032,-5.57068308070185,
126.561044594899));
#195641=CARTESIAN_POINT('Ctrl Pts',(181.341599223219,-6.58111222344223,
133.197518104296));
#195642=CARTESIAN_POINT('Ctrl Pts',(181.063151599407,-1.54382073804491,
137.634796795631));
#195643=CARTESIAN_POINT('Ctrl Pts',(180.784703975594,4.91216658577983,135.795238324681));
#195644=CARTESIAN_POINT('Ctrl Pts',(180.506256351781,6.85411278995147,129.369307058824));
#195645=CARTESIAN_POINT('Ctrl Pts',(180.227808727968,2.49746418218255,124.262119907186));
#195646=CARTESIAN_POINT('Ctrl Pts',(179.949361104155,-4.15423200110403,
125.16693236216));
#195647=CARTESIAN_POINT('Ctrl Pts',(179.670913480342,-6.98839192089168,
131.252265980172));
#195648=CARTESIAN_POINT('Ctrl Pts',(179.392465856529,-3.40056106730489,
136.925996451342));
#195649=CARTESIAN_POINT('Ctrl Pts',(179.114018232716,3.31221928049139,136.974242649806));
#195650=CARTESIAN_POINT('Ctrl Pts',(178.835570608904,6.98123192042358,131.352668676138));
#195651=CARTESIAN_POINT('Ctrl Pts',(178.55712298509,4.23483347762603,125.227226382977));
#195652=CARTESIAN_POINT('Ctrl Pts',(178.278675361277,-2.40317004799311,
124.22689799325));
#195653=CARTESIAN_POINT('Ctrl Pts',(178.000227737465,-6.83277770089014,
129.270936428355));
#195654=CARTESIAN_POINT('Ctrl Pts',(177.721780113652,-4.98339644641697,
135.724116781409));
#195655=CARTESIAN_POINT('Ctrl Pts',(177.443332489839,1.44548268986267,137.65628156334));
#195656=CARTESIAN_POINT('Ctrl Pts',(177.164884866026,6.54603384991367,133.291865731052));
#195657=CARTESIAN_POINT('Ctrl Pts',(176.886437242213,5.63109969342586,126.64155422085));
#195658=CARTESIAN_POINT('Ctrl Pts',(176.6079896184,-0.458539986806858,123.816658424832));
#195659=CARTESIAN_POINT('Ctrl Pts',(176.329541994587,-6.12680382008778,
127.413119575705));
#195660=CARTESIAN_POINT('Ctrl Pts',(176.051094370774,-6.16483425371434,
134.125965572714));
#195661=CARTESIAN_POINT('Ctrl Pts',(175.772646746962,-0.537683177073775,
137.786418885364));
#195662=CARTESIAN_POINT('Ctrl Pts',(175.494199123148,5.58357247201413,135.030701742416));
#195663=CARTESIAN_POINT('Ctrl Pts',(175.215751499336,6.57379779200069,128.391183573973));
#195664=CARTESIAN_POINT('Ctrl Pts',(174.937303875523,1.5230240890144,123.969257218339));
#195665=CARTESIAN_POINT('Ctrl Pts',(174.65885625171,-4.92733434791298,125.82845697323));
#195666=CARTESIAN_POINT('Ctrl Pts',(174.380408627897,-6.84971323277332,
132.260269090858));
#195667=CARTESIAN_POINT('Ctrl Pts',(174.101961004084,-2.4775402838095,137.354172446613));
#195668=CARTESIAN_POINT('Ctrl Pts',(173.823513380271,4.1713711514037,136.429118707571));
#195669=CARTESIAN_POINT('Ctrl Pts',(173.545065756458,6.98699628128659,130.335187068521));
#195670=CARTESIAN_POINT('Ctrl Pts',(173.266618132645,3.38191316241135,124.672403000642));
#195671=CARTESIAN_POINT('Ctrl Pts',(172.988170508833,-3.33098293707706,
124.644588419932));
#195672=CARTESIAN_POINT('Ctrl Pts',(172.709722885019,-6.98286844495469,
130.277303567246));
#195673=CARTESIAN_POINT('Ctrl Pts',(172.431275261207,-4.21783898400718,
136.394358395635));
#195674=CARTESIAN_POINT('Ctrl Pts',(172.152827637394,2.42317845035331,137.374478352552));
#195675=CARTESIAN_POINT('Ctrl Pts',(171.874380013581,6.83741326768756,132.316981079111));
#195676=CARTESIAN_POINT('Ctrl Pts',(171.595932389768,4.96839931822471,125.869459497128));
#195677=CARTESIAN_POINT('Ctrl Pts',(171.317484765955,-1.46633088488636,
123.956870961504));
#195678=CARTESIAN_POINT('Ctrl Pts',(171.039037142142,-6.55357463903296,
128.336790901335));
#195679=CARTESIAN_POINT('Ctrl Pts',(170.760589518329,-5.61840345982816,
134.984286862899));
#195680=CARTESIAN_POINT('Ctrl Pts',(170.482141894517,0.479806024690783,
137.79063480575));
#195681=CARTESIAN_POINT('Ctrl Pts',(170.203694270703,6.13709721234627,134.176938068128));
#195682=CARTESIAN_POINT('Ctrl Pts',(169.925246646891,6.15469587572206,127.464007413007));
#195683=CARTESIAN_POINT('Ctrl Pts',(169.646799023078,0.51642970291829,123.820698167548));
#195684=CARTESIAN_POINT('Ctrl Pts',(169.368351399265,-5.59641013787386,
126.595033542778));
#195685=CARTESIAN_POINT('Ctrl Pts',(169.089903775452,-6.56642246179436,
133.237534862678));
#195686=CARTESIAN_POINT('Ctrl Pts',(168.811456151639,-1.50221333089678,
137.644067918489));
#195687=CARTESIAN_POINT('Ctrl Pts',(168.533008527826,4.94245646389391,135.76524410303));
#195688=CARTESIAN_POINT('Ctrl Pts',(168.254560904013,6.84525022078748,129.32761071706));
#195689=CARTESIAN_POINT('Ctrl Pts',(167.976113280201,2.45759343384159,124.247038346411));
#195690=CARTESIAN_POINT('Ctrl Pts',(167.697665656387,-4.1884716586909,125.192324799951));
#195691=CARTESIAN_POINT('Ctrl Pts',(167.419218032575,-6.98553591510243,
131.294798006688));
#195692=CARTESIAN_POINT('Ctrl Pts',(167.140770408762,-3.36323392793624,
136.946583212019));
#195693=CARTESIAN_POINT('Ctrl Pts',(166.862322784949,3.34971573589186,136.953965917302));
#195694=CARTESIAN_POINT('Ctrl Pts',(166.583875161136,6.98444028114645,131.310161777048));
#195695=CARTESIAN_POINT('Ctrl Pts',(166.305427537323,4.20080541690416,125.20155108099));
#195696=CARTESIAN_POINT('Ctrl Pts',(166.02697991351,-2.44316440471955,124.241648636582));
#195697=CARTESIAN_POINT('Ctrl Pts',(165.748532289697,-6.84198549362249,
129.312557896394));
#195698=CARTESIAN_POINT('Ctrl Pts',(165.470084665885,-4.95335616345982,
135.754360978348));
#195699=CARTESIAN_POINT('Ctrl Pts',(165.191637042072,1.48716549602113,137.647355549705));
#195700=CARTESIAN_POINT('Ctrl Pts',(164.913189418259,6.56105471673207,133.251972077313));
#195701=CARTESIAN_POINT('Ctrl Pts',(164.634741794446,5.60565517810829,126.60735324588));
#195702=CARTESIAN_POINT('Ctrl Pts',(164.356294170633,-0.501067617717217,
123.819579153818));
#195703=CARTESIAN_POINT('Ctrl Pts',(164.07784654682,-6.1473337513746,127.450478001396));
#195704=CARTESIAN_POINT('Ctrl Pts',(163.799398923007,-6.14450048146789,
134.163431126959));
#195705=CARTESIAN_POINT('Ctrl Pts',(163.520951299194,-0.495171444628521,
137.789562554107));
#195706=CARTESIAN_POINT('Ctrl Pts',(163.242503675381,5.60919595935461,134.996634647659));
#195707=CARTESIAN_POINT('Ctrl Pts',(162.964056051569,6.55898630114736,128.351211711527));
#195708=CARTESIAN_POINT('Ctrl Pts',(162.685608427755,1.48138865648,123.960112777059));
#195709=CARTESIAN_POINT('Ctrl Pts',(162.407160803943,-4.95753279363329,
125.85854324792));
#195710=CARTESIAN_POINT('Ctrl Pts',(162.12871318013,-6.84072379533872,132.301938264875));
#195711=CARTESIAN_POINT('Ctrl Pts',(161.850265556317,-2.4376238170639,137.369132584688));
#195712=CARTESIAN_POINT('Ctrl Pts',(161.571817932504,4.20553336454888,136.403622173655));
#195713=CARTESIAN_POINT('Ctrl Pts',(161.293370308691,6.98401083586784,130.292663931709));
#195714=CARTESIAN_POINT('Ctrl Pts',(161.014922684878,3.34452353692138,124.651929946293));
#195715=CARTESIAN_POINT('Ctrl Pts',(160.736475061065,-3.36841750339773,
124.664979184829));
#195716=CARTESIAN_POINT('Ctrl Pts',(160.458027437253,-6.98594741443756,
130.319820034592));
#195717=CARTESIAN_POINT('Ctrl Pts',(160.179579813439,-4.18373293411359,
136.419930008985));
#195718=CARTESIAN_POINT('Ctrl Pts',(159.901132189627,2.46312772594441,137.35960604848));
#195719=CARTESIAN_POINT('Ctrl Pts',(159.622684565814,6.84649433633851,132.275331778507));
#195720=CARTESIAN_POINT('Ctrl Pts',(159.344236942001,4.93826712148011,125.839306872565));
#195721=CARTESIAN_POINT('Ctrl Pts',(159.065789318188,-1.50798633025781,
123.965923801919));
#195722=CARTESIAN_POINT('Ctrl Pts',(158.787341694375,-6.56847401371661,
128.376730088641));
#195723=CARTESIAN_POINT('Ctrl Pts',(158.508894070562,-5.59285496636459,
135.018410235101));
#195724=CARTESIAN_POINT('Ctrl Pts',(158.230446446749,0.522324568921774,
137.787584650814));
#195725=CARTESIAN_POINT('Ctrl Pts',(157.951998822937,6.15751334234277,134.139517329431));
#195726=CARTESIAN_POINT('Ctrl Pts',(157.673551199123,6.13424816540071,127.426603921307));
#195727=CARTESIAN_POINT('Ctrl Pts',(157.395103575311,0.473908599138188,
123.817683904457));
#195728=CARTESIAN_POINT('Ctrl Pts',(157.116655951498,-5.62192981801017,
126.62917846882));
#195729=CARTESIAN_POINT('Ctrl Pts',(156.838208327685,-6.55148937894732,
133.277461458893));
#195730=CARTESIAN_POINT('Ctrl Pts',(156.559760703872,-1.46055025868114,
137.653085593479));
#195731=CARTESIAN_POINT('Ctrl Pts',(156.281313080059,4.97256319746619,135.735066054016));
#195732=CARTESIAN_POINT('Ctrl Pts',(156.002865456246,6.83613399835919,129.285969096806));
#195733=CARTESIAN_POINT('Ctrl Pts',(155.724417832433,2.4176316184721,124.232199769625));
#195734=CARTESIAN_POINT('Ctrl Pts',(155.44597020862,-4.2225561109203,125.217925193794));
#195735=CARTESIAN_POINT('Ctrl Pts',(155.167522584808,-6.98242105771092,
131.337311859867));
#195736=CARTESIAN_POINT('Ctrl Pts',(154.889074960995,-3.3257821626974,136.96694237038));
#195737=CARTESIAN_POINT('Ctrl Pts',(154.610627337182,3.38708806634394,136.933461308912));
#195738=CARTESIAN_POINT('Ctrl Pts',(154.332179713369,6.98738983086623,131.267636135312));
#195739=CARTESIAN_POINT('Ctrl Pts',(154.053732089556,4.1666216937926,125.17608339317));
#195740=CARTESIAN_POINT('Ctrl Pts',(153.775284465743,-2.48306822909056,
124.256642463619));
#195741=CARTESIAN_POINT('Ctrl Pts',(153.49683684193,-6.85093975406627,129.354234643731));
#195742=CARTESIAN_POINT('Ctrl Pts',(153.218389218117,-4.92313233206838,
135.784421751204));
#195743=CARTESIAN_POINT('Ctrl Pts',(152.939941594304,1.52879319471521,137.638175966376));
#195744=CARTESIAN_POINT('Ctrl Pts',(152.661493970491,6.57583246125511,133.21198772643));
#195745=CARTESIAN_POINT('Ctrl Pts',(152.383046346679,5.58000294317656,126.573307792561));
#195746=CARTESIAN_POINT('Ctrl Pts',(152.104598722866,-0.543576681382813,
123.822758706449));
#195747=CARTESIAN_POINT('Ctrl Pts',(151.826151099053,-6.16763589094857,
127.487960706439));
#195748=CARTESIAN_POINT('Ctrl Pts',(151.54770347524,-6.12393902249645,134.200772209611));
#195749=CARTESIAN_POINT('Ctrl Pts',(151.269255851427,-0.452641363423277,
137.792447383624));
#195750=CARTESIAN_POINT('Ctrl Pts',(150.990808227614,5.63461159587598,134.962412206646));
#195751=CARTESIAN_POINT('Ctrl Pts',(150.712360603801,6.54393176464461,128.311330751416));
#195752=CARTESIAN_POINT('Ctrl Pts',(150.433912979988,1.4396983305442,123.951221951899));
#195753=CARTESIAN_POINT('Ctrl Pts',(150.155465356176,-4.98754753615285,
125.888812791691));
#195754=CARTESIAN_POINT('Ctrl Pts',(149.877017732362,-6.83148087236823,
132.343551945603));
#195755=CARTESIAN_POINT('Ctrl Pts',(149.59857010855,-2.39761702327129,137.383849462723));
#195756=CARTESIAN_POINT('Ctrl Pts',(149.320122484737,4.23953974010866,136.377918157044));
#195757=CARTESIAN_POINT('Ctrl Pts',(149.041674860924,6.98076659535922,130.250159756006));
#195758=CARTESIAN_POINT('Ctrl Pts',(148.763227237111,3.30700997888175,124.631684872525));
#195759=CARTESIAN_POINT('Ctrl Pts',(148.484779613298,-3.40572725176907,
124.685597446761));
#195760=CARTESIAN_POINT('Ctrl Pts',(148.206331989485,-6.98876751706998,
130.362354456768));
#195761=CARTESIAN_POINT('Ctrl Pts',(147.927884365672,-4.14947185445744,
136.445293535346));
#195762=CARTESIAN_POINT('Ctrl Pts',(147.649436741859,2.50298572943186,137.344490837378));
#195763=CARTESIAN_POINT('Ctrl Pts',(147.370989118047,6.85532170562399,132.233627970525));
#195764=CARTESIAN_POINT('Ctrl Pts',(147.092541494233,4.90795193543132,125.809338229895));
#195765=CARTESIAN_POINT('Ctrl Pts',(146.814093870421,-1.54958589664124,
123.975230043125));
#195766=CARTESIAN_POINT('Ctrl Pts',(146.535646246608,-6.58312999118006,
128.41675923269));
#195767=CARTESIAN_POINT('Ctrl Pts',(146.257198622795,-5.56709922760349,
135.052377454143));
#195768=CARTESIAN_POINT('Ctrl Pts',(145.978750998982,0.564823758223794,
137.784275729942));
#195769=CARTESIAN_POINT('Ctrl Pts',(145.700303375169,6.17770130341801,134.101973005276));
#195770=CARTESIAN_POINT('Ctrl Pts',(145.421855751356,6.11357314825767,127.389325593625));
#195771=CARTESIAN_POINT('Ctrl Pts',(145.143408127543,0.431369934500661,
123.81492853524));
#195772=CARTESIAN_POINT('Ctrl Pts',(144.864960503731,-5.64724117546963,
126.663478107772));
#195773=CARTESIAN_POINT('Ctrl Pts',(144.586512879918,-6.53631352825206,
133.317296413447));
#195774=CARTESIAN_POINT('Ctrl Pts',(144.308065256105,-1.41883306523854,
137.661849486446));
#195775=CARTESIAN_POINT('Ctrl Pts',(144.029617632292,5.00248567088053,135.704705295899));
#195776=CARTESIAN_POINT('Ctrl Pts',(143.751170008479,6.82676446047164,129.244383741109));
#195777=CARTESIAN_POINT('Ctrl Pts',(143.472722384666,2.37758021687388,124.217604726676));
#195778=CARTESIAN_POINT('Ctrl Pts',(143.194274760853,-4.25648409478009,
125.243732595056));
#195779=CARTESIAN_POINT('Ctrl Pts',(142.91582713704,-6.97904746413934,131.379805964341));
#195780=CARTESIAN_POINT('Ctrl Pts',(142.637379513228,-3.28820715937746,
136.987073172008));
#195781=CARTESIAN_POINT('Ctrl Pts',(142.358931889414,3.42433488700229,136.912729584442));
#195782=CARTESIAN_POINT('Ctrl Pts',(142.080484265602,6.99008046028611,131.225093326731));
#195783=CARTESIAN_POINT('Ctrl Pts',(141.802036641788,4.13228357498186,125.150824263232));
#195784=CARTESIAN_POINT('Ctrl Pts',(141.523589017976,-2.52288004245522,
124.271878918761));
#195785=CARTESIAN_POINT('Ctrl Pts',(141.245141394163,-6.859640150418,129.395965126019));
#195786=CARTESIAN_POINT('Ctrl Pts',(140.96669377035,-4.89272607219785,135.814297986063));
#195787=CARTESIAN_POINT('Ctrl Pts',(140.688246146537,1.57036424341533,137.628743153505));
#195788=CARTESIAN_POINT('Ctrl Pts',(140.409798522724,6.59036653588803,133.17191416004));
#195789=CARTESIAN_POINT('Ctrl Pts',(140.131350898911,5.55414393918375,126.539419122461));
#195790=CARTESIAN_POINT('Ctrl Pts',(139.852903275098,-0.586065602614643,
123.826196964908));
#195791=CARTESIAN_POINT('Ctrl Pts',(139.574455651286,-6.18770948650656,
127.525566301902));
#195792=CARTESIAN_POINT('Ctrl Pts',(139.296008027473,-6.10315063871238,
134.237987436982));
#195793=CARTESIAN_POINT('Ctrl Pts',(139.01756040366,-0.410094509425858,
137.795073267016));
#195794=CARTESIAN_POINT('Ctrl Pts',(138.739112779847,5.65981843979252,134.928035687503));
#195795=CARTESIAN_POINT('Ctrl Pts',(138.460665156034,6.52863474034383,128.271542171445));
#195796=CARTESIAN_POINT('Ctrl Pts',(138.182217532221,1.39795465605713,123.942585072312));
#195797=CARTESIAN_POINT('Ctrl Pts',(137.903769908408,-5.01737746326431,
125.919264482896));
#195798=CARTESIAN_POINT('Ctrl Pts',(137.625322284595,-6.82198480636163,
132.385108591028));
#195799=CARTESIAN_POINT('Ctrl Pts',(137.346874660782,-2.35752138489827,
137.39832253538));
#195800=CARTESIAN_POINT('Ctrl Pts',(137.06842703697,4.27338901796432,136.352007610208));
#195801=CARTESIAN_POINT('Ctrl Pts',(136.789979413157,6.9772636799772,130.20767611642));
#195802=CARTESIAN_POINT('Ctrl Pts',(136.511531789344,3.26937387837121,124.611668529527));
#195803=CARTESIAN_POINT('Ctrl Pts',(136.233084165531,-3.44291079966457,
124.706442441713));
#195804=CARTESIAN_POINT('Ctrl Pts',(135.954636541718,-6.99132864835187,
130.404905257644));
#195805=CARTESIAN_POINT('Ctrl Pts',(135.676188917905,-4.1150570145959,136.470448034864));
#195806=CARTESIAN_POINT('Ctrl Pts',(135.397741294092,2.54275098386259,137.329133279345));
#195807=CARTESIAN_POINT('Ctrl Pts',(135.11929367028,6.8638950484427,132.191871200516));
#195808=CARTESIAN_POINT('Ctrl Pts',(134.840846046466,4.87745488341857,125.779554679616));
#195809=CARTESIAN_POINT('Ctrl Pts',(134.562398422654,-1.59112804254939,
123.984789340275));
#195810=CARTESIAN_POINT('Ctrl Pts',(134.283950798841,-6.59754202834077,
128.456876850186));
#195811=CARTESIAN_POINT('Ctrl Pts',(134.005503175028,-5.54113719793324,
135.086187261361));
#195812=CARTESIAN_POINT('Ctrl Pts',(133.727055551215,0.607302017773813,
137.780708165749));
#195813=CARTESIAN_POINT('Ctrl Pts',(133.448607927402,6.19766034749954,134.064306486881));
#195814=CARTESIAN_POINT('Ctrl Pts',(133.170160303589,6.09267159041341,127.352173811322));
#195815=CARTESIAN_POINT('Ctrl Pts',(132.891712679776,0.388815285291658,
123.812432161999));
#195816=CARTESIAN_POINT('Ctrl Pts',(132.613265055963,-5.67234327233058,
126.697931188648));
#195817=CARTESIAN_POINT('Ctrl Pts',(132.334817432151,-6.52089547205522,
133.357038250242));
#195818=CARTESIAN_POINT('Ctrl Pts',(132.056369808337,-1.37706329641493,
137.670359272641));
#195819=CARTESIAN_POINT('Ctrl Pts',(131.777922184525,5.0322227753486,135.674162953708));
#195820=CARTESIAN_POINT('Ctrl Pts',(131.499474560712,6.81714195431646,129.20285619093));
#195821=CARTESIAN_POINT('Ctrl Pts',(131.221026936899,2.33744071316646,124.203253758389));
#195822=CARTESIAN_POINT('Ctrl Pts',(130.942579313086,-4.29025435305649,
125.269746047434));
#195823=CARTESIAN_POINT('Ctrl Pts',(130.664131689273,-6.97541525939744,
131.422278745477));
#195824=CARTESIAN_POINT('Ctrl Pts',(130.38568406546,-3.25051031033198,137.006974870947));
#195825=CARTESIAN_POINT('Ctrl Pts',(130.107236441647,3.46145481767177,136.891771512113));
#195826=CARTESIAN_POINT('Ctrl Pts',(129.828788817834,6.99251206970404,131.182534927744));
#195827=CARTESIAN_POINT('Ctrl Pts',(129.550341194022,4.09779233288376,125.125774627163));
#195828=CARTESIAN_POINT('Ctrl Pts',(129.271893570209,-2.5625983695722,124.287357437414));
#195829=CARTESIAN_POINT('Ctrl Pts',(128.993445946396,-6.86808636028122,
129.43774779692));
#195830=CARTESIAN_POINT('Ctrl Pts',(128.714998322583,-4.86213851056362,
135.84398857585));
#195831=CARTESIAN_POINT('Ctrl Pts',(128.43655069877,1.61187710169066,137.61905746063));
#195832=CARTESIAN_POINT('Ctrl Pts',(128.158103074957,6.60465640206541,133.131752863082));
#195833=CARTESIAN_POINT('Ctrl Pts',(127.879655451144,5.52807912434469,126.505688491336));
#195834=CARTESIAN_POINT('Ctrl Pts',(127.601207827331,-0.628532806970051,
123.829893801787));
#195835=CARTESIAN_POINT('Ctrl Pts',(127.322760203518,-6.20755379421381,
127.563293394292));
#195836=CARTESIAN_POINT('Ctrl Pts',(127.044312579706,-6.08213610043705,
134.275075430049));
#195837=CARTESIAN_POINT('Ctrl Pts',(126.765864955893,-0.367532459225645,
137.797440106979));
#195838=CARTESIAN_POINT('Ctrl Pts',(126.48741733208,5.68481555705546,134.893506364063));
#195839=CARTESIAN_POINT('Ctrl Pts',(126.208969708267,6.51309579508176,128.231847445991));
#195840=CARTESIAN_POINT('Ctrl Pts',(125.930522084454,1.35615917984635,123.934202458341));
#195841=CARTESIAN_POINT('Ctrl Pts',(125.652074460641,-5.04702146960864,
125.949897193134));
#195842=CARTESIAN_POINT('Ctrl Pts',(125.373626836828,-6.81223594919939,
132.426606661257));
#195843=CARTESIAN_POINT('Ctrl Pts',(125.095179213015,-2.3173383877032,137.412551266352));
#195844=CARTESIAN_POINT('Ctrl Pts',(124.816731589202,4.3070799438184,136.325891493273));
#195845=CARTESIAN_POINT('Ctrl Pts',(124.538283965389,6.97350221952356,130.165214587198));
#195846=CARTESIAN_POINT('Ctrl Pts',(124.259836341577,3.2316166300094,124.591881659011));
#195847=CARTESIAN_POINT('Ctrl Pts',(123.981388717764,-3.47996676923432,
124.727513397266));
#195848=CARTESIAN_POINT('Ctrl Pts',(123.702941093951,-6.99363071337966,
130.447470860486));
#195849=CARTESIAN_POINT('Ctrl Pts',(123.424493470138,-4.08048968978323,
136.495392575427));
#195850=CARTESIAN_POINT('Ctrl Pts',(123.146045846325,2.58242201572056,137.313533943462));
#195851=CARTESIAN_POINT('Ctrl Pts',(122.867598222512,6.87221404710605,132.150063015792));
#195852=CARTESIAN_POINT('Ctrl Pts',(122.589150598699,4.84677709552158,125.749957325369));
#195853=CARTESIAN_POINT('Ctrl Pts',(122.310702974886,-1.63261122862275,
123.994601339147));
#195854=CARTESIAN_POINT('Ctrl Pts',(122.032255351073,-6.6117095911554,128.497081454556));
#195855=CARTESIAN_POINT('Ctrl Pts',(121.753807727261,-5.51496983938628,
135.119838403918));
#195856=CARTESIAN_POINT('Ctrl Pts',(121.475360103447,0.649757773524084,
137.776882090432));
#195857=CARTESIAN_POINT('Ctrl Pts',(121.196912479635,6.21738973499768,134.026519169992));
#195858=CARTESIAN_POINT('Ctrl Pts',(120.918464855822,6.07154426638285,127.315149951069));
#195859=CARTESIAN_POINT('Ctrl Pts',(120.640017232009,0.346246228389124,
123.810194877238));
#195860=CARTESIAN_POINT('Ctrl Pts',(120.361569608196,-5.69723517842559,
126.732536434776));
#195861=CARTESIAN_POINT('Ctrl Pts',(120.083121984383,-6.50523578167861,
133.396685496627));
#195862=CARTESIAN_POINT('Ctrl Pts',(119.80467436057,-1.3352425000044,137.678614636731));
#195863=CARTESIAN_POINT('Ctrl Pts',(119.526226736757,5.06177340895125,135.6434401592));
#195864=CARTESIAN_POINT('Ctrl Pts',(119.247779112945,6.8072668364591,129.161387985085));
#195865=CARTESIAN_POINT('Ctrl Pts',(118.969331489131,2.29721459473369,124.189147396544));
#195866=CARTESIAN_POINT('Ctrl Pts',(118.690883865319,-4.32386563438011,
125.29596458699));
#195867=CARTESIAN_POINT('Ctrl Pts',(118.412436241506,-6.97152457807781,
131.464728629428));
#195868=CARTESIAN_POINT('Ctrl Pts',(118.133988617693,-3.21269301243169,
137.026646729736));
#195869=CARTESIAN_POINT('Ctrl Pts',(117.85554099388,3.49844648286018,136.870587868534));
#195870=CARTESIAN_POINT('Ctrl Pts',(117.577093370067,6.99468456901571,131.139962515369));
#195871=CARTESIAN_POINT('Ctrl Pts',(117.298645746254,4.06314924558364,125.100935413187));
#195872=CARTESIAN_POINT('Ctrl Pts',(117.020198122441,-2.60222173866402,
124.303077446017));
#195873=CARTESIAN_POINT('Ctrl Pts',(116.741750498628,-6.8762780706787,129.479581108162));
#195874=CARTESIAN_POINT('Ctrl Pts',(116.463302874816,-4.83137078059878,
135.873492420371));
#195875=CARTESIAN_POINT('Ctrl Pts',(116.184855251003,1.65333023126747,137.609119246659));
#195876=CARTESIAN_POINT('Ctrl Pts',(115.90640762719,6.61870153027093,133.09150532375));
#195877=CARTESIAN_POINT('Ctrl Pts',(115.627960003377,5.5018094645007,126.472117149089));
#195878=CARTESIAN_POINT('Ctrl Pts',(115.349512379564,-0.670976720811003,
123.833849080098));
#195879=CARTESIAN_POINT('Ctrl Pts',(115.071064755751,-6.22716807873245,
127.601140585621));
#195880=CARTESIAN_POINT('Ctrl Pts',(114.792617131938,-6.06089618637186,
134.312034814502));
#195881=CARTESIAN_POINT('Ctrl Pts',(114.514169508125,-0.324956789974863,
137.79954781581));
#195882=CARTESIAN_POINT('Ctrl Pts',(114.235721884312,5.70960202138734,134.858825515823));
#195883=CARTESIAN_POINT('Ctrl Pts',(113.957274260499,6.4973155046598,128.192248045959));
#195884=CARTESIAN_POINT('Ctrl Pts',(113.678826636687,1.31431345065849,123.926074420608));
#195885=CARTESIAN_POINT('Ctrl Pts',(113.400379012874,-5.07647845671644,
125.980709787299));
#195886=CARTESIAN_POINT('Ctrl Pts',(113.121931389061,-6.80223466212876,
132.468044618562));
#195887=CARTESIAN_POINT('Ctrl Pts',(112.843483765248,-2.27706952068197,
137.42653512839));
#195888=CARTESIAN_POINT('Ctrl Pts',(112.565036141435,4.34061126924124,136.299570773982));
#195889=CARTESIAN_POINT('Ctrl Pts',(112.286588517622,6.96948235338073,130.122776741767));
#195890=CARTESIAN_POINT('Ctrl Pts',(112.008140893809,3.1937396329048,124.572324994188));
#195891=CARTESIAN_POINT('Ctrl Pts',(111.729693269996,-3.51689378735575,
124.748809532627));
#195892=CARTESIAN_POINT('Ctrl Pts',(111.451245646184,-6.99567362684944,
130.490049688009));
#195893=CARTESIAN_POINT('Ctrl Pts',(111.172798022371,-4.0457711609245,136.52012623271));
#195894=CARTESIAN_POINT('Ctrl Pts',(110.894350398558,2.62199735498092,137.297693407768));
#195895=CARTESIAN_POINT('Ctrl Pts',(110.615902774745,6.88027839335069,132.108204965571));
#195896=CARTESIAN_POINT('Ctrl Pts',(110.337455150932,4.81591970851693,125.720547263895));
#195897=CARTESIAN_POINT('Ctrl Pts',(110.059007527119,-1.67403391768677,
124.004665676154));
#195898=CARTESIAN_POINT('Ctrl Pts',(109.780559903306,-6.62563215463966,
128.537371556004));
#195899=CARTESIAN_POINT('Ctrl Pts',(109.502112279493,-5.48859812160383,
135.153329634858));
#195900=CARTESIAN_POINT('Ctrl Pts',(109.22366465568,0.692189452261082,137.772797645767));
#195901=CARTESIAN_POINT('Ctrl Pts',(108.945217031867,6.23688873483282,133.988612454835));
#195902=CARTESIAN_POINT('Ctrl Pts',(108.666769408055,6.05019195904657,127.278255384801));
#195903=CARTESIAN_POINT('Ctrl Pts',(108.388321784241,0.303664341205276,
123.808216763862));
#195904=CARTESIAN_POINT('Ctrl Pts',(108.109874160429,-5.72191597137591,
126.767292563848));
#195905=CARTESIAN_POINT('Ctrl Pts',(107.831426536616,-6.48933503739778,
133.436236683461));
#195906=CARTESIAN_POINT('Ctrl Pts',(107.552978912803,-1.29337222569216,
137.68661527281));
#195907=CARTESIAN_POINT('Ctrl Pts',(107.27453128899,5.09113647667873,135.612538050821));
#195908=CARTESIAN_POINT('Ctrl Pts',(106.996083665177,6.79713947282576,129.119980660195));
#195909=CARTESIAN_POINT('Ctrl Pts',(106.717636041364,2.25690335216928,124.175286163858));
#195910=CARTESIAN_POINT('Ctrl Pts',(106.439188417551,-4.35731669327239,
125.322387242187));
#195911=CARTESIAN_POINT('Ctrl Pts',(106.160740793739,-6.96737556435125,
131.5071540432));
#195912=CARTESIAN_POINT('Ctrl Pts',(105.882293169926,-3.17475666701035,
137.046088019424));
#195913=CARTESIAN_POINT('Ctrl Pts',(105.603845546113,3.53530851182771,136.849179438675));
#195914=CARTESIAN_POINT('Ctrl Pts',(105.3253979223,6.99659787771835,131.097377667143));
#195915=CARTESIAN_POINT('Ctrl Pts',(105.046950298487,4.02835559679407,125.076307541727));
#195916=CARTESIAN_POINT('Ctrl Pts',(104.768502674674,-2.64174868147234,
124.319038362058));
#195917=CARTESIAN_POINT('Ctrl Pts',(104.490055050861,-6.88421497806359,
129.521463509594));
#195918=CARTESIAN_POINT('Ctrl Pts',(104.211607427049,-4.80042402241278,
135.902808426348));
#195919=CARTESIAN_POINT('Ctrl Pts',(103.933159803235,1.69472209608453,137.598928879852));
#195920=CARTESIAN_POINT('Ctrl Pts',(103.654712179423,6.63250140005722,133.051173033428));
#195921=CARTESIAN_POINT('Ctrl Pts',(103.37626455561,5.47533593308374,126.438706339714));
#195922=CARTESIAN_POINT('Ctrl Pts',(103.097816931797,-0.713395771362793,
123.838062653278));
#195923=CARTESIAN_POINT('Ctrl Pts',(102.819369307984,-6.24655161324796,
127.639106473447));
#195924=CARTESIAN_POINT('Ctrl Pts',(102.540921684171,-6.03943168356949,
134.348864220799));
#195925=CARTESIAN_POINT('Ctrl Pts',(102.262474060358,-0.282369079330704,
137.801396315408));
#195926=CARTESIAN_POINT('Ctrl Pts',(101.984026436545,5.73417691431645,134.823994427897));
#195927=CARTESIAN_POINT('Ctrl Pts',(101.705578812732,6.48129445382252,128.15274543872));
#195928=CARTESIAN_POINT('Ctrl Pts',(101.427131188919,1.27241901910234,123.9182012603));
#195929=CARTESIAN_POINT('Ctrl Pts',(101.148683565106,-5.1057473330482,126.01170112362));
#195930=CARTESIAN_POINT('Ctrl Pts',(100.870235941294,-6.7919813157512,132.509420927444));
#195931=CARTESIAN_POINT('Ctrl Pts',(100.591788317481,-2.23671627601227,
137.440273603317));
#195932=CARTESIAN_POINT('Ctrl Pts',(100.313340693668,4.37398175171709,136.273046427655));
#195933=CARTESIAN_POINT('Ctrl Pts',(100.034893069855,6.96520423050629,130.080364152676));
#195934=CARTESIAN_POINT('Ctrl Pts',(99.7564454460421,3.15574429060373,124.552999259737));
#195935=CARTESIAN_POINT('Ctrl Pts',(99.4779978222292,-3.55369048568456,
124.770330058661));
#195936=CARTESIAN_POINT('Ctrl Pts',(99.1995501984162,-6.99745731306031,
130.532640162439));
#195937=CARTESIAN_POINT('Ctrl Pts',(98.9211025746034,-4.01090271452764,
136.544648090195));
#195938=CARTESIAN_POINT('Ctrl Pts',(98.6426549507905,2.66147553516503,137.281612259238));
#195939=CARTESIAN_POINT('Ctrl Pts',(98.3642073269776,6.88808778834931,132.066298600918));
#195940=CARTESIAN_POINT('Ctrl Pts',(98.0857597031646,4.78488386583629,125.691325584995));
#195941=CARTESIAN_POINT('Ctrl Pts',(97.8073120793519,-1.71539457480834,
124.014981978356));
#195942=CARTESIAN_POINT('Ctrl Pts',(97.5288644555388,-6.63930920288774,
128.577745661565));
#195943=CARTESIAN_POINT('Ctrl Pts',(97.2504168317261,-5.46202302179963,
135.186659713151));
#195944=CARTESIAN_POINT('Ctrl Pts',(96.9719692079131,0.734595481663425,
137.768454983106));
#195945=CARTESIAN_POINT('Ctrl Pts',(96.6935215841003,6.25615662446226,133.950587746053));
#195946=CARTESIAN_POINT('Ctrl Pts',(96.4150739602873,6.0286154596223,127.24149147966));
#195947=CARTESIAN_POINT('Ctrl Pts',(96.1366263364746,0.26107120162757,123.806497895168));
#195948=CARTESIAN_POINT('Ctrl Pts',(95.8581787126614,-5.74638473662552,
126.80219828796));
#195949=CARTESIAN_POINT('Ctrl Pts',(95.5797310888487,-6.47319382842077,
133.47569034516));
#195950=CARTESIAN_POINT('Ctrl Pts',(95.3012834650358,-1.25145402499642,
137.694360884412));
#195951=CARTESIAN_POINT('Ctrl Pts',(95.0228358412229,5.12031089047184,135.581457773658));
#195952=CARTESIAN_POINT('Ctrl Pts',(94.7443882174101,6.78676023868958,129.078635750625));
#195953=CARTESIAN_POINT('Ctrl Pts',(94.465940593597,2.21650847922131,124.161670573963));
#195954=CARTESIAN_POINT('Ctrl Pts',(94.1874929697842,-4.39060629019222,
125.349013033923));
#195955=CARTESIAN_POINT('Ctrl Pts',(93.9090453459715,-6.96296837196094,
131.549553414704));
#195956=CARTESIAN_POINT('Ctrl Pts',(93.6305977221583,-3.13670267981308,
137.065298019608));
#195957=CARTESIAN_POINT('Ctrl Pts',(93.3521500983456,3.5720395386382,136.82754701583));
#195958=CARTESIAN_POINT('Ctrl Pts',(93.0737024745325,6.99825192491364,131.054781961061));
#195959=CARTESIAN_POINT('Ctrl Pts',(92.7952548507199,3.99341267580637,125.051891925383));
#195960=CARTESIAN_POINT('Ctrl Pts',(92.5168072269068,-2.68117773331193,
124.335239594101));
#195961=CARTESIAN_POINT('Ctrl Pts',(92.238359603094,-6.89189678833074,129.563393449252));
#195962=CARTESIAN_POINT('Ctrl Pts',(91.959911979281,-4.7692993827493,135.931935507467));
#195963=CARTESIAN_POINT('Ctrl Pts',(91.6814643554683,1.73605116235111,137.588486737821));
#195964=CARTESIAN_POINT('Ctrl Pts',(91.4030167316553,6.6460555000649,133.010757486647));
#195965=CARTESIAN_POINT('Ctrl Pts',(91.1245691078424,5.44865951108031,126.405457301267));
#195966=CARTESIAN_POINT('Ctrl Pts',(90.8461214840295,-0.755788386771977,
123.84253436519));
#195967=CARTESIAN_POINT('Ctrl Pts',(90.5676738602166,-6.26570367949625,
127.677189650927));
#195968=CARTESIAN_POINT('Ctrl Pts',(90.2892262364038,-6.01774338740505,
134.38556228421));
#195969=CARTESIAN_POINT('Ctrl Pts',(90.0107786125907,-0.239770905396614,
137.802985537273));
#195970=CARTESIAN_POINT('Ctrl Pts',(89.7323309887781,5.75853932521132,134.78901439096));
#195971=CARTESIAN_POINT('Ctrl Pts',(89.453883364965,6.46503323623579,128.113341088056));
#195972=CARTESIAN_POINT('Ctrl Pts',(89.1754357411521,1.23047743759138,123.910583269158));
#195973=CARTESIAN_POINT('Ctrl Pts',(88.8969881173393,-5.13482701403487,
126.042870053701));
#195974=CARTESIAN_POINT('Ctrl Pts',(88.6185404935264,-6.78147629000823,
132.550734054689));
#195975=CARTESIAN_POINT('Ctrl Pts',(88.3400928697134,-2.19628014899849,
137.453766182047));
#195976=CARTESIAN_POINT('Ctrl Pts',(88.0616452459006,4.4071901546906,136.246319437167));
#195977=CARTESIAN_POINT('Ctrl Pts',(87.7831976220877,6.96066800942769,130.037978391542));
#195978=CARTESIAN_POINT('Ctrl Pts',(87.5047499982748,3.1176320110373,124.533905171779));
#195979=CARTESIAN_POINT('Ctrl Pts',(87.2263023744621,-3.59035550070555,
124.792074177916));
#195980=CARTESIAN_POINT('Ctrl Pts',(86.9478547506488,-6.99898170591706,
130.57524070557));
#195981=CARTESIAN_POINT('Ctrl Pts',(86.6694071268362,-3.97588564265574,
136.568957239218));
#195982=CARTESIAN_POINT('Ctrl Pts',(86.3909595030232,2.70085509339449,137.265291093768));
#195983=CARTESIAN_POINT('Ctrl Pts',(86.1125118792103,6.89564194272181,132.024345474689));
#195984=CARTESIAN_POINT('Ctrl Pts',(85.8340642553976,4.75367071752436,125.662293371487));
#195985=CARTESIAN_POINT('Ctrl Pts',(85.5556166315845,-1.75669166735309,
124.025549863481));
#195986=CARTESIAN_POINT('Ctrl Pts',(85.2771690077717,-6.65274022909182,
128.618202275162));
#195987=CARTESIAN_POINT('Ctrl Pts',(84.9987213839588,-5.4352455247236,135.21982740374));
#195988=CARTESIAN_POINT('Ctrl Pts',(84.7202737601459,0.776974290360158,
137.763854263368));
#195989=CARTESIAN_POINT('Ctrl Pts',(84.4418261363329,6.27519268990729,133.912446452669));
#195990=CARTESIAN_POINT('Ctrl Pts',(84.1633785125202,6.00681556763514,127.204859597945));
#195991=CARTESIAN_POINT('Ctrl Pts',(83.8849308887072,0.218468387960617,
123.805038334852));
#195992=CARTESIAN_POINT('Ctrl Pts',(83.6064832648944,-5.77064056747553,
126.837252313669));
#195993=CARTESIAN_POINT('Ctrl Pts',(83.3280356410814,-6.45681275286598,
133.515045019753));
#195994=CARTESIAN_POINT('Ctrl Pts',(83.0495880172686,-1.20948945121144,
137.701851184522));
#195995=CARTESIAN_POINT('Ctrl Pts',(82.7711403934555,5.14929556926191,135.550200479404));
#195996=CARTESIAN_POINT('Ctrl Pts',(82.4926927696429,6.77612951865689,129.037354788424));
#195997=CARTESIAN_POINT('Ctrl Pts',(82.2142451458298,2.17603147273656,124.148301131391));
#195998=CARTESIAN_POINT('Ctrl Pts',(81.9357975220171,-4.42373319158141,
125.375840975569));
#195999=CARTESIAN_POINT('Ctrl Pts',(81.6573498982041,-6.95830316421689,
131.591925172815));
#196000=CARTESIAN_POINT('Ctrl Pts',(81.3789022743912,-3.09853246094448,
137.084276018453));
#196001=CARTESIAN_POINT('Ctrl Pts',(81.1004546505783,3.60863820220999,136.805691401599));
#196002=CARTESIAN_POINT('Ctrl Pts',(80.8220070267654,6.99964664931016,131.012176975526));
#196003=CARTESIAN_POINT('Ctrl Pts',(80.5435594029525,3.95832177744353,125.02768946888));
#196004=CARTESIAN_POINT('Ctrl Pts',(80.2651117791397,-2.72050743312451,
124.351680541802));
#196005=CARTESIAN_POINT('Ctrl Pts',(79.9866641553267,-6.89932321682792,
129.605369373404));
#196006=CARTESIAN_POINT('Ctrl Pts',(79.7082165315139,-4.73799801494326,
135.960872584412));
#196007=CARTESIAN_POINT('Ctrl Pts',(79.4297689077009,1.77731589860328,137.577793207502));
#196008=CARTESIAN_POINT('Ctrl Pts',(79.1513212838881,6.65936332804202,132.970260181018));
#196009=CARTESIAN_POINT('Ctrl Pts',(78.8728736600752,5.42178118699497,126.372371265798));
#196010=CARTESIAN_POINT('Ctrl Pts',(78.5944260362623,-0.798152996164653,
123.847264050135));
#196011=CARTESIAN_POINT('Ctrl Pts',(78.3159784124494,-6.28462356779051,
127.715388706879));
#196012=CARTESIAN_POINT('Ctrl Pts',(78.0375307886365,-5.99583210154638,
134.422127644877));
#196013=CARTESIAN_POINT('Ctrl Pts',(77.7590831648237,-0.197163846663491,
137.804315422519));
#196014=CARTESIAN_POINT('Ctrl Pts',(77.4806355410107,5.78268835131386,134.753886701214));
#196015=CARTESIAN_POINT('Ctrl Pts',(77.2021879171979,6.44853245446487,128.07403645411));
#196016=CARTESIAN_POINT('Ctrl Pts',(76.9237402933849,1.18849026028645,123.903220729472));
#196017=CARTESIAN_POINT('Ctrl Pts',(76.6452926695721,-5.16371642211823,
126.074215422566));
#196018=CARTESIAN_POINT('Ctrl Pts',(76.3668450457591,-6.77071997416741,
132.591982469425));
#196019=CARTESIAN_POINT('Ctrl Pts',(76.0883974219463,-2.15576263801617,
137.467012364608));
#196020=CARTESIAN_POINT('Ctrl Pts',(75.8099497981334,4.44023524761227,136.219390792892));
#196021=CARTESIAN_POINT('Ctrl Pts',(75.5315021743204,6.95587385823614,129.995621028982));
#196022=CARTESIAN_POINT('Ctrl Pts',(75.2530545505077,3.0794042064702,124.515043437855));
#196023=CARTESIAN_POINT('Ctrl Pts',(74.9746069266946,-3.62688747378295,
124.814041084656));
#196024=CARTESIAN_POINT('Ctrl Pts',(74.6961593028819,-7.0002467489329,130.617849738824));
#196025=CARTESIAN_POINT('Ctrl Pts',(74.4177116790688,-3.94072124287924,
136.593052778991));
#196026=CARTESIAN_POINT('Ctrl Pts',(74.1392640552561,2.74013457044532,137.248730516143));
#196027=CARTESIAN_POINT('Ctrl Pts',(73.860816431443,6.90294057654623,131.982347141473));
#196028=CARTESIAN_POINT('Ctrl Pts',(73.5823688076304,4.72228142019582,125.633451699173));
#196029=CARTESIAN_POINT('Ctrl Pts',(73.3039211838172,-1.79792366504193,
124.036368939932));
#196030=CARTESIAN_POINT('Ctrl Pts',(73.0254735600045,-6.66592473556012,
128.658739897661));
#196031=CARTESIAN_POINT('Ctrl Pts',(72.7470259361915,-5.40826662262595,
135.252831477583));
#196032=CARTESIAN_POINT('Ctrl Pts',(72.4685783123786,0.819324307988826,
137.758995657032));
#196033=CARTESIAN_POINT('Ctrl Pts',(72.1901306885658,6.2939962257795,133.87418998802));
#196034=CARTESIAN_POINT('Ctrl Pts',(71.9116830647529,5.98479309088811,127.168361097063));
#196035=CARTESIAN_POINT('Ctrl Pts',(71.63323544094,0.17585747886725,123.803838136996));
#196036=CARTESIAN_POINT('Ctrl Pts',(71.3547878171271,-5.79468256511725,
126.872453342036));
#196037=CARTESIAN_POINT('Ctrl Pts',(71.0763401933142,-6.44019241774003,
133.554299248939));
#196038=CARTESIAN_POINT('Ctrl Pts',(70.7978925695013,-1.16748005934989,
137.709085895581));
#196039=CARTESIAN_POINT('Ctrl Pts',(70.5194449456884,5.17808943901089,135.518767326308));
#196040=CARTESIAN_POINT('Ctrl Pts',(70.2409973218756,6.76524770665308,128.996139303274));
#196041=CARTESIAN_POINT('Ctrl Pts',(69.9625496980626,2.1354738326052,124.135178331551));
#196042=CARTESIAN_POINT('Ctrl Pts',(69.6841020742497,-4.45669616991057,
125.402870073008));
#196043=CARTESIAN_POINT('Ctrl Pts',(69.4056544504369,-6.95338011399016,
131.634267747431));
#196044=CARTESIAN_POINT('Ctrl Pts',(69.1272068266238,-3.06024742481583,
137.103021312725));
#196045=CARTESIAN_POINT('Ctrl Pts',(68.8487592028112,3.64510314636624,136.783613405848));
#196046=CARTESIAN_POINT('Ctrl Pts',(68.5703115789981,7.00078199922599,130.969564289278));
#196047=CARTESIAN_POINT('Ctrl Pts',(68.2918639551854,3.92308420201135,125.003701069051));
#196048=CARTESIAN_POINT('Ctrl Pts',(68.0134163313723,-2.75973632353393,
124.368360595937));
#196049=CARTESIAN_POINT('Ctrl Pts',(67.7349687075595,-6.90649398836592,
129.647389726619));
#196050=CARTESIAN_POINT('Ctrl Pts',(67.4565210837467,-4.70652107887851,
135.98961858491));
#196051=CARTESIAN_POINT('Ctrl Pts',(67.1780734599337,1.81851477576126,137.566848685147));
#196052=CARTESIAN_POINT('Ctrl Pts',(66.8996258361208,6.67242439086218,132.929682617185));
#196053=CARTESIAN_POINT('Ctrl Pts',(66.6211782123079,5.39470195681365,126.339449459324));
#196054=CARTESIAN_POINT('Ctrl Pts',(66.3427305884951,-0.840488029704522,
123.852251532852));
#196055=CARTESIAN_POINT('Ctrl Pts',(66.0642829646821,-6.30331057704718,
127.753702225821));
#196056=CARTESIAN_POINT('Ctrl Pts',(65.7858353408693,-5.97369863792435,
134.458558947856));
#196057=CARTESIAN_POINT('Ctrl Pts',(65.5073877170563,-0.154549481951222,
137.805385921867));
#196058=CARTESIAN_POINT('Ctrl Pts',(65.2289400932435,5.80662309777304,134.718612660325));
#196059=CARTESIAN_POINT('Ctrl Pts',(64.9504924694306,6.43179271995227,128.03483299333));
#196060=CARTESIAN_POINT('Ctrl Pts',(64.6720448456177,1.14645904303803,123.896113914062));
#196061=CARTESIAN_POINT('Ctrl Pts',(64.3935972218049,-5.19241448679041,
126.1057360687));
#196062=CARTESIAN_POINT('Ctrl Pts',(64.1151495979918,-6.75971276680813,
132.633164643176));
#196063=CARTESIAN_POINT('Ctrl Pts',(63.8367019741791,-2.11516524445634,
137.480011660159));
#196064=CARTESIAN_POINT('Ctrl Pts',(63.5582543503661,4.47311580598391,136.192261492683));
#196065=CARTESIAN_POINT('Ctrl Pts',(63.2798067265533,6.95082195458075,129.953293634565));
#196066=CARTESIAN_POINT('Ctrl Pts',(63.0013591027403,3.041062293448,124.496414756892));
#196067=CARTESIAN_POINT('Ctrl Pts',(62.7229114789275,-3.66328505121137,
124.836229964889));
#196068=CARTESIAN_POINT('Ctrl Pts',(62.4444638551145,-7.00125239523119,
130.660465683307));
#196069=CARTESIAN_POINT('Ctrl Pts',(62.1660162313017,-3.90541081822766,
136.616933816649));
#196070=CARTESIAN_POINT('Ctrl Pts',(61.8875686074887,2.77931251080179,137.231931140021));
#196071=CARTESIAN_POINT('Ctrl Pts',(61.609120983676,6.909983419369,131.940305157533));
#196072=CARTESIAN_POINT('Ctrl Pts',(61.3306733598629,4.69071713699276,125.604801636791));
#196073=CARTESIAN_POINT('Ctrl Pts',(61.0522257360502,-1.83908904000824,
124.047438806804));
#196074=CARTESIAN_POINT('Ctrl Pts',(60.7737781122372,-6.67886223373588,
128.699357026925));
#196075=CARTESIAN_POINT('Ctrl Pts',(60.4953304884244,-5.38108731521968,
135.285670711703));
#196076=CARTESIAN_POINT('Ctrl Pts',(60.2168828646114,0.861643965253713,
137.753879344138));
#196077=CARTESIAN_POINT('Ctrl Pts',(59.9384352407986,6.31256653530686,133.835819769716));
#196078=CARTESIAN_POINT('Ctrl Pts',(59.6599876169856,5.96254884543232,127.131997329482));
#196079=CARTESIAN_POINT('Ctrl Pts',(59.3815399931728,0.133240053310041,
123.802897346075));
#196080=CARTESIAN_POINT('Ctrl Pts',(59.1030923693598,-5.81850983866561,
126.907800068673));
#196081=CARTESIAN_POINT('Ctrl Pts',(58.824644745547,-6.42333343891552,133.593451578138));
#196082=CARTESIAN_POINT('Ctrl Pts',(58.5461971217341,-1.12542740608588,
137.716064749505));
#196083=CARTESIAN_POINT('Ctrl Pts',(58.2677494979212,5.20669143275151,135.487159479138));
#196084=CARTESIAN_POINT('Ctrl Pts',(57.9893018741083,6.75411520590753,128.954990822428));
#196085=CARTESIAN_POINT('Ctrl Pts',(57.7108542502954,2.09483706170563,124.122302660713));
#196086=CARTESIAN_POINT('Ctrl Pts',(57.4324066264825,-4.48949400372376,
125.430099324666));
#196087=CARTESIAN_POINT('Ctrl Pts',(57.1539590026696,-6.94819940370625,
131.676579569534));
#196088=CARTESIAN_POINT('Ctrl Pts',(56.8755113788568,-3.02184899009409,
137.121533207807));
#196089=CARTESIAN_POINT('Ctrl Pts',(56.5970637550437,3.68143301988451,136.761313846687));
#196090=CARTESIAN_POINT('Ctrl Pts',(56.318616131231,7.00165793259049,130.926945481348));
#196091=CARTESIAN_POINT('Ctrl Pts',(56.040168507418,3.88770125525153,124.979927614796));
#196092=CARTESIAN_POINT('Ctrl Pts',(55.7617208836052,-2.79886295089852,
124.385279138419));
#196093=CARTESIAN_POINT('Ctrl Pts',(55.4832732597923,-6.91340883722955,
129.689452951814));
#196094=CARTESIAN_POINT('Ctrl Pts',(55.2048256359794,-4.67486974094423,
136.018172443767));
#196095=CARTESIAN_POINT('Ctrl Pts',(54.9263780121665,1.85964626718557,137.555653576309));
#196096=CARTESIAN_POINT('Ctrl Pts',(54.6479303883536,6.68523820454244,132.889026298762));
#196097=CARTESIAN_POINT('Ctrl Pts',(54.3694827645407,5.36742282396772,126.306693101776));
#196098=CARTESIAN_POINT('Ctrl Pts',(54.0910351407278,-0.882791918651148,
123.857496628527));
#196099=CARTESIAN_POINT('Ctrl Pts',(53.8125875169149,-6.32176401481248,
127.792128788032));
#196100=CARTESIAN_POINT('Ctrl Pts',(53.534139893102,-5.95134381670231,134.494854843172));
#196101=CARTESIAN_POINT('Ctrl Pts',(53.2556922692892,-0.111929390351441,
137.806196995646));
#196102=CARTESIAN_POINT('Ctrl Pts',(52.9772446454762,5.83034267767769,134.683193575387));
#196103=CARTESIAN_POINT('Ctrl Pts',(52.6987970216634,6.41481465299549,127.995732158415));
#196104=CARTESIAN_POINT('Ctrl Pts',(52.4203493978505,1.10438534332797,123.889263086274));
#196105=CARTESIAN_POINT('Ctrl Pts',(52.1419017740376,-5.22092014463445,
126.137430824095));
#196106=CARTESIAN_POINT('Ctrl Pts',(51.8634541502246,-6.74845507580631,
132.674279049921));
#196107=CARTESIAN_POINT('Ctrl Pts',(51.5850065264118,-2.07448947267055,
137.492763587005));
#196108=CARTESIAN_POINT('Ctrl Pts',(51.3065589025989,4.50583061140446,136.164932541826));
#196109=CARTESIAN_POINT('Ctrl Pts',(51.028111278786,6.94551248566166,129.910997776748));
#196110=CARTESIAN_POINT('Ctrl Pts',(50.7496636549731,3.00260769274395,124.478019819181));
#196111=CARTESIAN_POINT('Ctrl Pts',(50.4712160311602,-3.69954688426507,
124.858639996399));
#196112=CARTESIAN_POINT('Ctrl Pts',(50.1927684073473,-7.00199860754717,
130.70308695987));
#196113=CARTESIAN_POINT('Ctrl Pts',(49.9143207835345,-3.86995567714208,
136.640599467269));
#196114=CARTESIAN_POINT('Ctrl Pts',(49.6358731597215,2.81838746271124,137.214893587909));
#196115=CARTESIAN_POINT('Ctrl Pts',(49.3574255359087,6.91677021021505,131.89822108075));
#196116=CARTESIAN_POINT('Ctrl Pts',(49.0789779120958,4.65897903754105,125.576344245977));
#196117=CARTESIAN_POINT('Ctrl Pts',(48.8005302882828,-1.88018626685394,
124.058759053897));
#196118=CARTESIAN_POINT('Ctrl Pts',(48.5220826644701,-6.69155224421552,
128.740052157871));
#196119=CARTESIAN_POINT('Ctrl Pts',(48.243635040657,-5.35370860964396,135.318343889229));
#196120=CARTESIAN_POINT('Ctrl Pts',(47.9651874168443,0.903931693984841,
137.748505514272));
#196121=CARTESIAN_POINT('Ctrl Pts',(47.6867397930313,6.33090293035988,133.797337219578));
#196122=CARTESIAN_POINT('Ctrl Pts',(47.4082921692184,5.94008365553619,127.095769642671));
#196123=CARTESIAN_POINT('Ctrl Pts',(47.1298445454056,0.0906176904940206,
123.80221599695));
#196124=CARTESIAN_POINT('Ctrl Pts',(46.8513969215926,-5.84212150519187,
126.943291183793));
#196125=CARTESIAN_POINT('Ctrl Pts',(46.5729492977799,-6.40623644110861,
133.632500556544));
#196126=CARTESIAN_POINT('Ctrl Pts',(46.2945016739667,-1.08333304969514,
137.722787487691));
#196127=CARTESIAN_POINT('Ctrl Pts',(46.016054050154,5.23510049062639,135.455378109134));
#196128=CARTESIAN_POINT('Ctrl Pts',(45.737606426341,6.7427324289391,128.913910870662));
#196129=CARTESIAN_POINT('Ctrl Pts',(45.4591588025282,2.0541226658487,124.10967459599));
#196130=CARTESIAN_POINT('Ctrl Pts',(45.1807111787153,-4.5221254776858,125.457527721552));
#196131=CARTESIAN_POINT('Ctrl Pts',(44.9022635549024,-6.94276122533821,
131.718859071242));
#196132=CARTESIAN_POINT('Ctrl Pts',(44.6238159310895,-2.98333857964632,
137.139811017737));
#196133=CARTESIAN_POINT('Ctrl Pts',(44.3453683072766,3.71762647654865,136.738793550433));
#196134=CARTESIAN_POINT('Ctrl Pts',(44.0669206834637,7.00227441694529,130.88432213099));
#196135=CARTESIAN_POINT('Ctrl Pts',(43.7884730596509,3.85217424829189,124.956369987047));
#196136=CARTESIAN_POINT('Ctrl Pts',(43.5100254358379,-2.8378858653675,124.402435542326));
#196137=CARTESIAN_POINT('Ctrl Pts',(43.2315778120251,-6.92006750718621,
129.731557490323));
#196138=CARTESIAN_POINT('Ctrl Pts',(42.9531301882121,-4.64304517399252,
136.04653310291));
#196139=CARTESIAN_POINT('Ctrl Pts',(42.6746825643993,1.90070884873357,137.544208295828));
#196140=CARTESIAN_POINT('Ctrl Pts',(42.3962349405864,6.69780429426274,132.848292732287));
#196141=CARTESIAN_POINT('Ctrl Pts',(42.1177873167735,5.33994479929498,126.274103406951));
#196142=CARTESIAN_POINT('Ctrl Pts',(41.8393396929606,-0.925063095418803,
123.862999142802));
#196143=CARTESIAN_POINT('Ctrl Pts',(41.5608920691476,-6.33998319728738,
127.8306669696));
#196144=CARTESIAN_POINT('Ctrl Pts',(41.2824444453348,-5.92876846624656,
134.531013985867));
#196145=CARTESIAN_POINT('Ctrl Pts',(41.0039968215219,-0.069305151166692,
137.806748613804));
#196146=CARTESIAN_POINT('Ctrl Pts',(40.725549197709,5.85384621209049,134.647630758868));
#196147=CARTESIAN_POINT('Ctrl Pts',(40.4471015738961,6.39759888272248,127.956735398261));
#196148=CARTESIAN_POINT('Ctrl Pts',(40.1686539500832,1.06227072021291,123.882668499967));
#196149=CARTESIAN_POINT('Ctrl Pts',(39.8902063262704,-5.24923233936253,
126.169298514289));
#196150=CARTESIAN_POINT('Ctrl Pts',(39.6117587024575,-6.73694731831984,
132.715324166149));
#196151=CARTESIAN_POINT('Ctrl Pts',(39.3333110786445,-2.03373682991476,
137.505267672621));
#196152=CARTESIAN_POINT('Ctrl Pts',(39.0548634548317,4.53837845161457,136.137404953004));
#196153=CARTESIAN_POINT('Ctrl Pts',(38.7764158310188,6.9399456482232,129.86873502282));
#196154=CARTESIAN_POINT('Ctrl Pts',(38.4979682072059,2.96404182930761,124.459859306355));
#196155=CARTESIAN_POINT('Ctrl Pts',(38.219520583393,-3.73567162924815,124.881270348773));
#196156=CARTESIAN_POINT('Ctrl Pts',(37.9410729595801,-7.00248535822977,
130.745711989165));
#196157=CARTESIAN_POINT('Ctrl Pts',(37.6626253357672,-3.83435713342598,
136.664048853912));
#196158=CARTESIAN_POINT('Ctrl Pts',(37.3841777119543,2.8573579782368,137.197618491141));
#196159=CARTESIAN_POINT('Ctrl Pts',(37.1057300881414,6.92330069759731,131.856096470565));
#196160=CARTESIAN_POINT('Ctrl Pts',(36.8272824643285,4.62706829790778,125.548080581235));
#196161=CARTESIAN_POINT('Ctrl Pts',(36.5488348405156,-1.92121382270608,
124.070329261737));
#196162=CARTESIAN_POINT('Ctrl Pts',(36.2703872167028,-6.70399429676593,
128.780823782526));
#196163=CARTESIAN_POINT('Ctrl Pts',(35.9919395928899,-5.32613152042688,
135.350849799446));
#196164=CARTESIAN_POINT('Ctrl Pts',(35.7134919690769,0.946185927194629,
137.742874366562));
#196165=CARTESIAN_POINT('Ctrl Pts',(35.4350443452641,6.34900473147662,133.758743763591));
#196166=CARTESIAN_POINT('Ctrl Pts',(35.1565967214512,5.91739835365575,127.059679379064));
#196167=CARTESIAN_POINT('Ctrl Pts',(34.8781490976383,0.0479919698059151,
123.80179411487));
#196168=CARTESIAN_POINT('Ctrl Pts',(34.5997014738253,-5.8655166897575,126.978925372262));
#196169=CARTESIAN_POINT('Ctrl Pts',(34.3212538500126,-6.38890205785425,
133.671444737187));
#196170=CARTESIAN_POINT('Ctrl Pts',(34.0428062261996,-1.04119854999986,
137.729253861025));
#196171=CARTESIAN_POINT('Ctrl Pts',(33.7643586023867,5.26331555992738,135.423424393967));
#196172=CARTESIAN_POINT('Ctrl Pts',(33.4859109785738,6.73109979754094,128.872900970206));
#196173=CARTESIAN_POINT('Ctrl Pts',(33.207463354761,2.01333215372067,124.097294605319));
#196174=CARTESIAN_POINT('Ctrl Pts',(32.9290157309481,-4.55458938262534,
125.485154247296));
#196175=CARTESIAN_POINT('Ctrl Pts',(32.6505681071352,-6.93706578039975,
131.761104685873));
#196176=CARTESIAN_POINT('Ctrl Pts',(32.3721204833222,-2.94471762049033,
137.157854065221));
#196177=CARTESIAN_POINT('Ctrl Pts',(32.0936728595094,3.75368217519627,136.716053351584));
#196178=CARTESIAN_POINT('Ctrl Pts',(31.8152252356965,7.00263142944649,130.84169581763));
#196179=CARTESIAN_POINT('Ctrl Pts',(31.5367776118836,3.8165044975991,124.933029058741));
#196180=CARTESIAN_POINT('Ctrl Pts',(31.2583299880707,-2.87680362093211,
124.41982917192));
#196181=CARTESIAN_POINT('Ctrl Pts',(30.9798823642578,-6.92646975149653,
129.773701781947));
#196182=CARTESIAN_POINT('Ctrl Pts',(30.7014347404449,-4.6110485572945,136.074699511423));
#196183=CARTESIAN_POINT('Ctrl Pts',(30.422987116632,1.94170099881587,137.532513267813));
#196184=CARTESIAN_POINT('Ctrl Pts',(30.1445394928192,6.71012219438185,132.807483427156));
#196185=CARTESIAN_POINT('Ctrl Pts',(29.8660918690062,5.31226890100394,126.241681582474));
#196186=CARTESIAN_POINT('Ctrl Pts',(29.5876442451933,-0.967299993633269,
123.868758871779));
#196187=CARTESIAN_POINT('Ctrl Pts',(29.3091966213805,-6.35796744935336,
127.869315342481));
#196188=CARTESIAN_POINT('Ctrl Pts',(29.0307489975676,-5.90597342309497,
134.567035036052));
#196189=CARTESIAN_POINT('Ctrl Pts',(28.7523013737546,-0.026678343854083,
137.807040755898));
#196190=CARTESIAN_POINT('Ctrl Pts',(28.4738537499418,5.87713283007914,134.611925528561));
#196191=CARTESIAN_POINT('Ctrl Pts',(28.1954061261289,6.38014604707014,127.917844157905));
#196192=CARTESIAN_POINT('Ctrl Pts',(27.916958502316,1.02011673426565,123.876330399509));
#196193=CARTESIAN_POINT('Ctrl Pts',(27.6385108785031,-5.27735002185588,
126.201337958415));
#196194=CARTESIAN_POINT('Ctrl Pts',(27.3600632546902,-6.72518992077305,
132.756298470923));
#196195=CARTESIAN_POINT('Ctrl Pts',(27.0816156308773,-1.99290882629253,
137.51752345366));
#196196=CARTESIAN_POINT('Ctrl Pts',(26.8031680070644,4.57075812054227,136.109679746264));
#196197=CARTESIAN_POINT('Ctrl Pts',(26.5247203832516,6.93412164854658,129.826506938842));
#196198=CARTESIAN_POINT('Ctrl Pts',(26.2462727594386,2.92536613221128,124.441933891359));
#196199=CARTESIAN_POINT('Ctrl Pts',(25.9678251356258,-3.7716579475455,124.904120183435));
#196200=CARTESIAN_POINT('Ctrl Pts',(25.6893775118128,-7.00271262924226,
130.788339191706));
#196201=CARTESIAN_POINT('Ctrl Pts',(25.410929888,-3.79861650619593,136.687281107654));
#196202=CARTESIAN_POINT('Ctrl Pts',(25.1324822641871,2.89622261331168,137.180106489852));
#196203=CARTESIAN_POINT('Ctrl Pts',(24.8540346403742,6.92957463952618,131.813932887921));
#196204=CARTESIAN_POINT('Ctrl Pts',(24.5755870165613,4.59498610055721,125.520011689881));
#196205=CARTESIAN_POINT('Ctrl Pts',(24.2971393927484,-1.96217018727317,
124.082149001586));
#196206=CARTESIAN_POINT('Ctrl Pts',(24.0186917689355,-6.71618793034234,
128.821670390082));
#196207=CARTESIAN_POINT('Ctrl Pts',(23.7402441451226,-5.29835706944761,
135.383187237832));
#196208=CARTESIAN_POINT('Ctrl Pts',(23.4617965213097,0.988405099136929,
137.736986109674));
#196209=CARTESIAN_POINT('Ctrl Pts',(23.1833488974968,6.36687126788796,133.720040831851));
#196210=CARTESIAN_POINT('Ctrl Pts',(22.9049012736839,5.89449378040337,127.023727875996));
#196211=CARTESIAN_POINT('Ctrl Pts',(22.6264536498711,0.00536447075796404,
123.801631715467));
#196212=CARTESIAN_POINT('Ctrl Pts',(22.3480060260581,-5.88869452544514,
127.01470131364));
#196213=CARTESIAN_POINT('Ctrl Pts',(22.0695584022453,-6.3713309314846,133.710282676972));
#196214=CARTESIAN_POINT('Ctrl Pts',(21.7911107784324,-0.999025468309402,
137.735463629893));
#196215=CARTESIAN_POINT('Ctrl Pts',(21.5126631546195,5.29133559513472,135.391299517692));
#196216=CARTESIAN_POINT('Ctrl Pts',(21.2342155308066,6.71921774276442,128.831962640697));
#196217=CARTESIAN_POINT('Ctrl Pts',(20.9557679069937,1.97246703682929,124.085163147446));
#196218=CARTESIAN_POINT('Ctrl Pts',(20.6773202831809,-4.58688451558038,
125.51297787819));
#196219=CARTESIAN_POINT('Ctrl Pts',(20.3988726593679,-6.93111327993769,
131.803314848003));
#196220=CARTESIAN_POINT('Ctrl Pts',(20.120425035555,-2.90598754374001,137.175661681671));
#196221=CARTESIAN_POINT('Ctrl Pts',(19.8419774117421,3.78959877977074,136.693094092787));
#196222=CARTESIAN_POINT('Ctrl Pts',(19.5635297879293,7.00272895686486,130.799068120799));
#196223=CARTESIAN_POINT('Ctrl Pts',(19.2850821641163,3.78069332492835,124.909905694786));
#196224=CARTESIAN_POINT('Ctrl Pts',(19.0066345403035,-2.91561477548059,
124.437459382677));
#196225=CARTESIAN_POINT('Ctrl Pts',(18.7281869164906,-6.932615332923,129.815884265012));
#196226=CARTESIAN_POINT('Ctrl Pts',(18.4497392926777,-4.57888107649638,
136.102670625591));
#196227=CARTESIAN_POINT('Ctrl Pts',(18.1712916688647,1.98262119845391,137.520568925627));
#196228=CARTESIAN_POINT('Ctrl Pts',(17.892844045052,6.72219144845534,132.766599895572));
#196229=CARTESIAN_POINT('Ctrl Pts',(17.614396421239,5.28439615463518,126.209428829746));
#196230=CARTESIAN_POINT('Ctrl Pts',(17.3359487974261,-1.00950104819076,
123.87477560203));
#196231=CARTESIAN_POINT('Ctrl Pts',(17.0575011736132,-6.37571610459714,
127.908072474542));
#196232=CARTESIAN_POINT('Ctrl Pts',(16.7790535498004,-5.88295953192644,
134.602916658952));
#196233=CARTESIAN_POINT('Ctrl Pts',(16.5006059259874,0.0159494520341194,
137.807073411106));
#196234=CARTESIAN_POINT('Ctrl Pts',(16.2221583021745,5.90020166874948,134.576079207535));
#196235=CARTESIAN_POINT('Ctrl Pts',(15.9437106783617,6.3624567927597,127.879059878479));
#196236=CARTESIAN_POINT('Ctrl Pts',(15.6652630545488,0.977924947517885,
123.870249019757));
#196237=CARTESIAN_POINT('Ctrl Pts',(15.3868154307359,-5.3052721502032,126.233547969238));
#196238=CARTESIAN_POINT('Ctrl Pts',(15.108367806923,-6.71318331884074,132.797200445919));
#196239=CARTESIAN_POINT('Ctrl Pts',(14.8299201831101,-1.95200697470083,
137.529530475982));
#196240=CARTESIAN_POINT('Ctrl Pts',(14.5514725592972,4.6029684183469,136.081757948972));
#196241=CARTESIAN_POINT('Ctrl Pts',(14.2730249354843,6.92804070244224,129.784315089592));
#196242=CARTESIAN_POINT('Ctrl Pts',(13.9945773116714,2.88658203459712,124.424244238425));
#196243=CARTESIAN_POINT('Ctrl Pts',(13.7161296878585,-3.80750450567058,
124.927188653676));
#196244=CARTESIAN_POINT('Ctrl Pts',(13.4376820640456,-7.00268041216303,
130.830966987928));
#196245=CARTESIAN_POINT('Ctrl Pts',(13.1592344402328,-3.7627351198343,136.710295367612));
#196246=CARTESIAN_POINT('Ctrl Pts',(12.8807868164199,2.93497992779253,137.162358232954));
#196247=CARTESIAN_POINT('Ctrl Pts',(12.602339192607,6.93559180351842,131.771731895206));
#196248=CARTESIAN_POINT('Ctrl Pts',(12.323891568794,4.56273363430679,125.49213861202));
#196249=CARTESIAN_POINT('Ctrl Pts',(12.0454439449812,-2.00305384290271,
124.094217835458));
#196250=CARTESIAN_POINT('Ctrl Pts',(11.7669963211683,-6.72813269310505,
128.862590466954));
#196251=CARTESIAN_POINT('Ctrl Pts',(11.4885486973554,-5.27038628589867,
135.415355006116));
#196252=CARTESIAN_POINT('Ctrl Pts',(11.2101010735425,1.03058764536478,137.730840961799));
#196253=CARTESIAN_POINT('Ctrl Pts',(10.9316534497296,6.38450187754329,133.681229858508));
#196254=CARTESIAN_POINT('Ctrl Pts',(10.6532058259167,5.87137078451608,126.987916465666));
#196255=CARTESIAN_POINT('Ctrl Pts',(10.3747582021038,-0.0372632270726686,
123.801728804758));
#196256=CARTESIAN_POINT('Ctrl Pts',(10.0963105782909,-5.91165415339157,
127.050617682238));
#196257=CARTESIAN_POINT('Ctrl Pts',(9.81786295447806,-6.35352371310424,
133.749012936746));
#196258=CARTESIAN_POINT('Ctrl Pts',(9.53941533066515,-0.956815367363035,
137.741416564191));
#196259=CARTESIAN_POINT('Ctrl Pts',(9.26096770685226,5.31915955795546,135.35900467071));
#196260=CARTESIAN_POINT('Ctrl Pts',(8.98252008303941,6.70708670490366,128.791097399121));
#196261=CARTESIAN_POINT('Ctrl Pts',(8.70407245922646,1.93152882944647,124.073280671906));
#196262=CARTESIAN_POINT('Ctrl Pts',(8.42562483541358,-4.61900967984285,
125.540997583217));
#196263=CARTESIAN_POINT('Ctrl Pts',(8.14717721160073,-6.92490394452403,
131.845487993513));
#196264=CARTESIAN_POINT('Ctrl Pts',(7.86872958778781,-2.86714978455288,
137.193233207215));
#196265=CARTESIAN_POINT('Ctrl Pts',(7.59028196397491,3.82537495936868,136.669916624805));
#196266=CARTESIAN_POINT('Ctrl Pts',(7.31183434016203,7.00256699558648,130.756440620084));
#196267=CARTESIAN_POINT('Ctrl Pts',(7.03338671634916,3.7447420572761,124.887000752025));
#196268=CARTESIAN_POINT('Ctrl Pts',(6.75493909253623,-2.95431789085107,
124.455325521299));
#196269=CARTESIAN_POINT('Ctrl Pts',(6.47649146872337,-6.9385040237388,129.858103376433));
#196270=CARTESIAN_POINT('Ctrl Pts',(6.19804384491048,-4.54654392357636,
136.130445408932));
#196271=CARTESIAN_POINT('Ctrl Pts',(5.91959622109758,2.02346793133434,137.508375711873));
#196272=CARTESIAN_POINT('Ctrl Pts',(5.64114859728465,6.73401160925262,132.725643652489));
#196273=CARTESIAN_POINT('Ctrl Pts',(5.36270097347181,5.25632759302358,126.177346343905));
#196274=CARTESIAN_POINT('Ctrl Pts',(5.08425334965889,-1.05166469531565,
123.881049110601));
#196275=CARTESIAN_POINT('Ctrl Pts',(4.80580572584599,-6.39322850533622,
127.946936929627));
#196276=CARTESIAN_POINT('Ctrl Pts',(4.5273581020331,-5.85972764552883,134.638657524961));
#196277=CARTESIAN_POINT('Ctrl Pts',(4.24891047822024,0.0585766569097649,
137.806846578216));
#196278=CARTESIAN_POINT('Ctrl Pts',(3.97046285440732,5.92305187327717,134.54009312409));
#196279=CARTESIAN_POINT('Ctrl Pts',(3.69201523059441,6.34453177527304,127.840383997147));
#196280=CARTESIAN_POINT('Ctrl Pts',(3.41356760678156,0.935696923401329,
123.864424586062));
#196281=CARTESIAN_POINT('Ctrl Pts',(3.13511998296867,-5.33299768974021,
126.265927353204));
#196282=CARTESIAN_POINT('Ctrl Pts',(2.85667235915575,-6.70092795743158,
132.838028575505));
#196283=CARTESIAN_POINT('Ctrl Pts',(2.57822473534285,-1.91103279077285,
137.541288294661));
#196284=CARTESIAN_POINT('Ctrl Pts',(2.29977711153,4.63500815146407,136.053640595781));
#196285=CARTESIAN_POINT('Ctrl Pts',(2.02132948771708,6.92170303524179,129.742161038504));
#196286=CARTESIAN_POINT('Ctrl Pts',(1.74288186390418,2.84769097362441,124.40679100305));
#196287=CARTESIAN_POINT('Ctrl Pts',(1.46443424009131,-3.84320997531586,
124.950474904685));
#196288=CARTESIAN_POINT('Ctrl Pts',(1.18598661627842,-7.00238870818588,
130.873593798241));
#196289=CARTESIAN_POINT('Ctrl Pts',(0.907538992465495,-3.72671430393905,
136.733090780986));
#196290=CARTESIAN_POINT('Ctrl Pts',(0.629091368652655,2.97362848551254,
137.144374378117));
#196291=CARTESIAN_POINT('Ctrl Pts',(0.350643744839755,6.94135196660579,
131.729495056193));
#196292=CARTESIAN_POINT('Ctrl Pts',(0.0721961210268491,4.53031209428387,
125.4644623805));
#196293=CARTESIAN_POINT('Ctrl Pts',(-0.206251502786054,-2.04386327463549,
124.106535316138));
#196294=CARTESIAN_POINT('Ctrl Pts',(-0.484699126598912,-6.73982814243653,
128.903582496833));
#196295=CARTESIAN_POINT('Ctrl Pts',(-0.763146750411823,-5.24222020624778,
135.447351912307));
#196296=CARTESIAN_POINT('Ctrl Pts',(-1.04159437422473,1.07273200278813,
137.724439150648));
#196297=CARTESIAN_POINT('Ctrl Pts',(-1.32004199803759,6.40189590713365,
133.642312281717));
#196298=CARTESIAN_POINT('Ctrl Pts',(-1.59848962185049,5.84803022282516,
126.952246475077));
#196299=CARTESIAN_POINT('Ctrl Pts',(-1.87693724566341,-0.0798895441007186,
123.802085379146));
#196300=CARTESIAN_POINT('Ctrl Pts',(-2.1553848694763,-5.93439472281934,
127.08667314716));
#196301=CARTESIAN_POINT('Ctrl Pts',(-2.43383249328916,-6.33548106256618,
133.787634081347));
#196302=CARTESIAN_POINT('Ctrl Pts',(-2.71228011710207,-0.914569811271147,
137.747112443329));
#196303=CARTESIAN_POINT('Ctrl Pts',(-2.99072774091498,5.34678641736288,
135.326541049718));
#196304=CARTESIAN_POINT('Ctrl Pts',(-3.26917536472784,6.6947071334783,128.750306759754));
#196305=CARTESIAN_POINT('Ctrl Pts',(-3.54762298854074,1.89051904855254,
124.061647619009));
#196306=CARTESIAN_POINT('Ctrl Pts',(-3.82607061235365,-4.65096368500298,
125.569212324096));
#196307=CARTESIAN_POINT('Ctrl Pts',(-4.10451823616654,-6.91843800424817,
131.887622559669));
#196308=CARTESIAN_POINT('Ctrl Pts',(-4.38296585997939,-2.82820578207579,
137.210567990736));
#196309=CARTESIAN_POINT('Ctrl Pts',(-4.66141348379231,3.86100938829084,
136.646521806489));
#196310=CARTESIAN_POINT('Ctrl Pts',(-4.93986110760522,7.00214555161287,
130.713814895061));
#196311=CARTESIAN_POINT('Ctrl Pts',(-5.21830873141809,3.70865202682979,
124.864315079211));
#196312=CARTESIAN_POINT('Ctrl Pts',(-5.49675635523098,-2.99291153288594,
124.473426925751));
#196313=CARTESIAN_POINT('Ctrl Pts',(-5.77520397904388,-6.9441356057364,
129.900357551763));
#196314=CARTESIAN_POINT('Ctrl Pts',(-6.05365160285679,-4.51403829679898,
136.158022832244));
#196315=CARTESIAN_POINT('Ctrl Pts',(-6.33209922666964,2.06423968386644,
137.495934078373));
#196316=CARTESIAN_POINT('Ctrl Pts',(-6.61054685048256,6.74558223877327,
132.684616215558));
#196317=CARTESIAN_POINT('Ctrl Pts',(-6.88899447429547,5.22806425626005,
126.145435313781));
#196318=CARTESIAN_POINT('Ctrl Pts',(-7.16744209810832,-1.09378937261818,
123.887579165027));
#196319=CARTESIAN_POINT('Ctrl Pts',(-7.44588972192122,-6.41050400264194,
127.985907267597));
#196320=CARTESIAN_POINT('Ctrl Pts',(-7.72433734573414,-5.8362786247684,
134.674256309687));
#196321=CARTESIAN_POINT('Ctrl Pts',(-8.002784969547,0.101201691205851,137.806360265633));
#196322=CARTESIAN_POINT('Ctrl Pts',(-8.28123259335988,5.94568259693924,
134.503968611703));
#196323=CARTESIAN_POINT('Ctrl Pts',(-8.55968021717279,6.32637165882838,
127.80181794706));
#196324=CARTESIAN_POINT('Ctrl Pts',(-8.8381278409857,0.893434226691435,
123.858857314246));
#196325=CARTESIAN_POINT('Ctrl Pts',(-9.11657546479855,-5.3605256130866,
126.298474910485));
#196326=CARTESIAN_POINT('Ctrl Pts',(-9.39502308861147,-6.68842429067269,
132.878781346775));
#196327=CARTESIAN_POINT('Ctrl Pts',(-9.67347071242438,-1.86998779282204,
137.552796474009));
#196328=CARTESIAN_POINT('Ctrl Pts',(-9.95191833623725,4.66687613264966,
136.025328728591));
#196329=CARTESIAN_POINT('Ctrl Pts',(-10.2303659600501,6.91510888178999,
129.700046347612));
#196330=CARTESIAN_POINT('Ctrl Pts',(-10.508813583863,2.80869439041515,124.389574831969));
#196331=CARTESIAN_POINT('Ctrl Pts',(-10.787261207676,-3.87877303340228,
124.973978073582));
#196332=CARTESIAN_POINT('Ctrl Pts',(-11.0657088314888,-7.00183752812002,
130.916218043094));
#196333=CARTESIAN_POINT('Ctrl Pts',(-11.3441564553017,-3.69055539327479,
136.755666503084));
#196334=CARTESIAN_POINT('Ctrl Pts',(-11.6226040791146,3.01216685433575,
137.126155591738));
#196335=CARTESIAN_POINT('Ctrl Pts',(-11.9010517029275,6.94685491534338,
131.687223935982));
#196336=CARTESIAN_POINT('Ctrl Pts',(-12.1794993267404,4.49772268187999,
125.436984020872));
#196337=CARTESIAN_POINT('Ctrl Pts',(-12.4579469505533,-2.08459697026297,
124.119100987199));
#196338=CARTESIAN_POINT('Ctrl Pts',(-12.7363945743662,-6.75127384495765,
128.944644960744));
#196339=CARTESIAN_POINT('Ctrl Pts',(-13.0148421981791,-5.21385987419926,
135.479176770748));
#196340=CARTESIAN_POINT('Ctrl Pts',(-13.2932898219919,1.11483660973293,
137.717780913442));
#196341=CARTESIAN_POINT('Ctrl Pts',(-13.5717374458049,6.41905271211686,
133.603289543584));
#196342=CARTESIAN_POINT('Ctrl Pts',(-13.8501850696177,5.82447296022373,
126.916719225995));
#196343=CARTESIAN_POINT('Ctrl Pts',(-14.1286326934306,-0.122512900792341,
123.802701425419));
#196344=CARTESIAN_POINT('Ctrl Pts',(-14.4070803172435,-5.95691539106803,
127.122866372359));
#196345=CARTESIAN_POINT('Ctrl Pts',(-14.6855279410564,-6.31720364844761,
133.826144679651));
#196346=CARTESIAN_POINT('Ctrl Pts',(-14.9639755648693,-0.872290365458834,
137.752551056246));
#196347=CARTESIAN_POINT('Ctrl Pts',(-15.2424231886822,5.37421514963333,
135.293909857666));
#196348=CARTESIAN_POINT('Ctrl Pts',(-15.5208708124951,6.68207948721813,
128.709592234107));
#196349=CARTESIAN_POINT('Ctrl Pts',(-15.799318436308,1.84943921378025,124.050264419823));
#196350=CARTESIAN_POINT('Ctrl Pts',(-16.0777660601209,-4.68274534699314,
125.59762105532));
#196351=CARTESIAN_POINT('Ctrl Pts',(-16.3562136839338,-6.91171569870797,
131.929716985153));
#196352=CARTESIAN_POINT('Ctrl Pts',(-16.6346613077467,-2.78915697939336,
137.227665389888));
#196353=CARTESIAN_POINT('Ctrl Pts',(-16.9131089315595,3.89650074609022,
136.622910504741));
#196354=CARTESIAN_POINT('Ctrl Pts',(-17.1915565553724,7.00146464056082,
130.671192525245));
#196355=CARTESIAN_POINT('Ctrl Pts',(-17.4700041791854,3.67242457091876,
124.841849516969));
#196356=CARTESIAN_POINT('Ctrl Pts',(-17.7484518029982,-3.0313942714833,
124.491762925279));
#196357=CARTESIAN_POINT('Ctrl Pts',(-18.0268994268111,-6.94950987023543,
129.942645225261));
#196358=CARTESIAN_POINT('Ctrl Pts',(-18.305347050624,-4.48136540067248,
136.185401873632));
#196359=CARTESIAN_POINT('Ctrl Pts',(-18.5837946744369,2.10493494523792,
137.483244486159));
#196360=CARTESIAN_POINT('Ctrl Pts',(-18.8622422982498,6.75690290826339,
132.643519105064));
#196361=CARTESIAN_POINT('Ctrl Pts',(-19.1406899220627,5.19960719165284,
126.113696921846));
#196362=CARTESIAN_POINT('Ctrl Pts',(-19.4191375458756,-1.1358735191536,
123.894365523333));
#196363=CARTESIAN_POINT('Ctrl Pts',(-19.6975851696885,-6.42754195636435,
128.024982044393));
#196364=CARTESIAN_POINT('Ctrl Pts',(-19.9760327935014,-5.81261333855723,
134.709711694007));
#196365=CARTESIAN_POINT('Ctrl Pts',(-20.2544804173143,0.143822975436045,
137.805614491377));
#196366=CARTESIAN_POINT('Ctrl Pts',(-20.5329280411272,5.96809300114641,
134.467707008981));
#196367=CARTESIAN_POINT('Ctrl Pts',(-20.81137566494,6.30797711635522,127.763363157294));
#196368=CARTESIAN_POINT('Ctrl Pts',(-21.089823288753,0.851138423447451,
123.853547410611));
#196369=CARTESIAN_POINT('Ctrl Pts',(-21.3682709125658,-5.38785490018508,
126.331189435016));
#196370=CARTESIAN_POINT('Ctrl Pts',(-21.6467185363787,-6.67567278189203,
132.919457249623));
#196371=CARTESIAN_POINT('Ctrl Pts',(-21.9251661601916,-1.82887350178604,
137.564054587584));
#196372=CARTESIAN_POINT('Ctrl Pts',(-22.2036137840045,4.69857118102365,
135.996823396506));
#196373=CARTESIAN_POINT('Ctrl Pts',(-22.4820614078173,6.90825848643574,
129.657972577492));
#196374=CARTESIAN_POINT('Ctrl Pts',(-22.7605090316303,2.76959373000234,
124.372596363135));
#196375=CARTESIAN_POINT('Ctrl Pts',(-23.0389566554432,-3.91419236212754,
124.997697289448));
#196376=CARTESIAN_POINT('Ctrl Pts',(-23.3174042792561,-7.0010268923895,
130.958838143028));
#196377=CARTESIAN_POINT('Ctrl Pts',(-23.5958519030689,-3.65425972772349,
136.778021697354));
#196378=CARTESIAN_POINT('Ctrl Pts',(-23.8742995268818,3.05059360620828,
137.107702548922));
#196379=CARTESIAN_POINT('Ctrl Pts',(-24.1527471506948,6.95210044581739,
131.644920100946));
#196380=CARTESIAN_POINT('Ctrl Pts',(-24.4311947745076,4.4649666047081,125.409704551357));
#196381=CARTESIAN_POINT('Ctrl Pts',(-24.7096423983205,-2.12525342038311,
124.131914383013));
#196382=CARTESIAN_POINT('Ctrl Pts',(-24.9880900221334,-6.76246937654364,
128.985776337104));
#196383=CARTESIAN_POINT('Ctrl Pts',(-25.2665376459463,-5.18530634065569,
135.510828402156));
#196384=CARTESIAN_POINT('Ctrl Pts',(-25.5449852697592,1.15689990599717,
137.710866496904));
#196385=CARTESIAN_POINT('Ctrl Pts',(-25.8234328935721,6.43597165674122,
133.564163090109));
#196386=CARTESIAN_POINT('Ctrl Pts',(-26.101880517385,5.8006998696348,126.881336034893));
#196387=CARTESIAN_POINT('Ctrl Pts',(-26.3803281411979,-0.165131717723356,
123.803576920747));
#196388=CARTESIAN_POINT('Ctrl Pts',(-26.6587757650107,-5.9792153236265,
127.15919601668));
#196389=CARTESIAN_POINT('Ctrl Pts',(-26.9372233888237,-6.29869214802456,
133.864543304637));
#196390=CARTESIAN_POINT('Ctrl Pts',(-27.2156710126366,-0.829978596605981,
137.75773220141));
#196391=CARTESIAN_POINT('Ctrl Pts',(-27.4941186364494,5.40144473838504,
135.261112303716));
#196392=CARTESIAN_POINT('Ctrl Pts',(-27.7725662602623,6.66920423404522,
128.668955330874));
#196393=CARTESIAN_POINT('Ctrl Pts',(-28.0510138840753,1.80829084735756,
124.039131496154));
#196394=CARTESIAN_POINT('Ctrl Pts',(-28.3294615078881,-4.71435348813263,
125.626222724194));
#196395=CARTESIAN_POINT('Ctrl Pts',(-28.607909131701,-6.9047372770006,131.971769710144));
#196396=CARTESIAN_POINT('Ctrl Pts',(-28.8863567555139,-2.75000482347336,
137.244524771118));
#196397=CARTESIAN_POINT('Ctrl Pts',(-29.1648043793268,3.93184771762154,
136.599083594488));
#196398=CARTESIAN_POINT('Ctrl Pts',(-29.4432520031397,7.00052428766157,
130.628575090021));
#196399=CARTESIAN_POINT('Ctrl Pts',(-29.7216996269525,3.63606103196502,
124.819604897767));
#196400=CARTESIAN_POINT('Ctrl Pts',(-30.0001472507655,-3.06976468065099,
124.510332840438));
#196401=CARTESIAN_POINT('Ctrl Pts',(-30.2785948745783,-6.95462661809053,
129.984964829937));
#196402=CARTESIAN_POINT('Ctrl Pts',(-30.5570424983912,-4.44852644590303,
136.212581518559));
#196403=CARTESIAN_POINT('Ctrl Pts',(-30.8354901222041,2.14555220747066,
137.470307405446));
#196404=CARTESIAN_POINT('Ctrl Pts',(-31.113937746017,6.7679731982313,132.602353843876));
#196405=CARTESIAN_POINT('Ctrl Pts',(-31.3923853698299,5.17095745368924,
126.082132344179));
#196406=CARTESIAN_POINT('Ctrl Pts',(-31.6708329936428,-1.17791557547805,
123.901407934047));
#196407=CARTESIAN_POINT('Ctrl Pts',(-31.9492806174558,-6.44434173515584,
128.064159812084));
#196408=CARTESIAN_POINT('Ctrl Pts',(-32.2277282412685,-5.78873266382121,
134.745022364106));
#196409=CARTESIAN_POINT('Ctrl Pts',(-32.5061758650815,0.186438930252996,
137.804609283086));
#196410=CARTESIAN_POINT('Ctrl Pts',(-32.7846234888944,5.99028225547263,
134.431309659613));
#196411=CARTESIAN_POINT('Ctrl Pts',(-33.0630711127073,6.28934882947028,
127.725021052809));
#196412=CARTESIAN_POINT('Ctrl Pts',(-33.3415187365202,0.808811080956172,
123.848495071916));
#196413=CARTESIAN_POINT('Ctrl Pts',(-33.619966360333,-5.41498453833882,
126.364069714552));
#196414=CARTESIAN_POINT('Ctrl Pts',(-33.898413984146,-6.66267390360147,
132.960054776787));
#196415=CARTESIAN_POINT('Ctrl Pts',(-34.1768616079588,-1.78769144116968,
137.575062218212));
#196416=CARTESIAN_POINT('Ctrl Pts',(-34.4553092317717,4.73009212211488,
135.968125655805));
#196417=CARTESIAN_POINT('Ctrl Pts',(-34.7337568555846,6.90115210302259,
129.615941287202));
#196418=CARTESIAN_POINT('Ctrl Pts',(-35.0122044793975,2.73039044127535,
124.355856225691));
#196419=CARTESIAN_POINT('Ctrl Pts',(-35.2906521032104,-3.94946664901538,
125.02163167336));
#196420=CARTESIAN_POINT('Ctrl Pts',(-35.5690997270233,-6.99995683103299,
131.00145251874));
#196421=CARTESIAN_POINT('Ctrl Pts',(-35.8475473508362,-3.61782865223385,
136.800155535415));
#196422=CARTESIAN_POINT('Ctrl Pts',(-36.125994974649,3.08890731721304,137.089015933453));
#196423=CARTESIAN_POINT('Ctrl Pts',(-36.404442598462,6.95708836365274,131.60258511867));
#196424=CARTESIAN_POINT('Ctrl Pts',(-36.6828902222748,4.43204507655667,
125.382624982808));
#196425=CARTESIAN_POINT('Ctrl Pts',(-36.9613378460878,-2.16583111845593,
124.144975028777));
#196426=CARTESIAN_POINT('Ctrl Pts',(-37.2397854699006,-6.7734143223399,
129.026975101771));
#196427=CARTESIAN_POINT('Ctrl Pts',(-37.5182330937135,-5.15656066367905,
135.54230563367));
#196428=CARTESIAN_POINT('Ctrl Pts',(-37.7966807175264,1.19892033290996,
137.703696157251));
#196429=CARTESIAN_POINT('Ctrl Pts',(-38.0751283413393,6.45265211406898,
133.524934371139));
#196430=CARTESIAN_POINT('Ctrl Pts',(-38.3535759651522,5.77671183197903,
126.846098212911));
#196431=CARTESIAN_POINT('Ctrl Pts',(-38.6320235889651,-0.207744415637528,
123.80471183269));
#196432=CARTESIAN_POINT('Ctrl Pts',(-38.910471212778,-6.00129369416227,
127.195660733917));
#196433=CARTESIAN_POINT('Ctrl Pts',(-39.1889188365908,-6.27994724724761,
133.902828533427));
#196434=CARTESIAN_POINT('Ctrl Pts',(-39.4673664604039,-0.787636072591,137.762655686833));
#196435=CARTESIAN_POINT('Ctrl Pts',(-39.7458140842166,5.42847417461558,
135.228149603194));
#196436=CARTESIAN_POINT('Ctrl Pts',(-40.0242617080296,6.65608185105682,
128.628397555869));
#196437=CARTESIAN_POINT('Ctrl Pts',(-40.3027093318424,1.76707547405252,
124.028249260538));
#196438=CARTESIAN_POINT('Ctrl Pts',(-40.5811569556554,-4.7457869371699,
125.655016270872));
#196439=CARTESIAN_POINT('Ctrl Pts',(-40.8596045794682,-6.89750299771422,
132.013779176361));
#196440=CARTESIAN_POINT('Ctrl Pts',(-41.1380522032811,-2.7107507651133,
137.261145509698));
#196441=CARTESIAN_POINT('Ctrl Pts',(-41.416499827094,3.96704899308973,136.575041958643));
#196442=CARTESIAN_POINT('Ctrl Pts',(-41.694947450907,6.99932452776054,130.585964168594));
#196443=CARTESIAN_POINT('Ctrl Pts',(-41.9733950747197,3.59956275743227,
124.79758204589));
#196444=CARTESIAN_POINT('Ctrl Pts',(-42.2518426985328,-3.10802133855968,
124.529135983109));
#196445=CARTESIAN_POINT('Ctrl Pts',(-42.5302903223456,-6.95948565969872,
130.027314797628));
#196446=CARTESIAN_POINT('Ctrl Pts',(-42.8087379461585,-4.41552264935019,
136.23956075987));
#196447=CARTESIAN_POINT('Ctrl Pts',(-43.0871855699714,2.18608996547759,
137.457123315624));
#196448=CARTESIAN_POINT('Ctrl Pts',(-43.3656331937842,6.77879269846351,
132.561121957388));
#196449=CARTESIAN_POINT('Ctrl Pts',(-43.6440808175972,5.14211610399531,
126.050742750417));
#196450=CARTESIAN_POINT('Ctrl Pts',(-43.92252844141,-1.21991398370768,123.908706136214));
#196451=CARTESIAN_POINT('Ctrl Pts',(-44.200976065223,-6.46090271649442,
128.103439118922));
#196452=CARTESIAN_POINT('Ctrl Pts',(-44.4794236890358,-5.76463748546755,
134.780187011534));
#196453=CARTESIAN_POINT('Ctrl Pts',(-44.7578713128487,0.229047976506494,
137.803344678006));
#196454=CARTESIAN_POINT('Ctrl Pts',(-45.0363189366615,6.01224953768695,
134.394777912313));
#196455=CARTESIAN_POINT('Ctrl Pts',(-45.3147665604746,6.27048748845154,
127.686793054383));
#196456=CARTESIAN_POINT('Ctrl Pts',(-45.5932141842873,0.766453767672844,
123.843700485376));
#196457=CARTESIAN_POINT('Ctrl Pts',(-45.8716618081003,-5.44191352224889,
126.397114530699));
#196458=CARTESIAN_POINT('Ctrl Pts',(-46.1501094319132,-6.6494281374793,
133.000572423912));
#196459=CARTESIAN_POINT('Ctrl Pts',(-46.4285570557261,-1.74644313698983,
137.585818958004));
#196460=CARTESIAN_POINT('Ctrl Pts',(-46.7070046795389,4.76143778790304,
135.93923656989));
#196461=CARTESIAN_POINT('Ctrl Pts',(-46.9854523033519,6.89378999488032,
129.573954034227));
#196462=CARTESIAN_POINT('Ctrl Pts',(-47.2638999271647,2.69108597692664,
124.339355039948));
#196463=CARTESIAN_POINT('Ctrl Pts',(-47.5423475509777,-3.98459458696386,
125.045780338419));
#196464=CARTESIAN_POINT('Ctrl Pts',(-47.8207951747905,-6.998627383702,131.044059591139));
#196465=CARTESIAN_POINT('Ctrl Pts',(-48.0992427986034,-3.58126351677304,
136.822067197091));
#196466=CARTESIAN_POINT('Ctrl Pts',(-48.3776904224163,3.1271065676212,137.070096437769));
#196467=CARTESIAN_POINT('Ctrl Pts',(-48.6561380462292,6.9618184840203,131.560220557891));
#196468=CARTESIAN_POINT('Ctrl Pts',(-48.9345856700421,4.39895931734504,
125.355746318666));
#196469=CARTESIAN_POINT('Ctrl Pts',(-49.213033293855,-2.20632856086043,
124.158282440523));
#196470=CARTESIAN_POINT('Ctrl Pts',(-49.4914809176678,-6.78410827677761,
129.068239728113));
#196471=CARTESIAN_POINT('Ctrl Pts',(-49.7699285414808,-5.12762390845042,
135.573607298891));
#196472=CARTESIAN_POINT('Ctrl Pts',(-50.0483761652936,1.2408963333889,137.696270160183));
#196473=CARTESIAN_POINT('Ctrl Pts',(-50.3268237891066,6.46909346599971,
133.485604840309));
#196474=CARTESIAN_POINT('Ctrl Pts',(-50.6052714129194,5.7525097361419,126.811007065796));
#196475=CARTESIAN_POINT('Ctrl Pts',(-50.8837190367324,-0.250349415506305,
123.806106119193));
#196476=CARTESIAN_POINT('Ctrl Pts',(-51.1621666605453,-6.02314968455324,
127.232259172855));
#196477=CARTESIAN_POINT('Ctrl Pts',(-51.4406142843581,-6.26096964071598,
133.94099894735));
#196478=CARTESIAN_POINT('Ctrl Pts',(-51.719061908171,-0.745264362431691,
137.767321330073));
#196479=CARTESIAN_POINT('Ctrl Pts',(-51.997509531984,5.45530245673899,135.195022977544));
#196480=CARTESIAN_POINT('Ctrl Pts',(-52.2759571557968,6.64271282450778,
128.587920411975));
#196481=CARTESIAN_POINT('Ctrl Pts',(-52.5544047796097,1.72579462111621,
124.01761811622));
#196482=CARTESIAN_POINT('Ctrl Pts',(-52.8328524034226,-4.77704452932697,
125.684000628399));
#196483=CARTESIAN_POINT('Ctrl Pts',(-53.1113000272355,-6.89001312891767,
132.05574382713));
#196484=CARTESIAN_POINT('Ctrl Pts',(-53.3897476510484,-2.67139625888694,
137.277526989739));
#196485=CARTESIAN_POINT('Ctrl Pts',(-53.6681952748612,4.00210326809833,
136.550786488079));
#196486=CARTESIAN_POINT('Ctrl Pts',(-53.9466428986742,6.99786540531528,
130.543361339928));
#196487=CARTESIAN_POINT('Ctrl Pts',(-54.225090522487,3.56293109977782,124.775781777402));
#196488=CARTESIAN_POINT('Ctrl Pts',(-54.5035381462999,-3.14616282759469,
124.548171656537));
#196489=CARTESIAN_POINT('Ctrl Pts',(-54.7819857701128,-6.9640868150063,
130.069693559035));
#196490=CARTESIAN_POINT('Ctrl Pts',(-55.0604333939257,-4.382355233982,136.266338597842));
#196491=CARTESIAN_POINT('Ctrl Pts',(-55.3388810177386,2.22654671711671,
137.443692705233));
#196492=CARTESIAN_POINT('Ctrl Pts',(-55.6173286415515,6.78936100803939,
132.519824973462));
#196493=CARTESIAN_POINT('Ctrl Pts',(-55.8957762653644,5.11308421129812,
126.019529303714));
#196494=CARTESIAN_POINT('Ctrl Pts',(-56.1742238891773,-1.26186718757599,
123.916259859391));
#196495=CARTESIAN_POINT('Ctrl Pts',(-56.4526715129901,-6.47722428670686,
128.142818509401));
#196496=CARTESIAN_POINT('Ctrl Pts',(-56.7311191368031,-5.74032869635189,
134.815204333253));
#196497=CARTESIAN_POINT('Ctrl Pts',(-57.0095667606159,0.271648535303317,
137.801820722997));
#196498=CARTESIAN_POINT('Ctrl Pts',(-57.2880143844289,6.03399403378365,
134.358113120779));
#196499=CARTESIAN_POINT('Ctrl Pts',(-57.5664620082417,6.25139379221294,
127.64868057857));
#196500=CARTESIAN_POINT('Ctrl Pts',(-57.8449096320546,0.724068053163303,
123.839163828657));
#196501=CARTESIAN_POINT('Ctrl Pts',(-58.1233572558676,-5.46864085405239,
126.430322658971));
#196502=CARTESIAN_POINT('Ctrl Pts',(-58.4018048796803,-6.63593597435208,
133.0410086896));
#196503=CARTESIAN_POINT('Ctrl Pts',(-58.6802525034934,-1.705130117717,137.596324408362));
#196504=CARTESIAN_POINT('Ctrl Pts',(-58.9587001273061,4.79260701686295,
135.910157209259));
#196505=CARTESIAN_POINT('Ctrl Pts',(-59.2371477511191,6.88617243481463,
129.532012374421));
#196506=CARTESIAN_POINT('Ctrl Pts',(-59.515595374932,2.65168179339722,124.323093417365));
#196507=CARTESIAN_POINT('Ctrl Pts',(-59.7940429987449,-4.01957487429483,
125.070142389788));
#196508=CARTESIAN_POINT('Ctrl Pts',(-60.0724906225578,-6.99703859965941,
131.086657781405));
#196509=CARTESIAN_POINT('Ctrl Pts',(-60.3509382463707,-3.5445656762756,
136.843755870437));
#196510=CARTESIAN_POINT('Ctrl Pts',(-60.6293858701835,3.16518994194552,
137.050944762941));
#196511=CARTESIAN_POINT('Ctrl Pts',(-60.9078334939965,6.96629063164357,
131.517827988445));
#196512=CARTESIAN_POINT('Ctrl Pts',(-61.1862811178092,4.36571055307847,
125.32906955493));
#196513=CARTESIAN_POINT('Ctrl Pts',(-61.4647287416223,-2.24674424694855,
124.171836125139));
#196514=CARTESIAN_POINT('Ctrl Pts',(-61.743176365435,-6.79455084358828,
129.109568687053));
#196515=CARTESIAN_POINT('Ctrl Pts',(-62.0216239892481,-5.09849714723216,
135.60473223792));
#196516=CARTESIAN_POINT('Ctrl Pts',(-62.3000716130609,1.2828263519976,137.688588780872));
#196517=CARTESIAN_POINT('Ctrl Pts',(-62.5785192368738,6.48529510329292,
133.446175954988));
#196518=CARTESIAN_POINT('Ctrl Pts',(-62.8569668606868,5.72809447894126,
126.776063893867));
#196519=CARTESIAN_POINT('Ctrl Pts',(-63.1354144844995,-0.292945138585431,
123.80775972859));
#196520=CARTESIAN_POINT('Ctrl Pts',(-63.4138621083125,-6.04478248491762,
127.268989977326));
#196521=CARTESIAN_POINT('Ctrl Pts',(-63.6923097321254,-6.24176003165182,
133.979053131985));
#196522=CARTESIAN_POINT('Ctrl Pts',(-63.9707573559382,-0.702865036227365,
137.771728958244));
#196523=CARTESIAN_POINT('Ctrl Pts',(-64.2492049797512,5.48192859062395,
135.161733654286));
#196524=CARTESIAN_POINT('Ctrl Pts',(-64.527652603564,6.62909764979204,128.547525399088));
#196525=CARTESIAN_POINT('Ctrl Pts',(-64.806100227377,1.68444981822529,124.007238457143));
#196526=CARTESIAN_POINT('Ctrl Pts',(-65.0845478511898,-4.80812510634223,
125.713174722747));
#196527=CARTESIAN_POINT('Ctrl Pts',(-65.3629954750027,-6.88226794815085,
132.097662107432));
#196528=CARTESIAN_POINT('Ctrl Pts',(-65.6414430988157,-2.63194276308962,
137.29366860422));
#196529=CARTESIAN_POINT('Ctrl Pts',(-65.9198907226284,4.03700924369883,
136.526318081592));
#196530=CARTESIAN_POINT('Ctrl Pts',(-66.1983383464414,6.99614697439381,
130.500768182686));
#196531=CARTESIAN_POINT('Ctrl Pts',(-66.4767859702543,3.5261674164012,124.75420490012));
#196532=CARTESIAN_POINT('Ctrl Pts',(-66.7552335940671,-3.18418773440913,
124.567439155348));
#196533=CARTESIAN_POINT('Ctrl Pts',(-67.0336812178801,-6.96842991351606,
130.112099543802));
#196534=CARTESIAN_POINT('Ctrl Pts',(-67.3121288416929,-4.34902542882876,
136.292914040211));
#196535=CARTESIAN_POINT('Ctrl Pts',(-67.5905764655059,2.26692096324861,
137.43001607195));
#196536=CARTESIAN_POINT('Ctrl Pts',(-67.8690240893187,6.79967773534632,
132.478464422373));
#196537=CARTESIAN_POINT('Ctrl Pts',(-68.1474717131316,5.08386285138514,
125.988493160695));
#196538=CARTESIAN_POINT('Ctrl Pts',(-68.4259193369445,-1.30377363249137,
123.924068823677));
#196539=CARTESIAN_POINT('Ctrl Pts',(-68.7043669607574,-6.49330584099122,
128.182296524302));
#196540=CARTESIAN_POINT('Ctrl Pts',(-68.9828145845703,-5.71580719724563,
134.850073031684));
#196541=CARTESIAN_POINT('Ctrl Pts',(-69.2612622083832,0.314239028063776,
137.800037474531));
#196542=CARTESIAN_POINT('Ctrl Pts',(-69.5397098321961,6.05551493801243,
134.32131664364));
#196543=CARTESIAN_POINT('Ctrl Pts',(-69.818157456009,6.23206844827842,127.610685037641));
#196544=CARTESIAN_POINT('Ctrl Pts',(-70.0966050798218,0.681655508046095,
123.834885269867));
#196545=CARTESIAN_POINT('Ctrl Pts',(-70.3750527036349,-5.49516554335789,
126.463692868828));
#196546=CARTESIAN_POINT('Ctrl Pts',(-70.6535003274475,-6.62219791417695,
133.081362075471));
#196547=CARTESIAN_POINT('Ctrl Pts',(-70.9319479512606,-1.66375391422059,
137.606578180005));
#196548=CARTESIAN_POINT('Ctrl Pts',(-71.2103955750734,4.82359865400735,
135.880888651457));
#196549=CARTESIAN_POINT('Ctrl Pts',(-71.4888431988863,6.87829970509706,
129.490117861946));
#196550=CARTESIAN_POINT('Ctrl Pts',(-71.7672908226993,2.6121793508235,124.307071960521));
#196551=CARTESIAN_POINT('Ctrl Pts',(-72.045738446512,-4.05440621480077,
125.094716924722));
#196552=CARTESIAN_POINT('Ctrl Pts',(-72.3241860703251,-6.99519053777849,
131.129245511046));
#196553=CARTESIAN_POINT('Ctrl Pts',(-72.6026336941378,-3.5077364905931,
136.865220751771));
#196554=CARTESIAN_POINT('Ctrl Pts',(-72.8810813179508,3.20315602899298,
137.031561618638));
#196555=CARTESIAN_POINT('Ctrl Pts',(-73.1595289417638,6.97050464080582,
131.475408981201));
#196556=CARTESIAN_POINT('Ctrl Pts',(-73.4379765655765,4.33230001580124,
125.302595680118));
#196557=CARTESIAN_POINT('Ctrl Pts',(-73.7164241893894,-2.28707667910305,
124.18563558039));
#196558=CARTESIAN_POINT('Ctrl Pts',(-73.9948718132024,-6.80474163581863,
129.150960447132));
#196559=CARTESIAN_POINT('Ctrl Pts',(-74.2733194370152,-5.0691814593271,
135.635679297414));
#196560=CARTESIAN_POINT('Ctrl Pts',(-74.5517670608282,1.32470883500465,
137.680652303954));
#196561=CARTESIAN_POINT('Ctrl Pts',(-74.830214684641,6.5012564255912,133.406649176227));
#196562=CARTESIAN_POINT('Ctrl Pts',(-75.108662308454,5.70346696509291,126.741269991954));
#196563=CARTESIAN_POINT('Ctrl Pts',(-75.3871099322667,-0.335530006474783,
123.809672599606));
#196564=CARTESIAN_POINT('Ctrl Pts',(-75.6655575560798,-6.06619129364391,
127.305851786256));
#196565=CARTESIAN_POINT('Ctrl Pts',(-75.9440051798925,-6.22231913187452,
134.016989677222));
#196566=CARTESIAN_POINT('Ctrl Pts',(-76.2224528037055,-0.66043966510086,
137.775878408018));
#196567=CARTESIAN_POINT('Ctrl Pts',(-76.5009004275184,5.50835158962877,
135.128282866967));
#196568=CARTESIAN_POINT('Ctrl Pts',(-76.7793480513312,6.61523683142527,
128.507214014061));
#196569=CARTESIAN_POINT('Ctrl Pts',(-77.0577956751442,1.64304259742666,
123.997110667925));
#196570=CARTESIAN_POINT('Ctrl Pts',(-77.336243298957,-4.83902751651344,
125.742537472861));
#196571=CARTESIAN_POINT('Ctrl Pts',(-77.6146909227699,-6.87426774241415,
132.139532463972));
#196572=CARTESIAN_POINT('Ctrl Pts',(-77.8931385465828,-2.59239173968542,
137.309569755007));
#196573=CARTESIAN_POINT('Ctrl Pts',(-78.1715861703958,4.07176562643718,
136.501637645866));
#196574=CARTESIAN_POINT('Ctrl Pts',(-78.4500337942086,6.99416929867323,
130.458186275174));
#196575=CARTESIAN_POINT('Ctrl Pts',(-78.7284814180215,3.48927306959449,
124.732852213582));
#196576=CARTESIAN_POINT('Ctrl Pts',(-79.0069290418344,-3.22209464997582,
124.586937765577));
#196577=CARTESIAN_POINT('Ctrl Pts',(-79.2853766656473,-6.97251479429268,
130.154531180556));
#196578=CARTESIAN_POINT('Ctrl Pts',(-79.5638242894601,-4.3155344689392,
136.319286102215));
#196579=CARTESIAN_POINT('Ctrl Pts',(-79.8422719132732,2.30721120779087,
137.416093922569));
#196580=CARTESIAN_POINT('Ctrl Pts',(-80.1207195370859,6.80974249809405,
132.437041836753));
#196581=CARTESIAN_POINT('Ctrl Pts',(-80.3991671608989,5.0544531070646,125.957635471416));
#196582=CARTESIAN_POINT('Ctrl Pts',(-80.6776147847117,-1.34563176559565,
123.932132739704));
#196583=CARTESIAN_POINT('Ctrl Pts',(-80.9560624085247,-6.50914678343976,
128.221871700751));
#196584=CARTESIAN_POINT('Ctrl Pts',(-81.2345100323374,-5.69107389680138,
134.884791814753));
#196585=CARTESIAN_POINT('Ctrl Pts',(-81.5129576561506,0.356817876581242,
137.797994998686));
#196586=CARTESIAN_POINT('Ctrl Pts',(-81.7914052799631,6.07681145290804,
134.284389844403));
#196587=CARTESIAN_POINT('Ctrl Pts',(-82.0698529037763,6.21251217275584,
127.572807839535));
#196588=CARTESIAN_POINT('Ctrl Pts',(-82.348300527589,0.639217703933302,
123.830864967548));
#196589=CARTESIAN_POINT('Ctrl Pts',(-82.626748151402,-5.52148660728364,
126.497223923725));
#196590=CARTESIAN_POINT('Ctrl Pts',(-82.9051957752149,-6.60821446602265,
133.121631086217));
#196591=CARTESIAN_POINT('Ctrl Pts',(-83.1836433990278,-1.62231605971109,
137.616579892973));
#196592=CARTESIAN_POINT('Ctrl Pts',(-83.4620910228406,4.85441155092967,
135.851431981043));
#196593=CARTESIAN_POINT('Ctrl Pts',(-83.7405386466535,6.87017209745416,
129.448272049221));
#196594=CARTESIAN_POINT('Ctrl Pts',(-84.0189862704665,2.57258011298421,
124.291291263097));
#196595=CARTESIAN_POINT('Ctrl Pts',(-84.2974338942792,-4.08908731779306,
125.119503032603));
#196596=CARTESIAN_POINT('Ctrl Pts',(-84.5758815180923,-6.99308326653956,
131.171821201958));
#196597=CARTESIAN_POINT('Ctrl Pts',(-84.8543291419051,-3.47077732444568,
136.886461045702));
#196598=CARTESIAN_POINT('Ctrl Pts',(-85.132776765718,3.2410034219148,137.011947723114));
#196599=CARTESIAN_POINT('Ctrl Pts',(-85.4112243895309,6.97446035535538,
131.432965108015));
#196600=CARTESIAN_POINT('Ctrl Pts',(-85.6896720133437,4.29872894355427,
125.27632567523));
#196601=CARTESIAN_POINT('Ctrl Pts',(-85.9681196371569,-2.327324362789,124.19968029493));
#196602=CARTESIAN_POINT('Ctrl Pts',(-86.2465672609694,-6.81468027584547,
129.192413474561));
#196603=CARTESIAN_POINT('Ctrl Pts',(-86.5250148847825,-5.03967793103904,
135.666447330617));
#196604=CARTESIAN_POINT('Ctrl Pts',(-86.8034625085954,1.36654223043768,
137.672461023519));
#196605=CARTESIAN_POINT('Ctrl Pts',(-87.0819101324082,6.51697684144191,
133.367025968708));
#196606=CARTESIAN_POINT('Ctrl Pts',(-87.3603577562212,5.67862810717874,
126.706626649358));
#196607=CARTESIAN_POINT('Ctrl Pts',(-87.638805380034,-0.378102441176264,
123.811844661359));
#196608=CARTESIAN_POINT('Ctrl Pts',(-87.917253003847,-6.08737531742114,
127.342843233717));
#196609=CARTESIAN_POINT('Ctrl Pts',(-88.1957006276599,-6.20264766177327,
134.054807177307));
#196610=CARTESIAN_POINT('Ctrl Pts',(-88.4741482514726,-0.617989821139493,
137.779769525637));
#196611=CARTESIAN_POINT('Ctrl Pts',(-88.7525958752857,5.53457047463998,
135.094671855119));
#196612=CARTESIAN_POINT('Ctrl Pts',(-89.0310434990984,6.6011308830247,128.466987750645));
#196613=CARTESIAN_POINT('Ctrl Pts',(-89.3094911229114,1.60157449308101,
123.987235123859));
#196614=CARTESIAN_POINT('Ctrl Pts',(-89.5879387467241,-4.86975061474005,
125.772087790693));
#196615=CARTESIAN_POINT('Ctrl Pts',(-89.8663863705374,-6.8660128081587,
132.181353345229));
#196616=CARTESIAN_POINT('Ctrl Pts',(-90.1448339943499,-2.55274465425183,
137.325229852876));
#196617=CARTESIAN_POINT('Ctrl Pts',(-90.4232816181632,4.10637112840284,
136.476746095445));
#196618=CARTESIAN_POINT('Ctrl Pts',(-90.7017292419757,6.99193245143733,
130.415617195278));
#196619=CARTESIAN_POINT('Ctrl Pts',(-90.9801768657889,3.45224942649073,
124.711724509022));
#196620=CARTESIAN_POINT('Ctrl Pts',(-91.2586244896016,-3.2598821696406,
124.606666764696));
#196621=CARTESIAN_POINT('Ctrl Pts',(-91.5370721134145,-6.97634130596949,
130.196986896981));
#196622=CARTESIAN_POINT('Ctrl Pts',(-91.8155197372274,-4.28188359533257,
136.345453806627));
#196623=CARTESIAN_POINT('Ctrl Pts',(-92.0939673610402,2.34741595777304,
137.401926772977));
#196624=CARTESIAN_POINT('Ctrl Pts',(-92.3724149848533,6.81955492332935,
132.395558751529));
#196625=CARTESIAN_POINT('Ctrl Pts',(-92.650862608666,5.02485606812542,125.926957379319));
#196626=CARTESIAN_POINT('Ctrl Pts',(-92.929310232479,-1.38744003581995,
123.940451308663));
#196627=CARTESIAN_POINT('Ctrl Pts',(-93.2077578562919,-6.52474652706058,
128.261542572277));
#196628=CARTESIAN_POINT('Ctrl Pts',(-93.4862054801047,-5.66612971152105,
134.919359395943));
#196629=CARTESIAN_POINT('Ctrl Pts',(-93.7646531039176,0.39938350308132,
137.795693371147));
#196630=CARTESIAN_POINT('Ctrl Pts',(-94.0431007277306,6.09788278932073,
134.247334091402));
#196631=CARTESIAN_POINT('Ctrl Pts',(-94.3215483515434,6.19272569030992,
127.535050387806));
#196632=CARTESIAN_POINT('Ctrl Pts',(-94.5999959753563,0.596756213373149,
123.827103070676));
#196633=CARTESIAN_POINT('Ctrl Pts',(-94.8784435991693,-5.54760307049237,
126.530914581157));
#196634=CARTESIAN_POINT('Ctrl Pts',(-95.1568912229821,-6.59398614805128,
133.161814229653));
#196635=CARTESIAN_POINT('Ctrl Pts',(-95.4353388467949,-1.58081808968337,
137.626329176652));
#196636=CARTESIAN_POINT('Ctrl Pts',(-95.7137864706081,4.88504456584684,
135.821788289543));
#196637=CARTESIAN_POINT('Ctrl Pts',(-95.9922340944205,6.86178991305786,
129.406476486855));
#196638=CARTESIAN_POINT('Ctrl Pts',(-96.2706817182339,2.53288554724217,
124.275751909854));
#196639=CARTESIAN_POINT('Ctrl Pts',(-96.5491293420464,-4.12361689815126,
125.144499794972));
#196640=CARTESIAN_POINT('Ctrl Pts',(-96.8275769658595,-6.99071686402826,
131.214383276482));
#196641=CARTESIAN_POINT('Ctrl Pts',(-97.1060245896722,-3.4336895473684,
136.907475965166));
#196642=CARTESIAN_POINT('Ctrl Pts',(-97.3844722134854,3.27873071826322,
136.992103803166));
#196643=CARTESIAN_POINT('Ctrl Pts',(-97.6629198372979,6.9781576287114,131.390497941658));
#196644=CARTESIAN_POINT('Ctrl Pts',(-97.9413674611112,4.26499858032525,
125.250260513709));
#196645=CARTESIAN_POINT('Ctrl Pts',(-98.2198150849237,-2.36748580661544,
124.21396974833));
#196646=CARTESIAN_POINT('Ctrl Pts',(-98.498262708737,-6.82436639538843,
129.233926233285));
#196647=CARTESIAN_POINT('Ctrl Pts',(-98.7767103325495,-5.00998765563179,
135.69703519741));
#196648=CARTESIAN_POINT('Ctrl Pts',(-99.0551579563628,1.40832498814648,
137.664015243098));
#196649=CARTESIAN_POINT('Ctrl Pts',(-99.3336055801754,6.53245576831905,
133.327307800681));
#196650=CARTESIAN_POINT('Ctrl Pts',(-99.6120532039884,5.65357882561176,
126.672135149802));
#196651=CARTESIAN_POINT('Ctrl Pts',(-99.8905008278013,-0.420660865152761,
123.814275833361));
#196652=CARTESIAN_POINT('Ctrl Pts',(-100.168948451614,-6.10833377126732,
127.379962948978));
#196653=CARTESIAN_POINT('Ctrl Pts',(-100.447396075427,-6.18274635028192,
134.092504230901));
#196654=CARTESIAN_POINT('Ctrl Pts',(-100.72584369924,-0.575517077338011,
137.783402166914));
#196655=CARTESIAN_POINT('Ctrl Pts',(-101.004291323053,5.56058427410689,
135.060901864211));
#196656=CARTESIAN_POINT('Ctrl Pts',(-101.282738946866,6.58678032729173,
128.426848099441));
#196657=CARTESIAN_POINT('Ctrl Pts',(-101.561186570679,1.56004704180311,
123.977612190885));
#196658=CARTESIAN_POINT('Ctrl Pts',(-101.839634194492,-4.90029326256724,
125.801824581246));
#196659=CARTESIAN_POINT('Ctrl Pts',(-102.118081818304,-6.85750345127332,
132.223123201514));
#196660=CARTESIAN_POINT('Ctrl Pts',(-102.396529442117,-2.51300297592632,
137.340648317539));
#196661=CARTESIAN_POINT('Ctrl Pts',(-102.67497706593,4.14082446727623,136.451644352694));
#196662=CARTESIAN_POINT('Ctrl Pts',(-102.953424689743,6.98943651557314,
130.373062520413));
#196663=CARTESIAN_POINT('Ctrl Pts',(-103.231872313556,3.41509785901489,
124.690822569333));
#196664=CARTESIAN_POINT('Ctrl Pts',(-103.510319937369,-3.29754889317273,
124.626625421641));
#196665=CARTESIAN_POINT('Ctrl Pts',(-103.788767561182,-6.97990930675369,
130.239465119861));
#196666=CARTESIAN_POINT('Ctrl Pts',(-104.067215184995,-4.24807405495459,
136.371416183792));
#196667=CARTESIAN_POINT('Ctrl Pts',(-104.345662808808,2.38753372339306,
137.387515148146));
#196668=CARTESIAN_POINT('Ctrl Pts',(-104.62411043262,6.82911464744894,132.354016703874));
#196669=CARTESIAN_POINT('Ctrl Pts',(-104.902558056433,4.99507283129728,
125.896460021193));
#196670=CARTESIAN_POINT('Ctrl Pts',(-105.181005680246,-1.42919689394351,
123.949024222305));
#196671=CARTESIAN_POINT('Ctrl Pts',(-105.459453304059,-6.54010449379936,
128.301307668861));
#196672=CARTESIAN_POINT('Ctrl Pts',(-105.737900927872,-5.64097556572054,
134.953774494342));
#196673=CARTESIAN_POINT('Ctrl Pts',(-106.016348551685,0.441934330278796,
137.793132677202));
#196674=CARTESIAN_POINT('Ctrl Pts',(-106.294796175498,6.11872816644418,
134.210150757753));
#196675=CARTESIAN_POINT('Ctrl Pts',(-106.573243799311,6.17270973413615,
127.49741408157));
#196676=CARTESIAN_POINT('Ctrl Pts',(-106.851691423124,0.554272609792058,
123.823599718647));
#196677=CARTESIAN_POINT('Ctrl Pts',(-107.130139046936,-5.57351396522919,
126.564763592701));
#196678=CARTESIAN_POINT('Ctrl Pts',(-107.40858667075,-6.57951348749827,
133.201910016778));
#196679=CARTESIAN_POINT('Ctrl Pts',(-107.687034294562,-1.53926154185996,
137.635825669776));
#196680=CARTESIAN_POINT('Ctrl Pts',(-107.965481918375,4.91549656364115,
135.791958675416));
#196681=CARTESIAN_POINT('Ctrl Pts',(-108.243929542188,6.85315346251289,
129.364732723601));
#196682=CARTESIAN_POINT('Ctrl Pts',(-108.522377166001,2.49309712449469,
124.260454476607));
#196683=CARTESIAN_POINT('Ctrl Pts',(-108.800824789814,-4.15799367636883,
125.169706285567));
#196684=CARTESIAN_POINT('Ctrl Pts',(-109.079272413627,-6.98809141793296,
131.256930157466));
#196685=CARTESIAN_POINT('Ctrl Pts',(-109.35772003744,-3.39647453366164,
136.928264731447));
#196686=CARTESIAN_POINT('Ctrl Pts',(-109.636167661252,3.31633652003941,
136.97203059412));
#196687=CARTESIAN_POINT('Ctrl Pts',(-109.914615285065,6.98159632387027,
131.348009055767));
#196688=CARTESIAN_POINT('Ctrl Pts',(-110.193062908878,4.23111017600536,
125.22440116141));
#196689=CARTESIAN_POINT('Ctrl Pts',(-110.471510532691,-2.40755952238467,
124.228503411086));
#196690=CARTESIAN_POINT('Ctrl Pts',(-110.749958156504,-6.83379963552497,
129.275497185033));
#196691=CARTESIAN_POINT('Ctrl Pts',(-111.028405780317,-4.98011173328953,
135.727441764346));
#196692=CARTESIAN_POINT('Ctrl Pts',(-111.30685340413,1.45005555985492,137.655315275653));
#196693=CARTESIAN_POINT('Ctrl Pts',(-111.585301027943,6.54769263264538,
133.287496143919));
#196694=CARTESIAN_POINT('Ctrl Pts',(-111.863748651756,5.62832004860235,
126.63779677138));
#196695=CARTESIAN_POINT('Ctrl Pts',(-112.142196275568,-0.463203701385527,
123.816966025527));
#196696=CARTESIAN_POINT('Ctrl Pts',(-112.420643899382,-6.12906587855929,
127.417209556553));
#196697=CARTESIAN_POINT('Ctrl Pts',(-112.699091523194,-6.16261593485082,
134.130079441122));
#196698=CARTESIAN_POINT('Ctrl Pts',(-112.977539147007,-0.533023007539609,
137.786776197239));
#196699=CARTESIAN_POINT('Ctrl Pts',(-113.25598677082,5.58639202407863,135.026974145601));
#196700=CARTESIAN_POINT('Ctrl Pts',(-113.534434394633,6.57218569599142,
128.386796547837));
#196701=CARTESIAN_POINT('Ctrl Pts',(-113.812882018446,1.5184617824084,123.968242225583));
#196702=CARTESIAN_POINT('Ctrl Pts',(-114.091329642259,-4.93065432822552,
125.831746742611));
#196703=CARTESIAN_POINT('Ctrl Pts',(-114.369777266072,-6.84873998707567,
132.26484048503));
#196704=CARTESIAN_POINT('Ctrl Pts',(-114.648224889884,-2.4731681773514,
137.355824577657));
#196705=CARTESIAN_POINT('Ctrl Pts',(-114.926672513697,4.17512436637621,
136.426333347767));
#196706=CARTESIAN_POINT('Ctrl Pts',(-115.20512013751,6.98668158356849,130.330523827459));
#196707=CARTESIAN_POINT('Ctrl Pts',(-115.483567761323,3.377819743832,124.670147169045));
#196708=CARTESIAN_POINT('Ctrl Pts',(-115.762015385136,-3.33509342481799,
124.646812996834));
#196709=CARTESIAN_POINT('Ctrl Pts',(-116.040463008949,-6.98321866443162,
130.281964275151));
#196710=CARTESIAN_POINT('Ctrl Pts',(-116.318910632762,-4.21410710063033,
136.397172271667));
#196711=CARTESIAN_POINT('Ctrl Pts',(-116.597358256575,2.42756301807353,
137.372859582102));
#196712=CARTESIAN_POINT('Ctrl Pts',(-116.875805880388,6.83842131621399,
132.312417233142));
#196713=CARTESIAN_POINT('Ctrl Pts',(-117.154253504201,4.96510450020791,
125.866144527128));
#196714=CARTESIAN_POINT('Ctrl Pts',(-117.432701128013,-1.47090079265054,
123.957851162959));
#196715=CARTESIAN_POINT('Ctrl Pts',(-117.711148751826,-6.55522011456102,
128.341165516992));
#196716=CARTESIAN_POINT('Ctrl Pts',(-117.989596375639,-5.61561239149597,
134.988035834682));
#196717=CARTESIAN_POINT('Ctrl Pts',(-118.268043999452,0.484468781437156,
137.790313011739));
#196718=CARTESIAN_POINT('Ctrl Pts',(-118.546491623265,6.13934681184524,
134.172841221298));
#196719=CARTESIAN_POINT('Ctrl Pts',(-118.824939247078,6.15246504593319,
127.459900315453));
#196720=CARTESIAN_POINT('Ctrl Pts',(-119.103386870891,0.511768467435545,
123.820355041281));
#196721=CARTESIAN_POINT('Ctrl Pts',(-119.381834494704,-5.59921833135585,
126.598769704074));
#196722=CARTESIAN_POINT('Ctrl Pts',(-119.660282118516,-6.56479702065358,
133.241916961827));
#196723=CARTESIAN_POINT('Ctrl Pts',(-119.93872974233,-1.49764795613459,
137.645069020452));
#196724=CARTESIAN_POINT('Ctrl Pts',(-120.217177366142,4.94576641590264,
135.761944244007));
#196725=CARTESIAN_POINT('Ctrl Pts',(-120.495624989955,6.84426306584611,
129.323042306287));
#196726=CARTESIAN_POINT('Ctrl Pts',(-120.774072613768,2.45321631911644,
124.245399530209));
#196727=CARTESIAN_POINT('Ctrl Pts',(-121.052520237581,-4.19221637860163,
125.195121570349));
#196728=CARTESIAN_POINT('Ctrl Pts',(-121.330967861394,-6.98520702554029,
131.299460268319));
#196729=CARTESIAN_POINT('Ctrl Pts',(-121.609415485207,-3.35913366234199,
136.948826574209));
#196730=CARTESIAN_POINT('Ctrl Pts',(-121.88786310902,3.3538194337463,136.951728839794));
#196731=CARTESIAN_POINT('Ctrl Pts',(-122.166310732833,6.98477631340985,
131.305500024783));
#196732=CARTESIAN_POINT('Ctrl Pts',(-122.444758356646,4.19706498634193,
125.198748576561));
#196733=CARTESIAN_POINT('Ctrl Pts',(-122.723205980458,-2.44754402515043,
124.24328074465));
#196734=CARTESIAN_POINT('Ctrl Pts',(-123.001653604271,-6.84297964670285,
129.317124789377));
#196735=CARTESIAN_POINT('Ctrl Pts',(-123.280101228084,-4.95005127107555,
135.7576659047));
#196736=CARTESIAN_POINT('Ctrl Pts',(-123.558548851897,1.49173239922134,
137.646361443563));
#196737=CARTESIAN_POINT('Ctrl Pts',(-123.83699647571,6.5626868698133,133.247592473656));
#196738=CARTESIAN_POINT('Ctrl Pts',(-124.115444099523,5.60285271212367,
126.603612786514));
#196739=CARTESIAN_POINT('Ctrl Pts',(-124.393891723336,-0.505729373435472,
123.819915138168));
#196740=CARTESIAN_POINT('Ctrl Pts',(-124.672339347149,-6.14957087106115,
127.454581676257));
#196741=CARTESIAN_POINT('Ctrl Pts',(-124.950786970961,-6.14225716141998,
134.167531415611));
#196742=CARTESIAN_POINT('Ctrl Pts',(-125.229234594775,-0.490509186377616,
137.789891491587));
#196743=CARTESIAN_POINT('Ctrl Pts',(-125.507682218587,5.6119927682395,134.992889956494));
#196744=CARTESIAN_POINT('Ctrl Pts',(-125.786129842401,6.55734752993325,
128.346834579959));
#196745=CARTESIAN_POINT('Ctrl Pts',(-126.064577466213,1.47682025585389,
123.959125575163));
#196746=CARTESIAN_POINT('Ctrl Pts',(-126.343025090026,-4.9608326866744,
125.861853166013));
#196747=CARTESIAN_POINT('Ctrl Pts',(-126.621472713839,-6.8397227402992,
132.306503649927));
#196748=CARTESIAN_POINT('Ctrl Pts',(-126.899920337652,-2.43324173462049,
137.370758070868));
#196749=CARTESIAN_POINT('Ctrl Pts',(-127.178367961465,4.20926955470684,
136.400814018573));
#196750=CARTESIAN_POINT('Ctrl Pts',(-127.456815585278,6.98366775750873,
130.288002692701));
#196751=CARTESIAN_POINT('Ctrl Pts',(-127.73526320909,3.34041646229627,124.649699074291));
#196752=CARTESIAN_POINT('Ctrl Pts',(-128.013710832904,-3.37251437334987,
124.66722874222));
#196753=CARTESIAN_POINT('Ctrl Pts',(-128.292158456716,-6.9862692563739,
130.324482788031));
#196754=CARTESIAN_POINT('Ctrl Pts',(-128.570606080529,-4.17998399101771,
136.422721115849));
#196755=CARTESIAN_POINT('Ctrl Pts',(-128.849053704342,2.46750235851359,
137.357960617914));
#196756=CARTESIAN_POINT('Ctrl Pts',(-129.127501328155,6.84747458476236,
132.270761880817));
#196757=CARTESIAN_POINT('Ctrl Pts',(-129.405948951968,4.93495218534535,
125.836012020477));
#196758=CARTESIAN_POINT('Ctrl Pts',(-129.684396575781,-1.51255018658779,
123.966931803538));
#196759=CARTESIAN_POINT('Ctrl Pts',(-129.962844199593,-6.57009282923063,
128.381114639724));
#196760=CARTESIAN_POINT('Ctrl Pts',(-130.241291823406,-5.59004112868908,
135.022142147398));
#196761=CARTESIAN_POINT('Ctrl Pts',(-130.519739447219,0.52698528042665,
137.78723447924));
#196762=CARTESIAN_POINT('Ctrl Pts',(-130.798187071032,6.15973796149245,
134.135406864555));
#196763=CARTESIAN_POINT('Ctrl Pts',(-131.076634694845,6.13199237587537,
127.422510479544));
#196764=CARTESIAN_POINT('Ctrl Pts',(-131.355082318658,0.4692453613103,123.81736915881));
#196765=CARTESIAN_POINT('Ctrl Pts',(-131.633529942471,-5.62471521638866,
126.632931655165));
#196766=CARTESIAN_POINT('Ctrl Pts',(-131.911977566284,-6.54983729284086,
133.281833582332));
#196767=CARTESIAN_POINT('Ctrl Pts',(-132.190425190097,-1.45597887451291,
137.654058886162));
#196768=CARTESIAN_POINT('Ctrl Pts',(-132.46887281391,4.97585300097076,135.731746107516));
#196769=CARTESIAN_POINT('Ctrl Pts',(-132.747320437723,6.83511905249447,
129.281406779768));
#196770=CARTESIAN_POINT('Ctrl Pts',(-133.025768061535,2.4132446089053,124.230587628526));
#196771=CARTESIAN_POINT('Ctrl Pts',(-133.304215685348,-4.22628373671482,
125.220744707546));
#196772=CARTESIAN_POINT('Ctrl Pts',(-133.582663309161,-6.98206379373247,
131.341972033073));
#196773=CARTESIAN_POINT('Ctrl Pts',(-133.861110932974,-3.32166831708915,
136.969160731525));
#196774=CARTESIAN_POINT('Ctrl Pts',(-134.139558556787,3.39117807044069,
136.931199292478));
#196775=CARTESIAN_POINT('Ctrl Pts',(-134.4180061806,6.98769747949419,131.262972423894));
#196776=CARTESIAN_POINT('Ctrl Pts',(-134.696453804413,4.16286427289247,
125.173303709728));
#196777=CARTESIAN_POINT('Ctrl Pts',(-134.974901428226,-2.48743783327188,
124.25830120144));
#196778=CARTESIAN_POINT('Ctrl Pts',(-135.253349052039,-6.85190608875344,
129.358807503792));
#196779=CARTESIAN_POINT('Ctrl Pts',(-135.531796675851,-4.91980738289134,
135.787706498505));
#196780=CARTESIAN_POINT('Ctrl Pts',(-135.810244299665,1.53335396189511,
137.637154078616));
#196781=CARTESIAN_POINT('Ctrl Pts',(-136.088691923477,6.57743792420584,
133.207598268539));
#196782=CARTESIAN_POINT('Ctrl Pts',(-136.36713954729,5.57717775987727,126.569584461903));
#196783=CARTESIAN_POINT('Ctrl Pts',(-136.645587171103,-0.548236305497475,
123.823123062006));
#196784=CARTESIAN_POINT('Ctrl Pts',(-136.924034794916,-6.1698479889529,
127.492077923251));
#196785=CARTESIAN_POINT('Ctrl Pts',(-137.202482418729,-6.12167078439119,
134.204858766568));
#196786=CARTESIAN_POINT('Ctrl Pts',(-137.480930042542,-0.447977189217358,
137.792747934521));
#196787=CARTESIAN_POINT('Ctrl Pts',(-137.759377666354,5.63738555794455,
134.958650559891));
#196788=CARTESIAN_POINT('Ctrl Pts',(-138.037825290167,6.54226637895086,
128.306963676612));
#196789=CARTESIAN_POINT('Ctrl Pts',(-138.31627291398,1.43512400518173,123.950262577445));
#196790=CARTESIAN_POINT('Ctrl Pts',(-138.594720537793,-4.99082721964375,
125.892142735845));
#196791=CARTESIAN_POINT('Ctrl Pts',(-138.873168161606,-6.83045204508126,
132.348111152362));
#196792=CARTESIAN_POINT('Ctrl Pts',(-139.151615785419,-2.39322512722196,
137.385448243807));
#196793=CARTESIAN_POINT('Ctrl Pts',(-139.430063409232,4.24325876700673,
136.375087310741));
#196794=CARTESIAN_POINT('Ctrl Pts',(-139.708511033045,6.98039514907165,
130.245500691775));
#196795=CARTESIAN_POINT('Ctrl Pts',(-139.986958656858,3.30288940040013,
124.629479042785));
#196796=CARTESIAN_POINT('Ctrl Pts',(-140.26540628067,-3.40981035212143,
124.687871901284));
#196797=CARTESIAN_POINT('Ctrl Pts',(-140.543853904484,-6.98906096953965,
130.36701908296));
#196798=CARTESIAN_POINT('Ctrl Pts',(-140.822301528296,-4.1457059905611,
136.448061769617));
#196799=CARTESIAN_POINT('Ctrl Pts',(-141.100749152109,2.50735026474636,
137.342818807668));
#196800=CARTESIAN_POINT('Ctrl Pts',(-141.379196775922,6.85627411762182,
132.229052190456));
#196801=CARTESIAN_POINT('Ctrl Pts',(-141.657644399735,4.90461700401472,
125.80606361781));
#196802=CARTESIAN_POINT('Ctrl Pts',(-141.936092023548,-1.5541435324211,
123.976265807557));
#196803=CARTESIAN_POINT('Ctrl Pts',(-142.214539647361,-6.58472208669408,
128.421153556726));
#196804=CARTESIAN_POINT('Ctrl Pts',(-142.492987271174,-5.56426272485295,
135.056092168669));
#196805=CARTESIAN_POINT('Ctrl Pts',(-142.771434894987,0.569482251782813,
137.783897193782));
#196806=CARTESIAN_POINT('Ctrl Pts',(-143.0498825188,6.17990085978423,134.097849074668));
#196807=CARTESIAN_POINT('Ctrl Pts',(-143.328330142612,6.11129248258502,
127.385245959334));
#196808=CARTESIAN_POINT('Ctrl Pts',(-143.606777766425,0.426704867125613,
123.814642181877));
#196809=CARTESIAN_POINT('Ctrl Pts',(-143.885225390238,-5.65000367553061,
126.667248180088));
#196810=CARTESIAN_POINT('Ctrl Pts',(-144.163673014051,-6.53463485839856,
133.321658399163));
#196811=CARTESIAN_POINT('Ctrl Pts',(-144.442120637864,-1.4142558410586,
137.662794933783));
#196812=CARTESIAN_POINT('Ctrl Pts',(-144.720568261677,5.00575520397605,
135.701365384942));
#196813=CARTESIAN_POINT('Ctrl Pts',(-144.99901588549,6.82572176129271,129.239827686864));
#196814=CARTESIAN_POINT('Ctrl Pts',(-145.277463509303,2.37318347502772,
124.216019320419));
#196815=CARTESIAN_POINT('Ctrl Pts',(-145.555911133116,-4.26019448832994,
125.246574747685));
#196816=CARTESIAN_POINT('Ctrl Pts',(-145.834358756928,-6.97866183898313,
131.384463876438));
#196817=CARTESIAN_POINT('Ctrl Pts',(-146.112806380741,-3.28407988619528,
136.989266449907));
#196818=CARTESIAN_POINT('Ctrl Pts',(-146.391254004554,3.42841104578457,
136.910442712901));
#196819=CARTESIAN_POINT('Ctrl Pts',(-146.669701628367,6.99035971387901,
131.220427828976));
#196820=CARTESIAN_POINT('Ctrl Pts',(-146.94814925218,4.12850930297597,125.148067503779));
#196821=CARTESIAN_POINT('Ctrl Pts',(-147.226596875993,-2.52723946847004,
124.27356422487));
#196822=CARTESIAN_POINT('Ctrl Pts',(-147.505044499806,-6.86057863090408,
129.400543783708));
#196823=CARTESIAN_POINT('Ctrl Pts',(-147.783492123619,-4.88938118943532,
135.817562432597));
#196824=CARTESIAN_POINT('Ctrl Pts',(-148.061939747432,1.57491870557395,
137.627693521995));
#196825=CARTESIAN_POINT('Ctrl Pts',(-148.340387371245,6.5919452492172,133.167515010566));
#196826=CARTESIAN_POINT('Ctrl Pts',(-148.618834995057,5.55129614325799,
126.535713058481));
#196827=CARTESIAN_POINT('Ctrl Pts',(-148.89728261887,-0.590722922461593,
123.826589678167));
#196828=CARTESIAN_POINT('Ctrl Pts',(-149.175730242683,-6.18989648085842,
127.529696908099));
#196829=CARTESIAN_POINT('Ctrl Pts',(-149.454177866496,-6.10085756660025,
134.242060110815));
#196830=CARTESIAN_POINT('Ctrl Pts',(-149.732625490309,-0.405428592098244,
137.795345420191));
#196831=CARTESIAN_POINT('Ctrl Pts',(-150.011073114122,5.66256945225453,
134.924257224548));
#196832=CARTESIAN_POINT('Ctrl Pts',(-150.289520737935,6.52694280188189,
128.267185315226));
#196833=CARTESIAN_POINT('Ctrl Pts',(-150.567968361748,1.39337457546175,
123.94165356085));
#196834=CARTESIAN_POINT('Ctrl Pts',(-150.84641598556,-5.02063681567507,
125.922614329717));
#196835=CARTESIAN_POINT('Ctrl Pts',(-151.124863609373,-6.8209282449509,
132.389661450552));
#196836=CARTESIAN_POINT('Ctrl Pts',(-151.403311233186,-2.35311983798619,
137.399894552124));
#196837=CARTESIAN_POINT('Ctrl Pts',(-151.681758856999,4.2770907437925,136.349154177582));
#196838=CARTESIAN_POINT('Ctrl Pts',(-151.960206480812,6.97686387952531,
130.20301939961));
#196839=CARTESIAN_POINT('Ctrl Pts',(-152.238654104625,3.26523994872261,
124.609487823786));
#196840=CARTESIAN_POINT('Ctrl Pts',(-152.517101728438,-3.44697997911642,
124.708741709087));
#196841=CARTESIAN_POINT('Ctrl Pts',(-152.795549352251,-6.99159370048095,
130.40957158374));
#196842=CARTESIAN_POINT('Ctrl Pts',(-153.073996976064,-4.11127436944443,
136.473193293963));
#196843=CARTESIAN_POINT('Ctrl Pts',(-153.352444599876,2.54710526019297,
137.327434712448));
#196844=CARTESIAN_POINT('Ctrl Pts',(-153.63089222369,6.86481958872245,132.187289707623));
#196845=CARTESIAN_POINT('Ctrl Pts',(-153.909339847502,4.87410008029735,
125.776300428876));
#196846=CARTESIAN_POINT('Ctrl Pts',(-154.187787471315,-1.5956792888948,
123.98585282914));
#196847=CARTESIAN_POINT('Ctrl Pts',(-154.466235095128,-6.5991073448593,
128.461280784342));
#196848=CARTESIAN_POINT('Ctrl Pts',(-154.744682718941,-5.53827813521478,
135.089884640464));
#196849=CARTESIAN_POINT('Ctrl Pts',(-155.023130342754,0.611958120764675,
137.78030127903));
#196850=CARTESIAN_POINT('Ctrl Pts',(-155.301577966567,6.19983475957701,
134.060169243357));
#196851=CARTESIAN_POINT('Ctrl Pts',(-155.58002559038,6.0903661331043,127.348108135675));
#196852=CARTESIAN_POINT('Ctrl Pts',(-155.858473214192,0.38414856123516,
123.812174211531));
#196853=CARTESIAN_POINT('Ctrl Pts',(-156.136920838005,-5.67508277170857,
126.701718007236));
#196854=CARTESIAN_POINT('Ctrl Pts',(-156.415368461818,-6.51919028065846,
133.3613899366));
#196855=CARTESIAN_POINT('Ctrl Pts',(-156.693816085631,-1.37248040183399,
137.671276839599));
#196856=CARTESIAN_POINT('Ctrl Pts',(-156.972263709444,5.03547191688086,
135.670803202055));
#196857=CARTESIAN_POINT('Ctrl Pts',(-157.250711333257,6.81607154046107,
129.198306568304));
#196858=CARTESIAN_POINT('Ctrl Pts',(-157.52915895707,2.33303440196427,124.201695145721));
#196859=CARTESIAN_POINT('Ctrl Pts',(-157.807606580883,-4.29394737687161,
125.272610733624));
#196860=CARTESIAN_POINT('Ctrl Pts',(-158.086054204696,-6.97500128735293,
131.426934223863));
#196861=CARTESIAN_POINT('Ctrl Pts',(-158.364501828508,-3.2463697625135,
137.009142984327));
#196862=CARTESIAN_POINT('Ctrl Pts',(-158.642949452322,3.46551698009634,
136.889459870208));
#196863=CARTESIAN_POINT('Ctrl Pts',(-158.921397076134,6.99276291791392,
131.177867816534));
#196864=CARTESIAN_POINT('Ctrl Pts',(-159.199844699947,4.09400134962899,
125.123040893851));
#196865=CARTESIAN_POINT('Ctrl Pts',(-159.47829232376,-2.56694745588028,
124.289069249361));
#196866=CARTESIAN_POINT('Ctrl Pts',(-159.756739947573,-6.86899695179061,
129.442332082575));
#196867=CARTESIAN_POINT('Ctrl Pts',(-160.035187571386,-4.85877381816122,
135.84723260065));
#196868=CARTESIAN_POINT('Ctrl Pts',(-160.313635195198,1.61642509006095,
137.617980124263));
#196869=CARTESIAN_POINT('Ctrl Pts',(-160.592082819012,6.60620830727321,
133.12734418504));
#196870=CARTESIAN_POINT('Ctrl Pts',(-160.870530442824,5.52520882131862,
126.501999831362));
#196871=CARTESIAN_POINT('Ctrl Pts',(-161.148978066638,-0.633187649970563,
123.830314858198));
#196872=CARTESIAN_POINT('Ctrl Pts',(-161.42742569045,-6.20971560387352,
127.567437236815));
#196873=CARTESIAN_POINT('Ctrl Pts',(-161.705873314263,-6.07981827928859,
134.279134069845));
#196874=CARTESIAN_POINT('Ctrl Pts',(-161.984320938076,-0.362864971672915,
137.79768385235));
#196875=CARTESIAN_POINT('Ctrl Pts',(-162.262768561889,5.68754351797111,
134.889711224922));
#196876=CARTESIAN_POINT('Ctrl Pts',(-162.541216185702,6.5113773665471,128.227500969805));
#196877=CARTESIAN_POINT('Ctrl Pts',(-162.819663809515,1.35157351373451,
123.93329884439));
#196878=CARTESIAN_POINT('Ctrl Pts',(-163.098111433328,-5.05026037016286,
125.953266818493));
#196879=CARTESIAN_POINT('Ctrl Pts',(-163.376559057141,-6.81115169281603,
132.431153004838));
#196880=CARTESIAN_POINT('Ctrl Pts',(-163.655006680953,-2.31292735302948,
137.414096460505));
#196881=CARTESIAN_POINT('Ctrl Pts',(-163.933454304766,4.31076423140788,
136.323015580059));
#196882=CARTESIAN_POINT('Ctrl Pts',(-164.211901928579,6.97307407972212,
130.160560390364));
#196883=CARTESIAN_POINT('Ctrl Pts',(-164.490349552392,3.2274695023783,124.589726158078));
#196884=CARTESIAN_POINT('Ctrl Pts',(-164.768797176205,-3.4840218770001,
124.729837392289));
#196885=CARTESIAN_POINT('Ctrl Pts',(-165.047244800018,-6.99386735534677,
130.452138713572));
#196886=CARTESIAN_POINT('Ctrl Pts',(-165.325692423831,-4.07669040354407,
136.498114757629));
#196887=CARTESIAN_POINT('Ctrl Pts',(-165.604140047644,2.58676587171747,
137.31180890232));
#196888=CARTESIAN_POINT('Ctrl Pts',(-165.882587671457,6.87311068140868,
132.145475979844));
#196889=CARTESIAN_POINT('Ctrl Pts',(-166.161035295269,4.84340254500906,
125.746723556562));
#196890=CARTESIAN_POINT('Ctrl Pts',(-166.439482919082,-1.63715591688565,
123.995692513036));
#196891=CARTESIAN_POINT('Ctrl Pts',(-166.717930542895,-6.61324807067504,
128.501494835643));
#196892=CARTESIAN_POINT('Ctrl Pts',(-166.996378166708,-5.5120883226436,
135.12351831059));
#196893=CARTESIAN_POINT('Ctrl Pts',(-167.274825790521,0.654411313413328,
137.776446868231));
#196894=CARTESIAN_POINT('Ctrl Pts',(-167.553273414334,6.21953892221278,
134.022368766858));
#196895=CARTESIAN_POINT('Ctrl Pts',(-167.831721038147,6.06921410286677,
127.311098384725));
#196896=CARTESIAN_POINT('Ctrl Pts',(-168.11016866196,0.3415780205785,123.809965339223));
#196897=CARTESIAN_POINT('Ctrl Pts',(-168.388616285773,-5.69995157560742,
126.736339859314));
#196898=CARTESIAN_POINT('Ctrl Pts',(-168.667063909585,-6.50350413192509,
133.401026722375));
#196899=CARTESIAN_POINT('Ctrl Pts',(-168.945511533399,-1.33065410484337,
137.679504289309));
#196900=CARTESIAN_POINT('Ctrl Pts',(-169.223959157211,5.06500203852252,
135.640060691349));
#196901=CARTESIAN_POINT('Ctrl Pts',(-169.502406781024,6.80616874759175,
129.156844962666));
#196902=CARTESIAN_POINT('Ctrl Pts',(-169.780854404837,2.29279887745254,
124.18761563522));
#196903=CARTESIAN_POINT('Ctrl Pts',(-170.05930202865,-4.32754115161411,
125.298851700587));
#196904=CARTESIAN_POINT('Ctrl Pts',(-170.337749652463,-6.97108227448498,
131.469381501595));
#196905=CARTESIAN_POINT('Ctrl Pts',(-170.616197276276,-3.20853934340632,
137.028789598255));
#196906=CARTESIAN_POINT('Ctrl Pts',(-170.894644900089,3.50249449840198,
136.868251541923));
#196907=CARTESIAN_POINT('Ctrl Pts',(-171.173092523901,6.99490700254731,
131.135293963646));
#196908=CARTESIAN_POINT('Ctrl Pts',(-171.451540147715,4.05934169155642,
125.098224807315));
#196909=CARTESIAN_POINT('Ctrl Pts',(-171.729987771527,-2.60656032410858,
124.304815700371));
#196910=CARTESIAN_POINT('Ctrl Pts',(-172.00843539534,-6.87716073946864,
129.484170851909));
#196911=CARTESIAN_POINT('Ctrl Pts',(-172.286883019153,-4.82798640323697,
135.876715903229));
#196912=CARTESIAN_POINT('Ctrl Pts',(-172.565330642966,1.65787157732142,
137.608014245356));
#196913=CARTESIAN_POINT('Ctrl Pts',(-172.843778266779,6.62022656985093,
133.087087280501));
#196914=CARTESIAN_POINT('Ctrl Pts',(-173.122225890592,5.49891676073447,
126.468446029806));
#196915=CARTESIAN_POINT('Ctrl Pts',(-173.400673514405,-0.675628914478315,
123.834298464058));
#196916=CARTESIAN_POINT('Ctrl Pts',(-173.679121138218,-6.22930462359329,
127.605297510917));
#196917=CARTESIAN_POINT('Ctrl Pts',(-173.95756876203,-6.05855370207473,
134.316079269865));
#196918=CARTESIAN_POINT('Ctrl Pts',(-174.236016385844,-0.320287905152608,
137.799763144343));
#196919=CARTESIAN_POINT('Ctrl Pts',(-174.514464009656,5.71230682967103,
134.855013841124));
#196920=CARTESIAN_POINT('Ctrl Pts',(-174.792911633469,6.49557064972945,
128.187912110866));
#196921=CARTESIAN_POINT('Ctrl Pts',(-175.071359257282,1.30972236895365,
123.925198737649));
#196922=CARTESIAN_POINT('Ctrl Pts',(-175.349806881095,-5.07969678539539,
125.984099066334));
#196923=CARTESIAN_POINT('Ctrl Pts',(-175.628254504908,-6.80112275095037,
132.472584277733));
#196924=CARTESIAN_POINT('Ctrl Pts',(-175.906702128721,-2.27264916169912,
137.428053442694));
#196925=CARTESIAN_POINT('Ctrl Pts',(-176.185149752534,4.34427798206938,
136.296672486746));
#196926=CARTESIAN_POINT('Ctrl Pts',(-176.463597376347,6.96902589009458,
130.118125237372));
#196927=CARTESIAN_POINT('Ctrl Pts',(-176.742045000159,3.18957946096438,
124.570194777934));
#196928=CARTESIAN_POINT('Ctrl Pts',(-177.020492623972,-3.52093467317244,
124.751158169184));
#196929=CARTESIAN_POINT('Ctrl Pts',(-177.298940247785,-6.99588184988549,
130.494718895118));
#196930=CARTESIAN_POINT('Ctrl Pts',(-177.577387871598,-4.04195537438161,
136.522825237142));
#196931=CARTESIAN_POINT('Ctrl Pts',(-177.855835495411,2.62633062968132,
137.295941956302));
#196932=CARTESIAN_POINT('Ctrl Pts',(-178.134283119224,6.88114708845103,
132.103612556543));
#196933=CARTESIAN_POINT('Ctrl Pts',(-178.412730743037,4.81252553565828,
125.717334096849));
#196934=CARTESIAN_POINT('Ctrl Pts',(-178.69117836685,-1.67857187946192,
124.005784494632));
#196935=CARTESIAN_POINT('Ctrl Pts',(-178.969625990663,-6.62714374015151,
128.541794220484));
#196936=CARTESIAN_POINT('Ctrl Pts',(-179.248073614475,-5.48569425761253,
135.15699193274));
#196937=CARTESIAN_POINT('Ctrl Pts',(-179.526521238288,0.696840256609583,
137.772334104211));
#196938=CARTESIAN_POINT('Ctrl Pts',(-179.804968862101,6.23901261754625,
133.984449045885));
#196939=CARTESIAN_POINT('Ctrl Pts',(-180.083416485914,6.0478371756692,127.27421807789));
#196940=CARTESIAN_POINT('Ctrl Pts',(-180.361864109727,0.298994822622653,
123.808015646805));
#196941=CARTESIAN_POINT('Ctrl Pts',(-180.64031173354,-5.72460916570447,
126.771112453397));
#196942=CARTESIAN_POINT('Ctrl Pts',(-180.918759357353,-6.48757699345442,
133.440567287733));
#196943=CARTESIAN_POINT('Ctrl Pts',(-181.197206981166,-1.28877849997557,
137.687476978041));
#196944=CARTESIAN_POINT('Ctrl Pts',(-181.475654604978,5.094344474651,135.609138992));
#196945=CARTESIAN_POINT('Ctrl Pts',(-181.754102228792,6.79601374963652,
129.115444406326));
#196946=CARTESIAN_POINT('Ctrl Pts',(-182.032549852604,2.25247839243521,
124.173781310638));
#196947=CARTESIAN_POINT('Ctrl Pts',(-182.310997476417,-4.36097456772779,
125.32529667621));
#196948=CARTESIAN_POINT('Ctrl Pts',(-182.58944510023,-6.96690494559973,
131.511804136733));
#196949=CARTESIAN_POINT('Ctrl Pts',(-182.867892724043,-3.17059003069381,
137.048205563678));
#196950=CARTESIAN_POINT('Ctrl Pts',(-183.146340347856,3.53934223048593,
136.84681851393));
#196951=CARTESIAN_POINT('Ctrl Pts',(-183.424787971669,6.99679188832936,
131.092707847901));
#196952=CARTESIAN_POINT('Ctrl Pts',(-183.703235595482,4.02453161308464,
125.07362016374));
#196953=CARTESIAN_POINT('Ctrl Pts',(-183.981683219295,-2.64607660528548,
124.320802994409));
#196954=CARTESIAN_POINT('Ctrl Pts',(-184.260130843107,-6.88506969142675,
129.52605854136));
#196955=CARTESIAN_POINT('Ctrl Pts',(-184.53857846692,-4.79702008550057,
135.906011247817));
#196956=CARTESIAN_POINT('Ctrl Pts',(-184.817026090733,1.6992566315413,137.597796254561));
#196957=CARTESIAN_POINT('Ctrl Pts',(-185.095473714546,6.63399951749853,
133.046745788687));
#196958=CARTESIAN_POINT('Ctrl Pts',(-185.373921338359,5.47242093576752,
126.435052897159));
#196959=CARTESIAN_POINT('Ctrl Pts',(-185.652368962172,-0.718045143308166,
123.838540348135));
#196960=CARTESIAN_POINT('Ctrl Pts',(-185.930816585985,-6.24866281413942,
127.64327632748));
#196961=CARTESIAN_POINT('Ctrl Pts',(-186.209264209798,-6.03706462292539,
134.35289434186));
#196962=CARTESIAN_POINT('Ctrl Pts',(-186.487711833611,-0.277698970246197,
137.801583219124));
#196963=CARTESIAN_POINT('Ctrl Pts',(-186.766159457423,5.73685846974069,
134.820166358884));
#196964=CARTESIAN_POINT('Ctrl Pts',(-187.044607081237,6.47952323715255,
128.148420205389));
#196965=CARTESIAN_POINT('Ctrl Pts',(-187.323054705049,1.2678226919294,123.917353540782));
#196966=CARTESIAN_POINT('Ctrl Pts',(-187.601502328862,-5.10894497059535,
126.01510993074));
#196967=CARTESIAN_POINT('Ctrl Pts',(-187.879949952675,-6.79084179098006,
132.513953733987));
#196968=CARTESIAN_POINT('Ctrl Pts',(-188.158397576488,-2.23228675651833,
137.44176498151));
#196969=CARTESIAN_POINT('Ctrl Pts',(-188.436845200301,4.37763075391265,
136.270125873797));
#196970=CARTESIAN_POINT('Ctrl Pts',(-188.715292824114,6.96471946064982,
130.075715513085));
#196971=CARTESIAN_POINT('Ctrl Pts',(-188.993740447926,3.15157122851057,
124.550894407098));
#196972=CARTESIAN_POINT('Ctrl Pts',(-189.27218807174,-3.55771699981564,
124.772703249722));
#196973=CARTESIAN_POINT('Ctrl Pts',(-189.550635695553,-6.99763710944952,
130.53731055055));
#196974=CARTESIAN_POINT('Ctrl Pts',(-189.829083319365,-4.00707056907658,
136.547323816845));
#196975=CARTESIAN_POINT('Ctrl Pts',(-190.107530943179,2.66579806799723,
137.279834462351));
#196976=CARTESIAN_POINT('Ctrl Pts',(-190.385978566991,6.88892851205765,
132.061700988983));
#196977=CARTESIAN_POINT('Ctrl Pts',(-190.664426190804,4.78147019640398,
125.688133138775));
#196978=CARTESIAN_POINT('Ctrl Pts',(-190.942873814617,-1.71992564193992,
124.016128399968));
#196979=CARTESIAN_POINT('Ctrl Pts',(-191.22132143843,-6.64079383837953,
128.582177445553));
#196980=CARTESIAN_POINT('Ctrl Pts',(-191.499769062243,-5.45909691816341,
135.190304266535));
#196981=CARTESIAN_POINT('Ctrl Pts',(-191.778216686055,0.739243378134395,
137.767963139373));
#196982=CARTESIAN_POINT('Ctrl Pts',(-192.056664309869,6.25825512397307,
133.946411485565));
#196983=CARTESIAN_POINT('Ctrl Pts',(-192.335111933681,6.0262361436405,127.237468581785));
#196984=CARTESIAN_POINT('Ctrl Pts',(-192.613559557494,0.256400545303713,
123.806325206523));
#196985=CARTESIAN_POINT('Ctrl Pts',(-192.892007181307,-5.74905462830365,
126.806034500975));
#196986=CARTESIAN_POINT('Ctrl Pts',(-193.17045480512,-6.47140945543246,
133.480010167483));
#196987=CARTESIAN_POINT('Ctrl Pts',(-193.448902428933,-1.24685513894648,
137.695194610365));
#196988=CARTESIAN_POINT('Ctrl Pts',(-193.727350052746,5.12349813797151,
135.578039249819));
#196989=CARTESIAN_POINT('Ctrl Pts',(-194.005797676559,6.78560692289256,
129.074106433399));
#196990=CARTESIAN_POINT('Ctrl Pts',(-194.284245300372,2.2120744410027,124.160192684611));
#196991=CARTESIAN_POINT('Ctrl Pts',(-194.562692924184,-4.39424638632456,
125.35194468056));
#196992=CARTESIAN_POINT('Ctrl Pts',(-194.841140547997,-6.9624694554897,
131.554200557291));
#196993=CARTESIAN_POINT('Ctrl Pts',(-195.11958817181,-3.13252323060231,
137.067390161131));
#196994=CARTESIAN_POINT('Ctrl Pts',(-195.398035795623,3.57605881094196,
136.825161580438));
#196995=CARTESIAN_POINT('Ctrl Pts',(-195.676483419436,6.99841750541489,
131.050111047343));
#196996=CARTESIAN_POINT('Ctrl Pts',(-195.954931043249,3.98957240411393,
125.04922787486));
#196997=CARTESIAN_POINT('Ctrl Pts',(-196.233378667062,-2.68549483512068,
124.337030539057));
#196998=CARTESIAN_POINT('Ctrl Pts',(-196.511826290875,-6.89272351459547,
129.567993598765));
#196999=CARTESIAN_POINT('Ctrl Pts',(-196.790273914688,-4.76587601242081,
135.935117548864));
#197000=CARTESIAN_POINT('Ctrl Pts',(-197.0687215385,1.74057871918182,137.58732653051));
#197001=CARTESIAN_POINT('Ctrl Pts',(-197.347169162313,6.64752663985393,
133.006321204467));
#197002=CARTESIAN_POINT('Ctrl Pts',(-197.625616786126,5.44572232823074,
126.401821670817));
#197003=CARTESIAN_POINT('Ctrl Pts',(-197.904064409939,-0.760434764710735,
123.843040353244));
#197004=CARTESIAN_POINT('Ctrl Pts',(-198.182512033752,-6.26778945818702,
127.681372279183));
#197005=CARTESIAN_POINT('Ctrl Pts',(-198.460959657565,-6.01535183812634,
134.389577921633));
#197006=CARTESIAN_POINT('Ctrl Pts',(-198.739407281378,-0.235099745102313,
137.803144009248));
#197007=CARTESIAN_POINT('Ctrl Pts',(-199.017854905191,5.76119752841001,
134.785170069484));
#197008=CARTESIAN_POINT('Ctrl Pts',(-199.296302529004,6.46323572345932,
128.10902671676));
#197009=CARTESIAN_POINT('Ctrl Pts',(-199.574750152817,1.22587603526843,
123.909763544495));
#197010=CARTESIAN_POINT('Ctrl Pts',(-199.853197776629,-5.13800384196074,
126.04629826259));
#197011=CARTESIAN_POINT('Ctrl Pts',(-200.131645400443,-6.78030919386985,
132.555259840639));
#197012=CARTESIAN_POINT('Ctrl Pts',(-200.410093024255,-2.19184163313082,
137.455230568865));
#197013=CARTESIAN_POINT('Ctrl Pts',(-200.688540648069,4.41082131103843,
136.243376724908));
#197014=CARTESIAN_POINT('Ctrl Pts',(-200.96698827188,6.96015495096418,130.03333278901));
#197015=CARTESIAN_POINT('Ctrl Pts',(-201.245435895694,3.11344621342587,
124.531825760752));
#197016=CARTESIAN_POINT('Ctrl Pts',(-201.523883519507,-3.59436749394705,
124.794471835542));
#197017=CARTESIAN_POINT('Ctrl Pts',(-201.80233114332,-6.99913306899709,
130.579912101622));
#197018=CARTESIAN_POINT('Ctrl Pts',(-202.080778767133,-3.97203728029775,
136.571609588935));
#197019=CARTESIAN_POINT('Ctrl Pts',(-202.359226390945,2.705166724186,137.263487017335));
#197020=CARTESIAN_POINT('Ctrl Pts',(-202.637674014758,6.89645466388467,
132.019742830214));
#197021=CARTESIAN_POINT('Ctrl Pts',(-202.916121638571,4.75023767801316,
125.659121764391));
#197022=CARTESIAN_POINT('Ctrl Pts',(-203.194569262384,-1.76121567194074,
124.026723845744));
#197023=CARTESIAN_POINT('Ctrl Pts',(-203.473016886197,-6.65419785954973,
128.622643014438));
#197024=CARTESIAN_POINT('Ctrl Pts',(-203.75146451001,-5.43229728987039,
135.223454077576));
#197025=CARTESIAN_POINT('Ctrl Pts',(-204.029912133822,0.781619106723946,
137.763334135682));
#197026=CARTESIAN_POINT('Ctrl Pts',(-204.308359757636,6.27726572845484,
133.908257495395));
#197027=CARTESIAN_POINT('Ctrl Pts',(-204.586807381448,6.00441180721532,
127.200851258176));
#197028=CARTESIAN_POINT('Ctrl Pts',(-204.865255005262,0.213796766968775,
123.804894081017));
#197029=CARTESIAN_POINT('Ctrl Pts',(-205.143702629074,-5.77328705756903,
126.841104707996));
#197030=CARTESIAN_POINT('Ctrl Pts',(-205.422150252887,-6.4550021169537,
133.519353900054));
#197031=CARTESIAN_POINT('Ctrl Pts',(-205.7005978767,-1.20488557524167,137.702656900301));
#197032=CARTESIAN_POINT('Ctrl Pts',(-205.979045500513,5.15246194818434,
135.546762617222));
#197033=CARTESIAN_POINT('Ctrl Pts',(-206.257493124326,6.77494865298866,
129.032832575676));
#197034=CARTESIAN_POINT('Ctrl Pts',(-206.535940748139,2.17158852033829,
124.14685026067));
#197035=CARTESIAN_POINT('Ctrl Pts',(-206.814388371952,-4.42735537450605,
125.378794726189));
#197036=CARTESIAN_POINT('Ctrl Pts',(-207.092835995765,-6.9577759685135,
131.596569192254));
#197037=CARTESIAN_POINT('Ctrl Pts',(-207.371283619578,-3.09434035370993,
137.086342679721));
#197038=CARTESIAN_POINT('Ctrl Pts',(-207.64973124339,3.61264287922363,136.803281543952));
#197039=CARTESIAN_POINT('Ctrl Pts',(-207.928178867203,6.99978379356611,
131.007505140413));
#197040=CARTESIAN_POINT('Ctrl Pts',(-208.206626491016,3.95446536007061,
125.025048844539));
#197041=CARTESIAN_POINT('Ctrl Pts',(-208.485074114829,-2.72481355295718,
124.353497733001));
#197042=CARTESIAN_POINT('Ctrl Pts',(-208.763521738642,-6.90012192535954,
129.609974470206));
#197043=CARTESIAN_POINT('Ctrl Pts',(-209.041969362455,-4.73455533805275,
135.964033727826));
#197044=CARTESIAN_POINT('Ctrl Pts',(-209.320416986268,1.78183630903778,
137.576605461163));
#197045=CARTESIAN_POINT('Ctrl Pts',(-209.598864610081,6.66080743566547,
132.965815025787));
#197046=CARTESIAN_POINT('Ctrl Pts',(-209.877312233893,5.41882192745001,
126.368753582173));
#197047=CARTESIAN_POINT('Ctrl Pts',(-210.155759857706,-0.802796207923886,
123.847798312635));
#197048=CARTESIAN_POINT('Ctrl Pts',(-210.434207481519,-6.28668384699127,
127.719583954367));
#197049=CARTESIAN_POINT('Ctrl Pts',(-210.712655105332,-5.99341615225276,
134.42612864986));
#197050=CARTESIAN_POINT('Ctrl Pts',(-210.991102729145,-0.19249180825093,
137.804445456879));
#197051=CARTESIAN_POINT('Ctrl Pts',(-211.269550352958,5.78532310378624,
134.750026269725));
#197052=CARTESIAN_POINT('Ctrl Pts',(-211.547997976771,6.44670871218949,
128.069733104719));
#197053=CARTESIAN_POINT('Ctrl Pts',(-211.826445600584,1.18388395332015,
123.902429030038));
#197054=CARTESIAN_POINT('Ctrl Pts',(-212.104893224396,-5.16687232270428,
126.077662906191));
#197055=CARTESIAN_POINT('Ctrl Pts',(-212.38334084821,-6.76952534990887,
132.596501067076));
#197056=CARTESIAN_POINT('Ctrl Pts',(-212.661788472022,-2.15131529024619,
137.468449705789));
#197057=CARTESIAN_POINT('Ctrl Pts',(-212.940236095835,4.44384842355829,
136.216426031276));
#197058=CARTESIAN_POINT('Ctrl Pts',(-213.218683719648,6.95533253017721,
129.990978635656));
#197059=CARTESIAN_POINT('Ctrl Pts',(-213.497131343461,3.0752058284468,124.512989545492));
#197060=CARTESIAN_POINT('Ctrl Pts',(-213.775578967274,-3.63088479746918,
124.81646312));
#197061=CARTESIAN_POINT('Ctrl Pts',(-214.054026591087,-7.00036967309483,
130.622521969716));
#197062=CARTESIAN_POINT('Ctrl Pts',(-214.3324742149,-3.93685680621679,136.595681653493));
#197063=CARTESIAN_POINT('Ctrl Pts',(-214.610921838713,2.74443513942699,
137.246900227015));
#197064=CARTESIAN_POINT('Ctrl Pts',(-214.889369462525,6.90372526504794,
131.977739635008));
#197065=CARTESIAN_POINT('Ctrl Pts',(-215.167817086339,4.71882913781829,
125.630301048724));
#197066=CARTESIAN_POINT('Ctrl Pts',(-215.446264710151,-1.80244043944716,
124.037570439344));
#197067=CARTESIAN_POINT('Ctrl Pts',(-215.724712333964,-6.66735530697114,
128.66318942767));
#197068=CARTESIAN_POINT('Ctrl Pts',(-216.003159957777,-5.40529636580357,
135.256440137483));
#197069=CARTESIAN_POINT('Ctrl Pts',(-216.28160758159,0.823965872130078,
137.758447264668));
#197070=CARTESIAN_POINT('Ctrl Pts',(-216.560055205403,6.29604372654653,
133.869988489185));
#197071=CARTESIAN_POINT('Ctrl Pts',(-216.838502829216,5.98236497510254,
127.164367463932));
#197072=CARTESIAN_POINT('Ctrl Pts',(-217.116950453029,0.171185066315507,
123.803722323317));
#197073=CARTESIAN_POINT('Ctrl Pts',(-217.395398076842,-5.79730555555969,
126.876321774922));
#197074=CARTESIAN_POINT('Ctrl Pts',(-217.673845700654,-6.43835558599724,
133.558597027552));
#197075=CARTESIAN_POINT('Ctrl Pts',(-217.952293324468,-1.16287136405879,
137.709863571333));
#197076=CARTESIAN_POINT('Ctrl Pts',(-218.23074094828,5.18123483202488,135.515310253174));
#197077=CARTESIAN_POINT('Ctrl Pts',(-218.509188572093,6.76403933487094,
128.991624362576));
#197078=CARTESIAN_POINT('Ctrl Pts',(-218.787636195906,2.13102213066266,
124.133754533223));
#197079=CARTESIAN_POINT('Ctrl Pts',(-219.066083819719,-4.46030030540597,
125.405845818157));
#197080=CARTESIAN_POINT('Ctrl Pts',(-219.344531443532,-6.95282465859006,
131.638908471637));
#197081=CARTESIAN_POINT('Ctrl Pts',(-219.622979067345,-3.0560428148978,
137.105062417155));
#197082=CARTESIAN_POINT('Ctrl Pts',(-219.901426691158,3.6490930796943,136.781179215245));
#197083=CARTESIAN_POINT('Ctrl Pts',(-220.179874314971,7.00089070215466,
130.964891705888));
#197084=CARTESIAN_POINT('Ctrl Pts',(-220.458321938783,3.91921178185968,
125.001083968743));
#197085=CARTESIAN_POINT('Ctrl Pts',(-220.736769562596,-2.76403130182543,
124.370203966041));
#197086=CARTESIAN_POINT('Ctrl Pts',(-221.015217186409,-6.90726464956813,
129.651999600063));
#197087=CARTESIAN_POINT('Ctrl Pts',(-221.293664810222,-4.7030592229955,
135.992758713204));
#197088=CARTESIAN_POINT('Ctrl Pts',(-221.572112434035,1.82302787229404,
137.565633443793));
#197089=CARTESIAN_POINT('Ctrl Pts',(-221.850560057848,6.67384141280798,
132.925228753618));
#197090=CARTESIAN_POINT('Ctrl Pts',(-222.129007681661,5.39172073022998,
126.33584985658));
#197091=CARTESIAN_POINT('Ctrl Pts',(-222.407455305474,-0.845127903228338,
123.85281405));
#197092=CARTESIAN_POINT('Ctrl Pts',(-222.685902929286,-6.30534528041361,
127.757909937084));
#197093=CARTESIAN_POINT('Ctrl Pts',(-222.964350553099,-5.9712583781396,
134.462545172141));
#197094=CARTESIAN_POINT('Ctrl Pts',(-223.242798176912,-0.14987673854478,
137.805487513793));
#197095=CARTESIAN_POINT('Ctrl Pts',(-223.521245800725,5.80923430188729,
134.714736261875));
#197096=CARTESIAN_POINT('Ctrl Pts',(-223.799693424538,6.42994281575757,
128.030540825308));
#197097=CARTESIAN_POINT('Ctrl Pts',(-224.078141048351,1.1418480021166,123.895350269195));
#197098=CARTESIAN_POINT('Ctrl Pts',(-224.356588672164,-5.19554934309376,
126.109202699315));
#197099=CARTESIAN_POINT('Ctrl Pts',(-224.635036295977,-6.75849065869668,
132.637675885092));
#197100=CARTESIAN_POINT('Ctrl Pts',(-224.913483919789,-2.11070922958169,
137.481421902441));
#197101=CARTESIAN_POINT('Ctrl Pts',(-225.191931543603,4.47671086764076,
136.189274791569));
#197102=CARTESIAN_POINT('Ctrl Pts',(-225.470379167415,6.95025237698553,
129.948654622468));
#197103=CARTESIAN_POINT('Ctrl Pts',(-225.748826791228,3.03685149058481,
124.494386459301));
#197104=CARTESIAN_POINT('Ctrl Pts',(-226.027274415041,-3.66726755721984,
124.838676288203));
#197105=CARTESIAN_POINT('Ctrl Pts',(-226.305722038854,-7.00134687591997,
130.665138575908));
#197106=CARTESIAN_POINT('Ctrl Pts',(-226.584169662667,-3.9015304504591,
136.619539118521));
#197107=CARTESIAN_POINT('Ctrl Pts',(-226.86261728648,2.78360185861461,137.230074706019));
#197108=CARTESIAN_POINT('Ctrl Pts',(-227.141064910293,6.91074004613266,
131.935692959814));
#197109=CARTESIAN_POINT('Ctrl Pts',(-227.419512534106,4.68724573967455,
125.601672059739));
#197110=CARTESIAN_POINT('Ctrl Pts',(-227.697960157918,-1.8435984168596,
124.048667778841));
#197111=CARTESIAN_POINT('Ctrl Pts',(-227.976407781732,-6.68026569308986,
128.703815182788));
#197112=CARTESIAN_POINT('Ctrl Pts',(-228.254855405544,-5.37809514649209,
135.289261223946));
#197113=CARTESIAN_POINT('Ctrl Pts',(-228.533303029357,0.86628210517778,
137.753302707416));
#197114=CARTESIAN_POINT('Ctrl Pts',(-228.81175065317,6.31458842242258,133.831605885006));
#197115=CARTESIAN_POINT('Ctrl Pts',(-229.090198276983,5.96009646425557,
127.128018550972));
#197116=CARTESIAN_POINT('Ctrl Pts',(-229.368645900796,0.128567022336676,
123.802809976843));
#197117=CARTESIAN_POINT('Ctrl Pts',(-229.647093524609,-5.82110923226107,
126.911684396774));
#197118=CARTESIAN_POINT('Ctrl Pts',(-229.925541148421,-6.42147047940683,
133.597738095807));
#197119=CARTESIAN_POINT('Ctrl Pts',(-230.203988772235,-1.12081406224988,
137.716814356412));
#197120=CARTESIAN_POINT('Ctrl Pts',(-230.482436396047,5.20981572330331,
135.483683323156));
#197121=CARTESIAN_POINT('Ctrl Pts',(-230.76088401986,6.75287937278817,128.950483321085));
#197122=CARTESIAN_POINT('Ctrl Pts',(-231.039331643673,2.0903767751783,124.120905987538));
#197123=CARTESIAN_POINT('Ctrl Pts',(-231.317779267486,-4.49307995823781,
125.433096954076));
#197124=CARTESIAN_POINT('Ctrl Pts',(-231.596226891299,-6.94761570919197,
131.681216826544));
#197125=CARTESIAN_POINT('Ctrl Pts',(-231.874674515112,-3.01763203329532,
137.123548679767));
#197126=CARTESIAN_POINT('Ctrl Pts',(-232.153122138925,3.68540806167951,
136.758855413326));
#197127=CARTESIAN_POINT('Ctrl Pts',(-232.431569762738,7.00173819016367,
130.922272322824));
#197128=CARTESIAN_POINT('Ctrl Pts',(-232.71001738655,3.88381297581431,124.977334135496));
#197129=CARTESIAN_POINT('Ctrl Pts',(-232.988465010364,-2.80314662849731,
124.38714861912));
#197130=CARTESIAN_POINT('Ctrl Pts',(-233.266912634176,-6.914151422545,129.694067431082));
#197131=CARTESIAN_POINT('Ctrl Pts',(-233.545360257989,-4.67138883434919,
136.021291440583));
#197132=CARTESIAN_POINT('Ctrl Pts',(-233.823807881803,1.86415188258208,
137.554410884971));
#197133=CARTESIAN_POINT('Ctrl Pts',(-234.102255505615,6.68662808830262,
132.884563891901));
#197134=CARTESIAN_POINT('Ctrl Pts',(-234.380703129428,5.36441974081549,
126.303111713297));
#197135=CARTESIAN_POINT('Ctrl Pts',(-234.659150753241,-0.887428282007554,
123.858087379481));
#197136=CARTESIAN_POINT('Ctrl Pts',(-234.937598377053,-6.32377306694735,
127.796348807152));
#197137=CARTESIAN_POINT('Ctrl Pts',(-235.216046000867,-5.94887933685163,
134.498826139047));
#197138=CARTESIAN_POINT('Ctrl Pts',(-235.494493624679,-0.107256115101469,
137.806270141374));
#197139=CARTESIAN_POINT('Ctrl Pts',(-235.772941248493,5.83293023667497,
134.679301353618));
#197140=CARTESIAN_POINT('Ctrl Pts',(-236.051388872305,6.41293865542997,
127.991451330808));
#197141=CARTESIAN_POINT('Ctrl Pts',(-236.329836496118,1.09976973931543,
123.88852752427));
#197142=CARTESIAN_POINT('Ctrl Pts',(-236.608284119931,-5.22403384049169,
126.140916473241));
#197143=CARTESIAN_POINT('Ctrl Pts',(-236.886731743744,-6.7472055291277,
132.678782768935));
#197144=CARTESIAN_POINT('Ctrl Pts',(-237.165179367557,-2.07002495581049,
137.494146678133));
#197145=CARTESIAN_POINT('Ctrl Pts',(-237.44362699137,4.50940742555574,136.161924011888));
#197146=CARTESIAN_POINT('Ctrl Pts',(-237.722074615182,6.94491467963605,
129.906362317783));
#197147=CARTESIAN_POINT('Ctrl Pts',(-238.000522238996,2.99838462107406,
124.476017191522));
#197148=CARTESIAN_POINT('Ctrl Pts',(-238.278969862808,-3.70351442502255,
124.861110517033));
#197149=CARTESIAN_POINT('Ctrl Pts',(-238.557417486622,-7.00206464126185,
130.707760341024));
#197150=CARTESIAN_POINT('Ctrl Pts',(-238.835865110434,-3.86605952205578,
136.64318109997));
#197151=CARTESIAN_POINT('Ctrl Pts',(-239.114312734247,2.82266543041169,
137.213011077826));
#197152=CARTESIAN_POINT('Ctrl Pts',(-239.39276035806,6.91749874720356,131.893604362681));
#197153=CARTESIAN_POINT('Ctrl Pts',(-239.671207981873,4.655488653916,125.573235858291));
#197154=CARTESIAN_POINT('Ctrl Pts',(-239.949655605686,-1.88468807905538,
124.060015453022));
#197155=CARTESIAN_POINT('Ctrl Pts',(-240.228103229498,-6.69292853950653,
128.74451877439));
#197156=CARTESIAN_POINT('Ctrl Pts',(-240.506550853312,-5.35069463988719,
135.321916120768));
#197157=CARTESIAN_POINT('Ctrl Pts',(-240.784998477124,0.908566237823527,
137.747900654559));
#197158=CARTESIAN_POINT('Ctrl Pts',(-241.063446100938,6.33289912890243,
133.79311110514));
#197159=CARTESIAN_POINT('Ctrl Pts',(-241.34189372475,5.9376070998423,127.091805866219));
#197160=CARTESIAN_POINT('Ctrl Pts',(-241.620341348563,0.0859442142595387,
123.802157075403));
#197161=CARTESIAN_POINT('Ctrl Pts',(-241.898788972376,-5.84469720561911,
126.947191263173));
#197162=CARTESIAN_POINT('Ctrl Pts',(-242.177236596189,-6.40434742286629,
133.636775654432));
#197163=CARTESIAN_POINT('Ctrl Pts',(-242.455684220002,-1.07871522826414,
137.723508997977));
#197164=CARTESIAN_POINT('Ctrl Pts',(-242.734131843815,5.23820356294377,
135.451882999115));
#197165=CARTESIAN_POINT('Ctrl Pts',(-243.012579467628,6.74146918027728,
128.909410975699));
#197166=CARTESIAN_POINT('Ctrl Pts',(-243.29102709144,2.04965396001378,124.108305099723));
#197167=CARTESIAN_POINT('Ctrl Pts',(-243.569474715254,-4.52569311833944,
125.460547124147));
#197168=CARTESIAN_POINT('Ctrl Pts',(-243.847922339066,-6.94214931333881,
131.72349268922));
#197169=CARTESIAN_POINT('Ctrl Pts',(-244.12636996288,-2.9791094322281,137.141800782542));
#197170=CARTESIAN_POINT('Ctrl Pts',(-244.404817586691,3.72158647951367,
136.736310965414));
#197171=CARTESIAN_POINT('Ctrl Pts',(-244.683265210505,7.00232622618917,
130.879648570499));
#197172=CARTESIAN_POINT('Ctrl Pts',(-244.961712834317,3.84827025365086,
124.953800224859));
#197173=CARTESIAN_POINT('Ctrl Pts',(-245.240160458131,-2.84215808354001,
124.404331064352));
#197174=CARTESIAN_POINT('Ctrl Pts',(-245.518608081943,-6.92078198909823,
129.736176404423));
#197175=CARTESIAN_POINT('Ctrl Pts',(-245.797055705757,-4.63954534567172,
136.049630852671));
#197176=CARTESIAN_POINT('Ctrl Pts',(-246.075503329569,1.90520681603656,
137.542938200555));
#197177=CARTESIAN_POINT('Ctrl Pts',(-246.353950953382,6.69916698833444,
132.843821947487));
#197178=CARTESIAN_POINT('Ctrl Pts',(-246.632398577195,5.33691997085474,
126.270540365447));
#197179=CARTESIAN_POINT('Ctrl Pts',(-246.910846201008,-0.929695776805409,
123.86361810567));
#197180=CARTESIAN_POINT('Ctrl Pts',(-247.189293824821,-6.34196652374499,
127.834899140205));
#197181=CARTESIAN_POINT('Ctrl Pts',(-247.467741448634,-5.9262798576518,
134.534970206175));
#197182=CARTESIAN_POINT('Ctrl Pts',(-247.746189072447,-0.0646315172428821,
137.806793310625));
#197183=CARTESIAN_POINT('Ctrl Pts',(-248.024636696259,5.85641003008765,
134.643722858007));
#197184=CARTESIAN_POINT('Ctrl Pts',(-248.303084320073,6.39569686130214,
127.952466069697));
#197185=CARTESIAN_POINT('Ctrl Pts',(-248.581531943885,1.05765072414216,
123.881961048084));
#197186=CARTESIAN_POINT('Ctrl Pts',(-248.859979567699,-5.25232475939459,
126.172803052805));
#197187=CARTESIAN_POINT('Ctrl Pts',(-249.138427191511,-6.73567037937639,
132.719820195375));
#197188=CARTESIAN_POINT('Ctrl Pts',(-249.416874815324,-2.02926397650361,
137.506623561341));
#197189=CARTESIAN_POINT('Ctrl Pts',(-249.695322439137,4.54193688572079,
136.134374705723));
#197190=CARTESIAN_POINT('Ctrl Pts',(-249.97377006295,6.93931963591783,129.864103288757));
#197191=CARTESIAN_POINT('Ctrl Pts',(-250.252217686763,2.95980664532115,
124.457882422832));
#197192=CARTESIAN_POINT('Ctrl Pts',(-250.530665310576,-3.73962405773988,
124.883764975191));
#197193=CARTESIAN_POINT('Ctrl Pts',(-250.809112934388,-7.00252294251614,
130.750385685678));
#197194=CARTESIAN_POINT('Ctrl Pts',(-251.087560558202,-3.83044533540895,
136.666606721818));
#197195=CARTESIAN_POINT('Ctrl Pts',(-251.366008182014,2.86162440732935,
137.195709974661));
#197196=CARTESIAN_POINT('Ctrl Pts',(-251.644455805827,6.9240011177651,131.851475403357));
#197197=CARTESIAN_POINT('Ctrl Pts',(-251.92290342964,4.62355905740654,125.54499349784));
#197198=CARTESIAN_POINT('Ctrl Pts',(-252.201351053453,-1.92570790361727,
124.071613041873));
#197199=CARTESIAN_POINT('Ctrl Pts',(-252.479798677266,-6.70534337666252,
128.785298693283));
#197200=CARTESIAN_POINT('Ctrl Pts',(-252.758246301079,-5.3230958619522,
135.354403619622));
#197201=CARTESIAN_POINT('Ctrl Pts',(-253.036693924892,0.950816704398073,
137.74224130304));
#197202=CARTESIAN_POINT('Ctrl Pts',(-253.315141548704,6.35097516523885,
133.754505582129));
#197203=CARTESIAN_POINT('Ctrl Pts',(-253.593589172518,5.91489771943887,
127.055730740027));
#197204=CARTESIAN_POINT('Ctrl Pts',(-253.87203679633,0.0433182135112656,
123.801763664947));
#197205=CARTESIAN_POINT('Ctrl Pts',(-254.150484420143,-5.86806858651122,
126.982841017323));
#197206=CARTESIAN_POINT('Ctrl Pts',(-254.428932043956,-6.38698707931617,
133.675708334441));
#197207=CARTESIAN_POINT('Ctrl Pts',(-254.707379667769,-1.03657636838919,
137.729947101491));
#197208=CARTESIAN_POINT('Ctrl Pts',(-254.985827291582,5.26639719763008,
135.41991073597));
#197209=CARTESIAN_POINT('Ctrl Pts',(-255.264274915395,6.72980937160111,
128.868408326187));
#197210=CARTESIAN_POINT('Ctrl Pts',(-255.542722539208,2.00885483266244,
124.095953322692));
#197211=CARTESIAN_POINT('Ctrl Pts',(-255.821170163021,-4.5581378946222,
125.488193449449));
#197212=CARTESIAN_POINT('Ctrl Pts',(-256.099617786833,-6.93642696247006,
131.765738008466));
#197213=CARTESIAN_POINT('Ctrl Pts',(-256.378065410647,-2.94047400549736,
137.159811411449));
#197214=CARTESIAN_POINT('Ctrl Pts',(-256.656513034459,3.7576223973322,136.713559240208));
#197215=CARTESIAN_POINT('Ctrl Pts',(-256.934960658272,7.0026634652268,130.836998362911));
#197216=CARTESIAN_POINT('Ctrl Pts',(-257.213408282085,3.81256854888166,
124.930527794066));
#197217=CARTESIAN_POINT('Ctrl Pts',(-257.491855905898,-2.88103328591622,
124.421666290213));
#197218=CARTESIAN_POINT('Ctrl Pts',(-257.770303529711,-6.92721451599304,
129.778484277494));
#197219=CARTESIAN_POINT('Ctrl Pts',(-258.048751153524,-4.60741964202412,
136.077475067175));
#197220=CARTESIAN_POINT('Ctrl Pts',(-258.327198777336,1.94598288966397,
137.53178391186));
#197221=CARTESIAN_POINT('Ctrl Pts',(-258.60564640115,6.71185090883407,132.801931226644));
#197222=CARTESIAN_POINT('Ctrl Pts',(-258.884094024962,5.30847971878909,
126.240167716581));
#197223=CARTESIAN_POINT('Ctrl Pts',(-259.162541648776,-0.970525071554103,
123.86553674091));
#197224=CARTESIAN_POINT('Ctrl Pts',(-259.440989272588,-6.36258613651914,
127.881151058581));
#197225=CARTESIAN_POINT('Ctrl Pts',(-259.673028959099,-5.97575359986218,
133.442106215535));
#197226=CARTESIAN_POINT('Ctrl Pts',(-259.858689921174,-2.9628379271774,
136.206922793942));
#197227=CARTESIAN_POINT('Ctrl Pts',(-259.951535008647,-1.00384119663989,
136.721969923993));
#197228=CARTESIAN_POINT('Ctrl Pts',(-259.997972158816,-0.016740685831905,
136.724751058381));
#197229=CARTESIAN_POINT('Ctrl Pts',(210.384788400103,3.2437100417032,135.350446923363));
#197230=CARTESIAN_POINT('Ctrl Pts',(210.338370536501,4.00135710969089,134.809856772425));
#197231=CARTESIAN_POINT('Ctrl Pts',(210.245544735596,5.2274450014198,133.344996311945));
#197232=CARTESIAN_POINT('Ctrl Pts',(210.059903060087,6.03752477204218,129.574087134129));
#197233=CARTESIAN_POINT('Ctrl Pts',(209.827863373576,3.30140998082846,125.08375145776));
#197234=CARTESIAN_POINT('Ctrl Pts',(209.549415749763,-3.03864792542705,
124.935284604053));
#197235=CARTESIAN_POINT('Ctrl Pts',(209.27096812595,-6.57501826603042,130.18815040753));
#197236=CARTESIAN_POINT('Ctrl Pts',(208.992520502138,-4.0751627655632,136.003208990552));
#197237=CARTESIAN_POINT('Ctrl Pts',(208.714072878324,2.17267791003586,137.042921783734));
#197238=CARTESIAN_POINT('Ctrl Pts',(208.435625254512,6.42228832295553,132.348569225854));
#197239=CARTESIAN_POINT('Ctrl Pts',(208.157177630698,4.77100074356668,126.235763887068));
#197240=CARTESIAN_POINT('Ctrl Pts',(207.878730006886,-1.26506482749479,
124.320958291314));
#197241=CARTESIAN_POINT('Ctrl Pts',(207.600282383073,-6.13835327551471,
128.364250828182));
#197242=CARTESIAN_POINT('Ctrl Pts',(207.32183475926,-5.37092434612766,134.649796015418));
#197243=CARTESIAN_POINT('Ctrl Pts',(207.043387135447,0.332190207827403,
137.40162108792));
#197244=CARTESIAN_POINT('Ctrl Pts',(206.764939511634,5.73000189292936,134.090861108297));
#197245=CARTESIAN_POINT('Ctrl Pts',(206.486491887821,5.86224098722307,127.759980958474));
#197246=CARTESIAN_POINT('Ctrl Pts',(206.208044264008,0.607356820266201,
124.226729984437));
#197247=CARTESIAN_POINT('Ctrl Pts',(205.929596640195,-5.20565320191231,
126.738003936844));
#197248=CARTESIAN_POINT('Ctrl Pts',(205.651149016382,-6.23492509722864,
132.986059061584));
#197249=CARTESIAN_POINT('Ctrl Pts',(205.37270139257,-1.53460390898592,137.229240938669));
#197250=CARTESIAN_POINT('Ctrl Pts',(205.094253768756,4.57594250116295,135.568271122458));
#197251=CARTESIAN_POINT('Ctrl Pts',(204.815806144944,6.48142172411287,129.529500574057));
#197252=CARTESIAN_POINT('Ctrl Pts',(204.537358521131,2.43079079302514,124.662263970705));
#197253=CARTESIAN_POINT('Ctrl Pts',(204.258910897318,-3.85361800715474,
125.439314209572));
#197254=CARTESIAN_POINT('Ctrl Pts',(203.980463273505,-6.5967401814699,131.146579956944));
#197255=CARTESIAN_POINT('Ctrl Pts',(203.702015649692,-3.27778036432047,
136.539362872731));
#197256=CARTESIAN_POINT('Ctrl Pts',(203.42356802588,3.05329946149495,136.661958874297));
#197257=CARTESIAN_POINT('Ctrl Pts',(203.145120402066,6.5785462535266,131.40170824395));
#197258=CARTESIAN_POINT('Ctrl Pts',(202.866672778254,4.05843041346184,125.592524323598));
#197259=CARTESIAN_POINT('Ctrl Pts',(202.58822515444,-2.19118470860141,124.572763346851));
#197260=CARTESIAN_POINT('Ctrl Pts',(202.309777530628,-6.42720813017419,
129.279535830482));
#197261=CARTESIAN_POINT('Ctrl Pts',(202.031329906815,-4.75694126595338,
135.387547802118));
#197262=CARTESIAN_POINT('Ctrl Pts',(201.752882283002,1.28472223178851,137.283834652022));
#197263=CARTESIAN_POINT('Ctrl Pts',(201.474434659189,6.14578876089344,133.225801404307));
#197264=CARTESIAN_POINT('Ctrl Pts',(201.195987035376,5.35917565710019,126.94258236746));
#197265=CARTESIAN_POINT('Ctrl Pts',(200.917539411563,-0.352258065224466,
124.208148884143));
#197266=CARTESIAN_POINT('Ctrl Pts',(200.63909178775,-5.73998383440169,127.535311740963));
#197267=CARTESIAN_POINT('Ctrl Pts',(200.360644163938,-5.85294487354697,
133.866570813476));
#197268=CARTESIAN_POINT('Ctrl Pts',(200.082196540124,-0.587335506164227,
137.383808313225));
#197269=CARTESIAN_POINT('Ctrl Pts',(199.803748916312,5.2180064984534,134.854854804556));
#197270=CARTESIAN_POINT('Ctrl Pts',(199.525301292498,6.22825544477889,128.603695015683));
#197271=CARTESIAN_POINT('Ctrl Pts',(199.246853668687,1.51504190454761,124.374839406449));
#197272=CARTESIAN_POINT('Ctrl Pts',(198.968406044873,-4.5904211320519,126.054399690658));
#197273=CARTESIAN_POINT('Ctrl Pts',(198.689958421061,-6.47751140283473,
132.098942018204));
#197274=CARTESIAN_POINT('Ctrl Pts',(198.411510797247,-2.41208513843682,
136.95382728238));
#197275=CARTESIAN_POINT('Ctrl Pts',(198.133063173434,3.86992953127461,136.15765309974));
#197276=CARTESIAN_POINT('Ctrl Pts',(197.854615549622,6.59566801831256,130.442064648858));
#197277=CARTESIAN_POINT('Ctrl Pts',(197.576167925809,3.26030981281707,125.059408494076));
#197278=CARTESIAN_POINT('Ctrl Pts',(197.297720301996,-3.07111383566833,
124.956082684267));
#197279=CARTESIAN_POINT('Ctrl Pts',(197.019272678183,-6.58033390142619,
130.227038590899));
#197280=CARTESIAN_POINT('Ctrl Pts',(196.74082505437,-4.04254857895594,136.028525236289));
#197281=CARTESIAN_POINT('Ctrl Pts',(196.462377430557,2.21014139809766,137.029259811701));
#197282=CARTESIAN_POINT('Ctrl Pts',(196.183929806745,6.43181940170927,132.309616130935));
#197283=CARTESIAN_POINT('Ctrl Pts',(195.905482182931,4.74296958699597,126.206716169203));
#197284=CARTESIAN_POINT('Ctrl Pts',(195.627034559119,-1.30443757122094,
124.328826848098));
#197285=CARTESIAN_POINT('Ctrl Pts',(195.348586935305,-6.15313032680387,
128.401636713722));
#197286=CARTESIAN_POINT('Ctrl Pts',(195.070139311493,-5.34739690918169,
134.682432467391));
#197287=CARTESIAN_POINT('Ctrl Pts',(194.791691687679,0.372333033116476,
137.399469645412));
#197288=CARTESIAN_POINT('Ctrl Pts',(194.513244063867,5.74990710746052,134.055923815831));
#197289=CARTESIAN_POINT('Ctrl Pts',(194.234796440054,5.84359744862664,127.724350254736));
#197290=CARTESIAN_POINT('Ctrl Pts',(193.956348816241,0.567307210110782,
124.223155750211));
#197291=CARTESIAN_POINT('Ctrl Pts',(193.677901192428,-5.23031063999889,
126.769767009054));
#197292=CARTESIAN_POINT('Ctrl Pts',(193.399453568615,-6.22152852682933,
133.023972693263));
#197293=CARTESIAN_POINT('Ctrl Pts',(193.121005944802,-1.49546563606909,
137.238463313985));
#197294=CARTESIAN_POINT('Ctrl Pts',(192.84255832099,4.60485711668079,135.540327880088));
#197295=CARTESIAN_POINT('Ctrl Pts',(192.564110697177,6.47354113897745,129.490069896797));
#197296=CARTESIAN_POINT('Ctrl Pts',(192.285663073364,2.39335710461987,124.64758087922));
#197297=CARTESIAN_POINT('Ctrl Pts',(192.007215449551,-3.88620518688872,
125.462871665772));
#197298=CARTESIAN_POINT('Ctrl Pts',(191.728767825738,-6.59453476332446,
131.18672985278));
#197299=CARTESIAN_POINT('Ctrl Pts',(191.450320201925,-3.24280905319821,
136.559209392401));
#197300=CARTESIAN_POINT('Ctrl Pts',(191.171872578112,3.08889975678785,136.643264047941));
#197301=CARTESIAN_POINT('Ctrl Pts',(190.893424954299,6.58206059142805,131.361651697256));
#197302=CARTESIAN_POINT('Ctrl Pts',(190.614977330486,4.02662929408197,125.567916069518));
#197303=CARTESIAN_POINT('Ctrl Pts',(190.336529706674,-2.22907761274862,
124.586217166899));
#197304=CARTESIAN_POINT('Ctrl Pts',(190.05808208286,-6.43637108995848,129.318688322246));
#197305=CARTESIAN_POINT('Ctrl Pts',(189.779634459048,-4.72895396970476,
135.416419737866));
#197306=CARTESIAN_POINT('Ctrl Pts',(189.501186835235,1.32414082646293,137.275894133543));
#197307=CARTESIAN_POINT('Ctrl Pts',(189.222739211422,6.16041489098677,133.188345380025));
#197308=CARTESIAN_POINT('Ctrl Pts',(188.944291587609,5.33556862369218,126.910031093937));
#197309=CARTESIAN_POINT('Ctrl Pts',(188.665843963796,-0.392404551757433,
124.210415391489));
#197310=CARTESIAN_POINT('Ctrl Pts',(188.387396339983,-5.75977711417006,
127.570313219673));
#197311=CARTESIAN_POINT('Ctrl Pts',(188.10894871617,-5.83419588941534,133.902142614521));
#197312=CARTESIAN_POINT('Ctrl Pts',(187.830501092358,-0.547273658602122,
137.387261689231));
#197313=CARTESIAN_POINT('Ctrl Pts',(187.552053468544,5.24256632866185,134.823016271676));
#197314=CARTESIAN_POINT('Ctrl Pts',(187.273605844732,6.214743973489,128.565822630237));
#197315=CARTESIAN_POINT('Ctrl Pts',(186.995158220918,1.47587551380139,124.365736040492));
#197316=CARTESIAN_POINT('Ctrl Pts',(186.716710597106,-4.61925044254253,
126.082430892781));
#197317=CARTESIAN_POINT('Ctrl Pts',(186.438262973293,-6.46951090511933,
132.138348483055));
#197318=CARTESIAN_POINT('Ctrl Pts',(186.15981534948,-2.37460689906969,136.968396393875));
#197319=CARTESIAN_POINT('Ctrl Pts',(185.881367725667,3.90244484122886,136.133996556155));
#197320=CARTESIAN_POINT('Ctrl Pts',(185.602920101854,6.59334041746713,130.401921658061));
#197321=CARTESIAN_POINT('Ctrl Pts',(185.324472478041,3.22527825263932,125.039668503516));
#197322=CARTESIAN_POINT('Ctrl Pts',(185.046024854228,-3.10665706276191,
124.974885780916));
#197323=CARTESIAN_POINT('Ctrl Pts',(184.767577230416,-6.5837263061198,130.26710564752));
#197324=CARTESIAN_POINT('Ctrl Pts',(184.489129606603,-4.01067270706429,
136.05303658523));
#197325=CARTESIAN_POINT('Ctrl Pts',(184.21068198279,2.247993177529,137.015690720733));
#197326=CARTESIAN_POINT('Ctrl Pts',(183.932234358977,6.44086315254518,132.270435931769));
#197327=CARTESIAN_POINT('Ctrl Pts',(183.653786735164,4.71489454403,126.177929550814));
#197328=CARTESIAN_POINT('Ctrl Pts',(183.375339111351,-1.34383181504516,
124.33688730648));
#197329=CARTESIAN_POINT('Ctrl Pts',(183.096891487538,-6.16764238592767,
128.439137081397));
#197330=CARTESIAN_POINT('Ctrl Pts',(182.818443863726,-5.32369091022383,
134.71491173846));
#197331=CARTESIAN_POINT('Ctrl Pts',(182.539996239912,0.412472435216218,
137.397080956463));
#197332=CARTESIAN_POINT('Ctrl Pts',(182.2615486161,5.76959376309122,134.020862255314));
#197333=CARTESIAN_POINT('Ctrl Pts',(181.983100992287,5.82474028301032,127.688835683913));
#197334=CARTESIAN_POINT('Ctrl Pts',(181.704653368474,0.527235037225083,
124.219824324685));
#197335=CARTESIAN_POINT('Ctrl Pts',(181.426205744661,-5.25477345090652,
126.801680146133));
#197336=CARTESIAN_POINT('Ctrl Pts',(181.147758120848,-6.20790184760947,
133.061803779016));
#197337=CARTESIAN_POINT('Ctrl Pts',(180.869310497035,-1.45627171922457,
137.247447428754));
#197338=CARTESIAN_POINT('Ctrl Pts',(180.590862873222,4.63360097629919,135.5122090613));
#197339=CARTESIAN_POINT('Ctrl Pts',(180.31241524941,6.46542073859599,129.450687965235));
#197340=CARTESIAN_POINT('Ctrl Pts',(180.033967625596,2.35583469548556,124.633125906077));
#197341=CARTESIAN_POINT('Ctrl Pts',(179.755520001784,-3.91864834385308,
125.4866270652));
#197342=CARTESIAN_POINT('Ctrl Pts',(179.477072377971,-6.59208499180493,
131.226865573221));
#197343=CARTESIAN_POINT('Ctrl Pts',(179.198624754158,-3.20771757354326,
136.578842667508));
#197344=CARTESIAN_POINT('Ctrl Pts',(178.920177130345,3.12438558908937,136.62435285703));
#197345=CARTESIAN_POINT('Ctrl Pts',(178.641729506532,6.58533103007041,131.32157450091));
#197346=CARTESIAN_POINT('Ctrl Pts',(178.363281882719,3.99467896572256,125.5435018533));
#197347=CARTESIAN_POINT('Ctrl Pts',(178.084834258906,-2.26688791720775,
124.599901402811));
#197348=CARTESIAN_POINT('Ctrl Pts',(177.806386635093,-6.44529554785546,
129.357895865998));
#197349=CARTESIAN_POINT('Ctrl Pts',(177.527939011281,-4.70079144021631,
135.445120772143));
#197350=CARTESIAN_POINT('Ctrl Pts',(177.249491387467,1.36351035455298,137.26771380997));
#197351=CARTESIAN_POINT('Ctrl Pts',(176.971043763655,6.17481274467203,133.150801016333));
#197352=CARTESIAN_POINT('Ctrl Pts',(176.692596139842,5.31176387881016,126.877624126216));
#197353=CARTESIAN_POINT('Ctrl Pts',(176.414148516029,-0.432536497586617,
124.212926239906));
#197354=CARTESIAN_POINT('Ctrl Pts',(176.135700892216,-5.77935696328393,
127.605434537195));
#197355=CARTESIAN_POINT('Ctrl Pts',(175.857253268403,-5.81523071700703,
133.937599626117));
#197356=CARTESIAN_POINT('Ctrl Pts',(175.57880564459,-0.50719153161477,137.390471133416));
#197357=CARTESIAN_POINT('Ctrl Pts',(175.300358020777,5.2669318936477,134.791028826034));
#197358=CARTESIAN_POINT('Ctrl Pts',(175.021910396965,6.20100221257536,128.528033194638));
#197359=CARTESIAN_POINT('Ctrl Pts',(174.743462773151,1.43665443394553,124.356871260137));
#197360=CARTESIAN_POINT('Ctrl Pts',(174.465015149339,-4.64790858500931,
126.110637067746));
#197361=CARTESIAN_POINT('Ctrl Pts',(174.186567525525,-6.46127067729819,
132.177705516496));
#197362=CARTESIAN_POINT('Ctrl Pts',(173.908119901713,-2.33704066777073,
136.982737094758));
#197363=CARTESIAN_POINT('Ctrl Pts',(173.6296722779,3.93481554465429,136.11014252095));
#197364=CARTESIAN_POINT('Ctrl Pts',(173.351224654087,6.59076849796787,130.361793579788));
#197365=CARTESIAN_POINT('Ctrl Pts',(173.072777030274,3.1901271785899,125.020142125741));
#197366=CARTESIAN_POINT('Ctrl Pts',(172.794329406461,-3.14208517153551,
124.993904890899));
#197367=CARTESIAN_POINT('Ctrl Pts',(172.515881782648,-6.58687474841394,
130.30719261232));
#197368=CARTESIAN_POINT('Ctrl Pts',(172.237434158836,-3.97864821822065,
136.077353442554));
#197369=CARTESIAN_POINT('Ctrl Pts',(171.958986535022,2.28576165674636,137.001891466644));
#197370=CARTESIAN_POINT('Ctrl Pts',(171.68053891121,6.44966823482829,132.231201406644));
#197371=CARTESIAN_POINT('Ctrl Pts',(171.402091287397,4.68664478891289,126.149314366529));
#197372=CARTESIAN_POINT('Ctrl Pts',(171.123643663584,-1.38317626268716,
124.345187419464));
#197373=CARTESIAN_POINT('Ctrl Pts',(170.845196039771,-6.18192590079466,
128.476725093301));
#197374=CARTESIAN_POINT('Ctrl Pts',(170.566748415958,-5.29978763994156,
134.747246102621));
#197375=CARTESIAN_POINT('Ctrl Pts',(170.288300792145,0.452596552998033,
137.394447971839));
#197376=CARTESIAN_POINT('Ctrl Pts',(170.009853168332,5.78906662430322,133.985681506144));
#197377=CARTESIAN_POINT('Ctrl Pts',(169.73140554452,5.80566727950083,127.653436560012));
#197378=CARTESIAN_POINT('Ctrl Pts',(169.452957920706,0.487143327451347,
124.216736891574));
#197379=CARTESIAN_POINT('Ctrl Pts',(169.174510296894,-5.27904154425138,
126.833741604011));
#197380=CARTESIAN_POINT('Ctrl Pts',(168.896062673081,-6.19404513230377,
133.099551214382));
#197381=CARTESIAN_POINT('Ctrl Pts',(168.617615049268,-1.41702383969606,
137.256192792574));
#197382=CARTESIAN_POINT('Ctrl Pts',(168.339167425455,4.66217313612931,135.483915791456));
#197383=CARTESIAN_POINT('Ctrl Pts',(168.060719801642,6.45706075967145,129.411356194513));
#197384=CARTESIAN_POINT('Ctrl Pts',(167.782272177829,2.3182249900303,124.618899610305));
#197385=CARTESIAN_POINT('Ctrl Pts',(167.503824554016,-3.95094629386185,
125.510579515201));
#197386=CARTESIAN_POINT('Ctrl Pts',(167.225376930203,-6.58939094815179,
131.266985637585));
#197387=CARTESIAN_POINT('Ctrl Pts',(166.946929306391,-3.1725072307341,136.59826196706));
#197388=CARTESIAN_POINT('Ctrl Pts',(166.668481682578,3.15975564613386,136.605226004165));
#197389=CARTESIAN_POINT('Ctrl Pts',(166.390034058765,6.58835744684964,131.281478139015));
#197390=CARTESIAN_POINT('Ctrl Pts',(166.111586434952,3.96258061306513,125.519282580138));
#197391=CARTESIAN_POINT('Ctrl Pts',(165.833138811139,-2.30461422130139,
124.613815547242));
#197392=CARTESIAN_POINT('Ctrl Pts',(165.554691187326,-6.45398117295568,
129.397157009033));
#197393=CARTESIAN_POINT('Ctrl Pts',(165.276243563513,-4.67245472117232,
135.473649841348));
#197394=CARTESIAN_POINT('Ctrl Pts',(164.9977959397,1.40282935726546,137.259293984466));
#197395=CARTESIAN_POINT('Ctrl Pts',(164.719348315888,6.18898178840028,133.11316970443));
#197396=CARTESIAN_POINT('Ctrl Pts',(164.440900692075,5.2877623045642,126.845362665158));
#197397=CARTESIAN_POINT('Ctrl Pts',(164.162453068262,-0.472652415616787,
124.215681336348));
#197398=CARTESIAN_POINT('Ctrl Pts',(163.884005444449,-5.79872265620017,
127.640674392099));
#197399=CARTESIAN_POINT('Ctrl Pts',(163.605557820636,-5.79605005908598,
133.97294053439));
#197400=CARTESIAN_POINT('Ctrl Pts',(163.327110196823,-0.467090610458611,
137.393436526853));
#197401=CARTESIAN_POINT('Ctrl Pts',(163.04866257301,5.29110229053537,134.758893652935));
#197402=CARTESIAN_POINT('Ctrl Pts',(162.770214949197,6.18703067124424,128.49032810919));
#197403=CARTESIAN_POINT('Ctrl Pts',(162.491767325384,1.39738011833125,124.34824539387));
#197404=CARTESIAN_POINT('Ctrl Pts',(162.213319701571,-4.67639449751423,
126.139017170363));
#197405=CARTESIAN_POINT('Ctrl Pts',(161.934872077759,-6.45279102471594,
132.217011660137));
#197406=CARTESIAN_POINT('Ctrl Pts',(161.656424453946,-2.29938783657033,
136.996848853628));
#197407=CARTESIAN_POINT('Ctrl Pts',(161.377976830133,3.96704044204275,136.086091878046));
#197408=CARTESIAN_POINT('Ctrl Pts',(161.09952920632,6.58795235511813,130.321681900999));
#197409=CARTESIAN_POINT('Ctrl Pts',(160.821081582507,3.15485789320466,125.000830084311));
#197410=CARTESIAN_POINT('Ctrl Pts',(160.542633958694,-3.17739684918762,
125.013139309456));
#197411=CARTESIAN_POINT('Ctrl Pts',(160.264186334881,-6.58977911164196,
130.347297999864));
#197412=CARTESIAN_POINT('Ctrl Pts',(159.985738711068,-3.94647629910411,
136.10147490719));
#197413=CARTESIAN_POINT('Ctrl Pts',(159.707291087255,2.32344543622502,136.98786256077));
#197414=CARTESIAN_POINT('Ctrl Pts',(159.428843463442,6.45823432228318,132.191914009409));
#197415=CARTESIAN_POINT('Ctrl Pts',(159.15039583963,4.65822136844951,126.120871676696));
#197416=CARTESIAN_POINT('Ctrl Pts',(158.871948215817,-1.42246945622416,
124.353726879487));
#197417=CARTESIAN_POINT('Ctrl Pts',(158.593500592004,-6.19598034212407,
128.514399356595));
#197418=CARTESIAN_POINT('Ctrl Pts',(158.315052968191,-5.2756879840792,134.779434361708));
#197419=CARTESIAN_POINT('Ctrl Pts',(158.036605344378,0.49270389964821,137.391570789103));
#197420=CARTESIAN_POINT('Ctrl Pts',(157.758157720565,5.80832496952254,133.950382871961));
#197421=CARTESIAN_POINT('Ctrl Pts',(157.479710096752,5.78637914485521,127.618154194761));
#197422=CARTESIAN_POINT('Ctrl Pts',(157.201262472939,0.447033566402335,
124.213893565282));
#197423=CARTESIAN_POINT('Ctrl Pts',(156.922814849126,-5.3031140207705,126.865950194636));
#197424=CARTESIAN_POINT('Ctrl Pts',(156.644367225313,-6.17995889437779,
133.137213600617));
#197425=CARTESIAN_POINT('Ctrl Pts',(156.365919601501,-1.37772345182797,
137.264699081378));
#197426=CARTESIAN_POINT('Ctrl Pts',(156.087471977688,4.69057253741941,135.455449118975));
#197427=CARTESIAN_POINT('Ctrl Pts',(155.809024353875,6.44846151198586,129.372076042081));
#197428=CARTESIAN_POINT('Ctrl Pts',(155.530576730062,2.28052938189546,124.604902519066));
#197429=CARTESIAN_POINT('Ctrl Pts',(155.252129106249,-3.98309784010292,
125.534728128207));
#197430=CARTESIAN_POINT('Ctrl Pts',(154.973681482436,-6.58645273219382,
131.307088559209));
#197431=CARTESIAN_POINT('Ctrl Pts',(154.695233858623,-3.13717932950269,
136.617466571466));
#197432=CARTESIAN_POINT('Ctrl Pts',(154.41678623481,3.19500861727094,136.585884198101));
#197433=CARTESIAN_POINT('Ctrl Pts',(154.138338610998,6.59113972962085,131.241364097354));
#197434=CARTESIAN_POINT('Ctrl Pts',(153.859890987185,3.93033542552574,125.495259147487));
#197435=CARTESIAN_POINT('Ctrl Pts',(153.581443363372,-2.3422551270676,124.627959084596));
#197436=CARTESIAN_POINT('Ctrl Pts',(153.302995739559,-6.46242764341012,
129.436470296516));
#197437=CARTESIAN_POINT('Ctrl Pts',(153.024548115746,-4.64394486260028,
135.502005888322));
#197438=CARTESIAN_POINT('Ctrl Pts',(152.746100491933,1.44209637762021,137.250634969033));
#197439=CARTESIAN_POINT('Ctrl Pts',(152.46765286812,6.20292149713234,133.075452838754));
#197440=CARTESIAN_POINT('Ctrl Pts',(152.189205244307,5.26356479034146,126.813247906226));
#197441=CARTESIAN_POINT('Ctrl Pts',(151.910757620494,-0.512750819337957,
124.218680578724));
#197442=CARTESIAN_POINT('Ctrl Pts',(151.632309996682,-5.8178734753159,127.676031478561));
#197443=CARTESIAN_POINT('Ctrl Pts',(151.353862372869,-5.77665462639848,
134.008164029768));
#197444=CARTESIAN_POINT('Ctrl Pts',(151.075414749056,-0.4269723810881,137.39615775966));
#197445=CARTESIAN_POINT('Ctrl Pts',(150.796967125243,5.31507662368183,134.72661194316));
#197446=CARTESIAN_POINT('Ctrl Pts',(150.51851950143,6.17282986721635,128.452708771068));
#197447=CARTESIAN_POINT('Ctrl Pts',(150.240071877617,1.35805402228283,124.339858761329));
#197448=CARTESIAN_POINT('Ctrl Pts',(149.961624253804,-4.70470712450132,
126.167570148998));
#197449=CARTESIAN_POINT('Ctrl Pts',(149.683176629991,-6.44407226158927,
132.256265457474));
#197450=CARTESIAN_POINT('Ctrl Pts',(149.404729006178,-2.26164980070799,
137.010731147569));
#197451=CARTESIAN_POINT('Ctrl Pts',(149.126281382365,3.99911833928874,136.061845518646));
#197452=CARTESIAN_POINT('Ctrl Pts',(148.847833758553,6.58489209327119,130.281588108047));
#197453=CARTESIAN_POINT('Ctrl Pts',(148.56938613474,3.11947170339994,124.981733094838));
#197454=CARTESIAN_POINT('Ctrl Pts',(148.290938510927,-3.21259078723097,
125.032588323847));
#197455=CARTESIAN_POINT('Ctrl Pts',(148.012490887114,-6.59243928818165,
130.387420324031));
#197456=CARTESIAN_POINT('Ctrl Pts',(147.734043263301,-3.91415814185689,
136.125400085308));
#197457=CARTESIAN_POINT('Ctrl Pts',(147.455595639488,2.36104311957866,136.973604522958));
#197458=CARTESIAN_POINT('Ctrl Pts',(147.177148015675,6.46656109749016,132.152575195872));
#197459=CARTESIAN_POINT('Ctrl Pts',(146.898700391862,4.6296253358803,126.092602535266));
#197460=CARTESIAN_POINT('Ctrl Pts',(146.62025276805,-1.46170993963237,124.362505370115));
#197461=CARTESIAN_POINT('Ctrl Pts',(146.341805144237,-6.20980518912327,
128.552158475246));
#197462=CARTESIAN_POINT('Ctrl Pts',(146.063357520424,-5.2513928356585,134.811475322978));
#197463=CARTESIAN_POINT('Ctrl Pts',(145.784909896611,0.532792988974217,
137.388449514872));
#197464=CARTESIAN_POINT('Ctrl Pts',(145.506462272798,5.82736808512415,133.914967660766));
#197465=CARTESIAN_POINT('Ctrl Pts',(145.228014648985,5.76687659380242,127.582989895561));
#197466=CARTESIAN_POINT('Ctrl Pts',(144.949567025172,0.406907240360106,
124.211294451169));
#197467=CARTESIAN_POINT('Ctrl Pts',(144.671119401359,-5.32698998844935,
126.898304724507));
#197468=CARTESIAN_POINT('Ctrl Pts',(144.392671777546,-6.16564365580234,
133.174789542127));
#197469=CARTESIAN_POINT('Ctrl Pts',(144.114224153734,-1.33837201191069,
137.272965979966));
#197470=CARTESIAN_POINT('Ctrl Pts',(143.83577652992,4.71879812781917,135.426810098699));
#197471=CARTESIAN_POINT('Ctrl Pts',(143.557328906108,6.43962331418753,129.332848963481));
#197472=CARTESIAN_POINT('Ctrl Pts',(143.278881282295,2.24274926790569,124.591135151027));
#197473=CARTESIAN_POINT('Ctrl Pts',(143.000433658482,-4.01510179118866,
125.559072009383));
#197474=CARTESIAN_POINT('Ctrl Pts',(142.721986034669,-6.58327045280769,
131.347172852065));
#197475=CARTESIAN_POINT('Ctrl Pts',(142.443538410856,-3.10173517893752,
136.636455769093));
#197476=CARTESIAN_POINT('Ctrl Pts',(142.165090787043,3.23014319618891,136.566328155556));
#197477=CARTESIAN_POINT('Ctrl Pts',(141.886643163231,6.5936777752854,131.201233862367));
#197478=CARTESIAN_POINT('Ctrl Pts',(141.608195539417,3.89794459796173,125.471432445543));
#197479=CARTESIAN_POINT('Ctrl Pts',(141.329747915605,-2.37980923970876,
124.642331490782));
#197480=CARTESIAN_POINT('Ctrl Pts',(141.051300291792,-6.47063464623165,
129.475834271677));
#197481=CARTESIAN_POINT('Ctrl Pts',(140.772852667979,-4.61526292094352,
135.530187862324));
#197482=CARTESIAN_POINT('Ctrl Pts',(140.494405044166,1.48130996056343,137.241737084533));
#197483=CARTESIAN_POINT('Ctrl Pts',(140.215957420353,6.21663135432719,133.037651816923));
#197484=CARTESIAN_POINT('Ctrl Pts',(139.93750979654,5.23917223278974,126.781281039444));
#197485=CARTESIAN_POINT('Ctrl Pts',(139.659062172727,-0.552830222889001,
124.221923855894));
#197486=CARTESIAN_POINT('Ctrl Pts',(139.380614548914,-5.83680871099059,
127.711504486408));
#197487=CARTESIAN_POINT('Ctrl Pts',(139.102166925101,-5.75704513764935,
134.043268807033));
#197488=CARTESIAN_POINT('Ctrl Pts',(138.823719301288,-0.386838330098996,
137.398634730999));
#197489=CARTESIAN_POINT('Ctrl Pts',(138.545271677476,5.33885400470937,134.694184892919));
#197490=CARTESIAN_POINT('Ctrl Pts',(138.266824053663,6.15840032670771,128.41517657427));
#197491=CARTESIAN_POINT('Ctrl Pts',(137.98837642985,1.31867760304303,124.331711673279));
#197492=CARTESIAN_POINT('Ctrl Pts',(137.709928806037,-4.7328454168358,126.196294945608));
#197493=CARTESIAN_POINT('Ctrl Pts',(137.431481182224,-6.43511471099507,
132.295465453942));
#197494=CARTESIAN_POINT('Ctrl Pts',(137.153033558411,-2.22382795858067,
137.024383462168));
#197495=CARTESIAN_POINT('Ctrl Pts',(136.874585934598,4.03104804773404,136.037404341212));
#197496=CARTESIAN_POINT('Ctrl Pts',(136.596138310785,6.5815878258261,130.241513686623));
#197497=CARTESIAN_POINT('Ctrl Pts',(136.317690686972,3.08396992042408,124.96285186497));
#197498=CARTESIAN_POINT('Ctrl Pts',(136.03924306316,-3.24766568154122,125.052251213384));
#197499=CARTESIAN_POINT('Ctrl Pts',(135.760795439346,-6.5948551794591,130.427558098075));
#197500=CARTESIAN_POINT('Ctrl Pts',(135.482347815534,-3.88169494404043,
136.149128090351));
#197501=CARTESIAN_POINT('Ctrl Pts',(135.203900191721,2.3985533136112,136.959117881544));
#197502=CARTESIAN_POINT('Ctrl Pts',(134.925452567908,6.47464825189767,132.113186423748));
#197503=CARTESIAN_POINT('Ctrl Pts',(134.647004944095,4.60085775084163,126.064507989766));
#197504=CARTESIAN_POINT('Ctrl Pts',(134.368557320282,-1.50089625884118,
124.371522566057));
#197505=CARTESIAN_POINT('Ctrl Pts',(134.090109696469,-6.22339992950755,
128.590001050074));
#197506=CARTESIAN_POINT('Ctrl Pts',(133.811662072656,-5.22690309494509,
134.843367799137));
#197507=CARTESIAN_POINT('Ctrl Pts',(133.533214448844,0.572862335460145,
137.385084264805));
#197508=CARTESIAN_POINT('Ctrl Pts',(133.25476682503,5.84619526545829,133.879437184883));
#197509=CARTESIAN_POINT('Ctrl Pts',(132.976319201218,5.7471603490167,127.547944965438));
#197510=CARTESIAN_POINT('Ctrl Pts',(132.697871577405,0.366765836220533,
124.208939645549));
#197511=CARTESIAN_POINT('Ctrl Pts',(132.419423953592,-5.35066856255522,
126.930803994717));
#197512=CARTESIAN_POINT('Ctrl Pts',(132.140976329779,-6.15109994703373,
133.212277646521));
#197513=CARTESIAN_POINT('Ctrl Pts',(131.862528705966,-1.29897097812634,
137.280993182001));
#197514=CARTESIAN_POINT('Ctrl Pts',(131.584081082153,4.74684886141891,135.397999791857));
#197515=CARTESIAN_POINT('Ctrl Pts',(131.30563345834,6.43054649377913,129.293676412286));
#197516=CARTESIAN_POINT('Ctrl Pts',(131.027185834528,2.20488604801711,124.577598016342));
#197517=CARTESIAN_POINT('Ctrl Pts',(130.748738210715,-4.04695696120101,
125.583610256657));
#197518=CARTESIAN_POINT('Ctrl Pts',(130.470290586902,-6.57984422791396,
131.387237030814));
#197519=CARTESIAN_POINT('Ctrl Pts',(130.191842963089,-3.06617609243459,
136.65522885629));
#197520=CARTESIAN_POINT('Ctrl Pts',(129.913395339276,3.26515808096253,136.546558601182));
#197521=CARTESIAN_POINT('Ctrl Pts',(129.634947715463,6.59597148979528,131.161088921098));
#197522=CARTESIAN_POINT('Ctrl Pts',(129.35650009165,3.86540933062731,125.447803357213));
#197523=CARTESIAN_POINT('Ctrl Pts',(129.078052467837,-2.41727516764341,
124.656932233223));
#197524=CARTESIAN_POINT('Ctrl Pts',(128.799604844024,-6.47860187730669,
129.515247475871));
#197525=CARTESIAN_POINT('Ctrl Pts',(128.521157220212,-4.58640995902212,
135.558194719059));
#197526=CARTESIAN_POINT('Ctrl Pts',(128.242709596398,1.52046865302106,137.232600660681));
#197527=CARTESIAN_POINT('Ctrl Pts',(127.964261972586,6.23011085196111,132.999768039666));
#197528=CARTESIAN_POINT('Ctrl Pts',(127.685814348773,5.2145855357842,126.749463249355));
#197529=CARTESIAN_POINT('Ctrl Pts',(127.40736672496,-0.592889141112855,
124.225411047681));
#197530=CARTESIAN_POINT('Ctrl Pts',(127.128919101147,-5.85552766157182,
127.747092101177));
#197531=CARTESIAN_POINT('Ctrl Pts',(126.850471477334,-5.7372223194756,134.078253565364));
#197532=CARTESIAN_POINT('Ctrl Pts',(126.572023853521,-0.346689944673359,
137.400867349086));
#197533=CARTESIAN_POINT('Ctrl Pts',(126.293576229708,5.36243355253846,134.66161370381));
#197534=CARTESIAN_POINT('Ctrl Pts',(126.015128605896,6.14374258441013,128.377732909565));
#197535=CARTESIAN_POINT('Ctrl Pts',(125.736680982083,1.27925231971985,124.323804431618));
#197536=CARTESIAN_POINT('Ctrl Pts',(125.45823335827,-4.76080833184274,126.225190495787));
#197537=CARTESIAN_POINT('Ctrl Pts',(125.179785734457,-6.42591870485886,
132.334610196974));
#197538=CARTESIAN_POINT('Ctrl Pts',(124.901338110644,-2.1859237116904,137.037805291532));
#197539=CARTESIAN_POINT('Ctrl Pts',(124.622890486831,4.06282838421153,136.012769251418));
#197540=CARTESIAN_POINT('Ctrl Pts',(124.344442863018,6.5780396752237,130.201460121699));
#197541=CARTESIAN_POINT('Ctrl Pts',(124.065995239205,3.04835385980878,124.944187094356));
#197542=CARTESIAN_POINT('Ctrl Pts',(123.787547615392,-3.28262023240536,
125.07212724945));
#197543=CARTESIAN_POINT('Ctrl Pts',(123.509099991579,-6.59702669595264,
130.467709834674));
#197544=CARTESIAN_POINT('Ctrl Pts',(123.230652367767,-3.84908790859021,
136.17265804307));
#197545=CARTESIAN_POINT('Ctrl Pts',(122.952204743954,2.43597462836867,136.944403173336));
#197546=CARTESIAN_POINT('Ctrl Pts',(122.673757120141,6.48249548583303,132.073749152604));
#197547=CARTESIAN_POINT('Ctrl Pts',(122.395309496328,4.57191967932717,126.036589081248));
#197548=CARTESIAN_POINT('Ctrl Pts',(122.116861872515,-1.54002696178715,
124.380778133181));
#197549=CARTESIAN_POINT('Ctrl Pts',(121.838414248702,-6.23676405951882,
128.627925678811));
#197550=CARTESIAN_POINT('Ctrl Pts',(121.559966624889,-5.20221966941523,
134.8751106084));
#197551=CARTESIAN_POINT('Ctrl Pts',(121.281519001076,0.612910454321425,
137.381475163605));
#197552=CARTESIAN_POINT('Ctrl Pts',(121.003071377263,5.86480581287692,133.843792760907));
#197553=CARTESIAN_POINT('Ctrl Pts',(120.724623753451,5.72723114109079,127.513020702994));
#197554=CARTESIAN_POINT('Ctrl Pts',(120.446176129638,0.326610841437887,
124.206829235678));
#197555=CARTESIAN_POINT('Ctrl Pts',(120.167728505825,-5.3741488656698,126.963446800991));
#197556=CARTESIAN_POINT('Ctrl Pts',(119.889280882012,-6.13632830699453,
133.249676524665));
#197557=CARTESIAN_POINT('Ctrl Pts',(119.610833258199,-1.25952181049465,
137.288780390037));
#197558=CARTESIAN_POINT('Ctrl Pts',(119.332385634386,4.77472369878856,135.369019266025));
#197559=CARTESIAN_POINT('Ctrl Pts',(119.053938010573,6.42123138710552,129.254559840052));
#197560=CARTESIAN_POINT('Ctrl Pts',(118.77549038676,2.16694112526505,124.564291616636));
#197561=CARTESIAN_POINT('Ctrl Pts',(118.497042762948,-4.07866216973492,
125.608341960757));
#197562=CARTESIAN_POINT('Ctrl Pts',(118.218595139134,-6.57617418447253,
131.427279610862));
#197563=CARTESIAN_POINT('Ctrl Pts',(117.940147515322,-3.03050338764912,
136.673785137412));
#197564=CARTESIAN_POINT('Ctrl Pts',(117.661699891509,3.30005197410286,136.526576267552));
#197565=CARTESIAN_POINT('Ctrl Pts',(117.383252267696,6.59802078815589,131.120930761129));
#197566=CARTESIAN_POINT('Ctrl Pts',(117.104804643883,3.83273082912851,125.424372758082));
#197567=CARTESIAN_POINT('Ctrl Pts',(116.82635702007,-2.45465152255762,124.671760770883));
#197568=CARTESIAN_POINT('Ctrl Pts',(116.547909396257,-6.48632904140672,
129.554708448625));
#197569=CARTESIAN_POINT('Ctrl Pts',(116.269461772444,-4.55738704599302,
135.586025420722));
#197570=CARTESIAN_POINT('Ctrl Pts',(115.991014148631,1.55957100395386,137.223226036031));
#197571=CARTESIAN_POINT('Ctrl Pts',(115.712566524818,6.24335949054626,132.961802910777));
#197572=CARTESIAN_POINT('Ctrl Pts',(115.434118901006,5.18980561039392,126.717795714978));
#197573=CARTESIAN_POINT('Ctrl Pts',(115.155671277193,-0.632926089611396,
124.229142024863));
#197574=CARTESIAN_POINT('Ctrl Pts',(114.87722365338,-5.87402963342224,127.782793004156));
#197575=CARTESIAN_POINT('Ctrl Pts',(114.598776029567,-5.71718690641897,
134.113117008387));
#197576=CARTESIAN_POINT('Ctrl Pts',(114.320328405754,-0.306528712524212,
137.40285553119));
#197577=CARTESIAN_POINT('Ctrl Pts',(114.041880781941,5.38581439342023,134.628899582769));
#197578=CARTESIAN_POINT('Ctrl Pts',(113.763433158128,6.12885718347172,128.340379164441));
#197579=CARTESIAN_POINT('Ctrl Pts',(113.484985534315,1.23977963323159,124.316137329349));
#197580=CARTESIAN_POINT('Ctrl Pts',(113.206537910502,-4.78859483334625,
126.254255728798));
#197581=CARTESIAN_POINT('Ctrl Pts',(112.92809028669,-6.41648458394181,132.373698236044));
#197582=CARTESIAN_POINT('Ctrl Pts',(112.649642662877,-2.14793846459313,
137.050996138312));
#197583=CARTESIAN_POINT('Ctrl Pts',(112.371195039064,4.09445817108915,135.987941162125));
#197584=CARTESIAN_POINT('Ctrl Pts',(112.092747415251,6.57424777294209,130.161428897475));
#197585=CARTESIAN_POINT('Ctrl Pts',(111.814299791438,3.01262484132005,124.925739474628));
#197586=CARTESIAN_POINT('Ctrl Pts',(111.535852167625,-3.31745314456969,
125.092215695531));
#197587=CARTESIAN_POINT('Ctrl Pts',(111.257404543812,-6.59895375719588,
130.507874045991));
#197588=CARTESIAN_POINT('Ctrl Pts',(110.978956919999,-3.816338243772,136.195989071554));
#197589=CARTESIAN_POINT('Ctrl Pts',(110.700509296186,2.47330567719032,136.929460943594));
#197590=CARTESIAN_POINT('Ctrl Pts',(110.422061672374,6.49010250851429,132.0342648438));
#197591=CARTESIAN_POINT('Ctrl Pts',(110.143614048561,4.54281219364771,126.008846844259));
#197592=CARTESIAN_POINT('Ctrl Pts',(109.865166424748,-1.57910059846782,
124.390271728514));
#197593=CARTESIAN_POINT('Ctrl Pts',(109.586718800935,-6.24989708394428,
128.665930956147));
#197594=CARTESIAN_POINT('Ctrl Pts',(109.308271177122,-5.17734347372243,
134.906702574525));
#197595=CARTESIAN_POINT('Ctrl Pts',(109.029823553309,0.652935861560398,
137.377622345005));
#197596=CARTESIAN_POINT('Ctrl Pts',(108.751375929496,5.88319903775945,133.808035709655));
#197597=CARTESIAN_POINT('Ctrl Pts',(108.472928305683,5.70708970850866,127.478218402361));
#197598=CARTESIAN_POINT('Ctrl Pts',(108.19448068187,0.286443743970404,124.204963299759));
#197599=CARTESIAN_POINT('Ctrl Pts',(107.916033058058,-5.39743002772183,
126.996231933739));
#197600=CARTESIAN_POINT('Ctrl Pts',(107.637585434244,-6.12132928305326,
133.286984790727));
#197601=CARTESIAN_POINT('Ctrl Pts',(107.359137810432,-1.22002597081922,
137.296327315513));
#197602=CARTESIAN_POINT('Ctrl Pts',(107.080690186619,4.80242160701559,135.339869595089));
#197603=CARTESIAN_POINT('Ctrl Pts',(106.802242562806,6.41167833934146,129.215500696253));
#197604=CARTESIAN_POINT('Ctrl Pts',(106.523794938993,2.12891590571267,124.551216444981));
#197605=CARTESIAN_POINT('Ctrl Pts',(106.24534731518,-4.11021624194206,125.633266205238));
#197606=CARTESIAN_POINT('Ctrl Pts',(105.966899691367,-6.57226045847839,
131.467299108419));
#197607=CARTESIAN_POINT('Ctrl Pts',(105.688452067554,-2.99471838644612,
136.692123924851));
#197608=CARTESIAN_POINT('Ctrl Pts',(105.410004443742,3.33482358260376,136.506381895117));
#197609=CARTESIAN_POINT('Ctrl Pts',(105.131556819929,6.59982559442975,131.080760870538));
#197610=CARTESIAN_POINT('Ctrl Pts',(104.853109196116,3.79991030437941,125.401141516381));
#197611=CARTESIAN_POINT('Ctrl Pts',(104.574661572303,-2.49193691945696,
124.686816554284));
#197612=CARTESIAN_POINT('Ctrl Pts',(104.29621394849,-6.49381585219884,129.594215727701));
#197613=CARTESIAN_POINT('Ctrl Pts',(104.017766324677,-4.52819525731082,
135.613678936038));
#197614=CARTESIAN_POINT('Ctrl Pts',(103.739318700864,1.59861556440955,137.213613557961));
#197615=CARTESIAN_POINT('Ctrl Pts',(103.460871077051,6.25637677914949,132.923757837073));
#197616=CARTESIAN_POINT('Ctrl Pts',(103.182423453238,5.16483337484823,126.686279609768));
#197617=CARTESIAN_POINT('Ctrl Pts',(102.903975829425,-0.672939584800916,
124.233116649188));
#197618=CARTESIAN_POINT('Ctrl Pts',(102.625528205613,-5.89231394094447,
127.818605872432));
#197619=CARTESIAN_POINT('Ctrl Pts',(102.347080581799,-5.69693964089892,
134.147857844226));
#197620=CARTESIAN_POINT('Ctrl Pts',(102.068632957987,-0.266356121840884,
137.40459920364));
#197621=CARTESIAN_POINT('Ctrl Pts',(101.790185334174,5.40899566096888,134.59604374203));
#197622=CARTESIAN_POINT('Ctrl Pts',(101.511737710361,6.11374467547657,128.303116723058));
#197623=CARTESIAN_POINT('Ctrl Pts',(101.233290086548,1.20026100625305,124.308710650579));
#197624=CARTESIAN_POINT('Ctrl Pts',(100.954842462735,-4.81620389170723,
126.28348956762));
#197625=CARTESIAN_POINT('Ctrl Pts',(100.676394838922,-6.40681269782886,
132.412728122731));
#197626=CARTESIAN_POINT('Ctrl Pts',(100.397947215109,-2.10987362484612,
137.063955513716));
#197627=CARTESIAN_POINT('Ctrl Pts',(100.119499591297,4.12593623631335,135.962920993349));
#197628=CARTESIAN_POINT('Ctrl Pts',(99.8410519674839,6.5702122594916,130.121421497322));
#197629=CARTESIAN_POINT('Ctrl Pts',(99.5626043436712,2.97678418891005,124.907509689368));
#197630=CARTESIAN_POINT('Ctrl Pts',(99.2841567198582,-3.35216312728773,
125.112515807244));
#197631=CARTESIAN_POINT('Ctrl Pts',(99.0057090960455,-6.6006362917809,130.548049243728));
#197632=CARTESIAN_POINT('Ctrl Pts',(98.7272614722323,-3.78344716313679,
136.219120311263));
#197633=CARTESIAN_POINT('Ctrl Pts',(98.4488138484198,2.51054507676055,136.914291746006));
#197634=CARTESIAN_POINT('Ctrl Pts',(98.1703662246066,6.49746903806041,131.994734960442));
#197635=CARTESIAN_POINT('Ctrl Pts',(97.8919186007939,4.51353637239165,125.981282306795));
#197636=CARTESIAN_POINT('Ctrl Pts',(97.6134709769809,-1.61811572099509,
124.400003000271));
#197637=CARTESIAN_POINT('Ctrl Pts',(97.335023353168,-6.26279851613479,128.704015473778));
#197638=CARTESIAN_POINT('Ctrl Pts',(97.0565757293552,-5.15227542966332,
134.938142526861));
#197639=CARTESIAN_POINT('Ctrl Pts',(96.7781281055422,0.692937074020952,
137.373525951775));
#197640=CARTESIAN_POINT('Ctrl Pts',(96.4996804817294,5.90137425853808,133.772167356118));
#197641=CARTESIAN_POINT('Ctrl Pts',(96.2212328579164,5.6867367976186,127.443539353151));
#197642=CARTESIAN_POINT('Ctrl Pts',(95.9427852341037,0.246266032224636,
124.203341906934));
#197643=CARTESIAN_POINT('Ctrl Pts',(95.6643376102905,-5.42051118601915,
127.029158178097));
#197644=CARTESIAN_POINT('Ctrl Pts',(95.3858899864779,-6.10610343100435,
133.324201062238));
#197645=CARTESIAN_POINT('Ctrl Pts',(95.1074423626648,-1.18048492263276,
137.303633678775));
#197646=CARTESIAN_POINT('Ctrl Pts',(94.828994738852,4.82994155974394,135.3105518592));
#197647=CARTESIAN_POINT('Ctrl Pts',(94.5505471150391,6.40188770447863,129.176500428244));
#197648=CARTESIAN_POINT('Ctrl Pts',(94.2720994912261,2.09081179839861,124.538372985881));
#197649=CARTESIAN_POINT('Ctrl Pts',(93.9936518674133,-4.14161800857485,
125.658382066524));
#197650=CARTESIAN_POINT('Ctrl Pts',(93.7152042436005,-6.56810319495607,
131.507294040545));
#197651=CARTESIAN_POINT('Ctrl Pts',(93.4367566197874,-2.95882241485189,
136.710244539055));
#197652=CARTESIAN_POINT('Ctrl Pts',(93.1583089959747,3.36947161799043,136.485976232185));
#197653=CARTESIAN_POINT('Ctrl Pts',(92.8798613721617,6.60138584173913,131.040580737834));
#197654=CARTESIAN_POINT('Ctrl Pts',(92.6014137483489,3.76694897255651,125.37811049295));
#197655=CARTESIAN_POINT('Ctrl Pts',(92.3229661245359,-2.5291299767175,124.702099025532));
#197656=CARTESIAN_POINT('Ctrl Pts',(92.044518500723,-6.50106203225643,129.633767849141));
#197657=CARTESIAN_POINT('Ctrl Pts',(91.7660708769102,-4.49883567468812,
135.641154240296));
#197658=CARTESIAN_POINT('Ctrl Pts',(91.4876232530973,1.63760088757763,137.203763582666));
#197659=CARTESIAN_POINT('Ctrl Pts',(91.2091756292845,6.26916223541028,132.885634228324));
#197660=CARTESIAN_POINT('Ctrl Pts',(90.9307280054714,5.13966975450256,126.654916101563));
#197661=CARTESIAN_POINT('Ctrl Pts',(90.6522803816587,-0.71292814396669,
124.237334773374));
#197662=CARTESIAN_POINT('Ctrl Pts',(90.3738327578456,-5.91037990660673,
127.85452937895));
#197663=CARTESIAN_POINT('Ctrl Pts',(90.0953851340328,-5.67648127318543,
134.182474785545));
#197664=CARTESIAN_POINT('Ctrl Pts',(89.8169375102199,-0.226173661233629,
137.406098301819));
#197665=CARTESIAN_POINT('Ctrl Pts',(89.5384898864071,5.43197649619419,134.563047399079));
#197666=CARTESIAN_POINT('Ctrl Pts',(89.260042262594,6.09840562042418,128.265946966186));
#197667=CARTESIAN_POINT('Ctrl Pts',(88.9815946387814,1.1606979031614,124.301524670509));
#197668=CARTESIAN_POINT('Ctrl Pts',(88.7031470149683,-4.84363448386183,
126.312890928981));
#197669=CARTESIAN_POINT('Ctrl Pts',(88.4246993911556,-6.39690340491527,
132.45169841077));
#197670=CARTESIAN_POINT('Ctrl Pts',(88.1462517673426,-2.07173060295614,
137.076682937528));
#197671=CARTESIAN_POINT('Ctrl Pts',(87.8678041435297,4.15726141345302,135.937709672222));
#197672=CARTESIAN_POINT('Ctrl Pts',(87.5893565197169,6.5659332844097,130.081439403729));
#197673=CARTESIAN_POINT('Ctrl Pts',(87.3109088959039,2.94083323066708,124.889498414087));
#197674=CARTESIAN_POINT('Ctrl Pts',(87.032461272091,-3.38674889436835,125.133026832359));
#197675=CARTESIAN_POINT('Ctrl Pts',(86.7540136482781,-6.60207423736065,
130.588233939178));
#197676=CARTESIAN_POINT('Ctrl Pts',(86.4755660244652,-3.75041588547566,
136.242050905059));
#197677=CARTESIAN_POINT('Ctrl Pts',(86.1971184006524,2.54769144715974,136.898896142674));
#197678=CARTESIAN_POINT('Ctrl Pts',(85.9186707768394,6.50459480150186,131.955160967326));
#197679=CARTESIAN_POINT('Ctrl Pts',(85.6402231530266,4.48409330038545,125.953896490271));
#197680=CARTESIAN_POINT('Ctrl Pts',(85.3617755292137,-1.65707088364924,
124.409971587854));
#197681=CARTESIAN_POINT('Ctrl Pts',(85.0833279054008,-6.27546787802325,
128.742177820471));
#197682=CARTESIAN_POINT('Ctrl Pts',(84.8048802815879,-5.12701646614329,
134.969429300388));
#197683=CARTESIAN_POINT('Ctrl Pts',(84.526432657775,0.732912609443495,137.369186135708));
#197684=CARTESIAN_POINT('Ctrl Pts',(84.2479850339622,5.91933080172332,133.73618902941));
#197685=CARTESIAN_POINT('Ctrl Pts',(83.9695374101491,5.6661731626052,127.408984840408));
#197686=CARTESIAN_POINT('Ctrl Pts',(83.6910897863363,0.206079195000604,
124.201965117285));
#197687=CARTESIAN_POINT('Ctrl Pts',(83.4126421625234,-5.44339148528112,
127.062224313968));
#197688=CARTESIAN_POINT('Ctrl Pts',(83.1341945387106,-6.09065131504733,
133.361323960135));
#197689=CARTESIAN_POINT('Ctrl Pts',(82.8557469148977,-1.14090013114324,
137.310699209084));
#197690=CARTESIAN_POINT('Ctrl Pts',(82.5772992910847,4.85728253721157,135.281067144739));
#197691=CARTESIAN_POINT('Ctrl Pts',(82.2988516672719,6.39185984531258,129.137560481192));
#197692=CARTESIAN_POINT('Ctrl Pts',(82.0204040434589,2.05263021528453,124.52576171526));
#197693=CARTESIAN_POINT('Ctrl Pts',(81.7419564196462,-4.17286630602932,
125.683688613938));
#197694=CARTESIAN_POINT('Ctrl Pts',(81.4635087958331,-6.56370254795435,
131.547262925216));
#197695=CARTESIAN_POINT('Ctrl Pts',(81.1850611720204,-2.92281680300497,
136.728146308557));
#197696=CARTESIAN_POINT('Ctrl Pts',(80.9066135482074,3.40399479636718,136.465360034899));
#197697=CARTESIAN_POINT('Ctrl Pts',(80.6281659243945,6.60270147226842,131.000391851905));
#197698=CARTESIAN_POINT('Ctrl Pts',(80.3497183005816,3.73384805505426,125.355280541214));
#197699=CARTESIAN_POINT('Ctrl Pts',(80.0712706767688,-2.56622931613655,
124.717607618327));
#197700=CARTESIAN_POINT('Ctrl Pts',(79.7928230529558,-6.50806731306963,
129.673363347327));
#197701=CARTESIAN_POINT('Ctrl Pts',(79.514375429143,-4.46930938605503,135.668450315387));
#197702=CARTESIAN_POINT('Ctrl Pts',(79.23592780533,1.67652552884245,137.193676475141));
#197703=CARTESIAN_POINT('Ctrl Pts',(78.9574801815173,6.28171538555901,132.847433497217));
#197704=CARTESIAN_POINT('Ctrl Pts',(78.6790325577042,5.11431568180404,126.62370635255));
#197705=CARTESIAN_POINT('Ctrl Pts',(78.4005849338915,-0.752890285318027,
124.241796241119));
#197706=CARTESIAN_POINT('Ctrl Pts',(78.1221373100785,-5.92822686096799,
127.890562192549));
#197707=CARTESIAN_POINT('Ctrl Pts',(77.8436896862655,-5.65581256137084,
134.216966549603));
#197708=CARTESIAN_POINT('Ctrl Pts',(77.5652420624528,-0.185982819678218,
137.407352770183));
#197709=CARTESIAN_POINT('Ctrl Pts',(77.2867944386398,5.45475604753291,134.529911776607));
#197710=CARTESIAN_POINT('Ctrl Pts',(77.008346814827,6.08284058670873,128.228871271165));
#197711=CARTESIAN_POINT('Ctrl Pts',(76.729899191014,1.12109178998211,124.294579655415));
#197712=CARTESIAN_POINT('Ctrl Pts',(76.4514515672013,-4.8708855933594,126.342458723402));
#197713=CARTESIAN_POINT('Ctrl Pts',(76.1730039433881,-6.38675707239351,
132.4906076561));
#197714=CARTESIAN_POINT('Ctrl Pts',(75.8945563195755,-2.03351081232684,
137.089177938131));
#197715=CARTESIAN_POINT('Ctrl Pts',(75.6161086957625,4.18843254174224,135.912308132958));
#197716=CARTESIAN_POINT('Ctrl Pts',(75.3376610719495,6.56141100625526,130.041484098248));
#197717=CARTESIAN_POINT('Ctrl Pts',(75.0592134481368,2.90477329876725,124.871706316201));
#197718=CARTESIAN_POINT('Ctrl Pts',(74.7807658243238,-3.42120916422307,
125.153748010832));
#197719=CARTESIAN_POINT('Ctrl Pts',(74.5023182005109,-6.60326754065171,
130.628426643279));
#197720=CARTESIAN_POINT('Ctrl Pts',(74.223870576698,-3.71724563477466,136.264780003243));
#197721=CARTESIAN_POINT('Ctrl Pts',(73.9454229528852,2.58474341191554,136.883274704086));
#197722=CARTESIAN_POINT('Ctrl Pts',(73.6669753290721,6.51147953479087,131.915544330879));
#197723=CARTESIAN_POINT('Ctrl Pts',(73.3885277052595,4.45448406865298,125.926690409479));
#197724=CARTESIAN_POINT('Ctrl Pts',(73.1100800814464,-1.6959646429323,124.420177121874));
#197725=CARTESIAN_POINT('Ctrl Pts',(72.8316324576336,-6.28790470014163,
128.780416582107));
#197726=CARTESIAN_POINT('Ctrl Pts',(72.5531848338207,-5.1015675191428,135.000561735763));
#197727=CARTESIAN_POINT('Ctrl Pts',(72.2747372100078,0.772860986519783,
137.364603057617));
#197728=CARTESIAN_POINT('Ctrl Pts',(71.996289586195,5.93706800192887,133.700102062723));
#197729=CARTESIAN_POINT('Ctrl Pts',(71.7178419623819,5.64539956546153,127.374556144564));
#197730=CARTESIAN_POINT('Ctrl Pts',(71.4393943385692,0.165884721436248,
124.20083298183));
#197731=CARTESIAN_POINT('Ctrl Pts',(71.1609467147562,-5.46607007766984,
127.095429116077));
#197732=CARTESIAN_POINT('Ctrl Pts',(70.8824990909434,-6.07497350776591,
133.398352108815));
#197733=CARTESIAN_POINT('Ctrl Pts',(70.6040514671303,-1.10127306317963,
137.317523644624));
#197734=CARTESIAN_POINT('Ctrl Pts',(70.3256038433176,4.88444352628841,135.251416544269));
#197735=CARTESIAN_POINT('Ctrl Pts',(70.0471562195047,6.38159513342946,129.098682298033));
#197736=CARTESIAN_POINT('Ctrl Pts',(69.7687085956917,2.01437257120279,124.513383100429));
#197737=CARTESIAN_POINT('Ctrl Pts',(69.4902609718789,-4.20395997638847,
125.709184909736));
#197738=CARTESIAN_POINT('Ctrl Pts',(69.211813348066,-6.5590586805409,131.587204281367));
#197739=CARTESIAN_POINT('Ctrl Pts',(68.9333657242531,-2.88670288510633,
136.745828570004));
#197740=CARTESIAN_POINT('Ctrl Pts',(68.6549181004402,3.43839183846502,136.444534067195));
#197741=CARTESIAN_POINT('Ctrl Pts',(68.3764704766273,6.60377243726651,130.960195701968));
#197742=CARTESIAN_POINT('Ctrl Pts',(68.0980228528144,3.70060877843901,125.332652507142));
#197743=CARTESIAN_POINT('Ctrl Pts',(67.8195752290015,-2.6032335629848,124.733341757993));
#197744=CARTESIAN_POINT('Ctrl Pts',(67.5411276051886,-6.51483143505509,
129.713000755032));
#197745=CARTESIAN_POINT('Ctrl Pts',(67.2626799813758,-4.43961748551916,
135.695566149845));
#197746=CARTESIAN_POINT('Ctrl Pts',(66.9842323575627,1.71538804583728,137.183352609169));
#197747=CARTESIAN_POINT('Ctrl Pts',(66.7057847337499,6.29403576443417,132.809157059292));
#197748=CARTESIAN_POINT('Ctrl Pts',(66.4273371099371,5.08877209625689,126.592651519219));
#197749=CARTESIAN_POINT('Ctrl Pts',(66.1488894861241,-0.792824528042931,
124.246500887099));
#197750=CARTESIAN_POINT('Ctrl Pts',(65.8704418623113,-5.94585414270274,
127.92670297802));
#197751=CARTESIAN_POINT('Ctrl Pts',(65.5919942384984,-5.63493427134196,
134.251331858291));
#197752=CARTESIAN_POINT('Ctrl Pts',(65.3135466146855,-0.145785086460763,
137.408362562243));
#197753=CARTESIAN_POINT('Ctrl Pts',(65.0350989908726,5.47733347088038,134.496638102466));
#197754=CARTESIAN_POINT('Ctrl Pts',(64.7566513670597,6.06705015109826,128.191891011849));
#197755=CARTESIAN_POINT('Ctrl Pts',(64.4782037432468,1.0814441343344,124.28787586265));
#197756=CARTESIAN_POINT('Ctrl Pts',(64.199756119434,-4.89795621039988,126.37219185524));
#197757=CARTESIAN_POINT('Ctrl Pts',(63.921308495621,-6.37637407623982,132.529454416925));
#197758=CARTESIAN_POINT('Ctrl Pts',(63.6428608718081,-1.99521566920641,
137.101440052517));
#197759=CARTESIAN_POINT('Ctrl Pts',(63.3644132479953,4.21944846612332,135.886717316821));
#197760=CARTESIAN_POINT('Ctrl Pts',(63.0859656241823,6.556645592603,130.001557061437));
#197761=CARTESIAN_POINT('Ctrl Pts',(62.8075180003696,2.86860572942485,124.854134055001));
#197762=CARTESIAN_POINT('Ctrl Pts',(62.5290703765565,-3.4555426599142,125.174678574835));
#197763=CARTESIAN_POINT('Ctrl Pts',(62.2506227527437,-6.60421615743575,
130.66862586668));
#197764=CARTESIAN_POINT('Ctrl Pts',(61.9721751289308,-3.68393764016947,
136.287306763578));
#197765=CARTESIAN_POINT('Ctrl Pts',(61.6937275051179,2.62169959805353,136.867428009101));
#197766=CARTESIAN_POINT('Ctrl Pts',(61.415279881305,6.51812298281107,131.875886519111));
#197767=CARTESIAN_POINT('Ctrl Pts',(61.1368322574921,4.42470977437533,125.899665072552));
#197768=CARTESIAN_POINT('Ctrl Pts',(60.8583846336791,-1.73479555762186,
124.430619224162));
#197769=CARTESIAN_POINT('Ctrl Pts',(60.5799370098664,-6.30010852163892,
128.818730341733));
#197770=CARTESIAN_POINT('Ctrl Pts',(60.3014893860534,-5.07592953168175,
135.031538679362));
#197771=CARTESIAN_POINT('Ctrl Pts',(60.0230417622406,0.81278072494776,137.35977688733));
#197772=CARTESIAN_POINT('Ctrl Pts',(59.7445941384276,5.95458520189618,133.663907793273));
#197773=CARTESIAN_POINT('Ctrl Pts',(59.4661465146148,5.62441677596096,127.340254541386));
#197774=CARTESIAN_POINT('Ctrl Pts',(59.1876988908018,0.125684100952275,
124.199945542519));
#197775=CARTESIAN_POINT('Ctrl Pts',(58.909251266989,-5.48854612282181,127.128771354006));
#197776=CARTESIAN_POINT('Ctrl Pts',(58.6308036431761,-6.05907059010694,
133.435284136186));
#197777=CARTESIAN_POINT('Ctrl Pts',(58.3523560193632,-1.06160518713815,
137.324106732513));
#197778=CARTESIAN_POINT('Ctrl Pts',(58.0739083955504,4.91142352051418,135.221601156507));
#197779=CARTESIAN_POINT('Ctrl Pts',(57.7954607717374,6.37109394919177,129.059867319411));
#197780=CARTESIAN_POINT('Ctrl Pts',(57.5170131479246,1.97604028380464,124.501237600083));
#197781=CARTESIAN_POINT('Ctrl Pts',(57.2385655241116,-4.23489786746425,
125.734870009144));
#197782=CARTESIAN_POINT('Ctrl Pts',(56.9601179002987,-6.554171764796,131.627116628959));
#197783=CARTESIAN_POINT('Ctrl Pts',(56.6816702764859,-2.85048199937133,
136.76329066817));
#197784=CARTESIAN_POINT('Ctrl Pts',(56.4032226526729,3.47266146968847,136.423499100792));
#197785=CARTESIAN_POINT('Ctrl Pts',(56.1247750288601,6.60459869704857,130.919993777505));
#197786=CARTESIAN_POINT('Ctrl Pts',(55.8463274050471,3.66723237440476,125.310227229228));
#197787=CARTESIAN_POINT('Ctrl Pts',(55.5678797812343,-2.6401413460556,124.749300861495));
#197788=CARTESIAN_POINT('Ctrl Pts',(55.2894321574214,-6.5213541475661,129.752678603477));
#197789=CARTESIAN_POINT('Ctrl Pts',(55.0109845336085,-4.40976107332459,
135.722500738884));
#197790=CARTESIAN_POINT('Ctrl Pts',(54.7325369097956,1.75418699849736,137.172792367301));
#197791=CARTESIAN_POINT('Ctrl Pts',(54.4540892859827,6.30612291549916,132.770806332897));
#197792=CARTESIAN_POINT('Ctrl Pts',(54.1756416621698,5.06303994438864,126.561752752318));
#197793=CARTESIAN_POINT('Ctrl Pts',(53.897194038357,-0.832729392363195,
124.251448536985));
#197794=CARTESIAN_POINT('Ctrl Pts',(53.618746414544,-5.96326109862574,127.962950396153));
#197795=CARTESIAN_POINT('Ctrl Pts',(53.3402987907312,-5.61384717675129,
134.285569438194));
#197796=CARTESIAN_POINT('Ctrl Pts',(53.0618511669183,-0.105581951123662,
137.409127640582));
#197797=CARTESIAN_POINT('Ctrl Pts',(52.7834035431054,5.49970792962155,134.463227609627));
#197798=CARTESIAN_POINT('Ctrl Pts',(52.5049559192925,6.05103489871361,128.155007558556));
#197799=CARTESIAN_POINT('Ctrl Pts',(52.2265082954796,1.04175640537643,124.281413540623));
#197800=CARTESIAN_POINT('Ctrl Pts',(51.9480606716666,-4.9248453318719,126.402089222721));
#197801=CARTESIAN_POINT('Ctrl Pts',(51.6696130478539,-6.36575480119974,
132.568237253767));
#197802=CARTESIAN_POINT('Ctrl Pts',(51.3911654240409,-1.95684659263562,
137.113468826308));
#197803=CARTESIAN_POINT('Ctrl Pts',(51.112717800228,4.25030803728985,135.860938172086));
#197804=CARTESIAN_POINT('Ctrl Pts',(50.8342701764151,6.55163722003711,129.961659772806));
#197805=CARTESIAN_POINT('Ctrl Pts',(50.5558225526023,2.83233186284197,124.836782281636));
#197806=CARTESIAN_POINT('Ctrl Pts',(50.2773749287893,-3.48974810920128,
125.195817748775));
#197807=CARTESIAN_POINT('Ctrl Pts',(49.9989273049765,-6.60492005256131,
130.708830119782));
#197808=CARTESIAN_POINT('Ctrl Pts',(49.7204796811635,-3.65049313590031,
136.309630351328));
#197809=CARTESIAN_POINT('Ctrl Pts',(49.4420320573507,2.65855863614892,136.851356644924));
#197810=CARTESIAN_POINT('Ctrl Pts',(49.1635844335378,6.52452489938715,131.836189001557));
#197811=CARTESIAN_POINT('Ctrl Pts',(48.8851368097249,4.39477152084969,125.87282148092));
#197812=CARTESIAN_POINT('Ctrl Pts',(48.606689185912,-1.77356218882415,124.441297507781));
#197813=CARTESIAN_POINT('Ctrl Pts',(48.3282415620992,-6.31207889029818,
128.857117679619));
#197814=CARTESIAN_POINT('Ctrl Pts',(48.0497939382862,-5.05010345378512,
135.062358983324));
#197815=CARTESIAN_POINT('Ctrl Pts',(47.7713463144734,0.852670345487299,
137.354707803682));
#197816=CARTESIAN_POINT('Ctrl Pts',(47.4928986906604,5.97188175251911,133.627607562248));
#197817=CARTESIAN_POINT('Ctrl Pts',(47.2144510668476,5.60322557162828,127.306081301933));
#197818=CARTESIAN_POINT('Ctrl Pts',(46.9360034430346,0.0854788231980546,
124.199302832238));
#197819=CARTESIAN_POINT('Ctrl Pts',(46.6575558192218,-5.5108187878785,127.162249792247));
#197820=CARTESIAN_POINT('Ctrl Pts',(46.3791081954089,-6.04294315135938,
133.47211867372));
#197821=CARTESIAN_POINT('Ctrl Pts',(46.100660571596,-1.02189797292572,137.330448228811));
#197822=CARTESIAN_POINT('Ctrl Pts',(45.822212947783,4.93822152013526,135.191622086273));
#197823=CARTESIAN_POINT('Ctrl Pts',(45.5437653239702,6.36035668172477,129.02111698363));
#197824=CARTESIAN_POINT('Ctrl Pts',(45.2653177001572,1.9376347735074,124.489325664279));
#197825=CARTESIAN_POINT('Ctrl Pts',(44.9868700763445,-4.26567883284234,
125.76074296039));
#197826=CARTESIAN_POINT('Ctrl Pts',(44.7084224525315,-6.54904198180601,
131.666998489025));
#197827=CARTESIAN_POINT('Ctrl Pts',(44.4299748287186,-2.81415548797717,
136.780531955991));
#197828=CARTESIAN_POINT('Ctrl Pts',(44.1515272049057,3.50680242016433,136.402255915145));
#197829=CARTESIAN_POINT('Ctrl Pts',(43.8730795810928,6.60518022099696,130.879787568212));
#197830=CARTESIAN_POINT('Ctrl Pts',(43.59463195728,3.63372007972613,125.288005538446));
#197831=CARTESIAN_POINT('Ctrl Pts',(43.316184333467,-2.6769512977182,124.765484337463));
#197832=CARTESIAN_POINT('Ctrl Pts',(43.0377367096542,-6.52763520890084,
129.792395422388));
#197833=CARTESIAN_POINT('Ctrl Pts',(42.7592890858413,-4.37974125581177,
135.749253084432));
#197834=CARTESIAN_POINT('Ctrl Pts',(42.4808414620283,1.79292094911309,137.161996140853));
#197835=CARTESIAN_POINT('Ctrl Pts',(42.2023938382155,6.31797639086063,132.732382739134));
#197836=CARTESIAN_POINT('Ctrl Pts',(41.9239462144025,5.0371201797131,126.531011196811));
#197837=CARTESIAN_POINT('Ctrl Pts',(41.6454985905898,-0.872603399589798,
124.256639007436));
#197838=CARTESIAN_POINT('Ctrl Pts',(41.3670509667768,-5.98044708371573,
127.999303103786));
#197839=CARTESIAN_POINT('Ctrl Pts',(41.0886033429639,-5.592552058989,134.319678020622));
#197840=CARTESIAN_POINT('Ctrl Pts',(40.810155719151,-0.0653749034083074,
137.409647976851));
#197841=CARTESIAN_POINT('Ctrl Pts',(40.5317080953382,5.52187859466303,134.429681536124));
#197842=CARTESIAN_POINT('Ctrl Pts',(40.2532604715252,6.03479542300531,128.118222278014));
#197843=CARTESIAN_POINT('Ctrl Pts',(39.9748128477124,1.00203007375177,124.275192928799));
#197844=CARTESIAN_POINT('Ctrl Pts',(39.6963652238994,-4.95155196138904,
126.432149717987));
#197845=CARTESIAN_POINT('Ctrl Pts',(39.4179176000866,-6.35489964077443,
132.60695472951));
#197846=CARTESIAN_POINT('Ctrl Pts',(39.1394699762736,-1.91840500439501,
137.125263813774));
#197847=CARTESIAN_POINT('Ctrl Pts',(38.8610223524608,4.28101011172891,135.834971654011));
#197848=CARTESIAN_POINT('Ctrl Pts',(38.5825747286478,6.54638607414467,129.921793710766));
#197849=CARTESIAN_POINT('Ctrl Pts',(38.304127104835,2.79595304316033,124.819651639079));
#197850=CARTESIAN_POINT('Ctrl Pts',(38.0256794810221,-3.52382424458856,
125.217164749334));
#197851=CARTESIAN_POINT('Ctrl Pts',(37.7472318572093,-6.60537919994535,
130.749037912801));
#197852=CARTESIAN_POINT('Ctrl Pts',(37.4687842333963,-3.61691336126579,
136.331749939282));
#197853=CARTESIAN_POINT('Ctrl Pts',(37.1903366095834,2.69531916037638,136.835061207086));
#197854=CARTESIAN_POINT('Ctrl Pts',(36.9118889857706,6.53068504729366,131.796453249222));
#197855=CARTESIAN_POINT('Ctrl Pts',(36.6334413619576,4.36467041744916,125.846160629286));
#197856=CARTESIAN_POINT('Ctrl Pts',(36.3549937381448,-1.8122631000273,124.452211577043));
#197857=CARTESIAN_POINT('Ctrl Pts',(36.0765461143319,-6.32381536255287,
128.895577173308));
#197858=CARTESIAN_POINT('Ctrl Pts',(35.798098490519,-5.02409024244786,135.093021505591));
#197859=CARTESIAN_POINT('Ctrl Pts',(35.5196508667061,0.892528370013623,
137.34939599451));
#197860=CARTESIAN_POINT('Ctrl Pts',(35.2412032428932,5.98895701286753,133.591202714771));
#197861=CARTESIAN_POINT('Ctrl Pts',(34.9627556190803,5.58182673771145,127.272037692505));
#197862=CARTESIAN_POINT('Ctrl Pts',(34.6843079952674,0.0452703779943793,
124.198904874802));
#197863=CARTESIAN_POINT('Ctrl Pts',(34.4058603714545,-5.53288724751859,
127.195863190245));
#197864=CARTESIAN_POINT('Ctrl Pts',(34.1274127476417,-6.02659178913083,
133.508854356496));
#197865=CARTESIAN_POINT('Ctrl Pts',(33.8489651238287,-0.982152891908117,
137.336547898535));
#197866=CARTESIAN_POINT('Ctrl Pts',(33.5705175000158,4.96483653214189,135.161480444452));
#197867=CARTESIAN_POINT('Ctrl Pts',(33.292069876203,6.34938372890195,128.982432726597));
#197868=CARTESIAN_POINT('Ctrl Pts',(33.0136222523901,1.89915746344075,124.477647734417));
#197869=CARTESIAN_POINT('Ctrl Pts',(32.7351746285772,-4.29630173192265,
125.786802804744));
#197870=CARTESIAN_POINT('Ctrl Pts',(32.4567270047643,-6.543669521657,131.706848383727));
#197871=CARTESIAN_POINT('Ctrl Pts',(32.1782793809514,-2.77772469701646,
136.797551794587));
#197872=CARTESIAN_POINT('Ctrl Pts',(31.8998317571386,3.54081342478663,136.380805297429));
#197873=CARTESIAN_POINT('Ctrl Pts',(31.6213841333256,6.60551698756319,130.839578563946));
#197874=CARTESIAN_POINT('Ctrl Pts',(31.3429365095127,3.6000731362139,125.26598825823));
#197875=CARTESIAN_POINT('Ctrl Pts',(31.0644888856998,-2.71366205396602,
124.781891586214));
#197876=CARTESIAN_POINT('Ctrl Pts',(30.7860412618869,-6.53367438631237,
129.83214974004));
#197877=CARTESIAN_POINT('Ctrl Pts',(30.507593638074,-4.34955914537615,135.775822195171));
#197878=CARTESIAN_POINT('Ctrl Pts',(30.2291460142612,1.83158846238341,137.150964329883));
#197879=CARTESIAN_POINT('Ctrl Pts',(29.9506983904483,6.32959575128355,132.693887701803));
#197880=CARTESIAN_POINT('Ctrl Pts',(29.6722507666353,5.01101376269691,126.500427991838));
#197881=CARTESIAN_POINT('Ctrl Pts',(29.3938031428225,-0.912445072176531,
124.26207210612));
#197882=CARTESIAN_POINT('Ctrl Pts',(29.1153555190096,-5.99741146113971,
128.035759753857));
#197883=CARTESIAN_POINT('Ctrl Pts',(28.8369078951967,-5.57104970715349,
134.353656341672));
#197884=CARTESIAN_POINT('Ctrl Pts',(28.5584602713837,-0.0251654332018655,
137.409923551768));
#197885=CARTESIAN_POINT('Ctrl Pts',(28.280012647571,5.54384464446253,134.396001125022));
#197886=CARTESIAN_POINT('Ctrl Pts',(28.001565023758,6.0183323257333,128.081536533317));
#197887=CARTESIAN_POINT('Ctrl Pts',(27.7231173999451,0.962266611534229,
124.269214257685));
#197888=CARTESIAN_POINT('Ctrl Pts',(27.4446697761322,-4.97807510932732,
126.462372227135));
#197889=CARTESIAN_POINT('Ctrl Pts',(27.1662221523194,-6.34380899720599,
132.645605409466));
#197890=CARTESIAN_POINT('Ctrl Pts',(26.8877745285064,-1.87989232895117,
137.136824577849));
#197891=CARTESIAN_POINT('Ctrl Pts',(26.6093269046936,4.31155355176403,135.808818724794));
#197892=CARTESIAN_POINT('Ctrl Pts',(26.3308792808807,6.5408923495088,129.881960352566));
#197893=CARTESIAN_POINT('Ctrl Pts',(26.0524316570678,2.75947061841045,124.802742762115));
#197894=CARTESIAN_POINT('Ctrl Pts',(25.7739840332549,-3.55776980337282,
125.238718785491));
#197895=CARTESIAN_POINT('Ctrl Pts',(25.4955364094419,-6.60559358257403,
130.789247755823));
#197896=CARTESIAN_POINT('Ctrl Pts',(25.2170887856292,-3.58319956057628,
136.353664707793));
#197897=CARTESIAN_POINT('Ctrl Pts',(24.9386411618162,2.73197980856112,136.81854229942));
#197898=CARTESIAN_POINT('Ctrl Pts',(24.6601935380033,6.5366031982641,131.756680734531));
#197899=CARTESIAN_POINT('Ctrl Pts',(24.3817459141905,4.3344075795813,125.819683505575));
#197900=CARTESIAN_POINT('Ctrl Pts',(24.1032982903775,-1.85089685715453,
124.463361027524));
#197901=CARTESIAN_POINT('Ctrl Pts',(23.8248506665647,-6.33531750350378,
128.934107397669));
#197902=CARTESIAN_POINT('Ctrl Pts',(23.5464030427517,-4.99789086159903,
135.123525109951));
#197903=CARTESIAN_POINT('Ctrl Pts',(23.2679554189389,0.932353321572971,
137.343841656646));
#197904=CARTESIAN_POINT('Ctrl Pts',(22.9895077951259,6.00581035021119,133.554694599836));
#197905=CARTESIAN_POINT('Ctrl Pts',(22.7110601713131,5.56022106715229,127.238124974604));
#197906=CARTESIAN_POINT('Ctrl Pts',(22.4326125475002,0.00506025528043594,
124.198751684957));
#197907=CARTESIAN_POINT('Ctrl Pts',(22.1541649236873,-5.554750683987,127.229610302442));
#197908=CARTESIAN_POINT('Ctrl Pts',(21.8757172998744,-6.01001710932725,
133.545489823263));
#197909=CARTESIAN_POINT('Ctrl Pts',(21.5972696760615,-0.942371416853923,
137.342405515655));
#197910=CARTESIAN_POINT('Ctrl Pts',(21.3188220522486,4.99126757030501,135.131177347952));
#197911=CARTESIAN_POINT('Ctrl Pts',(21.0403744284357,6.33817549733007,128.943815981773));
#197912=CARTESIAN_POINT('Ctrl Pts',(20.7619268046228,1.86060977939589,124.466204243228));
#197913=CARTESIAN_POINT('Ctrl Pts',(20.48347918081,-4.32676542996233,125.813048576547));
#197914=CARTESIAN_POINT('Ctrl Pts',(20.205031556997,-6.5380545834274,131.746664836412));
#197915=CARTESIAN_POINT('Ctrl Pts',(19.9265839331841,-2.74119097644563,
136.814349553278));
#197916=CARTESIAN_POINT('Ctrl Pts',(19.6481363093713,3.57469322326559,136.359148042506));
#197917=CARTESIAN_POINT('Ctrl Pts',(19.3696886855584,6.60560898426828,130.799368254665));
#197918=CARTESIAN_POINT('Ctrl Pts',(19.0912410617455,3.56629279066743,125.244176204439));
#197919=CARTESIAN_POINT('Ctrl Pts',(18.8127934379326,-2.75027225446848,
124.798521999768));
#197920=CARTESIAN_POINT('Ctrl Pts',(18.5343458141197,-6.53947145601676,
129.871940083324));
#197921=CARTESIAN_POINT('Ctrl Pts',(18.2558981903068,-4.31921586042675,
135.802207086573));
#197922=CARTESIAN_POINT('Ctrl Pts',(17.9774505664939,1.87018810546999,137.139697343177));
#197923=CARTESIAN_POINT('Ctrl Pts',(17.6990029426811,6.34098056620813,132.65532264735));
#197924=CARTESIAN_POINT('Ctrl Pts',(17.4205553188681,4.98472166072295,126.470004270672));
#197925=CARTESIAN_POINT('Ctrl Pts',(17.1421076950552,-0.95225293377558,
124.26774763171));
#197926=CARTESIAN_POINT('Ctrl Pts',(16.8636600712423,-6.01415360227624,
128.072318995452));
#197927=CARTESIAN_POINT('Ctrl Pts',(16.5852124474295,-5.54934091802252,
134.387503142263));
#197928=CARTESIAN_POINT('Ctrl Pts',(16.3067648236166,0.0150449695187284,
137.409954355121));
#197929=CARTESIAN_POINT('Ctrl Pts',(16.0283171998036,5.56560526505998,134.362187624359));
#197930=CARTESIAN_POINT('Ctrl Pts',(15.7498695759908,6.00164621694371,128.044951683866));
#197931=CARTESIAN_POINT('Ctrl Pts',(15.4714219521779,0.922467492173741,
124.263477748823));
#197932=CARTESIAN_POINT('Ctrl Pts',(15.192974328365,-5.00441379286154,126.492755630261));
#197933=CARTESIAN_POINT('Ctrl Pts',(14.9145267045521,-6.33248328146239,
132.684187861418));
#197934=CARTESIAN_POINT('Ctrl Pts',(14.6360790807393,-1.84130999340576,
137.148150690142));
#197935=CARTESIAN_POINT('Ctrl Pts',(14.3576314569263,4.34193722559672,135.782480353541));
#197936=CARTESIAN_POINT('Ctrl Pts',(14.0791838331134,6.53515624970152,129.842161174248));
#197937=CARTESIAN_POINT('Ctrl Pts',(13.8007362093005,2.72288594046203,124.786056277307));
#197938=CARTESIAN_POINT('Ctrl Pts',(13.5222885854877,-3.59158352768866,
125.260479058552));
#197939=CARTESIAN_POINT('Ctrl Pts',(13.2438409616747,-6.60556319250329,
130.829458158858));
#197940=CARTESIAN_POINT('Ctrl Pts',(12.9653933378619,-3.54935298310934,
136.375373844801));
#197941=CARTESIAN_POINT('Ctrl Pts',(12.686945714049,2.76853922222938,136.801800534039));
#197942=CARTESIAN_POINT('Ctrl Pts',(12.4084980902361,6.5422791329992,131.716872931266));
#197943=CARTESIAN_POINT('Ctrl Pts',(12.1300504664232,4.30398412864651,125.793391090908));
#197944=CARTESIAN_POINT('Ctrl Pts',(11.8516028426103,-1.88946202861834,
124.474745446076));
#197945=CARTESIAN_POINT('Ctrl Pts',(11.5731552187974,-6.34658488693473,
128.972706924952));
#197946=CARTESIAN_POINT('Ctrl Pts',(11.2947075949845,-4.97150628206636,
135.153868666082));
#197947=CARTESIAN_POINT('Ctrl Pts',(11.0162599711716,0.972143724437105,
137.338044995907));
#197948=CARTESIAN_POINT('Ctrl Pts',(10.7378123473587,6.0224411400439,133.518084570262));
#197949=CARTESIAN_POINT('Ctrl Pts',(10.4593647235458,5.53840936055655,127.204344404875));
#197950=CARTESIAN_POINT('Ctrl Pts',(10.1809170997329,-0.0351500549433496,
124.198843268382));
#197951=CARTESIAN_POINT('Ctrl Pts',(9.90246947592002,-5.57640828712608,
127.263489878326));
#197952=CARTESIAN_POINT('Ctrl Pts',(9.62402185210712,-5.99321972612948,
133.582023716479));
#197953=CARTESIAN_POINT('Ctrl Pts',(9.34557422829421,-0.902555021880531,
137.348020863117));
#197954=CARTESIAN_POINT('Ctrl Pts',(9.06712660448133,5.01751365521256,135.100713919668));
#197955=CARTESIAN_POINT('Ctrl Pts',(8.78867898066847,6.32673240233446,128.905268180115));
#197956=CARTESIAN_POINT('Ctrl Pts',(8.51023135685555,1.82199314977141,124.454995614755));
#197957=CARTESIAN_POINT('Ctrl Pts',(8.23178373304265,-4.35706879811783,
125.839479303254));
#197958=CARTESIAN_POINT('Ctrl Pts',(7.9533361092298,-6.53219737518076,131.786446371669));
#197959=CARTESIAN_POINT('Ctrl Pts',(7.67488848541689,-2.70455568003535,
136.83092460962));
#197960=CARTESIAN_POINT('Ctrl Pts',(7.39644086160398,3.60844056017245,136.337284952891));
#197961=CARTESIAN_POINT('Ctrl Pts',(7.1179932377911,6.60545620770325,130.759158130379));
#197962=CARTESIAN_POINT('Ctrl Pts',(6.83954561397822,3.53238029483008,125.222570185327));
#197963=CARTESIAN_POINT('Ctrl Pts',(6.5610979901653,-2.78678054262086,124.815374961881));
#197964=CARTESIAN_POINT('Ctrl Pts',(6.28265036635242,-6.54502620320144,
129.911764977794));
#197965=CARTESIAN_POINT('Ctrl Pts',(6.00420274253956,-4.28871252534551,
135.828406780936));
#197966=CARTESIAN_POINT('Ctrl Pts',(5.72575511872663,1.90871844804856,137.128195598241));
#197967=CARTESIAN_POINT('Ctrl Pts',(5.44730749491374,6.35213041376593,132.616689004818));
#197968=CARTESIAN_POINT('Ctrl Pts',(5.16885987110085,4.95824484805471,126.439741160674));
#197969=CARTESIAN_POINT('Ctrl Pts',(4.89041224728798,-0.992025509291961,
124.273665373899));
#197970=CARTESIAN_POINT('Ctrl Pts',(4.61196462347505,-6.03067288673954,
128.108979473854));
#197971=CARTESIAN_POINT('Ctrl Pts',(4.33351699966218,-5.52742649602286,
134.421217168191));
#197972=CARTESIAN_POINT('Ctrl Pts',(4.05506937584931,0.0552548147426717,
137.409740385768));
#197973=CARTESIAN_POINT('Ctrl Pts',(3.77662175203639,5.58715965010757,134.328242287108));
#197974=CARTESIAN_POINT('Ctrl Pts',(3.49817412822347,5.98473771494644,128.008469085329));
#197975=CARTESIAN_POINT('Ctrl Pts',(3.21972650441063,0.882634190440881,
124.25798361478));
#197976=CARTESIAN_POINT('Ctrl Pts',(2.94127888059773,-5.03056703600248,
126.523298801495));
#197977=CARTESIAN_POINT('Ctrl Pts',(2.66283125678483,-6.32092291322184,
132.722700655682));
#197978=CARTESIAN_POINT('Ctrl Pts',(2.38438363297192,-1.80265942744139,
137.159241730961));
#197979=CARTESIAN_POINT('Ctrl Pts',(2.10593600915906,4.37216000734877,135.755957516231));
#197980=CARTESIAN_POINT('Ctrl Pts',(1.82748838534615,6.529177987276,129.802397650584));
#197981=CARTESIAN_POINT('Ctrl Pts',(1.54904076153325,2.68620036497402,124.769592802981));
#197982=CARTESIAN_POINT('Ctrl Pts',(1.27059313772038,-3.62526416455594,
125.282444762183));
#197983=CARTESIAN_POINT('Ctrl Pts',(0.992145513907496,-6.60528803085927,
130.869667631896));
#197984=CARTESIAN_POINT('Ctrl Pts',(0.713697890094564,-3.51537488306232,
136.396876545864));
#197985=CARTESIAN_POINT('Ctrl Pts',(0.435250266281723,2.80499604665836,
136.784836531317));
#197986=CARTESIAN_POINT('Ctrl Pts',(0.156802642468823,6.54771264117505,
131.677031314524));
#197987=CARTESIAN_POINT('Ctrl Pts',(-0.121644981344083,4.27340119199728,
125.767284359559));
#197988=CARTESIAN_POINT('Ctrl Pts',(-0.400092605156985,-1.92795718537184,
124.486364410847));
#197989=CARTESIAN_POINT('Ctrl Pts',(-0.678540228969845,-6.35761709532873,
129.011374324836));
#197990=CARTESIAN_POINT('Ctrl Pts',(-0.956987852782752,-4.94493748154019,
135.184051049593));
#197991=CARTESIAN_POINT('Ctrl Pts',(-1.23543547659566,1.01189810415772,
137.332006227089));
#197992=CARTESIAN_POINT('Ctrl Pts',(-1.51388310040852,6.03884876610542,
133.48137398265));
#197993=CARTESIAN_POINT('Ctrl Pts',(-1.79233072422142,5.51639242616521,
127.170697235071));
#197994=CARTESIAN_POINT('Ctrl Pts',(-2.07077834803434,-0.0753590626689394,
124.19917962168));
#197995=CARTESIAN_POINT('Ctrl Pts',(-2.34922597184723,-5.59785925440532,
127.297500662476));
#197996=CARTESIAN_POINT('Ctrl Pts',(-2.6276735956601,-5.97620026197078,
133.618454682368));
#197997=CARTESIAN_POINT('Ctrl Pts',(-2.906121219473,-0.862705182398668,
137.353393732843));
#197998=CARTESIAN_POINT('Ctrl Pts',(-3.18456884328591,5.04357381430661,
135.070091288433));
#197999=CARTESIAN_POINT('Ctrl Pts',(-3.46301646709877,6.31505486794284,
128.866790750024));
#198000=CARTESIAN_POINT('Ctrl Pts',(-3.74146409091167,1.78330900552073,
124.444022264336));
#198001=CARTESIAN_POINT('Ctrl Pts',(-4.01991171472458,-4.38721071348669,
125.866094005463));
#198002=CARTESIAN_POINT('Ctrl Pts',(-4.29835933853748,-6.52609811395827,
131.826191515377));
#198003=CARTESIAN_POINT('Ctrl Pts',(-4.57680696235032,-2.66782016531947,
136.847276349416));
#198004=CARTESIAN_POINT('Ctrl Pts',(-4.85525458616324,3.64205418498746,
136.31521683873));
#198005=CARTESIAN_POINT('Ctrl Pts',(-5.13370220997616,6.60505866352928,
130.718949681087));
#198006=CARTESIAN_POINT('Ctrl Pts',(-5.41214983378902,3.49833690534187,
125.201171001511));
#198007=CARTESIAN_POINT('Ctrl Pts',(-5.69059745760191,-2.82318556559566,
124.832449848059));
#198008=CARTESIAN_POINT('Ctrl Pts',(-5.96904508141481,-6.55033842203324,
129.951622947723));
#198009=CARTESIAN_POINT('Ctrl Pts',(-6.24749270522772,-4.2580502704442,
135.854420307421));
#198010=CARTESIAN_POINT('Ctrl Pts',(-6.52594032904057,1.9471780623631,137.116459521273));
#198011=CARTESIAN_POINT('Ctrl Pts',(-6.80438795285348,6.36304488079526,
132.577988205793));
#198012=CARTESIAN_POINT('Ctrl Pts',(-7.0828355766664,4.93158430580029,126.409639783256));
#198013=CARTESIAN_POINT('Ctrl Pts',(-7.36128320047925,-1.03176132493798,
124.279825113401));
#198014=CARTESIAN_POINT('Ctrl Pts',(-7.63973082429214,-6.04696870240127,
128.145739830595));
#198015=CARTESIAN_POINT('Ctrl Pts',(-7.91817844810507,-5.50530725320171,
134.454797170168));
#198016=CARTESIAN_POINT('Ctrl Pts',(-8.19662607191793,0.09546261247915,
137.40928165164));
#198017=CARTESIAN_POINT('Ctrl Pts',(-8.47507369573082,5.60850700089942,
134.294166371127));
#198018=CARTESIAN_POINT('Ctrl Pts',(-8.75352131954372,5.96760744629241,
127.972090089581));
#198019=CARTESIAN_POINT('Ctrl Pts',(-9.03196894335663,0.842768182373745,
124.252732059145));
#198020=CARTESIAN_POINT('Ctrl Pts',(-9.31041656716948,-5.05653386963193,
126.554000609049));
#198021=CARTESIAN_POINT('Ctrl Pts',(-9.5888641909824,-6.30912832085822,
132.76114236515));
#198022=CARTESIAN_POINT('Ctrl Pts',(-9.86731181479532,-1.76394206326903,
137.170097289323));
#198023=CARTESIAN_POINT('Ctrl Pts',(-10.1457594386081,4.40222077710389,
135.729251195677));
#198024=CARTESIAN_POINT('Ctrl Pts',(-10.424207062421,6.52295778375913,129.762671255026));
#198025=CARTESIAN_POINT('Ctrl Pts',(-10.7026546862339,2.64941525134336,
124.753352949195));
#198026=CARTESIAN_POINT('Ctrl Pts',(-10.9811023100469,-3.65881046592654,
125.304615082438));
#198027=CARTESIAN_POINT('Ctrl Pts',(-11.2595499338597,-6.60476810783814,
130.909874684957));
#198028=CARTESIAN_POINT('Ctrl Pts',(-11.5379975576726,-3.48126651950624,
136.418172014193));
#198029=CARTESIAN_POINT('Ctrl Pts',(-11.8164451814855,2.84134893092756,
136.767650919861));
#198030=CARTESIAN_POINT('Ctrl Pts',(-12.0948928052984,6.5529035214511,131.637157360647));
#198031=CARTESIAN_POINT('Ctrl Pts',(-12.3733404291112,4.2426599028951,125.741364278924));
#198032=CARTESIAN_POINT('Ctrl Pts',(-12.6517880529242,-1.96638090096281,
124.498217491291));
#198033=CARTESIAN_POINT('Ctrl Pts',(-12.9302356767371,-6.36841371988325,
129.050108164486));
#198034=CARTESIAN_POINT('Ctrl Pts',(-13.2086833005499,-4.91818544453708,
135.214071142064));
#198035=CARTESIAN_POINT('Ctrl Pts',(-13.4871309243628,1.05161498762227,
137.325725573964));
#198036=CARTESIAN_POINT('Ctrl Pts',(-13.7655785481758,6.05503262040511,
133.444564197323));
#198037=CARTESIAN_POINT('Ctrl Pts',(-14.0440261719886,5.49417107982388,
127.137184712));
#198038=CARTESIAN_POINT('Ctrl Pts',(-14.3224737958015,-0.115565277936756,
124.199760732389));
#198039=CARTESIAN_POINT('Ctrl Pts',(-14.6009214196144,-5.61910279095105,
127.331641394614));
#198040=CARTESIAN_POINT('Ctrl Pts',(-14.8793690434273,-5.95895934751375,
133.654781370965));
#198041=CARTESIAN_POINT('Ctrl Pts',(-15.1578166672402,-0.822823375059262,
137.358523925738));
#198042=CARTESIAN_POINT('Ctrl Pts',(-15.4362642910531,5.06944708191823,
135.039310588977));
#198043=CARTESIAN_POINT('Ctrl Pts',(-15.714711914866,6.3031433268707,128.828385117298));
#198044=CARTESIAN_POINT('Ctrl Pts',(-15.9931595386788,1.74455878009922,
124.433284598595));
#198045=CARTESIAN_POINT('Ctrl Pts',(-16.2716071624918,-4.41719005914895,
125.892891696959));
#198046=CARTESIAN_POINT('Ctrl Pts',(-16.5500547863046,-6.51975702577033,
131.865898794765));
#198047=CARTESIAN_POINT('Ctrl Pts',(-16.8285024101176,-2.63098579354628,
136.863404166748));
#198048=CARTESIAN_POINT('Ctrl Pts',(-17.1069500339304,3.67553285214529,
136.292944517765));
#198049=CARTESIAN_POINT('Ctrl Pts',(-17.3853976577434,6.60441636647752,
130.678744396729));
#198050=CARTESIAN_POINT('Ctrl Pts',(-17.6638452815562,3.46416388369313,
125.179979445948));
#198051=CARTESIAN_POINT('Ctrl Pts',(-17.9422929053691,-2.8594859743911,
124.849746025587));
#198052=CARTESIAN_POINT('Ctrl Pts',(-18.220740529182,-6.55540791566593,
129.991512516161));
#198053=CARTESIAN_POINT('Ctrl Pts',(-18.4991881529949,-4.22723023192423,
135.880246702087));
#198054=CARTESIAN_POINT('Ctrl Pts',(-18.7776357768078,1.98556552327847,
137.104489547159));
#198055=CARTESIAN_POINT('Ctrl Pts',(-19.0560834006207,6.37372356285652,
132.539221684343));
#198056=CARTESIAN_POINT('Ctrl Pts',(-19.3345310244336,4.90474102187576,
126.379701253833));
#198057=CARTESIAN_POINT('Ctrl Pts',(-19.6129786482465,-1.07145890828896,
124.286226621967));
#198058=CARTESIAN_POINT('Ctrl Pts',(-19.8914262720594,-6.06304044541393,
128.182598703507));
#198059=CARTESIAN_POINT('Ctrl Pts',(-20.1698738958722,-5.48298400919569,
134.488241903877));
#198060=CARTESIAN_POINT('Ctrl Pts',(-20.4483215196851,0.135666872813404,
137.408578169733));
#198061=CARTESIAN_POINT('Ctrl Pts',(-20.7267691434981,5.62964652640204,
134.25996113911));
#198062=CARTESIAN_POINT('Ctrl Pts',(-21.0052167673109,5.95025604574973,
127.935816044659));
#198063=CARTESIAN_POINT('Ctrl Pts',(-21.2836643911238,0.802870945221437,
124.247723276515));
#198064=CARTESIAN_POINT('Ctrl Pts',(-21.5621120149367,-5.08231333153929,
126.584859915257));
#198065=CARTESIAN_POINT('Ctrl Pts',(-21.8405596387496,-6.29709994142449,
132.79951156535));
#198066=CARTESIAN_POINT('Ctrl Pts',(-22.1190072625625,-1.725159335575,137.180716962973));
#198067=CARTESIAN_POINT('Ctrl Pts',(-22.3974548863754,4.43211842094896,
135.702362381491));
#198068=CARTESIAN_POINT('Ctrl Pts',(-22.6759025101882,6.51649586964294,
129.722983459651));
#198069=CARTESIAN_POINT('Ctrl Pts',(-22.9543501340012,2.61253196265622,
124.737337317723));
#198070=CARTESIAN_POINT('Ctrl Pts',(-23.232797757814,-3.6922211887298,125.326989197785));
#198071=CARTESIAN_POINT('Ctrl Pts',(-23.511245381627,-6.60400344270576,
130.950077828156));
#198072=CARTESIAN_POINT('Ctrl Pts',(-23.7896930054398,-3.4470291563393,
136.439259460675));
#198073=CARTESIAN_POINT('Ctrl Pts',(-24.0681406292527,2.87759652796706,
136.75024433649));
#198074=CARTESIAN_POINT('Ctrl Pts',(-24.3465882530656,6.55785158147733,
131.597252547181));
#198075=CARTESIAN_POINT('Ctrl Pts',(-24.6250358768785,4.21176140046998,
125.715631809479));
#198076=CARTESIAN_POINT('Ctrl Pts',(-24.9034835006914,-2.00473175158637,
124.510304248187));
#198077=CARTESIAN_POINT('Ctrl Pts',(-25.1819311245043,-6.3789743605254,
129.088907008606));
#198078=CARTESIAN_POINT('Ctrl Pts',(-25.4603787483172,-4.89125116236366,
135.24392783109));
#198079=CARTESIAN_POINT('Ctrl Pts',(-25.73882637213,1.09129290310671,137.319203269261));
#198080=CARTESIAN_POINT('Ctrl Pts',(-26.017273995943,6.07099210324431,133.407656578282));
#198081=CARTESIAN_POINT('Ctrl Pts',(-26.2957216197559,5.47174614495268,
127.103808077481));
#198082=CARTESIAN_POINT('Ctrl Pts',(-26.5741692435687,-0.155767210890682,
124.200586578976));
#198083=CARTESIAN_POINT('Ctrl Pts',(-26.8526168673816,-5.64013810957666,
127.365910809639));
#198084=CARTESIAN_POINT('Ctrl Pts',(-27.1310644911945,-5.94149762162655,
133.691002436174));
#198085=CARTESIAN_POINT('Ctrl Pts',(-27.4095121150075,-0.782911077696857,
137.363411251701));
#198086=CARTESIAN_POINT('Ctrl Pts',(-27.6879597388203,5.09513249930392,
135.008372961895));
#198087=CARTESIAN_POINT('Ctrl Pts',(-27.9664073626332,6.29099822050462,
128.79005270507));
#198088=CARTESIAN_POINT('Ctrl Pts',(-28.2448549864461,1.70574390941038,
124.422783015417));
#198089=CARTESIAN_POINT('Ctrl Pts',(-28.523302610259,-4.44700572420938,
125.919871384741));
#198090=CARTESIAN_POINT('Ctrl Pts',(-28.8017502340719,-6.51317434558802,
131.905566738465));
#198091=CARTESIAN_POINT('Ctrl Pts',(-29.0801978578848,-2.59405392962697,
136.879307463993));
#198092=CARTESIAN_POINT('Ctrl Pts',(-29.3586454816977,3.7088753210816,136.270468815306));
#198093=CARTESIAN_POINT('Ctrl Pts',(-29.6370931055106,6.6035293403484,130.638543767126));
#198094=CARTESIAN_POINT('Ctrl Pts',(-29.9155407293234,3.42986249617799,
125.158996303897));
#198095=CARTESIAN_POINT('Ctrl Pts',(-30.1939883531365,-2.89568042388203,
124.86726285355));
#198096=CARTESIAN_POINT('Ctrl Pts',(-30.4724359769491,-6.56023449624756,
130.031432204983));
#198097=CARTESIAN_POINT('Ctrl Pts',(-30.7508836007622,-4.19625355183344,
135.905885007927));
#198098=CARTESIAN_POINT('Ctrl Pts',(-31.029331224575,2.02387940833292,137.092286119451));
#198099=CARTESIAN_POINT('Ctrl Pts',(-31.3077788483879,6.38416606424714,
132.50039087698));
#198100=CARTESIAN_POINT('Ctrl Pts',(-31.5862264722008,4.8777159909692,126.349926681791));
#198101=CARTESIAN_POINT('Ctrl Pts',(-31.8646740960137,-1.11111678833609,
124.292869662384));
#198102=CARTESIAN_POINT('Ctrl Pts',(-32.1431217198266,-6.07888752023319,
128.219554726771));
#198103=CARTESIAN_POINT('Ctrl Pts',(-32.4215693436394,-5.46045759120085,
134.52155013001));
#198104=CARTESIAN_POINT('Ctrl Pts',(-32.7000169674524,0.175866105961793,
137.407629966116));
#198105=CARTESIAN_POINT('Ctrl Pts',(-32.9784645912652,5.65057744328232,
134.225627858545));
#198106=CARTESIAN_POINT('Ctrl Pts',(-33.2569122150782,5.93268415628106,
127.89964829471));
#198107=CARTESIAN_POINT('Ctrl Pts',(-33.535359838891,0.762943957391,124.242957452493));
#198108=CARTESIAN_POINT('Ctrl Pts',(-33.813807462704,-5.10790446645711,
126.615875576613));
#198109=CARTESIAN_POINT('Ctrl Pts',(-34.0922550865168,-6.28483822063666,
132.837806834499));
#198110=CARTESIAN_POINT('Ctrl Pts',(-34.3707027103298,-1.68631268146717,
137.191100358392));
#198111=CARTESIAN_POINT('Ctrl Pts',(-34.6491503341426,4.46185183101625,
135.675292070049));
#198112=CARTESIAN_POINT('Ctrl Pts',(-34.9275979579556,6.5097924843757,129.683335735103));
#198113=CARTESIAN_POINT('Ctrl Pts',(-35.2060455817684,2.57555186563646,
124.721546502031));
#198114=CARTESIAN_POINT('Ctrl Pts',(-35.4844932055813,-3.72549509491909,
125.349566279145));
#198115=CARTESIAN_POINT('Ctrl Pts',(-35.7629408293942,-6.60299406379731,
130.990275571749));
#198116=CARTESIAN_POINT('Ctrl Pts',(-36.0413884532071,-3.41266406223907,
136.460138103909));
#198117=CARTESIAN_POINT('Ctrl Pts',(-36.3198360770199,2.91373749460914,
136.73261742621));
#198118=CARTESIAN_POINT('Ctrl Pts',(-36.5982837008328,6.56255663790157,
131.557318352812));
#198119=CARTESIAN_POINT('Ctrl Pts',(-36.8767313246458,4.18070682967726,
125.690087904753));
#198120=CARTESIAN_POINT('Ctrl Pts',(-37.1551789484586,-2.04300831613737,
124.522624233657));
#198121=CARTESIAN_POINT('Ctrl Pts',(-37.4336265722715,-6.38929862592666,
129.12776941949));
#198122=CARTESIAN_POINT('Ctrl Pts',(-37.7120741960844,-4.86413563307991,
135.273620010322));
#198123=CARTESIAN_POINT('Ctrl Pts',(-37.9905218198973,1.13093038033133,
137.312439554669));
#198124=CARTESIAN_POINT('Ctrl Pts',(-38.2689694437102,6.0867266232385,133.370652493151));
#198125=CARTESIAN_POINT('Ctrl Pts',(-38.5474170675231,5.44911845251588,
127.070568568297));
#198126=CARTESIAN_POINT('Ctrl Pts',(-38.825864691336,-0.195963371833029,
124.201657130839));
#198127=CARTESIAN_POINT('Ctrl Pts',(-39.1043123151489,-5.66096443081045,
127.400307637685));
#198128=CARTESIAN_POINT('Ctrl Pts',(-39.3827599389617,-5.92381573136,133.727116535809));
#198129=CARTESIAN_POINT('Ctrl Pts',(-39.6612075627747,-0.742969769276543,
137.368055529631));
#198130=CARTESIAN_POINT('Ctrl Pts',(-39.9396551865875,5.12062911468111,
134.977279553588));
#198131=CARTESIAN_POINT('Ctrl Pts',(-40.2181028104005,6.27861999888597,
128.751794933764));
#198132=CARTESIAN_POINT('Ctrl Pts',(-40.4965504342133,1.66686583175366,
124.412517903944));
#198133=CARTESIAN_POINT('Ctrl Pts',(-40.7749980580263,-4.47665660383728,
125.947032069068));
#198134=CARTESIAN_POINT('Ctrl Pts',(-41.0534456818391,-6.5063503173351,
131.945193876568));
#198135=CARTESIAN_POINT('Ctrl Pts',(-41.3318933056519,-2.55702594208532,
136.894985651848));
#198136=CARTESIAN_POINT('Ctrl Pts',(-41.6103409294649,3.74208035627896,
136.247790564197));
#198137=CARTESIAN_POINT('Ctrl Pts',(-41.8887885532778,6.60239761801125,
130.598349281928));
#198138=CARTESIAN_POINT('Ctrl Pts',(-42.1672361770906,3.39543401384647,
125.138222352896));
#198139=CARTESIAN_POINT('Ctrl Pts',(-42.4456838009036,-2.93176757287012,
124.884999682853));
#198140=CARTESIAN_POINT('Ctrl Pts',(-42.7241314247165,-6.56481798492739,
130.071380534953));
#198141=CARTESIAN_POINT('Ctrl Pts',(-43.0025790485293,-4.16512137802412,
135.931334274905));
#198142=CARTESIAN_POINT('Ctrl Pts',(-43.2810266723423,2.06211829779186,
137.079849690351));
#198143=CARTESIAN_POINT('Ctrl Pts',(-43.5594742961552,6.39437199801655,
132.461497222591));
#198144=CARTESIAN_POINT('Ctrl Pts',(-43.837921919968,4.85051021450257,126.320317170437));
#198145=CARTESIAN_POINT('Ctrl Pts',(-44.116369543781,-1.150733495542,124.299753988494));
#198146=CARTESIAN_POINT('Ctrl Pts',(-44.3948171675938,-6.09450933963988,
128.256606530968));
#198147=CARTESIAN_POINT('Ctrl Pts',(-44.6732647914067,-5.43772883394191,
134.554720614319));
#198148=CARTESIAN_POINT('Ctrl Pts',(-44.9517124152196,0.216058822326645,
137.406437075925));
#198149=CARTESIAN_POINT('Ctrl Pts',(-45.2301600390324,5.67129897593744,
134.191167801664));
#198150=CARTESIAN_POINT('Ctrl Pts',(-45.5086076628454,5.91489242901924,
127.863588179946));
#198151=CARTESIAN_POINT('Ctrl Pts',(-45.7870552866582,0.722988698391639,
124.238434763679));
#198152=CARTESIAN_POINT('Ctrl Pts',(-46.0655029104712,-5.13330632609627,
126.647046443824));
#198153=CARTESIAN_POINT('Ctrl Pts',(-46.343950534284,-6.27234361285742,
132.876026753548));
#198154=CARTESIAN_POINT('Ctrl Pts',(-46.622398158097,-1.64740354042306,
137.201247090823));
#198155=CARTESIAN_POINT('Ctrl Pts',(-46.9008457819097,4.49141990552312,
135.64804126445));
#198156=CARTESIAN_POINT('Ctrl Pts',(-47.1792934057228,6.50284787635396,
129.643729550545));
#198157=CARTESIAN_POINT('Ctrl Pts',(-47.4577410295356,2.53847633059532,
124.705981087252));
#198158=CARTESIAN_POINT('Ctrl Pts',(-47.7361886533485,-3.75863095151733,
125.372345489915));
#198159=CARTESIAN_POINT('Ctrl Pts',(-48.0146362771614,-6.60174000851572,
131.030466426196));
#198160=CARTESIAN_POINT('Ctrl Pts',(-48.2930839009743,-3.37817251061699,
136.480807170229));
#198161=CARTESIAN_POINT('Ctrl Pts',(-48.5715315247872,2.94977049163681,
136.714770842195));
#198162=CARTESIAN_POINT('Ctrl Pts',(-48.8499791486,6.56701851637621,131.517356257317));
#198163=CARTESIAN_POINT('Ctrl Pts',(-49.128426772413,4.14949734125552,125.664733511282));
#198164=CARTESIAN_POINT('Ctrl Pts',(-49.4068743962258,-2.08120917626415,
124.535176991179));
#198165=CARTESIAN_POINT('Ctrl Pts',(-49.6853220200388,-6.39938613351776,
129.166693957078));
#198166=CARTESIAN_POINT('Ctrl Pts',(-49.9637696438516,-4.83683986146123,
135.303146579501));
#198167=CARTESIAN_POINT('Ctrl Pts',(-50.2422172676646,1.17052595051479,
137.305434680818));
#198168=CARTESIAN_POINT('Ctrl Pts',(-50.5206648914774,6.10223559733929,
133.333553313131));
#198169=CARTESIAN_POINT('Ctrl Pts',(-50.7991125152903,5.42628884099088,
127.03746741615));
#198170=CARTESIAN_POINT('Ctrl Pts',(-51.0775601391032,-0.236152271280866,
124.202972348307));
#198171=CARTESIAN_POINT('Ctrl Pts',(-51.3560077629162,-5.68158098292544,
127.434830604167));
#198172=CARTESIAN_POINT('Ctrl Pts',(-51.634455386729,-5.90591433192304,
133.763122331648));
#198173=CARTESIAN_POINT('Ctrl Pts',(-51.9129030105419,-0.703000929838195,
137.372456587432));
#198174=CARTESIAN_POINT('Ctrl Pts',(-52.1913506343548,5.14593598326309,
134.946031516236));
#198175=CARTESIAN_POINT('Ctrl Pts',(-52.4697982581677,6.26600912069438,
128.713613221033));
#198176=CARTESIAN_POINT('Ctrl Pts',(-52.7482458819806,1.62792598777083,
124.402489644555));
#198177=CARTESIAN_POINT('Ctrl Pts',(-53.0266935057934,-4.50614159930848,
125.97437274349));
#198178=CARTESIAN_POINT('Ctrl Pts',(-53.3051411296064,-6.49928519387843,
131.984778740675));
#198179=CARTESIAN_POINT('Ctrl Pts',(-53.5835887534191,-2.51990320300721,
136.910438149353));
#198180=CARTESIAN_POINT('Ctrl Pts',(-53.8620363772322,3.7751467273123,136.22491060479));
#198181=CARTESIAN_POINT('Ctrl Pts',(-54.140484001045,6.60102124140245,130.558162430556));
#198182=CARTESIAN_POINT('Ctrl Pts',(-54.418931624858,3.36087971245889,125.117658362733));
#198183=CARTESIAN_POINT('Ctrl Pts',(-54.6973792486707,-2.96774608413265,
124.902955856252));
#198184=CARTESIAN_POINT('Ctrl Pts',(-54.9758268724838,-6.56915821186243,
130.111356025769));
#198185=CARTESIAN_POINT('Ctrl Pts',(-55.2542744962966,-4.13383486411065,
135.956593559989));
#198186=CARTESIAN_POINT('Ctrl Pts',(-55.5327221201095,2.10028077469877,
137.067180720695));
#198187=CARTESIAN_POINT('Ctrl Pts',(-55.8111697439224,6.40434098598004,
132.422542162396));
#198188=CARTESIAN_POINT('Ctrl Pts',(-56.0896173677353,4.82312470059616,
126.29087381696));
#198189=CARTESIAN_POINT('Ctrl Pts',(-56.3680649915482,-1.19030756189505,
124.306879345194));
#198190=CARTESIAN_POINT('Ctrl Pts',(-56.646512615361,-6.10990532476174,
128.293752743129));
#198191=CARTESIAN_POINT('Ctrl Pts',(-56.924960239174,-5.41479857964128,
134.587752127659));
#198192=CARTESIAN_POINT('Ctrl Pts',(-57.2034078629868,0.256243532552689,
137.404999543363));
#198193=CARTESIAN_POINT('Ctrl Pts',(-57.4818554867998,5.69181035652338,
134.156582245398));
#198194=CARTESIAN_POINT('Ctrl Pts',(-57.7603031106126,5.89688152324325,
127.827637036585));
#198195=CARTESIAN_POINT('Ctrl Pts',(-58.0387507344255,0.683006648780185,
124.234155377662));
#198196=CARTESIAN_POINT('Ctrl Pts',(-58.3171983582384,-5.15851796918197,
126.67837136184));
#198197=CARTESIAN_POINT('Ctrl Pts',(-58.5956459820513,-6.25961658107885,
132.91416990625));
#198198=CARTESIAN_POINT('Ctrl Pts',(-58.8740936058642,-1.60843335423465,
137.211156784272));
#198199=CARTESIAN_POINT('Ctrl Pts',(-59.1525412296771,4.52082154881365,
135.620610974484));
#198200=CARTESIAN_POINT('Ctrl Pts',(-59.4309888534899,6.49566230291273,
129.604166373598));
#198201=CARTESIAN_POINT('Ctrl Pts',(-59.7094364773029,2.50130673138007,
124.69064165017));
#198202=CARTESIAN_POINT('Ctrl Pts',(-59.9878841011157,-3.79162753066369,
125.395325986002));
#198203=CARTESIAN_POINT('Ctrl Pts',(-60.2663317249287,-6.60024132333016,
131.070648902209));
#198204=CARTESIAN_POINT('Ctrl Pts',(-60.5447793487415,-3.34355577957023,
136.501265893734));
#198205=CARTESIAN_POINT('Ctrl Pts',(-60.8232269725544,2.98569418383416,
136.696705245755));
#198206=CARTESIAN_POINT('Ctrl Pts',(-61.1016745963673,6.57123705156454,
131.477367741508));
#198207=CARTESIAN_POINT('Ctrl Pts',(-61.3801222201802,4.11813409168408,
125.639569568584));
#198208=CARTESIAN_POINT('Ctrl Pts',(-61.6585698439931,-2.11933291641938,
124.547962055604));
#198209=CARTESIAN_POINT('Ctrl Pts',(-61.937017467806,-6.40923650950231,
129.205679179005));
#198210=CARTESIAN_POINT('Ctrl Pts',(-62.2154650916189,-4.80936485896274,
135.332506444514));
#198211=CARTESIAN_POINT('Ctrl Pts',(-62.4939127154318,1.21007814642843,
137.298188907278));
#198212=CARTESIAN_POINT('Ctrl Pts',(-62.7723603392447,6.1175184508558,133.296360412945));
#198213=CARTESIAN_POINT('Ctrl Pts',(-63.0508079630576,5.40325815633759,
127.004505847616));
#198214=CARTESIAN_POINT('Ctrl Pts',(-63.3292555868704,-0.276332420019459,
124.204532182646));
#198215=CARTESIAN_POINT('Ctrl Pts',(-63.6077032106833,-5.70198700196771,
127.469478429822));
#198216=CARTESIAN_POINT('Ctrl Pts',(-63.8861508344962,-5.8877940866586,
133.799018489484));
#198217=CARTESIAN_POINT('Ctrl Pts',(-64.1645984583092,-0.663006040441876,
137.376614262022));
#198218=CARTESIAN_POINT('Ctrl Pts',(-64.4430460821219,5.17105216729505,
134.914630007745));
#198219=CARTESIAN_POINT('Ctrl Pts',(-64.721493705935,6.25316605323042,128.675508981716));
#198220=CARTESIAN_POINT('Ctrl Pts',(-64.9999413297477,1.58892582039159,
124.392698608848));
#198221=CARTESIAN_POINT('Ctrl Pts',(-65.2783889535607,-4.53545961804555,
126.00189239489));
#198222=CARTESIAN_POINT('Ctrl Pts',(-65.5568365773735,-6.49197923701883,
132.024319863954));
#198223=CARTESIAN_POINT('Ctrl Pts',(-65.8352842011867,-2.48268708798906,
136.92566438391));
#198224=CARTESIAN_POINT('Ctrl Pts',(-66.1137318249993,3.80807320889562,
136.201829784909));
#198225=CARTESIAN_POINT('Ctrl Pts',(-66.3921794488124,6.59940026152389,
130.517984702147));
#198226=CARTESIAN_POINT('Ctrl Pts',(-66.6706270726251,3.3262008724376,125.097305095413));
#198227=CARTESIAN_POINT('Ctrl Pts',(-66.9490746964381,-3.00361462447264,
124.921130708376));
#198228=CARTESIAN_POINT('Ctrl Pts',(-67.227522320251,-6.57325501622426,
130.151357196124));
#198229=CARTESIAN_POINT('Ctrl Pts',(-67.5059699440638,-4.10239516942585,
135.981661927186));
#198230=CARTESIAN_POINT('Ctrl Pts',(-67.7844175678767,2.13836542492937,
137.054279679937));
#198231=CARTESIAN_POINT('Ctrl Pts',(-68.0628651916897,6.41407265873309,
132.383527139888));
#198232=CARTESIAN_POINT('Ctrl Pts',(-68.3413128155024,4.79556046403026,
126.261597712398));
#198233=CARTESIAN_POINT('Ctrl Pts',(-68.6197604393155,-1.22983752096341,
124.314245468451));
#198234=CARTESIAN_POINT('Ctrl Pts',(-68.8982080631282,-6.12507490509475,
128.330991986789));
#198235=CARTESIAN_POINT('Ctrl Pts',(-69.1766556869413,-5.39166767798822,
134.620643446035));
#198236=CARTESIAN_POINT('Ctrl Pts',(-69.455103310754,0.296418747580413,
137.403317421698));
#198237=CARTESIAN_POINT('Ctrl Pts',(-69.733550934567,5.7121108249834,134.121872471326));
#198238=CARTESIAN_POINT('Ctrl Pts',(-70.0119985583799,5.87865210635384,
127.791796196812));
#198239=CARTESIAN_POINT('Ctrl Pts',(-70.2904461821926,0.642999290106501,
124.230119453016));
#198240=CARTESIAN_POINT('Ctrl Pts',(-70.5688938060058,-5.18353846148724,
126.709849169906));
#198241=CARTESIAN_POINT('Ctrl Pts',(-70.8473414298183,-6.24665759690589,
132.95223487919));
#198242=CARTESIAN_POINT('Ctrl Pts',(-71.1257890536316,-1.56940356695681,
137.220829071533));
#198243=CARTESIAN_POINT('Ctrl Pts',(-71.4042366774442,4.55005567139915,
135.593002216589));
#198244=CARTESIAN_POINT('Ctrl Pts',(-71.6826843012574,6.48823603031619,
129.56464767029));
#198245=CARTESIAN_POINT('Ctrl Pts',(-71.9611319250699,2.46404444532374,
124.675528759193));
#198246=CARTESIAN_POINT('Ctrl Pts',(-72.2395795488831,-3.82448360965763,
125.418506915858));
#198247=CARTESIAN_POINT('Ctrl Pts',(-72.518027172696,-6.59849806377525,
131.110821510811));
#198248=CARTESIAN_POINT('Ctrl Pts',(-72.7964747965087,-3.30881515183405,
136.52151351632));
#198249=CARTESIAN_POINT('Ctrl Pts',(-73.0749224203217,3.02150724003593,
136.678421306317));
#198250=CARTESIAN_POINT('Ctrl Pts',(-73.3533700441346,6.57521208714753,
131.437354287172));
#198251=CARTESIAN_POINT('Ctrl Pts',(-73.6318176679474,4.08661824313884,
125.614597009117));
#198252=CARTESIAN_POINT('Ctrl Pts',(-73.9102652917603,-2.15737812391465,
124.56097895318));
#198253=CARTESIAN_POINT('Ctrl Pts',(-74.1887129155733,-6.41884938887091,
129.244723640663));
#198254=CARTESIAN_POINT('Ctrl Pts',(-74.4671605393861,-4.78171164368069,
135.361698517417));
#198255=CARTESIAN_POINT('Ctrl Pts',(-74.745608163199,1.24958550245192,137.290702502541));
#198256=CARTESIAN_POINT('Ctrl Pts',(-75.0240557870119,6.13257461747648,
133.25907517079));
#198257=CARTESIAN_POINT('Ctrl Pts',(-75.3025034108249,5.380027251966,126.971685084098));
#198258=CARTESIAN_POINT('Ctrl Pts',(-75.5809510346376,-0.31650232915867,
124.206336576053));
#198259=CARTESIAN_POINT('Ctrl Pts',(-75.8593986584506,-5.72218173178456,
127.504249830764));
#198260=CARTESIAN_POINT('Ctrl Pts',(-76.1378462822634,-5.86945566701928,
133.83480367917));
#198261=CARTESIAN_POINT('Ctrl Pts',(-76.4162939060764,-0.622986583113102,
137.380528399336));
#198262=CARTESIAN_POINT('Ctrl Pts',(-76.6947415298893,5.19597673608708,
134.88307619171));
#198263=CARTESIAN_POINT('Ctrl Pts',(-76.9731891537022,6.24009127239896,
128.637483627779));
#198264=CARTESIAN_POINT('Ctrl Pts',(-77.2516367775151,1.54986677478153,
124.383145159635));
#198265=CARTESIAN_POINT('Ctrl Pts',(-77.5300844013279,-4.56460957365852,
126.029590003516));
#198266=CARTESIAN_POINT('Ctrl Pts',(-77.8085320251407,-6.48443271748106,
132.063815781194));
#198267=CARTESIAN_POINT('Ctrl Pts',(-78.0869796489538,-2.44537897608793,
136.940663791305));
#198268=CARTESIAN_POINT('Ctrl Pts',(-78.3654272727665,3.84085858092573,
136.178548959823));
#198269=CARTESIAN_POINT('Ctrl Pts',(-78.6438748965796,6.5975347384416,130.477817585504));
#198270=CARTESIAN_POINT('Ctrl Pts',(-78.9223225203923,3.29139877882003,
125.077163305135));
#198271=CARTESIAN_POINT('Ctrl Pts',(-79.2007701442053,-3.03937186476788,
124.939523565746));
#198272=CARTESIAN_POINT('Ctrl Pts',(-79.4792177680182,-6.57710824620412,
130.191382563762));
#198273=CARTESIAN_POINT('Ctrl Pts',(-79.7576653918309,-4.07080345897965,
136.00653844758));
#198274=CARTESIAN_POINT('Ctrl Pts',(-80.036113015644,2.17637083724304,137.041147046131));
#198275=CARTESIAN_POINT('Ctrl Pts',(-80.314560639457,6.42356665566488,132.344453600785));
#198276=CARTESIAN_POINT('Ctrl Pts',(-80.5930082632696,4.76781852620778,
126.232489941585));
#198277=CARTESIAN_POINT('Ctrl Pts',(-80.8714558870828,-1.26932190795047,
124.321852085313));
#198278=CARTESIAN_POINT('Ctrl Pts',(-81.1499035108954,-6.14001751852468,
128.368322882032));
#198279=CARTESIAN_POINT('Ctrl Pts',(-81.4283511347085,-5.36833698610627,
134.653393350648));
#198280=CARTESIAN_POINT('Ctrl Pts',(-81.7067987585213,0.336582978702201,
137.401390773263));
#198281=CARTESIAN_POINT('Ctrl Pts',(-81.9852463823341,5.73219962907597,
134.087039765632));
#198282=CARTESIAN_POINT('Ctrl Pts',(-82.2636940061471,5.86020485384888,
127.756066988721));
#198283=CARTESIAN_POINT('Ctrl Pts',(-82.54214162996,0.602968104857597,124.226327139294));
#198284=CARTESIAN_POINT('Ctrl Pts',(-82.8205892537728,-5.20836687586887,
126.741478701599));
#198285=CARTESIAN_POINT('Ctrl Pts',(-83.0990368775859,-6.23346714053832,
132.990220261861));
#198286=CARTESIAN_POINT('Ctrl Pts',(-83.3774845013985,-1.53031562485268,
137.230263594196));
#198287=CARTESIAN_POINT('Ctrl Pts',(-83.6559321252116,4.57912118999838,
135.56521601382));
#198288=CARTESIAN_POINT('Ctrl Pts',(-83.9343797490243,6.48056933374724,
129.525174905002));
#198289=CARTESIAN_POINT('Ctrl Pts',(-84.2128273728376,2.42669085319518,
124.660642974335));
#198290=CARTESIAN_POINT('Ctrl Pts',(-84.4912749966499,-3.85719797100462,
125.441887420503));
#198291=CARTESIAN_POINT('Ctrl Pts',(-84.7697226204634,-6.59651029444787,
131.150982763393));
#198292=CARTESIAN_POINT('Ctrl Pts',(-85.0481702442759,-3.27395191473627,
136.541549287701));
#198293=CARTESIAN_POINT('Ctrl Pts',(-85.326617868089,3.05720833317481,136.659919701402));
#198294=CARTESIAN_POINT('Ctrl Pts',(-85.6050654919017,6.57894347582879,
131.397317377022));
#198295=CARTESIAN_POINT('Ctrl Pts',(-85.8835131157147,4.05495096345227,
125.58981675825));
#198296=CARTESIAN_POINT('Ctrl Pts',(-86.1619607395276,-2.19534338896908,
124.574227201559));
#198297=CARTESIAN_POINT('Ctrl Pts',(-86.4404083633404,-6.42822441541511,
129.283825895241));
#198298=CARTESIAN_POINT('Ctrl Pts',(-86.7188559871533,-4.75388124031539,
135.390721716488));
#198299=CARTESIAN_POINT('Ctrl Pts',(-86.9973036109663,1.28904655462414,
137.282975744021));
#198300=CARTESIAN_POINT('Ctrl Pts',(-87.2757512347791,6.14740353928957,
133.221698968287));
#198301=CARTESIAN_POINT('Ctrl Pts',(-87.554198858592,5.35659698870609,126.939006341782));
#198302=CARTESIAN_POINT('Ctrl Pts',(-87.8326464824051,-0.356660510187587,
124.208385461669));
#198303=CARTESIAN_POINT('Ctrl Pts',(-88.1110941062178,-5.74216442405318,
127.539143518524));
#198304=CARTESIAN_POINT('Ctrl Pts',(-88.3895417300309,-5.85089975254147,
133.870476574676));
#198305=CARTESIAN_POINT('Ctrl Pts',(-88.6679893538435,-0.582944040787213,
137.384198854334));
#198306=CARTESIAN_POINT('Ctrl Pts',(-88.9464369776566,5.22070876605056,
134.851371237371));
#198307=CARTESIAN_POINT('Ctrl Pts',(-89.2248846014694,6.22678526269035,
128.599538568266));
#198308=CARTESIAN_POINT('Ctrl Pts',(-89.5033322252823,1.51075029828878,
124.373829650922));
#198309=CARTESIAN_POINT('Ctrl Pts',(-89.7817798490951,-4.59359038598471,
126.057464543021));
#198310=CARTESIAN_POINT('Ctrl Pts',(-90.0602274729082,-6.47664591490472,
132.103265028861));
#198311=CARTESIAN_POINT('Ctrl Pts',(-90.338675096721,-2.40798024976945,
136.955435815729));
#198312=CARTESIAN_POINT('Ctrl Pts',(-90.6171227205338,3.87350162852866,
136.155068992212));
#198313=CARTESIAN_POINT('Ctrl Pts',(-90.8955703443469,6.59542474128344,
130.437662569033));
#198314=CARTESIAN_POINT('Ctrl Pts',(-91.1740179681596,3.25647472121003,
125.057233738258));
#198315=CARTESIAN_POINT('Ctrl Pts',(-91.4524655919725,-3.07501648002118,
124.958133746811));
#198316=CARTESIAN_POINT('Ctrl Pts',(-91.7309132157855,-6.58071775901922,
130.231430645527));
#198317=CARTESIAN_POINT('Ctrl Pts',(-92.0093608395982,-4.03906090341396,
136.031222199361));
#198318=CARTESIAN_POINT('Ctrl Pts',(-92.2878084634112,2.21429560333469,
137.027783305909));
#198319=CARTESIAN_POINT('Ctrl Pts',(-92.5662560872241,6.4328226249721,132.305322992969));
#198320=CARTESIAN_POINT('Ctrl Pts',(-92.844703711037,4.73989991511645,126.203551583122));
#198321=CARTESIAN_POINT('Ctrl Pts',(-93.1231513348499,-1.30875925974737,
124.329698913911));
#198322=CARTESIAN_POINT('Ctrl Pts',(-93.4015989586628,-6.15473261134757,
128.40574404555));
#198323=CARTESIAN_POINT('Ctrl Pts',(-93.6800465824757,-5.34480736852315,
134.686000627937));
#198324=CARTESIAN_POINT('Ctrl Pts',(-93.9584942062885,0.37673473761816,
137.399219669449));
#198325=CARTESIAN_POINT('Ctrl Pts',(-94.2369418301014,5.75207602440345,
134.052085419056));
#198326=CARTESIAN_POINT('Ctrl Pts',(-94.5153894539144,5.84154044929785,
127.720450736271));
#198327=CARTESIAN_POINT('Ctrl Pts',(-94.7938370777271,0.56291457640357,
124.222778577022));
#198328=CARTESIAN_POINT('Ctrl Pts',(-95.0722847015402,-5.23300229230026,
126.773258784876));
#198329=CARTESIAN_POINT('Ctrl Pts',(-95.350732325353,-6.22004570075364,
133.028124646699));
#198330=CARTESIAN_POINT('Ctrl Pts',(-95.6291799491659,-1.49117097634027,
137.239460002661));
#198331=CARTESIAN_POINT('Ctrl Pts',(-95.9076275729788,4.60801702757804,
135.537253395802));
#198332=CARTESIAN_POINT('Ctrl Pts',(-96.1860751967916,6.47266249729856,
129.48574954041));
#198333=CARTESIAN_POINT('Ctrl Pts',(-96.4645228206046,2.38924733914408,
124.645984847192));
#198334=CARTESIAN_POINT('Ctrl Pts',(-96.7429704444176,-3.88976940246256,
125.465466633565));
#198335=CARTESIAN_POINT('Ctrl Pts',(-97.0214180682302,-6.59427808900543,
131.191131171763));
#198336=CARTESIAN_POINT('Ctrl Pts',(-97.2998656920433,-3.23896736014657,
136.561372465446));
#198337=CARTESIAN_POINT('Ctrl Pts',(-97.5783133158561,3.09279614033489,
136.641201116591));
#198338=CARTESIAN_POINT('Ctrl Pts',(-97.856760939669,6.58243107933991,131.357258494642));
#198339=CARTESIAN_POINT('Ctrl Pts',(-98.135208563482,4.02313342606635,125.565229734223));
#198340=CARTESIAN_POINT('Ctrl Pts',(-98.4136561872948,-2.2332273047675,
124.587706309824));
#198341=CARTESIAN_POINT('Ctrl Pts',(-98.6921038111079,-6.43736124173946,
129.322984493793));
#198342=CARTESIAN_POINT('Ctrl Pts',(-98.9705514349205,-4.72587468013238,
135.419574966262));
#198343=CARTESIAN_POINT('Ctrl Pts',(-99.2489990587337,1.32845984070286,
137.275008918035));
#198344=CARTESIAN_POINT('Ctrl Pts',(-99.5274466825463,6.16200466680371,
133.184233190419));
#198345=CARTESIAN_POINT('Ctrl Pts',(-99.8058943063594,5.3329682347749,126.906470831589));
#198346=CARTESIAN_POINT('Ctrl Pts',(-100.084341930172,-0.396805475030165,
124.210678763569));
#198347=CARTESIAN_POINT('Ctrl Pts',(-100.362789553985,-5.76193433830736,
127.574158200105));
#198348=CARTESIAN_POINT('Ctrl Pts',(-100.641237177798,-5.83212703082168,
133.906035854126));
#198349=CARTESIAN_POINT('Ctrl Pts',(-100.919684801611,-0.542879897255484,
137.387625491007));
#198350=CARTESIAN_POINT('Ctrl Pts',(-101.198132425424,5.24524734073077,
134.819516319564));
#198351=CARTESIAN_POINT('Ctrl Pts',(-101.476580049237,6.21324851716398,
128.561675209245));
#198352=CARTESIAN_POINT('Ctrl Pts',(-101.75502767305,1.47157784038775,124.3647524279));
#198353=CARTESIAN_POINT('Ctrl Pts',(-102.033475296863,-4.62240098113028,
126.085514980508));
#198354=CARTESIAN_POINT('Ctrl Pts',(-102.311922920676,-6.4686191178319,
132.142666145147));
#198355=CARTESIAN_POINT('Ctrl Pts',(-102.590370544489,-2.3704922948573,
136.969979909799));
#198356=CARTESIAN_POINT('Ctrl Pts',(-102.868818168302,3.90600114210426,
136.131390752135));
#198357=CARTESIAN_POINT('Ctrl Pts',(-103.147265792114,6.59307034823604,
130.397521140692));
#198358=CARTESIAN_POINT('Ctrl Pts',(-103.425713415927,3.22142999373166,
125.037517133282));
#198359=CARTESIAN_POINT('Ctrl Pts',(-103.70416103974,-3.11054714940797,
124.976960561963));
#198360=CARTESIAN_POINT('Ctrl Pts',(-103.982608663553,-6.58408342091771,
130.271499957422));
#198361=CARTESIAN_POINT('Ctrl Pts',(-104.261056287366,-4.00716867896111,
136.055712267864));
#198362=CARTESIAN_POINT('Ctrl Pts',(-104.539503911179,2.25213831788793,
137.014188954471));
#198363=CARTESIAN_POINT('Ctrl Pts',(-104.817951534992,6.44184022367115,
132.266136766442));
#198364=CARTESIAN_POINT('Ctrl Pts',(-105.096399158805,4.71180566529118,
126.17478370933));
#198365=CARTESIAN_POINT('Ctrl Pts',(-105.374846782618,-1.34814811498862,
124.337785663482));
#198366=CARTESIAN_POINT('Ctrl Pts',(-105.65329440643,-6.16921963829011,
128.443254090687));
#198367=CARTESIAN_POINT('Ctrl Pts',(-105.931742030243,-5.32107969713743,
134.718464069627));
#198368=CARTESIAN_POINT('Ctrl Pts',(-106.210189654056,0.416872536489867,
137.396804190707));
#198369=CARTESIAN_POINT('Ctrl Pts',(-106.488637277869,5.77173927443855,
134.017010726842));
#198370=CARTESIAN_POINT('Ctrl Pts',(-106.767084901682,5.82265958431723,
127.684948759235));
#198371=CARTESIAN_POINT('Ctrl Pts',(-107.045532525495,0.52284018894291,
124.219473897692));
#198372=CARTESIAN_POINT('Ctrl Pts',(-107.323980149308,-5.25744379790729,
126.805188242113));
#198373=CARTESIAN_POINT('Ctrl Pts',(-107.602427773121,-6.20639377488812,
133.065946629143));
#198374=CARTESIAN_POINT('Ctrl Pts',(-107.880875396933,-1.45197107193893,
137.248417956151));
#198375=CARTESIAN_POINT('Ctrl Pts',(-108.159323020746,4.63674211339212,
135.509115398702));
#198376=CARTESIAN_POINT('Ctrl Pts',(-108.437770644559,6.46451581396073,
129.446373037437));
#198377=CARTESIAN_POINT('Ctrl Pts',(-108.716218268372,2.35171529065418,
124.631554920928));
#198378=CARTESIAN_POINT('Ctrl Pts',(-108.994665892185,-3.92219669708481,
125.489243681306));
#198379=CARTESIAN_POINT('Ctrl Pts',(-109.273113515998,-6.59180153016358,
131.231265248209));
#198380=CARTESIAN_POINT('Ctrl Pts',(-109.551561139811,-3.20386278442967,
136.580982315001));
#198381=CARTESIAN_POINT('Ctrl Pts',(-109.830008763624,3.12826934279688,
136.622266245509));
#198382=CARTESIAN_POINT('Ctrl Pts',(-110.108456387437,6.5856747684467,131.317179124427));
#198383=CARTESIAN_POINT('Ctrl Pts',(-110.38690401125,3.99116680999183,125.540836848117));
#198384=CARTESIAN_POINT('Ctrl Pts',(-110.665351635062,-2.27102846750687,
124.601415778499));
#198385=CARTESIAN_POINT('Ctrl Pts',(-110.943799258875,-6.44625952927566,
129.362197985281));
#198386=CARTESIAN_POINT('Ctrl Pts',(-111.222246882688,-4.69769300092514,
135.448257197571));
#198387=CARTESIAN_POINT('Ctrl Pts',(-111.500694506501,1.36782390021364,
137.266802319797));
#198388=CARTESIAN_POINT('Ctrl Pts',(-111.779142130314,6.17637745896884,
133.1466792255));
#198389=CARTESIAN_POINT('Ctrl Pts',(-112.057589754127,5.30914186574463,
126.874079759138));
#198390=CARTESIAN_POINT('Ctrl Pts',(-112.33603737794,-0.436935736099303,
124.213216396775));
#198391=CARTESIAN_POINT('Ctrl Pts',(-112.614485001753,-5.78149074196569,
127.609292578024));
#198392=CARTESIAN_POINT('Ctrl Pts',(-112.892932625565,-5.81313819748998,
133.94148019986));
#198393=CARTESIAN_POINT('Ctrl Pts',(-113.171380249379,-0.502795637109545,
137.390808182378));
#198394=CARTESIAN_POINT('Ctrl Pts',(-113.449827873191,5.26959155084185,
134.787512618686));
#198395=CARTESIAN_POINT('Ctrl Pts',(-113.728275497004,6.19948153742887,
128.523894953756));
#198396=CARTESIAN_POINT('Ctrl Pts',(-114.006723120817,1.43235085262869,
124.355913826926));
#198397=CARTESIAN_POINT('Ctrl Pts',(-114.28517074463,-4.65104029150761,
126.113740276555));
#198398=CARTESIAN_POINT('Ctrl Pts',(-114.563618368443,-6.46035262369882,
132.182017670029));
#198399=CARTESIAN_POINT('Ctrl Pts',(-114.842065992256,-2.33291650048142,
136.984295534578));
#198400=CARTESIAN_POINT('Ctrl Pts',(-115.120513616069,3.93835591737112,
136.107515116997));
#198401=CARTESIAN_POINT('Ctrl Pts',(-115.398961239881,6.59047164654225,
130.357394787938));
#198402=CARTESIAN_POINT('Ctrl Pts',(-115.677408863695,3.18626589498021,
125.018014220813));
#198403=CARTESIAN_POINT('Ctrl Pts',(-115.955856487507,-3.14596255632626,
124.996003313566));
#198404=CARTESIAN_POINT('Ctrl Pts',(-116.23430411132,-6.58720510718372,
130.311589014666));
#198405=CARTESIAN_POINT('Ctrl Pts',(-116.512751735133,-3.97512796739924,
136.0800077456));
#198406=CARTESIAN_POINT('Ctrl Pts',(-116.791199358946,2.28989757862811,
137.00036449556));
#198407=CARTESIAN_POINT('Ctrl Pts',(-117.069646982759,6.45061911761184,
132.226896373261));
#198408=CARTESIAN_POINT('Ctrl Pts',(-117.348094606572,4.68353681777373,
126.146187386213));
#198409=CARTESIAN_POINT('Ctrl Pts',(-117.626542230384,-1.38748701410568,
124.346112034364));
#198410=CARTESIAN_POINT('Ctrl Pts',(-117.904989854198,-6.18347806253024,
128.480851627495));
#198411=CARTESIAN_POINT('Ctrl Pts',(-118.18343747801,-5.29715485118671,
134.750782472776));
#198412=CARTESIAN_POINT('Ctrl Pts',(-118.461885101824,0.45699488799644,
137.394144426544));
#198413=CARTESIAN_POINT('Ctrl Pts',(-118.740332725636,5.79118865055225,
133.981816988697));
#198414=CARTESIAN_POINT('Ctrl Pts',(-119.018780349449,5.80356295854445,
127.649562373154));
#198415=CARTESIAN_POINT('Ctrl Pts',(-119.297227973262,0.482746427446748,
124.216413223762));
#198416=CARTESIAN_POINT('Ctrl Pts',(-119.575675597075,-5.28169048700048,
126.837265890154));
#198417=CARTESIAN_POINT('Ctrl Pts',(-119.854123220888,-6.19251186881905,
133.103684807684));
#198418=CARTESIAN_POINT('Ctrl Pts',(-120.132570844701,-1.41271736421608,
137.257137122728));
#198419=CARTESIAN_POINT('Ctrl Pts',(-120.411018468513,4.66529538302207,
135.480803065184));
#198420=CARTESIAN_POINT('Ctrl Pts',(-120.689466092327,6.45612958561205,
129.407046855192));
#198421=CARTESIAN_POINT('Ctrl Pts',(-120.967913716139,2.31409609848935,
124.61735373025));
#198422=CARTESIAN_POINT('Ctrl Pts',(-121.246361339953,-3.95447865326606,
125.51321768266));
#198423=CARTESIAN_POINT('Ctrl Pts',(-121.524808963765,-6.5890807096919,
131.271383505546));
#198424=CARTESIAN_POINT('Ctrl Pts',(-121.803256587578,-3.16863948839908,
136.600378109714));
#198425=CARTESIAN_POINT('Ctrl Pts',(-122.081704211391,3.16362662608795,
136.603115789794));
#198426=CARTESIAN_POINT('Ctrl Pts',(-122.360151835204,6.58867442295306,
131.277080751534));
#198427=CARTESIAN_POINT('Ctrl Pts',(-122.638599459017,3.9590522997634,125.51663900382));
#198428=CARTESIAN_POINT('Ctrl Pts',(-122.91704708283,-2.30874547645122,
124.615355099576));
#198429=CARTESIAN_POINT('Ctrl Pts',(-123.195494706643,-6.45491894829438,
129.401464916637));
#198430=CARTESIAN_POINT('Ctrl Pts',(-123.473942330455,-4.66933724697619,
135.476767347585));
#198431=CARTESIAN_POINT('Ctrl Pts',(-123.752389954268,1.40713727450679,
137.258356253404));
#198432=CARTESIAN_POINT('Ctrl Pts',(-124.030837578081,6.19052138319586,
133.109038465103));
#198433=CARTESIAN_POINT('Ctrl Pts',(-124.309285201894,5.28511876451003,
126.841834324687));
#198434=CARTESIAN_POINT('Ctrl Pts',(-124.587732825707,-0.477049806354697,
124.215998267256));
#198435=CARTESIAN_POINT('Ctrl Pts',(-124.86618044952,-5.80083291035842,
127.644545350364));
#198436=CARTESIAN_POINT('Ctrl Pts',(-125.144628073333,-5.79393395618462,
133.976808298475));
#198437=CARTESIAN_POINT('Ctrl Pts',(-125.423075697146,-0.462692745686338,
137.393746810514));
#198438=CARTESIAN_POINT('Ctrl Pts',(-125.701523320958,5.2937404943001,134.755361320645));
#198439=CARTESIAN_POINT('Ctrl Pts',(-125.979970944772,6.18548483362552,
128.486199201761));
#198440=CARTESIAN_POINT('Ctrl Pts',(-126.258418568584,1.39307078858202,
124.34731417552));
#198441=CARTESIAN_POINT('Ctrl Pts',(-126.536866192397,-4.67950725587653,
126.142139385264));
#198442=CARTESIAN_POINT('Ctrl Pts',(-126.81531381621,-6.45184673882346,
132.221318145323));
#198443=CARTESIAN_POINT('Ctrl Pts',(-127.093761440023,-2.29525425902701,
136.998382159598));
#198444=CARTESIAN_POINT('Ctrl Pts',(-127.372209063836,3.97056475541062,
136.083442971518));
#198445=CARTESIAN_POINT('Ctrl Pts',(-127.650656687649,6.58762873249828,
130.317284997668));
#198446=CARTESIAN_POINT('Ctrl Pts',(-127.929104311462,3.15098372797424,
124.998725723536));
#198447=CARTESIAN_POINT('Ctrl Pts',(-128.207551935275,-3.18126138844507,
125.015261295985));
#198448=CARTESIAN_POINT('Ctrl Pts',(-128.485999559087,-6.59008270214206,
130.351696331743));
#198449=CARTESIAN_POINT('Ctrl Pts',(-128.764447182901,-3.94293995600869,
136.104107732291));
#198450=CARTESIAN_POINT('Ctrl Pts',(-129.042894806713,2.32757198637139,
136.986310441447));
#198451=CARTESIAN_POINT('Ctrl Pts',(-129.321342430526,6.45915898148892,
132.187603267495));
#198452=CARTESIAN_POINT('Ctrl Pts',(-129.599790054339,4.6550944200771,126.117763673416));
#198453=CARTESIAN_POINT('Ctrl Pts',(-129.878237678152,-1.42677449938118,
124.354677718024));
#198454=CARTESIAN_POINT('Ctrl Pts',(-130.156685301965,-6.19750735571679,
128.518535262782));
#198455=CARTESIAN_POINT('Ctrl Pts',(-130.435132925778,-5.27303371721495,
134.782954639811));
#198456=CARTESIAN_POINT('Ctrl Pts',(-130.713580549591,0.497100305389368,
137.391240475519));
#198457=CARTESIAN_POINT('Ctrl Pts',(-130.992028173403,5.81042343204081,
133.946505508738));
#198458=CARTESIAN_POINT('Ctrl Pts',(-131.270475797217,5.78425127961196,
127.614292889281));
#198459=CARTESIAN_POINT('Ctrl Pts',(-131.548923421029,0.442634777604211,
124.213596668645));
#198460=CARTESIAN_POINT('Ctrl Pts',(-131.827371044842,-5.30574146111081,
126.869490540348));
#198461=CARTESIAN_POINT('Ctrl Pts',(-132.105818668655,-6.17840049694519,
133.141337783923));
#198462=CARTESIAN_POINT('Ctrl Pts',(-132.384266292468,-1.37341130773126,
137.265617179298));
#198463=CARTESIAN_POINT('Ctrl Pts',(-132.662713916281,4.69367577841589,
135.45231744437));
#198464=CARTESIAN_POINT('Ctrl Pts',(-132.941161540094,6.44750412300737,
129.367772450924));
#198465=CARTESIAN_POINT('Ctrl Pts',(-133.219609163907,2.27639115664257,
124.603381801387));
#198466=CARTESIAN_POINT('Ctrl Pts',(-133.49805678772,-3.98661407478655,
125.537387749261));
#198467=CARTESIAN_POINT('Ctrl Pts',(-133.776504411532,-6.58611572841139,
131.311484457178));
#198468=CARTESIAN_POINT('Ctrl Pts',(-134.054952035345,-3.13329877726696,
136.619559130867));
#198469=CARTESIAN_POINT('Ctrl Pts',(-134.333399659158,3.19886668003099,
136.583750459073));
#198470=CARTESIAN_POINT('Ctrl Pts',(-134.611847282971,6.59142993170542,
131.236964861823));
#198471=CARTESIAN_POINT('Ctrl Pts',(-134.890294906784,3.92679108539655,
125.492637097993));
#198472=CARTESIAN_POINT('Ctrl Pts',(-135.168742530597,-2.34637693398254,
124.629523756529));
#198473=CARTESIAN_POINT('Ctrl Pts',(-135.44719015441,-6.46333917791768,
129.440783832808));
#198474=CARTESIAN_POINT('Ctrl Pts',(-135.725637778223,-4.64080846901838,
135.505104359849));
#198475=CARTESIAN_POINT('Ctrl Pts',(-136.004085402036,1.44639850681073,
137.24967103183));
#198476=CARTESIAN_POINT('Ctrl Pts',(-136.282533025848,6.20443591537649,
133.07131230402));
#198477=CARTESIAN_POINT('Ctrl Pts',(-136.560980649661,5.26089982125598,
126.809735723105));
#198478=CARTESIAN_POINT('Ctrl Pts',(-136.839428273474,-0.517146199354053,
124.219024271924));
#198479=CARTESIAN_POINT('Ctrl Pts',(-137.117875897287,-5.81996012675442,
127.679915210822));
#198480=CARTESIAN_POINT('Ctrl Pts',(-137.3963235211,-5.77451501852576,134.012018840873));
#198481=CARTESIAN_POINT('Ctrl Pts',(-137.674771144913,-0.422572709013315,
137.396441266521));
#198482=CARTESIAN_POINT('Ctrl Pts',(-137.953218768726,5.31769327625758,
134.723063616821));
#198483=CARTESIAN_POINT('Ctrl Pts',(-138.231666392539,6.17125892440694,
128.448589350091));
#198484=CARTESIAN_POINT('Ctrl Pts',(-138.510114016352,1.35373910378499,
124.338953792345));
#198485=CARTESIAN_POINT('Ctrl Pts',(-138.788561640165,-4.70780081938319,
126.170711254294));
#198486=CARTESIAN_POINT('Ctrl Pts',(-139.067009263977,-6.44310177839452,
132.260566114734));
#198487=CARTESIAN_POINT('Ctrl Pts',(-139.34545688779,-2.25750696608163,
137.012239262869));
#198488=CARTESIAN_POINT('Ctrl Pts',(-139.623904511603,4.00262646271346,
136.059175207703));
#198489=CARTESIAN_POINT('Ctrl Pts',(-139.902352135416,6.5845417114487,130.277193256163));
#198490=CARTESIAN_POINT('Ctrl Pts',(-140.180799759229,3.11558480010749,
124.979652356196));
#198491=CARTESIAN_POINT('Ctrl Pts',(-140.459247383042,-3.21644233775325,
125.034733795609));
#198492=CARTESIAN_POINT('Ctrl Pts',(-140.737695006855,-6.59271609916233,
130.391820422461));
#198493=CARTESIAN_POINT('Ctrl Pts',(-141.016142630668,-3.91060583752806,
136.128011334905));
#198494=CARTESIAN_POINT('Ctrl Pts',(-141.294590254481,2.36516014507876,
136.97202731291));
#198495=CARTESIAN_POINT('Ctrl Pts',(-141.573037878293,6.46745949885459,
132.148258905163));
#198496=CARTESIAN_POINT('Ctrl Pts',(-141.851485502106,4.62647952614482,
126.089513624195));
#198497=CARTESIAN_POINT('Ctrl Pts',(-142.129933125919,-1.4660091150024,
124.363482397054));
#198498=CARTESIAN_POINT('Ctrl Pts',(-142.408380749732,-6.21130699798892,
128.556303600169));
#198499=CARTESIAN_POINT('Ctrl Pts',(-142.686828373545,-5.24871718904012,
134.814979378581));
#198500=CARTESIAN_POINT('Ctrl Pts',(-142.965275997358,0.537187302547703,
137.388092445238));
#198501=CARTESIAN_POINT('Ctrl Pts',(-143.243723621171,5.82944290615228,
133.911077595444));
#198502=CARTESIAN_POINT('Ctrl Pts',(-143.522171244983,5.76472526312116,
127.579141614542));
#198503=CARTESIAN_POINT('Ctrl Pts',(-143.800618868797,0.402506725767204,
124.21102433671));
#198504=CARTESIAN_POINT('Ctrl Pts',(-144.079066492609,-5.32959582902011,
126.901860998601));
#198505=CARTESIAN_POINT('Ctrl Pts',(-144.357514116423,-6.1640601821688,
133.178904162615));
#198506=CARTESIAN_POINT('Ctrl Pts',(-144.635961740235,-1.33405435898536,
137.27385781163));
#198507=CARTESIAN_POINT('Ctrl Pts',(-144.914409364048,4.72188224792766,
135.423659591808));
#198508=CARTESIAN_POINT('Ctrl Pts',(-145.192856987861,6.43863974576633,
129.328551279958));
#198509=CARTESIAN_POINT('Ctrl Pts',(-145.471304611674,2.23860186228433,
124.589639652074));
#198510=CARTESIAN_POINT('Ctrl Pts',(-145.749752235487,-4.01860177085642,
125.56175298548));
#198511=CARTESIAN_POINT('Ctrl Pts',(-146.0281998593,-6.58290669619051,131.35156661715));
#198512=CARTESIAN_POINT('Ctrl Pts',(-146.306647483113,-3.09784196059638,
136.638524667701));
#198513=CARTESIAN_POINT('Ctrl Pts',(-146.585095106925,3.2339881987928,136.564170970937));
#198514=CARTESIAN_POINT('Ctrl Pts',(-146.863542730738,6.59394119259793,
131.196832941802));
#198515=CARTESIAN_POINT('Ctrl Pts',(-147.141990354551,3.89438436234147,
125.468832020033));
#198516=CARTESIAN_POINT('Ctrl Pts',(-147.420437978364,-2.38392144565404,
124.643921224334));
#198517=CARTESIAN_POINT('Ctrl Pts',(-147.698885602177,-6.47151990613084,
129.480153276819));
#198518=CARTESIAN_POINT('Ctrl Pts',(-147.97733322599,-4.61210772419611,
135.533267184325));
#198519=CARTESIAN_POINT('Ctrl Pts',(-148.255780849803,1.48560614228611,
137.240746976909));
#198520=CARTESIAN_POINT('Ctrl Pts',(-148.534228473616,6.21812053990256,
133.033502140209));
#198521=CARTESIAN_POINT('Ctrl Pts',(-148.812676097428,5.23648593342438,
126.777785143819));
#198522=CARTESIAN_POINT('Ctrl Pts',(-149.091123721242,-0.557223429310831,
124.222294298654));
#198523=CARTESIAN_POINT('Ctrl Pts',(-149.369571345054,-5.83887168238761,
127.715400848752));
#198524=CARTESIAN_POINT('Ctrl Pts',(-149.648018968867,-5.75488210408933,
134.047110522317));
#198525=CARTESIAN_POINT('Ctrl Pts',(-149.92646659268,-0.382437013753756,
137.398891450554));
#198526=CARTESIAN_POINT('Ctrl Pts',(-150.204914216493,5.34144900913504,
134.690620704017));
#198527=CARTESIAN_POINT('Ctrl Pts',(-150.483361840306,6.15680433691945,
128.411066792389));
#198528=CARTESIAN_POINT('Ctrl Pts',(-150.761809464119,1.31435725568762,
124.330832987197));
#198529=CARTESIAN_POINT('Ctrl Pts',(-151.040257087932,-4.73591993359918,
126.199454824906));
#198530=CARTESIAN_POINT('Ctrl Pts',(-151.318704711745,-6.43411806645975,
132.299760123916));
#198531=CARTESIAN_POINT('Ctrl Pts',(-151.597152335558,-2.21967602038541,
137.025866330917));
#198532=CARTESIAN_POINT('Ctrl Pts',(-151.87559995937,4.03453985122072,136.034712724799));
#198533=CARTESIAN_POINT('Ctrl Pts',(-152.154047583183,6.58121069778455,
130.237121049039));
#198534=CARTESIAN_POINT('Ctrl Pts',(-152.432495206996,3.08007042310019,
124.960794825562));
#198535=CARTESIAN_POINT('Ctrl Pts',(-152.710942830809,-3.25150410060774,
125.054420090877));
#198536=CARTESIAN_POINT('Ctrl Pts',(-152.989390454622,-6.59510520066311,
130.431959800007));
#198537=CARTESIAN_POINT('Ctrl Pts',(-153.267838078435,-3.87812681010997,
136.151717667683));
#198538=CARTESIAN_POINT('Ctrl Pts',(-153.546285702248,2.40266066190714,
136.957515639215));
#198539=CARTESIAN_POINT('Ctrl Pts',(-153.824733326061,6.47552036213011,
132.108864744186));
#198540=CARTESIAN_POINT('Ctrl Pts',(-154.103180949873,4.59769319631231,
126.061438285362));
#198541=CARTESIAN_POINT('Ctrl Pts',(-154.381628573686,-1.50518940711724,
124.372525745196));
#198542=CARTESIAN_POINT('Ctrl Pts',(-154.660076197499,-6.22487647799626,
128.594155240135));
#198543=CARTESIAN_POINT('Ctrl Pts',(-154.938523821312,-5.22420616771914,
134.846855502398));
#198544=CARTESIAN_POINT('Ctrl Pts',(-155.216971445125,0.577254394032953,
137.384700452354));
#198545=CARTESIAN_POINT('Ctrl Pts',(-155.495419068938,5.84824636811312,
133.87553456161));
#198546=CARTESIAN_POINT('Ctrl Pts',(-155.773866692751,5.74498563261573,
127.544109851479));
#198547=CARTESIAN_POINT('Ctrl Pts',(-156.052314316564,0.362363758895462,
124.208696323275));
#198548=CARTESIAN_POINT('Ctrl Pts',(-156.330761940377,-5.353252706796,126.934376065411));
#198549=CARTESIAN_POINT('Ctrl Pts',(-156.60920956419,-6.14949145587554,
133.216382551721));
#198550=CARTESIAN_POINT('Ctrl Pts',(-156.887657188002,-1.29464797636456,
137.281858714364));
#198551=CARTESIAN_POINT('Ctrl Pts',(-157.166104811815,4.74991374635575,
135.394830569423));
#198552=CARTESIAN_POINT('Ctrl Pts',(-157.444552435628,6.42953678236183,
129.28938479565));
#198553=CARTESIAN_POINT('Ctrl Pts',(-157.723000059441,2.20072961571137,
124.576127791533));
#198554=CARTESIAN_POINT('Ctrl Pts',(-158.001447683254,-4.05044055615985,
125.586312488451));
#198555=CARTESIAN_POINT('Ctrl Pts',(-158.279895307067,-6.57945373194114,
131.391628500203));
#198556=CARTESIAN_POINT('Ctrl Pts',(-158.55834293088,-3.06227035225273,
136.657274017441));
#198557=CARTESIAN_POINT('Ctrl Pts',(-158.836790554693,3.2689898809326,136.54437805091));
#198558=CARTESIAN_POINT('Ctrl Pts',(-159.115238178505,6.59620811257463,
131.156686478575));
#198559=CARTESIAN_POINT('Ctrl Pts',(-159.393685802319,3.86183333144169,
125.445224652049));
#198560=CARTESIAN_POINT('Ctrl Pts',(-159.672133426131,-2.42137762023968,
124.658546969484));
#198561=CARTESIAN_POINT('Ctrl Pts',(-159.950581049944,-6.47946082979399,
129.519571789819));
#198562=CARTESIAN_POINT('Ctrl Pts',(-160.229028673757,-4.58323607602601,
135.56125477743));
#198563=CARTESIAN_POINT('Ctrl Pts',(-160.50747629757,1.52475872807955,137.231584419323));
#198564=CARTESIAN_POINT('Ctrl Pts',(-160.785923921383,6.23157474968534,
132.99560937474));
#198565=CARTESIAN_POINT('Ctrl Pts',(-161.064371545196,5.2118780056808,126.745983770767));
#198566=CARTESIAN_POINT('Ctrl Pts',(-161.342819169009,-0.597280011148509,
124.225808226271));
#198567=CARTESIAN_POINT('Ctrl Pts',(-161.621266792821,-5.85756687648338,
127.751000949223));
#198568=CARTESIAN_POINT('Ctrl Pts',(-161.899714416635,-5.73503594038016,
134.08208204247));
#198569=CARTESIAN_POINT('Ctrl Pts',(-162.178162040447,-0.342287147149402,
137.401097271823));
#198570=CARTESIAN_POINT('Ctrl Pts',(-162.45660966426,5.36500681265522,134.658033784415));
#198571=CARTESIAN_POINT('Ctrl Pts',(-162.735057288073,6.14212160678308,
128.373632919072));
#198572=CARTESIAN_POINT('Ctrl Pts',(-163.013504911886,1.27492670359879,
124.322952060995));
#198573=CARTESIAN_POINT('Ctrl Pts',(-163.291952535699,-4.76386355656041,
126.228369031995));
#198574=CARTESIAN_POINT('Ctrl Pts',(-163.570400159512,-6.42489593591386,
132.338898720518));
#198575=CARTESIAN_POINT('Ctrl Pts',(-163.848847783325,-2.18176282377798,
137.039262858781));
#198576=CARTESIAN_POINT('Ctrl Pts',(-164.127295407138,4.06630373837012,
136.010056429275));
#198577=CARTESIAN_POINT('Ctrl Pts',(-164.405743030951,6.57763581493773,
130.197069861187));
#198578=CARTESIAN_POINT('Ctrl Pts',(-164.684190654763,3.04444191295097,
124.942153830408));
#198579=CARTESIAN_POINT('Ctrl Pts',(-164.962638278576,-3.28644537778151,
125.074319452304));
#198580=CARTESIAN_POINT('Ctrl Pts',(-165.241085902389,-6.59724991811553,
130.472112977002));
#198581=CARTESIAN_POINT('Ctrl Pts',(-165.519533526202,-3.84550407727676,
136.175225852179));
#198582=CARTESIAN_POINT('Ctrl Pts',(-165.797981150015,2.44007214726114,
136.942775958099));
#198583=CARTESIAN_POINT('Ctrl Pts',(-166.076428773828,6.48334127261722,
132.069422244329));
#198584=CARTESIAN_POINT('Ctrl Pts',(-166.354876397641,4.56873649726763,
126.03353869726));
#198585=CARTESIAN_POINT('Ctrl Pts',(-166.633324021454,-1.54431392388507,
124.381807427344));
#198586=CARTESIAN_POINT('Ctrl Pts',(-166.911771645267,-6.23821529291649,
128.632088780075));
#198587=CARTESIAN_POINT('Ctrl Pts',(-167.19021926908,-5.19950156151742,
134.878581830081));
#198588=CARTESIAN_POINT('Ctrl Pts',(-167.468666892892,0.617300095144361,
137.381064622557));
#198589=CARTESIAN_POINT('Ctrl Pts',(-167.747114516705,5.86683312115408,
133.839877724298));
#198590=CARTESIAN_POINT('Ctrl Pts',(-168.025562140518,5.72503311955499,
127.509198898206));
#198591=CARTESIAN_POINT('Ctrl Pts',(-168.304009764331,0.32220736450136,
124.206612714607));
#198592=CARTESIAN_POINT('Ctrl Pts',(-168.582457388144,-5.37671121782417,
126.967034535923));
#198593=CARTESIAN_POINT('Ctrl Pts',(-168.860905011957,-6.1346948579149,
133.253771562468));
#198594=CARTESIAN_POINT('Ctrl Pts',(-169.13935263577,-1.25519362008691,
137.289619591024));
#198595=CARTESIAN_POINT('Ctrl Pts',(-169.417800259582,4.77776923498369,
135.365831445486));
#198596=CARTESIAN_POINT('Ctrl Pts',(-169.696247883396,6.42019557010726,
129.250274449328));
#198597=CARTESIAN_POINT('Ctrl Pts',(-169.974695507208,2.16277582029264,
124.562846720449));
#198598=CARTESIAN_POINT('Ctrl Pts',(-170.253143131021,-4.08212925089891,
125.611065348116));
#198599=CARTESIAN_POINT('Ctrl Pts',(-170.531590754834,-6.57575696361412,
131.431668621828));
#198600=CARTESIAN_POINT('Ctrl Pts',(-170.810038378647,-3.02658527035502,
136.675806485322));
#198601=CARTESIAN_POINT('Ctrl Pts',(-171.08848600246,3.30387042945021,136.524372432426));
#198602=CARTESIAN_POINT('Ctrl Pts',(-171.366933626273,6.59823060763395,
131.116526959784));
#198603=CARTESIAN_POINT('Ctrl Pts',(-171.645381250086,3.82913919888762,
125.421815868818));
#198604=CARTESIAN_POINT('Ctrl Pts',(-171.923828873899,-2.45874406978715,
124.673400450021));
#198605=CARTESIAN_POINT('Ctrl Pts',(-172.202276497711,-6.48716165465291,
129.559037911142));
#198606=CARTESIAN_POINT('Ctrl Pts',(-172.480724121525,-4.55419459435809,
135.589066102071));
#198607=CARTESIAN_POINT('Ctrl Pts',(-172.759171745337,1.5638548133772,137.222183698596));
#198608=CARTESIAN_POINT('Ctrl Pts',(-173.03761936915,6.24479804617409,132.957635411742));
#198609=CARTESIAN_POINT('Ctrl Pts',(-173.316066992963,5.18707694988104,
126.714332782362));
#198610=CARTESIAN_POINT('Ctrl Pts',(-173.594514616776,-0.637314460555731,
124.229565924566));
#198611=CARTESIAN_POINT('Ctrl Pts',(-173.872962240589,-5.8760450162844,
127.786714193059));
#198612=CARTESIAN_POINT('Ctrl Pts',(-174.151409864401,-5.71497726280517,
134.11693210545));
#198613=CARTESIAN_POINT('Ctrl Pts',(-174.429857488215,-0.302124596968923,
137.403058648589));
#198614=CARTESIAN_POINT('Ctrl Pts',(-174.708305112027,5.38836581387496,
134.625304065538));
#198615=CARTESIAN_POINT('Ctrl Pts',(-174.98675273584,6.1272112780718,128.336289117263));
#198616=CARTESIAN_POINT('Ctrl Pts',(-175.265200359654,1.2354489086321,124.315311305772));
#198617=CARTESIAN_POINT('Ctrl Pts',(-175.543647983466,-4.79163065280562,
126.257452804136));
#198618=CARTESIAN_POINT('Ctrl Pts',(-175.822095607279,-6.41543572848632,
132.377980454247));
#198619=CARTESIAN_POINT('Ctrl Pts',(-176.100543231092,-2.14376878114676,
137.05242835005));
#198620=CARTESIAN_POINT('Ctrl Pts',(-176.378990854905,4.09791694713909,
135.985207234778));
#198621=CARTESIAN_POINT('Ctrl Pts',(-176.657438478718,6.57381719537689,
130.157041176716));
#198622=CARTESIAN_POINT('Ctrl Pts',(-176.93588610253,3.00870058988678,124.923730061481));
#198623=CARTESIAN_POINT('Ctrl Pts',(-177.214333726344,-3.32126487451375,
125.094431142515));
#198624=CARTESIAN_POINT('Ctrl Pts',(-177.492781350156,-6.59915017204588,
130.512278465557));
#198625=CARTESIAN_POINT('Ctrl Pts',(-177.771228973969,-3.81273884787578,
136.198535017289));
#198626=CARTESIAN_POINT('Ctrl Pts',(-178.049676597782,2.47739321484437,
136.927808815745));
#198627=CARTESIAN_POINT('Ctrl Pts',(-178.328124221595,6.49092194050925,
132.029932867148));
#198628=CARTESIAN_POINT('Ctrl Pts',(-178.606571845408,4.53961050201187,
126.005815893719));
#198629=CARTESIAN_POINT('Ctrl Pts',(-178.885019469221,-1.58338121553252,
124.391327099562));
#198630=CARTESIAN_POINT('Ctrl Pts',(-179.163467093034,-6.25132294847495,
128.670102814346));
#198631=CARTESIAN_POINT('Ctrl Pts',(-179.441914716847,-5.1746042858732,
134.910157185999));
#198632=CARTESIAN_POINT('Ctrl Pts',(-179.72036234066,0.657322921973241,
137.377185090575));
#198633=CARTESIAN_POINT('Ctrl Pts',(-179.998809964472,5.88520247653593,
133.804108404782));
#198634=CARTESIAN_POINT('Ctrl Pts',(-180.277257588285,5.70486846328706,
127.474410048364));
#198635=CARTESIAN_POINT('Ctrl Pts',(-180.555705212098,0.282039030594865,
124.204773587913));
#198636=CARTESIAN_POINT('Ctrl Pts',(-180.834152835911,-5.39997049284089,
126.999835199963));
#198637=CARTESIAN_POINT('Ctrl Pts',(-181.112600459724,-6.11967093658025,
133.291069809391));
#198638=CARTESIAN_POINT('Ctrl Pts',(-181.391048083537,-1.21569275214809,
137.297140154028));
#198639=CARTESIAN_POINT('Ctrl Pts',(-181.669495707349,4.8054476816156,135.336663294571));
#198640=CARTESIAN_POINT('Ctrl Pts',(-181.947943331163,6.41061645514481,
129.21122169024));
#198641=CARTESIAN_POINT('Ctrl Pts',(-182.226390954976,2.12474188242055,
124.549796930959));
#198642=CARTESIAN_POINT('Ctrl Pts',(-182.504838578788,-4.11366668083735,
125.636010647245));
#198643=CARTESIAN_POINT('Ctrl Pts',(-182.783286202602,-6.5718165281946,
131.471685498325));
#198644=CARTESIAN_POINT('Ctrl Pts',(-183.061733826414,-2.99078803722709,
136.694121384618));
#198645=CARTESIAN_POINT('Ctrl Pts',(-183.340181450227,3.33862855183402,
136.5041548568));
#198646=CARTESIAN_POINT('Ctrl Pts',(-183.61862907404,6.60000860283161,131.076355873553));
#198647=CARTESIAN_POINT('Ctrl Pts',(-183.897076697853,3.79630317617236,
125.398606537762));
#198648=CARTESIAN_POINT('Ctrl Pts',(-184.175524321666,-2.49601940966891,
124.68848111554));
#198649=CARTESIAN_POINT('Ctrl Pts',(-184.453971945479,-6.49462209535141,
129.598550178357));
#198650=CARTESIAN_POINT('Ctrl Pts',(-184.732419569291,-4.52498435533419,
135.616700127691));
#198651=CARTESIAN_POINT('Ctrl Pts',(-185.010867193105,1.60289294946002,
137.212545163075));
#198652=CARTESIAN_POINT('Ctrl Pts',(-185.289314816917,6.25778993937471,
132.919581658354));
#198653=CARTESIAN_POINT('Ctrl Pts',(-185.56776244073,5.16208368503734,126.682833351442));
#198654=CARTESIAN_POINT('Ctrl Pts',(-185.846210064543,-0.677325294041226,
124.233567254297));
#198655=CARTESIAN_POINT('Ctrl Pts',(-186.124657688356,-5.89430541707644,
127.822539256894));
#198656=CARTESIAN_POINT('Ctrl Pts',(-186.403105312169,-5.69470681464601,
134.151659419877));
#198657=CARTESIAN_POINT('Ctrl Pts',(-186.681552935982,-0.261950851450417,
137.404775508174));
#198658=CARTESIAN_POINT('Ctrl Pts',(-186.960000559794,5.41152514721792,
134.592432760195));
#198659=CARTESIAN_POINT('Ctrl Pts',(-187.238448183608,6.11207390329327,
128.299036770752));
#198660=CARTESIAN_POINT('Ctrl Pts',(-187.51689580742,1.19592533365239,124.307911004657));
#198661=CARTESIAN_POINT('Ctrl Pts',(-187.795343431234,-4.81922019341476,
126.286705063617));
#198662=CARTESIAN_POINT('Ctrl Pts',(-188.073791055046,-6.40573779472858,
132.417003876913));
#198663=CARTESIAN_POINT('Ctrl Pts',(-188.352238678859,-2.10569530037498,
137.065362316871));
#198664=CARTESIAN_POINT('Ctrl Pts',(-188.630686302672,4.12937830608858,
135.960166062105));
#198665=CARTESIAN_POINT('Ctrl Pts',(-188.909133926485,6.56975498060235,
130.117036478904));
#198666=CARTESIAN_POINT('Ctrl Pts',(-189.187581550298,2.97284777831579,
124.905524201484));
#198667=CARTESIAN_POINT('Ctrl Pts',(-189.466029174111,-3.35596130055467,
125.114754416262));
#198668=CARTESIAN_POINT('Ctrl Pts',(-189.744476797923,-6.60080589203976,
130.552454777323));
#198669=CARTESIAN_POINT('Ctrl Pts',(-190.022924421737,-3.77983233603489,
136.221644299282));
#198670=CARTESIAN_POINT('Ctrl Pts',(-190.301372045549,2.5146224817104,136.912614766765));
#198671=CARTESIAN_POINT('Ctrl Pts',(-190.579819669362,6.49826208490189,
131.990398075938));
#198672=CARTESIAN_POINT('Ctrl Pts',(-190.858267293175,4.51031628981952,
125.978270902017));
#198673=CARTESIAN_POINT('Ctrl Pts',(-191.136714916988,-1.62238983440674,
124.401084409096));
#198674=CARTESIAN_POINT('Ctrl Pts',(-191.415162540801,-6.26419895896261,
128.708195934325));
#198675=CARTESIAN_POINT('Ctrl Pts',(-191.693610164614,-5.14951526336424,
134.941580400114));
#198676=CARTESIAN_POINT('Ctrl Pts',(-191.972057788427,0.697321391460013,
137.373062000163));
#198677=CARTESIAN_POINT('Ctrl Pts',(-192.25050541224,5.90335375357599,133.768227928508));
#198678=CARTESIAN_POINT('Ctrl Pts',(-192.528953036052,5.68449241101982,
127.439744591064));
#198679=CARTESIAN_POINT('Ctrl Pts',(-192.807400659866,0.241860245628379,
124.203179011344));
#198680=CARTESIAN_POINT('Ctrl Pts',(-193.085848283678,-5.42302966996514,
127.032776842093));
#198681=CARTESIAN_POINT('Ctrl Pts',(-193.364295907491,-6.10442024858855,
133.32827591039));
#198682=CARTESIAN_POINT('Ctrl Pts',(-193.642743531304,-1.17614683626724,
137.304420124699));
#198683=CARTESIAN_POINT('Ctrl Pts',(-193.921191155117,4.83294806061645,
135.307327197512));
#198684=CARTESIAN_POINT('Ctrl Pts',(-194.19963877893,6.40079979243214,129.172227965502));
#198685=CARTESIAN_POINT('Ctrl Pts',(-194.478086402743,2.08662921145659,
124.536978906625));
#198686=CARTESIAN_POINT('Ctrl Pts',(-194.756534026555,-4.14505167734362,
125.661147461485));
#198687=CARTESIAN_POINT('Ctrl Pts',(-195.034981650369,-6.5676325716969,
131.511677646851));
#198688=CARTESIAN_POINT('Ctrl Pts',(-195.313429274181,-2.95487997934909,
136.712218036662));
#198689=CARTESIAN_POINT('Ctrl Pts',(-195.591876897994,3.3732629601091,136.483726073203));
#198690=CARTESIAN_POINT('Ctrl Pts',(-195.870324521807,6.60154203228333,
131.03617470844));
#198691=CARTESIAN_POINT('Ctrl Pts',(-196.14877214562,3.76332648004682,125.375597518911));
#198692=CARTESIAN_POINT('Ctrl Pts',(-196.427219769433,-2.53320225863353,
124.703788407225));
#198693=CARTESIAN_POINT('Ctrl Pts',(-196.705667393246,-6.50184187543975,
129.63810712732));
#198694=CARTESIAN_POINT('Ctrl Pts',(-196.984115017059,-4.49560644135098,
135.644155830301));
#198695=CARTESIAN_POINT('Ctrl Pts',(-197.262562640871,1.64187168975517,
137.202669169918));
#198696=CARTESIAN_POINT('Ctrl Pts',(-197.541010264685,6.27054994786743,
132.881449524674));
#198697=CARTESIAN_POINT('Ctrl Pts',(-197.819457888497,5.13689913728475,
126.651486645231));
#198698=CARTESIAN_POINT('Ctrl Pts',(-198.097905512311,-0.717311028988463,
124.237812067191));
#198699=CARTESIAN_POINT('Ctrl Pts',(-198.376353136123,-5.91234740221361,
127.858474813215));
#198700=CARTESIAN_POINT('Ctrl Pts',(-198.654800759936,-5.67422534703162,
134.186262698915));
#198701=CARTESIAN_POINT('Ctrl Pts',(-198.933248383749,-0.221767399246752,
137.406247786956));
#198702=CARTESIAN_POINT('Ctrl Pts',(-199.211696007562,5.43448395450644,
134.559421086446));
#198703=CARTESIAN_POINT('Ctrl Pts',(-199.490143631375,6.09671004336861,
128.261877259937));
#198704=CARTESIAN_POINT('Ctrl Pts',(-199.768591255188,1.15635744321901,
124.300751431872));
#198705=CARTESIAN_POINT('Ctrl Pts',(-200.047038879001,-4.84663115604747,
126.316124726487));
#198706=CARTESIAN_POINT('Ctrl Pts',(-200.325486502814,-6.39580249400115,
132.455967542492));
#198707=CARTESIAN_POINT('Ctrl Pts',(-200.603934126626,-2.06754379228947,
137.078064279972));
#198708=CARTESIAN_POINT('Ctrl Pts',(-200.882381750439,4.16068664940635,
135.934933839164));
#198709=CARTESIAN_POINT('Ctrl Pts',(-201.160829374253,6.56544932114097,
130.077057250143));
#198710=CARTESIAN_POINT('Ctrl Pts',(-201.439276998065,2.9368848067771,124.887536925038));
#198711=CARTESIAN_POINT('Ctrl Pts',(-201.717724621878,-3.39053337021544,
125.13528852046));
#198712=CARTESIAN_POINT('Ctrl Pts',(-201.996172245691,-6.60221701674386,
130.592640423553));
#198713=CARTESIAN_POINT('Ctrl Pts',(-202.274619869504,-3.74678576111652,
136.244552841837));
#198714=CARTESIAN_POINT('Ctrl Pts',(-202.553067493317,2.55175856831618,
136.897194374181));
#198715=CARTESIAN_POINT('Ctrl Pts',(-202.83151511713,6.50536143380309,131.950819335672));
#198716=CARTESIAN_POINT('Ctrl Pts',(-203.109962740942,4.48085494619837,
125.950904742844));
#198717=CARTESIAN_POINT('Ctrl Pts',(-203.388410364755,-1.66133833502902,
124.411078994385));
#198718=CARTESIAN_POINT('Ctrl Pts',(-203.666857988568,-6.27684284725421,
128.746366728457));
#198719=CARTESIAN_POINT('Ctrl Pts',(-203.945305612381,-5.12423542367342,
134.97285030803));
#198720=CARTESIAN_POINT('Ctrl Pts',(-204.223753236194,0.737294021446153,
137.368695504108));
#198721=CARTESIAN_POINT('Ctrl Pts',(-204.502200860007,5.9212862796718,133.732237625041));
#198722=CARTESIAN_POINT('Ctrl Pts',(-204.78064848382,5.66390571779574,127.405203810847));
#198723=CARTESIAN_POINT('Ctrl Pts',(-205.059096107633,0.20167249844203,
124.201829043986));
#198724=CARTESIAN_POINT('Ctrl Pts',(-205.337543731446,-5.44588789473034,
127.065858241646));
#198725=CARTESIAN_POINT('Ctrl Pts',(-205.615991355258,-6.08894335906002,
133.36538848678));
#198726=CARTESIAN_POINT('Ctrl Pts',(-205.894438979071,-1.13655733783284,
137.311459233274));
#198727=CARTESIAN_POINT('Ctrl Pts',(-206.172886602884,4.86026935294961,
135.277824241371));
#198728=CARTESIAN_POINT('Ctrl Pts',(-206.451334226697,6.39074594572923,
129.133294720038));
#198729=CARTESIAN_POINT('Ctrl Pts',(-206.72978185051,2.04843921967989,124.524393122426));
#198730=CARTESIAN_POINT('Ctrl Pts',(-207.008229474323,-4.17628307743617,
125.686474859378));
#198731=CARTESIAN_POINT('Ctrl Pts',(-207.286677098136,-6.56320524915893,
131.551643585487));
#198732=CARTESIAN_POINT('Ctrl Pts',(-207.565124721949,-2.9188624273063,
136.730095770877));
#198733=CARTESIAN_POINT('Ctrl Pts',(-207.843572345762,3.40777237088467,
136.463086838631));
#198734=CARTESIAN_POINT('Ctrl Pts',(-208.122019969575,6.60283083916734,
130.995984953369));
#198735=CARTESIAN_POINT('Ctrl Pts',(-208.400467593387,3.73021033247459,
125.352789664874));
#198736=CARTESIAN_POINT('Ctrl Pts',(-208.678915217201,-2.57029123885685,
124.719321757855));
#198737=CARTESIAN_POINT('Ctrl Pts',(-208.957362841013,-6.50882072738636,
129.677707292235));
#198738=CARTESIAN_POINT('Ctrl Pts',(-209.235810464827,-4.4660619410178,
135.671432192519));
#198739=CARTESIAN_POINT('Ctrl Pts',(-209.514258088639,1.68078958989102,
137.192556085085));
#198740=CARTESIAN_POINT('Ctrl Pts',(-209.792705712452,6.28307759882623,
132.8432404237));
#198741=CARTESIAN_POINT('Ctrl Pts',(-210.071153336265,5.11152423984512,
126.620293825292));
#198742=CARTESIAN_POINT('Ctrl Pts',(-210.349600960078,-0.757270183712145,
124.242300205957));
#198743=CARTESIAN_POINT('Ctrl Pts',(-210.62804858389,-5.93017030314353,
127.894519530418));
#198744=CARTESIAN_POINT('Ctrl Pts',(-210.906496207704,-5.65353361891029,
134.220740660327));
#198745=CARTESIAN_POINT('Ctrl Pts',(-211.184943831516,-0.181575729370575,
137.407475430382));
#198746=CARTESIAN_POINT('Ctrl Pts',(-211.463391455329,5.4572413849935,134.52627026755));
#198747=CARTESIAN_POINT('Ctrl Pts',(-211.741839079142,6.08112026761121,
128.224811961777));
#198748=CARTESIAN_POINT('Ctrl Pts',(-212.020286702955,1.11674670353533,
124.293832852717));
#198749=CARTESIAN_POINT('Ctrl Pts',(-212.298734326768,-4.87386252498038,
126.345710702588));
#198750=CARTESIAN_POINT('Ctrl Pts',(-212.577181950581,-6.38563019446009,
132.494870007167));
#198751=CARTESIAN_POINT('Ctrl Pts',(-212.855629574394,-2.02931567060901,
137.090533768676));
#198752=CARTESIAN_POINT('Ctrl Pts',(-213.134077198207,4.19184081695006,
135.909511500946));
#198753=CARTESIAN_POINT('Ctrl Pts',(-213.412524822019,6.56090037654053,
130.037104971874));
#198754=CARTESIAN_POINT('Ctrl Pts',(-213.690972445832,2.90081300789186,
124.869768898671));
#198755=CARTESIAN_POINT('Ctrl Pts',(-213.969420069645,-3.42497980241531,
125.156032694208));
#198756=CARTESIAN_POINT('Ctrl Pts',(-214.247867693459,-6.60338349386843,
130.632833915152));
#198757=CARTESIAN_POINT('Ctrl Pts',(-214.52631531727,-3.71360034767391,
136.267259796069));
#198758=CARTESIAN_POINT('Ctrl Pts',(-214.804762941084,2.58880009856982,
136.881548209402));
#198759=CARTESIAN_POINT('Ctrl Pts',(-215.083210564897,6.51221972414398,
131.911198112957));
#198760=CARTESIAN_POINT('Ctrl Pts',(-215.36165818871,4.45122756284936,125.923718430264));
#198761=CARTESIAN_POINT('Ctrl Pts',(-215.640105812523,-1.70022527414834,
124.421310485075));
#198762=CARTESIAN_POINT('Ctrl Pts',(-215.918553436335,-6.28925414482577,
128.784613782311));
#198763=CARTESIAN_POINT('Ctrl Pts',(-216.197001060149,-5.09876570355457,
135.003965751026));
#198764=CARTESIAN_POINT('Ctrl Pts',(-216.475448683961,0.77723933073121,
137.364085764208));
#198765=CARTESIAN_POINT('Ctrl Pts',(-216.753896307774,5.93899939032692,
133.696138828015));
#198766=CARTESIAN_POINT('Ctrl Pts',(-217.032343931587,5.64310914646246,
127.370788987637));
#198767=CARTESIAN_POINT('Ctrl Pts',(-217.3107915554,0.161477278206604,124.200723735865));
#198768=CARTESIAN_POINT('Ctrl Pts',(-217.589239179213,-5.46854432011718,
127.099078172778));
#198769=CARTESIAN_POINT('Ctrl Pts',(-217.867686803026,-6.07324084149572,
133.402406163341));
#198770=CARTESIAN_POINT('Ctrl Pts',(-218.146134426838,-1.09692572384833,
137.318257218917));
#198771=CARTESIAN_POINT('Ctrl Pts',(-218.424582050652,4.88741054621452,
135.24815551939));
#198772=CARTESIAN_POINT('Ctrl Pts',(-218.703029674464,6.38045528758512,
129.094423396537));
#198773=CARTESIAN_POINT('Ctrl Pts',(-218.981477298277,2.01017332223456,
124.512040044732));
#198774=CARTESIAN_POINT('Ctrl Pts',(-219.25992492209,-4.20735972382344,
125.711991902411));
#198775=CARTESIAN_POINT('Ctrl Pts',(-219.538372545903,-6.55853472463687,
131.591581833275));
#198776=CARTESIAN_POINT('Ctrl Pts',(-219.816820169716,-2.8827367157428,
136.747753924796));
#198777=CARTESIAN_POINT('Ctrl Pts',(-220.095267793529,3.44215550540127,
136.442237917877));
#198778=CARTESIAN_POINT('Ctrl Pts',(-220.373715417342,6.60387497572639,
130.955788097589));
#198779=CARTESIAN_POINT('Ctrl Pts',(-220.652163041155,3.69695596058723,
125.330183820803));
#198780=CARTESIAN_POINT('Ctrl Pts',(-220.930610664968,-2.60728497599312,
124.735080591838));
#198781=CARTESIAN_POINT('Ctrl Pts',(-221.20905828878,-6.51555839258729,
129.717349205704));
#198782=CARTESIAN_POINT('Ctrl Pts',(-221.487505912593,-4.43635194911701,
135.698528203611));
#198783=CARTESIAN_POINT('Ctrl Pts',(-221.765953536406,1.71964520775051,
137.182206283321));
#198784=CARTESIAN_POINT('Ctrl Pts',(-222.044401160219,6.295372428034,132.804955771283));
#198785=CARTESIAN_POINT('Ctrl Pts',(-222.322848784032,5.08595993299503,
126.589256047487));
#198786=CARTESIAN_POINT('Ctrl Pts',(-222.601296407845,-0.797201277510683,
124.247031504286));
#198787=CARTESIAN_POINT('Ctrl Pts',(-222.879744031658,-5.94777345943203,
127.930672072853));
#198788=CARTESIAN_POINT('Ctrl Pts',(-223.158191655471,-5.63263239702162,
134.255092026522));
#198789=CARTESIAN_POINT('Ctrl Pts',(-223.436639279283,-0.141377331138957,
137.40845839296));
#198790=CARTESIAN_POINT('Ctrl Pts',(-223.715086903097,5.47979659539413,
134.492981531924));
#198791=CARTESIAN_POINT('Ctrl Pts',(-223.993534526909,6.06530515370598,
128.187842249741));
#198792=CARTESIAN_POINT('Ctrl Pts',(-224.271982150722,1.07709458239186,
124.287155523561));
#198793=CARTESIAN_POINT('Ctrl Pts',(-224.550429774535,-4.90091329114502,
126.375461895601));
#198794=CARTESIAN_POINT('Ctrl Pts',(-224.828877398348,-6.37522127304402,
132.533709829396));
#198795=CARTESIAN_POINT('Ctrl Pts',(-225.107325022161,-1.99101235188949,
137.102770320923));
#198796=CARTESIAN_POINT('Ctrl Pts',(-225.385772645974,4.22283965429091,
135.883899989486));
#198797=CARTESIAN_POINT('Ctrl Pts',(-225.664220269787,6.55610831536389,
129.997181124546));
#198798=CARTESIAN_POINT('Ctrl Pts',(-225.9426678936,2.86463371831382,124.852220780782));
#198799=CARTESIAN_POINT('Ctrl Pts',(-226.221115517412,-3.45929932072906,
125.176986168825));
#198800=CARTESIAN_POINT('Ctrl Pts',(-226.499563141226,-6.60430528018926,
130.673033762736));
#198801=CARTESIAN_POINT('Ctrl Pts',(-226.778010765038,-3.68027732540471,
136.289764320562));
#198802=CARTESIAN_POINT('Ctrl Pts',(-227.056458388851,2.62574569988376,
136.865676852203));
#198803=CARTESIAN_POINT('Ctrl Pts',(-227.334906012664,6.51883670178814,
131.871535875972));
#198804=CARTESIAN_POINT('Ctrl Pts',(-227.613353636477,4.42143523762624,
125.896712971676));
#198805=CARTESIAN_POINT('Ctrl Pts',(-227.89180126029,-1.73904921079426,
124.431778502036));
#198806=CARTESIAN_POINT('Ctrl Pts',(-228.170248884103,-6.30143239177224,
128.822935678624));
#198807=CARTESIAN_POINT('Ctrl Pts',(-228.448696507916,-5.07310704679746,
135.034925576111));
#198808=CARTESIAN_POINT('Ctrl Pts',(-228.727144131728,0.81715583912702,
137.359232951281));
#198809=CARTESIAN_POINT('Ctrl Pts',(-229.005591755541,5.95649242917557,
133.659932875084));
#198810=CARTESIAN_POINT('Ctrl Pts',(-229.284039379354,5.62210346764449,
127.336501396687));
#198811=CARTESIAN_POINT('Ctrl Pts',(-229.562487003167,0.121276074371264,
124.199863127936));
#198812=CARTESIAN_POINT('Ctrl Pts',(-229.84093462698,-5.4909981065832,127.132435404515));
#198813=CARTESIAN_POINT('Ctrl Pts',(-230.119382250793,-6.0573132777586,
133.439327568368));
#198814=CARTESIAN_POINT('Ctrl Pts',(-230.397829874606,-1.05725346287773,
137.324813829725));
#198815=CARTESIAN_POINT('Ctrl Pts',(-230.676277498418,4.91437063468431,
135.218322130955));
#198816=CARTESIAN_POINT('Ctrl Pts',(-230.954725122232,6.3699281993239,129.055615435388));
#198817=CARTESIAN_POINT('Ctrl Pts',(-231.233172746044,1.97183293707754,
124.49992013129));
#198818=CARTESIAN_POINT('Ctrl Pts',(-231.511620369858,-4.23828046494889,
125.73769764504));
#198819=CARTESIAN_POINT('Ctrl Pts',(-231.79006799367,-6.55362117119865,
131.631490910294));
#198820=CARTESIAN_POINT('Ctrl Pts',(-232.068515617483,-2.84650418331021,
136.765191844092));
#198821=CARTESIAN_POINT('Ctrl Pts',(-232.346963241296,3.47641108958031,
136.421180083507));
#198822=CARTESIAN_POINT('Ctrl Pts',(-232.625410865109,6.60467440326965,
130.915585630608));
#198823=CARTESIAN_POINT('Ctrl Pts',(-232.903858488922,3.66356459663667,
125.307780824367));
#198824=CARTESIAN_POINT('Ctrl Pts',(-233.182306112735,-2.64418209922576,
124.751064325225));
#198825=CARTESIAN_POINT('Ctrl Pts',(-233.460753736548,-6.52205462137589,
129.75703139878));
#198826=CARTESIAN_POINT('Ctrl Pts',(-233.73920136036,-4.40647756656326,
135.725442859523));
#198827=CARTESIAN_POINT('Ctrl Pts',(-234.017648984174,1.75843710352442,
137.17162014814));
#198828=CARTESIAN_POINT('Ctrl Pts',(-234.296096607986,6.30743397990132,
132.766596986079));
#198829=CARTESIAN_POINT('Ctrl Pts',(-234.574544231799,5.06020716402928,
126.558374461932));
#198830=CARTESIAN_POINT('Ctrl Pts',(-234.852991855612,-0.837102830722735,
124.252005786856));
#198831=CARTESIAN_POINT('Ctrl Pts',(-235.131439479425,-5.96515621878728,
127.966931100874));
#198832=CARTESIAN_POINT('Ctrl Pts',(-235.409887103238,-5.6115224558684,
134.289315524594));
#198833=CARTESIAN_POINT('Ctrl Pts',(-235.688334727051,-0.101173694118813,
137.409196638266));
#198834=CARTESIAN_POINT('Ctrl Pts',(-235.966782350864,5.50214874991674,
134.459556113093));
#198835=CARTESIAN_POINT('Ctrl Pts',(-236.245229974676,6.04926528768773,
128.150969493757));
#198836=CARTESIAN_POINT('Ctrl Pts',(-236.52367759849,1.03740254911254,124.280719691838));
#198837=CARTESIAN_POINT('Ctrl Pts',(-236.802125222302,-4.92778245216537,
126.405377203086));
#198838=CARTESIAN_POINT('Ctrl Pts',(-237.080572846115,-6.36457611545918,
132.572485569954));
#198839=CARTESIAN_POINT('Ctrl Pts',(-237.359020469928,-1.95263525547508,
137.114773483282));
#198840=CARTESIAN_POINT('Ctrl Pts',(-237.637468093741,4.25368201275546,
135.858100253825));
#198841=CARTESIAN_POINT('Ctrl Pts',(-237.915915717553,6.55107331518259,
129.957287187551));
#198842=CARTESIAN_POINT('Ctrl Pts',(-238.194363341367,2.8283482786799,124.834893221623));
#198843=CARTESIAN_POINT('Ctrl Pts',(-238.47281096518,-3.49349065343433,
125.198148167872));
#198844=CARTESIAN_POINT('Ctrl Pts',(-238.751258588993,-6.60498234154917,
130.713238476685));
#198845=CARTESIAN_POINT('Ctrl Pts',(-239.029706212805,-3.64681792910581,
136.312065581403));
#198846=CARTESIAN_POINT('Ctrl Pts',(-239.308153836619,2.66259400322518,
136.8495808907));
#198847=CARTESIAN_POINT('Ctrl Pts',(-239.586601460431,6.52521212154101,
131.831834094415));
#198848=CARTESIAN_POINT('Ctrl Pts',(-239.865049084244,4.39147907449425,
125.869889367774));
#198849=CARTESIAN_POINT('Ctrl Pts',(-240.143496708057,-1.77780870633274,
124.44248265737));
#198850=CARTESIAN_POINT('Ctrl Pts',(-240.42194433187,-6.31337713682396,
128.861330997368));
#198851=CARTESIAN_POINT('Ctrl Pts',(-240.700391955683,-5.04726040419313,
135.065728636055));
#198852=CARTESIAN_POINT('Ctrl Pts',(-240.978839579496,0.857042067512721,
137.354137245149));
#198853=CARTESIAN_POINT('Ctrl Pts',(-241.257287203309,5.97376474800676,
133.623621107872));
#198854=CARTESIAN_POINT('Ctrl Pts',(-241.535734827122,5.60088945971499,
127.302342308534));
#198855=CARTESIAN_POINT('Ctrl Pts',(-241.814182450934,0.0810703766063902,
124.199247252091));
#198856=CARTESIAN_POINT('Ctrl Pts',(-242.092630074747,-5.51324842209508,
127.165928700792));
#198857=CARTESIAN_POINT('Ctrl Pts',(-242.37107769856,-6.04116125805038,
133.476151333726));
#198858=CARTESIAN_POINT('Ctrl Pts',(-242.649525322373,-1.01754202499167,
137.331128822742));
#198859=CARTESIAN_POINT('Ctrl Pts',(-242.927972946186,4.94114861934255,
135.188325181553));
#198860=CARTESIAN_POINT('Ctrl Pts',(-243.206420569999,6.35916507103108,
129.016872274634));
#198861=CARTESIAN_POINT('Ctrl Pts',(-243.484868193812,1.93341948492588,
124.488033831209));
#198862=CARTESIAN_POINT('Ctrl Pts',(-243.763315817625,-4.26904415503308,
125.763591134728));
#198863=CARTESIAN_POINT('Ctrl Pts',(-244.041763441437,-6.54846477091785,
131.671369337695));
#198864=CARTESIAN_POINT('Ctrl Pts',(-244.320211065251,-2.8101661726183,
136.782408882594));
#198865=CARTESIAN_POINT('Ctrl Pts',(-244.598658689063,3.51053785406796,
136.399914115825));
#198866=CARTESIAN_POINT('Ctrl Pts',(-244.877106312876,6.60522909217403,
130.875379042142));
#198867=CARTESIAN_POINT('Ctrl Pts',(-245.155553936689,3.6300374779527,125.285581505715));
#198868=CARTESIAN_POINT('Ctrl Pts',(-245.434001560502,-2.68098124131831,
124.767272365732));
#198869=CARTESIAN_POINT('Ctrl Pts',(-245.712449184315,-6.528309173032,129.796752401026));
#198870=CARTESIAN_POINT('Ctrl Pts',(-245.990896808128,-4.37643990036281,
135.752175162922));
#198871=CARTESIAN_POINT('Ctrl Pts',(-246.269344431941,1.79716383976481,
137.160798071814));
#198872=CARTESIAN_POINT('Ctrl Pts',(-246.547792055753,6.31926180748295,
132.728165489484));
#198873=CARTESIAN_POINT('Ctrl Pts',(-246.826239679567,5.03426688722615,
126.527650212955));
#198874=CARTESIAN_POINT('Ctrl Pts',(-247.104687303379,-0.876973364781528,
124.257222869343));
#198875=CARTESIAN_POINT('Ctrl Pts',(-247.383134927193,-5.98231793708558,
128.003295270889));
#198876=CARTESIAN_POINT('Ctrl Pts',(-247.661582551005,-5.59020457768662,
134.32340988638));
#198877=CARTESIAN_POINT('Ctrl Pts',(-247.940030174818,-0.0609663080697638,
137.409690138946));
#198878=CARTESIAN_POINT('Ctrl Pts',(-248.218477798631,5.524297020294,134.425995249648));
#198879=CARTESIAN_POINT('Ctrl Pts',(-248.496925422444,6.03300126391963,
128.114195060156));
#198880=CARTESIAN_POINT('Ctrl Pts',(-248.775373046256,0.997672074500306,
124.274525596028));
#198881=CARTESIAN_POINT('Ctrl Pts',(-249.05382067007,-4.95446901239483,
126.435455516518));
#198882=CARTESIAN_POINT('Ctrl Pts',(-249.332268293882,-6.35369511616563,
132.611195791991));
#198883=CARTESIAN_POINT('Ctrl Pts',(-249.610715917695,-1.91418580344349,
137.126542810973));
#198884=CARTESIAN_POINT('Ctrl Pts',(-249.889163541508,4.28436674946925,
135.832113249982));
#198885=CARTESIAN_POINT('Ctrl Pts',(-250.167611165321,6.54579556256923,
129.917424639176));
#198886=CARTESIAN_POINT('Ctrl Pts',(-250.446058789134,2.79195803356287,
124.817786863269));
#198887=CARTESIAN_POINT('Ctrl Pts',(-250.724506412947,-3.52755253356211,
125.219517907192));
#198888=CARTESIAN_POINT('Ctrl Pts',(-251.00295403676,-6.60541465285253,
130.75344656718));
#198889=CARTESIAN_POINT('Ctrl Pts',(-251.281401660573,-3.61322339864049,
136.334162752248));
#198890=CARTESIAN_POINT('Ctrl Pts',(-251.559849284386,2.6993436431913,136.83326092127));
#198891=CARTESIAN_POINT('Ctrl Pts',(-251.838296908198,6.53134574711249,
131.792094239578));
#198892=CARTESIAN_POINT('Ctrl Pts',(-252.116744532012,4.3613601835781,125.843248612281));
#198893=CARTESIAN_POINT('Ctrl Pts',(-252.395192155824,-1.81650232468185,
124.453422554885));
#198894=CARTESIAN_POINT('Ctrl Pts',(-252.673639779637,-6.32508793705065,
128.899798314935));
#198895=CARTESIAN_POINT('Ctrl Pts',(-252.95208740345,-5.02122673409033,
135.096373791053));
#198896=CARTESIAN_POINT('Ctrl Pts',(-253.230535027263,0.896896539007115,
137.348798831588));
#198897=CARTESIAN_POINT('Ctrl Pts',(-253.508982651076,5.99081570467794,
133.587204877683));
#198898=CARTESIAN_POINT('Ctrl Pts',(-253.787430274889,5.57946791275175,
127.26831297809));
#198899=CARTESIAN_POINT('Ctrl Pts',(-254.065877898701,0.0408616672245685,
124.198876151673));
#198900=CARTESIAN_POINT('Ctrl Pts',(-254.344325522515,-5.53529442795169,
127.199556781751));
#198901=CARTESIAN_POINT('Ctrl Pts',(-254.622773146327,-6.0247854077167,
133.512876168065));
#198902=CARTESIAN_POINT('Ctrl Pts',(-254.90122077014,-0.977792831057213,
137.337201825807));
#198903=CARTESIAN_POINT('Ctrl Pts',(-255.179668393953,4.96774341227684,
135.158166043599));
#198904=CARTESIAN_POINT('Ctrl Pts',(-255.458116017766,6.34816648213513,
128.97819485735));
#198905=CARTESIAN_POINT('Ctrl Pts',(-255.736563641579,1.89493404819936,
124.476382515012));
#198906=CARTESIAN_POINT('Ctrl Pts',(-256.015011265392,-4.29964901022966,
125.789669655819));
#198907=CARTESIAN_POINT('Ctrl Pts',(-256.293458889205,-6.54306693065544,
131.711218953762));
#198908=CARTESIAN_POINT('Ctrl Pts',(-256.571906513018,-2.77372173452912,
136.799398141047));
#198909=CARTESIAN_POINT('Ctrl Pts',(-256.85035413683,3.54453019961847,136.378452625405));
#198910=CARTESIAN_POINT('Ctrl Pts',(-257.128801760644,6.60554720661629,
130.835147498674));
#198911=CARTESIAN_POINT('Ctrl Pts',(-257.407249384456,3.5963603924579,125.263628838565));
#198912=CARTESIAN_POINT('Ctrl Pts',(-257.685697008269,-2.71765185753996,
124.783624522784));
#198913=CARTESIAN_POINT('Ctrl Pts',(-257.964144632082,-6.53437691572335,
129.836661023534));
#198914=CARTESIAN_POINT('Ctrl Pts',(-258.242592255895,-4.34613602341029,
135.778440351053));
#198915=CARTESIAN_POINT('Ctrl Pts',(-258.521039879708,1.83562753012831,
137.150276335207));
#198916=CARTESIAN_POINT('Ctrl Pts',(-258.799487503521,6.33122643152078,
132.688650362788));
#198917=CARTESIAN_POINT('Ctrl Pts',(-259.077935127334,5.00743946241547,
126.498999976245));
#198918=CARTESIAN_POINT('Ctrl Pts',(-259.356382751147,-0.915487258132909,
124.259032700089));
#198919=CARTESIAN_POINT('Ctrl Pts',(-259.634830374959,-6.00176822571329,
128.046924274587));
#198920=CARTESIAN_POINT('Ctrl Pts',(-259.86687006147,-5.63687269779404,
133.292521465648));
#198921=CARTESIAN_POINT('Ctrl Pts',(-260.052531023546,-2.79481741349804,
135.900547185714));
#198922=CARTESIAN_POINT('Ctrl Pts',(-260.145376111017,-0.946914048523564,
136.386386345067));
#198923=CARTESIAN_POINT('Ctrl Pts',(-260.191813261187,-0.0157913329746497,
136.389009763222));
#198924=CARTESIAN_POINT('Ctrl Pts',(210.190947297731,3.04870273111253,135.077142573452));
#198925=CARTESIAN_POINT('Ctrl Pts',(210.144529434129,3.76080111712433,134.569051946243));
#198926=CARTESIAN_POINT('Ctrl Pts',(210.051703633225,4.91317831978039,133.192256847685));
#198927=CARTESIAN_POINT('Ctrl Pts',(209.866061957716,5.67455722768035,129.648049455111));
#198928=CARTESIAN_POINT('Ctrl Pts',(209.634022271206,3.10293383059235,125.427666478792));
#198929=CARTESIAN_POINT('Ctrl Pts',(209.355574647392,-2.85596866243967,
125.28812524467));
#198930=CARTESIAN_POINT('Ctrl Pts',(209.07712702358,-6.17973736462657,130.225196103446));
#198931=CARTESIAN_POINT('Ctrl Pts',(208.798679399767,-3.83016968018938,
135.690661498217));
#198932=CARTESIAN_POINT('Ctrl Pts',(208.520231775954,2.04205955310628,136.667868212554));
#198933=CARTESIAN_POINT('Ctrl Pts',(208.241784152142,6.03618933210081,132.255733564264));
#198934=CARTESIAN_POINT('Ctrl Pts',(207.963336528328,4.48417485225333,126.510421532214));
#198935=CARTESIAN_POINT('Ctrl Pts',(207.684888904515,-1.18901089957204,
124.710731370568));
#198936=CARTESIAN_POINT('Ctrl Pts',(207.406441280703,-5.76932406256156,
128.510946815645));
#198937=CARTESIAN_POINT('Ctrl Pts',(207.12799365689,-5.04803188696711,134.418613818075));
#198938=CARTESIAN_POINT('Ctrl Pts',(206.849546033077,0.312219397189005,
137.005003016302));
#198939=CARTESIAN_POINT('Ctrl Pts',(206.571098409264,5.38552219392035,133.893281295751));
#198940=CARTESIAN_POINT('Ctrl Pts',(206.292650785451,5.50981125882569,127.943004805273));
#198941=CARTESIAN_POINT('Ctrl Pts',(206.014203161638,0.570843377758803,
124.622167937696));
#198942=CARTESIAN_POINT('Ctrl Pts',(205.735755537825,-4.89269661278007,
126.982467612715));
#198943=CARTESIAN_POINT('Ctrl Pts',(205.457307914013,-5.86009012142741,
132.854898402769));
#198944=CARTESIAN_POINT('Ctrl Pts',(205.178860290199,-1.44234566848361,
136.842986120511));
#198945=CARTESIAN_POINT('Ctrl Pts',(204.900412666387,4.30084323855829,135.281871486376));
#198946=CARTESIAN_POINT('Ctrl Pts',(204.621965042573,6.09176771588946,129.606143376667));
#198947=CARTESIAN_POINT('Ctrl Pts',(204.343517418761,2.28465505058828,125.031518229909));
#198948=CARTESIAN_POINT('Ctrl Pts',(204.065069794948,-3.62194388278553,
125.761853295313));
#198949=CARTESIAN_POINT('Ctrl Pts',(203.786622171135,-6.20015338889199,
131.126006208945));
#198950=CARTESIAN_POINT('Ctrl Pts',(203.508174547322,-3.08072479357708,
136.194582558939));
#198951=CARTESIAN_POINT('Ctrl Pts',(203.229726923509,2.86973936865286,136.309808260363));
#198952=CARTESIAN_POINT('Ctrl Pts',(202.951279299696,6.1830532544492,131.365796540178));
#198953=CARTESIAN_POINT('Ctrl Pts',(202.672831675884,3.81444325369211,125.905852631576));
#198954=CARTESIAN_POINT('Ctrl Pts',(202.39438405207,-2.05945374882828,124.947398258377));
#198955=CARTESIAN_POINT('Ctrl Pts',(202.115936428258,-6.04081336739099,
129.371206163854));
#198956=CARTESIAN_POINT('Ctrl Pts',(201.837488804444,-4.47096061076856,
135.112012999282));
#198957=CARTESIAN_POINT('Ctrl Pts',(201.559041180632,1.20748652821524,136.894297736177));
#198958=CARTESIAN_POINT('Ctrl Pts',(201.280593556819,5.77631253695961,133.08022777117));
#198959=CARTESIAN_POINT('Ctrl Pts',(201.002145933006,5.03698951269057,127.174747074221));
#198960=CARTESIAN_POINT('Ctrl Pts',(200.723698309193,-0.331080803069094,
124.604703907164));
#198961=CARTESIAN_POINT('Ctrl Pts',(200.44525068538,-5.39490403503349,127.731842386878));
#198962=CARTESIAN_POINT('Ctrl Pts',(200.166803061567,-5.50107401450091,
133.682475019745));
#198963=CARTESIAN_POINT('Ctrl Pts',(199.888355437754,-0.552025717056,136.988261120707));
#198964=CARTESIAN_POINT('Ctrl Pts',(199.609907813942,4.90430724641216,134.611344759621));
#198965=CARTESIAN_POINT('Ctrl Pts',(199.331460190128,5.85382143915379,128.735995953499));
#198966=CARTESIAN_POINT('Ctrl Pts',(199.053012566316,1.42395970438994,124.761373228423));
#198967=CARTESIAN_POINT('Ctrl Pts',(198.774564942502,-4.31445143441004,
126.339960697623));
#198968=CARTESIAN_POINT('Ctrl Pts',(198.49611731869,-6.088092477657,132.02111359519));
#198969=CARTESIAN_POINT('Ctrl Pts',(198.217669694877,-2.26707395378944,
136.584129948007));
#198970=CARTESIAN_POINT('Ctrl Pts',(197.939222071064,3.6372747808909,135.835820643578));
#198971=CARTESIAN_POINT('Ctrl Pts',(197.660774447251,6.19914568268399,130.46384537573));
#198972=CARTESIAN_POINT('Ctrl Pts',(197.382326823438,3.06430454719326,125.404786980035));
#198973=CARTESIAN_POINT('Ctrl Pts',(197.103879199626,-2.88648276756863,
125.307672973393));
#198974=CARTESIAN_POINT('Ctrl Pts',(196.825431575812,-6.1847334314575,130.261746383626));
#198975=CARTESIAN_POINT('Ctrl Pts',(196.546983952,-3.79951621286212,135.71445576667));
#198976=CARTESIAN_POINT('Ctrl Pts',(196.268536328187,2.07727078866752,136.65502757917));
#198977=CARTESIAN_POINT('Ctrl Pts',(195.990088704374,6.04514741573133,132.219122274927));
#198978=CARTESIAN_POINT('Ctrl Pts',(195.711641080561,4.45782888960729,126.483120122517));
#198979=CARTESIAN_POINT('Ctrl Pts',(195.433193456748,-1.22601660901765,
124.718126880723));
#198980=CARTESIAN_POINT('Ctrl Pts',(195.154745832935,-5.78321273819644,
128.54608511404));
#198981=CARTESIAN_POINT('Ctrl Pts',(194.876298209123,-5.02591888662151,
134.449288212205));
#198982=CARTESIAN_POINT('Ctrl Pts',(194.597850585309,0.349948891971121,
137.002980915508));
#198983=CARTESIAN_POINT('Ctrl Pts',(194.319402961497,5.40423073479611,133.860444384439));
#198984=CARTESIAN_POINT('Ctrl Pts',(194.040955337684,5.49228854369214,127.909516169605));
#198985=CARTESIAN_POINT('Ctrl Pts',(193.762507713871,0.533201494146887,
124.618808581434));
#198986=CARTESIAN_POINT('Ctrl Pts',(193.484060090058,-4.91587168017823,
127.012321133451));
#198987=CARTESIAN_POINT('Ctrl Pts',(193.205612466245,-5.84749893410212,
132.890532719942));
#198988=CARTESIAN_POINT('Ctrl Pts',(192.927164842432,-1.40556033379022,
136.851654059523));
#198989=CARTESIAN_POINT('Ctrl Pts',(192.648717218619,4.32801954783523,135.255608152653));
#198990=CARTESIAN_POINT('Ctrl Pts',(192.370269594806,6.08436090050943,129.569083216569));
#198991=CARTESIAN_POINT('Ctrl Pts',(192.091821970994,2.24947182316989,125.017717865345));
#198992=CARTESIAN_POINT('Ctrl Pts',(191.81337434718,-3.65257196685492,125.783994510198));
#198993=CARTESIAN_POINT('Ctrl Pts',(191.534926723368,-6.19808055740059,
131.163742349203));
#198994=CARTESIAN_POINT('Ctrl Pts',(191.256479099555,-3.04785590876364,
136.213235933607));
#198995=CARTESIAN_POINT('Ctrl Pts',(190.978031475742,2.90319942398833,136.292237340818));
#198996=CARTESIAN_POINT('Ctrl Pts',(190.699583851929,6.18635631527163,131.328148137043));
#198997=CARTESIAN_POINT('Ctrl Pts',(190.421136228116,3.7845539731278,125.882723791311));
#198998=CARTESIAN_POINT('Ctrl Pts',(190.142688604304,-2.09506858458051,
124.960043253581));
#198999=CARTESIAN_POINT('Ctrl Pts',(189.86424098049,-6.04942546284962,129.408004862578));
#199000=CARTESIAN_POINT('Ctrl Pts',(189.585793356678,-4.44465587162338,
135.139149194637));
#199001=CARTESIAN_POINT('Ctrl Pts',(189.307345732864,1.24453533211424,136.886834590562));
#199002=CARTESIAN_POINT('Ctrl Pts',(189.028898109051,5.79005936456987,133.045023550676));
#199003=CARTESIAN_POINT('Ctrl Pts',(188.750450485239,5.01480170111087,127.144152737732));
#199004=CARTESIAN_POINT('Ctrl Pts',(188.472002861426,-0.368813738986236,
124.606834155258));
#199005=CARTESIAN_POINT('Ctrl Pts',(188.193555237613,-5.41350737050784,
127.764739625646));
#199006=CARTESIAN_POINT('Ctrl Pts',(187.9151076138,-5.48345219307025,133.715908293866));
#199007=CARTESIAN_POINT('Ctrl Pts',(187.636659989987,-0.51437233173317,
136.991506884579));
#199008=CARTESIAN_POINT('Ctrl Pts',(187.358212366174,4.92739057398128,134.581420314804));
#199009=CARTESIAN_POINT('Ctrl Pts',(187.079764742362,5.84112225861874,128.700400402891));
#199010=CARTESIAN_POINT('Ctrl Pts',(186.801317118548,1.38714794227173,124.752817144095));
#199011=CARTESIAN_POINT('Ctrl Pts',(186.522869494736,-4.34154756707868,
126.366306703083));
#199012=CARTESIAN_POINT('Ctrl Pts',(186.244421870923,-6.08057295867359,
132.058150998494));
#199013=CARTESIAN_POINT('Ctrl Pts',(185.96597424711,-2.23184885375068,136.597823184897));
#199014=CARTESIAN_POINT('Ctrl Pts',(185.687526623297,3.66783531589119,135.813586298303));
#199015=CARTESIAN_POINT('Ctrl Pts',(185.409078999484,6.19695801394562,130.42611572539));
#199016=CARTESIAN_POINT('Ctrl Pts',(185.130631375671,3.03137903541329,125.386233730096));
#199017=CARTESIAN_POINT('Ctrl Pts',(184.852183751858,-2.9198891855651,125.325345654173));
#199018=CARTESIAN_POINT('Ctrl Pts',(184.573736128045,-6.18792188952598,
130.299404664846));
#199019=CARTESIAN_POINT('Ctrl Pts',(184.295288504232,-3.76955667380246,
135.737493527599));
#199020=CARTESIAN_POINT('Ctrl Pts',(184.01684088042,2.11284697206427,136.642274242971));
#199021=CARTESIAN_POINT('Ctrl Pts',(183.738393256607,6.05364746891681,132.182297534532));
#199022=CARTESIAN_POINT('Ctrl Pts',(183.459945632794,4.43144167895468,126.456064115361));
#199023=CARTESIAN_POINT('Ctrl Pts',(183.181498008981,-1.2630425260055,124.725702755623));
#199024=CARTESIAN_POINT('Ctrl Pts',(182.903050385168,-5.79685235262429,
128.581331012064));
#199025=CARTESIAN_POINT('Ctrl Pts',(182.624602761355,-5.00363805916239,
134.479814874928));
#199026=CARTESIAN_POINT('Ctrl Pts',(182.346155137542,0.387675169361259,
137.000735831198));
#199027=CARTESIAN_POINT('Ctrl Pts',(182.06770751373,5.42273385622678,133.827490675898));
#199028=CARTESIAN_POINT('Ctrl Pts',(181.789259889916,5.47456504449634,127.876136685104));
#199029=CARTESIAN_POINT('Ctrl Pts',(181.510812266103,0.495538404244469,
124.615677436551));
#199030=CARTESIAN_POINT('Ctrl Pts',(181.232364642291,-4.93886382111119,
127.042315697369));
#199031=CARTESIAN_POINT('Ctrl Pts',(180.953917018477,-5.83469147177671,
132.926089453735));
#199032=CARTESIAN_POINT('Ctrl Pts',(180.675469394665,-1.36872270040423,
136.860098061879));
#199033=CARTESIAN_POINT('Ctrl Pts',(180.397021770852,4.35503536681857,135.229179797918));
#199034=CARTESIAN_POINT('Ctrl Pts',(180.118574147039,6.07672868724052,129.532068871648));
#199035=CARTESIAN_POINT('Ctrl Pts',(179.840126523226,2.21420520878857,125.004131904969));
#199036=CARTESIAN_POINT('Ctrl Pts',(179.561678899413,-3.68306468660213,
125.80632176824));
#199037=CARTESIAN_POINT('Ctrl Pts',(179.2832312756,-6.19577806271818,131.20146516627));
#199038=CARTESIAN_POINT('Ctrl Pts',(179.004783651788,-3.01487407978163,
136.231688883676));
#199039=CARTESIAN_POINT('Ctrl Pts',(178.726336027974,2.93655189768736,136.274463064253));
#199040=CARTESIAN_POINT('Ctrl Pts',(178.447888404162,6.18943013971724,131.290480325685));
#199041=CARTESIAN_POINT('Ctrl Pts',(178.169440780348,3.75452445381909,125.859777323623));
#199042=CARTESIAN_POINT('Ctrl Pts',(177.890993156536,-2.13060578642238,
124.972904812372));
#199043=CARTESIAN_POINT('Ctrl Pts',(177.612545532723,-6.05781339482078,
129.44485530364));
#199044=CARTESIAN_POINT('Ctrl Pts',(177.33409790891,-4.41818643401566,135.166124762878));
#199045=CARTESIAN_POINT('Ctrl Pts',(177.055650285097,1.28153801924328,136.879146056599));
#199046=CARTESIAN_POINT('Ctrl Pts',(176.777202661284,5.80359163943039,133.009736301615));
#199047=CARTESIAN_POINT('Ctrl Pts',(176.498755037472,4.99242806419446,127.113694031581));
#199048=CARTESIAN_POINT('Ctrl Pts',(176.220307413658,-0.406533008366379,
124.60919405498));
#199049=CARTESIAN_POINT('Ctrl Pts',(175.941859789846,-5.43191010648008,
127.797749498684));
#199050=CARTESIAN_POINT('Ctrl Pts',(175.663412166033,-5.46562718029972,
133.749233679521));
#199051=CARTESIAN_POINT('Ctrl Pts',(175.38496454222,-0.476699886155768,
136.994523381468));
#199052=CARTESIAN_POINT('Ctrl Pts',(175.106516918407,4.95029131528126,134.551355909651));
#199053=CARTESIAN_POINT('Ctrl Pts',(174.828069294595,5.82820663315002,128.664882815304));
#199054=CARTESIAN_POINT('Ctrl Pts',(174.549621670781,1.35028477887665,124.744485301934));
#199055=CARTESIAN_POINT('Ctrl Pts',(174.271174046969,-4.36848282210566,
126.392817162263));
#199056=CARTESIAN_POINT('Ctrl Pts',(173.992726423155,-6.07282812182305,
132.095141942134));
#199057=CARTESIAN_POINT('Ctrl Pts',(173.714278799343,-2.19654105173196,
136.611301742902));
#199058=CARTESIAN_POINT('Ctrl Pts',(173.435831175529,3.69825993790488,135.791166334329));
#199059=CARTESIAN_POINT('Ctrl Pts',(173.157383551717,6.19454071464915,130.388400091055));
#199060=CARTESIAN_POINT('Ctrl Pts',(172.878935927904,2.99834119476844,125.367881250842));
#199061=CARTESIAN_POINT('Ctrl Pts',(172.600488304091,-2.95318740599396,
125.343221361866));
#199062=CARTESIAN_POINT('Ctrl Pts',(172.322040680278,-6.1908810518732,130.337081657394));
#199063=CARTESIAN_POINT('Ctrl Pts',(172.043593056465,-3.7394574524341,135.760348489473));
#199064=CARTESIAN_POINT('Ctrl Pts',(171.765145432652,2.14834486313941,136.629304580736));
#199065=CARTESIAN_POINT('Ctrl Pts',(171.486697808839,6.06192320196904,132.145421734178));
#199066=CARTESIAN_POINT('Ctrl Pts',(171.208250185027,4.40489025960108,126.42916923593));
#199067=CARTESIAN_POINT('Ctrl Pts',(170.929802561213,-1.30002164048796,
124.733503877423));
#199068=CARTESIAN_POINT('Ctrl Pts',(170.651354937401,-5.81027716255637,
128.616659285268));
#199069=CARTESIAN_POINT('Ctrl Pts',(170.372907313588,-4.98117182005496,
134.510205342342));
#199070=CARTESIAN_POINT('Ctrl Pts',(170.094459689775,0.42538708130529,136.998261137926));
#199071=CARTESIAN_POINT('Ctrl Pts',(169.816012065962,5.44103603626017,133.794424944161));
#199072=CARTESIAN_POINT('Ctrl Pts',(169.537564442149,5.45663868327959,127.842865707018));
#199073=CARTESIAN_POINT('Ctrl Pts',(169.259116818336,0.457856951984399,
124.612775615598));
#199074=CARTESIAN_POINT('Ctrl Pts',(168.980669194523,-4.9616729506289,127.072449665244));
#199075=CARTESIAN_POINT('Ctrl Pts',(168.702221570711,-5.82166780281318,
132.961567566087));
#199076=CARTESIAN_POINT('Ctrl Pts',(168.423773946897,-1.33183434849535,
136.868317666657));
#199077=CARTESIAN_POINT('Ctrl Pts',(168.145326323085,4.38188980836473,135.202587479883));
#199078=CARTESIAN_POINT('Ctrl Pts',(167.866878699272,6.06887129855542,129.495101671966));
#199079=CARTESIAN_POINT('Ctrl Pts',(167.588431075459,2.17885654621902,124.9907608742));
#199080=CARTESIAN_POINT('Ctrl Pts',(167.309983451646,-3.71342092903282,
125.82883423045));
#199081=CARTESIAN_POINT('Ctrl Pts',(167.031535827833,-6.19324598120115,
131.239173268482));
#199082=CARTESIAN_POINT('Ctrl Pts',(166.75308820402,-2.98178053353198,136.249940722101));
#199083=CARTESIAN_POINT('Ctrl Pts',(166.474640580207,2.96979555637586,136.25648609103));
#199084=CARTESIAN_POINT('Ctrl Pts',(166.196192956395,6.19227461255283,131.252794500981));
#199085=CARTESIAN_POINT('Ctrl Pts',(165.917745332582,3.7243558092261,125.837014079288));
#199086=CARTESIAN_POINT('Ctrl Pts',(165.639297708769,-2.16606403788322,
124.985982457902));
#199087=CARTESIAN_POINT('Ctrl Pts',(165.360850084956,-6.06597685228888,
129.481756121673));
#199088=CARTESIAN_POINT('Ctrl Pts',(165.082402461143,-4.39155327888481,
135.192938704347));
#199089=CARTESIAN_POINT('Ctrl Pts',(164.80395483733,1.31849321850979,136.871232419228));
#199090=CARTESIAN_POINT('Ctrl Pts',(164.525507213517,5.81690886006848,132.974367331546));
#199091=CARTESIAN_POINT('Ctrl Pts',(164.247059589704,4.96986943102014,127.083372084437));
#199092=CARTESIAN_POINT('Ctrl Pts',(163.968611965891,-0.444237213516358,
124.611783518878));
#199093=CARTESIAN_POINT('Ctrl Pts',(163.690164342078,-5.45011156102575,
127.830870782803));
#199094=CARTESIAN_POINT('Ctrl Pts',(163.411716718265,-5.44759963670407,
133.782449941821));
#199095=CARTESIAN_POINT('Ctrl Pts',(163.133269094453,-0.439009776288703,
136.9973104996));
#199096=CARTESIAN_POINT('Ctrl Pts',(162.85482147064,4.97300862171615,134.52115265821));
#199097=CARTESIAN_POINT('Ctrl Pts',(162.576373846827,5.81507504134112,128.629444506854));
#199098=CARTESIAN_POINT('Ctrl Pts',(162.297926223014,1.31337158018249,124.736378010682));
#199099=CARTESIAN_POINT('Ctrl Pts',(162.019478599201,-4.39525620139515,
126.419491092807));
#199100=CARTESIAN_POINT('Ctrl Pts',(161.741030975388,-6.06485825409316,
132.132085055398));
#199101=CARTESIAN_POINT('Ctrl Pts',(161.462583351575,-2.16115185607673,
136.624565122567));
#199102=CARTESIAN_POINT('Ctrl Pts',(161.184135727762,3.72854751953661,135.768561582436));
#199103=CARTESIAN_POINT('Ctrl Pts',(160.905688103949,6.19189387436843,130.350699870288));
#199104=CARTESIAN_POINT('Ctrl Pts',(160.627240480137,2.96519224948793,125.349730222329));
#199105=CARTESIAN_POINT('Ctrl Pts',(160.348792856324,-2.9863761949775,125.361299434083));
#199106=CARTESIAN_POINT('Ctrl Pts',(160.070345232511,-6.19361080884636,
130.374775965136));
#199107=CARTESIAN_POINT('Ctrl Pts',(159.791897608698,-3.70921966409463,
135.783019805394));
#199108=CARTESIAN_POINT('Ctrl Pts',(159.513449984885,2.18376314650564,136.616119073061));
#199109=CARTESIAN_POINT('Ctrl Pts',(159.235002361072,6.06997430822783,132.108496240312));
#199110=CARTESIAN_POINT('Ctrl Pts',(158.956554737259,4.37817561541891,126.402436480826));
#199111=CARTESIAN_POINT('Ctrl Pts',(158.678107113446,-1.3369525821905,124.741529957054));
#199112=CARTESIAN_POINT('Ctrl Pts',(158.399659489633,-5.82348667053154,
128.652068624549));
#199113=CARTESIAN_POINT('Ctrl Pts',(158.121211865821,-4.95852100179383,
134.540458488317));
#199114=CARTESIAN_POINT('Ctrl Pts',(157.842764242008,0.463083230374652,
136.995556927392));
#199115=CARTESIAN_POINT('Ctrl Pts',(157.564316618195,5.45913659670229,133.761248414491));
#199116=CARTESIAN_POINT('Ctrl Pts',(157.285868994382,5.43851012430973,127.809704468215));
#199117=CARTESIAN_POINT('Ctrl Pts',(157.007421370569,0.420158533666468,
124.610103226106));
#199118=CARTESIAN_POINT('Ctrl Pts',(156.728973746756,-4.98429822353081,
127.102721920452));
#199119=CARTESIAN_POINT('Ctrl Pts',(156.450526122943,-5.80842840980828,
132.996965742341));
#199120=CARTESIAN_POINT('Ctrl Pts',(156.172078499131,-1.2948966449748,136.876312569277));
#199121=CARTESIAN_POINT('Ctrl Pts',(155.893630875317,4.40858187737264,135.175832183934));
#199122=CARTESIAN_POINT('Ctrl Pts',(155.615183251505,6.06078902561252,129.458182987356));
#199123=CARTESIAN_POINT('Ctrl Pts',(155.336735627692,2.14342714531882,124.977605268507));
#199124=CARTESIAN_POINT('Ctrl Pts',(155.058288003879,-3.74363956928552,
125.85153106262));
#199125=CARTESIAN_POINT('Ctrl Pts',(154.779840380066,-6.19048440667673,
131.276865258552));
#199126=CARTESIAN_POINT('Ctrl Pts',(154.501392756253,-2.94857649630798,
136.267990772552));
#199127=CARTESIAN_POINT('Ctrl Pts',(154.22294513244,3.00292916819795,136.238307087292));
#199128=CARTESIAN_POINT('Ctrl Pts',(153.944497508627,6.19488962837548,131.215092059396));
#199129=CARTESIAN_POINT('Ctrl Pts',(153.666049884815,3.69404915725887,125.814434901805));
#199130=CARTESIAN_POINT('Ctrl Pts',(153.387602261001,-2.20144202504465,
124.999275705575));
#199131=CARTESIAN_POINT('Ctrl Pts',(153.109154637189,-6.07391553275397,
129.518705949301));
#199132=CARTESIAN_POINT('Ctrl Pts',(152.830707013376,-4.36475739313218,
135.219590025439));
#199133=CARTESIAN_POINT('Ctrl Pts',(152.552259389563,1.3553995605252,136.863093971691));
#199134=CARTESIAN_POINT('Ctrl Pts',(152.27381176575,5.83001053300956,132.93891795108));
#199135=CARTESIAN_POINT('Ctrl Pts',(151.995364141937,4.94712663750637,127.053188019893));
#199136=CARTESIAN_POINT('Ctrl Pts',(151.716916518124,-0.481924957293099,
124.614602450997));
#199137=CARTESIAN_POINT('Ctrl Pts',(151.438468894311,-5.46811105968323,
127.864102250682));
#199138=CARTESIAN_POINT('Ctrl Pts',(151.160021270498,-5.4293702303005,133.815555849925));
#199139=CARTESIAN_POINT('Ctrl Pts',(150.881573646685,-0.40130339875292,
136.999868135696));
#199140=CARTESIAN_POINT('Ctrl Pts',(150.603126022873,4.99554165148768,134.490811679673));
#199141=CARTESIAN_POINT('Ctrl Pts',(150.324678399059,5.80172796978809,128.59408679072));
#199142=CARTESIAN_POINT('Ctrl Pts',(150.046230775247,1.27640971402146,124.728495570759));
#199143=CARTESIAN_POINT('Ctrl Pts',(149.767783151434,-4.42186671284978,
126.446327506304));
#199144=CARTESIAN_POINT('Ctrl Pts',(149.489335527621,-6.05666365081033,
132.168978969345));
#199145=CARTESIAN_POINT('Ctrl Pts',(149.210887903808,-2.12568257814469,
136.637612832414));
#199146=CARTESIAN_POINT('Ctrl Pts',(148.932440279995,3.75869693846883,135.74577288025));
#199147=CARTESIAN_POINT('Ctrl Pts',(148.653992656183,6.18901759118317,130.313016460088));
#199148=CARTESIAN_POINT('Ctrl Pts',(148.375545032369,2.93193342791814,125.331781317152));
#199149=CARTESIAN_POINT('Ctrl Pts',(148.097097408557,-3.01945432269288,
125.379579200934));
#199150=CARTESIAN_POINT('Ctrl Pts',(147.818649784743,-6.19611105929333,
130.412486191295));
#199151=CARTESIAN_POINT('Ctrl Pts',(147.540202160931,-3.67884442925635,
135.805506635269));
#199152=CARTESIAN_POINT('Ctrl Pts',(147.261754537118,2.21910050972548,136.602718208539));
#199153=CARTESIAN_POINT('Ctrl Pts',(146.983306913305,6.07780048935632,132.071522421221));
#199154=CARTESIAN_POINT('Ctrl Pts',(146.704859289492,4.35129873632927,126.375866840638));
#199155=CARTESIAN_POINT('Ctrl Pts',(146.426411665679,-1.37383398262348,
124.749780697104));
#199156=CARTESIAN_POINT('Ctrl Pts',(146.147964041867,-5.83648038706648,
128.687557717801));
#199157=CARTESIAN_POINT('Ctrl Pts',(145.869516418053,-4.93568644371351,
134.570573191811));
#199158=CARTESIAN_POINT('Ctrl Pts',(145.591068794241,0.500762219724632,
136.992623299802));
#199159=CARTESIAN_POINT('Ctrl Pts',(145.312621170428,5.47703486683029,133.727962316256));
#199160=CARTESIAN_POINT('Ctrl Pts',(145.034173546615,5.42018003934715,127.776654197497));
#199161=CARTESIAN_POINT('Ctrl Pts',(144.755725922802,0.382444546219556,
124.607660367099));
#199162=CARTESIAN_POINT('Ctrl Pts',(144.477278298989,-5.00673880142907,
127.133131341243));
#199163=CARTESIAN_POINT('Ctrl Pts',(144.198830675176,-5.79497378335261,
133.032282670807));
#199164=CARTESIAN_POINT('Ctrl Pts',(143.920383051363,-1.25791095858285,
136.884082473484));
#199165=CARTESIAN_POINT('Ctrl Pts',(143.64193542755,4.43511058475782,135.148914901497));
#199166=CARTESIAN_POINT('Ctrl Pts',(143.363487803737,6.05248216790344,129.421314185853));
#199167=CARTESIAN_POINT('Ctrl Pts',(143.085040179924,2.10791831893749,124.964665575378));
#199168=CARTESIAN_POINT('Ctrl Pts',(142.806592556112,-3.77371948759721,
125.87441142371));
#199169=CARTESIAN_POINT('Ctrl Pts',(142.528144932299,-6.18749344147606,
131.314539739788));
#199170=CARTESIAN_POINT('Ctrl Pts',(142.249697308486,-2.91526319849757,
136.285838366179));
#199171=CARTESIAN_POINT('Ctrl Pts',(141.971249684673,3.03595150537554,136.219926726669));
#199172=CARTESIAN_POINT('Ctrl Pts',(141.69280206086,6.19727509028471,131.177374398005));
#199173=CARTESIAN_POINT('Ctrl Pts',(141.414354437047,3.6636056209416,125.792040627854));
#199174=CARTESIAN_POINT('Ctrl Pts',(141.135906813234,-2.23673843696229,
125.012784062803));
#199175=CARTESIAN_POINT('Ctrl Pts',(140.857459189421,-6.0816291420453,129.555703417335));
#199176=CARTESIAN_POINT('Ctrl Pts',(140.579011565609,-4.33779976968917,
135.246077738584));
#199177=CARTESIAN_POINT('Ctrl Pts',(140.300563941795,1.39225567771152,136.854731015561));
#199178=CARTESIAN_POINT('Ctrl Pts',(140.022116317983,5.84289617276637,132.903389473806));
#199179=CARTESIAN_POINT('Ctrl Pts',(139.74366869417,4.92420052639575,127.023142956427));
#199180=CARTESIAN_POINT('Ctrl Pts',(139.465221070357,-0.519594843163371,
124.617650746882));
#199181=CARTESIAN_POINT('Ctrl Pts',(139.186773446544,-5.48590793547459,
127.897442670915));
#199182=CARTESIAN_POINT('Ctrl Pts',(138.908325822731,-5.41093963658633,
133.848550177083));
#199183=CARTESIAN_POINT('Ctrl Pts',(138.629878198918,-0.363582150772119,
137.002196194983));
#199184=CARTESIAN_POINT('Ctrl Pts',(138.351430575105,5.0178895696262,134.460334098336));
#199185=CARTESIAN_POINT('Ctrl Pts',(138.072982951292,5.78816591307159,128.558810977095));
#199186=CARTESIAN_POINT('Ctrl Pts',(137.79453532748,1.23940055002892,124.720838274248));
#199187=CARTESIAN_POINT('Ctrl Pts',(137.516087703667,-4.44831337040726,
126.473325408321));
#199188=CARTESIAN_POINT('Ctrl Pts',(137.237640079854,-6.0482446156285,132.205822316857));
#199189=CARTESIAN_POINT('Ctrl Pts',(136.959192456041,-2.09013453226308,
136.650444388955));
#199190=CARTESIAN_POINT('Ctrl Pts',(136.680744832228,3.78870707750376,135.722801072215));
#199191=CARTESIAN_POINT('Ctrl Pts',(136.402297208415,6.18591197167502,130.275351256826));
#199192=CARTESIAN_POINT('Ctrl Pts',(136.123849584602,2.89856596247695,125.314035200413));
#199193=CARTESIAN_POINT('Ctrl Pts',(135.845401960789,-3.05242056341787,
125.398059985055));
#199194=CARTESIAN_POINT('Ctrl Pts',(135.566954336976,-6.19838171056633,
130.450210938505));
#199195=CARTESIAN_POINT('Ctrl Pts',(135.288506713164,-3.64833287348497,
135.827808145838));
#199196=CARTESIAN_POINT('Ctrl Pts',(135.01005908935,2.25435564335981,136.589102483743));
#199197=CARTESIAN_POINT('Ctrl Pts',(134.731611465538,6.08540145535266,132.034501646982));
#199198=CARTESIAN_POINT('Ctrl Pts',(134.453163841725,4.32426061826468,126.349461299917));
#199199=CARTESIAN_POINT('Ctrl Pts',(134.174716217912,-1.41066447513297,
124.75825579184));
#199200=CARTESIAN_POINT('Ctrl Pts',(133.896268594099,-5.84925783067434,
128.723125249964));
#199201=CARTESIAN_POINT('Ctrl Pts',(133.617820970286,-4.91266899195694,
134.600548336913));
#199202=CARTESIAN_POINT('Ctrl Pts',(133.339373346473,0.538422653146471,
136.989460363863));
#199203=CARTESIAN_POINT('Ctrl Pts',(133.06092572266,5.49473018341705,133.694567882885));
#199204=CARTESIAN_POINT('Ctrl Pts',(132.782478098847,5.40164910761999,127.743716119554));
#199205=CARTESIAN_POINT('Ctrl Pts',(132.504030475035,0.344716387149417,
124.605447129098));
#199206=CARTESIAN_POINT('Ctrl Pts',(132.225582851222,-5.02899385277987,
127.163676800786));
#199207=CARTESIAN_POINT('Ctrl Pts',(131.947135227409,-5.78130442201224,
133.067517042801));
#199208=CARTESIAN_POINT('Ctrl Pts',(131.668687603596,-1.22087865983776,
136.891627091362));
#199209=CARTESIAN_POINT('Ctrl Pts',(131.390239979783,4.46147494748924,135.121836630005));
#199210=CARTESIAN_POINT('Ctrl Pts',(131.11179235597,6.04395103324181,129.384496633644));
#199211=CARTESIAN_POINT('Ctrl Pts',(130.833344732157,2.07233138286776,124.951942274296));
#199212=CARTESIAN_POINT('Ctrl Pts',(130.554897108344,-3.80365956934553,
125.897474465882));
#199213=CARTESIAN_POINT('Ctrl Pts',(130.276449484532,-6.18427319643048,
131.35219531615));
#199214=CARTESIAN_POINT('Ctrl Pts',(129.998001860718,-2.88184187453723,
136.303482841632));
#199215=CARTESIAN_POINT('Ctrl Pts',(129.719554236906,3.0688613442533,136.201345690253));
#199216=CARTESIAN_POINT('Ctrl Pts',(129.441106613093,6.1994309098865,131.139642914452));
#199217=CARTESIAN_POINT('Ctrl Pts',(129.16265898928,3.63302632837089,125.769832087263));
#199218=CARTESIAN_POINT('Ctrl Pts',(128.884211365467,-2.27195196571463,
125.026507029031));
#199219=CARTESIAN_POINT('Ctrl Pts',(128.605763741654,-6.08911739433215,
129.592747154821));
#199220=CARTESIAN_POINT('Ctrl Pts',(128.327316117841,-4.31068140748063,
135.272400862266));
#199221=CARTESIAN_POINT('Ctrl Pts',(128.048868494028,1.42906020435147,136.846143860731));
#199222=CARTESIAN_POINT('Ctrl Pts',(127.770420870216,5.85556530185681,132.867783216248));
#199223=CARTESIAN_POINT('Ctrl Pts',(127.491973246402,4.9010919472237,126.993238007373));
#199224=CARTESIAN_POINT('Ctrl Pts',(127.21352562259,-0.557245475255655,
124.620928293575));
#199225=CARTESIAN_POINT('Ctrl Pts',(126.935077998777,-5.50350152892981,
127.930890808061));
#199226=CARTESIAN_POINT('Ctrl Pts',(126.656630374964,-5.39230853851415,
133.881431700678));
#199227=CARTESIAN_POINT('Ctrl Pts',(126.378182751151,-0.325847430121078,
137.004294591193));
#199228=CARTESIAN_POINT('Ctrl Pts',(126.099735127338,5.04005154802147,134.429721043558));
#199229=CARTESIAN_POINT('Ctrl Pts',(125.821287503525,5.77438937373851,128.523618373138));
#199230=CARTESIAN_POINT('Ctrl Pts',(125.542839879712,1.20234545959337,124.713406404895));
#199231=CARTESIAN_POINT('Ctrl Pts',(125.264392255899,-4.47459519407686,
126.50048379844));
#199232=CARTESIAN_POINT('Ctrl Pts',(124.985944632086,-6.03960146051831,
132.24261373269));
#199233=CARTESIAN_POINT('Ctrl Pts',(124.707497008274,-2.05450903567761,
136.663059316712));
#199234=CARTESIAN_POINT('Ctrl Pts',(124.429049384461,3.81857682460466,135.69964700956));
#199235=CARTESIAN_POINT('Ctrl Pts',(124.150601760648,6.18257713092382,130.237705656202));
#199236=CARTESIAN_POINT('Ctrl Pts',(123.872154136835,2.86509108960817,125.296492529702));
#199237=CARTESIAN_POINT('Ctrl Pts',(123.593706513022,-3.08527369557641,
125.416741101634));
#199238=CARTESIAN_POINT('Ctrl Pts',(123.315258889209,-6.20042267852561,
130.487948808862));
#199239=CARTESIAN_POINT('Ctrl Pts',(123.036811265396,-3.61768612739718,
135.849923510712));
#199240=CARTESIAN_POINT('Ctrl Pts',(122.758363641583,2.28952724101679,136.575272403211));
#199241=CARTESIAN_POINT('Ctrl Pts',(122.47991601777,6.09277692456002,131.997435289415));
#199242=CARTESIAN_POINT('Ctrl Pts',(122.201468393958,4.29706226313277,126.323220837128));
#199243=CARTESIAN_POINT('Ctrl Pts',(121.923020770144,-1.44744269495155,
124.766954927214));
#199244=CARTESIAN_POINT('Ctrl Pts',(121.644573146332,-5.86181852788225,
128.758769903068));
#199245=CARTESIAN_POINT('Ctrl Pts',(121.366125522519,-4.88946949944416,
134.630382812884));
#199246=CARTESIAN_POINT('Ctrl Pts',(121.087677898706,0.576063135118759,
136.986068236777));
#199247=CARTESIAN_POINT('Ctrl Pts',(120.809230274893,5.51222189075617,133.661066351821));
#199248=CARTESIAN_POINT('Ctrl Pts',(120.53078265108,5.38291801579874,127.710891454918));
#199249=CARTESIAN_POINT('Ctrl Pts',(120.252335027267,0.306975454486648,
124.603463594118));
#199250=CARTESIAN_POINT('Ctrl Pts',(119.973887403454,-5.05106255291402,
127.194357167205));
#199251=CARTESIAN_POINT('Ctrl Pts',(119.695439779642,-5.76742083231046,
133.102667552701));
#199252=CARTESIAN_POINT('Ctrl Pts',(119.416992155829,-1.18380112098488,
136.898946143343));
#199253=CARTESIAN_POINT('Ctrl Pts',(119.138544532016,4.48767398862585,135.09459837285));
#199254=CARTESIAN_POINT('Ctrl Pts',(118.860096908203,6.03519593775195,129.347731695017));
#199255=CARTESIAN_POINT('Ctrl Pts',(118.58164928439,2.0366676557964,124.939435836727));
#199256=CARTESIAN_POINT('Ctrl Pts',(118.303201660577,-3.83345870508974,
125.920719334523));
#199257=CARTESIAN_POINT('Ctrl Pts',(118.024754036764,-6.18082379086727,
131.389830592295));
#199258=CARTESIAN_POINT('Ctrl Pts',(117.746306412951,-2.84831376286653,
136.320923545089));
#199259=CARTESIAN_POINT('Ctrl Pts',(117.467858789138,3.10165746534553,136.18256466657));
#199260=CARTESIAN_POINT('Ctrl Pts',(117.189411165326,6.20135700729606,131.101899006891));
#199261=CARTESIAN_POINT('Ctrl Pts',(116.910963541513,3.60231241267338,125.747810102979));
#199262=CARTESIAN_POINT('Ctrl Pts',(116.6325159177,-2.30708130645123,125.040444095748));
#199263=CARTESIAN_POINT('Ctrl Pts',(116.354068293887,-6.09638001213474,
129.62983578909));
#199264=CARTESIAN_POINT('Ctrl Pts',(116.075620670074,-4.28340331138726,
135.298558421074));
#199265=CARTESIAN_POINT('Ctrl Pts',(115.797173046261,1.46581177664024,136.837332825402));
#199266=CARTESIAN_POINT('Ctrl Pts',(115.518725422448,5.86801745082159,132.832100497806));
#199267=CARTESIAN_POINT('Ctrl Pts',(115.240277798635,4.87780175628715,126.963474280869));
#199268=CARTESIAN_POINT('Ctrl Pts',(114.961830174822,-0.594875458411799,
124.624434969628));
#199269=CARTESIAN_POINT('Ctrl Pts',(114.68338255101,-5.52089118811201,127.964445422689));
#199270=CARTESIAN_POINT('Ctrl Pts',(114.404934927196,-5.37347762646609,
133.914199202272));
#199271=CARTESIAN_POINT('Ctrl Pts',(114.126487303384,-0.288100635073559,
137.006163246571));
#199272=CARTESIAN_POINT('Ctrl Pts',(113.848039679571,5.06202676545313,134.398973649715));
#199273=CARTESIAN_POINT('Ctrl Pts',(113.569592055758,5.76039886228364,128.488510282924));
#199274=CARTESIAN_POINT('Ctrl Pts',(113.291144431945,1.16524581580469,124.706200238089));
#199275=CARTESIAN_POINT('Ctrl Pts',(113.012696808132,-4.50071120997606,
126.527801670297));
#199276=CARTESIAN_POINT('Ctrl Pts',(112.734249184319,-6.03073450575487,
132.279351853526));
#199277=CARTESIAN_POINT('Ctrl Pts',(112.455801560506,-2.01880740850426,
136.675457148234));
#199278=CARTESIAN_POINT('Ctrl Pts',(112.177353936694,3.84830507293705,135.676311550269));
#199279=CARTESIAN_POINT('Ctrl Pts',(111.898906312881,6.17901319250346,130.200081053184));
#199280=CARTESIAN_POINT('Ctrl Pts',(111.620458689068,2.8315100497353,125.279153955068));
#199281=CARTESIAN_POINT('Ctrl Pts',(111.342011065255,-3.11801250178361,
125.435621858436));
#199282=CARTESIAN_POINT('Ctrl Pts',(111.063563441442,-6.20223388754234,
130.525698403974));
#199283=CARTESIAN_POINT('Ctrl Pts',(110.785115817629,-3.58690532661952,
135.871851910398));
#199284=CARTESIAN_POINT('Ctrl Pts',(110.506668193816,2.32461399939974,136.56122847942));
#199285=CARTESIAN_POINT('Ctrl Pts',(110.228220570003,6.09992662367788,131.960324722029));
#199286=CARTESIAN_POINT('Ctrl Pts',(109.94977294619,4.26970467877848,126.297146424621));
#199287=CARTESIAN_POINT('Ctrl Pts',(109.671325322378,-1.48416727924886,
124.775877780875));
#199288=CARTESIAN_POINT('Ctrl Pts',(109.392877698565,-5.8741620132489,128.794490356288));
#199289=CARTESIAN_POINT('Ctrl Pts',(109.114430074752,-4.86608882584101,
134.660075514194));
#199290=CARTESIAN_POINT('Ctrl Pts',(108.835982450939,0.61368227085971,136.982447044243));
#199291=CARTESIAN_POINT('Ctrl Pts',(108.557534827126,5.52950934068608,133.627458964475));
#199292=CARTESIAN_POINT('Ctrl Pts',(108.279087203313,5.36398745797076,127.67818141992));
#199293=CARTESIAN_POINT('Ctrl Pts',(108.0006395795,0.269223146735527,124.601709835656));
#199294=CARTESIAN_POINT('Ctrl Pts',(107.722191955687,-5.07294408406776,
127.225171303631));
#199295=CARTESIAN_POINT('Ctrl Pts',(107.443744331874,-5.75332352870873,
133.137732897993));
#199296=CARTESIAN_POINT('Ctrl Pts',(107.165296708062,-1.14667971594628,
136.906039358215));
#199297=CARTESIAN_POINT('Ctrl Pts',(106.886849084249,4.51370673735246,135.067201139359));
#199298=CARTESIAN_POINT('Ctrl Pts',(106.608401460436,6.02621720585718,129.31102073231));
#199299=CARTESIAN_POINT('Ctrl Pts',(106.329953836623,2.00092845925606,124.927146726103));
#199300=CARTESIAN_POINT('Ctrl Pts',(106.05150621281,-3.86311579061174,125.944145168289));
#199301=CARTESIAN_POINT('Ctrl Pts',(105.773058588997,-6.17714535260555,
131.427444173636));
#199302=CARTESIAN_POINT('Ctrl Pts',(105.494610965184,-2.81468010588189,
136.338159830278));
#199303=CARTESIAN_POINT('Ctrl Pts',(105.216163341371,3.13433865337982,136.163584351558));
#199304=CARTESIAN_POINT('Ctrl Pts',(104.937715717558,6.20305331114115,131.064144073934));
#199305=CARTESIAN_POINT('Ctrl Pts',(104.659268093745,3.57146501196475,125.725975491034));
#199306=CARTESIAN_POINT('Ctrl Pts',(104.380820469933,-2.34212515744159,
125.054594746511));
#199307=CARTESIAN_POINT('Ctrl Pts',(104.10237284612,-6.10341672633411,129.666967945808));
#199308=CARTESIAN_POINT('Ctrl Pts',(103.823925222307,-4.25596649220884,
135.324549445729));
#199309=CARTESIAN_POINT('Ctrl Pts',(103.545477598494,1.50250903273456,136.828298236068));
#199310=CARTESIAN_POINT('Ctrl Pts',(103.267029974681,5.88025215824177,132.796342640716));
#199311=CARTESIAN_POINT('Ctrl Pts',(102.988582350868,4.85433081661274,126.933852879821));
#199312=CARTESIAN_POINT('Ctrl Pts',(102.710134727055,-0.63248339823904,
124.628170645098));
#199313=CARTESIAN_POINT('Ctrl Pts',(102.431687103242,-5.53807626864099,
127.998105271418));
#199314=CARTESIAN_POINT('Ctrl Pts',(102.153239479429,-5.35444759822839,
133.946851467654));
#199315=CARTESIAN_POINT('Ctrl Pts',(101.874791855617,-0.250343164351048,
137.00780209187));
#199316=CARTESIAN_POINT('Ctrl Pts',(101.596344231803,5.0838144076213,134.368093056165));
#199317=CARTESIAN_POINT('Ctrl Pts',(101.317896607991,5.74619489713063,128.453488007394));
#199318=CARTESIAN_POINT('Ctrl Pts',(101.039448984178,1.12810299340375,124.69922004086));
#199319=CARTESIAN_POINT('Ctrl Pts',(100.761001360365,-4.52666045036627,
126.55527801162));
#199320=CARTESIAN_POINT('Ctrl Pts',(100.482553736552,-6.0216440799065,132.316035318018));
#199321=CARTESIAN_POINT('Ctrl Pts',(100.204106112739,-1.98303097367997,
136.687637424115));
#199322=CARTESIAN_POINT('Ctrl Pts',(99.9256584889259,3.87789072090961,135.652795559044));
#199323=CARTESIAN_POINT('Ctrl Pts',(99.6472108651132,6.17522028847693,130.162478841968));
#199324=CARTESIAN_POINT('Ctrl Pts',(99.3687632413001,2.79782408721636,125.262020118999));
#199325=CARTESIAN_POINT('Ctrl Pts',(99.0903156174874,-3.15063576889091,
125.454701555827));
#199326=CARTESIAN_POINT('Ctrl Pts',(98.8118679936743,-6.20381527050148,
130.563458325018));
#199327=CARTESIAN_POINT('Ctrl Pts',(98.5334203698616,-3.55599161174595,
135.89359253233));
#199328=CARTESIAN_POINT('Ctrl Pts',(98.2549727460486,2.35961461835606,136.546971232774));
#199329=CARTESIAN_POINT('Ctrl Pts',(97.9765251222358,6.10685028777152,131.923171319966));
#199330=CARTESIAN_POINT('Ctrl Pts',(97.6980774984228,4.24218887894701,126.271239028595));
#199331=CARTESIAN_POINT('Ctrl Pts',(97.4196298746099,-1.52083686718185,
124.785024022185));
#199332=CARTESIAN_POINT('Ctrl Pts',(97.141182250797,-5.88628782938184,128.830285285991));
#199333=CARTESIAN_POINT('Ctrl Pts',(96.8627346269842,-4.842527837527,134.689625340572));
#199334=CARTESIAN_POINT('Ctrl Pts',(96.5842870031713,0.651278666378471,
136.978596920444));
#199335=CARTESIAN_POINT('Ctrl Pts',(96.3058393793584,5.54659189261388,133.593746966183));
#199336=CARTESIAN_POINT('Ctrl Pts',(96.0273917555454,5.34485813561491,127.645587226641));
#199337=CARTESIAN_POINT('Ctrl Pts',(95.7489441317327,0.231460862821695,
124.6001859187));
#199338=CARTESIAN_POINT('Ctrl Pts',(95.4704965079195,-5.09463763541278,
127.256118068232));
#199339=CARTESIAN_POINT('Ctrl Pts',(95.192048884107,-5.73901303358793,133.172711779316));
#199340=CARTESIAN_POINT('Ctrl Pts',(94.9136012602939,-1.10951582026908,
136.912906473138));
#199341=CARTESIAN_POINT('Ctrl Pts',(94.635153636481,4.53957222901603,135.039645944743));
#199342=CARTESIAN_POINT('Ctrl Pts',(94.3567060126683,6.01701517026768,129.274365105863));
#199343=CARTESIAN_POINT('Ctrl Pts',(94.0782583888551,1.96511511757592,124.915075397801));
#199344=CARTESIAN_POINT('Ctrl Pts',(93.7998107650425,-3.89262972695748,
125.967751099126));
#199345=CARTESIAN_POINT('Ctrl Pts',(93.5213631412293,-6.17323801795121,
131.465034666385));
#199346=CARTESIAN_POINT('Ctrl Pts',(93.2429155174167,-2.7809421498907,136.355191058501));
#199347=CARTESIAN_POINT('Ctrl Pts',(92.9644678936037,3.16690369734264,136.14440544854));
#199348=CARTESIAN_POINT('Ctrl Pts',(92.6860202697908,6.20451975856463,131.026379514606));
#199349=CARTESIAN_POINT('Ctrl Pts',(92.4075726459779,3.54048526930663,125.704329060518));
#199350=CARTESIAN_POINT('Ctrl Pts',(92.129125022165,-2.37708222012305,125.068958456964));
#199351=CARTESIAN_POINT('Ctrl Pts',(91.850677398352,-6.1102272761821,129.70414224903));
#199352=CARTESIAN_POINT('Ctrl Pts',(91.5722297745392,-4.22837196662692,
135.350372973126));
#199353=CARTESIAN_POINT('Ctrl Pts',(91.2937821507264,1.53915061280415,136.819040427511));
#199354=CARTESIAN_POINT('Ctrl Pts',(91.0153345269133,5.89226897075567,132.76051097));
#199355=CARTESIAN_POINT('Ctrl Pts',(90.7368869031008,4.8306799979248,126.90437490186));
#199356=CARTESIAN_POINT('Ctrl Pts',(90.4584392792875,-0.670067901161403,
124.632135181558));
#199357=CARTESIAN_POINT('Ctrl Pts',(90.1799916554748,-5.5550561337172,128.031869106972));
#199358=CARTESIAN_POINT('Ctrl Pts',(89.9015440316619,-5.3352191589658,133.979387286881));
#199359=CARTESIAN_POINT('Ctrl Pts',(89.6230964078489,-0.212576417070642,
137.009211066365));
#199360=CARTESIAN_POINT('Ctrl Pts',(89.3446487840362,5.10541366717708,134.337080407198));
#199361=CARTESIAN_POINT('Ctrl Pts',(89.0662011602232,5.73177800461257,128.418552844315));
#199362=CARTESIAN_POINT('Ctrl Pts',(88.7877535364103,1.09091836873142,124.69246607186));
#199363=CARTESIAN_POINT('Ctrl Pts',(88.5093059125973,-4.5524419536888,126.58291180426));
#199364=CARTESIAN_POINT('Ctrl Pts',(88.2308582887847,-6.0123305198223,132.352662766849));
#199365=CARTESIAN_POINT('Ctrl Pts',(87.9524106649715,-1.94718105691378,
136.69959969301));
#199366=CARTESIAN_POINT('Ctrl Pts',(87.6739630411587,3.90733267221543,135.629099907278));
#199367=CARTESIAN_POINT('Ctrl Pts',(87.395515417346,6.17119855939173,130.124900415918));
#199368=CARTESIAN_POINT('Ctrl Pts',(87.1170677935327,2.76403445029686,125.245091656395));
#199369=CARTESIAN_POINT('Ctrl Pts',(86.8386201697203,-3.18314228803115,
125.473979486801));
#199370=CARTESIAN_POINT('Ctrl Pts',(86.5601725459069,-6.20516676880425,
130.601227172784));
#199371=CARTESIAN_POINT('Ctrl Pts',(86.2817249220945,-3.52494612829556,
135.915144570902));
#199372=CARTESIAN_POINT('Ctrl Pts',(86.0032772982812,2.394527800925,136.532501191579));
#199373=CARTESIAN_POINT('Ctrl Pts',(85.7248296744686,6.11354766028192,131.885976459962));
#199374=CARTESIAN_POINT('Ctrl Pts',(85.4463820506556,4.21451588324655,126.245499609054));
#199375=CARTESIAN_POINT('Ctrl Pts',(85.1679344268427,-1.55745009994542,
124.794393312227));
#199376=CARTESIAN_POINT('Ctrl Pts',(84.8894868030298,-5.89819552695468,
128.86615336578));
#199377=CARTESIAN_POINT('Ctrl Pts',(84.611039179217,-4.81878740756302,134.719031197036));
#199378=CARTESIAN_POINT('Ctrl Pts',(84.332591555404,0.68885092852684,136.974518008049));
#199379=CARTESIAN_POINT('Ctrl Pts',(84.0541439315912,5.56346891353935,133.559931606153));
#199380=CARTESIAN_POINT('Ctrl Pts',(83.7756963077782,5.32553075757526,127.613110082872));
#199381=CARTESIAN_POINT('Ctrl Pts',(83.4972486839655,0.193690002040587,
124.598891899719));
#199382=CARTESIAN_POINT('Ctrl Pts',(83.2188010601524,-5.11614240308669,
127.287196314267));
#199383=CARTESIAN_POINT('Ctrl Pts',(82.9403534363397,-5.72448987722869,
133.207602900518));
#199384=CARTESIAN_POINT('Ctrl Pts',(82.6619058125266,-1.07231081107503,
136.919547233648));
#199385=CARTESIAN_POINT('Ctrl Pts',(82.3834581887138,4.56526950516122,135.011933810073));
#199386=CARTESIAN_POINT('Ctrl Pts',(82.1050105649009,6.00759017196827,129.237766173961));
#199387=CARTESIAN_POINT('Ctrl Pts',(81.826562941088,1.92922895783247,124.903222299129));
#199388=CARTESIAN_POINT('Ctrl Pts',(81.5481153172751,-3.92199942047723,
125.991536252305));
#199389=CARTESIAN_POINT('Ctrl Pts',(81.2696676934623,-6.16910193169181,
131.502600677615));
#199390=CARTESIAN_POINT('Ctrl Pts',(80.9912200696492,-2.74710114506546,
136.372016598662));
#199391=CARTESIAN_POINT('Ctrl Pts',(80.7127724458365,3.19935139052435,136.125028668197));
#199392=CARTESIAN_POINT('Ctrl Pts',(80.4343248220235,6.20575629522666,130.988606728286));
#199393=CARTESIAN_POINT('Ctrl Pts',(80.1558771982107,3.50937433266497,125.682871613546));
#199394=CARTESIAN_POINT('Ctrl Pts',(79.8774295743978,-2.41195119914859,
125.083534694853));
#199395=CARTESIAN_POINT('Ctrl Pts',(79.5989819505849,-6.11681140931136,
129.741357321249));
#199396=CARTESIAN_POINT('Ctrl Pts',(79.320534326772,-4.20062075716678,135.376028046362));
#199397=CARTESIAN_POINT('Ctrl Pts',(79.0420867029591,1.57573515908161,136.809559742781));
#199398=CARTESIAN_POINT('Ctrl Pts',(78.7636390791462,5.90406744307602,132.724606813414));
#199399=CARTESIAN_POINT('Ctrl Pts',(78.4851914553333,4.80685017661309,126.875041439303));
#199400=CARTESIAN_POINT('Ctrl Pts',(78.2067438315204,-0.707627574471386,
124.636328432103));
#199401=CARTESIAN_POINT('Ctrl Pts',(77.9282962077074,-5.57183015414549,
128.065735678218));
#199402=CARTESIAN_POINT('Ctrl Pts',(77.6498485838947,-5.31579302119528,
134.011805454327));
#199403=CARTESIAN_POINT('Ctrl Pts',(77.3714009600817,-0.174801792692954,
137.010390117845));
#199404=CARTESIAN_POINT('Ctrl Pts',(77.0929533362689,5.12682374375196,134.305936852001));
#199405=CARTESIAN_POINT('Ctrl Pts',(76.814505712456,5.7171487189526,128.38370608822));
#199406=CARTESIAN_POINT('Ctrl Pts',(76.536058088643,1.05369331967776,124.68593858136));
#199407=CARTESIAN_POINT('Ctrl Pts',(76.2576104648302,-4.57805476460059,
126.610702024239));
#199408=CARTESIAN_POINT('Ctrl Pts',(75.9791628410172,-6.00279417061961,
132.389232842773));
#199409=CARTESIAN_POINT('Ctrl Pts',(75.7007152172044,-1.91125898663751,
136.711343511654));
#199410=CARTESIAN_POINT('Ctrl Pts',(75.4222675933915,3.93662983587222,135.605225473025));
#199411=CARTESIAN_POINT('Ctrl Pts',(75.1438199695785,6.16694815427437,130.087347167514));
#199412=CARTESIAN_POINT('Ctrl Pts',(74.8653723457658,2.73014239106432,125.228369194547));
#199413=CARTESIAN_POINT('Ctrl Pts',(74.5869247219528,-3.21553085466319,
125.493454937009));
#199414=CARTESIAN_POINT('Ctrl Pts',(74.3084770981399,-6.20628833237051,
130.639003547736));
#199415=CARTESIAN_POINT('Ctrl Pts',(74.0300294743271,-3.49377002667009,
135.936507227495));
#199416=CARTESIAN_POINT('Ctrl Pts',(73.7515818505141,2.42935225338577,136.517818892029));
#199417=CARTESIAN_POINT('Ctrl Pts',(73.4731342267013,6.1200184930355,131.848741520285));
#199418=CARTESIAN_POINT('Ctrl Pts',(73.1946866028884,4.18668671711015,126.219929119786));
#199419=CARTESIAN_POINT('Ctrl Pts',(72.9162389790755,-1.59400562082267,
124.803985303816));
#199420=CARTESIAN_POINT('Ctrl Pts',(72.6377913552626,-5.90988466472314,
128.902093266552));
#199421=CARTESIAN_POINT('Ctrl Pts',(72.3593437314497,-4.79486841565966,
134.748291993943));
#199422=CARTESIAN_POINT('Ctrl Pts',(72.0808961076369,0.726397665050741,
136.970210458201));
#199423=CARTESIAN_POINT('Ctrl Pts',(71.8024484838239,5.58013977807825,133.526014137426));
#199424=CARTESIAN_POINT('Ctrl Pts',(71.524000860011,5.30600604003494,127.580751192065));
#199425=CARTESIAN_POINT('Ctrl Pts',(71.2455532361981,0.155911964005252,
124.597827826664));
#199426=CARTESIAN_POINT('Ctrl Pts',(70.9671056123853,-5.13745759022245,
127.318404890117));
#199427=CARTESIAN_POINT('Ctrl Pts',(70.6886579885723,-5.70975459779179,
133.242404968692));
#199428=CARTESIAN_POINT('Ctrl Pts',(70.4102103647595,-1.03506606700937,
136.925961393668));
#199429=CARTESIAN_POINT('Ctrl Pts',(70.1317627409465,4.59079761356593,134.98406576223));
#199430=CARTESIAN_POINT('Ctrl Pts',(69.8533151171337,5.99794256020584,129.201225292793));
#199431=CARTESIAN_POINT('Ctrl Pts',(69.5748674933208,1.89327130980037,124.891587869307));
#199432=CARTESIAN_POINT('Ctrl Pts',(69.2964198695077,-3.95122378286636,
126.015499746463));
#199433=CARTESIAN_POINT('Ctrl Pts',(69.0179722456952,-6.16473724709165,
131.540140815303));
#199434=CARTESIAN_POINT('Ctrl Pts',(68.7395246218819,-2.71315834539685,
136.388635827283));
#199435=CARTESIAN_POINT('Ctrl Pts',(68.4610769980694,3.23168053056381,136.105454728543));
#199436=CARTESIAN_POINT('Ctrl Pts',(68.1826293742561,6.20676287530703,130.950827114659));
#199437=CARTESIAN_POINT('Ctrl Pts',(67.9041817504435,3.47813335486666,125.661603945233));
#199438=CARTESIAN_POINT('Ctrl Pts',(67.6257341266304,-2.44673080243567,
125.09832292005));
#199439=CARTESIAN_POINT('Ctrl Pts',(67.3472865028177,-6.12316888174425,
129.778611783445));
#199440=CARTESIAN_POINT('Ctrl Pts',(67.0688388790048,-4.17271389215982,
135.401513714782));
#199441=CARTESIAN_POINT('Ctrl Pts',(66.7903912551918,1.61226131591331,136.799856533191));
#199442=CARTESIAN_POINT('Ctrl Pts',(66.511943631379,5.91564713800617,132.688631501398));
#199443=CARTESIAN_POINT('Ctrl Pts',(66.233496007566,4.78284223570014,126.845853579115));
#199444=CARTESIAN_POINT('Ctrl Pts',(65.9550483837533,-0.745161026381345,
124.640750241348));
#199445=CARTESIAN_POINT('Ctrl Pts',(65.6766007599402,-5.58839770835831,
128.099703730218));
#199446=CARTESIAN_POINT('Ctrl Pts',(65.3981531361275,-5.2961699047596,134.044104768727));
#199447=CARTESIAN_POINT('Ctrl Pts',(65.1197055123145,-0.137020690970298,
137.011339202618));
#199448=CARTESIAN_POINT('Ctrl Pts',(64.8412578885016,5.14804384398771,134.274663544608));
#199449=CARTESIAN_POINT('Ctrl Pts',(64.5628102646887,5.70230758224426,128.348949030369));
#199450=CARTESIAN_POINT('Ctrl Pts',(64.2843626408759,1.01642922563077,124.679637811238));
#199451=CARTESIAN_POINT('Ctrl Pts',(64.0059150170629,-4.60349793400934,
126.638647641779));
#199452=CARTESIAN_POINT('Ctrl Pts',(63.72746739325,-5.9930353856715,132.425744190676));
#199453=CARTESIAN_POINT('Ctrl Pts',(63.4490197694371,-1.87526609395646,
136.722868444874));
#199454=CARTESIAN_POINT('Ctrl Pts',(63.1705721456243,3.96578112626272,135.581173140958));
#199455=CARTESIAN_POINT('Ctrl Pts',(62.8921245218114,6.16246923062527,130.049820488308));
#199456=CARTESIAN_POINT('Ctrl Pts',(62.6136768979985,2.69614916540168,125.211853353112));
#199457=CARTESIAN_POINT('Ctrl Pts',(62.3352292741856,-3.24780026861702,
125.513127184779));
#199458=CARTESIAN_POINT('Ctrl Pts',(62.0567816503727,-6.20717991964031,
130.676786050054));
#199459=CARTESIAN_POINT('Ctrl Pts',(61.7783340265599,-3.46246446211126,
135.957679710507));
#199460=CARTESIAN_POINT('Ctrl Pts',(61.4998864027468,2.46408668530527,136.502924878181));
#199461=CARTESIAN_POINT('Ctrl Pts',(61.2214387789342,6.12626254625314,131.81146788069));
#199462=CARTESIAN_POINT('Ctrl Pts',(60.942991155121,4.15870241175792,126.194528508313));
#199463=CARTESIAN_POINT('Ctrl Pts',(60.6645435313083,-1.63050207523548,
124.813799641521));
#199464=CARTESIAN_POINT('Ctrl Pts',(60.3860959074953,-5.92135480954196,
128.938103656541));
#199465=CARTESIAN_POINT('Ctrl Pts',(60.1076482836825,-4.77077174814381,
134.777406647022));
#199466=CARTESIAN_POINT('Ctrl Pts',(59.8292006598696,0.763917484641806,
136.965674430521));
#199467=CARTESIAN_POINT('Ctrl Pts',(59.5507530360567,5.59660386848551,133.491995816827));
#199468=CARTESIAN_POINT('Ctrl Pts',(59.2723054122438,5.28628470648961,127.548511753291));
#199469=CARTESIAN_POINT('Ctrl Pts',(58.9938577884309,0.11812814859451,124.596993738963));
#199470=CARTESIAN_POINT('Ctrl Pts',(58.715410164618,-5.15858240697801,127.34974263934));
#199471=CARTESIAN_POINT('Ctrl Pts',(58.4369625408051,-5.69480774129836,
133.277116694236));
#199472=CARTESIAN_POINT('Ctrl Pts',(58.1585149169922,-0.997782968190397,
136.932148715521));
#199473=CARTESIAN_POINT('Ctrl Pts',(57.8800672931793,4.61615560827684,134.956042833877));
#199474=CARTESIAN_POINT('Ctrl Pts',(57.6016196693665,5.98807269247603,129.164743816393));
#199475=CARTESIAN_POINT('Ctrl Pts',(57.3231720455535,1.85724350590365,124.880172539454));
#199476=CARTESIAN_POINT('Ctrl Pts',(57.0447244217407,-3.98030173120474,
126.039640693622));
#199477=CARTESIAN_POINT('Ctrl Pts',(56.7662767979277,-6.16014412588574,
131.577653688385));
#199478=CARTESIAN_POINT('Ctrl Pts',(56.4878291741149,-2.67911500864857,
136.405048128532));
#199479=CARTESIAN_POINT('Ctrl Pts',(56.209381550302,3.26388991949243,136.085684354897));
#199480=CARTESIAN_POINT('Ctrl Pts',(55.9309339264891,6.20753946150667,130.913042073662));
#199481=CARTESIAN_POINT('Ctrl Pts',(55.6524863026762,3.44676349355797,125.640526843659));
#199482=CARTESIAN_POINT('Ctrl Pts',(55.3740386788633,-2.48141974121268,
125.113322584571));
#199483=CARTESIAN_POINT('Ctrl Pts',(55.0955910550504,-6.12929945790263,
129.815904255142));
#199484=CARTESIAN_POINT('Ctrl Pts',(54.8171434312375,-4.14465240570495,
135.426829034002));
#199485=CARTESIAN_POINT('Ctrl Pts',(54.5386958074246,1.64872772980914,136.789931158292));
#199486=CARTESIAN_POINT('Ctrl Pts',(54.2602481836117,5.92700762645589,132.652586367033));
#199487=CARTESIAN_POINT('Ctrl Pts',(53.9818005597989,4.75865706480954,126.81681240286));
#199488=CARTESIAN_POINT('Ctrl Pts',(53.703352935986,-0.78266686607524,124.645400445441));
#199489=CARTESIAN_POINT('Ctrl Pts',(53.4249053121731,-5.604758182439,128.133772004274));
#199490=CARTESIAN_POINT('Ctrl Pts',(53.1464576883601,-5.27635053680027,
134.076284033214));
#199491=CARTESIAN_POINT('Ctrl Pts',(52.8680100645473,-0.0992345118958833,
137.012058285519));
#199492=CARTESIAN_POINT('Ctrl Pts',(52.5895624407343,5.1690731815654,134.243261643865));
#199493=CARTESIAN_POINT('Ctrl Pts',(52.3111148169216,5.68725514443172,128.314282958697));
#199494=CARTESIAN_POINT('Ctrl Pts',(52.0326671931086,0.979127467424884,
124.673563994973));
#199495=CARTESIAN_POINT('Ctrl Pts',(51.7542195692957,-4.62877051910935,
126.666747621346));
#199496=CARTESIAN_POINT('Ctrl Pts',(51.4757719454828,-5.98305452659317,
132.462195457613));
#199497=CARTESIAN_POINT('Ctrl Pts',(51.1973243216699,-1.83920371260068,
136.734174065611));
#199498=CARTESIAN_POINT('Ctrl Pts',(50.9188766978571,3.99478546317524,135.556943802347));
#199499=CARTESIAN_POINT('Ctrl Pts',(50.6404290740441,6.15776195441257,130.012321768865));
#199500=CARTESIAN_POINT('Ctrl Pts',(50.3619814502312,2.66205603294,125.195544744091));
#199501=CARTESIAN_POINT('Ctrl Pts',(50.0835338264184,-3.27994933413751,
125.532995501151));
#199502=CARTESIAN_POINT('Ctrl Pts',(49.8050862026055,-6.20784149757545,
130.714573279694));
#199503=CARTESIAN_POINT('Ctrl Pts',(49.5266385787925,-3.43103059465853,
135.978661235386));
#199504=CARTESIAN_POINT('Ctrl Pts',(49.2481909549797,2.4987298095866,136.487819701939));
#199505=CARTESIAN_POINT('Ctrl Pts',(48.9697433311668,6.13227958855924,131.774156922365));
#199506=CARTESIAN_POINT('Ctrl Pts',(48.6912957073539,4.13056400415832,126.169298715863));
#199507=CARTESIAN_POINT('Ctrl Pts',(48.412848083541,-1.66693811079436,124.823835961664));
#199508=CARTESIAN_POINT('Ctrl Pts',(48.1344004597282,-5.93260553638082,
128.974183201367));
#199509=CARTESIAN_POINT('Ctrl Pts',(47.8559528359152,-4.7464982979263,134.806374077418));
#199510=CARTESIAN_POINT('Ctrl Pts',(47.5775052121024,0.801408996989757,
136.960910093092));
#199511=CARTESIAN_POINT('Ctrl Pts',(47.2990575882894,5.61286057467834,133.457877904919));
#199512=CARTESIAN_POINT('Ctrl Pts',(47.0206099644766,5.26636748772036,127.516392961194));
#199513=CARTESIAN_POINT('Ctrl Pts',(46.7421623406636,0.0803399559020909,
124.596389667526));
#199514=CARTESIAN_POINT('Ctrl Pts',(46.4637147168508,-5.17951607056515,
127.381208400702));
#199515=CARTESIAN_POINT('Ctrl Pts',(46.1852670930379,-5.67964986161014,
133.311736790894));
#199516=CARTESIAN_POINT('Ctrl Pts',(45.9068194692249,-0.960462896156299,
136.938108969933));
#199517=CARTESIAN_POINT('Ctrl Pts',(45.6283718454121,4.64134254964412,134.927866063412));
#199518=CARTESIAN_POINT('Ctrl Pts',(45.3499242215992,5.97798093451044,129.128323096598));
#199519=CARTESIAN_POINT('Ctrl Pts',(45.0714765977863,1.82114688116607,124.868976732569));
#199520=CARTESIAN_POINT('Ctrl Pts',(44.7930289739735,-4.00923218799886,
126.063958199228));
#199521=CARTESIAN_POINT('Ctrl Pts',(44.5145813501605,-6.15532273827383,
131.615137906808));
#199522=CARTESIAN_POINT('Ctrl Pts',(44.2361337263477,-2.644972396308,136.421252894246));
#199523=CARTESIAN_POINT('Ctrl Pts',(43.9576861025347,3.29597836378001,136.065718279858));
#199524=CARTESIAN_POINT('Ctrl Pts',(43.6792384787219,6.20808602504863,130.875253005433));
#199525=CARTESIAN_POINT('Ctrl Pts',(43.4007908549089,3.41526591116036,125.619641089845));
#199526=CARTESIAN_POINT('Ctrl Pts',(43.1223432310961,-2.5160167300689,125.128533132602));
#199527=CARTESIAN_POINT('Ctrl Pts',(42.8438956072832,-6.13520291061547,
129.853233354452));
#199528=CARTESIAN_POINT('Ctrl Pts',(42.5654479834703,-4.11643733763101,
135.451973065955));
#199529=CARTESIAN_POINT('Ctrl Pts',(42.2870003596574,1.68513304949262,136.779783985877));
#199530=CARTESIAN_POINT('Ctrl Pts',(42.0085527358444,5.93814848745852,132.616472745983));
#199531=CARTESIAN_POINT('Ctrl Pts',(41.7301051120316,4.73429556013123,126.787918986671));
#199532=CARTESIAN_POINT('Ctrl Pts',(41.4516574882187,-0.820143703760798,
124.65027887207));
#199533=CARTESIAN_POINT('Ctrl Pts',(41.1732098644058,-5.62091097014408,
128.167939237972));
#199534=CARTESIAN_POINT('Ctrl Pts',(40.8947622405929,-5.25633565173145,
134.108342055376));
#199535=CARTESIAN_POINT('Ctrl Pts',(40.61631461678,-0.0614446556499193,
137.012547339898));
#199536=CARTESIAN_POINT('Ctrl Pts',(40.3378669929672,5.18991097723558,134.211732313379));
#199537=CARTESIAN_POINT('Ctrl Pts',(40.0594193691542,5.67199196328813,128.279709157768));
#199538=CARTESIAN_POINT('Ctrl Pts',(39.7809717453414,0.941789427290636,
124.66771735763));
#199539=CARTESIAN_POINT('Ctrl Pts',(39.5025241215285,-4.65387158341555,
126.695000921683));
#199540=CARTESIAN_POINT('Ctrl Pts',(39.2240764977156,-5.97285196322902,
132.49858529287));
#199541=CARTESIAN_POINT('Ctrl Pts',(38.9456288739027,-1.80307317887526,
136.745259954929));
#199542=CARTESIAN_POINT('Ctrl Pts',(38.6671812500898,4.02364177184326,135.532538355018));
#199543=CARTESIAN_POINT('Ctrl Pts',(38.3887336262769,6.15282650006613,129.974852398711));
#199544=CARTESIAN_POINT('Ctrl Pts',(38.110286002464,2.62786425701304,125.179443971804));
#199545=CARTESIAN_POINT('Ctrl Pts',(37.8318383786511,-3.31197685992897,
125.553059149895));
#199546=CARTESIAN_POINT('Ctrl Pts',(37.5533907548383,-6.20827304166094,
130.752363836438));
#199547=CARTESIAN_POINT('Ctrl Pts',(37.2749431310254,-3.3994695891056,135.999451024653));
#199548=CARTESIAN_POINT('Ctrl Pts',(36.9964955072125,2.53328034251594,136.47250392303));
#199549=CARTESIAN_POINT('Ctrl Pts',(36.7180478833995,6.13806939699002,131.73681002788));
#199550=CARTESIAN_POINT('Ctrl Pts',(36.4396002595867,4.10227253699055,126.144240677337));
#199551=CARTESIAN_POINT('Ctrl Pts',(36.1611526357737,-1.70331237734853,
124.834093892349));
#199552=CARTESIAN_POINT('Ctrl Pts',(35.8827050119609,-5.94363642833981,
129.01033056409));
#199553=CARTESIAN_POINT('Ctrl Pts',(35.604257388148,-4.72204896446884,134.835193211735));
#199554=CARTESIAN_POINT('Ctrl Pts',(35.3258097643351,0.838870812832614,
136.955917622458));
#199555=CARTESIAN_POINT('Ctrl Pts',(35.0473621405222,5.62890929425843,133.423661665951));
#199556=CARTESIAN_POINT('Ctrl Pts',(34.7689145167094,5.24625512176713,127.484396005948));
#199557=CARTESIAN_POINT('Ctrl Pts',(34.4904668928964,0.0425487861828518,
124.596015634733));
#199558=CARTESIAN_POINT('Ctrl Pts',(34.2120192690835,-5.20025780527969,
127.412801008228));
#199559=CARTESIAN_POINT('Ctrl Pts',(33.9335716452707,-5.66428152040741,
133.346263975806));
#199560=CARTESIAN_POINT('Ctrl Pts',(33.6551240214578,-0.923107233816384,
136.943841936043));
#199561=CARTESIAN_POINT('Ctrl Pts',(33.3766763976448,4.66635750435639,134.899536494936));
#199562=CARTESIAN_POINT('Ctrl Pts',(33.098228773832,5.96766766026296,129.091964482989));
#199563=CARTESIAN_POINT('Ctrl Pts',(32.8197811500191,1.78498277316083,124.858000863516));
#199564=CARTESIAN_POINT('Ctrl Pts',(32.5413335262063,-4.03801408121996,
126.08845136219));
#199565=CARTESIAN_POINT('Ctrl Pts',(32.2628859023933,-6.15027326291425,
131.65259208158));
#199566=CARTESIAN_POINT('Ctrl Pts',(31.9844382785804,-2.6107317735426,136.437249523951));
#199567=CARTESIAN_POINT('Ctrl Pts',(31.7059906547675,3.32794467437699,136.045557243275));
#199568=CARTESIAN_POINT('Ctrl Pts',(31.4275430309546,6.20840254567991,130.837461310262));
#199569=CARTESIAN_POINT('Ctrl Pts',(31.1490954071417,3.3836417748287,125.598947457719));
#199570=CARTESIAN_POINT('Ctrl Pts',(30.8706477833288,-2.55052048699994,
125.143954000505));
#199571=CARTESIAN_POINT('Ctrl Pts',(30.5922001595159,-6.14087902112821,
129.890597698133));
#199572=CARTESIAN_POINT('Ctrl Pts',(30.3137525357031,-4.08806973345779,
135.476944878919));
#199573=CARTESIAN_POINT('Ctrl Pts',(30.0353049118902,1.72147592595096,136.769415391952));
#199574=CARTESIAN_POINT('Ctrl Pts',(29.7568572880773,5.94906930818524,132.58029197645));
#199575=CARTESIAN_POINT('Ctrl Pts',(29.4784096642643,4.70975862438989,126.759174401203));
#199576=CARTESIAN_POINT('Ctrl Pts',(29.1999620404515,-0.857590150719802,
124.65538534046));
#199577=CARTESIAN_POINT('Ctrl Pts',(28.9215144166386,-5.63685547292606,
128.202204165235));
#199578=CARTESIAN_POINT('Ctrl Pts',(28.6430667928257,-5.23612599121204,
134.140277647291));
#199579=CARTESIAN_POINT('Ctrl Pts',(28.3646191690128,-0.0236525225496446,
137.012806347637));
#199580=CARTESIAN_POINT('Ctrl Pts',(28.0861715451999,5.2105564588459,134.180076721482));
#199581=CARTESIAN_POINT('Ctrl Pts',(27.807723921387,5.65651860439647,128.245228908728));
#199582=CARTESIAN_POINT('Ctrl Pts',(27.5292762975741,0.904416488802812,
124.662098115861));
#199583=CARTESIAN_POINT('Ctrl Pts',(27.2508286737613,-4.67880019679877,
126.723406495856));
#199584=CARTESIAN_POINT('Ctrl Pts',(26.9723810499484,-5.96242807363892,
132.53491234801));
#199585=CARTESIAN_POINT('Ctrl Pts',(26.6939334261354,-1.76687583160983,
136.756125702037));
#199586=CARTESIAN_POINT('Ctrl Pts',(26.4154858023226,4.05234898298581,135.507957703324));
#199587=CARTESIAN_POINT('Ctrl Pts',(26.1370381785097,6.14766305047102,129.937413766291));
#199588=CARTESIAN_POINT('Ctrl Pts',(25.8585905546968,2.59357510460964,125.163551632871));
#199589=CARTESIAN_POINT('Ctrl Pts',(25.5801429308839,-3.34388165920016,
125.573317387547));
#199590=CARTESIAN_POINT('Ctrl Pts',(25.301695307071,-6.2084745359058,130.790156319941));
#199591=CARTESIAN_POINT('Ctrl Pts',(25.0232476832582,-3.36778261495664,
136.020048307934));
#199592=CARTESIAN_POINT('Ctrl Pts',(24.7448000594452,2.56773700381057,136.456978108987));
#199593=CARTESIAN_POINT('Ctrl Pts',(24.4663524356323,6.14363175700203,131.69942858114));
#199594=CARTESIAN_POINT('Ctrl Pts',(24.1879048118195,4.07382905860539,126.11935532127));
#199595=CARTESIAN_POINT('Ctrl Pts',(23.9094571880065,-1.73962352703587,
124.844573053462));
#199596=CARTESIAN_POINT('Ctrl Pts',(23.6310095641937,-5.95444707666522,
129.046544405257));
#199597=CARTESIAN_POINT('Ctrl Pts',(23.3525619403807,-4.69742465375045,
134.863862982068));
#199598=CARTESIAN_POINT('Ctrl Pts',(23.0741143165679,0.876301544009003,
136.950697203617));
#199599=CARTESIAN_POINT('Ctrl Pts',(22.795666692755,5.64474943253441,133.389348367819));
#199600=CARTESIAN_POINT('Ctrl Pts',(22.5172190689421,5.22594835390121,127.452522073212));
#199601=CARTESIAN_POINT('Ctrl Pts',(22.2387714451292,0.0047560398029127,
124.595871654449));
#199602=CARTESIAN_POINT('Ctrl Pts',(21.9603238213163,-5.22080684252888,
127.444519291243));
#199603=CARTESIAN_POINT('Ctrl Pts',(21.6818761975034,-5.64870328716988,
133.380696969555));
#199604=CARTESIAN_POINT('Ctrl Pts',(21.4034285736905,-0.885717365398449,
136.949347401415));
#199605=CARTESIAN_POINT('Ctrl Pts',(21.1249809498776,4.69119954547528,134.871055178212));
#199606=CARTESIAN_POINT('Ctrl Pts',(20.8465333260648,5.95713325189572,129.055669322849));
#199607=CARTESIAN_POINT('Ctrl Pts',(20.5680857022518,1.74875252196249,124.847245339011));
#199608=CARTESIAN_POINT('Ctrl Pts',(20.289638078439,-4.06664634434428,126.113119274905));
#199609=CARTESIAN_POINT('Ctrl Pts',(20.011190454626,-6.14499588691713,131.690014824823));
#199610=CARTESIAN_POINT('Ctrl Pts',(19.7327428308132,-2.57639440915122,
136.453037424885));
#199611=CARTESIAN_POINT('Ctrl Pts',(19.4542952070003,3.35978766676044,136.025201992224));
#199612=CARTESIAN_POINT('Ctrl Pts',(19.1758475831874,6.20848901167171,130.799668388532));
#199613=CARTESIAN_POINT('Ctrl Pts',(18.8973999593745,3.3518922564065,125.578446714094));
#199614=CARTESIAN_POINT('Ctrl Pts',(18.6189523355616,-2.58492973345636,
125.159584616859));
#199615=CARTESIAN_POINT('Ctrl Pts',(18.3405047117487,-6.14632757911053,
129.927995901635));
#199616=CARTESIAN_POINT('Ctrl Pts',(18.0620570879358,-4.05955064435711,
135.501743547556));
#199617=CARTESIAN_POINT('Ctrl Pts',(17.7836094641229,1.75775501248606,136.758825760728));
#199618=CARTESIAN_POINT('Ctrl Pts',(17.5051618403101,5.95976968396092,132.544045399129));
#199619=CARTESIAN_POINT('Ctrl Pts',(17.2267142164972,4.68504716681072,126.730579711598));
#199620=CARTESIAN_POINT('Ctrl Pts',(16.9482665926842,-0.8950048193604,124.660719661391));
#199621=CARTESIAN_POINT('Ctrl Pts',(16.6698189688713,-5.65259109995534,
128.236565516362));
#199622=CARTESIAN_POINT('Ctrl Pts',(16.3913713450585,-5.21572230411858,
134.172089625574));
#199623=CARTESIAN_POINT('Ctrl Pts',(16.1129237212456,0.0141404870033325,
137.012835299135));
#199624=CARTESIAN_POINT('Ctrl Pts',(15.8344760974327,5.23100886137047,134.148296041183));
#199625=CARTESIAN_POINT('Ctrl Pts',(15.5560284736198,5.64083564112771,128.210843489254));
#199626=CARTESIAN_POINT('Ctrl Pts',(15.2775808498069,0.8670100368296,124.656706477888));
#199627=CARTESIAN_POINT('Ctrl Pts',(14.999133225994,-4.70355543551987,126.751963291284));
#199628=CARTESIAN_POINT('Ctrl Pts',(14.7206856021811,-5.95178324408404,
132.571175276918));
#199629=CARTESIAN_POINT('Ctrl Pts',(14.4422379783683,-1.73061301211068,
136.766770904302));
#199630=CARTESIAN_POINT('Ctrl Pts',(14.1637903545553,4.08090603284655,135.48320275811));
#199631=CARTESIAN_POINT('Ctrl Pts',(13.8853427307424,6.14227179696077,129.900007258904));
#199632=CARTESIAN_POINT('Ctrl Pts',(13.6068951069296,2.55918984632695,125.147868316191));
#199633=CARTESIAN_POINT('Ctrl Pts',(13.3284474831167,-3.37566254970675,
125.593769463429));
#199634=CARTESIAN_POINT('Ctrl Pts',(13.0499998593037,-6.20844597284355,
130.827949329789));
#199635=CARTESIAN_POINT('Ctrl Pts',(12.7715522354909,-3.33597084638438,
136.04045232199));
#199636=CARTESIAN_POINT('Ctrl Pts',(12.493104611678,2.60209851666622,136.441242835124));
#199637=CARTESIAN_POINT('Ctrl Pts',(12.2146569878651,6.14896646247997,131.662013967328));
#199638=CARTESIAN_POINT('Ctrl Pts',(11.9362093640522,4.04523462298623,126.094643569795));
#199639=CARTESIAN_POINT('Ctrl Pts',(11.6577617402393,-1.77587021433397,
124.855273056695));
#199640=CARTESIAN_POINT('Ctrl Pts',(11.3793141164265,-5.96503708076441,
129.08282338295));
#199641=CARTESIAN_POINT('Ctrl Pts',(11.1008664926135,-4.67262627823404,
134.892382326048));
#199642=CARTESIAN_POINT('Ctrl Pts',(10.8224188688007,0.913699803509421,
136.945249030013));
#199643=CARTESIAN_POINT('Ctrl Pts',(10.5439712449878,5.6603804025445,133.354939282016));
#199644=CARTESIAN_POINT('Ctrl Pts',(10.2655236211749,5.20544793659703,127.420772344084));
#199645=CARTESIAN_POINT('Ctrl Pts',(9.98707599736195,-0.0330368828140487,
124.595957732005));
#199646=CARTESIAN_POINT('Ctrl Pts',(9.70862837354909,-5.24116242086055,
127.476362074414));
#199647=CARTESIAN_POINT('Ctrl Pts',(9.43018074973619,-5.63291573915475,
133.415034496211));
#199648=CARTESIAN_POINT('Ctrl Pts',(9.15173312592329,-0.848294676398009,
136.954625162043));
#199649=CARTESIAN_POINT('Ctrl Pts',(8.87328550211039,4.71586775246963,134.842423168626));
#199650=CARTESIAN_POINT('Ctrl Pts',(8.59483787829755,5.94637809976527,129.019438961107));
#199651=CARTESIAN_POINT('Ctrl Pts',(8.3163902544846,1.71245747009635,124.836710557603));
#199652=CARTESIAN_POINT('Ctrl Pts',(8.03794263067172,-4.09512791639282,
126.137961023291));
#199653=CARTESIAN_POINT('Ctrl Pts',(7.75949500685887,-6.1394908058375,131.727404749824));
#199654=CARTESIAN_POINT('Ctrl Pts',(7.48104738304595,-2.54196157551782,
136.468616012024));
#199655=CARTESIAN_POINT('Ctrl Pts',(7.20259975923305,3.39150616097622,136.004653280976));
#199656=CARTESIAN_POINT('Ctrl Pts',(6.92415213542018,6.20834541982004,130.761875640674));
#199657=CARTESIAN_POINT('Ctrl Pts',(6.64570451160728,3.32001853238404,125.558139618628));
#199658=CARTESIAN_POINT('Ctrl Pts',(6.36725688779438,-2.61924319439064,
125.175424402463));
#199659=CARTESIAN_POINT('Ctrl Pts',(6.08880926398148,-6.15154838266407,
129.965426579154));
#199660=CARTESIAN_POINT('Ctrl Pts',(5.81036164016863,-4.03088112711464,
135.52636815294));
#199661=CARTESIAN_POINT('Ctrl Pts',(5.53191401635571,1.79396896476278,136.748015484609));
#199662=CARTESIAN_POINT('Ctrl Pts',(5.2534663925428,5.97024921827925,132.507734357147));
#199663=CARTESIAN_POINT('Ctrl Pts',(4.97501876872993,4.66016210308585,126.702135977443));
#199664=CARTESIAN_POINT('Ctrl Pts',(4.69657114491704,-0.932386323268277,
124.666281637197));
#199665=CARTESIAN_POINT('Ctrl Pts',(4.41812352110413,-5.66811726814286,
128.27102201808));
#199666=CARTESIAN_POINT('Ctrl Pts',(4.13967589729124,-5.19512534651691,
134.203776811419));
#199667=CARTESIAN_POINT('Ctrl Pts',(3.86122827347838,0.051932972575587,
137.012634193321));
#199668=CARTESIAN_POINT('Ctrl Pts',(3.58278064966546,5.25126742693796,134.116391450127));
#199669=CARTESIAN_POINT('Ctrl Pts',(3.30433302585255,5.62494365461986,128.176554173511));
#199670=CARTESIAN_POINT('Ctrl Pts',(3.02588540203969,0.829571457480427,
124.651542643499));
#199671=CARTESIAN_POINT('Ctrl Pts',(2.74743777822681,-4.72813638226476,
126.780670249786));
#199672=CARTESIAN_POINT('Ctrl Pts',(2.46899015441389,-5.9409178690121,132.607372735859));
#199673=CARTESIAN_POINT('Ctrl Pts',(2.19054253060099,-1.69428606410994,
136.77719516726));
#199674=CARTESIAN_POINT('Ctrl Pts',(1.91209490678813,4.10931186323347,135.458274436681));
#199675=CARTESIAN_POINT('Ctrl Pts',(1.63364728297522,6.13665293931019,129.862634262664));
#199676=CARTESIAN_POINT('Ctrl Pts',(1.35519965916232,2.52470975632363,125.132394602912));
#199677=CARTESIAN_POINT('Ctrl Pts',(1.07675203534945,-3.40731835379603,
125.614414619682));
#199678=CARTESIAN_POINT('Ctrl Pts',(0.798304411536565,-6.20818735353264,
130.86574146555));
#199679=CARTESIAN_POINT('Ctrl Pts',(0.519856787723634,-3.30403546218559,
136.060662310741));
#199680=CARTESIAN_POINT('Ctrl Pts',(0.241409163910791,2.63636360780418,
136.425298684517));
#199681=CARTESIAN_POINT('Ctrl Pts',(-0.0370384599021062,6.15407331574431,
131.624567572855));
#199682=CARTESIAN_POINT('Ctrl Pts',(-0.315486083715014,4.01649028971072,
126.070106338619));
#199683=CARTESIAN_POINT('Ctrl Pts',(-0.593933707527915,-1.81205109610819,
124.866193505555));
#199684=CARTESIAN_POINT('Ctrl Pts',(-0.872381331340776,-5.97540604822092,
129.119166152838));
#199685=CARTESIAN_POINT('Ctrl Pts',(-1.15082895515369,-4.6476547568326,
134.920750186879));
#199686=CARTESIAN_POINT('Ctrl Pts',(-1.42927657896659,0.951064205527318,
136.939573303531));
#199687=CARTESIAN_POINT('Ctrl Pts',(-1.70772420277945,5.67580162507719,
133.320435683583));
#199688=CARTESIAN_POINT('Ctrl Pts',(-1.98617182659235,5.18475462950527,
127.389147995065));
#199689=CARTESIAN_POINT('Ctrl Pts',(-2.26461945040527,-0.0708285812371651,
124.596273864213));
#199690=CARTESIAN_POINT('Ctrl Pts',(-2.54306707421816,-5.26132378599129,
127.508328177794));
#199691=CARTESIAN_POINT('Ctrl Pts',(-2.82151469803103,-5.61691946137538,
133.449275283389));
#199692=CARTESIAN_POINT('Ctrl Pts',(-3.09996232184393,-0.810840553526189,
136.959675022356));
#199693=CARTESIAN_POINT('Ctrl Pts',(-3.37840994565684,4.74036121125036,
134.813641527147));
#199694=CARTESIAN_POINT('Ctrl Pts',(-3.6568575694697,5.93540260240737,128.983274740293));
#199695=CARTESIAN_POINT('Ctrl Pts',(-3.9353051932826,1.6760989624889,124.826396909662));
#199696=CARTESIAN_POINT('Ctrl Pts',(-4.21375281709551,-4.12345774197041,
126.162975686831));
#199697=CARTESIAN_POINT('Ctrl Pts',(-4.49220044090841,-6.13375822366836,
131.764760471086));
#199698=CARTESIAN_POINT('Ctrl Pts',(-4.77064806472125,-2.50743454856317,
136.483984708096));
#199699=CARTESIAN_POINT('Ctrl Pts',(-5.04909568853418,3.4230989816841,135.983911870971));
#199700=CARTESIAN_POINT('Ctrl Pts',(-5.32754331234708,6.20797177544568,
130.724084467112));
#199701=CARTESIAN_POINT('Ctrl Pts',(-5.60599093615995,3.28802178385396,
125.538026923812));
#199702=CARTESIAN_POINT('Ctrl Pts',(-5.88443855997284,-2.65345959830539,
125.191472770368));
#199703=CARTESIAN_POINT('Ctrl Pts',(-6.16288618378574,-6.15654123833006,
130.002888343683));
#199704=CARTESIAN_POINT('Ctrl Pts',(-6.44133380759864,-4.00206224408943,
135.550817782599));
#199705=CARTESIAN_POINT('Ctrl Pts',(-6.71978143141151,1.83011644085978,
136.736984964173));
#199706=CARTESIAN_POINT('Ctrl Pts',(-6.9982290552244,5.98050752281724,132.471360196026));
#199707=CARTESIAN_POINT('Ctrl Pts',(-7.27667667903734,4.63510435534053,
126.673844252731));
#199708=CARTESIAN_POINT('Ctrl Pts',(-7.55512430285017,-0.969733277257762,
124.672071061776));
#199709=CARTESIAN_POINT('Ctrl Pts',(-7.83357192666308,-5.68343340216059,
128.305572393592));
#199710=CARTESIAN_POINT('Ctrl Pts',(-8.112019550476,-5.17433588163501,134.235338030648));
#199711=CARTESIAN_POINT('Ctrl Pts',(-8.39046717428886,0.0897235337524442,
137.012203037646));
#199712=CARTESIAN_POINT('Ctrl Pts',(-8.66891479810176,5.27133140485959,
134.084364130551));
#199713=CARTESIAN_POINT('Ctrl Pts',(-8.94736242191464,5.60884323375645,
128.142362232103));
#199714=CARTESIAN_POINT('Ctrl Pts',(-9.22581004572757,0.792102138056052,
124.646606804043));
#199715=CARTESIAN_POINT('Ctrl Pts',(-9.50425766954039,-4.75254212617725,
126.809526307613));
#199716=CARTESIAN_POINT('Ctrl Pts',(-9.78270529335335,-5.92983235104376,
132.643503383524));
#199717=CARTESIAN_POINT('Ctrl Pts',(-10.0611529171662,-1.65789633371603,
136.787398104638));
#199718=CARTESIAN_POINT('Ctrl Pts',(-10.3396005409791,4.13756542155812,
135.433173662763));
#199719=CARTESIAN_POINT('Ctrl Pts',(-10.618048164792,6.13080668572826,129.82529616244));
#199720=CARTESIAN_POINT('Ctrl Pts',(-10.8964957886049,2.49013611227157,
125.11713106642));
#199721=CARTESIAN_POINT('Ctrl Pts',(-11.1749434124178,-3.4388478984508,
125.635252091294));
#199722=CARTESIAN_POINT('Ctrl Pts',(-11.4533910362307,-6.20769868755626,
130.90353132682));
#199723=CARTESIAN_POINT('Ctrl Pts',(-11.7318386600436,-3.2719776457377,
136.080677525301));
#199724=CARTESIAN_POINT('Ctrl Pts',(-12.0102862838565,2.67053100751937,
136.409146247984));
#199725=CARTESIAN_POINT('Ctrl Pts',(-12.2887339076694,6.15895212755882,
131.587090785312));
#199726=CARTESIAN_POINT('Ctrl Pts',(-12.5671815314823,3.98759712391021,
126.045744536976));
#199727=CARTESIAN_POINT('Ctrl Pts',(-12.8456291552951,-1.84816483166266,
124.877333995382));
#199728=CARTESIAN_POINT('Ctrl Pts',(-13.1240767791081,-5.98555359480885,
129.155571368227));
#199729=CARTESIAN_POINT('Ctrl Pts',(-13.4025244029209,-4.62251101487491,
134.948965513381));
#199730=CARTESIAN_POINT('Ctrl Pts',(-13.6809720267338,0.988393365511613,
136.933670234486));
#199731=CARTESIAN_POINT('Ctrl Pts',(-13.9594196505467,5.69101252869335,
133.285838851062));
#199732=CARTESIAN_POINT('Ctrl Pts',(-14.2378672743596,5.16386919942402,
127.357650198006));
#199733=CARTESIAN_POINT('Ctrl Pts',(-14.5163148981725,-0.108617655081171,
124.59682003936));
#199734=CARTESIAN_POINT('Ctrl Pts',(-14.7947625219854,-5.28129019083405,
127.540416416869));
#199735=CARTESIAN_POINT('Ctrl Pts',(-15.0732101457983,-5.60071504657988,
133.483418062279));
#199736=CARTESIAN_POINT('Ctrl Pts',(-15.3516577696111,-0.77335638465969,
136.96449679523));
#199737=CARTESIAN_POINT('Ctrl Pts',(-15.6301053934241,4.76467901420313,
134.784711320289));
#199738=CARTESIAN_POINT('Ctrl Pts',(-15.908553017237,5.92420716652329,128.947178000488));
#199739=CARTESIAN_POINT('Ctrl Pts',(-16.1870006410499,1.63967834641818,
124.816304777366));
#199740=CARTESIAN_POINT('Ctrl Pts',(-16.4654482648627,-4.15163477130477,
126.188162338596));
#199741=CARTESIAN_POINT('Ctrl Pts',(-16.7438958886757,-6.12779835283271,
131.802080604377));
#199742=CARTESIAN_POINT('Ctrl Pts',(-17.0223435124885,-2.4728146076992,
136.499142943608));
#199743=CARTESIAN_POINT('Ctrl Pts',(-17.3007911363014,3.45456495820035,
135.96297853079));
#199744=CARTESIAN_POINT('Ctrl Pts',(-17.5792387601143,6.20736809239421,
130.686296268213));
#199745=CARTESIAN_POINT('Ctrl Pts',(-17.8576863839272,3.25590319646751,
125.518109374927));
#199746=CARTESIAN_POINT('Ctrl Pts',(-18.13613400774,-2.6875776772989,125.207729125896));
#199747=CARTESIAN_POINT('Ctrl Pts',(-18.414581631553,-6.16130596109642,
130.040379807061));
#199748=CARTESIAN_POINT('Ctrl Pts',(-18.6930292553659,-3.97309506317598,
135.575091530542));
#199749=CARTESIAN_POINT('Ctrl Pts',(-18.9714768791788,1.86619610131902,
136.72573460816));
#199750=CARTESIAN_POINT('Ctrl Pts',(-19.2499245029916,5.99054421744964,
132.434924263623));
#199751=CARTESIAN_POINT('Ctrl Pts',(-19.5283721268046,4.6098748520987,126.645705585822));
#199752=CARTESIAN_POINT('Ctrl Pts',(-19.8068197506174,-1.00704429742433,
124.678087720601));
#199753=CARTESIAN_POINT('Ctrl Pts',(-20.0852673744304,-5.6985389344635,
128.340215362621));
#199754=CARTESIAN_POINT('Ctrl Pts',(-20.3637149982432,-5.15335467983417,
134.266772113748));
#199755=CARTESIAN_POINT('Ctrl Pts',(-20.6421626220562,0.127510770190762,
137.011541848088));
#199756=CARTESIAN_POINT('Ctrl Pts',(-20.920610245869,5.29120005165768,134.05221526924));
#199757=CARTESIAN_POINT('Ctrl Pts',(-21.1990578696819,5.59253497514422,
128.108268932023));
#199758=CARTESIAN_POINT('Ctrl Pts',(-21.4775054934948,0.754603466995427,
124.64189914242));
#199759=CARTESIAN_POINT('Ctrl Pts',(-21.7559531173077,-4.77677176289349,
126.838530395495));
#199760=CARTESIAN_POINT('Ctrl Pts',(-22.0344007411205,-5.91852710095694,
132.679565881077));
#199761=CARTESIAN_POINT('Ctrl Pts',(-22.3128483649335,-1.62144516936395,
136.797379338361));
#199762=CARTESIAN_POINT('Ctrl Pts',(-22.5912959887463,4.16566566087426,
135.407901366475));
#199763=CARTESIAN_POINT('Ctrl Pts',(-22.8697436125593,6.12473325285015,
129.787994341809));
#199764=CARTESIAN_POINT('Ctrl Pts',(-23.1481912363721,2.45547019531011,
125.102078272311));
#199765=CARTESIAN_POINT('Ctrl Pts',(-23.426638860185,-3.47025001533206,
125.656281106122));
#199766=CARTESIAN_POINT('Ctrl Pts',(-23.7050864839979,-6.20697999302203,
130.941317513284));
#199767=CARTESIAN_POINT('Ctrl Pts',(-23.9835341078108,-3.23979858495512,
136.100497223997));
#199768=CARTESIAN_POINT('Ctrl Pts',(-24.2619817316237,2.70459944972584,
136.392786124057));
#199769=CARTESIAN_POINT('Ctrl Pts',(-24.5404293554366,6.16360271713728,
131.549584993415));
#199770=CARTESIAN_POINT('Ctrl Pts',(-24.8188769792495,3.95855619623184,
126.021559067602));
#199771=CARTESIAN_POINT('Ctrl Pts',(-25.0973246030624,-1.88421008278963,
124.88869411336));
#199772=CARTESIAN_POINT('Ctrl Pts',(-25.3757722268753,-5.99547934450715,
129.192037680109));
#199773=CARTESIAN_POINT('Ctrl Pts',(-25.6542198506882,-4.59719598407162,
134.977027260026));
#199774=CARTESIAN_POINT('Ctrl Pts',(-25.932667474501,1.02568590021626,136.92754004162));
#199775=CARTESIAN_POINT('Ctrl Pts',(-26.211115098314,5.7060125497474,133.251150066453));
#199776=CARTESIAN_POINT('Ctrl Pts',(-26.4895627221268,5.14279242027056,
127.326280120068));
#199777=CARTESIAN_POINT('Ctrl Pts',(-26.7680103459397,-0.146402704058008,
124.597596237205));
#199778=CARTESIAN_POINT('Ctrl Pts',(-27.0464579697526,-5.30106089552683,
127.572625602596));
#199779=CARTESIAN_POINT('Ctrl Pts',(-27.3249055935655,-5.58430309522854,
133.517461567711));
#199780=CARTESIAN_POINT('Ctrl Pts',(-27.6033532173784,-0.735843558787732,
136.969090301993));
#199781=CARTESIAN_POINT('Ctrl Pts',(-27.8818008411913,4.78882026022281,
134.755633620073));
#199782=CARTESIAN_POINT('Ctrl Pts',(-28.1602484650042,5.91279220696403,
128.911150079267));
#199783=CARTESIAN_POINT('Ctrl Pts',(-28.4386960888171,1.60319697146318,
124.806434534681));
#199784=CARTESIAN_POINT('Ctrl Pts',(-28.7171437126299,-4.17965796028613,
126.213520045287));
#199785=CARTESIAN_POINT('Ctrl Pts',(-28.9955913364429,-6.12161141417542,
131.839363766787));
#199786=CARTESIAN_POINT('Ctrl Pts',(-29.2740389602557,-2.43810303578058,
136.514090156867));
#199787=CARTESIAN_POINT('Ctrl Pts',(-29.5524865840687,3.48590292454168,
135.941854036124));
#199788=CARTESIAN_POINT('Ctrl Pts',(-29.8309342078815,6.20653439303521,
130.648512444231));
#199789=CARTESIAN_POINT('Ctrl Pts',(-30.1093818316944,3.22366396039099,
125.498387710026));
#199790=CARTESIAN_POINT('Ctrl Pts',(-30.3878294555073,-2.72159616711309,
125.224192866663));
#199791=CARTESIAN_POINT('Ctrl Pts',(-30.6662770793202,-6.16584237440457,
130.077899580028));
#199792=CARTESIAN_POINT('Ctrl Pts',(-30.9447247031331,-3.94398065776386,
135.599188497297));
#199793=CARTESIAN_POINT('Ctrl Pts',(-31.2231723269461,1.90220660919519,
136.714264833456));
#199794=CARTESIAN_POINT('Ctrl Pts',(-31.5016199507588,6.00035893026297,
132.398427910084));
#199795=CARTESIAN_POINT('Ctrl Pts',(-31.7800675745718,4.58447452824918,
126.617721019404));
#199796=CARTESIAN_POINT('Ctrl Pts',(-32.0585151983846,-1.04431800119413,
124.68433139072));
#199797=CARTESIAN_POINT('Ctrl Pts',(-32.3369628221976,-5.71343330531054,
128.374949641459));
#199798=CARTESIAN_POINT('Ctrl Pts',(-32.6154104460104,-5.1321825185805,
134.298077895915));
#199799=CARTESIAN_POINT('Ctrl Pts',(-32.8938580698234,0.165293281670594,
137.010650649146));
#199800=CARTESIAN_POINT('Ctrl Pts',(-33.1723056936362,5.31087263109202,
134.019946057479));
#199801=CARTESIAN_POINT('Ctrl Pts',(-33.4507533174492,5.57601948309184,
128.074275536613));
#199802=CARTESIAN_POINT('Ctrl Pts',(-33.729200941262,0.717076833825826,
124.637419833072));
#199803=CARTESIAN_POINT('Ctrl Pts',(-34.0076485650749,-4.80082439457541,
126.867681438675));
#199804=CARTESIAN_POINT('Ctrl Pts',(-34.2860961888878,-5.90700253767186,
132.715558892209));
#199805=CARTESIAN_POINT('Ctrl Pts',(-34.5645438127007,-1.58493392176466,
136.807138498572));
#199806=CARTESIAN_POINT('Ctrl Pts',(-34.8429914365135,4.19361153991761,
135.382458484293));
#199807=CARTESIAN_POINT('Ctrl Pts',(-35.1214390603265,6.11843286572883,
129.750730183006));
#199808=CARTESIAN_POINT('Ctrl Pts',(-35.3998866841394,2.42071328999757,
125.087236778371));
#199809=CARTESIAN_POINT('Ctrl Pts',(-35.6783343079523,-3.50152354082281,
125.677500884929));
#199810=CARTESIAN_POINT('Ctrl Pts',(-35.9567819317651,-6.20603129656164,
130.979098624759));
#199811=CARTESIAN_POINT('Ctrl Pts',(-36.2352295555781,-3.2074994722443,
136.120120672404));
#199812=CARTESIAN_POINT('Ctrl Pts',(-36.5136771793909,2.73856767200523,
136.376218918968));
#199813=CARTESIAN_POINT('Ctrl Pts',(-36.7921248032039,6.1680249121504,131.512051586954));
#199814=CARTESIAN_POINT('Ctrl Pts',(-37.0705724270167,3.92936858279784,
125.997550826698));
#199815=CARTESIAN_POINT('Ctrl Pts',(-37.3490200508296,-1.92018551381882,
124.900273438536));
#199816=CARTESIAN_POINT('Ctrl Pts',(-37.6274676746425,-6.00518292951342,
129.228563737208));
#199817=CARTESIAN_POINT('Ctrl Pts',(-37.9059152984554,-4.57171060248077,
135.004934386972));
#199818=CARTESIAN_POINT('Ctrl Pts',(-38.1843629222683,1.0629404277527,136.921182952087));
#199819=CARTESIAN_POINT('Ctrl Pts',(-38.4628105460811,5.72080113240803,
133.216370615161));
#199820=CARTESIAN_POINT('Ctrl Pts',(-38.7412581698941,5.12152507305273,
127.295038923683));
#199821=CARTESIAN_POINT('Ctrl Pts',(-39.0197057937069,-0.184182328028525,
124.598602428988));
#199822=CARTESIAN_POINT('Ctrl Pts',(-39.2981534175199,-5.32063516745863,
127.604954541453));
#199823=CARTESIAN_POINT('Ctrl Pts',(-39.5766010413327,-5.56768421547239,
133.55140453819));
#199824=CARTESIAN_POINT('Ctrl Pts',(-39.8550486651457,-0.698303465962086,
136.973455372429));
#199825=CARTESIAN_POINT('Ctrl Pts',(-40.1334962889585,4.81278405474664,
134.726409503982));
#199826=CARTESIAN_POINT('Ctrl Pts',(-40.4119439127715,5.90115814671511,
128.875192311658));
#199827=CARTESIAN_POINT('Ctrl Pts',(-40.6903915365843,1.56665618945481,
124.796786547352));
#199828=CARTESIAN_POINT('Ctrl Pts',(-40.9688391603973,-4.20752627050468,
126.239047867263));
#199829=CARTESIAN_POINT('Ctrl Pts',(-41.2472867842101,-6.11519763695597,
131.876608576776));
#199830=CARTESIAN_POINT('Ctrl Pts',(-41.5257344080229,-2.40330111905734,
136.528825793999));
#199831=CARTESIAN_POINT('Ctrl Pts',(-41.8041820318359,3.51711171946819,
135.920539169751));
#199832=CARTESIAN_POINT('Ctrl Pts',(-42.0826296556488,6.20547070826194,
130.610734395262));
#199833=CARTESIAN_POINT('Ctrl Pts',(-42.3610772794617,3.19130527026066,
125.478862659902));
#199834=CARTESIAN_POINT('Ctrl Pts',(-42.6395249032745,-2.75551380718057,
125.240863382598));
#199835=CARTESIAN_POINT('Ctrl Pts',(-42.9179725270875,-6.17015031015604,
130.115446272278));
#199836=CARTESIAN_POINT('Ctrl Pts',(-43.1964201509003,-3.91472010669807,
135.623107789941));
#199837=CARTESIAN_POINT('Ctrl Pts',(-43.4748677747133,1.93814663010615,
136.702576065077));
#199838=CARTESIAN_POINT('Ctrl Pts',(-43.7533153985261,6.00995129756958,
132.361872487794));
#199839=CARTESIAN_POINT('Ctrl Pts',(-44.031763022339,4.55890432500984,126.589891590455));
#199840=CARTESIAN_POINT('Ctrl Pts',(-44.3102106461518,-1.08155300737633,
124.690801840773));
#199841=CARTESIAN_POINT('Ctrl Pts',(-44.5886582699649,-5.72811596278534,
128.409773943013));
#199842=CARTESIAN_POINT('Ctrl Pts',(-44.8671058937777,-5.11082018241628,
134.329254217104));
#199843=CARTESIAN_POINT('Ctrl Pts',(-45.1455535175906,0.2030696681468,137.009529473845));
#199844=CARTESIAN_POINT('Ctrl Pts',(-45.4240011414034,5.33034841418793,
133.987557691017));
#199845=CARTESIAN_POINT('Ctrl Pts',(-45.7024487652165,5.55929736958694,
128.040383305508));
#199846=CARTESIAN_POINT('Ctrl Pts',(-45.9808963890292,0.679523629110432,
124.633169041983));
#199847=CARTESIAN_POINT('Ctrl Pts',(-46.2593440128422,-4.82469912994364,
126.896978356949));
#199848=CARTESIAN_POINT('Ctrl Pts',(-46.537791636655,-5.89525908823553,
132.751481083186));
#199849=CARTESIAN_POINT('Ctrl Pts',(-46.816239260468,-1.54836394385628,
136.816675223641));
#199850=CARTESIAN_POINT('Ctrl Pts',(-47.0946868842807,4.22140202314317,
135.35684595901));
#199851=CARTESIAN_POINT('Ctrl Pts',(-47.3731345080937,6.11190575782758,
129.713505066864));
#199852=CARTESIAN_POINT('Ctrl Pts',(-47.6515821319066,2.38586668426401,
125.072607134557));
#199853=CARTESIAN_POINT('Ctrl Pts',(-47.9300297557195,-3.53266731607082,
125.69891064141));
#199854=CARTESIAN_POINT('Ctrl Pts',(-48.2084773795324,-6.20485263332943,
131.016873261253));
#199855=CARTESIAN_POINT('Ctrl Pts',(-48.4869250033452,-3.17508150446096,
136.139547143367));
#199856=CARTESIAN_POINT('Ctrl Pts',(-48.7653726271582,2.77243441565242,
136.359445246621));
#199857=CARTESIAN_POINT('Ctrl Pts',(-49.043820250971,6.1722185487321,131.474491956744));
#199858=CARTESIAN_POINT('Ctrl Pts',(-49.322267874784,3.900035365166,125.973720703898));
#199859=CARTESIAN_POINT('Ctrl Pts',(-49.6007154985968,-1.95608979166789,
124.912071541833));
#199860=CARTESIAN_POINT('Ctrl Pts',(-49.8791631224098,-6.0146639902579,
129.265148186042));
#199861=CARTESIAN_POINT('Ctrl Pts',(-50.1576107462225,-4.54605581447205,
135.032685860113));
#199862=CARTESIAN_POINT('Ctrl Pts',(-50.4360583700356,1.10015556764067,
136.914599201455));
#199863=CARTESIAN_POINT('Ctrl Pts',(-50.7145059938484,5.73537772867887,
133.181501785951));
#199864=CARTESIAN_POINT('Ctrl Pts',(-50.9929536176612,5.10006794583985,
127.263927766504));
#199865=CARTESIAN_POINT('Ctrl Pts',(-51.2714012414742,-0.221955127055423,
124.599838577421));
#199866=CARTESIAN_POINT('Ctrl Pts',(-51.5498488652871,-5.34001228129766,
127.637402035479));
#199867=CARTESIAN_POINT('Ctrl Pts',(-51.8282964891,-5.5508590231301,133.585245715947));
#199868=CARTESIAN_POINT('Ctrl Pts',(-52.1067441129128,-0.660737497244709,
136.977591844792));
#199869=CARTESIAN_POINT('Ctrl Pts',(-52.3851917367258,4.8365695097872,134.697040054928));
#199870=CARTESIAN_POINT('Ctrl Pts',(-52.6636393605386,5.889305416881,128.83930603009));
#199871=CARTESIAN_POINT('Ctrl Pts',(-52.9420869843516,1.53005735442545,
124.78736117289));
#199872=CARTESIAN_POINT('Ctrl Pts',(-53.2205346081644,-4.23523866929,126.264744858582));
#199873=CARTESIAN_POINT('Ctrl Pts',(-53.4989822319774,-6.1085572588392,
131.913813654221));
#199874=CARTESIAN_POINT('Ctrl Pts',(-53.7774298557902,-2.36841014712749,
136.543349308967));
#199875=CARTESIAN_POINT('Ctrl Pts',(-54.0558774796031,3.54819018652628,
135.8990347215));
#199876=CARTESIAN_POINT('Ctrl Pts',(-54.334325103416,6.20417707748961,130.572963521183));
#199877=CARTESIAN_POINT('Ctrl Pts',(-54.6127727272289,3.15882832513996,
125.459534948064));
#199878=CARTESIAN_POINT('Ctrl Pts',(-54.8912203510417,-2.7893293406706,
125.257740055968));
#199879=CARTESIAN_POINT('Ctrl Pts',(-55.1696679748547,-6.17422960871856,
130.153018492501));
#199880=CARTESIAN_POINT('Ctrl Pts',(-55.4481155986676,-3.88531449423931,
135.646848522136));
#199881=CARTESIAN_POINT('Ctrl Pts',(-55.7265632224805,1.97401483228084,
136.690668736158));
#199882=CARTESIAN_POINT('Ctrl Pts',(-56.0050108462934,6.01932096392068,
132.32525935133));
#199883=CARTESIAN_POINT('Ctrl Pts',(-56.2834584701062,4.53316518989421,
126.562218330207));
#199884=CARTESIAN_POINT('Ctrl Pts',(-56.5619060939192,-1.11874793621411,
124.697498830995));
#199885=CARTESIAN_POINT('Ctrl Pts',(-56.840353717732,-5.74258636281662,
128.444686976857));
#199886=CARTESIAN_POINT('Ctrl Pts',(-57.118801341545,-5.08926846293066,
134.360299922064));
#199887=CARTESIAN_POINT('Ctrl Pts',(-57.3972489653578,0.240838529802063,
137.00817836373));
#199888=CARTESIAN_POINT('Ctrl Pts',(-57.6756965891708,5.34962667926312,
133.955051370017));
#199889=CARTESIAN_POINT('Ctrl Pts',(-57.9541442129836,5.54236925427356,
128.0065934946));
#199890=CARTESIAN_POINT('Ctrl Pts',(-58.2325918367966,0.641945244397073,
124.629146926667));
#199891=CARTESIAN_POINT('Ctrl Pts',(-58.5110394606094,-4.84839508431156,
126.92642006471));
#199892=CARTESIAN_POINT('Ctrl Pts',(-58.7894870844223,-5.88329718780563,
132.787331122898));
#199893=CARTESIAN_POINT('Ctrl Pts',(-59.0679347082352,-1.5117365907523,
136.825989160181));
#199894=CARTESIAN_POINT('Ctrl Pts',(-59.3463823320481,4.24903608076433,
135.331064739709));
#199895=CARTESIAN_POINT('Ctrl Pts',(-59.624829955861,6.10515217101086,129.676320372777));
#199896=CARTESIAN_POINT('Ctrl Pts',(-59.9032775796738,2.3509316693629,125.058189882977));
#199897=CARTESIAN_POINT('Ctrl Pts',(-60.1817252034868,-3.56368018703254,
125.720509582217));
#199898=CARTESIAN_POINT('Ctrl Pts',(-60.4601728272995,-6.20344404700091,
131.054640023013));
#199899=CARTESIAN_POINT('Ctrl Pts',(-60.7386204511126,-3.14254588286485,
136.158775917031));
#199900=CARTESIAN_POINT('Ctrl Pts',(-61.0170680749254,2.80619842572279,
136.342465728569));
#199901=CARTESIAN_POINT('Ctrl Pts',(-61.2955156987383,6.17618347148551,
131.436907494571));
#199902=CARTESIAN_POINT('Ctrl Pts',(-61.5739633225512,3.87055763028967,
125.950069582238));
#199903=CARTESIAN_POINT('Ctrl Pts',(-61.8524109463641,-1.9919215858902,
124.924087986069));
#199904=CARTESIAN_POINT('Ctrl Pts',(-62.130858570177,-6.02392217541635,
129.301789670958));
#199905=CARTESIAN_POINT('Ctrl Pts',(-62.4093061939898,-4.5202325706933,
135.060280651108));
#199906=CARTESIAN_POINT('Ctrl Pts',(-62.6877538178028,1.13732994085927,
136.907789033684));
#199907=CARTESIAN_POINT('Ctrl Pts',(-62.9662014416156,5.74974179841868,
133.146544870902));
#199908=CARTESIAN_POINT('Ctrl Pts',(-63.2446490654287,5.0784218337339,127.232947801366));
#199909=CARTESIAN_POINT('Ctrl Pts',(-63.5230966892413,-0.25971970145348,
124.601304636701));
#199910=CARTESIAN_POINT('Ctrl Pts',(-63.8015443130544,-5.3591915190178,
127.669966882319));
#199911=CARTESIAN_POINT('Ctrl Pts',(-64.0799919368672,-5.53382814166538,
133.618983846983));
#199912=CARTESIAN_POINT('Ctrl Pts',(-64.3584395606801,-0.623147044656387,
136.9814995658));
#199913=CARTESIAN_POINT('Ctrl Pts',(-64.636887184493,4.86017574396616,134.667526361205));
#199914=CARTESIAN_POINT('Ctrl Pts',(-64.9153348083059,5.8772344566688,128.803492564343));
#199915=CARTESIAN_POINT('Ctrl Pts',(-65.1937824321189,1.4934018225579,124.778158760555));
#199916=CARTESIAN_POINT('Ctrl Pts',(-65.4722300559316,-4.26279412974889,
126.290610067033));
#199917=CARTESIAN_POINT('Ctrl Pts',(-65.7506776797446,-6.10169052588679,
131.950977620477));
#199918=CARTESIAN_POINT('Ctrl Pts',(-66.0291253035574,-2.33343141288849,
136.5576601636));
#199919=CARTESIAN_POINT('Ctrl Pts',(-66.3075729273703,3.57913717409239,
135.877341488227));
#199920=CARTESIAN_POINT('Ctrl Pts',(-66.5860205511832,6.20265354865397,
130.535201221608));
#199921=CARTESIAN_POINT('Ctrl Pts',(-66.8644681749961,3.126234328474,125.440405290707));
#199922=CARTESIAN_POINT('Ctrl Pts',(-67.142915798809,-2.82304151453613,
125.274822261403));
#199923=CARTESIAN_POINT('Ctrl Pts',(-67.421363422622,-6.17808011893247,
130.190614848446));
#199924=CARTESIAN_POINT('Ctrl Pts',(-67.6998110464348,-3.85576491002292,
135.670409814162));
#199925=CARTESIAN_POINT('Ctrl Pts',(-67.9782586702478,2.00980988661012,
136.678543287925));
#199926=CARTESIAN_POINT('Ctrl Pts',(-68.2567062940606,6.02846758211988,
132.288589857404));
#199927=CARTESIAN_POINT('Ctrl Pts',(-68.5351539178734,4.50725807667536,
126.534702264101));
#199928=CARTESIAN_POINT('Ctrl Pts',(-68.8136015416864,-1.15590140943545,
124.704422113226));
#199929=CARTESIAN_POINT('Ctrl Pts',(-69.0920491654993,-5.75684396919829,
128.479687449276));
#199930=CARTESIAN_POINT('Ctrl Pts',(-69.3704967893121,-5.0675281587308,
134.391213860386));
#199931=CARTESIAN_POINT('Ctrl Pts',(-69.648944413125,0.278598467097045,
137.006597368867));
#199932=CARTESIAN_POINT('Ctrl Pts',(-69.9273920369379,5.36870671195437,
133.922428299012));
#199933=CARTESIAN_POINT('Ctrl Pts',(-70.2058396607509,5.52523576442926,
127.972907355982));
#199934=CARTESIAN_POINT('Ctrl Pts',(-70.4842872845636,0.604343072166899,
124.625353636165));
#199935=CARTESIAN_POINT('Ctrl Pts',(-70.7627349083767,-4.87191137961658,
126.956005470983));
#199936=CARTESIAN_POINT('Ctrl Pts',(-71.0411825321895,-5.87111727963483,
132.823107682909));
#199937=CARTESIAN_POINT('Ctrl Pts',(-71.3196301560023,-1.47505321969301,
136.835079963061));
#199938=CARTESIAN_POINT('Ctrl Pts',(-71.5980777798154,4.27651268879093,
135.305115781721));
#199939=CARTESIAN_POINT('Ctrl Pts',(-71.8765254036282,6.09817235553532,
129.639177478635));
#199940=CARTESIAN_POINT('Ctrl Pts',(-72.1549730274411,2.31590953982396,
125.043985557866));
#199941=CARTESIAN_POINT('Ctrl Pts',(-72.433420651254,-3.5945610045145,125.742296906994));
#199942=CARTESIAN_POINT('Ctrl Pts',(-72.7118682750669,-6.20180558977201,
131.092397510578));
#199943=CARTESIAN_POINT('Ctrl Pts',(-72.9903158988798,-3.109893813075,136.177806280867));
#199944=CARTESIAN_POINT('Ctrl Pts',(-73.2687635226926,2.8398584510789,136.325280993997));
#199945=CARTESIAN_POINT('Ctrl Pts',(-73.5472111465057,6.17991953348924,
131.399299593141));
#199946=CARTESIAN_POINT('Ctrl Pts',(-73.8256587703184,3.84093647047644,
125.926598338115));
#199947=CARTESIAN_POINT('Ctrl Pts',(-74.1041063941314,-2.02767956872624,
124.93632232597));
#199948=CARTESIAN_POINT('Ctrl Pts',(-74.3825540179442,-6.0329571419232,
129.338486834193));
#199949=CARTESIAN_POINT('Ctrl Pts',(-74.6610016417573,-4.49424182803428,
135.08771773742));
#199950=CARTESIAN_POINT('Ctrl Pts',(-74.9394492655699,1.17446216989917,
136.900752701129));
#199951=CARTESIAN_POINT('Ctrl Pts',(-75.217896889383,5.76389280936176,133.111501165354));
#199952=CARTESIAN_POINT('Ctrl Pts',(-75.4963445131958,5.05658753883907,
127.202100176243));
#199953=CARTESIAN_POINT('Ctrl Pts',(-75.7747921370087,-0.297474651842549,
124.603000552501));
#199954=CARTESIAN_POINT('Ctrl Pts',(-76.0532397608216,-5.37817216992523,
127.702647875272));
#199955=CARTESIAN_POINT('Ctrl Pts',(-76.3316873846344,-5.51659220216403,
133.65261768112));
#199956=CARTESIAN_POINT('Ctrl Pts',(-76.6101350084474,-0.585533501125347,
136.985178390654));
#199957=CARTESIAN_POINT('Ctrl Pts',(-76.8885826322602,4.8836018825454,134.637869516455));
#199958=CARTESIAN_POINT('Ctrl Pts',(-77.1670302560731,5.86494571337264,
128.767753241497));
#199959=CARTESIAN_POINT('Ctrl Pts',(-77.4454778798861,1.4566909521364,124.769179651345));
#199960=CARTESIAN_POINT('Ctrl Pts',(-77.7239255036988,-4.29019163080361,
126.316642534169));
#199961=CARTESIAN_POINT('Ctrl Pts',(-78.0023731275119,-6.09459769254796,
131.988099098418));
#199962=CARTESIAN_POINT('Ctrl Pts',(-78.2808207513247,-2.29836621249045,
136.571757827603));
#199963=CARTESIAN_POINT('Ctrl Pts',(-78.5592683751376,3.60995153541429,
135.855460273781));
#199964=CARTESIAN_POINT('Ctrl Pts',(-78.8377159989505,6.20090017820995,
130.497448895834));
#199965=CARTESIAN_POINT('Ctrl Pts',(-79.1161636227633,3.09352448804556,
125.421474396687));
#199966=CARTESIAN_POINT('Ctrl Pts',(-79.3946112465763,-2.85664907955992,
125.292109365916));
#199967=CARTESIAN_POINT('Ctrl Pts',(-79.6730588703891,-6.18170169811556,
130.228233946967));
#199968=CARTESIAN_POINT('Ctrl Pts',(-79.9515064942021,-3.8260724490201,
135.693790792945));
#199969=CARTESIAN_POINT('Ctrl Pts',(-80.2299541180149,2.04553046669522,
136.666200169693));
#199970=CARTESIAN_POINT('Ctrl Pts',(-80.5084017418279,6.03739081323573,
132.251865364817));
#199971=CARTESIAN_POINT('Ctrl Pts',(-80.7868493656406,4.48118394535095,
126.507344411756));
#199972=CARTESIAN_POINT('Ctrl Pts',(-81.0652969894537,-1.19301205030527,
124.711571430921));
#199973=CARTESIAN_POINT('Ctrl Pts',(-81.3437446132665,-5.77088825360962,
128.514774063314));
#199974=CARTESIAN_POINT('Ctrl Pts',(-81.6221922370794,-5.04560007541116,
134.421994886542));
#199975=CARTESIAN_POINT('Ctrl Pts',(-81.9006398608923,0.316348080823153,
137.00478654784));
#199976=CARTESIAN_POINT('Ctrl Pts',(-82.179087484705,5.38758780524389,133.889689686862));
#199977=CARTESIAN_POINT('Ctrl Pts',(-82.4575351085182,5.50789753494193,
127.939326137905));
#199978=CARTESIAN_POINT('Ctrl Pts',(-82.7359827323308,0.566718505781886,
124.621789311041));
#199979=CARTESIAN_POINT('Ctrl Pts',(-83.0144303561439,-4.89524714445407,
126.985733479472));
#199980=CARTESIAN_POINT('Ctrl Pts',(-83.2928779799568,-5.858719815054,132.858809437506));
#199981=CARTESIAN_POINT('Ctrl Pts',(-83.5713256037696,-1.43831518999427,
136.843947295418));
#199982=CARTESIAN_POINT('Ctrl Pts',(-83.8497732275826,4.30383082906709,
135.279000046597));
#199983=CARTESIAN_POINT('Ctrl Pts',(-84.1282208513953,6.09096657004034,
129.602077760783));
#199984=CARTESIAN_POINT('Ctrl Pts',(-84.4066684752085,2.28080159340614,
125.029994685571));
#199985=CARTESIAN_POINT('Ctrl Pts',(-84.685116099021,-3.6253086242162,125.764271808403));
#199986=CARTESIAN_POINT('Ctrl Pts',(-84.9635637228342,-6.19993732235617,
131.130144324829));
#199987=CARTESIAN_POINT('Ctrl Pts',(-85.242011346647,-3.07712650502686,
136.196637529698));
#199988=CARTESIAN_POINT('Ctrl Pts',(-85.5204589704598,2.87341324443482,
136.307891679689));
#199989=CARTESIAN_POINT('Ctrl Pts',(-85.7989065942728,6.18342659630218,
131.361669646028));
#199990=CARTESIAN_POINT('Ctrl Pts',(-86.0773542180856,3.81117298335027,
125.903307841269));
#199991=CARTESIAN_POINT('Ctrl Pts',(-86.3558018418987,-2.06336241514917,
124.948774108188));
#199992=CARTESIAN_POINT('Ctrl Pts',(-86.6342494657113,-6.04176855498474,
129.375238315919));
#199993=CARTESIAN_POINT('Ctrl Pts',(-86.9126970895244,-4.46808454959173,
135.114996102359));
#199994=CARTESIAN_POINT('Ctrl Pts',(-87.1911447133372,1.2115508788106,136.893490464523));
#199995=CARTESIAN_POINT('Ctrl Pts',(-87.4695923371502,5.77783023713722,
133.076371967865));
#199996=CARTESIAN_POINT('Ctrl Pts',(-87.7480399609628,5.03456587023344,
127.171386034204));
#199997=CARTESIAN_POINT('Ctrl Pts',(-88.026487584776,-0.33521857919891,
124.60492626198));
#199998=CARTESIAN_POINT('Ctrl Pts',(-88.3049352085887,-5.39695353068522,
127.735443803332));
#199999=CARTESIAN_POINT('Ctrl Pts',(-88.5833828324018,-5.49915184330967,
133.686145972045));
#200000=CARTESIAN_POINT('Ctrl Pts',(-88.8618304562145,-0.547898260434929,
136.988628183031));
#200001=CARTESIAN_POINT('Ctrl Pts',(-89.1402780800275,4.90684705746115,
134.608070619623));
#200002=CARTESIAN_POINT('Ctrl Pts',(-89.4187257038403,5.85243964235601,
128.732089385887));
#200003=CARTESIAN_POINT('Ctrl Pts',(-89.6971733276532,1.41992610349655,
124.760424177987));
#200004=CARTESIAN_POINT('Ctrl Pts',(-89.9756209514662,-4.31743015722937,
126.342841295349));
#200005=CARTESIAN_POINT('Ctrl Pts',(-90.254068575279,-6.08727902165076,
132.025176712493));
#200006=CARTESIAN_POINT('Ctrl Pts',(-90.5325161990919,-2.26321584528708,
136.585641778581));
#200007=CARTESIAN_POINT('Ctrl Pts',(-90.8109638229048,3.64063212865448,
135.833391888981));
#200008=CARTESIAN_POINT('Ctrl Pts',(-91.0894114467178,6.19891703112955,
130.459707942787));
#200009=CARTESIAN_POINT('Ctrl Pts',(-91.3678590705306,3.06070001592934,
125.402742967496));
#200010=CARTESIAN_POINT('Ctrl Pts',(-91.6463066943433,-2.89015079040179,
125.309600728926));
#200011=CARTESIAN_POINT('Ctrl Pts',(-91.9247543181566,-6.18509421206894,
130.265874394073));
#200012=CARTESIAN_POINT('Ctrl Pts',(-92.2032019419691,-3.79623821149537,
135.716990592095));
#200013=CARTESIAN_POINT('Ctrl Pts',(-92.4816495657822,2.08117524889636,
136.653639838841));
#200014=CARTESIAN_POINT('Ctrl Pts',(-92.7600971895951,6.04609032661485,
132.21508723441));
#200015=CARTESIAN_POINT('Ctrl Pts',(-93.0385448134079,4.45494376210749,
126.480145786926));
#200016=CARTESIAN_POINT('Ctrl Pts',(-93.3169924372209,-1.23007848367479,
124.718946519161));
#200017=CARTESIAN_POINT('Ctrl Pts',(-93.5954400610337,-5.78471869563455,
128.549945518824));
#200018=CARTESIAN_POINT('Ctrl Pts',(-93.8738876848466,-5.02348502552524,
134.45264185993));
#200019=CARTESIAN_POINT('Ctrl Pts',(-94.1523353086595,0.354085972155003,
137.002745967751));
#200020=CARTESIAN_POINT('Ctrl Pts',(-94.4307829324724,5.40626925948619,
133.85683674671));
#200021=CARTESIAN_POINT('Ctrl Pts',(-94.7092305562852,5.49035520828578,
127.905851084735));
#200022=CARTESIAN_POINT('Ctrl Pts',(-94.9876781800983,0.529072939433998,
124.618454083368));
#200023=CARTESIAN_POINT('Ctrl Pts',(-95.2661258039109,-4.91840151410816,
127.015602988595));
#200024=CARTESIAN_POINT('Ctrl Pts',(-95.5445734277241,-5.84610525345601,
132.894435063746));
#200025=CARTESIAN_POINT('Ctrl Pts',(-95.8230210515366,-1.40152386299717,
136.85259082867));
#200026=CARTESIAN_POINT('Ctrl Pts',(-96.10146867535,4.33098948930923,135.252718502061));
#200027=CARTESIAN_POINT('Ctrl Pts',(-96.3799162991623,6.08353508153927,
129.565022593965));
#200028=CARTESIAN_POINT('Ctrl Pts',(-96.6583639229758,2.245609131046,125.01621778453));
#200029=CARTESIAN_POINT('Ctrl Pts',(-96.9368115467883,-3.65592190677386,
125.786433472156));
#200030=CARTESIAN_POINT('Ctrl Pts',(-97.2152591706015,-6.19783931398261,
131.167879067045));
#200031=CARTESIAN_POINT('Ctrl Pts',(-97.493706794414,-3.04424517292474,
136.215268965725));
#200032=CARTESIAN_POINT('Ctrl Pts',(-97.7721544182274,2.90686156240656,
136.290298430015));
#200033=CARTESIAN_POINT('Ctrl Pts',(-98.0506020420397,6.18670452996842,
131.324019047625));
#200034=CARTESIAN_POINT('Ctrl Pts',(-98.3290496658531,3.78126827180747,
125.880198954735));
#200035=CARTESIAN_POINT('Ctrl Pts',(-98.6074972896656,-2.09896880291958,
124.961442871316));
#200036=CARTESIAN_POINT('Ctrl Pts',(-98.8859449134787,-6.05035608809047,
129.412042754299));
#200037=CARTESIAN_POINT('Ctrl Pts',(-99.1643925372916,-4.44176170463296,
135.142114735114));
#200038=CARTESIAN_POINT('Ctrl Pts',(-99.4428401611044,1.24859469325925,
136.886002592972));
#200039=CARTESIAN_POINT('Ctrl Pts',(-99.7212877849174,5.79155356528836,
133.041158580159));
#200040=CARTESIAN_POINT('Ctrl Pts',(-99.9997354087301,5.01235764393804,
127.140806513377));
#200041=CARTESIAN_POINT('Ctrl Pts',(-100.278183032543,-0.37295008490757,
124.607081693777));
#200042=CARTESIAN_POINT('Ctrl Pts',(-100.556630656356,-5.41553490534739,
127.768353451233));
#200043=CARTESIAN_POINT('Ctrl Pts',(-100.835078280169,-5.48150771136145,
133.719567477352));
#200044=CARTESIAN_POINT('Ctrl Pts',(-101.113525903981,-0.510242717172956,
136.9918488151));
#200045=CARTESIAN_POINT('Ctrl Pts',(-101.391973527794,4.92991040735466,
134.578130774917));
#200046=CARTESIAN_POINT('Ctrl Pts',(-101.670421151607,5.83971670703623,
128.696502319049));
#200047=CARTESIAN_POINT('Ctrl Pts',(-101.94886877542,1.38310863897239,124.751892664915));
#200048=CARTESIAN_POINT('Ctrl Pts',(-102.227316399233,-4.34450869969331,
126.36920537977));
#200049=CARTESIAN_POINT('Ctrl Pts',(-102.505764023046,-6.07973478439049,
132.062209088779));
#200050=CARTESIAN_POINT('Ctrl Pts',(-102.784211646859,-2.22798161378826,
136.599311502058));
#200051=CARTESIAN_POINT('Ctrl Pts',(-103.062659270672,3.6711778169323,135.811137151577));
#200052=CARTESIAN_POINT('Ctrl Pts',(-103.341106894485,6.19670418089893,
130.42197976097));
#200053=CARTESIAN_POINT('Ctrl Pts',(-103.619554518298,3.02776212844844,
125.384211697232));
#200054=CARTESIAN_POINT('Ctrl Pts',(-103.89800214211,-2.92354540564323,
125.327295702285));
#200055=CARTESIAN_POINT('Ctrl Pts',(-104.176449765923,-6.18825753508174,
130.303534794984));
#200056=CARTESIAN_POINT('Ctrl Pts',(-104.454897389736,-3.76626330296762,
135.740008351935));
#200057=CARTESIAN_POINT('Ctrl Pts',(-104.733345013549,2.1167429123828,136.640862760796));
#200058=CARTESIAN_POINT('Ctrl Pts',(-105.011792637362,6.05456579989334,
132.17825682901));
#200059=CARTESIAN_POINT('Ctrl Pts',(-105.290240261175,4.42853849928509,
126.453107397468));
#200060=CARTESIAN_POINT('Ctrl Pts',(-105.568687884988,-1.26709933603374,
124.726547104658));
#200061=CARTESIAN_POINT('Ctrl Pts',(-105.847135508801,-5.79833478278087,
128.585200512514));
#200062=CARTESIAN_POINT('Ctrl Pts',(-106.125583132613,-5.00118382855433,
134.483153644914));
#200063=CARTESIAN_POINT('Ctrl Pts',(-106.404030756427,0.391810742700936,
137.000475704212));
#200064=CARTESIAN_POINT('Ctrl Pts',(-106.682478380239,5.42475038243292,
133.823870695931));
#200065=CARTESIAN_POINT('Ctrl Pts',(-106.960926004052,5.47260943449832,
127.872483436902));
#200066=CARTESIAN_POINT('Ctrl Pts',(-107.239373627865,0.491407768093767,
124.615348076738));
#200067=CARTESIAN_POINT('Ctrl Pts',(-107.517821251678,-4.94137363058539,
127.045612891524));
#200068=CARTESIAN_POINT('Ctrl Pts',(-107.796268875491,-5.83327406227795,
132.929983241508));
#200069=CARTESIAN_POINT('Ctrl Pts',(-108.074716499304,-1.36468060201792,
136.861010242526));
#200070=CARTESIAN_POINT('Ctrl Pts',(-108.353164123117,4.3579876631431,135.22627212199));
#200071=CARTESIAN_POINT('Ctrl Pts',(-108.631611746929,6.07587816540856,
129.528013351273));
#200072=CARTESIAN_POINT('Ctrl Pts',(-108.910059370743,2.21033345681367,
125.00265536525));
#200073=CARTESIAN_POINT('Ctrl Pts',(-109.188506994555,-3.68639971780079,
125.808781077045));
#200074=CARTESIAN_POINT('Ctrl Pts',(-109.466954618368,-6.19551164239422,
131.205600338952));
#200075=CARTESIAN_POINT('Ctrl Pts',(-109.745402242181,-3.01125103519769,
136.233699898554));
#200076=CARTESIAN_POINT('Ctrl Pts',(-110.023849865994,2.94020216555433,
136.272501896897));
#200077=CARTESIAN_POINT('Ctrl Pts',(-110.302297489807,6.18975321302316,
131.286349193086));
#200078=CARTESIAN_POINT('Ctrl Pts',(-110.58074511362,3.75122344397827,125.857272534824));
#200079=CARTESIAN_POINT('Ctrl Pts',(-110.859192737433,-2.13449741262907,
124.974328145912));
#200080=CARTESIAN_POINT('Ctrl Pts',(-111.137640361246,-6.05871942302636,
129.44889878553));
#200081=CARTESIAN_POINT('Ctrl Pts',(-111.416087985058,-4.41527426856075,
135.169072630797));
#200082=CARTESIAN_POINT('Ctrl Pts',(-111.694535608871,1.28559224057236,
136.878289363941));
#200083=CARTESIAN_POINT('Ctrl Pts',(-111.972983232684,5.8050622852923,133.005862307081));
#200084=CARTESIAN_POINT('Ctrl Pts',(-112.251430856497,4.9899636828869,127.110362746893));
#200085=CARTESIAN_POINT('Ctrl Pts',(-112.52987848031,-0.410667770813077,
124.609466768025));
#200086=CARTESIAN_POINT('Ctrl Pts',(-112.808326104123,-5.43391560537209,
127.801375599495));
#200087=CARTESIAN_POINT('Ctrl Pts',(-113.086773727936,-5.46366046012913,
133.752880958598));
#200088=CARTESIAN_POINT('Ctrl Pts',(-113.365221351749,-0.472568266679477,
136.994840167519));
#200089=CARTESIAN_POINT('Ctrl Pts',(-113.643668975562,4.95279107760506,
134.548051091771));
#200090=CARTESIAN_POINT('Ctrl Pts',(-113.922116599375,5.8267773788663,128.660993359675));
#200091=CARTESIAN_POINT('Ctrl Pts',(-114.200564223187,1.34623992284899,
124.74358542827));
#200092=CARTESIAN_POINT('Ctrl Pts',(-114.479011847001,-4.37142625478972,
126.395733810498));
#200093=CARTESIAN_POINT('Ctrl Pts',(-114.757459470813,-6.07196526032194,
132.099194855029));
#200094=CARTESIAN_POINT('Ctrl Pts',(-115.035907094626,-2.19266482361144,
136.612766491501));
#200095=CARTESIAN_POINT('Ctrl Pts',(-115.314354718439,3.70158746836604,
135.788696886227));
#200096=CARTESIAN_POINT('Ctrl Pts',(-115.592802342252,6.19426170951602,
130.384265748418));
#200097=CARTESIAN_POINT('Ctrl Pts',(-115.871249966065,2.99471204612843,
125.36588127258));
#200098=CARTESIAN_POINT('Ctrl Pts',(-116.149697589878,-2.95683168783455,
125.345193630298));
#200099=CARTESIAN_POINT('Ctrl Pts',(-116.428145213691,-6.19119154993583,
130.34121375418));
#200100=CARTESIAN_POINT('Ctrl Pts',(-116.706592837503,-3.73614883416816,
135.762843219532));
#200101=CARTESIAN_POINT('Ctrl Pts',(-116.985040461316,2.1522321391827,136.627869409019));
#200102=CARTESIAN_POINT('Ctrl Pts',(-117.263488085129,6.06281691900968,
132.14137551338));
#200103=CARTESIAN_POINT('Ctrl Pts',(-117.541935708942,4.40196913533955,
126.426230245297));
#200104=CARTESIAN_POINT('Ctrl Pts',(-117.820383332755,-1.30407323556081,
124.73437290577));
#200105=CARTESIAN_POINT('Ctrl Pts',(-118.098830956568,-5.81173601049948,
128.620537737998));
#200106=CARTESIAN_POINT('Ctrl Pts',(-118.377278580381,-4.97869731087745,
134.51352911087));
#200107=CARTESIAN_POINT('Ctrl Pts',(-118.655726204194,0.429520994555717,
136.997975841351));
#200108=CARTESIAN_POINT('Ctrl Pts',(-118.934173828006,5.44303048925927,
133.790792756097));
#200109=CARTESIAN_POINT('Ctrl Pts',(-119.21262145182,5.45466087115571,127.839224430854));
#200110=CARTESIAN_POINT('Ctrl Pts',(-119.491069075632,0.453724387457947,
124.612471406243));
#200111=CARTESIAN_POINT('Ctrl Pts',(-119.769516699445,-4.96416264264509,
127.075762076232));
#200112=CARTESIAN_POINT('Ctrl Pts',(-120.047964323258,-5.82022671698453,
132.965452653541));
#200113=CARTESIAN_POINT('Ctrl Pts',(-120.326411947071,-1.32778677229758,
136.869205225004));
#200114=CARTESIAN_POINT('Ctrl Pts',(-120.604859570884,4.38482435014149,
135.199661886361));
#200115=CARTESIAN_POINT('Ctrl Pts',(-120.883307194697,6.06799610537801,
129.491051404098));
#200116=CARTESIAN_POINT('Ctrl Pts',(-121.16175481851,2.17497587786225,124.989307930291));
#200117=CARTESIAN_POINT('Ctrl Pts',(-121.440202442323,-3.71674092793051,
125.831313794972));
#200118=CARTESIAN_POINT('Ctrl Pts',(-121.718650066136,-6.19295439384353,
131.243306742772));
#200119=CARTESIAN_POINT('Ctrl Pts',(-121.997097689948,-2.97814531445616,
136.251929645219));
#200120=CARTESIAN_POINT('Ctrl Pts',(-122.275545313761,2.97343381842962,
136.254502739794));
#200121=CARTESIAN_POINT('Ctrl Pts',(-122.553992937574,6.19257253249627,
131.248661478285));
#200122=CARTESIAN_POINT('Ctrl Pts',(-122.832440561387,3.72103961318487,
125.83452943108));
#200123=CARTESIAN_POINT('Ctrl Pts',(-123.1108881852,-2.16994692775201,124.987429454503));
#200124=CARTESIAN_POINT('Ctrl Pts',(-123.389335809013,-6.06685824988591,
129.485805043896));
#200125=CARTESIAN_POINT('Ctrl Pts',(-123.667783432826,-4.38862322287681,
135.19586879047));
#200126=CARTESIAN_POINT('Ctrl Pts',(-123.946231056639,1.32254214979223,
136.870351063246));
#200127=CARTESIAN_POINT('Ctrl Pts',(-124.224678680451,5.81835589657845,
132.97048445655));
#200128=CARTESIAN_POINT('Ctrl Pts',(-124.503126304264,4.96738481689638,
127.080055862859));
#200129=CARTESIAN_POINT('Ctrl Pts',(-124.781573928077,-0.448370239273912,
124.612081396343));
#200130=CARTESIAN_POINT('Ctrl Pts',(-125.06002155189,-5.4520949496557,127.834509024472));
#200131=CARTESIAN_POINT('Ctrl Pts',(-125.338469175703,-5.44561075094924,
133.786085181339));
#200132=CARTESIAN_POINT('Ctrl Pts',(-125.616916799516,-0.434876304995071,
136.997602129441));
#200133=CARTESIAN_POINT('Ctrl Pts',(-125.895364423329,4.97548822036069,
134.517832684797));
#200134=CARTESIAN_POINT('Ctrl Pts',(-126.173812047142,5.8136221373178,128.625563823564));
#200135=CARTESIAN_POINT('Ctrl Pts',(-126.452259670955,1.30932132131015,
124.735502775877));
#200136=CARTESIAN_POINT('Ctrl Pts',(-126.730707294768,-4.39818182507867,
126.422425604514));
#200137=CARTESIAN_POINT('Ctrl Pts',(-127.00915491858,-6.0639707373477,132.136132640718));
#200138=CARTESIAN_POINT('Ctrl Pts',(-127.287602542393,-2.15726678343353,
136.626006248326));
#200139=CARTESIAN_POINT('Ctrl Pts',(-127.566050166206,3.73185995611441,
135.766071924465));
#200140=CARTESIAN_POINT('Ctrl Pts',(-127.844497790019,6.19158970748781,
130.346567302635));
#200141=CARTESIAN_POINT('Ctrl Pts',(-128.122945413832,2.96155099365221,
125.34775237278));
#200142=CARTESIAN_POINT('Ctrl Pts',(-128.401393037645,-2.99000840354028,
125.363293849751));
#200143=CARTESIAN_POINT('Ctrl Pts',(-128.679840661458,-6.19389614791022,
130.378909875453));
#200144=CARTESIAN_POINT('Ctrl Pts',(-128.958288285271,-3.70589592099968,
135.785494348734));
#200145=CARTESIAN_POINT('Ctrl Pts',(-129.236735909083,2.18764161422919,
136.614660264981));
#200146=CARTESIAN_POINT('Ctrl Pts',(-129.515183532897,6.07084337821547,
132.104444654172));
#200147=CARTESIAN_POINT('Ctrl Pts',(-129.793631156709,4.37523665480886,
126.399515326358));
#200148=CARTESIAN_POINT('Ctrl Pts',(-130.072078780522,-1.34099881217456,
124.742423632508));
#200149=CARTESIAN_POINT('Ctrl Pts',(-130.350526404335,-5.82492188220296,
128.655955885842));
#200150=CARTESIAN_POINT('Ctrl Pts',(-130.628974028148,-4.95602630574081,
134.543767132223));
#200151=CARTESIAN_POINT('Ctrl Pts',(-130.907421651961,0.467215330352083,
136.995246471799));
#200152=CARTESIAN_POINT('Ctrl Pts',(-131.185869275774,5.46110890258918,
133.757604152921));
#200153=CARTESIAN_POINT('Ctrl Pts',(-131.464316899587,5.43651018334856,
127.80607529902));
#200154=CARTESIAN_POINT('Ctrl Pts',(-131.742764523399,0.416024193898128,
124.60982417848));
#200155=CARTESIAN_POINT('Ctrl Pts',(-132.021212147213,-4.98676770583297,
127.106049425532));
#200156=CARTESIAN_POINT('Ctrl Pts',(-132.299659771025,-5.80696370104951,
133.000841985516));
#200157=CARTESIAN_POINT('Ctrl Pts',(-132.578107394838,-1.2908437409496,
136.877175472434));
#200158=CARTESIAN_POINT('Ctrl Pts',(-132.856555018651,4.41149855586104,
135.172888781227));
#200159=CARTESIAN_POINT('Ctrl Pts',(-133.135002642464,6.05988919352027,
129.454138122079));
#200160=CARTESIAN_POINT('Ctrl Pts',(-133.413450266277,2.13953770437982,
124.976175974248));
#200161=CARTESIAN_POINT('Ctrl Pts',(-133.69189789009,-3.74694441285829,
125.854030790976));
#200162=CARTESIAN_POINT('Ctrl Pts',(-133.970345513903,-6.19016766309031,
131.280996881284));
#200163=CARTESIAN_POINT('Ctrl Pts',(-134.248793137716,-2.94492923744478,
136.269957530209));
#200164=CARTESIAN_POINT('Ctrl Pts',(-134.527240761528,3.00655528962129,
136.236301625668));
#200165=CARTESIAN_POINT('Ctrl Pts',(-134.805688385342,6.19516238391663,
131.210957299752));
#200166=CARTESIAN_POINT('Ctrl Pts',(-135.084136009154,3.69071789790064,
125.811970486258));
#200167=CARTESIAN_POINT('Ctrl Pts',(-135.362583632967,-2.2053160346932,
125.000746311619));
#200168=CARTESIAN_POINT('Ctrl Pts',(-135.64103125678,-6.07477226708194,
129.522760161825));
#200169=CARTESIAN_POINT('Ctrl Pts',(-135.919478880593,-4.36180955514542,
135.222502221193));
#200170=CARTESIAN_POINT('Ctrl Pts',(-136.197926504406,1.35944305172635,
136.862187985044));
#200171=CARTESIAN_POINT('Ctrl Pts',(-136.476374128219,5.83143390654715,
132.935026339502));
#200172=CARTESIAN_POINT('Ctrl Pts',(-136.754821752032,4.9446218826347,127.049886984307));
#200173=CARTESIAN_POINT('Ctrl Pts',(-137.033269375845,-0.486056093210629,
124.614925481843));
#200174=CARTESIAN_POINT('Ctrl Pts',(-137.311716999657,-5.47007226455594,
127.867752498391));
#200175=CARTESIAN_POINT('Ctrl Pts',(-137.59016462347,-5.42735925266033,
133.819178915179));
#200176=CARTESIAN_POINT('Ctrl Pts',(-137.868612247283,-0.397168228809268,
137.000134598521));
#200177=CARTESIAN_POINT('Ctrl Pts',(-138.147059871096,4.99800099457058,
134.487476673751));
#200178=CARTESIAN_POINT('Ctrl Pts',(-138.425507494909,5.80025146986304,
128.590215023569));
#200179=CARTESIAN_POINT('Ctrl Pts',(-138.703955118722,1.27235420238826,
124.727645007244));
#200180=CARTESIAN_POINT('Ctrl Pts',(-138.982402742535,-4.42477441912264,
126.449279772744));
#200181=CARTESIAN_POINT('Ctrl Pts',(-139.260850366348,-6.05575151170779,
132.173021077107));
#200182=CARTESIAN_POINT('Ctrl Pts',(-139.539297990161,-2.12178880494131,
136.639030281933));
#200183=CARTESIAN_POINT('Ctrl Pts',(-139.817745613973,3.76199415842019,
135.743263104665));
#200184=CARTESIAN_POINT('Ctrl Pts',(-140.096193237787,6.18868827382574,
130.308885820552));
#200185=CARTESIAN_POINT('Ctrl Pts',(-140.374640861599,2.92828019981485,
125.329825669606));
#200186=CARTESIAN_POINT('Ctrl Pts',(-140.653088485412,-3.02307432338508,
125.381595689934));
#200187=CARTESIAN_POINT('Ctrl Pts',(-140.931536109225,-6.19637122878504,
130.416621761961));
#200188=CARTESIAN_POINT('Ctrl Pts',(-141.209983733038,-3.675505684495,135.807960900193));
#200189=CARTESIAN_POINT('Ctrl Pts',(-141.488431356851,2.22297002541115,
136.601235818153));
#200190=CARTESIAN_POINT('Ctrl Pts',(-141.766878980664,6.07864488008735,
132.06746561987));
#200191=CARTESIAN_POINT('Ctrl Pts',(-142.045326604476,4.34834204827492,
126.372963630579));
#200192=CARTESIAN_POINT('Ctrl Pts',(-142.32377422829,-1.3778746975837,124.750698986551));
#200193=CARTESIAN_POINT('Ctrl Pts',(-142.602221852102,-5.83789190928377,
128.691453643612));
#200194=CARTESIAN_POINT('Ctrl Pts',(-142.880669475915,-4.93317165322728,
134.573866588494));
#200195=CARTESIAN_POINT('Ctrl Pts',(-143.159117099728,0.504892353312588,
136.992287696695));
#200196=CARTESIAN_POINT('Ctrl Pts',(-143.437564723541,5.47898495252035,
133.72430611622));
#200197=CARTESIAN_POINT('Ctrl Pts',(-143.716012347354,5.4181580436573,127.77303726975));
#200198=CARTESIAN_POINT('Ctrl Pts',(-143.994459971167,0.378308584408798,
124.607406491544));
#200199=CARTESIAN_POINT('Ctrl Pts',(-144.27290759498,-5.00918798250961,
127.136473817112));
#200200=CARTESIAN_POINT('Ctrl Pts',(-144.551355218793,-5.79348550593904,
133.036149926065));
#200201=CARTESIAN_POINT('Ctrl Pts',(-144.829802842605,-1.2538528769121,
136.884920689477));
#200202=CARTESIAN_POINT('Ctrl Pts',(-145.108250466418,4.43800929187927,
135.145953798675));
#200203=CARTESIAN_POINT('Ctrl Pts',(-145.386698090231,6.05155773023994,
129.417274873051));
#200204=CARTESIAN_POINT('Ctrl Pts',(-145.665145714044,2.10402024954095,
124.963259983731));
#200205=CARTESIAN_POINT('Ctrl Pts',(-145.943593337857,-3.77700905338292,
125.876931223274));
#200206=CARTESIAN_POINT('Ctrl Pts',(-146.22204096167,-6.18715155339789,
131.318669357863));
#200207=CARTESIAN_POINT('Ctrl Pts',(-146.500488585483,-2.9116040349975,
136.287782885497));
#200208=CARTESIAN_POINT('Ctrl Pts',(-146.778936209295,3.03956535180104,
136.217899228972));
#200209=CARTESIAN_POINT('Ctrl Pts',(-147.057383833109,6.19752267131684,
131.173238054629));
#200210=CARTESIAN_POINT('Ctrl Pts',(-147.335831456921,3.66025942170698,
125.789596536289));
#200211=CARTESIAN_POINT('Ctrl Pts',(-147.614279080735,-2.24060342283806,
125.014278223797));
#200212=CARTESIAN_POINT('Ctrl Pts',(-147.892726704547,-6.08246118135759,
129.559762769929));
#200213=CARTESIAN_POINT('Ctrl Pts',(-148.17117432836,-4.33483425895693,
135.248971936054));
#200214=CARTESIAN_POINT('Ctrl Pts',(-148.449621952173,1.39629357899829,
136.853800431821));
#200215=CARTESIAN_POINT('Ctrl Pts',(-148.728069575986,5.84429583058792,
132.899489269852));
#200216=CARTESIAN_POINT('Ctrl Pts',(-149.006517199799,4.9216757235908,127.019857229157));
#200217=CARTESIAN_POINT('Ctrl Pts',(-149.284964823612,-0.52372393616008,
124.617998919139));
#200218=CARTESIAN_POINT('Ctrl Pts',(-149.563412447425,-5.48784688391679,
127.901104789406));
#200219=CARTESIAN_POINT('Ctrl Pts',(-149.841860071237,-5.40890664157841,
133.852160933818));
#200220=CARTESIAN_POINT('Ctrl Pts',(-150.12030769505,-0.359445435409253,
137.002437480918));
#200221=CARTESIAN_POINT('Ctrl Pts',(-150.398755318863,5.02032856601553,
134.456984183485));
#200222=CARTESIAN_POINT('Ctrl Pts',(-150.677202942676,5.78666587195703,
128.554948269553));
#200223=CARTESIAN_POINT('Ctrl Pts',(-150.955650566489,1.23533993591347,
124.720012413542));
#200224=CARTESIAN_POINT('Ctrl Pts',(-151.234098190302,-4.45120305152329,
126.476295320094));
#200225=CARTESIAN_POINT('Ctrl Pts',(-151.512545814115,-6.0473078879686,
132.209858797279));
#200226=CARTESIAN_POINT('Ctrl Pts',(-151.790993437928,-2.08623220278462,
136.651838109709));
#200227=CARTESIAN_POINT('Ctrl Pts',(-152.069441061741,3.79198895864895,
135.720271272016));
#200228=CARTESIAN_POINT('Ctrl Pts',(-152.347888685554,6.18555751604382,
130.27122269847));
#200229=CARTESIAN_POINT('Ctrl Pts',(-152.626336309366,2.89490089747778,
125.312101827337));
#200230=CARTESIAN_POINT('Ctrl Pts',(-152.904783933179,-3.05602822209906,
125.400098472666));
#200231=CARTESIAN_POINT('Ctrl Pts',(-153.183231556992,-6.19861670084527,
130.454348016274));
#200232=CARTESIAN_POINT('Ctrl Pts',(-153.461679180805,-3.64497925077551,
135.830242041403));
#200233=CARTESIAN_POINT('Ctrl Pts',(-153.740126804618,2.25821606362131,
136.587596565983));
#200234=CARTESIAN_POINT('Ctrl Pts',(-154.018574428431,6.08622113553776,
132.030439780749));
#200235=CARTESIAN_POINT('Ctrl Pts',(-154.297022052244,4.32128631232727,
126.346576141847));
#200236=CARTESIAN_POINT('Ctrl Pts',(-154.575469676057,-1.41469952533967,
124.759198661251));
#200237=CARTESIAN_POINT('Ctrl Pts',(-154.85391729987,-5.85064561113321,
128.727029695929));
#200238=CARTESIAN_POINT('Ctrl Pts',(-155.132364923682,-4.9101342002235,
134.603826364333));
#200239=CARTESIAN_POINT('Ctrl Pts',(-155.410812547495,0.542550667301237,
136.989099625678));
#200240=CARTESIAN_POINT('Ctrl Pts',(-155.689260171308,5.49665797664923,
133.690899879866));
#200241=CARTESIAN_POINT('Ctrl Pts',(-155.967707795121,5.39960513212718,
127.740111567281));
#200242=CARTESIAN_POINT('Ctrl Pts',(-156.246155418934,0.340578956555753,
124.605218435021));
#200243=CARTESIAN_POINT('Ctrl Pts',(-156.524603042747,-5.03142264188343,
127.167034123586));
#200244=CARTESIAN_POINT('Ctrl Pts',(-156.80305066656,-5.77979263109261,
133.071375166841));
#200245=CARTESIAN_POINT('Ctrl Pts',(-157.081498290373,-1.21681555089514,
136.89244058913));
#200246=CARTESIAN_POINT('Ctrl Pts',(-157.359945914186,4.46435557583064,
135.118857936792));
#200247=CARTESIAN_POINT('Ctrl Pts',(-157.638393537999,6.04300202426259,
129.380463022997));
#200248=CARTESIAN_POINT('Ctrl Pts',(-157.916841161811,2.06842482945845,
124.950560437346));
#200249=CARTESIAN_POINT('Ctrl Pts',(-158.195288785624,-3.80693373544809,
125.900014243279));
#200250=CARTESIAN_POINT('Ctrl Pts',(-158.473736409437,-6.18390617652933,
131.356322776543));
#200251=CARTESIAN_POINT('Ctrl Pts',(-158.75218403325,-2.87817094199197,
136.305405050556));
#200252=CARTESIAN_POINT('Ctrl Pts',(-159.030631657063,3.07246278176887,
136.199296231612));
#200253=CARTESIAN_POINT('Ctrl Pts',(-159.309079280876,6.19965330723533,
131.135505140616));
#200254=CARTESIAN_POINT('Ctrl Pts',(-159.587526904689,3.62966531325439,
125.767408410247));
#200255=CARTESIAN_POINT('Ctrl Pts',(-159.865974528502,-2.27580778459908,
125.028024689608));
#200256=CARTESIAN_POINT('Ctrl Pts',(-160.144422152314,-6.08992470779737,
129.596811497064));
#200257=CARTESIAN_POINT('Ctrl Pts',(-160.422869776128,-4.3076983338908,
135.275276954208));
#200258=CARTESIAN_POINT('Ctrl Pts',(-160.70131739994,1.43309236609815,136.845188714382));
#200259=CARTESIAN_POINT('Ctrl Pts',(-160.979765023753,5.85694119209746,
132.863874564441));
#200260=CARTESIAN_POINT('Ctrl Pts',(-161.258212647566,4.89854719004298,
126.989967710171));
#200261=CARTESIAN_POINT('Ctrl Pts',(-161.536660271379,-0.561372372326459,
124.621301594343));
#200262=CARTESIAN_POINT('Ctrl Pts',(-161.815107895192,-5.50541814909322,
127.934564661631));
#200263=CARTESIAN_POINT('Ctrl Pts',(-162.093555519005,-5.39025360147175,
133.885030015096));
#200264=CARTESIAN_POINT('Ctrl Pts',(-162.372003142818,-0.32170932262588,
137.004510691297));
#200265=CARTESIAN_POINT('Ctrl Pts',(-162.650450766631,5.04247010733932,
134.426356343909));
#200266=CARTESIAN_POINT('Ctrl Pts',(-162.928898390443,5.77286584701905,
128.519764868338));
#200267=CARTESIAN_POINT('Ctrl Pts',(-163.207346014257,1.19827989346308,
124.712605277602));
#200268=CARTESIAN_POINT('Ctrl Pts',(-163.485793638069,-4.47746674295796,
126.503471245498));
#200269=CARTESIAN_POINT('Ctrl Pts',(-163.764241261882,-6.03864017901171,
132.246644436198));
#200270=CARTESIAN_POINT('Ctrl Pts',(-164.042688885695,-2.05059829452646,
136.664429257056));
#200271=CARTESIAN_POINT('Ctrl Pts',(-164.321136509508,3.82184324533235,
135.697097278492));
#200272=CARTESIAN_POINT('Ctrl Pts',(-164.599584133321,6.18219755015336,
130.23357933201));
#200273=CARTESIAN_POINT('Ctrl Pts',(-164.878031757134,2.86141432352365,
125.294581502737));
#200274=CARTESIAN_POINT('Ctrl Pts',(-165.156479380946,-3.08886887856293,
125.418801512319));
#200275=CARTESIAN_POINT('Ctrl Pts',(-165.43492700476,-6.20063248088431,
130.492087240433));
#200276=CARTESIAN_POINT('Ctrl Pts',(-165.713374628572,-3.61431775100944,
135.85233694673));
#200277=CARTESIAN_POINT('Ctrl Pts',(-165.991822252385,2.2933784228048,136.573743013877));
#200278=CARTESIAN_POINT('Ctrl Pts',(-166.270269876198,6.09357186382579,
131.993368508814));
#200279=CARTESIAN_POINT('Ctrl Pts',(-166.548717500011,4.2940704495262,126.320353837957));
#200280=CARTESIAN_POINT('Ctrl Pts',(-166.827165123824,-1.45147193088449,
124.767922341652));
#200281=CARTESIAN_POINT('Ctrl Pts',(-167.105612747637,-5.86318251515793,
128.762682724506));
#200282=CARTESIAN_POINT('Ctrl Pts',(-167.38406037145,-4.88691480039125,
134.633645349573));
#200283=CARTESIAN_POINT('Ctrl Pts',(-167.662507995262,0.580188876875391,
136.985682376883));
#200284=CARTESIAN_POINT('Ctrl Pts',(-167.940955619076,5.51412732009539,
133.657386681736));
#200285=CARTESIAN_POINT('Ctrl Pts',(-168.219403242888,5.38085213624319,
127.707299411689));
#200286=CARTESIAN_POINT('Ctrl Pts',(-168.497850866701,0.302836708424229,
124.60326008999));
#200287=CARTESIAN_POINT('Ctrl Pts',(-168.776298490514,-5.05347086004094,
127.197729212531));
#200288=CARTESIAN_POINT('Ctrl Pts',(-169.054746114327,-5.7658855839047,
133.106516402559));
#200289=CARTESIAN_POINT('Ctrl Pts',(-169.33319373814,-1.17973313533045,
136.899734892741));
#200290=CARTESIAN_POINT('Ctrl Pts',(-169.611641361953,4.49053643144484,
135.091602199623));
#200291=CARTESIAN_POINT('Ctrl Pts',(-169.890088985766,6.03422239262278,
129.34370393599));
#200292=CARTESIAN_POINT('Ctrl Pts',(-170.168536609579,2.03275276313275,
124.938077805679));
#200293=CARTESIAN_POINT('Ctrl Pts',(-170.446984233392,-3.83671735018369,
125.923278995643));
#200294=CARTESIAN_POINT('Ctrl Pts',(-170.725431857205,-6.18043165274327,
131.393955742061));
#200295=CARTESIAN_POINT('Ctrl Pts',(-171.003879481017,-2.84463119730373,
136.32282337239));
#200296=CARTESIAN_POINT('Ctrl Pts',(-171.282327104831,3.10524636049842,
136.180493322929));
#200297=CARTESIAN_POINT('Ctrl Pts',(-171.560774728643,6.20155421272058,
131.097759955922));
#200298=CARTESIAN_POINT('Ctrl Pts',(-171.839222352457,3.59893670621881,
125.745406930321));
#200299=CARTESIAN_POINT('Ctrl Pts',(-172.117669976268,-2.31092781546573,
125.04198519967));
#200300=CARTESIAN_POINT('Ctrl Pts',(-172.396117600082,-6.09716256983718,
129.633904970377));
#200301=CARTESIAN_POINT('Ctrl Pts',(-172.674565223895,-4.2804027854792,
135.301416300912));
#200302=CARTESIAN_POINT('Ctrl Pts',(-172.953012847708,1.469838049433,136.836353151837));
#200303=CARTESIAN_POINT('Ctrl Pts',(-173.23146047152,5.86936952249723,132.828183542982));
#200304=CARTESIAN_POINT('Ctrl Pts',(-173.509908095334,4.8752371390276,126.960219534917));
#200305=CARTESIAN_POINT('Ctrl Pts',(-173.788355719146,-0.599000006633149,
124.624833385073));
#200306=CARTESIAN_POINT('Ctrl Pts',(-174.06680334296,-5.5227854089755,127.968130875202));
#200307=CARTESIAN_POINT('Ctrl Pts',(-174.345250966772,-5.37140082353563,
133.917784941036));
#200308=CARTESIAN_POINT('Ctrl Pts',(-174.623698590585,-0.283961288785237,
137.006354152836));
#200309=CARTESIAN_POINT('Ctrl Pts',(-174.902146214398,5.06442479807889,
134.39559428995));
#200310=CARTESIAN_POINT('Ctrl Pts',(-175.18059383821,5.75885190641417,128.484666123661));
#200311=CARTESIAN_POINT('Ctrl Pts',(-175.459041462024,1.16117544831056,
124.705423873895));
#200312=CARTESIAN_POINT('Ctrl Pts',(-175.737489085836,-4.50356452021585,
126.530806541938));
#200313=CARTESIAN_POINT('Ctrl Pts',(-176.01593670965,-6.02974870602229,
132.28337663076));
#200314=CARTESIAN_POINT('Ctrl Pts',(-176.294384333462,-2.01488840059438,
136.676803257405));
#200315=CARTESIAN_POINT('Ctrl Pts',(-176.572831957276,3.85155591220881,
135.67374198281));
#200316=CARTESIAN_POINT('Ctrl Pts',(-176.851279581088,6.17860850065921,
130.195957116059));
#200317=CARTESIAN_POINT('Ctrl Pts',(-177.129727204901,2.82782171880919,
125.277265345029));
#200318=CARTESIAN_POINT('Ctrl Pts',(-177.408174828714,-3.12159507585506,
125.437704115845));
#200319=CARTESIAN_POINT('Ctrl Pts',(-177.686622452527,-6.20241849420629,
130.529838035997));
#200320=CARTESIAN_POINT('Ctrl Pts',(-177.965070076339,-3.58352232136993,
135.874244797437));
#200321=CARTESIAN_POINT('Ctrl Pts',(-178.243517700153,2.32845580000743,
136.559675675186));
#200322=CARTESIAN_POINT('Ctrl Pts',(-178.521965323965,6.10069679256748,
131.956253177754));
#200323=CARTESIAN_POINT('Ctrl Pts',(-178.800412947778,4.26669546836545,
126.294297690589));
#200324=CARTESIAN_POINT('Ctrl Pts',(-179.078860571591,-1.48819055160311,
124.776869704492));
#200325=CARTESIAN_POINT('Ctrl Pts',(-179.357308195404,-5.8755021567984,
128.798411408209));
#200326=CARTESIAN_POINT('Ctrl Pts',(-179.635755819217,-4.86351431413387,
134.663322439258));
#200327=CARTESIAN_POINT('Ctrl Pts',(-179.91420344303,0.617805587336893,
136.982036076937));
#200328=CARTESIAN_POINT('Ctrl Pts',(-180.192651066843,5.53139233552561,
133.623767763677));
#200329=CARTESIAN_POINT('Ctrl Pts',(-180.471098690656,5.36189975090491,
127.674602018838));
#200330=CARTESIAN_POINT('Ctrl Pts',(-180.749546314469,0.265083238567079,
124.601531529021));
#200331=CARTESIAN_POINT('Ctrl Pts',(-181.027993938281,-5.07533181997731,
127.22855794653));
#200332=CARTESIAN_POINT('Ctrl Pts',(-181.306441562095,-5.75176487970607,
133.141572331048));
#200333=CARTESIAN_POINT('Ctrl Pts',(-181.584889185907,-1.14260700432061,
136.906803330016));
#200334=CARTESIAN_POINT('Ctrl Pts',(-181.86333680972,4.5165508885802,135.064187597142));
#200335=CARTESIAN_POINT('Ctrl Pts',(-182.141784433533,6.02521916065313,
129.306998974155));
#200336=CARTESIAN_POINT('Ctrl Pts',(-182.420232057346,1.99700537240587,
124.925812551278));
#200337=CARTESIAN_POINT('Ctrl Pts',(-182.698679681159,-3.86635879394691,
125.946724618282));
#200338=CARTESIAN_POINT('Ctrl Pts',(-182.977127304972,-6.17672811078948,
131.431566859916));
#200339=CARTESIAN_POINT('Ctrl Pts',(-183.255574928785,-2.81098604376035,
136.340037205557));
#200340=CARTESIAN_POINT('Ctrl Pts',(-183.534022552597,3.13791487318212,
136.161491199671));
#200341=CARTESIAN_POINT('Ctrl Pts',(-183.81247017641,6.20322531733387,131.060003899207));
#200342=CARTESIAN_POINT('Ctrl Pts',(-184.090917800223,3.56807473926006,
125.723592911784));
#200343=CARTESIAN_POINT('Ctrl Pts',(-184.369365424036,-2.34596221405232,
125.056159236672));
#200344=CARTESIAN_POINT('Ctrl Pts',(-184.647813047849,-6.10417449927606,
129.671041815353));
#200345=CARTESIAN_POINT('Ctrl Pts',(-184.926260671662,-4.25294862516783,
135.327389007565));
#200346=CARTESIAN_POINT('Ctrl Pts',(-185.204708295475,1.50652926737877,
136.827294071589));
#200347=CARTESIAN_POINT('Ctrl Pts',(-185.483155919288,5.88158036125089,
132.792417528021));
#200348=CARTESIAN_POINT('Ctrl Pts',(-185.761603543101,4.85174643430717,
126.930613805724));
#200349=CARTESIAN_POINT('Ctrl Pts',(-186.040051166913,-0.6366054447743,
124.628594160457));
#200350=CARTESIAN_POINT('Ctrl Pts',(-186.318498790727,-5.53994802001346,
128.001802186308));
#200351=CARTESIAN_POINT('Ctrl Pts',(-186.596946414539,-5.35234900636664,
133.950424497894));
#200352=CARTESIAN_POINT('Ctrl Pts',(-186.875394038353,-0.246202732654624,
137.007967797222));
#200353=CARTESIAN_POINT('Ctrl Pts',(-187.153841662165,5.08619182469514,
134.364699161505));
#200354=CARTESIAN_POINT('Ctrl Pts',(-187.432289285978,5.744624569434,128.449653336115));
#200355=CARTESIAN_POINT('Ctrl Pts',(-187.71073690979,1.12402797537536,124.698468468532));
#200356=CARTESIAN_POINT('Ctrl Pts',(-187.989184533604,-4.52949541623416,
126.558300196495));
#200357=CARTESIAN_POINT('Ctrl Pts',(-188.267632157416,-6.0206337984771,
132.32005401984));
#200358=CARTESIAN_POINT('Ctrl Pts',(-188.54607978123,-1.97910384423165,
136.688959652232));
#200359=CARTESIAN_POINT('Ctrl Pts',(-188.824527405043,3.88112585826452,
135.650206250412));
#200360=CARTESIAN_POINT('Ctrl Pts',(-189.102975028855,6.17479050055486,
130.158357444724));
#200361=CARTESIAN_POINT('Ctrl Pts',(-189.381422652668,2.79412432812102,
125.260153995869));
#200362=CARTESIAN_POINT('Ctrl Pts',(-189.659870276481,-3.15420560129371,
125.456805582802));
#200363=CARTESIAN_POINT('Ctrl Pts',(-189.938317900294,-6.20397467462999,
130.567599004095));
#200364=CARTESIAN_POINT('Ctrl Pts',(-190.216765524107,-3.55259410299321,
135.89596478172));
#200365=CARTESIAN_POINT('Ctrl Pts',(-190.49521314792,2.36344689542356,136.545395071179));
#200366=CARTESIAN_POINT('Ctrl Pts',(-190.773660771733,6.10759565774615,
131.919095162891));
#200367=CARTESIAN_POINT('Ctrl Pts',(-191.052108395545,4.23916238323504,
126.26840866526));
#200368=CARTESIAN_POINT('Ctrl Pts',(-191.330556019359,-1.52485402687357,
124.786040418225));
#200369=CARTESIAN_POINT('Ctrl Pts',(-191.609003643171,-5.88760407954571,
128.834214423098));
#200370=CARTESIAN_POINT('Ctrl Pts',(-191.887451266984,-4.83993360856504,
134.692856533694));
#200371=CARTESIAN_POINT('Ctrl Pts',(-192.165898890797,0.655399404785621,
136.978160860955));
#200372=CARTESIAN_POINT('Ctrl Pts',(-192.44434651461,5.54845238317892,133.59004437145));
#200373=CARTESIAN_POINT('Ctrl Pts',(-192.722794138423,5.34274867839911,
127.642020600343));
#200374=CARTESIAN_POINT('Ctrl Pts',(-193.001241762236,0.227319945953055,
124.600032816164));
#200375=CARTESIAN_POINT('Ctrl Pts',(-193.279689386049,-5.09700471162664,
127.259519183211));
#200376=CARTESIAN_POINT('Ctrl Pts',(-193.558137009861,-5.73743104174462,
133.176541653297));
#200377=CARTESIAN_POINT('Ctrl Pts',(-193.836584633675,-1.105438533588,136.913645639033));
#200378=CARTESIAN_POINT('Ctrl Pts',(-194.115032257487,4.5423979832614,135.036615145204));
#200379=CARTESIAN_POINT('Ctrl Pts',(-194.3934798813,6.01599266197172,129.270349497605));
#200380=CARTESIAN_POINT('Ctrl Pts',(-194.671927505113,1.96118398191049,
124.913765128639));
#200381=CARTESIAN_POINT('Ctrl Pts',(-194.950375128926,-3.89585696836267,
125.970350242409));
#200382=CARTESIAN_POINT('Ctrl Pts',(-195.228822752739,-6.17279568790409,
131.469154736412));
#200383=CARTESIAN_POINT('Ctrl Pts',(-195.507270376552,-2.77723672809589,
136.357045912194));
#200384=CARTESIAN_POINT('Ctrl Pts',(-195.785718000365,3.17046710927626,
136.142290565968));
#200385=CARTESIAN_POINT('Ctrl Pts',(-196.064165624178,6.20466655915177,
131.022238369536));
#200386=CARTESIAN_POINT('Ctrl Pts',(-196.342613247991,3.5370805559797,125.701967162963));
#200387=CARTESIAN_POINT('Ctrl Pts',(-196.621060871803,-2.38090968214636,
125.070546275391));
#200388=CARTESIAN_POINT('Ctrl Pts',(-196.899508495616,-6.11096023628406,
129.708220655875));
#200389=CARTESIAN_POINT('Ctrl Pts',(-197.177956119429,-4.22533687028115,
135.353194111738));
#200390=CARTESIAN_POINT('Ctrl Pts',(-197.456403743242,1.54316466032852,
136.818011809327));
#200391=CARTESIAN_POINT('Ctrl Pts',(-197.734851367055,5.89357325588093,
132.75657784488));
#200392=CARTESIAN_POINT('Ctrl Pts',(-198.013298990868,4.82807594633875,
126.901151619645));
#200393=CARTESIAN_POINT('Ctrl Pts',(-198.291746614681,-0.674187293266194,
124.632583781138));
#200394=CARTESIAN_POINT('Ctrl Pts',(-198.570194238494,-5.55690534624021,
128.035577347248));
#200395=CARTESIAN_POINT('Ctrl Pts',(-198.848641862306,-5.33309885593691,
133.982947476197));
#200396=CARTESIAN_POINT('Ctrl Pts',(-199.12708948612,-0.2084350533912,137.009351564664));
#200397=CARTESIAN_POINT('Ctrl Pts',(-199.405537109932,5.10777038060287,
134.333672103408));
#200398=CARTESIAN_POINT('Ctrl Pts',(-199.683984733745,5.7301843632779,128.414727803113));
#200399=CARTESIAN_POINT('Ctrl Pts',(-199.962432357558,1.08683885116959,
124.691739319248));
#200400=CARTESIAN_POINT('Ctrl Pts',(-200.240879981371,-4.5552584701342,
126.585951190383));
#200401=CARTESIAN_POINT('Ctrl Pts',(-200.519327605184,-6.01129579413245,
132.356675244344));
#200402=CARTESIAN_POINT('Ctrl Pts',(-200.797775228997,-1.94324595144814,
136.700897991079));
#200403=CARTESIAN_POINT('Ctrl Pts',(-201.076222852809,3.91055198777426,
135.626490953421));
#200404=CARTESIAN_POINT('Ctrl Pts',(-201.354670476623,6.17074369131775,
130.120781711275));
#200405=CARTESIAN_POINT('Ctrl Pts',(-201.633118100435,2.76032340012831,
125.243248089324));
#200406=CARTESIAN_POINT('Ctrl Pts',(-201.911565724248,-3.18669924648382,
125.476105205376));
#200407=CARTESIAN_POINT('Ctrl Pts',(-202.190013348061,-6.20530096449064,
130.605368745483));
#200408=CARTESIAN_POINT('Ctrl Pts',(-202.468460971874,-3.52153424193529,
135.91749609474));
#200409=CARTESIAN_POINT('Ctrl Pts',(-202.746908595687,2.39835041244635,
136.530901731028));
#200410=CARTESIAN_POINT('Ctrl Pts',(-203.0253562195,6.11426820372151,131.881895841131));
#200411=CARTESIAN_POINT('Ctrl Pts',(-203.303803843313,4.21147221438356,
126.242687721299));
#200412=CARTESIAN_POINT('Ctrl Pts',(-203.582251467125,-1.56146099811728,
124.795434143027));
#200413=CARTESIAN_POINT('Ctrl Pts',(-203.860699090939,-5.89948783495869,
128.870090442477));
#200414=CARTESIAN_POINT('Ctrl Pts',(-204.139146714752,-4.81617355747646,
134.722246538484));
#200415=CARTESIAN_POINT('Ctrl Pts',(-204.417594338564,0.69296893616836,
136.974056872534));
#200416=CARTESIAN_POINT('Ctrl Pts',(-204.696041962377,5.56530683088876,
133.556217754686));
#200417=CARTESIAN_POINT('Ctrl Pts',(-204.97448958619,5.32339962837619,127.60955636352));
#200418=CARTESIAN_POINT('Ctrl Pts',(-205.252937210003,0.18954822991528,
124.598764006957));
#200419=CARTESIAN_POINT('Ctrl Pts',(-205.531384833816,-5.11848873189165,
127.290611775294));
#200420=CARTESIAN_POINT('Ctrl Pts',(-205.809832457629,-5.72288460116635,
133.211423073505));
#200421=CARTESIAN_POINT('Ctrl Pts',(-206.088280081441,-1.06822910042401,
136.920261566246));
#200422=CARTESIAN_POINT('Ctrl Pts',(-206.366727705255,4.56807675771487,
135.00888586552));
#200423=CARTESIAN_POINT('Ctrl Pts',(-206.645175329067,6.00654323846982,
129.233756864401));
#200424=CARTESIAN_POINT('Ctrl Pts',(-206.92362295288,1.92528991902147,124.901935984182));
#200425=CARTESIAN_POINT('Ctrl Pts',(-207.202070576693,-3.92521078036628,
125.994154992568));
#200426=CARTESIAN_POINT('Ctrl Pts',(-207.480518200506,-6.16863452980439,
131.506717978718));
#200427=CARTESIAN_POINT('Ctrl Pts',(-207.758965824319,-2.74338450090264,
136.373848862034));
#200428=CARTESIAN_POINT('Ctrl Pts',(-208.037413448132,3.20290186254569,
136.12289213331));
#200429=CARTESIAN_POINT('Ctrl Pts',(-208.315861071945,6.20587788476857,
130.984464766326));
#200430=CARTESIAN_POINT('Ctrl Pts',(-208.594308695758,3.50595530487857,
125.680530485208));
#200431=CARTESIAN_POINT('Ctrl Pts',(-208.872756319571,-2.41576892475653,
125.085145782709));
#200432=CARTESIAN_POINT('Ctrl Pts',(-209.151203943383,-6.11751952941318,
129.745440114266));
#200433=CARTESIAN_POINT('Ctrl Pts',(-209.429651567197,-4.19756854398286,
135.378830657213));
#200434=CARTESIAN_POINT('Ctrl Pts',(-209.708099191009,1.57974287074426,
136.808506709009));
#200435=CARTESIAN_POINT('Ctrl Pts',(-209.986546814822,5.90534776198698,
132.720665821612));
#200436=CARTESIAN_POINT('Ctrl Pts',(-210.264994438635,4.80422655224024,
126.87183406841));
#200437=CARTESIAN_POINT('Ctrl Pts',(-210.543442062448,-0.711744159500396,
124.63680209928));
#200438=CARTESIAN_POINT('Ctrl Pts',(-210.821889686261,-5.57365675929581,
128.06945510647));
#200439=CARTESIAN_POINT('Ctrl Pts',(-211.100337310074,-5.31365108556781,
134.015352670796));
#200440=CARTESIAN_POINT('Ctrl Pts',(-211.378784933887,-0.170659650490228,
137.010505403884));
#200441=CARTESIAN_POINT('Ctrl Pts',(-211.657232557699,5.12915966620077,
134.302514265376));
#200442=CARTESIAN_POINT('Ctrl Pts',(-211.935680181513,5.71553182303293,
128.379890818834));
#200443=CARTESIAN_POINT('Ctrl Pts',(-212.214127805325,1.04960945375051,
124.685236675394));
#200444=CARTESIAN_POINT('Ctrl Pts',(-212.492575429138,-4.58085272725645,
126.613758498985));
#200445=CARTESIAN_POINT('Ctrl Pts',(-212.771023052951,-6.00173503901134,
132.393238947258));
#200446=CARTESIAN_POINT('Ctrl Pts',(-213.049470676764,-1.90731605097184,
136.712617831564));
#200447=CARTESIAN_POINT('Ctrl Pts',(-213.327918300577,3.93983321034183,
135.602596970618));
#200448=CARTESIAN_POINT('Ctrl Pts',(-213.60636592439,6.16646822290386,130.083231308093));
#200449=CARTESIAN_POINT('Ctrl Pts',(-213.884813548203,2.72642018733693,
125.226548251849));
#200450=CARTESIAN_POINT('Ctrl Pts',(-214.163261172015,-3.21907480736146,
125.495602268416));
#200451=CARTESIAN_POINT('Ctrl Pts',(-214.441708795829,-6.20639731464204,
130.643145860587));
#200452=CARTESIAN_POINT('Ctrl Pts',(-214.720156419641,-3.49034388913101,
135.938837938644));
#200453=CARTESIAN_POINT('Ctrl Pts',(-214.998604043455,2.43316505771265,
136.516196191791));
#200454=CARTESIAN_POINT('Ctrl Pts',(-215.277051667267,6.12071418324004,
131.844656590906));
#200455=CARTESIAN_POINT('Ctrl Pts',(-215.55549929108,4.18362598788043,126.217135811804));
#200456=CARTESIAN_POINT('Ctrl Pts',(-215.833946914893,-1.59801010884951,
124.805050530808));
#200457=CARTESIAN_POINT('Ctrl Pts',(-216.112394538706,-5.91115298268039,
128.90603813695));
#200458=CARTESIAN_POINT('Ctrl Pts',(-216.390842162519,-4.79223504130557,
134.75149136457));
#200459=CARTESIAN_POINT('Ctrl Pts',(-216.669289786332,0.730512789332353,
136.969724263749));
#200460=CARTESIAN_POINT('Ctrl Pts',(-216.947737410145,5.5819550541073,133.522289166845));
#200461=CARTESIAN_POINT('Ctrl Pts',(-217.226185033957,5.3038533178224,127.577210511344));
#200462=CARTESIAN_POINT('Ctrl Pts',(-217.50463265777,0.151769490097695,
124.597725148413));
#200463=CARTESIAN_POINT('Ctrl Pts',(-217.783080281583,-5.13978308467467,
127.321834570635));
#200464=CARTESIAN_POINT('Ctrl Pts',(-218.061527905396,-5.70812609699421,
133.24621529913));
#200465=CARTESIAN_POINT('Ctrl Pts',(-218.339975529209,-1.03098008363786,
136.9266508665));
#200466=CARTESIAN_POINT('Ctrl Pts',(-218.618423153022,4.59358626040416,
134.981000785606));
#200467=CARTESIAN_POINT('Ctrl Pts',(-218.896870776835,5.99687124029931,
129.197222430498));
#200468=CARTESIAN_POINT('Ctrl Pts',(-219.175318400648,1.88932451380644,
124.890325556239));
#200469=CARTESIAN_POINT('Ctrl Pts',(-219.45376602446,-3.95441914224089,
126.018137986666));
#200470=CARTESIAN_POINT('Ctrl Pts',(-219.732213648274,-6.16424479068368,
131.544255194914));
#200471=CARTESIAN_POINT('Ctrl Pts',(-220.010661272086,-2.70943061658779,
136.390445432439));
#200472=CARTESIAN_POINT('Ctrl Pts',(-220.289108895899,3.23521793110825,
136.103296620509));
#200473=CARTESIAN_POINT('Ctrl Pts',(-220.567556519712,6.20685924929812,
130.94668448929));
#200474=CARTESIAN_POINT('Ctrl Pts',(-220.846004143525,3.47470013931478,
125.659283672863));
#200475=CARTESIAN_POINT('Ctrl Pts',(-221.124451767337,-2.45053865016082,
125.099957217636));
#200476=CARTESIAN_POINT('Ctrl Pts',(-221.402899391151,-6.12385213560643,
129.782698811345));
#200477=CARTESIAN_POINT('Ctrl Pts',(-221.681347014963,-4.16964467523852,
135.404297694017));
#200478=CARTESIAN_POINT('Ctrl Pts',(-221.959794638777,1.61626254320698,
136.79877912285));
#200479=CARTESIAN_POINT('Ctrl Pts',(-222.238242262589,5.91690344326002,
132.684682788949));
#200480=CARTESIAN_POINT('Ctrl Pts',(-222.516689886402,4.7801991357601,126.842662238393));
#200481=CARTESIAN_POINT('Ctrl Pts',(-222.795137510215,-0.749274651793031,
124.64124895857));
#200482=CARTESIAN_POINT('Ctrl Pts',(-223.073585134028,-5.59020163845046,
128.103434208622));
#200483=CARTESIAN_POINT('Ctrl Pts',(-223.352032757841,-5.29400641590365,
134.047638880903));
#200484=CARTESIAN_POINT('Ctrl Pts',(-223.630480381654,-0.132877923733138,
137.011429272127));
#200485=CARTESIAN_POINT('Ctrl Pts',(-223.908928005467,5.15035888890098,
134.271226801972));
#200486=CARTESIAN_POINT('Ctrl Pts',(-224.187375629279,5.70066749165438,
128.345143674176));
#200487=CARTESIAN_POINT('Ctrl Pts',(-224.465823253093,1.01234116266713,
124.678960777928));
#200488=CARTESIAN_POINT('Ctrl Pts',(-224.744270876905,-4.60627723919628,
126.641721091889));
#200489=CARTESIAN_POINT('Ctrl Pts',(-225.022718500718,-5.99195188739136,
132.4297437737));
#200490=CARTESIAN_POINT('Ctrl Pts',(-225.301166124531,-1.87131547419729,
136.724118739406));
#200491=CARTESIAN_POINT('Ctrl Pts',(-225.579613748344,3.96896844094108,
135.578525187401));
#200492=CARTESIAN_POINT('Ctrl Pts',(-225.858061372157,6.16196425374224,
130.045707626623));
#200493=CARTESIAN_POINT('Ctrl Pts',(-226.13650899597,2.69241594604283,125.210055102262));
#200494=CARTESIAN_POINT('Ctrl Pts',(-226.414956619783,-3.25133108423828,
125.515296049447));
#200495=CARTESIAN_POINT('Ctrl Pts',(-226.693404243596,-6.20726368445854,
130.680928949564));
#200496=CARTESIAN_POINT('Ctrl Pts',(-226.971851867408,-3.45902420035033,
135.959989522602));
#200497=CARTESIAN_POINT('Ctrl Pts',(-227.250299491222,2.46788954115291,
136.501278998386));
#200498=CARTESIAN_POINT('Ctrl Pts',(-227.528747115034,6.12693335744362,
131.80737879213));
#200499=CARTESIAN_POINT('Ctrl Pts',(-227.807194738847,4.15562473557794,
126.191753883612));
#200500=CARTESIAN_POINT('Ctrl Pts',(-228.08564236266,-1.63450000472891,
124.81488922523));
#200501=CARTESIAN_POINT('Ctrl Pts',(-228.364089986473,-5.9225990904546,
128.942056174461));
#200502=CARTESIAN_POINT('Ctrl Pts',(-228.642537610286,-4.76811894710285,
134.780589928275));
#200503=CARTESIAN_POINT('Ctrl Pts',(-228.920985234099,0.768029573076269,
136.965163195147));
#200504=CARTESIAN_POINT('Ctrl Pts',(-229.199432857912,5.59839643592858,
133.48825986516));
#200505=CARTESIAN_POINT('Ctrl Pts',(-229.477880481725,5.28411047103341,
127.544984242401));
#200506=CARTESIAN_POINT('Ctrl Pts',(-229.756328105537,0.11398512640586,
124.59691627903));
#200507=CARTESIAN_POINT('Ctrl Pts',(-230.03477572935,-5.16088698090536,
127.353186412258));
#200508=CARTESIAN_POINT('Ctrl Pts',(-230.313223353163,-5.69315607611037,
133.280917040931));
#200509=CARTESIAN_POINT('Ctrl Pts',(-230.591670976976,-0.993692863505588,
136.932813303039));
#200510=CARTESIAN_POINT('Ctrl Pts',(-230.870118600789,4.6189255460653,134.952960938754));
#200511=CARTESIAN_POINT('Ctrl Pts',(-231.148566224602,5.98697702585963,
129.160747549691));
#200512=CARTESIAN_POINT('Ctrl Pts',(-231.427013848415,1.85328909897679,
124.878934275042));
#200513=CARTESIAN_POINT('Ctrl Pts',(-231.705461472227,-3.98348097165998,
126.042298336002));
#200514=CARTESIAN_POINT('Ctrl Pts',(-231.983909096041,-6.15962663320533,
131.581764994044));
#200515=CARTESIAN_POINT('Ctrl Pts',(-232.262356719853,-2.6753763333251,
136.406835008417));
#200516=CARTESIAN_POINT('Ctrl Pts',(-232.540804343666,3.26741411748112,
136.083504753687));
#200517=CARTESIAN_POINT('Ctrl Pts',(-232.819251967479,6.20761061637562,
130.90889893839));
#200518=CARTESIAN_POINT('Ctrl Pts',(-233.097699591292,3.44331621745904,
125.638227513236));
#200519=CARTESIAN_POINT('Ctrl Pts',(-233.376147215105,-2.48521756995422,
125.114980031328));
#200520=CARTESIAN_POINT('Ctrl Pts',(-233.654594838918,-6.12995782020675,
129.819995366479));
#200521=CARTESIAN_POINT('Ctrl Pts',(-233.933042462731,-4.14156629877734,
135.429594278462));
#200522=CARTESIAN_POINT('Ctrl Pts',(-234.211490086544,1.65272232446679,
136.788829411307));
#200523=CARTESIAN_POINT('Ctrl Pts',(-234.489937710357,5.92823987150001,
132.648630080257));
#200524=CARTESIAN_POINT('Ctrl Pts',(-234.768385334169,4.75599458724306,
126.813637210565));
#200525=CARTESIAN_POINT('Ctrl Pts',(-235.046832957982,-0.786777379437916,
124.64592419423));
#200526=CARTESIAN_POINT('Ctrl Pts',(-235.325280581795,-5.6065393706272,
128.137513394595));
#200527=CARTESIAN_POINT('Ctrl Pts',(-235.603728205608,-5.27416557488518,
134.079804910139));
#200528=CARTESIAN_POINT('Ctrl Pts',(-235.882175829421,-0.0950912731361558,
137.012123135159));
#200529=CARTESIAN_POINT('Ctrl Pts',(-236.160623453234,5.17136726315852,
134.239810872567));
#200530=CARTESIAN_POINT('Ctrl Pts',(-236.439071077047,5.68559191994549,
128.310487656705));
#200531=CARTESIAN_POINT('Ctrl Pts',(-236.71751870086,0.975035358909668,
124.672911859406));
#200532=CARTESIAN_POINT('Ctrl Pts',(-236.995966324673,-4.63153106383903,
126.669837932931));
#200533=CARTESIAN_POINT('Ctrl Pts',(-237.274413948486,-5.98194670179065,
132.466188370973));
#200534=CARTESIAN_POINT('Ctrl Pts',(-237.552861572298,-1.83524555513966,
136.735400288432));
#200535=CARTESIAN_POINT('Ctrl Pts',(-237.831309196112,3.99795659995517,
135.554276495761));
#200536=CARTESIAN_POINT('Ctrl Pts',(-238.109756819924,6.15723195072914,
130.008212057319));
#200537=CARTESIAN_POINT('Ctrl Pts',(-238.388204443737,2.65831193628575,
125.193769251723));
#200538=CARTESIAN_POINT('Ctrl Pts',(-238.66665206755,-3.28346688184612,
125.535185818711));
#200539=CARTESIAN_POINT('Ctrl Pts',(-238.945099691363,-6.20790004183648,
130.718716612347));
#200540=CARTESIAN_POINT('Ctrl Pts',(-239.223547315176,-3.42757633615586,
135.980950062836));
#200541=CARTESIAN_POINT('Ctrl Pts',(-239.501994938989,2.50252257603867,
136.486150703575));
#200542=CARTESIAN_POINT('Ctrl Pts',(-239.780442562802,6.13292549587844,
131.770063826148));
#200543=CARTESIAN_POINT('Ctrl Pts',(-240.058890186614,4.12746949507249,
126.166542877259));
#200544=CARTESIAN_POINT('Ctrl Pts',(-240.337337810428,-1.67092933361012,
124.824949861719));
#200545=CARTESIAN_POINT('Ctrl Pts',(-240.61578543424,-5.93382573414137,
128.978143220346));
#200546=CARTESIAN_POINT('Ctrl Pts',(-240.894233058053,-4.74382616849909,
134.80954115134));
#200547=CARTESIAN_POINT('Ctrl Pts',(-241.172680681866,0.805517897201924,
136.960373835741));
#200548=CARTESIAN_POINT('Ctrl Pts',(-241.451128305679,5.6146303671111,133.454131110603));
#200549=CARTESIAN_POINT('Ctrl Pts',(-241.729575929492,5.26417181958768,
127.512878750849));
#200550=CARTESIAN_POINT('Ctrl Pts',(-242.008023553305,0.0761965389532375,
124.596337428779));
#200551=CARTESIAN_POINT('Ctrl Pts',(-242.286471177117,-5.18179963857104,
127.384666138411));
#200552=CARTESIAN_POINT('Ctrl Pts',(-242.564918800931,-5.67797509323448,
133.315527013022));
#200553=CARTESIAN_POINT('Ctrl Pts',(-242.843366424743,-0.956368821719198,
136.938748647509));
#200554=CARTESIAN_POINT('Ctrl Pts',(-243.121814048556,4.64409367574132,
134.924767363992));
#200555=CARTESIAN_POINT('Ctrl Pts',(-243.400261672369,5.9768609617849,129.124333573571));
#200556=CARTESIAN_POINT('Ctrl Pts',(-243.678709296182,1.81718500983798,
124.867762562695));
#200557=CARTESIAN_POINT('Ctrl Pts',(-243.957156919995,-4.01239519172672,
126.066635145309));
#200558=CARTESIAN_POINT('Ctrl Pts',(-244.235604543808,-6.15478022849689,
131.619245986169));
#200559=CARTESIAN_POINT('Ctrl Pts',(-244.514052167621,-2.64122291300849,
136.423016982646));
#200560=CARTESIAN_POINT('Ctrl Pts',(-244.792499791433,3.29948922862226,
136.063517266237));
#200561=CARTESIAN_POINT('Ctrl Pts',(-245.070947415247,6.20813195815889,
130.871109513785));
#200562=CARTESIAN_POINT('Ctrl Pts',(-245.349395039059,3.41180470225455,
125.617362786572));
#200563=CARTESIAN_POINT('Ctrl Pts',(-245.627842662872,-2.51980439909662,
125.13021366711));
#200564=CARTESIAN_POINT('Ctrl Pts',(-245.906290286685,-6.13583635696575,
129.857328397629));
#200565=CARTESIAN_POINT('Ctrl Pts',(-246.184737910498,-4.1133344550539,
135.454719473173));
#200566=CARTESIAN_POINT('Ctrl Pts',(-246.463185534311,1.68912086349306,
136.778657943074));
#200567=CARTESIAN_POINT('Ctrl Pts',(-246.741633158124,5.93935662663147,
132.612509031482));
#200568=CARTESIAN_POINT('Ctrl Pts',(-247.020080781937,4.73161380359756,
126.784760060463));
#200569=CARTESIAN_POINT('Ctrl Pts',(-247.29852840575,-0.824250952757648,
124.650827633015));
#200570=CARTESIAN_POINT('Ctrl Pts',(-247.576976029562,-5.62266935042617,
128.171691401572));
#200571=CARTESIAN_POINT('Ctrl Pts',(-247.855423653376,-5.25412929772145,
134.111849566585));
#200572=CARTESIAN_POINT('Ctrl Pts',(-248.133871277188,-0.0573010988966442,
137.012586967267));
#200573=CARTESIAN_POINT('Ctrl Pts',(-248.412318901001,5.19218401050035,
134.208267641291));
#200574=CARTESIAN_POINT('Ctrl Pts',(-248.690766524814,5.67030566653712,
128.275924050614));
#200575=CARTESIAN_POINT('Ctrl Pts',(-248.969214148627,0.937693424858449,
124.667090143972));
#200576=CARTESIAN_POINT('Ctrl Pts',(-249.24766177244,-4.65661326539506,
126.698107980232));
#200577=CARTESIAN_POINT('Ctrl Pts',(-249.526109396252,-5.97171985295489,
132.502571388608));
#200578=CARTESIAN_POINT('Ctrl Pts',(-249.804557020066,-1.79910763038337,
136.746462060605));
#200579=CARTESIAN_POINT('Ctrl Pts',(-250.083004643878,4.02679661321771,
135.52985179424));
#200580=CARTESIAN_POINT('Ctrl Pts',(-250.361452267692,6.15227148922063,
129.970745989595));
#200581=CARTESIAN_POINT('Ctrl Pts',(-250.639899891504,2.62410942180459,
125.177691303707));
#200582=CARTESIAN_POINT('Ctrl Pts',(-250.918347515317,-3.31548100938434,
125.555270839195));
#200583=CARTESIAN_POINT('Ctrl Pts',(-251.19679513913,-6.20830636318893,
130.756507448682));
#200584=CARTESIAN_POINT('Ctrl Pts',(-251.475242762943,-3.39600146187203,
136.001718782677));
#200585=CARTESIAN_POINT('Ctrl Pts',(-251.753690386756,2.53706287905323,
136.47081186788));
#200586=CARTESIAN_POINT('Ctrl Pts',(-252.032138010569,6.13869037645988,
131.732713075798));
#200587=CARTESIAN_POINT('Ctrl Pts',(-252.310585634382,4.09916130974965,
126.141503726722));
#200588=CARTESIAN_POINT('Ctrl Pts',(-252.589033258195,-1.70729674574642,
124.835232067896));
#200589=CARTESIAN_POINT('Ctrl Pts',(-252.867480882007,-5.94483249743877,
129.014297936587));
#200590=CARTESIAN_POINT('Ctrl Pts',(-253.14592850582,-4.71935760622846,
134.838343962485));
#200591=CARTESIAN_POINT('Ctrl Pts',(-253.424376129633,0.842976373616159,
136.955356360136));
#200592=CARTESIAN_POINT('Ctrl Pts',(-253.702823753446,5.63065624411703,
133.419904173236));
#200593=CARTESIAN_POINT('Ctrl Pts',(-253.981271377259,5.24403810606461,
127.480895216153));
#200594=CARTESIAN_POINT('Ctrl Pts',(-254.259719001072,0.0384051209378723,
124.595988638398));
#200595=CARTESIAN_POINT('Ctrl Pts',(-254.538166624885,-5.20252026939218,
127.416272546179));
#200596=CARTESIAN_POINT('Ctrl Pts',(-254.816614248698,-5.66258373611722,
133.350044001689));
#200597=CARTESIAN_POINT('Ctrl Pts',(-255.095061872511,-0.919009293725241,
136.944456550123));
#200598=CARTESIAN_POINT('Ctrl Pts',(-255.373509496324,4.6690896269236,134.896421351226));
#200599=CARTESIAN_POINT('Ctrl Pts',(-255.651957120136,5.96652359266914,
129.087981388513));
#200600=CARTESIAN_POINT('Ctrl Pts',(-255.93040474395,1.78101326373629,124.856811707331));
#200601=CARTESIAN_POINT('Ctrl Pts',(-256.208852367762,-4.04116012583712,
126.091145862189));
#200602=CARTESIAN_POINT('Ctrl Pts',(-256.487299991575,-6.14970689884083,
131.656699899059));
#200603=CARTESIAN_POINT('Ctrl Pts',(-256.765747615388,-2.60696946356087,
136.438984870644));
#200604=CARTESIAN_POINT('Ctrl Pts',(-257.044195239201,3.33143800190474,
136.043346010603));
#200605=CARTESIAN_POINT('Ctrl Pts',(-257.322642863014,6.2084309480058,130.833296634437));
#200606=CARTESIAN_POINT('Ctrl Pts',(-257.601090486826,3.38015223603414,
125.596729883064));
#200607=CARTESIAN_POINT('Ctrl Pts',(-257.87953811064,-2.5542704291637,125.145582755354));
#200608=CARTESIAN_POINT('Ctrl Pts',(-258.157985734452,-6.14153931545366,
129.894837769574));
#200609=CARTESIAN_POINT('Ctrl Pts',(-258.436433358265,-4.08485240479644,
135.479405634932));
#200610=CARTESIAN_POINT('Ctrl Pts',(-258.714880982078,1.72527217059264,
136.768768758555));
#200611=CARTESIAN_POINT('Ctrl Pts',(-258.993328605892,5.95060195420752,
132.575369498931));
#200612=CARTESIAN_POINT('Ctrl Pts',(-259.271776229703,4.70639920604184,
126.75783223591));
#200613=CARTESIAN_POINT('Ctrl Pts',(-259.550223853517,-0.860449444711704,
124.652528659269));
#200614=CARTESIAN_POINT('Ctrl Pts',(-259.82867147733,-5.64095031490746,
128.212697490595));
#200615=CARTESIAN_POINT('Ctrl Pts',(-260.060711163841,-5.29799179572588,
133.142936715762));
#200616=CARTESIAN_POINT('Ctrl Pts',(-260.246372125917,-2.62679689981868,
135.594171577488));
#200617=CARTESIAN_POINT('Ctrl Pts',(-260.339217213388,-0.889986900407246,
136.05080276614));
#200618=CARTESIAN_POINT('Ctrl Pts',(-260.385654363559,-0.0148419801173944,
136.053268468065));
#200619=CARTESIAN_POINT('Ctrl Pts',(209.997106195361,2.85369542052185,134.803838223542));
#200620=CARTESIAN_POINT('Ctrl Pts',(209.950688331758,3.52024512455777,134.328247120061));
#200621=CARTESIAN_POINT('Ctrl Pts',(209.857862530854,4.598911638141,133.039517383424));
#200622=CARTESIAN_POINT('Ctrl Pts',(209.672220855345,5.31158968331849,129.722011776094));
#200623=CARTESIAN_POINT('Ctrl Pts',(209.440181168834,2.90445768035623,125.771581499823));
#200624=CARTESIAN_POINT('Ctrl Pts',(209.161733545021,-2.67328939945229,
125.640965885288));
#200625=CARTESIAN_POINT('Ctrl Pts',(208.883285921209,-5.78445646322271,
130.262241799363));
#200626=CARTESIAN_POINT('Ctrl Pts',(208.604838297395,-3.58517659481558,
135.378114005881));
#200627=CARTESIAN_POINT('Ctrl Pts',(208.326390673583,1.91144119617671,136.292814641374));
#200628=CARTESIAN_POINT('Ctrl Pts',(208.04794304977,5.65009034124608,132.162897902674));
#200629=CARTESIAN_POINT('Ctrl Pts',(207.769495425957,4.19734896093999,126.785079177362));
#200630=CARTESIAN_POINT('Ctrl Pts',(207.491047802144,-1.1129569716493,125.100504449821));
#200631=CARTESIAN_POINT('Ctrl Pts',(207.212600178331,-5.4002948496084,128.657642803108));
#200632=CARTESIAN_POINT('Ctrl Pts',(206.934152554519,-4.72513942780656,
134.187431620732));
#200633=CARTESIAN_POINT('Ctrl Pts',(206.655704930705,0.292248586550605,
136.608384944684));
#200634=CARTESIAN_POINT('Ctrl Pts',(206.377257306892,5.04104249491135,133.695701483205));
#200635=CARTESIAN_POINT('Ctrl Pts',(206.09880968308,5.15738153042831,128.12602865207));
#200636=CARTESIAN_POINT('Ctrl Pts',(205.820362059267,0.534329935251406,
125.017605890956));
#200637=CARTESIAN_POINT('Ctrl Pts',(205.541914435454,-4.57974002364783,
127.226931288585));
#200638=CARTESIAN_POINT('Ctrl Pts',(205.263466811641,-5.48525514562618,
132.723737743954));
#200639=CARTESIAN_POINT('Ctrl Pts',(204.985019187828,-1.35008742798131,
136.456731302353));
#200640=CARTESIAN_POINT('Ctrl Pts',(204.706571564015,4.02574397595362,134.995471850294));
#200641=CARTESIAN_POINT('Ctrl Pts',(204.428123940202,5.70211370766606,129.682786179275));
#200642=CARTESIAN_POINT('Ctrl Pts',(204.149676316389,2.13851930815143,125.40077248911));
#200643=CARTESIAN_POINT('Ctrl Pts',(203.871228692576,-3.39026975841633,
126.084392381055));
#200644=CARTESIAN_POINT('Ctrl Pts',(203.592781068764,-5.8035665963141,131.105432460946));
#200645=CARTESIAN_POINT('Ctrl Pts',(203.314333444951,-2.88366922283368,
135.849802245147));
#200646=CARTESIAN_POINT('Ctrl Pts',(203.035885821138,2.68617927581077,135.957657646429));
#200647=CARTESIAN_POINT('Ctrl Pts',(202.757438197325,5.78756025537181,131.329884836407));
#200648=CARTESIAN_POINT('Ctrl Pts',(202.478990573512,3.57045609392238,126.219180939555));
#200649=CARTESIAN_POINT('Ctrl Pts',(202.200542949699,-1.92772278905516,
125.322033169903));
#200650=CARTESIAN_POINT('Ctrl Pts',(201.922095325886,-5.6544186046078,129.462876497226));
#200651=CARTESIAN_POINT('Ctrl Pts',(201.643647702073,-4.18497995558374,
134.836478196445));
#200652=CARTESIAN_POINT('Ctrl Pts',(201.36520007826,1.13025082464198,136.504760820331));
#200653=CARTESIAN_POINT('Ctrl Pts',(201.086752454448,5.4068363130258,132.934654138033));
#200654=CARTESIAN_POINT('Ctrl Pts',(200.808304830635,4.71480336828096,127.406911780982));
#200655=CARTESIAN_POINT('Ctrl Pts',(200.529857206822,-0.309903540913717,
125.001258930184));
#200656=CARTESIAN_POINT('Ctrl Pts',(200.251409583008,-5.04982423566531,
127.928373032793));
#200657=CARTESIAN_POINT('Ctrl Pts',(199.972961959197,-5.14920315545485,
133.498379226012));
#200658=CARTESIAN_POINT('Ctrl Pts',(199.694514335383,-0.516715927947778,
136.59271392819));
#200659=CARTESIAN_POINT('Ctrl Pts',(199.416066711571,4.59060799437092,134.367834714685));
#200660=CARTESIAN_POINT('Ctrl Pts',(199.137619087757,5.47938743352869,128.868296891315));
#200661=CARTESIAN_POINT('Ctrl Pts',(198.859171463945,1.33287750423228,125.147907050397));
#200662=CARTESIAN_POINT('Ctrl Pts',(198.580723840131,-4.03848173676817,
126.625521704588));
#200663=CARTESIAN_POINT('Ctrl Pts',(198.302276216319,-5.69867355247927,
131.943285172176));
#200664=CARTESIAN_POINT('Ctrl Pts',(198.023828592506,-2.12206276914206,
136.214432613634));
#200665=CARTESIAN_POINT('Ctrl Pts',(197.745380968693,3.4046200305072,135.513988187415));
#200666=CARTESIAN_POINT('Ctrl Pts',(197.46693334488,5.80262334705539,130.485626102603));
#200667=CARTESIAN_POINT('Ctrl Pts',(197.188485721067,2.86829928156946,125.750165465994));
#200668=CARTESIAN_POINT('Ctrl Pts',(196.910038097254,-2.70185169946893,
125.65926326252));
#200669=CARTESIAN_POINT('Ctrl Pts',(196.631590473441,-5.78913296148881,
130.296454176353));
#200670=CARTESIAN_POINT('Ctrl Pts',(196.353142849628,-3.5564838467683,135.400386297052));
#200671=CARTESIAN_POINT('Ctrl Pts',(196.074695225815,1.94440017923737,136.280795346639));
#200672=CARTESIAN_POINT('Ctrl Pts',(195.796247602003,5.6584754297534,132.128628418917));
#200673=CARTESIAN_POINT('Ctrl Pts',(195.51779997819,4.17268819221861,126.759524075833));
#200674=CARTESIAN_POINT('Ctrl Pts',(195.239352354377,-1.14759564681435,
125.107426913349));
#200675=CARTESIAN_POINT('Ctrl Pts',(194.960904730564,-5.41329514958902,
128.690533514357));
#200676=CARTESIAN_POINT('Ctrl Pts',(194.682457106751,-4.70444086406131,
134.216143957018));
#200677=CARTESIAN_POINT('Ctrl Pts',(194.404009482938,0.327564750825761,
136.606492185605));
#200678=CARTESIAN_POINT('Ctrl Pts',(194.125561859125,5.0585543621317,133.664964953048));
#200679=CARTESIAN_POINT('Ctrl Pts',(193.847114235312,5.14097963875765,128.094682084473));
#200680=CARTESIAN_POINT('Ctrl Pts',(193.568666611499,0.499095778182989,
125.014461412655));
#200681=CARTESIAN_POINT('Ctrl Pts',(193.290218987687,-4.60143272035756,
127.254875257849));
#200682=CARTESIAN_POINT('Ctrl Pts',(193.011771363874,-5.4734693413749,132.757092746623));
#200683=CARTESIAN_POINT('Ctrl Pts',(192.733323740061,-1.31565503151135,
136.464844805061));
#200684=CARTESIAN_POINT('Ctrl Pts',(192.454876116248,4.05118197898966,134.970888425217));
#200685=CARTESIAN_POINT('Ctrl Pts',(192.176428492435,5.69518066204141,129.648096536341));
#200686=CARTESIAN_POINT('Ctrl Pts',(191.897980868622,2.1055865417199,125.38785485147));
#200687=CARTESIAN_POINT('Ctrl Pts',(191.619533244809,-3.4189387468211,126.105117354624));
#200688=CARTESIAN_POINT('Ctrl Pts',(191.341085620997,-5.80162635147675,
131.140754845624));
#200689=CARTESIAN_POINT('Ctrl Pts',(191.062637997183,-2.85290276432908,
135.867262474811));
#200690=CARTESIAN_POINT('Ctrl Pts',(190.784190373371,2.71749909118881,135.941210633695));
#200691=CARTESIAN_POINT('Ctrl Pts',(190.505742749557,5.79065203911519,131.29464457683));
#200692=CARTESIAN_POINT('Ctrl Pts',(190.227295125745,3.54247865217362,126.197531513104));
#200693=CARTESIAN_POINT('Ctrl Pts',(189.948847501932,-1.96105955641241,
125.333869340265));
#200694=CARTESIAN_POINT('Ctrl Pts',(189.670399878119,-5.66247983574075,
129.497321402909));
#200695=CARTESIAN_POINT('Ctrl Pts',(189.391952254306,-4.160357773542,134.861878651407));
#200696=CARTESIAN_POINT('Ctrl Pts',(189.113504630493,1.16492983776554,136.497775047581));
#200697=CARTESIAN_POINT('Ctrl Pts',(188.83505700668,5.41970383815296,132.901701721328));
#200698=CARTESIAN_POINT('Ctrl Pts',(188.556609382867,4.69403477852959,127.378274381527));
#200699=CARTESIAN_POINT('Ctrl Pts',(188.278161759054,-0.345222926215044,
125.003252919028));
#200700=CARTESIAN_POINT('Ctrl Pts',(187.999714135242,-5.0672376268456,127.959166031618));
#200701=CARTESIAN_POINT('Ctrl Pts',(187.721266511429,-5.13270849672517,
133.529673973213));
#200702=CARTESIAN_POINT('Ctrl Pts',(187.442818887616,-0.48147100486422,
136.595752079925));
#200703=CARTESIAN_POINT('Ctrl Pts',(187.164371263803,4.61221481930072,134.339824357932));
#200704=CARTESIAN_POINT('Ctrl Pts',(186.88592363999,5.4675005437485,128.834978175547));
#200705=CARTESIAN_POINT('Ctrl Pts',(186.607476016177,1.29842037074208,125.139898247696));
#200706=CARTESIAN_POINT('Ctrl Pts',(186.329028392364,-4.06384469161484,
126.650182513385));
#200707=CARTESIAN_POINT('Ctrl Pts',(186.050580768551,-5.69163501222784,
131.977953513933));
#200708=CARTESIAN_POINT('Ctrl Pts',(185.772133144738,-2.08909080843167,
136.227249975919));
#200709=CARTESIAN_POINT('Ctrl Pts',(185.493685520926,3.4332257905535,135.493176040453));
#200710=CARTESIAN_POINT('Ctrl Pts',(185.215237897112,5.80057561042411,130.450309792719));
#200711=CARTESIAN_POINT('Ctrl Pts',(184.9367902733,2.83747981818726,125.732798956676));
#200712=CARTESIAN_POINT('Ctrl Pts',(184.658342649487,-2.73312130836828,
125.675805527429));
#200713=CARTESIAN_POINT('Ctrl Pts',(184.379895025674,-5.79211747293216,
130.331703682172));
#200714=CARTESIAN_POINT('Ctrl Pts',(184.101447401861,-3.52844064054064,
135.421950469967));
#200715=CARTESIAN_POINT('Ctrl Pts',(183.822999778048,1.97770076659953,136.26885776521));
#200716=CARTESIAN_POINT('Ctrl Pts',(183.544552154236,5.66643178528845,132.094159137294));
#200717=CARTESIAN_POINT('Ctrl Pts',(183.266104530422,4.14798881387936,126.734198679909));
#200718=CARTESIAN_POINT('Ctrl Pts',(182.98765690661,-1.18225323696583,125.114518204765));
#200719=CARTESIAN_POINT('Ctrl Pts',(182.709209282797,-5.42606231932092,
128.72352494273));
#200720=CARTESIAN_POINT('Ctrl Pts',(182.430761658984,-4.68358520810093,
134.244718011395));
#200721=CARTESIAN_POINT('Ctrl Pts',(182.152314035171,0.362877903506298,
136.604390705933));
#200722=CARTESIAN_POINT('Ctrl Pts',(181.873866411358,5.07587394936235,133.634119096483));
#200723=CARTESIAN_POINT('Ctrl Pts',(181.595418787545,5.12438980598236,128.063437686296));
#200724=CARTESIAN_POINT('Ctrl Pts',(181.316971163732,0.463841771263853,
125.011530548415));
#200725=CARTESIAN_POINT('Ctrl Pts',(181.038523539919,-4.62295419131585,
127.282951248603));
#200726=CARTESIAN_POINT('Ctrl Pts',(180.760075916106,-5.46148109594396,
132.790375128456));
#200727=CARTESIAN_POINT('Ctrl Pts',(180.481628292294,-1.2811736815839,136.472748695004));
#200728=CARTESIAN_POINT('Ctrl Pts',(180.203180668481,4.07646975733793,134.946150534538));
#200729=CARTESIAN_POINT('Ctrl Pts',(179.924733044668,5.68803663588505,129.61344977806));
#200730=CARTESIAN_POINT('Ctrl Pts',(179.646285420855,2.07257572209157,125.37513790386));
#200731=CARTESIAN_POINT('Ctrl Pts',(179.367837797042,-3.44748102935117,
126.12601647128));
#200732=CARTESIAN_POINT('Ctrl Pts',(179.089390173229,-5.79947113363144,
131.176064759319));
#200733=CARTESIAN_POINT('Ctrl Pts',(178.810942549416,-2.82203058602,135.884535099843));
#200734=CARTESIAN_POINT('Ctrl Pts',(178.532494925603,2.74871820628535,135.924573271475));
#200735=CARTESIAN_POINT('Ctrl Pts',(178.254047301791,5.79352924936408,131.259386150458));
#200736=CARTESIAN_POINT('Ctrl Pts',(177.975599677977,3.51436994191561,126.176052793945));
#200737=CARTESIAN_POINT('Ctrl Pts',(177.697152054165,-1.99432365563702,
125.345908221933));
#200738=CARTESIAN_POINT('Ctrl Pts',(177.418704430351,-5.6703312417861,129.531814741282));
#200739=CARTESIAN_POINT('Ctrl Pts',(177.140256806539,-4.135581427815,134.887128753614));
#200740=CARTESIAN_POINT('Ctrl Pts',(176.861809182726,1.19956568393359,136.490578303229));
#200741=CARTESIAN_POINT('Ctrl Pts',(176.583361558913,5.43237053418876,132.868671586896));
#200742=CARTESIAN_POINT('Ctrl Pts',(176.3049139351,4.67309224957875,127.349763936946));
#200743=CARTESIAN_POINT('Ctrl Pts',(176.026466311287,-0.380529519146142,
125.005461870054));
#200744=CARTESIAN_POINT('Ctrl Pts',(175.748018687475,-5.08446324967622,
127.990064460173));
#200745=CARTESIAN_POINT('Ctrl Pts',(175.469571063661,-5.11602364359241,
133.560867732924));
#200746=CARTESIAN_POINT('Ctrl Pts',(175.191123439849,-0.446208240696769,
136.59857562952));
#200747=CARTESIAN_POINT('Ctrl Pts',(174.912675816035,4.63365073691483,134.311682993269));
#200748=CARTESIAN_POINT('Ctrl Pts',(174.634228192223,5.45541105372469,128.801732435971));
#200749=CARTESIAN_POINT('Ctrl Pts',(174.35578056841,1.26391512380778,125.132099343732));
#200750=CARTESIAN_POINT('Ctrl Pts',(174.077332944597,-4.089057059202,126.674997256779));
#200751=CARTESIAN_POINT('Ctrl Pts',(173.798885320784,-5.68438556634791,
132.012578367773));
#200752=CARTESIAN_POINT('Ctrl Pts',(173.520437696972,-2.0560414356932,136.239866391045));
#200753=CARTESIAN_POINT('Ctrl Pts',(173.241990073158,3.46170433115548,135.472190147709));
#200754=CARTESIAN_POINT('Ctrl Pts',(172.963542449346,5.79831293133042,130.41500660232));
#200755=CARTESIAN_POINT('Ctrl Pts',(172.685094825533,2.80655521094699,125.715620375941));
#200756=CARTESIAN_POINT('Ctrl Pts',(172.40664720172,-2.76428964045241,125.692537832834));
#200757=CARTESIAN_POINT('Ctrl Pts',(172.128199577907,-5.79488735533246,
130.366970702468));
#200758=CARTESIAN_POINT('Ctrl Pts',(171.849751954094,-3.50026668664755,
135.443343536393));
#200759=CARTESIAN_POINT('Ctrl Pts',(171.571304330281,2.01092806953244,136.256717694829));
#200760=CARTESIAN_POINT('Ctrl Pts',(171.292856706468,5.6741781691098,132.059642061713));
#200761=CARTESIAN_POINT('Ctrl Pts',(171.014409082656,4.12313573028927,126.709024105332));
#200762=CARTESIAN_POINT('Ctrl Pts',(170.735961458842,-1.21686701828875,
125.121820335384));
#200763=CARTESIAN_POINT('Ctrl Pts',(170.45751383503,-5.43862842431808,128.756593477234));
#200764=CARTESIAN_POINT('Ctrl Pts',(170.179066211217,-4.66255600016836,
134.273164582064));
#200765=CARTESIAN_POINT('Ctrl Pts',(169.900618587404,0.398177609612544,
136.602074304013));
#200766=CARTESIAN_POINT('Ctrl Pts',(169.62217096359,5.09300544821711,133.603168382178));
#200767=CARTESIAN_POINT('Ctrl Pts',(169.343723339778,5.10761008705837,128.032294854024));
#200768=CARTESIAN_POINT('Ctrl Pts',(169.065275715965,0.428570576517446,
125.008814339624));
#200769=CARTESIAN_POINT('Ctrl Pts',(168.786828092152,-4.64430435700642,
127.311157726477));
#200770=CARTESIAN_POINT('Ctrl Pts',(168.508380468339,-5.4492904733226,132.823583917792));
#200771=CARTESIAN_POINT('Ctrl Pts',(168.229932844526,-1.24664485729461,
136.480442540741));
#200772=CARTESIAN_POINT('Ctrl Pts',(167.951485220714,4.10160648060013,134.92125916831));
#200773=CARTESIAN_POINT('Ctrl Pts',(167.673037596901,5.6806818374394,129.578847149419));
#200774=CARTESIAN_POINT('Ctrl Pts',(167.394589973088,2.03948810240773,125.362622138095));
#200775=CARTESIAN_POINT('Ctrl Pts',(167.116142349275,-3.47589556420378,
126.147088945699));
#200776=CARTESIAN_POINT('Ctrl Pts',(166.837694725462,-5.79710101425052,
131.21136089938));
#200777=CARTESIAN_POINT('Ctrl Pts',(166.559247101649,-2.79105383632985,
135.901619477142));
#200778=CARTESIAN_POINT('Ctrl Pts',(166.280799477836,2.77983546661788,135.907746177893));
#200779=CARTESIAN_POINT('Ctrl Pts',(166.002351854023,5.79619177825601,131.224110862948));
#200780=CARTESIAN_POINT('Ctrl Pts',(165.72390423021,3.48613100538707,126.154745578436));
#200781=CARTESIAN_POINT('Ctrl Pts',(165.445456606397,-2.02751385446508,
125.358149368562));
#200782=CARTESIAN_POINT('Ctrl Pts',(165.167008982585,-5.67797253162207,
129.566355234311));
#200783=CARTESIAN_POINT('Ctrl Pts',(164.888561358772,-4.11065183659732,
134.912227567346));
#200784=CARTESIAN_POINT('Ctrl Pts',(164.610113734959,1.23415707975413,136.483170853989));
#200785=CARTESIAN_POINT('Ctrl Pts',(164.331666111146,5.44483593173667,132.835564958663));
#200786=CARTESIAN_POINT('Ctrl Pts',(164.053218487333,4.65197655747607,127.321381503715));
#200787=CARTESIAN_POINT('Ctrl Pts',(163.77477086352,-0.415822011415935,
125.007885701408));
#200788=CARTESIAN_POINT('Ctrl Pts',(163.496323239708,-5.10150046585131,
128.021067173507));
#200789=CARTESIAN_POINT('Ctrl Pts',(163.217875615894,-5.09914921432216,
133.591959349252));
#200790=CARTESIAN_POINT('Ctrl Pts',(162.939427992082,-0.41092894211879,
136.601184472346));
#200791=CARTESIAN_POINT('Ctrl Pts',(162.660980368268,4.65491495289691,134.283411663486));
#200792=CARTESIAN_POINT('Ctrl Pts',(162.382532744456,5.443119411438,128.768560904517));
#200793=CARTESIAN_POINT('Ctrl Pts',(162.104085120643,1.22936304203373,125.124510627495));
#200794=CARTESIAN_POINT('Ctrl Pts',(161.82563749683,-4.11411790527609,126.69996501525));
#200795=CARTESIAN_POINT('Ctrl Pts',(161.547189873017,-5.67692548347038,
132.04715845066));
#200796=CARTESIAN_POINT('Ctrl Pts',(161.268742249204,-2.02291587558315,
136.252281391507));
#200797=CARTESIAN_POINT('Ctrl Pts',(160.990294625391,3.49005459703047,135.451031286826));
#200798=CARTESIAN_POINT('Ctrl Pts',(160.711847001578,5.79583539361873,130.379717839577));
#200799=CARTESIAN_POINT('Ctrl Pts',(160.433399377766,2.77552660577121,125.698630360346));
#200800=CARTESIAN_POINT('Ctrl Pts',(160.154951753952,-2.79535554076737,
125.70945955871));
#200801=CARTESIAN_POINT('Ctrl Pts',(159.87650413014,-5.79744250605075,130.402253930408));
#200802=CARTESIAN_POINT('Ctrl Pts',(159.598056506327,-3.47196302908515,
135.4645647036));
#200803=CARTESIAN_POINT('Ctrl Pts',(159.319608882514,2.04408085678626,136.244375585352));
#200804=CARTESIAN_POINT('Ctrl Pts',(159.041161258701,5.68171429417248,132.025078471215));
#200805=CARTESIAN_POINT('Ctrl Pts',(158.762713634888,4.09812986238831,126.684001284956));
#200806=CARTESIAN_POINT('Ctrl Pts',(158.484266011075,-1.25143570815684,
125.129333034622));
#200807=CARTESIAN_POINT('Ctrl Pts',(158.205818387262,-5.450992998939,128.789737892503));
#200808=CARTESIAN_POINT('Ctrl Pts',(157.927370763449,-4.64135401950845,
134.301482614925));
#200809=CARTESIAN_POINT('Ctrl Pts',(157.648923139637,0.43346256110109,136.59954306568));
#200810=CARTESIAN_POINT('Ctrl Pts',(157.370475515823,5.10994822388206,133.572113957021));
#200811=CARTESIAN_POINT('Ctrl Pts',(157.092027892011,5.09064110376424,128.001254741669));
#200812=CARTESIAN_POINT('Ctrl Pts',(156.813580268198,0.39328350093061,125.006312886931));
#200813=CARTESIAN_POINT('Ctrl Pts',(156.535132644385,-4.66548242629113,
127.339493646268));
#200814=CARTESIAN_POINT('Ctrl Pts',(156.256685020572,-5.43689792523874,
132.856717884066));
#200815=CARTESIAN_POINT('Ctrl Pts',(155.978237396759,-1.21206983812162,
136.487926057176));
#200816=CARTESIAN_POINT('Ctrl Pts',(155.699789772946,4.12659121732586,134.896215248893));
#200817=CARTESIAN_POINT('Ctrl Pts',(155.421342149133,5.67311653923917,129.544289932631));
#200818=CARTESIAN_POINT('Ctrl Pts',(155.142894525321,2.0063249087422,125.350308017949));
#200819=CARTESIAN_POINT('Ctrl Pts',(154.864446901507,-3.50418129846815,
126.168333997033));
#200820=CARTESIAN_POINT('Ctrl Pts',(154.585999277695,-5.79451608115961,
131.246641957895));
#200821=CARTESIAN_POINT('Ctrl Pts',(154.307551653882,-2.75997366311328,
135.918514973638));
#200822=CARTESIAN_POINT('Ctrl Pts',(154.029104030069,2.81084971912495,135.890729976482));
#200823=CARTESIAN_POINT('Ctrl Pts',(153.750656406256,5.79863952713012,131.188820021437));
#200824=CARTESIAN_POINT('Ctrl Pts',(153.472208782443,3.457762888992,126.133610656121));
#200825=CARTESIAN_POINT('Ctrl Pts',(153.19376115863,-2.0606289230217,125.370592326552));
#200826=CARTESIAN_POINT('Ctrl Pts',(152.915313534817,-5.68540342209783,
129.600941602086));
#200827=CARTESIAN_POINT('Ctrl Pts',(152.636865911004,-4.08556992366409,
134.937174162558));
#200828=CARTESIAN_POINT('Ctrl Pts',(152.358418287191,1.26870274343019,136.475552974349));
#200829=CARTESIAN_POINT('Ctrl Pts',(152.079970663379,5.45709956888678,132.802383063404));
#200830=CARTESIAN_POINT('Ctrl Pts',(151.801523039566,4.63068848467127,127.293128133558));
#200831=CARTESIAN_POINT('Ctrl Pts',(151.523075415753,-0.451099095248245,
125.010524323271));
#200832=CARTESIAN_POINT('Ctrl Pts',(151.24462779194,-5.11834864405056,128.052173022803));
#200833=CARTESIAN_POINT('Ctrl Pts',(150.966180168127,-5.08208583420252,
133.622947670083));
#200834=CARTESIAN_POINT('Ctrl Pts',(150.687732544314,-0.375634416417742,
136.603578511732));
#200835=CARTESIAN_POINT('Ctrl Pts',(150.409284920501,4.67600667929353,134.255011416186));
#200836=CARTESIAN_POINT('Ctrl Pts',(150.130837296688,5.43062607235983,128.735464810371));
#200837=CARTESIAN_POINT('Ctrl Pts',(149.852389672876,1.19476540576009,125.117132380189));
#200838=CARTESIAN_POINT('Ctrl Pts',(149.573942049063,-4.13902630119825,
126.725084863609));
#200839=CARTESIAN_POINT('Ctrl Pts',(149.29549442525,-5.66925504003138,132.081692481218));
#200840=CARTESIAN_POINT('Ctrl Pts',(149.017046801437,-1.98971535558138,
136.264494517259));
#200841=CARTESIAN_POINT('Ctrl Pts',(148.738599177624,3.5182755376489,135.429700241853));
#200842=CARTESIAN_POINT('Ctrl Pts',(148.460151553811,5.79314308909515,130.344444812129));
#200843=CARTESIAN_POINT('Ctrl Pts',(148.181703929998,2.74439515243632,125.681829539465));
#200844=CARTESIAN_POINT('Ctrl Pts',(147.903256306185,-2.82631785815477,
125.726570078021));
#200845=CARTESIAN_POINT('Ctrl Pts',(147.624808682372,-5.79978283040501,
130.437552058559));
#200846=CARTESIAN_POINT('Ctrl Pts',(147.346361058559,-3.4435307166558,135.48561318523));
#200847=CARTESIAN_POINT('Ctrl Pts',(147.067913434747,2.07715789987228,136.23183189412));
#200848=CARTESIAN_POINT('Ctrl Pts',(146.789465810933,5.68903988122249,131.990469646568));
#200849=CARTESIAN_POINT('Ctrl Pts',(146.511018187121,4.07297213677825,126.65913114601));
#200850=CARTESIAN_POINT('Ctrl Pts',(146.232570563308,-1.2859580256146,125.137056024094));
#200851=CARTESIAN_POINT('Ctrl Pts',(145.954122939495,-5.46315558500969,
128.822956960357));
#200852=CARTESIAN_POINT('Ctrl Pts',(145.675675315682,-4.61998005176852,
134.329671060644));
#200853=CARTESIAN_POINT('Ctrl Pts',(145.397227691869,0.468731450475054,
136.596797084732));
#200854=CARTESIAN_POINT('Ctrl Pts',(145.118780068056,5.12670164853643,133.540956971746));
#200855=CARTESIAN_POINT('Ctrl Pts',(144.840332444244,5.07348348489189,127.970318499433));
#200856=CARTESIAN_POINT('Ctrl Pts',(144.56188482043,0.357981852079004,125.004026283029));
#200857=CARTESIAN_POINT('Ctrl Pts',(144.283437196618,-4.6864876144088,127.367957957979));
#200858=CARTESIAN_POINT('Ctrl Pts',(144.004989572805,-5.42430391090288,
132.889775799486));
#200859=CARTESIAN_POINT('Ctrl Pts',(143.726541948992,-1.17744990525502,
136.495198967004));
#200860=CARTESIAN_POINT('Ctrl Pts',(143.448094325179,4.15142304169647,134.871019704297));
#200861=CARTESIAN_POINT('Ctrl Pts',(143.169646701366,5.66534102161933,129.509779408224));
#200862=CARTESIAN_POINT('Ctrl Pts',(142.891199077553,1.9730873699693,125.338195999729));
#200863=CARTESIAN_POINT('Ctrl Pts',(142.61275145374,-3.53233718400576,126.189750838038));
#200864=CARTESIAN_POINT('Ctrl Pts',(142.334303829928,-5.79171643014443,
131.281906627513));
#200865=CARTESIAN_POINT('Ctrl Pts',(142.055856206114,-2.72879121805762,
135.935220963265));
#200866=CARTESIAN_POINT('Ctrl Pts',(141.777408582302,2.84175981456215,135.873525297782));
#200867=CARTESIAN_POINT('Ctrl Pts',(141.498960958489,5.80087240528401,131.153514933643));
#200868=CARTESIAN_POINT('Ctrl Pts',(141.220513334676,3.42926664392146,126.112648810165));
#200869=CARTESIAN_POINT('Ctrl Pts',(140.942065710863,-2.09366763421581,
125.383236634823));
#200870=CARTESIAN_POINT('Ctrl Pts',(140.66361808705,-5.69262363785895,129.635572562993));
#200871=CARTESIAN_POINT('Ctrl Pts',(140.385170463237,-4.06033661843482,
134.961967614844));
#200872=CARTESIAN_POINT('Ctrl Pts',(140.106722839424,1.30320139485961,136.467724946589));
#200873=CARTESIAN_POINT('Ctrl Pts',(139.828275215611,5.46916099120554,132.769127130691));
#200874=CARTESIAN_POINT('Ctrl Pts',(139.549827591798,4.60922882000175,127.26500487341));
#200875=CARTESIAN_POINT('Ctrl Pts',(139.271379967986,-0.486359463437733,
125.013377637868));
#200876=CARTESIAN_POINT('Ctrl Pts',(138.992932344173,-5.13500715995863,
128.083380855422));
#200877=CARTESIAN_POINT('Ctrl Pts',(138.71448472036,-5.06483413552331,133.653831547135));
#200878=CARTESIAN_POINT('Ctrl Pts',(138.436037096547,-0.340325971445257,
136.605757658967));
#200879=CARTESIAN_POINT('Ctrl Pts',(138.157589472734,4.69692513454305,134.226483303753));
#200880=CARTESIAN_POINT('Ctrl Pts',(137.879141848921,5.41793149943546,128.70244537992));
#200881=CARTESIAN_POINT('Ctrl Pts',(137.600694225109,1.16012349701482,125.109964875215));
#200882=CARTESIAN_POINT('Ctrl Pts',(137.322246601295,-4.16378132397874,
126.750355871033));
#200883=CARTESIAN_POINT('Ctrl Pts',(137.043798977483,-5.66137452026194,
132.116179179772));
#200884=CARTESIAN_POINT('Ctrl Pts',(136.765351353669,-1.95644110594549,
136.276505315742));
#200885=CARTESIAN_POINT('Ctrl Pts',(136.486903729857,3.54636610727348,135.408197803219));
#200886=CARTESIAN_POINT('Ctrl Pts',(136.208456106044,5.79023611752392,130.309188827029));
#200887=CARTESIAN_POINT('Ctrl Pts',(135.930008482231,2.71316200452982,125.665218535856));
#200888=CARTESIAN_POINT('Ctrl Pts',(135.651560858418,-2.85717544529452,
125.743868756725));
#200889=CARTESIAN_POINT('Ctrl Pts',(135.373113234605,-5.80190824167357,
130.472863778936));
#200890=CARTESIAN_POINT('Ctrl Pts',(135.094665610792,-3.41497080292952,
135.506488201326));
#200891=CARTESIAN_POINT('Ctrl Pts',(134.816217986979,2.11015797310843,136.219087085943));
#200892=CARTESIAN_POINT('Ctrl Pts',(134.537770363167,5.69615465880763,131.955816870215));
#200893=CARTESIAN_POINT('Ctrl Pts',(134.259322739353,4.04766348568775,126.634414610068));
#200894=CARTESIAN_POINT('Ctrl Pts',(133.980875115541,-1.32043269142476,
125.144989017623));
#200895=CARTESIAN_POINT('Ctrl Pts',(133.702427491728,-5.47511573184112,
128.856249449853));
#200896=CARTESIAN_POINT('Ctrl Pts',(133.423979867915,-4.59843488896879,
134.357728874689));
#200897=CARTESIAN_POINT('Ctrl Pts',(133.145532244102,0.503982970832797,
136.59383646292));
#200898=CARTESIAN_POINT('Ctrl Pts',(132.867084620289,5.14326510137581,133.509698580887));
#200899=CARTESIAN_POINT('Ctrl Pts',(132.588636996476,5.05613786622328,127.93948727367));
#200900=CARTESIAN_POINT('Ctrl Pts',(132.310189372663,0.322666938078297,
125.001954612649));
#200901=CARTESIAN_POINT('Ctrl Pts',(132.03174174885,-4.70731914300451,127.396549606854));
#200902=CARTESIAN_POINT('Ctrl Pts',(131.753294125038,-5.41150889699075,
132.92275643908));
#200903=CARTESIAN_POINT('Ctrl Pts',(131.474846501225,-1.14278634154918,
136.502261000723));
#200904=CARTESIAN_POINT('Ctrl Pts',(131.196398877412,4.17610103355955,134.845673468154));
#200905=CARTESIAN_POINT('Ctrl Pts',(130.917951253599,5.65735557270449,129.475316855001));
#200906=CARTESIAN_POINT('Ctrl Pts',(130.639503629786,1.93977671771839,125.326286532249));
#200907=CARTESIAN_POINT('Ctrl Pts',(130.361056005973,-3.56036217749005,
126.211338675105));
#200908=CARTESIAN_POINT('Ctrl Pts',(130.08260838216,-5.788702164947,131.317153601487));
#200909=CARTESIAN_POINT('Ctrl Pts',(129.804160758347,-2.69750765663984,
135.951736826975));
#200910=CARTESIAN_POINT('Ctrl Pts',(129.525713134534,2.87256460754407,135.856132779323));
#200911=CARTESIAN_POINT('Ctrl Pts',(129.247265510721,5.80289032997773,131.118196907806));
#200912=CARTESIAN_POINT('Ctrl Pts',(128.968817886909,3.40064332611445,126.091860817314));
#200913=CARTESIAN_POINT('Ctrl Pts',(128.690370263096,-2.12662876378584,
125.396081824838));
#200914=CARTESIAN_POINT('Ctrl Pts',(128.411922639283,-5.69963291135762,
129.670246833772));
#200915=CARTESIAN_POINT('Ctrl Pts',(128.13347501547,-4.03495285593914,134.986607005474));
#200916=CARTESIAN_POINT('Ctrl Pts',(127.855027391657,1.33765175568188,136.459687060782));
#200917=CARTESIAN_POINT('Ctrl Pts',(127.576579767844,5.48101975175251,132.73579839283));
#200918=CARTESIAN_POINT('Ctrl Pts',(127.298132144031,4.5875983586632,127.237012765392));
#200919=CARTESIAN_POINT('Ctrl Pts',(127.019684520218,-0.521601809398458,
125.016445539469));
#200920=CARTESIAN_POINT('Ctrl Pts',(126.741236896406,-5.15147539628782,
128.114689514947));
#200921=CARTESIAN_POINT('Ctrl Pts',(126.462789272592,-5.0473947575527,133.684609835992));
#200922=CARTESIAN_POINT('Ctrl Pts',(126.18434164878,-0.305004915568794,
136.607721833301));
#200923=CARTESIAN_POINT('Ctrl Pts',(125.905894024967,4.71766954350447,134.197828383304));
#200924=CARTESIAN_POINT('Ctrl Pts',(125.627446401154,5.40503616306688,128.669503836711));
#200925=CARTESIAN_POINT('Ctrl Pts',(125.348998777341,1.12543859946687,125.10300837817));
#200926=CARTESIAN_POINT('Ctrl Pts',(125.070551153528,-4.18838205631096,
126.775777101093));
#200927=CARTESIAN_POINT('Ctrl Pts',(124.792103529715,-5.65328421617778,
132.150617268407));
#200928=CARTESIAN_POINT('Ctrl Pts',(124.513655905902,-1.9230943596648,136.288313341892));
#200929=CARTESIAN_POINT('Ctrl Pts',(124.23520828209,3.57432526499779,135.386524767704));
#200930=CARTESIAN_POINT('Ctrl Pts',(123.956760658277,5.78711458662396,130.273951190703));
#200931=CARTESIAN_POINT('Ctrl Pts',(123.678313034464,2.68182831940755,125.648797965047));
#200932=CARTESIAN_POINT('Ctrl Pts',(123.399865410651,-2.88792715874745,
125.761354953818));
#200933=CARTESIAN_POINT('Ctrl Pts',(123.121417786838,-5.8038186610986,130.50818778305));
#200934=CARTESIAN_POINT('Ctrl Pts',(122.842970163025,-3.38628434620416,
135.527188978355));
#200935=CARTESIAN_POINT('Ctrl Pts',(122.564522539212,2.1430798536649,136.206141633086));
#200936=CARTESIAN_POINT('Ctrl Pts',(122.286074915399,5.703058363287,131.921121426228));
#200937=CARTESIAN_POINT('Ctrl Pts',(122.007627291586,4.02220484693838,126.609852593007));
#200938=CARTESIAN_POINT('Ctrl Pts',(121.729179667773,-1.35485842811595,
125.153131721247));
#200939=CARTESIAN_POINT('Ctrl Pts',(121.450732043961,-5.48687299624567,
128.889614127324));
#200940=CARTESIAN_POINT('Ctrl Pts',(121.172284420148,-4.57671932947311,
134.385655017367));
#200941=CARTESIAN_POINT('Ctrl Pts',(120.893836796335,0.539215815916097,
136.59066130995));
#200942=CARTESIAN_POINT('Ctrl Pts',(120.615389172522,5.15963796863542,133.478339942736));
#200943=CARTESIAN_POINT('Ctrl Pts',(120.336941548709,5.0386048905067,127.908762206842));
#200944=CARTESIAN_POINT('Ctrl Pts',(120.058493924896,0.287340067535411,
125.000097952557));
#200945=CARTESIAN_POINT('Ctrl Pts',(119.780046301083,-4.72797624015824,
127.42526753342));
#200946=CARTESIAN_POINT('Ctrl Pts',(119.50159867727,-5.39851335762638,132.955658580739));
#200947=CARTESIAN_POINT('Ctrl Pts',(119.223151053457,-1.10808043147514,
136.509111896649));
#200948=CARTESIAN_POINT('Ctrl Pts',(118.944703429644,4.20062427846316,134.820177479675));
#200949=CARTESIAN_POINT('Ctrl Pts',(118.666255805832,5.64916048839838,129.440903549983));
#200950=CARTESIAN_POINT('Ctrl Pts',(118.387808182019,1.90639418632776,125.314580056818));
#200951=CARTESIAN_POINT('Ctrl Pts',(118.109360558206,-3.58825524044456,
126.23309670829));
#200952=CARTESIAN_POINT('Ctrl Pts',(117.830912934393,-5.785473397262,131.352381573729));
#200953=CARTESIAN_POINT('Ctrl Pts',(117.55246531058,-2.66612413808396,135.968061952766));
#200954=CARTESIAN_POINT('Ctrl Pts',(117.274017686767,2.9032629565882,135.838553065588));
#200955=CARTESIAN_POINT('Ctrl Pts',(116.995570062954,5.80469322643624,131.082867252651));
#200956=CARTESIAN_POINT('Ctrl Pts',(116.717122439142,3.37189399621826,126.071247447876));
#200957=CARTESIAN_POINT('Ctrl Pts',(116.438674815328,-2.15951109034483,
125.409127420613));
#200958=CARTESIAN_POINT('Ctrl Pts',(116.160227191516,-5.70643098286277,
129.704963129555));
#200959=CARTESIAN_POINT('Ctrl Pts',(115.881779567703,-4.00941957678149,
135.011091421425));
#200960=CARTESIAN_POINT('Ctrl Pts',(115.60333194389,1.37205254932662,136.451439614773));
#200961=CARTESIAN_POINT('Ctrl Pts',(115.324884320077,5.49267541109693,132.702398084833));
#200962=CARTESIAN_POINT('Ctrl Pts',(115.046436696264,4.56579790218037,127.20915284676));
#200963=CARTESIAN_POINT('Ctrl Pts',(114.767989072451,-0.556824827212187,
125.019727914392));
#200964=CARTESIAN_POINT('Ctrl Pts',(114.489541448638,-5.1677527428018,128.146097841224));
#200965=CARTESIAN_POINT('Ctrl Pts',(114.211093824825,-5.02976834651319,
133.715281396157));
#200966=CARTESIAN_POINT('Ctrl Pts',(113.932646201012,-0.269672557622912,
136.60947096195));
#200967=CARTESIAN_POINT('Ctrl Pts',(113.6541985772,4.73823913748602,134.169047716661));
#200968=CARTESIAN_POINT('Ctrl Pts',(113.375750953387,5.39194054109557,128.636641401405));
#200969=CARTESIAN_POINT('Ctrl Pts',(113.097303329574,1.09071199837779,125.09626314683));
#200970=CARTESIAN_POINT('Ctrl Pts',(112.818855705761,-4.21282758660586,
126.801347611796));
#200971=CARTESIAN_POINT('Ctrl Pts',(112.540408081948,-5.64498442756793,
132.185005471008));
#200972=CARTESIAN_POINT('Ctrl Pts',(112.261960458135,-1.8896763524154,136.299918158156));
#200973=CARTESIAN_POINT('Ctrl Pts',(111.983512834322,3.60215197478495,135.364681938413));
#200974=CARTESIAN_POINT('Ctrl Pts',(111.705065210509,5.78377861206482,130.238733208892));
#200975=CARTESIAN_POINT('Ctrl Pts',(111.426617586696,2.65039525815055,125.632568435507));
#200976=CARTESIAN_POINT('Ctrl Pts',(111.148169962883,-2.91857185899754,
125.77902802134));
#200977=CARTESIAN_POINT('Ctrl Pts',(110.869722339071,-5.80551401788879,
130.543522761958));
#200978=CARTESIAN_POINT('Ctrl Pts',(110.591274715258,-3.35747240946702,
135.547714749242));
#200979=CARTESIAN_POINT('Ctrl Pts',(110.312827091445,2.17592232160915,136.192996015246));
#200980=CARTESIAN_POINT('Ctrl Pts',(110.034379467632,5.70975073884148,131.886384600257));
#200981=CARTESIAN_POINT('Ctrl Pts',(109.755931843819,3.99659716390926,126.585446004984));
#200982=CARTESIAN_POINT('Ctrl Pts',(109.477484220006,-1.38923396002991,
125.161483833236));
#200983=CARTESIAN_POINT('Ctrl Pts',(109.199036596193,-5.49842694255352,
128.923049756431));
#200984=CARTESIAN_POINT('Ctrl Pts',(108.92058897238,-4.55483417795961,134.413448453863));
#200985=CARTESIAN_POINT('Ctrl Pts',(108.642141348568,0.57442868015902,136.58727174348));
#200986=CARTESIAN_POINT('Ctrl Pts',(108.363693724754,5.17581964361271,133.446882219296));
#200987=CARTESIAN_POINT('Ctrl Pts',(108.085246100942,5.02088520743284,127.878144437479));
#200988=CARTESIAN_POINT('Ctrl Pts',(107.806798477129,0.252002549500665,
124.998456371553));
#200989=CARTESIAN_POINT('Ctrl Pts',(107.528350853316,-4.74845814041369,
127.454110673523));
#200990=CARTESIAN_POINT('Ctrl Pts',(107.249903229503,-5.38531777436419,
132.988481005259));
#200991=CARTESIAN_POINT('Ctrl Pts',(106.97145560569,-1.07333346107335,136.515751400918));
#200992=CARTESIAN_POINT('Ctrl Pts',(106.693007981877,4.22499186768932,134.794532683627));
#200993=CARTESIAN_POINT('Ctrl Pts',(106.414560358064,5.64075607237289,129.406540768369));
#200994=CARTESIAN_POINT('Ctrl Pts',(106.136112734251,1.87294101279944,125.303077007226));
#200995=CARTESIAN_POINT('Ctrl Pts',(105.857665110439,-3.61601533928142,
126.25502413134));
#200996=CARTESIAN_POINT('Ctrl Pts',(105.579217486626,-5.78203024673271,
131.387589238853));
#200997=CARTESIAN_POINT('Ctrl Pts',(105.300769862813,-2.63464182531766,
135.984195735705));
#200998=CARTESIAN_POINT('Ctrl Pts',(105.022322239,2.93385372415587,135.820786808));
#200999=CARTESIAN_POINT('Ctrl Pts',(104.743874615187,5.80628102785255,131.047527277329));
#201000=CARTESIAN_POINT('Ctrl Pts',(104.465426991374,3.34301971955009,126.050809465687));
#201001=CARTESIAN_POINT('Ctrl Pts',(104.186979367561,-2.19231339542621,
125.422372938737));
#201002=CARTESIAN_POINT('Ctrl Pts',(103.908531743748,-5.71301760046937,
129.739720163916));
#201003=CARTESIAN_POINT('Ctrl Pts',(103.630084119935,-3.98373772710686,
135.03541995542));
#201004=CARTESIAN_POINT('Ctrl Pts',(103.351636496123,1.40640250105958,136.442982914176));
#201005=CARTESIAN_POINT('Ctrl Pts',(103.07318887231,5.50412753733405,132.66892744436));
#201006=CARTESIAN_POINT('Ctrl Pts',(102.794741248497,4.54382825837723,127.181426149873));
#201007=CARTESIAN_POINT('Ctrl Pts',(102.516293624684,-0.592027211677165,
125.023224641008));
#201008=CARTESIAN_POINT('Ctrl Pts',(102.237846000871,-5.18383859633749,
128.177604670405));
#201009=CARTESIAN_POINT('Ctrl Pts',(101.959398377058,-5.01195555555783,
133.745845091081));
#201010=CARTESIAN_POINT('Ctrl Pts',(101.680950753245,-0.234330206861215,
136.611004980102));
#201011=CARTESIAN_POINT('Ctrl Pts',(101.402503129432,4.75863315427373,134.140142370299));
#201012=CARTESIAN_POINT('Ctrl Pts',(101.124055505619,5.37864511878468,128.603859291732));
#201013=CARTESIAN_POINT('Ctrl Pts',(100.845607881807,1.05594498055446,125.089729431141));
#201014=CARTESIAN_POINT('Ctrl Pts',(100.567160257994,-4.23711700902531,
126.827066455619));
#201015=CARTESIAN_POINT('Ctrl Pts',(100.288712634181,-5.63647546198416,
132.219342513305));
#201016=CARTESIAN_POINT('Ctrl Pts',(100.010265010368,-1.85618832251382,
136.311319334515));
#201017=CARTESIAN_POINT('Ctrl Pts',(99.731817386555,3.62984520550588,135.342670124737));
#201018=CARTESIAN_POINT('Ctrl Pts',(99.4533697627421,5.78022831746224,130.203536186614));
#201019=CARTESIAN_POINT('Ctrl Pts',(99.1749221389292,2.61886398552269,125.616530548629));
#201020=CARTESIAN_POINT('Ctrl Pts',(98.8964745151164,-2.9491084104941,125.796887304409));
#201021=CARTESIAN_POINT('Ctrl Pts',(98.6180268913035,-5.80699424922206,
130.578867406308));
#201022=CARTESIAN_POINT('Ctrl Pts',(98.3395792674906,-3.32853606035512,
135.568064753397));
#201023=CARTESIAN_POINT('Ctrl Pts',(98.0611316436778,2.20868415995158,136.179650719541));
#201024=CARTESIAN_POINT('Ctrl Pts',(97.7826840198649,5.71623153748262,131.851607679491));
#201025=CARTESIAN_POINT('Ctrl Pts',(97.5042363960519,3.97084138550236,126.561195750394));
#201026=CARTESIAN_POINT('Ctrl Pts',(97.2257887722391,-1.42355801336861,
125.170045044101));
#201027=CARTESIAN_POINT('Ctrl Pts',(96.9473411484261,-5.50977714262889,
128.956555098203));
#201028=CARTESIAN_POINT('Ctrl Pts',(96.6688935246133,-4.53278024539068,
134.441108154283));
#201029=CARTESIAN_POINT('Ctrl Pts',(96.3904459008004,0.609620258735999,
136.583667889112));
#201030=CARTESIAN_POINT('Ctrl Pts',(96.1119982769875,5.19180952668969,133.415326576248));
#201031=CARTESIAN_POINT('Ctrl Pts',(95.8335506531746,5.00297947361121,127.847635100131));
#201032=CARTESIAN_POINT('Ctrl Pts',(95.5551030293618,0.216655693418756,
124.997029930466));
#201033=CARTESIAN_POINT('Ctrl Pts',(95.2766554055487,-4.7687640848064,127.483077958369));
#201034=CARTESIAN_POINT('Ctrl Pts',(94.9982077817361,-5.37192263617151,
133.021222496396));
#201035=CARTESIAN_POINT('Ctrl Pts',(94.7197601579228,-1.03854671790542,
136.522179267501));
#201036=CARTESIAN_POINT('Ctrl Pts',(94.4413125341102,4.24920289828813,134.768740030285));
#201037=CARTESIAN_POINT('Ctrl Pts',(94.1628649102971,5.63214263605674,129.372229783482));
#201038=CARTESIAN_POINT('Ctrl Pts',(93.8844172864844,1.83941843675322,125.29177780972));
#201039=CARTESIAN_POINT('Ctrl Pts',(93.6059696626714,-3.6436414453401,126.277120131727));
#201040=CARTESIAN_POINT('Ctrl Pts',(93.3275220388585,-5.77837284094635,
131.422775292226));
#201041=CARTESIAN_POINT('Ctrl Pts',(93.0490744150458,-2.60306188492951,
136.000137577949));
#201042=CARTESIAN_POINT('Ctrl Pts',(92.7706267912327,2.96433577669487,135.802834664895));
#201043=CARTESIAN_POINT('Ctrl Pts',(92.49217916742,5.80765367539012,131.012178291378));
#201044=CARTESIAN_POINT('Ctrl Pts',(92.213731543607,3.31402156605677,126.030547628085));
#201045=CARTESIAN_POINT('Ctrl Pts',(91.9352839197941,-2.22503446352861,
125.435817888395));
#201046=CARTESIAN_POINT('Ctrl Pts',(91.6568362959812,-5.71939252010779,
129.77451664892));
#201047=CARTESIAN_POINT('Ctrl Pts',(91.3783886721684,-3.95790825856573,
135.059591705955));
#201048=CARTESIAN_POINT('Ctrl Pts',(91.0999410483554,1.44070033803066,136.434317272356));
#201049=CARTESIAN_POINT('Ctrl Pts',(90.8214934245425,5.51537570610103,132.635387711677));
#201050=CARTESIAN_POINT('Ctrl Pts',(90.5430458007297,4.52169024134706,127.153833702157));
#201051=CARTESIAN_POINT('Ctrl Pts',(90.2645981769166,-0.627207658356129,
125.026935589742));
#201052=CARTESIAN_POINT('Ctrl Pts',(89.9861505531037,-5.19973236082766,
128.209208834995));
#201053=CARTESIAN_POINT('Ctrl Pts',(89.707702929291,-4.99395704474619,133.776299788217));
#201054=CARTESIAN_POINT('Ctrl Pts',(89.4292553054779,-0.198979172907652,
136.61232383091));
#201055=CARTESIAN_POINT('Ctrl Pts',(89.1508076816652,4.77885083815996,134.111113415317));
#201056=CARTESIAN_POINT('Ctrl Pts',(88.8723600578521,5.36515038880097,128.571158722445));
#201057=CARTESIAN_POINT('Ctrl Pts',(88.5939124340396,1.02113883430145,125.08340747321));
#201058=CARTESIAN_POINT('Ctrl Pts',(88.3154648102263,-4.26124942351577,
126.85293267954));
#201059=CARTESIAN_POINT('Ctrl Pts',(88.0370171864138,-5.62775763472933,
132.253627122929));
#201060=CARTESIAN_POINT('Ctrl Pts',(87.7585695626006,-1.82263151087143,
136.322516448493));
#201061=CARTESIAN_POINT('Ctrl Pts',(87.480121938788,3.65740393097785,135.320490142334));
#201062=CARTESIAN_POINT('Ctrl Pts',(87.2016743149749,5.77646383437373,130.168361428106));
#201063=CARTESIAN_POINT('Ctrl Pts',(86.9232266911622,2.58723566992664,125.600684898703));
#201064=CARTESIAN_POINT('Ctrl Pts',(86.6447790673492,-2.97953568169397,
125.814932141244));
#201065=CARTESIAN_POINT('Ctrl Pts',(86.3663314435363,-5.80825930024783,
130.614220406392));
#201066=CARTESIAN_POINT('Ctrl Pts',(86.0878838197235,-3.29947637111547,
135.588238236744));
#201067=CARTESIAN_POINT('Ctrl Pts',(85.8094361959104,2.24136415469026,136.166106240484));
#201068=CARTESIAN_POINT('Ctrl Pts',(85.5309885720977,5.72250051906197,131.816791952599));
#201069=CARTESIAN_POINT('Ctrl Pts',(85.2525409482847,3.94493846610766,126.537102727838));
#201070=CARTESIAN_POINT('Ctrl Pts',(84.9740933244718,-1.45782931624159,
125.178815036599));
#201071=CARTESIAN_POINT('Ctrl Pts',(84.6956457006588,-5.52092317588609,
128.990128911089));
#201072=CARTESIAN_POINT('Ctrl Pts',(84.417198076846,-4.51055834898274,134.468633093685));
#201073=CARTESIAN_POINT('Ctrl Pts',(84.138750453033,0.644789247610192,136.579849880389));
#201074=CARTESIAN_POINT('Ctrl Pts',(83.8603028292202,5.20760702535536,133.383674182895));
#201075=CARTESIAN_POINT('Ctrl Pts',(83.5818552054073,4.98488835254533,127.817235325336));
#201076=CARTESIAN_POINT('Ctrl Pts',(83.3034075815944,0.181300809080568,
124.995818682153));
#201077=CARTESIAN_POINT('Ctrl Pts',(83.0249599577814,-4.78889332089225,
127.512168314565));
#201078=CARTESIAN_POINT('Ctrl Pts',(82.7465123339688,-5.35832843941005,
133.053881840899));
#201079=CARTESIAN_POINT('Ctrl Pts',(82.4680647101557,-1.00372149100682,
136.528395258211));
#201080=CARTESIAN_POINT('Ctrl Pts',(82.1896170863428,4.27325647311088,134.742800475408));
#201081=CARTESIAN_POINT('Ctrl Pts',(81.91116946253,5.62332049862395,129.337971866731));
#201082=CARTESIAN_POINT('Ctrl Pts',(81.632721838717,1.80582770038043,125.280682882997));
#201083=CARTESIAN_POINT('Ctrl Pts',(81.3542742149043,-3.67113253492515,
126.299383890674));
#201084=CARTESIAN_POINT('Ctrl Pts',(81.0758265910913,-5.77450131542928,
131.457938430015));
#201085=CARTESIAN_POINT('Ctrl Pts',(80.7973789672785,-2.57138548712596,
136.015886888767));
#201086=CARTESIAN_POINT('Ctrl Pts',(80.5189313434656,2.99470798468153,135.784697301496));
#201087=CARTESIAN_POINT('Ctrl Pts',(80.2404837196526,5.80881111818491,130.976821604667));
#201088=CARTESIAN_POINT('Ctrl Pts',(79.9620360958398,3.2849006102757,126.010462685879));
#201089=CARTESIAN_POINT('Ctrl Pts',(79.6835884720269,-2.25767308216064,
125.449461771377));
#201090=CARTESIAN_POINT('Ctrl Pts',(79.4051408482139,-5.72555550555307,
129.809351295171));
#201091=CARTESIAN_POINT('Ctrl Pts',(79.1266932244012,-3.93193212827854,
135.083605777338));
#201092=CARTESIAN_POINT('Ctrl Pts',(78.8482456005881,1.47494478932078,136.425443010422));
#201093=CARTESIAN_POINT('Ctrl Pts',(78.5697979767754,5.526419500593,132.601780129612));
#201094=CARTESIAN_POINT('Ctrl Pts',(78.2913503529625,4.49938467142216,127.126376526057));
#201095=CARTESIAN_POINT('Ctrl Pts',(78.0129027291494,-0.662364863624755,
125.030860623086));
#201096=CARTESIAN_POINT('Ctrl Pts',(77.7344551053368,-5.21543344732299,
128.240909163888));
#201097=CARTESIAN_POINT('Ctrl Pts',(77.4560074815235,-4.97577348101974,
133.806644359053));
#201098=CARTESIAN_POINT('Ctrl Pts',(77.1775598577108,-0.163620765707691,
136.613427465507));
#201099=CARTESIAN_POINT('Ctrl Pts',(76.8991122338979,4.79889143997102,134.081961927395));
#201100=CARTESIAN_POINT('Ctrl Pts',(76.620664610085,5.35145685119646,128.538540905275));
#201101=CARTESIAN_POINT('Ctrl Pts',(76.3422169862721,0.986294849373407,
125.077297507303));
#201102=CARTESIAN_POINT('Ctrl Pts',(76.0637693624593,-4.28522393584178,
126.878945325076));
#201103=CARTESIAN_POINT('Ctrl Pts',(75.7853217386464,-5.61883126884571,
132.287858029448));
#201104=CARTESIAN_POINT('Ctrl Pts',(75.5068741148335,-1.78900716094817,
136.333509085178));
#201105=CARTESIAN_POINT('Ctrl Pts',(75.2284264910206,3.68482713000219,135.298142813091));
#201106=CARTESIAN_POINT('Ctrl Pts',(74.9499788672077,5.77248530229349,130.133210236781));
#201107=CARTESIAN_POINT('Ctrl Pts',(74.6715312433948,2.55551148336137,125.585032072894));
#201108=CARTESIAN_POINT('Ctrl Pts',(74.3930836195819,-3.0098525451033,125.833161863185));
#201109=CARTESIAN_POINT('Ctrl Pts',(74.1146359957691,-5.80930912408932,
130.649580452192));
#201110=CARTESIAN_POINT('Ctrl Pts',(73.8361883719562,-3.27029441856551,
135.608234451746));
#201111=CARTESIAN_POINT('Ctrl Pts',(73.5577407481433,2.273961094856,136.152363079971));
#201112=CARTESIAN_POINT('Ctrl Pts',(73.2792931243304,5.72855745128013,131.781938709691));
#201113=CARTESIAN_POINT('Ctrl Pts',(73.0008455005175,3.91888936556733,126.513167830092));
#201114=CARTESIAN_POINT('Ctrl Pts',(72.7223978767045,-1.49204659871303,
125.187793485758));
#201115=CARTESIAN_POINT('Ctrl Pts',(72.4439502528918,-5.53186462930466,
129.023769950998));
#201116=CARTESIAN_POINT('Ctrl Pts',(72.1655026290786,-4.48816931217651,
134.496022252122));
#201117=CARTESIAN_POINT('Ctrl Pts',(71.8870550052659,0.679934343581693,
136.575817858786));
#201118=CARTESIAN_POINT('Ctrl Pts',(71.6086073814528,5.22321155422762,133.351926212129));
#201119=CARTESIAN_POINT('Ctrl Pts',(71.3301597576401,4.96661251460835,127.786946239566));
#201120=CARTESIAN_POINT('Ctrl Pts',(71.0517121338272,0.145939206574258,
124.994822671498));
#201121=CARTESIAN_POINT('Ctrl Pts',(70.7732645100143,-4.80884510277506,
127.541380664158));
#201122=CARTESIAN_POINT('Ctrl Pts',(70.4948168862015,-5.34453568781766,
133.086457828568));
#201123=CARTESIAN_POINT('Ctrl Pts',(70.2163692623885,-0.968859070839113,
136.534399142713));
#201124=CARTESIAN_POINT('Ctrl Pts',(69.9379216385757,4.29715170084345,134.716714980192));
#201125=CARTESIAN_POINT('Ctrl Pts',(69.6594740147628,5.61428998698222,129.303768287553));
#201126=CARTESIAN_POINT('Ctrl Pts',(69.3810263909498,1.77217004839796,125.269792638185));
#201127=CARTESIAN_POINT('Ctrl Pts',(69.102578767137,-3.69848758934425,126.321814583191));
#201128=CARTESIAN_POINT('Ctrl Pts',(68.8241311433241,-5.77041581364239,
131.493077349239));
#201129=CARTESIAN_POINT('Ctrl Pts',(68.5456835195112,-2.53961380568736,
136.031443084562));
#201130=CARTESIAN_POINT('Ctrl Pts',(68.2672358956983,3.02496922266262,135.76637538989));
#201131=CARTESIAN_POINT('Ctrl Pts',(67.9887882718854,5.80975331334755,130.94145852735));
#201132=CARTESIAN_POINT('Ctrl Pts',(67.7103406480725,3.25565793129432,125.990555383323));
#201133=CARTESIAN_POINT('Ctrl Pts',(67.4318930242597,-2.29022804188655,
125.463304082106));
#201134=CARTESIAN_POINT('Ctrl Pts',(67.1534454004468,-5.73150632843341,
129.844222811859));
#201135=CARTESIAN_POINT('Ctrl Pts',(66.8749977766338,-3.90581029880048,
135.107461279717));
#201136=CARTESIAN_POINT('Ctrl Pts',(66.5965501528209,1.50913458598933,136.416360457212));
#201137=CARTESIAN_POINT('Ctrl Pts',(66.3181025290079,5.53725851157817,132.568105943505));
#201138=CARTESIAN_POINT('Ctrl Pts',(66.0396549051952,4.47691237514338,127.09905563901));
#201139=CARTESIAN_POINT('Ctrl Pts',(65.7612072813823,-0.69749752471975,
125.034999595595));
#201140=CARTESIAN_POINT('Ctrl Pts',(65.4827596575694,-5.23094127401388,
128.272704482416));
#201141=CARTESIAN_POINT('Ctrl Pts',(65.2043120337565,-4.95740553817722,
133.836877679162));
#201142=CARTESIAN_POINT('Ctrl Pts',(64.9258644099437,-0.128256295479839,
136.614315842995));
#201143=CARTESIAN_POINT('Ctrl Pts',(64.6474167861306,4.81875421709505,134.05268898675));
#201144=CARTESIAN_POINT('Ctrl Pts',(64.3689691623179,5.33756501339024,128.506007048888));
#201145=CARTESIAN_POINT('Ctrl Pts',(64.0905215385049,0.951414316927145,
125.071399759827));
#201146=CARTESIAN_POINT('Ctrl Pts',(63.8120739146922,-4.30903965761881,
126.905103428319));
#201147=CARTESIAN_POINT('Ctrl Pts',(63.5336262908791,-5.60969669510319,
132.322033964426));
#201148=CARTESIAN_POINT('Ctrl Pts',(63.2551786670663,-1.75531651870651,
136.344296837232));
#201149=CARTESIAN_POINT('Ctrl Pts',(62.9767310432534,3.71211378640213,135.275628965096));
#201150=CARTESIAN_POINT('Ctrl Pts',(62.6982834194405,5.76829286864752,130.098083915181));
#201151=CARTESIAN_POINT('Ctrl Pts',(62.4198357956276,2.52369260137852,125.569572651222));
#201152=CARTESIAN_POINT('Ctrl Pts',(62.1413881718147,-3.04005787731984,
125.851575794724));
#201153=CARTESIAN_POINT('Ctrl Pts',(61.8629405480017,-5.81014368184488,
130.684946233427));
#201154=CARTESIAN_POINT('Ctrl Pts',(61.5844929241889,-3.24099128405306,
135.628052657436));
#201155=CARTESIAN_POINT('Ctrl Pts',(61.3060453003759,2.306473772557,136.138421747261));
#201156=CARTESIAN_POINT('Ctrl Pts',(61.0275976765631,5.73440210969521,131.747049242268));
#201157=CARTESIAN_POINT('Ctrl Pts',(60.7491500527502,3.89269504914048,126.489391944074));
#201158=CARTESIAN_POINT('Ctrl Pts',(60.4707024289374,-1.5262085928491,125.196980058879));
#201159=CARTESIAN_POINT('Ctrl Pts',(60.1922548051244,-5.54260109744501,
129.057476971348));
#201160=CARTESIAN_POINT('Ctrl Pts',(59.9138071813117,-4.46561396460588,
134.52327461468));
#201161=CARTESIAN_POINT('Ctrl Pts',(59.6353595574987,0.715054244335847,
136.571571973714));
#201162=CARTESIAN_POINT('Ctrl Pts',(59.3569119336859,5.23862253507484,133.320083840384));
#201163=CARTESIAN_POINT('Ctrl Pts',(59.0784643098728,4.94815263701827,127.756768965196));
#201164=CARTESIAN_POINT('Ctrl Pts',(58.80001668606,0.110572196236736,124.994041935407));
#201165=CARTESIAN_POINT('Ctrl Pts',(58.5215690622471,-4.82861869113419,
127.570713924673));
#201166=CARTESIAN_POINT('Ctrl Pts',(58.2431214384343,-5.3305448924898,133.118949252284));
#201167=CARTESIAN_POINT('Ctrl Pts',(57.9646738146213,-0.933960749242644,
136.54019069853));
#201168=CARTESIAN_POINT('Ctrl Pts',(57.6862261908085,4.32088769603949,134.690484511247));
#201169=CARTESIAN_POINT('Ctrl Pts',(57.4077785669955,5.6050514357603,129.269620313377));
#201170=CARTESIAN_POINT('Ctrl Pts',(57.1293309431827,1.73844672800264,125.259107478825));
#201171=CARTESIAN_POINT('Ctrl Pts',(56.8508833193697,-3.72570559494523,
126.3444113781));
#201172=CARTESIAN_POINT('Ctrl Pts',(56.5724356955568,-5.76611648697549,
131.528190747811));
#201173=CARTESIAN_POINT('Ctrl Pts',(56.293988071744,-2.50774801792579,136.046805588895));
#201174=CARTESIAN_POINT('Ctrl Pts',(56.0155404479311,3.05511836929639,135.747869609001));
#201175=CARTESIAN_POINT('Ctrl Pts',(55.7370928241181,5.81048022596477,130.906090369819));
#201176=CARTESIAN_POINT('Ctrl Pts',(55.4586452003054,3.22629461271119,125.97082645809));
#201177=CARTESIAN_POINT('Ctrl Pts',(55.1801975764924,-2.32269813636975,
125.477344307648));
#201178=CARTESIAN_POINT('Ctrl Pts',(54.9017499526795,-5.73724476823917,
129.879129906805));
#201179=CARTESIAN_POINT('Ctrl Pts',(54.6233023288666,-3.87954373808533,
135.131157329118));
#201180=CARTESIAN_POINT('Ctrl Pts',(54.3448547050537,1.54326846112093,136.407069949284));
#201181=CARTESIAN_POINT('Ctrl Pts',(54.0664070812409,5.54789233741261,132.534366401168));
#201182=CARTESIAN_POINT('Ctrl Pts',(53.7879594574279,4.45427418523046,127.071872053402));
#201183=CARTESIAN_POINT('Ctrl Pts',(53.5095118336151,-0.732604339787292,
125.039352353899));
#201184=CARTESIAN_POINT('Ctrl Pts',(53.2310642098022,-5.24625526625226,
128.304593612394));
#201185=CARTESIAN_POINT('Ctrl Pts',(52.9526165859893,-4.93885389684926,
133.866998628235));
#201186=CARTESIAN_POINT('Ctrl Pts',(52.6741689621764,-0.0928870726681018,
136.614988930455));
#201187=CARTESIAN_POINT('Ctrl Pts',(52.3957213383635,4.83843843350925,134.023295678104));
#201188=CARTESIAN_POINT('Ctrl Pts',(52.1172737145507,5.32347539014984,128.473558358838));
#201189=CARTESIAN_POINT('Ctrl Pts',(51.8388260907377,0.91649852947334,125.065714449322));
#201190=CARTESIAN_POINT('Ctrl Pts',(51.5603784669247,-4.33269570634681,
126.931406019971));
#201191=CARTESIAN_POINT('Ctrl Pts',(51.2819308431118,-5.6003542519866,132.356153661459));
#201192=CARTESIAN_POINT('Ctrl Pts',(51.0034832192991,-1.72156083256576,
136.354879304913));
#201193=CARTESIAN_POINT('Ctrl Pts',(50.7250355954861,3.73926288906064,135.252949432607));
#201194=CARTESIAN_POINT('Ctrl Pts',(50.4465879716733,5.76388668878802,130.062983764924));
#201195=CARTESIAN_POINT('Ctrl Pts',(50.1681403478604,2.49178020303801,125.554307206545));
#201196=CARTESIAN_POINT('Ctrl Pts',(49.8896927240475,-3.07015055907373,
125.870173253527));
#201197=CARTESIAN_POINT('Ctrl Pts',(49.6112451002346,-5.81076294258959,
130.720316439607));
#201198=CARTESIAN_POINT('Ctrl Pts',(49.3327974764216,-3.21156805341676,
135.647692119444));
#201199=CARTESIAN_POINT('Ctrl Pts',(49.0543498526089,2.33890098302428,136.124282758954));
#201200=CARTESIAN_POINT('Ctrl Pts',(48.7759022287959,5.74003427773134,131.712124843171));
#201201=CARTESIAN_POINT('Ctrl Pts',(48.497454604983,3.86635648746696,126.465775950806));
#201202=CARTESIAN_POINT('Ctrl Pts',(48.2190069811701,-1.56031403276457,
125.206374415548));
#201203=CARTESIAN_POINT('Ctrl Pts',(47.9405593573573,-5.55313218246346,
129.091248723115));
#201204=CARTESIAN_POINT('Ctrl Pts',(47.6621117335443,-4.44289314206747,
134.550389171513));
#201205=CARTESIAN_POINT('Ctrl Pts',(47.3836641097315,0.750147648492217,
136.567112382502));
#201206=CARTESIAN_POINT('Ctrl Pts',(47.1052164859186,5.25383939683757,133.288148247589));
#201207=CARTESIAN_POINT('Ctrl Pts',(46.8267688621057,4.92950940381243,127.726704620456));
#201208=CARTESIAN_POINT('Ctrl Pts',(46.5483212382927,0.0752010886061242,
124.993476502813));
#201209=CARTESIAN_POINT('Ctrl Pts',(46.2698736144798,-4.84821335325179,
127.600167009156));
#201210=CARTESIAN_POINT('Ctrl Pts',(45.991425990667,-5.31635657186091,133.151354908068));
#201211=CARTESIAN_POINT('Ctrl Pts',(45.7129783668541,-0.899027819386881,
136.545769711054));
#201212=CARTESIAN_POINT('Ctrl Pts',(45.4345307430412,4.344463579153,134.664110040551));
#201213=CARTESIAN_POINT('Ctrl Pts',(45.1560831192283,5.5956051872961,129.235529209567));
#201214=CARTESIAN_POINT('Ctrl Pts',(44.8776354954154,1.70465898882477,125.248627800858));
#201215=CARTESIAN_POINT('Ctrl Pts',(44.5991878716026,-3.7527855431554,126.367173438067));
#201216=CARTESIAN_POINT('Ctrl Pts',(44.3207402477896,-5.76160349474165,
131.563277324591));
#201217=CARTESIAN_POINT('Ctrl Pts',(44.0422926239769,-2.47578930463884,
136.0619738325));
#201218=CARTESIAN_POINT('Ctrl Pts',(43.7638450001637,3.08515430739569,135.72918064457));
#201219=CARTESIAN_POINT('Ctrl Pts',(43.485397376351,5.8109918291003,130.870718442656));
#201220=CARTESIAN_POINT('Ctrl Pts',(43.206949752538,3.19681174259461,125.951276641244));
#201221=CARTESIAN_POINT('Ctrl Pts',(42.9285021287252,-2.3550821624196,125.491581927739));
#201222=CARTESIAN_POINT('Ctrl Pts',(42.6500545049123,-5.74277061233009,
129.914071286517));
#201223=CARTESIAN_POINT('Ctrl Pts',(42.3716068810994,-3.85313341945026,
135.154693047476));
#201224=CARTESIAN_POINT('Ctrl Pts',(42.0931592572865,1.57734514987214,136.397571830902));
#201225=CARTESIAN_POINT('Ctrl Pts',(41.8147116334736,5.5583205840564,132.50056275283));
#201226=CARTESIAN_POINT('Ctrl Pts',(41.5362640096606,4.43147094054935,127.04482677653));
#201227=CARTESIAN_POINT('Ctrl Pts',(41.2578163858478,-0.767684007931795,
125.043918736703));
#201228=CARTESIAN_POINT('Ctrl Pts',(40.9793687620349,-5.26137485657243,
128.336575372158));
#201229=CARTESIAN_POINT('Ctrl Pts',(40.700921138222,-4.9201192444739,133.897006090131));
#201230=CARTESIAN_POINT('Ctrl Pts',(40.4224735144091,-0.0575144078915333,
136.615446702946));
#201231=CARTESIAN_POINT('Ctrl Pts',(40.1440258905964,4.85794335980812,133.993783090635));
#201232=CARTESIAN_POINT('Ctrl Pts',(39.8655782667833,5.30918850357096,128.441196037522));
#201233=CARTESIAN_POINT('Ctrl Pts',(39.5871306429705,0.8815487808295,125.060241786462));
#201234=CARTESIAN_POINT('Ctrl Pts',(39.3086830191576,-4.35619120544207,
126.957852125381));
#201235=CARTESIAN_POINT('Ctrl Pts',(39.0302353953447,-5.59080428568363,
132.39021585623));
#201236=CARTESIAN_POINT('Ctrl Pts',(38.7517877715318,-1.6877413533555,136.365256096082));
#201237=CARTESIAN_POINT('Ctrl Pts',(38.4733401477189,3.76627343195761,135.230105056025));
#201238=CARTESIAN_POINT('Ctrl Pts',(38.194892523906,5.7592669259876,130.027911086658));
#201239=CARTESIAN_POINT('Ctrl Pts',(37.9164449000932,2.45977547086574,125.539236304527));
#201240=CARTESIAN_POINT('Ctrl Pts',(37.6379972762802,-3.10012947526937,
125.888953550457));
#201241=CARTESIAN_POINT('Ctrl Pts',(37.3595496524674,-5.81116688337655,
130.755689760074));
#201242=CARTESIAN_POINT('Ctrl Pts',(37.0811020286545,-3.18202581694541,
135.667152110023));
#201243=CARTESIAN_POINT('Ctrl Pts',(36.8026544048415,2.3712415246555,136.109946638975));
#201244=CARTESIAN_POINT('Ctrl Pts',(36.5242067810287,5.74545374668639,131.677166806538));
#201245=CARTESIAN_POINT('Ctrl Pts',(36.2457591572158,3.83987465653194,126.442320725389));
#201246=CARTESIAN_POINT('Ctrl Pts',(35.9673115334029,-1.59436165466975,
125.215976207654));
#201247=CARTESIAN_POINT('Ctrl Pts',(35.6888639095901,-5.56345749412674,
129.125083954872));
#201248=CARTESIAN_POINT('Ctrl Pts',(35.4104162857771,-4.42000768648982,
134.57736491788));
#201249=CARTESIAN_POINT('Ctrl Pts',(35.1319686619643,0.785213255651605,
136.562439250406));
#201250=CARTESIAN_POINT('Ctrl Pts',(34.8535210381513,5.26886157564935,133.25612061713));
#201251=CARTESIAN_POINT('Ctrl Pts',(34.5750734143385,4.91068350582282,127.69675431939));
#201252=CARTESIAN_POINT('Ctrl Pts',(34.2966257905255,0.0398271943713243,
124.993126394665));
#201253=CARTESIAN_POINT('Ctrl Pts',(34.0181781667127,-4.86762836304081,
127.629738826211));
#201254=CARTESIAN_POINT('Ctrl Pts',(33.7397305428998,-5.30197125168398,
133.183673595116));
#201255=CARTESIAN_POINT('Ctrl Pts',(33.4612829190869,-0.864061575724654,
136.551135973552));
#201256=CARTESIAN_POINT('Ctrl Pts',(33.182835295274,4.36787847657091,134.637592545421));
#201257=CARTESIAN_POINT('Ctrl Pts',(32.9043876714611,5.58595159162396,129.201496239381));
#201258=CARTESIAN_POINT('Ctrl Pts',(32.6259400476482,1.67080808288091,125.238353992614));
#201259=CARTESIAN_POINT('Ctrl Pts',(32.3474924238352,-3.77972643051725,
126.390099919638));
#201260=CARTESIAN_POINT('Ctrl Pts',(32.0690448000224,-5.75687700417149,
131.598335779433));
#201261=CARTESIAN_POINT('Ctrl Pts',(31.7905971762095,-2.44373885006871,
136.076947253315));
#201262=CARTESIAN_POINT('Ctrl Pts',(31.5121495523967,3.11507592396733,135.71030918912));
#201263=CARTESIAN_POINT('Ctrl Pts',(31.2337019285837,5.81128810379662,130.835344056578));
#201264=CARTESIAN_POINT('Ctrl Pts',(30.9552543047708,3.16721041344351,125.931906657209));
#201265=CARTESIAN_POINT('Ctrl Pts',(30.676806680958,-2.38737892003384,125.506016414799));
#201266=CARTESIAN_POINT('Ctrl Pts',(30.398359057145,-5.74808365594406,129.949045656226));
#201267=CARTESIAN_POINT('Ctrl Pts',(30.1199114333322,-3.82658032153943,
135.178067562667));
#201268=CARTESIAN_POINT('Ctrl Pts',(29.8414638095193,1.61136338951851,136.387866454021));
#201269=CARTESIAN_POINT('Ctrl Pts',(29.5630161857064,5.56854286508694,132.466696251098));
#201270=CARTESIAN_POINT('Ctrl Pts',(29.2845685618935,4.40850348608286,127.017920810568));
#201271=CARTESIAN_POINT('Ctrl Pts',(29.0061209380806,-0.802735229263066,
125.048698574801));
#201272=CARTESIAN_POINT('Ctrl Pts',(28.7276733142678,-5.27629948471241,
128.368648576612));
#201273=CARTESIAN_POINT('Ctrl Pts',(28.4492256904548,-4.90120227527057,
133.926898952911));
#201274=CARTESIAN_POINT('Ctrl Pts',(28.170778066642,-0.0221396118974229,
136.615689143506));
#201275=CARTESIAN_POINT('Ctrl Pts',(27.892330442829,4.87726827322928,133.964152317942));
#201276=CARTESIAN_POINT('Ctrl Pts',(27.6138828190162,5.29470488305963,128.408921284139));
#201277=CARTESIAN_POINT('Ctrl Pts',(27.3354351952032,0.846566366071392,
125.054981974037));
#201278=CARTESIAN_POINT('Ctrl Pts',(27.0569875713904,-4.37952528427021,
126.984440764576));
#201279=CARTESIAN_POINT('Ctrl Pts',(26.7785399475775,-5.58104715007188,
132.424219286554));
#201280=CARTESIAN_POINT('Ctrl Pts',(26.5000923237646,-1.65385933426847,
136.375426826225));
#201281=CARTESIAN_POINT('Ctrl Pts',(26.2216446999517,3.79314441420758,135.207096681855));
#201282=CARTESIAN_POINT('Ctrl Pts',(25.9431970761388,5.75443375143326,129.992867180015));
#201283=CARTESIAN_POINT('Ctrl Pts',(25.6647494523259,2.42767959080881,125.524360503627));
#201284=CARTESIAN_POINT('Ctrl Pts',(25.3863018285131,-3.12999351502748,
125.907915989602));
#201285=CARTESIAN_POINT('Ctrl Pts',(25.1078542047001,-5.81135548923757,
130.791064884058));
#201286=CARTESIAN_POINT('Ctrl Pts',(24.8294065808873,-3.152365669337,135.686431908074));
#201287=CARTESIAN_POINT('Ctrl Pts',(24.5509589570743,2.40349419906,136.095413918554));
#201288=CARTESIAN_POINT('Ctrl Pts',(24.2725113332615,5.75066031573997,131.64217642775));
#201289=CARTESIAN_POINT('Ctrl Pts',(23.9940637094486,3.81325053762949,126.419027136963));
#201290=CARTESIAN_POINT('Ctrl Pts',(23.7156160856357,-1.62835019691723,
125.2257850794));
#201291=CARTESIAN_POINT('Ctrl Pts',(23.4371684618228,-5.57357664982666,
129.158981412844));
#201292=CARTESIAN_POINT('Ctrl Pts',(23.1587208380098,-4.39695844590187,
134.604200854185));
#201293=CARTESIAN_POINT('Ctrl Pts',(22.880273214197,0.820249766445046,136.557552750588));
#201294=CARTESIAN_POINT('Ctrl Pts',(22.6018255903841,5.28368851485763,133.224002135804));
#201295=CARTESIAN_POINT('Ctrl Pts',(22.3233779665712,4.89167564065013,127.666919171818));
#201296=CARTESIAN_POINT('Ctrl Pts',(22.0449303427584,0.00445182432539013,
124.992991623939));
#201297=CARTESIAN_POINT('Ctrl Pts',(21.7664827189454,-4.88686300107076,
127.659428280044));
#201298=CARTESIAN_POINT('Ctrl Pts',(21.4880350951325,-5.28738946501251,
133.215904115845));
#201299=CARTESIAN_POINT('Ctrl Pts',(21.2095874713197,-0.829063313942982,
136.556289287176));
#201300=CARTESIAN_POINT('Ctrl Pts',(20.9311398475068,4.39113152064558,134.610933008472));
#201301=CARTESIAN_POINT('Ctrl Pts',(20.6526922236938,5.57609100646137,129.167522663925));
#201302=CARTESIAN_POINT('Ctrl Pts',(20.374244599881,1.6368952645291,125.228286434793));
#201303=CARTESIAN_POINT('Ctrl Pts',(20.0957969760681,-3.80652725872624,
126.413189973261));
#201304=CARTESIAN_POINT('Ctrl Pts',(19.8173493522552,-5.75193719040684,
131.633364813234));
#201305=CARTESIAN_POINT('Ctrl Pts',(19.5389017284423,-2.41159784185683,
136.091725296493));
#201306=CARTESIAN_POINT('Ctrl Pts',(19.2604541046294,3.14488211025528,135.691255941942));
#201307=CARTESIAN_POINT('Ctrl Pts',(18.9820064808165,5.81136903907515,130.799968522399));
#201308=CARTESIAN_POINT('Ctrl Pts',(18.7035588570036,3.13749172214556,125.912717223747));
#201309=CARTESIAN_POINT('Ctrl Pts',(18.4251112331907,-2.41958721244422,
125.52064723395));
#201310=CARTESIAN_POINT('Ctrl Pts',(18.1466636093778,-5.75318370220431,
129.984051719947));
#201311=CARTESIAN_POINT('Ctrl Pts',(17.868215985565,-3.79988542828747,135.201280008538));
#201312=CARTESIAN_POINT('Ctrl Pts',(17.589768361752,1.64532191950215,136.377954178279));
#201313=CARTESIAN_POINT('Ctrl Pts',(17.3113207379392,5.57855880171371,132.432768150908));
#201314=CARTESIAN_POINT('Ctrl Pts',(17.0328731141263,4.38537267289848,126.991155152525));
#201315=CARTESIAN_POINT('Ctrl Pts',(16.7544254903134,-0.83775670494522,
125.053691691071));
#201316=CARTESIAN_POINT('Ctrl Pts',(16.4759778665005,-5.29102859763445,
128.400812037271));
#201317=CARTESIAN_POINT('Ctrl Pts',(16.1975302426876,-4.88210369021464,
133.956676108886));
#201318=CARTESIAN_POINT('Ctrl Pts',(15.9190826188747,0.013236004487936,
136.61571624315));
#201319=CARTESIAN_POINT('Ctrl Pts',(15.6406349950618,4.89641245768097,133.934404458007));
#201320=CARTESIAN_POINT('Ctrl Pts',(15.3621873712489,5.2800250653117,128.376735294641));
#201321=CARTESIAN_POINT('Ctrl Pts',(15.0837397474361,0.811552581485459,
125.049935206953));
#201322=CARTESIAN_POINT('Ctrl Pts',(14.8052921236231,-4.40269707817821,
127.011170952307));
#201323=CARTESIAN_POINT('Ctrl Pts',(14.5268444998103,-5.57108320670569,
132.458162692417));
#201324=CARTESIAN_POINT('Ctrl Pts',(14.2483968759974,-1.6199160308156,136.385391118461));
#201325=CARTESIAN_POINT('Ctrl Pts',(13.9699492521845,3.81987484009636,135.18392516268));
#201326=CARTESIAN_POINT('Ctrl Pts',(13.6915016283715,5.74938734422005,129.95785334356));
#201327=CARTESIAN_POINT('Ctrl Pts',(13.4130540045587,2.39549375219187,125.509680355073));
#201328=CARTESIAN_POINT('Ctrl Pts',(13.1346063807458,-3.15974157172482,
125.927059868305));
#201329=CARTESIAN_POINT('Ctrl Pts',(12.8561587569329,-5.81132875318382,
130.82644050072));
#201330=CARTESIAN_POINT('Ctrl Pts',(12.57771113312,-3.12258870965941,135.705530799178));
#201331=CARTESIAN_POINT('Ctrl Pts',(12.2992635093071,2.43565781110307,136.080685136208));
#201332=CARTESIAN_POINT('Ctrl Pts',(12.0208158854942,5.75565379196074,131.607155003388));
#201333=CARTESIAN_POINT('Ctrl Pts',(11.7423682616813,3.78648511732596,126.395896048684));
#201334=CARTESIAN_POINT('Ctrl Pts',(11.4639206378685,-1.66227840004959,
125.235800667314));
#201335=CARTESIAN_POINT('Ctrl Pts',(11.1854730140555,-5.58348927459409,
129.192939840948));
#201336=CARTESIAN_POINT('Ctrl Pts',(10.9070253902426,-4.37374627440173,
134.630895986013));
#201337=CARTESIAN_POINT('Ctrl Pts',(10.6285777664298,0.855255882581734,
136.552453064119));
#201338=CARTESIAN_POINT('Ctrl Pts',(10.3501301426169,5.29831966504511,133.19179399377));
#201339=CARTESIAN_POINT('Ctrl Pts',(10.071682518804,4.87248651263752,127.637200283293));
#201340=CARTESIAN_POINT('Ctrl Pts',(9.79323489499104,-0.0309237106847325,
124.993072195629));
#201341=CARTESIAN_POINT('Ctrl Pts',(9.51478727117816,-4.90591655459505,
127.689234270502));
#201342=CARTESIAN_POINT('Ctrl Pts',(9.23633964736526,-5.27261175218,133.248045275945));
#201343=CARTESIAN_POINT('Ctrl Pts',(8.95789202355236,-0.794034330915497,
136.561229460968));
#201344=CARTESIAN_POINT('Ctrl Pts',(8.67944439973947,4.41422184972672,134.584132417584));
#201345=CARTESIAN_POINT('Ctrl Pts',(8.40099677592661,5.56602379719609,129.1336097421));
#201346=CARTESIAN_POINT('Ctrl Pts',(8.12254915211368,1.60292179042129,125.218425500451));
#201347=CARTESIAN_POINT('Ctrl Pts',(7.84410152830078,-3.83318703466779,
126.436442743329));
#201348=CARTESIAN_POINT('Ctrl Pts',(7.56565390448795,-5.74678423649425,
131.668363127979));
#201349=CARTESIAN_POINT('Ctrl Pts',(7.28720628067502,-2.37936747100029,
136.106307414428));
#201350=CARTESIAN_POINT('Ctrl Pts',(7.00875865686212,3.17457176177998,135.672021609062));
#201351=CARTESIAN_POINT('Ctrl Pts',(6.73031103304925,5.81123463193681,130.764593150968));
#201352=CARTESIAN_POINT('Ctrl Pts',(6.45186340923634,3.10765676993803,125.89370905193));
#201353=CARTESIAN_POINT('Ctrl Pts',(6.17341578542346,-2.45170584616043,
125.535473843045));
#201354=CARTESIAN_POINT('Ctrl Pts',(5.89496816161054,-5.75807056212669,
130.019088180515));
#201355=CARTESIAN_POINT('Ctrl Pts',(5.61652053779771,-3.77304972888379,
135.224329524944));
#201356=CARTESIAN_POINT('Ctrl Pts',(5.33807291398477,1.67921948147701,136.367835370977));
#201357=CARTESIAN_POINT('Ctrl Pts',(5.05962529017187,5.58836802279258,132.398779709476));
#201358=CARTESIAN_POINT('Ctrl Pts',(4.781177666359,4.36207935811697,126.964530794212));
#201359=CARTESIAN_POINT('Ctrl Pts',(4.50273004254611,-0.872747137244579,
125.058897900495));
#201360=CARTESIAN_POINT('Ctrl Pts',(4.2242824187332,-5.30556164954619,128.433064562307));
#201361=CARTESIAN_POINT('Ctrl Pts',(3.94583479492031,-4.86282419701095,
133.986336454649));
#201362=CARTESIAN_POINT('Ctrl Pts',(3.66738717110745,0.0486111304084952,
136.615528000873));
#201363=CARTESIAN_POINT('Ctrl Pts',(3.38893954729453,4.91537520376836,133.904540613147));
#201364=CARTESIAN_POINT('Ctrl Pts',(3.11049192348162,5.26514959429328,128.344639261694));
#201365=CARTESIAN_POINT('Ctrl Pts',(2.83204429966877,0.776508724519974,
125.045101672218));
#201366=CARTESIAN_POINT('Ctrl Pts',(2.55359667585587,-4.42570572852705,
127.038041698076));
#201367=CARTESIAN_POINT('Ctrl Pts',(2.27514905204296,-5.56091282480238,
132.492044816037));
#201368=CARTESIAN_POINT('Ctrl Pts',(1.99670142823006,-1.58591270077849,
136.395148603559));
#201369=CARTESIAN_POINT('Ctrl Pts',(1.7182538044172,3.84646371911817,135.160591357131));
#201370=CARTESIAN_POINT('Ctrl Pts',(1.43980618060429,5.7441278913444,129.922870874744));
#201371=CARTESIAN_POINT('Ctrl Pts',(1.16135855679139,2.36321914767325,125.495196402842));
#201372=CARTESIAN_POINT('Ctrl Pts',(0.882910932978526,-3.18937254303613,
125.946384477181));
#201373=CARTESIAN_POINT('Ctrl Pts',(0.604463309165634,-5.81108667620601,
130.861815299204));
#201374=CARTESIAN_POINT('Ctrl Pts',(0.326015685352703,-3.09269604130886,
135.724448075619));
#201375=CARTESIAN_POINT('Ctrl Pts',(0.0475680615398608,2.46773116894999,
136.065760837718));
#201376=CARTESIAN_POINT('Ctrl Pts',(-0.230879562273037,5.76043399031358,
131.572103831187));
#201377=CARTESIAN_POINT('Ctrl Pts',(-0.509327186085944,3.75957938742415,
126.37292831768));
#201378=CARTESIAN_POINT('Ctrl Pts',(-0.787774809898847,-1.69614500684454,
125.246022600264));
#201379=CARTESIAN_POINT('Ctrl Pts',(-1.06622243371171,-5.59319500111311,
129.226957980841));
#201380=CARTESIAN_POINT('Ctrl Pts',(-1.34467005752462,-4.35037203212501,
134.657449324165));
#201381=CARTESIAN_POINT('Ctrl Pts',(-1.62311768133752,0.890230306896913,
136.547140379971));
#201382=CARTESIAN_POINT('Ctrl Pts',(-1.90156530515039,5.31275448404895,
133.159497384516));
#201383=CARTESIAN_POINT('Ctrl Pts',(-2.18001292896328,4.85311683284533,
127.607598755059));
#201384=CARTESIAN_POINT('Ctrl Pts',(-2.4584605527762,-0.0662980998053887,
124.993368106748));
#201385=CARTESIAN_POINT('Ctrl Pts',(-2.73690817658909,-4.92478831757726,
127.719155693111));
#201386=CARTESIAN_POINT('Ctrl Pts',(-3.01535580040196,-5.25763866077998,
133.280095884409));
#201387=CARTESIAN_POINT('Ctrl Pts',(-3.29380342421486,-0.758975924653704,
136.565956311869));
#201388=CARTESIAN_POINT('Ctrl Pts',(-3.57225104802777,4.43714860819409,
134.557191765862));
#201389=CARTESIAN_POINT('Ctrl Pts',(-3.85069867184063,5.55575033687191,
129.099758730564));
#201390=CARTESIAN_POINT('Ctrl Pts',(-4.12914629565353,1.56888891945708,
125.208771554989));
#201391=CARTESIAN_POINT('Ctrl Pts',(-4.40759391946644,-3.85970477045413,
126.459857368199));
#201392=CARTESIAN_POINT('Ctrl Pts',(-4.68604154327934,-5.74141833337845,
131.703329426794));
#201393=CARTESIAN_POINT('Ctrl Pts',(-4.96448916709218,-2.34704893180687,
136.120693066776));
#201394=CARTESIAN_POINT('Ctrl Pts',(-5.24293679090511,3.20414377838073,
135.652606903212));
#201395=CARTESIAN_POINT('Ctrl Pts',(-5.52138441471801,5.81088488736209,
130.729219253137));
#201396=CARTESIAN_POINT('Ctrl Pts',(-5.79983203853088,3.07770666236606,
125.874882846113));
#201397=CARTESIAN_POINT('Ctrl Pts',(-6.07827966234377,-2.48373363101511,
125.550495692676));
#201398=CARTESIAN_POINT('Ctrl Pts',(-6.35672728615668,-5.7627440546269,
130.054153739642));
#201399=CARTESIAN_POINT('Ctrl Pts',(-6.63517490996957,-3.74607421773465,
135.247215257776));
#201400=CARTESIAN_POINT('Ctrl Pts',(-6.91362253378244,1.71305481935644,
136.357510407073));
#201401=CARTESIAN_POINT('Ctrl Pts',(-7.19207015759534,5.59797016483923,
132.36473218626));
#201402=CARTESIAN_POINT('Ctrl Pts',(-7.47051778140826,4.33862440488076,
126.938048722207));
#201403=CARTESIAN_POINT('Ctrl Pts',(-7.74896540522111,-0.907705229577551,
125.064317010151));
#201404=CARTESIAN_POINT('Ctrl Pts',(-8.027413029034,-5.31989810191992,128.46540495659));
#201405=CARTESIAN_POINT('Ctrl Pts',(-8.30586065284694,-4.84336451006833,
134.015878891129));
#201406=CARTESIAN_POINT('Ctrl Pts',(-8.58430827665978,0.0839844550257475,
136.615124423653));
#201407=CARTESIAN_POINT('Ctrl Pts',(-8.86275590047269,4.93415580881975,
133.874561889976));
#201408=CARTESIAN_POINT('Ctrl Pts',(-9.14120352428557,5.25007902122049,
128.312634374625));
#201409=CARTESIAN_POINT('Ctrl Pts',(-9.4196511480985,0.741436093738357,
125.040481548942));
#201410=CARTESIAN_POINT('Ctrl Pts',(-9.69809877191133,-4.44855038272257,
127.065052006178));
#201411=CARTESIAN_POINT('Ctrl Pts',(-9.97654639572428,-5.5505363812293,
132.525864401898));
#201412=CARTESIAN_POINT('Ctrl Pts',(-10.2549940195371,-1.55185060416301,
136.404698919952));
#201413=CARTESIAN_POINT('Ctrl Pts',(-10.53344164335,3.87291006601234,135.137096129849));
#201414=CARTESIAN_POINT('Ctrl Pts',(-10.8118892671629,5.7386555876974,129.887921069854));
#201415=CARTESIAN_POINT('Ctrl Pts',(-11.0903368909758,2.33085697319978,
125.480909183646));
#201416=CARTESIAN_POINT('Ctrl Pts',(-11.3687845147887,-3.21888533097506,
125.965889100148));
#201417=CARTESIAN_POINT('Ctrl Pts',(-11.6472321386015,-5.81062926727439,
130.897187968684));
#201418=CARTESIAN_POINT('Ctrl Pts',(-11.9256797624145,-3.06268877196916,
135.743183036409));
#201419=CARTESIAN_POINT('Ctrl Pts',(-12.2041273862274,2.49971308411117,
136.050641576106));
#201420=CARTESIAN_POINT('Ctrl Pts',(-12.4825750100403,5.76500073366654,
131.537024209977));
#201421=CARTESIAN_POINT('Ctrl Pts',(-12.7610226338531,3.73253434492532,
126.350124795028));
#201422=CARTESIAN_POINT('Ctrl Pts',(-13.039470257666,-1.7299487623625,125.256450499474));
#201423=CARTESIAN_POINT('Ctrl Pts',(-13.3179178814789,-5.60269346973446,
129.261034571969));
#201424=CARTESIAN_POINT('Ctrl Pts',(-13.5963655052918,-4.32683658521273,
134.683859884699));
#201425=CARTESIAN_POINT('Ctrl Pts',(-13.8748131291047,0.925171743400955,
136.541614895008));
#201426=CARTESIAN_POINT('Ctrl Pts',(-14.1532607529176,5.3269924369816,133.127113504801));
#201427=CARTESIAN_POINT('Ctrl Pts',(-14.4317083767304,4.83356731902416,
127.578115684011));
#201428=CARTESIAN_POINT('Ctrl Pts',(-14.7101560005434,-0.101670032225581,
124.99387934633));
#201429=CARTESIAN_POINT('Ctrl Pts',(-14.9886036243562,-4.94347759071707,
127.749191439124));
#201430=CARTESIAN_POINT('Ctrl Pts',(-15.2670512481692,-5.24247074564602,
133.312054753593));
#201431=CARTESIAN_POINT('Ctrl Pts',(-15.545498871982,-0.723889394260118,
136.570469664722));
#201432=CARTESIAN_POINT('Ctrl Pts',(-15.823946495795,4.45991094648802,134.530112051601));
#201433=CARTESIAN_POINT('Ctrl Pts',(-16.1023941196078,5.54527100617588,
129.065970883678));
#201434=CARTESIAN_POINT('Ctrl Pts',(-16.3808417434207,1.53479791273714,
125.199324956138));
#201435=CARTESIAN_POINT('Ctrl Pts',(-16.6592893672336,-3.88607948346057,
126.483432980235));
#201436=CARTESIAN_POINT('Ctrl Pts',(-16.9377369910465,-5.73583967989507,
131.738262413989));
#201437=CARTESIAN_POINT('Ctrl Pts',(-17.2161846148594,-2.31464342185212,
136.134881720468));
#201438=CARTESIAN_POINT('Ctrl Pts',(-17.4946322386723,3.23359706425542,
135.633012543814));
#201439=CARTESIAN_POINT('Ctrl Pts',(-17.7730798624852,5.81031981831091,
130.693848139697));
#201440=CARTESIAN_POINT('Ctrl Pts',(-18.0515274862981,3.04764250924188,
125.856239303907));
#201441=CARTESIAN_POINT('Ctrl Pts',(-18.3299751101109,-2.51566938020671,
125.565712226204));
#201442=CARTESIAN_POINT('Ctrl Pts',(-18.6084227339239,-5.76720400652691,
130.089247097961));
#201443=CARTESIAN_POINT('Ctrl Pts',(-18.8868703577367,-3.71895989442774,
135.269936358996));
#201444=CARTESIAN_POINT('Ctrl Pts',(-19.1653179815497,1.74682667935956,
136.346979669161));
#201445=CARTESIAN_POINT('Ctrl Pts',(-19.4437656053625,5.60736487204277,
132.330626842902));
#201446=CARTESIAN_POINT('Ctrl Pts',(-19.7222132291754,4.31500868232164,
126.91170991781));
#201447=CARTESIAN_POINT('Ctrl Pts',(-20.0006608529883,-0.942629686559699,
125.069948819234));
#201448=CARTESIAN_POINT('Ctrl Pts',(-20.2791084768012,-5.33403742351306,
128.497832021735));
#201449=CARTESIAN_POINT('Ctrl Pts',(-20.5575561006141,-4.82372535047263,
134.045302323618));
#201450=CARTESIAN_POINT('Ctrl Pts',(-20.836003724427,0.119354667568119,
136.614505526443));
#201451=CARTESIAN_POINT('Ctrl Pts',(-21.1144513482399,4.95275357691331,
133.844469399368));
#201452=CARTESIAN_POINT('Ctrl Pts',(-21.3928989720528,5.23481390453873,
128.280721819388));
#201453=CARTESIAN_POINT('Ctrl Pts',(-21.6713465958657,0.706335988769417,
125.036075008324));
#201454=CARTESIAN_POINT('Ctrl Pts',(-21.9497942196786,-4.47123019424771,
127.092200875735));
#201455=CARTESIAN_POINT('Ctrl Pts',(-22.2282418434914,-5.53995426048939,
132.559620196804));
#201456=CARTESIAN_POINT('Ctrl Pts',(-22.5066894673044,-1.5177310031529,
136.41404171375));
#201457=CARTESIAN_POINT('Ctrl Pts',(-22.7851370911172,3.89921290079955,
135.11344035146));
#201458=CARTESIAN_POINT('Ctrl Pts',(-23.0635847149301,5.73297063605735,
129.853005223969));
#201459=CARTESIAN_POINT('Ctrl Pts',(-23.342032338743,2.298408427964,125.466819226899));
#201460=CARTESIAN_POINT('Ctrl Pts',(-23.6204799625559,-3.24827884193431,
125.985573014458));
#201461=CARTESIAN_POINT('Ctrl Pts',(-23.8989275863688,-5.80995654333829,
130.932557198412));
#201462=CARTESIAN_POINT('Ctrl Pts',(-24.1773752101816,-3.03256801357094,
135.761734987319));
#201463=CARTESIAN_POINT('Ctrl Pts',(-24.4558228339946,2.53160237148462,
136.035327911625));
#201464=CARTESIAN_POINT('Ctrl Pts',(-24.7342704578075,5.76935385279724,
131.501917439649));
#201465=CARTESIAN_POINT('Ctrl Pts',(-25.0127180816204,3.70535099199371,
126.327486325724));
#201466=CARTESIAN_POINT('Ctrl Pts',(-25.2911657054332,-1.76368841399288,
125.267083978533));
#201467=CARTESIAN_POINT('Ctrl Pts',(-25.5696133292462,-5.61198432848891,
129.295168351611));
#201468=CARTESIAN_POINT('Ctrl Pts',(-25.8480609530591,-4.30314080577957,
134.71012668896));
#201469=CARTESIAN_POINT('Ctrl Pts',(-26.1265085768719,0.960078897325804,
136.535876813977));
#201470=CARTESIAN_POINT('Ctrl Pts',(-26.4049562006848,5.3410329962505,133.094643554625));
#201471=CARTESIAN_POINT('Ctrl Pts',(-26.6834038244978,4.81383869558843,
127.548752162656));
#201472=CARTESIAN_POINT('Ctrl Pts',(-26.9618514483106,-0.137038197225328,
124.994605895435));
#201473=CARTESIAN_POINT('Ctrl Pts',(-27.2402990721235,-4.96198368147699,
127.779340395554));
#201474=CARTESIAN_POINT('Ctrl Pts',(-27.5187466959364,-5.22710856883054,
133.343920699249));
#201475=CARTESIAN_POINT('Ctrl Pts',(-27.7971943197493,-0.688776039878604,
136.574769352283));
#201476=CARTESIAN_POINT('Ctrl Pts',(-28.0756419435621,4.48250802114168,
134.502894278251));
#201477=CARTESIAN_POINT('Ctrl Pts',(-28.3540895673751,5.53458619342344,
129.032247453463));
#201478=CARTESIAN_POINT('Ctrl Pts',(-28.632537191188,1.50065003351598,125.190086053944));
#201479=CARTESIAN_POINT('Ctrl Pts',(-28.9109848150008,-3.91231019636288,
126.507168705834));
#201480=CARTESIAN_POINT('Ctrl Pts',(-29.1894324388138,-5.73004848276283,
131.773160795109));
#201481=CARTESIAN_POINT('Ctrl Pts',(-29.4678800626266,-2.28215214193419,
136.148872849742));
#201482=CARTESIAN_POINT('Ctrl Pts',(-29.7463276864396,3.26293052800175,
135.613239256942));
#201483=CARTESIAN_POINT('Ctrl Pts',(-30.0247753102524,5.80953944572202,
130.658481121338));
#201484=CARTESIAN_POINT('Ctrl Pts',(-30.3032229340653,3.01746542460398,
125.837779116156));
#201485=CARTESIAN_POINT('Ctrl Pts',(-30.5816705578782,-2.54751191034413,
125.581122879776));
#201486=CARTESIAN_POINT('Ctrl Pts',(-30.8601181816911,-5.77145025256159,
130.124366955075));
#201487=CARTESIAN_POINT('Ctrl Pts',(-31.138565805504,-3.69170776369427,
135.292491986665));
#201488=CARTESIAN_POINT('Ctrl Pts',(-31.4170134293169,1.78053381005746,
136.336243547461));
#201489=CARTESIAN_POINT('Ctrl Pts',(-31.6954610531298,5.6165517962788,132.296464943187));
#201490=CARTESIAN_POINT('Ctrl Pts',(-31.9739086769427,4.29123306552915,
126.885515357016));
#201491=CARTESIAN_POINT('Ctrl Pts',(-32.2523563007555,-0.977519214052166,
125.075793119056));
#201492=CARTESIAN_POINT('Ctrl Pts',(-32.5308039245685,-5.34797909038788,
128.530344556146));
#201493=CARTESIAN_POINT('Ctrl Pts',(-32.8092515483813,-4.80390744596015,
134.07460566182));
#201494=CARTESIAN_POINT('Ctrl Pts',(-33.0876991721943,0.154720457379397,
136.613671332177));
#201495=CARTESIAN_POINT('Ctrl Pts',(-33.3661467960071,4.9711678189017,133.814264256411));
#201496=CARTESIAN_POINT('Ctrl Pts',(-33.64459441982,5.21935480990263,128.248902778514));
#201497=CARTESIAN_POINT('Ctrl Pts',(-33.9230420436329,0.671209710260644,
125.031882213649));
#201498=CARTESIAN_POINT('Ctrl Pts',(-34.2014896674458,-4.49374432269368,
127.119487300736));
#201499=CARTESIAN_POINT('Ctrl Pts',(-34.4799372912587,-5.52916685470707,
132.59331094992));
#201500=CARTESIAN_POINT('Ctrl Pts',(-34.7583849150716,-1.48355516206214,
136.423176638752));
#201501=CARTESIAN_POINT('Ctrl Pts',(-35.0368325388844,3.92537124881898,
135.089624898536));
#201502=CARTESIAN_POINT('Ctrl Pts',(-35.3152801626974,5.72707324708195,
129.818124630907));
#201503=CARTESIAN_POINT('Ctrl Pts',(-35.5937277865103,2.26587471435868,
125.45292705471));
#201504=CARTESIAN_POINT('Ctrl Pts',(-35.8721754103231,-3.27755198672651,
126.005435490714));
#201505=CARTESIAN_POINT('Ctrl Pts',(-36.1506230341361,-5.80906852932597,
130.967921677768));
#201506=CARTESIAN_POINT('Ctrl Pts',(-36.4290706579489,-3.00233488224952,
135.780103240898));
#201507=CARTESIAN_POINT('Ctrl Pts',(-36.7075182817618,2.56339784940132,
136.019820411726));
#201508=CARTESIAN_POINT('Ctrl Pts',(-36.9859659055747,5.77349318639923,
131.466784821096));
#201509=CARTESIAN_POINT('Ctrl Pts',(-37.2644135293876,3.67803033591843,
126.305013748643));
#201510=CARTESIAN_POINT('Ctrl Pts',(-37.5428611532005,-1.79736271150026,
125.277922643415));
#201511=CARTESIAN_POINT('Ctrl Pts',(-37.8213087770133,-5.62106723310019,
129.329358054928));
#201512=CARTESIAN_POINT('Ctrl Pts',(-38.0997564008263,-4.27928557188161,
134.736248763623));
#201513=CARTESIAN_POINT('Ctrl Pts',(-38.3782040246392,0.994950475174061,
136.529926349506));
#201514=CARTESIAN_POINT('Ctrl Pts',(-38.656651648452,5.35487564157755,133.062088737171));
#201515=CARTESIAN_POINT('Ctrl Pts',(-38.9350992722649,4.79393169358958,
127.51950927907));
#201516=CARTESIAN_POINT('Ctrl Pts',(-39.2135468960779,-0.172401284224016,
124.995547727136));
#201517=CARTESIAN_POINT('Ctrl Pts',(-39.4919945198907,-4.98030590410683,
127.809601445221));
#201518=CARTESIAN_POINT('Ctrl Pts',(-39.7704421437036,-5.21155269958477,
133.375692540572));
#201519=CARTESIAN_POINT('Ctrl Pts',(-40.0488897675166,-0.65363716264763,
136.578855215227));
#201520=CARTESIAN_POINT('Ctrl Pts',(-40.3273373913294,4.50493899481217,
134.475539454375));
#201521=CARTESIAN_POINT('Ctrl Pts',(-40.6057850151423,5.52369629454426,
128.998589689552));
#201522=CARTESIAN_POINT('Ctrl Pts',(-40.8842326389552,1.46644654715595,
125.181055190758));
#201523=CARTESIAN_POINT('Ctrl Pts',(-41.1626802627681,-3.93839593717207,
126.531063665459));
#201524=CARTESIAN_POINT('Ctrl Pts',(-41.441127886581,-5.72404495657686,
131.808023276983));
#201525=CARTESIAN_POINT('Ctrl Pts',(-41.7195755103939,-2.24957629602936,
136.162665936149));
#201526=CARTESIAN_POINT('Ctrl Pts',(-41.9980231342068,3.29214308265742,
135.593287775304));
#201527=CARTESIAN_POINT('Ctrl Pts',(-42.2764707580197,5.80854379851262,
130.623119508596));
#201528=CARTESIAN_POINT('Ctrl Pts',(-42.5549183818325,2.98717652667487,
125.81950296691));
#201529=CARTESIAN_POINT('Ctrl Pts',(-42.8333660056454,-2.57926004149102,
125.596727082342));
#201530=CARTESIAN_POINT('Ctrl Pts',(-43.1118136294584,-5.7754826353847,
130.159512009603));
#201531=CARTESIAN_POINT('Ctrl Pts',(-43.3902612532712,-3.66431883537201,
135.314881304976));
#201532=CARTESIAN_POINT('Ctrl Pts',(-43.6687088770841,1.81417496242045,
136.325302439805));
#201533=CARTESIAN_POINT('Ctrl Pts',(-43.947156500897,5.62553059712261,132.262247752997));
#201534=CARTESIAN_POINT('Ctrl Pts',(-44.2256041247099,4.26729843551711,
126.859466010475));
#201535=CARTESIAN_POINT('Ctrl Pts',(-44.5040517485228,-1.01237251921066,
125.081849693053));
#201536=CARTESIAN_POINT('Ctrl Pts',(-44.7824993723357,-5.3617225859308,
128.562941355057));
#201537=CARTESIAN_POINT('Ctrl Pts',(-45.0609469961486,-4.78391153089065,
134.103787819889));
#201538=CARTESIAN_POINT('Ctrl Pts',(-45.3393946199614,0.190080513966956,
136.612621871764));
#201539=CARTESIAN_POINT('Ctrl Pts',(-45.6178422437743,4.98939785243841,
133.783947580368));
#201540=CARTESIAN_POINT('Ctrl Pts',(-45.8962898675873,5.20370231015464,
128.217178431071));
#201541=CARTESIAN_POINT('Ctrl Pts',(-46.1747374914001,0.636058559829223,
125.027903320286));
#201542=CARTESIAN_POINT('Ctrl Pts',(-46.453185115213,-4.51609193379101,
127.146910270074));
#201543=CARTESIAN_POINT('Ctrl Pts',(-46.7316327390259,-5.51817456361365,
132.626935412823));
#201544=CARTESIAN_POINT('Ctrl Pts',(-47.0100803628388,-1.4493243472895,
136.43210335646));
#201545=CARTESIAN_POINT('Ctrl Pts',(-47.2885279866517,3.95138414076325,
135.06565065357));
#201546=CARTESIAN_POINT('Ctrl Pts',(-47.5669756104645,5.72096363930122,
129.783280583183));
#201547=CARTESIAN_POINT('Ctrl Pts',(-47.8454232342775,2.23325703793269,
125.439233181862));
#201548=CARTESIAN_POINT('Ctrl Pts',(-48.1238708580903,-3.30670368062431,
126.025475792906));
#201549=CARTESIAN_POINT('Ctrl Pts',(-48.4023184819033,-5.80796525814313,
131.00328009631));
#201550=CARTESIAN_POINT('Ctrl Pts',(-48.6807661057162,-2.97199049830493,
135.798287116504));
#201551=CARTESIAN_POINT('Ctrl Pts',(-48.9592137295291,2.59509833966803,
136.004119651047));
#201552=CARTESIAN_POINT('Ctrl Pts',(-49.2376613533419,5.77741858108801,
131.431627656171));
#201553=CARTESIAN_POINT('Ctrl Pts',(-49.5161089771548,3.65057338907646,
126.282707896514));
#201554=CARTESIAN_POINT('Ctrl Pts',(-49.7945566009678,-1.8309704070716,
125.288966092489));
#201555=CARTESIAN_POINT('Ctrl Pts',(-50.0730042247805,-5.62994184699806,
129.363602415007));
#201556=CARTESIAN_POINT('Ctrl Pts',(-50.3514518485936,-4.25527176748286,
134.762225140725));
#201557=CARTESIAN_POINT('Ctrl Pts',(-50.6298994724063,1.02978518476655,
136.52376372209));
#201558=CARTESIAN_POINT('Ctrl Pts',(-50.9083470962193,5.36851986001845,
133.029450258773));
#201559=CARTESIAN_POINT('Ctrl Pts',(-51.1867947200322,4.77384705068883,
127.490388116857));
#201560=CARTESIAN_POINT('Ctrl Pts',(-51.465242343845,-0.207757982829986,
124.996704806535));
#201561=CARTESIAN_POINT('Ctrl Pts',(-51.743689967658,-4.99844357966987,
127.839973466791));
#201562=CARTESIAN_POINT('Ctrl Pts',(-52.0221375914708,-5.19580371433717,
133.407369100245));
#201563=CARTESIAN_POINT('Ctrl Pts',(-52.3005852152837,-0.618474064651215,
136.58272710215));
#201564=CARTESIAN_POINT('Ctrl Pts',(-52.5790328390967,4.52720303631132,
134.448048593619));
#201565=CARTESIAN_POINT('Ctrl Pts',(-52.8574804629095,5.51260171306762,
128.964998839148));
#201566=CARTESIAN_POINT('Ctrl Pts',(-53.1359280867224,1.43218872108006,
125.172232701224));
#201567=CARTESIAN_POINT('Ctrl Pts',(-53.4143757105353,-3.96433573927151,
126.555116973674));
#201568=CARTESIAN_POINT('Ctrl Pts',(-53.6928233343482,-5.71782932379997,
131.842848567767));
#201569=CARTESIAN_POINT('Ctrl Pts',(-53.9712709581611,-2.21691709124776,
136.176260468582));
#201570=CARTESIAN_POINT('Ctrl Pts',(-54.249718581974,3.32123364574025,135.573158838211));
#201571=CARTESIAN_POINT('Ctrl Pts',(-54.5281662057869,5.80733291357678,
130.58776461181));
#201572=CARTESIAN_POINT('Ctrl Pts',(-54.8066138295998,2.95677693782102,
125.801411533396));
#201573=CARTESIAN_POINT('Ctrl Pts',(-55.0850614534126,-2.61091259720856,
125.612524255684));
#201574=CARTESIAN_POINT('Ctrl Pts',(-55.3635090772256,-5.77930100557468,
130.194680959234));
#201575=CARTESIAN_POINT('Ctrl Pts',(-55.6419567010384,-3.63679412436797,
135.337103484283));
#201576=CARTESIAN_POINT('Ctrl Pts',(-55.9204043248514,1.8477488898629,136.314156751619));
#201577=CARTESIAN_POINT('Ctrl Pts',(-56.1988519486642,5.63430094186134,
132.227976540264));
#201578=CARTESIAN_POINT('Ctrl Pts',(-56.4772995724772,4.24320567919224,
126.833562843453));
#201579=CARTESIAN_POINT('Ctrl Pts',(-56.7557471962901,-1.04718831053316,
125.088118316796));
#201580=CARTESIAN_POINT('Ctrl Pts',(-57.0341948201028,-5.3752674008715,
128.595621210585));
#201581=CARTESIAN_POINT('Ctrl Pts',(-57.3126424439159,-4.76373834622006,
134.13284771647));
#201582=CARTESIAN_POINT('Ctrl Pts',(-57.5910900677287,0.225433527051438,
136.611357184097));
#201583=CARTESIAN_POINT('Ctrl Pts',(-57.8695376915416,5.00744300200284,
133.753520494635));
#201584=CARTESIAN_POINT('Ctrl Pts',(-58.1479853153544,5.18785698530388,
128.185549952615));
#201585=CARTESIAN_POINT('Ctrl Pts',(-58.4264329391674,0.600883840013963,
125.024138475672));
#201586=CARTESIAN_POINT('Ctrl Pts',(-58.7048805629802,-4.53827219944114,
127.174468767579));
#201587=CARTESIAN_POINT('Ctrl Pts',(-58.9833281867932,-5.5069777945324,
132.660492339548));
#201588=CARTESIAN_POINT('Ctrl Pts',(-59.261775810606,-1.41503982726995,
136.440821536091));
#201589=CARTESIAN_POINT('Ctrl Pts',(-59.540223434419,3.97725061271504,135.041518504932));
#201590=CARTESIAN_POINT('Ctrl Pts',(-59.8186710582318,5.71464203910897,
129.748474371954));
#201591=CARTESIAN_POINT('Ctrl Pts',(-60.0971186820448,2.20055660734573,
125.425738115783));
#201592=CARTESIAN_POINT('Ctrl Pts',(-60.3755663058576,-3.3357328434014,
126.045693178431));
#201593=CARTESIAN_POINT('Ctrl Pts',(-60.6540139296705,-5.80664677067165,
131.038631143817));
#201594=CARTESIAN_POINT('Ctrl Pts',(-60.9324615534834,-2.94153598615947,
135.816285940328));
#201595=CARTESIAN_POINT('Ctrl Pts',(-61.2109091772963,2.62670266761142,
135.988226211385));
#201596=CARTESIAN_POINT('Ctrl Pts',(-61.4893568011092,5.78112989140647,
131.396447247635));
#201597=CARTESIAN_POINT('Ctrl Pts',(-61.767804424922,3.62298116889529,126.260569595891));
#201598=CARTESIAN_POINT('Ctrl Pts',(-62.046252048735,-1.86451025536104,
125.300213916535));
#201599=CARTESIAN_POINT('Ctrl Pts',(-62.3246996725479,-5.63860784133039,
129.39790016291));
#201600=CARTESIAN_POINT('Ctrl Pts',(-62.6031472963608,-4.23110028242386,
134.788054857702));
#201601=CARTESIAN_POINT('Ctrl Pts',(-62.8815949201736,1.0645817352901,136.517389160091));
#201602=CARTESIAN_POINT('Ctrl Pts',(-63.1600425439866,5.38196514598156,
132.99672932886));
#201603=CARTESIAN_POINT('Ctrl Pts',(-63.4384901677994,4.75358551113023,
127.461389755115));
#201604=CARTESIAN_POINT('Ctrl Pts',(-63.7169377916123,-0.243106982887504,
124.998077090756));
#201605=CARTESIAN_POINT('Ctrl Pts',(-63.9953854154252,-5.0163960360679,
127.870455334816));
#201606=CARTESIAN_POINT('Ctrl Pts',(-64.2738330392381,-5.17986219667218,
133.438949204482));
#201607=CARTESIAN_POINT('Ctrl Pts',(-64.552280663051,-0.583288048870894,
136.586384869579));
#201608=CARTESIAN_POINT('Ctrl Pts',(-64.8307282868638,4.54929932063727,
134.420422714664));
#201609=CARTESIAN_POINT('Ctrl Pts',(-65.1091759106768,5.50130286010717,
128.93147614697));
#201610=CARTESIAN_POINT('Ctrl Pts',(-65.3876235344896,1.39787782472419,
125.16361891226));
#201611=CARTESIAN_POINT('Ctrl Pts',(-65.6660711583025,-3.99012864145221,
126.579327739175));
#201612=CARTESIAN_POINT('Ctrl Pts',(-65.9445187821156,-5.71140181475477,
131.877635376998));
#201613=CARTESIAN_POINT('Ctrl Pts',(-66.2229664059283,-2.18417573778792,
136.189655943291));
#201614=CARTESIAN_POINT('Ctrl Pts',(-66.5014140297413,3.35020113928917,
135.552853191544));
#201615=CARTESIAN_POINT('Ctrl Pts',(-66.7798616535541,5.80590683578406,
130.552417741069));
#201616=CARTESIAN_POINT('Ctrl Pts',(-67.0583092773671,2.92626778451039,
125.783505486001));
#201617=CARTESIAN_POINT('Ctrl Pts',(-67.3367569011799,-2.64246840459962,
125.628513814431));
#201618=CARTESIAN_POINT('Ctrl Pts',(-67.6152045249929,-5.78290522164069,
130.229872500769));
#201619=CARTESIAN_POINT('Ctrl Pts',(-67.8936521488056,-3.60913465062,135.359157701137));
#201620=CARTESIAN_POINT('Ctrl Pts',(-68.1720997726187,1.88125434829088,
136.302806895912));
#201621=CARTESIAN_POINT('Ctrl Pts',(-68.4505473964314,5.64286250550667,
132.193652574919));
#201622=CARTESIAN_POINT('Ctrl Pts',(-68.7289950202444,4.21895568932047,
126.807806815805));
#201623=CARTESIAN_POINT('Ctrl Pts',(-69.0074426440573,-1.08196529790749,
125.094598758));
#201624=CARTESIAN_POINT('Ctrl Pts',(-69.2858902678701,-5.38861303330182,
128.628382911763));
#201625=CARTESIAN_POINT('Ctrl Pts',(-69.564337891683,-4.74338863947339,
134.161784274737));
#201626=CARTESIAN_POINT('Ctrl Pts',(-69.8427855154959,0.260778186613682,
136.609877316035));
#201627=CARTESIAN_POINT('Ctrl Pts',(-70.1212331393089,5.02530259892534,
133.722984126697));
#201628=CARTESIAN_POINT('Ctrl Pts',(-70.3996807631217,5.17181942250469,
128.154018515153));
#201629=CARTESIAN_POINT('Ctrl Pts',(-70.6781283869345,0.5656868542273,125.020587819316));
#201630=CARTESIAN_POINT('Ctrl Pts',(-70.9565760107477,-4.56028429774593,
127.202161772061));
#201631=CARTESIAN_POINT('Ctrl Pts',(-71.2350236345604,-5.49557696236377,
132.693980486629));
#201632=CARTESIAN_POINT('Ctrl Pts',(-71.5134712583732,-1.38070287242923,
136.449330854589));
#201633=CARTESIAN_POINT('Ctrl Pts',(-71.7919188821862,4.00296970618273,
135.017229346852));
#201634=CARTESIAN_POINT('Ctrl Pts',(-72.0703665059991,5.70810868075446,
129.71370728698));
#201635=CARTESIAN_POINT('Ctrl Pts',(-72.348814129812,2.16777463432419,125.412442356538));
#201636=CARTESIAN_POINT('Ctrl Pts',(-72.6272617536249,-3.36463839937136,
126.06608689813));
#201637=CARTESIAN_POINT('Ctrl Pts',(-72.9057093774378,-5.80511311576878,
131.073973510343));
#201638=CARTESIAN_POINT('Ctrl Pts',(-73.1841570012506,-2.91097247431594,
135.834099045416));
#201639=CARTESIAN_POINT('Ctrl Pts',(-73.4626046250635,2.65820966212185,
135.972140681676));
#201640=CARTESIAN_POINT('Ctrl Pts',(-73.7410522488765,5.78462697983096,
131.361244899111));
#201641=CARTESIAN_POINT('Ctrl Pts',(-74.0194998726893,3.59525469781404,
126.238599667113));
#201642=CARTESIAN_POINT('Ctrl Pts',(-74.2979474965022,-1.89798101353784,
125.31166569876));
#201643=CARTESIAN_POINT('Ctrl Pts',(-74.5763951203151,-5.64706489497548,
129.432250027724));
#201644=CARTESIAN_POINT('Ctrl Pts',(-74.854842744128,-4.20677201238788,
134.813736957424));
#201645=CARTESIAN_POINT('Ctrl Pts',(-75.1332903679409,1.09933883734644,
136.510802899716));
#201646=CARTESIAN_POINT('Ctrl Pts',(-75.4117379917539,5.39521100124704,
132.963927159917));
#201647=CARTESIAN_POINT('Ctrl Pts',(-75.6901856155667,4.73314782571214,
127.432515268386));
#201648=CARTESIAN_POINT('Ctrl Pts',(-75.9686332393795,-0.278446974526432,
124.99966452895));
#201649=CARTESIAN_POINT('Ctrl Pts',(-76.2470808631926,-5.03416260806588,
127.901045919781));
#201650=CARTESIAN_POINT('Ctrl Pts',(-76.5255284870053,-5.16372873730878,
133.470431683069));
#201651=CARTESIAN_POINT('Ctrl Pts',(-76.8039761108183,-0.548080419137594,
136.589828381972));
#201652=CARTESIAN_POINT('Ctrl Pts',(-77.0824237346311,4.57122702900371,
134.392662841198));
#201653=CARTESIAN_POINT('Ctrl Pts',(-77.360871358444,5.48980015434633,128.898022855216));
#201654=CARTESIAN_POINT('Ctrl Pts',(-77.639318982257,1.36351512949127,125.155214143056));
#201655=CARTESIAN_POINT('Ctrl Pts',(-77.9177666060698,-4.0157736879487,
126.603695064822));
#201656=CARTESIAN_POINT('Ctrl Pts',(-78.1962142298826,-5.70476266761487,
131.91238241564));
#201657=CARTESIAN_POINT('Ctrl Pts',(-78.4746618536957,-2.15135344889296,
136.202851863901));
#201658=CARTESIAN_POINT('Ctrl Pts',(-78.7531094775085,3.37904448990285,
135.532371587738));
#201659=CARTESIAN_POINT('Ctrl Pts',(-79.0315571013213,5.8042656179783,130.517080206165));
#201660=CARTESIAN_POINT('Ctrl Pts',(-79.3100047251342,2.8956501972711,125.765785488239));
#201661=CARTESIAN_POINT('Ctrl Pts',(-79.5884523489472,-2.67392629435197,
125.644695166086));
#201662=CARTESIAN_POINT('Ctrl Pts',(-79.8668999727601,-5.78629515002701,
130.265085330171));
#201663=CARTESIAN_POINT('Ctrl Pts',(-80.1453475965729,-3.58134143906054,
135.38104313831));
#201664=CARTESIAN_POINT('Ctrl Pts',(-80.4237952203859,1.91469009614739,
136.291253293255));
#201665=CARTESIAN_POINT('Ctrl Pts',(-80.7022428441988,5.65121497080658,
132.15927712885));
#201666=CARTESIAN_POINT('Ctrl Pts',(-80.9806904680116,4.19454936449412,
126.782198881926));
#201667=CARTESIAN_POINT('Ctrl Pts',(-81.2591380918246,-1.11670219266007,
125.10129077653));
#201668=CARTESIAN_POINT('Ctrl Pts',(-81.5375857156372,-5.40175898869456,
128.661225244595));
#201669=CARTESIAN_POINT('Ctrl Pts',(-81.8160333394505,-4.72286316471603,
134.190596422436));
#201670=CARTESIAN_POINT('Ctrl Pts',(-82.0944809632629,0.296113182944105,
136.608182322418));
#201671=CARTESIAN_POINT('Ctrl Pts',(-82.3729285870762,5.04297598141181,
133.692339608092));
#201672=CARTESIAN_POINT('Ctrl Pts',(-82.6513762108889,5.15559021603496,
128.122585287091));
#201673=CARTESIAN_POINT('Ctrl Pts',(-82.9298238347018,0.530468906706182,
125.017251482786));
#201674=CARTESIAN_POINT('Ctrl Pts',(-83.2082714585147,-4.58212741303929,
127.229988257347));
#201675=CARTESIAN_POINT('Ctrl Pts',(-83.4867190823277,-5.48397248956967,
132.72739861315));
#201676=CARTESIAN_POINT('Ctrl Pts',(-83.7651667061405,-1.34631475513585,
136.45763099664));
#201677=CARTESIAN_POINT('Ctrl Pts',(-84.0436143299535,4.02854046813582,
134.992784079373));
#201678=CARTESIAN_POINT('Ctrl Pts',(-84.3220619537663,5.70136380633342,
129.678980616565));
#201679=CARTESIAN_POINT('Ctrl Pts',(-84.6005095775792,2.13491233361711,
125.399346396808));
#201680=CARTESIAN_POINT('Ctrl Pts',(-84.8789572013921,-3.39341927742779,
126.086656196302));
#201681=CARTESIAN_POINT('Ctrl Pts',(-85.1574048252049,-5.80336435026449,
131.109305886265));
#201682=CARTESIAN_POINT('Ctrl Pts',(-85.4358524490179,-2.88030109531746,
135.851725771696));
#201683=CARTESIAN_POINT('Ctrl Pts',(-85.7143000728307,2.68961815569484,
135.955863657977));
#201684=CARTESIAN_POINT('Ctrl Pts',(-85.9927476966438,5.78790971677558,
131.326021915035));
#201685=CARTESIAN_POINT('Ctrl Pts',(-86.2711953204564,3.56739500324825,
126.216798924288));
#201686=CARTESIAN_POINT('Ctrl Pts',(-86.5496429442695,-1.93138144132926,
125.323321014816));
#201687=CARTESIAN_POINT('Ctrl Pts',(-86.8280905680822,-5.65531269455438,
129.466650736599));
#201688=CARTESIAN_POINT('Ctrl Pts',(-87.1065381918953,-4.18228785886808,
134.83927048823));
#201689=CARTESIAN_POINT('Ctrl Pts',(-87.3849858157081,1.13405520299706,
136.504005185026));
#201690=CARTESIAN_POINT('Ctrl Pts',(-87.663433439521,5.40825693498488,132.931044967442));
#201691=CARTESIAN_POINT('Ctrl Pts',(-87.9418810633338,4.71253475176078,
127.403765726628));
#201692=CARTESIAN_POINT('Ctrl Pts',(-88.2203286871468,-0.313776648210234,
125.00146706229));
#201693=CARTESIAN_POINT('Ctrl Pts',(-88.4987763109598,-5.05174263731727,
127.931744088139));
#201694=CARTESIAN_POINT('Ctrl Pts',(-88.7772239347726,-5.14740393407785,
133.501815369412));
#201695=CARTESIAN_POINT('Ctrl Pts',(-89.0556715585855,-0.512852480082647,
136.593057511728));
#201696=CARTESIAN_POINT('Ctrl Pts',(-89.3341191823985,4.59298534887173,
134.364770001874));
#201697=CARTESIAN_POINT('Ctrl Pts',(-89.6125668062112,5.47809402202166,
128.864640203508));
#201698=CARTESIAN_POINT('Ctrl Pts',(-89.8910144300243,1.32910190870433,
125.147018705051));
#201699=CARTESIAN_POINT('Ctrl Pts',(-90.169462053837,-4.04126992847403,
126.628218047677));
#201700=CARTESIAN_POINT('Ctrl Pts',(-90.44790967765,-5.69791212839678,131.947088396125));
#201701=CARTESIAN_POINT('Ctrl Pts',(-90.7263573014627,-2.1184514408047,
136.215847741432));
#201702=CARTESIAN_POINT('Ctrl Pts',(-91.0048049252757,3.40776262878029,
135.511714785749));
#201703=CARTESIAN_POINT('Ctrl Pts',(-91.2832525490887,5.80240932097568,
130.48175331654));
#201704=CARTESIAN_POINT('Ctrl Pts',(-91.5617001729014,2.86492531064864,
125.748252196732));
#201705=CARTESIAN_POINT('Ctrl Pts',(-91.8401477967144,-2.70528510078237,
125.661067711041));
#201706=CARTESIAN_POINT('Ctrl Pts',(-92.1185954205271,-5.78947066511866,
130.30031814262));
#201707=CARTESIAN_POINT('Ctrl Pts',(-92.3970430443404,-3.55341551957677,
135.402758984829));
#201708=CARTESIAN_POINT('Ctrl Pts',(-92.6754906681528,1.94805489445803,
136.279496371773));
#201709=CARTESIAN_POINT('Ctrl Pts',(-92.9539382919661,5.6593580282576,132.124851475851));
#201710=CARTESIAN_POINT('Ctrl Pts',(-93.2323859157787,4.16998760909852,
126.75673999073));
#201711=CARTESIAN_POINT('Ctrl Pts',(-93.5108335395918,-1.15139770760221,
125.10819412441));
#201712=CARTESIAN_POINT('Ctrl Pts',(-93.7892811634045,-5.41470477992152,
128.694146992097));
#201713=CARTESIAN_POINT('Ctrl Pts',(-94.0677287872175,-4.70216268252734,
134.219283091922));
#201714=CARTESIAN_POINT('Ctrl Pts',(-94.3461764110305,0.331437206691851,
136.606272266052));
#201715=CARTESIAN_POINT('Ctrl Pts',(-94.6246240348431,5.0604624945689,133.661588074364));
#201716=CARTESIAN_POINT('Ctrl Pts',(-94.9030716586564,5.13916996727372,
128.0912514332));
#201717=CARTESIAN_POINT('Ctrl Pts',(-95.1815192824688,0.495231302464415,
125.014129589715));
#201718=CARTESIAN_POINT('Ctrl Pts',(-95.459966906282,-4.60380073591605,
127.257947192314));
#201719=CARTESIAN_POINT('Ctrl Pts',(-95.7384145300948,-5.47216480615837,
132.760745480792));
#201720=CARTESIAN_POINT('Ctrl Pts',(-96.0168621539077,-1.31187674965409,
136.465721654678));
#201721=CARTESIAN_POINT('Ctrl Pts',(-96.2953097777207,4.05396195104042,
134.96818360832));
#201722=CARTESIAN_POINT('Ctrl Pts',(-96.5737574015334,5.69440766577999,
129.64429564752));
#201723=CARTESIAN_POINT('Ctrl Pts',(-96.8522050253465,2.10197092294792,
125.386450721867));
#201724=CARTESIAN_POINT('Ctrl Pts',(-97.1306526491593,-3.42207441108517,
126.107400310748));
#201725=CARTESIAN_POINT('Ctrl Pts',(-97.4091002729722,-5.80140053895979,
131.144626962327));
#201726=CARTESIAN_POINT('Ctrl Pts',(-97.6875478967851,-2.8495229857029,
135.869165466005));
#201727=CARTESIAN_POINT('Ctrl Pts',(-97.965995520598,2.72092698447821,135.93939574344));
#201728=CARTESIAN_POINT('Ctrl Pts',(-98.2444431444108,5.79097798059694,
131.290779600608));
#201729=CARTESIAN_POINT('Ctrl Pts',(-98.5228907682237,3.53940311754856,
126.195168175249));
#201730=CARTESIAN_POINT('Ctrl Pts',(-98.8013383920368,-1.96471030107164,
125.33517943281));
#201731=CARTESIAN_POINT('Ctrl Pts',(-99.0797860158496,-5.6633509344415,
129.501101014807));
#201732=CARTESIAN_POINT('Ctrl Pts',(-99.3582336396624,-4.15764872913354,
134.864654503967));
#201733=CARTESIAN_POINT('Ctrl Pts',(-99.6366812634755,1.16872954581563,
136.496996267908));
#201734=CARTESIAN_POINT('Ctrl Pts',(-99.9151288872883,5.42110246377302,
132.898083969897));
#201735=CARTESIAN_POINT('Ctrl Pts',(-100.193576511101,4.69174705310118,
127.375142195163));
#201736=CARTESIAN_POINT('Ctrl Pts',(-100.472024134914,-0.34909469478497,
125.003484623986));
#201737=CARTESIAN_POINT('Ctrl Pts',(-100.750471758727,-5.06913547238742,
127.96254870236));
#201738=CARTESIAN_POINT('Ctrl Pts',(-101.02891938254,-5.13088839190121,
133.533099100579));
#201739=CARTESIAN_POINT('Ctrl Pts',(-101.307367006353,-0.47760553709043,
136.596072139193));
#201740=CARTESIAN_POINT('Ctrl Pts',(-101.585814630166,4.61457347397855,
134.33674523027));
#201741=CARTESIAN_POINT('Ctrl Pts',(-101.864262253979,5.46618489690847,
128.831329428852));
#201742=CARTESIAN_POINT('Ctrl Pts',(-102.142709877791,1.29463943755703,
125.139032901931));
#201743=CARTESIAN_POINT('Ctrl Pts',(-102.421157501604,-4.06661641825637,
126.652895779031));
#201744=CARTESIAN_POINT('Ctrl Pts',(-102.699605125417,-5.69085045094906,
131.981752032413));
#201745=CARTESIAN_POINT('Ctrl Pts',(-102.97805274923,-2.08547093271925,
136.228643094318));
#201746=CARTESIAN_POINT('Ctrl Pts',(-103.256500373043,3.43635449176034,
135.490883551018));
#201747=CARTESIAN_POINT('Ctrl Pts',(-103.534947996856,5.80033801356182,
130.446438381249));
#201748=CARTESIAN_POINT('Ctrl Pts',(-103.813395620669,2.83409426316523,
125.730906261181));
#201749=CARTESIAN_POINT('Ctrl Pts',(-104.091843244482,-2.73654366187847,
125.677630842606));
#201750=CARTESIAN_POINT('Ctrl Pts',(-104.370290868295,-5.79243164924577,
130.335569632546));
#201751=CARTESIAN_POINT('Ctrl Pts',(-104.648738492108,-3.52535792697413,
135.424304436005));
#201752=CARTESIAN_POINT('Ctrl Pts',(-104.92718611592,1.98134750687769,136.267536567122));
#201753=CARTESIAN_POINT('Ctrl Pts',(-105.205633739733,5.66729137611554,
132.090376891579));
#201754=CARTESIAN_POINT('Ctrl Pts',(-105.484081363546,4.14527133327901,
126.731431085605));
#201755=CARTESIAN_POINT('Ctrl Pts',(-105.762528987359,-1.18605055707886,
125.115308545834));
#201756=CARTESIAN_POINT('Ctrl Pts',(-106.040976611172,-5.42744992727162,
128.72714693434));
#201757=CARTESIAN_POINT('Ctrl Pts',(-106.319424234985,-4.68128795997122,
134.247843220201));
#201758=CARTESIAN_POINT('Ctrl Pts',(-106.597871858798,0.366748948912009,
136.604147217717));
#201759=CARTESIAN_POINT('Ctrl Pts',(-106.876319482611,5.07776149042729,
133.630730665021));
#201760=CARTESIAN_POINT('Ctrl Pts',(-107.154767106424,5.12255928467941,
128.060018114567));
#201761=CARTESIAN_POINT('Ctrl Pts',(-107.433214730236,0.45997534724462,
125.011222255784));
#201762=CARTESIAN_POINT('Ctrl Pts',(-107.711662354049,-4.62530346326349,
127.286037540936));
#201763=CARTESIAN_POINT('Ctrl Pts',(-107.990109977862,-5.46015434966779,
132.794019853873));
#201764=CARTESIAN_POINT('Ctrl Pts',(-108.268557601675,-1.2773901320969,
136.473602528901));
#201765=CARTESIAN_POINT('Ctrl Pts',(-108.547005225488,4.07923321289408,
134.943428845277));
#201766=CARTESIAN_POINT('Ctrl Pts',(-108.825452849301,5.6872405168564,129.609653665109));
#201767=CARTESIAN_POINT('Ctrl Pts',(-109.103900473114,2.06895162297316,
125.373755809571));
#201768=CARTESIAN_POINT('Ctrl Pts',(-109.382348096927,-3.45060273851677,
126.128318472786));
#201769=CARTESIAN_POINT('Ctrl Pts',(-109.66079572074,-5.79922175462486,
131.179935429694));
#201770=CARTESIAN_POINT('Ctrl Pts',(-109.939243344552,-2.81863928596571,
135.886417482107));
#201771=CARTESIAN_POINT('Ctrl Pts',(-110.217690968365,2.7521349883118,135.922737548286));
#201772=CARTESIAN_POINT('Ctrl Pts',(-110.496138592178,5.79383165759959,
131.255519261747));
#201773=CARTESIAN_POINT('Ctrl Pts',(-110.774586215991,3.51128007796473,
126.17370822153));
#201774=CARTESIAN_POINT('Ctrl Pts',(-111.053033839804,-1.99796635775128,
125.347240513325));
#201775=CARTESIAN_POINT('Ctrl Pts',(-111.331481463617,-5.67117931677705,
129.535599585778));
#201776=CARTESIAN_POINT('Ctrl Pts',(-111.60992908743,-4.13285553619637,
134.889888064022));
#201777=CARTESIAN_POINT('Ctrl Pts',(-111.888376711243,1.20336058093108,
136.489776408084));
#201778=CARTESIAN_POINT('Ctrl Pts',(-112.166824335056,5.43374711161577,
132.865045388662));
#201779=CARTESIAN_POINT('Ctrl Pts',(-112.445271958868,4.67078550002918,
127.34664573465));
#201780=CARTESIAN_POINT('Ctrl Pts',(-112.723719582681,-0.384399805526852,
125.005717139274));
#201781=CARTESIAN_POINT('Ctrl Pts',(-113.002167206494,-5.08634046877848,
127.993458620965));
#201782=CARTESIAN_POINT('Ctrl Pts',(-113.280614830307,-5.11418272276831,
133.564281717336));
#201783=CARTESIAN_POINT('Ctrl Pts',(-113.55906245412,-0.442340896249408,
136.598872152659));
#201784=CARTESIAN_POINT('Ctrl Pts',(-113.837510077933,4.63599060436829,
134.308589564856));
#201785=CARTESIAN_POINT('Ctrl Pts',(-114.115957701746,5.45407322030374,
128.798091765594));
#201786=CARTESIAN_POINT('Ctrl Pts',(-114.394405325558,1.26012899306928,
125.131257029612));
#201787=CARTESIAN_POINT('Ctrl Pts',(-114.672852949372,-4.09181221807183,
126.677727344441));
#201788=CARTESIAN_POINT('Ctrl Pts',(-114.951300573184,-5.68357789694507,
132.016372040028));
#201789=CARTESIAN_POINT('Ctrl Pts',(-115.229748196997,-2.05241314674147,
136.241237448422));
#201790=CARTESIAN_POINT('Ctrl Pts',(-115.50819582081,3.46481901936097,135.469878655457));
#201791=CARTESIAN_POINT('Ctrl Pts',(-115.786643444623,5.79805177248978,
130.411136708898));
#201792=CARTESIAN_POINT('Ctrl Pts',(-116.065091068436,2.80315819727665,
125.713748324348));
#201793=CARTESIAN_POINT('Ctrl Pts',(-116.343538692249,-2.76770081934284,
125.694383947029));
#201794=CARTESIAN_POINT('Ctrl Pts',(-116.621986316062,-5.79517799268792,
130.370838493694));
#201795=CARTESIAN_POINT('Ctrl Pts',(-116.900433939875,-3.49716970093708,
135.445678693465));
#201796=CARTESIAN_POINT('Ctrl Pts',(-117.178881563688,2.0145666997373,136.255374322477));
#201797=CARTESIAN_POINT('Ctrl Pts',(-117.4573291875,5.67501472040751,132.055854653499));
#201798=CARTESIAN_POINT('Ctrl Pts',(-117.735776811314,4.12040145290537,
126.706273104381));
#201799=CARTESIAN_POINT('Ctrl Pts',(-118.014224435126,-1.22065945701595,
125.122633777175));
#201800=CARTESIAN_POINT('Ctrl Pts',(-118.29267205894,-5.43999395846872,
128.760223848501));
#201801=CARTESIAN_POINT('Ctrl Pts',(-118.571119682752,-4.6602397705682,
134.276275748964));
#201802=CARTESIAN_POINT('Ctrl Pts',(-118.849567306565,0.402047101114997,
136.601807256156));
#201803=CARTESIAN_POINT('Ctrl Pts',(-119.128014930377,5.09487232796628,
133.599768523497));
#201804=CARTESIAN_POINT('Ctrl Pts',(-119.406462554191,5.10575878376697,
128.028886488555));
#201805=CARTESIAN_POINT('Ctrl Pts',(-119.684910178003,0.424702347469154,
125.008529588725));
#201806=CARTESIAN_POINT('Ctrl Pts',(-119.963357801817,-4.64663479828973,
127.314258262312));
#201807=CARTESIAN_POINT('Ctrl Pts',(-120.241805425629,-5.44794156515001,
132.827220499399));
#201808=CARTESIAN_POINT('Ctrl Pts',(-120.520253049442,-1.24285618037906,
136.48127332728));
#201809=CARTESIAN_POINT('Ctrl Pts',(-120.798700673255,4.10435331726091,
134.918520707537));
#201810=CARTESIAN_POINT('Ctrl Pts',(-121.077148297068,5.67986262514396,
129.575055953004));
#201811=CARTESIAN_POINT('Ctrl Pts',(-121.355595920881,2.03585565723516,
125.361262130332));
#201812=CARTESIAN_POINT('Ctrl Pts',(-121.634043544694,-3.47900320259493,
126.149409907283));
#201813=CARTESIAN_POINT('Ctrl Pts',(-121.912491168507,-5.79682807799514,
131.215229979999));
#201814=CARTESIAN_POINT('Ctrl Pts',(-122.19093879232,-2.78765114051323,
135.903481180724));
#201815=CARTESIAN_POINT('Ctrl Pts',(-122.469386416133,2.78324101077128,
135.905889689793));
#201816=CARTESIAN_POINT('Ctrl Pts',(-122.747834039945,5.79647064203949,
131.220242205036));
#201817=CARTESIAN_POINT('Ctrl Pts',(-123.026281663758,3.48302692660634,
126.152419858339));
#201818=CARTESIAN_POINT('Ctrl Pts',(-123.304729287571,-2.03114837905279,
125.359503809431));
#201819=CARTESIAN_POINT('Ctrl Pts',(-123.583176911384,-5.67879755147744,
129.570145171156));
#201820=CARTESIAN_POINT('Ctrl Pts',(-123.861624535197,-4.10790919877744,
134.914970233354));
#201821=CARTESIAN_POINT('Ctrl Pts',(-124.14007215901,1.23794702507767,136.482345873087));
#201822=CARTESIAN_POINT('Ctrl Pts',(-124.418519782823,5.44619040996103,
132.831930447996));
#201823=CARTESIAN_POINT('Ctrl Pts',(-124.696967406636,4.64965086928273,
127.318277401031));
#201824=CARTESIAN_POINT('Ctrl Pts',(-124.975415030448,-0.419690672193134,
125.00816452543));
#201825=CARTESIAN_POINT('Ctrl Pts',(-125.253862654262,-5.10335698895296,
128.024472698579));
#201826=CARTESIAN_POINT('Ctrl Pts',(-125.532310278074,-5.09728754571388,
133.595362064203));
#201827=CARTESIAN_POINT('Ctrl Pts',(-125.810757901887,-0.407059864303788,
136.601457448367));
#201828=CARTESIAN_POINT('Ctrl Pts',(-126.0892055257,4.65723594642128,134.280304048949));
#201829=CARTESIAN_POINT('Ctrl Pts',(-126.367653149513,5.44175944101008,
128.764928445366));
#201830=CARTESIAN_POINT('Ctrl Pts',(-126.646100773326,1.22557185403828,
125.123691376234));
#201831=CARTESIAN_POINT('Ctrl Pts',(-126.924548397139,-4.11685639428078,
126.702711823764));
#201832=CARTESIAN_POINT('Ctrl Pts',(-127.202996020952,-5.67609473587197,
132.050947136115));
#201833=CARTESIAN_POINT('Ctrl Pts',(-127.481443644765,-2.01927930784003,
136.253630337055));
#201834=CARTESIAN_POINT('Ctrl Pts',(-127.759891268577,3.4931551568182,135.44870087741));
#201835=CARTESIAN_POINT('Ctrl Pts',(-128.038338892391,5.79555068247735,
130.375849607603));
#201836=CARTESIAN_POINT('Ctrl Pts',(-128.316786516203,2.77211825933019,
125.696779022025));
#201837=CARTESIAN_POINT('Ctrl Pts',(-128.595234140016,-2.7987554186355,
125.711326403516));
#201838=CARTESIAN_POINT('Ctrl Pts',(-128.873681763829,-5.79770959367839,
130.406123419165));
#201839=CARTESIAN_POINT('Ctrl Pts',(-129.152129387642,-3.46885188599067,
135.466880965177));
#201840=CARTESIAN_POINT('Ctrl Pts',(-129.430577011455,2.04771124208698,
136.243010088514));
#201841=CARTESIAN_POINT('Ctrl Pts',(-129.709024635268,5.68252777494204,
132.021286040849));
#201842=CARTESIAN_POINT('Ctrl Pts',(-129.98747225908,4.09537888954061,126.681266979298));
#201843=CARTESIAN_POINT('Ctrl Pts',(-130.265919882893,-1.25522312496795,
125.130169546993));
#201844=CARTESIAN_POINT('Ctrl Pts',(-130.544367506706,-5.45233640868912,
128.793376508901));
#201845=CARTESIAN_POINT('Ctrl Pts',(-130.822815130519,-4.63901889426667,
134.304579624636));
#201846=CARTESIAN_POINT('Ctrl Pts',(-131.101262754332,0.437330355314798,
136.599252468079));
#201847=CARTESIAN_POINT('Ctrl Pts',(-131.379710378145,5.11179437313754,
133.568702797104));
#201848=CARTESIAN_POINT('Ctrl Pts',(-131.658158001958,5.08876908708517,
127.997857708758));
#201849=CARTESIAN_POINT('Ctrl Pts',(-131.936605625771,0.389413610192037,
125.006051688315));
#201850=CARTESIAN_POINT('Ctrl Pts',(-132.215053249584,-4.66779395055513,
127.342608310716));
#201851=CARTESIAN_POINT('Ctrl Pts',(-132.493500873397,-5.43552690515385,
132.860346187109));
#201852=CARTESIAN_POINT('Ctrl Pts',(-132.77194849721,-1.20827617416795,
136.488733765571));
#201853=CARTESIAN_POINT('Ctrl Pts',(-133.050396121022,4.12932133330617,
134.893460118082));
#201854=CARTESIAN_POINT('Ctrl Pts',(-133.328843744835,5.67227426403318,
129.540503793235));
#201855=CARTESIAN_POINT('Ctrl Pts',(-133.607291368648,2.00268425211708,
125.348970147109));
#201856=CARTESIAN_POINT('Ctrl Pts',(-133.885738992461,-3.50727475093002,
126.170673832692));
#201857=CARTESIAN_POINT('Ctrl Pts',(-134.164186616274,-5.79421959776922,
131.25050930539));
#201858=CARTESIAN_POINT('Ctrl Pts',(-134.442634240087,-2.75655969762259,
135.920355929551));
#201859=CARTESIAN_POINT('Ctrl Pts',(-134.7210818639,2.81424389921159,135.888852792264));
#201860=CARTESIAN_POINT('Ctrl Pts',(-134.999529487713,5.79889483612785,
131.18494973768));
#201861=CARTESIAN_POINT('Ctrl Pts',(-135.277977111526,3.45464471040472,
126.131303874523));
#201862=CARTESIAN_POINT('Ctrl Pts',(-135.556424735338,-2.06425513540386,
125.371968866708));
#201863=CARTESIAN_POINT('Ctrl Pts',(-135.834872359151,-5.68620535624619,
129.604736490841));
#201864=CARTESIAN_POINT('Ctrl Pts',(-136.113319982964,-4.08281064127246,
134.939900082537));
#201865=CARTESIAN_POINT('Ctrl Pts',(-136.391767606777,1.27248759664198,
136.474704938258));
#201866=CARTESIAN_POINT('Ctrl Pts',(-136.67021523059,5.45843189771781,132.798740374984));
#201867=CARTESIAN_POINT('Ctrl Pts',(-136.948662854403,4.62834394401342,
127.290038245509));
#201868=CARTESIAN_POINT('Ctrl Pts',(-137.227110478216,-0.454965987067202,
125.010826691762));
#201869=CARTESIAN_POINT('Ctrl Pts',(-137.505558102029,-5.12018440235748,
128.055589785961));
#201870=CARTESIAN_POINT('Ctrl Pts',(-137.784005725841,-5.0802034867949,
133.626338989485));
#201871=CARTESIAN_POINT('Ctrl Pts',(-138.062453349655,-0.371763748605222,
136.603827930521));
#201872=CARTESIAN_POINT('Ctrl Pts',(-138.340900973467,4.67830871288359,
134.251889730681));
#201873=CARTESIAN_POINT('Ctrl Pts',(-138.61934859728,5.42924401531914,128.731840697047));
#201874=CARTESIAN_POINT('Ctrl Pts',(-138.897796221093,1.19096930099152,
125.116336222143));
#201875=CARTESIAN_POINT('Ctrl Pts',(-139.176243844906,-4.14174801886209,
126.727848291193));
#201876=CARTESIAN_POINT('Ctrl Pts',(-139.454691468719,-5.66840124502105,
132.085476039479));
#201877=CARTESIAN_POINT('Ctrl Pts',(-139.733139092532,-1.98607064380098,
136.265821300996));
#201878=CARTESIAN_POINT('Ctrl Pts',(-140.011586716345,3.52136185412693,
135.427351001626));
#201879=CARTESIAN_POINT('Ctrl Pts',(-140.290034340158,5.79283483620279,
130.340578384942));
#201880=CARTESIAN_POINT('Ctrl Pts',(-140.56848196397,2.7409755995222,125.679998983016));
#201881=CARTESIAN_POINT('Ctrl Pts',(-140.846929587784,-2.82970630901691,
125.72845758426));
#201882=CARTESIAN_POINT('Ctrl Pts',(-141.125377211596,-5.80002635840773,
130.441423101462));
#201883=CARTESIAN_POINT('Ctrl Pts',(-141.403824835409,-3.44040553146196,
135.487910465481));
#201884=CARTESIAN_POINT('Ctrl Pts',(-141.682272459222,2.08077990574355,
136.230444323395));
#201885=CARTESIAN_POINT('Ctrl Pts',(-141.960720083035,5.68983026132012,
131.986672334579));
#201886=CARTESIAN_POINT('Ctrl Pts',(-142.239167706848,4.07020457040501,
126.656413636965));
#201887=CARTESIAN_POINT('Ctrl Pts',(-142.517615330661,-1.289740280165,125.137915576048));
#201888=CARTESIAN_POINT('Ctrl Pts',(-142.796062954474,-5.46447682057862,
128.826603687055));
#201889=CARTESIAN_POINT('Ctrl Pts',(-143.074510578287,-4.61762611741445,
134.332753798405));
#201890=CARTESIAN_POINT('Ctrl Pts',(-143.352958202099,0.472597404077474,
136.596482948152));
#201891=CARTESIAN_POINT('Ctrl Pts',(-143.631405825913,5.12852699888841,
133.537534636997));
#201892=CARTESIAN_POINT('Ctrl Pts',(-143.909853449725,5.07159082419343,
127.966932924958));
#201893=CARTESIAN_POINT('Ctrl Pts',(-144.188301073538,0.354110443050382,
125.003788646376));
#201894=CARTESIAN_POINT('Ctrl Pts',(-144.466748697351,-4.6887801359991,
127.371086635623));
#201895=CARTESIAN_POINT('Ctrl Pts',(-144.745196321164,-5.4229108297093,
132.893395689516));
#201896=CARTESIAN_POINT('Ctrl Pts',(-145.023643944977,-1.17365139483885,
136.495983567324));
#201897=CARTESIAN_POINT('Ctrl Pts',(-145.30209156879,4.15413633583088,134.868248005541));
#201898=CARTESIAN_POINT('Ctrl Pts',(-145.580539192603,5.66447571471356,
129.505998466145));
#201899=CARTESIAN_POINT('Ctrl Pts',(-145.858986816416,1.96943863679757,
125.336880315387));
#201900=CARTESIAN_POINT('Ctrl Pts',(-146.137434440228,-3.53541633590941,
126.192109461069));
#201901=CARTESIAN_POINT('Ctrl Pts',(-146.415882064041,-5.79139641060527,
131.285772098575));
#201902=CARTESIAN_POINT('Ctrl Pts',(-146.694329687854,-2.72536610939861,
135.937041103293));
#201903=CARTESIAN_POINT('Ctrl Pts',(-146.972777311667,2.84514250480927,
135.871627487008));
#201904=CARTESIAN_POINT('Ctrl Pts',(-147.25122493548,5.80110415003576,131.149643167454));
#201905=CARTESIAN_POINT('Ctrl Pts',(-147.529672559293,3.42613448107249,
126.110361052543));
#201906=CARTESIAN_POINT('Ctrl Pts',(-147.808120183106,-2.09728540002206,
125.38463522326));
#201907=CARTESIAN_POINT('Ctrl Pts',(-148.086567806919,-5.69340245658434,
129.639372263039));
#201908=CARTESIAN_POINT('Ctrl Pts',(-148.365015430732,-4.05756079371773,
134.964676687782));
#201909=CARTESIAN_POINT('Ctrl Pts',(-148.643463054544,1.30698101571045,
136.466853886735));
#201910=CARTESIAN_POINT('Ctrl Pts',(-148.921910678358,5.47047112127328,
132.765476399497));
#201911=CARTESIAN_POINT('Ctrl Pts',(-149.20035830217,4.60686551375719,127.261929314495));
#201912=CARTESIAN_POINT('Ctrl Pts',(-149.478805925983,-0.49022444300932,
125.013703539625));
#201913=CARTESIAN_POINT('Ctrl Pts',(-149.757253549796,-5.13682208544599,
128.086808730058));
#201914=CARTESIAN_POINT('Ctrl Pts',(-150.035701173609,-5.06293117906749,
133.657211345319));
#201915=CARTESIAN_POINT('Ctrl Pts',(-150.314148797422,-0.336453857064764,
136.605983511281));
#201916=CARTESIAN_POINT('Ctrl Pts',(-150.592596421235,4.69920812289605,
134.223347662954));
#201917=CARTESIAN_POINT('Ctrl Pts',(-150.871044045047,5.41652740699458,
128.698829746717));
#201918=CARTESIAN_POINT('Ctrl Pts',(-151.14949166886,1.15632261613933,125.109191839888));
#201919=CARTESIAN_POINT('Ctrl Pts',(-151.427939292673,-4.1664861694474,
126.753135815284));
#201920=CARTESIAN_POINT('Ctrl Pts',(-151.706386916486,-5.66049770947745,
132.119957470642));
#201921=CARTESIAN_POINT('Ctrl Pts',(-151.984834540299,-1.95278838518384,
136.277809888502));
#201922=CARTESIAN_POINT('Ctrl Pts',(-152.263282164112,3.54943806607717,
135.405829819234));
#201923=CARTESIAN_POINT('Ctrl Pts',(-152.541729787925,5.78990433430307,
130.3053243479));
#201924=CARTESIAN_POINT('Ctrl Pts',(-152.820177411738,2.70973137185537,
125.663408829112));
#201925=CARTESIAN_POINT('Ctrl Pts',(-153.09862503555,-2.86055234359039,
125.745776854456));
#201926=CARTESIAN_POINT('Ctrl Pts',(-153.377072659364,-5.80212820102742,
130.476736232542));
#201927=CARTESIAN_POINT('Ctrl Pts',(-153.655520283176,-3.41183169144105,
135.508766415124));
#201928=CARTESIAN_POINT('Ctrl Pts',(-153.933967906989,2.1137714653355,136.21767749275));
#201929=CARTESIAN_POINT('Ctrl Pts',(-154.212415530802,5.69692190894542,
131.952014817313));
#201930=CARTESIAN_POINT('Ctrl Pts',(-154.490863154615,4.04487942834225,
126.631713998332));
#201931=CARTESIAN_POINT('Ctrl Pts',(-154.769310778428,-1.32420964356211,
125.145871577308));
#201932=CARTESIAN_POINT('Ctrl Pts',(-155.047758402241,-5.47641474427016,
128.859904151722));
#201933=CARTESIAN_POINT('Ctrl Pts',(-155.326206026054,-4.59606223272787,
134.360797226267));
#201934=CARTESIAN_POINT('Ctrl Pts',(-155.604653649866,0.507846940569522,
136.593498799002));
#201935=CARTESIAN_POINT('Ctrl Pts',(-155.88310127368,5.14506958518534,133.50626519812));
#201936=CARTESIAN_POINT('Ctrl Pts',(-156.161548897493,5.05422463163864,
127.936113283085));
#201937=CARTESIAN_POINT('Ctrl Pts',(-156.439996521305,0.318794154216047,
125.001740546765));
#201938=CARTESIAN_POINT('Ctrl Pts',(-156.718444145118,-4.70959257697085,
127.399692181761));
#201939=CARTESIAN_POINT('Ctrl Pts',(-156.996891768931,-5.41009380630968,
132.926367781962));
#201940=CARTESIAN_POINT('Ctrl Pts',(-157.275339392744,-1.1389831254257,
136.503022463895));
#201941=CARTESIAN_POINT('Ctrl Pts',(-157.553787016557,4.17879740530553,
134.84288530416));
#201942=CARTESIAN_POINT('Ctrl Pts',(-157.83223464037,5.65646726616335,129.471541250343));
#201943=CARTESIAN_POINT('Ctrl Pts',(-158.110682264183,1.93612004320555,
125.324993083158));
#201944=CARTESIAN_POINT('Ctrl Pts',(-158.389129887996,-3.56342691473634,
126.213715998108));
#201945=CARTESIAN_POINT('Ctrl Pts',(-158.667577511808,-5.78835862111754,
131.321017052882));
#201946=CARTESIAN_POINT('Ctrl Pts',(-158.946025135621,-2.69407153173119,
135.95353608367));
#201947=CARTESIAN_POINT('Ctrl Pts',(-159.224472759434,2.87593568260513,
135.854214412314));
#201948=CARTESIAN_POINT('Ctrl Pts',(-159.502920383247,5.80309850189603,
131.114323802656));
#201949=CARTESIAN_POINT('Ctrl Pts',(-159.78136800706,3.39749729506709,126.089592168444));
#201950=CARTESIAN_POINT('Ctrl Pts',(-160.059815630873,-2.13023794895846,
125.39750240973));
#201951=CARTESIAN_POINT('Ctrl Pts',(-160.338263254686,-5.70038858580074,
129.674051204309));
#201952=CARTESIAN_POINT('Ctrl Pts',(-160.616710878499,-4.03216059175559,
134.989299130986));
#201953=CARTESIAN_POINT('Ctrl Pts',(-160.895158502312,1.34142600411673,
136.458793009441));
#201954=CARTESIAN_POINT('Ctrl Pts',(-161.173606126125,5.48230763450959,
132.732139754142));
#201955=CARTESIAN_POINT('Ctrl Pts',(-161.452053749937,4.58521637440516,
127.233951649575));
#201956=CARTESIAN_POINT('Ctrl Pts',(-161.730501373751,-0.525464733504406,
125.016794962416));
#201957=CARTESIAN_POINT('Ctrl Pts',(-162.008948997563,-5.15326942170307,
128.118128374039));
#201958=CARTESIAN_POINT('Ctrl Pts',(-162.287396621376,-5.04547126256333,
133.687977987722));
#201959=CARTESIAN_POINT('Ctrl Pts',(-162.565844245189,-0.301131498102361,
136.607924110772));
#201960=CARTESIAN_POINT('Ctrl Pts',(-162.844291869002,4.71993340202341,
134.194678903404));
#201961=CARTESIAN_POINT('Ctrl Pts',(-163.122739492814,5.40361008725504,
128.665896817606));
#201962=CARTESIAN_POINT('Ctrl Pts',(-163.401187116628,1.12163308332736,
125.102258494207));
#201963=CARTESIAN_POINT('Ctrl Pts',(-163.67963474044,-4.19106992935549,
126.778573459));
#201964=CARTESIAN_POINT('Ctrl Pts',(-163.958082364253,-5.65238442210956,
132.154390151878));
#201965=CARTESIAN_POINT('Ctrl Pts',(-164.236529988066,-1.91943376527495,
136.289595655332));
#201966=CARTESIAN_POINT('Ctrl Pts',(-164.514977611879,3.57738275229458,
135.384138127707));
#201967=CARTESIAN_POINT('Ctrl Pts',(-164.793425235692,5.78675928536899,
130.270088802833));
#201968=CARTESIAN_POINT('Ctrl Pts',(-165.071872859505,2.67838673409632,
125.647009175068));
#201969=CARTESIAN_POINT('Ctrl Pts',(-165.350320483318,-2.89129237934434,
125.763283572333));
#201970=CARTESIAN_POINT('Ctrl Pts',(-165.628768107131,-5.80401504365309,
130.512061503863));
#201971=CARTESIAN_POINT('Ctrl Pts',(-165.907215730944,-3.38313142474212,
135.52944804128));
#201972=CARTESIAN_POINT('Ctrl Pts',(-166.185663354757,2.14668469834846,
136.204710069657));
#201973=CARTESIAN_POINT('Ctrl Pts',(-166.464110978569,5.70380245503433,
131.917314773299));
#201974=CARTESIAN_POINT('Ctrl Pts',(-166.742558602383,4.01940440178476,
126.607168978656));
#201975=CARTESIAN_POINT('Ctrl Pts',(-167.021006226195,-1.3586299378839,
125.15403725596));
#201976=CARTESIAN_POINT('Ctrl Pts',(-167.299453850008,-5.48814973739939,
128.893276668938));
#201977=CARTESIAN_POINT('Ctrl Pts',(-167.577901473821,-4.57432803926507,
134.388708869063));
#201978=CARTESIAN_POINT('Ctrl Pts',(-167.856349097634,0.543077658606429,
136.590300131209));
#201979=CARTESIAN_POINT('Ctrl Pts',(-168.134796721447,5.16142151903669,
133.474895639175));
#201980=CARTESIAN_POINT('Ctrl Pts',(-168.413244345259,5.03667115293141,
127.905399925171));
#201981=CARTESIAN_POINT('Ctrl Pts',(-168.691691969073,0.283466052347084,
124.999907465374));
#201982=CARTESIAN_POINT('Ctrl Pts',(-168.970139592885,-4.7302305022577,
127.42842388914));
#201983=CARTESIAN_POINT('Ctrl Pts',(-169.248587216698,-5.39707630989451,
132.959261242652));
#201984=CARTESIAN_POINT('Ctrl Pts',(-169.527034840511,-1.10427265057399,
136.509850194457));
#201985=CARTESIAN_POINT('Ctrl Pts',(-169.805482464324,4.20330362790601,
134.81737295376));
#201986=CARTESIAN_POINT('Ctrl Pts',(-170.083930088137,5.6482492151383,129.437133422652));
#201987=CARTESIAN_POINT('Ctrl Pts',(-170.36237771195,1.90272970597286,125.313308890908));
#201988=CARTESIAN_POINT('Ctrl Pts',(-170.640825335763,-3.59130544946847,
126.235492643171));
#201989=CARTESIAN_POINT('Ctrl Pts',(-170.919272959575,-5.78510634187241,
131.356242862295));
#201990=CARTESIAN_POINT('Ctrl Pts',(-171.197720583389,-2.66267712425244,
135.969840259458));
#201991=CARTESIAN_POINT('Ctrl Pts',(-171.476168207202,2.90662229154664,
135.836614213432));
#201992=CARTESIAN_POINT('Ctrl Pts',(-171.754615831014,5.80487781780722,
131.07899295206));
#201993=CARTESIAN_POINT('Ctrl Pts',(-172.033063454828,3.36873421355001,
126.068997991823));
#201994=CARTESIAN_POINT('Ctrl Pts',(-172.31151107864,-2.16311156114431,
125.410569949319));
#201995=CARTESIAN_POINT('Ctrl Pts',(-172.589958702453,-5.70716348502144,
129.70877202961));
#201996=CARTESIAN_POINT('Ctrl Pts',(-172.868406326266,-4.00661097660031,
135.013766499754));
#201997=CARTESIAN_POINT('Ctrl Pts',(-173.146853950079,1.3758212854888,136.450522605077));
#201998=CARTESIAN_POINT('Ctrl Pts',(-173.425301573892,5.49394099882038,
132.698731674224));
#201999=CARTESIAN_POINT('Ctrl Pts',(-173.703749197705,4.56339732817417,
127.206106287473));
#202000=CARTESIAN_POINT('Ctrl Pts',(-173.982196821517,-0.560685552710569,
125.02010084558));
#202001=CARTESIAN_POINT('Ctrl Pts',(-174.260644445331,-5.1695258016666,
128.149547557344));
#202002=CARTESIAN_POINT('Ctrl Pts',(-174.539092069143,-5.02782438426607,
133.718637776622));
#202003=CARTESIAN_POINT('Ctrl Pts',(-174.817539692956,-0.265797980601551,
136.609649657082));
#202004=CARTESIAN_POINT('Ctrl Pts',(-175.095987316769,4.74048378228282,
134.165884514362));
#202005=CARTESIAN_POINT('Ctrl Pts',(-175.374434940582,5.39049253475655,
128.633043130058));
#202006=CARTESIAN_POINT('Ctrl Pts',(-175.652882564395,1.08690198798901,
125.095536442018));
#202007=CARTESIAN_POINT('Ctrl Pts',(-175.931330188208,-4.21549838762608,
126.80416027974));
#202008=CARTESIAN_POINT('Ctrl Pts',(-176.209777812021,-5.64406168355824,
132.188772807274));
#202009=CARTESIAN_POINT('Ctrl Pts',(-176.488225435833,-1.886008020042,136.301178164761));
#202010=CARTESIAN_POINT('Ctrl Pts',(-176.766673059646,3.60519487727851,
135.362276730843));
#202011=CARTESIAN_POINT('Ctrl Pts',(-177.045120683459,5.78339980594152,
130.234873055403));
#202012=CARTESIAN_POINT('Ctrl Pts',(-177.323568307272,2.64694284773159,
125.630800628577));
#202013=CARTESIAN_POINT('Ctrl Pts',(-177.602015931085,-2.92192527719638,
125.780977089175));
#202014=CARTESIAN_POINT('Ctrl Pts',(-177.880463554898,-5.80568681636668,
130.547397606436));
#202015=CARTESIAN_POINT('Ctrl Pts',(-178.158911178711,-3.35430579486411,
135.549954577584));
#202016=CARTESIAN_POINT('Ctrl Pts',(-178.437358802524,2.17951838517049,
136.191542534628));
#202017=CARTESIAN_POINT('Ctrl Pts',(-178.715806426336,5.71047164462571,
131.88257348836));
#202018=CARTESIAN_POINT('Ctrl Pts',(-178.99425405015,3.99378043471903,126.582779487459));
#202019=CARTESIAN_POINT('Ctrl Pts',(-179.272701673962,-1.39299988767372,
125.162412309422));
#202020=CARTESIAN_POINT('Ctrl Pts',(-179.551149297775,-5.49968136512185,
128.926720002072));
#202021=CARTESIAN_POINT('Ctrl Pts',(-179.829596921588,-4.55242434239454,
134.416487692516));
#202022=CARTESIAN_POINT('Ctrl Pts',(-180.108044545401,0.578288252700551,
136.5868870633));
#202023=CARTESIAN_POINT('Ctrl Pts',(-180.386492169214,5.17758219451528,
133.443427122574));
#202024=CARTESIAN_POINT('Ctrl Pts',(-180.664939793027,5.01893103852278,
127.874793989312));
#202025=CARTESIAN_POINT('Ctrl Pts',(-180.94338741684,0.248127446539293,
124.998289470128));
#202026=CARTESIAN_POINT('Ctrl Pts',(-181.221835040653,-4.75069314711374,
127.457280693096));
#202027=CARTESIAN_POINT('Ctrl Pts',(-181.500282664465,-5.38385882283189,
132.992074852706));
#202028=CARTESIAN_POINT('Ctrl Pts',(-181.778730288279,-1.06952125649312,
136.516466506004));
#202029=CARTESIAN_POINT('Ctrl Pts',(-182.057177912091,4.22765409554481,
134.791711899713));
#202030=CARTESIAN_POINT('Ctrl Pts',(-182.335625535904,5.63982186616143,
129.402776258069));
#202031=CARTESIAN_POINT('Ctrl Pts',(-182.614073159717,1.86926886239121,
125.301828171599));
#202032=CARTESIAN_POINT('Ctrl Pts',(-182.89252078353,-3.61905090705647,
126.257438589318));
#202033=CARTESIAN_POINT('Ctrl Pts',(-183.170968407343,-5.78163969338434,
131.391448221508));
#202034=CARTESIAN_POINT('Ctrl Pts',(-183.449416031155,-2.63118405029363,
135.985953026497));
#202035=CARTESIAN_POINT('Ctrl Pts',(-183.727863654969,2.93720119453022,
135.818827542541));
#202036=CARTESIAN_POINT('Ctrl Pts',(-184.006311278781,5.80644203183612,
131.04365192486));
#202037=CARTESIAN_POINT('Ctrl Pts',(-184.284758902595,3.33984630234777,
126.048579285806));
#202038=CARTESIAN_POINT('Ctrl Pts',(-184.563206526407,-2.19590501843575,
125.423837357804));
#202039=CARTESIAN_POINT('Ctrl Pts',(-184.84165415022,-5.71372690320071,
129.743533452349));
#202040=CARTESIAN_POINT('Ctrl Pts',(-185.120101774033,-3.98091289500146,
135.03807788744));
#202041=CARTESIAN_POINT('Ctrl Pts',(-185.398549397846,1.41016558529749,
136.442042980103));
#202042=CARTESIAN_POINT('Ctrl Pts',(-185.676997021659,5.50537078312707,
132.665253397689));
#202043=CARTESIAN_POINT('Ctrl Pts',(-185.955444645472,4.54140918357699,
127.178394260007));
#202044=CARTESIAN_POINT('Ctrl Pts',(-186.233892269285,-0.595885595507362,
125.023621066618));
#202045=CARTESIAN_POINT('Ctrl Pts',(-186.512339893098,-5.18559062295048,
128.181065115723));
#202046=CARTESIAN_POINT('Ctrl Pts',(-186.79078751691,-5.00999119808726,
133.749189575911));
#202047=CARTESIAN_POINT('Ctrl Pts',(-187.069235140724,-0.230454613858838,
136.611160086272));
#202048=CARTESIAN_POINT('Ctrl Pts',(-187.347682764536,4.76085850217237,
134.136965562817));
#202049=CARTESIAN_POINT('Ctrl Pts',(-187.626130388349,5.37717523557474,
128.600269901479));
#202050=CARTESIAN_POINT('Ctrl Pts',(-187.904578012162,1.05213061709833,
125.089025932407));
#202051=CARTESIAN_POINT('Ctrl Pts',(-188.183025635975,-4.23977063905356,
126.829895329374));
#202052=CARTESIAN_POINT('Ctrl Pts',(-188.461473259788,-5.63552980222562,
132.223104162766));
#202053=CARTESIAN_POINT('Ctrl Pts',(-188.739920883601,-1.85251238808831,
136.312556987595));
#202054=CARTESIAN_POINT('Ctrl Pts',(-189.018368507414,3.63287341044046,
135.340246438718));
#202055=CARTESIAN_POINT('Ctrl Pts',(-189.296816131227,5.77982602050738,
130.199678410544));
#202056=CARTESIAN_POINT('Ctrl Pts',(-189.575263755039,2.61540087792624,
125.614783790254));
#202057=CARTESIAN_POINT('Ctrl Pts',(-189.853711378852,-2.95244990203274,
125.798856749341));
#202058=CARTESIAN_POINT('Ctrl Pts',(-190.132159002665,-5.80714345722022,
130.582743230867));
#202059=CARTESIAN_POINT('Ctrl Pts',(-190.410606626478,-3.32535586995153,
135.570285264159));
#202060=CARTESIAN_POINT('Ctrl Pts',(-190.689054250291,2.21227130913674,
136.178175375592));
#202061=CARTESIAN_POINT('Ctrl Pts',(-190.967501874104,5.7169292305904,131.847792249846));
#202062=CARTESIAN_POINT('Ctrl Pts',(-191.245949497917,3.96800847665057,
126.558546428502));
#202063=CARTESIAN_POINT('Ctrl Pts',(-191.52439712173,-1.4273182193404,125.170996427354));
#202064=CARTESIAN_POINT('Ctrl Pts',(-191.802844745543,-5.51100920012879,
128.960232911869));
#202065=CARTESIAN_POINT('Ctrl Pts',(-192.081292369355,-4.53035195376586,
134.444132667273));
#202066=CARTESIAN_POINT('Ctrl Pts',(-192.359739993168,0.613477418111232,
136.583259721745));
#202067=CARTESIAN_POINT('Ctrl Pts',(-192.638187616981,5.19355101278185,
133.411860814392));
#202068=CARTESIAN_POINT('Ctrl Pts',(-192.916635240794,5.00100494577841,
127.844296609621));
#202069=CARTESIAN_POINT('Ctrl Pts',(-193.195082864607,0.21277964627773,
124.996886620986));
#202070=CARTESIAN_POINT('Ctrl Pts',(-193.47353048842,-4.77097975328813,
127.486261524329));
#202071=CARTESIAN_POINT('Ctrl Pts',(-193.751978112233,-5.3704418349007,
133.024807396204));
#202072=CARTESIAN_POINT('Ctrl Pts',(-194.030425736046,-1.03473023090876,
136.522871153366));
#202073=CARTESIAN_POINT('Ctrl Pts',(-194.308873359859,4.25184790590635,
134.765903092897));
#202074=CARTESIAN_POINT('Ctrl Pts',(-194.587320983671,5.63118553151129,
129.368471029708));
#202075=CARTESIAN_POINT('Ctrl Pts',(-194.865768607484,1.83573875236439,
125.290551350653));
#202076=CARTESIAN_POINT('Ctrl Pts',(-195.144216231297,-3.64666225938173,
126.279553023333));
#202077=CARTESIAN_POINT('Ctrl Pts',(-195.42266385511,-5.77795880411129,
131.426631825972));
#202078=CARTESIAN_POINT('Ctrl Pts',(-195.701111478923,-2.59959347684268,
136.001873787725));
#202079=CARTESIAN_POINT('Ctrl Pts',(-195.979559102736,2.96767125844341,
135.800855058734));
#202080=CARTESIAN_POINT('Ctrl Pts',(-196.258006726549,5.80779108602021,
131.008302030633));
#202081=CARTESIAN_POINT('Ctrl Pts',(-196.536454350362,3.31083463191258,
126.028336807015));
#202082=CARTESIAN_POINT('Ctrl Pts',(-196.814901974175,-2.22861710565919,
125.437304143558));
#202083=CARTESIAN_POINT('Ctrl Pts',(-197.093349597988,-5.72007859712835,
129.778334184429));
#202084=CARTESIAN_POINT('Ctrl Pts',(-197.3717972218,-3.95506729921131,135.062232393175));
#202085=CARTESIAN_POINT('Ctrl Pts',(-197.650244845613,1.44445763090186,
136.433354448736));
#202086=CARTESIAN_POINT('Ctrl Pts',(-197.928692469426,5.51659656389443,
132.631706165088));
#202087=CARTESIAN_POINT('Ctrl Pts',(-198.207140093239,4.51925275539276,
127.150816594059));
#202088=CARTESIAN_POINT('Ctrl Pts',(-198.485587717052,-0.631063557543924,
125.027355495085));
#202089=CARTESIAN_POINT('Ctrl Pts',(-198.764035340865,-5.2014632902668,
128.212679881281));
#202090=CARTESIAN_POINT('Ctrl Pts',(-199.042482964678,-4.99197236484219,
133.779632253479));
#202091=CARTESIAN_POINT('Ctrl Pts',(-199.320930588491,-0.19510270753564,
136.612455342372));
#202092=CARTESIAN_POINT('Ctrl Pts',(-199.599378212304,4.7810568066993,134.10792312037));
#202093=CARTESIAN_POINT('Ctrl Pts',(-199.877825836116,5.36365868318719,
128.56757834629));
#202094=CARTESIAN_POINT('Ctrl Pts',(-200.156273459929,1.01732025912016,
125.082727206624));
#202095=CARTESIAN_POINT('Ctrl Pts',(-200.434721083742,-4.26388578422093,
126.855777654281));
#202096=CARTESIAN_POINT('Ctrl Pts',(-200.713168707555,-5.62678909426374,
132.257382946195));
#202097=CARTESIAN_POINT('Ctrl Pts',(-200.991616331368,-1.8189481106068,
136.323731702186));
#202098=CARTESIAN_POINT('Ctrl Pts',(-201.270063955181,3.66041732614217,
135.318048067677));
#202099=CARTESIAN_POINT('Ctrl Pts',(-201.548511578994,5.77603806149454,
130.164506172408));
#202100=CARTESIAN_POINT('Ctrl Pts',(-201.826959202806,2.58376199347953,
125.59895925361));
#202101=CARTESIAN_POINT('Ctrl Pts',(-202.10540682662,-2.9828651227522,125.816921890294));
#202102=CARTESIAN_POINT('Ctrl Pts',(-202.383854450432,-5.80838491223743,
130.618097067413));
#202103=CARTESIAN_POINT('Ctrl Pts',(-202.662302074245,-3.29628272275406,
135.590439347642));
#202104=CARTESIAN_POINT('Ctrl Pts',(-202.940749698058,2.24494225657654,
136.164609087875));
#202105=CARTESIAN_POINT('Ctrl Pts',(-203.219197321871,5.72317497363993,
131.812972346589));
#202106=CARTESIAN_POINT('Ctrl Pts',(-203.497644945684,3.94208948256877,
126.534470699752));
#202107=CARTESIAN_POINT('Ctrl Pts',(-203.776092569497,-1.46158366120557,
125.179789291667));
#202108=CARTESIAN_POINT('Ctrl Pts',(-204.05454019331,-5.52213282266317,
128.993814156497));
#202109=CARTESIAN_POINT('Ctrl Pts',(-204.332987817123,-4.5081116912795,
134.471642768938));
#202110=CARTESIAN_POINT('Ctrl Pts',(-204.611435440935,0.648643850890564,
136.579418240959));
#202111=CARTESIAN_POINT('Ctrl Pts',(-204.889883064748,5.20932738210573,
133.380197884332));
#202112=CARTESIAN_POINT('Ctrl Pts',(-205.168330688562,4.98289353895661,
127.813908916192));
#202113=CARTESIAN_POINT('Ctrl Pts',(-205.446778312374,0.177423961388546,
124.995698969927));
#202114=CARTESIAN_POINT('Ctrl Pts',(-205.725225936187,-4.79108956905296,
127.515365308944));
#202115=CARTESIAN_POINT('Ctrl Pts',(-206.00367356,-5.35682584327266,133.057457660231));
#202116=CARTESIAN_POINT('Ctrl Pts',(-206.282121183813,-0.999900863015179,
136.529063899218));
#202117=CARTESIAN_POINT('Ctrl Pts',(-206.560568807626,4.27588416248015,
134.739947489669));
#202118=CARTESIAN_POINT('Ctrl Pts',(-206.839016431439,5.62234053121038,
129.334219008764));
#202119=CARTESIAN_POINT('Ctrl Pts',(-207.117464055252,1.80214061836306,
125.279478845937));
#202120=CARTESIAN_POINT('Ctrl Pts',(-207.395911679064,-3.67413848329639,
126.301835125757));
#202121=CARTESIAN_POINT('Ctrl Pts',(-207.674359302878,-5.77406381044983,
131.461792371951));
#202122=CARTESIAN_POINT('Ctrl Pts',(-207.95280692669,-2.56790657449899,
136.01760195319));
#202123=CARTESIAN_POINT('Ctrl Pts',(-208.231254550503,2.99803135420673,
135.782697427989));
#202124=CARTESIAN_POINT('Ctrl Pts',(-208.509702174316,5.8089249303698,130.972944579282));
#202125=CARTESIAN_POINT('Ctrl Pts',(-208.788149798129,3.28170027728254,
126.008271305542));
#202126=CARTESIAN_POINT('Ctrl Pts',(-209.066597421942,-2.2612466106562,
125.450969807563));
#202127=CARTESIAN_POINT('Ctrl Pts',(-209.345045045754,-5.72621833144002,
129.813172936296));
#202128=CARTESIAN_POINT('Ctrl Pts',(-209.623492669568,-3.92907514694791,
135.086229121905));
#202129=CARTESIAN_POINT('Ctrl Pts',(-209.90194029338,1.4786961515975,136.424457332932));
#202130=CARTESIAN_POINT('Ctrl Pts',(-210.180387917194,5.52761792514773,
132.598091219525));
#202131=CARTESIAN_POINT('Ctrl Pts',(-210.458835541006,4.49692886463537,
127.123374311529));
#202132=CARTESIAN_POINT('Ctrl Pts',(-210.73728316482,-0.666218135288655,
125.031303992602));
#202133=CARTESIAN_POINT('Ctrl Pts',(-211.015730788632,-5.21714321544808,
128.244390682522));
#202134=CARTESIAN_POINT('Ctrl Pts',(-211.294178412445,-4.97376855222533,
133.809964681263));
#202135=CARTESIAN_POINT('Ctrl Pts',(-211.572626036258,-0.159743571609885,
136.613535377387));
#202136=CARTESIAN_POINT('Ctrl Pts',(-211.851073660071,4.80107794740803,
134.0787582632));
#202137=CARTESIAN_POINT('Ctrl Pts',(-212.129521283884,5.34994337845465,
128.534969675892));
#202138=CARTESIAN_POINT('Ctrl Pts',(-212.407968907697,0.982472203965689,
125.076640498072));
#202139=CARTESIAN_POINT('Ctrl Pts',(-212.686416531509,-4.28784292953254,
126.881806295382));
#202140=CARTESIAN_POINT('Ctrl Pts',(-212.964864155322,-5.61783988356258,
132.291607887347));
#202141=CARTESIAN_POINT('Ctrl Pts',(-213.243311779135,-1.78531643133465,
136.334701894451));
#202142=CARTESIAN_POINT('Ctrl Pts',(-213.521759402948,3.68782560373359,
135.295682440288));
#202143=CARTESIAN_POINT('Ctrl Pts',(-213.800207026761,5.77203606926717,
130.129357644311));
#202144=CARTESIAN_POINT('Ctrl Pts',(-214.078654650574,2.55202736678199,
125.583327605028));
#202145=CARTESIAN_POINT('Ctrl Pts',(-214.357102274386,-3.0131698123076,
125.835171842623));
#202146=CARTESIAN_POINT('Ctrl Pts',(-214.6355498982,-5.80941113541564,130.653457806023));
#202147=CARTESIAN_POINT('Ctrl Pts',(-214.913997522012,-3.26708743058812,
135.610416081219));
#202148=CARTESIAN_POINT('Ctrl Pts',(-215.192445145826,2.27753001685547,
136.15084417418));
#202149=CARTESIAN_POINT('Ctrl Pts',(-215.470892769638,5.72920864233609,
131.778115068854));
#202150=CARTESIAN_POINT('Ctrl Pts',(-215.749340393451,3.9160244129115,126.510553193344));
#202151=CARTESIAN_POINT('Ctrl Pts',(-216.027788017264,-1.49579494355069,
125.18879057654));
#202152=CARTESIAN_POINT('Ctrl Pts',(-216.306235641077,-5.53305182053502,
129.02746249159));
#202153=CARTESIAN_POINT('Ctrl Pts',(-216.58468326489,-4.48570437905656,
134.499016978113));
#202154=CARTESIAN_POINT('Ctrl Pts',(-216.863130888703,0.683786247933482,
136.57536276329));
#202155=CARTESIAN_POINT('Ctrl Pts',(-217.141578512516,5.2249107178877,133.348439505674));
#202156=CARTESIAN_POINT('Ctrl Pts',(-217.420026136328,4.96459748918233,
127.78363203505));
#202157=CARTESIAN_POINT('Ctrl Pts',(-217.698473760142,0.142061701988793,
124.994726560962));
#202158=CARTESIAN_POINT('Ctrl Pts',(-217.976921383954,-4.81102184923216,
127.544590968491));
#202159=CARTESIAN_POINT('Ctrl Pts',(-218.255369007768,-5.34301135249269,
133.090024434919));
#202160=CARTESIAN_POINT('Ctrl Pts',(-218.53381663158,-0.965034443427401,
136.535044514085));
#202161=CARTESIAN_POINT('Ctrl Pts',(-218.812264255394,4.29976197459382,
134.713846051821));
#202162=CARTESIAN_POINT('Ctrl Pts',(-219.090711879206,5.61328719301349,
129.300021464458));
#202163=CARTESIAN_POINT('Ctrl Pts',(-219.369159503019,1.76847570537835,
125.268611067748));
#202164=CARTESIAN_POINT('Ctrl Pts',(-219.647607126831,-3.70147856065836,
126.324284070919));
#202165=CARTESIAN_POINT('Ctrl Pts',(-219.926054750645,-5.76995485673049,
131.496928556552));
#202166=CARTESIAN_POINT('Ctrl Pts',(-220.204502374457,-2.5361245174328,
136.033136940081));
#202167=CARTESIAN_POINT('Ctrl Pts',(-220.48294999827,3.02828035681523,135.764355323142));
#202168=CARTESIAN_POINT('Ctrl Pts',(-220.761397622083,5.80984352286985,
130.937580880991));
#202169=CARTESIAN_POINT('Ctrl Pts',(-221.039845245896,3.25244431804234,
125.988383524923));
#202170=CARTESIAN_POINT('Ctrl Pts',(-221.318292869709,-2.29379232432851,
125.464833843433));
#202171=CARTESIAN_POINT('Ctrl Pts',(-221.596740493522,-5.73214587862558,
129.848048416986));
#202172=CARTESIAN_POINT('Ctrl Pts',(-221.875188117335,-3.90293740136003,
135.110067184424));
#202173=CARTESIAN_POINT('Ctrl Pts',(-222.153635741148,1.51287987866345,
136.415351962378));
#202174=CARTESIAN_POINT('Ctrl Pts',(-222.432083364961,5.53843445848603,
132.564409806615));
#202175=CARTESIAN_POINT('Ctrl Pts',(-222.710530988774,4.47443833852516,
127.0960684293));
#202176=CARTESIAN_POINT('Ctrl Pts',(-222.988978612586,-0.701348026075381,
125.035466412855));
#202177=CARTESIAN_POINT('Ctrl Pts',(-223.267426236399,-5.23262981746888,
128.27619634439));
#202178=CARTESIAN_POINT('Ctrl Pts',(-223.545873860212,-4.95538043478568,
133.840185735283));
#202179=CARTESIAN_POINT('Ctrl Pts',(-223.824321484025,-0.124378516327312,
136.614400151295));
#202180=CARTESIAN_POINT('Ctrl Pts',(-224.102769107838,4.82092118240782,
134.049472072021));
#202181=CARTESIAN_POINT('Ctrl Pts',(-224.381216731651,5.33602982960279,
128.502445098609));
#202182=CARTESIAN_POINT('Ctrl Pts',(-224.659664355464,0.947587742942381,
125.070766032295));
#202183=CARTESIAN_POINT('Ctrl Pts',(-224.938111979277,-4.31164118724753,
126.907980288176));
#202184=CARTESIAN_POINT('Ctrl Pts',(-225.216559603089,-5.60868250173869,
132.325777718005));
#202185=CARTESIAN_POINT('Ctrl Pts',(-225.495007226903,-1.75161859650508,
136.345467157888));
#202186=CARTESIAN_POINT('Ctrl Pts',(-225.773454850715,3.71509722759125,
135.273150385318));
#202187=CARTESIAN_POINT('Ctrl Pts',(-226.051902474528,5.7678201921206,130.0942341287));
#202188=CARTESIAN_POINT('Ctrl Pts',(-226.330350098341,2.52019817377184,
125.567889423742));
#202189=CARTESIAN_POINT('Ctrl Pts',(-226.608797722154,-3.04336284774751,
125.853605930069));
#202190=CARTESIAN_POINT('Ctrl Pts',(-226.887245345967,-5.81022208872781,
130.688824136393));
#202191=CARTESIAN_POINT('Ctrl Pts',(-227.16569296978,-3.23777107529596,
135.630214724643));
#202192=CARTESIAN_POINT('Ctrl Pts',(-227.444140593593,2.31003338242206,
136.13688114457));
#202193=CARTESIAN_POINT('Ctrl Pts',(-227.722588217406,5.73503001309909,
131.74322170829));
#202194=CARTESIAN_POINT('Ctrl Pts',(-228.001035841218,3.88981423352964,
126.486794795549));
#202195=CARTESIAN_POINT('Ctrl Pts',(-228.279483465031,-1.52995079866356,
125.197999948425));
#202196=CARTESIAN_POINT('Ctrl Pts',(-228.557931088844,-5.54376578913698,
129.061176670297));
#202197=CARTESIAN_POINT('Ctrl Pts',(-228.836378712657,-4.46313084740822,
134.526254280438));
#202198=CARTESIAN_POINT('Ctrl Pts',(-229.11482633647,0.718903307025501,
136.571093439014));
#202199=CARTESIAN_POINT('Ctrl Pts',(-229.393273960283,5.24030044268158,
133.316586855238));
#202200=CARTESIAN_POINT('Ctrl Pts',(-229.671721584096,4.94611747442232,
127.753467088116));
#202201=CARTESIAN_POINT('Ctrl Pts',(-229.950169207909,0.106694178440453,
124.993969430123));
#202202=CARTESIAN_POINT('Ctrl Pts',(-230.228616831722,-4.83077585522751,
127.57393742));
#202203=CARTESIAN_POINT('Ctrl Pts',(-230.507064455534,-5.32899887446215,
133.122506513493));
#202204=CARTESIAN_POINT('Ctrl Pts',(-230.785512079348,-0.930132264133436,
136.540812776352));
#202205=CARTESIAN_POINT('Ctrl Pts',(-231.06395970316,4.3234804574463,134.687599746553));
#202206=CARTESIAN_POINT('Ctrl Pts',(-231.342407326973,5.60402585239536,
129.265879663993));
#202207=CARTESIAN_POINT('Ctrl Pts',(-231.620854950786,1.73474526087603,
125.257948418793));
#202208=CARTESIAN_POINT('Ctrl Pts',(-231.899302574599,-3.72868147837107,
126.346899026965));
#202209=CARTESIAN_POINT('Ctrl Pts',(-232.177750198412,-5.76563209521201,
131.532039077795));
#202210=CARTESIAN_POINT('Ctrl Pts',(-232.456197822225,-2.50424848333998,
136.048478172742));
#202211=CARTESIAN_POINT('Ctrl Pts',(-232.734645446038,3.05841714538193,
135.745829423867));
#202212=CARTESIAN_POINT('Ctrl Pts',(-233.01309306985,5.81054682948159,130.902212246173));
#202213=CARTESIAN_POINT('Ctrl Pts',(-233.291540693664,3.22306783828139,
125.968674202107));
#202214=CARTESIAN_POINT('Ctrl Pts',(-233.569988317476,-2.32625304068266,
125.478895737432));
#202215=CARTESIAN_POINT('Ctrl Pts',(-233.84843594129,-5.73786101903762,
129.882959334177));
#202216=CARTESIAN_POINT('Ctrl Pts',(-234.126883565102,-3.87665503099142,
135.133745697402));
#202217=CARTESIAN_POINT('Ctrl Pts',(-234.405331188915,1.54700754540913,
136.406038674476));
#202218=CARTESIAN_POINT('Ctrl Pts',(-234.683778812728,5.54904576309872,
132.530663174436));
#202219=CARTESIAN_POINT('Ctrl Pts',(-234.962226436541,4.45178201045685,
127.0688999592));
#202220=CARTESIAN_POINT('Ctrl Pts',(-235.240674060353,-0.736451928153096,
125.039842601604));
#202221=CARTESIAN_POINT('Ctrl Pts',(-235.519121684167,-5.24792252246713,
128.308095688315));
#202222=CARTESIAN_POINT('Ctrl Pts',(-235.797569307979,-4.93680869390195,
133.870294295687));
#202223=CARTESIAN_POINT('Ctrl Pts',(-236.076016931792,-0.0890088521534987,
136.61504963205));
#202224=CARTESIAN_POINT('Ctrl Pts',(-236.354464555605,4.8405857764003,134.020065632043));
#202225=CARTESIAN_POINT('Ctrl Pts',(-236.632912179418,5.32191855220324,
128.470005819654));
#202226=CARTESIAN_POINT('Ctrl Pts',(-236.911359803231,0.912668168706789,
125.065104026974));
#202227=CARTESIAN_POINT('Ctrl Pts',(-237.189807427044,-4.33527967551271,
126.934298662776));
#202228=CARTESIAN_POINT('Ctrl Pts',(-237.468255050857,-5.59931728812211,
132.359891171993));
#202229=CARTESIAN_POINT('Ctrl Pts',(-237.74670267467,-1.71785585480426,
136.356027093583));
#202230=CARTESIAN_POINT('Ctrl Pts',(-238.025150298482,3.7422311871549,135.250452737698));
#202231=CARTESIAN_POINT('Ctrl Pts',(-238.303597922296,5.76339058627568,
130.059136927086));
#202232=CARTESIAN_POINT('Ctrl Pts',(-238.582045546108,2.48827559389159,
125.552645281824));
#202233=CARTESIAN_POINT('Ctrl Pts',(-238.860493169922,-3.07344311025789,
125.87222346955));
#202234=CARTESIAN_POINT('Ctrl Pts',(-239.138940793734,-5.81081774212379,
130.724194748009));
#202235=CARTESIAN_POINT('Ctrl Pts',(-239.417388417547,-3.20833474320591,
135.649834544268));
#202236=CARTESIAN_POINT('Ctrl Pts',(-239.69583604136,2.34245114885216,136.12272051645));
#202237=CARTESIAN_POINT('Ctrl Pts',(-239.974283665173,5.7406388702159,131.708293557882));
#202238=CARTESIAN_POINT('Ctrl Pts',(-240.252731288985,3.86345991565072,
126.463196386742));
#202239=CARTESIAN_POINT('Ctrl Pts',(-240.531178912799,-1.56404996088748,
125.207417066067));
#202240=CARTESIAN_POINT('Ctrl Pts',(-240.809626536611,-5.5542743314588,
129.094955443325));
#202241=CARTESIAN_POINT('Ctrl Pts',(-241.088074160425,-4.44039193280503,
134.553353666625));
#202242=CARTESIAN_POINT('Ctrl Pts',(-241.366521784237,0.753993726891117,
136.566610426332));
#202243=CARTESIAN_POINT('Ctrl Pts',(-241.64496940805,5.25549598621542,133.284641113335));
#202244=CARTESIAN_POINT('Ctrl Pts',(-241.923417031863,4.92745417946037,
127.723415193164));
#202245=CARTESIAN_POINT('Ctrl Pts',(-242.201864655676,0.071322701300089,
124.993427605467));
#202246=CARTESIAN_POINT('Ctrl Pts',(-242.480312279489,-4.85035085504701,
127.603403576029));
#202247=CARTESIAN_POINT('Ctrl Pts',(-242.758759903302,-5.31478892841856,
133.154902692318));
#202248=CARTESIAN_POINT('Ctrl Pts',(-243.037207527115,-0.895195618446729,
136.546368472274));
#202249=CARTESIAN_POINT('Ctrl Pts',(-243.315655150928,4.34703873214009,
134.661209546432));
#202250=CARTESIAN_POINT('Ctrl Pts',(-243.59410277474,5.59455685253872,129.231794872506));
#202251=CARTESIAN_POINT('Ctrl Pts',(-243.872550398553,1.7009505347501,125.247491294183));
#202252=CARTESIAN_POINT('Ctrl Pts',(-244.150998022366,-3.75574622842035,
126.36967915589));
#202253=CARTESIAN_POINT('Ctrl Pts',(-244.429445646179,-5.76109568607594,
131.567122634643));
#202254=CARTESIAN_POINT('Ctrl Pts',(-244.707893269992,-2.47227965339868,
136.063625082699));
#202255=CARTESIAN_POINT('Ctrl Pts',(-244.986340893805,3.08844060317656,
135.727120416648));
#202256=CARTESIAN_POINT('Ctrl Pts',(-245.264788517618,5.81103482414375,
130.866839985428));
#202257=CARTESIAN_POINT('Ctrl Pts',(-245.543236141431,3.1935719265564,125.949144067427));
#202258=CARTESIAN_POINT('Ctrl Pts',(-245.821683765243,-2.35862755687492,
125.49315496849));
#202259=CARTESIAN_POINT('Ctrl Pts',(-246.100131389057,-5.74336354089951,
129.917904394232));
#202260=CARTESIAN_POINT('Ctrl Pts',(-246.378579012869,-3.85022900974501,
135.157263783424));
#202261=CARTESIAN_POINT('Ctrl Pts',(-246.657026636682,1.58107788722132,
136.396517814333));
#202262=CARTESIAN_POINT('Ctrl Pts',(-246.935474260495,5.55945144577998,
132.496852573479));
#202263=CARTESIAN_POINT('Ctrl Pts',(-247.213921884308,4.42896071996899,
127.04186990797));
#202264=CARTESIAN_POINT('Ctrl Pts',(-247.492369508121,-0.77152854073377,
125.044432396689));
#202265=CARTESIAN_POINT('Ctrl Pts',(-247.770817131934,-5.26302076376676,
128.340087532256));
#202266=CARTESIAN_POINT('Ctrl Pts',(-248.049264755747,-4.91805401775627,
133.90028924679));
#202267=CARTESIAN_POINT('Ctrl Pts',(-248.32771237956,-0.0536358897235281,
136.615483795589));
#202268=CARTESIAN_POINT('Ctrl Pts',(-248.606160003372,4.86007100070672,
133.990540032933));
#202269=CARTESIAN_POINT('Ctrl Pts',(-248.884607627186,5.30761006915461,
128.437653041073));
#202270=CARTESIAN_POINT('Ctrl Pts',(-249.163055250998,0.877714775216597,
125.059654691916));
#202271=CARTESIAN_POINT('Ctrl Pts',(-249.441502874812,-4.35875751839529,
126.960760443945));
#202272=CARTESIAN_POINT('Ctrl Pts',(-249.719950498624,-5.58974458974414,
132.393946985223));
#202273=CARTESIAN_POINT('Ctrl Pts',(-249.998398122437,-1.68402945732324,
136.366381310236));
#202274=CARTESIAN_POINT('Ctrl Pts',(-250.27684574625,3.76922647696617,135.227590338499));
#202275=CARTESIAN_POINT('Ctrl Pts',(-250.555293370063,5.75874741587205,
130.024067340013));
#202276=CARTESIAN_POINT('Ctrl Pts',(-250.833740993876,2.45626081004631,
125.537595744144));
#202277=CARTESIAN_POINT('Ctrl Pts',(-251.112188617689,-3.10340948520656,
125.891023771197));
#202278=CARTESIAN_POINT('Ctrl Pts',(-251.390636241501,-5.81119807352532,
130.759568330183));
#202279=CARTESIAN_POINT('Ctrl Pts',(-251.669083865314,-3.17877952510356,
135.669274813107));
#202280=CARTESIAN_POINT('Ctrl Pts',(-251.947531489127,2.37478211491517,
136.10836281449));
#202281=CARTESIAN_POINT('Ctrl Pts',(-252.22597911294,5.74603500580729,131.673331912019));
#202282=CARTESIAN_POINT('Ctrl Pts',(-252.504426736753,3.83696243592119,
126.439758841162));
#202283=CARTESIAN_POINT('Ctrl Pts',(-252.782874360566,-1.59809116681098,
125.217041580908));
#202284=CARTESIAN_POINT('Ctrl Pts',(-253.061321984379,-5.5645770578269,
129.128797558239));
#202285=CARTESIAN_POINT('Ctrl Pts',(-253.339769608192,-4.41748847836656,
134.580314133917));
#202286=CARTESIAN_POINT('Ctrl Pts',(-253.618217232004,0.789056208225191,
136.561913888683));
#202287=CARTESIAN_POINT('Ctrl Pts',(-253.896664855818,5.27049678355612,
133.252603468789));
#202288=CARTESIAN_POINT('Ctrl Pts',(-254.17511247963,4.90860829937749,127.693477454216));
#202289=CARTESIAN_POINT('Ctrl Pts',(-254.453560103444,0.0359485746511809,
124.993101125124));
#202290=CARTESIAN_POINT('Ctrl Pts',(-254.732007727256,-4.86974611083267,
127.632988310607));
#202291=CARTESIAN_POINT('Ctrl Pts',(-255.010455351069,-5.30038206451776,
133.187211835313));
#202292=CARTESIAN_POINT('Ctrl Pts',(-255.288902974882,-0.860225756393269,
136.55171127444));
#202293=CARTESIAN_POINT('Ctrl Pts',(-255.567350598695,4.37043584157037,
134.634676658854));
#202294=CARTESIAN_POINT('Ctrl Pts',(-255.845798222508,5.58488070320316,
129.197767919676));
#202295=CARTESIAN_POINT('Ctrl Pts',(-256.12424584632,1.66709247927321,125.23724089965));
#202296=CARTESIAN_POINT('Ctrl Pts',(-256.402693470134,-3.78267124144458,
126.39262206856));
#202297=CARTESIAN_POINT('Ctrl Pts',(-256.681141093946,-5.75634686702621,
131.602180844355));
#202298=CARTESIAN_POINT('Ctrl Pts',(-256.95958871776,-2.44021719259262,
136.078571600242));
#202299=CARTESIAN_POINT('Ctrl Pts',(-257.238036341572,3.118345804191,135.708239395799));
#202300=CARTESIAN_POINT('Ctrl Pts',(-257.516483965385,5.81131468939531,
130.8314457702));
#202301=CARTESIAN_POINT('Ctrl Pts',(-257.794931589198,3.16394407961038,
125.929830927563));
#202302=CARTESIAN_POINT('Ctrl Pts',(-258.073379213011,-2.39088900078744,
125.507540987923));
#202303=CARTESIAN_POINT('Ctrl Pts',(-258.351826836824,-5.74870171518396,
129.953014515613));
#202304=CARTESIAN_POINT('Ctrl Pts',(-258.630274460636,-3.82356878618261,
135.180370918811));
#202305=CARTESIAN_POINT('Ctrl Pts',(-258.908722084449,1.61491681105698,
136.387261181902));
#202306=CARTESIAN_POINT('Ctrl Pts',(-259.187169708263,5.56997747689423,
132.462088635074));
#202307=CARTESIAN_POINT('Ctrl Pts',(-259.465617332075,4.40535894966821,
127.016664495574));
#202308=CARTESIAN_POINT('Ctrl Pts',(-259.744064955888,-0.805411631290512,
125.046024618449));
#202309=CARTESIAN_POINT('Ctrl Pts',(-260.022512579701,-5.28013240410161,
128.378470706602));
#202310=CARTESIAN_POINT('Ctrl Pts',(-260.254552266212,-4.95911089365773,
132.993351965875));
#202311=CARTESIAN_POINT('Ctrl Pts',(-260.440213228287,-2.45877638613931,
135.28779596926));
#202312=CARTESIAN_POINT('Ctrl Pts',(-260.53305831576,-0.833059752290926,
135.715219187214));
#202313=CARTESIAN_POINT('Ctrl Pts',(-260.579495465929,-0.013892627260139,
135.717527172907));
#202314=CARTESIAN_POINT('Ctrl Pts',(-260.,-4.31895139421945,128.437223181));
#202315=CARTESIAN_POINT('Ctrl Pts',(-260.,-4.38498592260266,128.532528358389));
#202316=CARTESIAN_POINT('Ctrl Pts',(-260.,-4.44726778822742,128.630071853281));
#202317=CARTESIAN_POINT('Ctrl Pts',(-260.,-4.50561806400233,128.729703648768));
#202318=CARTESIAN_POINT('Ctrl Pts',(-260.,-4.57674440789476,128.851150295837));
#202319=CARTESIAN_POINT('Ctrl Pts',(-260.,-4.64203105700707,128.975698709901));
#202320=CARTESIAN_POINT('Ctrl Pts',(-260.,-4.70159679832533,129.102914350821));
#202321=CARTESIAN_POINT('Ctrl Pts',(-260.,-4.76218361828822,129.232310728038));
#202322=CARTESIAN_POINT('Ctrl Pts',(-260.,-4.81685192576391,129.364467086494));
#202323=CARTESIAN_POINT('Ctrl Pts',(-260.,-4.86568579910616,129.49896261564));
#202324=CARTESIAN_POINT('Ctrl Pts',(-260.,-4.91551630739491,129.636203021146));
#202325=CARTESIAN_POINT('Ctrl Pts',(-260.,-4.95927207158199,129.775879658827));
#202326=CARTESIAN_POINT('Ctrl Pts',(-260.,-4.99699647319888,129.917574401433));
#202327=CARTESIAN_POINT('Ctrl Pts',(-260.,-5.01778238392898,129.995647323587));
#202328=CARTESIAN_POINT('Ctrl Pts',(-260.,-5.03673638081373,130.074333384798));
#202329=CARTESIAN_POINT('Ctrl Pts',(-260.,-5.053859498905,130.15356521114));
#202330=CARTESIAN_POINT('Ctrl Pts',(-260.,-5.05814608601775,130.173400040516));
#202331=CARTESIAN_POINT('Ctrl Pts',(-260.,-5.06231835353811,130.193271261708));
#202332=CARTESIAN_POINT('Ctrl Pts',(-260.,-5.06637485462738,130.213170843715));
#202333=CARTESIAN_POINT('Ctrl Pts',(-260.,-5.09672834375308,130.362072996763));
#202334=CARTESIAN_POINT('Ctrl Pts',(-260.,-5.12052632024444,130.512171985573));
#202335=CARTESIAN_POINT('Ctrl Pts',(-260.,-5.13789473816522,130.662975483895));
#202336=CARTESIAN_POINT('Ctrl Pts',(-260.,-5.15519305516581,130.813170322059));
#202337=CARTESIAN_POINT('Ctrl Pts',(-260.,-5.16611366644811,130.964064788806));
#202338=CARTESIAN_POINT('Ctrl Pts',(-260.,-5.17073417372998,131.11520219772));
#202339=CARTESIAN_POINT('Ctrl Pts',(-260.,-5.17540412114875,131.2679568001));
#202340=CARTESIAN_POINT('Ctrl Pts',(-260.,-5.17363860431495,131.420960346613));
#202341=CARTESIAN_POINT('Ctrl Pts',(-260.,-5.16546781393087,131.573760002852));
#202342=CARTESIAN_POINT('Ctrl Pts',(-260.,-5.15737174576717,131.725162299834));
#202343=CARTESIAN_POINT('Ctrl Pts',(-260.,-5.14298704854922,131.876365240673));
#202344=CARTESIAN_POINT('Ctrl Pts',(-260.,-5.12229299840987,132.026934500077));
#202345=CARTESIAN_POINT('Ctrl Pts',(-260.,-5.11634124929555,132.070239239858));
#202346=CARTESIAN_POINT('Ctrl Pts',(-260.,-5.10986728447182,132.113491559525));
#202347=CARTESIAN_POINT('Ctrl Pts',(-260.,-5.10286982789351,132.156681074128));
#202348=CARTESIAN_POINT('Ctrl Pts',(-260.,-5.09953420587344,132.177269111271));
#202349=CARTESIAN_POINT('Ctrl Pts',(-260.,-5.0960793138402,132.197844652096));
#202350=CARTESIAN_POINT('Ctrl Pts',(-260.,-5.09250595955024,132.218400979179));
#202351=CARTESIAN_POINT('Ctrl Pts',(-260.,-5.06560675391027,132.37314322541));
#202352=CARTESIAN_POINT('Ctrl Pts',(-260.,-5.03208029934396,132.526333519448));
#202353=CARTESIAN_POINT('Ctrl Pts',(-260.,-4.99200835226872,132.677496527965));
#202354=CARTESIAN_POINT('Ctrl Pts',(-260.,-4.95190447601151,132.828779982617));
#202355=CARTESIAN_POINT('Ctrl Pts',(-260.,-4.90524475131742,132.97803376827));
#202356=CARTESIAN_POINT('Ctrl Pts',(-260.,-4.85206024555845,133.124791279933));
#202357=CARTESIAN_POINT('Ctrl Pts',(-260.,-4.79923677150287,133.270552559447));
#202358=CARTESIAN_POINT('Ctrl Pts',(-260.,-4.73997682017671,133.413852179291));
#202359=CARTESIAN_POINT('Ctrl Pts',(-260.,-4.67426001308823,133.554230102829));
#202360=CARTESIAN_POINT('Ctrl Pts',(-260.,-4.64640462459469,133.61373210497));
#202361=CARTESIAN_POINT('Ctrl Pts',(-260.,-4.61738853077812,133.672709069641));
#202362=CARTESIAN_POINT('Ctrl Pts',(-260.,-4.58720737938296,133.731125241234));
#202363=CARTESIAN_POINT('Ctrl Pts',(-260.,-4.53403293595749,133.834045350902));
#202364=CARTESIAN_POINT('Ctrl Pts',(-260.,-4.477242909968,133.935225161206));
#202365=CARTESIAN_POINT('Ctrl Pts',(-260.,-4.41699723107283,134.034557632499));
#202366=CARTESIAN_POINT('Ctrl Pts',(-260.,-4.40019967051461,134.062253281922));
#202367=CARTESIAN_POINT('Ctrl Pts',(-260.,-4.38313337868994,134.089805274928));
#202368=CARTESIAN_POINT('Ctrl Pts',(-260.,-4.36580161636001,134.117211179373));
#202369=CARTESIAN_POINT('Ctrl Pts',(-260.,-4.35192553122814,134.139152783231));
#202370=CARTESIAN_POINT('Ctrl Pts',(-260.,-4.33787717656154,134.161003821598));
#202371=CARTESIAN_POINT('Ctrl Pts',(-260.,-4.32367327517883,134.182740366414));
#202372=CARTESIAN_POINT('Ctrl Pts',(-260.,-4.24013902539044,134.310574678643));
#202373=CARTESIAN_POINT('Ctrl Pts',(-260.,-4.15113473789727,134.434602661712));
#202374=CARTESIAN_POINT('Ctrl Pts',(-260.,-4.05711762681074,134.554623908161));
#202375=CARTESIAN_POINT('Ctrl Pts',(-260.,-3.95953065717921,134.67920239815));
#202376=CARTESIAN_POINT('Ctrl Pts',(-260.,-3.85654276687757,134.799464700792));
#202377=CARTESIAN_POINT('Ctrl Pts',(-260.,-3.74861015630072,134.91517188258));
#202378=CARTESIAN_POINT('Ctrl Pts',(-260.,-3.64067754572386,135.030879064368));
#202379=CARTESIAN_POINT('Ctrl Pts',(-260.,-3.52779965481179,135.142031672907));
#202380=CARTESIAN_POINT('Ctrl Pts',(-260.,-3.41038485629795,135.248367627085));
#202381=CARTESIAN_POINT('Ctrl Pts',(-260.,-3.30440767937894,135.344345173113));
#202382=CARTESIAN_POINT('Ctrl Pts',(-260.,-3.19473354753115,135.436398761565));
#202383=CARTESIAN_POINT('Ctrl Pts',(-260.,-3.08163501453677,135.524313841136));
#202384=CARTESIAN_POINT('Ctrl Pts',(-260.,-3.02508574804119,135.56827138092));
#202385=CARTESIAN_POINT('Ctrl Pts',(-260.,-2.96768000449005,135.611193935658));
#202386=CARTESIAN_POINT('Ctrl Pts',(-260.,-2.90944981012801,135.653052319656));
#202387=CARTESIAN_POINT('Ctrl Pts',(-260.,-2.89195167916156,135.665630733541));
#202388=CARTESIAN_POINT('Ctrl Pts',(-260.,-2.87437909205552,135.678113041256));
#202389=CARTESIAN_POINT('Ctrl Pts',(-260.,-2.85673289693263,135.690498419844));
#202390=CARTESIAN_POINT('Ctrl Pts',(-260.,-2.83758770402918,135.703935903709));
#202391=CARTESIAN_POINT('Ctrl Pts',(-260.,-2.81836309546151,135.717254192549));
#202392=CARTESIAN_POINT('Ctrl Pts',(-260.,-2.79906452111251,135.730449689892));
#202393=CARTESIAN_POINT('Ctrl Pts',(-260.,-2.77695728342425,135.745565624929));
#202394=CARTESIAN_POINT('Ctrl Pts',(-260.,-2.75475127711875,135.76052162606));
#202395=CARTESIAN_POINT('Ctrl Pts',(-260.,-2.73244855505852,135.775316560448));
#202396=CARTESIAN_POINT('Ctrl Pts',(-260.,-2.59643078163644,135.86554653453));
#202397=CARTESIAN_POINT('Ctrl Pts',(-260.,-2.45681907361406,135.949788593943));
#202398=CARTESIAN_POINT('Ctrl Pts',(-260.,-2.31402220930489,136.027954478872));
#202399=CARTESIAN_POINT('Ctrl Pts',(-260.,-2.17122534499573,136.106120363801));
#202400=CARTESIAN_POINT('Ctrl Pts',(-260.,-2.02524274150512,136.178210426187));
#202401=CARTESIAN_POINT('Ctrl Pts',(-260.,-1.8764471723442,136.244098466396));
#202402=CARTESIAN_POINT('Ctrl Pts',(-260.,-1.80305579306763,136.276596841018));
#202403=CARTESIAN_POINT('Ctrl Pts',(-260.,-1.7289795719389,136.307585759908));
#202404=CARTESIAN_POINT('Ctrl Pts',(-260.,-1.65426068122485,136.337046274096));
#202405=CARTESIAN_POINT('Ctrl Pts',(-260.,-1.61863281016888,136.351093797964));
#202406=CARTESIAN_POINT('Ctrl Pts',(-260.,-1.5828587981496,136.364793781341));
#202407=CARTESIAN_POINT('Ctrl Pts',(-260.,-1.5469431056621,136.378143953878));
#202408=CARTESIAN_POINT('Ctrl Pts',(-260.,-1.52194835513068,136.387434718138));
#202409=CARTESIAN_POINT('Ctrl Pts',(-260.,-1.4968838979741,136.396556379419));
#202410=CARTESIAN_POINT('Ctrl Pts',(-260.,-1.47176771023595,136.405502461703));
#202411=CARTESIAN_POINT('Ctrl Pts',(-260.,-1.31515450873548,136.461286189794));
#202412=CARTESIAN_POINT('Ctrl Pts',(-260.,-1.15638749404024,136.510301323187));
#202413=CARTESIAN_POINT('Ctrl Pts',(-260.,-0.995868207088328,136.55243688218));
#202414=CARTESIAN_POINT('Ctrl Pts',(-260.,-0.835850940924087,136.594440663073));
#202415=CARTESIAN_POINT('Ctrl Pts',(-260.,-0.674091715028761,136.629608166435));
#202416=CARTESIAN_POINT('Ctrl Pts',(-260.,-0.510961125684827,136.657785834748));
#202417=CARTESIAN_POINT('Ctrl Pts',(-260.,-0.348088738648444,136.685918903584));
#202418=CARTESIAN_POINT('Ctrl Pts',(-260.,-0.183848703485478,136.707084599764));
#202419=CARTESIAN_POINT('Ctrl Pts',(-260.,-0.0185920708335254,136.72108140677));
#202420=CARTESIAN_POINT('Origin',(-260.,0.,130.804360617566));
#279247=UNCERTAINTY_MEASURE_WITH_UNIT(LENGTH_MEASURE(0.01),#279267,
'DISTANCE_ACCURACY_VALUE',
'Maximum model space distance between geometric entities at asserted c
onnectivities');
#279255=UNCERTAINTY_MEASURE_WITH_UNIT(LENGTH_MEASURE(0.01),#279267,
'DISTANCE_ACCURACY_VALUE',
'Maximum model space distance between geometric entities at asserted c
onnectivities');
#279258=(
GEOMETRIC_REPRESENTATION_CONTEXT(3)
GLOBAL_UNCERTAINTY_ASSIGNED_CONTEXT((#279247))
GLOBAL_UNIT_ASSIGNED_CONTEXT((#279267,#279269,#279270))
REPRESENTATION_CONTEXT('','3D')
);
#279266=(
GEOMETRIC_REPRESENTATION_CONTEXT(3)
GLOBAL_UNCERTAINTY_ASSIGNED_CONTEXT((#279255))
GLOBAL_UNIT_ASSIGNED_CONTEXT((#279267,#279269,#279270))
REPRESENTATION_CONTEXT('','3D')
);
#279267=(
LENGTH_UNIT()
NAMED_UNIT(*)
SI_UNIT(.MILLI.,.METRE.)
);
#279269=(
NAMED_UNIT(*)
PLANE_ANGLE_UNIT()
SI_UNIT($,.RADIAN.)
);
#279270=(
NAMED_UNIT(*)
SI_UNIT($,.STERADIAN.)
SOLID_ANGLE_UNIT()
);
#279273=SHAPE_DEFINITION_REPRESENTATION(#279283,#279302);
#279283=PRODUCT_DEFINITION_SHAPE('',$,#279313);
#279302=SHAPE_REPRESENTATION('',(#15104),#279258);
#279310=PRODUCT_DEFINITION_CONTEXT('part definition',#279342,'design');
#279313=PRODUCT_DEFINITION('Screw','Screw',#279323,#279310);
#279323=PRODUCT_DEFINITION_FORMATION('',$,#279346);
#279342=APPLICATION_CONTEXT(
'Core Data for Automotive Mechanical Design Process');
#279343=PRODUCT_CONTEXT('part definition',#279342,'mechanical');
#279346=PRODUCT('Screw','Screw',$,(#279343));
#279355=PRESENTATION_STYLE_ASSIGNMENT((#279357));
#279357=SURFACE_STYLE_USAGE(.BOTH.,#279359);
#279359=SURFACE_SIDE_STYLE('',(#279361));
#279361=SURFACE_STYLE_FILL_AREA(#279363);
#279363=FILL_AREA_STYLE('Opaque(160,160,160)',(#279365));
#279365=FILL_AREA_STYLE_COLOUR('Opaque(160,160,160)',#279367);
#279367=COLOUR_RGB('Opaque(160,160,160)', 0.66274510, 0.83137255, 0.94901961);
ENDSEC;
END-ISO-10303-21;
